#56648=CARTESIAN_POINT('Ctrl Pts',(60.6124491601336,1.13409814708177,126.018652262966));
#56649=CARTESIAN_POINT('Ctrl Pts',(60.6047028268683,1.00058046167255,125.987011772488));
#56650=CARTESIAN_POINT('Ctrl Pts',(60.596956493603,0.865738447375988,125.960963260593));
#56651=CARTESIAN_POINT('Ctrl Pts',(60.5892101603376,0.730079703962902,125.940600067502));
#56652=CARTESIAN_POINT('Ctrl Pts',(60.5814620923347,0.59439058071519,125.920232314215));
#56653=CARTESIAN_POINT('Ctrl Pts',(60.5737140243317,0.457884750959189,125.905552471252));
#56654=CARTESIAN_POINT('Ctrl Pts',(60.5659659563288,0.321076384654983,125.896602166122));
#56655=CARTESIAN_POINT('Ctrl Pts',(60.5582096535869,0.184122616790654,125.887642348502));
#56656=CARTESIAN_POINT('Ctrl Pts',(60.5504533508451,0.0468660608217313,
125.884424258552));
#56657=CARTESIAN_POINT('Ctrl Pts',(60.5426970481032,-0.0901770931478938,
125.886937394538));
#56658=CARTESIAN_POINT('Ctrl Pts',(60.5349366055891,-0.227293391175082,
125.889451871861));
#56659=CARTESIAN_POINT('Ctrl Pts',(60.5271761630749,-0.364195670183447,
125.89770364678));
#56660=CARTESIAN_POINT('Ctrl Pts',(60.5194157205608,-0.500372403011901,
125.911630242734));
#56661=CARTESIAN_POINT('Ctrl Pts',(60.5116428202953,-0.636767738821279,
125.925579194896));
#56662=CARTESIAN_POINT('Ctrl Pts',(60.5038699200299,-0.77243481383313,125.945221116175));
#56663=CARTESIAN_POINT('Ctrl Pts',(60.4960970197645,-0.906870949584289,
125.97044210943));
#56664=CARTESIAN_POINT('Ctrl Pts',(60.4886066840024,-1.03641999317725,125.994746256052));
#56665=CARTESIAN_POINT('Ctrl Pts',(60.4811163482404,-1.16482573901601,126.024230821351));
#56666=CARTESIAN_POINT('Ctrl Pts',(60.4736260124783,-1.29165317458304,126.05875052622));
#56667=CARTESIAN_POINT('Ctrl Pts',(60.4658516783592,-1.4232893109174,126.09457905619));
#56668=CARTESIAN_POINT('Ctrl Pts',(60.4580773442401,-1.55364207483918,126.135945571518));
#56669=CARTESIAN_POINT('Ctrl Pts',(60.450303010121,-1.68220999257674,126.18274265376));
#56670=CARTESIAN_POINT('Ctrl Pts',(60.4425382571739,-1.81061946184613,126.22948206278));
#56671=CARTESIAN_POINT('Ctrl Pts',(60.4347735042268,-1.93724809774762,126.28163858982));
#56672=CARTESIAN_POINT('Ctrl Pts',(60.4270087512797,-2.06160686232993,126.339054333816));
#56673=CARTESIAN_POINT('Ctrl Pts',(60.4192517103947,-2.18584211203394,126.396413051686));
#56674=CARTESIAN_POINT('Ctrl Pts',(60.4114946695097,-2.30781162424967,126.459020428634));
#56675=CARTESIAN_POINT('Ctrl Pts',(60.4037376286247,-2.42704406006311,126.526669629076));
#56676=CARTESIAN_POINT('Ctrl Pts',(60.3959864373845,-2.5461865817697,126.594267814729));
#56677=CARTESIAN_POINT('Ctrl Pts',(60.3882352461444,-2.66259579677202,126.666900063919));
#56678=CARTESIAN_POINT('Ctrl Pts',(60.3804840549043,-2.77582313223473,126.744312711315));
#56679=CARTESIAN_POINT('Ctrl Pts',(60.3727361581272,-2.88900234305896,126.821692456271));
#56680=CARTESIAN_POINT('Ctrl Pts',(60.3649882613501,-2.99900204206298,126.903848338149));
#56681=CARTESIAN_POINT('Ctrl Pts',(60.357240364573,-3.10540112192147,126.990482416251));
#56682=CARTESIAN_POINT('Ctrl Pts',(60.3494940884889,-3.21177794538616,127.077098372371));
#56683=CARTESIAN_POINT('Ctrl Pts',(60.3417478124048,-3.31455534482194,127.168190414784));
#56684=CARTESIAN_POINT('Ctrl Pts',(60.3340015363208,-3.4133442266439,127.263419464011));
#56685=CARTESIAN_POINT('Ctrl Pts',(60.3262552030554,-3.51213383770307,127.358649216198));
#56686=CARTESIAN_POINT('Ctrl Pts',(60.31850886979,-3.60693459091922,127.458015764801));
#56687=CARTESIAN_POINT('Ctrl Pts',(60.3107625365247,-3.69739358644646,127.561142504425));
#56688=CARTESIAN_POINT('Ctrl Pts',(60.3030144685217,-3.78787283963893,127.664292338568));
#56689=CARTESIAN_POINT('Ctrl Pts',(60.2952664005186,-3.87400814260205,127.771203745493));
#56690=CARTESIAN_POINT('Ctrl Pts',(60.2875183325156,-3.95548655151164,127.881466640134));
#56691=CARTESIAN_POINT('Ctrl Pts',(60.2797620297737,-4.03705155664337,127.991846723491));
#56692=CARTESIAN_POINT('Ctrl Pts',(60.2720057270319,-4.1139495480378,128.105585095111));
#56693=CARTESIAN_POINT('Ctrl Pts',(60.2642494242901,-4.18591034774258,128.222241793197));
#56694=CARTESIAN_POINT('Ctrl Pts',(60.2564889817759,-4.25790955509305,128.338960754475));
#56695=CARTESIAN_POINT('Ctrl Pts',(60.2487285392617,-4.32496612897891,128.458600804984));
#56696=CARTESIAN_POINT('Ctrl Pts',(60.2409680967475,-4.38685613977697,128.580697812328));
#56697=CARTESIAN_POINT('Ctrl Pts',(60.2331951964821,-4.44884550191454,128.702990820626));
#56698=CARTESIAN_POINT('Ctrl Pts',(60.2254222962167,-4.50565156515005,128.827748311357));
#56699=CARTESIAN_POINT('Ctrl Pts',(60.2176493959513,-4.55709844438776,128.954485802705));
#56700=CARTESIAN_POINT('Ctrl Pts',(60.2101590601893,-4.6066750999779,129.076616067008));
#56701=CARTESIAN_POINT('Ctrl Pts',(60.2026687244273,-4.65127534225548,129.200584585365));
#56702=CARTESIAN_POINT('Ctrl Pts',(60.1951783886654,-4.69078626375652,129.325946842518));
#56703=CARTESIAN_POINT('Ctrl Pts',(60.1901117826114,-4.71751220508084,129.410744265652));
#56704=CARTESIAN_POINT('Ctrl Pts',(60.1850451765575,-4.74194769037687,129.496295894021));
#56705=CARTESIAN_POINT('Ctrl Pts',(60.1799785705036,-4.76405452823407,129.582490119308));
#56706=CARTESIAN_POINT('Origin',(213.235140564004,0.,130.804360617566));
#56707=CARTESIAN_POINT('',(58.0850005708557,-4.76405452823401,129.582490119308));
#56708=CARTESIAN_POINT('',(58.429932073253,-4.76405452823401,129.582490119308));
#56709=CARTESIAN_POINT('',(213.235140564004,-4.76405452823405,129.582490119308));
#56710=CARTESIAN_POINT('',(59.7648594359381,-4.91824913396613,130.80727930587));
#56711=CARTESIAN_POINT('Ctrl Pts',(59.7648594359381,-4.91824913396613,130.80727930587));
#56712=CARTESIAN_POINT('Ctrl Pts',(59.7559438277098,-4.91815530429253,130.965390643192));
#56713=CARTESIAN_POINT('Ctrl Pts',(59.7470282194816,-4.91043248621711,131.123221752801));
#56714=CARTESIAN_POINT('Ctrl Pts',(59.7381126112533,-4.8951889725416,131.280079006539));
#56715=CARTESIAN_POINT('Ctrl Pts',(59.7294177150926,-4.88032282262348,131.433053150129));
#56716=CARTESIAN_POINT('Ctrl Pts',(59.7207228189319,-4.85830408773118,131.585100927552));
#56717=CARTESIAN_POINT('Ctrl Pts',(59.7120279227713,-4.82928394905967,131.735596141939));
#56718=CARTESIAN_POINT('Ctrl Pts',(59.7030019585092,-4.79915883546559,131.891821633489));
#56719=CARTESIAN_POINT('Ctrl Pts',(59.6939759942471,-4.76148881981934,132.046373734296));
#56720=CARTESIAN_POINT('Ctrl Pts',(59.684950029985,-4.71649769137675,132.198574585986));
#56721=CARTESIAN_POINT('Ctrl Pts',(59.6759240657229,-4.67150656293416,132.350775437676));
#56722=CARTESIAN_POINT('Ctrl Pts',(59.6668981014609,-4.6191944896861,132.500624835296));
#56723=CARTESIAN_POINT('Ctrl Pts',(59.6578721371988,-4.55983845854355,132.647471111944));
#56724=CARTESIAN_POINT('Ctrl Pts',(59.6500978030798,-4.50871332612744,132.773954220635));
#56725=CARTESIAN_POINT('Ctrl Pts',(59.6423234689607,-4.45224054805438,132.898508855189));
#56726=CARTESIAN_POINT('Ctrl Pts',(59.6345491348417,-4.390586019346,133.020649738873));
#56727=CARTESIAN_POINT('Ctrl Pts',(59.6267843818947,-4.32900747433403,133.142640094834));
#56728=CARTESIAN_POINT('Ctrl Pts',(59.6190196289477,-4.26226005949961,133.262222273087));
#56729=CARTESIAN_POINT('Ctrl Pts',(59.6112548760006,-4.19055833035914,133.378929308115));
#56730=CARTESIAN_POINT('Ctrl Pts',(59.6034978351157,-4.11892781638696,133.495520428071));
#56731=CARTESIAN_POINT('Ctrl Pts',(59.5957407942307,-4.04235298384866,133.609241756677));
#56732=CARTESIAN_POINT('Ctrl Pts',(59.5879837533458,-3.96109488986182,133.719649683167));
#56733=CARTESIAN_POINT('Ctrl Pts',(59.5802325621057,-3.87989807323564,133.82997435018));
#56734=CARTESIAN_POINT('Ctrl Pts',(59.5724813708657,-3.79402525557015,133.93699027491));
#56735=CARTESIAN_POINT('Ctrl Pts',(59.5647301796256,-3.70378130707953,134.040281984322));
#56736=CARTESIAN_POINT('Ctrl Pts',(59.5569822828486,-3.61357571467447,134.143529792002));
#56737=CARTESIAN_POINT('Ctrl Pts',(59.5492343860716,-3.51900294325448,134.243056238808));
#56738=CARTESIAN_POINT('Ctrl Pts',(59.5414864892946,-3.42040858458665,134.338478354284));
#56739=CARTESIAN_POINT('Ctrl Pts',(59.5337402132105,-3.3218348497332,134.433880509511));
#56740=CARTESIAN_POINT('Ctrl Pts',(59.5259939371264,-3.21924148164196,134.525179769361));
#56741=CARTESIAN_POINT('Ctrl Pts',(59.5182476610424,-3.1130111418139,134.612029811895));
#56742=CARTESIAN_POINT('Ctrl Pts',(59.5105013277771,-3.00678001781775,134.698880495536));
#56743=CARTESIAN_POINT('Ctrl Pts',(59.5027549945118,-2.89691217119505,134.781281648864));
#56744=CARTESIAN_POINT('Ctrl Pts',(59.4950086612465,-2.7838232519097,134.858927322484));
#56745=CARTESIAN_POINT('Ctrl Pts',(59.4872605932436,-2.67070900714497,134.936590384314));
#56746=CARTESIAN_POINT('Ctrl Pts',(59.4795125252408,-2.55437257658767,135.009495626044));
#56747=CARTESIAN_POINT('Ctrl Pts',(59.4717644572379,-2.43525813638147,135.077380728879));
#56748=CARTESIAN_POINT('Ctrl Pts',(59.4640081544961,-2.31601709993057,135.14533798081));
#56749=CARTESIAN_POINT('Ctrl Pts',(59.4562518517543,-2.19399249610628,135.208264241788));
#56750=CARTESIAN_POINT('Ctrl Pts',(59.4484955490125,-2.06965311764546,135.26594318826));
#56751=CARTESIAN_POINT('Ctrl Pts',(59.4407351064984,-1.94524737551457,135.323652919723));
#56752=CARTESIAN_POINT('Ctrl Pts',(59.4329746639843,-1.81852475804048,135.376109606687));
#56753=CARTESIAN_POINT('Ctrl Pts',(59.4252142214702,-1.68997259704823,135.423145704981));
#56754=CARTESIAN_POINT('Ctrl Pts',(59.4174413212048,-1.56121407271484,135.470257309795));
#56755=CARTESIAN_POINT('Ctrl Pts',(59.4096684209395,-1.43062050858531,135.511930818425));
#56756=CARTESIAN_POINT('Ctrl Pts',(59.4018955206741,-1.29869376899297,135.548048798389));
#56757=CARTESIAN_POINT('Ctrl Pts',(59.3944051849114,-1.17156289867661,135.582853798809));
#56758=CARTESIAN_POINT('Ctrl Pts',(59.3869148491488,-1.04319439876613,135.612500103617));
#56759=CARTESIAN_POINT('Ctrl Pts',(59.3794245133861,-0.914043008567175,
135.636928096763));
#56760=CARTESIAN_POINT('Ctrl Pts',(59.371650179267,-0.77999480416525,135.662282284691));
#56761=CARTESIAN_POINT('Ctrl Pts',(59.3638758451479,-0.644678546570666,
135.682094959499));
#56762=CARTESIAN_POINT('Ctrl Pts',(59.3561015110288,-0.50859218315392,135.696243389438));
#56763=CARTESIAN_POINT('Ctrl Pts',(59.3483367580817,-0.372673534017698,
135.710374382701));
#56764=CARTESIAN_POINT('Ctrl Pts',(59.3405720051347,-0.235987052594861,
135.718854980519));
#56765=CARTESIAN_POINT('Ctrl Pts',(59.3328072521876,-0.0990415826969921,
135.721613288255));
#56766=CARTESIAN_POINT('Ctrl Pts',(59.3250502113026,0.037767871029396,135.724368856401));
#56767=CARTESIAN_POINT('Ctrl Pts',(59.3172931704176,0.174835412972991,135.721413436983));
#56768=CARTESIAN_POINT('Ctrl Pts',(59.3095361295326,0.311646713083914,135.712726882294));
#56769=CARTESIAN_POINT('Ctrl Pts',(59.3017849382925,0.448354842729186,135.704046878204));
#56770=CARTESIAN_POINT('Ctrl Pts',(59.2940337470523,0.584806726561502,135.689644365982));
#56771=CARTESIAN_POINT('Ctrl Pts',(59.2862825558122,0.720488025554324,135.669551268253));
#56772=CARTESIAN_POINT('Ctrl Pts',(59.2785346590351,0.856111656375657,135.649466710626));
#56773=CARTESIAN_POINT('Ctrl Pts',(59.2707867622581,0.990964967830361,135.623696435157));
#56774=CARTESIAN_POINT('Ctrl Pts',(59.263038865481,1.12453895523701,135.592324193101));
#56775=CARTESIAN_POINT('Ctrl Pts',(59.2552925893969,1.2580850018452,135.560958513443));
#56776=CARTESIAN_POINT('Ctrl Pts',(59.2475463133127,1.3903518763231,135.523993287329));
#56777=CARTESIAN_POINT('Ctrl Pts',(59.2398000372286,1.52084137032635,135.481563263251));
#56778=CARTESIAN_POINT('Ctrl Pts',(59.2320537039633,1.65133182757321,135.439132925965));
#56779=CARTESIAN_POINT('Ctrl Pts',(59.2243073706979,1.78004450636128,135.391237831114));
#56780=CARTESIAN_POINT('Ctrl Pts',(59.2165610374326,1.90649733384231,135.338062303667));
#56781=CARTESIAN_POINT('Ctrl Pts',(59.2088129694296,2.03297847955729,135.284874867928));
#56782=CARTESIAN_POINT('Ctrl Pts',(59.2010649014266,2.15719840660112,135.226404798045));
#56783=CARTESIAN_POINT('Ctrl Pts',(59.1933168334236,2.27869633068629,135.162884002271));
#56784=CARTESIAN_POINT('Ctrl Pts',(59.1855605306818,2.40032338421102,135.099295695838));
#56785=CARTESIAN_POINT('Ctrl Pts',(59.17780422794,2.51922230872019,135.030646121841));
#56786=CARTESIAN_POINT('Ctrl Pts',(59.1700479251981,2.63495771115671,134.957212760722));
#56787=CARTESIAN_POINT('Ctrl Pts',(59.162287482684,2.75075488506239,134.883740206007));
#56788=CARTESIAN_POINT('Ctrl Pts',(59.1545270401698,2.86338485157338,134.805478999584));
#56789=CARTESIAN_POINT('Ctrl Pts',(59.1467665976556,2.97244323627699,134.722748585801));
#56790=CARTESIAN_POINT('Ctrl Pts',(59.1389936973902,3.08167669118148,134.639885365814));
#56791=CARTESIAN_POINT('Ctrl Pts',(59.1312207971247,3.18732680558401,134.552538851055));
#56792=CARTESIAN_POINT('Ctrl Pts',(59.1234478968593,3.28902351028198,134.461067799077));
#56793=CARTESIAN_POINT('Ctrl Pts',(59.1159575610973,3.38702328360564,134.372921950239));
#56794=CARTESIAN_POINT('Ctrl Pts',(59.1084672253352,3.48135186923592,134.280946447587));
#56795=CARTESIAN_POINT('Ctrl Pts',(59.1009768895732,3.57171331279927,134.185491652245));
#56796=CARTESIAN_POINT('Ctrl Pts',(59.0932025554541,3.66550083796009,134.086417659325));
#56797=CARTESIAN_POINT('Ctrl Pts',(59.085428221335,3.75531154491298,133.98328149414));
#56798=CARTESIAN_POINT('Ctrl Pts',(59.0776538872159,3.840773023246,133.876435754409));
#56799=CARTESIAN_POINT('Ctrl Pts',(59.0698891342688,3.92612917794488,133.769721692502));
#56800=CARTESIAN_POINT('Ctrl Pts',(59.0621243813217,4.00714652703377,133.659307454789));
#56801=CARTESIAN_POINT('Ctrl Pts',(59.0543596283746,4.08348954101034,133.545582285173));
#56802=CARTESIAN_POINT('Ctrl Pts',(59.0466025874896,4.15975673002908,133.431970068999));
#56803=CARTESIAN_POINT('Ctrl Pts',(59.0388455466046,4.23135860645275,133.315053787623));
#56804=CARTESIAN_POINT('Ctrl Pts',(59.0310885057196,4.2980002114886,133.195255271152));
#56805=CARTESIAN_POINT('Ctrl Pts',(59.0233373144794,4.36459156157178,133.075547095674));
#56806=CARTESIAN_POINT('Ctrl Pts',(59.0155861232394,4.4262298963735,132.95296135163));
#56807=CARTESIAN_POINT('Ctrl Pts',(59.0078349319992,4.48266406049338,132.82794802197));
#56808=CARTESIAN_POINT('Ctrl Pts',(59.0000870352221,4.53907423858807,132.702987826309));
#56809=CARTESIAN_POINT('Ctrl Pts',(58.992339138445,4.59028448480026,132.575602452772));
#56810=CARTESIAN_POINT('Ctrl Pts',(58.9845912416679,4.63609013197015,132.446265411014));
#56811=CARTESIAN_POINT('Ctrl Pts',(58.9768449655838,4.68188619758612,132.316955423777));
#56812=CARTESIAN_POINT('Ctrl Pts',(58.9690986894997,4.72227978240038,132.185694948646));
#56813=CARTESIAN_POINT('Ctrl Pts',(58.9613524134156,4.75711496035481,132.052975977262));
#56814=CARTESIAN_POINT('Ctrl Pts',(58.9536060801503,4.79195039545456,131.920256026176));
#56815=CARTESIAN_POINT('Ctrl Pts',(58.9458597468849,4.82122724256446,131.78607793551));
#56816=CARTESIAN_POINT('Ctrl Pts',(58.9381134136195,4.8448400073489,131.65094691895));
#56817=CARTESIAN_POINT('Ctrl Pts',(58.9303653456165,4.86845806004833,131.515785640736));
#56818=CARTESIAN_POINT('Ctrl Pts',(58.9226172776136,4.88640943910494,131.37967139704));
#56819=CARTESIAN_POINT('Ctrl Pts',(58.9148692096106,4.89864019033708,131.243117210809));
#56820=CARTESIAN_POINT('Ctrl Pts',(58.9071129068688,4.91088394055718,131.106417893164));
#56821=CARTESIAN_POINT('Ctrl Pts',(58.8993566041269,4.91739488266153,130.969278088977));
#56822=CARTESIAN_POINT('Ctrl Pts',(58.891600301385,4.91817112822213,130.832214091716));
#56823=CARTESIAN_POINT('Ctrl Pts',(58.8838398588708,4.91894778808837,130.695076939272));
#56824=CARTESIAN_POINT('Ctrl Pts',(58.8760794163567,4.91398366669107,130.558016064892));
#56825=CARTESIAN_POINT('Ctrl Pts',(58.8683189738425,4.90332894736035,130.421544347695));
#56826=CARTESIAN_POINT('Ctrl Pts',(58.8605460735771,4.89265712412829,130.284853553982));
#56827=CARTESIAN_POINT('Ctrl Pts',(58.8527731733116,4.87627649496156,130.148754195784));
#56828=CARTESIAN_POINT('Ctrl Pts',(58.8450002730462,4.8542888613066,130.013751540022));
#56829=CARTESIAN_POINT('Ctrl Pts',(58.8375099372842,4.83310053351864,129.883656570849));
#56830=CARTESIAN_POINT('Ctrl Pts',(58.8300196015222,4.8067058428928,129.754580254425));
#56831=CARTESIAN_POINT('Ctrl Pts',(58.8225292657602,4.77523958759863,129.626960964292));
#56832=CARTESIAN_POINT('Ctrl Pts',(58.8147549316412,4.74258027967089,129.494502949983));
#56833=CARTESIAN_POINT('Ctrl Pts',(58.806980597522,4.70435378378937,129.363195042129));
#56834=CARTESIAN_POINT('Ctrl Pts',(58.799206263403,4.66065545347599,129.233541147835));
#56835=CARTESIAN_POINT('Ctrl Pts',(58.7914415104559,4.6170109774493,129.104047040379));
#56836=CARTESIAN_POINT('Ctrl Pts',(58.7836767575089,4.56790820830916,128.976203257559));
#56837=CARTESIAN_POINT('Ctrl Pts',(58.7759120045618,4.51349326608363,128.850502485685));
#56838=CARTESIAN_POINT('Ctrl Pts',(58.7681549636768,4.45913236954584,128.72492656159));
#56839=CARTESIAN_POINT('Ctrl Pts',(58.7603979227918,4.39946995396238,128.601489769161));
#56840=CARTESIAN_POINT('Ctrl Pts',(58.7526408819068,4.33470148451864,128.480668275062));
#56841=CARTESIAN_POINT('Ctrl Pts',(58.7448896906666,4.26998185748153,128.359937893391));
#56842=CARTESIAN_POINT('Ctrl Pts',(58.7371384994265,4.20016402476987,128.241819227656));
#56843=CARTESIAN_POINT('Ctrl Pts',(58.7293873081864,4.12549081415279,128.126766808782));
#56844=CARTESIAN_POINT('Ctrl Pts',(58.7216394114093,4.05084934164219,128.011763290254));
#56845=CARTESIAN_POINT('Ctrl Pts',(58.7138915146323,3.97135680810245,127.899823753809));
#56846=CARTESIAN_POINT('Ctrl Pts',(58.7061436178552,3.88730096301673,127.791376335259));
#56847=CARTESIAN_POINT('Ctrl Pts',(58.6983973417711,3.80326270060176,127.682951601571));
#56848=CARTESIAN_POINT('Ctrl Pts',(58.690651065687,3.71466326464459,127.578017841637));
#56849=CARTESIAN_POINT('Ctrl Pts',(58.6829047896029,3.62183229980335,127.476972173966));
#56850=CARTESIAN_POINT('Ctrl Pts',(58.6751584563375,3.52900064970502,127.375925760399));
#56851=CARTESIAN_POINT('Ctrl Pts',(58.6674121230722,3.43193767289633,127.278767784275));
#56852=CARTESIAN_POINT('Ctrl Pts',(58.6596657898068,3.33101139769506,127.185860081304));
#56853=CARTESIAN_POINT('Ctrl Pts',(58.6519177218038,3.23006252075423,127.092931572298));
#56854=CARTESIAN_POINT('Ctrl Pts',(58.6441696538009,3.12524891144429,127.004255495195));
#56855=CARTESIAN_POINT('Ctrl Pts',(58.636421585798,3.01697302694656,126.920154544611));
#56856=CARTESIAN_POINT('Ctrl Pts',(58.6286652830561,2.90858206555029,126.835964210537));
#56857=CARTESIAN_POINT('Ctrl Pts',(58.6209089803142,2.79672178753323,126.756358956556));
#56858=CARTESIAN_POINT('Ctrl Pts',(58.6131526775724,2.68182554446955,126.681619440687));
#56859=CARTESIAN_POINT('Ctrl Pts',(58.6053922350582,2.56686797782134,126.606840034089));
#56860=CARTESIAN_POINT('Ctrl Pts',(58.597631792544,2.44887155356918,126.536931739511));
#56861=CARTESIAN_POINT('Ctrl Pts',(58.5898713500299,2.32829489675721,126.472129559989));
#56862=CARTESIAN_POINT('Ctrl Pts',(58.5820984497645,2.20752467959159,126.407223354256));
#56863=CARTESIAN_POINT('Ctrl Pts',(58.5743255494991,2.0841663048219,126.34743981398));
#56864=CARTESIAN_POINT('Ctrl Pts',(58.5665526492336,1.9586998939876,126.292966399833));
#56865=CARTESIAN_POINT('Ctrl Pts',(58.5590623134716,1.83779450321693,126.240473231501));
#56866=CARTESIAN_POINT('Ctrl Pts',(58.5515719777095,1.71493196756685,126.192910930368));
#56867=CARTESIAN_POINT('Ctrl Pts',(58.5440816419474,1.59055396481745,126.150403038526));
#56868=CARTESIAN_POINT('Ctrl Pts',(58.5363073078283,1.46146013229102,126.106283447045));
#56869=CARTESIAN_POINT('Ctrl Pts',(58.5285329737093,1.33032471582221,126.067469349091));
#56870=CARTESIAN_POINT('Ctrl Pts',(58.5207586395902,1.19762320763845,126.034152895147));
#56871=CARTESIAN_POINT('Ctrl Pts',(58.5129938866431,1.06508524220348,126.000877500754));
#56872=CARTESIAN_POINT('Ctrl Pts',(58.505229133696,0.930985400870419,125.973086363722));
#56873=CARTESIAN_POINT('Ctrl Pts',(58.4974643807489,0.79581717603026,125.950922858118));
#56874=CARTESIAN_POINT('Ctrl Pts',(58.4897073398639,0.660783202176733,125.92878136562));
#56875=CARTESIAN_POINT('Ctrl Pts',(58.4819502989789,0.524683339836303,125.912256444159));
#56876=CARTESIAN_POINT('Ctrl Pts',(58.4741932580939,0.388023855216127,125.901441023051));
#56877=CARTESIAN_POINT('Ctrl Pts',(58.4664420668538,0.251467426576173,125.890633757936));
#56878=CARTESIAN_POINT('Ctrl Pts',(58.4586908756136,0.114352603822298,125.885527453901));
#56879=CARTESIAN_POINT('Ctrl Pts',(58.4509396843735,-0.0228069489639163,
125.886163498135));
#56880=CARTESIAN_POINT('Ctrl Pts',(58.4431917875964,-0.159908205281159,
125.886799272033));
#56881=CARTESIAN_POINT('Ctrl Pts',(58.4354438908193,-0.297053763675912,
125.893172538122));
#56882=CARTESIAN_POINT('Ctrl Pts',(58.4276959940423,-0.433727885739765,
125.905272622476));
#56883=CARTESIAN_POINT('Ctrl Pts',(58.4199497179582,-0.570373418523635,
125.917370175754));
#56884=CARTESIAN_POINT('Ctrl Pts',(58.412203441874,-0.706547321930654,125.935192130097));
#56885=CARTESIAN_POINT('Ctrl Pts',(58.4044571657899,-0.841737307923214,
125.958675798374));
#56886=CARTESIAN_POINT('Ctrl Pts',(58.3967108325246,-0.976928291857541,
125.982159640002));
#56887=CARTESIAN_POINT('Ctrl Pts',(58.3889644992593,-1.11113495868771,126.011305212047));
#56888=CARTESIAN_POINT('Ctrl Pts',(58.3812181659939,-1.24385395748742,126.045998462902));
#56889=CARTESIAN_POINT('Ctrl Pts',(58.3734700979909,-1.37660267778671,126.08069948307));
#56890=CARTESIAN_POINT('Ctrl Pts',(58.365722029988,-1.50786268893686,126.12095055535));
#56891=CARTESIAN_POINT('Ctrl Pts',(58.357973961985,-1.63714496088211,126.16658750544));
#56892=CARTESIAN_POINT('Ctrl Pts',(58.3502176592431,-1.76656463556447,126.212272959024));
#56893=CARTESIAN_POINT('Ctrl Pts',(58.3424613565013,-1.8940020028837,126.263355594724));
#56894=CARTESIAN_POINT('Ctrl Pts',(58.3347050537594,-2.01898670018973,126.319622524103));
#56895=CARTESIAN_POINT('Ctrl Pts',(58.3269446112453,-2.1440381055921,126.375919484837));
#56896=CARTESIAN_POINT('Ctrl Pts',(58.3191841687311,-2.26663388325725,126.437406077568));
#56897=CARTESIAN_POINT('Ctrl Pts',(58.311423726217,-2.38632842043751,126.50382347294));
#56898=CARTESIAN_POINT('Ctrl Pts',(58.3036508259515,-2.50621510191484,126.57034748741));
#56899=CARTESIAN_POINT('Ctrl Pts',(58.2958779256861,-2.62319090226604,126.641817917981));
#56900=CARTESIAN_POINT('Ctrl Pts',(58.2881050254206,-2.73683858809815,126.717932151877));
#56901=CARTESIAN_POINT('Ctrl Pts',(58.2806146896586,-2.84635489428918,126.79127944165));
#56902=CARTESIAN_POINT('Ctrl Pts',(58.2731243538965,-2.95278060686873,126.868938587004));
#56903=CARTESIAN_POINT('Ctrl Pts',(58.2656340181345,-3.05577304874891,126.95060476943));
#56904=CARTESIAN_POINT('Ctrl Pts',(58.2579584955031,-3.16131181812213,127.034290020847));
#56905=CARTESIAN_POINT('Ctrl Pts',(58.2502829728717,-3.26359770182087,127.12246271423));
#56906=CARTESIAN_POINT('Ctrl Pts',(58.2426074502402,-3.36221779805692,127.214837732707));
#56907=CARTESIAN_POINT('Ctrl Pts',(58.2349407074451,-3.46072508525823,127.307107085735));
#56908=CARTESIAN_POINT('Ctrl Pts',(58.2272739646499,-3.55557463086907,127.403568936786));
#56909=CARTESIAN_POINT('Ctrl Pts',(58.2196072218548,-3.6463842256354,127.503896234856));
#56910=CARTESIAN_POINT('Ctrl Pts',(58.2119474876462,-3.73711080641249,127.604131818286));
#56911=CARTESIAN_POINT('Ctrl Pts',(58.2042877534376,-3.82380451202177,127.708225527098));
#56912=CARTESIAN_POINT('Ctrl Pts',(58.196628019229,-3.906118243966,127.815811918506));
#56913=CARTESIAN_POINT('Ctrl Pts',(58.1889735286932,-3.98837562587644,127.923324658814));
#56914=CARTESIAN_POINT('Ctrl Pts',(58.1813190381574,-4.06625875475251,128.034325008515));
#56915=CARTESIAN_POINT('Ctrl Pts',(58.1736645476217,-4.13945963983709,128.148413149588));
#56916=CARTESIAN_POINT('Ctrl Pts',(58.1660126001096,-4.21263620565627,128.26246338757));
#56917=CARTESIAN_POINT('Ctrl Pts',(58.1583606525976,-4.28113340026512,128.379599042323));
#56918=CARTESIAN_POINT('Ctrl Pts',(58.1507087050855,-4.34468576966756,128.49939020011));
#56919=CARTESIAN_POINT('Ctrl Pts',(58.1430584659616,-4.40822395024907,128.619154613099));
#56920=CARTESIAN_POINT('Ctrl Pts',(58.1354082268377,-4.46681931675069,128.741572993394));
#56921=CARTESIAN_POINT('Ctrl Pts',(58.1277579877138,-4.52025207441814,128.86619028289));
#56922=CARTESIAN_POINT('Ctrl Pts',(58.1201050400426,-4.57370374981474,128.990851692813));
#56923=CARTESIAN_POINT('Ctrl Pts',(58.1124520923714,-4.62198900403304,129.117713198785));
#56924=CARTESIAN_POINT('Ctrl Pts',(58.1047991447002,-4.66493598282515,129.246299213563));
#56925=CARTESIAN_POINT('Ctrl Pts',(58.0981996200853,-4.70197133911506,129.35718545062));
#56926=CARTESIAN_POINT('Ctrl Pts',(58.0916000954705,-4.7350376245353,129.46935365218));
#56927=CARTESIAN_POINT('Ctrl Pts',(58.0850005708556,-4.76405452823401,129.582490119308));
#56928=CARTESIAN_POINT('Ctrl Pts',(59.834681232118,-4.76405452823407,129.582490119308));
#56929=CARTESIAN_POINT('Ctrl Pts',(59.826858033056,-4.79847138378228,129.716680916742));
#56930=CARTESIAN_POINT('Ctrl Pts',(59.8190348339941,-4.82723403352823,129.85240374661));
#56931=CARTESIAN_POINT('Ctrl Pts',(59.8112116349321,-4.85021766907435,129.989147991867));
#56932=CARTESIAN_POINT('Ctrl Pts',(59.8033904177206,-4.87319548217733,130.125857595712));
#56933=CARTESIAN_POINT('Ctrl Pts',(59.7955692005092,-4.89039712729127,130.263587726225));
#56934=CARTESIAN_POINT('Ctrl Pts',(59.7877479832978,-4.90174887817213,130.401817454864));
#56935=CARTESIAN_POINT('Ctrl Pts',(59.780118467529,-4.91282239269153,130.536659112609));
#56936=CARTESIAN_POINT('Ctrl Pts',(59.77248895176,-4.9183294285159,130.671975811274));
#56937=CARTESIAN_POINT('Ctrl Pts',(59.7648594359912,-4.91824913396669,130.807279304929));
#56938=CARTESIAN_POINT('',(60.1101405640517,-4.91824820688785,130.800160862287));
#56939=CARTESIAN_POINT('Ctrl Pts',(60.1799785705036,-4.76405452823407,129.582490119308));
#56940=CARTESIAN_POINT('Ctrl Pts',(60.1705897890123,-4.80502007161657,129.742214151218));
#56941=CARTESIAN_POINT('Ctrl Pts',(60.1612010075211,-4.83798653576062,129.904146054801));
#56942=CARTESIAN_POINT('Ctrl Pts',(60.1518122260298,-4.86274682488788,130.067559165652));
#56943=CARTESIAN_POINT('Ctrl Pts',(60.1425322321957,-4.88722021695095,130.229078811467));
#56944=CARTESIAN_POINT('Ctrl Pts',(60.1332522383617,-4.90367645610653,130.39204551948));
#56945=CARTESIAN_POINT('Ctrl Pts',(60.1239722445276,-4.91196185149144,130.555736741012));
#56946=CARTESIAN_POINT('Ctrl Pts',(60.119361684369,-4.91607826735803,130.637063112324));
#56947=CARTESIAN_POINT('Ctrl Pts',(60.1147511242104,-4.91817853369338,130.718567997687));
#56948=CARTESIAN_POINT('Ctrl Pts',(60.1101405640517,-4.91824820688785,130.800160862287));
#56949=CARTESIAN_POINT('Ctrl Pts',(60.1101405640086,-4.91824820688851,130.80016086305));
#56950=CARTESIAN_POINT('Ctrl Pts',(60.1020818223771,-4.91836998778967,130.942776031742));
#56951=CARTESIAN_POINT('Ctrl Pts',(60.0940230807456,-4.91228351706248,131.085495793871));
#56952=CARTESIAN_POINT('Ctrl Pts',(60.0859643391141,-4.89999351809681,131.227735847249));
#56953=CARTESIAN_POINT('Ctrl Pts',(60.0782578572168,-4.88824073349627,131.363758373662));
#56954=CARTESIAN_POINT('Ctrl Pts',(60.0705513753195,-4.87081531724437,131.499341807809));
#56955=CARTESIAN_POINT('Ctrl Pts',(60.0628448934223,-4.8477746302262,131.633977515318));
#56956=CARTESIAN_POINT('Ctrl Pts',(60.0551389575367,-4.82473557566313,131.768603683755));
#56957=CARTESIAN_POINT('Ctrl Pts',(60.0474330216512,-4.79608210801656,131.90228186953));
#56958=CARTESIAN_POINT('Ctrl Pts',(60.0397270857656,-4.76192304593058,132.034511814426));
#56959=CARTESIAN_POINT('Ctrl Pts',(60.0320199848852,-4.72775881962653,132.166761750042));
#56960=CARTESIAN_POINT('Ctrl Pts',(60.0243128840048,-4.68808744182136,132.297562626526));
#56961=CARTESIAN_POINT('Ctrl Pts',(60.0166057831243,-4.64306799604225,132.426428016483));
#56962=CARTESIAN_POINT('Ctrl Pts',(60.0088958057678,-4.598031747919,132.555341502114));
#56963=CARTESIAN_POINT('Ctrl Pts',(60.0011858284111,-4.54764359099658,132.68231769126));
#56964=CARTESIAN_POINT('Ctrl Pts',(59.9934758510546,-4.49211108833518,132.806889277175));
#56965=CARTESIAN_POINT('Ctrl Pts',(59.9857569937017,-4.43651462589887,132.931604338897));
#56966=CARTESIAN_POINT('Ctrl Pts',(59.9780381363489,-4.37576215104937,133.053908907796));
#56967=CARTESIAN_POINT('Ctrl Pts',(59.970319278996,-4.31010778649247,133.173359125653));
#56968=CARTESIAN_POINT('Ctrl Pts',(59.9625952002613,-4.24440901037383,133.292890145003));
#56969=CARTESIAN_POINT('Ctrl Pts',(59.9548711215266,-4.17380194550736,133.409562631417));
#56970=CARTESIAN_POINT('Ctrl Pts',(59.9471470427918,-4.09858390753986,133.522961915174));
#56971=CARTESIAN_POINT('Ctrl Pts',(59.9394117226403,-4.02325639925976,133.636526237204));
#56972=CARTESIAN_POINT('Ctrl Pts',(59.9316764024889,-3.9433047543799,133.746807529783));
#56973=CARTESIAN_POINT('Ctrl Pts',(59.9239410823374,-3.8590666051325,133.853424080279));
#56974=CARTESIAN_POINT('Ctrl Pts',(59.9215376431757,-3.83289299333098,133.886550878876));
#56975=CARTESIAN_POINT('Ctrl Pts',(59.9191342040141,-3.80630582714366,133.91932415076));
#56976=CARTESIAN_POINT('Ctrl Pts',(59.9167307648524,-3.77931593418707,133.951733193557));
#56977=CARTESIAN_POINT('Ctrl Pts',(59.9089564307333,-3.69201251955062,134.056565773138));
#56978=CARTESIAN_POINT('Ctrl Pts',(59.9011820966143,-3.60020566815491,134.157929147634));
#56979=CARTESIAN_POINT('Ctrl Pts',(59.8934077624952,-3.50420152484457,134.255411868385));
#56980=CARTESIAN_POINT('Ctrl Pts',(59.8856430095481,-3.40831569806085,134.352774450394));
#56981=CARTESIAN_POINT('Ctrl Pts',(59.8778782566011,-3.30824314336715,134.44626561864));
#56982=CARTESIAN_POINT('Ctrl Pts',(59.870113503654,-3.20433075125238,134.535506218997));
#56983=CARTESIAN_POINT('Ctrl Pts',(59.862356462769,-3.10052156639065,134.624658184331));
#56984=CARTESIAN_POINT('Ctrl Pts',(59.854599421884,-2.99288042838321,134.709567730124));
#56985=CARTESIAN_POINT('Ctrl Pts',(59.8468423809991,-2.88179137759845,134.789892140274));
#56986=CARTESIAN_POINT('Ctrl Pts',(59.839091189759,-2.77078609993059,134.870155977162));
#56987=CARTESIAN_POINT('Ctrl Pts',(59.8313399985188,-2.65633840036138,134.945841332569));
#56988=CARTESIAN_POINT('Ctrl Pts',(59.8235888072787,-2.53886544860995,135.016645662094));
#56989=CARTESIAN_POINT('Ctrl Pts',(59.8158409105016,-2.42144242599672,135.087419897891));
#56990=CARTESIAN_POINT('Ctrl Pts',(59.8080930137246,-2.30099704273012,135.153317032561));
#56991=CARTESIAN_POINT('Ctrl Pts',(59.8003451169475,-2.17797532123207,135.214077905851));
#56992=CARTESIAN_POINT('Ctrl Pts',(59.7925988408634,-2.05497933322628,135.274826069277));
#56993=CARTESIAN_POINT('Ctrl Pts',(59.7848525647793,-1.9294084292378,135.330439935328));
#56994=CARTESIAN_POINT('Ctrl Pts',(59.7771062886952,-1.80173274106393,135.380706560814));
#56995=CARTESIAN_POINT('Ctrl Pts',(59.7693599554299,-1.67405611041678,135.430973557356));
#56996=CARTESIAN_POINT('Ctrl Pts',(59.7616136221646,-1.5442750283675,135.475893091344));
#56997=CARTESIAN_POINT('Ctrl Pts',(59.7538672888992,-1.41287871264106,135.515300736679));
#56998=CARTESIAN_POINT('Ctrl Pts',(59.7461192208963,-1.28145297162128,135.554717207083));
#56999=CARTESIAN_POINT('Ctrl Pts',(59.7383711528933,-1.14841165155659,135.58861922033));
#57000=CARTESIAN_POINT('Ctrl Pts',(59.7306230848904,-1.01425781211474,135.616892607388));
#57001=CARTESIAN_POINT('Ctrl Pts',(59.7228667821486,-0.879961392375511,
135.645196043739));
#57002=CARTESIAN_POINT('Ctrl Pts',(59.7151104794067,-0.744550474461484,
135.667858823115));
#57003=CARTESIAN_POINT('Ctrl Pts',(59.7073541766648,-0.608537515089716,
135.684818091536));
#57004=CARTESIAN_POINT('Ctrl Pts',(59.6995937341507,-0.472451961506259,
135.701786411629));
#57005=CARTESIAN_POINT('Ctrl Pts',(59.6918332916365,-0.335764115647522,
135.713045122989));
#57006=CARTESIAN_POINT('Ctrl Pts',(59.6840728491224,-0.19898919391101,135.718583482191));
#57007=CARTESIAN_POINT('Ctrl Pts',(59.676299948857,-0.0619947089278186,
135.724130732059));
#57008=CARTESIAN_POINT('Ctrl Pts',(59.6685270485915,0.0750867400721471,
135.723939280121));
#57009=CARTESIAN_POINT('Ctrl Pts',(59.6607541483261,0.211741399057937,135.71805053884));
#57010=CARTESIAN_POINT('Ctrl Pts',(59.653263812564,0.343428316979685,135.712375868137));
#57011=CARTESIAN_POINT('Ctrl Pts',(59.6457734768018,0.474718628998842,135.701410963868));
#57012=CARTESIAN_POINT('Ctrl Pts',(59.6382831410397,0.605161109052965,135.685237904959));
#57013=CARTESIAN_POINT('Ctrl Pts',(59.6305088069206,0.740549355383369,135.668451639606));
#57014=CARTESIAN_POINT('Ctrl Pts',(59.6227344728015,0.875453078793381,135.646001315275));
#57015=CARTESIAN_POINT('Ctrl Pts',(59.6149601386824,1.00936063710604,135.617922102242));
#57016=CARTESIAN_POINT('Ctrl Pts',(59.6071953857353,1.14310316632074,135.589877494331));
#57017=CARTESIAN_POINT('Ctrl Pts',(59.5994306327882,1.27585159419434,135.556217879951));
#57018=CARTESIAN_POINT('Ctrl Pts',(59.5916658798411,1.40709942483922,135.517030165828));
#57019=CARTESIAN_POINT('Ctrl Pts',(59.5839088389561,1.53821689828878,135.477881373495));
#57020=CARTESIAN_POINT('Ctrl Pts',(59.576151798071,1.66783636830249,135.433215519066));
#57021=CARTESIAN_POINT('Ctrl Pts',(59.568394757186,1.79546191491862,135.383170460154));
#57022=CARTESIAN_POINT('Ctrl Pts',(59.5606435659458,1.92299121811709,135.33316314061));
#57023=CARTESIAN_POINT('Ctrl Pts',(59.5528923747057,2.04852922829915,135.277784832949));
#57024=CARTESIAN_POINT('Ctrl Pts',(59.5451411834655,2.17159591587006,135.217222981234));
#57025=CARTESIAN_POINT('Ctrl Pts',(59.5373932866884,2.29461029681568,135.156686869921));
#57026=CARTESIAN_POINT('Ctrl Pts',(59.5296453899114,2.41515509421585,135.090971768705));
#57027=CARTESIAN_POINT('Ctrl Pts',(59.5218974931343,2.53277118319451,135.020312846432));
#57028=CARTESIAN_POINT('Ctrl Pts',(59.5141512170502,2.65036266942285,134.949668704482));
#57029=CARTESIAN_POINT('Ctrl Pts',(59.506404940966,2.76502633084446,134.874082999649));
#57030=CARTESIAN_POINT('Ctrl Pts',(59.4986586648819,2.87632889460038,134.79383616613));
#57031=CARTESIAN_POINT('Ctrl Pts',(59.4909123316166,2.98763227996654,134.713588740247));
#57032=CARTESIAN_POINT('Ctrl Pts',(59.4831659983511,3.09557420102438,134.628680345668));
#57033=CARTESIAN_POINT('Ctrl Pts',(59.4754196650858,3.19975188731087,134.539433698799));
#57034=CARTESIAN_POINT('Ctrl Pts',(59.4676715970828,3.30395290346817,134.450167065762));
#57035=CARTESIAN_POINT('Ctrl Pts',(59.4599235290798,3.40438771057849,134.356560501527));
#57036=CARTESIAN_POINT('Ctrl Pts',(59.4521754610768,3.50068833896314,134.258975533291));
#57037=CARTESIAN_POINT('Ctrl Pts',(59.4444191583349,3.59709131680136,134.161286850589));
#57038=CARTESIAN_POINT('Ctrl Pts',(59.436662855593,3.68935106366185,134.059611596133));
#57039=CARTESIAN_POINT('Ctrl Pts',(59.4289065528512,3.77713770333707,133.95434694016));
#57040=CARTESIAN_POINT('Ctrl Pts',(59.421146110337,3.8649711973852,133.849026101271));
#57041=CARTESIAN_POINT('Ctrl Pts',(59.4133856678228,3.94832658958905,133.740112353848));
#57042=CARTESIAN_POINT('Ctrl Pts',(59.4056252253086,4.026916354152,133.628033356954));
#57043=CARTESIAN_POINT('Ctrl Pts',(59.3978523250431,4.10563227798191,133.515774440904));
#57044=CARTESIAN_POINT('Ctrl Pts',(59.3900794247777,4.1795670756285,133.400340451062));
#57045=CARTESIAN_POINT('Ctrl Pts',(59.3823065245122,4.24847789196826,133.282186007693));
#57046=CARTESIAN_POINT('Ctrl Pts',(59.3748161887503,4.31488362655663,133.168326775956));
#57047=CARTESIAN_POINT('Ctrl Pts',(59.3673258529885,4.37662416264115,133.051941719534));
#57048=CARTESIAN_POINT('Ctrl Pts',(59.3598355172267,4.43352465683783,132.933454833356));
#57049=CARTESIAN_POINT('Ctrl Pts',(59.3520611831075,4.49258255056777,132.810475480873));
#57050=CARTESIAN_POINT('Ctrl Pts',(59.3442868489884,4.54661321459122,132.684842209016));
#57051=CARTESIAN_POINT('Ctrl Pts',(59.3365125148694,4.59536968356444,132.557004487232));
#57052=CARTESIAN_POINT('Ctrl Pts',(59.3287477619223,4.64406606454714,132.429324314014));
#57053=CARTESIAN_POINT('Ctrl Pts',(59.3209830089752,4.68750104550558,132.299445458259));
#57054=CARTESIAN_POINT('Ctrl Pts',(59.3132182560281,4.72547397013043,132.16784102451));
#57055=CARTESIAN_POINT('Ctrl Pts',(59.3054612151431,4.76340917951127,132.036367302139));
#57056=CARTESIAN_POINT('Ctrl Pts',(59.297704174258,4.79589302085066,131.903171785659));
#57057=CARTESIAN_POINT('Ctrl Pts',(59.289947133373,4.82277342081136,131.768746221988));
#57058=CARTESIAN_POINT('Ctrl Pts',(59.2821959421329,4.84963355005316,131.63442202968));
#57059=CARTESIAN_POINT('Ctrl Pts',(59.2744447508928,4.87089857236288,131.498870018313));
#57060=CARTESIAN_POINT('Ctrl Pts',(59.2666935596527,4.886466722017,131.362595368473));
#57061=CARTESIAN_POINT('Ctrl Pts',(59.2589456628757,4.9020282547923,131.226378638994));
#57062=CARTESIAN_POINT('Ctrl Pts',(59.2511977660986,4.91189768645576,131.089440269548));
#57063=CARTESIAN_POINT('Ctrl Pts',(59.2434498693215,4.91602470300874,130.952293649401));
#57064=CARTESIAN_POINT('Ctrl Pts',(59.2357035932374,4.92015085627883,130.81517571737));
#57065=CARTESIAN_POINT('Ctrl Pts',(59.2279573171533,4.91853697191796,130.677850011827));
#57066=CARTESIAN_POINT('Ctrl Pts',(59.2202110410692,4.91118479259633,130.540832639031));
#57067=CARTESIAN_POINT('Ctrl Pts',(59.2124647078038,4.90383255900258,130.403814254805));
#57068=CARTESIAN_POINT('Ctrl Pts',(59.2047183745385,4.89074196687274,130.267104598272));
#57069=CARTESIAN_POINT('Ctrl Pts',(59.1969720412731,4.87196681938482,130.131216967731));
#57070=CARTESIAN_POINT('Ctrl Pts',(59.1892239732701,4.85318746733278,129.995298906097));
#57071=CARTESIAN_POINT('Ctrl Pts',(59.1814759052671,4.82872108026649,129.860203623977));
#57072=CARTESIAN_POINT('Ctrl Pts',(59.1737278372641,4.79867292465472,129.726436118964));
#57073=CARTESIAN_POINT('Ctrl Pts',(59.1659715345222,4.76859283350563,129.592526444256));
#57074=CARTESIAN_POINT('Ctrl Pts',(59.1582152317803,4.73291920908674,129.4599477477));
#57075=CARTESIAN_POINT('Ctrl Pts',(59.1504589290385,4.69180789581938,129.329192243709));
#57076=CARTESIAN_POINT('Ctrl Pts',(59.1426984865243,4.6506746402063,129.198366951569));
#57077=CARTESIAN_POINT('Ctrl Pts',(59.1349380440102,4.60409804545684,129.069367158512));
#57078=CARTESIAN_POINT('Ctrl Pts',(59.127177601496,4.55228249853596,128.942665928305));
#57079=CARTESIAN_POINT('Ctrl Pts',(59.1194047012306,4.50038377269927,128.815761306035));
#57080=CARTESIAN_POINT('Ctrl Pts',(59.1116318009651,4.44322945187069,128.691162975691));
#57081=CARTESIAN_POINT('Ctrl Pts',(59.1038589006997,4.3810707518285,128.569320991525));
#57082=CARTESIAN_POINT('Ctrl Pts',(59.0963685649377,4.32117167710184,128.451908270386));
#57083=CARTESIAN_POINT('Ctrl Pts',(59.0888782291758,4.25662590078738,128.337055242935));
#57084=CARTESIAN_POINT('Ctrl Pts',(59.0813878934138,4.18769563470786,128.225138189479));
#57085=CARTESIAN_POINT('Ctrl Pts',(59.0736135592947,4.11615185663832,128.108977766923));
#57086=CARTESIAN_POINT('Ctrl Pts',(59.0658392251757,4.03965792058266,127.99561238685));
#57087=CARTESIAN_POINT('Ctrl Pts',(59.0580648910566,3.9584584871163,127.885492777413));
#57088=CARTESIAN_POINT('Ctrl Pts',(59.0503001381095,3.87735912469468,127.775508880554));
#57089=CARTESIAN_POINT('Ctrl Pts',(59.0425353851624,3.79156603315425,127.668763106928));
#57090=CARTESIAN_POINT('Ctrl Pts',(59.0347706322153,3.70136878910965,127.565679998934));
#57091=CARTESIAN_POINT('Ctrl Pts',(59.0270135913303,3.61126113023965,127.462699274535));
#57092=CARTESIAN_POINT('Ctrl Pts',(59.0192565504454,3.51675827963859,127.363374268688));
#57093=CARTESIAN_POINT('Ctrl Pts',(59.0114995095604,3.41819175856144,127.268098726218));
#57094=CARTESIAN_POINT('Ctrl Pts',(59.0037483183203,3.31969956726484,127.172895031775));
#57095=CARTESIAN_POINT('Ctrl Pts',(58.9959971270802,3.21715008505486,127.081734993063));
#57096=CARTESIAN_POINT('Ctrl Pts',(58.9882459358401,3.11091332780757,126.994977290915));
#57097=CARTESIAN_POINT('Ctrl Pts',(58.980498039063,3.0047217240155,126.908256463103));
#57098=CARTESIAN_POINT('Ctrl Pts',(58.972750142286,2.89484626439237,126.825934497136));
#57099=CARTESIAN_POINT('Ctrl Pts',(58.9650022455089,2.78169168192374,126.748331223045));
#57100=CARTESIAN_POINT('Ctrl Pts',(58.9572559694248,2.66856076895459,126.670744181886));
#57101=CARTESIAN_POINT('Ctrl Pts',(58.9495096933407,2.55215241969669,126.597874090294));
#57102=CARTESIAN_POINT('Ctrl Pts',(58.9417634172567,2.43290179092059,126.52999845015));
#57103=CARTESIAN_POINT('Ctrl Pts',(58.9340170839913,2.31365028186361,126.462122308964));
#57104=CARTESIAN_POINT('Ctrl Pts',(58.926270750726,2.19155679120304,126.399240886193));
#57105=CARTESIAN_POINT('Ctrl Pts',(58.9185244174606,2.0670822532658,126.341586365967));
#57106=CARTESIAN_POINT('Ctrl Pts',(58.9107763494577,1.94257984011883,126.283918934411));
#57107=CARTESIAN_POINT('Ctrl Pts',(58.9030282814547,1.81569567334134,126.231480898903));
#57108=CARTESIAN_POINT('Ctrl Pts',(58.8952802134518,1.68691152080732,126.184456659315));
#57109=CARTESIAN_POINT('Ctrl Pts',(58.88752391071,1.55799049494325,126.137382441805));
#57110=CARTESIAN_POINT('Ctrl Pts',(58.8797676079681,1.42716581733296,126.095733648455));
#57111=CARTESIAN_POINT('Ctrl Pts',(58.8720113052263,1.2949358396169,126.059645216852));
#57112=CARTESIAN_POINT('Ctrl Pts',(58.8642508627121,1.16263528677999,126.023537523766));
#57113=CARTESIAN_POINT('Ctrl Pts',(58.8564904201979,1.02892832025904,125.992996192904));
#57114=CARTESIAN_POINT('Ctrl Pts',(58.8487299776838,0.894323418144604,125.968104970244));
#57115=CARTESIAN_POINT('Ctrl Pts',(58.8409570774184,0.759502436291817,125.943173789983));
#57116=CARTESIAN_POINT('Ctrl Pts',(58.8331841771529,0.623781025685959,125.923910897756));
#57117=CARTESIAN_POINT('Ctrl Pts',(58.8254112768875,0.487673617979483,125.91034820393));
#57118=CARTESIAN_POINT('Ctrl Pts',(58.8179209411253,0.356514057373872,125.897278548186));
#57119=CARTESIAN_POINT('Ctrl Pts',(58.8104306053631,0.224996383851764,125.889501871051));
#57120=CARTESIAN_POINT('Ctrl Pts',(58.8029402696009,0.0935789045873223,
125.887000954991));
#57121=CARTESIAN_POINT('Ctrl Pts',(58.7951659354818,-0.0428213083436484,
125.884405215939));
#57122=CARTESIAN_POINT('Ctrl Pts',(58.7873916013627,-0.179545654179816,
125.88748497373));
#57123=CARTESIAN_POINT('Ctrl Pts',(58.7796172672437,-0.31608267754306,125.896278018072));
#57124=CARTESIAN_POINT('Ctrl Pts',(58.7718525142966,-0.452451431227674,
125.905060225772));
#57125=CARTESIAN_POINT('Ctrl Pts',(58.7640877613495,-0.588632935366884,
125.919541685416));
#57126=CARTESIAN_POINT('Ctrl Pts',(58.7563230084024,-0.724113487184336,
125.939708243534));
#57127=CARTESIAN_POINT('Ctrl Pts',(58.7485659675174,-0.859459477807414,
125.959854771941));
#57128=CARTESIAN_POINT('Ctrl Pts',(58.7408089266324,-0.994105517367409,
125.985675104803));
#57129=CARTESIAN_POINT('Ctrl Pts',(58.7330518857475,-1.12754114185477,126.017103152595));
#57130=CARTESIAN_POINT('Ctrl Pts',(58.7253006945074,-1.26087614149972,126.048507500251));
#57131=CARTESIAN_POINT('Ctrl Pts',(58.7175495032673,-1.39300216389963,126.085511056355));
#57132=CARTESIAN_POINT('Ctrl Pts',(58.7097983120272,-1.52341743809267,126.127996391822));
#57133=CARTESIAN_POINT('Ctrl Pts',(58.7020504152501,-1.65377728231558,126.170463669889));
#57134=CARTESIAN_POINT('Ctrl Pts',(58.694302518473,-1.7824274535464,126.218407972474));
#57135=CARTESIAN_POINT('Ctrl Pts',(58.6865546216959,-1.90888010165679,126.271661662198));
#57136=CARTESIAN_POINT('Ctrl Pts',(58.6788083456118,-2.03530629859919,126.324904212397));
#57137=CARTESIAN_POINT('Ctrl Pts',(58.6710620695277,-2.15953552665045,126.383453789027));
#57138=CARTESIAN_POINT('Ctrl Pts',(58.6633157934436,-2.28109910275321,126.447094278918));
#57139=CARTESIAN_POINT('Ctrl Pts',(58.6555694601783,-2.40266357621084,126.510735238588));
#57140=CARTESIAN_POINT('Ctrl Pts',(58.6478231269129,-2.52156201208438,126.579467005176));
#57141=CARTESIAN_POINT('Ctrl Pts',(58.6400767936476,-2.6373499210266,126.653027282773));
#57142=CARTESIAN_POINT('Ctrl Pts',(58.6323287256445,-2.75316375986853,126.726604033685));
#57143=CARTESIAN_POINT('Ctrl Pts',(58.6245806576416,-2.86586535572596,126.805011237679));
#57144=CARTESIAN_POINT('Ctrl Pts',(58.6168325896386,-2.9750391604602,126.887943242435));
#57145=CARTESIAN_POINT('Ctrl Pts',(58.6090762868967,-3.0843289964127,126.970963388312));
#57146=CARTESIAN_POINT('Ctrl Pts',(58.6013199841549,-3.19008323963164,127.058517704599));
#57147=CARTESIAN_POINT('Ctrl Pts',(58.5935636814131,-3.29191899206923,127.150259851009));
#57148=CARTESIAN_POINT('Ctrl Pts',(58.5858032388989,-3.39380909731424,127.242050962964));
#57149=CARTESIAN_POINT('Ctrl Pts',(58.5780427963847,-3.4917762653225,127.338034085332));
#57150=CARTESIAN_POINT('Ctrl Pts',(58.5702823538706,-3.58547519340248,127.43782668784));
#57151=CARTESIAN_POINT('Ctrl Pts',(58.5625094536051,-3.67932453532001,127.537779486293));
#57152=CARTESIAN_POINT('Ctrl Pts',(58.5547365533398,-3.76889168971608,127.641553689095));
#57153=CARTESIAN_POINT('Ctrl Pts',(58.5469636530744,-3.85387174662136,127.74873373866));
#57154=CARTESIAN_POINT('Ctrl Pts',(58.5394733173123,-3.93576256440708,127.852017523454));
#57155=CARTESIAN_POINT('Ctrl Pts',(58.5319829815502,-4.01339381816233,127.958463583014));
#57156=CARTESIAN_POINT('Ctrl Pts',(58.5244926457881,-4.08653226726503,128.067677024035));
#57157=CARTESIAN_POINT('Ctrl Pts',(58.5165831192501,-4.16376385240355,128.183002509768));
#57158=CARTESIAN_POINT('Ctrl Pts',(58.5086735927121,-4.23622414022661,128.301770154107));
#57159=CARTESIAN_POINT('Ctrl Pts',(58.5007640661741,-4.30359753563025,128.423555855764));
#57160=CARTESIAN_POINT('Ctrl Pts',(58.4928642412395,-4.3708882927165,128.545192178496));
#57161=CARTESIAN_POINT('Ctrl Pts',(58.4849644163049,-4.43310439364135,128.669838869824));
#57162=CARTESIAN_POINT('Ctrl Pts',(58.4770645913703,-4.48997264878427,128.797041839776));
#57163=CARTESIAN_POINT('Ctrl Pts',(58.4691757325853,-4.54676196220404,128.924068232803));
#57164=CARTESIAN_POINT('Ctrl Pts',(58.4612868738004,-4.59821806827637,129.053643497022));
#57165=CARTESIAN_POINT('Ctrl Pts',(58.4533980150154,-4.6441133165706,129.185288486575));
#57166=CARTESIAN_POINT('Ctrl Pts',(58.445576034428,-4.689619485587,129.315817449102));
#57167=CARTESIAN_POINT('Ctrl Pts',(58.4377540538405,-4.72965858030162,129.448380840351));
#57168=CARTESIAN_POINT('Ctrl Pts',(58.429932073253,-4.76405452823401,129.582490119308));
#57169=CARTESIAN_POINT('Origin',(213.235140564004,0.,130.804360617566));
#57170=CARTESIAN_POINT('',(56.3348795324218,-4.7640545282341,129.582490119308));
#57171=CARTESIAN_POINT('',(56.6802739192585,-4.76405452823399,129.582490119308));
#57172=CARTESIAN_POINT('',(213.235140564004,-4.76405452823405,129.582490119308));
#57173=CARTESIAN_POINT('',(58.014859436029,-4.91824920186863,130.807162548786));
#57174=CARTESIAN_POINT('Ctrl Pts',(58.0148594359912,-4.91824920186825,130.807162549451));
#57175=CARTESIAN_POINT('Ctrl Pts',(58.005635088768,-4.91815684843496,130.969271129642));
#57176=CARTESIAN_POINT('Ctrl Pts',(57.9964107415448,-4.91005038252175,131.1311482706));
#57177=CARTESIAN_POINT('Ctrl Pts',(57.9871863943216,-4.89399391332884,131.292219858331));
#57178=CARTESIAN_POINT('Ctrl Pts',(57.9794120602026,-4.88046142661098,131.427971940275));
#57179=CARTESIAN_POINT('Ctrl Pts',(57.9716377260835,-4.86125488480983,131.563375560627));
#57180=CARTESIAN_POINT('Ctrl Pts',(57.9638633919644,-4.83639717007311,131.697918380561));
#57181=CARTESIAN_POINT('Ctrl Pts',(57.9560986390173,-4.81157009024821,131.832295388494));
#57182=CARTESIAN_POINT('Ctrl Pts',(57.9483338860702,-4.78110576524688,131.965813326035));
#57183=CARTESIAN_POINT('Ctrl Pts',(57.9405691331231,-4.74507892226327,132.097963757634));
#57184=CARTESIAN_POINT('Ctrl Pts',(57.9328120922381,-4.70908786164799,132.229982935561));
#57185=CARTESIAN_POINT('Ctrl Pts',(57.9250550513531,-4.66754537976121,132.360636935718));
#57186=CARTESIAN_POINT('Ctrl Pts',(57.9172980104681,-4.62057739380636,132.489426672754));
#57187=CARTESIAN_POINT('Ctrl Pts',(57.909546819228,-4.57364482677502,132.618119288447));
#57188=CARTESIAN_POINT('Ctrl Pts',(57.9017956279878,-4.5212950327972,132.744950073473));
#57189=CARTESIAN_POINT('Ctrl Pts',(57.8940444367477,-4.46370388256866,132.869434638332));
#57190=CARTESIAN_POINT('Ctrl Pts',(57.8862965399706,-4.40613721011535,132.99386629393));
#57191=CARTESIAN_POINT('Ctrl Pts',(57.8785486431936,-4.34333377598378,133.115953358639));
#57192=CARTESIAN_POINT('Ctrl Pts',(57.8708007464165,-4.27551766356744,133.235231196396));
#57193=CARTESIAN_POINT('Ctrl Pts',(57.8630544703324,-4.20771573681978,133.354484083801));
#57194=CARTESIAN_POINT('Ctrl Pts',(57.8553081942482,-4.13490341051346,133.470928573425));
#57195=CARTESIAN_POINT('Ctrl Pts',(57.8475619181641,-4.05735064073519,133.584124787532));
#57196=CARTESIAN_POINT('Ctrl Pts',(57.8398155848988,-3.9797972984801,133.697321837227));
#57197=CARTESIAN_POINT('Ctrl Pts',(57.8320692516335,-3.89750366389842,133.80727024103));
#57198=CARTESIAN_POINT('Ctrl Pts',(57.8243229183681,-3.81078269508045,133.913559600162));
#57199=CARTESIAN_POINT('Ctrl Pts',(57.8165748503652,-3.7240423057028,134.019872762058));
#57200=CARTESIAN_POINT('Ctrl Pts',(57.8088267823621,-3.63287285628821,134.122524945865));
#57201=CARTESIAN_POINT('Ctrl Pts',(57.8010787143592,-3.53762693966327,134.221139612214));
#57202=CARTESIAN_POINT('Ctrl Pts',(57.7933224116173,-3.4422797945447,134.319859087404));
#57203=CARTESIAN_POINT('Ctrl Pts',(57.7855661088755,-3.34284779958689,134.414532191494));
#57204=CARTESIAN_POINT('Ctrl Pts',(57.7778098061336,-3.23972009453267,134.504819612283));
#57205=CARTESIAN_POINT('Ctrl Pts',(57.7700493636195,-3.13653734711714,134.595155222187));
#57206=CARTESIAN_POINT('Ctrl Pts',(57.7622889211053,-3.02965526374008,134.681100239727));
#57207=CARTESIAN_POINT('Ctrl Pts',(57.7545284785912,-2.91949448048244,134.762356959269));
#57208=CARTESIAN_POINT('Ctrl Pts',(57.7467555783257,-2.80915685735589,134.843744119311));
#57209=CARTESIAN_POINT('Ctrl Pts',(57.7389826780604,-2.69553034093435,134.920427723032));
#57210=CARTESIAN_POINT('Ctrl Pts',(57.7312097777949,-2.57906359271026,134.992154075612));
#57211=CARTESIAN_POINT('Ctrl Pts',(57.7237194420329,-2.46683070414553,135.061272994609));
#57212=CARTESIAN_POINT('Ctrl Pts',(57.7162291062708,-2.35196076637003,135.125788671392));
#57213=CARTESIAN_POINT('Ctrl Pts',(57.7087387705087,-2.23487345645436,135.185516138218));
#57214=CARTESIAN_POINT('Ctrl Pts',(57.7009644363896,-2.11334674559567,135.247508190102));
#57215=CARTESIAN_POINT('Ctrl Pts',(57.6931901022706,-1.98904623997409,135.304538146744));
#57216=CARTESIAN_POINT('Ctrl Pts',(57.6854157681515,-1.86241535311417,135.356348327895));
#57217=CARTESIAN_POINT('Ctrl Pts',(57.6776510152044,-1.73594052750498,135.408094657627));
#57218=CARTESIAN_POINT('Ctrl Pts',(57.6698862622573,-1.60714139343105,135.454633864807));
#57219=CARTESIAN_POINT('Ctrl Pts',(57.6621215093102,-1.47648610399494,135.495753997705));
#57220=CARTESIAN_POINT('Ctrl Pts',(57.6543644684252,-1.34596058323421,135.536833289507));
#57221=CARTESIAN_POINT('Ctrl Pts',(57.6466074275401,-1.21358294639676,135.572504101437));
#57222=CARTESIAN_POINT('Ctrl Pts',(57.6388503866551,-1.07984114944792,135.602602603383));
#57223=CARTESIAN_POINT('Ctrl Pts',(57.631099195415,-0.9462002082287,135.632678407815));
#57224=CARTESIAN_POINT('Ctrl Pts',(57.6233480041749,-0.811197534392437,
135.657190180838));
#57225=CARTESIAN_POINT('Ctrl Pts',(57.6155968129347,-0.675335720949953,
135.676024063096));
#57226=CARTESIAN_POINT('Ctrl Pts',(57.6078489161576,-0.539531652402228,
135.694849940451));
#57227=CARTESIAN_POINT('Ctrl Pts',(57.6001010193805,-0.402869556969357,
135.708002673248));
#57228=CARTESIAN_POINT('Ctrl Pts',(57.5923531226034,-0.265861468678331,
135.715419642051));
#57229=CARTESIAN_POINT('Ctrl Pts',(57.5846068465193,-0.128882039525824,
135.722835059384));
#57230=CARTESIAN_POINT('Ctrl Pts',(57.5768605704352,0.00844284838225112,
135.724517078066));
#57231=CARTESIAN_POINT('Ctrl Pts',(57.5691142943511,0.145597195590896,135.720455055139));
#57232=CARTESIAN_POINT('Ctrl Pts',(57.5613679610858,0.282752555241587,135.716393002227));
#57233=CARTESIAN_POINT('Ctrl Pts',(57.5536216278204,0.419736980886966,135.706586834671));
#57234=CARTESIAN_POINT('Ctrl Pts',(57.5458752945551,0.556036030918943,135.691078022411));
#57235=CARTESIAN_POINT('Ctrl Pts',(57.5381272265521,0.69236560417833,135.675565737061));
#57236=CARTESIAN_POINT('Ctrl Pts',(57.5303791585491,0.828009108022459,135.654348309982));
#57237=CARTESIAN_POINT('Ctrl Pts',(57.5226310905462,0.962459164181244,135.627518858779));
#57238=CARTESIAN_POINT('Ctrl Pts',(57.5148747878043,1.09705211545969,135.600660892917));
#57239=CARTESIAN_POINT('Ctrl Pts',(57.5071184850624,1.23044870124893,135.568179064778));
#57240=CARTESIAN_POINT('Ctrl Pts',(57.4993621823205,1.3621531090474,135.530217362116));
#57241=CARTESIAN_POINT('Ctrl Pts',(57.4916017398063,1.49392781145386,135.492235398151));
#57242=CARTESIAN_POINT('Ctrl Pts',(57.4838412972922,1.62400816560539,135.448767855652));
#57243=CARTESIAN_POINT('Ctrl Pts',(57.476080854778,1.75191633924377,135.4000077105));
#57244=CARTESIAN_POINT('Ctrl Pts',(57.4683079545126,1.88002984243764,135.351169291234));
#57245=CARTESIAN_POINT('Ctrl Pts',(57.4605350542471,2.0059638376489,135.29702144581));
#57246=CARTESIAN_POINT('Ctrl Pts',(57.4527621539817,2.12926237174458,135.237804517603));
#57247=CARTESIAN_POINT('Ctrl Pts',(57.4452718182197,2.24807869355462,135.180740273894));
#57248=CARTESIAN_POINT('Ctrl Pts',(57.4377814824578,2.36444756683125,135.118969241143));
#57249=CARTESIAN_POINT('Ctrl Pts',(57.4302911466958,2.47798652726619,135.05274452597));
#57250=CARTESIAN_POINT('Ctrl Pts',(57.4225168125767,2.59583035189627,134.984008880593));
#57251=CARTESIAN_POINT('Ctrl Pts',(57.4147424784576,2.71099872908913,134.91025742944));
#57252=CARTESIAN_POINT('Ctrl Pts',(57.4069681443385,2.82303518931051,134.831723946397));
#57253=CARTESIAN_POINT('Ctrl Pts',(57.3992033913914,2.93493357460766,134.753287248854));
#57254=CARTESIAN_POINT('Ctrl Pts',(57.3914386384444,3.04370740572751,134.670080467841));
#57255=CARTESIAN_POINT('Ctrl Pts',(57.3836738854973,3.14892531348982,134.582382908734));
#57256=CARTESIAN_POINT('Ctrl Pts',(57.3759168446123,3.25403871734283,134.49477245208));
#57257=CARTESIAN_POINT('Ctrl Pts',(57.3681598037273,3.35560292788416,134.402680342236));
#57258=CARTESIAN_POINT('Ctrl Pts',(57.3604027628423,3.45321635808074,134.306428556196));
#57259=CARTESIAN_POINT('Ctrl Pts',(57.3526515716021,3.55075617723029,134.210249354378));
#57260=CARTESIAN_POINT('Ctrl Pts',(57.344900380362,3.64435086891673,134.109916993458));
#57261=CARTESIAN_POINT('Ctrl Pts',(57.3371491891219,3.73363297623808,134.005792775405));
#57262=CARTESIAN_POINT('Ctrl Pts',(57.3294012923448,3.82287713628215,133.901712812923));
#57263=CARTESIAN_POINT('Ctrl Pts',(57.3216533955677,3.90781210362773,133.793844494914));
#57264=CARTESIAN_POINT('Ctrl Pts',(57.3139054987906,3.98810842787089,133.682584762772));
#57265=CARTESIAN_POINT('Ctrl Pts',(57.3061592227065,4.068387955854,133.571348303767));
#57266=CARTESIAN_POINT('Ctrl Pts',(57.2984129466224,4.14403054206982,133.45672215851));
#57267=CARTESIAN_POINT('Ctrl Pts',(57.2906666705383,4.21474832198624,133.339134699178));
#57268=CARTESIAN_POINT('Ctrl Pts',(57.282920337273,4.28546662392524,133.221546371843));
#57269=CARTESIAN_POINT('Ctrl Pts',(57.2751740040076,4.3512598455273,133.100997021854));
#57270=CARTESIAN_POINT('Ctrl Pts',(57.2674276707423,4.41188480837251,132.977941879022));
#57271=CARTESIAN_POINT('Ctrl Pts',(57.2596796027393,4.47252334775781,132.854859178844));
#57272=CARTESIAN_POINT('Ctrl Pts',(57.2519315347363,4.52799115255192,132.729269919836));
#57273=CARTESIAN_POINT('Ctrl Pts',(57.2441834667333,4.57809231488464,132.601651306045));
#57274=CARTESIAN_POINT('Ctrl Pts',(57.2364271639914,4.6282467253289,132.473897057673));
#57275=CARTESIAN_POINT('Ctrl Pts',(57.2286708612496,4.67302295639439,132.34410951054));
#57276=CARTESIAN_POINT('Ctrl Pts',(57.2209145585077,4.71227415028793,132.212783634642));
#57277=CARTESIAN_POINT('Ctrl Pts',(57.2131541159935,4.75154629372549,132.081387666169));
#57278=CARTESIAN_POINT('Ctrl Pts',(57.2053936734793,4.78528742796441,131.94845211168));
#57279=CARTESIAN_POINT('Ctrl Pts',(57.1976332309652,4.81340162907112,131.814483293163));
#57280=CARTESIAN_POINT('Ctrl Pts',(57.1898603306997,4.84156096158931,131.680299416005));
#57281=CARTESIAN_POINT('Ctrl Pts',(57.1820874304343,4.86407524620841,131.545079346112));
#57282=CARTESIAN_POINT('Ctrl Pts',(57.1743145301689,4.88090023680959,131.409336601232));
#57283=CARTESIAN_POINT('Ctrl Pts',(57.1668241944069,4.89711359662268,131.278528447044));
#57284=CARTESIAN_POINT('Ctrl Pts',(57.159333858645,4.90804409579596,131.147235266175));
#57285=CARTESIAN_POINT('Ctrl Pts',(57.151843522883,4.91369794879832,131.015915646991));
#57286=CARTESIAN_POINT('Ctrl Pts',(57.1440691887639,4.91956616935576,130.879617004532));
#57287=CARTESIAN_POINT('Ctrl Pts',(57.1362948546449,4.91976830576783,130.742858126234));
#57288=CARTESIAN_POINT('Ctrl Pts',(57.1285205205258,4.91425430569275,130.606149413341));
#57289=CARTESIAN_POINT('Ctrl Pts',(57.1207557675787,4.90874710112997,130.469609181719));
#57290=CARTESIAN_POINT('Ctrl Pts',(57.1129910146315,4.89753779239387,130.333119379387));
#57291=CARTESIAN_POINT('Ctrl Pts',(57.1052262616844,4.88062820142956,130.197193900831));
#57292=CARTESIAN_POINT('Ctrl Pts',(57.0974692207994,4.86373540530941,130.061403425378));
#57293=CARTESIAN_POINT('Ctrl Pts',(57.0897121799145,4.84115364175492,129.926176543756));
#57294=CARTESIAN_POINT('Ctrl Pts',(57.0819551390295,4.81293673153005,129.792025158941));
#57295=CARTESIAN_POINT('Ctrl Pts',(57.0742039477894,4.78474109989663,129.657974938729));
#57296=CARTESIAN_POINT('Ctrl Pts',(57.0664527565493,4.75091886012837,129.524998982043));
#57297=CARTESIAN_POINT('Ctrl Pts',(57.0587015653091,4.71157536637377,129.39360173332));
#57298=CARTESIAN_POINT('Ctrl Pts',(57.0509536685321,4.67224859465355,129.262260331933));
#57299=CARTESIAN_POINT('Ctrl Pts',(57.0432057717549,4.62740534822537,129.132496677708));
#57300=CARTESIAN_POINT('Ctrl Pts',(57.0354578749779,4.57720150913501,129.004802503119));
#57301=CARTESIAN_POINT('Ctrl Pts',(57.0277115988938,4.52700817160558,128.877135039399));
#57302=CARTESIAN_POINT('Ctrl Pts',(57.0199653228097,4.47145661474297,128.751536557896));
#57303=CARTESIAN_POINT('Ctrl Pts',(57.0122190467256,4.41075164237998,128.628480792819));
#57304=CARTESIAN_POINT('Ctrl Pts',(57.0044727134603,4.35004622190669,128.505424119372));
#57305=CARTESIAN_POINT('Ctrl Pts',(56.9967263801949,4.28418748299094,128.384910550427));
#57306=CARTESIAN_POINT('Ctrl Pts',(56.9889800469296,4.213426979489,128.267390741707));
#57307=CARTESIAN_POINT('Ctrl Pts',(56.9812319789266,4.14265062966281,128.149844615242));
#57308=CARTESIAN_POINT('Ctrl Pts',(56.9734839109236,4.06697053255439,128.035293917956));
#57309=CARTESIAN_POINT('Ctrl Pts',(56.9657358429207,3.98668228045549,127.924161413135));
#57310=CARTESIAN_POINT('Ctrl Pts',(56.9579795401788,3.90630869704693,127.812910795366));
#57311=CARTESIAN_POINT('Ctrl Pts',(56.950223237437,3.82131740448047,127.705085944579));
#57312=CARTESIAN_POINT('Ctrl Pts',(56.9424669346951,3.73204545480885,127.601077959769));
#57313=CARTESIAN_POINT('Ctrl Pts',(56.934706492181,3.64272585800965,127.497014462766));
#57314=CARTESIAN_POINT('Ctrl Pts',(56.9269460496668,3.54912131831683,127.3967721766));
#57315=CARTESIAN_POINT('Ctrl Pts',(56.9191856071527,3.45160596953027,127.300705484194));
#57316=CARTESIAN_POINT('Ctrl Pts',(56.9114127068872,3.35393408044883,127.204484577006));
#57317=CARTESIAN_POINT('Ctrl Pts',(56.9036398066218,3.25233912679516,127.112452921007));
#57318=CARTESIAN_POINT('Ctrl Pts',(56.8958669063564,3.14722922948623,127.024925310597));
#57319=CARTESIAN_POINT('Ctrl Pts',(56.8883765705942,3.04594034169891,126.940579549292));
#57320=CARTESIAN_POINT('Ctrl Pts',(56.8808862348321,2.94138787201112,126.860416239494));
#57321=CARTESIAN_POINT('Ctrl Pts',(56.87339589907,2.83396100287565,126.784678031008));
#57322=CARTESIAN_POINT('Ctrl Pts',(56.8656215649509,2.72246101134678,126.706068185327));
#57323=CARTESIAN_POINT('Ctrl Pts',(56.8578472308319,2.60751115349037,126.631976607998));
#57324=CARTESIAN_POINT('Ctrl Pts',(56.8500728967128,2.48951378981403,126.562721293811));
#57325=CARTESIAN_POINT('Ctrl Pts',(56.8423081437657,2.3716618473427,126.493551330609));
#57326=CARTESIAN_POINT('Ctrl Pts',(56.8345433908186,2.25077020587402,126.429205967404));
#57327=CARTESIAN_POINT('Ctrl Pts',(56.8267786378715,2.12727220419992,126.369961443863));
#57328=CARTESIAN_POINT('Ctrl Pts',(56.8190215969865,2.00389686248211,126.310775762818));
#57329=CARTESIAN_POINT('Ctrl Pts',(56.8112645561015,1.87792066235791,126.256681007429));
#57330=CARTESIAN_POINT('Ctrl Pts',(56.8035075152166,1.74980337373552,126.207908592823));
#57331=CARTESIAN_POINT('Ctrl Pts',(56.7957563239764,1.62178269935692,126.159172957875));
#57332=CARTESIAN_POINT('Ctrl Pts',(56.7880051327362,1.49162451417256,126.11575181338));
#57333=CARTESIAN_POINT('Ctrl Pts',(56.7802539414961,1.3598101680658,126.07782918645));
#57334=CARTESIAN_POINT('Ctrl Pts',(56.772506044719,1.22805184657257,126.039922677649));
#57335=CARTESIAN_POINT('Ctrl Pts',(56.764758147942,1.09463913912374,126.007510146134));
#57336=CARTESIAN_POINT('Ctrl Pts',(56.7570102511649,0.960070012230005,125.980726237338));
#57337=CARTESIAN_POINT('Ctrl Pts',(56.7492639750808,0.825529034296639,125.953947931159));
#57338=CARTESIAN_POINT('Ctrl Pts',(56.7415176989967,0.689832501267799,125.932795982084));
#57339=CARTESIAN_POINT('Ctrl Pts',(56.7337714229126,0.553489680624103,125.917354147758));
#57340=CARTESIAN_POINT('Ctrl Pts',(56.7260250896473,0.417145853528676,125.901912199445));
#57341=CARTESIAN_POINT('Ctrl Pts',(56.7182787563819,0.280156117780283,125.892180493989));
#57342=CARTESIAN_POINT('Ctrl Pts',(56.7105324231166,0.143035593806511,125.888190982433));
#57343=CARTESIAN_POINT('Ctrl Pts',(56.7027843551136,0.00588436264212172,
125.884200577454));
#57344=CARTESIAN_POINT('Ctrl Pts',(56.6950362871106,-0.131397324304559,
125.885954936584));
#57345=CARTESIAN_POINT('Ctrl Pts',(56.6872882191077,-0.268294009455447,
125.893433883538));
#57346=CARTESIAN_POINT('Ctrl Pts',(56.6795319163658,-0.405336190032405,
125.900920779206));
#57347=CARTESIAN_POINT('Ctrl Pts',(56.671775613624,-0.541992160417936,125.914144395102));
#57348=CARTESIAN_POINT('Ctrl Pts',(56.6640193108822,-0.677750693083948,
125.933032558348));
#57349=CARTESIAN_POINT('Ctrl Pts',(56.656258868368,-0.81358168416664,125.951930802775));
#57350=CARTESIAN_POINT('Ctrl Pts',(56.6484984258538,-0.948513898649796,
125.97649954881));
#57351=CARTESIAN_POINT('Ctrl Pts',(56.6407379833396,-1.08204695568472,126.006615579718));
#57352=CARTESIAN_POINT('Ctrl Pts',(56.6329650830742,-1.21579437183731,126.036779955552));
#57353=CARTESIAN_POINT('Ctrl Pts',(56.6251921828088,-1.34813776454576,126.072509309314));
#57354=CARTESIAN_POINT('Ctrl Pts',(56.6174192825434,-1.47859168904217,126.11363043138));
#57355=CARTESIAN_POINT('Ctrl Pts',(56.6099289467813,-1.60430328478988,126.153256697081));
#57356=CARTESIAN_POINT('Ctrl Pts',(56.6024386110192,-1.72826011136683,126.197889423865));
#57357=CARTESIAN_POINT('Ctrl Pts',(56.5949482752572,-1.85004765799785,126.24733233966));
#57358=CARTESIAN_POINT('Ctrl Pts',(56.5871735890506,-1.9764585411689,126.298652222727));
#57359=CARTESIAN_POINT('Ctrl Pts',(56.579398902844,-2.10093263870519,126.355317294945));
#57360=CARTESIAN_POINT('Ctrl Pts',(56.5716242166374,-2.22298486132498,126.417160899201));
#57361=CARTESIAN_POINT('Ctrl Pts',(56.5638591924093,-2.34488540374524,126.47892764742));
#57362=CARTESIAN_POINT('Ctrl Pts',(56.5560941681812,-2.46436971456976,126.545859947179));
#57363=CARTESIAN_POINT('Ctrl Pts',(56.5483291439531,-2.58097110765602,126.617742506973));
#57364=CARTESIAN_POINT('Ctrl Pts',(56.5405719122506,-2.69745548638277,126.689552929621));
#57365=CARTESIAN_POINT('Ctrl Pts',(56.5328146805481,-2.81106237440224,126.766303521817));
#57366=CARTESIAN_POINT('Ctrl Pts',(56.5250574488456,-2.92134852833313,126.84773252808));
#57367=CARTESIAN_POINT('Ctrl Pts',(56.5171333689946,-3.03400679660734,126.93091296829));
#57368=CARTESIAN_POINT('Ctrl Pts',(56.5092092891436,-3.14319947597826,127.018975197812));
#57369=CARTESIAN_POINT('Ctrl Pts',(56.5012852092927,-3.24848352729114,127.111592301598));
#57370=CARTESIAN_POINT('Ctrl Pts',(56.4935376544102,-3.35142216258106,127.202146171337));
#57371=CARTESIAN_POINT('Ctrl Pts',(56.4857900995278,-3.45062417595126,127.297053837237));
#57372=CARTESIAN_POINT('Ctrl Pts',(56.4780425446454,-3.54570794400332,127.395968292975));
#57373=CARTESIAN_POINT('Ctrl Pts',(56.4702966872692,-3.64077087899478,127.49486107634));
#57374=CARTESIAN_POINT('Ctrl Pts',(56.4625508298929,-3.73171709344343,127.597758621025));
#57375=CARTESIAN_POINT('Ctrl Pts',(56.4548049725166,-3.81820176637489,127.704277016475));
#57376=CARTESIAN_POINT('Ctrl Pts',(56.4470591348612,-3.90468621911755,127.810795140732));
#57377=CARTESIAN_POINT('Ctrl Pts',(56.4393132972058,-3.98670890717965,127.920933793503));
#57378=CARTESIAN_POINT('Ctrl Pts',(56.4315674595503,-4.06396551489316,128.034276258515));
#57379=CARTESIAN_POINT('Ctrl Pts',(56.4235101322896,-4.14432890476678,128.152176655317));
#57380=CARTESIAN_POINT('Ctrl Pts',(56.4154528050289,-4.21953462021701,128.273543546488));
#57381=CARTESIAN_POINT('Ctrl Pts',(56.4073954777682,-4.28929058584831,128.397875767696));
#57382=CARTESIAN_POINT('Ctrl Pts',(56.3996411023675,-4.35642375872829,128.517533153633));
#57383=CARTESIAN_POINT('Ctrl Pts',(56.3918867269668,-4.41850943101319,128.639936542851));
#57384=CARTESIAN_POINT('Ctrl Pts',(56.3841323515661,-4.47533513597769,128.764615907269));
#57385=CARTESIAN_POINT('Ctrl Pts',(56.3763737897062,-4.53219152020112,128.889362584015));
#57386=CARTESIAN_POINT('Ctrl Pts',(56.3686152278464,-4.58378213233051,129.01638732268));
#57387=CARTESIAN_POINT('Ctrl Pts',(56.3608566659866,-4.62994337852036,129.145201983138));
#57388=CARTESIAN_POINT('Ctrl Pts',(56.3530891692021,-4.67615778498204,129.274164989297));
#57389=CARTESIAN_POINT('Ctrl Pts',(56.3453216724176,-4.71693023038613,129.404921659424));
#57390=CARTESIAN_POINT('Ctrl Pts',(56.3375541756331,-4.75214743207228,129.53697044625));
#57391=CARTESIAN_POINT('Ctrl Pts',(56.336662627896,-4.75618963734661,129.552126911756));
#57392=CARTESIAN_POINT('Ctrl Pts',(56.3357710801589,-4.76015871201734,129.567300391007));
#57393=CARTESIAN_POINT('Ctrl Pts',(56.3348795324218,-4.7640545282341,129.582490119308));
#57394=CARTESIAN_POINT('Ctrl Pts',(58.0850005708556,-4.76405452823401,129.582490119308));
#57395=CARTESIAN_POINT('Ctrl Pts',(58.0773406290219,-4.7977338926578,129.713805450041));
#57396=CARTESIAN_POINT('Ctrl Pts',(58.0696806871882,-4.82595685688633,129.846425082283));
#57397=CARTESIAN_POINT('Ctrl Pts',(58.0620207453545,-4.84864573011683,129.979850068016));
#57398=CARTESIAN_POINT('Ctrl Pts',(58.0541605271336,-4.87192782528797,130.116763575552));
#57399=CARTESIAN_POINT('Ctrl Pts',(58.0463003089126,-4.88938240304201,130.254524676396));
#57400=CARTESIAN_POINT('Ctrl Pts',(58.0384400906917,-4.90098241019879,130.392590684931));
#57401=CARTESIAN_POINT('Ctrl Pts',(58.0305798724708,-4.91258241735558,130.530656693466));
#57402=CARTESIAN_POINT('Ctrl Pts',(58.0227196542499,-4.91832789773181,130.669027157201));
#57403=CARTESIAN_POINT('Ctrl Pts',(58.014859436029,-4.91824920186863,130.807162548786));
#57404=CARTESIAN_POINT('',(58.360140563961,-4.91824943933405,130.80670901921));
#57405=CARTESIAN_POINT('Ctrl Pts',(58.429932073253,-4.76405452823401,129.582490119308));
#57406=CARTESIAN_POINT('Ctrl Pts',(58.4220562464825,-4.79868725641491,129.71752260086));
#57407=CARTESIAN_POINT('Ctrl Pts',(58.4141804197121,-4.82759868947349,129.854122001551));
#57408=CARTESIAN_POINT('Ctrl Pts',(58.4063045929416,-4.85065810554657,129.991772772718));
#57409=CARTESIAN_POINT('Ctrl Pts',(58.398432893145,-4.87370543836646,130.129351414169));
#57410=CARTESIAN_POINT('Ctrl Pts',(58.3905611933484,-4.89090679894885,130.267979961966));
#57411=CARTESIAN_POINT('Ctrl Pts',(58.3826894935518,-4.90218243012851,130.407132113756));
#57412=CARTESIAN_POINT('Ctrl Pts',(58.3751731837041,-4.91294899133708,130.54000185166));
#57413=CARTESIAN_POINT('Ctrl Pts',(58.3676568738563,-4.91831311720544,130.673348625442));
#57414=CARTESIAN_POINT('Ctrl Pts',(58.3601405640086,-4.91824943933446,130.806709018365));
#57415=CARTESIAN_POINT('Ctrl Pts',(58.360140563961,-4.91824943933405,130.80670901921));
#57416=CARTESIAN_POINT('Ctrl Pts',(58.3516434233677,-4.91817745187903,130.957472097261));
#57417=CARTESIAN_POINT('Ctrl Pts',(58.3431462827744,-4.91116916197694,131.108002699756));
#57418=CARTESIAN_POINT('Ctrl Pts',(58.3346491421812,-4.89731318198262,131.257689041646));
#57419=CARTESIAN_POINT('Ctrl Pts',(58.3261097318004,-4.88338827417381,131.408120011662));
#57420=CARTESIAN_POINT('Ctrl Pts',(58.3175703214197,-4.86254746430372,131.557698053368));
#57421=CARTESIAN_POINT('Ctrl Pts',(58.3090309110389,-4.83493105773902,131.705817621205));
#57422=CARTESIAN_POINT('Ctrl Pts',(58.3004697617653,-4.80724434771368,131.854314259035));
#57423=CARTESIAN_POINT('Ctrl Pts',(58.2919086124917,-4.77274761906352,132.001344755767));
#57424=CARTESIAN_POINT('Ctrl Pts',(58.2833474632182,-4.73163116557672,132.146317984789));
#57425=CARTESIAN_POINT('Ctrl Pts',(58.2747562731633,-4.69037043585458,132.291799919935));
#57426=CARTESIAN_POINT('Ctrl Pts',(58.2661650831084,-4.64244356693815,132.435209897501));
#57427=CARTESIAN_POINT('Ctrl Pts',(58.2575738930536,-4.58809023710242,132.57597317078));
#57428=CARTESIAN_POINT('Ctrl Pts',(58.2537309360275,-4.56377724792976,132.638938511625));
#57429=CARTESIAN_POINT('Ctrl Pts',(58.2498879790014,-4.53817901021214,132.701374596378));
#57430=CARTESIAN_POINT('Ctrl Pts',(58.2460450219752,-4.51131992370108,132.763231621108));
#57431=CARTESIAN_POINT('Ctrl Pts',(58.2382706878561,-4.45698376764921,132.888368898106));
#57432=CARTESIAN_POINT('Ctrl Pts',(58.2304963537371,-4.39735091938783,133.011441864516));
#57433=CARTESIAN_POINT('Ctrl Pts',(58.2227220196179,-4.33259960350039,133.131969635045));
#57434=CARTESIAN_POINT('Ctrl Pts',(58.2149572666708,-4.2679280878227,133.252348865869));
#57435=CARTESIAN_POINT('Ctrl Pts',(58.2071925137237,-4.19815083891782,133.370188800859));
#57436=CARTESIAN_POINT('Ctrl Pts',(58.1994277607765,-4.12349425874082,133.485028101726));
#57437=CARTESIAN_POINT('Ctrl Pts',(58.1916707198915,-4.04891182853172,133.59975334258));
#57438=CARTESIAN_POINT('Ctrl Pts',(58.1839136790064,-3.9694599229629,133.71148355452));
#57439=CARTESIAN_POINT('Ctrl Pts',(58.1761566381214,-3.88541083446654,133.819781933056));
#57440=CARTESIAN_POINT('Ctrl Pts',(58.1684054468812,-3.80142512804163,133.927998642942));
#57441=CARTESIAN_POINT('Ctrl Pts',(58.160654255641,-3.71284937782166,134.032788363015));
#57442=CARTESIAN_POINT('Ctrl Pts',(58.1529030644009,-3.6199989570318,134.133743535404));
#57443=CARTESIAN_POINT('Ctrl Pts',(58.1451551676238,-3.52718800014777,134.234655799151));
#57444=CARTESIAN_POINT('Ctrl Pts',(58.1374072708467,-3.43010625037576,134.331736469572));
#57445=CARTESIAN_POINT('Ctrl Pts',(58.1296593740695,-3.32910895981231,134.424611519948));
#57446=CARTESIAN_POINT('Ctrl Pts',(58.1219130979854,-3.2281327957048,134.517467142865));
#57447=CARTESIAN_POINT('Ctrl Pts',(58.1141668219013,-3.12324300753604,134.606118631086));
#57448=CARTESIAN_POINT('Ctrl Pts',(58.1064205458172,-3.01483096984557,134.69022954044));
#57449=CARTESIAN_POINT('Ctrl Pts',(58.0986742125518,-2.90641813188207,134.774341070682));
#57450=CARTESIAN_POINT('Ctrl Pts',(58.0909278792864,-2.79448330141324,134.853911715517));
#57451=CARTESIAN_POINT('Ctrl Pts',(58.083181546021,-2.67944980044767,134.928646231994));
#57452=CARTESIAN_POINT('Ctrl Pts',(58.075433478018,-2.56439053852699,135.003397484748));
#57453=CARTESIAN_POINT('Ctrl Pts',(58.067685410015,-2.44623155306565,135.073310241108));
#57454=CARTESIAN_POINT('Ctrl Pts',(58.0599373420119,-2.32542356957031,135.138133602459));
#57455=CARTESIAN_POINT('Ctrl Pts',(58.0521810392701,-2.20448718991249,135.20302585885));
#57456=CARTESIAN_POINT('Ctrl Pts',(58.0444247365281,-2.08089653323544,135.262817729883));
#57457=CARTESIAN_POINT('Ctrl Pts',(58.0366684337862,-1.95512575988806,135.31730492539));
#57458=CARTESIAN_POINT('Ctrl Pts',(58.028907991272,-1.82928785889206,135.371821202354));
#57459=CARTESIAN_POINT('Ctrl Pts',(58.0211475487578,-1.70126788742459,135.421027022057));
#57460=CARTESIAN_POINT('Ctrl Pts',(58.0133871062436,-1.57155729410359,135.464767330917));
#57461=CARTESIAN_POINT('Ctrl Pts',(58.0056142059781,-1.44163847782304,135.508577855604));
#57462=CARTESIAN_POINT('Ctrl Pts',(57.9978413057127,-1.31002399196821,135.546905227379));
#57463=CARTESIAN_POINT('Ctrl Pts',(57.9900684054472,-1.17721853415224,135.579644858881));
#57464=CARTESIAN_POINT('Ctrl Pts',(57.9825780696855,-1.04924088925148,135.61119432231));
#57465=CARTESIAN_POINT('Ctrl Pts',(57.9750877339239,-0.920157660517325,
135.637555187488));
#57466=CARTESIAN_POINT('Ctrl Pts',(57.9675973981622,-0.790424960486675,
135.658679462094));
#57467=CARTESIAN_POINT('Ctrl Pts',(57.9598230640431,-0.655773405696139,
135.680604669993));
#57468=CARTESIAN_POINT('Ctrl Pts',(57.952048729924,-0.519995622350196,135.696957810429));
#57469=CARTESIAN_POINT('Ctrl Pts',(57.9442743958049,-0.383592527604621,
135.707628898546));
#57470=CARTESIAN_POINT('Ctrl Pts',(57.9365096428578,-0.247357537482625,
135.718286835501));
#57471=CARTESIAN_POINT('Ctrl Pts',(57.9287448899108,-0.110499155338198,
135.723276623065));
#57472=CARTESIAN_POINT('Ctrl Pts',(57.9209801369637,0.0264721060725106,
135.722539375003));
#57473=CARTESIAN_POINT('Ctrl Pts',(57.9132230960787,0.163307325695244,135.721802859185));
#57474=CARTESIAN_POINT('Ctrl Pts',(57.9054660551937,0.300254813044118,135.715350629551));
#57475=CARTESIAN_POINT('Ctrl Pts',(57.8977090143087,0.436799891420765,135.703175669939));
#57476=CARTESIAN_POINT('Ctrl Pts',(57.8899578230685,0.573242000091827,135.691009891559));
#57477=CARTESIAN_POINT('Ctrl Pts',(57.8822066318283,0.709281915964279,135.673130007634));
#57478=CARTESIAN_POINT('Ctrl Pts',(57.8744554405882,0.844406282128312,135.649581055606));
#57479=CARTESIAN_POINT('Ctrl Pts',(57.8667075438111,0.979473216832164,135.626042112512));
#57480=CARTESIAN_POINT('Ctrl Pts',(57.8589596470341,1.11362499143005,135.59683896062));
#57481=CARTESIAN_POINT('Ctrl Pts',(57.851211750257,1.2463549042146,135.562068313005));
#57482=CARTESIAN_POINT('Ctrl Pts',(57.8434654741729,1.37905705276273,135.52730493866));
#57483=CARTESIAN_POINT('Ctrl Pts',(57.8357191980888,1.51033755312422,135.486976484057));
#57484=CARTESIAN_POINT('Ctrl Pts',(57.8279729220046,1.63970179779126,135.441230367389));
#57485=CARTESIAN_POINT('Ctrl Pts',(57.8202265887393,1.76906699739577,135.395483913033));
#57486=CARTESIAN_POINT('Ctrl Pts',(57.8124802554739,1.89651554448227,135.344319847155));
#57487=CARTESIAN_POINT('Ctrl Pts',(57.8047339222086,2.02157022690707,135.287934736523));
#57488=CARTESIAN_POINT('Ctrl Pts',(57.7969858542056,2.14665291446093,135.231536998836));
#57489=CARTESIAN_POINT('Ctrl Pts',(57.7892377862026,2.26934031425386,135.169916050458));
#57490=CARTESIAN_POINT('Ctrl Pts',(57.7814897181996,2.38917771002942,135.103315482693));
#57491=CARTESIAN_POINT('Ctrl Pts',(57.7737334154578,2.50914247041529,135.036644131052));
#57492=CARTESIAN_POINT('Ctrl Pts',(57.7659771127159,2.62625083371306,134.964982778112));
#57493=CARTESIAN_POINT('Ctrl Pts',(57.758220809974,2.74007462956671,134.888619924577));
#57494=CARTESIAN_POINT('Ctrl Pts',(57.7504603674599,2.85395917660753,134.812216313888));
#57495=CARTESIAN_POINT('Ctrl Pts',(57.7426999249457,2.96455534794491,134.731106433647));
#57496=CARTESIAN_POINT('Ctrl Pts',(57.7349394824315,3.07146705262637,134.645619943247));
#57497=CARTESIAN_POINT('Ctrl Pts',(57.727166582166,3.17855038146722,134.559996222343));
#57498=CARTESIAN_POINT('Ctrl Pts',(57.7193936819006,3.28193712929566,134.46998210852));
#57499=CARTESIAN_POINT('Ctrl Pts',(57.7116207816352,3.38126650241594,134.375945686151));
#57500=CARTESIAN_POINT('Ctrl Pts',(57.7041304458732,3.4769850026265,134.285327724599));
#57501=CARTESIAN_POINT('Ctrl Pts',(57.6966401101113,3.56893578324734,134.190975039964));
#57502=CARTESIAN_POINT('Ctrl Pts',(57.6891497743494,3.65683192701093,134.093245431617));
#57503=CARTESIAN_POINT('Ctrl Pts',(57.6813754402303,3.74806067978168,133.991810375464));
#57504=CARTESIAN_POINT('Ctrl Pts',(57.6736011061112,3.83521024843067,133.886415952762));
#57505=CARTESIAN_POINT('Ctrl Pts',(57.6658267719921,3.9179173416248,133.777424149799));
#57506=CARTESIAN_POINT('Ctrl Pts',(57.658062019045,4.00052250571843,133.668566669493));
#57507=CARTESIAN_POINT('Ctrl Pts',(57.650297266098,4.07869585381554,133.556120938625));
#57508=CARTESIAN_POINT('Ctrl Pts',(57.6425325131509,4.15211189864189,133.440484636586));
#57509=CARTESIAN_POINT('Ctrl Pts',(57.6347754722659,4.22545502561742,133.324963186153));
#57510=CARTESIAN_POINT('Ctrl Pts',(57.6270184313808,4.29405004412983,133.206257798771));
#57511=CARTESIAN_POINT('Ctrl Pts',(57.6192613904958,4.35761285595699,133.084797694115));
#57512=CARTESIAN_POINT('Ctrl Pts',(57.6115101992557,4.42112773457331,132.963429183469));
#57513=CARTESIAN_POINT('Ctrl Pts',(57.6037590080156,4.4796177793311,132.839310435393));
#57514=CARTESIAN_POINT('Ctrl Pts',(57.5960078167755,4.53284339955716,132.712897695432));
#57515=CARTESIAN_POINT('Ctrl Pts',(57.5882599199984,4.58604639747478,132.586538684259));
#57516=CARTESIAN_POINT('Ctrl Pts',(57.5805120232213,4.63398926972184,132.45788797999));
#57517=CARTESIAN_POINT('Ctrl Pts',(57.5727641264442,4.67647949909547,132.327424160902));
#57518=CARTESIAN_POINT('Ctrl Pts',(57.5650178503601,4.71896084042909,132.196987632032));
#57519=CARTESIAN_POINT('Ctrl Pts',(57.557271574276,4.75599168656037,132.064739114232));
#57520=CARTESIAN_POINT('Ctrl Pts',(57.5495252981919,4.78742871714996,131.931174417938));
#57521=CARTESIAN_POINT('Ctrl Pts',(57.5417789649266,4.81886597980057,131.797608735699));
#57522=CARTESIAN_POINT('Ctrl Pts',(57.5340326316612,4.84470925494023,131.662727236147));
#57523=CARTESIAN_POINT('Ctrl Pts',(57.5262862983959,4.86486597493708,131.527037660511));
#57524=CARTESIAN_POINT('Ctrl Pts',(57.5185382303929,4.88502720889162,131.391317698135));
#57525=CARTESIAN_POINT('Ctrl Pts',(57.5107901623899,4.89949929621964,131.254789686228));
#57526=CARTESIAN_POINT('Ctrl Pts',(57.5030420943869,4.90824139194049,131.117967857505));
#57527=CARTESIAN_POINT('Ctrl Pts',(57.4952857916451,4.9169927788647,130.981000612914));
#57528=CARTESIAN_POINT('Ctrl Pts',(57.4875294889032,4.92000198397472,130.8437393185));
#57529=CARTESIAN_POINT('Ctrl Pts',(57.4797731861614,4.91728029454729,130.70670014779));
#57530=CARTESIAN_POINT('Ctrl Pts',(57.4720127436472,4.91455715247226,130.569587835147));
#57531=CARTESIAN_POINT('Ctrl Pts',(57.464252301133,4.90609704514428,130.432698272466));
#57532=CARTESIAN_POINT('Ctrl Pts',(57.4564918586188,4.89196322751154,130.296542891236));
#57533=CARTESIAN_POINT('Ctrl Pts',(57.4487189583534,4.87780672101999,130.160168941301));
#57534=CARTESIAN_POINT('Ctrl Pts',(57.440946058088,4.85795836029175,130.02453191505));
#57535=CARTESIAN_POINT('Ctrl Pts',(57.4331731578226,4.83253280732908,129.890134317032));
#57536=CARTESIAN_POINT('Ctrl Pts',(57.4256828220605,4.80803153725963,129.760622410229));
#57537=CARTESIAN_POINT('Ctrl Pts',(57.4181924862984,4.77835159441672,129.632261683571));
#57538=CARTESIAN_POINT('Ctrl Pts',(57.4107021505364,4.74363891975441,129.505486927983));
#57539=CARTESIAN_POINT('Ctrl Pts',(57.4029278164173,4.70761010348175,129.373905469005));
#57540=CARTESIAN_POINT('Ctrl Pts',(57.3951534822982,4.66604526133884,129.243615808824));
#57541=CARTESIAN_POINT('Ctrl Pts',(57.3873791481791,4.61905257480261,129.115119257159));
#57542=CARTESIAN_POINT('Ctrl Pts',(57.379614395232,4.57211780255267,128.98678106601));
#57543=CARTESIAN_POINT('Ctrl Pts',(57.371849642285,4.51976862868185,128.860231950098));
#57544=CARTESIAN_POINT('Ctrl Pts',(57.3640848893379,4.46216369830185,128.73596070651));
#57545=CARTESIAN_POINT('Ctrl Pts',(57.3563278484529,4.4046159819508,128.611812890873));
#57546=CARTESIAN_POINT('Ctrl Pts',(57.3485708075679,4.34182306066696,128.489938797666));
#57547=CARTESIAN_POINT('Ctrl Pts',(57.3408137666829,4.27399248709164,128.370809450489));
#57548=CARTESIAN_POINT('Ctrl Pts',(57.3330625754428,4.2062130650795,128.251769939679));
#57549=CARTESIAN_POINT('Ctrl Pts',(57.3253113842027,4.13340374498811,128.135471393396));
#57550=CARTESIAN_POINT('Ctrl Pts',(57.3175601929626,4.0558188745049,128.02236199792));
#57551=CARTESIAN_POINT('Ctrl Pts',(57.3098122961855,3.97826697966128,127.909300676955));
#57552=CARTESIAN_POINT('Ctrl Pts',(57.3020643994084,3.89594379210233,127.799426132596));
#57553=CARTESIAN_POINT('Ctrl Pts',(57.2943165026313,3.80914789303409,127.693159018265));
#57554=CARTESIAN_POINT('Ctrl Pts',(57.2865702265472,3.72237014979684,127.586914132723));
#57555=CARTESIAN_POINT('Ctrl Pts',(57.2788239504631,3.63112180316098,127.484275478884));
#57556=CARTESIAN_POINT('Ctrl Pts',(57.271077674379,3.53574252434591,127.38563163386));
#57557=CARTESIAN_POINT('Ctrl Pts',(57.2633313411137,3.44036254146268,127.286987060669));
#57558=CARTESIAN_POINT('Ctrl Pts',(57.2555850078483,3.34085183731661,127.192337636203));
#57559=CARTESIAN_POINT('Ctrl Pts',(57.247838674583,3.23758755391919,127.102035686768));
#57560=CARTESIAN_POINT('Ctrl Pts',(57.24009060658,3.13430014520149,127.011713514838));
#57561=CARTESIAN_POINT('Ctrl Pts',(57.232342538577,3.02725777881118,126.92574101258));
#57562=CARTESIAN_POINT('Ctrl Pts',(57.2245944705741,2.91687101558521,126.844430499377));
#57563=CARTESIAN_POINT('Ctrl Pts',(57.2168381678322,2.80636693199382,126.763033568393));
#57564=CARTESIAN_POINT('Ctrl Pts',(57.2090818650904,2.6925116664282,126.686308756485));
#57565=CARTESIAN_POINT('Ctrl Pts',(57.2013255623486,2.57574559134194,126.614525571746));
#57566=CARTESIAN_POINT('Ctrl Pts',(57.1935651198344,2.45891719468549,126.542704074159));
#57567=CARTESIAN_POINT('Ctrl Pts',(57.1858046773202,2.33917523402769,126.475829649714));
#57568=CARTESIAN_POINT('Ctrl Pts',(57.1780442348061,2.21698418201019,126.414125521445));
#57569=CARTESIAN_POINT('Ctrl Pts',(57.1702713345407,2.09459697806837,126.35232234023));
#57570=CARTESIAN_POINT('Ctrl Pts',(57.1624984342752,1.96975318264655,126.295706202438));
#57571=CARTESIAN_POINT('Ctrl Pts',(57.1547255340098,1.84293754466647,126.244452255662));
#57572=CARTESIAN_POINT('Ctrl Pts',(57.1472351982477,1.72073197455491,126.195061518952));
#57573=CARTESIAN_POINT('Ctrl Pts',(57.1397448624856,1.5966957257728,126.150649987302));
#57574=CARTESIAN_POINT('Ctrl Pts',(57.1322545267235,1.47127348488866,126.111329891568));
#57575=CARTESIAN_POINT('Ctrl Pts',(57.1244801926044,1.34109582162124,126.070518962453));
#57576=CARTESIAN_POINT('Ctrl Pts',(57.1167058584853,1.20901262805993,126.035063897496));
#57577=CARTESIAN_POINT('Ctrl Pts',(57.1089315243663,1.07550414499935,126.005144650703));
#57578=CARTESIAN_POINT('Ctrl Pts',(57.1011667714192,0.942160199212331,125.975262276708));
#57579=CARTESIAN_POINT('Ctrl Pts',(57.093402018472,0.807394836761404,125.950902231007));
#57580=CARTESIAN_POINT('Ctrl Pts',(57.085637265525,0.671705048036853,125.932195247739));
#57581=CARTESIAN_POINT('Ctrl Pts',(57.0778802246399,0.536150028323353,125.91350684451));
#57582=CARTESIAN_POINT('Ctrl Pts',(57.070123183755,0.399672794298141,125.900460383256));
#57583=CARTESIAN_POINT('Ctrl Pts',(57.06236614287,0.262781818728084,125.893135843821));
#57584=CARTESIAN_POINT('Ctrl Pts',(57.0546149516299,0.125994073707748,125.885816827879));
#57585=CARTESIAN_POINT('Ctrl Pts',(57.0468637603897,-0.0112064030019008,
125.884211165923));
#57586=CARTESIAN_POINT('Ctrl Pts',(57.0391125691496,-0.148305058451984,
125.888347123673));
#57587=CARTESIAN_POINT('Ctrl Pts',(57.0313646723725,-0.285345443316461,
125.892481323531));
#57588=CARTESIAN_POINT('Ctrl Pts',(57.0236167755954,-0.422283703026263,
125.902352277677));
#57589=CARTESIAN_POINT('Ctrl Pts',(57.0158688788183,-0.558604539508258,
125.917936154736));
#57590=CARTESIAN_POINT('Ctrl Pts',(57.0081226027342,-0.694896860610184,
125.933516771985));
#57591=CARTESIAN_POINT('Ctrl Pts',(57.0003763266501,-0.830571627184759,
125.954807890808));
#57592=CARTESIAN_POINT('Ctrl Pts',(56.992630050566,-0.965118317710622,125.981733771612));
#57593=CARTESIAN_POINT('Ctrl Pts',(56.9848837173007,-1.09966600142941,126.008659851176));
#57594=CARTESIAN_POINT('Ctrl Pts',(56.9771373840353,-1.23308520911929,126.041220698999));
#57595=CARTESIAN_POINT('Ctrl Pts',(56.9693910507699,-1.36487566420962,126.0792894558));
#57596=CARTESIAN_POINT('Ctrl Pts',(56.9616429827669,-1.4966956328586,126.117366737836));
#57597=CARTESIAN_POINT('Ctrl Pts',(56.9538949147639,-1.62688574756502,126.160954274813));
#57598=CARTESIAN_POINT('Ctrl Pts',(56.9461468467609,-1.75496132702647,126.209875466524));
#57599=CARTESIAN_POINT('Ctrl Pts',(56.9383905440191,-1.88317302673807,126.258848652261));
#57600=CARTESIAN_POINT('Ctrl Pts',(56.9306342412772,-2.00926533606393,126.313166676787));
#57601=CARTESIAN_POINT('Ctrl Pts',(56.9228779385354,-2.1327734781451,126.372604717991));
#57602=CARTESIAN_POINT('Ctrl Pts',(56.9151174960212,-2.25634754024046,126.432074483067));
#57603=CARTESIAN_POINT('Ctrl Pts',(56.907357053507,-2.37733434210384,126.496669525926));
#57604=CARTESIAN_POINT('Ctrl Pts',(56.8995966109928,-2.49529502106704,126.566119730082));
#57605=CARTESIAN_POINT('Ctrl Pts',(56.8918237107274,-2.61344506098418,126.635681421872));
#57606=CARTESIAN_POINT('Ctrl Pts',(56.8840508104619,-2.72855894206567,126.710113637318));
#57607=CARTESIAN_POINT('Ctrl Pts',(56.8762779101965,-2.84022728904805,126.789103214977));
#57608=CARTESIAN_POINT('Ctrl Pts',(56.8687875744345,-2.94783621034038,126.865221322524));
#57609=CARTESIAN_POINT('Ctrl Pts',(56.8612972386726,-3.0522455119358,126.945571013843));
#57610=CARTESIAN_POINT('Ctrl Pts',(56.8538069029107,-3.1531204068837,127.029838825048));
#57611=CARTESIAN_POINT('Ctrl Pts',(56.8461428595284,-3.25633468133444,127.116060882554));
#57612=CARTESIAN_POINT('Ctrl Pts',(56.8384788161462,-3.35619520654422,127.206674880249));
#57613=CARTESIAN_POINT('Ctrl Pts',(56.830814772764,-3.45229711328055,127.30138649489));
#57614=CARTESIAN_POINT('Ctrl Pts',(56.8231595226317,-3.54828875862553,127.395989443276));
#57615=CARTESIAN_POINT('Ctrl Pts',(56.8155042724994,-3.64053007409822,127.49468038369));
#57616=CARTESIAN_POINT('Ctrl Pts',(56.8078490223671,-3.72864790079033,127.597123817074));
#57617=CARTESIAN_POINT('Ctrl Pts',(56.8002007863767,-3.81668498930518,127.699473386408));
#57618=CARTESIAN_POINT('Ctrl Pts',(56.7925525503864,-3.90060584027376,127.805568309344));
#57619=CARTESIAN_POINT('Ctrl Pts',(56.784904314396,-3.98007334735288,127.915035573167));
#57620=CARTESIAN_POINT('Ctrl Pts',(56.777261320038,-4.0594863922711,128.024427814834));
#57621=CARTESIAN_POINT('Ctrl Pts',(56.76961832568,-4.1344519278296,128.137187475971));
#57622=CARTESIAN_POINT('Ctrl Pts',(56.761975331322,-4.20467280688083,128.252908158754));
#57623=CARTESIAN_POINT('Ctrl Pts',(56.7543350965373,-4.27486833203923,128.368587059523));
#57624=CARTESIAN_POINT('Ctrl Pts',(56.7466948617526,-4.34032239617133,128.487224513723));
#57625=CARTESIAN_POINT('Ctrl Pts',(56.7390546269679,-4.40078116245027,128.608385157156));
#57626=CARTESIAN_POINT('Ctrl Pts',(56.7314160671341,-4.46122667449377,128.729519238821));
#57627=CARTESIAN_POINT('Ctrl Pts',(56.7237775073004,-4.51667889069151,128.853175047383));
#57628=CARTESIAN_POINT('Ctrl Pts',(56.7161389474666,-4.56693025803882,128.978893258036));
#57629=CARTESIAN_POINT('Ctrl Pts',(56.7084983915517,-4.61719475689396,129.104644320923));
#57630=CARTESIAN_POINT('Ctrl Pts',(56.7008578356368,-4.6622555425973,129.232458488203));
#57631=CARTESIAN_POINT('Ctrl Pts',(56.6932172797219,-4.70195355749686,129.361857305389));
#57632=CARTESIAN_POINT('Ctrl Pts',(56.6889028262341,-4.72437015136132,129.434925964835));
#57633=CARTESIAN_POINT('Ctrl Pts',(56.6845883727463,-4.7450776601896,129.508499598817));
#57634=CARTESIAN_POINT('Ctrl Pts',(56.6802739192584,-4.76405452823399,129.582490119308));
#57635=CARTESIAN_POINT('Origin',(213.235140564004,0.,130.804360617566));
#57636=CARTESIAN_POINT('',(54.5845740201626,-4.7640545282341,129.582490119308));
#57637=CARTESIAN_POINT('',(54.9301858291403,-4.76405452823401,129.582490119308));
#57638=CARTESIAN_POINT('',(213.235140564004,-4.76405452823405,129.582490119308));
#57639=CARTESIAN_POINT('',(56.2648594359518,-4.91824814598434,130.800090134965));
#57640=CARTESIAN_POINT('Ctrl Pts',(56.2648594359517,-4.91824814598434,130.800090134965));
#57641=CARTESIAN_POINT('Ctrl Pts',(56.2572127733997,-4.91836515257441,130.934844798205));
#57642=CARTESIAN_POINT('Ctrl Pts',(56.2495661108478,-4.912939801848,131.069789027858));
#57643=CARTESIAN_POINT('Ctrl Pts',(56.2419194482958,-4.90195208324078,131.204421658048));
#57644=CARTESIAN_POINT('Ctrl Pts',(56.2342795697229,-4.89097411273652,131.338934844631));
#57645=CARTESIAN_POINT('Ctrl Pts',(56.22663969115,-4.8744436226077,131.473136581709));
#57646=CARTESIAN_POINT('Ctrl Pts',(56.2189998125771,-4.85239265815541,131.606525534263));
#57647=CARTESIAN_POINT('Ctrl Pts',(56.2113643828619,-4.83035453443104,131.7398368117));
#57648=CARTESIAN_POINT('Ctrl Pts',(56.2037289531468,-4.80280239497657,131.872335848918));
#57649=CARTESIAN_POINT('Ctrl Pts',(56.1960935234316,-4.7698200926489,132.0035267221));
#57650=CARTESIAN_POINT('Ctrl Pts',(56.1884603794111,-4.73684766369814,132.134678322798));
#57651=CARTESIAN_POINT('Ctrl Pts',(56.1808272353906,-4.69844840147115,132.264522146939));
#57652=CARTESIAN_POINT('Ctrl Pts',(56.1731940913702,-4.65475710850639,132.392573236616));
#57653=CARTESIAN_POINT('Ctrl Pts',(56.1655614659798,-4.61106878412397,132.520615625927));
#57654=CARTESIAN_POINT('Ctrl Pts',(56.1579288405894,-4.56208927434166,132.646865141058));
#57655=CARTESIAN_POINT('Ctrl Pts',(56.1502962151989,-4.50800284216768,132.770853291722));
#57656=CARTESIAN_POINT('Ctrl Pts',(56.1426623420016,-4.4539075677641,132.894861712381));
#57657=CARTESIAN_POINT('Ctrl Pts',(56.1350284688042,-4.39470387265641,133.016607663781));
#57658=CARTESIAN_POINT('Ctrl Pts',(56.1273945956068,-4.33062338238191,133.135644423212));
#57659=CARTESIAN_POINT('Ctrl Pts',(56.1197530945517,-4.2664788621123,133.254800125602));
#57660=CARTESIAN_POINT('Ctrl Pts',(56.1121115934966,-4.19744800635254,133.371240873789));
#57661=CARTESIAN_POINT('Ctrl Pts',(56.1044700924415,-4.12380763749675,133.484545990152));
#57662=CARTESIAN_POINT('Ctrl Pts',(56.0968247204177,-4.05012996450993,133.597908503687));
#57663=CARTESIAN_POINT('Ctrl Pts',(56.089179348394,-3.97183836277016,133.708131894121));
#57664=CARTESIAN_POINT('Ctrl Pts',(56.0815339763703,-3.88925109250205,133.814827193028));
#57665=CARTESIAN_POINT('Ctrl Pts',(56.0738766440318,-3.80653462384529,133.921689404591));
#57666=CARTESIAN_POINT('Ctrl Pts',(56.0662193116933,-3.71950932307574,134.025012191351));
#57667=CARTESIAN_POINT('Ctrl Pts',(56.0585619793549,-3.62853201158557,134.124441716485));
#57668=CARTESIAN_POINT('Ctrl Pts',(56.0517256621137,-3.54730923900561,134.213210460861));
#57669=CARTESIAN_POINT('Ctrl Pts',(56.0448893448725,-3.46293714824102,134.298876441918));
#57670=CARTESIAN_POINT('Ctrl Pts',(56.0380530276313,-3.37569157973648,134.381215300244));
#57671=CARTESIAN_POINT('Ctrl Pts',(56.0302786935123,-3.27647497289476,134.474851943049));
#57672=CARTESIAN_POINT('Ctrl Pts',(56.0225043593932,-3.17320225053233,134.564505590316));
#57673=CARTESIAN_POINT('Ctrl Pts',(56.0147300252741,-3.06622657670409,134.649804368658));
#57674=CARTESIAN_POINT('Ctrl Pts',(56.006965272327,-2.95938274083331,134.73499802388));
#57675=CARTESIAN_POINT('Ctrl Pts',(55.9992005193799,-2.84884533636479,134.815847247478));
#57676=CARTESIAN_POINT('Ctrl Pts',(55.9914357664329,-2.7350041173699,134.892017102701));
#57677=CARTESIAN_POINT('Ctrl Pts',(55.9836787255479,-2.6212759670786,134.968111304951));
#57678=CARTESIAN_POINT('Ctrl Pts',(55.9759216846628,-2.50425085522174,135.039535171784));
#57679=CARTESIAN_POINT('Ctrl Pts',(55.9681646437778,-2.38435106029703,135.105994386701));
#57680=CARTESIAN_POINT('Ctrl Pts',(55.9604134525377,-2.26454168274003,135.172403484207));
#57681=CARTESIAN_POINT('Ctrl Pts',(55.9526622612976,-2.1418622775962,135.233855192998));
#57682=CARTESIAN_POINT('Ctrl Pts',(55.9449110700574,-2.01676320950764,135.290099042762));
#57683=CARTESIAN_POINT('Ctrl Pts',(55.9371631732803,-1.89171731186048,135.346318987388));
#57684=CARTESIAN_POINT('Ctrl Pts',(55.9294152765033,-1.76425415255729,135.397335315446));
#57685=CARTESIAN_POINT('Ctrl Pts',(55.9216673797262,-1.6348475521722,135.442944080613));
#57686=CARTESIAN_POINT('Ctrl Pts',(55.9139211036421,-1.50546802085839,135.48854330541));
#57687=CARTESIAN_POINT('Ctrl Pts',(55.906174827558,-1.37414622556528,135.52873708735));
#57688=CARTESIAN_POINT('Ctrl Pts',(55.8984285514739,-1.24137439465677,135.563370249285));
#57689=CARTESIAN_POINT('Ctrl Pts',(55.8906822182086,-1.10860158365659,135.598003666873));
#57690=CARTESIAN_POINT('Ctrl Pts',(55.8829358849432,-0.974379093989027,
135.627076283868));
#57691=CARTESIAN_POINT('Ctrl Pts',(55.8751895516779,-0.839212299300182,
135.650483374905));
#57692=CARTESIAN_POINT('Ctrl Pts',(55.8674414836749,-0.704015234944847,
135.673895707799));
#57693=CARTESIAN_POINT('Ctrl Pts',(55.8596934156719,-0.567873829924174,
135.69163992336));
#57694=CARTESIAN_POINT('Ctrl Pts',(55.8519453476689,-0.431301188699605,
135.703662848203));
#57695=CARTESIAN_POINT('Ctrl Pts',(55.8441890449271,-0.294583396446707,
135.715698551154));
#57696=CARTESIAN_POINT('Ctrl Pts',(55.8364327421852,-0.157433842520411,
135.722000782282));
#57697=CARTESIAN_POINT('Ctrl Pts',(55.8286764394434,-0.020368822663326,
135.722568438873));
#57698=CARTESIAN_POINT('Ctrl Pts',(55.8209159969292,0.116769352921991,135.723136398439));
#57699=CARTESIAN_POINT('Ctrl Pts',(55.8131555544151,0.253822514040031,135.717963699471));
#57700=CARTESIAN_POINT('Ctrl Pts',(55.8053951119009,0.390277858536041,135.707101305756));
#57701=CARTESIAN_POINT('Ctrl Pts',(55.7976222116355,0.526952253264972,135.696221474763));
#57702=CARTESIAN_POINT('Ctrl Pts',(55.78984931137,0.663026525333134,135.67963374451));
#57703=CARTESIAN_POINT('Ctrl Pts',(55.7820764111046,0.797995563328515,135.657440685256));
#57704=CARTESIAN_POINT('Ctrl Pts',(55.7745860753425,0.928058136826458,135.636054399607));
#57705=CARTESIAN_POINT('Ctrl Pts',(55.7670957395805,1.05709413555759,135.609463307364));
#57706=CARTESIAN_POINT('Ctrl Pts',(55.7596054038185,1.18466539162675,135.577802873672));
#57707=CARTESIAN_POINT('Ctrl Pts',(55.7518310696994,1.31707355064403,135.544942025014));
#57708=CARTESIAN_POINT('Ctrl Pts',(55.7440567355802,1.44832313222639,135.506515745115));
#57709=CARTESIAN_POINT('Ctrl Pts',(55.7362824014612,1.57791037496313,135.462620154247));
#57710=CARTESIAN_POINT('Ctrl Pts',(55.7285176485141,1.70733791300475,135.418778660773));
#57711=CARTESIAN_POINT('Ctrl Pts',(55.720752895567,1.83510682172838,135.369481392018));
#57712=CARTESIAN_POINT('Ctrl Pts',(55.7129881426199,1.96072463776384,135.314875217627));
#57713=CARTESIAN_POINT('Ctrl Pts',(55.7052311017349,2.08621768841351,135.260323278859));
#57714=CARTESIAN_POINT('Ctrl Pts',(55.6974740608499,2.2095635418646,135.200473082578));
#57715=CARTESIAN_POINT('Ctrl Pts',(55.6897170199649,2.3302863294695,135.135520818388));
#57716=CARTESIAN_POINT('Ctrl Pts',(55.6819658287249,2.45091807908036,135.070617535207));
#57717=CARTESIAN_POINT('Ctrl Pts',(55.6742146374847,2.56893035717939,135.000620026842));
#57718=CARTESIAN_POINT('Ctrl Pts',(55.6664634462446,2.68386900290952,134.925771812499));
#57719=CARTESIAN_POINT('Ctrl Pts',(55.6587155494676,2.79875879664992,134.850955410644));
#57720=CARTESIAN_POINT('Ctrl Pts',(55.6509676526906,2.91057722936676,134.771292616236));
#57721=CARTESIAN_POINT('Ctrl Pts',(55.6432197559135,3.01889660364952,134.687071829976));
#57722=CARTESIAN_POINT('Ctrl Pts',(55.6354734798294,3.12719331985427,134.602868660888));
#57723=CARTESIAN_POINT('Ctrl Pts',(55.6277272037452,3.23199212501721,134.514109636208));
#57724=CARTESIAN_POINT('Ctrl Pts',(55.6199809276611,3.33289640275313,134.421125004558));
#57725=CARTESIAN_POINT('Ctrl Pts',(55.6122345943957,3.43380142534151,134.328139686517));
#57726=CARTESIAN_POINT('Ctrl Pts',(55.6044882611304,3.53081157563075,134.230928964205));
#57727=CARTESIAN_POINT('Ctrl Pts',(55.5967419278651,3.62356557840581,134.129861416167));
#57728=CARTESIAN_POINT('Ctrl Pts',(55.5889938598621,3.71634035279655,134.028771234751));
#57729=CARTESIAN_POINT('Ctrl Pts',(55.5812457918591,3.80485681874277,133.92382279692));
#57730=CARTESIAN_POINT('Ctrl Pts',(55.5734977238561,3.88879289447455,133.815419050474));
#57731=CARTESIAN_POINT('Ctrl Pts',(55.5657414211143,3.97281817846658,133.706900091235));
#57732=CARTESIAN_POINT('Ctrl Pts',(55.5579851183724,4.05225310796458,133.594918797105));
#57733=CARTESIAN_POINT('Ctrl Pts',(55.5502288156305,4.12681768476306,133.479908946269));
#57734=CARTESIAN_POINT('Ctrl Pts',(55.5424683731164,4.20142205892128,133.364837711213));
#57735=CARTESIAN_POINT('Ctrl Pts',(55.5347079306022,4.27115070207514,133.246735035075));
#57736=CARTESIAN_POINT('Ctrl Pts',(55.5269474880881,4.33576930941126,133.126059900003));
#57737=CARTESIAN_POINT('Ctrl Pts',(55.5191745878226,4.40049164827245,133.005191046491));
#57738=CARTESIAN_POINT('Ctrl Pts',(55.5114016875572,4.46008738887331,132.881741834197));
#57739=CARTESIAN_POINT('Ctrl Pts',(55.5036287872917,4.5143698014213,132.756192669387));
#57740=CARTESIAN_POINT('Ctrl Pts',(55.4961384515297,4.56667891154403,132.635207532957));
#57741=CARTESIAN_POINT('Ctrl Pts',(55.4886481157677,4.61405418173537,132.512272757855));
#57742=CARTESIAN_POINT('Ctrl Pts',(55.4811577800057,4.65637274220682,132.387830209359));
#57743=CARTESIAN_POINT('Ctrl Pts',(55.4733834458866,4.70029582376101,132.258669383813));
#57744=CARTESIAN_POINT('Ctrl Pts',(55.4656091117675,4.73891031098766,132.127475050747));
#57745=CARTESIAN_POINT('Ctrl Pts',(55.4578347776484,4.77202477724665,131.994722994258));
#57746=CARTESIAN_POINT('Ctrl Pts',(55.4500700247014,4.80509843288537,131.862134542815));
#57747=CARTESIAN_POINT('Ctrl Pts',(55.4423052717543,4.83268546060512,131.727992563388));
#57748=CARTESIAN_POINT('Ctrl Pts',(55.4345405188072,4.85464323751589,131.592790765988));
#57749=CARTESIAN_POINT('Ctrl Pts',(55.4267834779222,4.87657920565311,131.45772325292));
#57750=CARTESIAN_POINT('Ctrl Pts',(55.4190264370373,4.89289698715673,131.321598400063));
#57751=CARTESIAN_POINT('Ctrl Pts',(55.4112693961523,4.9035044232689,131.184922614463));
#57752=CARTESIAN_POINT('Ctrl Pts',(55.4035182049122,4.91410386023096,131.048349897136));
#57753=CARTESIAN_POINT('Ctrl Pts',(55.3957670136721,4.91900149293363,130.911227462234));
#57754=CARTESIAN_POINT('Ctrl Pts',(55.388015822432,4.91815671594552,130.774069036228));
#57755=CARTESIAN_POINT('Ctrl Pts',(55.3802679256549,4.91731229801016,130.636968906211));
#57756=CARTESIAN_POINT('Ctrl Pts',(55.3725200288778,4.91073032710799,130.499833205655));
#57757=CARTESIAN_POINT('Ctrl Pts',(55.3647721321007,4.89842226201817,130.363177656126));
#57758=CARTESIAN_POINT('Ctrl Pts',(55.3570258560166,4.8861167715102,130.226550691992));
#57759=CARTESIAN_POINT('Ctrl Pts',(55.3492795799325,4.86808760430425,130.090404068252));
#57760=CARTESIAN_POINT('Ctrl Pts',(55.3415333038484,4.84439822707602,129.955249976953));
#57761=CARTESIAN_POINT('Ctrl Pts',(55.333786970583,4.82070867497819,129.820094887976));
#57762=CARTESIAN_POINT('Ctrl Pts',(55.3260406373177,4.79135889698251,129.685932731154));
#57763=CARTESIAN_POINT('Ctrl Pts',(55.3182943040523,4.75646371057833,129.553266683262));
#57764=CARTESIAN_POINT('Ctrl Pts',(55.3105462360494,4.72156070963934,129.42057092573));
#57765=CARTESIAN_POINT('Ctrl Pts',(55.3027981680464,4.68110992857659,129.289372321857));
#57766=CARTESIAN_POINT('Ctrl Pts',(55.2950501000435,4.63527628572367,129.160159651289));
#57767=CARTESIAN_POINT('Ctrl Pts',(55.2872937973016,4.58939393032945,129.030809651955));
#57768=CARTESIAN_POINT('Ctrl Pts',(55.2795374945597,4.5381174158025,128.903450171282));
#57769=CARTESIAN_POINT('Ctrl Pts',(55.2717811918179,4.48166034614662,128.778551247394));
#57770=CARTESIAN_POINT('Ctrl Pts',(55.2640207493037,4.42517314365262,128.653585661189));
#57771=CARTESIAN_POINT('Ctrl Pts',(55.2562603067895,4.36350005221747,128.531083597615));
#57772=CARTESIAN_POINT('Ctrl Pts',(55.2484998642753,4.2969005790462,128.411490275008));
#57773=CARTESIAN_POINT('Ctrl Pts',(55.2407269640099,4.23019419448835,128.291704970583));
#57774=CARTESIAN_POINT('Ctrl Pts',(55.2329540637445,4.15854582942361,128.174838071517));
#57775=CARTESIAN_POINT('Ctrl Pts',(55.225181163479,4.08225873123598,128.061306350194));
#57776=CARTESIAN_POINT('Ctrl Pts',(55.2176908277169,4.00874486122184,127.951901792908));
#57777=CARTESIAN_POINT('Ctrl Pts',(55.2102004919547,3.93092384397705,127.845594387566));
#57778=CARTESIAN_POINT('Ctrl Pts',(55.2027101561926,3.84910101915288,127.742726346975));
#57779=CARTESIAN_POINT('Ctrl Pts',(55.1949358220735,3.76417585705744,127.635958033361));
#57780=CARTESIAN_POINT('Ctrl Pts',(55.1871614879544,3.67467042258962,127.532556830017));
#57781=CARTESIAN_POINT('Ctrl Pts',(55.1793871538353,3.5808815356104,127.432940962521));
#57782=CARTESIAN_POINT('Ctrl Pts',(55.1716224008882,3.48720823505236,127.333447862679));
#57783=CARTESIAN_POINT('Ctrl Pts',(55.1638576479411,3.38926225099517,127.237731098473));
#57784=CARTESIAN_POINT('Ctrl Pts',(55.156092894994,3.28738186449743,127.146177524899));
#57785=CARTESIAN_POINT('Ctrl Pts',(55.148335854109,3.18560266703541,127.054714883625));
#57786=CARTESIAN_POINT('Ctrl Pts',(55.140578813224,3.07989713255731,126.967407463899));
#57787=CARTESIAN_POINT('Ctrl Pts',(55.1328217723389,2.97064150159132,126.884606526871));
#57788=CARTESIAN_POINT('Ctrl Pts',(55.1250705810988,2.86146826114637,126.801868030673));
#57789=CARTESIAN_POINT('Ctrl Pts',(55.1173193898586,2.74875056326018,126.723629488105));
#57790=CARTESIAN_POINT('Ctrl Pts',(55.1095681986185,2.6328986723348,126.650202743373));
#57791=CARTESIAN_POINT('Ctrl Pts',(55.1018203018414,2.51709602155398,126.576807206967));
#57792=CARTESIAN_POINT('Ctrl Pts',(55.0940724050643,2.39816215674454,126.508219609622));
#57793=CARTESIAN_POINT('Ctrl Pts',(55.0863245082872,2.27653716281707,126.444709070847));
#57794=CARTESIAN_POINT('Ctrl Pts',(55.0785782322031,2.15493761021641,126.381211817107));
#57795=CARTESIAN_POINT('Ctrl Pts',(55.070831956119,2.03064839452989,126.322789690393));
#57796=CARTESIAN_POINT('Ctrl Pts',(55.0630856800349,1.90413474271972,126.269666146704));
#57797=CARTESIAN_POINT('Ctrl Pts',(55.0553393467695,1.77762015701433,126.216542210869));
#57798=CARTESIAN_POINT('Ctrl Pts',(55.0475930135042,1.64888146289512,126.16871708747));
#57799=CARTESIAN_POINT('Ctrl Pts',(55.0398466802388,1.51840405889225,126.126366156642));
#57800=CARTESIAN_POINT('Ctrl Pts',(55.0320986122359,1.3878974353796,126.084005741616));
#57801=CARTESIAN_POINT('Ctrl Pts',(55.0243505442329,1.25565169897352,126.047122079252));
#57802=CARTESIAN_POINT('Ctrl Pts',(55.0166024762299,1.12216721621925,126.015840616423));
#57803=CARTESIAN_POINT('Ctrl Pts',(55.008846173488,0.988540864568406,125.984525907284));
#57804=CARTESIAN_POINT('Ctrl Pts',(55.0010898707462,0.853673517869801,125.95882538095));
#57805=CARTESIAN_POINT('Ctrl Pts',(54.9933335680043,0.71807609069216,125.938813393412));
#57806=CARTESIAN_POINT('Ctrl Pts',(54.9855731254902,0.582406291084875,125.918790724873));
#57807=CARTESIAN_POINT('Ctrl Pts',(54.977812682976,0.446006023191823,125.90446268573));
#57808=CARTESIAN_POINT('Ctrl Pts',(54.9700522404619,0.309390131792696,125.895851596606));
#57809=CARTESIAN_POINT('Ctrl Pts',(54.9622793401964,0.172554932436135,125.887226684197));
#57810=CARTESIAN_POINT('Ctrl Pts',(54.954506439931,0.0355038089827734,125.884337069335));
#57811=CARTESIAN_POINT('Ctrl Pts',(54.9467335396655,-0.10124868353825,125.887152897062));
#57812=CARTESIAN_POINT('Ctrl Pts',(54.9392432039036,-0.233029878495543,
125.889866362359));
#57813=CARTESIAN_POINT('Ctrl Pts',(54.9317528681417,-0.36453347009346,125.897877638882));
#57814=CARTESIAN_POINT('Ctrl Pts',(54.9242625323797,-0.495306501463842,
125.911114810118));
#57815=CARTESIAN_POINT('Ctrl Pts',(54.9164881982606,-0.631037832067771,
125.924853872725));
#57816=CARTESIAN_POINT('Ctrl Pts',(54.9087138641416,-0.766412066537457,
125.944266453546));
#57817=CARTESIAN_POINT('Ctrl Pts',(54.9009395300225,-0.900916901462603,
125.969328890766));
#57818=CARTESIAN_POINT('Ctrl Pts',(54.8931747770754,-1.03525597119956,125.994360440773));
#57819=CARTESIAN_POINT('Ctrl Pts',(54.8854100241284,-1.1687273926123,126.025027922069));
#57820=CARTESIAN_POINT('Ctrl Pts',(54.8776452711813,-1.30082284446051,126.061255833795));
#57821=CARTESIAN_POINT('Ctrl Pts',(54.8698882302963,-1.43278709724409,126.097447763449));
#57822=CARTESIAN_POINT('Ctrl Pts',(54.8621311894112,-1.56337772552062,126.139189030377));
#57823=CARTESIAN_POINT('Ctrl Pts',(54.8543741485262,-1.69209583614093,126.186352958));
#57824=CARTESIAN_POINT('Ctrl Pts',(54.8466229572861,-1.82071687943326,126.233481318938));
#57825=CARTESIAN_POINT('Ctrl Pts',(54.8388717660459,-1.94746785011645,126.28602406716));
#57826=CARTESIAN_POINT('Ctrl Pts',(54.8311205748058,-2.07186462689798,126.343804595016));
#57827=CARTESIAN_POINT('Ctrl Pts',(54.8233726780287,-2.19620853173031,126.401560564606));
#57828=CARTESIAN_POINT('Ctrl Pts',(54.8156247812516,-2.31819987892907,126.464549721742));
#57829=CARTESIAN_POINT('Ctrl Pts',(54.8078768844745,-2.43737437398574,126.532547276192));
#57830=CARTESIAN_POINT('Ctrl Pts',(54.8001306083904,-2.55652394030714,126.600530607021));
#57831=CARTESIAN_POINT('Ctrl Pts',(54.7923843323063,-2.67285748712374,126.673520057702));
#57832=CARTESIAN_POINT('Ctrl Pts',(54.7846380562222,-2.78593554803751,126.751245003044));
#57833=CARTESIAN_POINT('Ctrl Pts',(54.7768917229569,-2.8990144436683,126.828970522134));
#57834=CARTESIAN_POINT('Ctrl Pts',(54.7691453896915,-3.0088374832503,126.911431384176));
#57835=CARTESIAN_POINT('Ctrl Pts',(54.7613990564261,-3.11499474474874,126.998314006884));
#57836=CARTESIAN_POINT('Ctrl Pts',(54.7536509884232,-3.22117577942869,127.085216086351));
#57837=CARTESIAN_POINT('Ctrl Pts',(54.7459029204202,-3.32368909998309,127.176541649342));
#57838=CARTESIAN_POINT('Ctrl Pts',(54.7381548524173,-3.42215870406584,127.271937530408));
#57839=CARTESIAN_POINT('Ctrl Pts',(54.7303985496754,-3.52073296281641,127.367434799353));
#57840=CARTESIAN_POINT('Ctrl Pts',(54.7226422469336,-3.61525463870687,127.467010755518));
#57841=CARTESIAN_POINT('Ctrl Pts',(54.7148859441917,-3.70538501213266,127.570275743237));
#57842=CARTESIAN_POINT('Ctrl Pts',(54.7071255016775,-3.79556349085239,127.673595846589));
#57843=CARTESIAN_POINT('Ctrl Pts',(54.6993650591634,-3.88134575253328,127.780608599885));
#57844=CARTESIAN_POINT('Ctrl Pts',(54.6916046166493,-3.96243473202198,127.890892914473));
#57845=CARTESIAN_POINT('Ctrl Pts',(54.6838317163838,-4.04365388273929,128.001354267233));
#57846=CARTESIAN_POINT('Ctrl Pts',(54.6760588161184,-4.12016447744683,128.115097351468));
#57847=CARTESIAN_POINT('Ctrl Pts',(54.668285915853,-4.19171350440472,128.231673120125));
#57848=CARTESIAN_POINT('Ctrl Pts',(54.660795580091,-4.26066154401186,128.344011065954));
#57849=CARTESIAN_POINT('Ctrl Pts',(54.6533052443289,-4.32500233359532,128.458979052589));
#57850=CARTESIAN_POINT('Ctrl Pts',(54.6458149085668,-4.38455154430366,128.576157121957));
#57851=CARTESIAN_POINT('Ctrl Pts',(54.6375218026115,-4.45048288965953,128.705893648566));
#57852=CARTESIAN_POINT('Ctrl Pts',(54.6292286966562,-4.51072777099052,128.838707251713));
#57853=CARTESIAN_POINT('Ctrl Pts',(54.620935590701,-4.56500784274803,128.974091113327));
#57854=CARTESIAN_POINT('Ctrl Pts',(54.6126624204053,-4.61915743154251,129.109149527924));
#57855=CARTESIAN_POINT('Ctrl Pts',(54.6043892501097,-4.66737068634018,129.246765592799));
#57856=CARTESIAN_POINT('Ctrl Pts',(54.5961160798141,-4.70941595869355,129.386409846029));
#57857=CARTESIAN_POINT('Ctrl Pts',(54.592268726597,-4.72896868250741,129.45134997753));
#57858=CARTESIAN_POINT('Ctrl Pts',(54.5884213733797,-4.74718815391943,129.516728381839));
#57859=CARTESIAN_POINT('Ctrl Pts',(54.5845740201626,-4.76405452823409,129.582490119308));
#57860=CARTESIAN_POINT('Ctrl Pts',(56.3348795324218,-4.7640545282341,129.582490119308));
#57861=CARTESIAN_POINT('Ctrl Pts',(56.3287532387626,-4.79082473154765,129.686866735733));
#57862=CARTESIAN_POINT('Ctrl Pts',(56.3226269451034,-4.81413419198721,129.792010703334));
#57863=CARTESIAN_POINT('Ctrl Pts',(56.3165006514442,-4.83395290102421,129.8976730125));
#57864=CARTESIAN_POINT('Ctrl Pts',(56.3048853013623,-4.87152884113435,130.098006979447));
#57865=CARTESIAN_POINT('Ctrl Pts',(56.2932699512804,-4.89665970140022,130.300742953123));
#57866=CARTESIAN_POINT('Ctrl Pts',(56.2816546011985,-4.90910818688879,130.504627616511));
#57867=CARTESIAN_POINT('Ctrl Pts',(56.2760562127961,-4.91510813147043,130.602896332211));
#57868=CARTESIAN_POINT('Ctrl Pts',(56.2704578243936,-4.91816248136354,130.701431544498));
#57869=CARTESIAN_POINT('Ctrl Pts',(56.2648594359911,-4.91824814598373,130.800090134272));
#57870=CARTESIAN_POINT('',(56.6101405640451,-4.9182488539182,130.807718210793));
#57871=CARTESIAN_POINT('Ctrl Pts',(56.6802739192584,-4.76405452823399,129.582490119308));
#57872=CARTESIAN_POINT('Ctrl Pts',(56.6726269392178,-4.7976893168761,129.713631649744));
#57873=CARTESIAN_POINT('Ctrl Pts',(56.6649799591772,-4.82588445460891,129.846083118555));
#57874=CARTESIAN_POINT('Ctrl Pts',(56.6573329791366,-4.84856017054484,129.979347081249));
#57875=CARTESIAN_POINT('Ctrl Pts',(56.6494675766213,-4.87188357824431,130.116417493594));
#57876=CARTESIAN_POINT('Ctrl Pts',(56.6416021741061,-4.88936747251833,130.254347052025));
#57877=CARTESIAN_POINT('Ctrl Pts',(56.6337367715908,-4.90098238976537,130.392590441728));
#57878=CARTESIAN_POINT('Ctrl Pts',(56.6258713690756,-4.91259730701242,130.530833831431));
#57879=CARTESIAN_POINT('Ctrl Pts',(56.6180059665604,-4.91834328750372,130.669390592671));
#57880=CARTESIAN_POINT('Ctrl Pts',(56.6101405640451,-4.9182488539182,130.807718210793));
#57881=CARTESIAN_POINT('Ctrl Pts',(56.6101405640086,-4.91824885391776,130.807718211435));
#57882=CARTESIAN_POINT('Ctrl Pts',(56.5985468023716,-4.91810965688516,131.011615905063));
#57883=CARTESIAN_POINT('Ctrl Pts',(56.5869530407347,-4.90529105125989,131.215084519275));
#57884=CARTESIAN_POINT('Ctrl Pts',(56.5753592790977,-4.8799506832259,131.416948890212));
#57885=CARTESIAN_POINT('Ctrl Pts',(56.5675849449786,-4.86295839944731,131.552311433926));
#57886=CARTESIAN_POINT('Ctrl Pts',(56.5598106108596,-4.8403028006108,131.687180835548));
#57887=CARTESIAN_POINT('Ctrl Pts',(56.5520362767405,-4.81201983558532,131.821045507015));
#57888=CARTESIAN_POINT('Ctrl Pts',(56.5442715237934,-4.78377172678651,131.954745202238));
#57889=CARTESIAN_POINT('Ctrl Pts',(56.5365067708463,-4.74991013087439,132.087442252188));
#57890=CARTESIAN_POINT('Ctrl Pts',(56.5287420178992,-4.71052272527471,132.21863029382));
#57891=CARTESIAN_POINT('Ctrl Pts',(56.5209849770142,-4.67117443980159,132.349688037639));
#57892=CARTESIAN_POINT('Ctrl Pts',(56.5132279361292,-4.62631137832631,132.479239383728));
#57893=CARTESIAN_POINT('Ctrl Pts',(56.5054708952443,-4.5760721530097,132.606788622494));
#57894=CARTESIAN_POINT('Ctrl Pts',(56.4977197040041,-4.52587081348363,132.734241675388));
#57895=CARTESIAN_POINT('Ctrl Pts',(56.489968512764,-4.47030152246953,132.859695263841));
#57896=CARTESIAN_POINT('Ctrl Pts',(56.4822173215239,-4.40955245433536,132.982669644074));
#57897=CARTESIAN_POINT('Ctrl Pts',(56.4744694247468,-4.34882920617569,133.105591756914));
#57898=CARTESIAN_POINT('Ctrl Pts',(56.4667215279697,-4.28293073239527,133.226036407528));
#57899=CARTESIAN_POINT('Ctrl Pts',(56.4589736311926,-4.21209290027906,133.343544829457));
#57900=CARTESIAN_POINT('Ctrl Pts',(56.4512273551085,-4.14126988591024,133.461028671158));
#57901=CARTESIAN_POINT('Ctrl Pts',(56.4434810790245,-4.06550977003041,133.575577171225));
#57902=CARTESIAN_POINT('Ctrl Pts',(56.4357348029404,-3.98509364588115,133.686757484074));
#57903=CARTESIAN_POINT('Ctrl Pts',(56.4279884696751,-3.90467692811833,133.797938617631));
#57904=CARTESIAN_POINT('Ctrl Pts',(56.4202421364097,-3.81960436263369,133.905751197572));
#57905=CARTESIAN_POINT('Ctrl Pts',(56.4124958031444,-3.73019927840682,134.009792945018));
#57906=CARTESIAN_POINT('Ctrl Pts',(56.4047477351414,-3.64077417253122,134.113857991892));
#57907=CARTESIAN_POINT('Ctrl Pts',(56.3969996671385,-3.54701487201289,134.214150229444));
#57908=CARTESIAN_POINT('Ctrl Pts',(56.3892515991355,-3.44928346361555,134.310302238604));
#57909=CARTESIAN_POINT('Ctrl Pts',(56.3814952963936,-3.35144818511435,134.406556439264));
#57910=CARTESIAN_POINT('Ctrl Pts',(56.3737389936517,-3.2496326447677,134.49866134686));
#57911=CARTESIAN_POINT('Ctrl Pts',(56.3659826909099,-3.14423451436854,134.586287689993));
#57912=CARTESIAN_POINT('Ctrl Pts',(56.3582222483957,-3.0387801298137,134.673960801943));
#57913=CARTESIAN_POINT('Ctrl Pts',(56.3504618058816,-2.92973965579445,134.757150349439));
#57914=CARTESIAN_POINT('Ctrl Pts',(56.3427013633674,-2.81754118844338,134.835569457843));
#57915=CARTESIAN_POINT('Ctrl Pts',(56.334928463102,-2.70516261015201,134.914114451561));
#57916=CARTESIAN_POINT('Ctrl Pts',(56.3271555628366,-2.58961623780505,134.98787349271));
#57917=CARTESIAN_POINT('Ctrl Pts',(56.3193826625712,-2.47135706072542,135.056604418303));
#57918=CARTESIAN_POINT('Ctrl Pts',(56.3118923268091,-2.3573969026084,135.122836801628));
#57919=CARTESIAN_POINT('Ctrl Pts',(56.304401991047,-2.24091802236904,135.184400147977));
#57920=CARTESIAN_POINT('Ctrl Pts',(56.2969116552849,-2.12234468052803,135.241120259414));
#57921=CARTESIAN_POINT('Ctrl Pts',(56.2891373211658,-1.99927559439256,135.299990931117));
#57922=CARTESIAN_POINT('Ctrl Pts',(56.2813629870467,-1.87356024254338,135.35383034012));
#57923=CARTESIAN_POINT('Ctrl Pts',(56.2735886529277,-1.74564846974714,135.402392205384));
#57924=CARTESIAN_POINT('Ctrl Pts',(56.2658238999806,-1.61789433677907,135.450894222488));
#57925=CARTESIAN_POINT('Ctrl Pts',(56.2580591470334,-1.48794953077456,135.494131499641));
#57926=CARTESIAN_POINT('Ctrl Pts',(56.2502943940863,-1.35628746109362,135.531904100748));
#57927=CARTESIAN_POINT('Ctrl Pts',(56.2425373532013,-1.22475616003675,135.569639185576));
#57928=CARTESIAN_POINT('Ctrl Pts',(56.2347803123164,-1.09151136291889,135.601920288398));
#57929=CARTESIAN_POINT('Ctrl Pts',(56.2270232714314,-0.957045047517442,
135.628596084407));
#57930=CARTESIAN_POINT('Ctrl Pts',(56.2192720801913,-0.822680134210064,
135.65525176399));
#57931=CARTESIAN_POINT('Ctrl Pts',(56.2115208889511,-0.687095918065139,
135.676310474589));
#57932=CARTESIAN_POINT('Ctrl Pts',(56.203769697711,-0.550797733954898,135.691671219397));
#57933=CARTESIAN_POINT('Ctrl Pts',(56.1960218009339,-0.414557480208963,
135.707025435478));
#57934=CARTESIAN_POINT('Ctrl Pts',(56.1882739041568,-0.277604249739808,
135.716686458826));
#57935=CARTESIAN_POINT('Ctrl Pts',(56.1805260073798,-0.14045150778993,135.720604756791));
#57936=CARTESIAN_POINT('Ctrl Pts',(56.1727797312957,-0.00332745523699676,
135.724522235132));
#57937=CARTESIAN_POINT('Ctrl Pts',(56.1650334552115,0.133995635228279,135.722699366293));
#57938=CARTESIAN_POINT('Ctrl Pts',(56.1572871791274,0.271001660594019,135.715138678368));
#57939=CARTESIAN_POINT('Ctrl Pts',(56.1495408458621,0.408008697306929,135.707577934632));
#57940=CARTESIAN_POINT('Ctrl Pts',(56.1417945125968,0.544698273878758,135.694279308836));
#57941=CARTESIAN_POINT('Ctrl Pts',(56.1340481793314,0.680557174485788,135.675297385248));
#57942=CARTESIAN_POINT('Ctrl Pts',(56.1263001113285,0.816446499751629,135.65631121079));
#57943=CARTESIAN_POINT('Ctrl Pts',(56.1185520433255,0.951504391756165,135.631639260033));
#57944=CARTESIAN_POINT('Ctrl Pts',(56.1108039753225,1.08522601368991,135.601387567846));
#57945=CARTESIAN_POINT('Ctrl Pts',(56.1030476725807,1.21908975655493,135.5711037238));
#57946=CARTESIAN_POINT('Ctrl Pts',(56.0952913698389,1.35161401040232,135.535228378483));
#57947=CARTESIAN_POINT('Ctrl Pts',(56.087535067097,1.48230679856,135.493918125204));
#57948=CARTESIAN_POINT('Ctrl Pts',(56.0797746245828,1.61306934139398,135.452585823398));
#57949=CARTESIAN_POINT('Ctrl Pts',(56.0720141820686,1.74199810342242,135.405812966859));
#57950=CARTESIAN_POINT('Ctrl Pts',(56.0642537395545,1.86862033246999,135.353804662236));
#57951=CARTESIAN_POINT('Ctrl Pts',(56.056480839289,1.99544582676044,135.301712869265));
#57952=CARTESIAN_POINT('Ctrl Pts',(56.0487079390237,2.11995703367442,135.244368997172));
#57953=CARTESIAN_POINT('Ctrl Pts',(56.0409350387582,2.24170428178922,135.18202494635));
#57954=CARTESIAN_POINT('Ctrl Pts',(56.0334447029962,2.35902571077323,135.12194725881));
#57955=CARTESIAN_POINT('Ctrl Pts',(56.025954367234,2.47378037754475,135.057226770481));
#57956=CARTESIAN_POINT('Ctrl Pts',(56.018464031472,2.58559240127427,134.988126265517));
#57957=CARTESIAN_POINT('Ctrl Pts',(56.0106896973529,2.70164381186705,134.916405793905));
#57958=CARTESIAN_POINT('Ctrl Pts',(56.0029153632338,2.81489264991569,134.839739423617));
#57959=CARTESIAN_POINT('Ctrl Pts',(55.9951410291147,2.92488856012024,134.758372500879));
#57960=CARTESIAN_POINT('Ctrl Pts',(55.9873762761676,3.03474891019622,134.6771058556));
#57961=CARTESIAN_POINT('Ctrl Pts',(55.9796115232205,3.1413639977316,134.59115041451));
#57962=CARTESIAN_POINT('Ctrl Pts',(55.9718467702734,3.24430972150662,134.50079639997));
#57963=CARTESIAN_POINT('Ctrl Pts',(55.9640897293884,3.34715319813736,134.410532126311));
#57964=CARTESIAN_POINT('Ctrl Pts',(55.9563326885034,3.44633427171678,134.315878229392));
#57965=CARTESIAN_POINT('Ctrl Pts',(55.9485756476184,3.54145970239391,134.217166829296));
#57966=CARTESIAN_POINT('Ctrl Pts',(55.9408244563783,3.6365133982438,134.118529868234));
#57967=CARTESIAN_POINT('Ctrl Pts',(55.9330732651382,3.72751726853929,134.015841774714));
#57968=CARTESIAN_POINT('Ctrl Pts',(55.9253220738981,3.81411319596449,133.909473110032));
#57969=CARTESIAN_POINT('Ctrl Pts',(55.917574177121,3.90067231781051,133.803149654871));
#57970=CARTESIAN_POINT('Ctrl Pts',(55.9098262803439,3.98282697670444,133.693149042463));
#57971=CARTESIAN_POINT('Ctrl Pts',(55.9020783835668,4.06025795891991,133.579876492053));
#57972=CARTESIAN_POINT('Ctrl Pts',(55.8943321074827,4.13767274424313,133.466627635818));
#57973=CARTESIAN_POINT('Ctrl Pts',(55.8865858313987,4.21036559776212,133.350108525484));
#57974=CARTESIAN_POINT('Ctrl Pts',(55.8788395553146,4.27805968014959,133.230754739628));
#57975=CARTESIAN_POINT('Ctrl Pts',(55.8710932220492,4.34575426223939,133.11140007273));
#57976=CARTESIAN_POINT('Ctrl Pts',(55.8633468887839,4.40844980668608,132.98921102863));
#57977=CARTESIAN_POINT('Ctrl Pts',(55.8556005555185,4.46591483109181,132.864648894467));
#57978=CARTESIAN_POINT('Ctrl Pts',(55.8478524875156,4.52339272439132,132.740058865477));
#57979=CARTESIAN_POINT('Ctrl Pts',(55.8401044195126,4.57563760307485,132.613095043865));
#57980=CARTESIAN_POINT('Ctrl Pts',(55.8323563515096,4.62246580065241,132.484239477573));
#57981=CARTESIAN_POINT('Ctrl Pts',(55.8246000487677,4.66934376779563,132.355246962052));
#57982=CARTESIAN_POINT('Ctrl Pts',(55.8168437460259,4.71079342002766,132.22435905356));
#57983=CARTESIAN_POINT('Ctrl Pts',(55.809087443284,4.74668057832452,132.092074308515));
#57984=CARTESIAN_POINT('Ctrl Pts',(55.8013270007699,4.78258689067836,131.959718959117));
#57985=CARTESIAN_POINT('Ctrl Pts',(55.7935665582557,4.8129247069318,131.82596566872));
#57986=CARTESIAN_POINT('Ctrl Pts',(55.7858061157415,4.83761105502072,131.691323042273));
#57987=CARTESIAN_POINT('Ctrl Pts',(55.7780332154761,4.86233703182713,131.556464275528));
#57988=CARTESIAN_POINT('Ctrl Pts',(55.7702603152106,4.88139335686474,131.420713707242));
#57989=CARTESIAN_POINT('Ctrl Pts',(55.7624874149452,4.89474890268087,131.284585817034));
#57990=CARTESIAN_POINT('Ctrl Pts',(55.7549970791832,4.90761894076603,131.153406518521));
#57991=CARTESIAN_POINT('Ctrl Pts',(55.7475067434211,4.9151954613839,131.021877162518));
#57992=CARTESIAN_POINT('Ctrl Pts',(55.7400164076591,4.91749637951566,130.890456029467));
#57993=CARTESIAN_POINT('Ctrl Pts',(55.73224207354,4.91988453765773,130.754052024212));
#57994=CARTESIAN_POINT('Ctrl Pts',(55.7244677394209,4.91659671225258,130.617332523567));
#57995=CARTESIAN_POINT('Ctrl Pts',(55.7166934053018,4.90759589198655,130.480809039828));
#57996=CARTESIAN_POINT('Ctrl Pts',(55.7089286523547,4.89860616442708,130.344453809081));
#57997=CARTESIAN_POINT('Ctrl Pts',(55.7011638994076,4.88391747648488,130.208294500954));
#57998=CARTESIAN_POINT('Ctrl Pts',(55.6933991464605,4.86354476338292,130.072844796089));
#57999=CARTESIAN_POINT('Ctrl Pts',(55.6856421055755,4.84319228474684,129.937529621781));
#58000=CARTESIAN_POINT('Ctrl Pts',(55.6778850646906,4.81716707343298,129.80292303229));
#58001=CARTESIAN_POINT('Ctrl Pts',(55.6701280238056,4.78553599572897,129.669535390457));
#58002=CARTESIAN_POINT('Ctrl Pts',(55.6623768325655,4.75392877126671,129.536248337283));
#58003=CARTESIAN_POINT('Ctrl Pts',(55.6546256413253,4.71672418469763,129.404178780996));
#58004=CARTESIAN_POINT('Ctrl Pts',(55.6468744500852,4.67404042858048,129.273828313269));
#58005=CARTESIAN_POINT('Ctrl Pts',(55.6391265533081,4.63137481419825,129.143533247969));
#58006=CARTESIAN_POINT('Ctrl Pts',(55.6313786565311,4.58323478347159,129.01495618878));
#58007=CARTESIAN_POINT('Ctrl Pts',(55.623630759754,4.52978871601037,128.88858473015));
#58008=CARTESIAN_POINT('Ctrl Pts',(55.6158844836699,4.47635382831429,128.762239705705));
#58009=CARTESIAN_POINT('Ctrl Pts',(55.6081382075857,4.41761526374631,128.638099723998));
#58010=CARTESIAN_POINT('Ctrl Pts',(55.6003919315016,4.35378984848113,128.516633138655));
#58011=CARTESIAN_POINT('Ctrl Pts',(55.5926455982363,4.28996396207132,128.395165656675));
#58012=CARTESIAN_POINT('Ctrl Pts',(55.5848992649709,4.22105133189382,128.276371956532));
#58013=CARTESIAN_POINT('Ctrl Pts',(55.5771529317056,4.14731492999175,128.160696127891));
#58014=CARTESIAN_POINT('Ctrl Pts',(55.5694048637026,4.07356201533362,128.04499439445));
#58015=CARTESIAN_POINT('Ctrl Pts',(55.5616567956997,3.99498338948993,127.932412251517));
#58016=CARTESIAN_POINT('Ctrl Pts',(55.5539087276967,3.91188533682192,127.823364781598));
#58017=CARTESIAN_POINT('Ctrl Pts',(55.5461524249548,3.82869896655476,127.714201414731));
#58018=CARTESIAN_POINT('Ctrl Pts',(55.538396122213,3.74098381169831,127.608580536739));
#58019=CARTESIAN_POINT('Ctrl Pts',(55.5306398194711,3.64908679484475,127.506884518155));
#58020=CARTESIAN_POINT('Ctrl Pts',(55.522879376957,3.55714072978619,127.405134221343));
#58021=CARTESIAN_POINT('Ctrl Pts',(55.5151189344428,3.4610086292125,127.307313236752));
#58022=CARTESIAN_POINT('Ctrl Pts',(55.5073584919286,3.36107354844426,127.213766284527));
#58023=CARTESIAN_POINT('Ctrl Pts',(55.4995855916632,3.26097804301254,127.12006916243));
#58024=CARTESIAN_POINT('Ctrl Pts',(55.4918126913978,3.15706765441735,127.030660038422));
#58025=CARTESIAN_POINT('Ctrl Pts',(55.4840397911323,3.04975840378438,126.945843189713));
#58026=CARTESIAN_POINT('Ctrl Pts',(55.4765494553703,2.94635011470789,126.864109647095));
#58027=CARTESIAN_POINT('Ctrl Pts',(55.4690591196084,2.83978603685906,126.786640476018));
#58028=CARTESIAN_POINT('Ctrl Pts',(55.4615687838464,2.73046141803724,126.713668315875));
#58029=CARTESIAN_POINT('Ctrl Pts',(55.4537944497273,2.61699172306397,126.637929394101));
#58030=CARTESIAN_POINT('Ctrl Pts',(55.4460201156082,2.5001885851331,126.566795305073));
#58031=CARTESIAN_POINT('Ctrl Pts',(55.4382457814891,2.3804623485064,126.500573672346));
#58032=CARTESIAN_POINT('Ctrl Pts',(55.430481028542,2.26088366376594,126.434433651864));
#58033=CARTESIAN_POINT('Ctrl Pts',(55.4227162755949,2.13838938698267,126.373194229116));
#58034=CARTESIAN_POINT('Ctrl Pts',(55.4149515226478,2.01341976508197,126.317120495612));
#58035=CARTESIAN_POINT('Ctrl Pts',(55.4071944817628,1.88857426477168,126.26110245533));
#58036=CARTESIAN_POINT('Ctrl Pts',(55.3994374408778,1.76125866635961,126.210240053112));
#58037=CARTESIAN_POINT('Ctrl Pts',(55.3916803999928,1.63193849542028,126.164752896038));
#58038=CARTESIAN_POINT('Ctrl Pts',(55.3839292087527,1.50271584582782,126.119300041183));
#58039=CARTESIAN_POINT('Ctrl Pts',(55.3761780175125,1.37149199990593,126.0792144924));
#58040=CARTESIAN_POINT('Ctrl Pts',(55.3684268262724,1.23875284690055,126.044667933495));
#58041=CARTESIAN_POINT('Ctrl Pts',(55.3606789294953,1.10607011157614,126.010136057799));
#58042=CARTESIAN_POINT('Ctrl Pts',(55.3529310327182,0.971873727695399,125.981138587885));
#58043=CARTESIAN_POINT('Ctrl Pts',(55.3451831359411,0.836664935568744,125.957797417928));
#58044=CARTESIAN_POINT('Ctrl Pts',(55.337436859857,0.701484426206638,125.93446113044));
#58045=CARTESIAN_POINT('Ctrl Pts',(55.3296905837729,0.565292314851211,125.916778855973));
#58046=CARTESIAN_POINT('Ctrl Pts',(55.3219443076888,0.428599840517179,125.904821329101));
#58047=CARTESIAN_POINT('Ctrl Pts',(55.3141979744234,0.291906357150353,125.892863713962));
#58048=CARTESIAN_POINT('Ctrl Pts',(55.3064516411581,0.154712892912518,125.886630964813));
#58049=CARTESIAN_POINT('Ctrl Pts',(55.2987053078927,0.0175352158270222,
125.886141877137));
#58050=CARTESIAN_POINT('Ctrl Pts',(55.2909572398897,-0.119673181248134,
125.885652679933));
#58051=CARTESIAN_POINT('Ctrl Pts',(55.2832091718868,-0.256865393247976,
125.890909705091));
#58052=CARTESIAN_POINT('Ctrl Pts',(55.2754611038838,-0.39352664532523,125.901879629136));
#58053=CARTESIAN_POINT('Ctrl Pts',(55.2677048011419,-0.53033314260748,125.912861212147));
#58054=CARTESIAN_POINT('Ctrl Pts',(55.2599484984001,-0.66660716236299,125.929567791662));
#58055=CARTESIAN_POINT('Ctrl Pts',(55.2521921956582,-0.801839485297545,
125.951914172491));
#58056=CARTESIAN_POINT('Ctrl Pts',(55.244431753144,-0.937143985794801,125.974272480257));
#58057=CARTESIAN_POINT('Ctrl Pts',(55.2366713106299,-1.07140529908273,126.002276507491));
#58058=CARTESIAN_POINT('Ctrl Pts',(55.2289108681157,-1.20412635158235,126.035790308561));
#58059=CARTESIAN_POINT('Ctrl Pts',(55.2211379678503,-1.33706045969769,126.06935790896));
#58060=CARTESIAN_POINT('Ctrl Pts',(55.2133650675848,-1.46844899111134,126.108452846314));
#58061=CARTESIAN_POINT('Ctrl Pts',(55.2055921673193,-1.59781107921,126.152889579534));
#58062=CARTESIAN_POINT('Ctrl Pts',(55.1981018315573,-1.72247052956302,126.195710925571));
#58063=CARTESIAN_POINT('Ctrl Pts',(55.1906114957953,-1.84524802428055,126.243492323061));
#58064=CARTESIAN_POINT('Ctrl Pts',(55.1831211600332,-1.96573419616374,126.296026986108));
#58065=CARTESIAN_POINT('Ctrl Pts',(55.1753463323093,-2.09079657778077,126.35055697885));
#58066=CARTESIAN_POINT('Ctrl Pts',(55.1675715045853,-2.21378632720528,126.410381188876));
#58067=CARTESIAN_POINT('Ctrl Pts',(55.1597966768613,-2.3342227398772,126.475320624318));
#58068=CARTESIAN_POINT('Ctrl Pts',(55.1520315424838,-2.45450899721224,126.540179095851));
#58069=CARTESIAN_POINT('Ctrl Pts',(55.1442664081063,-2.57224791122007,126.61013991905));
#58070=CARTESIAN_POINT('Ctrl Pts',(55.1365012737288,-2.68697842258056,126.684975952463));
#58071=CARTESIAN_POINT('Ctrl Pts',(55.1287439631096,-2.80159333725745,126.759736584858));
#58072=CARTESIAN_POINT('Ctrl Pts',(55.1209866524904,-2.91320555633316,126.839362439414));
#58073=CARTESIAN_POINT('Ctrl Pts',(55.1132293418711,-3.02137864805867,126.92358052491));
#58074=CARTESIAN_POINT('Ctrl Pts',(55.1054783623063,-3.12946345535509,127.007729876625));
#58075=CARTESIAN_POINT('Ctrl Pts',(55.0977273827415,-3.2341144168565,127.096463757374));
#58076=CARTESIAN_POINT('Ctrl Pts',(55.0899764031767,-3.33492449257867,127.189466194308));
#58077=CARTESIAN_POINT('Ctrl Pts',(55.082228882296,-3.4356895842839,127.282427131193));
#58078=CARTESIAN_POINT('Ctrl Pts',(55.0744813614152,-3.53261691328355,127.379652570323));
#58079=CARTESIAN_POINT('Ctrl Pts',(55.0667338405344,-3.62533305166879,127.480786738896));
#58080=CARTESIAN_POINT('Ctrl Pts',(55.0589880990026,-3.71802789622737,127.5818976803));
#58081=CARTESIAN_POINT('Ctrl Pts',(55.0512423574709,-3.80651321101492,127.686915276679));
#58082=CARTESIAN_POINT('Ctrl Pts',(55.0434966159391,-3.89045321884099,127.795447721766));
#58083=CARTESIAN_POINT('Ctrl Pts',(55.0357509759684,-3.9743921260574,127.903978743792));
#58084=CARTESIAN_POINT('Ctrl Pts',(55.0280053359977,-4.05378560671355,128.016024212992));
#58085=CARTESIAN_POINT('Ctrl Pts',(55.020259696027,-4.1283391397021,128.131160473524));
#58086=CARTESIAN_POINT('Ctrl Pts',(55.0125088500431,-4.20294278174242,128.246374119643));
#58087=CARTESIAN_POINT('Ctrl Pts',(55.0047580040593,-4.27269976305797,128.36468237964));
#58088=CARTESIAN_POINT('Ctrl Pts',(54.9970071580754,-4.33735960634371,128.485633659134));
#58089=CARTESIAN_POINT('Ctrl Pts',(54.9892537440566,-4.40204087293446,128.606625012591));
#58090=CARTESIAN_POINT('Ctrl Pts',(54.9815003300378,-4.46162146331655,128.730260779794));
#58091=CARTESIAN_POINT('Ctrl Pts',(54.9737469160189,-4.51589804062317,128.856067018235));
#58092=CARTESIAN_POINT('Ctrl Pts',(54.9659840490561,-4.5702407918047,128.982026639345));
#58093=CARTESIAN_POINT('Ctrl Pts',(54.9582211820932,-4.61926646590382,129.110161654877));
#58094=CARTESIAN_POINT('Ctrl Pts',(54.9504583151303,-4.66282061557448,129.239979919183));
#58095=CARTESIAN_POINT('Ctrl Pts',(54.9437008198003,-4.70073405199019,129.352985374383));
#58096=CARTESIAN_POINT('Ctrl Pts',(54.9369433244703,-4.73450216614208,129.467265908031));
#58097=CARTESIAN_POINT('Ctrl Pts',(54.9301858291403,-4.76405452823401,129.582490119308));
#58098=CARTESIAN_POINT('Origin',(213.235140564004,0.,130.804360617566));
#58099=CARTESIAN_POINT('',(52.8348764518332,-4.76405452823407,129.582490119308));
#58100=CARTESIAN_POINT('',(53.1798562900863,-4.764054528234,129.582490119308));
#58101=CARTESIAN_POINT('',(213.235140564004,-4.76405452823405,129.582490119308));
#58102=CARTESIAN_POINT('',(54.5148594360289,-4.91824993385995,130.80355402808));
#58103=CARTESIAN_POINT('Ctrl Pts',(54.5148594359912,-4.91824993386006,130.803554028749));
#58104=CARTESIAN_POINT('Ctrl Pts',(54.5068376887833,-4.91827329161115,130.945980077076));
#58105=CARTESIAN_POINT('Ctrl Pts',(54.4988159415755,-4.91210560527091,131.088319782868));
#58106=CARTESIAN_POINT('Ctrl Pts',(54.4907941943676,-4.89979539987938,131.230022574782));
#58107=CARTESIAN_POINT('Ctrl Pts',(54.4827650289623,-4.8874738104923,131.371856407885));
#58108=CARTESIAN_POINT('Ctrl Pts',(54.474735863557,-4.86899840424747,131.513051804552));
#58109=CARTESIAN_POINT('Ctrl Pts',(54.4667066981516,-4.84446927726166,131.653065798514));
#58110=CARTESIAN_POINT('Ctrl Pts',(54.4584284137018,-4.81917909076744,131.797423974047));
#58111=CARTESIAN_POINT('Ctrl Pts',(54.4501501292521,-4.78745354683138,131.940525851146));
#58112=CARTESIAN_POINT('Ctrl Pts',(54.4418718448023,-4.74945803535454,132.08179219417));
#58113=CARTESIAN_POINT('Ctrl Pts',(54.4338185529847,-4.71249519075356,132.219219108077));
#58114=CARTESIAN_POINT('Ctrl Pts',(54.425765261167,-4.66959895055311,132.354908664619));
#58115=CARTESIAN_POINT('Ctrl Pts',(54.4177119693495,-4.62097090322452,132.488347248764));
#58116=CARTESIAN_POINT('Ctrl Pts',(54.4093211885835,-4.57030500244111,132.627377837824));
#58117=CARTESIAN_POINT('Ctrl Pts',(54.4009304078176,-4.51341667649597,132.763964305249));
#58118=CARTESIAN_POINT('Ctrl Pts',(54.3925396270517,-4.4505871748321,132.897553600002));
#58119=CARTESIAN_POINT('Ctrl Pts',(54.3841488462858,-4.38775767316832,133.031142894755));
#58120=CARTESIAN_POINT('Ctrl Pts',(54.3757580655199,-4.31898725652325,133.161734677998));
#58121=CARTESIAN_POINT('Ctrl Pts',(54.367367284754,-4.24460791517983,133.288809592468));
#58122=CARTESIAN_POINT('Ctrl Pts',(54.3595929506349,-4.17569301115675,133.406548676686));
#58123=CARTESIAN_POINT('Ctrl Pts',(54.3518186165158,-4.10176637874171,133.521604683362));
#58124=CARTESIAN_POINT('Ctrl Pts',(54.3440442823967,-4.02306248621924,133.633521499254));
#58125=CARTESIAN_POINT('Ctrl Pts',(54.3362795294496,-3.94445558921022,133.745300387674));
#58126=CARTESIAN_POINT('Ctrl Pts',(54.3285147765025,-3.86108336929452,133.853947466279));
#58127=CARTESIAN_POINT('Ctrl Pts',(54.3207500235554,-3.77322578799594,133.959031791445));
#58128=CARTESIAN_POINT('Ctrl Pts',(54.3129929826704,-3.68545546808591,134.064011745377));
#58129=CARTESIAN_POINT('Ctrl Pts',(54.3052359417854,-3.59320890144388,134.165435689794));
#58130=CARTESIAN_POINT('Ctrl Pts',(54.2974789009004,-3.49680867583896,134.262902528123));
#58131=CARTESIAN_POINT('Ctrl Pts',(54.2897277096603,-3.40048114639432,134.36029586595));
#58132=CARTESIAN_POINT('Ctrl Pts',(54.2819765184202,-3.30000646646958,134.453737760481));
#58133=CARTESIAN_POINT('Ctrl Pts',(54.2742253271801,-3.19574649682287,134.54286130508));
#58134=CARTESIAN_POINT('Ctrl Pts',(54.266477430403,-3.09153084044406,134.631946969796));
#58135=CARTESIAN_POINT('Ctrl Pts',(54.258729533626,-2.98353339078297,134.716717681571));
#58136=CARTESIAN_POINT('Ctrl Pts',(54.2509816368489,-2.87215159014095,134.796844594459));
#58137=CARTESIAN_POINT('Ctrl Pts',(54.2432353607648,-2.76079308817067,134.876954746525));
#58138=CARTESIAN_POINT('Ctrl Pts',(54.2354890846807,-2.64605196051,134.952422803668));
#58139=CARTESIAN_POINT('Ctrl Pts',(54.2277428085966,-2.52835701691984,135.022961553598));
#58140=CARTESIAN_POINT('Ctrl Pts',(54.2199964753312,-2.41066120453218,135.09350082423));
#58141=CARTESIAN_POINT('Ctrl Pts',(54.2122501420658,-2.29001186805411,135.159110514055));
#58142=CARTESIAN_POINT('Ctrl Pts',(54.2045038088004,-2.16686460684491,135.219548137718));
#58143=CARTESIAN_POINT('Ctrl Pts',(54.1967557407975,-2.0436897676604,135.279999295967));
#58144=CARTESIAN_POINT('Ctrl Pts',(54.1890076727945,-1.91801624152583,135.335275911058));
#58145=CARTESIAN_POINT('Ctrl Pts',(54.1812596047915,-1.79032153007529,135.385182801568));
#58146=CARTESIAN_POINT('Ctrl Pts',(54.1735033020497,-1.66249110316584,135.435142733716));
#58147=CARTESIAN_POINT('Ctrl Pts',(54.1657469993079,-1.53263556452254,135.479721398379));
#58148=CARTESIAN_POINT('Ctrl Pts',(54.157990696566,-1.40125010706227,135.518772691193));
#58149=CARTESIAN_POINT('Ctrl Pts',(54.1502302540518,-1.26979452522724,135.557844826858));
#58150=CARTESIAN_POINT('Ctrl Pts',(54.1424698115376,-1.1368077764126,135.591383616741));
#58151=CARTESIAN_POINT('Ctrl Pts',(54.1347093690234,-1.00279632800082,135.619293907555));
#58152=CARTESIAN_POINT('Ctrl Pts',(54.1269364687579,-0.868569752515257,
135.647249002447));
#58153=CARTESIAN_POINT('Ctrl Pts',(54.1191635684926,-0.733315576296101,
135.669557479067));
#58154=CARTESIAN_POINT('Ctrl Pts',(54.1113906682271,-0.597547383831778,
135.686175872835));
#58155=CARTESIAN_POINT('Ctrl Pts',(54.1039003324651,-0.466714707143525,
135.70219014613));
#58156=CARTESIAN_POINT('Ctrl Pts',(54.0964099967031,-0.335405043950435,
135.712920826775));
#58157=CARTESIAN_POINT('Ctrl Pts',(54.0889196609411,-0.204076972630477,
135.718374827124));
#58158=CARTESIAN_POINT('Ctrl Pts',(54.081145326822,-0.0677695575697286,
135.724035617555));
#58159=CARTESIAN_POINT('Ctrl Pts',(54.073370992703,0.0689894699806697,135.724029630001));
#58160=CARTESIAN_POINT('Ctrl Pts',(54.0655966585839,0.205689633197736,135.718307588922));
#58161=CARTESIAN_POINT('Ctrl Pts',(54.0578319056368,0.342221325680881,135.712592599747));
#58162=CARTESIAN_POINT('Ctrl Pts',(54.0500671526897,0.478693911300481,135.701175589746));
#58163=CARTESIAN_POINT('Ctrl Pts',(54.0423023997427,0.614593498937375,135.684059162923));
#58164=CARTESIAN_POINT('Ctrl Pts',(54.0345453588576,0.750358109188164,135.666959736377));
#58165=CARTESIAN_POINT('Ctrl Pts',(54.0267883179726,0.885550468619621,135.644172206678));
#58166=CARTESIAN_POINT('Ctrl Pts',(54.0190312770876,1.01965875675565,135.615751173556));
#58167=CARTESIAN_POINT('Ctrl Pts',(54.0112800858475,1.1536659127882,135.587351572957));
#58168=CARTESIAN_POINT('Ctrl Pts',(54.0035288946073,1.28659024379954,135.553327005585));
#58169=CARTESIAN_POINT('Ctrl Pts',(53.9957777033672,1.41792746626644,135.513783593145));
#58170=CARTESIAN_POINT('Ctrl Pts',(53.9880298065901,1.54920886691043,135.474256987709));
#58171=CARTESIAN_POINT('Ctrl Pts',(53.9802819098131,1.67890412708408,135.429216315017));
#58172=CARTESIAN_POINT('Ctrl Pts',(53.972534013036,1.80652175210833,135.378818205265));
#58173=CARTESIAN_POINT('Ctrl Pts',(53.9647877369519,1.93411268227637,135.328430637712));
#58174=CARTESIAN_POINT('Ctrl Pts',(53.9570414608677,2.05962647832543,135.272688005669));
#58175=CARTESIAN_POINT('Ctrl Pts',(53.9492951847836,2.18258971827225,135.211795833674));
#58176=CARTESIAN_POINT('Ctrl Pts',(53.9415488515183,2.30555386590577,135.150903212188));
#58177=CARTESIAN_POINT('Ctrl Pts',(53.933802518253,2.42596706950877,135.084861148398));
#58178=CARTESIAN_POINT('Ctrl Pts',(53.9260561849876,2.54337905670134,135.013921881692));
#58179=CARTESIAN_POINT('Ctrl Pts',(53.9183081169846,2.66081733749453,134.942966728629));
#58180=CARTESIAN_POINT('Ctrl Pts',(53.9105600489817,2.77525272990735,134.867112392496));
#58181=CARTESIAN_POINT('Ctrl Pts',(53.9028119809787,2.88626292098648,134.786655108615));
#58182=CARTESIAN_POINT('Ctrl Pts',(53.8950556782369,2.99739109501743,134.706112313776));
#58183=CARTESIAN_POINT('Ctrl Pts',(53.887299375495,3.10508647866565,134.62095702856));
#58184=CARTESIAN_POINT('Ctrl Pts',(53.8795430727532,3.20895848632532,134.531526899816));
#58185=CARTESIAN_POINT('Ctrl Pts',(53.871782630239,3.31288593360315,134.44204903952));
#58186=CARTESIAN_POINT('Ctrl Pts',(53.8640221877248,3.4129856535157,134.348292056524));
#58187=CARTESIAN_POINT('Ctrl Pts',(53.8562617452107,3.50890383291668,134.250630623506));
#58188=CARTESIAN_POINT('Ctrl Pts',(53.8484888449453,3.60497598869444,134.152812415686));
#58189=CARTESIAN_POINT('Ctrl Pts',(53.8407159446798,3.6968529278972,134.051077523164));
#58190=CARTESIAN_POINT('Ctrl Pts',(53.8329430444144,3.78422047758097,133.945834545447));
#58191=CARTESIAN_POINT('Ctrl Pts',(53.8254527086523,3.86841199676875,133.844417415061));
#58192=CARTESIAN_POINT('Ctrl Pts',(53.8179623728903,3.94841610267741,133.739743071533));
#58193=CARTESIAN_POINT('Ctrl Pts',(53.8104720371282,4.02399073805242,133.632201066136));
#58194=CARTESIAN_POINT('Ctrl Pts',(53.8026977030091,4.10243080869763,133.520581572919));
#58195=CARTESIAN_POINT('Ctrl Pts',(53.79492336889,4.17634736611468,133.405519093404));
#58196=CARTESIAN_POINT('Ctrl Pts',(53.7871490347709,4.24542302820429,133.287416471568));
#58197=CARTESIAN_POINT('Ctrl Pts',(53.7793842818238,4.31441356071384,133.169459400658));
#58198=CARTESIAN_POINT('Ctrl Pts',(53.7716195288767,4.37857487290968,133.04846997649));
#58199=CARTESIAN_POINT('Ctrl Pts',(53.7638547759296,4.43763138491084,132.924881957745));
#58200=CARTESIAN_POINT('Ctrl Pts',(53.7560977350447,4.49662924115157,132.801416688363));
#58201=CARTESIAN_POINT('Ctrl Pts',(53.7483406941597,4.55053221956859,132.675358311108));
#58202=CARTESIAN_POINT('Ctrl Pts',(53.7405836532747,4.59910960499256,132.547166947531));
#58203=CARTESIAN_POINT('Ctrl Pts',(53.7328324620346,4.64765035783256,132.419072254058));
#58204=CARTESIAN_POINT('Ctrl Pts',(53.7250812707944,4.69087337344552,132.288848140004));
#58205=CARTESIAN_POINT('Ctrl Pts',(53.7173300795542,4.72859535746534,132.156976234753));
#58206=CARTESIAN_POINT('Ctrl Pts',(53.7095821827772,4.76630130863558,132.02516037858));
#58207=CARTESIAN_POINT('Ctrl Pts',(53.701834286,4.79851077118784,131.891698499265));
#58208=CARTESIAN_POINT('Ctrl Pts',(53.6940863892229,4.82508985766454,131.75708876765));
#58209=CARTESIAN_POINT('Ctrl Pts',(53.6863401131388,4.85166338436933,131.622507193489));
#58210=CARTESIAN_POINT('Ctrl Pts',(53.6785938370548,4.87260880192745,131.486778627929));
#58211=CARTESIAN_POINT('Ctrl Pts',(53.6708475609707,4.88784312780795,131.350412465325));
#58212=CARTESIAN_POINT('Ctrl Pts',(53.6631012277053,4.90307756614477,131.214045296096));
#58213=CARTESIAN_POINT('Ctrl Pts',(53.65535489444,4.91260078527364,131.077040908981));
#58214=CARTESIAN_POINT('Ctrl Pts',(53.6476085611746,4.91638161811415,130.939914472433));
#58215=CARTESIAN_POINT('Ctrl Pts',(53.6398604931717,4.92016329764596,130.80275732737));
#58216=CARTESIAN_POINT('Ctrl Pts',(53.6321124251687,4.91820002118929,130.66547846923));
#58217=CARTESIAN_POINT('Ctrl Pts',(53.6243643571657,4.91051274944456,130.528593324287));
#58218=CARTESIAN_POINT('Ctrl Pts',(53.6166080544239,4.90281730757593,130.391562696183));
#58219=CARTESIAN_POINT('Ctrl Pts',(53.608851751682,4.88938573986858,130.254927008135));
#58220=CARTESIAN_POINT('Ctrl Pts',(53.6010954489401,4.87029099711833,130.119197377244));
#58221=CARTESIAN_POINT('Ctrl Pts',(53.5933350064259,4.8511860629289,129.983395303362));
#58222=CARTESIAN_POINT('Ctrl Pts',(53.5855745639118,4.8264120014831,129.848500634578));
#58223=CARTESIAN_POINT('Ctrl Pts',(53.5778141213976,4.79609279086751,129.715013563644));
#58224=CARTESIAN_POINT('Ctrl Pts',(53.5700412211322,4.76572490916348,129.581312207414));
#58225=CARTESIAN_POINT('Ctrl Pts',(53.5622683208667,4.72979419266053,129.449023341951));
#58226=CARTESIAN_POINT('Ctrl Pts',(53.5544954206013,4.68847458954646,129.318632147866));
#58227=CARTESIAN_POINT('Ctrl Pts',(53.5470050848393,4.64865705808367,129.192981002122));
#58228=CARTESIAN_POINT('Ctrl Pts',(53.5395147490773,4.60383574179493,129.069092242499));
#58229=CARTESIAN_POINT('Ctrl Pts',(53.5320244133154,4.55420754334088,128.947380080598));
#58230=CARTESIAN_POINT('Ctrl Pts',(53.5242500791963,4.502697676658,128.821053165085));
#58231=CARTESIAN_POINT('Ctrl Pts',(53.5164757450772,4.44584605869994,128.696670991169));
#58232=CARTESIAN_POINT('Ctrl Pts',(53.5087014109582,4.38382006073538,128.57471832841));
#58233=CARTESIAN_POINT('Ctrl Pts',(53.5009366580111,4.3218705042698,128.452915961408));
#58234=CARTESIAN_POINT('Ctrl Pts',(53.493171905064,4.25475943158813,128.333537493221));
#58235=CARTESIAN_POINT('Ctrl Pts',(53.4854071521169,4.18270281849537,128.21704923417));
#58236=CARTESIAN_POINT('Ctrl Pts',(53.4776501112319,4.11071777304664,128.1006766729));
#58237=CARTESIAN_POINT('Ctrl Pts',(53.4698930703468,4.03379716659119,127.987188938493));
#58238=CARTESIAN_POINT('Ctrl Pts',(53.4621360294618,3.95220340523599,127.877028845091));
#58239=CARTESIAN_POINT('Ctrl Pts',(53.4543848382217,3.87067117437092,127.766951824273));
#58240=CARTESIAN_POINT('Ctrl Pts',(53.4466336469816,3.78447303479879,127.660197762551));
#58241=CARTESIAN_POINT('Ctrl Pts',(53.4388824557415,3.69391511987863,127.557181203115));
#58242=CARTESIAN_POINT('Ctrl Pts',(53.4311345589644,3.6033956944879,127.454208428465));
#58243=CARTESIAN_POINT('Ctrl Pts',(53.4233866621873,3.50852043685308,127.354970289643));
#58244=CARTESIAN_POINT('Ctrl Pts',(53.4156387654103,3.40963610277082,127.259848703468));
#58245=CARTESIAN_POINT('Ctrl Pts',(53.4078924893262,3.31077245315983,127.164747014679));
#58246=CARTESIAN_POINT('Ctrl Pts',(53.400146213242,3.20790167673188,127.073760436642));
#58247=CARTESIAN_POINT('Ctrl Pts',(53.392399937158,3.10140748730035,126.987234125004));
#58248=CARTESIAN_POINT('Ctrl Pts',(53.3846536038926,2.99491251175262,126.900707174648));
#58249=CARTESIAN_POINT('Ctrl Pts',(53.3769072706272,2.88479437326305,126.818640802929));
#58250=CARTESIAN_POINT('Ctrl Pts',(53.3691609373619,2.77146965107501,126.741339692728));
#58251=CARTESIAN_POINT('Ctrl Pts',(53.3614128693589,2.65811955060102,126.664021271479));
#58252=CARTESIAN_POINT('Ctrl Pts',(53.3536648013559,2.54156176042712,126.591470455517));
#58253=CARTESIAN_POINT('Ctrl Pts',(53.3459167333529,2.42224125304778,126.523948210504));
#58254=CARTESIAN_POINT('Ctrl Pts',(53.3381604306111,2.30279393041359,126.456354202045));
#58255=CARTESIAN_POINT('Ctrl Pts',(53.3304041278693,2.18057836590518,126.393799633457));
#58256=CARTESIAN_POINT('Ctrl Pts',(53.3226478251274,2.05606400850246,126.336499400446));
#58257=CARTESIAN_POINT('Ctrl Pts',(53.3148873826132,1.93148319403798,126.279168584577));
#58258=CARTESIAN_POINT('Ctrl Pts',(53.3071269400991,1.80460150342239,126.227097840645));
#58259=CARTESIAN_POINT('Ctrl Pts',(53.2993664975849,1.67590677617028,126.180453228778));
#58260=CARTESIAN_POINT('Ctrl Pts',(53.2915935973195,1.54700545671699,126.133733738839));
#58261=CARTESIAN_POINT('Ctrl Pts',(53.283820697054,1.41628565766153,126.092457905126));
#58262=CARTESIAN_POINT('Ctrl Pts',(53.2760477967886,1.28424959843668,126.056741632073));
#58263=CARTESIAN_POINT('Ctrl Pts',(53.2685574610265,1.15701338254359,126.022323735509));
#58264=CARTESIAN_POINT('Ctrl Pts',(53.2610671252645,1.02855524408416,125.99306827758));
#58265=CARTESIAN_POINT('Ctrl Pts',(53.2535767895025,0.899330101708337,125.969033489991));
#58266=CARTESIAN_POINT('Ctrl Pts',(53.2458024553834,0.765205348782019,125.944087416125));
#58267=CARTESIAN_POINT('Ctrl Pts',(53.2380281212643,0.629829414996312,125.92468668923));
#58268=CARTESIAN_POINT('Ctrl Pts',(53.2302537871452,0.493700618968488,125.910952524904));
#58269=CARTESIAN_POINT('Ctrl Pts',(53.2224890341981,0.357739589515404,125.897235286708));
#58270=CARTESIAN_POINT('Ctrl Pts',(53.214724281251,0.221027929192346,125.889170754803));
#58271=CARTESIAN_POINT('Ctrl Pts',(53.2069595283039,0.0840746982764856,
125.886829274747));
#58272=CARTESIAN_POINT('Ctrl Pts',(53.199202487419,-0.0527425087593545,
125.884490120281));
#58273=CARTESIAN_POINT('Ctrl Pts',(53.191445446534,-0.189800420535316,125.887862712458));
#58274=CARTESIAN_POINT('Ctrl Pts',(53.183688405649,-0.32658464806115,125.896965633448));
#58275=CARTESIAN_POINT('Ctrl Pts',(53.1759372144088,-0.463265725537165,
125.906061689854));
#58276=CARTESIAN_POINT('Ctrl Pts',(53.1681860231687,-0.599673141040839,
125.920879447961));
#58277=CARTESIAN_POINT('Ctrl Pts',(53.1604348319286,-0.73529265508951,125.941385419822));
#58278=CARTESIAN_POINT('Ctrl Pts',(53.1526869351515,-0.870854527226942,
125.961882676098));
#58279=CARTESIAN_POINT('Ctrl Pts',(53.1449390383744,-1.0056287781965,125.988063279294));
#58280=CARTESIAN_POINT('Ctrl Pts',(53.1371911415973,-1.13910666058445,126.019841929306));
#58281=CARTESIAN_POINT('Ctrl Pts',(53.1294448655132,-1.27255662227703,126.051613931909));
#58282=CARTESIAN_POINT('Ctrl Pts',(53.1216985894291,-1.40471037467112,126.08898156167));
#58283=CARTESIAN_POINT('Ctrl Pts',(53.113952313345,-1.53507012185805,126.131808554348));
#58284=CARTESIAN_POINT('Ctrl Pts',(53.1062059800796,-1.66543083133103,126.174635863166));
#58285=CARTESIAN_POINT('Ctrl Pts',(53.0984596468143,-1.79399713773751,126.222922493288));
#58286=CARTESIAN_POINT('Ctrl Pts',(53.0907133135489,-1.92028753148398,126.27648265334));
#58287=CARTESIAN_POINT('Ctrl Pts',(53.0829652455459,-2.04660620708816,126.330054807817));
#58288=CARTESIAN_POINT('Ctrl Pts',(53.075217177543,-2.17064759597379,126.388902689599));
#58289=CARTESIAN_POINT('Ctrl Pts',(53.06746910954,-2.29195162183667,126.452792989037));
#58290=CARTESIAN_POINT('Ctrl Pts',(53.0597128067981,-2.41338457106194,126.516751191846));
#58291=CARTESIAN_POINT('Ctrl Pts',(53.0519565040563,-2.53207399915068,126.585762335289));
#58292=CARTESIAN_POINT('Ctrl Pts',(53.0442002013144,-2.64758535961753,126.659547615024));
#58293=CARTESIAN_POINT('Ctrl Pts',(53.0364397588002,-2.76315837197544,126.733372276185));
#58294=CARTESIAN_POINT('Ctrl Pts',(53.0286793162861,-2.87554961660038,126.811975926982));
#58295=CARTESIAN_POINT('Ctrl Pts',(53.0209188737719,-2.9843556932314,126.895037893771));
#58296=CARTESIAN_POINT('Ctrl Pts',(53.0131459735065,-3.09333643503599,126.978233199003));
#58297=CARTESIAN_POINT('Ctrl Pts',(53.0053730732411,-3.19872020732929,127.065900871786));
#58298=CARTESIAN_POINT('Ctrl Pts',(52.9976001729756,-3.30013803455746,127.157681029863));
#58299=CARTESIAN_POINT('Ctrl Pts',(52.9901098372136,-3.39786906831007,127.246124748015));
#58300=CARTESIAN_POINT('Ctrl Pts',(52.9826195014515,-3.4919172752251,127.33838692841));
#58301=CARTESIAN_POINT('Ctrl Pts',(52.9751291656895,-3.5819877686786,127.434116310763));
#58302=CARTESIAN_POINT('Ctrl Pts',(52.9674484309785,-3.67434778930741,127.532279065178));
#58303=CARTESIAN_POINT('Ctrl Pts',(52.9597676962676,-3.76283341313691,127.634415575219));
#58304=CARTESIAN_POINT('Ctrl Pts',(52.9520869615566,-3.84707694345011,127.740183394611));
#58305=CARTESIAN_POINT('Ctrl Pts',(52.9444153230666,-3.93122070495366,127.845825954183));
#58306=CARTESIAN_POINT('Ctrl Pts',(52.9367436845765,-4.01113211449058,127.955090962074));
#58307=CARTESIAN_POINT('Ctrl Pts',(52.9290720460865,-4.08647997867179,128.067598946098));
#58308=CARTESIAN_POINT('Ctrl Pts',(52.921222413232,-4.16357603461273,128.182717296491));
#58309=CARTESIAN_POINT('Ctrl Pts',(52.9133727803776,-4.2358938671708,128.301230672763));
#58310=CARTESIAN_POINT('Ctrl Pts',(52.9055231475232,-4.30312156478415,128.422695682864));
#58311=CARTESIAN_POINT('Ctrl Pts',(52.8978650440355,-4.36870892092036,128.541196972636));
#58312=CARTESIAN_POINT('Ctrl Pts',(52.8902069405478,-4.4294514484076,128.662507154076));
#58313=CARTESIAN_POINT('Ctrl Pts',(52.8825488370601,-4.48510316096557,128.786185031053));
#58314=CARTESIAN_POINT('Ctrl Pts',(52.8746034395223,-4.54284264968404,128.914502688394));
#58315=CARTESIAN_POINT('Ctrl Pts',(52.8666580419845,-4.59510166066938,129.045368783277));
#58316=CARTESIAN_POINT('Ctrl Pts',(52.8587126444467,-4.64165819593947,129.178263371222));
#58317=CARTESIAN_POINT('Ctrl Pts',(52.8507672469089,-4.68821473120951,129.311157959166));
#58318=CARTESIAN_POINT('Ctrl Pts',(52.8428218493711,-4.7290686185793,129.44608058855));
#58319=CARTESIAN_POINT('Ctrl Pts',(52.8348764518333,-4.76405452823406,129.582490119308));
#58320=CARTESIAN_POINT('Ctrl Pts',(54.5845740201626,-4.76405452823409,129.582490119308));
#58321=CARTESIAN_POINT('Ctrl Pts',(54.5763264523982,-4.80021096026599,129.72346349905));
#58322=CARTESIAN_POINT('Ctrl Pts',(54.5680788846337,-4.83014611411045,129.866199623673));
#58323=CARTESIAN_POINT('Ctrl Pts',(54.5598313168694,-4.85369976884236,130.010143004792));
#58324=CARTESIAN_POINT('Ctrl Pts',(54.5516042144782,-4.87719497793954,130.153729207276));
#58325=CARTESIAN_POINT('Ctrl Pts',(54.543377112087,-4.89434021591618,130.298516386051));
#58326=CARTESIAN_POINT('Ctrl Pts',(54.5351500096957,-4.90502581197444,130.443937468525));
#58327=CARTESIAN_POINT('Ctrl Pts',(54.5283864851401,-4.91381047124995,130.563488558988));
#58328=CARTESIAN_POINT('Ctrl Pts',(54.5216229605845,-4.91823023978955,130.683467711439));
#58329=CARTESIAN_POINT('Ctrl Pts',(54.5148594360288,-4.91824993385995,130.80355402808));
#58330=CARTESIAN_POINT('',(54.8601405639799,-4.91824840592091,130.800400799834));
#58331=CARTESIAN_POINT('Ctrl Pts',(54.9301858291403,-4.76405452823401,129.582490119308));
#58332=CARTESIAN_POINT('Ctrl Pts',(54.9224099595592,-4.79806051746806,129.715078955219));
#58333=CARTESIAN_POINT('Ctrl Pts',(54.9146340899781,-4.82648327833249,129.848917122839));
#58334=CARTESIAN_POINT('Ctrl Pts',(54.906858220397,-4.84926406211354,129.983494539333));
#58335=CARTESIAN_POINT('Ctrl Pts',(54.9061299923381,-4.85139753487553,129.996098023709));
#58336=CARTESIAN_POINT('Ctrl Pts',(54.9054017642793,-4.85348156097654,130.008707990245));
#58337=CARTESIAN_POINT('Ctrl Pts',(54.9046735362204,-4.85551611554211,130.021324019308));
#58338=CARTESIAN_POINT('Ctrl Pts',(54.8919953708024,-4.8909369140413,130.240964146374));
#58339=CARTESIAN_POINT('Ctrl Pts',(54.8793172053843,-4.91146097444499,130.463068264155));
#58340=CARTESIAN_POINT('Ctrl Pts',(54.8666390399663,-4.91682660785611,130.686042526058));
#58341=CARTESIAN_POINT('Ctrl Pts',(54.8644728813137,-4.9177433661454,130.724139333505));
#58342=CARTESIAN_POINT('Ctrl Pts',(54.8623067226612,-4.91821769887402,130.762261452176));
#58343=CARTESIAN_POINT('Ctrl Pts',(54.8601405640086,-4.9182484059205,130.80040079933));
#58344=CARTESIAN_POINT('Ctrl Pts',(54.86014056398,-4.91824840592091,130.800400799834));
#58345=CARTESIAN_POINT('Ctrl Pts',(54.852492109661,-4.91835682891756,130.935066399749));
#58346=CARTESIAN_POINT('Ctrl Pts',(54.8448436553421,-4.91293021809761,131.069935130745));
#58347=CARTESIAN_POINT('Ctrl Pts',(54.8371952010231,-4.90194516963234,131.204506361537));
#58348=CARTESIAN_POINT('Ctrl Pts',(54.82955414848,-4.89097075192503,131.338947361299));
#58349=CARTESIAN_POINT('Ctrl Pts',(54.8219130959369,-4.87444862781496,131.473091033895));
#58350=CARTESIAN_POINT('Ctrl Pts',(54.8142720433938,-4.85240743479849,131.606436143444));
#58351=CARTESIAN_POINT('Ctrl Pts',(54.8064367879361,-4.82980604881087,131.743170316056));
#58352=CARTESIAN_POINT('Ctrl Pts',(54.7986015324783,-4.8014012748303,131.879064358487));
#58353=CARTESIAN_POINT('Ctrl Pts',(54.7907662770205,-4.76728078796237,132.013582247882));
#58354=CARTESIAN_POINT('Ctrl Pts',(54.7831334019653,-4.73404161478038,132.14462561309));
#58355=CARTESIAN_POINT('Ctrl Pts',(54.77550052691,-4.69537848645466,132.27436263008));
#58356=CARTESIAN_POINT('Ctrl Pts',(54.7678676518548,-4.65142422714408,132.402307963894));
#58357=CARTESIAN_POINT('Ctrl Pts',(54.7602358035559,-4.60747588045612,132.530236086806));
#58358=CARTESIAN_POINT('Ctrl Pts',(54.7526039552569,-4.55823794898747,132.656372624051));
#58359=CARTESIAN_POINT('Ctrl Pts',(54.7449721069579,-4.50389280758113,132.780248428227));
#58360=CARTESIAN_POINT('Ctrl Pts',(54.7373395184934,-4.44954239557686,132.904136246348));
#58361=CARTESIAN_POINT('Ctrl Pts',(54.7297069300288,-4.39008395131953,133.025762525944));
#58362=CARTESIAN_POINT('Ctrl Pts',(54.7220743415642,-4.32574733667684,133.144679621833));
#58363=CARTESIAN_POINT('Ctrl Pts',(54.7140869724678,-4.25842020513429,133.269124263536));
#58364=CARTESIAN_POINT('Ctrl Pts',(54.7060996033714,-4.18575073073993,133.390601374145));
#58365=CARTESIAN_POINT('Ctrl Pts',(54.698112234275,-4.10805454349081,133.508629637136));
#58366=CARTESIAN_POINT('Ctrl Pts',(54.6904686914493,-4.03370288558408,133.621577226251));
#58367=CARTESIAN_POINT('Ctrl Pts',(54.6828251486237,-3.95474855325779,133.731366409381));
#58368=CARTESIAN_POINT('Ctrl Pts',(54.675181605798,-3.87151022752934,133.837608319393));
#58369=CARTESIAN_POINT('Ctrl Pts',(54.6675329846001,-3.7882165982317,133.943920816562));
#58370=CARTESIAN_POINT('Ctrl Pts',(54.6598843634022,-3.70063357168755,134.046681044275));
#58371=CARTESIAN_POINT('Ctrl Pts',(54.6522357422043,-3.60911751086314,134.145536137541));
#58372=CARTESIAN_POINT('Ctrl Pts',(54.6445767165599,-3.51747696041644,134.244525703742));
#58373=CARTESIAN_POINT('Ctrl Pts',(54.6369176909155,-3.42189298822956,134.339599256715));
#58374=CARTESIAN_POINT('Ctrl Pts',(54.6292586652711,-3.32275596349902,134.430443334429));
#58375=CARTESIAN_POINT('Ctrl Pts',(54.6282477476499,-3.30967083102071,134.44243387777));
#58376=CARTESIAN_POINT('Ctrl Pts',(54.6272368300286,-3.29652384142501,134.454350798694));
#58377=CARTESIAN_POINT('Ctrl Pts',(54.6262259124074,-3.28331592988795,134.466193432844));
#58378=CARTESIAN_POINT('Ctrl Pts',(54.6184515782884,-3.18174215656343,134.557267713085));
#58379=CARTESIAN_POINT('Ctrl Pts',(54.6106772441693,-3.07621522909855,134.644256788446));
#58380=CARTESIAN_POINT('Ctrl Pts',(54.6029029100503,-2.96709768623001,134.726797918896));
#58381=CARTESIAN_POINT('Ctrl Pts',(54.5951381571032,-2.8581146209808,134.809237324781));
#58382=CARTESIAN_POINT('Ctrl Pts',(54.5873734041561,-2.74555005379505,134.887239459094));
#58383=CARTESIAN_POINT('Ctrl Pts',(54.579608651209,-2.62980215893878,134.960479440138));
#58384=CARTESIAN_POINT('Ctrl Pts',(54.571851610324,-2.51416922652359,135.033646678202));
#58385=CARTESIAN_POINT('Ctrl Pts',(54.5640945694389,-2.39535958665857,135.10206096789));
#58386=CARTESIAN_POINT('Ctrl Pts',(54.5563375285539,-2.27380289087217,135.165438864509));
#58387=CARTESIAN_POINT('Ctrl Pts',(54.5485863373138,-2.15233786193547,135.228768967364));
#58388=CARTESIAN_POINT('Ctrl Pts',(54.5408351460737,-2.02813024569562,135.287070056785));
#58389=CARTESIAN_POINT('Ctrl Pts',(54.5330839548336,-1.90163665178557,135.340103236706));
#58390=CARTESIAN_POINT('Ctrl Pts',(54.5253360580565,-1.77519682102744,135.393113876111));
#58391=CARTESIAN_POINT('Ctrl Pts',(54.5175881612794,-1.64647330484419,135.440860908369));
#58392=CARTESIAN_POINT('Ctrl Pts',(54.5098402645023,-1.51594497393495,135.483152544816));
#58393=CARTESIAN_POINT('Ctrl Pts',(54.5020939884183,-1.38544394673884,135.525435334764));
#58394=CARTESIAN_POINT('Ctrl Pts',(54.4943477123341,-1.25313922743567,135.562264878283));
#58395=CARTESIAN_POINT('Ctrl Pts',(54.4866014362501,-1.11952684399851,135.593498609738));
#58396=CARTESIAN_POINT('Ctrl Pts',(54.4788551029847,-0.985913474264903,
135.624732571754));
#58397=CARTESIAN_POINT('Ctrl Pts',(54.4711087697194,-0.850992801837409,
135.650370550286));
#58398=CARTESIAN_POINT('Ctrl Pts',(54.463362436454,-0.715272708231192,135.670320750506));
#58399=CARTESIAN_POINT('Ctrl Pts',(54.4556143684511,-0.579522221051399,
135.690275418435));
#58400=CARTESIAN_POINT('Ctrl Pts',(54.4478663004481,-0.442972343188713,
135.704539716612));
#58401=CARTESIAN_POINT('Ctrl Pts',(54.4401182324452,-0.306137368921437,
135.713073582677));
#58402=CARTESIAN_POINT('Ctrl Pts',(54.4323619297034,-0.169156964814779,
135.721616518637));
#58403=CARTESIAN_POINT('Ctrl Pts',(54.4246056269615,-0.0318912498499723,
135.724416831938));
#58404=CARTESIAN_POINT('Ctrl Pts',(54.4168493242196,0.105143620223701,135.721486595373));
#58405=CARTESIAN_POINT('Ctrl Pts',(54.4090888817055,0.24225162993376,135.718554794852));
#58406=CARTESIAN_POINT('Ctrl Pts',(54.4013284391913,0.379128159255964,135.709886374709));
#58407=CARTESIAN_POINT('Ctrl Pts',(54.3935679966771,0.515261873555775,135.695545368131));
#58408=CARTESIAN_POINT('Ctrl Pts',(54.3857950964117,0.651614121778978,135.681181340096));
#58409=CARTESIAN_POINT('Ctrl Pts',(54.3780221961463,0.787220785138221,135.661126585887));
#58410=CARTESIAN_POINT('Ctrl Pts',(54.3702492958809,0.921579534162419,135.635496532101));
#58411=CARTESIAN_POINT('Ctrl Pts',(54.3627589601188,1.05105400423141,135.610798195329));
#58412=CARTESIAN_POINT('Ctrl Pts',(54.3552686243567,1.1793694144294,135.580922943679));
#58413=CARTESIAN_POINT('Ctrl Pts',(54.3477782885946,1.30609119643344,135.546017379617));
#58414=CARTESIAN_POINT('Ctrl Pts',(54.3400039544755,1.43761767331749,135.509788360483));
#58415=CARTESIAN_POINT('Ctrl Pts',(54.3322296203564,1.567843928011,135.468025287788));
#58416=CARTESIAN_POINT('Ctrl Pts',(54.3244552862373,1.69626881600993,135.420837105791));
#58417=CARTESIAN_POINT('Ctrl Pts',(54.3166905332902,1.82453543181206,135.373707079011));
#58418=CARTESIAN_POINT('Ctrl Pts',(54.3089257803432,1.95100473465113,135.321165379547));
#58419=CARTESIAN_POINT('Ctrl Pts',(54.3011610273961,2.07518816943759,135.263371396195));
#58420=CARTESIAN_POINT('Ctrl Pts',(54.2934039865111,2.1992482634861,135.205634814641));
#58421=CARTESIAN_POINT('Ctrl Pts',(54.285646945626,2.3210266554283,135.142656494447));
#58422=CARTESIAN_POINT('Ctrl Pts',(54.277889904741,2.44005263806973,135.074644704831));
#58423=CARTESIAN_POINT('Ctrl Pts',(54.2701387135009,2.55898886229112,135.006684203435));
#58424=CARTESIAN_POINT('Ctrl Pts',(54.2623875222608,2.67517647051101,134.933697981066));
#58425=CARTESIAN_POINT('Ctrl Pts',(54.2546363310207,2.78816766404181,134.85594106718));
#58426=CARTESIAN_POINT('Ctrl Pts',(54.2468884342436,2.90111083330153,134.778217202056));
#58427=CARTESIAN_POINT('Ctrl Pts',(54.2391405374666,3.01085996855044,134.695726899473));
#58428=CARTESIAN_POINT('Ctrl Pts',(54.2313926406895,3.11699487124277,134.608769380455));
#58429=CARTESIAN_POINT('Ctrl Pts',(54.2236463646054,3.22310757280147,134.521830051075));
#58430=CARTESIAN_POINT('Ctrl Pts',(54.2159000885213,3.32560724333658,134.430425611544));
#58431=CARTESIAN_POINT('Ctrl Pts',(54.2081538124372,3.42410582310673,134.334896324037));
#58432=CARTESIAN_POINT('Ctrl Pts',(54.2004074791719,3.52260512997115,134.239366331354));
#58433=CARTESIAN_POINT('Ctrl Pts',(54.1926611459065,3.61710300648337,134.139711702128));
#58434=CARTESIAN_POINT('Ctrl Pts',(54.1849148126411,3.70724770068939,134.036310114113));
#58435=CARTESIAN_POINT('Ctrl Pts',(54.1771667446381,3.79741258217466,133.932885370031));
#58436=CARTESIAN_POINT('Ctrl Pts',(54.1694186766352,3.88322208461788,133.82571229208));
#58437=CARTESIAN_POINT('Ctrl Pts',(54.1616706086322,3.96436451380227,133.71520191592));
#58438=CARTESIAN_POINT('Ctrl Pts',(54.1539143058903,4.04559318212589,133.604574088018));
#58439=CARTESIAN_POINT('Ctrl Pts',(54.1461580031485,4.12214463685522,133.490602192192));
#58440=CARTESIAN_POINT('Ctrl Pts',(54.1384017004066,4.19375004038174,133.373727010531));
#58441=CARTESIAN_POINT('Ctrl Pts',(54.1306412578924,4.2653936618683,133.256789449066));
#58442=CARTESIAN_POINT('Ctrl Pts',(54.1228808153783,4.3320857819934,133.136945855578));
#58443=CARTESIAN_POINT('Ctrl Pts',(54.1151203728641,4.39360388483041,133.014661041876));
#58444=CARTESIAN_POINT('Ctrl Pts',(54.1073474725987,4.45522074198733,132.892179925735));
#58445=CARTESIAN_POINT('Ctrl Pts',(54.0995745723332,4.51164682321409,132.767250114756));
#58446=CARTESIAN_POINT('Ctrl Pts',(54.0918016720678,4.56270771882563,132.640356623844));
#58447=CARTESIAN_POINT('Ctrl Pts',(54.0843113363058,4.61191242226692,132.518076030953));
#58448=CARTESIAN_POINT('Ctrl Pts',(54.0768210005438,4.65613514043298,132.393972339013));
#58449=CARTESIAN_POINT('Ctrl Pts',(54.0693306647818,4.69526431933435,132.268490404875));
#58450=CARTESIAN_POINT('Ctrl Pts',(54.0615563306627,4.73587709294693,132.138250785065));
#58451=CARTESIAN_POINT('Ctrl Pts',(54.0537819965436,4.77113110871178,132.00611378788));
#58452=CARTESIAN_POINT('Ctrl Pts',(54.0460076624245,4.80084714367447,131.87255992742));
#58453=CARTESIAN_POINT('Ctrl Pts',(54.0382429094774,4.83052655627995,131.739170660156));
#58454=CARTESIAN_POINT('Ctrl Pts',(54.0304781565302,4.85468148383218,131.604368381918));
#58455=CARTESIAN_POINT('Ctrl Pts',(54.0227134035831,4.87318194867812,131.468650281476));
#58456=CARTESIAN_POINT('Ctrl Pts',(54.0149563626981,4.89166403860154,131.333066978164));
#58457=CARTESIAN_POINT('Ctrl Pts',(54.0071993218131,4.90450278963085,131.196570047684));
#58458=CARTESIAN_POINT('Ctrl Pts',(53.9994422809281,4.91161899582196,131.059668083929));
#58459=CARTESIAN_POINT('Ctrl Pts',(53.991691089688,4.91872983562658,130.922869359011));
#58460=CARTESIAN_POINT('Ctrl Pts',(53.9839398984479,4.9201266999531,130.785666597634));
#58461=CARTESIAN_POINT('Ctrl Pts',(53.9761887072078,4.91578210617702,130.648574395165));
#58462=CARTESIAN_POINT('Ctrl Pts',(53.9684408104307,4.91143935896917,130.51154046054));
#58463=CARTESIAN_POINT('Ctrl Pts',(53.9606929136535,4.90136001953327,130.374617381314));
#58464=CARTESIAN_POINT('Ctrl Pts',(53.9529450168764,4.88556870341262,130.238320418697));
#58465=CARTESIAN_POINT('Ctrl Pts',(53.9451987407923,4.86978069049489,130.102051966467));
#58466=CARTESIAN_POINT('Ctrl Pts',(53.9374524647083,4.84828312242722,129.96640975846));
#58467=CARTESIAN_POINT('Ctrl Pts',(53.9297061886242,4.82115251564445,129.831904200345));
#58468=CARTESIAN_POINT('Ctrl Pts',(53.9219598553588,4.7940217085897,129.697397649339));
#58469=CARTESIAN_POINT('Ctrl Pts',(53.9142135220935,4.7612578571496,129.564028148214));
#58470=CARTESIAN_POINT('Ctrl Pts',(53.9064671888281,4.722988581793,129.432295779902));
#58471=CARTESIAN_POINT('Ctrl Pts',(53.8987191208252,4.68471073629768,129.300533911041));
#58472=CARTESIAN_POINT('Ctrl Pts',(53.8909710528222,4.64092512260295,129.170410279904));
#58473=CARTESIAN_POINT('Ctrl Pts',(53.8832229848192,4.59180907831169,129.042409298478));
#58474=CARTESIAN_POINT('Ctrl Pts',(53.8754666820774,4.54264083290387,128.914272276086));
#58475=CARTESIAN_POINT('Ctrl Pts',(53.8677103793355,4.48813098024788,128.78826277556));
#58476=CARTESIAN_POINT('Ctrl Pts',(53.8599540765937,4.42850504950473,128.66484523108));
#58477=CARTESIAN_POINT('Ctrl Pts',(53.8521936340795,4.36884729460704,128.54136181494));
#58478=CARTESIAN_POINT('Ctrl Pts',(53.8444331915653,4.30406820523118,128.420473455837));
#58479=CARTESIAN_POINT('Ctrl Pts',(53.8366727490511,4.23443856542452,128.302618604859));
#58480=CARTESIAN_POINT('Ctrl Pts',(53.8288998487857,4.16469714993862,128.184574562811));
#58481=CARTESIAN_POINT('Ctrl Pts',(53.8211269485202,4.09008983695267,128.069574088191));
#58482=CARTESIAN_POINT('Ctrl Pts',(53.8133540482548,4.01093041054784,127.958026079209));
#58483=CARTESIAN_POINT('Ctrl Pts',(53.8058637124928,3.93464862868371,127.850533121327));
#58484=CARTESIAN_POINT('Ctrl Pts',(53.7983733767309,3.85414013722455,127.746246219187));
#58485=CARTESIAN_POINT('Ctrl Pts',(53.7908830409689,3.76971890918094,127.645499682314));
#58486=CARTESIAN_POINT('Ctrl Pts',(53.7831087068498,3.68209682461642,127.540933309873));
#58487=CARTESIAN_POINT('Ctrl Pts',(53.7753343727307,3.58998188321917,127.43984983336));
#58488=CARTESIAN_POINT('Ctrl Pts',(53.7675600386116,3.49368148072396,127.342659767731));
#58489=CARTESIAN_POINT('Ctrl Pts',(53.7597952856645,3.3974997598686,127.245589480172));
#58490=CARTESIAN_POINT('Ctrl Pts',(53.7520305327175,3.2971431137477,127.152403331404));
#58491=CARTESIAN_POINT('Ctrl Pts',(53.7442657797704,3.19295958525813,127.063479417981));
#58492=CARTESIAN_POINT('Ctrl Pts',(53.7365087388854,3.08887953331793,126.974643825043));
#58493=CARTESIAN_POINT('Ctrl Pts',(53.7287516980005,2.98098045844711,126.890062295143));
#58494=CARTESIAN_POINT('Ctrl Pts',(53.7209946571155,2.86964744234516,126.810076373907));
#58495=CARTESIAN_POINT('Ctrl Pts',(53.7132434658753,2.75839838333549,126.730150770676));
#58496=CARTESIAN_POINT('Ctrl Pts',(53.7054922746351,2.64372085369219,126.654814105268));
#58497=CARTESIAN_POINT('Ctrl Pts',(53.697741083395,2.52603294204318,126.584367650959));
#58498=CARTESIAN_POINT('Ctrl Pts',(53.6899931866179,2.40839505089669,126.513951138273));
#58499=CARTESIAN_POINT('Ctrl Pts',(53.6822452898408,2.28774965731439,126.448420903148));
#58500=CARTESIAN_POINT('Ctrl Pts',(53.6744973930637,2.16454357044688,126.388034747101));
#58501=CARTESIAN_POINT('Ctrl Pts',(53.6667511169796,2.0413632556369,126.327661222536));
#58502=CARTESIAN_POINT('Ctrl Pts',(53.6590048408955,1.91562366380614,126.272429808721));
#58503=CARTESIAN_POINT('Ctrl Pts',(53.6512585648114,1.78779557270011,126.222552016944));
#58504=CARTESIAN_POINT('Ctrl Pts',(53.643512231546,1.65996653799563,126.17267385698));
#58505=CARTESIAN_POINT('Ctrl Pts',(53.6357658982807,1.53004933747325,126.128149540027));
#58506=CARTESIAN_POINT('Ctrl Pts',(53.6280195650153,1.39853368704842,126.089142002412));
#58507=CARTESIAN_POINT('Ctrl Pts',(53.6202714970123,1.26698858460625,126.05012572933));
#58508=CARTESIAN_POINT('Ctrl Pts',(53.6125234290093,1.1338446947131,126.016628805129));
#58509=CARTESIAN_POINT('Ctrl Pts',(53.6047753610064,0.999605422197866,125.988763867171));
#58510=CARTESIAN_POINT('Ctrl Pts',(53.5970190582645,0.865223478586152,125.960869314026));
#58511=CARTESIAN_POINT('Ctrl Pts',(53.5892627555227,0.729744210181454,125.938618783877));
#58512=CARTESIAN_POINT('Ctrl Pts',(53.5815064527808,0.593680262633053,125.922073570673));
#58513=CARTESIAN_POINT('Ctrl Pts',(53.5737460102667,0.457543693659038,125.90551952679));
#58514=CARTESIAN_POINT('Ctrl Pts',(53.5659855677526,0.320822213284483,125.894676898364));
#58515=CARTESIAN_POINT('Ctrl Pts',(53.5582251252384,0.184031068219737,125.889554860628));
#58516=CARTESIAN_POINT('Ctrl Pts',(53.550452224973,0.0470203338650006,125.884424600543));
#58517=CARTESIAN_POINT('Ctrl Pts',(53.5426793247075,-0.0900598974694271,
125.885033280372));
#58518=CARTESIAN_POINT('Ctrl Pts',(53.5349064244421,-0.226696000177562,
125.891337924152));
#58519=CARTESIAN_POINT('Ctrl Pts',(53.52741608868,-0.358365036386869,125.89741337825));
#58520=CARTESIAN_POINT('Ctrl Pts',(53.519925752918,-0.48962136687944,125.908777834277));
#58521=CARTESIAN_POINT('Ctrl Pts',(53.512435417156,-0.620014017502905,125.925347840313));
#58522=CARTESIAN_POINT('Ctrl Pts',(53.5046610830369,-0.755350545106557,
125.942546103163));
#58523=CARTESIAN_POINT('Ctrl Pts',(53.4968867489178,-0.890185312586909,
125.965406924036));
#58524=CARTESIAN_POINT('Ctrl Pts',(53.4891124147987,-1.02400678718314,125.993893575552));
#58525=CARTESIAN_POINT('Ctrl Pts',(53.4813476618516,-1.15766333877208,126.022345119816));
#58526=CARTESIAN_POINT('Ctrl Pts',(53.4735829089045,-1.29030870347633,126.056408618839));
#58527=CARTESIAN_POINT('Ctrl Pts',(53.4658181559574,-1.42143665226848,126.095995624696));
#58528=CARTESIAN_POINT('Ctrl Pts',(53.4580611150724,-1.55243436293331,126.13554331218));
#58529=CARTESIAN_POINT('Ctrl Pts',(53.4503040741874,-1.6819172850617,126.1806034768));
#58530=CARTESIAN_POINT('Ctrl Pts',(53.4425470333024,-1.80938992058016,126.23103675217));
#58531=CARTESIAN_POINT('Ctrl Pts',(53.4347958420622,-1.93676642799223,126.281431995414));
#58532=CARTESIAN_POINT('Ctrl Pts',(53.4270446508221,-2.06213530417115,126.337192141085));
#58533=CARTESIAN_POINT('Ctrl Pts',(53.419293459582,-2.18501709226091,126.398128284946));
#58534=CARTESIAN_POINT('Ctrl Pts',(53.4115455628049,-2.30784665231276,126.45903852932));
#58535=CARTESIAN_POINT('Ctrl Pts',(53.4037976660278,-2.42819087719435,126.525120223046));
#58536=CARTESIAN_POINT('Ctrl Pts',(53.3960497692507,-2.5455913599293,126.596136800948));
#58537=CARTESIAN_POINT('Ctrl Pts',(53.3883034931666,-2.66296728501429,126.667138523713));
#58538=CARTESIAN_POINT('Ctrl Pts',(53.3805572170825,-2.77740035843642,126.743072875181));
#58539=CARTESIAN_POINT('Ctrl Pts',(53.3728109409984,-2.8884581628889,126.82365810372));
#58540=CARTESIAN_POINT('Ctrl Pts',(53.365064607733,-2.99951678714487,126.904243927121));
#58541=CARTESIAN_POINT('Ctrl Pts',(53.3573182744677,-3.10719977627718,126.989480466486));
#58542=CARTESIAN_POINT('Ctrl Pts',(53.3495719412024,-3.21110534392616,127.079043781013));
#58543=CARTESIAN_POINT('Ctrl Pts',(53.3418238731994,-3.3150341805063,127.168627152622));
#58544=CARTESIAN_POINT('Ctrl Pts',(53.3340758051964,-3.41518361622664,127.262538972281));
#58545=CARTESIAN_POINT('Ctrl Pts',(53.3263277371935,-3.51118678347731,127.360416594497));
#58546=CARTESIAN_POINT('Ctrl Pts',(53.3185714344516,-3.60729198403673,127.458398242214));
#58547=CARTESIAN_POINT('Ctrl Pts',(53.3108151317097,-3.6992418390565,127.560353832651));
#58548=CARTESIAN_POINT('Ctrl Pts',(53.3030588289679,-3.78670768270662,127.665885193378));
#58549=CARTESIAN_POINT('Ctrl Pts',(53.2952983864537,-3.87422020951093,127.77147287937));
#58550=CARTESIAN_POINT('Ctrl Pts',(53.2875379439396,-3.9572437196356,127.880639827452));
#58551=CARTESIAN_POINT('Ctrl Pts',(53.2797775014255,-4.03549199026289,127.992957505413));
#58552=CARTESIAN_POINT('Ctrl Pts',(53.27200460116,-4.11386587196086,128.105455485681));
#58553=CARTESIAN_POINT('Ctrl Pts',(53.2642317008947,-4.18744898578896,128.221113972932));
#58554=CARTESIAN_POINT('Ctrl Pts',(53.2564588006292,-4.25599986145627,128.339477609838));
#58555=CARTESIAN_POINT('Ctrl Pts',(53.2489684648672,-4.32205874012393,128.453538430403));
#58556=CARTESIAN_POINT('Ctrl Pts',(53.2414781291051,-4.38344475415493,128.570110864694));
#58557=CARTESIAN_POINT('Ctrl Pts',(53.2339877933431,-4.43998435146986,128.688770387582));
#58558=CARTESIAN_POINT('Ctrl Pts',(53.2255778333685,-4.50346558455553,128.821998305502));
#58559=CARTESIAN_POINT('Ctrl Pts',(53.2171678733939,-4.56101434039324,128.958227943729));
#58560=CARTESIAN_POINT('Ctrl Pts',(53.2087579134193,-4.61235985925138,129.096929918748));
#58561=CARTESIAN_POINT('Ctrl Pts',(53.2003695126458,-4.66357375223106,129.235276326821));
#58562=CARTESIAN_POINT('Ctrl Pts',(53.1919811118724,-4.70861601874745,129.37608216204));
#58563=CARTESIAN_POINT('Ctrl Pts',(53.1835927110989,-4.74726330354813,129.518796854353));
#58564=CARTESIAN_POINT('Ctrl Pts',(53.1823472374281,-4.75300148618504,129.539986518095));
#58565=CARTESIAN_POINT('Ctrl Pts',(53.1811017637572,-4.75859877524437,129.561218221204));
#58566=CARTESIAN_POINT('Ctrl Pts',(53.1798562900863,-4.764054528234,129.582490119308));
#58567=CARTESIAN_POINT('Origin',(213.235140564004,0.,130.804360617566));
#58568=CARTESIAN_POINT('',(51.084953843968,-4.7640545282341,129.582490119308));
#58569=CARTESIAN_POINT('',(51.4301221724605,-4.76405452823404,129.582490119308));
#58570=CARTESIAN_POINT('',(213.235140564004,-4.76405452823405,129.582490119308));
#58571=CARTESIAN_POINT('',(52.7648594359568,-4.91824789652852,130.808909330876));
#58572=CARTESIAN_POINT('Ctrl Pts',(52.7648594359567,-4.91824789652852,130.808909330876));
#58573=CARTESIAN_POINT('Ctrl Pts',(52.7548231293723,-4.91808396720261,130.986156171337));
#58574=CARTESIAN_POINT('Ctrl Pts',(52.7447868227878,-4.90833502185388,131.16297489367));
#58575=CARTESIAN_POINT('Ctrl Pts',(52.7347505162034,-4.88916015830731,131.338491695973));
#58576=CARTESIAN_POINT('Ctrl Pts',(52.7244724401057,-4.86952338206541,131.518236608637));
#58577=CARTESIAN_POINT('Ctrl Pts',(52.7141943640081,-4.84000106204612,131.696616434439));
#58578=CARTESIAN_POINT('Ctrl Pts',(52.7039162879104,-4.80081190051794,131.872718309702));
#58579=CARTESIAN_POINT('Ctrl Pts',(52.7015047058992,-4.79161680640899,131.914037726925));
#58580=CARTESIAN_POINT('Ctrl Pts',(52.6990931238879,-4.78188972917596,131.95523183297));
#58581=CARTESIAN_POINT('Ctrl Pts',(52.6966815418767,-4.77163386947856,131.996289003898));
#58582=CARTESIAN_POINT('Ctrl Pts',(52.6889072077576,-4.7385715561945,132.128647000972));
#58583=CARTESIAN_POINT('Ctrl Pts',(52.6811328736385,-4.6999455812719,132.259837952312));
#58584=CARTESIAN_POINT('Ctrl Pts',(52.6733585395194,-4.65585283151093,132.389358243372));
#58585=CARTESIAN_POINT('Ctrl Pts',(52.6655937865723,-4.61181442212335,132.518718912249));
#58586=CARTESIAN_POINT('Ctrl Pts',(52.6578290336252,-4.56232276792526,132.646412650967));
#58587=CARTESIAN_POINT('Ctrl Pts',(52.6500642806781,-4.50752548783554,132.771947220238));
#58588=CARTESIAN_POINT('Ctrl Pts',(52.6423072397931,-4.45278263317699,132.897357106804));
#58589=CARTESIAN_POINT('Ctrl Pts',(52.6345501989081,-4.39274479481001,133.020611735612));
#58590=CARTESIAN_POINT('Ctrl Pts',(52.6267931580231,-4.32760888630213,133.141235537132));
#58591=CARTESIAN_POINT('Ctrl Pts',(52.619041966783,-4.26252209728937,133.261768375306));
#58592=CARTESIAN_POINT('Ctrl Pts',(52.6112907755428,-4.19234507538148,133.379673992458));
#58593=CARTESIAN_POINT('Ctrl Pts',(52.6035395843026,-4.11732203065863,133.494498598851));
#58594=CARTESIAN_POINT('Ctrl Pts',(52.5957916875256,-4.0423308727313,133.609274401723));
#58595=CARTESIAN_POINT('Ctrl Pts',(52.5880437907485,-3.96249800195209,133.720971471744));
#58596=CARTESIAN_POINT('Ctrl Pts',(52.5802958939715,-3.87811246956949,133.829162550895));
#58597=CARTESIAN_POINT('Ctrl Pts',(52.5725496178874,-3.793744588821,133.937330998804));
#58598=CARTESIAN_POINT('Ctrl Pts',(52.5648033418033,-3.70482618098061,134.041994606486));
#58599=CARTESIAN_POINT('Ctrl Pts',(52.5570570657192,-3.6116880978717,134.142757260596));
#58600=CARTESIAN_POINT('Ctrl Pts',(52.5493107324538,-3.51854932723861,134.243520658513));
#58601=CARTESIAN_POINT('Ctrl Pts',(52.5415643991884,-3.42119108456039,134.340382758294));
#58602=CARTESIAN_POINT('Ctrl Pts',(52.5338180659231,-3.31998249775356,134.432982846059));
#58603=CARTESIAN_POINT('Ctrl Pts',(52.5260699979201,-3.21875124598558,134.52560367097));
#58604=CARTESIAN_POINT('Ctrl Pts',(52.5183219299171,-3.11366822268962,134.613960320759));
#58605=CARTESIAN_POINT('Ctrl Pts',(52.5105738619142,-3.00513686535423,134.697731327245));
#58606=CARTESIAN_POINT('Ctrl Pts',(52.5028175591723,-2.89649015960073,134.781591366555));
#58607=CARTESIAN_POINT('Ctrl Pts',(52.4950612564305,-2.78438810870268,134.860855787601));
#58608=CARTESIAN_POINT('Ctrl Pts',(52.4873049536886,-2.66926491645348,134.93524525264));
#58609=CARTESIAN_POINT('Ctrl Pts',(52.4795445111745,-2.55408027949013,135.009674421576));
#58610=CARTESIAN_POINT('Ctrl Pts',(52.4717840686603,-2.43587162498801,135.079223251817));
#58611=CARTESIAN_POINT('Ctrl Pts',(52.4640236261461,-2.31509829113535,135.143658137313));
#58612=CARTESIAN_POINT('Ctrl Pts',(52.4562507258807,-2.19413108120543,135.208196459407));
#58613=CARTESIAN_POINT('Ctrl Pts',(52.4484778256153,-2.07059131729113,135.267604262311));
#58614=CARTESIAN_POINT('Ctrl Pts',(52.4407049253498,-1.94495968927383,135.321695547544));
#58615=CARTESIAN_POINT('Ctrl Pts',(52.4332145895878,-1.82389508738227,135.373820478311));
#58616=CARTESIAN_POINT('Ctrl Pts',(52.4257242538257,-1.70088835754032,135.421008607842));
#58617=CARTESIAN_POINT('Ctrl Pts',(52.4182339180637,-1.57638155150185,135.463137738934));
#58618=CARTESIAN_POINT('Ctrl Pts',(52.4104595839446,-1.44715403206905,135.506864208837));
#58619=CARTESIAN_POINT('Ctrl Pts',(52.4026852498255,-1.31590108624763,135.545278995907));
#58620=CARTESIAN_POINT('Ctrl Pts',(52.3949109157064,-1.18309878890254,135.578191397788));
#58621=CARTESIAN_POINT('Ctrl Pts',(52.3871461627594,-1.05046015852005,135.611063238076));
#58622=CARTESIAN_POINT('Ctrl Pts',(52.3793814098123,-0.91627635166687,135.638446092593));
#58623=CARTESIAN_POINT('Ctrl Pts',(52.3716166568652,-0.781041294829518,
135.660198089956));
#58624=CARTESIAN_POINT('Ctrl Pts',(52.3638596159802,-0.64594055535728,135.68192848293));
#58625=CARTESIAN_POINT('Ctrl Pts',(52.3561025750952,-0.509791027245484,
135.698039086684));
#58626=CARTESIAN_POINT('Ctrl Pts',(52.3483455342102,-0.37309925720116,135.708438513234));
#58627=CARTESIAN_POINT('Ctrl Pts',(52.34059434297,-0.236510567483933,135.718830097495));
#58628=CARTESIAN_POINT('Ctrl Pts',(52.3328431517299,-0.0993808380037102,
135.723519047522));
#58629=CARTESIAN_POINT('Ctrl Pts',(52.3250919604898,0.0377761435688174,
135.722465539736));
#58630=CARTESIAN_POINT('Ctrl Pts',(52.3173440637127,0.174874829765394,135.721412479719));
#58631=CARTESIAN_POINT('Ctrl Pts',(52.3095961669357,0.312000354881666,135.714621819247));
#58632=CARTESIAN_POINT('Ctrl Pts',(52.3018482701586,0.448637015385838,135.702105801926));
#58633=CARTESIAN_POINT('Ctrl Pts',(52.2941019940745,0.585245094446364,135.689592402686));
#58634=CARTESIAN_POINT('Ctrl Pts',(52.2863557179903,0.721364123206853,135.671356064373));
#58635=CARTESIAN_POINT('Ctrl Pts',(52.2786094419062,0.856482006800656,135.647461033057));
#58636=CARTESIAN_POINT('Ctrl Pts',(52.2708631086409,0.991600887803797,135.623565825353));
#58637=CARTESIAN_POINT('Ctrl Pts',(52.2631167753755,1.12571822390223,135.59401190938));
#58638=CARTESIAN_POINT('Ctrl Pts',(52.2553704421101,1.25833101363501,135.558914868242));
#58639=CARTESIAN_POINT('Ctrl Pts',(52.2476223741072,1.39097350108239,135.523809967366));
#58640=CARTESIAN_POINT('Ctrl Pts',(52.2398743061043,1.52211039382675,135.483159571203));
#58641=CARTESIAN_POINT('Ctrl Pts',(52.2321262381013,1.65125316376758,135.437129341736));
#58642=CARTESIAN_POINT('Ctrl Pts',(52.2243699353594,1.78053318818129,135.391050190793));
#58643=CARTESIAN_POINT('Ctrl Pts',(52.2166136326176,1.90781448724799,135.339579916194));
#58644=CARTESIAN_POINT('Ctrl Pts',(52.2088573298757,2.03262734845544,135.282932837014));
#58645=CARTESIAN_POINT('Ctrl Pts',(52.2010968873616,2.15750682604496,135.226255523582));
#58646=CARTESIAN_POINT('Ctrl Pts',(52.1933364448474,2.27991489181693,135.164396076276));
#58647=CARTESIAN_POINT('Ctrl Pts',(52.1855760023332,2.39940672287524,135.097614679548));
#58648=CARTESIAN_POINT('Ctrl Pts',(52.1778031020678,2.51909037282892,135.030726079392));
#58649=CARTESIAN_POINT('Ctrl Pts',(52.1700302018024,2.63584809995036,134.958899945769));
#58650=CARTESIAN_POINT('Ctrl Pts',(52.162257301537,2.7492635938284,134.882440159967));
#58651=CARTESIAN_POINT('Ctrl Pts',(52.1547669657749,2.85855614882788,134.808759879969));
#58652=CARTESIAN_POINT('Ctrl Pts',(52.1472766300128,2.96474500072612,134.730777171067));
#58653=CARTESIAN_POINT('Ctrl Pts',(52.1397862942508,3.06748840178517,134.648797893347));
#58654=CARTESIAN_POINT('Ctrl Pts',(52.1320119601317,3.17412735012311,134.563710346395));
#58655=CARTESIAN_POINT('Ctrl Pts',(52.1242376260127,3.27739222169619,134.474047656544));
#58656=CARTESIAN_POINT('Ctrl Pts',(52.1164632918936,3.37686524311802,134.380107279778));
#58657=CARTESIAN_POINT('Ctrl Pts',(52.1086985389465,3.4762156729311,134.286282676131));
#58658=CARTESIAN_POINT('Ctrl Pts',(52.1009337859995,3.57178326918456,134.188191140872));
#58659=CARTESIAN_POINT('Ctrl Pts',(52.0931690330524,3.66318169213571,134.086171543397));
#58660=CARTESIAN_POINT('Ctrl Pts',(52.0854119921674,3.7544893368847,133.984253273223));
#58661=CARTESIAN_POINT('Ctrl Pts',(52.0776549512823,3.84163578968079,133.878414994121));
#58662=CARTESIAN_POINT('Ctrl Pts',(52.0698979103973,3.92427036235503,133.76903348074));
#58663=CARTESIAN_POINT('Ctrl Pts',(52.0621467191572,4.00684261965522,133.65973445281));
#58664=CARTESIAN_POINT('Ctrl Pts',(52.0543955279171,4.08490953447537,133.546897819707));
#58665=CARTESIAN_POINT('Ctrl Pts',(52.0466443366769,4.1581598873237,133.43093431993));
#58666=CARTESIAN_POINT('Ctrl Pts',(52.0388964398999,4.23137910681805,133.315020107735));
#58667=CARTESIAN_POINT('Ctrl Pts',(52.0311485431228,4.29978562764388,133.195982002002));
#58668=CARTESIAN_POINT('Ctrl Pts',(52.0234006463457,4.36311100033826,133.074260496686));
#58669=CARTESIAN_POINT('Ctrl Pts',(52.0156543702616,4.42642312672981,132.952564452884));
#58670=CARTESIAN_POINT('Ctrl Pts',(52.0079080941776,4.48465603876369,132.828186472591));
#58671=CARTESIAN_POINT('Ctrl Pts',(52.0001618180935,4.53758698869521,132.701592122292));
#58672=CARTESIAN_POINT('Ctrl Pts',(51.9924154848281,4.59051832935098,132.574996837501));
#58673=CARTESIAN_POINT('Ctrl Pts',(51.9846691515628,4.63814747899145,132.446185510763));
#58674=CARTESIAN_POINT('Ctrl Pts',(51.9769228182975,4.68029979638086,132.315643806944));
#58675=CARTESIAN_POINT('Ctrl Pts',(51.9691747502945,4.72246155348949,132.185072869216));
#58676=CARTESIAN_POINT('Ctrl Pts',(51.9614266822915,4.75914391764377,132.052771155293));
#58677=CARTESIAN_POINT('Ctrl Pts',(51.9536786142885,4.79022220358968,131.91923922205));
#58678=CARTESIAN_POINT('Ctrl Pts',(51.9459223115466,4.82133351990773,131.78556536948));
#58679=CARTESIAN_POINT('Ctrl Pts',(51.9381660088048,4.84682877133794,131.650659067129));
#58680=CARTESIAN_POINT('Ctrl Pts',(51.930409706063,4.86663437950127,131.515031342133));
#58681=CARTESIAN_POINT('Ctrl Pts',(51.9226492635488,4.88645055851403,131.379331228536));
#58682=CARTESIAN_POINT('Ctrl Pts',(51.9148888210346,4.90057100307806,131.242909313755));
#58683=CARTESIAN_POINT('Ctrl Pts',(51.9071283785204,4.90897417610009,131.106280475943));
#58684=CARTESIAN_POINT('Ctrl Pts',(51.899355478255,4.91739083864145,130.969432309391));
#58685=CARTESIAN_POINT('Ctrl Pts',(51.8915825779896,4.92007188167751,130.832376947139));
#58686=CARTESIAN_POINT('Ctrl Pts',(51.8838096777242,4.91704794319729,130.695628898186));
#58687=CARTESIAN_POINT('Ctrl Pts',(51.8763193419621,4.91413393249765,130.563851985259));
#58688=CARTESIAN_POINT('Ctrl Pts',(51.8688290062,4.90592253917078,130.432360737737));
#58689=CARTESIAN_POINT('Ctrl Pts',(51.861338670438,4.89248636897057,130.301608002518));
#58690=CARTESIAN_POINT('Ctrl Pts',(51.8535643363189,4.87854076229345,130.165897737603));
#58691=CARTESIAN_POINT('Ctrl Pts',(51.8457900021997,4.85892218741209,130.030553202538));
#58692=CARTESIAN_POINT('Ctrl Pts',(51.8380156680807,4.83365508575137,129.89608666413));
#58693=CARTESIAN_POINT('Ctrl Pts',(51.8302509151336,4.80841912353526,129.761785843713));
#58694=CARTESIAN_POINT('Ctrl Pts',(51.8224861621865,4.77754855696881,129.628361247544));
#58695=CARTESIAN_POINT('Ctrl Pts',(51.8147214092394,4.74111966040295,129.496321081374));
#58696=CARTESIAN_POINT('Ctrl Pts',(51.8069643683544,4.70472694553076,129.364412059359));
#58697=CARTESIAN_POINT('Ctrl Pts',(51.7992073274694,4.66278699023241,129.233885105407));
#58698=CARTESIAN_POINT('Ctrl Pts',(51.7914502865844,4.61542723017222,129.10523891931));
#58699=CARTESIAN_POINT('Ctrl Pts',(51.7836990953443,4.56810318447544,128.976689746302));
#58700=CARTESIAN_POINT('Ctrl Pts',(51.7759479041042,4.51536760369651,128.850018883513));
#58701=CARTESIAN_POINT('Ctrl Pts',(51.7681967128641,4.4573978320316,128.725710182909));
#58702=CARTESIAN_POINT('Ctrl Pts',(51.760448816087,4.39945269906604,128.601454316819));
#58703=CARTESIAN_POINT('Ctrl Pts',(51.7527009193099,4.3362779648067,128.479558969658));
#58704=CARTESIAN_POINT('Ctrl Pts',(51.7449530225328,4.26809912580147,128.360488093306));
#58705=CARTESIAN_POINT('Ctrl Pts',(51.7372067464487,4.19993454833959,128.241442124014));
#58706=CARTESIAN_POINT('Ctrl Pts',(51.7294604703645,4.12676814232369,128.125219789429));
#58707=CARTESIAN_POINT('Ctrl Pts',(51.7217141942804,4.04887120142656,128.012260143593));
#58708=CARTESIAN_POINT('Ctrl Pts',(51.7139678610151,3.97097368551191,127.899299663915));
#58709=CARTESIAN_POINT('Ctrl Pts',(51.7062215277497,3.88834578698797,127.789602242901));
#58710=CARTESIAN_POINT('Ctrl Pts',(51.6984751944843,3.80130171160818,127.683577324893));
#58711=CARTESIAN_POINT('Ctrl Pts',(51.6907271264814,3.71423814331134,127.57752866334));
#58712=CARTESIAN_POINT('Ctrl Pts',(51.6829790584785,3.62275667825065,127.475154443454));
#58713=CARTESIAN_POINT('Ctrl Pts',(51.6752309904755,3.52721105367583,127.376830129689));
#58714=CARTESIAN_POINT('Ctrl Pts',(51.6674746877337,3.43156388207406,127.278401315673));
#58715=CARTESIAN_POINT('Ctrl Pts',(51.6597183849917,3.33184419531554,127.184031286891));
#58716=CARTESIAN_POINT('Ctrl Pts',(51.6519620822499,3.22844216409022,127.094058169567));
#58717=CARTESIAN_POINT('Ctrl Pts',(51.6442016397357,3.12498494408731,127.004037030882));
#58718=CARTESIAN_POINT('Ctrl Pts',(51.6364411972215,3.01784176871079,126.918417723729));
#58719=CARTESIAN_POINT('Ctrl Pts',(51.6286807547073,2.90743417820678,126.837496672093));
#58720=CARTESIAN_POINT('Ctrl Pts',(51.6209078544419,2.79684935163712,126.756445718801));
#58721=CARTESIAN_POINT('Ctrl Pts',(51.6131349541765,2.68298996301386,126.680108310303));
#58722=CARTESIAN_POINT('Ctrl Pts',(51.6053620539111,2.56630544391106,126.608736774673));
#58723=CARTESIAN_POINT('Ctrl Pts',(51.5978717181491,2.45386270098901,126.539959774138));
#58724=CARTESIAN_POINT('Ctrl Pts',(51.5903813823871,2.33879693175673,126.475794020765));
#58725=CARTESIAN_POINT('Ctrl Pts',(51.5828910466251,2.22152837431909,126.416423204089));
#58726=CARTESIAN_POINT('Ctrl Pts',(51.575116712506,2.09981354388233,126.354801324852));
#58727=CARTESIAN_POINT('Ctrl Pts',(51.567342378387,1.97534003444174,126.29814996035));
#58728=CARTESIAN_POINT('Ctrl Pts',(51.5595680442679,1.84855204175805,126.246725440041));
#58729=CARTESIAN_POINT('Ctrl Pts',(51.5518032913208,1.72192030394415,126.195364295858));
#58730=CARTESIAN_POINT('Ctrl Pts',(51.5440385383737,1.59298011712144,126.149217324504));
#58731=CARTESIAN_POINT('Ctrl Pts',(51.5362737854266,1.46220027733216,126.10849505183));
#58732=CARTESIAN_POINT('Ctrl Pts',(51.5285167445416,1.33155032992344,126.067813225091));
#58733=CARTESIAN_POINT('Ctrl Pts',(51.5207597036566,1.19906473656917,126.032545490375));
#58734=CARTESIAN_POINT('Ctrl Pts',(51.5130026627716,1.06523194961701,126.002854191868));
#58735=CARTESIAN_POINT('Ctrl Pts',(51.5052514715315,0.931500087010555,125.973185283801));
#58736=CARTESIAN_POINT('Ctrl Pts',(51.4975002802914,0.796423433092171,125.949084526014));
#58737=CARTESIAN_POINT('Ctrl Pts',(51.4897490890512,0.660504925093427,125.93066424762));
#58738=CARTESIAN_POINT('Ctrl Pts',(51.4820011922741,0.524644186086142,125.912251798335));
#58739=CARTESIAN_POINT('Ctrl Pts',(51.474253295497,0.38794269126859,125.899515078869));
#58740=CARTESIAN_POINT('Ctrl Pts',(51.4665053987199,0.250912662888079,125.892515149913));
#58741=CARTESIAN_POINT('Ctrl Pts',(51.4587591226358,0.113911298235665,125.885516685191));
#58742=CARTESIAN_POINT('Ctrl Pts',(51.4510128465517,-0.0234180730788876,
125.884252644021));
#58743=CARTESIAN_POINT('Ctrl Pts',(51.4432665704676,-0.160559421597148,
125.888732098787));
#58744=CARTESIAN_POINT('Ctrl Pts',(51.4355202372022,-0.297701782461875,
125.893211586619));
#58745=CARTESIAN_POINT('Ctrl Pts',(51.4277739039369,-0.434655727003954,
125.903434642224));
#58746=CARTESIAN_POINT('Ctrl Pts',(51.4200275706716,-0.570906942218394,
125.919358230072));
#58747=CARTESIAN_POINT('Ctrl Pts',(51.4122795026686,-0.707188669947411,
125.935285383896));
#58748=CARTESIAN_POINT('Ctrl Pts',(51.4045314346657,-0.842766966950066,
125.956915564863));
#58749=CARTESIAN_POINT('Ctrl Pts',(51.3967833666627,-0.977134740724373,
125.984154111516));
#58750=CARTESIAN_POINT('Ctrl Pts',(51.3890270639208,-1.11164532216801,126.01142160762));
#58751=CARTESIAN_POINT('Ctrl Pts',(51.381270761179,-1.24494242656168,126.044309298625));
#58752=CARTESIAN_POINT('Ctrl Pts',(51.3735144584371,-1.37653068194959,126.082671688364));
#58753=CARTESIAN_POINT('Ctrl Pts',(51.3657540159229,-1.50818916995145,126.121054553265));
#58754=CARTESIAN_POINT('Ctrl Pts',(51.3579935734088,-1.63813662133238,126.164917814277));
#58755=CARTESIAN_POINT('Ctrl Pts',(51.3502331308947,-1.76589579339966,126.214067042058));
#58756=CARTESIAN_POINT('Ctrl Pts',(51.3424602306292,-1.89386005583188,126.263295168542));
#58757=CARTESIAN_POINT('Ctrl Pts',(51.3346873303637,-2.01962866030996,126.317826062918));
#58758=CARTESIAN_POINT('Ctrl Pts',(51.3269144300983,-2.14274638733545,126.377417995162));
#58759=CARTESIAN_POINT('Ctrl Pts',(51.3194240943363,-2.26138847486888,126.434843610565));
#58760=CARTESIAN_POINT('Ctrl Pts',(51.3119337585742,-2.37756879935849,126.496968544019));
#58761=CARTESIAN_POINT('Ctrl Pts',(51.3044434228122,-2.49090566863703,126.563538525984));
#58762=CARTESIAN_POINT('Ctrl Pts',(51.2966678953229,-2.60855779674132,126.632643135065));
#58763=CARTESIAN_POINT('Ctrl Pts',(51.2888923678337,-2.72351839674755,126.706756922238));
#58764=CARTESIAN_POINT('Ctrl Pts',(51.2811168403445,-2.83533150450471,126.78564461341));
#58765=CARTESIAN_POINT('Ctrl Pts',(51.2729433821621,-2.95286690795564,126.868569565547));
#58766=CARTESIAN_POINT('Ctrl Pts',(51.2647699239798,-3.06692375881384,126.956769812886));
#58767=CARTESIAN_POINT('Ctrl Pts',(51.2565964657974,-3.17700074393878,127.049916672651));
#58768=CARTESIAN_POINT('Ctrl Pts',(51.2488405326635,-3.28145466260714,127.138305308141));
#58769=CARTESIAN_POINT('Ctrl Pts',(51.2410845995295,-3.38232484246005,127.231147469214));
#58770=CARTESIAN_POINT('Ctrl Pts',(51.2333286663955,-3.47921249652988,127.328117894957));
#58771=CARTESIAN_POINT('Ctrl Pts',(51.2255779942255,-3.57603443027332,127.425022544229));
#58772=CARTESIAN_POINT('Ctrl Pts',(51.2178273220555,-3.66887893771196,127.526049611477));
#58773=CARTESIAN_POINT('Ctrl Pts',(51.2100766498855,-3.75738161869157,127.630834749699));
#58774=CARTESIAN_POINT('Ctrl Pts',(51.202329556529,-3.84584343423647,127.735571504187));
#58775=CARTESIAN_POINT('Ctrl Pts',(51.1945824631724,-3.92996716150484,127.844062578221));
#58776=CARTESIAN_POINT('Ctrl Pts',(51.1868353698159,-4.00942675444775,127.955908377626));
#58777=CARTESIAN_POINT('Ctrl Pts',(51.1790901759024,-4.088866865378,128.067726754524));
#58778=CARTESIAN_POINT('Ctrl Pts',(51.171344981989,-4.16364489307399,128.182897900499));
#58779=CARTESIAN_POINT('Ctrl Pts',(51.1635997880755,-4.23347667225136,128.30099122253));
#58780=CARTESIAN_POINT('Ctrl Pts',(51.1558527688126,-4.30332490904099,128.419112376217));
#58781=CARTESIAN_POINT('Ctrl Pts',(51.1481057495497,-4.36822436574079,128.540156747432));
#58782=CARTESIAN_POINT('Ctrl Pts',(51.1403587302867,-4.42793561778904,128.663666985302));
#58783=CARTESIAN_POINT('Ctrl Pts',(51.1326106529049,-4.48765502543907,128.787194092694));
#58784=CARTESIAN_POINT('Ctrl Pts',(51.1248625755231,-4.54218465436355,128.913187382096));
#58785=CARTESIAN_POINT('Ctrl Pts',(51.1171144981413,-4.59133260736094,129.041168072469));
#58786=CARTESIAN_POINT('Ctrl Pts',(51.1093610395618,-4.6405146946135,129.169237648041));
#58787=CARTESIAN_POINT('Ctrl Pts',(51.1016075809823,-4.68430751131722,129.299297012578));
#58788=CARTESIAN_POINT('Ctrl Pts',(51.0938541224028,-4.72256850915155,129.430850610733));
#58789=CARTESIAN_POINT('Ctrl Pts',(51.0908873629246,-4.73720857936148,129.481187873805));
#58790=CARTESIAN_POINT('Ctrl Pts',(51.0879206034463,-4.75103925705807,129.531743774527));
#58791=CARTESIAN_POINT('Ctrl Pts',(51.084953843968,-4.7640545282341,129.582490119308));
#58792=CARTESIAN_POINT('Ctrl Pts',(52.8348764518333,-4.76405452823406,129.582490119308));
#58793=CARTESIAN_POINT('Ctrl Pts',(52.827220890531,-4.79776420415706,129.713923634116));
#58794=CARTESIAN_POINT('Ctrl Pts',(52.8195653292287,-4.82602643062361,129.846737056546));
#58795=CARTESIAN_POINT('Ctrl Pts',(52.8119097679264,-4.84874494536196,129.980433729228));
#58796=CARTESIAN_POINT('Ctrl Pts',(52.8040680459372,-4.87201590741839,130.117381510932));
#58797=CARTESIAN_POINT('Ctrl Pts',(52.796226323948,-4.88946999659759,130.255255614782));
#58798=CARTESIAN_POINT('Ctrl Pts',(52.7883846019588,-4.9010600126408,130.393515372987));
#58799=CARTESIAN_POINT('Ctrl Pts',(52.7805428799695,-4.912650028684,130.531775131192));
#58800=CARTESIAN_POINT('Ctrl Pts',(52.7727011579803,-4.9183759803035,130.670420092754));
#58801=CARTESIAN_POINT('Ctrl Pts',(52.7648594359911,-4.91824789652908,130.80890933027));
#58802=CARTESIAN_POINT('',(53.1101405640403,-4.91824977699176,130.802879529943));
#58803=CARTESIAN_POINT('Ctrl Pts',(53.1798562900863,-4.764054528234,129.582490119308));
#58804=CARTESIAN_POINT('Ctrl Pts',(53.1714950727012,-4.80068054274802,129.725294394021));
#58805=CARTESIAN_POINT('Ctrl Pts',(53.163133855316,-4.83092384607784,129.869911740266));
#58806=CARTESIAN_POINT('Ctrl Pts',(53.1547726379309,-4.85461763059599,130.015772814461));
#58807=CARTESIAN_POINT('Ctrl Pts',(53.1464377560349,-4.87823678633974,130.16117446719));
#58808=CARTESIAN_POINT('Ctrl Pts',(53.1381028741389,-4.89534751386974,130.307811751342));
#58809=CARTESIAN_POINT('Ctrl Pts',(53.1297679922429,-4.90583356353445,130.455104108108));
#58810=CARTESIAN_POINT('Ctrl Pts',(53.1232255161754,-4.91406460145802,130.570721429517));
#58811=CARTESIAN_POINT('Ctrl Pts',(53.1166830401079,-4.91821480319711,130.686742000312));
#58812=CARTESIAN_POINT('Ctrl Pts',(53.1101405640404,-4.91824977699175,130.802879529943));
#58813=CARTESIAN_POINT('Ctrl Pts',(53.1101405640086,-4.91824977699192,130.802879530507));
#58814=CARTESIAN_POINT('Ctrl Pts',(53.1021882788582,-4.91829228711791,130.944043020104));
#58815=CARTESIAN_POINT('Ctrl Pts',(53.0942359937077,-4.91225293971663,131.085150680015));
#58816=CARTESIAN_POINT('Ctrl Pts',(53.0862837085573,-4.90017239467302,131.225660469197));
#58817=CARTESIAN_POINT('Ctrl Pts',(53.0783262621069,-4.88808400895026,131.366261453948));
#58818=CARTESIAN_POINT('Ctrl Pts',(53.0703688156565,-4.86994664079856,131.50626343506));
#58819=CARTESIAN_POINT('Ctrl Pts',(53.0624113692061,-4.84585264216121,131.645131236082));
#58820=CARTESIAN_POINT('Ctrl Pts',(53.0544474601463,-4.82173907567583,131.784111818052));
#58821=CARTESIAN_POINT('Ctrl Pts',(53.0464835510865,-4.79165929709876,131.921956028801));
#58822=CARTESIAN_POINT('Ctrl Pts',(53.0385196420267,-4.7557563841171,132.058140613191));
#58823=CARTESIAN_POINT('Ctrl Pts',(53.0305422080014,-4.71979249785521,132.194556477445));
#58824=CARTESIAN_POINT('Ctrl Pts',(53.0225647739761,-4.67798581071775,132.329306734823));
#58825=CARTESIAN_POINT('Ctrl Pts',(53.0145873399508,-4.63052908993263,132.461883893357));
#58826=CARTESIAN_POINT('Ctrl Pts',(53.0066023422531,-4.58302737384138,132.594586752734));
#58827=CARTESIAN_POINT('Ctrl Pts',(52.9986173445555,-4.52986507690039,132.725112071137));
#58828=CARTESIAN_POINT('Ctrl Pts',(52.9906323468578,-4.47128225528688,132.852974308835));
#58829=CARTESIAN_POINT('Ctrl Pts',(52.9826327569507,-4.41259237630968,132.981070208787));
#58830=CARTESIAN_POINT('Ctrl Pts',(52.9746331670437,-4.348462343365,133.106492983004));
#58831=CARTESIAN_POINT('Ctrl Pts',(52.9666335771366,-4.27917763168596,133.228782581453));
#58832=CARTESIAN_POINT('Ctrl Pts',(52.9629357746011,-4.2471508421262,133.285310827584));
#58833=CARTESIAN_POINT('Ctrl Pts',(52.9592379720656,-4.21402322918207,133.341170016988));
#58834=CARTESIAN_POINT('Ctrl Pts',(52.9555401695301,-4.17982597172962,133.39631700388));
#58835=CARTESIAN_POINT('Ctrl Pts',(52.947765835411,-4.10792897267713,133.512259133738));
#58836=CARTESIAN_POINT('Ctrl Pts',(52.9399915012919,-4.03109034571519,133.625391167482));
#58837=CARTESIAN_POINT('Ctrl Pts',(52.9322171671729,-3.94955612214741,133.735263123708));
#58838=CARTESIAN_POINT('Ctrl Pts',(52.9244524142258,-3.86812238222315,133.844999672567));
#58839=CARTESIAN_POINT('Ctrl Pts',(52.9166876612787,-3.78200479065436,133.951483827095));
#58840=CARTESIAN_POINT('Ctrl Pts',(52.9089229083316,-3.6914942148754,134.054291928231));
#58841=CARTESIAN_POINT('Ctrl Pts',(52.9011658674466,-3.60107353547641,134.156997918912));
#58842=CARTESIAN_POINT('Ctrl Pts',(52.8934088265615,-3.50626881145433,134.256034830523));
#58843=CARTESIAN_POINT('Ctrl Pts',(52.8856517856765,-3.40741276095235,134.351009929099));
#58844=CARTESIAN_POINT('Ctrl Pts',(52.8779005944364,-3.30863125856704,134.445913406215));
#58845=CARTESIAN_POINT('Ctrl Pts',(52.8701494031963,-3.20580479155851,134.536760897331));
#58846=CARTESIAN_POINT('Ctrl Pts',(52.8623982119562,-3.09930446578999,134.623194849479));
#58847=CARTESIAN_POINT('Ctrl Pts',(52.8546503151791,-2.99284940550091,134.709592064892));
#58848=CARTESIAN_POINT('Ctrl Pts',(52.8469024184021,-2.88272389506647,134.791579226446));
#58849=CARTESIAN_POINT('Ctrl Pts',(52.839154521625,-2.76933363905012,134.868837737458));
#58850=CARTESIAN_POINT('Ctrl Pts',(52.8314082455409,-2.65596710183092,134.946080087655));
#58851=CARTESIAN_POINT('Ctrl Pts',(52.8236619694568,-2.53933750027575,135.018595534746));
#58852=CARTESIAN_POINT('Ctrl Pts',(52.8159156933727,-2.41988083375982,135.086107902601));
#58853=CARTESIAN_POINT('Ctrl Pts',(52.8081693601074,-2.30042328544208,135.153620768816));
#58854=CARTESIAN_POINT('Ctrl Pts',(52.8004230268421,-2.17813897088937,135.216130289737));
#58855=CARTESIAN_POINT('Ctrl Pts',(52.7926766935767,-2.05348952898221,135.273405685235));
#58856=CARTESIAN_POINT('Ctrl Pts',(52.7849286255738,-1.92881217269695,135.330693907161));
#58857=CARTESIAN_POINT('Ctrl Pts',(52.7771805575708,-1.80176899029603,135.382745508022));
#58858=CARTESIAN_POINT('Ctrl Pts',(52.7694324895679,-1.67284230867172,135.429377555137));
#58859=CARTESIAN_POINT('Ctrl Pts',(52.761676186826,-1.54377860223557,135.476059163346));
#58860=CARTESIAN_POINT('Ctrl Pts',(52.7539198840842,-1.41282776599566,135.517309578464));
#58861=CARTESIAN_POINT('Ctrl Pts',(52.7461635813424,-1.2804885599877,135.552995380342));
#58862=CARTESIAN_POINT('Ctrl Pts',(52.7384031388282,-1.14807872056084,135.588700228806));
#58863=CARTESIAN_POINT('Ctrl Pts',(52.730642696314,-1.0142794160562,135.618834460189));
#58864=CARTESIAN_POINT('Ctrl Pts',(52.7228822537998,-0.87959937710309,135.643315876535));
#58865=CARTESIAN_POINT('Ctrl Pts',(52.7151093535344,-0.74470313779512,135.667836592623));
#58866=CARTESIAN_POINT('Ctrl Pts',(52.707336453269,-0.608923726223788,135.686686306338));
#58867=CARTESIAN_POINT('Ctrl Pts',(52.6995635530036,-0.472775668782891,
135.699834673212));
#58868=CARTESIAN_POINT('Ctrl Pts',(52.6920732172415,-0.34157693616476,135.712505063833));
#58869=CARTESIAN_POINT('Ctrl Pts',(52.6845828814794,-0.210036202295073,
135.719881410388));
#58870=CARTESIAN_POINT('Ctrl Pts',(52.6770925457173,-0.0786117198208892,
135.721982325262));
#58871=CARTESIAN_POINT('Ctrl Pts',(52.6693182115982,0.057795761850565,135.724162896963));
#58872=CARTESIAN_POINT('Ctrl Pts',(52.6615438774791,0.194510100665746,135.720667011559));
#58873=CARTESIAN_POINT('Ctrl Pts',(52.65376954336,0.331019728596693,135.711458436214));
#58874=CARTESIAN_POINT('Ctrl Pts',(52.6460047904129,0.467361120611432,135.702261209615));
#58875=CARTESIAN_POINT('Ctrl Pts',(52.6382400374658,0.603497917385632,135.687365327394));
#58876=CARTESIAN_POINT('Ctrl Pts',(52.6304752845187,0.73891646160067,135.66678650649));
#58877=CARTESIAN_POINT('Ctrl Pts',(52.6227182436337,0.874200506208711,135.646228124761));
#58878=CARTESIAN_POINT('Ctrl Pts',(52.6149612027487,1.00876733388674,135.619998095269));
#58879=CARTESIAN_POINT('Ctrl Pts',(52.6072041618636,1.14210668414339,135.588164060908));
#58880=CARTESIAN_POINT('Ctrl Pts',(52.5994529706235,1.2753454821586,135.556354032841));
#58881=CARTESIAN_POINT('Ctrl Pts',(52.5917017793834,1.40735826646417,135.518948501972));
#58882=CARTESIAN_POINT('Ctrl Pts',(52.5839505881433,1.5376436258362,135.47606642406));
#58883=CARTESIAN_POINT('Ctrl Pts',(52.5762026913662,1.66787361045484,135.433202572174));
#58884=CARTESIAN_POINT('Ctrl Pts',(52.5684547945891,1.79637725982186,135.384866924796));
#58885=CARTESIAN_POINT('Ctrl Pts',(52.560706897812,1.9226672362991,135.331228603377));
#58886=CARTESIAN_POINT('Ctrl Pts',(52.5529606217279,2.04893079563594,135.277601501938));
#58887=CARTESIAN_POINT('Ctrl Pts',(52.5452143456438,2.1729812434949,135.218674085469));
#58888=CARTESIAN_POINT('Ctrl Pts',(52.5374680695597,2.29435055676372,135.154663892647));
#58889=CARTESIAN_POINT('Ctrl Pts',(52.5297217362944,2.41572076595306,135.090653227316));
#58890=CARTESIAN_POINT('Ctrl Pts',(52.521975403029,2.53440945524215,135.021559893149));
#58891=CARTESIAN_POINT('Ctrl Pts',(52.5142290697637,2.64997293568108,134.947647537713));
#58892=CARTESIAN_POINT('Ctrl Pts',(52.5064810017607,2.76556229576036,134.873718630117));
#58893=CARTESIAN_POINT('Ctrl Pts',(52.4987329337577,2.87802472503326,134.794968764409));
#58894=CARTESIAN_POINT('Ctrl Pts',(52.4909848657547,2.98694560758643,134.711704856281));
#58895=CARTESIAN_POINT('Ctrl Pts',(52.4832285630129,3.0959822525496,134.628352454281));
#58896=CARTESIAN_POINT('Ctrl Pts',(52.475472260271,3.20146952070079,134.540476664001));
#58897=CARTESIAN_POINT('Ctrl Pts',(52.4677159575292,3.30302556990645,134.448424989534));
#58898=CARTESIAN_POINT('Ctrl Pts',(52.459955515015,3.40463582263364,134.356324184316));
#58899=CARTESIAN_POINT('Ctrl Pts',(52.4521950725008,3.50231039725711,134.260043328175));
#58900=CARTESIAN_POINT('Ctrl Pts',(52.4444346299867,3.59570515697534,134.159966000593));
#58901=CARTESIAN_POINT('Ctrl Pts',(52.4366617297212,3.68924984225294,134.059728020001));
#58902=CARTESIAN_POINT('Ctrl Pts',(52.4288888294558,3.77850072880353,133.955681686265));
#58903=CARTESIAN_POINT('Ctrl Pts',(52.4211159291904,3.86315417288444,133.848243483089));
#58904=CARTESIAN_POINT('Ctrl Pts',(52.4136255934284,3.94473025104327,133.74471092922));
#58905=CARTESIAN_POINT('Ctrl Pts',(52.4061352576664,4.02203716002516,133.63802907988));
#58906=CARTESIAN_POINT('Ctrl Pts',(52.3986449219044,4.09484286220777,133.528593536449));
#58907=CARTESIAN_POINT('Ctrl Pts',(52.3908705877854,4.17040901471789,133.415008711126));
#58908=CARTESIAN_POINT('Ctrl Pts',(52.3830962536663,4.24136526688172,133.298097454477));
#58909=CARTESIAN_POINT('Ctrl Pts',(52.3753219195472,4.30740461997317,133.178270578439));
#58910=CARTESIAN_POINT('Ctrl Pts',(52.3675571666001,4.37336258546413,133.058591378317));
#58911=CARTESIAN_POINT('Ctrl Pts',(52.359792413653,4.4344155218605,132.936004047404));
#58912=CARTESIAN_POINT('Ctrl Pts',(52.3520276607059,4.49029900794166,132.810949235539));
#58913=CARTESIAN_POINT('Ctrl Pts',(52.3442706198209,4.54612698975663,132.686018629876));
#58914=CARTESIAN_POINT('Ctrl Pts',(52.3365135789359,4.59679558040917,132.558625774976));
#58915=CARTESIAN_POINT('Ctrl Pts',(52.3287565380509,4.64208588152368,132.429236530077));
#58916=CARTESIAN_POINT('Ctrl Pts',(52.3210053468108,4.68734202886951,132.299944858615));
#58917=CARTESIAN_POINT('Ctrl Pts',(52.3132541555707,4.72722783087796,132.168660161268));
#58918=CARTESIAN_POINT('Ctrl Pts',(52.3055029643306,4.76157234338392,132.035868587991));
#58919=CARTESIAN_POINT('Ctrl Pts',(52.2977550675536,4.79590225855609,131.903133454675));
#58920=CARTESIAN_POINT('Ctrl Pts',(52.2900071707765,4.82469547083971,131.768893096979));
#58921=CARTESIAN_POINT('Ctrl Pts',(52.2822592739994,4.84783084900366,131.633648940134));
#58922=CARTESIAN_POINT('Ctrl Pts',(52.2745129979153,4.87096138774524,131.498433073452));
#58923=CARTESIAN_POINT('Ctrl Pts',(52.2667667218312,4.88843638052679,131.362214210394));
#58924=CARTESIAN_POINT('Ctrl Pts',(52.2590204457472,4.90018587087492,131.225503697027));
#58925=CARTESIAN_POINT('Ctrl Pts',(52.2512741124818,4.91193544795512,131.088792174494));
#58926=CARTESIAN_POINT('Ctrl Pts',(52.2435277792164,4.91795940478863,130.951589383941));
#58927=CARTESIAN_POINT('Ctrl Pts',(52.2357814459511,4.91823973082573,130.814411121397));
#58928=CARTESIAN_POINT('Ctrl Pts',(52.2280333779481,4.9185201196399,130.677202138732));
#58929=CARTESIAN_POINT('Ctrl Pts',(52.2202853099451,4.91305431737767,130.540018085897));
#58930=CARTESIAN_POINT('Ctrl Pts',(52.2125372419422,4.90187643087385,130.403373686428));
#58931=CARTESIAN_POINT('Ctrl Pts',(52.2047809392003,4.89068666437921,130.266584059665));
#58932=CARTESIAN_POINT('Ctrl Pts',(52.1970246364585,4.87377271835034,130.130335622283));
#58933=CARTESIAN_POINT('Ctrl Pts',(52.1892683337167,4.85122056282258,129.995137463333));
#58934=CARTESIAN_POINT('Ctrl Pts',(52.1815078912025,4.82865637053038,129.859867145054));
#58935=CARTESIAN_POINT('Ctrl Pts',(52.1737474486883,4.80044805286173,129.725648604601));
#58936=CARTESIAN_POINT('Ctrl Pts',(52.1659870061741,4.76673231175148,129.592978708091));
#58937=CARTESIAN_POINT('Ctrl Pts',(52.1582141059087,4.73296244714045,129.460095838084));
#58938=CARTESIAN_POINT('Ctrl Pts',(52.1504412056432,4.69366760407845,129.328766954656));
#58939=CARTESIAN_POINT('Ctrl Pts',(52.1426683053778,4.6490340552396,129.1994726415));
#58940=CARTESIAN_POINT('Ctrl Pts',(52.1351779696157,4.6060230483258,129.074878502298));
#58941=CARTESIAN_POINT('Ctrl Pts',(52.1276876338536,4.55805485971953,128.952173864907));
#58942=CARTESIAN_POINT('Ctrl Pts',(52.1201972980915,4.50533689806242,128.831767781358));
#58943=CARTESIAN_POINT('Ctrl Pts',(52.1124229639725,4.45062011886634,128.706796464556));
#58944=CARTESIAN_POINT('Ctrl Pts',(52.1046486298534,4.39061295504604,128.58390557009));
#58945=CARTESIAN_POINT('Ctrl Pts',(52.0968742957344,4.32549509400887,128.46357543857));
#58946=CARTESIAN_POINT('Ctrl Pts',(52.0891095427873,4.26045748491567,128.343393603183));
#58947=CARTESIAN_POINT('Ctrl Pts',(52.0813447898402,4.19032189498778,128.225766591963));
#58948=CARTESIAN_POINT('Ctrl Pts',(52.0735800368931,4.11531612928665,128.111155051974));
#58949=CARTESIAN_POINT('Ctrl Pts',(52.0658229960081,4.0403848603692,127.996657345782));
#58950=CARTESIAN_POINT('Ctrl Pts',(52.058065955123,3.96059325448489,127.88516947564));
#58951=CARTESIAN_POINT('Ctrl Pts',(52.050308914238,3.87621493228729,127.777127415249));
#58952=CARTESIAN_POINT('Ctrl Pts',(52.0425577229978,3.79190024043905,127.669166830216));
#58953=CARTESIAN_POINT('Ctrl Pts',(52.0348065317577,3.70300595663472,127.564647189637));
#58954=CARTESIAN_POINT('Ctrl Pts',(52.0270553405176,3.60984869310465,127.463975089608));
#58955=CARTESIAN_POINT('Ctrl Pts',(52.0193074437405,3.51673102389662,127.363345777907));
#58956=CARTESIAN_POINT('Ctrl Pts',(52.0115595469635,3.41935424363475,127.266561040609));
#58957=CARTESIAN_POINT('Ctrl Pts',(52.0038116501864,3.3180747411787,127.173993821435));
#58958=CARTESIAN_POINT('Ctrl Pts',(51.9960653741023,3.21681642421138,127.081445965328));
#58959=CARTESIAN_POINT('Ctrl Pts',(51.9883190980182,3.11165729725033,126.99311413617));
#58960=CARTESIAN_POINT('Ctrl Pts',(51.9805728219341,3.00298975704259,126.909333585362));
#58961=CARTESIAN_POINT('Ctrl Pts',(51.9728264886688,2.89432141467575,126.825552416106));
#58962=CARTESIAN_POINT('Ctrl Pts',(51.9650801554035,2.78214491701042,126.746322830957));
#58963=CARTESIAN_POINT('Ctrl Pts',(51.9573338221382,2.66688448271236,126.671938783052));
#58964=CARTESIAN_POINT('Ctrl Pts',(51.9495857541352,2.55159823663935,126.597538077356));
#58965=CARTESIAN_POINT('Ctrl Pts',(51.9418376861322,2.43322700810209,126.527985280134));
#58966=CARTESIAN_POINT('Ctrl Pts',(51.9340896181293,2.31222228416855,126.463529916986));
#58967=CARTESIAN_POINT('Ctrl Pts',(51.9263333153874,2.19108895497411,126.399006049911));
#58968=CARTESIAN_POINT('Ctrl Pts',(51.9185770126456,2.06731688487346,126.339590623275));
#58969=CARTESIAN_POINT('Ctrl Pts',(51.9108207099037,1.94138085380819,126.28548648312));
#58970=CARTESIAN_POINT('Ctrl Pts',(51.9030602673896,1.81537760689129,126.231353465956));
#58971=CARTESIAN_POINT('Ctrl Pts',(51.8952998248753,1.6872084628153,126.182537522926));
#58972=CARTESIAN_POINT('Ctrl Pts',(51.8875393823612,1.55736533985158,126.139192211096));
#58973=CARTESIAN_POINT('Ctrl Pts',(51.8797664820957,1.42731378117977,126.095777317522));
#58974=CARTESIAN_POINT('Ctrl Pts',(51.8719935818304,1.29558324961926,126.057850712499));
#58975=CARTESIAN_POINT('Ctrl Pts',(51.8642206815649,1.16267875877338,126.025515446775));
#58976=CARTESIAN_POINT('Ctrl Pts',(51.8567303458029,1.03460568093487,125.994355649407));
#58977=CARTESIAN_POINT('Ctrl Pts',(51.8492400100407,0.905442816692088,125.968387791274));
#58978=CARTESIAN_POINT('Ctrl Pts',(51.8417496742786,0.775646422541445,125.947658476226));
#58979=CARTESIAN_POINT('Ctrl Pts',(51.8339753401595,0.640928758656959,125.926143202897));
#58980=CARTESIAN_POINT('Ctrl Pts',(51.8262010060404,0.505101830890329,125.910203399075));
#58981=CARTESIAN_POINT('Ctrl Pts',(51.8184266719213,0.368666888833184,125.899947524486));
#58982=CARTESIAN_POINT('Ctrl Pts',(51.8106619189742,0.232400090648583,125.889704289345));
#58983=CARTESIAN_POINT('Ctrl Pts',(51.8028971660272,0.0955271552260384,
125.885131074731));
#58984=CARTESIAN_POINT('Ctrl Pts',(51.7951324130801,-0.0414412278135017,
125.886285212782));
#58985=CARTESIAN_POINT('Ctrl Pts',(51.787375372195,-0.178273571924836,125.887438204528));
#58986=CARTESIAN_POINT('Ctrl Pts',(51.77961833131,-0.315200786575555,125.894307225319));
#58987=CARTESIAN_POINT('Ctrl Pts',(51.7718612904249,-0.451708176096456,
125.906897724787));
#58988=CARTESIAN_POINT('Ctrl Pts',(51.7641100991848,-0.588112624331933,
125.919478729661));
#58989=CARTESIAN_POINT('Ctrl Pts',(51.7563589079447,-0.724097489860024,
125.937772589476));
#58990=CARTESIAN_POINT('Ctrl Pts',(51.7486077167046,-0.859149555227231,
125.961732704516));
#58991=CARTESIAN_POINT('Ctrl Pts',(51.7408598199275,-0.994144219864393,
125.985682635868));
#58992=CARTESIAN_POINT('Ctrl Pts',(51.7331119231504,-1.12820648873137,126.015293964348));
#58993=CARTESIAN_POINT('Ctrl Pts',(51.7253640263733,-1.26082995682914,126.050468435105));
#58994=CARTESIAN_POINT('Ctrl Pts',(51.7176177502892,-1.39342568295641,126.085635548122));
#58995=CARTESIAN_POINT('Ctrl Pts',(51.7098714742051,-1.52458282929203,126.12636338861));
#58996=CARTESIAN_POINT('Ctrl Pts',(51.702125198121,-1.65380723930944,126.172503033647));
#58997=CARTESIAN_POINT('Ctrl Pts',(51.6943788648557,-1.78303260323173,126.218643019276));
#58998=CARTESIAN_POINT('Ctrl Pts',(51.6866325315904,-1.91032483416792,126.270194757702));
#58999=CARTESIAN_POINT('Ctrl Pts',(51.678886198325,-2.03520732046639,126.326960230598));
#59000=CARTESIAN_POINT('Ctrl Pts',(51.6711381303221,-2.16011777333162,126.383738415729));
#59001=CARTESIAN_POINT('Ctrl Pts',(51.6633900623191,-2.28261705187411,126.445732496925));
#59002=CARTESIAN_POINT('Ctrl Pts',(51.6556419943161,-2.40225118335179,126.512697500011));
#59003=CARTESIAN_POINT('Ctrl Pts',(51.6478856915743,-2.52201246340839,126.579733674299));
#59004=CARTESIAN_POINT('Ctrl Pts',(51.6401293888324,-2.63890217176005,126.651751132883));
#59005=CARTESIAN_POINT('Ctrl Pts',(51.6323730860906,-2.75249301813096,126.728460073191));
#59006=CARTESIAN_POINT('Ctrl Pts',(51.6246126435764,-2.86614449135657,126.805209955369));
#59007=CARTESIAN_POINT('Ctrl Pts',(51.6168522010623,-2.97649327984469,126.886656076616));
#59008=CARTESIAN_POINT('Ctrl Pts',(51.6090917585481,-3.08314429784728,126.972467573501));
#59009=CARTESIAN_POINT('Ctrl Pts',(51.6013188582827,-3.18996652153214,127.058416822619));
#59010=CARTESIAN_POINT('Ctrl Pts',(51.5935459580174,-3.29307881848113,127.148745193199));
#59011=CARTESIAN_POINT('Ctrl Pts',(51.5857730577519,-3.39212151699185,127.243083504442));
#59012=CARTESIAN_POINT('Ctrl Pts',(51.5782827219899,-3.48756376393847,127.333992380447));
#59013=CARTESIAN_POINT('Ctrl Pts',(51.5707923862278,-3.57922694153472,127.428624494595));
#59014=CARTESIAN_POINT('Ctrl Pts',(51.5633020504658,-3.66682522286025,127.526621175893));
#59015=CARTESIAN_POINT('Ctrl Pts',(51.5556023183827,-3.75687236074222,127.627357406551));
#59016=CARTESIAN_POINT('Ctrl Pts',(51.5479025862996,-3.84292231403989,127.731983074538));
#59017=CARTESIAN_POINT('Ctrl Pts',(51.5402028542165,-3.9246153017362,127.840144398078));
#59018=CARTESIAN_POINT('Ctrl Pts',(51.5325123610161,-4.00621026629049,127.948175939208));
#59019=CARTESIAN_POINT('Ctrl Pts',(51.5248218678156,-4.0834584230912,128.059734384513));
#59020=CARTESIAN_POINT('Ctrl Pts',(51.5171313746152,-4.15603749327386,128.174429930836));
#59021=CARTESIAN_POINT('Ctrl Pts',(51.5094496720891,-4.22853360142158,128.28899437358));
#59022=CARTESIAN_POINT('Ctrl Pts',(51.5017679695631,-4.29637103494933,128.406688444264));
#59023=CARTESIAN_POINT('Ctrl Pts',(51.4940862670369,-4.3592688727129,128.527090770162));
#59024=CARTESIAN_POINT('Ctrl Pts',(51.4864096958712,-4.42212469485984,128.647412667572));
#59025=CARTESIAN_POINT('Ctrl Pts',(51.4787331247054,-4.48004729878422,128.770438870475));
#59026=CARTESIAN_POINT('Ctrl Pts',(51.4710565535396,-4.53280012004181,128.895720752571));
#59027=CARTESIAN_POINT('Ctrl Pts',(51.4633830021108,-4.58553218989361,129.020953352465));
#59028=CARTESIAN_POINT('Ctrl Pts',(51.4557094506819,-4.63309836484631,129.148439500688));
#59029=CARTESIAN_POINT('Ctrl Pts',(51.448035899253,-4.67530912500759,129.27770818557));
#59030=CARTESIAN_POINT('Ctrl Pts',(51.4420646569889,-4.70815580329139,129.378299761941));
#59031=CARTESIAN_POINT('Ctrl Pts',(51.4360934147247,-4.73776052669814,129.479970206387));
#59032=CARTESIAN_POINT('Ctrl Pts',(51.4301221724605,-4.76405452823404,129.582490119308));
#59033=CARTESIAN_POINT('Origin',(213.235140564004,0.,130.804360617566));
#59034=CARTESIAN_POINT('',(49.3346698100615,-4.76405452823405,129.582490119308));
#59035=CARTESIAN_POINT('',(49.6802330064605,-4.76405452823399,129.582490119308));
#59036=CARTESIAN_POINT('',(213.235140564004,-4.76405452823405,129.582490119308));
#59037=CARTESIAN_POINT('',(51.0148594359441,-4.91824985095919,130.803149816199));
#59038=CARTESIAN_POINT('Ctrl Pts',(51.0148594359441,-4.91824985095919,130.803149816199));
#59039=CARTESIAN_POINT('Ctrl Pts',(51.0071353012034,-4.91828322888797,130.938730265459));
#59040=CARTESIAN_POINT('Ctrl Pts',(50.9994111664627,-4.91270608195937,131.074537070603));
#59041=CARTESIAN_POINT('Ctrl Pts',(50.991687031722,-4.90148835380578,131.210063686332));
#59042=CARTESIAN_POINT('Ctrl Pts',(50.9839722803074,-4.89028425301693,131.3454256635));
#59043=CARTESIAN_POINT('Ctrl Pts',(50.9762575288928,-4.8734532339703,131.480507737074));
#59044=CARTESIAN_POINT('Ctrl Pts',(50.9685427774782,-4.85101721727347,131.614801867884));
#59045=CARTESIAN_POINT('Ctrl Pts',(50.9608354919237,-4.82860291276832,131.748966037125));
#59046=CARTESIAN_POINT('Ctrl Pts',(50.9531282063692,-4.80059446742222,131.882343392155));
#59047=CARTESIAN_POINT('Ctrl Pts',(50.9454209208147,-4.76706568556513,132.014429959384));
#59048=CARTESIAN_POINT('Ctrl Pts',(50.9377191907425,-4.73356107156231,132.146421317401));
#59049=CARTESIAN_POINT('Ctrl Pts',(50.9300174606703,-4.69454413678102,132.277123356345));
#59050=CARTESIAN_POINT('Ctrl Pts',(50.9223157305981,-4.65013987091716,132.406041685509));
#59051=CARTESIAN_POINT('Ctrl Pts',(50.9146168686266,-4.60575214106635,132.53491200588));
#59052=CARTESIAN_POINT('Ctrl Pts',(50.9069180066552,-4.55598119723129,132.661999562747));
#59053=CARTESIAN_POINT('Ctrl Pts',(50.8992191446838,-4.50100197519907,132.786824811884));
#59054=CARTESIAN_POINT('Ctrl Pts',(50.8915215491434,-4.4460317970224,132.911629527782));
#59055=CARTESIAN_POINT('Ctrl Pts',(50.883823953603,-4.38585520413647,133.034172313289));
#59056=CARTESIAN_POINT('Ctrl Pts',(50.8761263580627,-4.32069520911287,133.153993774561));
#59057=CARTESIAN_POINT('Ctrl Pts',(50.8684283077829,-4.25553136472944,133.273822314346));
#59058=CARTESIAN_POINT('Ctrl Pts',(50.8607302575032,-4.18538372205302,133.390928861787));
#59059=CARTESIAN_POINT('Ctrl Pts',(50.8530322072234,-4.11052093495727,133.504879216979));
#59060=CARTESIAN_POINT('Ctrl Pts',(50.8453319810314,-4.03563698732653,133.618861781104));
#59061=CARTESIAN_POINT('Ctrl Pts',(50.8376317548393,-3.95603546178864,133.729686047173));
#59062=CARTESIAN_POINT('Ctrl Pts',(50.8299315286472,-3.87202767655376,133.836947753083));
#59063=CARTESIAN_POINT('Ctrl Pts',(50.8222229943479,-3.78792925168435,133.944325188288));
#59064=CARTESIAN_POINT('Ctrl Pts',(50.8145144600486,-3.69941531952466,134.048132076211));
#59065=CARTESIAN_POINT('Ctrl Pts',(50.8068059257493,-3.60683699387736,134.147997852988));
#59066=CARTESIAN_POINT('Ctrl Pts',(50.7990927726815,-3.51420319752235,134.247923466938));
#59067=CARTESIAN_POINT('Ctrl Pts',(50.7913796196137,-3.41750043865668,134.343902988288));
#59068=CARTESIAN_POINT('Ctrl Pts',(50.7836664665459,-3.31711499612581,134.435604366611));
#59069=CARTESIAN_POINT('Ctrl Pts',(50.7759418527052,-3.21658039348492,134.527442001619));
#59070=CARTESIAN_POINT('Ctrl Pts',(50.7682172388645,-3.11235248358655,134.614988546159));
#59071=CARTESIAN_POINT('Ctrl Pts',(50.7604926250238,-3.00484915483977,134.697953382502));
#59072=CARTESIAN_POINT('Ctrl Pts',(50.7561778084113,-2.94479992023208,134.744295900262));
#59073=CARTESIAN_POINT('Ctrl Pts',(50.7518629917988,-2.88372922305448,134.789209658533));
#59074=CARTESIAN_POINT('Ctrl Pts',(50.7475481751863,-2.82171334507904,134.832650187682));
#59075=CARTESIAN_POINT('Ctrl Pts',(50.7397738410673,-2.70997460868076,134.910920301627));
#59076=CARTESIAN_POINT('Ctrl Pts',(50.7319995069481,-2.5947997739891,134.984661667943));
#59077=CARTESIAN_POINT('Ctrl Pts',(50.7242251728291,-2.47659216751477,135.053557517958));
#59078=CARTESIAN_POINT('Ctrl Pts',(50.716460419882,-2.35853024135089,135.122368459996));
#59079=CARTESIAN_POINT('Ctrl Pts',(50.7086956669349,-2.23744331469214,135.186345572587));
#59080=CARTESIAN_POINT('Ctrl Pts',(50.7009309139878,-2.11376556510177,135.245213936275));
#59081=CARTESIAN_POINT('Ctrl Pts',(50.6931738731028,-1.99021065399618,135.304023831075));
#59082=CARTESIAN_POINT('Ctrl Pts',(50.6854168322178,-1.8640703915577,135.357734907682));
#59083=CARTESIAN_POINT('Ctrl Pts',(50.6776597913328,-1.73580524991296,135.406117151421));
#59084=CARTESIAN_POINT('Ctrl Pts',(50.6699086000927,-1.60763683400894,135.454462909733));
#59085=CARTESIAN_POINT('Ctrl Pts',(50.6621574088526,-1.4773470926808,135.497487696361));
#59086=CARTESIAN_POINT('Ctrl Pts',(50.6544062176125,-1.34541793369754,135.535008950108));
#59087=CARTESIAN_POINT('Ctrl Pts',(50.6466583208354,-1.21354484812635,135.572514256322));
#59088=CARTESIAN_POINT('Ctrl Pts',(50.6389104240584,-1.08003410603958,135.604520575315));
#59089=CARTESIAN_POINT('Ctrl Pts',(50.6311625272813,-0.945384081455753,
135.630894777916));
#59090=CARTESIAN_POINT('Ctrl Pts',(50.6234162511972,-0.810762222754529,
135.657263463604));
#59091=CARTESIAN_POINT('Ctrl Pts',(50.6156699751131,-0.675001939005924,
135.678002301136));
#59092=CARTESIAN_POINT('Ctrl Pts',(50.607923699029,-0.53861275026113,135.693029083289));
#59093=CARTESIAN_POINT('Ctrl Pts',(50.6001773657637,-0.402222554722327,
135.708055976367));
#59094=CARTESIAN_POINT('Ctrl Pts',(50.5924310324983,-0.265203833537383,
135.717370687113));
#59095=CARTESIAN_POINT('Ctrl Pts',(50.584684699233,-0.128071801995861,135.720942832483));
#59096=CARTESIAN_POINT('Ctrl Pts',(50.5769366312301,0.00909093931313087,
135.724515777809));
#59097=CARTESIAN_POINT('Ctrl Pts',(50.5691885632271,0.14636665071432,135.722343588573));
#59098=CARTESIAN_POINT('Ctrl Pts',(50.5614404952242,0.28323993842686,135.714448009841));
#59099=CARTESIAN_POINT('Ctrl Pts',(50.5536841924823,0.420258696698767,135.706544039595));
#59100=CARTESIAN_POINT('Ctrl Pts',(50.5459278897404,0.556873785965126,135.692904551183));
#59101=CARTESIAN_POINT('Ctrl Pts',(50.5381715869986,0.692574200735226,135.673603273152));
#59102=CARTESIAN_POINT('Ctrl Pts',(50.5304111444844,0.828347042902733,135.654291693447));
#59103=CARTESIAN_POINT('Ctrl Pts',(50.5226507019702,0.963203853577455,135.629312373967));
#59104=CARTESIAN_POINT('Ctrl Pts',(50.5148902594561,1.09664462925778,135.598790053862));
#59105=CARTESIAN_POINT('Ctrl Pts',(50.5071173591906,1.23029961591755,135.568218736619));
#59106=CARTESIAN_POINT('Ctrl Pts',(50.4993444589252,1.36253364775798,135.53208674059));
#59107=CARTESIAN_POINT('Ctrl Pts',(50.4915715586598,1.49286180945023,135.490568752123));
#59108=CARTESIAN_POINT('Ctrl Pts',(50.4840812228977,1.61845221418903,135.450560047113));
#59109=CARTESIAN_POINT('Ctrl Pts',(50.4765908871356,1.74227261993963,135.405550245124));
#59110=CARTESIAN_POINT('Ctrl Pts',(50.4691005513735,1.86390911523152,135.355736878946));
#59111=CARTESIAN_POINT('Ctrl Pts',(50.4613262172544,1.99015749521196,135.30403482385));
#59112=CARTESIAN_POINT('Ctrl Pts',(50.4535518831354,2.11445300661022,135.24699398323));
#59113=CARTESIAN_POINT('Ctrl Pts',(50.4457775490163,2.23631113514054,135.184782465898));
#59114=CARTESIAN_POINT('Ctrl Pts',(50.4380127960692,2.35801908441822,135.122647618701));
#59115=CARTESIAN_POINT('Ctrl Pts',(50.4302480431222,2.47729528273821,135.055354950026));
#59116=CARTESIAN_POINT('Ctrl Pts',(50.4224832901751,2.59367374899857,134.983121145074));
#59117=CARTESIAN_POINT('Ctrl Pts',(50.4147262492901,2.70993662652575,134.910959083754));
#59118=CARTESIAN_POINT('Ctrl Pts',(50.4069692084051,2.82330716944753,134.833865857359));
#59119=CARTESIAN_POINT('Ctrl Pts',(50.3992121675201,2.93334296347093,134.752104545578));
#59120=CARTESIAN_POINT('Ctrl Pts',(50.39146097628,3.04329577864551,134.670404890639));
#59121=CARTESIAN_POINT('Ctrl Pts',(50.3837097850398,3.14991853785197,134.584044389374));
#59122=CARTESIAN_POINT('Ctrl Pts',(50.3759585937998,3.25279716426536,134.493329805652));
#59123=CARTESIAN_POINT('Ctrl Pts',(50.3682106970227,3.35563206451844,134.402653778047));
#59124=CARTESIAN_POINT('Ctrl Pts',(50.3604628002456,3.45472570443246,134.307627606723));
#59125=CARTESIAN_POINT('Ctrl Pts',(50.3527149034686,3.54969669533472,134.208598628286));
#59126=CARTESIAN_POINT('Ctrl Pts',(50.3449686273845,3.64464782035316,134.109590364576));
#59127=CARTESIAN_POINT('Ctrl Pts',(50.3372223513004,3.73547774121884,134.006581241188));
#59128=CARTESIAN_POINT('Ctrl Pts',(50.3294760752163,3.82184188663316,133.899955496757));
#59129=CARTESIAN_POINT('Ctrl Pts',(50.321729741951,3.90820666956787,133.793328965241));
#59130=CARTESIAN_POINT('Ctrl Pts',(50.3139834086857,3.99010536519393,133.683086063219));
#59131=CARTESIAN_POINT('Ctrl Pts',(50.3062370754203,4.06723392494572,133.569643833128));
#59132=CARTESIAN_POINT('Ctrl Pts',(50.2984890074174,4.14437975710328,133.456176198438));
#59133=CARTESIAN_POINT('Ctrl Pts',(50.2907409394145,4.21675310793709,133.339508133245));
#59134=CARTESIAN_POINT('Ctrl Pts',(50.2829928714116,4.28409368926029,133.220085006676));
#59135=CARTESIAN_POINT('Ctrl Pts',(50.2752365686697,4.35150584095505,133.100534955786));
#59136=CARTESIAN_POINT('Ctrl Pts',(50.2674802659279,4.41387434582178,132.978224335396));
#59137=CARTESIAN_POINT('Ctrl Pts',(50.259723963186,4.47098502282337,132.853622920979));
#59138=CARTESIAN_POINT('Ctrl Pts',(50.2519635206719,4.52812618151293,132.728955003035));
#59139=CARTESIAN_POINT('Ctrl Pts',(50.2442030781577,4.58000377281345,132.601994216538));
#59140=CARTESIAN_POINT('Ctrl Pts',(50.2364426356436,4.62645247919981,132.473228653154));
#59141=CARTESIAN_POINT('Ctrl Pts',(50.2286697353782,4.67297574917319,132.344256383855));
#59142=CARTESIAN_POINT('Ctrl Pts',(50.2208968351127,4.71405260180808,132.213473921379));
#59143=CARTESIAN_POINT('Ctrl Pts',(50.2131239348473,4.74956789709703,132.081383660962));
#59144=CARTESIAN_POINT('Ctrl Pts',(50.2056335990851,4.78379212194542,131.954095214224));
#59145=CARTESIAN_POINT('Ctrl Pts',(50.1981432633229,4.8128520545781,131.825592702687));
#59146=CARTESIAN_POINT('Ctrl Pts',(50.1906529275607,4.83669015566738,131.696331133093));
#59147=CARTESIAN_POINT('Ctrl Pts',(50.1828785934416,4.86143208560437,131.562168571803));
#59148=CARTESIAN_POINT('Ctrl Pts',(50.1751042593225,4.8806267709077,131.426763270177));
#59149=CARTESIAN_POINT('Ctrl Pts',(50.1673299252034,4.89415375447531,131.290613730723));
#59150=CARTESIAN_POINT('Ctrl Pts',(50.1595651722563,4.90766406724457,131.15463198341));
#59151=CARTESIAN_POINT('Ctrl Pts',(50.1518004193092,4.91552053793604,131.017908208552));
#59152=CARTESIAN_POINT('Ctrl Pts',(50.1440356663622,4.91765359577738,130.880951572892));
#59153=CARTESIAN_POINT('Ctrl Pts',(50.1362786254772,4.91978453503561,130.744130964493));
#59154=CARTESIAN_POINT('Ctrl Pts',(50.1285215845921,4.91620336795408,130.607078343939));
#59155=CARTESIAN_POINT('Ctrl Pts',(50.1207645437071,4.9068922951956,130.470308127903));
#59156=CARTESIAN_POINT('Ctrl Pts',(50.113013352467,4.89758824398954,130.333641051351));
#59157=CARTESIAN_POINT('Ctrl Pts',(50.1052621612269,4.8825629141755,130.19725634391));
#59158=CARTESIAN_POINT('Ctrl Pts',(50.0975109699867,4.86185057624597,130.061668193506));
#59159=CARTESIAN_POINT('Ctrl Pts',(50.0897630732096,4.84114704161254,129.926137671681));
#59160=CARTESIAN_POINT('Ctrl Pts',(50.0820151764326,4.81476136526627,129.791403419199));
#59161=CARTESIAN_POINT('Ctrl Pts',(50.0742672796555,4.78277962143859,129.657974053072));
#59162=CARTESIAN_POINT('Ctrl Pts',(50.0665210035714,4.75080456750228,129.524572597492));
#59163=CARTESIAN_POINT('Ctrl Pts',(50.0587747274873,4.71323586549744,129.392475865301));
#59164=CARTESIAN_POINT('Ctrl Pts',(50.0510284514032,4.6702105370682,129.262181444462));
#59165=CARTESIAN_POINT('Ctrl Pts',(50.0432821181378,4.62718489103582,129.131886061818));
#59166=CARTESIAN_POINT('Ctrl Pts',(50.0355357848724,4.57870266079615,129.003393388321));
#59167=CARTESIAN_POINT('Ctrl Pts',(50.0277894516071,4.52495037028572,128.877184650263));
#59168=CARTESIAN_POINT('Ctrl Pts',(50.0200413836041,4.47118604232237,128.750947648633));
#59169=CARTESIAN_POINT('Ctrl Pts',(50.0122933156011,4.41214945880708,128.626995959843));
#59170=CARTESIAN_POINT('Ctrl Pts',(50.0045452475981,4.34807462927492,128.505789304608));
#59171=CARTESIAN_POINT('Ctrl Pts',(49.9967889448562,4.28393170025152,128.384453829497));
#59172=CARTESIAN_POINT('Ctrl Pts',(49.9890326421144,4.2147400116167,128.265869562061));
#59173=CARTESIAN_POINT('Ctrl Pts',(49.9812763393726,4.14077902869673,128.15047062399));
#59174=CARTESIAN_POINT('Ctrl Pts',(49.9735158968584,4.06677857057324,128.03501009403));
#59175=CARTESIAN_POINT('Ctrl Pts',(49.9657554543442,3.98800397045543,127.922738600928));
#59176=CARTESIAN_POINT('Ctrl Pts',(49.95799501183,3.90477651552403,127.814059056467));
#59177=CARTESIAN_POINT('Ctrl Pts',(49.9502221115645,3.82141545649326,127.705205049952));
#59178=CARTESIAN_POINT('Ctrl Pts',(49.9424492112991,3.73358750906663,127.599954814966));
#59179=CARTESIAN_POINT('Ctrl Pts',(49.9346763110337,3.64165311660002,127.498676778954));
#59180=CARTESIAN_POINT('Ctrl Pts',(49.9271859752717,3.55306077086919,127.401080454657));
#59181=CARTESIAN_POINT('Ctrl Pts',(49.9196956395097,3.46065557195196,127.307172763982));
#59182=CARTESIAN_POINT('Ctrl Pts',(49.9122053037477,3.36478922849466,127.217248058654));
#59183=CARTESIAN_POINT('Ctrl Pts',(49.9044309696286,3.26528808348653,127.12391383079));
#59184=CARTESIAN_POINT('Ctrl Pts',(49.8966566355097,3.16174296461367,127.034574925435));
#59185=CARTESIAN_POINT('Ctrl Pts',(49.8888823013906,3.05450816614984,126.949602139344));
#59186=CARTESIAN_POINT('Ctrl Pts',(49.8811175484435,2.9474055249914,126.864734074618));
#59187=CARTESIAN_POINT('Ctrl Pts',(49.8733527954964,2.83662255529905,126.784221663344));
#59188=CARTESIAN_POINT('Ctrl Pts',(49.8655880425493,2.72255002877106,126.708398654444));
#59189=CARTESIAN_POINT('Ctrl Pts',(49.8578310016643,2.60859080068472,126.632650954027));
#59190=CARTESIAN_POINT('Ctrl Pts',(49.8500739607794,2.49134884119863,126.561583602211));
#59191=CARTESIAN_POINT('Ctrl Pts',(49.8423169198944,2.3712473226527,126.49548962886));
#59192=CARTESIAN_POINT('Ctrl Pts',(49.8345657286543,2.25123637359583,126.429445497489));
#59193=CARTESIAN_POINT('Ctrl Pts',(49.8268145374142,2.12837049883189,126.368367467247));
#59194=CARTESIAN_POINT('Ctrl Pts',(49.819063346174,2.0031008232624,126.312504636533));
#59195=CARTESIAN_POINT('Ctrl Pts',(49.811315449397,1.87788439064671,126.256665549011));
#59196=CARTESIAN_POINT('Ctrl Pts',(49.8035675526198,1.75026654559043,126.206037411269));
#59197=CARTESIAN_POINT('Ctrl Pts',(49.7958196558428,1.62072172721546,126.160822726536));
#59198=CARTESIAN_POINT('Ctrl Pts',(49.7880733797587,1.49120400682364,126.11561749974));
#59199=CARTESIAN_POINT('Ctrl Pts',(49.7803271036746,1.3597604837576,126.075823602347));
#59200=CARTESIAN_POINT('Ctrl Pts',(49.7725808275904,1.22688385640715,126.041594712613));
#59201=CARTESIAN_POINT('Ctrl Pts',(49.7648344943251,1.09400624819162,126.007365570208));
#59202=CARTESIAN_POINT('Ctrl Pts',(49.7570881610598,0.9596958931877,125.978701614964));
#59203=CARTESIAN_POINT('Ctrl Pts',(49.7493418277944,0.824458481448597,125.955706033574));
#59204=CARTESIAN_POINT('Ctrl Pts',(49.7415937597915,0.689190784229912,125.932705302483));
#59205=CARTESIAN_POINT('Ctrl Pts',(49.7338456917885,0.552996002519423,125.915375536718));
#59206=CARTESIAN_POINT('Ctrl Pts',(49.7260976237856,0.416387400243408,125.903768347705));
#59207=CARTESIAN_POINT('Ctrl Pts',(49.7183413210438,0.279633608718113,125.892148822433));
#59208=CARTESIAN_POINT('Ctrl Pts',(49.7105850183019,0.142465508235302,125.886264056561));
#59209=CARTESIAN_POINT('Ctrl Pts',(49.7028287155601,0.00539939550242816,
125.886113581372));
#59210=CARTESIAN_POINT('Ctrl Pts',(49.6950682730459,-0.131739873541793,
125.88596302587));
#59211=CARTESIAN_POINT('Ctrl Pts',(49.6873078305317,-0.268776655922635,
125.891552843556));
#59212=CARTESIAN_POINT('Ctrl Pts',(49.6795473880175,-0.405198306976869,
125.902830510087));
#59213=CARTESIAN_POINT('Ctrl Pts',(49.6717744877521,-0.541838954176136,
125.914126280529));
#59214=CARTESIAN_POINT('Ctrl Pts',(49.6640015874867,-0.677862108612464,
125.931128097226));
#59215=CARTESIAN_POINT('Ctrl Pts',(49.6562286872213,-0.812762973402048,
125.953731853007));
#59216=CARTESIAN_POINT('Ctrl Pts',(49.6487383514591,-0.942759851963584,
125.975513905331));
#59217=CARTESIAN_POINT('Ctrl Pts',(49.641248015697,-1.07171431887242,126.002497615599));
#59218=CARTESIAN_POINT('Ctrl Pts',(49.6337576799349,-1.19918862057225,126.034546185663));
#59219=CARTESIAN_POINT('Ctrl Pts',(49.6259833458158,-1.33149614916414,126.067809887002));
#59220=CARTESIAN_POINT('Ctrl Pts',(49.6182090116968,-1.46262816642929,126.106635467491));
#59221=CARTESIAN_POINT('Ctrl Pts',(49.6104346775777,-1.59208120584745,126.150925274028));
#59222=CARTESIAN_POINT('Ctrl Pts',(49.6026699246306,-1.72137470596408,126.195160497337));
#59223=CARTESIAN_POINT('Ctrl Pts',(49.5949051716835,-1.84899297894216,126.244846422357));
#59224=CARTESIAN_POINT('Ctrl Pts',(49.5871404187364,-1.9744440107132,126.299834681237));
#59225=CARTESIAN_POINT('Ctrl Pts',(49.5793833778514,-2.09977044275076,126.354768325003));
#59226=CARTESIAN_POINT('Ctrl Pts',(49.5716263369664,-2.22293356146207,126.414993666411));
#59227=CARTESIAN_POINT('Ctrl Pts',(49.5638692960815,-2.3434580975374,126.480313068384));
#59228=CARTESIAN_POINT('Ctrl Pts',(49.5561181048414,-2.46389174512236,126.545583212488));
#59229=CARTESIAN_POINT('Ctrl Pts',(49.5483669136013,-2.58169042825956,126.61593958541));
#59230=CARTESIAN_POINT('Ctrl Pts',(49.5406157223612,-2.69640072938429,126.691137286761));
#59231=CARTESIAN_POINT('Ctrl Pts',(49.5328678255841,-2.8110622755712,126.766303027084));
#59232=CARTESIAN_POINT('Ctrl Pts',(49.525119928807,-2.92263772420907,126.846305789344));
#59233=CARTESIAN_POINT('Ctrl Pts',(49.5173720320299,-3.03070025766095,126.930855872414));
#59234=CARTESIAN_POINT('Ctrl Pts',(49.5096257559458,-3.13874018676054,127.01538826943));
#59235=CARTESIAN_POINT('Ctrl Pts',(49.5018794798617,-3.24326835456314,127.104465854498));
#59236=CARTESIAN_POINT('Ctrl Pts',(49.4941332037776,-3.34388915168383,127.197757173361));
#59237=CARTESIAN_POINT('Ctrl Pts',(49.4863868705123,-3.4445106915648,127.29104918088));
#59238=CARTESIAN_POINT('Ctrl Pts',(49.4786405372469,-3.54122451651026,127.388554718446));
#59239=CARTESIAN_POINT('Ctrl Pts',(49.4708942039816,-3.63367047480488,127.489904109625));
#59240=CARTESIAN_POINT('Ctrl Pts',(49.4631461359786,-3.72613713573001,127.591276197297));
#59241=CARTESIAN_POINT('Ctrl Pts',(49.4553980679757,-3.81433376472951,127.696493562688));
#59242=CARTESIAN_POINT('Ctrl Pts',(49.4476499999727,-3.89793950795982,127.805152279556));
#59243=CARTESIAN_POINT('Ctrl Pts',(49.4398936972309,-3.98163410836929,127.913926480203));
#59244=CARTESIAN_POINT('Ctrl Pts',(49.4321373944891,-4.06072783739054,128.026149028244));
#59245=CARTESIAN_POINT('Ctrl Pts',(49.4243810917473,-4.13494201838662,128.141385295284));
#59246=CARTESIAN_POINT('Ctrl Pts',(49.4166206492331,-4.20919580972574,128.256683067391));
#59247=CARTESIAN_POINT('Ctrl Pts',(49.4088602067189,-4.27856466598069,128.374997426489));
#59248=CARTESIAN_POINT('Ctrl Pts',(49.4010997642048,-4.34281568040714,128.495868679415));
#59249=CARTESIAN_POINT('Ctrl Pts',(49.3933268639394,-4.40716983626589,128.616933965606));
#59250=CARTESIAN_POINT('Ctrl Pts',(49.3855539636739,-4.46638956388585,128.740563995026));
#59251=CARTESIAN_POINT('Ctrl Pts',(49.3777810634085,-4.52028959653083,128.866277795292));
#59252=CARTESIAN_POINT('Ctrl Pts',(49.3702907276464,-4.57223022722405,128.987421582266));
#59253=CARTESIAN_POINT('Ctrl Pts',(49.3628003918843,-4.61923110680947,129.11049998197));
#59254=CARTESIAN_POINT('Ctrl Pts',(49.3553100561221,-4.66117071095364,129.2350707572));
#59255=CARTESIAN_POINT('Ctrl Pts',(49.3484299741019,-4.69969340547216,129.349492483824));
#59256=CARTESIAN_POINT('Ctrl Pts',(49.3415498920817,-4.73402183531188,129.465393105414));
#59257=CARTESIAN_POINT('Ctrl Pts',(49.3346698100615,-4.76405452823405,129.582490119308));
#59258=CARTESIAN_POINT('Ctrl Pts',(51.084953843968,-4.7640545282341,129.582490119308));
#59259=CARTESIAN_POINT('Ctrl Pts',(51.0771911324384,-4.79810979842364,129.715271100917));
#59260=CARTESIAN_POINT('Ctrl Pts',(51.0694284209086,-4.82657877292075,129.84935629399));
#59261=CARTESIAN_POINT('Ctrl Pts',(51.061665709379,-4.84938950445108,129.984235933984));
#59262=CARTESIAN_POINT('Ctrl Pts',(51.053891502998,-4.87223401360747,130.119315300763));
#59263=CARTESIAN_POINT('Ctrl Pts',(51.046117296617,-4.88940349871459,130.255191076787));
#59264=CARTESIAN_POINT('Ctrl Pts',(51.038343090236,-4.9008779442993,130.391349192082));
#59265=CARTESIAN_POINT('Ctrl Pts',(51.0342273264905,-4.90695266174609,130.463433030242));
#59266=CARTESIAN_POINT('Ctrl Pts',(51.0301115627449,-4.91143206568912,130.535596003573));
#59267=CARTESIAN_POINT('Ctrl Pts',(51.0259957989994,-4.91431908962279,130.607762174365));
#59268=CARTESIAN_POINT('Ctrl Pts',(51.0222836779967,-4.91692297625045,130.672850837089));
#59269=CARTESIAN_POINT('Ctrl Pts',(51.0185715569939,-4.91823380993961,130.737991574334));
#59270=CARTESIAN_POINT('Ctrl Pts',(51.0148594359912,-4.91824985095898,130.803149815373));
#59271=CARTESIAN_POINT('',(51.3601405639582,-4.9182479625051,130.808837426072));
#59272=CARTESIAN_POINT('Ctrl Pts',(51.4301221724605,-4.76405452823404,129.582490119308));
#59273=CARTESIAN_POINT('Ctrl Pts',(51.4224494757503,-4.79784078076855,129.714222205162));
#59274=CARTESIAN_POINT('Ctrl Pts',(51.4147767790401,-4.82615905439274,129.847356967975));
#59275=CARTESIAN_POINT('Ctrl Pts',(51.4071040823299,-4.84890845285665,129.981396536749));
#59276=CARTESIAN_POINT('Ctrl Pts',(51.3992768292764,-4.87211610791191,130.118136155636));
#59277=CARTESIAN_POINT('Ctrl Pts',(51.3914495762228,-4.88952803686276,130.255817000296));
#59278=CARTESIAN_POINT('Ctrl Pts',(51.3836223231693,-4.90109248538486,130.393902931313));
#59279=CARTESIAN_POINT('Ctrl Pts',(51.3757950701157,-4.91265693390694,130.53198886233));
#59280=CARTESIAN_POINT('Ctrl Pts',(51.3679678170622,-4.91837390208594,130.670479439719));
#59281=CARTESIAN_POINT('Ctrl Pts',(51.3601405640086,-4.91824796250591,130.808837425181));
#59282=CARTESIAN_POINT('Ctrl Pts',(51.3601405639582,-4.9182479625051,130.808837426072));
#59283=CARTESIAN_POINT('Ctrl Pts',(51.3504651616975,-4.91809228639094,130.979864113998));
#59284=CARTESIAN_POINT('Ctrl Pts',(51.3407897594369,-4.90901213047814,131.150492424705));
#59285=CARTESIAN_POINT('Ctrl Pts',(51.3311143571762,-4.89115351568566,131.319918905731));
#59286=CARTESIAN_POINT('Ctrl Pts',(51.3212665221831,-4.87297662888093,131.492364865461));
#59287=CARTESIAN_POINT('Ctrl Pts',(51.3114186871899,-4.84570562792725,131.663565909079));
#59288=CARTESIAN_POINT('Ctrl Pts',(51.3015708521968,-4.80954295808226,131.832698887233));
#59289=CARTESIAN_POINT('Ctrl Pts',(51.2959987103488,-4.78908124988764,131.928398393378));
#59290=CARTESIAN_POINT('Ctrl Pts',(51.2904265685008,-4.76577368212046,132.023436216678));
#59291=CARTESIAN_POINT('Ctrl Pts',(51.2848544266528,-4.73966362282522,132.117666295985));
#59292=CARTESIAN_POINT('Ctrl Pts',(51.2770800925336,-4.70323448473597,132.249137486165));
#59293=CARTESIAN_POINT('Ctrl Pts',(51.2693057584145,-4.66127327820999,132.379300033773));
#59294=CARTESIAN_POINT('Ctrl Pts',(51.2615314242953,-4.61388971003747,132.50765296068));
#59295=CARTESIAN_POINT('Ctrl Pts',(51.2537666713481,-4.566564537878,132.635847704075));
#59296=CARTESIAN_POINT('Ctrl Pts',(51.2460019184009,-4.51383043450627,132.762236900944));
#59297=CARTESIAN_POINT('Ctrl Pts',(51.2382371654537,-4.45584753202936,132.886332239325));
#59298=CARTESIAN_POINT('Ctrl Pts',(51.2304801245686,-4.39792221898846,133.010304324466));
#59299=CARTESIAN_POINT('Ctrl Pts',(51.2227230836835,-4.33475864573901,133.13198673311));
#59300=CARTESIAN_POINT('Ctrl Pts',(51.2149660427984,-4.26656579759478,133.250909075556));
#59301=CARTESIAN_POINT('Ctrl Pts',(51.2072148515582,-4.19842437420781,133.369741737739));
#59302=CARTESIAN_POINT('Ctrl Pts',(51.1994636603179,-4.12526141859278,133.485818138811));
#59303=CARTESIAN_POINT('Ctrl Pts',(51.1917124690777,-4.04733264138388,133.598690868715));
#59304=CARTESIAN_POINT('Ctrl Pts',(51.1839645723005,-3.96943698598421,133.711515624698));
#59305=CARTESIAN_POINT('Ctrl Pts',(51.1762166755233,-3.8867797594212,133.821139096662));
#59306=CARTESIAN_POINT('Ctrl Pts',(51.1684687787462,-3.79966082184224,133.927141541912));
#59307=CARTESIAN_POINT('Ctrl Pts',(51.160722502662,-3.71256010766695,134.033121813735));
#59308=CARTESIAN_POINT('Ctrl Pts',(51.1529762265778,-3.62099978692932,134.135482263581));
#59309=CARTESIAN_POINT('Ctrl Pts',(51.1452299504936,-3.52532071197048,134.233835349978));
#59310=CARTESIAN_POINT('Ctrl Pts',(51.1374836172282,-3.42964093073059,134.332189162395));
#59311=CARTESIAN_POINT('Ctrl Pts',(51.1297372839628,-3.32984260721947,134.426535272099));
#59312=CARTESIAN_POINT('Ctrl Pts',(51.1219909506973,-3.22630395406181,134.516522502304));
#59313=CARTESIAN_POINT('Ctrl Pts',(51.1142428826943,-3.12274211414066,134.606529884526));
#59314=CARTESIAN_POINT('Ctrl Pts',(51.1064948146912,-3.01543857283784,134.692176188423));
#59315=CARTESIAN_POINT('Ctrl Pts',(51.0987467466881,-2.90480483968136,134.773150345665));
#59316=CARTESIAN_POINT('Ctrl Pts',(51.0909904439462,-2.79405352367658,134.854210563205));
#59317=CARTESIAN_POINT('Ctrl Pts',(51.0832341412043,-2.6799652615433,134.930588483465));
#59318=CARTESIAN_POINT('Ctrl Pts',(51.0754778384623,-2.56298124398526,135.002015939943));
#59319=CARTESIAN_POINT('Ctrl Pts',(51.0677173959481,-2.44593478853458,135.073481519405));
#59320=CARTESIAN_POINT('Ctrl Pts',(51.0599569534338,-2.32598983976687,135.139991180753));
#59321=CARTESIAN_POINT('Ctrl Pts',(51.0521965109195,-2.2036115475865,135.201323115683));
#59322=CARTESIAN_POINT('Ctrl Pts',(51.044423610654,-2.08103680290745,135.262753506079));
#59323=CARTESIAN_POINT('Ctrl Pts',(51.0366507103885,-1.95602126570306,135.318989400059));
#59324=CARTESIAN_POINT('Ctrl Pts',(51.028877810123,-1.82905021573878,135.36985712625));
#59325=CARTESIAN_POINT('Ctrl Pts',(51.021387474362,-1.70669488327935,135.418875682459));
#59326=CARTESIAN_POINT('Ctrl Pts',(51.0138971386009,-1.58252403561694,135.462909484716));
#59327=CARTESIAN_POINT('Ctrl Pts',(51.0064068028399,-1.45698269885223,135.501847656159));
#59328=CARTESIAN_POINT('Ctrl Pts',(50.9986324687208,-1.32668142412954,135.542262180211));
#59329=CARTESIAN_POINT('Ctrl Pts',(50.9908581346018,-1.19449092934741,135.577315065137));
#59330=CARTESIAN_POINT('Ctrl Pts',(50.9830838004827,-1.06089200079412,135.606827819448));
#59331=CARTESIAN_POINT('Ctrl Pts',(50.9753190475356,-0.927457720980185,
135.636304201927));
#59332=CARTESIAN_POINT('Ctrl Pts',(50.9675542945886,-0.792618839153976,
135.660253955388));
#59333=CARTESIAN_POINT('Ctrl Pts',(50.9597895416415,-0.656872741313494,
135.678547858965));
#59334=CARTESIAN_POINT('Ctrl Pts',(50.9520325007565,-0.521261468410889,
135.696823592779));
#59335=CARTESIAN_POINT('Ctrl Pts',(50.9442754598715,-0.384745157598823,
135.70945460385));
#59336=CARTESIAN_POINT('Ctrl Pts',(50.9365184189865,-0.247832522720093,
135.716362460316));
#59337=CARTESIAN_POINT('Ctrl Pts',(50.9287672277464,-0.11102313472435,135.723265107515));
#59338=CARTESIAN_POINT('Ctrl Pts',(50.9210160365063,0.0261815935647434,
135.724453170977));
#59339=CARTESIAN_POINT('Ctrl Pts',(50.9132648452661,0.163267025550551,135.719899951237));
#59340=CARTESIAN_POINT('Ctrl Pts',(50.9055169484891,0.300294192570704,135.715348666737));
#59341=CARTESIAN_POINT('Ctrl Pts',(50.897769051712,0.437201774202527,135.705060965355));
#59342=CARTESIAN_POINT('Ctrl Pts',(50.8900211549349,0.573474547294229,135.689062246745));
#59343=CARTESIAN_POINT('Ctrl Pts',(50.8822748788509,0.709718815059501,135.673066874723));
#59344=CARTESIAN_POINT('Ctrl Pts',(50.8745286027667,0.845328150355438,135.651362907199));
#59345=CARTESIAN_POINT('Ctrl Pts',(50.8667823266827,0.979792264550653,135.62402763727));
#59346=CARTESIAN_POINT('Ctrl Pts',(50.8590359934173,1.11425737132923,135.596692165559));
#59347=CARTESIAN_POINT('Ctrl Pts',(50.851289660152,1.24757685700965,135.563725386382));
#59348=CARTESIAN_POINT('Ctrl Pts',(50.8435433268867,1.3792508334545,135.525255681102));
#59349=CARTESIAN_POINT('Ctrl Pts',(50.8357952588837,1.51095429737359,135.486777360797));
#59350=CARTESIAN_POINT('Ctrl Pts',(50.8280471908807,1.64101114357892,135.44279377179));
#59351=CARTESIAN_POINT('Ctrl Pts',(50.8202991228778,1.76893723052337,135.39348298867));
#59352=CARTESIAN_POINT('Ctrl Pts',(50.8125428201359,1.89699927883535,135.344119797463));
#59353=CARTESIAN_POINT('Ctrl Pts',(50.804786517394,2.02292567872778,135.28941824292));
#59354=CARTESIAN_POINT('Ctrl Pts',(50.7970302146522,2.14625233977566,135.22960456073));
#59355=CARTESIAN_POINT('Ctrl Pts',(50.789269772138,2.26964482397584,135.169758954176));
#59356=CARTESIAN_POINT('Ctrl Pts',(50.7815093296239,2.39043446034551,135.10479596831));
#59357=CARTESIAN_POINT('Ctrl Pts',(50.7737488871097,2.50818321039096,135.034987054113));
#59358=CARTESIAN_POINT('Ctrl Pts',(50.7659759868443,2.62612098118323,134.96506607645));
#59359=CARTESIAN_POINT('Ctrl Pts',(50.758203086579,2.74100778300454,134.890283838713));
#59360=CARTESIAN_POINT('Ctrl Pts',(50.7504301863135,2.85243519564335,134.810954746893));
#59361=CARTESIAN_POINT('Ctrl Pts',(50.7429398505513,2.95981194116658,134.734509467377));
#59362=CARTESIAN_POINT('Ctrl Pts',(50.7354495147891,3.06397620232771,134.653842362231));
#59363=CARTESIAN_POINT('Ctrl Pts',(50.727959179027,3.16459414780303,134.569267912864));
#59364=CARTESIAN_POINT('Ctrl Pts',(50.7201848449079,3.26902705326087,134.481486797546));
#59365=CARTESIAN_POINT('Ctrl Pts',(50.7124105107888,3.36997022945993,134.389218130973));
#59366=CARTESIAN_POINT('Ctrl Pts',(50.7046361766698,3.46701362972503,134.292769933257));
#59367=CARTESIAN_POINT('Ctrl Pts',(50.6968714237227,3.5639374326722,134.196440599325));
#59368=CARTESIAN_POINT('Ctrl Pts',(50.6891066707756,3.65697074780113,134.09594225596));
#59369=CARTESIAN_POINT('Ctrl Pts',(50.6813419178285,3.74573600865641,133.991623521055));
#59370=CARTESIAN_POINT('Ctrl Pts',(50.6735848769435,3.83441310660324,133.887408396987));
#59371=CARTESIAN_POINT('Ctrl Pts',(50.6658278360586,3.91883033453536,133.779380728371));
#59372=CARTESIAN_POINT('Ctrl Pts',(50.6580707951736,3.99864673325042,133.667926116235));
#59373=CARTESIAN_POINT('Ctrl Pts',(50.6503196039335,4.07840294179842,133.556555552888));
#59374=CARTESIAN_POINT('Ctrl Pts',(50.6425684126934,4.15356500028906,133.44176350646));
#59375=CARTESIAN_POINT('Ctrl Pts',(50.6348172214532,4.22383227205413,133.323968523581));
#59376=CARTESIAN_POINT('Ctrl Pts',(50.6270693246762,4.29406967835416,133.206223606712));
#59377=CARTESIAN_POINT('Ctrl Pts',(50.6193214278991,4.3594162358441,133.085478626973));
#59378=CARTESIAN_POINT('Ctrl Pts',(50.611573531122,4.41961482327418,132.962180785327));
#59379=CARTESIAN_POINT('Ctrl Pts',(50.6038272550379,4.4798008184575,132.838908734931));
#59380=CARTESIAN_POINT('Ctrl Pts',(50.5960809789538,4.53484081406104,132.713085235895));
#59381=CARTESIAN_POINT('Ctrl Pts',(50.5883347028697,4.58452401548642,132.585181387303));
#59382=CARTESIAN_POINT('Ctrl Pts',(50.5805883696044,4.63420758366191,132.457276594555));
#59383=CARTESIAN_POINT('Ctrl Pts',(50.5728420363391,4.67853413719242,132.327291786044));
#59384=CARTESIAN_POINT('Ctrl Pts',(50.5650957030738,4.7173414852052,132.195716925081));
#59385=CARTESIAN_POINT('Ctrl Pts',(50.5573476350708,4.75615752385449,132.06411259884));
#59386=CARTESIAN_POINT('Ctrl Pts',(50.5495995670679,4.78945178693184,131.930917886509));
#59387=CARTESIAN_POINT('Ctrl Pts',(50.5418514990649,4.81711240330117,131.796636363748));
#59388=CARTESIAN_POINT('Ctrl Pts',(50.5340951963231,4.84480241770275,131.662212124988));
#59389=CARTESIAN_POINT('Ctrl Pts',(50.5263388935813,4.8668467457021,131.526699151947));
#59390=CARTESIAN_POINT('Ctrl Pts',(50.5185825908394,4.88318487358148,131.39061018296));
#59391=CARTESIAN_POINT('Ctrl Pts',(50.5108221483253,4.89953172161167,131.254448579193));
#59392=CARTESIAN_POINT('Ctrl Pts',(50.5030617058111,4.9101662706639,131.117710756505));
#59393=CARTESIAN_POINT('Ctrl Pts',(50.495301263297,4.91508012963144,130.980911974973));
#59394=CARTESIAN_POINT('Ctrl Pts',(50.4875283630316,4.92000187676161,130.843893591892));
#59395=CARTESIAN_POINT('Ctrl Pts',(50.4797554627661,4.91918458486074,130.706814445602));
#59396=CARTESIAN_POINT('Ctrl Pts',(50.4719825625007,4.91267201149314,130.570188095711));
#59397=CARTESIAN_POINT('Ctrl Pts',(50.4644922267385,4.90639618657151,130.438528457777));
#59398=CARTESIAN_POINT('Ctrl Pts',(50.4570018909764,4.8948319939123,130.307289574042));
#59399=CARTESIAN_POINT('Ctrl Pts',(50.4495115552142,4.87806357164692,130.176922291138));
#59400=CARTESIAN_POINT('Ctrl Pts',(50.4417372210951,4.86065936955502,130.04161209308));
#59401=CARTESIAN_POINT('Ctrl Pts',(50.433962886976,4.83759337959216,129.906812272014));
#59402=CARTESIAN_POINT('Ctrl Pts',(50.4261885528569,4.80890310755886,129.773034304215));
#59403=CARTESIAN_POINT('Ctrl Pts',(50.4184237999098,4.78024819372172,129.639421205805));
#59404=CARTESIAN_POINT('Ctrl Pts',(50.4106590469627,4.74598287047987,129.506827833549));
#59405=CARTESIAN_POINT('Ctrl Pts',(50.4028942940157,4.70619635604785,129.375760281285));
#59406=CARTESIAN_POINT('Ctrl Pts',(50.3951372531306,4.66644935814285,129.244822907162));
#59407=CARTESIAN_POINT('Ctrl Pts',(50.3873802122456,4.62119219473625,129.115408708873));
#59408=CARTESIAN_POINT('Ctrl Pts',(50.3796231713606,4.5705649861163,128.988012971825));
#59409=CARTESIAN_POINT('Ctrl Pts',(50.3718719801204,4.51997595586819,128.860713304894));
#59410=CARTESIAN_POINT('Ctrl Pts',(50.3641207888804,4.46402508467799,128.73542943134));
#59411=CARTESIAN_POINT('Ctrl Pts',(50.3563695976402,4.4029020062171,128.612640519983));
#59412=CARTESIAN_POINT('Ctrl Pts',(50.3486217008631,4.34180490669507,128.489903797189));
#59413=CARTESIAN_POINT('Ctrl Pts',(50.340873804086,4.27554014606638,128.369660276752));
#59414=CARTESIAN_POINT('Ctrl Pts',(50.3331259073089,4.20434498685076,128.252368005107));
#59415=CARTESIAN_POINT('Ctrl Pts',(50.3253796312248,4.13316472012766,128.135100268477));
#59416=CARTESIAN_POINT('Ctrl Pts',(50.3176333551408,4.05705630893208,128.020782886723));
#59417=CARTESIAN_POINT('Ctrl Pts',(50.3098870790567,3.97630216263665,127.909847847874));
#59418=CARTESIAN_POINT('Ctrl Pts',(50.3021407457913,3.89554742023246,127.798911990127));
#59419=CARTESIAN_POINT('Ctrl Pts',(50.2943944125259,3.8101471043905,127.691358841193));
#59420=CARTESIAN_POINT('Ctrl Pts',(50.2866480792605,3.72042576699122,127.587589693983));
#59421=CARTESIAN_POINT('Ctrl Pts',(50.2789000112576,3.63068433712052,127.483797308392));
#59422=CARTESIAN_POINT('Ctrl Pts',(50.2711519432546,3.53662021581656,127.383790906446));
#59423=CARTESIAN_POINT('Ctrl Pts',(50.2634038752516,3.43859660646317,127.287936803445));
#59424=CARTESIAN_POINT('Ctrl Pts',(50.2556475725097,3.34046881645126,127.191980825562));
#59425=CARTESIAN_POINT('Ctrl Pts',(50.2478912697678,3.23837341205098,127.100186236071));
#59426=CARTESIAN_POINT('Ctrl Pts',(50.240134967026,3.13270906540218,127.012881094471));
#59427=CARTESIAN_POINT('Ctrl Pts',(50.2323745245118,3.02698832250993,126.925529355489));
#59428=CARTESIAN_POINT('Ctrl Pts',(50.2246140819976,2.91769515319169,126.842672075015));
#59429=CARTESIAN_POINT('Ctrl Pts',(50.2168536394834,2.80525852474488,126.764594823384));
#59430=CARTESIAN_POINT('Ctrl Pts',(50.209080739218,2.69264140304059,126.686392235217));
#59431=CARTESIAN_POINT('Ctrl Pts',(50.2013078389526,2.57687106874703,126.612985219126));
#59432=CARTESIAN_POINT('Ctrl Pts',(50.1935349386871,2.45840324614048,126.544614552145));
#59433=CARTESIAN_POINT('Ctrl Pts',(50.1860446029252,2.34424202728925,126.478729331126));
#59434=CARTESIAN_POINT('Ctrl Pts',(50.1785542671632,2.22757630892479,126.41752079158));
#59435=CARTESIAN_POINT('Ctrl Pts',(50.1710639314013,2.10883087980123,126.361161839332));
#59436=CARTESIAN_POINT('Ctrl Pts',(50.1632895972822,1.98558318163933,126.302666020279));
#59437=CARTESIAN_POINT('Ctrl Pts',(50.1555152631631,1.85970454345402,126.249209494943));
#59438=CARTESIAN_POINT('Ctrl Pts',(50.147740929044,1.73164555752309,126.201037174051));
#59439=CARTESIAN_POINT('Ctrl Pts',(50.1399761760969,1.60374439284735,126.15292422124));
#59440=CARTESIAN_POINT('Ctrl Pts',(50.1322114231498,1.47366858933964,126.11008265165));
#59441=CARTESIAN_POINT('Ctrl Pts',(50.1244466702027,1.34189216270387,126.072710959553));
#59442=CARTESIAN_POINT('Ctrl Pts',(50.1166896293177,1.21024661827275,126.035376385547));
#59443=CARTESIAN_POINT('Ctrl Pts',(50.1089325884327,1.07690418576258,126.003500983578));
#59444=CARTESIAN_POINT('Ctrl Pts',(50.1011755475477,0.94235730125259,125.977234580339));
#59445=CARTESIAN_POINT('Ctrl Pts',(50.0934243563075,0.807911879594832,125.950987984799));
#59446=CARTESIAN_POINT('Ctrl Pts',(50.0856731650674,0.672264195995571,125.930342043457));
#59447=CARTESIAN_POINT('Ctrl Pts',(50.0779219738273,0.535919890385907,125.915396214588));
#59448=CARTESIAN_POINT('Ctrl Pts',(50.0701740770502,0.399633534743231,125.900456738094));
#59449=CARTESIAN_POINT('Ctrl Pts',(50.0624261802731,0.262651533800107,125.891212598019));
#59450=CARTESIAN_POINT('Ctrl Pts',(50.054678283496,0.125487501181038,125.887711763972));
#59451=CARTESIAN_POINT('Ctrl Pts',(50.0469320074119,-0.0116478396793211,
125.884211662224));
#59452=CARTESIAN_POINT('Ctrl Pts',(50.0391857313278,-0.148964745887869,
125.886452486869));
#59453=CARTESIAN_POINT('Ctrl Pts',(50.0314394552437,-0.285947124517925,
125.894430138987));
#59454=CARTESIAN_POINT('Ctrl Pts',(50.0236931219784,-0.422930514320783,
125.902407849994));
#59455=CARTESIAN_POINT('Ctrl Pts',(50.015946788713,-0.559578981313767,125.916122450243));
#59456=CARTESIAN_POINT('Ctrl Pts',(50.0082004554476,-0.695379478186064,
125.935517793669));
#59457=CARTESIAN_POINT('Ctrl Pts',(50.0004523874446,-0.831210386638062,
125.954917480546));
#59458=CARTESIAN_POINT('Ctrl Pts',(49.9927043194417,-0.966192560132653,
125.98000038679));
#59459=CARTESIAN_POINT('Ctrl Pts',(49.9849562514387,-1.09982148693239,126.010658941472));
#59460=CARTESIAN_POINT('Ctrl Pts',(49.9771999486969,-1.23359243614573,126.041350080432));
#59461=CARTESIAN_POINT('Ctrl Pts',(49.969443645955,-1.36600688393938,126.077628617819));
#59462=CARTESIAN_POINT('Ctrl Pts',(49.9616873432131,-1.49657333253622,126.119336463643));
#59463=CARTESIAN_POINT('Ctrl Pts',(49.9539269006989,-1.62720946837813,126.1610665702));
#59464=CARTESIAN_POINT('Ctrl Pts',(49.9461664581847,-1.75599527273129,126.208231624894));
#59465=CARTESIAN_POINT('Ctrl Pts',(49.9384060156706,-1.88245861988423,126.260625083127));
#59466=CARTESIAN_POINT('Ctrl Pts',(49.9306331154051,-2.00912497722873,126.313102647991));
#59467=CARTESIAN_POINT('Ctrl Pts',(49.9228602151397,-2.13346107239415,126.370825223755));
#59468=CARTESIAN_POINT('Ctrl Pts',(49.9150873148743,-2.2550180027388,126.433539542548));
#59469=CARTESIAN_POINT('Ctrl Pts',(49.9075969791123,-2.372156032481,126.493974037884));
#59470=CARTESIAN_POINT('Ctrl Pts',(49.9001066433503,-2.4867131808113,126.559043500163));
#59471=CARTESIAN_POINT('Ctrl Pts',(49.8926163075884,-2.59831436846585,126.628484002396));
#59472=CARTESIAN_POINT('Ctrl Pts',(49.884840623724,-2.71416705940923,126.700569875434));
#59473=CARTESIAN_POINT('Ctrl Pts',(49.8770649398596,-2.82720115807032,126.777594810078));
#59474=CARTESIAN_POINT('Ctrl Pts',(49.8692892559952,-2.93696682574024,126.859311957917));
#59475=CARTESIAN_POINT('Ctrl Pts',(49.8614119122646,-3.04816757787158,126.942097481793));
#59476=CARTESIAN_POINT('Ctrl Pts',(49.8535345685339,-3.15601345051436,127.029698638517));
#59477=CARTESIAN_POINT('Ctrl Pts',(49.8456572248033,-3.26006276520945,127.121810708957));
#59478=CARTESIAN_POINT('Ctrl Pts',(49.8379009985295,-3.36251227814322,127.212506517763));
#59479=CARTESIAN_POINT('Ctrl Pts',(49.8301447722556,-3.46128082528066,127.307575264625));
#59480=CARTESIAN_POINT('Ctrl Pts',(49.8223885459818,-3.55597677385618,127.406683139303));
#59481=CARTESIAN_POINT('Ctrl Pts',(49.8146376892888,-3.6506071650933,127.505722402298));
#59482=CARTESIAN_POINT('Ctrl Pts',(49.8068868325958,-3.74117029849785,127.608794948126));
#59483=CARTESIAN_POINT('Ctrl Pts',(49.7991359759027,-3.82730976560157,127.715528634335));
#59484=CARTESIAN_POINT('Ctrl Pts',(49.7913888064269,-3.91340825466433,127.822211545475));
#59485=CARTESIAN_POINT('Ctrl Pts',(49.7836416369511,-3.99508702078494,127.932551827118));
#59486=CARTESIAN_POINT('Ctrl Pts',(49.7758944674753,-4.07202876268352,128.046142928844));
#59487=CARTESIAN_POINT('Ctrl Pts',(49.7679226790574,-4.15120132871993,128.163027454469));
#59488=CARTESIAN_POINT('Ctrl Pts',(49.7599508906395,-4.22535772592946,128.283353848185));
#59489=CARTESIAN_POINT('Ctrl Pts',(49.7519791022216,-4.2941990691015,128.406645576651));
#59490=CARTESIAN_POINT('Ctrl Pts',(49.744232553407,-4.36109532843337,128.526453748034));
#59491=CARTESIAN_POINT('Ctrl Pts',(49.7364860045924,-4.42297266520529,128.649061571292));
#59492=CARTESIAN_POINT('Ctrl Pts',(49.7287394557779,-4.47960302675391,128.77400602164));
#59493=CARTESIAN_POINT('Ctrl Pts',(49.7206550475583,-4.53870327530838,128.904399822229));
#59494=CARTESIAN_POINT('Ctrl Pts',(49.7125706393387,-4.59208832374198,129.037338255335));
#59495=CARTESIAN_POINT('Ctrl Pts',(49.7044862311191,-4.63955485263867,129.172271823457));
#59496=CARTESIAN_POINT('Ctrl Pts',(49.6964018228996,-4.68702138153536,129.307205391578));
#59497=CARTESIAN_POINT('Ctrl Pts',(49.6883174146801,-4.72856926789924,129.444133627827));
#59498=CARTESIAN_POINT('Ctrl Pts',(49.6802330064605,-4.76405452823399,129.582490119308));
#59499=CARTESIAN_POINT('Origin',(213.235140564004,0.,130.804360617566));
#59500=CARTESIAN_POINT('',(47.584673688373,-4.76405452823404,129.582490119308));
#59501=CARTESIAN_POINT('',(47.9299877718525,-4.76405452823408,129.582490119308));
#59502=CARTESIAN_POINT('',(213.235140564004,-4.76405452823405,129.582490119308));
#59503=CARTESIAN_POINT('',(49.2648594360413,-4.91824840372241,130.800398070159));
#59504=CARTESIAN_POINT('Ctrl Pts',(49.2648594359912,-4.91824840372313,130.800398071045));
#59505=CARTESIAN_POINT('Ctrl Pts',(49.2570262275045,-4.91836015682128,130.939104202001));
#59506=CARTESIAN_POINT('Ctrl Pts',(49.2491930190177,-4.91259963290899,131.077889086034));
#59507=CARTESIAN_POINT('Ctrl Pts',(49.241359810531,-4.90097509382102,131.216217622176));
#59508=CARTESIAN_POINT('Ctrl Pts',(49.2336305484484,-4.88950481196243,131.352710543454));
#59509=CARTESIAN_POINT('Ctrl Pts',(49.2259012863658,-4.87232524866436,131.488758754675));
#59510=CARTESIAN_POINT('Ctrl Pts',(49.2181720242833,-4.84949672177395,131.623851073889));
#59511=CARTESIAN_POINT('Ctrl Pts',(49.2104426438067,-4.82666784520474,131.758945462395));
#59512=CARTESIAN_POINT('Ctrl Pts',(49.2027132633302,-4.79818989785096,131.893083542743));
#59513=CARTESIAN_POINT('Ctrl Pts',(49.1949838828536,-4.76417460104857,132.025762858117));
#59514=CARTESIAN_POINT('Ctrl Pts',(49.1872526954078,-4.7301513521732,132.158473191172));
#59515=CARTESIAN_POINT('Ctrl Pts',(49.1795215079621,-4.6905882753529,132.289723700585));
#59516=CARTESIAN_POINT('Ctrl Pts',(49.1717903205162,-4.64564727057392,132.419026062762));
#59517=CARTESIAN_POINT('Ctrl Pts',(49.1638796631656,-4.5996630162419,132.551330018521));
#59518=CARTESIAN_POINT('Ctrl Pts',(49.155969005815,-4.54804822638849,132.681593858697));
#59519=CARTESIAN_POINT('Ctrl Pts',(49.1480583484644,-4.49102842017358,132.809316176099));
#59520=CARTESIAN_POINT('Ctrl Pts',(49.1403142332452,-4.43520904517906,132.934349570695));
#59521=CARTESIAN_POINT('Ctrl Pts',(49.1325701180259,-4.3742102145194,133.056947071731));
#59522=CARTESIAN_POINT('Ctrl Pts',(49.1248260028067,-4.30828963720264,133.176664026591));
#59523=CARTESIAN_POINT('Ctrl Pts',(49.1168320743904,-4.24024256386856,133.300242865525));
#59524=CARTESIAN_POINT('Ctrl Pts',(49.1088381459742,-4.16695111041679,133.420751794026));
#59525=CARTESIAN_POINT('Ctrl Pts',(49.1008442175579,-4.08874597150404,133.53773571861));
#59526=CARTESIAN_POINT('Ctrl Pts',(49.0928502891417,-4.01054083259129,133.654719643194));
#59527=CARTESIAN_POINT('Ctrl Pts',(49.0848563607253,-3.92742233257059,133.768178241303));
#59528=CARTESIAN_POINT('Ctrl Pts',(49.0768624323091,-3.83976462881858,133.877696046343));
#59529=CARTESIAN_POINT('Ctrl Pts',(49.06908809819,-3.75451489407085,133.984205382433));
#59530=CARTESIAN_POINT('Ctrl Pts',(49.0613137640709,-3.66469515649169,134.087333683076));
#59531=CARTESIAN_POINT('Ctrl Pts',(49.0535394299518,-3.57060350750201,134.186663628048));
#59532=CARTESIAN_POINT('Ctrl Pts',(49.0457746770047,-3.47662781806025,134.28587115774));
#59533=CARTESIAN_POINT('Ctrl Pts',(49.0380099240576,-3.37839095877677,134.38128936471));
#59534=CARTESIAN_POINT('Ctrl Pts',(49.0302451711105,-3.2762323865968,134.472532425363));
#59535=CARTESIAN_POINT('Ctrl Pts',(49.0224881302255,-3.17417527975104,134.563684862121));
#59536=CARTESIAN_POINT('Ctrl Pts',(49.0147310893405,-3.06820450114081,134.65067014616));
#59537=CARTESIAN_POINT('Ctrl Pts',(49.0069740484555,-2.95869735866967,134.733138163101));
#59538=CARTESIAN_POINT('Ctrl Pts',(48.9992228572154,-2.84927279638665,134.81554399027));
#59539=CARTESIAN_POINT('Ctrl Pts',(48.9914716659752,-2.73631748939105,134.893439096542));
#59540=CARTESIAN_POINT('Ctrl Pts',(48.9837204747351,-2.62024264933108,134.966512887862));
#59541=CARTESIAN_POINT('Ctrl Pts',(48.975972577958,-2.50421714417454,135.03955562087));
#59542=CARTESIAN_POINT('Ctrl Pts',(48.968224681181,-2.38507507320559,135.10778090675));
#59543=CARTESIAN_POINT('Ctrl Pts',(48.9604767844039,-2.2632573384036,135.170920966704));
#59544=CARTESIAN_POINT('Ctrl Pts',(48.9527305083198,-2.14146508524564,135.234047819119));
#59545=CARTESIAN_POINT('Ctrl Pts',(48.9449842322357,-2.01699862840108,135.292091381607));
#59546=CARTESIAN_POINT('Ctrl Pts',(48.9372379561516,-1.89032387280038,135.344829615194));
#59547=CARTESIAN_POINT('Ctrl Pts',(48.9294916228862,-1.76364818211542,135.397568238083));
#59548=CARTESIAN_POINT('Ctrl Pts',(48.9217452896209,-1.6347645210809,135.445001303658));
#59549=CARTESIAN_POINT('Ctrl Pts',(48.9139989563555,-1.50415881977546,135.486954909985));
#59550=CARTESIAN_POINT('Ctrl Pts',(48.9062508883526,-1.37352387022878,135.528917911531));
#59551=CARTESIAN_POINT('Ctrl Pts',(48.8985028203496,-1.2411664851953,135.56539889252));
#59552=CARTESIAN_POINT('Ctrl Pts',(48.8907547523466,-1.10758741071973,135.596273929607));
#59553=CARTESIAN_POINT('Ctrl Pts',(48.8829984496048,-0.973866366814014,
135.62718178105));
#59554=CARTESIAN_POINT('Ctrl Pts',(48.8752421468629,-0.838921421250006,
135.65247169853));
#59555=CARTESIAN_POINT('Ctrl Pts',(48.8674858441211,-0.703263712543963,
135.67207088145));
#59556=CARTESIAN_POINT('Ctrl Pts',(48.8597254016069,-0.567533599234209,
135.691680525043));
#59557=CARTESIAN_POINT('Ctrl Pts',(48.8519649590928,-0.431090353515187,
135.705593342325));
#59558=CARTESIAN_POINT('Ctrl Pts',(48.8442045165786,-0.294448885718147,
135.713788579783));
#59559=CARTESIAN_POINT('Ctrl Pts',(48.8364316163132,-0.157588068906726,
135.721996972964));
#59560=CARTESIAN_POINT('Ctrl Pts',(48.8286587160477,-0.0205287852715254,
135.724469437965));
#59561=CARTESIAN_POINT('Ctrl Pts',(48.8208858157823,0.11621450340992,135.721237395735));
#59562=CARTESIAN_POINT('Ctrl Pts',(48.8133954800203,0.247986829112416,135.718122846381));
#59563=CARTESIAN_POINT('Ctrl Pts',(48.8059051442583,0.379465428026367,135.709711355268));
#59564=CARTESIAN_POINT('Ctrl Pts',(48.7984148084963,0.510197564270782,135.696076217221));
#59565=CARTESIAN_POINT('Ctrl Pts',(48.7906404743772,0.645886449196257,135.681924098772));
#59566=CARTESIAN_POINT('Ctrl Pts',(48.7828661402581,0.781200971403702,135.662099575266));
#59567=CARTESIAN_POINT('Ctrl Pts',(48.775091806139,0.915628901874171,135.636627867683));
#59568=CARTESIAN_POINT('Ctrl Pts',(48.7673270531919,1.04989116193451,135.611187551703));
#59569=CARTESIAN_POINT('Ctrl Pts',(48.7595623002448,1.18326862385331,135.580113971362));
#59570=CARTESIAN_POINT('Ctrl Pts',(48.7517975472977,1.31525319854346,135.543484174324));
#59571=CARTESIAN_POINT('Ctrl Pts',(48.7440405064127,1.44710668429356,135.506890758518));
#59572=CARTESIAN_POINT('Ctrl Pts',(48.7362834655276,1.57756966162535,135.464752211981));
#59573=CARTESIAN_POINT('Ctrl Pts',(48.7285264246426,1.70614362526044,135.417196729166));
#59574=CARTESIAN_POINT('Ctrl Pts',(48.7207752334025,1.83462063026886,135.369677108312));
#59575=CARTESIAN_POINT('Ctrl Pts',(48.7130240421623,1.9612110917978,135.31674881711));
#59576=CARTESIAN_POINT('Ctrl Pts',(48.7052728509222,2.08543142833007,135.258589935892));
#59577=CARTESIAN_POINT('Ctrl Pts',(48.6975249541451,2.20959896790597,135.20045577375));
#59578=CARTESIAN_POINT('Ctrl Pts',(48.6897770573681,2.33139803272242,135.137095608677));
#59579=CARTESIAN_POINT('Ctrl Pts',(48.682029160591,2.45036501460562,135.068735643018));
#59580=CARTESIAN_POINT('Ctrl Pts',(48.6742828845069,2.56930711116083,135.000389976789));
#59581=CARTESIAN_POINT('Ctrl Pts',(48.6665366084228,2.68541796434803,134.92704678489));
#59582=CARTESIAN_POINT('Ctrl Pts',(48.6587903323386,2.79825893349477,134.848978028844));
#59583=CARTESIAN_POINT('Ctrl Pts',(48.6510439990733,2.91110073560791,134.770908696513));
#59584=CARTESIAN_POINT('Ctrl Pts',(48.6432976658079,3.02067228399814,134.68811395287));
#59585=CARTESIAN_POINT('Ctrl Pts',(48.6355513325425,3.12656461296599,134.600908626409));
#59586=CARTESIAN_POINT('Ctrl Pts',(48.6278032645395,3.23248065578671,134.51368377092));
#59587=CARTESIAN_POINT('Ctrl Pts',(48.6200551965365,3.33471553790816,134.422046615657));
#59588=CARTESIAN_POINT('Ctrl Pts',(48.6123071285336,3.43289433364003,134.326351468855));
#59589=CARTESIAN_POINT('Ctrl Pts',(48.6045508257917,3.53117747496434,134.230554616111));
#59590=CARTESIAN_POINT('Ctrl Pts',(48.5967945230498,3.62539563807892,134.130691429707));
#59591=CARTESIAN_POINT('Ctrl Pts',(48.5890382203079,3.71521129092596,134.027152594451));
#59592=CARTESIAN_POINT('Ctrl Pts',(48.5812777777938,3.80507488109122,133.923558497401));
#59593=CARTESIAN_POINT('Ctrl Pts',(48.5735173352796,3.89053103542438,133.816285148084));
#59594=CARTESIAN_POINT('Ctrl Pts',(48.5657568927654,3.97128397179708,133.705754537365));
#59595=CARTESIAN_POINT('Ctrl Pts',(48.5579839924999,4.05216653995226,133.595046493097));
#59596=CARTESIAN_POINT('Ctrl Pts',(48.5502110922345,4.1283305854456,133.48107106378));
#59597=CARTESIAN_POINT('Ctrl Pts',(48.5424381919691,4.19952446445392,133.364278064468));
#59598=CARTESIAN_POINT('Ctrl Pts',(48.5349478562071,4.26813026663278,133.251730784866));
#59599=CARTESIAN_POINT('Ctrl Pts',(48.5274575204452,4.33212083518902,133.136567499525));
#59600=CARTESIAN_POINT('Ctrl Pts',(48.5199671846832,4.39131312033296,133.019208725607));
#59601=CARTESIAN_POINT('Ctrl Pts',(48.5121928505641,4.45274969895984,132.897400258104));
#59602=CARTESIAN_POINT('Ctrl Pts',(48.5044185164451,4.50921157036847,132.772840679068));
#59603=CARTESIAN_POINT('Ctrl Pts',(48.496644182326,4.56044308138651,132.645974573837));
#59604=CARTESIAN_POINT('Ctrl Pts',(48.4888794293789,4.61161145414598,132.519264819743));
#59605=CARTESIAN_POINT('Ctrl Pts',(48.4811146764318,4.65756214704797,132.390254554396));
#59606=CARTESIAN_POINT('Ctrl Pts',(48.4733499234847,4.69808534791299,132.25941289368));
#59607=CARTESIAN_POINT('Ctrl Pts',(48.4655928825997,4.73856830056364,132.128701186747));
#59608=CARTESIAN_POINT('Ctrl Pts',(48.4578358417147,4.77363437391953,131.99616207532));
#59609=CARTESIAN_POINT('Ctrl Pts',(48.4500788008297,4.80312196732493,131.862284258242));
#59610=CARTESIAN_POINT('Ctrl Pts',(48.4423276095895,4.83258732390692,131.728507399466));
#59611=CARTESIAN_POINT('Ctrl Pts',(48.4345764183493,4.85648249011215,131.593394224713));
#59612=CARTESIAN_POINT('Ctrl Pts',(48.4268252271092,4.8746959023445,131.457447841577));
#59613=CARTESIAN_POINT('Ctrl Pts',(48.4190773303321,4.89290157339069,131.32155923928));
#59614=CARTESIAN_POINT('Ctrl Pts',(48.411329433555,4.90543024170309,131.184838519642));
#59615=CARTESIAN_POINT('Ctrl Pts',(48.4035815367779,4.91222162617665,131.04779799724));
#59616=CARTESIAN_POINT('Ctrl Pts',(48.3958352606938,4.919011590039,130.91078614076));
#59617=CARTESIAN_POINT('Ctrl Pts',(48.3880889846097,4.92006663781996,130.773455004815));
#59618=CARTESIAN_POINT('Ctrl Pts',(48.3803427085255,4.91537848245433,130.636320632072));
#59619=CARTESIAN_POINT('Ctrl Pts',(48.3725963752602,4.91069029248181,130.499185247033));
#59620=CARTESIAN_POINT('Ctrl Pts',(48.3648500419948,4.90025882812449,130.362247018832));
#59621=CARTESIAN_POINT('Ctrl Pts',(48.3571037087295,4.8841279075608,130.226020194384));
#59622=CARTESIAN_POINT('Ctrl Pts',(48.3493556407265,4.8679933745893,130.089762862884));
#59623=CARTESIAN_POINT('Ctrl Pts',(48.3416075727236,4.8461568915804,129.954217640332));
#59624=CARTESIAN_POINT('Ctrl Pts',(48.3338595047206,4.81871389159144,129.819891474584));
#59625=CARTESIAN_POINT('Ctrl Pts',(48.3261032019787,4.79124172485552,129.685422545389));
#59626=CARTESIAN_POINT('Ctrl Pts',(48.3183468992369,4.75815121643137,129.552175644818));
#59627=CARTESIAN_POINT('Ctrl Pts',(48.310590596495,4.7195886161914,129.420645922834));
#59628=CARTESIAN_POINT('Ctrl Pts',(48.3028301539808,4.68100543393058,129.289045999477));
#59629=CARTESIAN_POINT('Ctrl Pts',(48.2950697114666,4.63694446581079,129.15916545099));
#59630=CARTESIAN_POINT('Ctrl Pts',(48.2873092689524,4.58760086723276,129.031481223624));
#59631=CARTESIAN_POINT('Ctrl Pts',(48.279536368687,4.53817805792977,128.9035920262));
#59632=CARTESIAN_POINT('Ctrl Pts',(48.2717634684216,4.48345582829295,128.777906554099));
#59633=CARTESIAN_POINT('Ctrl Pts',(48.2639905681561,4.42367660083347,128.654879658418));
#59634=CARTESIAN_POINT('Ctrl Pts',(48.2565002323942,4.36607049886774,128.536325100283));
#59635=CARTESIAN_POINT('Ctrl Pts',(48.2490098966323,4.30376883067783,128.420239453904));
#59636=CARTESIAN_POINT('Ctrl Pts',(48.2415195608704,4.23702644637958,128.30700402405));
#59637=CARTESIAN_POINT('Ctrl Pts',(48.2337452267513,4.16775350429406,128.189475238454));
#59638=CARTESIAN_POINT('Ctrl Pts',(48.2259708926322,4.09347702339569,128.07464477195));
#59639=CARTESIAN_POINT('Ctrl Pts',(48.2181965585132,4.01443285913479,127.962968022024));
#59640=CARTESIAN_POINT('Ctrl Pts',(48.2104318055661,3.93548610974164,127.851428903712));
#59641=CARTESIAN_POINT('Ctrl Pts',(48.202667052619,3.85178359166624,127.743036084711));
#59642=CARTESIAN_POINT('Ctrl Pts',(48.1949022996719,3.76360657677979,127.638219654545));
#59643=CARTESIAN_POINT('Ctrl Pts',(48.1871452587869,3.67551714054784,127.533507329535));
#59644=CARTESIAN_POINT('Ctrl Pts',(48.179388217902,3.5829623015873,127.432364621724));
#59645=CARTESIAN_POINT('Ctrl Pts',(48.171631177017,3.4862658669731,127.335191643982));
#59646=CARTESIAN_POINT('Ctrl Pts',(48.1638799857769,3.38964235189244,127.238091945138));
#59647=CARTESIAN_POINT('Ctrl Pts',(48.1561287945368,3.28888373237513,127.144956293787));
#59648=CARTESIAN_POINT('Ctrl Pts',(48.1483776032966,3.18435298424078,127.056150493486));
#59649=CARTESIAN_POINT('Ctrl Pts',(48.1406297065196,3.07986666446284,126.967382438019));
#59650=CARTESIAN_POINT('Ctrl Pts',(48.1328818097425,2.97161170215211,126.882940825983));
#59651=CARTESIAN_POINT('Ctrl Pts',(48.1251339129655,2.85998653866297,126.803153292125));
#59652=CARTESIAN_POINT('Ctrl Pts',(48.1173876368814,2.74838472475152,126.723382448098));
#59653=CARTESIAN_POINT('Ctrl Pts',(48.1096413607972,2.63341442975789,126.648263973041));
#59654=CARTESIAN_POINT('Ctrl Pts',(48.1018950847131,2.5155053356322,126.578083772764));
#59655=CARTESIAN_POINT('Ctrl Pts',(48.0941487514478,2.39759537112803,126.507903054433));
#59656=CARTESIAN_POINT('Ctrl Pts',(48.0864024181824,2.27674690016223,126.442660883586));
#59657=CARTESIAN_POINT('Ctrl Pts',(48.078656084917,2.1534162580258,126.382598357768));
#59658=CARTESIAN_POINT('Ctrl Pts',(48.0709080169141,2.03005799684767,126.322522381365));
#59659=CARTESIAN_POINT('Ctrl Pts',(48.0631599489111,1.90421680982264,126.267628529296));
#59660=CARTESIAN_POINT('Ctrl Pts',(48.0554118809081,1.77637079043816,126.218110528727));
#59661=CARTESIAN_POINT('Ctrl Pts',(48.0476555781663,1.64838889478272,126.168539899837));
#59662=CARTESIAN_POINT('Ctrl Pts',(48.0398992754245,1.51839827550077,126.124356677252));
#59663=CARTESIAN_POINT('Ctrl Pts',(48.0321429726826,1.3868945679069,126.085705457458));
#59664=CARTESIAN_POINT('Ctrl Pts',(48.0243825301684,1.25532067282479,126.047033608345));
#59665=CARTESIAN_POINT('Ctrl Pts',(48.0166220876543,1.1222324594565,126.01389973973));
#59666=CARTESIAN_POINT('Ctrl Pts',(48.0088616451402,0.988136682452456,125.986397462944));
#59667=CARTESIAN_POINT('Ctrl Pts',(48.0010887448747,0.853825643002705,125.958851037063));
#59668=CARTESIAN_POINT('Ctrl Pts',(47.9933158446093,0.718504193942803,125.936954330961));
#59669=CARTESIAN_POINT('Ctrl Pts',(47.9855429443439,0.582686049673517,125.920749245844));
#59670=CARTESIAN_POINT('Ctrl Pts',(47.9780526085818,0.451805237052026,125.905133256388));
#59671=CARTESIAN_POINT('Ctrl Pts',(47.9705622728196,0.320463521573599,125.894802286893));
#59672=CARTESIAN_POINT('Ctrl Pts',(47.9630719370575,0.189119458453297,125.88974802928));
#59673=CARTESIAN_POINT('Ctrl Pts',(47.9552976029384,0.0527954452601593,
125.884502137954));
#59674=CARTESIAN_POINT('Ctrl Pts',(47.9475232688194,-0.0839629306078813,
125.884924372917));
#59675=CARTESIAN_POINT('Ctrl Pts',(47.9397489347003,-0.220645044714559,
125.891062455766));
#59676=CARTESIAN_POINT('Ctrl Pts',(47.9319841817532,-0.357158710331046,
125.897192973977));
#59677=CARTESIAN_POINT('Ctrl Pts',(47.924219428806,-0.493595914367787,125.909025306701));
#59678=CARTESIAN_POINT('Ctrl Pts',(47.9164546758589,-0.629442776011608,
125.926555285839));
#59679=CARTESIAN_POINT('Ctrl Pts',(47.9086976349739,-0.765154712637708,
125.944067853955));
#59680=CARTESIAN_POINT('Ctrl Pts',(47.9009405940889,-0.900277088465724,
125.967266757142));
#59681=CARTESIAN_POINT('Ctrl Pts',(47.8931835532039,-1.03429825157307,125.996095838117));
#59682=CARTESIAN_POINT('Ctrl Pts',(47.8854323619638,-1.16821834827861,126.024903178857));
#59683=CARTESIAN_POINT('Ctrl Pts',(47.8776811707236,-1.30103850451456,126.05933216457));
#59684=CARTESIAN_POINT('Ctrl Pts',(47.8699299794835,-1.43225476209144,126.099275139175));
#59685=CARTESIAN_POINT('Ctrl Pts',(47.8621820827064,-1.56341524925855,126.13920113695));
#59686=CARTESIAN_POINT('Ctrl Pts',(47.8544341859294,-1.69297282037823,126.184636348776));
#59687=CARTESIAN_POINT('Ctrl Pts',(47.8466862891523,-1.82043645977644,126.235422649239));
#59688=CARTESIAN_POINT('Ctrl Pts',(47.8389400130682,-1.94787343652891,126.286198326303));
#59689=CARTESIAN_POINT('Ctrl Pts',(47.8311937369841,-2.07321698980928,126.34232272097));
#59690=CARTESIAN_POINT('Ctrl Pts',(47.8234474609,-2.19599432537318,126.403588868721));
#59691=CARTESIAN_POINT('Ctrl Pts',(47.8157011276346,-2.31877256725115,126.464855468725));
#59692=CARTESIAN_POINT('Ctrl Pts',(47.8079547943694,-2.43898420378337,126.531263722983));
#59693=CARTESIAN_POINT('Ctrl Pts',(47.800208461104,-2.5561797324055,126.602560022804));
#59694=CARTESIAN_POINT('Ctrl Pts',(47.7924603931011,-2.673401506154,126.673872288938));
#59695=CARTESIAN_POINT('Ctrl Pts',(47.784712325098,-2.7876054940033,126.750074575689));
#59696=CARTESIAN_POINT('Ctrl Pts',(47.7769642570951,-2.89837028659462,126.830869363733));
#59697=CARTESIAN_POINT('Ctrl Pts',(47.7692079543532,-3.00925280132562,126.911750021439));
#59698=CARTESIAN_POINT('Ctrl Pts',(47.7614516516114,-3.11668850274028,126.997232699924));
#59699=CARTESIAN_POINT('Ctrl Pts',(47.7536953488695,-3.22028783472276,127.086978565095));
#59700=CARTESIAN_POINT('Ctrl Pts',(47.7459349063553,-3.32394246078833,127.176772330336));
#59701=CARTESIAN_POINT('Ctrl Pts',(47.7381744638411,-3.42375635304082,127.27083354817));
#59702=CARTESIAN_POINT('Ctrl Pts',(47.730414021327,-3.51937684034752,127.368786470771));
#59703=CARTESIAN_POINT('Ctrl Pts',(47.7226411210615,-3.61515082614912,127.466896636099));
#59704=CARTESIAN_POINT('Ctrl Pts',(47.7148682207961,-3.70671769376669,127.568910699191));
#59705=CARTESIAN_POINT('Ctrl Pts',(47.7070953205306,-3.79376451534785,127.674419106198));
#59706=CARTESIAN_POINT('Ctrl Pts',(47.6996049847686,-3.87764696570682,127.77609201685));
#59707=CARTESIAN_POINT('Ctrl Pts',(47.6921146490066,-3.95733210834618,127.881009380511));
#59708=CARTESIAN_POINT('Ctrl Pts',(47.6846243132446,-4.03257907279263,127.988780910974));
#59709=CARTESIAN_POINT('Ctrl Pts',(47.6767527933233,-4.1116553650274,128.102036948611));
#59710=CARTESIAN_POINT('Ctrl Pts',(47.6688812734021,-4.18607751906586,128.218799537863));
#59711=CARTESIAN_POINT('Ctrl Pts',(47.6610097534808,-4.25552329444847,128.338654926915));
#59712=CARTESIAN_POINT('Ctrl Pts',(47.6531519072033,-4.32484843534068,128.458302114768));
#59713=CARTESIAN_POINT('Ctrl Pts',(47.6452940609259,-4.38921423111591,128.581031074442));
#59714=CARTESIAN_POINT('Ctrl Pts',(47.6374362146484,-4.44834071839569,128.706397816284));
#59715=CARTESIAN_POINT('Ctrl Pts',(47.6295863185946,-4.50740738409309,128.831637717564));
#59716=CARTESIAN_POINT('Ctrl Pts',(47.6217364225407,-4.56124512815604,128.959509750956));
#59717=CARTESIAN_POINT('Ctrl Pts',(47.6138865264869,-4.60961876995572,129.089543467497));
#59718=CARTESIAN_POINT('Ctrl Pts',(47.6060446040402,-4.65794327576532,129.219445101044));
#59719=CARTESIAN_POINT('Ctrl Pts',(47.5982026815935,-4.70081460317361,129.351503690871));
#59720=CARTESIAN_POINT('Ctrl Pts',(47.5903607591468,-4.7380450070248,129.485227351399));
#59721=CARTESIAN_POINT('Ctrl Pts',(47.5884650688889,-4.74704500853698,129.517553434989));
#59722=CARTESIAN_POINT('Ctrl Pts',(47.5865693786309,-4.75571559087855,129.54997672912));
#59723=CARTESIAN_POINT('Ctrl Pts',(47.584673688373,-4.76405452823404,129.582490119308));
#59724=CARTESIAN_POINT('Ctrl Pts',(49.3346698100615,-4.76405452823405,129.582490119308));
#59725=CARTESIAN_POINT('Ctrl Pts',(49.3254862744199,-4.80414217617995,129.738791250234));
#59726=CARTESIAN_POINT('Ctrl Pts',(49.3163027387783,-4.83657436684548,129.897224746301));
#59727=CARTESIAN_POINT('Ctrl Pts',(49.3071192031367,-4.86115052127794,130.057099838467));
#59728=CARTESIAN_POINT('Ctrl Pts',(49.2980231085379,-4.8854926738339,130.2154526798));
#59729=CARTESIAN_POINT('Ctrl Pts',(49.2889270139392,-4.90212761659773,130.375219717216));
#59730=CARTESIAN_POINT('Ctrl Pts',(49.2798309193404,-4.91090720595042,130.535709399359));
#59731=CARTESIAN_POINT('Ctrl Pts',(49.2748404249074,-4.91572405248973,130.62376068957));
#59732=CARTESIAN_POINT('Ctrl Pts',(49.2698499304744,-4.91817720641674,130.712029150127));
#59733=CARTESIAN_POINT('Ctrl Pts',(49.2648594360413,-4.91824840372241,130.800398070159));
#59734=CARTESIAN_POINT('',(49.6101405639704,-4.91824998000026,130.803917077946));
#59735=CARTESIAN_POINT('Ctrl Pts',(49.6802330064605,-4.76405452823399,129.582490119308));
#59736=CARTESIAN_POINT('Ctrl Pts',(49.6724719190686,-4.79812062176887,129.715313300975));
#59737=CARTESIAN_POINT('Ctrl Pts',(49.6647108316767,-4.82659962982157,129.849452307907));
#59738=CARTESIAN_POINT('Ctrl Pts',(49.6569497442848,-4.84941681015589,129.98439740871));
#59739=CARTESIAN_POINT('Ctrl Pts',(49.6491764923101,-4.87226975371082,130.119554019933));
#59740=CARTESIAN_POINT('Ctrl Pts',(49.6414032403354,-4.88944309030547,130.25551886157));
#59741=CARTESIAN_POINT('Ctrl Pts',(49.6336299883607,-4.90091400340569,130.391777300257));
#59742=CARTESIAN_POINT('Ctrl Pts',(49.6271428868324,-4.91048695667491,130.505490624966));
#59743=CARTESIAN_POINT('Ctrl Pts',(49.620655785304,-4.91608934210965,130.619408272993));
#59744=CARTESIAN_POINT('Ctrl Pts',(49.6141686837756,-4.91773564682657,130.733232771885));
#59745=CARTESIAN_POINT('Ctrl Pts',(49.6128259771866,-4.91807640057942,130.756792277464));
#59746=CARTESIAN_POINT('Ctrl Pts',(49.6114832705976,-4.9182478550434,130.780354237637));
#59747=CARTESIAN_POINT('Ctrl Pts',(49.6101405640086,-4.9182499800002,130.803917077276));
#59748=CARTESIAN_POINT('Ctrl Pts',(49.6101405639704,-4.91824998000026,130.803917077946));
#59749=CARTESIAN_POINT('Ctrl Pts',(49.6023858624895,-4.91826225251079,130.940002495971));
#59750=CARTESIAN_POINT('Ctrl Pts',(49.5946311610085,-4.91262212522694,131.076308917794));
#59751=CARTESIAN_POINT('Ctrl Pts',(49.5868764595276,-4.90130053173813,131.212326498595));
#59752=CARTESIAN_POINT('Ctrl Pts',(49.5791313051447,-4.8899928766792,131.348176623152));
#59753=CARTESIAN_POINT('Ctrl Pts',(49.5713861507619,-4.87301770363844,131.483738226168));
#59754=CARTESIAN_POINT('Ctrl Pts',(49.563640996379,-4.85039792117699,131.618500082733));
#59755=CARTESIAN_POINT('Ctrl Pts',(49.5559034995563,-4.82780050267849,131.753128701537));
#59756=CARTESIAN_POINT('Ctrl Pts',(49.5481660027335,-4.79956964437166,131.886958762052));
#59757=CARTESIAN_POINT('Ctrl Pts',(49.5404285059108,-4.76578012873537,132.019483173957));
#59758=CARTESIAN_POINT('Ctrl Pts',(49.5326967839559,-4.73201583184741,132.15190867649));
#59759=CARTESIAN_POINT('Ctrl Pts',(49.524965062001,-4.69270123139867,132.283030090413));
#59760=CARTESIAN_POINT('Ctrl Pts',(49.5172333400461,-4.64796228752467,132.412349932284));
#59761=CARTESIAN_POINT('Ctrl Pts',(49.5095047957713,-4.60324173102356,132.541616624663));
#59762=CARTESIAN_POINT('Ctrl Pts',(49.5017762514966,-4.55310139271184,132.669082846602));
#59763=CARTESIAN_POINT('Ctrl Pts',(49.4940477072218,-4.49771717862265,132.794265952908));
#59764=CARTESIAN_POINT('Ctrl Pts',(49.4863206784171,-4.44234382467905,132.919424512387));
#59765=CARTESIAN_POINT('Ctrl Pts',(49.4785936496123,-4.38172879902203,133.042300487275));
#59766=CARTESIAN_POINT('Ctrl Pts',(49.4708666208076,-4.31609611074062,133.162431317386));
#59767=CARTESIAN_POINT('Ctrl Pts',(49.463139411378,-4.25046188824779,133.282564955641));
#59768=CARTESIAN_POINT('Ctrl Pts',(49.4554122019484,-4.17980995816366,133.399952976335));
#59769=CARTESIAN_POINT('Ctrl Pts',(49.4476849925188,-4.10441002871984,133.514157912318));
#59770=CARTESIAN_POINT('Ctrl Pts',(49.4399559065927,-4.02899178895314,133.628390582136));
#59771=CARTESIAN_POINT('Ctrl Pts',(49.4322268206667,-3.94882347236212,133.73943830128));
#59772=CARTESIAN_POINT('Ctrl Pts',(49.4244977347406,-3.8642175489307,133.846893410657));
#59773=CARTESIAN_POINT('Ctrl Pts',(49.4167603993979,-3.77952132381062,133.954463209142));
#59774=CARTESIAN_POINT('Ctrl Pts',(49.4090230640552,-3.69037827561775,134.05843243005));
#59775=CARTESIAN_POINT('Ctrl Pts',(49.4012857287126,-3.59714085074586,134.15842692019));
#59776=CARTESIAN_POINT('Ctrl Pts',(49.3935440914271,-3.50385158605436,134.258477007063));
#59777=CARTESIAN_POINT('Ctrl Pts',(49.3858024541417,-3.40646368920475,134.354547684766));
#59778=CARTESIAN_POINT('Ctrl Pts',(49.3780608168562,-3.3053649772015,134.446303152806));
#59779=CARTESIAN_POINT('Ctrl Pts',(49.3703070839518,-3.20410830746311,134.538201980594));
#59780=CARTESIAN_POINT('Ctrl Pts',(49.3625533510475,-3.0991295414686,134.625771877587));
#59781=CARTESIAN_POINT('Ctrl Pts',(49.3547996181431,-2.99084852814562,134.708718201624));
#59782=CARTESIAN_POINT('Ctrl Pts',(49.3484400987496,-2.90203773047353,134.776749788839));
#59783=CARTESIAN_POINT('Ctrl Pts',(49.3420805793561,-2.81100612753598,134.841671806076));
#59784=CARTESIAN_POINT('Ctrl Pts',(49.3357210599626,-2.71799811049721,134.903344556768));
#59785=CARTESIAN_POINT('Ctrl Pts',(49.3279467258435,-2.60429841788268,134.978737765005));
#59786=CARTESIAN_POINT('Ctrl Pts',(49.3201723917244,-2.48727931327768,135.049516015972));
#59787=CARTESIAN_POINT('Ctrl Pts',(49.3123980576053,-2.36735207534362,135.115372936484));
#59788=CARTESIAN_POINT('Ctrl Pts',(49.3046333046582,-2.24757263701227,135.181148694228));
#59789=CARTESIAN_POINT('Ctrl Pts',(49.2968685517111,-2.1248925358767,135.242015002876));
#59790=CARTESIAN_POINT('Ctrl Pts',(49.289103798764,-1.99975282367048,135.29770811211));
#59791=CARTESIAN_POINT('Ctrl Pts',(49.2813467578789,-1.87473740199042,135.353345906162));
#59792=CARTESIAN_POINT('Ctrl Pts',(49.2735897169939,-1.7472675856387,135.403820567902));
#59793=CARTESIAN_POINT('Ctrl Pts',(49.2658326761089,-1.61780956644197,135.448913908167));
#59794=CARTESIAN_POINT('Ctrl Pts',(49.2580814848688,-1.48844917254455,135.493973243192));
#59795=CARTESIAN_POINT('Ctrl Pts',(49.2503302936286,-1.35710392782053,135.533659206053));
#59796=CARTESIAN_POINT('Ctrl Pts',(49.2425791023885,-1.22426024181166,135.56780159262));
#59797=CARTESIAN_POINT('Ctrl Pts',(49.2348312056114,-1.09147301791324,135.601929467761));
#59798=CARTESIAN_POINT('Ctrl Pts',(49.2270833088343,-0.957188997297075,
135.63051835573));
#59799=CARTESIAN_POINT('Ctrl Pts',(49.2193354120572,-0.821909788955781,
135.653447888519));
#59800=CARTESIAN_POINT('Ctrl Pts',(49.2115891359731,-0.686658878108406,
135.676372624944));
#59801=CARTESIAN_POINT('Ctrl Pts',(49.203842859889,-0.550413578824121,135.693640295569));
#59802=CARTESIAN_POINT('Ctrl Pts',(49.1960965838049,-0.413685343041333,
135.705181722182));
#59803=CARTESIAN_POINT('Ctrl Pts',(49.1883502505395,-0.276956097961955,
135.716723233992));
#59804=CARTESIAN_POINT('Ctrl Pts',(49.1806039172741,-0.139744298850251,
135.722538384558));
#59805=CARTESIAN_POINT('Ctrl Pts',(49.1728575840087,-0.00256576854755872,
135.722609948307));
#59806=CARTESIAN_POINT('Ctrl Pts',(49.1651095160057,0.13464348193624,135.722681528081));
#59807=CARTESIAN_POINT('Ctrl Pts',(49.1573614480027,0.271819057895434,135.717006961373));
#59808=CARTESIAN_POINT('Ctrl Pts',(49.1496133799997,0.408446288292338,135.705621138297));
#59809=CARTESIAN_POINT('Ctrl Pts',(49.1418570772578,0.545218727735405,135.694223214234));
#59810=CARTESIAN_POINT('Ctrl Pts',(49.134100774516,0.681441267198078,135.677101940863));
#59811=CARTESIAN_POINT('Ctrl Pts',(49.1263444717741,0.816604949049659,135.654344062866));
#59812=CARTESIAN_POINT('Ctrl Pts',(49.1185840292599,0.951840771827943,135.631574038305));
#59813=CARTESIAN_POINT('Ctrl Pts',(49.1108235867457,1.08601622860084,135.603161495531));
#59814=CARTESIAN_POINT('Ctrl Pts',(49.1030631442315,1.21863466186354,135.569243892464));
#59815=CARTESIAN_POINT('Ctrl Pts',(49.0952902439661,1.35146598600862,135.53527184185));
#59816=CARTESIAN_POINT('Ctrl Pts',(49.0875173437006,1.48273491729863,135.495777184086));
#59817=CARTESIAN_POINT('Ctrl Pts',(49.0797444434352,1.61196115607087,135.450946922997));
#59818=CARTESIAN_POINT('Ctrl Pts',(49.0722541076733,1.73648969555917,135.40774635482));
#59819=CARTESIAN_POINT('Ctrl Pts',(49.0647637719115,1.85912119143873,135.359591486192));
#59820=CARTESIAN_POINT('Ctrl Pts',(49.0572734361496,1.97944690779201,135.30669034802));
#59821=CARTESIAN_POINT('Ctrl Pts',(49.0494991020305,2.1043348102562,135.251783447115));
#59822=CARTESIAN_POINT('Ctrl Pts',(49.0417247679115,2.22713424172844,135.19158933376));
#59823=CARTESIAN_POINT('Ctrl Pts',(49.0339504337924,2.34736513560895,135.126288426152));
#59824=CARTESIAN_POINT('Ctrl Pts',(49.0261856808453,2.46744785565794,135.061067996076));
#59825=CARTESIAN_POINT('Ctrl Pts',(49.0184209278982,2.58496799623908,134.990753479077));
#59826=CARTESIAN_POINT('Ctrl Pts',(49.0106561749511,2.69946525750274,134.915573380977));
#59827=CARTESIAN_POINT('Ctrl Pts',(49.0028991340661,2.81384879847238,134.840467952811));
#59828=CARTESIAN_POINT('Ctrl Pts',(48.9951420931811,2.92521511027227,134.760506773765));
#59829=CARTESIAN_POINT('Ctrl Pts',(48.9873850522961,3.03312863610992,134.675964127652));
#59830=CARTESIAN_POINT('Ctrl Pts',(48.9796338610559,3.14096078351843,134.591485235806));
#59831=CARTESIAN_POINT('Ctrl Pts',(48.9718826698158,3.24534502109734,134.502431993839));
#59832=CARTESIAN_POINT('Ctrl Pts',(48.9641314785756,3.34587523505336,134.409121632385));
#59833=CARTESIAN_POINT('Ctrl Pts',(48.9563835817986,3.44636272098658,134.315850930323));
#59834=CARTESIAN_POINT('Ctrl Pts',(48.9486356850215,3.54299915532662,134.218326972927));
#59835=CARTESIAN_POINT('Ctrl Pts',(48.9408877882444,3.63541213714717,134.116906716201));
#59836=CARTESIAN_POINT('Ctrl Pts',(48.9331415121603,3.72780578816425,134.015507674406));
#59837=CARTESIAN_POINT('Ctrl Pts',(48.9253952360761,3.81597748074614,133.91021424321));
#59838=CARTESIAN_POINT('Ctrl Pts',(48.917648959992,3.89959256103934,133.801419329101));
#59839=CARTESIAN_POINT('Ctrl Pts',(48.9099026267266,3.98320825856018,133.692623611892));
#59840=CARTESIAN_POINT('Ctrl Pts',(48.9021562934613,4.06226703842993,133.580326670183));
#59841=CARTESIAN_POINT('Ctrl Pts',(48.8944099601959,4.13647559343899,133.464953169496));
#59842=CARTESIAN_POINT('Ctrl Pts',(48.8866618921929,4.21070076693912,133.349553831713));
#59843=CARTESIAN_POINT('Ctrl Pts',(48.8789138241899,4.28007334276029,133.23107689273));
#59844=CARTESIAN_POINT('Ctrl Pts',(48.871165756187,4.34434448267861,133.109974218827));
#59845=CARTESIAN_POINT('Ctrl Pts',(48.8634094534451,4.40868393072945,132.988742835561));
#59846=CARTESIAN_POINT('Ctrl Pts',(48.8556531507032,4.46791092854265,132.864880488621));
#59847=CARTESIAN_POINT('Ctrl Pts',(48.8478968479613,4.52182335284511,132.738862266096));
#59848=CARTESIAN_POINT('Ctrl Pts',(48.8401364054471,4.57576455183176,132.612776783851));
#59849=CARTESIAN_POINT('Ctrl Pts',(48.8323759629329,4.62438538671388,132.484533498637));
#59850=CARTESIAN_POINT('Ctrl Pts',(48.8246155204187,4.66753304922153,132.354624561843));
#59851=CARTESIAN_POINT('Ctrl Pts',(48.8168426201533,4.71074997618745,132.224507083691));
#59852=CARTESIAN_POINT('Ctrl Pts',(48.8090697198879,4.74847606584788,132.092718986835));
#59853=CARTESIAN_POINT('Ctrl Pts',(48.8012968196225,4.78060903611737,131.95976544112));
#59854=CARTESIAN_POINT('Ctrl Pts',(48.7938064838606,4.81157389197885,131.831645091685));
#59855=CARTESIAN_POINT('Ctrl Pts',(48.7863161480987,4.83734515614878,131.702442858355));
#59856=CARTESIAN_POINT('Ctrl Pts',(48.7788258123368,4.85787691917531,131.572615068021));
#59857=CARTESIAN_POINT('Ctrl Pts',(48.7710514782177,4.87918715023787,131.437864817554));
#59858=CARTESIAN_POINT('Ctrl Pts',(48.7632771440986,4.89492023014025,131.302013789405));
#59859=CARTESIAN_POINT('Ctrl Pts',(48.7555028099796,4.9049684620969,131.165563397642));
#59860=CARTESIAN_POINT('Ctrl Pts',(48.7477380570325,4.91500431050568,131.029281168793));
#59861=CARTESIAN_POINT('Ctrl Pts',(48.7399733040854,4.91936922251657,130.892401432213));
#59862=CARTESIAN_POINT('Ctrl Pts',(48.7322085511383,4.91800664323881,130.755434964183));
#59863=CARTESIAN_POINT('Ctrl Pts',(48.7244515102534,4.91664541729399,130.618604533179));
#59864=CARTESIAN_POINT('Ctrl Pts',(48.7166944693684,4.90956802454522,130.48168793057));
#59865=CARTESIAN_POINT('Ctrl Pts',(48.7089374284834,4.89676979864831,130.34519985972));
#59866=CARTESIAN_POINT('Ctrl Pts',(48.7011862372433,4.88398122399307,130.208814715586));
#59867=CARTESIAN_POINT('Ctrl Pts',(48.6934350460031,4.86548043954567,130.072857847666));
#59868=CARTESIAN_POINT('Ctrl Pts',(48.685683854763,4.84131482599757,129.937842401903));
#59869=CARTESIAN_POINT('Ctrl Pts',(48.6779359579859,4.81715948347998,129.802884341306));
#59870=CARTESIAN_POINT('Ctrl Pts',(48.6701880612089,4.7873441693381,129.668867291083));
#59871=CARTESIAN_POINT('Ctrl Pts',(48.6624401644318,4.75196790897045,129.536297506118));
#59872=CARTESIAN_POINT('Ctrl Pts',(48.6546938883477,4.7165990485538,129.403755451894));
#59873=CARTESIAN_POINT('Ctrl Pts',(48.6469476122636,4.67567165637769,129.272660438277));
#59874=CARTESIAN_POINT('Ctrl Pts',(48.6392013361796,4.62933540721616,129.143506394585));
#59875=CARTESIAN_POINT('Ctrl Pts',(48.6314550029142,4.5829988160109,129.014351397507));
#59876=CARTESIAN_POINT('Ctrl Pts',(48.6237086696489,4.53125342017473,128.887137766943));
#59877=CARTESIAN_POINT('Ctrl Pts',(48.6159623363835,4.47429796312652,128.762341812642));
#59878=CARTESIAN_POINT('Ctrl Pts',(48.6082142683806,4.41732975129861,128.637517911153));
#59879=CARTESIAN_POINT('Ctrl Pts',(48.6004662003776,4.35514931884176,128.515113118901));
#59880=CARTESIAN_POINT('Ctrl Pts',(48.5927181323746,4.28800233051721,128.395581035292));
#59881=CARTESIAN_POINT('Ctrl Pts',(48.5849618296328,4.22078397757449,128.275921911563));
#59882=CARTESIAN_POINT('Ctrl Pts',(48.5772055268909,4.14858871614824,128.15914193688));
#59883=CARTESIAN_POINT('Ctrl Pts',(48.5694492241491,4.07170699873664,128.045667959994));
#59884=CARTESIAN_POINT('Ctrl Pts',(48.561688781635,3.99478424723779,127.932133418631));
#59885=CARTESIAN_POINT('Ctrl Pts',(48.5539283391208,3.91317028823315,127.821908705057));
#59886=CARTESIAN_POINT('Ctrl Pts',(48.5461678966067,3.82719658602265,127.715388401045));
#59887=CARTESIAN_POINT('Ctrl Pts',(48.5383949963413,3.74108487119274,127.608697101185));
#59888=CARTESIAN_POINT('Ctrl Pts',(48.5306220960759,3.65059968584837,127.505722388042));
#59889=CARTESIAN_POINT('Ctrl Pts',(48.5228491958105,3.5561107577211,127.406823371071));
#59890=CARTESIAN_POINT('Ctrl Pts',(48.5153588600483,3.46505674013221,127.311519582477));
#59891=CARTESIAN_POINT('Ctrl Pts',(48.5078685242861,3.37028523981213,127.220000524991));
#59892=CARTESIAN_POINT('Ctrl Pts',(48.5003781885239,3.27215536231819,127.132551479368));
#59893=CARTESIAN_POINT('Ctrl Pts',(48.4926038544048,3.17030486069543,127.041786776603));
#59894=CARTESIAN_POINT('Ctrl Pts',(48.4848295202857,3.06451365720145,126.955119291837));
#59895=CARTESIAN_POINT('Ctrl Pts',(48.4770551861666,2.95514539294957,126.872910659977));
#59896=CARTESIAN_POINT('Ctrl Pts',(48.4692904332195,2.84591191530886,126.790803342908));
#59897=CARTESIAN_POINT('Ctrl Pts',(48.4615256802724,2.7331104578492,126.713144177718));
#59898=CARTESIAN_POINT('Ctrl Pts',(48.4537609273253,2.61714018182043,126.640256832692));
#59899=CARTESIAN_POINT('Ctrl Pts',(48.4460038864403,2.50128508910469,126.567441880405));
#59900=CARTESIAN_POINT('Ctrl Pts',(48.4382468455553,2.38226776999332,126.499389523282));
#59901=CARTESIAN_POINT('Ctrl Pts',(48.4304898046703,2.26051873673281,126.436381896993));
#59902=CARTESIAN_POINT('Ctrl Pts',(48.4227386134302,2.1388615153655,126.373421785245));
#59903=CARTESIAN_POINT('Ctrl Pts',(48.4149874221901,2.01447702598552,126.315499011128));
#59904=CARTESIAN_POINT('Ctrl Pts',(48.40723623095,1.88782260322829,126.262851079842));
#59905=CARTESIAN_POINT('Ctrl Pts',(48.3994883341729,1.76122201197917,126.21022552533));
#59906=CARTESIAN_POINT('Ctrl Pts',(48.3917404373958,1.63235376649237,126.162870504337));
#59907=CARTESIAN_POINT('Ctrl Pts',(48.3839925406187,1.50169731898762,126.120976347122));
#59908=CARTESIAN_POINT('Ctrl Pts',(48.3762462645346,1.37106820199506,126.079090953261));
#59909=CARTESIAN_POINT('Ctrl Pts',(48.3684999884505,1.23865199905632,126.042664270389));
#59910=CARTESIAN_POINT('Ctrl Pts',(48.3607537123663,1.10494516976763,126.011837353741));
#59911=CARTESIAN_POINT('Ctrl Pts',(48.353007379101,0.971237353485504,125.981010209535));
#59912=CARTESIAN_POINT('Ctrl Pts',(48.3452610458356,0.836239272813611,125.955783001873));
#59913=CARTESIAN_POINT('Ctrl Pts',(48.3375147125703,0.700459086306537,125.93624597934));
#59914=CARTESIAN_POINT('Ctrl Pts',(48.3297666445673,0.564648492767759,125.916704581626));
#59915=CARTESIAN_POINT('Ctrl Pts',(48.3220185765643,0.428055831776927,125.902855960378));
#59916=CARTESIAN_POINT('Ctrl Pts',(48.3142705085613,0.291195517166221,125.894738612433));
#59917=CARTESIAN_POINT('Ctrl Pts',(48.3065142058194,0.154189745784861,125.886612637275));
#59918=CARTESIAN_POINT('Ctrl Pts',(48.2987579030776,0.0169161434348984,
125.884230126563));
#59919=CARTESIAN_POINT('Ctrl Pts',(48.2910016003357,-0.120109173270614,
125.887577436563));
#59920=CARTESIAN_POINT('Ctrl Pts',(48.2832411578215,-0.257207624513591,
125.890926533122));
#59921=CARTESIAN_POINT('Ctrl Pts',(48.2754807153074,-0.394057136144087,
125.900011518186));
#59922=CARTESIAN_POINT('Ctrl Pts',(48.2677202727932,-0.530146570791028,
125.914766802536));
#59923=CARTESIAN_POINT('Ctrl Pts',(48.2599473725277,-0.666454468279731,
125.929545773379));
#59924=CARTESIAN_POINT('Ctrl Pts',(48.2521744722623,-0.801999463745009,
125.950013174732));
#59925=CARTESIAN_POINT('Ctrl Pts',(48.2444015719969,-0.936279581361401,
125.976052051616));
#59926=CARTESIAN_POINT('Ctrl Pts',(48.2369112362349,-1.06567827846977,126.001144349737));
#59927=CARTESIAN_POINT('Ctrl Pts',(48.229420900473,-1.19390216432778,126.031410010976));
#59928=CARTESIAN_POINT('Ctrl Pts',(48.221930564711,-1.32051711883283,126.066701110872));
#59929=CARTESIAN_POINT('Ctrl Pts',(48.2141562305919,-1.45193271782338,126.103330283547));
#59930=CARTESIAN_POINT('Ctrl Pts',(48.2063818964729,-1.5820312568905,126.145489526722));
#59931=CARTESIAN_POINT('Ctrl Pts',(48.1986075623538,-1.7103119254403,126.19306837133));
#59932=CARTESIAN_POINT('Ctrl Pts',(48.1908428094067,-1.83843449953018,126.240588579264));
#59933=CARTESIAN_POINT('Ctrl Pts',(48.1830780564596,-1.96474329771196,126.293514964412));
#59934=CARTESIAN_POINT('Ctrl Pts',(48.1753133035125,-2.08875025228365,126.351686651724));
#59935=CARTESIAN_POINT('Ctrl Pts',(48.1675562626275,-2.21263404140089,126.409800562098));
#59936=CARTESIAN_POINT('Ctrl Pts',(48.1597992217425,-2.33422018493114,126.473149242116));
#59937=CARTESIAN_POINT('Ctrl Pts',(48.1520421808574,-2.45303861176011,126.541522990854));
#59938=CARTESIAN_POINT('Ctrl Pts',(48.1442909896173,-2.57176743668864,126.609845178416));
#59939=CARTESIAN_POINT('Ctrl Pts',(48.1365397983772,-2.68773236178119,126.683184697831));
#59940=CARTESIAN_POINT('Ctrl Pts',(48.128788607137,-2.80048636664627,126.761285157878));
#59941=CARTESIAN_POINT('Ctrl Pts',(48.1210407103599,-2.91319244805147,126.839352423147));
#59942=CARTESIAN_POINT('Ctrl Pts',(48.1132928135829,-3.02269000284436,126.922176382256));
#59943=CARTESIAN_POINT('Ctrl Pts',(48.1055449168058,-3.12855974515137,127.009456536628));
#59944=CARTESIAN_POINT('Ctrl Pts',(48.0977986407217,-3.23440734179072,127.096718433874));
#59945=CARTESIAN_POINT('Ctrl Pts',(48.0900523646376,-3.33662833388241,127.188434423764));
#59946=CARTESIAN_POINT('Ctrl Pts',(48.0823060885535,-3.43483569912353,127.284263064582));
#59947=CARTESIAN_POINT('Ctrl Pts',(48.0745597552881,-3.53304378930899,127.380092412784));
#59948=CARTESIAN_POINT('Ctrl Pts',(48.0668134220227,-3.62723791370176,127.480034199447));
#59949=CARTESIAN_POINT('Ctrl Pts',(48.0590670887573,-3.71706747149833,127.583709677953));
#59950=CARTESIAN_POINT('Ctrl Pts',(48.0513190207544,-3.80691714600129,127.687408373863));
#59951=CARTESIAN_POINT('Ctrl Pts',(48.0435709527514,-3.89240005299712,127.794842130003));
#59952=CARTESIAN_POINT('Ctrl Pts',(48.0358228847485,-3.97320575076395,127.905598963929));
#59953=CARTESIAN_POINT('Ctrl Pts',(48.0280665820066,-4.05409732978829,128.016473511536));
#59954=CARTESIAN_POINT('Ctrl Pts',(48.0203102792647,-4.1303015386904,128.130677875748));
#59955=CARTESIAN_POINT('Ctrl Pts',(48.0125539765228,-4.20155088269604,128.247770458269));
#59956=CARTESIAN_POINT('Ctrl Pts',(48.0047935340087,-4.27283825462176,128.364925536626));
#59957=CARTESIAN_POINT('Ctrl Pts',(47.9970330914945,-4.33916530315918,128.48497156288));
#59958=CARTESIAN_POINT('Ctrl Pts',(47.9892726489803,-4.40031092813965,128.60744305011));
#59959=CARTESIAN_POINT('Ctrl Pts',(47.9814997487149,-4.46155470950558,128.730111139445));
#59960=CARTESIAN_POINT('Ctrl Pts',(47.9737268484495,-4.5176002859999,128.855212113339));
#59961=CARTESIAN_POINT('Ctrl Pts',(47.965953948184,-4.56827472496393,128.982260428291));
#59962=CARTESIAN_POINT('Ctrl Pts',(47.9584636124221,-4.61710702042993,129.104690216978));
#59963=CARTESIAN_POINT('Ctrl Pts',(47.9509732766601,-4.66095180481061,129.228927932819));
#59964=CARTESIAN_POINT('Ctrl Pts',(47.9434829408981,-4.69969887862443,129.354528381493));
#59965=CARTESIAN_POINT('Ctrl Pts',(47.9389845512163,-4.72296878835696,129.429958880246));
#59966=CARTESIAN_POINT('Ctrl Pts',(47.9344861615344,-4.74442940765616,129.505972072028));
#59967=CARTESIAN_POINT('Ctrl Pts',(47.9299877718525,-4.76405452823408,129.582490119308));
#59968=CARTESIAN_POINT('Origin',(213.235140564004,0.,130.804360617566));
#59969=CARTESIAN_POINT('',(45.8349994066072,-4.76405452823404,129.582490119308));
#59970=CARTESIAN_POINT('',(46.1799254115191,-4.76405452823402,129.582490119308));
#59971=CARTESIAN_POINT('',(213.235140564004,-4.76405452823405,129.582490119308));
#59972=CARTESIAN_POINT('',(47.5148594359393,-4.91824920960731,130.807148931941));
#59973=CARTESIAN_POINT('Ctrl Pts',(47.5148594359393,-4.91824920960731,130.807148931941));
#59974=CARTESIAN_POINT('Ctrl Pts',(47.505802540397,-4.91815813926165,130.9677860034));
#59975=CARTESIAN_POINT('Ctrl Pts',(47.4967456448546,-4.9101921353692,131.128139470124));
#59976=CARTESIAN_POINT('Ctrl Pts',(47.4876887493124,-4.89446417761299,131.287479108791));
#59977=CARTESIAN_POINT('Ctrl Pts',(47.479032267672,-4.8794315677169,131.43977419161));
#59978=CARTESIAN_POINT('Ctrl Pts',(47.4703757860316,-4.85730870168485,131.591143020276));
#59979=CARTESIAN_POINT('Ctrl Pts',(47.4617193043913,-4.82824555908569,131.740965061112));
#59980=CARTESIAN_POINT('Ctrl Pts',(47.4530368824345,-4.79909532485441,131.891236063928));
#59981=CARTESIAN_POINT('Ctrl Pts',(47.4443544604778,-4.7629632741104,132.039950790789));
#59982=CARTESIAN_POINT('Ctrl Pts',(47.435672038521,-4.72004930543188,132.18650301862));
#59983=CARTESIAN_POINT('Ctrl Pts',(47.426957849973,-4.67697832635815,132.3335914407));
#59984=CARTESIAN_POINT('Ctrl Pts',(47.418243661425,-4.62707582962666,132.478501311877));
#59985=CARTESIAN_POINT('Ctrl Pts',(47.409529472877,-4.57059100507844,132.620642789145));
#59986=CARTESIAN_POINT('Ctrl Pts',(47.4084118783952,-4.56334682762346,132.63887243035));
#59987=CARTESIAN_POINT('Ctrl Pts',(47.4072942839134,-4.55599444550586,132.657056570192));
#59988=CARTESIAN_POINT('Ctrl Pts',(47.4061766894317,-4.54853443858162,132.675193994309));
#59989=CARTESIAN_POINT('Ctrl Pts',(47.3984023553126,-4.49664031481259,132.80136354637));
#59990=CARTESIAN_POINT('Ctrl Pts',(47.3906280211935,-4.43941038363547,132.925572107387));
#59991=CARTESIAN_POINT('Ctrl Pts',(47.3828536870744,-4.37701349101544,133.047335419468));
#59992=CARTESIAN_POINT('Ctrl Pts',(47.3750889341273,-4.314693496989,133.16894866915));
#59993=CARTESIAN_POINT('Ctrl Pts',(47.3673241811802,-4.24721938816846,133.288122321364));
#59994=CARTESIAN_POINT('Ctrl Pts',(47.3595594282331,-4.17480855864665,133.404390725305));
#59995=CARTESIAN_POINT('Ctrl Pts',(47.3518023873481,-4.10246964858174,133.520543649828));
#59996=CARTESIAN_POINT('Ctrl Pts',(47.3440453464632,-4.02520398079192,133.633796738702));
#59997=CARTESIAN_POINT('Ctrl Pts',(47.3362883055782,-3.94327530794265,133.743707978507));
#59998=CARTESIAN_POINT('Ctrl Pts',(47.3285371143381,-3.86140841814278,133.853536333391));
#59999=CARTESIAN_POINT('Ctrl Pts',(47.3207859230979,-3.77488575519245,133.960027543149));
#60000=CARTESIAN_POINT('Ctrl Pts',(47.3130347318578,-3.68401471275957,134.062767998277));
#60001=CARTESIAN_POINT('Ctrl Pts',(47.3052868350807,-3.5931822929438,134.165464785971));
#60002=CARTESIAN_POINT('Ctrl Pts',(47.2975389383037,-3.49800542800665,134.26441369748));
#60003=CARTESIAN_POINT('Ctrl Pts',(47.2897910415266,-3.39883203456208,134.35923387316));
#60004=CARTESIAN_POINT('Ctrl Pts',(47.2820447654425,-3.29967938605348,134.454034214503));
#60005=CARTESIAN_POINT('Ctrl Pts',(47.2742984893584,-3.19653215427026,134.544707267839));
#60006=CARTESIAN_POINT('Ctrl Pts',(47.2665522132743,-3.08977510178349,134.630909047012));
#60007=CARTESIAN_POINT('Ctrl Pts',(47.258805880009,-2.98301726124041,134.717111462508));
#60008=CARTESIAN_POINT('Ctrl Pts',(47.2510595467437,-2.87264985100474,134.798842292367));
#60009=CARTESIAN_POINT('Ctrl Pts',(47.2433132134783,-2.75909037574016,134.875798123042));
#60010=CARTESIAN_POINT('Ctrl Pts',(47.2355651454754,-2.64550546961845,134.952771187442));
#60011=CARTESIAN_POINT('Ctrl Pts',(47.2278170774723,-2.52872739960516,135.024966905534));
#60012=CARTESIAN_POINT('Ctrl Pts',(47.2200690094694,-2.40920193042337,135.09212566721));
#60013=CARTESIAN_POINT('Ctrl Pts',(47.2123127067275,-2.28954942815057,135.159355806016));
#60014=CARTESIAN_POINT('Ctrl Pts',(47.2045564039857,-2.16714403514731,135.221538102717));
#60015=CARTESIAN_POINT('Ctrl Pts',(47.1968001012438,-2.04245585228769,135.278459091444));
#60016=CARTESIAN_POINT('Ctrl Pts',(47.1890396587297,-1.91770111959041,135.335410460616));
#60017=CARTESIAN_POINT('Ctrl Pts',(47.1812792162155,-1.79066153124912,135.387094779138));
#60018=CARTESIAN_POINT('Ctrl Pts',(47.1735187737014,-1.66182542994866,135.43334747247));
#60019=CARTESIAN_POINT('Ctrl Pts',(47.165745873436,-1.53278250950103,135.479674414731));
#60020=CARTESIAN_POINT('Ctrl Pts',(47.1579729731705,-1.40193768649131,135.520552191155));
#60021=CARTESIAN_POINT('Ctrl Pts',(47.1502000729051,-1.26979353079927,135.555866426427));
#60022=CARTESIAN_POINT('Ctrl Pts',(47.1427097371431,-1.14245314801696,135.589896900296));
#60023=CARTESIAN_POINT('Ctrl Pts',(47.135219401381,-1.01390656101556,135.61876124033));
#60024=CARTESIAN_POINT('Ctrl Pts',(47.1277290656189,-0.884608863575147,
135.64240259971));
#60025=CARTESIAN_POINT('Ctrl Pts',(47.1199547314998,-0.750408804637845,
135.666940328416));
#60026=CARTESIAN_POINT('Ctrl Pts',(47.1121803973807,-0.614974448765209,
135.685928927673));
#60027=CARTESIAN_POINT('Ctrl Pts',(47.1044060632616,-0.478804481204911,
135.699248699155));
#60028=CARTESIAN_POINT('Ctrl Pts',(47.0966413103146,-0.342802330959771,
135.712552055208));
#60029=CARTESIAN_POINT('Ctrl Pts',(47.0888765573675,-0.206066758215026,
135.720200446491));
#60030=CARTESIAN_POINT('Ctrl Pts',(47.0811118044204,-0.0691070349976097,
135.722125077177));
#60031=CARTESIAN_POINT('Ctrl Pts',(47.0733547635354,0.0677166578917276,
135.724047796293));
#60032=CARTESIAN_POINT('Ctrl Pts',(47.0655977226504,0.204763669814227,135.7202580626));
#60033=CARTESIAN_POINT('Ctrl Pts',(47.0578406817654,0.341519557604534,135.710738859638));
#60034=CARTESIAN_POINT('Ctrl Pts',(47.0500894905253,0.478172316716238,135.70122683518));
#60035=CARTESIAN_POINT('Ctrl Pts',(47.0423382992852,0.614534000231392,135.685993968457));
#60036=CARTESIAN_POINT('Ctrl Pts',(47.034587108045,0.750090472975039,135.665075312428));
#60037=CARTESIAN_POINT('Ctrl Pts',(47.026839211268,0.885589330601681,135.644165547387));
#60038=CARTESIAN_POINT('Ctrl Pts',(47.0190913144908,1.02028327255562,135.617574858998));
#60039=CARTESIAN_POINT('Ctrl Pts',(47.0113434177137,1.15366381340378,135.585390095424));
#60040=CARTESIAN_POINT('Ctrl Pts',(47.0035971416296,1.28701645391815,135.553212064207));
#60041=CARTESIAN_POINT('Ctrl Pts',(46.9958508655456,1.41905585997372,135.515442376967));
#60042=CARTESIAN_POINT('Ctrl Pts',(46.9881045894615,1.54928465270907,135.472218812432));
#60043=CARTESIAN_POINT('Ctrl Pts',(46.9803582561962,1.67951440676379,135.428994928831));
#60044=CARTESIAN_POINT('Ctrl Pts',(46.9726119229308,1.80793314976746,135.380317210757));
#60045=CARTESIAN_POINT('Ctrl Pts',(46.9648655896655,1.9340599398419,135.326372914276));
#60046=CARTESIAN_POINT('Ctrl Pts',(46.9571175216625,2.06021497513649,135.272416537344));
#60047=CARTESIAN_POINT('Ctrl Pts',(46.9493694536595,2.18407667676163,135.213191388823));
#60048=CARTESIAN_POINT('Ctrl Pts',(46.9416213856566,2.30518568065845,135.148932177592));
#60049=CARTESIAN_POINT('Ctrl Pts',(46.9338650829147,2.42642340064584,135.084604670907));
#60050=CARTESIAN_POINT('Ctrl Pts',(46.9261087801728,2.54490223279135,135.015232597327));
#60051=CARTESIAN_POINT('Ctrl Pts',(46.918352477431,2.66018848120692,134.941096082513));
#60052=CARTESIAN_POINT('Ctrl Pts',(46.9105920349168,2.77553626136447,134.86691999881));
#60053=CARTESIAN_POINT('Ctrl Pts',(46.9028315924027,2.88768774292624,134.787974631811));
#60054=CARTESIAN_POINT('Ctrl Pts',(46.8950711498885,2.99624050352007,134.70458188149));
#60055=CARTESIAN_POINT('Ctrl Pts',(46.8872982496231,3.10496752264206,134.621055261723));
#60056=CARTESIAN_POINT('Ctrl Pts',(46.8795253493577,3.21008397656531,134.533067243059));
#60057=CARTESIAN_POINT('Ctrl Pts',(46.8717524490922,3.31122198680281,134.440978829121));
#60058=CARTESIAN_POINT('Ctrl Pts',(46.8642621133301,3.40868337561786,134.352238060986));
#60059=CARTESIAN_POINT('Ctrl Pts',(46.856771777568,3.50245033256831,134.259690057551));
#60060=CARTESIAN_POINT('Ctrl Pts',(46.8492814418059,3.59222904151158,134.16368697501));
#60061=CARTESIAN_POINT('Ctrl Pts',(46.8415071076869,3.68541173749129,134.064043906416));
#60062=CARTESIAN_POINT('Ctrl Pts',(46.8337327735678,3.77459296134874,133.960362948841));
#60063=CARTESIAN_POINT('Ctrl Pts',(46.8259584394487,3.85940245593429,133.852998960438));
#60064=CARTESIAN_POINT('Ctrl Pts',(46.8181936865016,3.94410743039741,133.745767288555));
#60065=CARTESIAN_POINT('Ctrl Pts',(46.8104289335545,4.02445115561818,133.634861920963));
#60066=CARTESIAN_POINT('Ctrl Pts',(46.8026641806074,4.100100477749,133.520674136816));
#60067=CARTESIAN_POINT('Ctrl Pts',(46.7949071397224,4.17567466390661,133.406599765587));
#60068=CARTESIAN_POINT('Ctrl Pts',(46.7871500988374,4.24656351112388,133.289249789453));
#60069=CARTESIAN_POINT('Ctrl Pts',(46.7793930579524,4.31247463387257,133.169047826206));
#60070=CARTESIAN_POINT('Ctrl Pts',(46.7716418667122,4.37833605253089,133.048936508194));
#60071=CARTESIAN_POINT('Ctrl Pts',(46.7638906754721,4.43922703109902,132.925977825342));
#60072=CARTESIAN_POINT('Ctrl Pts',(46.756139484232,4.49489915800388,132.800623281114));
#60073=CARTESIAN_POINT('Ctrl Pts',(46.7483915874549,4.55054762276969,132.675322015911));
#60074=CARTESIAN_POINT('Ctrl Pts',(46.7406436906778,4.60098148924961,132.547627271227));
#60075=CARTESIAN_POINT('Ctrl Pts',(46.7328957939008,4.64599897646354,132.418013793809));
#60076=CARTESIAN_POINT('Ctrl Pts',(46.7251495178166,4.6910070469896,132.288427428737));
#60077=CARTESIAN_POINT('Ctrl Pts',(46.7174032417325,4.730600863636,132.156923498343));
#60078=CARTESIAN_POINT('Ctrl Pts',(46.7096569656484,4.76462749812631,132.023994934318));
#60079=CARTESIAN_POINT('Ctrl Pts',(46.701910632383,4.79865438379351,131.891065389044));
#60080=CARTESIAN_POINT('Ctrl Pts',(46.6941642991177,4.82711390834911,131.756711567909));
#60081=CARTESIAN_POINT('Ctrl Pts',(46.6864179658523,4.84990365479118,131.621439317413));
#60082=CARTESIAN_POINT('Ctrl Pts',(46.6786698978494,4.87269850483896,131.486136773633));
#60083=CARTESIAN_POINT('Ctrl Pts',(46.6709218298464,4.88982098526288,131.34991577668));
#60084=CARTESIAN_POINT('Ctrl Pts',(46.6631737618434,4.90122026579724,131.213289668427));
#60085=CARTESIAN_POINT('Ctrl Pts',(46.6554174591016,4.91263166162261,131.076518352321));
#60086=CARTESIAN_POINT('Ctrl Pts',(46.6476611563597,4.91830767418128,130.939341455065));
#60087=CARTESIAN_POINT('Ctrl Pts',(46.6399048536178,4.91824955790514,130.802275272055));
#60088=CARTESIAN_POINT('Ctrl Pts',(46.6321444111037,4.91819141061059,130.665135932696));
#60089=CARTESIAN_POINT('Ctrl Pts',(46.6243839685895,4.91239305274211,130.528107815752));
#60090=CARTESIAN_POINT('Ctrl Pts',(46.6166235260754,4.90090778874081,130.391703485361));
#60091=CARTESIAN_POINT('Ctrl Pts',(46.6088506258099,4.88940408757413,130.255080186629));
#60092=CARTESIAN_POINT('Ctrl Pts',(46.6010777255445,4.87219528647958,130.119083063576));
#60093=CARTESIAN_POINT('Ctrl Pts',(46.5933048252791,4.84938626072064,129.984216754068));
#60094=CARTESIAN_POINT('Ctrl Pts',(46.5858144895171,4.82740640050065,129.854253174619));
#60095=CARTESIAN_POINT('Ctrl Pts',(46.5783241537551,4.80022647473307,129.725339921653));
#60096=CARTESIAN_POINT('Ctrl Pts',(46.5708338179931,4.76798394759412,129.597914540037));
#60097=CARTESIAN_POINT('Ctrl Pts',(46.563059483874,4.73451893523855,129.465657786346));
#60098=CARTESIAN_POINT('Ctrl Pts',(46.555285149755,4.69549383910071,129.334585006854));
#60099=CARTESIAN_POINT('Ctrl Pts',(46.5475108156359,4.65100707836144,129.205199518886));
#60100=CARTESIAN_POINT('Ctrl Pts',(46.5397460626888,4.60657514357895,129.075973486969));
#60101=CARTESIAN_POINT('Ctrl Pts',(46.5319813097417,4.55669506280702,128.94843097529));
#60102=CARTESIAN_POINT('Ctrl Pts',(46.5242165567946,4.50151595248786,128.823063771559));
#60103=CARTESIAN_POINT('Ctrl Pts',(46.5164595159096,4.44639164683888,128.697821084302));
#60104=CARTESIAN_POINT('Ctrl Pts',(46.5087024750246,4.38597894187071,128.574749760928));
#60105=CARTESIAN_POINT('Ctrl Pts',(46.5009454341396,4.32047619770884,128.454324769428));
#60106=CARTESIAN_POINT('Ctrl Pts',(46.4931942428995,4.25502284967587,128.333990591352));
#60107=CARTESIAN_POINT('Ctrl Pts',(46.4854430516594,4.18448728868249,128.216299115046));
#60108=CARTESIAN_POINT('Ctrl Pts',(46.4776918604193,4.10911510485752,128.101703384854));
#60109=CARTESIAN_POINT('Ctrl Pts',(46.4699439636422,4.0337749562213,127.987156360904));
#60110=CARTESIAN_POINT('Ctrl Pts',(46.4621960668651,3.95360248776345,127.875702792054));
#60111=CARTESIAN_POINT('Ctrl Pts',(46.454448170088,3.86888804982,127.76776905457));
#60112=CARTESIAN_POINT('Ctrl Pts',(46.4467018940039,3.78419133231074,127.659857894497));
#60113=CARTESIAN_POINT('Ctrl Pts',(46.4389556179198,3.69495477631535,127.555465408657));
#60114=CARTESIAN_POINT('Ctrl Pts',(46.4312093418357,3.60151043775749,127.45498670156));
#60115=CARTESIAN_POINT('Ctrl Pts',(46.4234630085703,3.50806540941487,127.354507252752));
#60116=CARTESIAN_POINT('Ctrl Pts',(46.415716675305,3.41041280278097,127.257941926629));
#60117=CARTESIAN_POINT('Ctrl Pts',(46.4079703420397,3.30892284195152,127.165650311907));
#60118=CARTESIAN_POINT('Ctrl Pts',(46.4002222740367,3.20741015314888,127.073338029117));
#60119=CARTESIAN_POINT('Ctrl Pts',(46.3924742060337,3.10205868934166,126.985301625166));
#60120=CARTESIAN_POINT('Ctrl Pts',(46.3847261380307,2.99327286458827,126.901861338819));
#60121=CARTESIAN_POINT('Ctrl Pts',(46.3769698352889,2.88437142096591,126.818332371143));
#60122=CARTESIAN_POINT('Ctrl Pts',(46.3692135325471,2.77202863568509,126.739409517326));
#60123=CARTESIAN_POINT('Ctrl Pts',(46.3614572298052,2.65667956073602,126.66537079225));
#60124=CARTESIAN_POINT('Ctrl Pts',(46.353696787291,2.5412689205124,126.591292550478));
#60125=CARTESIAN_POINT('Ctrl Pts',(46.3459363447769,2.42284913082927,126.522103828865));
#60126=CARTESIAN_POINT('Ctrl Pts',(46.3381759022627,2.30188023876371,126.458036834311));
#60127=CARTESIAN_POINT('Ctrl Pts',(46.3304030019973,2.18071715669349,126.39386699373));
#60128=CARTESIAN_POINT('Ctrl Pts',(46.3226301017319,2.05699714809038,126.334835478545));
#60129=CARTESIAN_POINT('Ctrl Pts',(46.3148572014664,1.93120146672462,126.281126823319));
#60130=CARTESIAN_POINT('Ctrl Pts',(46.3073668657043,1.80997877523568,126.229370612994));
#60131=CARTESIAN_POINT('Ctrl Pts',(46.2998765299422,1.68682899071688,126.182557092208));
#60132=CARTESIAN_POINT('Ctrl Pts',(46.2923861941801,1.56219453480081,126.140807112144));
#60133=CARTESIAN_POINT('Ctrl Pts',(46.284611860061,1.43283452560796,126.097474168896));
#60134=CARTESIAN_POINT('Ctrl Pts',(46.2768375259419,1.30146526634353,126.059459048579));
#60135=CARTESIAN_POINT('Ctrl Pts',(46.2690631918229,1.16856341009971,126.026951003656));
#60136=CARTESIAN_POINT('Ctrl Pts',(46.2612984388757,1.03582534351575,125.994483021994));
#60137=CARTESIAN_POINT('Ctrl Pts',(46.2535336859287,0.901558814202811,125.967508703664));
#60138=CARTESIAN_POINT('Ctrl Pts',(46.2457689329815,0.76625817816726,125.946168416048));
#60139=CARTESIAN_POINT('Ctrl Pts',(46.2380118920966,0.631091924631192,125.924849323907));
#60140=CARTESIAN_POINT('Ctrl Pts',(46.2302548512116,0.494893992018743,125.909153187106));
#60141=CARTESIAN_POINT('Ctrl Pts',(46.2224978103266,0.358171202844252,125.899169851454));
#60142=CARTESIAN_POINT('Ctrl Pts',(46.2147466190865,0.221551517388626,125.889194044313));
#60143=CARTESIAN_POINT('Ctrl Pts',(46.2069954278463,0.084408151533053,125.88492249173));
#60144=CARTESIAN_POINT('Ctrl Pts',(46.1992442366062,-0.0527449882223296,
125.886393453308));
#60145=CARTESIAN_POINT('Ctrl Pts',(46.1914963398291,-0.189839834234823,
125.887863789688));
#60146=CARTESIAN_POINT('Ctrl Pts',(46.183748443052,-0.326944055760556,125.895071781636));
#60147=CARTESIAN_POINT('Ctrl Pts',(46.1760005462749,-0.463541988921763,
125.908003615977));
#60148=CARTESIAN_POINT('Ctrl Pts',(46.1682542701908,-0.600111348740063,
125.920932745258));
#60149=CARTESIAN_POINT('Ctrl Pts',(46.1605079941067,-0.73617424186564,125.939583298602));
#60150=CARTESIAN_POINT('Ctrl Pts',(46.1527617180226,-0.871218771346769,
125.963889471598));
#60151=CARTESIAN_POINT('Ctrl Pts',(46.1450153847573,-1.00626429769594,125.988195824015));
#60152=CARTESIAN_POINT('Ctrl Pts',(46.1372690514919,-1.14029106061802,126.018157810134));
#60153=CARTESIAN_POINT('Ctrl Pts',(46.1295227182265,-1.27279641277715,126.053658316419));
#60154=CARTESIAN_POINT('Ctrl Pts',(46.1217746502235,-1.40533143859117,126.089166772797));
#60155=CARTESIAN_POINT('Ctrl Pts',(46.1140265822206,-1.53634399809588,126.130216116262));
#60156=CARTESIAN_POINT('Ctrl Pts',(46.1062785142176,-1.66534606967169,126.176639198689));
#60157=CARTESIAN_POINT('Ctrl Pts',(46.0985222114757,-1.79448524618432,126.223111620121));
#60158=CARTESIAN_POINT('Ctrl Pts',(46.0907659087339,-1.92160929788193,126.274969056805));
#60159=CARTESIAN_POINT('Ctrl Pts',(46.083009605992,-2.04624916674153,126.331995761015));
#60160=CARTESIAN_POINT('Ctrl Pts',(46.0752491634778,-2.17095555965215,126.389052902095));
#60161=CARTESIAN_POINT('Ctrl Pts',(46.0674887209636,-2.29317477955967,126.451284630918));
#60162=CARTESIAN_POINT('Ctrl Pts',(46.0597282784495,-2.41246279754036,126.51842941035));
#60163=CARTESIAN_POINT('Ctrl Pts',(46.051955378184,-2.53194230723723,126.585681976544));
#60164=CARTESIAN_POINT('Ctrl Pts',(46.0441824779185,-2.64848087950111,126.657863147832));
#60165=CARTESIAN_POINT('Ctrl Pts',(46.0364095776531,-2.76166313075925,126.734667777227));
#60166=CARTESIAN_POINT('Ctrl Pts',(46.0289192418911,-2.87073092209435,126.808680364884));
#60167=CARTESIAN_POINT('Ctrl Pts',(46.0214289061292,-2.97668192959079,126.886985914913));
#60168=CARTESIAN_POINT('Ctrl Pts',(46.0139385703672,-3.0791753380265,126.969277528481));
#60169=CARTESIAN_POINT('Ctrl Pts',(46.0062662665041,-3.18415869237542,127.053568311263));
#60170=CARTESIAN_POINT('Ctrl Pts',(45.9985939626409,-3.28586538037238,127.142323491893));
#60171=CARTESIAN_POINT('Ctrl Pts',(45.9909216587777,-3.38388442460361,127.235255790943));
#60172=CARTESIAN_POINT('Ctrl Pts',(45.9832581368705,-3.4817912732094,127.328081716813));
#60173=CARTESIAN_POINT('Ctrl Pts',(45.9755946149633,-3.5760185804573,127.425074983214));
#60174=CARTESIAN_POINT('Ctrl Pts',(45.9679310930561,-3.6661863034484,127.525906553391));
#60175=CARTESIAN_POINT('Ctrl Pts',(45.9602745796377,-3.75627156572728,127.626645910491));
#60176=CARTESIAN_POINT('Ctrl Pts',(45.9526180662192,-3.84230435958751,127.731216294445));
#60177=CARTESIAN_POINT('Ctrl Pts',(45.9449615528008,-3.92393997776921,127.839250482451));
#60178=CARTESIAN_POINT('Ctrl Pts',(45.9373102808078,-4.00551971059158,127.947210713407));
#60179=CARTESIAN_POINT('Ctrl Pts',(45.9296590088148,-4.08270801339723,128.058629712873));
#60180=CARTESIAN_POINT('Ctrl Pts',(45.9220077368217,-4.15519949093131,128.1731061158));
#60181=CARTESIAN_POINT('Ctrl Pts',(45.9143590574688,-4.22766640466617,128.287543728299));
#60182=CARTESIAN_POINT('Ctrl Pts',(45.9067103781159,-4.29543943944494,128.405036347591));
#60183=CARTESIAN_POINT('Ctrl Pts',(45.8990616987629,-4.35825592345803,128.52515277971));
#60184=CARTESIAN_POINT('Ctrl Pts',(45.8914147178437,-4.42105845870593,128.645242539278));
#60185=CARTESIAN_POINT('Ctrl Pts',(45.8837677369244,-4.47890644962051,128.767954594915));
#60186=CARTESIAN_POINT('Ctrl Pts',(45.8761207560051,-4.53158303530208,128.892832889108));
#60187=CARTESIAN_POINT('Ctrl Pts',(45.868471240813,-4.58427707844028,129.017752569002));
#60188=CARTESIAN_POINT('Ctrl Pts',(45.8608217256209,-4.63179613443582,129.144839551711));
#60189=CARTESIAN_POINT('Ctrl Pts',(45.8531722104289,-4.67397141950254,129.273617584862));
#60190=CARTESIAN_POINT('Ctrl Pts',(45.847114609155,-4.70736975313983,129.375596070828));
#60191=CARTESIAN_POINT('Ctrl Pts',(45.8410570078811,-4.73741796184024,129.478634551205));
#60192=CARTESIAN_POINT('Ctrl Pts',(45.8349994066072,-4.76405452823404,129.582490119308));
#60193=CARTESIAN_POINT('Ctrl Pts',(47.584673688373,-4.76405452823404,129.582490119308));
#60194=CARTESIAN_POINT('Ctrl Pts',(47.5768386373108,-4.79852007433907,129.716870760484));
#60195=CARTESIAN_POINT('Ctrl Pts',(47.5690035862485,-4.82731639010679,129.852791560815));
#60196=CARTESIAN_POINT('Ctrl Pts',(47.5611685351863,-4.85031727127793,129.989740810268));
#60197=CARTESIAN_POINT('Ctrl Pts',(47.5533359516971,-4.87331090854572,130.126646928889));
#60198=CARTESIAN_POINT('Ctrl Pts',(47.5455033682079,-4.89051267838828,130.264580479608));
#60199=CARTESIAN_POINT('Ctrl Pts',(47.5376707847186,-4.90184743077124,130.40301933145));
#60200=CARTESIAN_POINT('Ctrl Pts',(47.5300670018095,-4.91285107938441,130.537414193253));
#60201=CARTESIAN_POINT('Ctrl Pts',(47.5224632189003,-4.91832566835751,130.67228490252));
#60202=CARTESIAN_POINT('Ctrl Pts',(47.5148594359912,-4.91824920960783,130.80714893102));
#60203=CARTESIAN_POINT('',(47.8601405640491,-4.91824815320621,130.800098460401));
#60204=CARTESIAN_POINT('Ctrl Pts',(47.9299877718525,-4.76405452823408,129.582490119308));
#60205=CARTESIAN_POINT('Ctrl Pts',(47.9205281284413,-4.80532410594932,129.743399576467));
#60206=CARTESIAN_POINT('Ctrl Pts',(47.9110684850301,-4.83847374891171,129.90654298482));
#60207=CARTESIAN_POINT('Ctrl Pts',(47.9016088416188,-4.86329419106527,130.071180780384));
#60208=CARTESIAN_POINT('Ctrl Pts',(47.8922659995719,-4.88780816696217,130.233785738312));
#60209=CARTESIAN_POINT('Ctrl Pts',(47.8829231575249,-4.9041973201447,130.397848411231));
#60210=CARTESIAN_POINT('Ctrl Pts',(47.8735803154779,-4.91230617172183,130.562635282188));
#60211=CARTESIAN_POINT('Ctrl Pts',(47.869100398335,-4.91619438721422,130.641651016846));
#60212=CARTESIAN_POINT('Ctrl Pts',(47.864620481192,-4.91817946166017,130.72083294852));
#60213=CARTESIAN_POINT('Ctrl Pts',(47.8601405640491,-4.91824815320621,130.8000984604));
#60214=CARTESIAN_POINT('Ctrl Pts',(47.8601405640086,-4.91824815320683,130.800098461117));
#60215=CARTESIAN_POINT('Ctrl Pts',(47.8524381977585,-4.91836625524756,130.936380446706));
#60216=CARTESIAN_POINT('Ctrl Pts',(47.8447358315084,-4.91281565009925,131.07276389767));
#60217=CARTESIAN_POINT('Ctrl Pts',(47.8370334652582,-4.90159787939591,131.208738276694));
#60218=CARTESIAN_POINT('Ctrl Pts',(47.82933331255,-4.89038333250777,131.344673578767));
#60219=CARTESIAN_POINT('Ctrl Pts',(47.8216331598417,-4.87350488796626,131.480199648344));
#60220=CARTESIAN_POINT('Ctrl Pts',(47.8139330071335,-4.85101614673146,131.614808275747));
#60221=CARTESIAN_POINT('Ctrl Pts',(47.8062336919552,-4.82852985155125,131.749402262043));
#60222=CARTESIAN_POINT('Ctrl Pts',(47.7985343767769,-4.80043453830914,131.883078614066));
#60223=CARTESIAN_POINT('Ctrl Pts',(47.7908350615986,-4.76683532933868,132.015337085326));
#60224=CARTESIAN_POINT('Ctrl Pts',(47.7831348669977,-4.73323228263685,132.147610663266));
#60225=CARTESIAN_POINT('Ctrl Pts',(47.7754346723968,-4.69412418708643,132.278465654424));
#60226=CARTESIAN_POINT('Ctrl Pts',(47.7677344777959,-4.64966653709696,132.40741525054));
#60227=CARTESIAN_POINT('Ctrl Pts',(47.7600316865266,-4.605193895048,132.536408331186));
#60228=CARTESIAN_POINT('Ctrl Pts',(47.7523288952573,-4.55536823880411,132.663494364407));
#60229=CARTESIAN_POINT('Ctrl Pts',(47.744626103988,-4.50039368934766,132.788205294798));
#60230=CARTESIAN_POINT('Ctrl Pts',(47.7369146038724,-4.44535698516225,132.913057224508));
#60231=CARTESIAN_POINT('Ctrl Pts',(47.7292031037567,-4.38515992568094,133.035528327846));
#60232=CARTESIAN_POINT('Ctrl Pts',(47.7214916036411,-4.32005337966299,133.155173638494));
#60233=CARTESIAN_POINT('Ctrl Pts',(47.7137751213887,-4.25490477053053,133.274896247888));
#60234=CARTESIAN_POINT('Ctrl Pts',(47.7060586391363,-4.18484056161315,133.391789090369));
#60235=CARTESIAN_POINT('Ctrl Pts',(47.698342156884,-4.11015503604208,133.505436077859));
#60236=CARTESIAN_POINT('Ctrl Pts',(47.6906142195231,-4.03535863989877,133.619251774164));
#60237=CARTESIAN_POINT('Ctrl Pts',(47.6828862821622,-3.95592746153042,133.729811675631));
#60238=CARTESIAN_POINT('Ctrl Pts',(47.6751583448013,-3.87219640440636,133.836732307877));
#60239=CARTESIAN_POINT('Ctrl Pts',(47.6717840022293,-3.83563590223619,133.883418354149));
#60240=CARTESIAN_POINT('Ctrl Pts',(47.6684096596573,-3.79825608211373,133.929411020072));
#60241=CARTESIAN_POINT('Ctrl Pts',(47.6650353170852,-3.76008696201467,133.974680648823));
#60242=CARTESIAN_POINT('Ctrl Pts',(47.6572609829662,-3.67214701924133,134.078979845434));
#60243=CARTESIAN_POINT('Ctrl Pts',(47.6494866488471,-3.57972484118302,134.179782487539));
#60244=CARTESIAN_POINT('Ctrl Pts',(47.641712314728,-3.48312907161698,134.276678997691));
#60245=CARTESIAN_POINT('Ctrl Pts',(47.6339475617809,-3.38665234770393,134.373456091554));
#60246=CARTESIAN_POINT('Ctrl Pts',(47.6261828088339,-3.28601253984568,134.466336357582));
#60247=CARTESIAN_POINT('Ctrl Pts',(47.6184180558868,-3.18155884012283,134.554942760292));
#60248=CARTESIAN_POINT('Ctrl Pts',(47.6106610150018,-3.07720888528708,134.643461157874));
#60249=CARTESIAN_POINT('Ctrl Pts',(47.6029039741168,-2.9690528731147,134.727713888331));
#60250=CARTESIAN_POINT('Ctrl Pts',(47.5951469332318,-2.85747692306889,134.807360579673));
#60251=CARTESIAN_POINT('Ctrl Pts',(47.5873957419917,-2.7459851133151,134.886947208826));
#60252=CARTESIAN_POINT('Ctrl Pts',(47.5796445507515,-2.6310788159564,134.961934486326));
#60253=CARTESIAN_POINT('Ctrl Pts',(47.5718933595114,-2.51317703465633,135.032022412811));
#60254=CARTESIAN_POINT('Ctrl Pts',(47.5641454627343,-2.39532536475829,135.102080550058));
#60255=CARTESIAN_POINT('Ctrl Pts',(47.5563975659573,-2.27448107850308,135.167243278573));
#60256=CARTESIAN_POINT('Ctrl Pts',(47.5486496691802,-2.15109176763085,135.227254157968));
#60257=CARTESIAN_POINT('Ctrl Pts',(47.5409033930961,-2.02772826714266,135.287252484381));
#60258=CARTESIAN_POINT('Ctrl Pts',(47.5331571170121,-1.90182115230442,135.342100934302));
#60259=CARTESIAN_POINT('Ctrl Pts',(47.525410840928,-1.77384184244861,135.391589430311));
#60260=CARTESIAN_POINT('Ctrl Pts',(47.5176645076626,-1.64586158787843,135.441078291633));
#60261=CARTESIAN_POINT('Ctrl Pts',(47.5099181743973,-1.51580947241909,135.485206979082));
#60262=CARTESIAN_POINT('Ctrl Pts',(47.5021718411319,-1.38417570563983,135.523814047617));
#60263=CARTESIAN_POINT('Ctrl Pts',(47.494423773129,-1.25251246039118,135.562429761936));
#60264=CARTESIAN_POINT('Ctrl Pts',(47.486675705126,-1.11926723409643,135.595521286781));
#60265=CARTESIAN_POINT('Ctrl Pts',(47.478927637123,-0.984943772082143,135.622977517501));
#60266=CARTESIAN_POINT('Ctrl Pts',(47.4711713343811,-0.850477549493772,
135.650462929029));
#60267=CARTESIAN_POINT('Ctrl Pts',(47.4634150316393,-0.714931185659699,
135.672301003825));
#60268=CARTESIAN_POINT('Ctrl Pts',(47.4556587288974,-0.578817510412338,
135.688432008541));
#60269=CARTESIAN_POINT('Ctrl Pts',(47.4478982863833,-0.442631187198379,
135.70457162286));
#60270=CARTESIAN_POINT('Ctrl Pts',(47.4401378438691,-0.305877338877144,
135.714998067908));
#60271=CARTESIAN_POINT('Ctrl Pts',(47.432377401355,-0.169071237698675,135.719703736727));
#60272=CARTESIAN_POINT('Ctrl Pts',(47.4246045010896,-0.0320455232213341,
135.724416959503));
#60273=CARTESIAN_POINT('Ctrl Pts',(47.4168316008241,0.105032220554808,135.723391057423));
#60274=CARTESIAN_POINT('Ctrl Pts',(47.4090587005587,0.241648501206889,135.71667056955));
#60275=CARTESIAN_POINT('Ctrl Pts',(47.4015683647966,0.373298435942736,135.71019438834));
#60276=CARTESIAN_POINT('Ctrl Pts',(47.3940780290345,0.50451956897092,135.698430485831));
#60277=CARTESIAN_POINT('Ctrl Pts',(47.3865876932724,0.634861182226907,135.681463686172));
#60278=CARTESIAN_POINT('Ctrl Pts',(47.3788133591533,0.770144737364827,135.663853585146));
#60279=CARTESIAN_POINT('Ctrl Pts',(47.3710390250342,0.904909299824789,135.640582479512));
#60280=CARTESIAN_POINT('Ctrl Pts',(47.3632646909151,1.03864345100084,135.611688653408));
#60281=CARTESIAN_POINT('Ctrl Pts',(47.355499937968,1.17221278678756,135.582830436362));
#60282=CARTESIAN_POINT('Ctrl Pts',(47.347735185021,1.30475385951347,135.548363368258));
#60283=CARTESIAN_POINT('Ctrl Pts',(47.3399704320739,1.43576071170107,135.508377437395));
#60284=CARTESIAN_POINT('Ctrl Pts',(47.3322133911889,1.56663744603638,135.468431221123));
#60285=CARTESIAN_POINT('Ctrl Pts',(47.3244563503039,1.69598262076747,135.422977163744));
#60286=CARTESIAN_POINT('Ctrl Pts',(47.3166993094189,1.82330116429928,135.372156139124));
#60287=CARTESIAN_POINT('Ctrl Pts',(47.3089481181787,1.9505236959272,135.321373439034));
#60288=CARTESIAN_POINT('Ctrl Pts',(47.3011969269386,2.07572227670362,135.265231971906));
#60289=CARTESIAN_POINT('Ctrl Pts',(47.2934457356985,2.19841802695287,135.203922100404));
#60290=CARTESIAN_POINT('Ctrl Pts',(47.2856978389214,2.32106162823508,135.142638287233));
#60291=CARTESIAN_POINT('Ctrl Pts',(47.2779499421443,2.441204165746,135.076190613168));
#60292=CARTESIAN_POINT('Ctrl Pts',(47.2702020453672,2.55838795465559,135.004817037525));
#60293=CARTESIAN_POINT('Ctrl Pts',(47.2624557692831,2.67554723124274,134.933458391695));
#60294=CARTESIAN_POINT('Ctrl Pts',(47.254709493199,2.78974865657309,134.857176097037));
#60295=CARTESIAN_POINT('Ctrl Pts',(47.2469632171149,2.90056067289784,134.776253220009));
#60296=CARTESIAN_POINT('Ctrl Pts',(47.2392168838495,3.01137350721171,134.695329745626));
#60297=CARTESIAN_POINT('Ctrl Pts',(47.2314705505842,3.11879656685803,134.609765851093));
#60298=CARTESIAN_POINT('Ctrl Pts',(47.2237242173188,3.22242905330253,134.519886698612));
#60299=CARTESIAN_POINT('Ctrl Pts',(47.2159761493158,3.32608474752369,134.429987418318));
#60300=CARTESIAN_POINT('Ctrl Pts',(47.2082280813129,3.42594788408402,134.335771213219));
#60301=CARTESIAN_POINT('Ctrl Pts',(47.2004800133099,3.52165270084111,134.237601843748));
#60302=CARTESIAN_POINT('Ctrl Pts',(47.1927237105681,3.61745923381635,134.139328138703));
#60303=CARTESIAN_POINT('Ctrl Pts',(47.1849674078262,3.70909834518456,134.037093156789));
#60304=CARTESIAN_POINT('Ctrl Pts',(47.1772111050843,3.79624258253802,133.931296068935));
#60305=CARTESIAN_POINT('Ctrl Pts',(47.1694506625702,3.88343333139493,133.825442513989));
#60306=CARTESIAN_POINT('Ctrl Pts',(47.161690220056,3.96612419032239,133.716023376554));
#60307=CARTESIAN_POINT('Ctrl Pts',(47.1539297775419,4.0440302421331,133.603468058021));
#60308=CARTESIAN_POINT('Ctrl Pts',(47.1461568772764,4.12206135565435,133.490732055699));
#60309=CARTESIAN_POINT('Ctrl Pts',(47.138383977011,4.19529210400014,133.374850142483));
#60310=CARTESIAN_POINT('Ctrl Pts',(47.1306110767455,4.2634824039491,133.256278408544));
#60311=CARTESIAN_POINT('Ctrl Pts',(47.1231207409836,4.32919381473354,133.142017055799));
#60312=CARTESIAN_POINT('Ctrl Pts',(47.1156304052215,4.39022473803754,133.025258323553));
#60313=CARTESIAN_POINT('Ctrl Pts',(47.1081400694596,4.44640291469404,132.906427263203));
#60314=CARTESIAN_POINT('Ctrl Pts',(47.1003657353405,4.50471110399385,132.783090687081));
#60315=CARTESIAN_POINT('Ctrl Pts',(47.0925914012214,4.5579760015696,132.657130842929));
#60316=CARTESIAN_POINT('Ctrl Pts',(47.0848170671023,4.60595338270132,132.528998695217));
#60317=CARTESIAN_POINT('Ctrl Pts',(47.0770523141552,4.65387163599859,132.401024458924));
#60318=CARTESIAN_POINT('Ctrl Pts',(47.0692875612081,4.69651520274848,132.270883608466));
#60319=CARTESIAN_POINT('Ctrl Pts',(47.061522808261,4.73368631028101,132.139050461072));
#60320=CARTESIAN_POINT('Ctrl Pts',(47.053765767376,4.77082049894551,132.007348252218));
#60321=CARTESIAN_POINT('Ctrl Pts',(47.046008726491,4.80249293952037,131.873957465181));
#60322=CARTESIAN_POINT('Ctrl Pts',(47.038251685606,4.82855455488895,131.739370763479));
#60323=CARTESIAN_POINT('Ctrl Pts',(47.0305004943659,4.85459651699055,131.604885554657));
#60324=CARTESIAN_POINT('Ctrl Pts',(47.0227493031258,4.8750360017413,131.469206608528));
#60325=CARTESIAN_POINT('Ctrl Pts',(47.0149981118857,4.8897743204808,131.332839715796));
#60326=CARTESIAN_POINT('Ctrl Pts',(47.0072502151086,4.90450637504174,131.196530782631));
#60327=CARTESIAN_POINT('Ctrl Pts',(46.9995023183315,4.91354204112497,131.059534872303));
#60328=CARTESIAN_POINT('Ctrl Pts',(46.9917544215544,4.91683413081026,130.922365670845));
#60329=CARTESIAN_POINT('Ctrl Pts',(46.9840081454703,4.92012553186136,130.785225162226));
#60330=CARTESIAN_POINT('Ctrl Pts',(46.9762618693862,4.91767573685475,130.647911825182));
#60331=CARTESIAN_POINT('Ctrl Pts',(46.9685155933021,4.90948963011366,130.510941745803));
#60332=CARTESIAN_POINT('Ctrl Pts',(46.9607692600368,4.9013034629446,130.373970655343));
#60333=CARTESIAN_POINT('Ctrl Pts',(46.9530229267714,4.88738092287106,130.237343217874));
#60334=CARTESIAN_POINT('Ctrl Pts',(46.9452765935061,4.86777893666666,130.101572394668));
#60335=CARTESIAN_POINT('Ctrl Pts',(46.9375285255031,4.84817256073334,129.965771166527));
#60336=CARTESIAN_POINT('Ctrl Pts',(46.9297804575001,4.82288426364582,129.830827321253));
#60337=CARTESIAN_POINT('Ctrl Pts',(46.9220323894972,4.79202238398621,129.697245206294));
#60338=CARTESIAN_POINT('Ctrl Pts',(46.9142760867553,4.76112770395369,129.563521118675));
#60339=CARTESIAN_POINT('Ctrl Pts',(46.9065197840135,4.72464769632839,129.431162033973));
#60340=CARTESIAN_POINT('Ctrl Pts',(46.8987634812716,4.68274119889307,129.300659208812));
#60341=CARTESIAN_POINT('Ctrl Pts',(46.8910030387575,4.64081233469817,129.170086730363));
#60342=CARTESIAN_POINT('Ctrl Pts',(46.8832425962433,4.59345134455043,129.041372852326));
#60343=CARTESIAN_POINT('Ctrl Pts',(46.8754821537291,4.54086549130139,128.91498938554));
#60344=CARTESIAN_POINT('Ctrl Pts',(46.8677092534637,4.48819522257243,128.788403036793));
#60345=CARTESIAN_POINT('Ctrl Pts',(46.8599363531982,4.43028349527913,128.664154929541));
#60346=CARTESIAN_POINT('Ctrl Pts',(46.8521634529328,4.36738426015332,128.542693580475));
#60347=CARTESIAN_POINT('Ctrl Pts',(46.8446731171707,4.30677157065743,128.425647657389));
#60348=CARTESIAN_POINT('Ctrl Pts',(46.8371827814086,4.24152784724818,128.311189666356));
#60349=CARTESIAN_POINT('Ctrl Pts',(46.8296924456465,4.17191758741517,128.199694284556));
#60350=CARTESIAN_POINT('Ctrl Pts',(46.8219181115274,4.09966803342372,128.083971521467));
#60351=CARTESIAN_POINT('Ctrl Pts',(46.8141437774084,4.02248542737804,127.971073882093));
#60352=CARTESIAN_POINT('Ctrl Pts',(46.8063694432893,3.94061716903076,127.861450596916));
#60353=CARTESIAN_POINT('Ctrl Pts',(46.7986046903422,3.858849805995,127.751962412642));
#60354=CARTESIAN_POINT('Ctrl Pts',(46.7908399373951,3.77240851217956,127.645740863667));
#60355=CARTESIAN_POINT('Ctrl Pts',(46.7830751844481,3.68158544314398,127.543208721789));
#60356=CARTESIAN_POINT('Ctrl Pts',(46.775318143563,3.59085258086095,127.44077841628));
#60357=CARTESIAN_POINT('Ctrl Pts',(46.767561102678,3.495746861676,127.342030516369));
#60358=CARTESIAN_POINT('Ctrl Pts',(46.759804061793,3.39660219753829,127.247356741524));
#60359=CARTESIAN_POINT('Ctrl Pts',(46.7520528705528,3.2975322991629,127.152754360909));
#60360=CARTESIAN_POINT('Ctrl Pts',(46.7443016793127,3.19442979992645,127.062220258986));
#60361=CARTESIAN_POINT('Ctrl Pts',(46.7365504880726,3.08766689224149,126.976110857551));
#60362=CARTESIAN_POINT('Ctrl Pts',(46.7288025912955,2.98094936164044,126.890038054909));
#60363=CARTESIAN_POINT('Ctrl Pts',(46.7210546945184,2.87057482058224,126.808386457286));
#60364=CARTESIAN_POINT('Ctrl Pts',(46.7133067977413,2.75694994144988,126.731473425065));
#60365=CARTESIAN_POINT('Ctrl Pts',(46.7055605216572,2.64334883019276,126.654576481392));
#60366=CARTESIAN_POINT('Ctrl Pts',(46.6978142455731,2.52649905678103,126.582416350576));
#60367=CARTESIAN_POINT('Ctrl Pts',(46.690067969489,2.40683745915553,126.515267880435));
#60368=CARTESIAN_POINT('Ctrl Pts',(46.6823216362236,2.28717497821513,126.448118914621));
#60369=CARTESIAN_POINT('Ctrl Pts',(46.6745753029583,2.16470097259514,126.385981874628));
#60370=CARTESIAN_POINT('Ctrl Pts',(46.6668289696929,2.03987778145311,126.329086134449));
#60371=CARTESIAN_POINT('Ctrl Pts',(46.6590809016899,1.9150266370234,126.272177652864));
#60372=CARTESIAN_POINT('Ctrl Pts',(46.651332833687,1.78782561590957,126.220512968849));
#60373=CARTESIAN_POINT('Ctrl Pts',(46.643584765684,1.65875759955394,126.174273546201));
#60374=CARTESIAN_POINT('Ctrl Pts',(46.6358284629422,1.52955240817425,126.127984979744));
#60375=CARTESIAN_POINT('Ctrl Pts',(46.6280721602003,1.39847662641538,126.087133324995));
#60376=CARTESIAN_POINT('Ctrl Pts',(46.6203158574584,1.26602941808786,126.051850483433));
#60377=CARTESIAN_POINT('Ctrl Pts',(46.6125554149442,1.13351151869698,126.016548810356));
#60378=CARTESIAN_POINT('Ctrl Pts',(46.60479497243,0.999621115706425,125.98682195761));
#60379=CARTESIAN_POINT('Ctrl Pts',(46.5970345299158,0.864867187571389,125.962750574371));
#60380=CARTESIAN_POINT('Ctrl Pts',(46.5892616296504,0.729896940468386,125.938640549612));
#60381=CARTESIAN_POINT('Ctrl Pts',(46.5814887293849,0.594060785773303,125.920204189031));
#60382=CARTESIAN_POINT('Ctrl Pts',(46.5737158291195,0.457873339854812,125.907470270912));
#60383=CARTESIAN_POINT('Ctrl Pts',(46.5662254933575,0.326636650632228,125.895199262792));
#60384=CARTESIAN_POINT('Ctrl Pts',(46.5587351575956,0.195074074991304,125.88822331515));
#60385=CARTESIAN_POINT('Ctrl Pts',(46.5512448218336,0.0636438068067698,
125.886522420924));
#60386=CARTESIAN_POINT('Ctrl Pts',(46.5434704877146,-0.0727696799445072,
125.884757036775));
#60387=CARTESIAN_POINT('Ctrl Pts',(46.5356961535955,-0.209472745235359,
125.888669017406));
#60388=CARTESIAN_POINT('Ctrl Pts',(46.5279218194764,-0.345953713127084,
125.898293038448));
#60389=CARTESIAN_POINT('Ctrl Pts',(46.5201570665293,-0.482266480423721,
125.907905198744));
#60390=CARTESIAN_POINT('Ctrl Pts',(46.5123923135823,-0.618357308680023,
125.923215365549));
#60391=CARTESIAN_POINT('Ctrl Pts',(46.5046275606352,-0.753712590793564,
125.9442062586));
#60392=CARTESIAN_POINT('Ctrl Pts',(46.4968705197502,-0.88893343613255,125.9651763032));
#60393=CARTESIAN_POINT('Ctrl Pts',(46.4891134788651,-1.02341980531881,125.99181578633));
#60394=CARTESIAN_POINT('Ctrl Pts',(46.4813564379801,-1.15666164610616,126.024055512353));
#60395=CARTESIAN_POINT('Ctrl Pts',(46.47360524674,-1.28980300818526,126.056270926147));
#60396=CARTESIAN_POINT('Ctrl Pts',(46.4658540554999,-1.42170133144778,126.094078085262));
#60397=CARTESIAN_POINT('Ctrl Pts',(46.4581028642597,-1.55185556905271,126.137356508365));
#60398=CARTESIAN_POINT('Ctrl Pts',(46.4503549674827,-1.68195448763432,126.180616536984));
#60399=CARTESIAN_POINT('Ctrl Pts',(46.4426070707056,-1.81031042469731,126.229343081379));
#60400=CARTESIAN_POINT('Ctrl Pts',(46.4348591739285,-1.93643655960838,126.283365537596));
#60401=CARTESIAN_POINT('Ctrl Pts',(46.4271128978444,-2.06253631165116,126.33737669348));
#60402=CARTESIAN_POINT('Ctrl Pts',(46.4193666217602,-2.18640683013136,126.396681403893));
#60403=CARTESIAN_POINT('Ctrl Pts',(46.4116203456761,-2.3075807562174,126.461060706665));
#60404=CARTESIAN_POINT('Ctrl Pts',(46.4038740124107,-2.42875557678216,126.52544048467));
#60405=CARTESIAN_POINT('Ctrl Pts',(46.3961276791454,-2.54723341997167,126.594894746345));
#60406=CARTESIAN_POINT('Ctrl Pts',(46.38838134588,-2.6625714013437,126.669158494907));
#60407=CARTESIAN_POINT('Ctrl Pts',(46.3806332778771,-2.77793521185586,126.743438874319));
#60408=CARTESIAN_POINT('Ctrl Pts',(46.3728852098742,-2.89015743270729,126.822530672212));
#60409=CARTESIAN_POINT('Ctrl Pts',(46.3651371418712,-2.99882438405085,126.906125712366));
#60410=CARTESIAN_POINT('Ctrl Pts',(46.3573808391294,-3.10760682792435,126.989809598324));
#60411=CARTESIAN_POINT('Ctrl Pts',(46.3496245363875,-3.21282614378835,127.078006048528));
#60412=CARTESIAN_POINT('Ctrl Pts',(46.3418682336456,-3.31410154896094,127.170366398298));
#60413=CARTESIAN_POINT('Ctrl Pts',(46.3341077911315,-3.4154310078662,127.262776043567));
#60414=CARTESIAN_POINT('Ctrl Pts',(46.3263473486174,-3.51281208426044,127.359353741548));
#60415=CARTESIAN_POINT('Ctrl Pts',(46.3185869061032,-3.60590181042014,127.4597148671));
#60416=CARTESIAN_POINT('Ctrl Pts',(46.3108140058378,-3.69914097247252,127.560237101241));
#60417=CARTESIAN_POINT('Ctrl Pts',(46.3030411055723,-3.78807476436956,127.664554602038));
#60418=CARTESIAN_POINT('Ctrl Pts',(46.2952682053069,-3.87240081140812,127.772249963532));
#60419=CARTESIAN_POINT('Ctrl Pts',(46.2877778695449,-3.95366139423257,127.876030327368));
#60420=CARTESIAN_POINT('Ctrl Pts',(46.2802875337828,-4.0306432422824,127.982946978204));
#60421=CARTESIAN_POINT('Ctrl Pts',(46.2727971980208,-4.10311552308458,128.092603610251));
#60422=CARTESIAN_POINT('Ctrl Pts',(46.2648734482723,-4.17978127413056,128.208605314075));
#60423=CARTESIAN_POINT('Ctrl Pts',(46.2569496985237,-4.25163626346315,128.328030286094));
#60424=CARTESIAN_POINT('Ctrl Pts',(46.2490259487752,-4.31836681451101,128.450450866146));
#60425=CARTESIAN_POINT('Ctrl Pts',(46.241112019846,-4.38501465867017,128.572719716216));
#60426=CARTESIAN_POINT('Ctrl Pts',(46.2331980909168,-4.44655052719398,128.697976463837));
#60427=CARTESIAN_POINT('Ctrl Pts',(46.2252841619876,-4.50270335582552,128.825763753135));
#60428=CARTESIAN_POINT('Ctrl Pts',(46.2173814468959,-4.55877661731677,128.95336997107));
#60429=CARTESIAN_POINT('Ctrl Pts',(46.2094787318042,-4.60948188764378,129.083499249448));
#60430=CARTESIAN_POINT('Ctrl Pts',(46.2015760167124,-4.65459381296858,129.21566949001));
#60431=CARTESIAN_POINT('Ctrl Pts',(46.1943591483146,-4.69579064525495,129.336369176279));
#60432=CARTESIAN_POINT('Ctrl Pts',(46.1871422799169,-4.73232327563257,129.458770447004));
#60433=CARTESIAN_POINT('Ctrl Pts',(46.1799254115191,-4.76405452823402,129.582490119308));
#60434=CARTESIAN_POINT('Origin',(213.235140564004,0.,130.804360617566));
#60435=CARTESIAN_POINT('',(44.0848860644534,-4.76405452823407,129.582490119308));
#60436=CARTESIAN_POINT('',(44.4302709800425,-4.764054528234,129.582490119308));
#60437=CARTESIAN_POINT('',(213.235140564004,-4.76405452823405,129.582490119308));
#60438=CARTESIAN_POINT('',(45.764859436029,-4.91824911967543,130.807303288442));
#60439=CARTESIAN_POINT('Ctrl Pts',(45.7648594359911,-4.91824911967503,130.807303289108));
#60440=CARTESIAN_POINT('Ctrl Pts',(45.7550699395122,-4.91814616794528,130.979372188753));
#60441=CARTESIAN_POINT('Ctrl Pts',(45.7452804430333,-4.90901394869115,131.15116886393));
#60442=CARTESIAN_POINT('Ctrl Pts',(45.7354909465544,-4.89093350128723,131.322001949461));
#60443=CARTESIAN_POINT('Ctrl Pts',(45.7277166124353,-4.87657490384115,131.457669140146));
#60444=CARTESIAN_POINT('Ctrl Pts',(45.7199422783162,-4.85654447762349,131.592953336111));
#60445=CARTESIAN_POINT('Ctrl Pts',(45.7121679441971,-4.83086822310986,131.727342347313));
#60446=CARTESIAN_POINT('Ctrl Pts',(45.70440319125,-4.80522361228517,131.86156573607));
#60447=CARTESIAN_POINT('Ctrl Pts',(45.6966384383029,-4.77394709013444,131.99489575484));
#60448=CARTESIAN_POINT('Ctrl Pts',(45.6888736853558,-4.7371164774588,132.126824432378));
#60449=CARTESIAN_POINT('Ctrl Pts',(45.6811166444708,-4.70032244546698,132.258622076494));
#60450=CARTESIAN_POINT('Ctrl Pts',(45.6733596035858,-4.65798540528323,132.389020775057));
#60451=CARTESIAN_POINT('Ctrl Pts',(45.6656025627009,-4.6102343098522,132.517522218455));
#60452=CARTESIAN_POINT('Ctrl Pts',(45.6578513714607,-4.56251922389369,132.645926757916));
#60453=CARTESIAN_POINT('Ctrl Pts',(45.6501001802206,-4.50939834484913,132.772436525006));
#60454=CARTESIAN_POINT('Ctrl Pts',(45.6423489889805,-4.45105048877216,132.896568209776));
#60455=CARTESIAN_POINT('Ctrl Pts',(45.6346010922034,-4.39272743209042,133.020647135269));
#60456=CARTESIAN_POINT('Ctrl Pts',(45.6268531954264,-4.3291819829457,133.142349635659));
#60457=CARTESIAN_POINT('Ctrl Pts',(45.6191052986493,-4.26064104895134,133.261212447549));
#60458=CARTESIAN_POINT('Ctrl Pts',(45.6113590225652,-4.19211445224281,133.380050395902));
#60459=CARTESIAN_POINT('Ctrl Pts',(45.6036127464811,-4.11859464432113,133.496049498781));
#60460=CARTESIAN_POINT('Ctrl Pts',(45.595866470397,-4.04035425393199,133.608771529903));
#60461=CARTESIAN_POINT('Ctrl Pts',(45.5881201371317,-3.96211328599007,133.721494393113));
#60462=CARTESIAN_POINT('Ctrl Pts',(45.5803738038664,-3.87915188897781,133.830939815115));
#60463=CARTESIAN_POINT('Ctrl Pts',(45.572627470601,-3.79178551340098,133.936699309799));
#60464=CARTESIAN_POINT('Ctrl Pts',(45.5648794025981,-3.70439957272998,134.042482488589));
#60465=CARTESIAN_POINT('Ctrl Pts',(45.557131334595,-3.612606939495,134.144577796174));
#60466=CARTESIAN_POINT('Ctrl Pts',(45.5493832665921,-3.51676249209189,134.242610846493));
#60467=CARTESIAN_POINT('Ctrl Pts',(45.5416269638502,-3.42081618006964,134.340748087504));
#60468=CARTESIAN_POINT('Ctrl Pts',(45.5338706611084,-3.32080972530035,134.434814166746));
#60469=CARTESIAN_POINT('Ctrl Pts',(45.5261143583666,-3.21713432580663,134.524472147106));
#60470=CARTESIAN_POINT('Ctrl Pts',(45.5183539158524,-3.11340359163046,134.61417798063));
#60471=CARTESIAN_POINT('Ctrl Pts',(45.5105934733382,-3.00600031681478,134.69947078423));
#60472=CARTESIAN_POINT('Ctrl Pts',(45.502833030824,-2.89534694186584,134.780055418318));
#60473=CARTESIAN_POINT('Ctrl Pts',(45.4950601305586,-2.78451593629623,134.860769414015));
#60474=CARTESIAN_POINT('Ctrl Pts',(45.4872872302932,-2.67042473024954,134.93675992011));
#60475=CARTESIAN_POINT('Ctrl Pts',(45.4795143300277,-2.55352352121795,135.007775977614));
#60476=CARTESIAN_POINT('Ctrl Pts',(45.4720239942657,-2.4408719655904,135.076210422549));
#60477=CARTESIAN_POINT('Ctrl Pts',(45.4645336585036,-2.32561143085241,135.14002565809));
#60478=CARTESIAN_POINT('Ctrl Pts',(45.4570433227416,-2.20816271225007,135.199039274616));
#60479=CARTESIAN_POINT('Ctrl Pts',(45.4492689886225,-2.08626088978468,135.260290410348));
#60480=CARTESIAN_POINT('Ctrl Pts',(45.4414946545035,-1.96161552963054,135.3165626579));
#60481=CARTESIAN_POINT('Ctrl Pts',(45.4337203203844,-1.8346716056696,135.367601040977));
#60482=CARTESIAN_POINT('Ctrl Pts',(45.4259555674373,-1.7078841287498,135.418576523808));
#60483=CARTESIAN_POINT('Ctrl Pts',(45.4181908144901,-1.57880408366228,135.464330831838));
#60484=CARTESIAN_POINT('Ctrl Pts',(45.410426061543,-1.4479009050461,135.504654867043));
#60485=CARTESIAN_POINT('Ctrl Pts',(45.402669020658,-1.31712774131233,135.544938851848));
#60486=CARTESIAN_POINT('Ctrl Pts',(45.3949119797731,-1.18453541876935,135.579803182633));
#60487=CARTESIAN_POINT('Ctrl Pts',(45.3871549388881,-1.05061288162221,135.609087002645));
#60488=CARTESIAN_POINT('Ctrl Pts',(45.3794037476479,-0.916791336501912,
135.6383487395));
#60489=CARTESIAN_POINT('Ctrl Pts',(45.3716525564078,-0.781641953832756,
135.662038258783));
#60490=CARTESIAN_POINT('Ctrl Pts',(45.3639013651677,-0.645668010407917,
135.680044762672));
#60491=CARTESIAN_POINT('Ctrl Pts',(45.3561534683906,-0.509751859536257,
135.698043613316));
#60492=CARTESIAN_POINT('Ctrl Pts',(45.3484055716135,-0.373012231717856,
135.710364201459));
#60493=CARTESIAN_POINT('Ctrl Pts',(45.3406576748364,-0.235961532675184,
135.716947025722));
#60494=CARTESIAN_POINT('Ctrl Pts',(45.3329113987523,-0.09893950168428,135.723528473));
#60495=CARTESIAN_POINT('Ctrl Pts',(45.3251651226682,0.0383930808367228,
135.724374524948));
#60496=CARTESIAN_POINT('Ctrl Pts',(45.317418846584,0.175520160206388,135.71947767984));
#60497=CARTESIAN_POINT('Ctrl Pts',(45.3096725133187,0.312648251817003,135.714580798585));
#60498=CARTESIAN_POINT('Ctrl Pts',(45.3019261800533,0.4495704465331,135.703940949635));
#60499=CARTESIAN_POINT('Ctrl Pts',(45.294179846788,0.585772564717304,135.687602733714));
#60500=CARTESIAN_POINT('Ctrl Pts',(45.286431778785,0.72200518442133,135.671260858963));
#60501=CARTESIAN_POINT('Ctrl Pts',(45.278683710782,0.857517018604362,135.649218124486));
#60502=CARTESIAN_POINT('Ctrl Pts',(45.270935642779,0.991801265230155,135.621570734718));
#60503=CARTESIAN_POINT('Ctrl Pts',(45.2631793400371,1.12622823075127,135.593893960975));
#60504=CARTESIAN_POINT('Ctrl Pts',(45.2554230372953,1.25942461890314,135.560600711769));
#60505=CARTESIAN_POINT('Ctrl Pts',(45.2476667345535,1.3908955028648,135.521837990337));
#60506=CARTESIAN_POINT('Ctrl Pts',(45.2399062920393,1.52243655679592,135.483054580074));
#60507=CARTESIAN_POINT('Ctrl Pts',(45.2321458495251,1.65224990159093,135.438796006891));
#60508=CARTESIAN_POINT('Ctrl Pts',(45.2243854070109,1.7798588885437,135.389258151794));
#60509=CARTESIAN_POINT('Ctrl Pts',(45.2166125067455,1.90767272477092,135.339640774134));
#60510=CARTESIAN_POINT('Ctrl Pts',(45.2088396064801,2.03327477341276,135.284727335972));
#60511=CARTESIAN_POINT('Ctrl Pts',(45.2010667062146,2.15621055282234,135.224760951744));
#60512=CARTESIAN_POINT('Ctrl Pts',(45.1935763704526,2.27467730699366,135.166974496628));
#60513=CARTESIAN_POINT('Ctrl Pts',(45.1860860346906,2.39066800641625,135.104496237989));
#60514=CARTESIAN_POINT('Ctrl Pts',(45.1785956989285,2.50380173459983,135.037581605929));
#60515=CARTESIAN_POINT('Ctrl Pts',(45.1708213648095,2.62122496247376,134.968129885255));
#60516=CARTESIAN_POINT('Ctrl Pts',(45.1630470306905,2.73594225984691,134.893678737945));
#60517=CARTESIAN_POINT('Ctrl Pts',(45.1552726965714,2.84749858869034,134.814464712213));
#60518=CARTESIAN_POINT('Ctrl Pts',(45.1475079436243,2.95891743432839,134.735348310689));
#60519=CARTESIAN_POINT('Ctrl Pts',(45.1397431906772,3.06718274682794,134.651480934121));
#60520=CARTESIAN_POINT('Ctrl Pts',(45.1319784377301,3.17186486521209,134.563144508578));
#60521=CARTESIAN_POINT('Ctrl Pts',(45.1242213968451,3.27644301184065,134.474895820019));
#60522=CARTESIAN_POINT('Ctrl Pts',(45.1164643559601,3.37744474982086,134.382187166251));
#60523=CARTESIAN_POINT('Ctrl Pts',(45.1087073150751,3.47447045952549,134.28534296288));
#60524=CARTESIAN_POINT('Ctrl Pts',(45.100956123835,3.57142300138768,134.188571790475));
#60525=CARTESIAN_POINT('Ctrl Pts',(45.0932049325949,3.66440520742259,134.087671551027));
#60526=CARTESIAN_POINT('Ctrl Pts',(45.0854537413547,3.75305182688401,133.983005776627));
#60527=CARTESIAN_POINT('Ctrl Pts',(45.0777058445777,3.84166076916742,133.878384487973));
#60528=CARTESIAN_POINT('Ctrl Pts',(45.0699579478006,3.92593753779637,133.770001145261));
#60529=CARTESIAN_POINT('Ctrl Pts',(45.0622100510235,4.00555510476579,133.658254687987));
#60530=CARTESIAN_POINT('Ctrl Pts',(45.0544637749394,4.08515601745656,133.546531605663));
#60531=CARTESIAN_POINT('Ctrl Pts',(45.0467174988553,4.16009944030952,133.431447126272));
#60532=CARTESIAN_POINT('Ctrl Pts',(45.0389712227712,4.23010012174904,133.313431366365));
#60533=CARTESIAN_POINT('Ctrl Pts',(45.0312248895059,4.30010131991768,133.195414735293));
#60534=CARTESIAN_POINT('Ctrl Pts',(45.0234785562406,4.3651595044144,133.07446711679));
#60535=CARTESIAN_POINT('Ctrl Pts',(45.0157322229752,4.42503427243789,132.951045212529));
#60536=CARTESIAN_POINT('Ctrl Pts',(45.0079841549723,4.48492244900046,132.827595668788));
#60537=CARTESIAN_POINT('Ctrl Pts',(45.0002360869693,4.53962472863854,132.701671088387));
#60538=CARTESIAN_POINT('Ctrl Pts',(44.9924880189664,4.58894811198817,132.573749859079));
#60539=CARTESIAN_POINT('Ctrl Pts',(44.9847317162245,4.63832391681664,132.445692673565));
#60540=CARTESIAN_POINT('Ctrl Pts',(44.9769754134826,4.68230926464487,132.315634965467));
#60541=CARTESIAN_POINT('Ctrl Pts',(44.9692191107408,4.72076031342351,132.184072589575));
#60542=CARTESIAN_POINT('Ctrl Pts',(44.9614586682266,4.75923188468466,132.052439994882));
#60543=CARTESIAN_POINT('Ctrl Pts',(44.9536982257125,4.7921631773269,131.91930151152));
#60544=CARTESIAN_POINT('Ctrl Pts',(44.9459377831983,4.81946135131954,131.785164036013));
#60545=CARTESIAN_POINT('Ctrl Pts',(44.9381648829329,4.84680334676447,131.650811231122));
#60546=CARTESIAN_POINT('Ctrl Pts',(44.9303919826674,4.86849409130069,131.515456615703));
#60547=CARTESIAN_POINT('Ctrl Pts',(44.922619082402,4.88449246555745,131.379613967328));
#60548=CARTESIAN_POINT('Ctrl Pts',(44.9151287466399,4.89990925861265,131.248709541387));
#60549=CARTESIAN_POINT('Ctrl Pts',(44.9076384108779,4.91004033641195,131.117352256024));
#60550=CARTESIAN_POINT('Ctrl Pts',(44.9001480751158,4.91489470486667,130.986000653278));
#60551=CARTESIAN_POINT('Ctrl Pts',(44.8923737409967,4.91993312817675,130.849668814593));
#60552=CARTESIAN_POINT('Ctrl Pts',(44.8845994068775,4.91930277073469,130.712911239658));
#60553=CARTESIAN_POINT('Ctrl Pts',(44.8768250727585,4.9129566880833,130.576238624945));
#60554=CARTESIAN_POINT('Ctrl Pts',(44.8690603198114,4.90661842641161,130.439734447014));
#60555=CARTESIAN_POINT('Ctrl Pts',(44.8612955668643,4.89457847319077,130.303315407765));
#60556=CARTESIAN_POINT('Ctrl Pts',(44.8535308139172,4.87684177855376,130.167495381074));
#60557=CARTESIAN_POINT('Ctrl Pts',(44.8457737730322,4.8591227002519,130.031810252747));
#60558=CARTESIAN_POINT('Ctrl Pts',(44.8380167321472,4.83571819067468,129.896723338171));
#60559=CARTESIAN_POINT('Ctrl Pts',(44.8302596912622,4.8066851856876,129.762746203211));
#60560=CARTESIAN_POINT('Ctrl Pts',(44.8225085000221,4.77767407471542,129.628870101452));
#60561=CARTESIAN_POINT('Ctrl Pts',(44.8147573087819,4.7430429992034,129.496102494075));
#60562=CARTESIAN_POINT('Ctrl Pts',(44.8070061175418,4.70290038204455,129.364947174852));
#60563=CARTESIAN_POINT('Ctrl Pts',(44.7992582207647,4.66277482656883,129.233847600139));
#60564=CARTESIAN_POINT('Ctrl Pts',(44.7915103239876,4.61714250278745,129.104359323703));
#60565=CARTESIAN_POINT('Ctrl Pts',(44.7837624272105,4.56616228317317,128.976973120009));
#60566=CARTESIAN_POINT('Ctrl Pts',(44.7760161511264,4.51519272752183,128.849613562763));
#60567=CARTESIAN_POINT('Ctrl Pts',(44.7682698750424,4.45887764629468,128.724355566403));
#60568=CARTESIAN_POINT('Ctrl Pts',(44.7605235989583,4.39742472328459,128.601671609661));
#60569=CARTESIAN_POINT('Ctrl Pts',(44.7527772656929,4.33597134664297,128.478986747294));
#60570=CARTESIAN_POINT('Ctrl Pts',(44.7450309324275,4.26938022763687,128.358876312022));
#60571=CARTESIAN_POINT('Ctrl Pts',(44.7372845991622,4.19790565873112,128.241789419942));
#60572=CARTESIAN_POINT('Ctrl Pts',(44.7295365311592,4.12641508359124,128.124676307064));
#60573=CARTESIAN_POINT('Ctrl Pts',(44.7217884631562,4.05003908605181,128.010588418369));
#60574=CARTESIAN_POINT('Ctrl Pts',(44.7140403951532,3.96907582640807,127.899946709955));
#60575=CARTESIAN_POINT('Ctrl Pts',(44.7062840924113,3.88802651804852,127.789187410217));
#60576=CARTESIAN_POINT('Ctrl Pts',(44.6985277896695,3.80238043970247,127.681881923296));
#60577=CARTESIAN_POINT('Ctrl Pts',(44.6907714869276,3.71247701790846,127.578419289209));
#60578=CARTESIAN_POINT('Ctrl Pts',(44.6830110444135,3.62252561195119,127.474901433999));
#60579=CARTESIAN_POINT('Ctrl Pts',(44.6752506018993,3.5283126032853,127.375230802491));
#60580=CARTESIAN_POINT('Ctrl Pts',(44.6674901593851,3.4302142760083,127.279759493585));
#60581=CARTESIAN_POINT('Ctrl Pts',(44.6597172591197,3.33195847258772,127.184134925658));
#60582=CARTESIAN_POINT('Ctrl Pts',(44.6519443588542,3.22980517844126,127.092723412112));
#60583=CARTESIAN_POINT('Ctrl Pts',(44.6441714585888,3.1241644231672,127.005837257164));
#60584=CARTESIAN_POINT('Ctrl Pts',(44.6366811228268,3.02236397544136,126.922109632803));
#60585=CARTESIAN_POINT('Ctrl Pts',(44.6291907870649,2.91732546605125,126.842584248806));
#60586=CARTESIAN_POINT('Ctrl Pts',(44.621700451303,2.80943954731722,126.767501381418));
#60587=CARTESIAN_POINT('Ctrl Pts',(44.6139261171839,2.69746310118208,126.689571724292));
#60588=CARTESIAN_POINT('Ctrl Pts',(44.6061517830648,2.58206435661931,126.616181252119));
#60589=CARTESIAN_POINT('Ctrl Pts',(44.5983774489457,2.46364760240628,126.547645504517));
#60590=CARTESIAN_POINT('Ctrl Pts',(44.5906126959987,2.34537678625976,126.479194221099));
#60591=CARTESIAN_POINT('Ctrl Pts',(44.5828479430515,2.22409569614404,126.415585951799));
#60592=CARTESIAN_POINT('Ctrl Pts',(44.5750831901044,2.10023934437156,126.357094293311));
#60593=CARTESIAN_POINT('Ctrl Pts',(44.5673261492194,1.97650600847355,126.298660729563));
#60594=CARTESIAN_POINT('Ctrl Pts',(44.5595691083345,1.85020285226648,126.24533382931));
#60595=CARTESIAN_POINT('Ctrl Pts',(44.5518120674494,1.72179104582964,126.197342204644));
#60596=CARTESIAN_POINT('Ctrl Pts',(44.5440608762093,1.59347607573494,126.149386770836));
#60597=CARTESIAN_POINT('Ctrl Pts',(44.5363096849692,1.46305598524942,126.106758740651));
#60598=CARTESIAN_POINT('Ctrl Pts',(44.5285584937291,1.33101323556341,126.069639207678));
#60599=CARTESIAN_POINT('Ctrl Pts',(44.520810596952,1.19902660756837,126.032535451496));
#60600=CARTESIAN_POINT('Ctrl Pts',(44.5130627001749,1.06541906766878,126.000935641527));
#60601=CARTESIAN_POINT('Ctrl Pts',(44.5053148033978,0.930689392774144,125.974971389446));
#60602=CARTESIAN_POINT('Ctrl Pts',(44.4975685273137,0.795987900423058,125.949012568527));
#60603=CARTESIAN_POINT('Ctrl Pts',(44.4898222512295,0.660165123618893,125.92868703466));
#60604=CARTESIAN_POINT('Ctrl Pts',(44.4820759751454,0.52373083026329,125.914075443884));
#60605=CARTESIAN_POINT('Ctrl Pts',(44.4743296418801,0.387295529780727,125.899463745249));
#60606=CARTESIAN_POINT('Ctrl Pts',(44.4665833086147,0.250249092481418,125.890566115502));
#60607=CARTESIAN_POINT('Ctrl Pts',(44.4588369753494,0.113106823744031,125.887411369412));
#60608=CARTESIAN_POINT('Ctrl Pts',(44.4510889073464,-0.0240661570535617,
125.884255916838));
#60609=CARTESIAN_POINT('Ctrl Pts',(44.4433408393434,-0.161334621206717,
125.886845916057));
#60610=CARTESIAN_POINT('Ctrl Pts',(44.4355927713405,-0.29818324350635,125.895158053423));
#60611=CARTESIAN_POINT('Ctrl Pts',(44.4278364685986,-0.435177310150283,
125.903479025026));
#60612=CARTESIAN_POINT('Ctrl Pts',(44.4200801658567,-0.571750252714067,
125.917534259599));
#60613=CARTESIAN_POINT('Ctrl Pts',(44.4123238631148,-0.707391292478267,
125.937248473612));
#60614=CARTESIAN_POINT('Ctrl Pts',(44.4045634206007,-0.843104727949646,
125.956973209695));
#60615=CARTESIAN_POINT('Ctrl Pts',(44.3968029780865,-0.977884885520969,
125.982362871216));
#60616=CARTESIAN_POINT('Ctrl Pts',(44.3890425355723,-1.11123214366968,126.013291197763));
#60617=CARTESIAN_POINT('Ctrl Pts',(44.3812696353069,-1.24479346267501,126.044269173205));
#60618=CARTESIAN_POINT('Ctrl Pts',(44.3734967350414,-1.37691690864932,126.08080347678));
#60619=CARTESIAN_POINT('Ctrl Pts',(44.365723834776,-1.50711810019504,126.122717947032));
#60620=CARTESIAN_POINT('Ctrl Pts',(44.3582334990139,-1.63258615047159,126.163108720715));
#60621=CARTESIAN_POINT('Ctrl Pts',(44.3507431632519,-1.75626898833957,126.208495180944));
#60622=CARTESIAN_POINT('Ctrl Pts',(44.3432528274898,-1.87775330546755,126.25867853604));
#60623=CARTESIAN_POINT('Ctrl Pts',(44.3354781077651,-2.00384999146667,126.310767191757));
#60624=CARTESIAN_POINT('Ctrl Pts',(44.3277033880404,-2.12797737304117,126.368189193849));
#60625=CARTESIAN_POINT('Ctrl Pts',(44.3199286683157,-2.249651378157,126.430774933113));
#60626=CARTESIAN_POINT('Ctrl Pts',(44.3121636180535,-2.37117405663129,126.493282834142));
#60627=CARTESIAN_POINT('Ctrl Pts',(44.3043985677913,-2.49024908562383,126.560941516447));
#60628=CARTESIAN_POINT('Ctrl Pts',(44.296633517529,-2.60641109361732,126.633532849177));
#60629=CARTESIAN_POINT('Ctrl Pts',(44.2888762672442,-2.72245641710769,126.706051264058));
#60630=CARTESIAN_POINT('Ctrl Pts',(44.2811190169592,-2.83559421356403,126.783492262603));
#60631=CARTESIAN_POINT('Ctrl Pts',(44.2733617666743,-2.94538283824572,126.865591393726));
#60632=CARTESIAN_POINT('Ctrl Pts',(44.2655086124151,-3.05652879510756,126.948705527933));
#60633=CARTESIAN_POINT('Ctrl Pts',(44.2576554581559,-3.16424184388855,127.036593573022));
#60634=CARTESIAN_POINT('Ctrl Pts',(44.2498023038967,-3.26809253596495,127.128934895439));
#60635=CARTESIAN_POINT('Ctrl Pts',(44.242054748587,-3.37054677973221,127.220034532501));
#60636=CARTESIAN_POINT('Ctrl Pts',(44.2343071932773,-3.46924159716566,127.315468153682));
#60637=CARTESIAN_POINT('Ctrl Pts',(44.2265596379676,-3.5637971673641,127.414886792267));
#60638=CARTESIAN_POINT('Ctrl Pts',(44.2188138061074,-3.65833170360465,127.514283315101));
#60639=CARTESIAN_POINT('Ctrl Pts',(44.2110679742472,-3.74872855568951,127.617662808277));
#60640=CARTESIAN_POINT('Ctrl Pts',(44.203322142387,-3.83464489437725,127.724639591803));
#60641=CARTESIAN_POINT('Ctrl Pts',(44.1955763561873,-3.92056072660066,127.831615744716));
#60642=CARTESIAN_POINT('Ctrl Pts',(44.1878305699877,-4.00199585391208,127.942188840526));
#60643=CARTESIAN_POINT('Ctrl Pts',(44.1800847837881,-4.07864812024744,128.055940603503));
#60644=CARTESIAN_POINT('Ctrl Pts',(44.1721515571768,-4.15715529607555,128.172445047321));
#60645=CARTESIAN_POINT('Ctrl Pts',(44.1642183305656,-4.23064491744802,128.292283618335));
#60646=CARTESIAN_POINT('Ctrl Pts',(44.1562851039544,-4.29884027181409,128.414976726282));
#60647=CARTESIAN_POINT('Ctrl Pts',(44.1485309979343,-4.3654958753593,128.53489960427));
#60648=CARTESIAN_POINT('Ctrl Pts',(44.1407768919142,-4.42709360075255,128.657549114743));
#60649=CARTESIAN_POINT('Ctrl Pts',(44.1330227858941,-4.48342265354858,128.782454494091));
#60650=CARTESIAN_POINT('Ctrl Pts',(44.1249999989873,-4.54170351611003,128.911687862763));
#60651=CARTESIAN_POINT('Ctrl Pts',(44.1169772120806,-4.59434381810093,129.04333582851));
#60652=CARTESIAN_POINT('Ctrl Pts',(44.1089544251738,-4.64116551597762,129.176857709489));
#60653=CARTESIAN_POINT('Ctrl Pts',(44.100931638267,-4.68798721385437,129.310379590468));
#60654=CARTESIAN_POINT('Ctrl Pts',(44.0929088513602,-4.72899022487565,129.445774932689));
#60655=CARTESIAN_POINT('Ctrl Pts',(44.0848860644534,-4.76405452823407,129.582490119308));
#60656=CARTESIAN_POINT('Ctrl Pts',(45.8349994066072,-4.76405452823404,129.582490119308));
#60657=CARTESIAN_POINT('Ctrl Pts',(45.8273430242476,-4.79772127647897,129.713756259751));
#60658=CARTESIAN_POINT('Ctrl Pts',(45.819686641888,-4.8259362161401,129.84632770776));
#60659=CARTESIAN_POINT('Ctrl Pts',(45.8120302595285,-4.84862121517186,129.979705917534));
#60660=CARTESIAN_POINT('Ctrl Pts',(45.8041684556119,-4.87191485515217,130.116662678931));
#60661=CARTESIAN_POINT('Ctrl Pts',(45.7963066516953,-4.88937757302127,130.254469649115));
#60662=CARTESIAN_POINT('Ctrl Pts',(45.7884448477787,-4.90098179813617,130.392583400083));
#60663=CARTESIAN_POINT('Ctrl Pts',(45.7805830438621,-4.91258602325106,130.530697151051));
#60664=CARTESIAN_POINT('Ctrl Pts',(45.7727212399455,-4.91833179871113,130.669117228304));
#60665=CARTESIAN_POINT('Ctrl Pts',(45.7648594360289,-4.91824911967543,130.807303288442));
#60666=CARTESIAN_POINT('',(46.1101405639631,-4.91824950622351,130.80656448512));
#60667=CARTESIAN_POINT('Ctrl Pts',(46.1799254115191,-4.76405452823402,129.582490119308));
#60668=CARTESIAN_POINT('Ctrl Pts',(46.1720358594244,-4.79874344822382,129.717741691871));
#60669=CARTESIAN_POINT('Ctrl Pts',(46.1641463073297,-4.82769341870851,129.854568823594));
#60670=CARTESIAN_POINT('Ctrl Pts',(46.1562567552351,-4.85077228469552,129.992454647315));
#60671=CARTESIAN_POINT('Ctrl Pts',(46.1483718873479,-4.87383744823192,130.130258605068));
#60672=CARTESIAN_POINT('Ctrl Pts',(46.1404870194608,-4.89103838901357,130.269119637774));
#60673=CARTESIAN_POINT('Ctrl Pts',(46.1326021515737,-4.90229388879109,130.408510026532));
#60674=CARTESIAN_POINT('Ctrl Pts',(46.1251149557187,-4.91298171926418,130.540870283659));
#60675=CARTESIAN_POINT('Ctrl Pts',(46.1176277598636,-4.91830903941853,130.673707492938));
#60676=CARTESIAN_POINT('Ctrl Pts',(46.1101405640086,-4.91824950622387,130.806564484312));
#60677=CARTESIAN_POINT('Ctrl Pts',(46.1101405639631,-4.91824950622351,130.80656448512));
#60678=CARTESIAN_POINT('Ctrl Pts',(46.1016750146247,-4.9181821937889,130.956781927965));
#60679=CARTESIAN_POINT('Ctrl Pts',(46.0932094652862,-4.91122864733905,131.106774266232));
#60680=CARTESIAN_POINT('Ctrl Pts',(46.0847439159477,-4.89747532373009,131.255933995828));
#60681=CARTESIAN_POINT('Ctrl Pts',(46.0762382420686,-4.88365681288149,131.405800704428));
#60682=CARTESIAN_POINT('Ctrl Pts',(46.0677325681894,-4.86297399945099,131.554826638305));
#60683=CARTESIAN_POINT('Ctrl Pts',(46.0592268943102,-4.83556502632671,131.702410693378));
#60684=CARTESIAN_POINT('Ctrl Pts',(46.0507006717052,-4.80808983628866,131.850351294485));
#60685=CARTESIAN_POINT('Ctrl Pts',(46.0421744491002,-4.77385606786064,131.9968428017));
#60686=CARTESIAN_POINT('Ctrl Pts',(46.0336482264952,-4.73305186516659,132.141298575791));
#60687=CARTESIAN_POINT('Ctrl Pts',(46.0250926202755,-4.69210704041427,132.286252182629));
#60688=CARTESIAN_POINT('Ctrl Pts',(46.0165370140557,-4.64454654209171,132.429155766391));
#60689=CARTESIAN_POINT('Ctrl Pts',(46.007981407836,-4.59060790677837,132.569439116875));
#60690=CARTESIAN_POINT('Ctrl Pts',(46.0034374632933,-4.56196070618539,132.643944622212));
#60691=CARTESIAN_POINT('Ctrl Pts',(45.9988935187506,-4.53151518136126,132.717711426559));
#60692=CARTESIAN_POINT('Ctrl Pts',(45.9943495742079,-4.49931213559914,132.790657012606));
#60693=CARTESIAN_POINT('Ctrl Pts',(45.9865752400889,-4.4442152401473,132.915461211496));
#60694=CARTESIAN_POINT('Ctrl Pts',(45.9788009059698,-4.38383431666588,133.038168895575));
#60695=CARTESIAN_POINT('Ctrl Pts',(45.9710265718507,-4.31835051372151,133.158300273365));
#60696=CARTESIAN_POINT('Ctrl Pts',(45.9632618189036,-4.25294741371182,133.278283599968));
#60697=CARTESIAN_POINT('Ctrl Pts',(45.9554970659565,-4.18245413248686,133.395696597737));
#60698=CARTESIAN_POINT('Ctrl Pts',(45.9477323130094,-4.10709987610411,133.510079315104));
#60699=CARTESIAN_POINT('Ctrl Pts',(45.9399752721244,-4.03182046263121,133.624348425943));
#60700=CARTESIAN_POINT('Ctrl Pts',(45.9322182312394,-3.95168989560982,133.735592921479));
#60701=CARTESIAN_POINT('Ctrl Pts',(45.9244611903544,-3.86698312138009,133.843377662839));
#60702=CARTESIAN_POINT('Ctrl Pts',(45.9167099991143,-3.78234022518784,133.951081122887));
#60703=CARTESIAN_POINT('Ctrl Pts',(45.9089588078741,-3.69312823130316,134.055329715716));
#60704=CARTESIAN_POINT('Ctrl Pts',(45.901207616634,-3.5996649880285,134.155717810773));
#60705=CARTESIAN_POINT('Ctrl Pts',(45.8934597198569,-3.5062414691252,134.256063238213));
#60706=CARTESIAN_POINT('Ctrl Pts',(45.8857118230799,-3.40857056045793,134.352551145788));
#60707=CARTESIAN_POINT('Ctrl Pts',(45.8779639263028,-3.30700978434805,134.44480967623));
#60708=CARTESIAN_POINT('Ctrl Pts',(45.8702176502187,-3.20547025256313,134.537048908176));
#60709=CARTESIAN_POINT('Ctrl Pts',(45.8624713741346,-3.10004276098854,134.625060259979));
#60710=CARTESIAN_POINT('Ctrl Pts',(45.8547250980504,-2.99112072494369,134.708509676108));
#60711=CARTESIAN_POINT('Ctrl Pts',(45.8469787647851,-2.88219788486127,134.791959708242));
#60712=CARTESIAN_POINT('Ctrl Pts',(45.8392324315197,-2.76978075918621,134.870847499733));
#60713=CARTESIAN_POINT('Ctrl Pts',(45.8314860982544,-2.65429445931159,134.944880389982));
#60714=CARTESIAN_POINT('Ctrl Pts',(45.8237380302514,-2.53878229708083,135.018929859383));
#60715=CARTESIAN_POINT('Ctrl Pts',(45.8159899622484,-2.420199922041,135.088122053139));
#60716=CARTESIAN_POINT('Ctrl Pts',(45.8082418942454,-2.29899957863895,135.152208820979));
#60717=CARTESIAN_POINT('Ctrl Pts',(45.8004855915036,-2.17767042206963,135.216363700997));
#60718=CARTESIAN_POINT('Ctrl Pts',(45.7927292887618,-2.05371808515203,135.27540213282));
#60719=CARTESIAN_POINT('Ctrl Pts',(45.7849729860199,-1.92761796302219,135.32912271641));
#60720=CARTESIAN_POINT('Ctrl Pts',(45.7772125435057,-1.80145053746019,135.382871972293));
#60721=CARTESIAN_POINT('Ctrl Pts',(45.7694521009916,-1.67313340811606,135.431297586424));
#60722=CARTESIAN_POINT('Ctrl Pts',(45.7616916584774,-1.54315895835751,135.47424749968));
#60723=CARTESIAN_POINT('Ctrl Pts',(45.753918758212,-1.41297586207361,135.51726635995));
#60724=CARTESIAN_POINT('Ctrl Pts',(45.7461458579465,-1.28113050514035,135.554791846875));
#60725=CARTESIAN_POINT('Ctrl Pts',(45.7383729576811,-1.14812821247293,135.586722447271));
#60726=CARTESIAN_POINT('Ctrl Pts',(45.7308826219191,-1.01996088815652,135.617492289915));
#60727=CARTESIAN_POINT('Ctrl Pts',(45.723392286157,-0.890719584960743,135.643066900438));
#60728=CARTESIAN_POINT('Ctrl Pts',(45.715901950395,-0.760860699114758,135.663401063893));
#60729=CARTESIAN_POINT('Ctrl Pts',(45.7081276162759,-0.626078174142351,
135.684506203336));
#60730=CARTESIAN_POINT('Ctrl Pts',(45.7003532821568,-0.490203360237131,
135.700032522881));
#60731=CARTESIAN_POINT('Ctrl Pts',(45.6925789480377,-0.353737834783081,
135.709873088934));
#60732=CARTESIAN_POINT('Ctrl Pts',(45.6848141950907,-0.217440490892878,
135.719701527368));
#60733=CARTESIAN_POINT('Ctrl Pts',(45.6770494421436,-0.0805542701644052,
135.723858126666));
#60734=CARTESIAN_POINT('Ctrl Pts',(45.6692846891965,0.0564099656475737,
135.722287109318));
#60735=CARTESIAN_POINT('Ctrl Pts',(45.6615276483115,0.193238166649687,135.720717652326));
#60736=CARTESIAN_POINT('Ctrl Pts',(45.6537706074265,0.330143840125569,135.713431904011));
#60737=CARTESIAN_POINT('Ctrl Pts',(45.6460135665415,0.466612276203251,135.700425981325));
#60738=CARTESIAN_POINT('Ctrl Pts',(45.6382623753014,0.602977800371718,135.687429866506));
#60739=CARTESIAN_POINT('Ctrl Pts',(45.6305111840612,0.738906355810972,135.668722200273));
#60740=CARTESIAN_POINT('Ctrl Pts',(45.6227599928211,0.873884869278215,135.644351144183));
#60741=CARTESIAN_POINT('Ctrl Pts',(45.615012096044,1.00880601327656,135.619990446443));
#60742=CARTESIAN_POINT('Ctrl Pts',(45.607264199267,1.14277753447811,135.58997121569));
#60743=CARTESIAN_POINT('Ctrl Pts',(45.5995163024899,1.27529332928342,135.554393247642));
#60744=CARTESIAN_POINT('Ctrl Pts',(45.5917700264058,1.40778140464117,135.518822721738));
#60745=CARTESIAN_POINT('Ctrl Pts',(45.5840237503217,1.53881398192906,135.47769587266));
#60746=CARTESIAN_POINT('Ctrl Pts',(45.5762774742376,1.66789736017958,135.431163126687));
#60747=CARTESIAN_POINT('Ctrl Pts',(45.5685311409723,1.79698169129427,135.384630037219));
#60748=CARTESIAN_POINT('Ctrl Pts',(45.5607848077069,1.92411642686306,135.332691103813));
#60749=CARTESIAN_POINT('Ctrl Pts',(45.5530384744416,2.0488255601416,135.27554579452));
#60750=CARTESIAN_POINT('Ctrl Pts',(45.5452904064386,2.17356262116587,135.218387687931));
#60751=CARTESIAN_POINT('Ctrl Pts',(45.5375423384356,2.29587264364235,135.156021048221));
#60752=CARTESIAN_POINT('Ctrl Pts',(45.5297942704326,2.41530240254885,135.088692230168));
#60753=CARTESIAN_POINT('Ctrl Pts',(45.5220379676907,2.53485909282436,135.021291854246));
#60754=CARTESIAN_POINT('Ctrl Pts',(45.5142816649489,2.65152906337995,134.948918957179));
#60755=CARTESIAN_POINT('Ctrl Pts',(45.5065253622071,2.7648859079783,134.871864640719));
#60756=CARTESIAN_POINT('Ctrl Pts',(45.4987649196929,2.87830325453789,134.79476919805));
#60757=CARTESIAN_POINT('Ctrl Pts',(45.4910044771787,2.98840363792147,134.712987590302));
#60758=CARTESIAN_POINT('Ctrl Pts',(45.4832440346646,3.09479298124552,134.626851881877));
#60759=CARTESIAN_POINT('Ctrl Pts',(45.4754711343992,3.20135311018812,134.540577900766));
#60760=CARTESIAN_POINT('Ctrl Pts',(45.4676982341337,3.30419000103959,134.449936110218));
#60761=CARTESIAN_POINT('Ctrl Pts',(45.4599253338683,3.40294510742288,134.355296784039));
#60762=CARTESIAN_POINT('Ctrl Pts',(45.4524349981062,3.49811021694071,134.264097835748));
#60763=CARTESIAN_POINT('Ctrl Pts',(45.4449446623442,3.58948494235635,134.169187168747));
#60764=CARTESIAN_POINT('Ctrl Pts',(45.4374543265821,3.6767845497445,134.070924322327));
#60765=CARTESIAN_POINT('Ctrl Pts',(45.429679992463,3.76739414828029,133.968935810219));
#60766=CARTESIAN_POINT('Ctrl Pts',(45.421905658344,3.85390053648416,133.863012836071));
#60767=CARTESIAN_POINT('Ctrl Pts',(45.4141313242249,3.93594263326725,133.753519590923));
#60768=CARTESIAN_POINT('Ctrl Pts',(45.4063665712778,4.01788362049837,133.644161286413));
#60769=CARTESIAN_POINT('Ctrl Pts',(45.3986018183307,4.09537103114464,133.531241775546));
#60770=CARTESIAN_POINT('Ctrl Pts',(45.3908370653836,4.16808180474964,133.415160711678));
#60771=CARTESIAN_POINT('Ctrl Pts',(45.3830800244986,4.24072036098926,133.299194941159));
#60772=CARTESIAN_POINT('Ctrl Pts',(45.3753229836136,4.30859151520928,133.180074195765));
#60773=CARTESIAN_POINT('Ctrl Pts',(45.3675659427286,4.37141378723327,133.058229416606));
#60774=CARTESIAN_POINT('Ctrl Pts',(45.3598147514885,4.43418868449323,132.936476521544));
#60775=CARTESIAN_POINT('Ctrl Pts',(45.3520635602483,4.49192209951736,132.812004027597));
#60776=CARTESIAN_POINT('Ctrl Pts',(45.3443123690082,4.54437722336763,132.685269630314));
#60777=CARTESIAN_POINT('Ctrl Pts',(45.3365644722311,4.59681005239105,132.558589098531));
#60778=CARTESIAN_POINT('Ctrl Pts',(45.328816575454,4.64396890301551,132.429648935991));
#60779=CARTESIAN_POINT('Ctrl Pts',(45.321068678677,4.68566417484683,132.298928884009));
#60780=CARTESIAN_POINT('Ctrl Pts',(45.3133224025929,4.72735072492607,132.168236175843));
#60781=CARTESIAN_POINT('Ctrl Pts',(45.3055761265088,4.76357585069709,132.03576469103));
#60782=CARTESIAN_POINT('Ctrl Pts',(45.2978298504247,4.79419925261481,131.902011103252));
#60783=CARTESIAN_POINT('Ctrl Pts',(45.2900835171593,4.82482288058756,131.768256528136));
#60784=CARTESIAN_POINT('Ctrl Pts',(45.282337183894,4.84984461493951,131.633220212274));
#60785=CARTESIAN_POINT('Ctrl Pts',(45.2745908506286,4.86917498051886,131.497410450976));
#60786=CARTESIAN_POINT('Ctrl Pts',(45.2668427826256,4.88850967499952,131.361570276023));
#60787=CARTESIAN_POINT('Ctrl Pts',(45.2590947146227,4.90215040943353,131.224956697961));
#60788=CARTESIAN_POINT('Ctrl Pts',(45.2513466466197,4.91005946987748,131.088084188611));
#60789=CARTESIAN_POINT('Ctrl Pts',(45.2435903438778,4.91797693616498,130.951066209529));
#60790=CARTESIAN_POINT('Ctrl Pts',(45.235834041136,4.92015053706289,130.813789140364));
#60791=CARTESIAN_POINT('Ctrl Pts',(45.2280777383941,4.91659470173358,130.676769076368));
#60792=CARTESIAN_POINT('Ctrl Pts',(45.22031729588,4.91303696854789,130.539675880638));
#60793=CARTESIAN_POINT('Ctrl Pts',(45.2125568533658,4.90374373234417,130.402840353278));
#60794=CARTESIAN_POINT('Ctrl Pts',(45.2047964108516,4.88878136012727,130.266773531251));
#60795=CARTESIAN_POINT('Ctrl Pts',(45.1970235105862,4.87379496898219,130.130488282683));
#60796=CARTESIAN_POINT('Ctrl Pts',(45.1892506103208,4.85312131492092,129.994974592077));
#60797=CARTESIAN_POINT('Ctrl Pts',(45.1814777100554,4.82687811670912,129.860734256693));
#60798=CARTESIAN_POINT('Ctrl Pts',(45.1739873742933,4.80158892485491,129.731373895631));
#60799=CARTESIAN_POINT('Ctrl Pts',(45.1664970385313,4.77112816373635,129.603196217437));
#60800=CARTESIAN_POINT('Ctrl Pts',(45.1590067027693,4.73564441829933,129.476635116594));
#60801=CARTESIAN_POINT('Ctrl Pts',(45.1512323686502,4.69881529586907,129.345275413147));
#60802=CARTESIAN_POINT('Ctrl Pts',(45.1434580345311,4.65645811368422,129.215241183923));
#60803=CARTESIAN_POINT('Ctrl Pts',(45.135683700412,4.6086841028319,129.087033070822));
#60804=CARTESIAN_POINT('Ctrl Pts',(45.1279189474649,4.56096896917827,128.958982962763));
#60805=CARTESIAN_POINT('Ctrl Pts',(45.1201541945178,4.50785042482883,128.832754855793));
#60806=CARTESIAN_POINT('Ctrl Pts',(45.1123894415707,4.44949008740258,128.708836572224));
#60807=CARTESIAN_POINT('Ctrl Pts',(45.1046324006857,4.39118771428619,128.585041366042));
#60808=CARTESIAN_POINT('Ctrl Pts',(45.0968753598006,4.3276540742123,128.463551769214));
#60809=CARTESIAN_POINT('Ctrl Pts',(45.0891183189156,4.25909958323108,128.344837533181));
#60810=CARTESIAN_POINT('Ctrl Pts',(45.0813671276755,4.19059678972479,128.226212820478));
#60811=CARTESIAN_POINT('Ctrl Pts',(45.0736159364354,4.11708087636066,128.110359639935));
#60812=CARTESIAN_POINT('Ctrl Pts',(45.0658647451952,4.03880891435073,127.997724621242));
#60813=CARTESIAN_POINT('Ctrl Pts',(45.0581168484181,3.96057022001263,127.885137475437));
#60814=CARTESIAN_POINT('Ctrl Pts',(45.0503689516411,3.8775797201739,127.775766091407));
#60815=CARTESIAN_POINT('Ctrl Pts',(45.042621054864,3.79013855114537,127.670029297233));
#60816=CARTESIAN_POINT('Ctrl Pts',(45.0348747787799,3.70271567292438,127.564314620916));
#60817=CARTESIAN_POINT('Ctrl Pts',(45.0271285026958,3.61084422629065,127.462233323319));
#60818=CARTESIAN_POINT('Ctrl Pts',(45.0193822266117,3.51486624154943,127.364171906679));
#60819=CARTESIAN_POINT('Ctrl Pts',(45.0116358933464,3.41888754832052,127.266109766172));
#60820=CARTESIAN_POINT('Ctrl Pts',(45.0038895600809,3.31880252996573,127.17206784524));
#60821=CARTESIAN_POINT('Ctrl Pts',(44.9961432268156,3.21499046621918,127.082396167894));
#60822=CARTESIAN_POINT('Ctrl Pts',(44.9883951588126,3.11115515448074,126.992704409198));
#60823=CARTESIAN_POINT('Ctrl Pts',(44.9806470908096,3.00359143231425,126.907385097078));
#60824=CARTESIAN_POINT('Ctrl Pts',(44.9728990228066,2.89271175412661,126.82674804593));
#60825=CARTESIAN_POINT('Ctrl Pts',(44.9651427200648,2.78171423169752,126.746025292764));
#60826=CARTESIAN_POINT('Ctrl Pts',(44.957386417323,2.66739402989875,126.669994971707));
#60827=CARTESIAN_POINT('Ctrl Pts',(44.9496301145811,2.55019315359706,126.598923905184));
#60828=CARTESIAN_POINT('Ctrl Pts',(44.9418696720669,2.43292972365869,126.527814905894));
#60829=CARTESIAN_POINT('Ctrl Pts',(44.9341092295527,2.31278289793891,126.461670623779));
#60830=CARTESIAN_POINT('Ctrl Pts',(44.9263487870385,2.19021849929572,126.400711450359));
#60831=CARTESIAN_POINT('Ctrl Pts',(44.9185758867731,2.06745734939925,126.339654419863));
#60832=CARTESIAN_POINT('Ctrl Pts',(44.9108029865077,1.94227122854329,126.283799290654));
#60833=CARTESIAN_POINT('Ctrl Pts',(44.9030300862423,1.81514594284144,126.233318256278));
#60834=CARTESIAN_POINT('Ctrl Pts',(44.8955397504803,1.69264198148515,126.184672334656));
#60835=CARTESIAN_POINT('Ctrl Pts',(44.8880494147183,1.56833768521108,126.141016669702));
#60836=CARTESIAN_POINT('Ctrl Pts',(44.8805590789563,1.4426784155298,126.102460783258));
#60837=CARTESIAN_POINT('Ctrl Pts',(44.8727847448373,1.31225473644414,126.062443038661));
#60838=CARTESIAN_POINT('Ctrl Pts',(44.8650104107182,1.17995816503496,126.027792658493));
#60839=CARTESIAN_POINT('Ctrl Pts',(44.8572360765991,1.04627002863025,125.998686670065));
#60840=CARTESIAN_POINT('Ctrl Pts',(44.849471323652,0.912746650905595,125.969616552167));
#60841=CARTESIAN_POINT('Ctrl Pts',(44.8417065707049,0.777835498832337,125.946077312813));
#60842=CARTESIAN_POINT('Ctrl Pts',(44.8339418177578,0.642034349408489,125.928196658399));
#60843=CARTESIAN_POINT('Ctrl Pts',(44.8261847768728,0.50636807960071,125.910333763303));
#60844=CARTESIAN_POINT('Ctrl Pts',(44.8184277359879,0.369813956669882,125.89811831943));
#60845=CARTESIAN_POINT('Ctrl Pts',(44.8106706951029,0.232880930822069,125.891627209924));
#60846=CARTESIAN_POINT('Ctrl Pts',(44.8029195038627,0.0960511672342309,
125.885140995415));
#60847=CARTESIAN_POINT('Ctrl Pts',(44.7951683126226,-0.0411565415886018,
125.884370541452));
#60848=CARTESIAN_POINT('Ctrl Pts',(44.7874171213825,-0.178227480169567,
125.889340981002));
#60849=CARTESIAN_POINT('Ctrl Pts',(44.7796692246054,-0.315240159945149,
125.894309307982));
#60850=CARTESIAN_POINT('Ctrl Pts',(44.7719213278283,-0.452115795206562,
125.905013661296));
#60851=CARTESIAN_POINT('Ctrl Pts',(44.7641734310512,-0.588339242496301,
125.921427073247));
#60852=CARTESIAN_POINT('Ctrl Pts',(44.7564271549671,-0.724534194777504,
125.937837051865));
#60853=CARTESIAN_POINT('Ctrl Pts',(44.748680878883,-0.860076842529294,125.959953667027));
#60854=CARTESIAN_POINT('Ctrl Pts',(44.7409346027989,-0.994457134737505,
125.98769807285));
#60855=CARTESIAN_POINT('Ctrl Pts',(44.7331882695336,-1.12883841891032,126.015442683476));
#60856=CARTESIAN_POINT('Ctrl Pts',(44.7254419362682,-1.26205694752857,126.048815088608));
#60857=CARTESIAN_POINT('Ctrl Pts',(44.7176956030029,-1.39361322551899,126.08768538599));
#60858=CARTESIAN_POINT('Ctrl Pts',(44.7099475349999,-1.52519896462572,126.126564388106));
#60859=CARTESIAN_POINT('Ctrl Pts',(44.7021994669969,-1.6551213375015,126.170943621687));
#60860=CARTESIAN_POINT('Ctrl Pts',(44.6944513989939,-1.78289674683951,126.220643539407));
#60861=CARTESIAN_POINT('Ctrl Pts',(44.6866950962521,-1.91080795740329,126.27039627879));
#60862=CARTESIAN_POINT('Ctrl Pts',(44.6789387935102,-2.03656728129799,126.325480856605));
#60863=CARTESIAN_POINT('Ctrl Pts',(44.6711824907684,-2.15971131883188,126.385669625676));
#60864=CARTESIAN_POINT('Ctrl Pts',(44.6634220482542,-2.28292108204657,126.445890519306));
#60865=CARTESIAN_POINT('Ctrl Pts',(44.65566160574,-2.40351243394462,126.511220846371));
#60866=CARTESIAN_POINT('Ctrl Pts',(44.6479011632258,-2.52104816426468,126.58138782391));
#60867=CARTESIAN_POINT('Ctrl Pts',(44.6401282629604,-2.63877257337322,126.65166743971));
#60868=CARTESIAN_POINT('Ctrl Pts',(44.632355362695,-2.75343123163921,126.726799006967));
#60869=CARTESIAN_POINT('Ctrl Pts',(44.6245824624296,-2.86461667768654,126.806466878055));
#60870=CARTESIAN_POINT('Ctrl Pts',(44.6170921266675,-2.97176025271142,126.883238621358));
#60871=CARTESIAN_POINT('Ctrl Pts',(44.6096017909054,-3.07567850846933,126.964222393039));
#60872=CARTESIAN_POINT('Ctrl Pts',(44.6021114551433,-3.1760385723561,127.049102697076));
#60873=CARTESIAN_POINT('Ctrl Pts',(44.5944493708478,-3.27869982731611,127.135929251348));
#60874=CARTESIAN_POINT('Ctrl Pts',(44.5867872865522,-3.37798281463037,127.227125378155));
#60875=CARTESIAN_POINT('Ctrl Pts',(44.5791252022567,-3.47348456891262,127.322394504574));
#60876=CARTESIAN_POINT('Ctrl Pts',(44.5714719163122,-3.56887665878399,127.417554233707));
#60877=CARTESIAN_POINT('Ctrl Pts',(44.5638186303677,-3.6604958645176,127.516777384094));
#60878=CARTESIAN_POINT('Ctrl Pts',(44.5561653444232,-3.74797117485307,127.619726394461));
#60879=CARTESIAN_POINT('Ctrl Pts',(44.5485190763818,-3.83536627215974,127.72258100274));
#60880=CARTESIAN_POINT('Ctrl Pts',(44.5408728083403,-3.91862477014325,127.829154373051));
#60881=CARTESIAN_POINT('Ctrl Pts',(44.5332265402989,-3.99741193415087,127.93907164589));
#60882=CARTESIAN_POINT('Ctrl Pts',(44.5255855163638,-4.07614506287385,128.048913533211));
#60883=CARTESIAN_POINT('Ctrl Pts',(44.5179444924288,-4.15041272296012,128.162094435488));
#60884=CARTESIAN_POINT('Ctrl Pts',(44.5103034684937,-4.21992033996254,128.278206349341));
#60885=CARTESIAN_POINT('Ctrl Pts',(44.5026652587937,-4.28940235689147,128.394275498478));
#60886=CARTESIAN_POINT('Ctrl Pts',(44.4950270490937,-4.35412760826144,128.51327316857));
#60887=CARTESIAN_POINT('Ctrl Pts',(44.4873888393937,-4.41384501075719,128.634762663217));
#60888=CARTESIAN_POINT('Ctrl Pts',(44.47975229993,-4.47354935493497,128.756225591933));
#60889=CARTESIAN_POINT('Ctrl Pts',(44.4721157604663,-4.52824785426733,128.880178898073));
#60890=CARTESIAN_POINT('Ctrl Pts',(44.4644792210026,-4.57773585379053,129.006162209319));
#60891=CARTESIAN_POINT('Ctrl Pts',(44.4568408472416,-4.62723574033409,129.132175781765));
#60892=CARTESIAN_POINT('Ctrl Pts',(44.4492024734807,-4.67152248030369,129.260219957805));
#60893=CARTESIAN_POINT('Ctrl Pts',(44.4415640997197,-4.71044003946876,129.389815568064));
#60894=CARTESIAN_POINT('Ctrl Pts',(44.4377997264939,-4.72961954315858,129.453683383479));
#60895=CARTESIAN_POINT('Ctrl Pts',(44.4340353532682,-4.74749576595898,129.517927756512));
#60896=CARTESIAN_POINT('Ctrl Pts',(44.4302709800425,-4.764054528234,129.582490119308));
#60897=CARTESIAN_POINT('Origin',(213.235140564004,0.,130.804360617566));
#60898=CARTESIAN_POINT('',(42.3345736784939,-4.76405452823401,129.582490119308));
#60899=CARTESIAN_POINT('',(42.6801909902419,-4.76405452823402,129.582490119308));
#60900=CARTESIAN_POINT('',(213.235140564004,-4.76405452823405,129.582490119308));
#60901=CARTESIAN_POINT('',(44.0148594359472,-4.91824820103065,130.800154008622));
#60902=CARTESIAN_POINT('Ctrl Pts',(44.0148594359472,-4.91824820103065,130.800154008622));
#60903=CARTESIAN_POINT('Ctrl Pts',(44.0072128060144,-4.9183634320627,130.934878872191));
#60904=CARTESIAN_POINT('Ctrl Pts',(43.9995661760815,-4.91293875693969,131.06979677328));
#60905=CARTESIAN_POINT('Ctrl Pts',(43.9919195461486,-4.90195330182934,131.204406726389));
#60906=CARTESIAN_POINT('Ctrl Pts',(43.9842798532381,-4.89097781272339,131.338894561355));
#60907=CARTESIAN_POINT('Ctrl Pts',(43.9766401603276,-4.87445161028033,131.473074604134));
#60908=CARTESIAN_POINT('Ctrl Pts',(43.9690004674171,-4.85240587338236,131.606445589663));
#60909=CARTESIAN_POINT('Ctrl Pts',(43.9613654289013,-4.83037356759492,131.73973532046));
#60910=CARTESIAN_POINT('Ctrl Pts',(43.9537303903854,-4.80282848067744,131.872216577364));
#60911=CARTESIAN_POINT('Ctrl Pts',(43.9460953518696,-4.7698536067849,132.003393407919));
#60912=CARTESIAN_POINT('Ctrl Pts',(43.9384627361299,-4.73688919659057,132.134528612999));
#60913=CARTESIAN_POINT('Ctrl Pts',(43.9308301203903,-4.69849852268592,132.264359823546));
#60914=CARTESIAN_POINT('Ctrl Pts',(43.9231975046506,-4.65481555042062,132.392401943874));
#60915=CARTESIAN_POINT('Ctrl Pts',(43.9155655441217,-4.61113632805664,132.520433072612));
#60916=CARTESIAN_POINT('Ctrl Pts',(43.9079335835928,-4.56216584101016,132.646675034525));
#60917=CARTESIAN_POINT('Ctrl Pts',(43.900301623064,-4.50808754941105,132.770659096776));
#60918=CARTESIAN_POINT('Ctrl Pts',(43.8926685509213,-4.454001381176,132.894661217611));
#60919=CARTESIAN_POINT('Ctrl Pts',(43.8850354787787,-4.39480609090367,133.016404415087));
#60920=CARTESIAN_POINT('Ctrl Pts',(43.877402406636,-4.33073254764309,133.135441625014));
#60921=CARTESIAN_POINT('Ctrl Pts',(43.8697617828695,-4.26659561453228,133.254596601972));
#60922=CARTESIAN_POINT('Ctrl Pts',(43.862121159103,-4.19757098066915,133.371039888361));
#60923=CARTESIAN_POINT('Ctrl Pts',(43.8544805353364,-4.1239347749985,133.484350362706));
#60924=CARTESIAN_POINT('Ctrl Pts',(43.8468361622809,-4.05026243570526,133.59771643902));
#60925=CARTESIAN_POINT('Ctrl Pts',(43.8391917892253,-3.97197425240201,133.707946313502));
#60926=CARTESIAN_POINT('Ctrl Pts',(43.8315474161698,-3.88938786305494,133.814650489525));
#60927=CARTESIAN_POINT('Ctrl Pts',(43.8238909228139,-3.80667053140055,133.921523847071));
#60928=CARTESIAN_POINT('Ctrl Pts',(43.816234429458,-3.7196416392557,134.024860029935));
#60929=CARTESIAN_POINT('Ctrl Pts',(43.8085779361021,-3.62865750495909,134.124304558991));
#60930=CARTESIAN_POINT('Ctrl Pts',(43.8011711506894,-3.5406407161542,134.220505816269));
#60931=CARTESIAN_POINT('Ctrl Pts',(43.7937643652767,-3.4489229241383,134.313065116144));
#60932=CARTESIAN_POINT('Ctrl Pts',(43.786357579864,-3.35385570630374,134.401697822193));
#60933=CARTESIAN_POINT('Ctrl Pts',(43.7785832457449,-3.25407094489395,134.494728770481));
#60934=CARTESIAN_POINT('Ctrl Pts',(43.7708089116258,-3.15025438873821,134.5837521063));
#60935=CARTESIAN_POINT('Ctrl Pts',(43.7630345775067,-3.042761459047,134.668398112964));
#60936=CARTESIAN_POINT('Ctrl Pts',(43.7552698245596,-2.93540100478456,134.752939800989));
#60937=CARTESIAN_POINT('Ctrl Pts',(43.7475050716126,-2.82437349614604,134.833114654083));
#60938=CARTESIAN_POINT('Ctrl Pts',(43.7397403186655,-2.71007071883661,134.908590114244));
#60939=CARTESIAN_POINT('Ctrl Pts',(43.7319832777805,-2.5958814686573,134.983990611114));
#60940=CARTESIAN_POINT('Ctrl Pts',(43.7242262368954,-2.4784237476548,135.054700789556));
#60941=CARTESIAN_POINT('Ctrl Pts',(43.7164691960105,-2.358121618091,135.120428909054));
#60942=CARTESIAN_POINT('Ctrl Pts',(43.7087180047703,-2.23791020929892,135.186107462467));
#60943=CARTESIAN_POINT('Ctrl Pts',(43.7009668135302,-2.11485900312718,135.24681124834));
#60944=CARTESIAN_POINT('Ctrl Pts',(43.6932156222901,-1.98941988055753,135.3022925425));
#60945=CARTESIAN_POINT('Ctrl Pts',(43.685467725513,-1.86403407296118,135.35775025563));
#60946=CARTESIAN_POINT('Ctrl Pts',(43.677719828736,-1.73626272438607,135.407989734045));
#60947=CARTESIAN_POINT('Ctrl Pts',(43.6699719319589,-1.60658088810668,135.452809919481));
#60948=CARTESIAN_POINT('Ctrl Pts',(43.6622256558748,-1.47692617847183,135.4976207295));
#60949=CARTESIAN_POINT('Ctrl Pts',(43.6544793797907,-1.34536214530822,135.537014373701));
#60950=CARTESIAN_POINT('Ctrl Pts',(43.6467331037066,-1.21238195246728,135.570838674143));
#60951=CARTESIAN_POINT('Ctrl Pts',(43.6389867704412,-1.07940077799659,135.604663224269));
#60952=CARTESIAN_POINT('Ctrl Pts',(43.6312404371759,-0.945003801889273,
135.632918252224));
#60953=CARTESIAN_POINT('Ctrl Pts',(43.6234941039106,-0.809697025921017,
135.655502110938));
#60954=CARTESIAN_POINT('Ctrl Pts',(43.6157460359076,-0.674359948938434,
135.678091027151));
#60955=CARTESIAN_POINT('Ctrl Pts',(43.6079979679046,-0.538113052225963,
135.695006182579));
#60956=CARTESIAN_POINT('Ctrl Pts',(43.6002498999016,-0.401469754419894,
135.706197528234));
#60957=CARTESIAN_POINT('Ctrl Pts',(43.5924935971597,-0.264681230490841,
135.717400768185));
#60958=CARTESIAN_POINT('Ctrl Pts',(43.5847372944179,-0.127495854158278,
135.722868014285));
#60959=CARTESIAN_POINT('Ctrl Pts',(43.5769809916761,0.00957008168842241,
135.722601306678));
#60960=CARTESIAN_POINT('Ctrl Pts',(43.5692205491619,0.14670917375206,135.722334456722));
#60961=CARTESIAN_POINT('Ctrl Pts',(43.5614601066477,0.283728307905655,135.7163275721));
#60962=CARTESIAN_POINT('Ctrl Pts',(43.5536996641336,0.420115001726524,135.704634737228));
#60963=CARTESIAN_POINT('Ctrl Pts',(43.5459267638681,0.556720635576155,135.692923131979));
#60964=CARTESIAN_POINT('Ctrl Pts',(43.5381538636027,0.692691412281017,135.675507386341));
#60965=CARTESIAN_POINT('Ctrl Pts',(43.5303809633373,0.82752285416191,135.65249314343));
#60966=CARTESIAN_POINT('Ctrl Pts',(43.5228906275753,0.957452833509977,135.630315526218));
#60967=CARTESIAN_POINT('Ctrl Pts',(43.5154002918133,1.08632457397627,135.602939447898));
#60968=CARTESIAN_POINT('Ctrl Pts',(43.5079099560513,1.21370074039864,135.570503038356));
#60969=CARTESIAN_POINT('Ctrl Pts',(43.5001356219322,1.34590641288663,135.536836792488));
#60970=CARTESIAN_POINT('Ctrl Pts',(43.4923612878131,1.47691965104582,135.497612271082));
#60971=CARTESIAN_POINT('Ctrl Pts',(43.484586953694,1.60623728791046,135.45292865917));
#60972=CARTESIAN_POINT('Ctrl Pts',(43.4768222007469,1.73539555234493,135.408300115817));
#60973=CARTESIAN_POINT('Ctrl Pts',(43.4690574477999,1.86286200733933,135.358225994814));
#60974=CARTESIAN_POINT('Ctrl Pts',(43.4612926948528,1.98814509268487,135.302856160849));
#60975=CARTESIAN_POINT('Ctrl Pts',(43.4535356539678,2.11330374510369,135.247541320983));
#60976=CARTESIAN_POINT('Ctrl Pts',(43.4457786130828,2.23628298810924,135.186941392368));
#60977=CARTESIAN_POINT('Ctrl Pts',(43.4380215721978,2.35660815613244,135.12125545772));
#60978=CARTESIAN_POINT('Ctrl Pts',(43.4302703809576,2.47684258601109,135.055619057346));
#60979=CARTESIAN_POINT('Ctrl Pts',(43.4225191897175,2.594426582916,134.98490447164));
#60980=CARTESIAN_POINT('Ctrl Pts',(43.4147679984773,2.70890747677517,134.9093579799));
#60981=CARTESIAN_POINT('Ctrl Pts',(43.4070201017003,2.8233397132001,134.833843597436));
#60982=CARTESIAN_POINT('Ctrl Pts',(43.3992722049232,2.93467114413965,134.753501608457));
#60983=CARTESIAN_POINT('Ctrl Pts',(43.3915243081461,3.04247583568445,134.668623011837));
#60984=CARTESIAN_POINT('Ctrl Pts',(43.383778032062,3.15025797681178,134.583762169989));
#60985=CARTESIAN_POINT('Ctrl Pts',(43.3760317559779,3.25451453891941,134.494366849736));
#60986=CARTESIAN_POINT('Ctrl Pts',(43.3682854798938,3.35485092328759,134.400769707897));
#60987=CARTESIAN_POINT('Ctrl Pts',(43.3605391466285,3.45518804831616,134.307171875146));
#60988=CARTESIAN_POINT('Ctrl Pts',(43.3527928133631,3.55160465197346,134.209372425604));
#60989=CARTESIAN_POINT('Ctrl Pts',(43.3450464800978,3.64374170938024,134.107742130171));
#60990=CARTESIAN_POINT('Ctrl Pts',(43.3372984120948,3.73589940024208,134.006089075339));
#60991=CARTESIAN_POINT('Ctrl Pts',(43.3295503440918,3.82377537525408,133.900603757107));
#60992=CARTESIAN_POINT('Ctrl Pts',(43.3218022760889,3.9070500114714,133.791691076414));
#60993=CARTESIAN_POINT('Ctrl Pts',(43.314045973347,3.99041315296318,133.682662642028));
#60994=CARTESIAN_POINT('Ctrl Pts',(43.3062896706052,4.06916494879436,133.57019987969));
#60995=CARTESIAN_POINT('Ctrl Pts',(43.2985333678633,4.14302804647811,133.454738263977));
#60996=CARTESIAN_POINT('Ctrl Pts',(43.2907729253492,4.21693056712117,133.339215022923));
#60997=CARTESIAN_POINT('Ctrl Pts',(43.283012482835,4.28593899385358,133.220690076912));
#60998=CARTESIAN_POINT('Ctrl Pts',(43.2752520403209,4.3498218201577,133.099623825867));
#60999=CARTESIAN_POINT('Ctrl Pts',(43.2674791400554,4.41380719684576,132.978363228528));
#61000=CARTESIAN_POINT('Ctrl Pts',(43.25970623979,4.47265036288119,132.854553527274));
#61001=CARTESIAN_POINT('Ctrl Pts',(43.2519333395246,4.52616751630043,132.728676256147));
#61002=CARTESIAN_POINT('Ctrl Pts',(43.2444430037625,4.57773918639153,132.607374940891));
#61003=CARTESIAN_POINT('Ctrl Pts',(43.2369526680005,4.62436523995985,132.484154056768));
#61004=CARTESIAN_POINT('Ctrl Pts',(43.2294623322385,4.66592549925278,132.359456208815));
#61005=CARTESIAN_POINT('Ctrl Pts',(43.2216879981194,4.70906152840864,132.230030404056));
#61006=CARTESIAN_POINT('Ctrl Pts',(43.2139136640003,4.74687668305547,132.098603444373));
#61007=CARTESIAN_POINT('Ctrl Pts',(43.2061393298812,4.77918243633268,131.965652270317));
#61008=CARTESIAN_POINT('Ctrl Pts',(43.1983745769341,4.81144837565618,131.832864946701));
#61009=CARTESIAN_POINT('Ctrl Pts',(43.1906098239869,4.8382183319494,131.698557522546));
#61010=CARTESIAN_POINT('Ctrl Pts',(43.1828450710398,4.85935269031777,131.563224566902));
#61011=CARTESIAN_POINT('Ctrl Pts',(43.1750880301548,4.88046605774353,131.428026025856));
#61012=CARTESIAN_POINT('Ctrl Pts',(43.1673309892699,4.89595490630023,131.29180436411));
#61013=CARTESIAN_POINT('Ctrl Pts',(43.1595739483849,4.90573016158091,131.155066540321));
#61014=CARTESIAN_POINT('Ctrl Pts',(43.1518227571447,4.91549804526556,131.018431831588));
#61015=CARTESIAN_POINT('Ctrl Pts',(43.1440715659045,4.91956088404505,130.881282123965));
#61016=CARTESIAN_POINT('Ctrl Pts',(43.1363203746644,4.91788120043917,130.744131381584));
#61017=CARTESIAN_POINT('Ctrl Pts',(43.1285724778873,4.91620223074363,130.607038931927));
#61018=CARTESIAN_POINT('Ctrl Pts',(43.1208245811102,4.90878559785686,130.469945838502));
#61019=CARTESIAN_POINT('Ctrl Pts',(43.1130766843331,4.8956458996893,130.33336774357));
#61020=CARTESIAN_POINT('Ctrl Pts',(43.105330408249,4.88250895006333,130.19681821783));
#61021=CARTESIAN_POINT('Ctrl Pts',(43.0975841321649,4.86365135375417,130.060783865231));
#61022=CARTESIAN_POINT('Ctrl Pts',(43.0898378560808,4.83913969412001,129.925776481986));
#61023=CARTESIAN_POINT('Ctrl Pts',(43.0820915228155,4.81462785354638,129.790768102149));
#61024=CARTESIAN_POINT('Ctrl Pts',(43.0743451895501,4.78446193620564,129.65678709147));
#61025=CARTESIAN_POINT('Ctrl Pts',(43.0665988562847,4.74875982043973,129.524335918477));
#61026=CARTESIAN_POINT('Ctrl Pts',(43.0588507882818,4.71304970943258,129.391855083963));
#61027=CARTESIAN_POINT('Ctrl Pts',(43.0511027202788,4.67180103468843,129.260905146282));
#61028=CARTESIAN_POINT('Ctrl Pts',(43.0433546522759,4.62518168682574,129.131973872117));
#61029=CARTESIAN_POINT('Ctrl Pts',(43.035598349534,4.57851279136523,129.00290556826));
#61030=CARTESIAN_POINT('Ctrl Pts',(43.0278420467921,4.52646195356534,128.875860581961));
#61031=CARTESIAN_POINT('Ctrl Pts',(43.0200857440503,4.46924563472774,128.751307642369));
#61032=CARTESIAN_POINT('Ctrl Pts',(43.0123253015361,4.41199877781795,128.626688225122));
#61033=CARTESIAN_POINT('Ctrl Pts',(43.0045648590219,4.34958112421101,128.50456385284));
#61034=CARTESIAN_POINT('Ctrl Pts',(42.9968044165078,4.28225488647429,128.385378155917));
#61035=CARTESIAN_POINT('Ctrl Pts',(42.9890315162423,4.2148205706839,128.266001131532));
#61036=CARTESIAN_POINT('Ctrl Pts',(42.9812586159769,4.14246213111183,128.149572541674));
#61037=CARTESIAN_POINT('Ctrl Pts',(42.9734857157114,4.06548534653542,128.03650730505));
#61038=CARTESIAN_POINT('Ctrl Pts',(42.9659953799494,3.9913068619716,127.927552274573));
#61039=CARTESIAN_POINT('Ctrl Pts',(42.9585050441875,3.91284016322174,127.821720557482));
#61040=CARTESIAN_POINT('Ctrl Pts',(42.9510147084255,3.83039266742636,127.719352501559));
#61041=CARTESIAN_POINT('Ctrl Pts',(42.9432403743064,3.74481914976805,127.613103129681));
#61042=CARTESIAN_POINT('Ctrl Pts',(42.9354660401873,3.65468594115511,127.510248687106));
#61043=CARTESIAN_POINT('Ctrl Pts',(42.9276917060682,3.56029240180694,127.411205584837));
#61044=CARTESIAN_POINT('Ctrl Pts',(42.9199269531211,3.46601519405995,127.31228454434));
#61045=CARTESIAN_POINT('Ctrl Pts',(42.9121622001741,3.3674883696036,127.217165778549));
#61046=CARTESIAN_POINT('Ctrl Pts',(42.904397447227,3.2650525581251,127.12623407608));
#61047=CARTESIAN_POINT('Ctrl Pts',(42.896640406342,3.16271848733865,127.035392688261));
#61048=CARTESIAN_POINT('Ctrl Pts',(42.888883365457,3.05648344629503,126.94873034573));
#61049=CARTESIAN_POINT('Ctrl Pts',(42.881126324572,2.94672580677788,126.866596012848));
#61050=CARTESIAN_POINT('Ctrl Pts',(42.8733751333318,2.83705093635018,126.784523618105));
#61051=CARTESIAN_POINT('Ctrl Pts',(42.8656239420917,2.72385906664683,126.706972669736));
#61052=CARTESIAN_POINT('Ctrl Pts',(42.8578727508515,2.60756235275282,126.634252508775));
#61053=CARTESIAN_POINT('Ctrl Pts',(42.8501248540745,2.49131506806484,126.561563255822));
#61054=CARTESIAN_POINT('Ctrl Pts',(42.8423769572974,2.3719658946521,126.493700913438));
#61055=CARTESIAN_POINT('Ctrl Pts',(42.8346290605203,2.24995654747828,126.430931917226));
#61056=CARTESIAN_POINT('Ctrl Pts',(42.8268827844362,2.12797272202968,126.368176050934));
#61057=CARTESIAN_POINT('Ctrl Pts',(42.8191365083521,2.00333017706715,126.31051159038));
#61058=CARTESIAN_POINT('Ctrl Pts',(42.811390232268,1.87649549117341,126.258159155454));
#61059=CARTESIAN_POINT('Ctrl Pts',(42.8036438990026,1.74965986901465,126.205806334075));
#61060=CARTESIAN_POINT('Ctrl Pts',(42.7958975657373,1.62063243502493,126.158765765737));
#61061=CARTESIAN_POINT('Ctrl Pts',(42.7881512324719,1.48989964632975,126.117209872565));
#61062=CARTESIAN_POINT('Ctrl Pts',(42.780403164469,1.35913758093299,126.075644673238));
#61063=CARTESIAN_POINT('Ctrl Pts',(42.772655096466,1.22666977341246,126.039566711577));
#61064=CARTESIAN_POINT('Ctrl Pts',(42.764907028463,1.09299734467351,126.009098386255));
#61065=CARTESIAN_POINT('Ctrl Pts',(42.7571507257212,0.959182847286747,125.978597678834));
#61066=CARTESIAN_POINT('Ctrl Pts',(42.7493944229793,0.824161552969223,125.953718604491));
#61067=CARTESIAN_POINT('Ctrl Pts',(42.7416381202374,0.688444819449609,125.934532407755));
#61068=CARTESIAN_POINT('Ctrl Pts',(42.7338776777233,0.55265564982278,125.915335970768));
#61069=CARTESIAN_POINT('Ctrl Pts',(42.7261172352091,0.41617069026953,125.901838504235));
#61070=CARTESIAN_POINT('Ctrl Pts',(42.7183567926949,0.279504911902632,125.894059194362));
#61071=CARTESIAN_POINT('Ctrl Pts',(42.7105838924295,0.142619745495867,125.88626739645));
#61072=CARTESIAN_POINT('Ctrl Pts',(42.7028109921641,0.00555357137691959,
125.884212104214));
#61073=CARTESIAN_POINT('Ctrl Pts',(42.6950380918987,-0.131179246694201,
125.887860331007));
#61074=CARTESIAN_POINT('Ctrl Pts',(42.6875477561367,-0.262941482419246,
125.891375935567));
#61075=CARTESIAN_POINT('Ctrl Pts',(42.6800574203747,-0.394393870647627,
125.900187563347));
#61076=CARTESIAN_POINT('Ctrl Pts',(42.6725670846126,-0.52508390067963,125.914220541889));
#61077=CARTESIAN_POINT('Ctrl Pts',(42.6647927504936,-0.660729082922493,
125.928785585077));
#61078=CARTESIAN_POINT('Ctrl Pts',(42.6570184163745,-0.795982639331584,
125.949021867617));
#61079=CARTESIAN_POINT('Ctrl Pts',(42.6492440822554,-0.930332420024554,
125.974902609595));
#61080=CARTESIAN_POINT('Ctrl Pts',(42.6414793293083,-1.06451662662055,126.000751455873));
#61081=CARTESIAN_POINT('Ctrl Pts',(42.6337145763613,-1.19779889345439,126.032230847398));
#61082=CARTESIAN_POINT('Ctrl Pts',(42.6259498234141,-1.32967136829897,126.069262190413));
#61083=CARTESIAN_POINT('Ctrl Pts',(42.6181927825291,-1.46141286554227,126.106256753377));
#61084=CARTESIAN_POINT('Ctrl Pts',(42.6104357416441,-1.59174698333753,126.148792189156));
#61085=CARTESIAN_POINT('Ctrl Pts',(42.6026787007591,-1.72017560889519,126.196738786614));
#61086=CARTESIAN_POINT('Ctrl Pts',(42.594927509519,-1.84850738542694,126.24464922717));
#61087=CARTESIAN_POINT('Ctrl Pts',(42.5871763182789,-1.97493616508553,126.297962571032));
#61088=CARTESIAN_POINT('Ctrl Pts',(42.5794251270387,-2.09897891060893,126.356499266836));
#61089=CARTESIAN_POINT('Ctrl Pts',(42.5716772302617,-2.22296893465688,126.415011082983));
#61090=CARTESIAN_POINT('Ctrl Pts',(42.5639293334846,-2.34457458876074,126.478741669032));
#61091=CARTESIAN_POINT('Ctrl Pts',(42.5561814367075,-2.46333295537625,126.547463412622));
#61092=CARTESIAN_POINT('Ctrl Pts',(42.5484351606234,-2.58206648030144,126.616170781106));
#61093=CARTESIAN_POINT('Ctrl Pts',(42.5406888845393,-2.69795356422367,126.689867034781));
#61094=CARTESIAN_POINT('Ctrl Pts',(42.5329426084552,-2.81055639625962,126.768278878311));
#61095=CARTESIAN_POINT('Ctrl Pts',(42.5251962751899,-2.92316005950409,126.846691300661));
#61096=CARTESIAN_POINT('Ctrl Pts',(42.5174499419245,-3.03247910164669,126.929819158906));
#61097=CARTESIAN_POINT('Ctrl Pts',(42.5097036086592,-3.13810551711191,127.017346381262));
#61098=CARTESIAN_POINT('Ctrl Pts',(42.5019555406562,-3.24375558688036,127.104893204732));
#61099=CARTESIAN_POINT('Ctrl Pts',(42.4942074726533,-3.34571108347773,127.19684110335));
#61100=CARTESIAN_POINT('Ctrl Pts',(42.4864594046503,-3.44359816134269,127.292834629381));
#61101=CARTESIAN_POINT('Ctrl Pts',(42.4787031019085,-3.54158927475915,127.388930178474));
#61102=CARTESIAN_POINT('Ctrl Pts',(42.4709467991666,-3.63550305227369,127.489079669997));
#61103=CARTESIAN_POINT('Ctrl Pts',(42.4631904964247,-3.72500315250208,127.59289139362));
#61104=CARTESIAN_POINT('Ctrl Pts',(42.4554300539105,-3.81455102162901,127.696758524686));
#61105=CARTESIAN_POINT('Ctrl Pts',(42.4476696113964,-3.89968027696046,127.804291476259));
#61106=CARTESIAN_POINT('Ctrl Pts',(42.4399091688822,-3.98009642213317,127.915067359168));
#61107=CARTESIAN_POINT('Ctrl Pts',(42.4321362686167,-4.06064165844091,128.026021069359));
#61108=CARTESIAN_POINT('Ctrl Pts',(42.4243633683513,-4.13645844914655,128.140227787904));
#61109=CARTESIAN_POINT('Ctrl Pts',(42.4165904680858,-4.20729652067481,128.257236935917));
#61110=CARTESIAN_POINT('Ctrl Pts',(42.4091001323238,-4.27555944987259,128.369992506671));
#61111=CARTESIAN_POINT('Ctrl Pts',(42.4016097965618,-4.33919920460351,128.485350023863));
#61112=CARTESIAN_POINT('Ctrl Pts',(42.3941194607998,-4.39803401583533,128.60288841514));
#61113=CARTESIAN_POINT('Ctrl Pts',(42.3857998701641,-4.46338242745931,128.733439478599));
#61114=CARTESIAN_POINT('Ctrl Pts',(42.3774802795283,-4.52298784870698,128.867049546495));
#61115=CARTESIAN_POINT('Ctrl Pts',(42.3691606888926,-4.57657376185162,129.003206636133));
#61116=CARTESIAN_POINT('Ctrl Pts',(42.3608614078734,-4.63002886214853,129.139031341837));
#61117=CARTESIAN_POINT('Ctrl Pts',(42.3525621268542,-4.6774936438987,129.277390386455));
#61118=CARTESIAN_POINT('Ctrl Pts',(42.3442628458349,-4.71873845908369,129.417749490658));
#61119=CARTESIAN_POINT('Ctrl Pts',(42.3410331233879,-4.73478916336948,129.472371204085));
#61120=CARTESIAN_POINT('Ctrl Pts',(42.3378034009409,-4.74989839087753,129.527295554605));
#61121=CARTESIAN_POINT('Ctrl Pts',(42.3345736784939,-4.76405452823401,129.582490119308));
#61122=CARTESIAN_POINT('Ctrl Pts',(44.0848860644534,-4.76405452823407,129.582490119308));
#61123=CARTESIAN_POINT('Ctrl Pts',(44.0781924441946,-4.79330959060179,129.696555163473));
#61124=CARTESIAN_POINT('Ctrl Pts',(44.0714988239357,-4.81843174048182,129.811538591869));
#61125=CARTESIAN_POINT('Ctrl Pts',(44.0648052036769,-4.8393826038738,129.92711545467));
#61126=CARTESIAN_POINT('Ctrl Pts',(44.0529708853409,-4.87642372320972,130.131455308709));
#61127=CARTESIAN_POINT('Ctrl Pts',(44.0411365670048,-4.90053067147628,130.338205890149));
#61128=CARTESIAN_POINT('Ctrl Pts',(44.0293022486687,-4.91146188999161,130.546048469845));
#61129=CARTESIAN_POINT('Ctrl Pts',(44.0244879777762,-4.91590877452044,130.630600064051));
#61130=CARTESIAN_POINT('Ctrl Pts',(44.0196737068837,-4.91817565227183,130.715332067349));
#61131=CARTESIAN_POINT('Ctrl Pts',(44.0148594359912,-4.91824820102998,130.800154007847));
#61132=CARTESIAN_POINT('',(44.3601405640442,-4.91824877153122,130.807836798172));
#61133=CARTESIAN_POINT('Ctrl Pts',(44.4302709800425,-4.764054528234,129.582490119308));
#61134=CARTESIAN_POINT('Ctrl Pts',(44.4226263315709,-4.79768188373925,129.713602668057));
#61135=CARTESIAN_POINT('Ctrl Pts',(44.4149816830993,-4.82587262023684,129.846027035517));
#61136=CARTESIAN_POINT('Ctrl Pts',(44.4073370346278,-4.84854638452371,129.979266065638));
#61137=CARTESIAN_POINT('Ctrl Pts',(44.3994709561972,-4.87187690244891,130.116364411604));
#61138=CARTESIAN_POINT('Ctrl Pts',(44.3916048777666,-4.88936592869409,130.25432487215));
#61139=CARTESIAN_POINT('Ctrl Pts',(44.383738799336,-4.90098333508911,130.392601693341));
#61140=CARTESIAN_POINT('Ctrl Pts',(44.3758727209054,-4.91260074148413,130.530878514532));
#61141=CARTESIAN_POINT('Ctrl Pts',(44.3680066424748,-4.91834656725249,130.669471235366));
#61142=CARTESIAN_POINT('Ctrl Pts',(44.3601405640442,-4.91824877153122,130.807836798172));
#61143=CARTESIAN_POINT('Ctrl Pts',(44.3601405640086,-4.91824877153078,130.807836798798));
#61144=CARTESIAN_POINT('Ctrl Pts',(44.3479816531159,-4.91809760476005,131.021713963081));
#61145=CARTESIAN_POINT('Ctrl Pts',(44.3358227422232,-4.90399509209797,131.235104433717));
#61146=CARTESIAN_POINT('Ctrl Pts',(44.3236638313304,-4.87613127035324,131.446643185275));
#61147=CARTESIAN_POINT('Ctrl Pts',(44.3158894972113,-4.85831531117819,131.581899784181));
#61148=CARTESIAN_POINT('Ctrl Pts',(44.3081151630922,-4.83483914376921,131.716628775925));
#61149=CARTESIAN_POINT('Ctrl Pts',(44.3003408289731,-4.80574183051092,131.850318800754));
#61150=CARTESIAN_POINT('Ctrl Pts',(44.292576076026,-4.77668037709073,131.983844064576));
#61151=CARTESIAN_POINT('Ctrl Pts',(44.284811323079,-4.74201164394849,132.116332530811));
#61152=CARTESIAN_POINT('Ctrl Pts',(44.2770465701319,-4.70182638926108,132.247278379515));
#61153=CARTESIAN_POINT('Ctrl Pts',(44.269289529247,-4.66168104713524,132.378094170956));
#61154=CARTESIAN_POINT('Ctrl Pts',(44.2615324883619,-4.61603020105383,132.507370022569));
#61155=CARTESIAN_POINT('Ctrl Pts',(44.253775447477,-4.56501547813448,132.63461107772));
#61156=CARTESIAN_POINT('Ctrl Pts',(44.2460242562368,-4.51403922581445,132.761756179401));
#61157=CARTESIAN_POINT('Ctrl Pts',(44.2382730649967,-4.45770729276966,132.886869177443));
#61158=CARTESIAN_POINT('Ctrl Pts',(44.2305218737566,-4.39621077021821,133.009471482425));
#61159=CARTESIAN_POINT('Ctrl Pts',(44.2227739769795,-4.33474038532924,133.132021678156));
#61160=CARTESIAN_POINT('Ctrl Pts',(44.2150260802025,-4.26810995172021,133.252062954496));
#61161=CARTESIAN_POINT('Ctrl Pts',(44.2072781834254,-4.19655812494766,133.369137989276));
#61162=CARTESIAN_POINT('Ctrl Pts',(44.1995319073413,-4.12502126527479,133.486188534483));
#61163=CARTESIAN_POINT('Ctrl Pts',(44.1917856312571,-4.04856526382163,133.600273738903));
#61164=CARTESIAN_POINT('Ctrl Pts',(44.184039355173,-3.96747384347568,133.710962476066));
#61165=CARTESIAN_POINT('Ctrl Pts',(44.1762930219077,-3.8863818245314,133.821652030308));
#61166=CARTESIAN_POINT('Ctrl Pts',(44.1685466886423,-3.80065454946935,133.928944751878));
#61167=CARTESIAN_POINT('Ctrl Pts',(44.160800355377,-3.71061779006429,134.032440337548));
#61168=CARTESIAN_POINT('Ctrl Pts',(44.153052287374,-3.62056086755124,134.135959100336));
#61169=CARTESIAN_POINT('Ctrl Pts',(44.145304219371,-3.52619279685923,134.235678740231));
#61170=CARTESIAN_POINT('Ctrl Pts',(44.1375561513681,-3.42787789462754,134.331234049095));
#61171=CARTESIAN_POINT('Ctrl Pts',(44.1297998486262,-3.3294585021478,134.426890915278));
#61172=CARTESIAN_POINT('Ctrl Pts',(44.1220435458844,-3.22708417949222,134.51837433629));
#61173=CARTESIAN_POINT('Ctrl Pts',(44.1142872431426,-3.12115459545429,134.605357467575));
#61174=CARTESIAN_POINT('Ctrl Pts',(44.1065268006284,-3.01516847360774,134.692387024375));
#61175=CARTESIAN_POINT('Ctrl Pts',(44.0987663581142,-2.90562362146811,134.774911270247));
#61176=CARTESIAN_POINT('Ctrl Pts',(44.0910059156001,-2.79294987352374,134.852645941809));
#61177=CARTESIAN_POINT('Ctrl Pts',(44.0832330153346,-2.68009525167647,134.930505399967));
#61178=CARTESIAN_POINT('Ctrl Pts',(44.0754601150692,-2.56410202791718,135.003559710968));
#61179=CARTESIAN_POINT('Ctrl Pts',(44.0676872148038,-2.44542665725375,135.071569485959));
#61180=CARTESIAN_POINT('Ctrl Pts',(44.0601968790417,-2.33106543523915,135.137106934323));
#61181=CARTESIAN_POINT('Ctrl Pts',(44.0527065432797,-2.21421395952165,135.19796010004));
#61182=CARTESIAN_POINT('Ctrl Pts',(44.0452162075177,-2.09529754315362,135.253957370998));
#61183=CARTESIAN_POINT('Ctrl Pts',(44.0374418733986,-1.9718723747153,135.312077795505));
#61184=CARTESIAN_POINT('Ctrl Pts',(44.0296675392795,-1.84583161631654,135.36515094196));
#61185=CARTESIAN_POINT('Ctrl Pts',(44.0218932051605,-1.71762660357202,135.412933272218));
#61186=CARTESIAN_POINT('Ctrl Pts',(44.0141284522134,-1.58957959204769,135.460656715024));
#61187=CARTESIAN_POINT('Ctrl Pts',(44.0063636992663,-1.45937399604142,135.503102180172));
#61188=CARTESIAN_POINT('Ctrl Pts',(43.9985989463192,-1.32748443320978,135.540072617053));
#61189=CARTESIAN_POINT('Ctrl Pts',(43.9908419054342,-1.19572586495127,135.577006334375));
#61190=CARTESIAN_POINT('Ctrl Pts',(43.9830848645492,-1.06228703231538,135.608475740203));
#61191=CARTESIAN_POINT('Ctrl Pts',(43.9753278236642,-0.927660825121338,
135.634332507343));
#61192=CARTESIAN_POINT('Ctrl Pts',(43.967576632424,-0.793136140597192,135.660169775694));
#61193=CARTESIAN_POINT('Ctrl Pts',(43.959825441184,-0.657426246165173,135.680402756517));
#61194=CARTESIAN_POINT('Ctrl Pts',(43.9520742499438,-0.521037082131064,
135.694933530993));
#61195=CARTESIAN_POINT('Ctrl Pts',(43.9443263531667,-0.384705887130155,
135.709458129502));
#61196=CARTESIAN_POINT('Ctrl Pts',(43.9365784563896,-0.247696384695925,
135.718285300667));
#61197=CARTESIAN_POINT('Ctrl Pts',(43.9288305596125,-0.110522332076842,
135.721368638366));
#61198=CARTESIAN_POINT('Ctrl Pts',(43.9210842835285,0.0266230266875624,
135.724451331097));
#61199=CARTESIAN_POINT('Ctrl Pts',(43.9133380074443,0.163932476554009,135.721792571403));
#61200=CARTESIAN_POINT('Ctrl Pts',(43.9055917313602,0.300889939462038,135.713398028997));
#61201=CARTESIAN_POINT('Ctrl Pts',(43.8978453980949,0.437848413358758,135.705003424624));
#61202=CARTESIAN_POINT('Ctrl Pts',(43.8900990648296,0.574454504879496,135.690872976971));
#61203=CARTESIAN_POINT('Ctrl Pts',(43.8823527315642,0.710195339979163,135.671064393385));
#61204=CARTESIAN_POINT('Ctrl Pts',(43.8746046635613,0.845966573297689,135.651251373804));
#61205=CARTESIAN_POINT('Ctrl Pts',(43.8668565955583,0.980871777825297,135.625757744439));
#61206=CARTESIAN_POINT('Ctrl Pts',(43.8591085275553,1.11440677157029,135.594692611278));
#61207=CARTESIAN_POINT('Ctrl Pts',(43.8513522248135,1.24808368789591,135.563594461723));
#61208=CARTESIAN_POINT('Ctrl Pts',(43.8435959220716,1.38038710296623,135.526913068346));
#61209=CARTESIAN_POINT('Ctrl Pts',(43.8358396193298,1.51082600245228,135.484808016353));
#61210=CARTESIAN_POINT('Ctrl Pts',(43.8280791768156,1.64133452110641,135.442680491627));
#61211=CARTESIAN_POINT('Ctrl Pts',(43.8203187343015,1.76997617472984,135.395123675711));
#61212=CARTESIAN_POINT('Ctrl Pts',(43.8125582917873,1.89627946844864,135.342345549233));
#61213=CARTESIAN_POINT('Ctrl Pts',(43.8047853915219,2.0227855154272,135.289482698622));
#61214=CARTESIAN_POINT('Ctrl Pts',(43.7970124912565,2.14694534701132,135.231381953921));
#61215=CARTESIAN_POINT('Ctrl Pts',(43.789239590991,2.26831083349889,135.168297948135));
#61216=CARTESIAN_POINT('Ctrl Pts',(43.7817492552289,2.38526437885274,135.107507204857));
#61217=CARTESIAN_POINT('Ctrl Pts',(43.7742589194668,2.49962294750406,135.042089371421));
#61218=CARTESIAN_POINT('Ctrl Pts',(43.7667685837047,2.61101226522926,134.972309515204));
#61219=CARTESIAN_POINT('Ctrl Pts',(43.7589942495856,2.72662494279093,134.89988393453));
#61220=CARTESIAN_POINT('Ctrl Pts',(43.7512199154665,2.83940499264457,134.822529606872));
#61221=CARTESIAN_POINT('Ctrl Pts',(43.7434455813474,2.94890356132639,134.740494615348));
#61222=CARTESIAN_POINT('Ctrl Pts',(43.7356808284003,3.05826718280847,134.658560724619));
#61223=CARTESIAN_POINT('Ctrl Pts',(43.7279160754532,3.16435705984621,134.571957879786));
#61224=CARTESIAN_POINT('Ctrl Pts',(43.7201513225061,3.26675086574333,134.480978879456));
#61225=CARTESIAN_POINT('Ctrl Pts',(43.7123942816211,3.3690429726688,134.390090240752));
#61226=CARTESIAN_POINT('Ctrl Pts',(43.7046372407361,3.4676460235161,134.294834354205));
#61227=CARTESIAN_POINT('Ctrl Pts',(43.6968801998511,3.56216880742927,134.195545727506));
#61228=CARTESIAN_POINT('Ctrl Pts',(43.689129008611,3.65662031097582,134.096331975133));
#61229=CARTESIAN_POINT('Ctrl Pts',(43.6813778173709,3.74699740360873,133.993091817796));
#61230=CARTESIAN_POINT('Ctrl Pts',(43.6736266261308,3.832944230359,133.886197989891));
#61231=CARTESIAN_POINT('Ctrl Pts',(43.6658787293537,3.91885452741531,133.779349594713));
#61232=CARTESIAN_POINT('Ctrl Pts',(43.6581308325766,4.00033805922415,133.668850921635));
#61233=CARTESIAN_POINT('Ctrl Pts',(43.6503829357995,4.07707808465801,133.555109125536));
#61234=CARTESIAN_POINT('Ctrl Pts',(43.6426366597154,4.15380205773286,133.441391121769));
#61235=CARTESIAN_POINT('Ctrl Pts',(43.6348903836313,4.22578427952503,133.324431668233));
#61236=CARTESIAN_POINT('Ctrl Pts',(43.6271441075472,4.29275056732684,133.204668020632));
#61237=CARTESIAN_POINT('Ctrl Pts',(43.6193977742818,4.35971734945848,133.084903488964));
#61238=CARTESIAN_POINT('Ctrl Pts',(43.6116514410165,4.42166793290908,132.96233506317));
#61239=CARTESIAN_POINT('Ctrl Pts',(43.6039051077511,4.47837364755536,132.837425430941));
#61240=CARTESIAN_POINT('Ctrl Pts',(43.5961570397481,4.53509206105334,132.712487826065));
#61241=CARTESIAN_POINT('Ctrl Pts',(43.5884089717452,4.58656310694151,132.585208327393));
#61242=CARTESIAN_POINT('Ctrl Pts',(43.5806609037423,4.63260605649545,132.456070091966));
#61243=CARTESIAN_POINT('Ctrl Pts',(43.5729046010004,4.67869794104403,132.326794606885));
#61244=CARTESIAN_POINT('Ctrl Pts',(43.5651482982585,4.71935007346054,132.195656807646));
#61245=CARTESIAN_POINT('Ctrl Pts',(43.5573919955167,4.75443131206144,132.063156058211));
#61246=CARTESIAN_POINT('Ctrl Pts',(43.5496315530025,4.78953127457571,131.930584589137));
#61247=CARTESIAN_POINT('Ctrl Pts',(43.5418711104883,4.81905433449726,131.796649101981));
#61248=CARTESIAN_POINT('Ctrl Pts',(43.5341106679741,4.84292061732194,131.661858697341));
#61249=CARTESIAN_POINT('Ctrl Pts',(43.5263377677087,4.86682521242255,131.526851915178));
#61250=CARTESIAN_POINT('Ctrl Pts',(43.5185648674433,4.88505483215077,131.390987860777));
#61251=CARTESIAN_POINT('Ctrl Pts',(43.5107919671779,4.89758148141411,131.254781193705));
#61252=CARTESIAN_POINT('Ctrl Pts',(43.5033016314158,4.90965275542396,131.123525982066));
#61253=CARTESIAN_POINT('Ctrl Pts',(43.4958112956538,4.91642847914391,130.991952942567));
#61254=CARTESIAN_POINT('Ctrl Pts',(43.4883209598918,4.91792935690632,130.860520238104));
#61255=CARTESIAN_POINT('Ctrl Pts',(43.4805466257728,4.91948714090528,130.724104222703));
#61256=CARTESIAN_POINT('Ctrl Pts',(43.4727722916537,4.91536712600988,130.587407269081));
#61257=CARTESIAN_POINT('Ctrl Pts',(43.4649979575346,4.90553541531272,130.450941105353));
#61258=CARTESIAN_POINT('Ctrl Pts',(43.4572332045875,4.89571582132031,130.314643123976));
#61259=CARTESIAN_POINT('Ctrl Pts',(43.4494684516404,4.88019856517031,130.178575752779));
#61260=CARTESIAN_POINT('Ctrl Pts',(43.4417036986933,4.85900170872886,130.043252571971));
#61261=CARTESIAN_POINT('Ctrl Pts',(43.4339466578083,4.83782590530404,129.908063796053));
#61262=CARTESIAN_POINT('Ctrl Pts',(43.4261896169234,4.81098178766093,129.773618123358));
#61263=CARTESIAN_POINT('Ctrl Pts',(43.4184325760384,4.77853932757177,129.640425500238));
#61264=CARTESIAN_POINT('Ctrl Pts',(43.4106813847982,4.74612133259413,129.50733331871));
#61265=CARTESIAN_POINT('Ctrl Pts',(43.4029301935581,4.70811349046494,129.375492684244));
#61266=CARTESIAN_POINT('Ctrl Pts',(43.3951790023179,4.664637044884,129.245404459749));
#61267=CARTESIAN_POINT('Ctrl Pts',(43.3874311055409,4.6211790779522,129.115371526219));
#61268=CARTESIAN_POINT('Ctrl Pts',(43.3796832087638,4.57225725409508,128.987089891296));
#61269=CARTESIAN_POINT('Ctrl Pts',(43.3719353119867,4.5180429179286,128.861046115419));
#61270=CARTESIAN_POINT('Ctrl Pts',(43.3641890359026,4.46383992223251,128.735028705183));
#61271=CARTESIAN_POINT('Ctrl Pts',(43.3564427598186,4.40434677065039,128.611248581816));
#61272=CARTESIAN_POINT('Ctrl Pts',(43.3486964837345,4.33978313634112,128.490172770387));
#61273=CARTESIAN_POINT('Ctrl Pts',(43.3409501504692,4.27521902543786,128.369096065204));
#61274=CARTESIAN_POINT('Ctrl Pts',(43.3332038172038,4.20558454108145,128.250724056774));
#61275=CARTESIAN_POINT('Ctrl Pts',(43.3254574839385,4.13114535374258,128.135499225745));
#61276=CARTESIAN_POINT('Ctrl Pts',(43.3177094159355,4.05668949626383,128.020248590915));
#61277=CARTESIAN_POINT('Ctrl Pts',(43.3099613479325,3.97742700684167,127.908146864267));
#61278=CARTESIAN_POINT('Ctrl Pts',(43.3022132799296,3.8936666908876,127.799607256178));
#61279=CARTESIAN_POINT('Ctrl Pts',(43.2944569771877,3.80981735347287,127.690952290902));
#61280=CARTESIAN_POINT('Ctrl Pts',(43.2867006744459,3.72146087951199,127.585867316864));
#61281=CARTESIAN_POINT('Ctrl Pts',(43.278944371704,3.62894651276743,127.484732585697));
#61282=CARTESIAN_POINT('Ctrl Pts',(43.2711839291899,3.53638276831979,127.383543875878));
#61283=CARTESIAN_POINT('Ctrl Pts',(43.2634234866757,3.43965698475331,127.286309887065));
#61284=CARTESIAN_POINT('Ctrl Pts',(43.2556630441615,3.33915430870082,127.19337300125));
#61285=CARTESIAN_POINT('Ctrl Pts',(43.2478901438961,3.23849029683053,127.100286924896));
#61286=CARTESIAN_POINT('Ctrl Pts',(43.2401172436307,3.13403757473917,127.011511989461));
#61287=CARTESIAN_POINT('Ctrl Pts',(43.2323443433653,3.02621400806626,126.927349934078));
#61288=CARTESIAN_POINT('Ctrl Pts',(43.2248540076032,2.92231009963191,126.846247381398));
#61289=CARTESIAN_POINT('Ctrl Pts',(43.217363671841,2.81527641933454,126.769428331433));
#61290=CARTESIAN_POINT('Ctrl Pts',(43.2098733360789,2.7055096237925,126.697123013279));
#61291=CARTESIAN_POINT('Ctrl Pts',(43.2020990019599,2.5915809868357,126.622076217012));
#61292=CARTESIAN_POINT('Ctrl Pts',(43.1943246678407,2.47434699960622,126.551654459786));
#61293=CARTESIAN_POINT('Ctrl Pts',(43.1865503337216,2.35421987135499,126.486162861578));
#61294=CARTESIAN_POINT('Ctrl Pts',(43.1787855807746,2.23424078905326,126.420751975912));
#61295=CARTESIAN_POINT('Ctrl Pts',(43.1710208278275,2.11137600005726,126.36025934522));
#61296=CARTESIAN_POINT('Ctrl Pts',(43.1632560748804,1.98606735682288,126.304947376191));
#61297=CARTESIAN_POINT('Ctrl Pts',(43.1554990339954,1.8608831718995,126.249690343789));
#61298=CARTESIAN_POINT('Ctrl Pts',(43.1477419931104,1.73326031847178,126.199603890118));
#61299=CARTESIAN_POINT('Ctrl Pts',(43.1399849522253,1.60366565029975,126.154904784401));
#61300=CARTESIAN_POINT('Ctrl Pts',(43.1322337609852,1.47416871047527,126.110239386629));
#61301=CARTESIAN_POINT('Ctrl Pts',(43.1244825697451,1.34270328371439,126.070953377335));
#61302=CARTESIAN_POINT('Ctrl Pts',(43.116731378505,1.20975629534869,126.037215479397));
#61303=CARTESIAN_POINT('Ctrl Pts',(43.1089834817279,1.07686581299934,126.003491920967));
#61304=CARTESIAN_POINT('Ctrl Pts',(43.1012355849508,0.942495399636922,125.975311879787));
#61305=CARTESIAN_POINT('Ctrl Pts',(43.0934876881738,0.807147028289451,125.952794196582));
#61306=CARTESIAN_POINT('Ctrl Pts',(43.0857414120896,0.671826968903493,125.93028122359));
#61307=CARTESIAN_POINT('Ctrl Pts',(43.0779951360055,0.535529743848918,125.913428316773));
#61308=CARTESIAN_POINT('Ctrl Pts',(43.0702488599214,0.398767013249796,125.902303097336));
#61309=CARTESIAN_POINT('Ctrl Pts',(43.0625025266561,0.262003273099265,125.891177795775));
#61310=CARTESIAN_POINT('Ctrl Pts',(43.0547561933907,0.124774410225408,125.885780297662));
#61311=CARTESIAN_POINT('Ctrl Pts',(43.0470098601254,-0.0124037024909772,
125.886126258503));
#61312=CARTESIAN_POINT('Ctrl Pts',(43.0392617921224,-0.149612535294579,
125.886472296821));
#61313=CARTESIAN_POINT('Ctrl Pts',(43.0315137241194,-0.286770204436251,
125.892564352512));
#61314=CARTESIAN_POINT('Ctrl Pts',(43.0237656561165,-0.423362147455745,
125.90436596914));
#61315=CARTESIAN_POINT('Ctrl Pts',(43.0160093533746,-0.560099262017746,
125.916180128667));
#61316=CARTESIAN_POINT('Ctrl Pts',(43.0082530506327,-0.696269059239914,
125.933715937285));
#61317=CARTESIAN_POINT('Ctrl Pts',(43.0004967478909,-0.831362847869982,
125.956885101621));
#61318=CARTESIAN_POINT('Ctrl Pts',(42.9927363053767,-0.966528740122822,
125.980066632038));
#61319=CARTESIAN_POINT('Ctrl Pts',(42.9849758628625,-1.10061709739733,126.008887427144));
#61320=CARTESIAN_POINT('Ctrl Pts',(42.9772154203484,-1.23313168286379,126.043208517998));
#61321=CARTESIAN_POINT('Ctrl Pts',(42.9694425200829,-1.36585899250675,126.077584704114));
#61322=CARTESIAN_POINT('Ctrl Pts',(42.9616696198175,-1.49700710761508,126.117478716414));
#61323=CARTESIAN_POINT('Ctrl Pts',(42.953896719552,-1.62609629992612,126.162702090071));
#61324=CARTESIAN_POINT('Ctrl Pts',(42.9464063837901,-1.75049277493955,126.206281480185));
#61325=CARTESIAN_POINT('Ctrl Pts',(42.9389160480282,-1.87297713594478,126.254809373854));
#61326=CARTESIAN_POINT('Ctrl Pts',(42.9314257122662,-1.99314128209203,126.308076497082));
#61327=CARTESIAN_POINT('Ctrl Pts',(42.9236508504031,-2.11786995472762,126.3633670125));
#61328=CARTESIAN_POINT('Ctrl Pts',(42.9158759885401,-2.24049378767229,126.423939076832));
#61329=CARTESIAN_POINT('Ctrl Pts',(42.908101126677,-2.36053316856388,126.489610772835));
#61330=CARTESIAN_POINT('Ctrl Pts',(42.900335965639,-2.48042277431546,126.555200529165));
#61331=CARTESIAN_POINT('Ctrl Pts',(42.8925708046009,-2.5977340046897,126.625877070276));
#61332=CARTESIAN_POINT('Ctrl Pts',(42.8848056435628,-2.71200718697745,126.701410449665));
#61333=CARTESIAN_POINT('Ctrl Pts',(42.8770483137291,-2.82616512418129,126.776867653257));
#61334=CARTESIAN_POINT('Ctrl Pts',(42.8692909838953,-2.93729078688686,126.857171732654));
#61335=CARTESIAN_POINT('Ctrl Pts',(42.8615336540616,-3.04494941021352,126.942047042552));
#61336=CARTESIAN_POINT('Ctrl Pts',(42.8537826840201,-3.15251977037426,127.026852768023));
#61337=CARTESIAN_POINT('Ctrl Pts',(42.8460317139787,-3.25662844520335,127.116222020501));
#61338=CARTESIAN_POINT('Ctrl Pts',(42.8382807439373,-3.35687032746872,127.20983635599));
#61339=CARTESIAN_POINT('Ctrl Pts',(42.830533243161,-3.45706734236119,127.303408790537));
#61340=CARTESIAN_POINT('Ctrl Pts',(42.8227857423846,-3.55340072294593,127.401222261656));
#61341=CARTESIAN_POINT('Ctrl Pts',(42.8150382416083,-3.64549921708986,127.502918732465));
#61342=CARTESIAN_POINT('Ctrl Pts',(42.8072925307566,-3.73757643348692,127.604591708083));
#61343=CARTESIAN_POINT('Ctrl Pts',(42.7995468199049,-3.82542044845213,127.710145608475));
#61344=CARTESIAN_POINT('Ctrl Pts',(42.7918011090532,-3.90869788019213,127.819186595188));
#61345=CARTESIAN_POINT('Ctrl Pts',(42.784055510342,-3.99197410626239,127.928226003233));
#61346=CARTESIAN_POINT('Ctrl Pts',(42.7763099116306,-4.07068364444426,128.04075208582));
#61347=CARTESIAN_POINT('Ctrl Pts',(42.7685643129194,-4.14453456265979,128.156339408924));
#61348=CARTESIAN_POINT('Ctrl Pts',(42.7608136355511,-4.21843390366331,128.272002520665));
#61349=CARTESIAN_POINT('Ctrl Pts',(42.7530629581829,-4.2874680485546,128.390730553733));
#61350=CARTESIAN_POINT('Ctrl Pts',(42.7453122808146,-4.35138928918499,128.512070427283));
#61351=CARTESIAN_POINT('Ctrl Pts',(42.7375590397133,-4.41533167338616,128.633450437073));
#61352=CARTESIAN_POINT('Ctrl Pts',(42.729805798612,-4.47415761250167,128.757443657138));
#61353=CARTESIAN_POINT('Ctrl Pts',(42.7220525575107,-4.52766667012813,128.883574948442));
#61354=CARTESIAN_POINT('Ctrl Pts',(42.7142901688683,-4.58123885958533,129.009855053792));
#61355=CARTESIAN_POINT('Ctrl Pts',(42.7065277802259,-4.62948149385214,129.138277905235));
#61356=CARTESIAN_POINT('Ctrl Pts',(42.6987653915834,-4.67224314834394,129.268350518233));
#61357=CARTESIAN_POINT('Ctrl Pts',(42.6925739244696,-4.70635086823736,129.372099549992));
#61358=CARTESIAN_POINT('Ctrl Pts',(42.6863824573558,-4.73697251997796,129.476897780145));
#61359=CARTESIAN_POINT('Ctrl Pts',(42.6801909902419,-4.76405452823402,129.582490119308));
#61360=CARTESIAN_POINT('Origin',(213.235140564004,0.,130.804360617566));
#61361=CARTESIAN_POINT('',(40.5848681886094,-4.76405452823408,129.582490119308));
#61362=CARTESIAN_POINT('',(40.9298575685393,-4.7640545282341,129.582490119308));
#61363=CARTESIAN_POINT('',(213.235140564004,-4.76405452823405,129.582490119308));
#61364=CARTESIAN_POINT('',(42.264859436036,-4.9182499044007,130.80339089469));
#61365=CARTESIAN_POINT('Ctrl Pts',(42.2648594359912,-4.91824990440086,130.803390895484));
#61366=CARTESIAN_POINT('Ctrl Pts',(42.2568550863798,-4.91827792430065,130.945502611918));
#61367=CARTESIAN_POINT('Ctrl Pts',(42.2488507367685,-4.91214217362805,131.08753530788));
#61368=CARTESIAN_POINT('Ctrl Pts',(42.2408463871571,-4.89988927847153,131.228940552584));
#61369=CARTESIAN_POINT('Ctrl Pts',(42.2328351978916,-4.88762591331188,131.370466626964));
#61370=CARTESIAN_POINT('Ctrl Pts',(42.2248240086261,-4.86923501125477,131.511363830092));
#61371=CARTESIAN_POINT('Ctrl Pts',(42.2168128193606,-4.8448147996154,131.651091164982));
#61372=CARTESIAN_POINT('Ctrl Pts',(42.2083844041628,-4.81912277361354,131.798095555205));
#61373=CARTESIAN_POINT('Ctrl Pts',(42.1999559889649,-4.78675670518386,131.943804511185));
#61374=CARTESIAN_POINT('Ctrl Pts',(42.1915275737671,-4.74789083996242,132.087604800994));
#61375=CARTESIAN_POINT('Ctrl Pts',(42.1834930844567,-4.7108414811763,132.224684176438));
#61376=CARTESIAN_POINT('Ctrl Pts',(42.1754585951463,-4.66788626722541,132.36002894379));
#61377=CARTESIAN_POINT('Ctrl Pts',(42.1674241058359,-4.61922601848707,132.493127638985));
#61378=CARTESIAN_POINT('Ctrl Pts',(42.1593809267226,-4.57051314064548,132.626370288745));
#61379=CARTESIAN_POINT('Ctrl Pts',(42.1513377476093,-4.51608305489379,132.757361696482));
#61380=CARTESIAN_POINT('Ctrl Pts',(42.143294568496,-4.45618358258824,132.885612870603));
#61381=CARTESIAN_POINT('Ctrl Pts',(42.135236943681,-4.39617652969784,133.014094386257));
#61382=CARTESIAN_POINT('Ctrl Pts',(42.127179318866,-4.33068062810157,133.139825524779));
#61383=CARTESIAN_POINT('Ctrl Pts',(42.119121694051,-4.25998870793906,133.262343382097));
#61384=CARTESIAN_POINT('Ctrl Pts',(42.1179717416962,-4.24989983660076,133.279828646273));
#61385=CARTESIAN_POINT('Ctrl Pts',(42.1168217893414,-4.23970520285251,133.297248514659));
#61386=CARTESIAN_POINT('Ctrl Pts',(42.1156718369867,-4.22940572634524,133.314601694526));
#61387=CARTESIAN_POINT('Ctrl Pts',(42.1078975028676,-4.15977538793196,133.43191909273));
#61388=CARTESIAN_POINT('Ctrl Pts',(42.1001231687486,-4.085149746637,133.54652295529));
#61389=CARTESIAN_POINT('Ctrl Pts',(42.0923488346295,-4.00576604289151,133.65795860469));
#61390=CARTESIAN_POINT('Ctrl Pts',(42.0845840816824,-3.92648017246617,133.769256919612));
#61391=CARTESIAN_POINT('Ctrl Pts',(42.0768193287354,-3.84244813163981,133.877394474871));
#61392=CARTESIAN_POINT('Ctrl Pts',(42.0690545757883,-3.75395250002539,133.981942039033));
#61393=CARTESIAN_POINT('Ctrl Pts',(42.0612975349033,-3.66554476351985,134.08638576508));
#61394=CARTESIAN_POINT('Ctrl Pts',(42.0535404940183,-3.57268250965602,134.187246299313));
#61395=CARTESIAN_POINT('Ctrl Pts',(42.0457834531333,-3.47569076181493,134.284124516272));
#61396=CARTESIAN_POINT('Ctrl Pts',(42.0380322618932,-3.37877215620549,134.380929676613));
#61397=CARTESIAN_POINT('Ctrl Pts',(42.0302810706531,-3.27773053050994,134.473758221988));
#61398=CARTESIAN_POINT('Ctrl Pts',(42.022529879413,-3.1729299722468,134.562245455306));
#61399=CARTESIAN_POINT('Ctrl Pts',(42.0147819826359,-3.06817395701628,134.65069507919));
#61400=CARTESIAN_POINT('Ctrl Pts',(42.0070340858589,-2.95966248491463,134.734806809231));
#61401=CARTESIAN_POINT('Ctrl Pts',(41.9992861890819,-2.84779499265814,134.814254224919));
#61402=CARTESIAN_POINT('Ctrl Pts',(41.9915399129978,-2.73595090066944,134.893685021921));
#61403=CARTESIAN_POINT('Ctrl Pts',(41.9837936369136,-2.62075250341194,134.968453219004));
#61404=CARTESIAN_POINT('Ctrl Pts',(41.9760473608295,-2.50263035104442,135.038274219487));
#61405=CARTESIAN_POINT('Ctrl Pts',(41.9683010275642,-2.38450732672601,135.108095735373));
#61406=CARTESIAN_POINT('Ctrl Pts',(41.9605546942989,-2.2634608407967,135.172969782847));
#61407=CARTESIAN_POINT('Ctrl Pts',(41.9528083610335,-2.13994796025175,135.232656654408));
#61408=CARTESIAN_POINT('Ctrl Pts',(41.9450602930306,-2.01640741985358,135.292356892431));
#61409=CARTESIAN_POINT('Ctrl Pts',(41.9373122250276,-1.89039973771314,135.34686747295));
#61410=CARTESIAN_POINT('Ctrl Pts',(41.9295641570246,-1.76240359474225,135.395996124849));
#61411=CARTESIAN_POINT('Ctrl Pts',(41.9218078542828,-1.63427141594761,135.445176991264));
#61412=CARTESIAN_POINT('Ctrl Pts',(41.914051551541,-1.50414692024234,135.488964362466));
#61413=CARTESIAN_POINT('Ctrl Pts',(41.9062952487991,-1.37252618074724,135.527215151178));
#61414=CARTESIAN_POINT('Ctrl Pts',(41.898534806285,-1.24083519130045,135.565486355489));
#61415=CARTESIAN_POINT('Ctrl Pts',(41.8907743637708,-1.10764674628935,135.59821499589));
#61416=CARTESIAN_POINT('Ctrl Pts',(41.8830139212567,-0.973467882937817,
135.625309003868));
#61417=CARTESIAN_POINT('Ctrl Pts',(41.8752410209913,-0.839073623762808,
135.652446505553));
#61418=CARTESIAN_POINT('Ctrl Pts',(41.8674681207258,-0.703686155461381,
135.673931238289));
#61419=CARTESIAN_POINT('Ctrl Pts',(41.8596952204604,-0.567819317587671,
135.689722864634));
#61420=CARTESIAN_POINT('Ctrl Pts',(41.8522048846982,-0.43689158149619,135.704940425584));
#61421=CARTESIAN_POINT('Ctrl Pts',(41.8447145489361,-0.305519030465423,
135.714871588225));
#61422=CARTESIAN_POINT('Ctrl Pts',(41.8372242131739,-0.174160192299514,
135.719526056279));
#61423=CARTESIAN_POINT('Ctrl Pts',(41.8294498790548,-0.037820843861379,
135.724356999904));
#61424=CARTESIAN_POINT('Ctrl Pts',(41.8216755449358,0.0989356134130586,
135.723518521443));
#61425=CARTESIAN_POINT('Ctrl Pts',(41.8139012108167,0.235598412204566,135.716964453687));
#61426=CARTESIAN_POINT('Ctrl Pts',(41.8061364578697,0.372092786310282,135.710418463233));
#61427=CARTESIAN_POINT('Ctrl Pts',(41.7983717049226,0.50849334482837,135.698170917399));
#61428=CARTESIAN_POINT('Ctrl Pts',(41.7906069519755,0.644286222012198,135.680227548341));
#61429=CARTESIAN_POINT('Ctrl Pts',(41.7828499110905,0.779944227796062,135.66230200089));
#61430=CARTESIAN_POINT('Ctrl Pts',(41.7750928702055,0.914995368264727,135.638691939127));
#61431=CARTESIAN_POINT('Ctrl Pts',(41.7673358293205,1.04892816478898,135.609455077367));
#61432=CARTESIAN_POINT('Ctrl Pts',(41.7595846380803,1.18275996155007,135.580240263352));
#61433=CARTESIAN_POINT('Ctrl Pts',(41.7518334468403,1.31547471258287,135.545407178245));
#61434=CARTESIAN_POINT('Ctrl Pts',(41.7440822556001,1.44656878970031,135.505065011502));
#61435=CARTESIAN_POINT('Ctrl Pts',(41.7363343588231,1.57760714833758,135.464739991255));
#61436=CARTESIAN_POINT('Ctrl Pts',(41.7285864620459,1.70702583019955,135.418910661201));
#61437=CARTESIAN_POINT('Ctrl Pts',(41.7208385652688,1.83433430316589,135.367736640504));
#61438=CARTESIAN_POINT('Ctrl Pts',(41.7130922891848,1.96161614594413,135.316573324309));
#61439=CARTESIAN_POINT('Ctrl Pts',(41.7053460131007,2.08678829529036,135.260067686947));
#61440=CARTESIAN_POINT('Ctrl Pts',(41.6975997370166,2.20937858907897,135.198428131));
#61441=CARTESIAN_POINT('Ctrl Pts',(41.6898534037512,2.33196978780145,135.136788120045));
#61442=CARTESIAN_POINT('Ctrl Pts',(41.6821070704858,2.4519787436396,135.070014290514));
#61443=CARTESIAN_POINT('Ctrl Pts',(41.6743607372205,2.56895672800876,134.998361618057));
#61444=CARTESIAN_POINT('Ctrl Pts',(41.6666126692175,2.6859609087866,134.92669289948));
#61445=CARTESIAN_POINT('Ctrl Pts',(41.6588646012145,2.79993243410273,134.850143368037));
#61446=CARTESIAN_POINT('Ctrl Pts',(41.6511165332115,2.9104508020968,134.769011824302));
#61447=CARTESIAN_POINT('Ctrl Pts',(41.6433602304697,3.02108663032711,134.687794052997));
#61448=CARTESIAN_POINT('Ctrl Pts',(41.6356039277278,3.12826165423825,134.601984773143));
#61449=CARTESIAN_POINT('Ctrl Pts',(41.627847624986,3.23158735081323,134.51192400294));
#61450=CARTESIAN_POINT('Ctrl Pts',(41.6200871824718,3.3349681954237,134.421815164591));
#61451=CARTESIAN_POINT('Ctrl Pts',(41.6123267399576,3.43449533535338,134.327450583289));
#61452=CARTESIAN_POINT('Ctrl Pts',(41.6045662974435,3.52981724475025,134.229207078528));
#61453=CARTESIAN_POINT('Ctrl Pts',(41.5967933971781,3.62529217333835,134.130805864572));
#61454=CARTESIAN_POINT('Ctrl Pts',(41.5890204969126,3.71654812110762,134.028513575955));
#61455=CARTESIAN_POINT('Ctrl Pts',(41.5812475966472,3.80327340819616,133.922740717074));
#61456=CARTESIAN_POINT('Ctrl Pts',(41.5737572608851,3.88684601265181,133.820812968039));
#61457=CARTESIAN_POINT('Ctrl Pts',(41.5662669251231,3.9662114538305,133.715653556183));
#61458=CARTESIAN_POINT('Ctrl Pts',(41.558776589361,4.04113005027163,133.607653499034));
#61459=CARTESIAN_POINT('Ctrl Pts',(41.5510022552419,4.1188892080674,133.495558586894));
#61460=CARTESIAN_POINT('Ctrl Pts',(41.5432279211228,4.1921039780104,133.380048288156));
#61461=CARTESIAN_POINT('Ctrl Pts',(41.5354535870037,4.26045943610733,133.261527371326));
#61462=CARTESIAN_POINT('Ctrl Pts',(41.5276888340566,4.32873065221135,133.143152520934));
#61463=CARTESIAN_POINT('Ctrl Pts',(41.5199240811095,4.39215427868095,133.021774770302));
#61464=CARTESIAN_POINT('Ctrl Pts',(41.5121593281624,4.45045738115321,132.897829547605));
#61465=CARTESIAN_POINT('Ctrl Pts',(41.5044022872773,4.50870257616224,132.774007429051));
#61466=CARTESIAN_POINT('Ctrl Pts',(41.4966452463923,4.56183720276016,132.647623264636));
#61467=CARTESIAN_POINT('Ctrl Pts',(41.4888882055073,4.60963335094272,132.519138571814));
#61468=CARTESIAN_POINT('Ctrl Pts',(41.4811370142672,4.65739345567781,132.3907507703));
#61469=CARTESIAN_POINT('Ctrl Pts',(41.4733858230271,4.69982295932381,132.260265958234));
#61470=CARTESIAN_POINT('Ctrl Pts',(41.465634631787,4.7367415027254,132.128166871841));
#61471=CARTESIAN_POINT('Ctrl Pts',(41.4578867350099,4.77364435476136,131.996123931084));
#61472=CARTESIAN_POINT('Ctrl Pts',(41.4501388382328,4.80504080020648,131.862468456368));
#61473=CARTESIAN_POINT('Ctrl Pts',(41.4423909414557,4.83079998659112,131.727699424316));
#61474=CARTESIAN_POINT('Ctrl Pts',(41.4346446653716,4.85655378470931,131.592958583041));
#61475=CARTESIAN_POINT('Ctrl Pts',(41.4268983892875,4.87667259589443,131.457105031514));
#61476=CARTESIAN_POINT('Ctrl Pts',(41.4191521132034,4.89107653998105,131.320648659793));
#61477=CARTESIAN_POINT('Ctrl Pts',(41.411405779938,4.9054805903943,131.184191280783));
#61478=CARTESIAN_POINT('Ctrl Pts',(41.4036594466727,4.9141696484891,131.047131461503));
#61479=CARTESIAN_POINT('Ctrl Pts',(41.3959131134073,4.9171156837391,130.909984550588));
#61480=CARTESIAN_POINT('Ctrl Pts',(41.3881650454044,4.92006237873327,130.772806926573));
#61481=CARTESIAN_POINT('Ctrl Pts',(41.3804169774014,4.91726348327764,130.635542562912));
#61482=CARTESIAN_POINT('Ctrl Pts',(41.3726689093984,4.90874309523034,130.49870674874));
#61483=CARTESIAN_POINT('Ctrl Pts',(41.3649126066566,4.9002136516132,130.361725503835));
#61484=CARTESIAN_POINT('Ctrl Pts',(41.3571563039147,4.88595059254669,130.225174109095));
#61485=CARTESIAN_POINT('Ctrl Pts',(41.3494000011729,4.86602997878986,130.089563228078));
#61486=CARTESIAN_POINT('Ctrl Pts',(41.3416395586587,4.84609873280165,129.953879967451));
#61487=CARTESIAN_POINT('Ctrl Pts',(41.3338791161444,4.82050398822523,129.819138604696));
#61488=CARTESIAN_POINT('Ctrl Pts',(41.3261186736302,4.78937276566545,129.685838568609));
#61489=CARTESIAN_POINT('Ctrl Pts',(41.3183457733648,4.75819156850356,129.552324547471));
#61490=CARTESIAN_POINT('Ctrl Pts',(41.3105728730994,4.72145623784141,129.420256853484));
#61491=CARTESIAN_POINT('Ctrl Pts',(41.302799972834,4.67934367207602,129.290119599398));
#61492=CARTESIAN_POINT('Ctrl Pts',(41.295309637072,4.6387620041517,129.164713162295));
#61493=CARTESIAN_POINT('Ctrl Pts',(41.28781930131,4.59318737225453,129.041099538118));
#61494=CARTESIAN_POINT('Ctrl Pts',(41.2803289655481,4.54281919682059,128.919691732192));
#61495=CARTESIAN_POINT('Ctrl Pts',(41.272554631429,4.49054129670563,128.793680712402));
#61496=CARTESIAN_POINT('Ctrl Pts',(41.26478029731,4.43293358247985,128.669646914935));
#61497=CARTESIAN_POINT('Ctrl Pts',(41.2570059631909,4.37016637324084,128.548074081531));
#61498=CARTESIAN_POINT('Ctrl Pts',(41.2492412102438,4.30747651897746,128.426651075778));
#61499=CARTESIAN_POINT('Ctrl Pts',(41.2414764572967,4.239639999089,128.307683343545));
#61500=CARTESIAN_POINT('Ctrl Pts',(41.2337117043496,4.1668756239422,128.191635871808));
#61501=CARTESIAN_POINT('Ctrl Pts',(41.2259546634646,4.09418351939859,128.075703660056));
#61502=CARTESIAN_POINT('Ctrl Pts',(41.2181976225795,4.01657350605268,127.962686265877));
#61503=CARTESIAN_POINT('Ctrl Pts',(41.2104405816945,3.93431068068503,127.853024897871));
#61504=CARTESIAN_POINT('Ctrl Pts',(41.2026893904544,3.85210989035424,127.743446226356));
#61505=CARTESIAN_POINT('Ctrl Pts',(41.1949381992143,3.76526350556008,127.637218855082));
#61506=CARTESIAN_POINT('Ctrl Pts',(41.1871870079742,3.67408017743169,127.534755456036));
#61507=CARTESIAN_POINT('Ctrl Pts',(41.1794391111971,3.58293560464977,127.432335606667));
#61508=CARTESIAN_POINT('Ctrl Pts',(41.1716912144201,3.48745801411554,127.333676839121));
#61509=CARTESIAN_POINT('Ctrl Pts',(41.163943317643,3.38799648003716,127.239158952336));
#61510=CARTESIAN_POINT('Ctrl Pts',(41.1561970415589,3.2885557511677,127.144660836657));
#61511=CARTESIAN_POINT('Ctrl Pts',(41.1484507654748,3.18513301957122,127.054302148005));
#61512=CARTESIAN_POINT('Ctrl Pts',(41.1407044893907,3.07811409301214,126.968425699857));
#61513=CARTESIAN_POINT('Ctrl Pts',(41.1329581561253,2.9710943764638,126.882548617788));
#61514=CARTESIAN_POINT('Ctrl Pts',(41.12521182286,2.86047871691068,126.801154086934));
#61515=CARTESIAN_POINT('Ctrl Pts',(41.1174654895947,2.74668554056907,126.724544248692));
#61516=CARTESIAN_POINT('Ctrl Pts',(41.1097174215917,2.63286688103476,126.647917254209));
#61517=CARTESIAN_POINT('Ctrl Pts',(41.1019693535888,2.51586961299823,126.576077302798));
#61518=CARTESIAN_POINT('Ctrl Pts',(41.0942212855858,2.39614028928167,126.509282646611));
#61519=CARTESIAN_POINT('Ctrl Pts',(41.086464982844,2.27628371581475,126.442417000269));
#61520=CARTESIAN_POINT('Ctrl Pts',(41.0787086801021,2.15368962826356,126.380607551502));
#61521=CARTESIAN_POINT('Ctrl Pts',(41.0709523773603,2.02882877504139,126.324066334367));
#61522=CARTESIAN_POINT('Ctrl Pts',(41.0631919348461,1.90390127982238,126.267494939483));
#61523=CARTESIAN_POINT('Ctrl Pts',(41.0554314923319,1.77670497063303,126.216197525165));
#61524=CARTESIAN_POINT('Ctrl Pts',(41.0476710498178,1.64772868880453,126.170337178848));
#61525=CARTESIAN_POINT('Ctrl Pts',(41.0398981495523,1.51854536279828,126.124403213431));
#61526=CARTESIAN_POINT('Ctrl Pts',(41.0321252492869,1.38757672796261,126.083923872983));
#61527=CARTESIAN_POINT('Ctrl Pts',(41.0243523490215,1.25532569996852,126.049012002638));
#61528=CARTESIAN_POINT('Ctrl Pts',(41.0168620132594,1.12788232996117,126.015369266718));
#61529=CARTESIAN_POINT('Ctrl Pts',(41.0093716774973,0.999248485256093,125.986896311974));
#61530=CARTESIAN_POINT('Ctrl Pts',(41.0018813417352,0.869879430547576,125.963648599814));
#61531=CARTESIAN_POINT('Ctrl Pts',(40.9941070076161,0.735605308810048,125.939519443581));
#61532=CARTESIAN_POINT('Ctrl Pts',(40.9863326734969,0.600113785495589,125.92094314787));
#61533=CARTESIAN_POINT('Ctrl Pts',(40.9785583393779,0.463903907862529,125.908037892625));
#61534=CARTESIAN_POINT('Ctrl Pts',(40.9707935864308,0.327861896730224,125.895148541955));
#61535=CARTESIAN_POINT('Ctrl Pts',(40.9630288334837,0.191103678263022,125.887916362147));
#61536=CARTESIAN_POINT('Ctrl Pts',(40.9552640805366,0.0541387315197604,
125.886408598661));
#61537=CARTESIAN_POINT('Ctrl Pts',(40.9475070396516,-0.0826901797075282,
125.884902332707));
#61538=CARTESIAN_POINT('Ctrl Pts',(40.9397499987666,-0.219725022192236,
125.889109172808));
#61539=CARTESIAN_POINT('Ctrl Pts',(40.9319929578816,-0.3564513033596,125.899044569559));
#61540=CARTESIAN_POINT('Ctrl Pts',(40.9242417666415,-0.493074478174202,
125.90897247395));
#61541=CARTESIAN_POINT('Ctrl Pts',(40.9164905754014,-0.629389166464533,
125.924620308174));
#61542=CARTESIAN_POINT('Ctrl Pts',(40.9087393841613,-0.764881342126213,
125.945951454582));
#61543=CARTESIAN_POINT('Ctrl Pts',(40.9009914873842,-0.900315929999418,
125.967273534684));
#61544=CARTESIAN_POINT('Ctrl Pts',(40.8932435906071,-1.0349283151517,125.994274061933));
#61545=CARTESIAN_POINT('Ctrl Pts',(40.8854956938301,-1.16821027884121,126.026864640916));
#61546=CARTESIAN_POINT('Ctrl Pts',(40.877749417746,-1.30146436281679,126.059448402652));
#61547=CARTESIAN_POINT('Ctrl Pts',(40.8700031416618,-1.43338819933889,126.097619797478));
#61548=CARTESIAN_POINT('Ctrl Pts',(40.8622568655778,-1.56348483120099,126.141239533452));
#61549=CARTESIAN_POINT('Ctrl Pts',(40.8545105323124,-1.69358242340704,126.184859591418));
#61550=CARTESIAN_POINT('Ctrl Pts',(40.8467641990471,-1.82185241335442,126.2339279465));
#61551=CARTESIAN_POINT('Ctrl Pts',(40.8390178657817,-1.94781443133571,126.288255879677));
#61552=CARTESIAN_POINT('Ctrl Pts',(40.8312697977788,-2.07380465763723,126.342595979219));
#61553=CARTESIAN_POINT('Ctrl Pts',(40.8235217297759,-2.19748552456353,126.402197845827));
#61554=CARTESIAN_POINT('Ctrl Pts',(40.8157736617729,-2.31839838455661,126.466825373561));
#61555=CARTESIAN_POINT('Ctrl Pts',(40.8080173590311,-2.43943975217667,126.531521588201));
#61556=CARTESIAN_POINT('Ctrl Pts',(40.8002610562892,-2.55770689080747,126.601253949265));
#61557=CARTESIAN_POINT('Ctrl Pts',(40.7925047535473,-2.67276695917592,126.675741012367));
#61558=CARTESIAN_POINT('Ctrl Pts',(40.7847443110331,-2.78788843856741,126.750267831457));
#61559=CARTESIAN_POINT('Ctrl Pts',(40.776983868519,-2.89979911811035,126.829554183317));
#61560=CARTESIAN_POINT('Ctrl Pts',(40.7692234260048,-3.00809755704936,126.913276944632));
#61561=CARTESIAN_POINT('Ctrl Pts',(40.7614505257393,-3.11656984625669,126.997134105156));
#61562=CARTESIAN_POINT('Ctrl Pts',(40.7536776254739,-3.22141800802557,127.085441654592));
#61563=CARTESIAN_POINT('Ctrl Pts',(40.7459047252085,-3.32227526434383,127.177837471296));
#61564=CARTESIAN_POINT('Ctrl Pts',(40.7384143894464,-3.4194661053511,127.266874467333));
#61565=CARTESIAN_POINT('Ctrl Pts',(40.7309240536844,-3.51295094369156,127.359707436453));
#61566=CARTESIAN_POINT('Ctrl Pts',(40.7234337179223,-3.60243703642587,127.455983329821));
#61567=CARTESIAN_POINT('Ctrl Pts',(40.715748964601,-3.69424581111858,127.554758139766));
#61568=CARTESIAN_POINT('Ctrl Pts',(40.7080642112797,-3.78215134313305,127.657486478633));
#61569=CARTESIAN_POINT('Ctrl Pts',(40.7003794579584,-3.86578782177955,127.763823234227));
#61570=CARTESIAN_POINT('Ctrl Pts',(40.692703831564,-3.94932496815152,127.87003369718));
#61571=CARTESIAN_POINT('Ctrl Pts',(40.6850282051695,-4.0286028972979,127.979843744061));
#61572=CARTESIAN_POINT('Ctrl Pts',(40.6773525787751,-4.10329254126362,128.092871472592));
#61573=CARTESIAN_POINT('Ctrl Pts',(40.6696455462613,-4.17828779049929,128.20636167313));
#61574=CARTESIAN_POINT('Ctrl Pts',(40.6619385137475,-4.24865682752416,128.323095663254));
#61575=CARTESIAN_POINT('Ctrl Pts',(40.6542314812337,-4.31410685386605,128.442652524696));
#61576=CARTESIAN_POINT('Ctrl Pts',(40.6465694208885,-4.379174965429,128.561511746507));
#61577=CARTESIAN_POINT('Ctrl Pts',(40.6389073605433,-4.43938111500533,128.683160634019));
#61578=CARTESIAN_POINT('Ctrl Pts',(40.6312453001981,-4.49448096616251,128.807156595113));
#61579=CARTESIAN_POINT('Ctrl Pts',(40.6235157816,-4.55006592700635,128.932244240496));
#61580=CARTESIAN_POINT('Ctrl Pts',(40.6157862630018,-4.60045401555403,129.059720140441));
#61581=CARTESIAN_POINT('Ctrl Pts',(40.6080567444037,-4.64544223829743,129.189105382892));
#61582=CARTESIAN_POINT('Ctrl Pts',(40.6003272258056,-4.69043046104083,129.318490625343));
#61583=CARTESIAN_POINT('Ctrl Pts',(40.5925977072075,-4.73001866836183,129.449784818233));
#61584=CARTESIAN_POINT('Ctrl Pts',(40.5848681886094,-4.76405452823407,129.582490119308));
#61585=CARTESIAN_POINT('Ctrl Pts',(42.3345736784939,-4.76405452823401,129.582490119308));
#61586=CARTESIAN_POINT('Ctrl Pts',(42.3263003656675,-4.80031713428966,129.723877469957));
#61587=CARTESIAN_POINT('Ctrl Pts',(42.318027052841,-4.83032222928608,129.867039220305));
#61588=CARTESIAN_POINT('Ctrl Pts',(42.3097537400146,-4.85390803146789,130.011416808364));
#61589=CARTESIAN_POINT('Ctrl Pts',(42.3015021780208,-4.87743182573972,130.155414822626));
#61590=CARTESIAN_POINT('Ctrl Pts',(42.2932506160271,-4.89456993314338,130.300621998682));
#61591=CARTESIAN_POINT('Ctrl Pts',(42.2849990540334,-4.90521111842529,130.446468250817));
#61592=CARTESIAN_POINT('Ctrl Pts',(42.2782858480343,-4.91386844523521,130.565124080529));
#61593=CARTESIAN_POINT('Ctrl Pts',(42.271572642035,-4.91822640423858,130.684202544152));
#61594=CARTESIAN_POINT('Ctrl Pts',(42.2648594360359,-4.9182499044007,130.80339089469));
#61595=CARTESIAN_POINT('',(42.6101405639782,-4.91824847792861,130.800491269695));
#61596=CARTESIAN_POINT('Ctrl Pts',(42.6801909902419,-4.76405452823402,129.582490119308));
#61597=CARTESIAN_POINT('Ctrl Pts',(42.6724154236971,-4.79806552328429,129.71509847282));
#61598=CARTESIAN_POINT('Ctrl Pts',(42.6646398571522,-4.82649231743152,129.848959149606));
#61599=CARTESIAN_POINT('Ctrl Pts',(42.6568642906074,-4.84927547674462,129.983561974083));
#61600=CARTESIAN_POINT('Ctrl Pts',(42.6555688898893,-4.85307112568726,130.005986654584));
#61601=CARTESIAN_POINT('Ctrl Pts',(42.6542734891712,-4.85671025160539,130.028431928163));
#61602=CARTESIAN_POINT('Ctrl Pts',(42.6529780884531,-4.86019272010058,130.05089543192));
#61603=CARTESIAN_POINT('Ctrl Pts',(42.6399837889497,-4.89512572423288,130.276229177405));
#61604=CARTESIAN_POINT('Ctrl Pts',(42.6269894894463,-4.91439406463795,130.504051802434));
#61605=CARTESIAN_POINT('Ctrl Pts',(42.6139951899428,-4.91772728215714,130.732656776474));
#61606=CARTESIAN_POINT('Ctrl Pts',(42.6127103146314,-4.9180568704429,130.755261218301));
#61607=CARTESIAN_POINT('Ctrl Pts',(42.61142543932,-4.9182306836054,130.777873274665));
#61608=CARTESIAN_POINT('Ctrl Pts',(42.6101405640086,-4.91824847792818,130.80049126916));
#61609=CARTESIAN_POINT('Ctrl Pts',(42.6101405639782,-4.91824847792861,130.800491269695));
#61610=CARTESIAN_POINT('Ctrl Pts',(42.602490936903,-4.91835441810297,130.935149645914));
#61611=CARTESIAN_POINT('Ctrl Pts',(42.5948413098278,-4.91292591779319,131.070013994383));
#61612=CARTESIAN_POINT('Ctrl Pts',(42.5871916827525,-4.90193885387951,131.204583724503));
#61613=CARTESIAN_POINT('Ctrl Pts',(42.5795495955671,-4.89096261941543,131.339020815356));
#61614=CARTESIAN_POINT('Ctrl Pts',(42.5719075083817,-4.87443875066124,131.473163465993));
#61615=CARTESIAN_POINT('Ctrl Pts',(42.5642654211963,-4.85239516194762,131.606510388374));
#61616=CARTESIAN_POINT('Ctrl Pts',(42.5563597980065,-4.8295914040353,131.74445575543));
#61617=CARTESIAN_POINT('Ctrl Pts',(42.5484541748166,-4.80088036594323,131.881549087371));
#61618=CARTESIAN_POINT('Ctrl Pts',(42.5405485516268,-4.76635154074265,132.017239858282));
#61619=CARTESIAN_POINT('Ctrl Pts',(42.5329149785985,-4.73301092958273,132.148261206523));
#61620=CARTESIAN_POINT('Ctrl Pts',(42.5252814055703,-4.69424643173644,132.277974505326));
#61621=CARTESIAN_POINT('Ctrl Pts',(42.517647832542,-4.65019063055263,132.405894308133));
#61622=CARTESIAN_POINT('Ctrl Pts',(42.5100153953198,-4.60614138447046,132.533795077639));
#61623=CARTESIAN_POINT('Ctrl Pts',(42.5023829580976,-4.55680253169002,132.659902500209));
#61624=CARTESIAN_POINT('Ctrl Pts',(42.4947505208754,-4.50235621997596,132.783747272806));
#61625=CARTESIAN_POINT('Ctrl Pts',(42.4871174528635,-4.44790540849718,132.907602280667));
#61626=CARTESIAN_POINT('Ctrl Pts',(42.4794843848517,-4.38834646157192,133.029193897404));
#61627=CARTESIAN_POINT('Ctrl Pts',(42.4718513168399,-4.3239090338387,133.148074279596));
#61628=CARTESIAN_POINT('Ctrl Pts',(42.4642158511133,-4.25945136489127,133.266992004734));
#61629=CARTESIAN_POINT('Ctrl Pts',(42.4565803853868,-4.19011236062939,133.383196447527));
#61630=CARTESIAN_POINT('Ctrl Pts',(42.4489449196602,-4.11616654113823,133.496266274924));
#61631=CARTESIAN_POINT('Ctrl Pts',(42.4413012514732,-4.04214128475504,133.609457568493));
#61632=CARTESIAN_POINT('Ctrl Pts',(42.4336575832861,-3.96349955767633,133.719507188693));
#61633=CARTESIAN_POINT('Ctrl Pts',(42.426013915099,-3.88055806622757,133.826024423673));
#61634=CARTESIAN_POINT('Ctrl Pts',(42.4183653414255,-3.79756334531459,133.932610018352));
#61635=CARTESIAN_POINT('Ctrl Pts',(42.410716767752,-3.71026362787921,134.035658409125));
#61636=CARTESIAN_POINT('Ctrl Pts',(42.4030681940785,-3.61901352737722,134.134814663362));
#61637=CARTESIAN_POINT('Ctrl Pts',(42.395409002189,-3.52763674792596,134.234108572353));
#61638=CARTESIAN_POINT('Ctrl Pts',(42.3877498102996,-3.43229892749435,134.329499280756));
#61639=CARTESIAN_POINT('Ctrl Pts',(42.3800906184101,-3.33338899354607,134.420671013564));
#61640=CARTESIAN_POINT('Ctrl Pts',(42.3782372338201,-3.30945459550316,134.442732908221));
#61641=CARTESIAN_POINT('Ctrl Pts',(42.3763838492302,-3.28531116972019,134.464547956016));
#61642=CARTESIAN_POINT('Ctrl Pts',(42.3745304646402,-3.2609644819492,134.486112063545));
#61643=CARTESIAN_POINT('Ctrl Pts',(42.3667561305212,-3.15883819555765,134.576566348002));
#61644=CARTESIAN_POINT('Ctrl Pts',(42.3589817964021,-3.05278369607015,134.662911439298));
#61645=CARTESIAN_POINT('Ctrl Pts',(42.351207462283,-2.94316572360792,134.744786810997));
#61646=CARTESIAN_POINT('Ctrl Pts',(42.3434427093359,-2.83368284549992,134.826561278619));
#61647=CARTESIAN_POINT('Ctrl Pts',(42.3356779563888,-2.72064554274382,134.903876755263));
#61648=CARTESIAN_POINT('Ctrl Pts',(42.3279132034417,-2.6044539598755,134.976410789051));
#61649=CARTESIAN_POINT('Ctrl Pts',(42.3201561625567,-2.48837778012531,135.048872781015));
#61650=CARTESIAN_POINT('Ctrl Pts',(42.3123991216717,-2.36915388432812,135.116562575144));
#61651=CARTESIAN_POINT('Ctrl Pts',(42.3046420807867,-2.24721364146024,135.179199347409));
#61652=CARTESIAN_POINT('Ctrl Pts',(42.2968908895466,-2.12536535467789,135.241788884797));
#61653=CARTESIAN_POINT('Ctrl Pts',(42.2891396983065,-2.00080514443834,135.29933280702));
#61654=CARTESIAN_POINT('Ctrl Pts',(42.2813885070663,-1.87399106614283,135.351595001949));
#61655=CARTESIAN_POINT('Ctrl Pts',(42.2736406102893,-1.74723088721381,135.403834984052));
#61656=CARTESIAN_POINT('Ctrl Pts',(42.2658927135122,-1.61821910624177,135.450797555089));
#61657=CARTESIAN_POINT('Ctrl Pts',(42.2581448167352,-1.48743575252551,135.492293844971));
#61658=CARTESIAN_POINT('Ctrl Pts',(42.2503985406511,-1.35667975586748,135.533781454724));
#61659=CARTESIAN_POINT('Ctrl Pts',(42.242652264567,-1.22415329597946,135.569804939498));
#61660=CARTESIAN_POINT('Ctrl Pts',(42.234905988483,-1.09035325948175,135.600224755762));
#61661=CARTESIAN_POINT('Ctrl Pts',(42.2271596552176,-0.956552235302742,
135.630644796579));
#61662=CARTESIAN_POINT('Ctrl Pts',(42.2194133219523,-0.821477996990924,
135.655460999671));
#61663=CARTESIAN_POINT('Ctrl Pts',(42.211666988687,-0.685638975432793,135.674584663528));
#61664=CARTESIAN_POINT('Ctrl Pts',(42.203918920684,-0.549769533666885,135.693712609997));
#61665=CARTESIAN_POINT('Ctrl Pts',(42.196170852681,-0.413135354924745,135.707145426026));
#61666=CARTESIAN_POINT('Ctrl Pts',(42.188422784678,-0.276250967826932,135.714846180652));
#61667=CARTESIAN_POINT('Ctrl Pts',(42.1806664819362,-0.139221098374127,
135.722555119732));
#61668=CARTESIAN_POINT('Ctrl Pts',(42.1729101791943,-0.001940880323405,
135.724519805782));
#61669=CARTESIAN_POINT('Ctrl Pts',(42.1651538764525,0.135073613629645,135.720755453358));
#61670=CARTESIAN_POINT('Ctrl Pts',(42.1573934339384,0.272161236343732,135.716989091786));
#61671=CARTESIAN_POINT('Ctrl Pts',(42.1496329914242,0.408982462526884,135.707487625964));
#61672=CARTESIAN_POINT('Ctrl Pts',(42.14187254891,0.545026356806567,135.692318200533));
#61673=CARTESIAN_POINT('Ctrl Pts',(42.1340996486446,0.681288640822758,135.677124423794));
#61674=CARTESIAN_POINT('Ctrl Pts',(42.1263267483792,0.816770712723501,135.656244564904));
#61675=CARTESIAN_POINT('Ctrl Pts',(42.1185538481138,0.950970954979181,135.629797106143));
#61676=CARTESIAN_POINT('Ctrl Pts',(42.1110635123517,1.08029268040031,135.604311079124));
#61677=CARTESIAN_POINT('Ctrl Pts',(42.1035731765896,1.20842385407488,135.573655288672));
#61678=CARTESIAN_POINT('Ctrl Pts',(42.0960828408274,1.3349308081423,135.537978979873));
#61679=CARTESIAN_POINT('Ctrl Pts',(42.0883085067084,1.46623431182285,135.500949992983));
#61680=CARTESIAN_POINT('Ctrl Pts',(42.0805341725892,1.59620393004817,135.458394969886));
#61681=CARTESIAN_POINT('Ctrl Pts',(42.0727598384701,1.72433919077393,135.410425903432));
#61682=CARTESIAN_POINT('Ctrl Pts',(42.0649950855231,1.85231653624261,135.362515954565));
#61683=CARTESIAN_POINT('Ctrl Pts',(42.057230332576,1.97846365966066,135.309205374035));
#61684=CARTESIAN_POINT('Ctrl Pts',(42.0494655796289,2.10229298523511,135.250656521656));
#61685=CARTESIAN_POINT('Ctrl Pts',(42.0417085387439,2.22599932177772,135.192165820823));
#61686=CARTESIAN_POINT('Ctrl Pts',(42.0339514978589,2.3473920905378,135.128447367835));
#61687=CARTESIAN_POINT('Ctrl Pts',(42.0261944569739,2.46600186083584,135.05971229338));
#61688=CARTESIAN_POINT('Ctrl Pts',(42.0184432657337,2.58452218658345,134.99102905258));
#61689=CARTESIAN_POINT('Ctrl Pts',(42.0106920744936,2.70026335426499,134.917336915527));
#61690=CARTESIAN_POINT('Ctrl Pts',(42.0029408832534,2.81277912592624,134.83889363283));
#61691=CARTESIAN_POINT('Ctrl Pts',(41.9951929864764,2.92524707538293,134.760483690621));
#61692=CARTESIAN_POINT('Ctrl Pts',(41.9874450896993,3.03449203534917,134.677326842256));
#61693=CARTESIAN_POINT('Ctrl Pts',(41.9796971929222,3.1400956365078,134.589724861081));
#61694=CARTESIAN_POINT('Ctrl Pts',(41.9719509168381,3.24567714766962,134.502141204353));
#61695=CARTESIAN_POINT('Ctrl Pts',(41.964204640754,3.34761851435612,134.410114513748));
#61696=CARTESIAN_POINT('Ctrl Pts',(41.9564583646699,3.44553375528819,134.313987407364));
#61697=CARTESIAN_POINT('Ctrl Pts',(41.9487120314045,3.54344971900859,134.217859591392));
#61698=CARTESIAN_POINT('Ctrl Pts',(41.9409656981392,3.63733921868066,134.117631573139));
#61699=CARTESIAN_POINT('Ctrl Pts',(41.9332193648738,3.72685280789925,134.013683164577));
#61700=CARTESIAN_POINT('Ctrl Pts',(41.9254712968708,3.81638644306539,133.90971147749));
#61701=CARTESIAN_POINT('Ctrl Pts',(41.9177232288679,3.9015419627124,133.802018038411));
#61702=CARTESIAN_POINT('Ctrl Pts',(41.9099751608649,3.98201018048921,133.691015772755));
#61703=CARTESIAN_POINT('Ctrl Pts',(41.902218858123,4.06256392084534,133.579895532571));
#61704=CARTESIAN_POINT('Ctrl Pts',(41.8944625553811,4.1384201779745,133.465459757947));
#61705=CARTESIAN_POINT('Ctrl Pts',(41.8867062526393,4.2093128024148,133.348150859297));
#61706=CARTESIAN_POINT('Ctrl Pts',(41.8789458101251,4.28024326438338,133.230779349356));
#61707=CARTESIAN_POINT('Ctrl Pts',(41.8711853676109,4.3462046268886,133.110532002427));
#61708=CARTESIAN_POINT('Ctrl Pts',(41.8634249250968,4.40697720756797,132.987874976226));
#61709=CARTESIAN_POINT('Ctrl Pts',(41.8556520248314,4.46784734578889,132.865021050079));
#61710=CARTESIAN_POINT('Ctrl Pts',(41.8478791245659,4.52351189835222,132.739750072188));
#61711=CARTESIAN_POINT('Ctrl Pts',(41.8401062243005,4.5737994112277,132.612548110154));
#61712=CARTESIAN_POINT('Ctrl Pts',(41.8326158885385,4.62225884634341,132.489970259843));
#61713=CARTESIAN_POINT('Ctrl Pts',(41.8251255527765,4.66572529076719,132.365599671021));
#61714=CARTESIAN_POINT('Ctrl Pts',(41.8176352170145,4.70408990054633,132.239881871354));
#61715=CARTESIAN_POINT('Ctrl Pts',(41.8098608828954,4.74390911616609,132.109397443102));
#61716=CARTESIAN_POINT('Ctrl Pts',(41.8020865487763,4.77835812334886,131.97704829291));
#61717=CARTESIAN_POINT('Ctrl Pts',(41.7943122146572,4.80726062748651,131.843316016954));
#61718=CARTESIAN_POINT('Ctrl Pts',(41.7865474617101,4.83612751187087,131.709748554077));
#61719=CARTESIAN_POINT('Ctrl Pts',(41.7787827087631,4.85946141215908,131.574801735513));
#61720=CARTESIAN_POINT('Ctrl Pts',(41.771017955816,4.87713537963544,131.438973532033));
#61721=CARTESIAN_POINT('Ctrl Pts',(41.763260914931,4.89479179307817,131.303280235039));
#61722=CARTESIAN_POINT('Ctrl Pts',(41.755503874046,4.90679941067691,131.166707680409));
#61723=CARTESIAN_POINT('Ctrl Pts',(41.747746833161,4.91308212391046,131.029764934764));
#61724=CARTESIAN_POINT('Ctrl Pts',(41.7399956419208,4.91936009930108,130.892925458708));
#61725=CARTESIAN_POINT('Ctrl Pts',(41.7322444506807,4.91992174559568,130.75571673627));
#61726=CARTESIAN_POINT('Ctrl Pts',(41.7244932594406,4.91474271316701,130.618653520578));
#61727=CARTESIAN_POINT('Ctrl Pts',(41.7167453626635,4.90956588196528,130.481648560409));
#61728=CARTESIAN_POINT('Ctrl Pts',(41.7089974658864,4.89865323962955,130.344789373851));
#61729=CARTESIAN_POINT('Ctrl Pts',(41.7012495691094,4.88203253778829,130.208591062724));
#61730=CARTESIAN_POINT('Ctrl Pts',(41.6935032930253,4.86541531263955,130.072421241348));
#61731=CARTESIAN_POINT('Ctrl Pts',(41.6857570169412,4.84309245025204,129.936912408276));
#61732=CARTESIAN_POINT('Ctrl Pts',(41.6780107408571,4.8151435726271,129.802574493941));
#61733=CARTESIAN_POINT('Ctrl Pts',(41.6702644075917,4.78719448868986,129.668235587953));
#61734=CARTESIAN_POINT('Ctrl Pts',(41.6625180743263,4.75361938627987,129.535068000719));
#61735=CARTESIAN_POINT('Ctrl Pts',(41.654771741061,4.71454892764822,129.403571029044));
#61736=CARTESIAN_POINT('Ctrl Pts',(41.647023673058,4.67546971945842,129.272044609535));
#61737=CARTESIAN_POINT('Ctrl Pts',(41.639275605055,4.63089281753342,129.142189924746));
#61738=CARTESIAN_POINT('Ctrl Pts',(41.6315275370521,4.58099850494366,129.014490298184));
#61739=CARTESIAN_POINT('Ctrl Pts',(41.6237712343102,4.5310511640846,128.886654950939));
#61740=CARTESIAN_POINT('Ctrl Pts',(41.6160149315683,4.47577526577443,128.760979602022));
#61741=CARTESIAN_POINT('Ctrl Pts',(41.6082586288265,4.41539916213832,128.637927304148));
#61742=CARTESIAN_POINT('Ctrl Pts',(41.6004981863123,4.35499083395765,128.514809329557));
#61743=CARTESIAN_POINT('Ctrl Pts',(41.5927377437981,4.289477063034,128.394317538938));
#61744=CARTESIAN_POINT('Ctrl Pts',(41.5849773012839,4.21913129737396,128.276888726917));
#61745=CARTESIAN_POINT('Ctrl Pts',(41.5772044010185,4.14867260644606,128.159271407743));
#61746=CARTESIAN_POINT('Ctrl Pts',(41.5694315007531,4.07336663523073,128.044727219706));
#61747=CARTESIAN_POINT('Ctrl Pts',(41.5616586004876,3.99352965107491,127.933663143347));
#61748=CARTESIAN_POINT('Ctrl Pts',(41.5541682647256,3.91659494239102,127.826636525919));
#61749=CARTESIAN_POINT('Ctrl Pts',(41.5466779289637,3.83545311859458,127.722841634013));
#61750=CARTESIAN_POINT('Ctrl Pts',(41.5391875932017,3.75042018191592,127.622610859716));
#61751=CARTESIAN_POINT('Ctrl Pts',(41.5314132590827,3.66216319559726,127.518579805147));
#61752=CARTESIAN_POINT('Ctrl Pts',(41.5236389249636,3.5694346370642,127.418058931271));
#61753=CARTESIAN_POINT('Ctrl Pts',(41.5158645908445,3.47254439527722,127.321456874232));
#61754=CARTESIAN_POINT('Ctrl Pts',(41.5080998378974,3.37577356205404,127.224973870595));
#61755=CARTESIAN_POINT('Ctrl Pts',(41.5003350849504,3.27485152477227,127.13240034774));
#61756=CARTESIAN_POINT('Ctrl Pts',(41.4925703320033,3.17012862146141,127.04411227658));
#61757=CARTESIAN_POINT('Ctrl Pts',(41.4848132911183,3.06550973041472,126.955911894377));
#61758=CARTESIAN_POINT('Ctrl Pts',(41.4770562502333,2.95709778288425,126.871988743871));
#61759=CARTESIAN_POINT('Ctrl Pts',(41.4692992093484,2.84527993251994,126.792682020258));
#61760=CARTESIAN_POINT('Ctrl Pts',(41.4615480181082,2.73354640486565,126.713435102462));
#61761=CARTESIAN_POINT('Ctrl Pts',(41.4537968268681,2.6184124042664,126.63879790754));
#61762=CARTESIAN_POINT('Ctrl Pts',(41.446045635628,2.50029784553984,126.569069158163));
#61763=CARTESIAN_POINT('Ctrl Pts',(41.4382977388509,2.38223348865171,126.499370045365));
#61764=CARTESIAN_POINT('Ctrl Pts',(41.4305498420737,2.26119142920822,126.434575427118));
#61765=CARTESIAN_POINT('Ctrl Pts',(41.4228019452966,2.13762003739266,126.374940380307));
#61766=CARTESIAN_POINT('Ctrl Pts',(41.4150556692125,2.01407449404855,126.315317807863));
#61767=CARTESIAN_POINT('Ctrl Pts',(41.4073093931285,1.88800102258879,126.260852829943));
#61768=CARTESIAN_POINT('Ctrl Pts',(41.3995631170444,1.75987167956568,126.211754088158));
#61769=CARTESIAN_POINT('Ctrl Pts',(41.391816783779,1.63174139072086,126.162654983937));
#61770=CARTESIAN_POINT('Ctrl Pts',(41.3840704505137,1.50155556510905,126.118922334792));
#61771=CARTESIAN_POINT('Ctrl Pts',(41.3763241172483,1.36980490141204,126.080716092989));
#61772=CARTESIAN_POINT('Ctrl Pts',(41.3685760492453,1.23802473306704,126.042501295163));
#61773=CARTESIAN_POINT('Ctrl Pts',(41.3608279812424,1.1046794047361,126.00981547623));
#61774=CARTESIAN_POINT('Ctrl Pts',(41.3530799132394,0.970272997576767,125.982768207099));
#61775=CARTESIAN_POINT('Ctrl Pts',(41.3453236104975,0.835723741688818,125.955692191808));
#61776=CARTESIAN_POINT('Ctrl Pts',(41.3375673077556,0.700111538108701,125.93426677467));
#61777=CARTESIAN_POINT('Ctrl Pts',(41.3298110050138,0.563949396101245,125.918550127879));
#61778=CARTESIAN_POINT('Ctrl Pts',(41.3220505624996,0.427714580258837,125.90282509264));
#61779=CARTESIAN_POINT('Ctrl Pts',(41.3142901199854,0.290929630859906,125.892814927559));
#61780=CARTESIAN_POINT('Ctrl Pts',(41.3065296774712,0.154109840920753,125.888525671249));
#61781=CARTESIAN_POINT('Ctrl Pts',(41.2987567772058,0.0170704157083132,
125.884229529444));
#61782=CARTESIAN_POINT('Ctrl Pts',(41.2909838769404,-0.120003570640024,
125.885672644272));
#61783=CARTESIAN_POINT('Ctrl Pts',(41.283210976675,-0.256598763641481,125.89280891398));
#61784=CARTESIAN_POINT('Ctrl Pts',(41.2757206409129,-0.38822837731555,125.899685762309));
#61785=CARTESIAN_POINT('Ctrl Pts',(41.2682303051508,-0.519413097263414,
125.911849002319));
#61786=CARTESIAN_POINT('Ctrl Pts',(41.2607399693888,-0.649702465683745,
125.929212438425));
#61787=CARTESIAN_POINT('Ctrl Pts',(41.2529656352697,-0.784931795107384,
125.947234214488));
#61788=CARTESIAN_POINT('Ctrl Pts',(41.2451913011506,-0.919624904106275,
125.970915389302));
#61789=CARTESIAN_POINT('Ctrl Pts',(41.2374169670315,-1.05327049296709,126.000216122326));
#61790=CARTESIAN_POINT('Ctrl Pts',(41.2296522140844,-1.18675137558388,126.029480744815));
#61791=CARTESIAN_POINT('Ctrl Pts',(41.2218874611373,-1.31918692848946,126.064351062703));
#61792=CARTESIAN_POINT('Ctrl Pts',(41.2141227081902,-1.45007147044329,126.104735548148));
#61793=CARTESIAN_POINT('Ctrl Pts',(41.2063656673053,-1.58082601602474,126.145079923151));
#61794=CARTESIAN_POINT('Ctrl Pts',(41.1986086264202,-1.71003224512234,126.190927452209));
#61795=CARTESIAN_POINT('Ctrl Pts',(41.1908515855353,-1.83719551720577,126.24213575528));
#61796=CARTESIAN_POINT('Ctrl Pts',(41.1831003942951,-1.96426289447705,126.293305441771));
#61797=CARTESIAN_POINT('Ctrl Pts',(41.175349203055,-2.08929002002813,126.34982771027));
#61798=CARTESIAN_POINT('Ctrl Pts',(41.1675980118148,-2.21179859579991,126.411510741447));
#61799=CARTESIAN_POINT('Ctrl Pts',(41.1598501150377,-2.33425510215862,126.47316755569));
#61800=CARTESIAN_POINT('Ctrl Pts',(41.1521022182607,-2.45419483931453,126.53998059453));
#61801=CARTESIAN_POINT('Ctrl Pts',(41.1443543214836,-2.57116084882389,126.61171050672));
#61802=CARTESIAN_POINT('Ctrl Pts',(41.1366080453995,-2.68810239156556,126.683425414559));
#61803=CARTESIAN_POINT('Ctrl Pts',(41.1288617693154,-2.80207111085763,126.760054945737));
#61804=CARTESIAN_POINT('Ctrl Pts',(41.1211154932313,-2.91263631250718,126.841314721596));
#61805=CARTESIAN_POINT('Ctrl Pts',(41.113369159966,-3.02320233032363,126.922575097296));
#61806=CARTESIAN_POINT('Ctrl Pts',(41.1056228267007,-3.13036446533105,127.008465554344));
#61807=CARTESIAN_POINT('Ctrl Pts',(41.0978764934354,-3.23372291053355,127.098659712151));
#61808=CARTESIAN_POINT('Ctrl Pts',(41.0901284254324,-3.33710450214294,127.188874068314));
#61809=CARTESIAN_POINT('Ctrl Pts',(41.0823803574295,-3.43668041442428,127.283393786046));
#61810=CARTESIAN_POINT('Ctrl Pts',(41.0746322894265,-3.53208599409094,127.381853993344));
#61811=CARTESIAN_POINT('Ctrl Pts',(41.0668759866847,-3.62759297194367,127.480418845322));
#61812=CARTESIAN_POINT('Ctrl Pts',(41.0591196839428,-3.7189204907284,127.582932271623));
#61813=CARTESIAN_POINT('Ctrl Pts',(41.051363381201,-3.80574231449314,127.688994106515));
#61814=CARTESIAN_POINT('Ctrl Pts',(41.0436029386868,-3.89261047767926,127.795112549802));
#61815=CARTESIAN_POINT('Ctrl Pts',(41.0358424961727,-3.97496791937254,127.904782862944));
#61816=CARTESIAN_POINT('Ctrl Pts',(41.0280820536585,-4.05253103065552,128.017574779351));
#61817=CARTESIAN_POINT('Ctrl Pts',(41.0203091533931,-4.13021865313057,128.130547759356));
#61818=CARTESIAN_POINT('Ctrl Pts',(41.0125362531276,-4.2030963575945,128.246652025022));
#61819=CARTESIAN_POINT('Ctrl Pts',(41.0047633528622,-4.2709254501196,128.365430757562));
#61820=CARTESIAN_POINT('Ctrl Pts',(40.9972730171001,-4.33628878428097,128.479891583989));
#61821=CARTESIAN_POINT('Ctrl Pts',(40.989782681338,-4.39696405147731,128.596835532555));
#61822=CARTESIAN_POINT('Ctrl Pts',(40.9822923455758,-4.45278028704966,128.715837029535));
#61823=CARTESIAN_POINT('Ctrl Pts',(40.9735532160698,-4.51790224241996,128.854678534984));
#61824=CARTESIAN_POINT('Ctrl Pts',(40.9648140865637,-4.57659685686595,128.996719232411));
#61825=CARTESIAN_POINT('Ctrl Pts',(40.9560749570576,-4.62856642545606,129.141364553938));
#61826=CARTESIAN_POINT('Ctrl Pts',(40.9473358275515,-4.68053599404616,129.286009875465));
#61827=CARTESIAN_POINT('Ctrl Pts',(40.9385966980454,-4.72578031392211,129.433259538598));
#61828=CARTESIAN_POINT('Ctrl Pts',(40.9298575685393,-4.7640545282341,129.582490119308));
#61829=CARTESIAN_POINT('Origin',(213.235140564004,0.,130.804360617566));
#61830=CARTESIAN_POINT('',(38.8349537180509,-4.76405452823399,129.582490119308));
#61831=CARTESIAN_POINT('',(39.1801134839906,-4.76405452823399,129.582490119308));
#61832=CARTESIAN_POINT('',(213.235140564004,-4.76405452823405,129.582490119308));
#61833=CARTESIAN_POINT('',(40.5148594359403,-4.91824790287309,130.808902465697));
#61834=CARTESIAN_POINT('Ctrl Pts',(40.5148594359403,-4.91824790287309,130.808902465697));
#61835=CARTESIAN_POINT('Ctrl Pts',(40.5049161768737,-4.91808570323451,130.984544188899));
#61836=CARTESIAN_POINT('Ctrl Pts',(40.4949729178071,-4.90851119862581,131.159764942237));
#61837=CARTESIAN_POINT('Ctrl Pts',(40.4850296587406,-4.88968022370207,131.333709625723));
#61838=CARTESIAN_POINT('Ctrl Pts',(40.4748644570866,-4.87042892428828,131.511536912775));
#61839=CARTESIAN_POINT('Ctrl Pts',(40.4646992554327,-4.8415033080866,131.688030791579));
#61840=CARTESIAN_POINT('Ctrl Pts',(40.4545340537788,-4.80311786982472,131.862302861297));
#61841=CARTESIAN_POINT('Ctrl Pts',(40.4513514005557,-4.79109965877848,131.916866221992));
#61842=CARTESIAN_POINT('Ctrl Pts',(40.4481687473327,-4.77815447652257,131.971211951237));
#61843=CARTESIAN_POINT('Ctrl Pts',(40.4449860941096,-4.76428985575759,132.02531320994));
#61844=CARTESIAN_POINT('Ctrl Pts',(40.4372117599905,-4.73042245434591,132.15746749504));
#61845=CARTESIAN_POINT('Ctrl Pts',(40.4294374258714,-4.69099859851613,132.288420888444));
#61846=CARTESIAN_POINT('Ctrl Pts',(40.4216630917524,-4.646118238918,132.417670374709));
#61847=CARTESIAN_POINT('Ctrl Pts',(40.4138983388053,-4.60129319035206,132.546760572534));
#61848=CARTESIAN_POINT('Ctrl Pts',(40.4061335858583,-4.55102514508867,132.674150675636));
#61849=CARTESIAN_POINT('Ctrl Pts',(40.3983688329113,-4.49546471571193,132.799349352444));
#61850=CARTESIAN_POINT('Ctrl Pts',(40.3906117920263,-4.43995946973684,132.924423680161));
#61851=CARTESIAN_POINT('Ctrl Pts',(40.3828547511413,-4.37917245782283,133.047310557983));
#61852=CARTESIAN_POINT('Ctrl Pts',(40.3750977102563,-4.31330348481578,133.167535623861));
#61853=CARTESIAN_POINT('Ctrl Pts',(40.3673465190162,-4.24748418411366,133.287670027081));
#61854=CARTESIAN_POINT('Ctrl Pts',(40.3595953277762,-4.17659073746674,133.405146272263));
#61855=CARTESIAN_POINT('Ctrl Pts',(40.351844136536,-4.10087011277746,133.519512064655));
#61856=CARTESIAN_POINT('Ctrl Pts',(40.344096239759,-4.02518167137358,133.633829248534));
#61857=CARTESIAN_POINT('Ctrl Pts',(40.3363483429819,-3.94467034794428,133.745038283723));
#61858=CARTESIAN_POINT('Ctrl Pts',(40.3286004462048,-3.85962778922341,133.852713679656));
#61859=CARTESIAN_POINT('Ctrl Pts',(40.3208541701207,-3.77460301957251,133.960366552218));
#61860=CARTESIAN_POINT('Ctrl Pts',(40.3131078940367,-3.68504914209772,134.064486949139));
#61861=CARTESIAN_POINT('Ctrl Pts',(40.3053616179526,-3.59129941374683,134.164680778402));
#61862=CARTESIAN_POINT('Ctrl Pts',(40.2976152846872,-3.49754899335675,134.264875347274));
#61863=CARTESIAN_POINT('Ctrl Pts',(40.2898689514219,-3.39960292740766,134.361143005168));
#61864=CARTESIAN_POINT('Ctrl Pts',(40.2821226181566,-3.29783253274478,134.453125291873));
#61865=CARTESIAN_POINT('Ctrl Pts',(40.2743745501536,-3.19603934730779,134.545128177373));
#61866=CARTESIAN_POINT('Ctrl Pts',(40.2666264821506,-3.09042041895151,134.632843519928));
#61867=CARTESIAN_POINT('Ctrl Pts',(40.2588784141477,-2.9813811345578,134.715952313155));
#61868=CARTESIAN_POINT('Ctrl Pts',(40.2511221114058,-2.87222596191505,134.799149435397));
#61869=CARTESIAN_POINT('Ctrl Pts',(40.243365808664,-2.75964348298006,134.877729990855));
#61870=CARTESIAN_POINT('Ctrl Pts',(40.2356095059222,-2.64406959390957,134.951417290082));
#61871=CARTESIAN_POINT('Ctrl Pts',(40.227849063408,-2.52843401957462,135.02514391844));
#61872=CARTESIAN_POINT('Ctrl Pts',(40.2200886208939,-2.40980419173579,135.093971890471));
#61873=CARTESIAN_POINT('Ctrl Pts',(40.2123281783797,-2.28864086209718,135.157670400575));
#61874=CARTESIAN_POINT('Ctrl Pts',(40.2045552781143,-2.16728303032528,135.221471165182));
#61875=CARTESIAN_POINT('Ctrl Pts',(40.1967823778489,-2.04338392315899,135.280125845789));
#61876=CARTESIAN_POINT('Ctrl Pts',(40.1890094775835,-1.91742535379917,135.333451373458));
#61877=CARTESIAN_POINT('Ctrl Pts',(40.1815191418212,-1.79604569570078,135.38483838388));
#61878=CARTESIAN_POINT('Ctrl Pts',(40.1740288060588,-1.67275399734529,135.431276862248));
#61879=CARTESIAN_POINT('Ctrl Pts',(40.1665384702965,-1.54799304614553,135.472647304519));
#61880=CARTESIAN_POINT('Ctrl Pts',(40.1587641361774,-1.41850174556604,135.515586319682));
#61881=CARTESIAN_POINT('Ctrl Pts',(40.1509898020583,-1.28701738984544,135.553201421079));
#61882=CARTESIAN_POINT('Ctrl Pts',(40.1432154679392,-1.15401720588747,135.585304807892));
#61883=CARTESIAN_POINT('Ctrl Pts',(40.1354507149921,-1.02118093276966,135.61736863015));
#61884=CARTESIAN_POINT('Ctrl Pts',(40.127685962045,-0.88683292482405,135.643934162408));
#61885=CARTESIAN_POINT('Ctrl Pts',(40.1199212090979,-0.751467962997216,
135.664862542582));
#61886=CARTESIAN_POINT('Ctrl Pts',(40.1121641682129,-0.616237447558963,
135.685770136395));
#61887=CARTESIAN_POINT('Ctrl Pts',(40.1044071273279,-0.47999237216484,135.701051660835));
#61888=CARTESIAN_POINT('Ctrl Pts',(40.0966500864429,-0.343239830441347,
135.710618813106));
#61889=CARTESIAN_POINT('Ctrl Pts',(40.0888988952028,-0.206590414873348,
135.720178750712));
#61890=CARTESIAN_POINT('Ctrl Pts',(40.0811477039627,-0.069434683119747,
135.724032866279));
#61891=CARTESIAN_POINT('Ctrl Pts',(40.0733965127226,0.0677133442506273,
135.722144464535));
#61892=CARTESIAN_POINT('Ctrl Pts',(40.0656486159455,0.204803080051012,135.720256865413));
#61893=CARTESIAN_POINT('Ctrl Pts',(40.0579007191685,0.341884727871334,135.712631608764));
#61894=CARTESIAN_POINT('Ctrl Pts',(40.0501528223914,0.478442668264895,135.699284077201));
#61895=CARTESIAN_POINT('Ctrl Pts',(40.0424065463073,0.614972043681175,135.685939337654));
#61896=CARTESIAN_POINT('Ctrl Pts',(40.0346602702231,0.750977540703882,135.666874742054));
#61897=CARTESIAN_POINT('Ctrl Pts',(40.0269139941391,0.885947465038371,135.642157652549));
#61898=CARTESIAN_POINT('Ctrl Pts',(40.0191676608737,1.02091838569,135.617440380588));
#61899=CARTESIAN_POINT('Ctrl Pts',(40.0114213276084,1.15485333382986,135.587070601889));
#61900=CARTESIAN_POINT('Ctrl Pts',(40.003674994343,1.28725002090361,135.551166959327));
#61901=CARTESIAN_POINT('Ctrl Pts',(39.99592692634,1.41967635729765,135.515255276394));
#61902=CARTESIAN_POINT('Ctrl Pts',(39.988178858337,1.55056336988004,135.473807365901));
#61903=CARTESIAN_POINT('Ctrl Pts',(39.9804307903341,1.67942354803305,135.426991860572));
#61904=CARTESIAN_POINT('Ctrl Pts',(39.9726744875922,1.80842068031668,135.380126599166));
#61905=CARTESIAN_POINT('Ctrl Pts',(39.9649181848504,1.93538630698516,135.327882480798));
#61906=CARTESIAN_POINT('Ctrl Pts',(39.9571618821086,2.05985202885001,135.270476679845));
#61907=CARTESIAN_POINT('Ctrl Pts',(39.9494014395944,2.18438418181837,135.213040239687));
#61908=CARTESIAN_POINT('Ctrl Pts',(39.9416409970802,2.30641342363896,135.150436805853));
#61909=CARTESIAN_POINT('Ctrl Pts',(39.9338805545661,2.4254965234738,135.082929265738));
#61910=CARTESIAN_POINT('Ctrl Pts',(39.9261076543006,2.5447707860722,135.015313356525));
#61911=CARTESIAN_POINT('Ctrl Pts',(39.9183347540352,2.66108912388129,134.942777816249));
#61912=CARTESIAN_POINT('Ctrl Pts',(39.9105618537698,2.77403708401481,134.865629054768));
#61913=CARTESIAN_POINT('Ctrl Pts',(39.9030715180078,2.88287910129842,134.791284845092));
#61914=CARTESIAN_POINT('Ctrl Pts',(39.8955811822458,2.98859128287934,134.712657179348));
#61915=CARTESIAN_POINT('Ctrl Pts',(39.8880908464837,3.09083374920857,134.63005399227));
#61916=CARTESIAN_POINT('Ctrl Pts',(39.8803165123647,3.19695276972476,134.544318880247));
#61917=CARTESIAN_POINT('Ctrl Pts',(39.8725421782456,3.29966992579652,134.454029249055));
#61918=CARTESIAN_POINT('Ctrl Pts',(39.8647678441265,3.39856926247682,134.359485092271));
#61919=CARTESIAN_POINT('Ctrl Pts',(39.8570030911794,3.49734671456355,134.265057452711));
#61920=CARTESIAN_POINT('Ctrl Pts',(39.8492383382324,3.59231542915399,134.166385987778));
#61921=CARTESIAN_POINT('Ctrl Pts',(39.8414735852853,3.68309113645761,134.063811912347));
#61922=CARTESIAN_POINT('Ctrl Pts',(39.8337165444003,3.7737766840489,133.961339714933));
#61923=CARTESIAN_POINT('Ctrl Pts',(39.8259595035153,3.86027725457758,133.854972911575));
#61924=CARTESIAN_POINT('Ctrl Pts',(39.8182024626303,3.94224445990638,133.745090404683));
#61925=CARTESIAN_POINT('Ctrl Pts',(39.8104512713902,4.02414985312813,133.635290761044));
#61926=CARTESIAN_POINT('Ctrl Pts',(39.80270008015,4.10152845293663,133.521981003073));
#61927=CARTESIAN_POINT('Ctrl Pts',(39.7949488889099,4.17407154588811,133.405573756143));
#61928=CARTESIAN_POINT('Ctrl Pts',(39.7872009921328,4.24658380608992,133.289215985399));
#61929=CARTESIAN_POINT('Ctrl Pts',(39.7794530953558,4.31426444076474,133.169763675257));
#61930=CARTESIAN_POINT('Ctrl Pts',(39.7717051985787,4.37684768683512,133.047658945641));
#61931=CARTESIAN_POINT('Ctrl Pts',(39.7639589224946,4.43941784183948,132.925579757703));
#61932=CARTESIAN_POINT('Ctrl Pts',(39.7562126464105,4.49689255088361,132.800849601582));
#61933=CARTESIAN_POINT('Ctrl Pts',(39.7484663703264,4.54905190438516,132.673935391067));
#61934=CARTESIAN_POINT('Ctrl Pts',(39.7407200370611,4.60121164291528,132.547020243699));
#61935=CARTESIAN_POINT('Ctrl Pts',(39.7329737037957,4.64805579899109,132.417921371384));
#61936=CARTESIAN_POINT('Ctrl Pts',(39.7252273705303,4.68941269099244,132.28712549308));
#61937=CARTESIAN_POINT('Ctrl Pts',(39.7174793025274,4.73077884458294,132.156300323947));
#61938=CARTESIAN_POINT('Ctrl Pts',(39.7097312345245,4.76665517101362,132.023777765306));
#61939=CARTESIAN_POINT('Ctrl Pts',(39.7019831665215,4.79692003437235,131.890059123753));
#61940=CARTESIAN_POINT('Ctrl Pts',(39.6942268637797,4.82721706358803,131.756198364437));
#61941=CARTESIAN_POINT('Ctrl Pts',(39.6864705610378,4.85189062969693,131.621139364756));
#61942=CARTESIAN_POINT('Ctrl Pts',(39.6787142582959,4.87087026645046,131.485393590269));
#61943=CARTESIAN_POINT('Ctrl Pts',(39.6709538157817,4.88986003320762,131.349575364175));
#61944=CARTESIAN_POINT('Ctrl Pts',(39.6631933732676,4.90314977723614,131.213070021823));
#61945=CARTESIAN_POINT('Ctrl Pts',(39.6554329307534,4.91072109605126,131.076392562927));
#61946=CARTESIAN_POINT('Ctrl Pts',(39.647660030488,4.9183045690195,130.939495697241));
#61947=CARTESIAN_POINT('Ctrl Pts',(39.6398871302226,4.92015126749114,130.802426554038));
#61948=CARTESIAN_POINT('Ctrl Pts',(39.6321142299571,4.91629496084988,130.665699446281));
#61949=CARTESIAN_POINT('Ctrl Pts',(39.624623894195,4.91257884066842,130.533942713284));
#61950=CARTESIAN_POINT('Ctrl Pts',(39.6171335584329,4.9035671749343,130.402503887071));
#61951=CARTESIAN_POINT('Ctrl Pts',(39.6096432226708,4.88933532466376,130.271835364179));
#61952=CARTESIAN_POINT('Ctrl Pts',(39.6018688885517,4.87456386946474,130.136212504527));
#61953=CARTESIAN_POINT('Ctrl Pts',(39.5940945544325,4.85412177746983,130.000989900916));
#61954=CARTESIAN_POINT('Ctrl Pts',(39.5863202203134,4.82803660796453,129.866679661881));
#61955=CARTESIAN_POINT('Ctrl Pts',(39.5785554673663,4.80198358609935,129.732534948212));
#61956=CARTESIAN_POINT('Ctrl Pts',(39.5707907144193,4.7703013981057,129.599300741992));
#61957=CARTESIAN_POINT('Ctrl Pts',(39.5630259614722,4.73306941051397,129.467484775254));
#61958=CARTESIAN_POINT('Ctrl Pts',(39.5552689205872,4.6958744022572,129.335799729993));
#61959=CARTESIAN_POINT('Ctrl Pts',(39.5475118797022,4.65314066939234,129.205530494815));
#61960=CARTESIAN_POINT('Ctrl Pts',(39.5397548388172,4.60499868094981,129.077174984534));
#61961=CARTESIAN_POINT('Ctrl Pts',(39.5320036475771,4.55689299675532,128.948916268143));
#61962=CARTESIAN_POINT('Ctrl Pts',(39.5242524563369,4.50338731154936,128.822568768721));
#61963=CARTESIAN_POINT('Ctrl Pts',(39.5165012650968,4.44466191158653,128.698615249723));
#61964=CARTESIAN_POINT('Ctrl Pts',(39.5087533683197,4.38596147148516,128.574714414277));
#61965=CARTESIAN_POINT('Ctrl Pts',(39.5010054715426,4.32204589613112,128.453205888094));
#61966=CARTESIAN_POINT('Ctrl Pts',(39.4932575747656,4.25314350210117,128.334552241794));
#61967=CARTESIAN_POINT('Ctrl Pts',(39.4855112986814,4.18425552096667,128.215923415279));
#61968=CARTESIAN_POINT('Ctrl Pts',(39.4777650225973,4.11038299221635,128.100148618704));
#61969=CARTESIAN_POINT('Ctrl Pts',(39.4700187465132,4.03179987714314,127.987665246538));
#61970=CARTESIAN_POINT('Ctrl Pts',(39.4622724132479,3.95321618198722,127.875181044046));
#61971=CARTESIAN_POINT('Ctrl Pts',(39.4545260799825,3.86992205502932,127.765988634942));
#61972=CARTESIAN_POINT('Ctrl Pts',(39.4467797467172,3.78223418860525,127.660495543323));
#61973=CARTESIAN_POINT('Ctrl Pts',(39.4390316787142,3.69452668509149,127.554978827257));
#61974=CARTESIAN_POINT('Ctrl Pts',(39.4312836107112,3.60242373403662,127.453163377772));
#61975=CARTESIAN_POINT('Ctrl Pts',(39.4235355427082,3.50628135169511,127.355422499064));
#61976=CARTESIAN_POINT('Ctrl Pts',(39.4157792399664,3.41003678808554,127.257577740187));
#61977=CARTESIAN_POINT('Ctrl Pts',(39.4080229372245,3.30974449175124,127.163816481901));
#61978=CARTESIAN_POINT('Ctrl Pts',(39.4002666344827,3.20579668442348,127.074474469084));
#61979=CARTESIAN_POINT('Ctrl Pts',(39.3925061919685,3.10179339702101,126.985084771744));
#61980=CARTESIAN_POINT('Ctrl Pts',(39.3847457494543,2.99413101773505,126.900119261838));
#61981=CARTESIAN_POINT('Ctrl Pts',(39.3769853069401,2.88323288341853,126.819871791823));
#61982=CARTESIAN_POINT('Ctrl Pts',(39.3692124066747,2.77215672557187,126.739495501444));
#61983=CARTESIAN_POINT('Ctrl Pts',(39.3614395064092,2.6578347590267,126.663852601717));
#61984=CARTESIAN_POINT('Ctrl Pts',(39.3536666061438,2.54071794302273,126.593192680223));
#61985=CARTESIAN_POINT('Ctrl Pts',(39.3461762703818,2.42785861828093,126.525101424858));
#61986=CARTESIAN_POINT('Ctrl Pts',(39.3386859346199,2.31240438579782,126.461637298325));
#61987=CARTESIAN_POINT('Ctrl Pts',(39.3311955988579,2.19477659406254,126.402981428646));
#61988=CARTESIAN_POINT('Ctrl Pts',(39.3234212647388,2.07268890885039,126.34210160384));
#61989=CARTESIAN_POINT('Ctrl Pts',(39.3156469306198,1.94787285268034,126.286208994538));
#61990=CARTESIAN_POINT('Ctrl Pts',(39.3078725965007,1.82077417343337,126.235557221505));
#61991=CARTESIAN_POINT('Ctrl Pts',(39.3001078435536,1.6938321319496,126.184967872255));
#61992=CARTESIAN_POINT('Ctrl Pts',(39.2923430906065,1.56461342437721,126.139606651412));
#61993=CARTESIAN_POINT('Ctrl Pts',(39.2845783376594,1.43358811960335,126.099681227232));
#61994=CARTESIAN_POINT('Ctrl Pts',(39.2768212967744,1.30269295100914,126.059795457546));
#61995=CARTESIAN_POINT('Ctrl Pts',(39.2690642558894,1.16999512759449,126.025334853671));
#61996=CARTESIAN_POINT('Ctrl Pts',(39.2613072150044,1.03598408089232,125.996458783435));
#61997=CARTESIAN_POINT('Ctrl Pts',(39.2535560237643,0.902074092962925,125.967604488869));
#61998=CARTESIAN_POINT('Ctrl Pts',(39.2458048325241,0.766853233548651,125.944326427545));
#61999=CARTESIAN_POINT('Ctrl Pts',(39.238053641284,0.630825114341994,125.926733864973));
#62000=CARTESIAN_POINT('Ctrl Pts',(39.2303057445069,0.49485481071467,125.909148779708));
#62001=CARTESIAN_POINT('Ctrl Pts',(39.2225578477298,0.358078316632711,125.897244437024));
#62002=CARTESIAN_POINT('Ctrl Pts',(39.2148099509527,0.221008216546887,125.891078778437));
#62003=CARTESIAN_POINT('Ctrl Pts',(39.2070636748686,0.0839667885711129,
125.884914409572));
#62004=CARTESIAN_POINT('Ctrl Pts',(39.1993173987846,-0.0533677329258113,
125.884486354684));
#62005=CARTESIAN_POINT('Ctrl Pts',(39.1915711227005,-0.19047927282011,125.889800544769));
#62006=CARTESIAN_POINT('Ctrl Pts',(39.1838247894351,-0.327591824840462,
125.895114774083));
#62007=CARTESIAN_POINT('Ctrl Pts',(39.1760784561697,-0.464481001301833,
125.906171317812));
#62008=CARTESIAN_POINT('Ctrl Pts',(39.1683321229044,-0.600632760697747,
125.922924010452));
#62009=CARTESIAN_POINT('Ctrl Pts',(39.1605840549014,-0.736815010336169,
125.939680454741));
#62010=CARTESIAN_POINT('Ctrl Pts',(39.1528359868984,-0.872259126336232,
125.962135538527));
#62011=CARTESIAN_POINT('Ctrl Pts',(39.1450879188954,-1.00645860182237,125.990191515289));
#62012=CARTESIAN_POINT('Ctrl Pts',(39.1373316161535,-1.14080070610824,126.018277310277));
#62013=CARTESIAN_POINT('Ctrl Pts',(39.1295753134117,-1.27389514410548,126.051975809259));
#62014=CARTESIAN_POINT('Ctrl Pts',(39.1218190106699,-1.40524743871289,126.091138503291));
#62015=CARTESIAN_POINT('Ctrl Pts',(39.1140585681557,-1.53666983999487,126.130322099632));
#62016=CARTESIAN_POINT('Ctrl Pts',(39.1062981256415,-1.66634787563082,126.17497557498));
#62017=CARTESIAN_POINT('Ctrl Pts',(39.0985376831273,-1.79380549531682,126.224901598482));
#62018=CARTESIAN_POINT('Ctrl Pts',(39.0907647828619,-1.92146772128909,126.274907767669));
#62019=CARTESIAN_POINT('Ctrl Pts',(39.0829918825965,-2.04690205053444,126.330203240907));
#62020=CARTESIAN_POINT('Ctrl Pts',(39.0752189823311,-2.1696547434678,126.390543521599));
#62021=CARTESIAN_POINT('Ctrl Pts',(39.067728646569,-2.28794506681733,126.448690281101));
#62022=CARTESIAN_POINT('Ctrl Pts',(39.060238310807,-2.40374506665103,126.511521286134));
#62023=CARTESIAN_POINT('Ctrl Pts',(39.052747975045,-2.51667460568438,126.578779948403));
#62024=CARTESIAN_POINT('Ctrl Pts',(39.0449724104948,-2.63390445335527,126.648599791819));
#62025=CARTESIAN_POINT('Ctrl Pts',(39.0371968459445,-2.74841230454186,126.723412384054));
#62026=CARTESIAN_POINT('Ctrl Pts',(39.0294212813942,-2.85974362927395,126.802979676275));
#62027=CARTESIAN_POINT('Ctrl Pts',(39.0213184662549,-2.97576056125208,126.885895721256));
#62028=CARTESIAN_POINT('Ctrl Pts',(39.0132156511156,-3.08832735937844,126.97397528201));
#62029=CARTESIAN_POINT('Ctrl Pts',(39.0051128359763,-3.19695741531961,127.066895387342));
#62030=CARTESIAN_POINT('Ctrl Pts',(38.9973568344204,-3.30093792930302,127.155838361992));
#62031=CARTESIAN_POINT('Ctrl Pts',(38.9896008328644,-3.40131135378676,127.249215834932));
#62032=CARTESIAN_POINT('Ctrl Pts',(38.9818448313085,-3.49768059149839,127.346700492228));
#62033=CARTESIAN_POINT('Ctrl Pts',(38.9740941166275,-3.59398413916415,127.444118699152));
#62034=CARTESIAN_POINT('Ctrl Pts',(38.9663434019464,-3.68628865685686,127.54563824343));
#62035=CARTESIAN_POINT('Ctrl Pts',(38.9585926872654,-3.77423163532291,127.650892903219));
#62036=CARTESIAN_POINT('Ctrl Pts',(38.9508455772586,-3.86213371358698,127.756098611553));
#62037=CARTESIAN_POINT('Ctrl Pts',(38.9430984672518,-3.94567803950475,127.865035678907));
#62038=CARTESIAN_POINT('Ctrl Pts',(38.9353513572451,-4.02454063916857,127.977302834962));
#62039=CARTESIAN_POINT('Ctrl Pts',(38.927606172512,-4.10338364028701,128.089542090936));
#62040=CARTESIAN_POINT('Ctrl Pts',(38.919860987779,-4.17754700765423,128.205109468018));
#62041=CARTESIAN_POINT('Ctrl Pts',(38.9121158030459,-4.24674880726832,128.323572913939));
#62042=CARTESIAN_POINT('Ctrl Pts',(38.9043689020301,-4.31596594155246,128.442062610593));
#62043=CARTESIAN_POINT('Ctrl Pts',(38.8966220010143,-4.3802191108475,128.563449322638));
#62044=CARTESIAN_POINT('Ctrl Pts',(38.8888750999985,-4.43927126633542,128.687274486491));
#62045=CARTESIAN_POINT('Ctrl Pts',(38.8811271588079,-4.49833135074438,128.811116276325));
#62046=CARTESIAN_POINT('Ctrl Pts',(38.8733792176173,-4.5521888696628,128.937396813788));
#62047=CARTESIAN_POINT('Ctrl Pts',(38.8656312764266,-4.60065440837986,129.065636350422));
#62048=CARTESIAN_POINT('Ctrl Pts',(38.8578781666516,-4.64915227803773,129.19396143454));
#62049=CARTESIAN_POINT('Ctrl Pts',(38.8501250568766,-4.69225085665429,129.324247758232));
#62050=CARTESIAN_POINT('Ctrl Pts',(38.8423719471015,-4.72981017110029,129.455999090432));
#62051=CARTESIAN_POINT('Ctrl Pts',(38.8398992040847,-4.74178917503666,129.498019285697));
#62052=CARTESIAN_POINT('Ctrl Pts',(38.8374264610678,-4.7532051111186,129.540188406638));
#62053=CARTESIAN_POINT('Ctrl Pts',(38.8349537180509,-4.76405452823399,129.582490119308));
#62054=CARTESIAN_POINT('Ctrl Pts',(40.5848681886094,-4.76405452823407,129.582490119308));
#62055=CARTESIAN_POINT('Ctrl Pts',(40.5772090494279,-4.79778048213594,129.713987101709));
#62056=CARTESIAN_POINT('Ctrl Pts',(40.5695499102464,-4.82605472140716,129.846869198006));
#62057=CARTESIAN_POINT('Ctrl Pts',(40.5618907710649,-4.84877990805882,129.980639508388));
#62058=CARTESIAN_POINT('Ctrl Pts',(40.5540522152193,-4.87203743615042,130.1175434115));
#62059=CARTESIAN_POINT('Ctrl Pts',(40.5462136593737,-4.88948262910061,130.255377224386));
#62060=CARTESIAN_POINT('Ctrl Pts',(40.5383751035281,-4.9010672107594,130.393601249908));
#62061=CARTESIAN_POINT('Ctrl Pts',(40.5305365476825,-4.9126517924182,130.531825275429));
#62062=CARTESIAN_POINT('Ctrl Pts',(40.5226979918368,-4.91837576946825,130.670439064928));
#62063=CARTESIAN_POINT('Ctrl Pts',(40.5148594359912,-4.91824790287392,130.808902464798));
#62064=CARTESIAN_POINT('',(40.8601405640435,-4.91824972738764,130.802723073242));
#62065=CARTESIAN_POINT('Ctrl Pts',(40.9298575685393,-4.7640545282341,129.582490119308));
#62066=CARTESIAN_POINT('Ctrl Pts',(40.9214669057054,-4.80080258504007,129.725770235065));
#62067=CARTESIAN_POINT('Ctrl Pts',(40.9130762428715,-4.83112548624056,129.870876032944));
#62068=CARTESIAN_POINT('Ctrl Pts',(40.9046855800376,-4.85485483549579,130.017234459467));
#62069=CARTESIAN_POINT('Ctrl Pts',(40.8963228592268,-4.87850516286214,130.163105492966));
#62070=CARTESIAN_POINT('Ctrl Pts',(40.8879601384161,-4.89560567749403,130.310220558013));
#62071=CARTESIAN_POINT('Ctrl Pts',(40.8795974176054,-4.90603855309564,130.457995524003));
#62072=CARTESIAN_POINT('Ctrl Pts',(40.8731117997514,-4.91412965715151,130.572600803729));
#62073=CARTESIAN_POINT('Ctrl Pts',(40.8666261818975,-4.91821139772449,130.687602613548));
#62074=CARTESIAN_POINT('Ctrl Pts',(40.8601405640435,-4.91824972738764,130.802723073242));
#62075=CARTESIAN_POINT('Ctrl Pts',(40.8601405640087,-4.91824972738784,130.802723073859));
#62076=CARTESIAN_POINT('Ctrl Pts',(40.8522035403277,-4.91829663476603,130.94360615321));
#62077=CARTESIAN_POINT('Ctrl Pts',(40.8442665166468,-4.9122858041172,131.084440600289));
#62078=CARTESIAN_POINT('Ctrl Pts',(40.8363294929658,-4.90025605756969,131.224686244612));
#62079=CARTESIAN_POINT('Ctrl Pts',(40.8283877865347,-4.88821921361388,131.365014632208));
#62080=CARTESIAN_POINT('Ctrl Pts',(40.8204460801035,-4.87015640705927,131.504753162815));
#62081=CARTESIAN_POINT('Ctrl Pts',(40.8125043736724,-4.84615817870192,131.643368346673));
#62082=CARTESIAN_POINT('Ctrl Pts',(40.8045566451859,-4.82214175291309,131.782088639969));
#62083=CARTESIAN_POINT('Ctrl Pts',(40.7966089166995,-4.79218099659783,131.91968353129));
#62084=CARTESIAN_POINT('Ctrl Pts',(40.7886611882131,-4.75641721715871,132.05563129924));
#62085=CARTESIAN_POINT('Ctrl Pts',(40.7807003308895,-4.72059435960237,132.191803639041));
#62086=CARTESIAN_POINT('Ctrl Pts',(40.7727394735659,-4.67894941910968,132.326323067667));
#62087=CARTESIAN_POINT('Ctrl Pts',(40.7647786162423,-4.63167343917663,132.45868350483));
#62088=CARTESIAN_POINT('Ctrl Pts',(40.7568105101511,-4.58435441204664,132.591164462939));
#62089=CARTESIAN_POINT('Ctrl Pts',(40.7488424040599,-4.53139425756292,132.721482173791));
#62090=CARTESIAN_POINT('Ctrl Pts',(40.7408742979687,-4.47303136480114,132.849152409413));
#62091=CARTESIAN_POINT('Ctrl Pts',(40.7328915946058,-4.4145615534073,132.977056532122));
#62092=CARTESIAN_POINT('Ctrl Pts',(40.7249088912429,-4.35066939059248,133.102303164801));
#62093=CARTESIAN_POINT('Ctrl Pts',(40.71692618788,-4.28163876750627,133.224433452645));
#62094=CARTESIAN_POINT('Ctrl Pts',(40.7125656991743,-4.24393133449366,133.291146158424));
#62095=CARTESIAN_POINT('Ctrl Pts',(40.7082052104686,-4.20469143898111,133.35692952447));
#62096=CARTESIAN_POINT('Ctrl Pts',(40.7038447217628,-4.16397055502691,133.421712767998));
#62097=CARTESIAN_POINT('Ctrl Pts',(40.6960703876438,-4.09136911540656,133.537215092277));
#62098=CARTESIAN_POINT('Ctrl Pts',(40.6882960535247,-4.01384324528631,133.649877291414));
#62099=CARTESIAN_POINT('Ctrl Pts',(40.6805217194056,-3.93164171057593,133.759250890006));
#62100=CARTESIAN_POINT('Ctrl Pts',(40.6727569664586,-3.84954148191063,133.868489695412));
#62101=CARTESIAN_POINT('Ctrl Pts',(40.6649922135115,-3.76277728662918,133.974447654812));
#62102=CARTESIAN_POINT('Ctrl Pts',(40.6572274605645,-3.67164256570979,134.076702887587));
#62103=CARTESIAN_POINT('Ctrl Pts',(40.6494704196795,-3.58059836107999,134.178856559024));
#62104=CARTESIAN_POINT('Ctrl Pts',(40.6417133787945,-3.48519252777902,134.277314532446));
#62105=CARTESIAN_POINT('Ctrl Pts',(40.6339563379096,-3.38576016846868,134.371686106516));
#62106=CARTESIAN_POINT('Ctrl Pts',(40.6262051466694,-3.28640279187396,134.465986514247));
#62107=CARTESIAN_POINT('Ctrl Pts',(40.6184539554293,-3.18302521553785,134.55620638828));
#62108=CARTESIAN_POINT('Ctrl Pts',(40.6107027641892,-3.07600071497427,134.641990441295));
#62109=CARTESIAN_POINT('Ctrl Pts',(40.6029548674121,-2.9690217026784,134.7277380338));
#62110=CARTESIAN_POINT('Ctrl Pts',(40.595206970635,-2.85839915349167,134.809053311082));
#62111=CARTESIAN_POINT('Ctrl Pts',(40.587459073858,-2.74454070384922,134.885620152001));
#62112=CARTESIAN_POINT('Ctrl Pts',(40.5797127977739,-2.63070607093977,134.962170976787));
#62113=CARTESIAN_POINT('Ctrl Pts',(40.5719665216897,-2.51363720815222,135.033975122847));
#62114=CARTESIAN_POINT('Ctrl Pts',(40.5642202456056,-2.39377178794625,135.100759073218));
#62115=CARTESIAN_POINT('Ctrl Pts',(40.5564739123403,-2.27390548292081,135.167543516574));
#62116=CARTESIAN_POINT('Ctrl Pts',(40.5487275790749,-2.15124292081674,135.229307500008));
#62117=CARTESIAN_POINT('Ctrl Pts',(40.5409812458096,-2.0262471367856,135.285823057793));
#62118=CARTESIAN_POINT('Ctrl Pts',(40.5332331778066,-1.90122336081511,135.342351271846));
#62119=CARTESIAN_POINT('Ctrl Pts',(40.5254851098036,-1.77386567936097,135.393628560402));
#62120=CARTESIAN_POINT('Ctrl Pts',(40.5177370418006,-1.64465752394219,135.439474930228));
#62121=CARTESIAN_POINT('Ctrl Pts',(40.5099807390587,-1.51531204455876,135.485370026121));
#62122=CARTESIAN_POINT('Ctrl Pts',(40.502224436317,-1.38411253154962,135.525822542056));
#62123=CARTESIAN_POINT('Ctrl Pts',(40.4944681335751,-1.25155854787594,135.560702096449));
#62124=CARTESIAN_POINT('Ctrl Pts',(40.486707691061,-1.11893381614987,135.595600267109));
#62125=CARTESIAN_POINT('Ctrl Pts',(40.4789472485467,-0.984953555016894,
135.624919465832));
#62126=CARTESIAN_POINT('Ctrl Pts',(40.4711868060326,-0.850126986043015,
135.64858059297));
#62127=CARTESIAN_POINT('Ctrl Pts',(40.4634139057671,-0.715083981491278,
135.672279703049));
#62128=CARTESIAN_POINT('Ctrl Pts',(40.4556410055017,-0.579192342040389,
135.690302539705));
#62129=CARTESIAN_POINT('Ctrl Pts',(40.4478681052363,-0.44296676926654,135.702621891102));
#62130=CARTESIAN_POINT('Ctrl Pts',(40.4403777694742,-0.311693339193058,
135.714493403046));
#62131=CARTESIAN_POINT('Ctrl Pts',(40.4328874337121,-0.180110140553368,
135.721068887151));
#62132=CARTESIAN_POINT('Ctrl Pts',(40.42539709795,-0.0486753042053006,135.722369744973));
#62133=CARTESIAN_POINT('Ctrl Pts',(40.4176227638309,0.0877429239103127,
135.723719925215));
#62134=CARTESIAN_POINT('Ctrl Pts',(40.4098484297119,0.224433449278738,135.719391885597));
#62135=CARTESIAN_POINT('Ctrl Pts',(40.4020740955928,0.360884492790618,135.709352508014));
#62136=CARTESIAN_POINT('Ctrl Pts',(40.3943093426457,0.49716737258635,135.699325503067));
#62137=CARTESIAN_POINT('Ctrl Pts',(40.3865445896986,0.633210971597971,135.68360119351));
#62138=CARTESIAN_POINT('Ctrl Pts',(40.3787798367515,0.768501737697219,135.662198422769));
#62139=CARTESIAN_POINT('Ctrl Pts',(40.3710227958665,0.903658131100496,135.640816909561));
#62140=CARTESIAN_POINT('Ctrl Pts',(40.3632657549815,1.03806279593239,135.613768219576));
#62141=CARTESIAN_POINT('Ctrl Pts',(40.3555087140965,1.17120589291698,135.581123100556));
#62142=CARTESIAN_POINT('Ctrl Pts',(40.3477575228563,1.30424858565607,135.548502599473));
#62143=CARTESIAN_POINT('Ctrl Pts',(40.3400063316162,1.43603122598697,135.510294162354));
#62144=CARTESIAN_POINT('Ctrl Pts',(40.3322551403761,1.56605313609324,135.466619794986));
#62145=CARTESIAN_POINT('Ctrl Pts',(40.324507243599,1.69601978341925,135.422963990388));
#62146=CARTESIAN_POINT('Ctrl Pts',(40.316759346822,1.8242268191064,135.373847000371));
#62147=CARTESIAN_POINT('Ctrl Pts',(40.3090114500449,1.95018794403604,135.319440909813));
#62148=CARTESIAN_POINT('Ctrl Pts',(40.3012651739608,2.07612272061392,135.265046199836));
#62149=CARTESIAN_POINT('Ctrl Pts',(40.2935188978767,2.19981216219578,135.20536474487));
#62150=CARTESIAN_POINT('Ctrl Pts',(40.2857726217926,2.32078957856036,135.14061692855));
#62151=CARTESIAN_POINT('Ctrl Pts',(40.2780262885272,2.44176788795276,135.075868634276));
#62152=CARTESIAN_POINT('Ctrl Pts',(40.2702799552619,2.56003378747939,135.006054088509));
#62153=CARTESIAN_POINT('Ctrl Pts',(40.2625336219966,2.67514520130848,134.931439634791));
#62154=CARTESIAN_POINT('Ctrl Pts',(40.2547855539936,2.79028239354058,134.856808471683));
#62155=CARTESIAN_POINT('Ctrl Pts',(40.2470374859906,2.90226336636071,134.777375474301));
#62156=CARTESIAN_POINT('Ctrl Pts',(40.2392894179876,3.01067537982031,134.693450076532));
#62157=CARTESIAN_POINT('Ctrl Pts',(40.2315331152458,3.11920261485793,134.609435481853));
#62158=CARTESIAN_POINT('Ctrl Pts',(40.2237768125039,3.22415300369695,134.520919188765));
#62159=CARTESIAN_POINT('Ctrl Pts',(40.216020509762,3.32514682663451,134.428251019306));
#62160=CARTESIAN_POINT('Ctrl Pts',(40.2082600672478,3.42619455301623,134.335533390054));
#62161=CARTESIAN_POINT('Ctrl Pts',(40.2004996247337,3.52328122905683,134.238659744916));
#62162=CARTESIAN_POINT('Ctrl Pts',(40.1927391822195,3.61606505928803,134.138015751124));
#62163=CARTESIAN_POINT('Ctrl Pts',(40.1849662819541,3.70899783436048,134.037210194658));
#62164=CARTESIAN_POINT('Ctrl Pts',(40.1771933816887,3.79761370773354,133.932622493182));
#62165=CARTESIAN_POINT('Ctrl Pts',(40.1694204814232,3.88161157654487,133.824670971045));
#62166=CARTESIAN_POINT('Ctrl Pts',(40.1619301456613,3.96255591124648,133.720643758652));
#62167=CARTESIAN_POINT('Ctrl Pts',(40.1544398098993,4.03921198521355,133.613493296783));
#62168=CARTESIAN_POINT('Ctrl Pts',(40.1469494741373,4.11135017326076,133.503616591965));
#62169=CARTESIAN_POINT('Ctrl Pts',(40.1391751400182,4.18622350263413,133.389573878487));
#62170=CARTESIAN_POINT('Ctrl Pts',(40.1314008058991,4.25646676814036,133.272232857086));
#62171=CARTESIAN_POINT('Ctrl Pts',(40.1236264717801,4.32177547747018,133.152006200877));
#62172=CARTESIAN_POINT('Ctrl Pts',(40.115861718833,4.38700369965256,133.031927713276));
#62173=CARTESIAN_POINT('Ctrl Pts',(40.1080969658859,4.44730928100165,132.908971007069));
#62174=CARTESIAN_POINT('Ctrl Pts',(40.1003322129388,4.50243048755657,132.783578333539));
#62175=CARTESIAN_POINT('Ctrl Pts',(40.0925751720538,4.55749694695214,132.65831020178));
#62176=CARTESIAN_POINT('Ctrl Pts',(40.0848181311688,4.60738912236687,132.530611273081));
#62177=CARTESIAN_POINT('Ctrl Pts',(40.0770610902838,4.65189095529825,132.400948730548));
#62178=CARTESIAN_POINT('Ctrl Pts',(40.0693098990437,4.69635922905119,132.271383967546));
#62179=CARTESIAN_POINT('Ctrl Pts',(40.0615587078035,4.7354451248525,132.139858906402));
#62180=CARTESIAN_POINT('Ctrl Pts',(40.0538075165634,4.76898066103704,132.006860728649));
#62181=CARTESIAN_POINT('Ctrl Pts',(40.0460596197863,4.80250194372415,131.873919078669));
#62182=CARTESIAN_POINT('Ctrl Pts',(40.0383117230092,4.83047746337694,131.73950593568));
#62183=CARTESIAN_POINT('Ctrl Pts',(40.0305638262321,4.85278914332629,131.604123452983));
#62184=CARTESIAN_POINT('Ctrl Pts',(40.022817550148,4.87509615615314,131.468769289383));
#62185=CARTESIAN_POINT('Ctrl Pts',(40.0150712740638,4.8917416222805,131.332446574903));
#62186=CARTESIAN_POINT('Ctrl Pts',(40.0073249979797,4.90265869923977,131.195667071983));
#62187=CARTESIAN_POINT('Ctrl Pts',(39.9995786647144,4.91357585678645,131.058886559388));
#62188=CARTESIAN_POINT('Ctrl Pts',(39.991832331449,4.91876450968101,130.921649641349));
#62189=CARTESIAN_POINT('Ctrl Pts',(39.9840859981836,4.91820978750425,130.784472213976));
#62190=CARTESIAN_POINT('Ctrl Pts',(39.9763379301807,4.91765494110131,130.64726406667));
#62191=CARTESIAN_POINT('Ctrl Pts',(39.9685898621777,4.91135416184055,130.510115827427));
#62192=CARTESIAN_POINT('Ctrl Pts',(39.9608417941748,4.89934468919312,130.37354200263));
#62193=CARTESIAN_POINT('Ctrl Pts',(39.9530854914329,4.88732245273522,130.236823025547));
#62194=CARTESIAN_POINT('Ctrl Pts',(39.945329188691,4.86957943717226,130.100680072523));
#62195=CARTESIAN_POINT('Ctrl Pts',(39.9375728859492,4.84620470991631,129.965621699854));
#62196=CARTESIAN_POINT('Ctrl Pts',(39.929812443435,4.82281750686462,129.830491242464));
#62197=CARTESIAN_POINT('Ctrl Pts',(39.9220520009209,4.79379268547922,129.696446900806));
#62198=CARTESIAN_POINT('Ctrl Pts',(39.9142915584067,4.75926996972727,129.563984699648));
#62199=CARTESIAN_POINT('Ctrl Pts',(39.9065186581413,4.72469183504721,129.431309858404));
#62200=CARTESIAN_POINT('Ctrl Pts',(39.8987457578758,4.68459828383862,129.300222607059));
#62201=CARTESIAN_POINT('Ctrl Pts',(39.8909728576104,4.63917851077378,129.171202386507));
#62202=CARTESIAN_POINT('Ctrl Pts',(39.8834825218483,4.59540986086505,129.046872375954));
#62203=CARTESIAN_POINT('Ctrl Pts',(39.8759921860863,4.54669562304279,128.924462007975));
#62204=CARTESIAN_POINT('Ctrl Pts',(39.8685018503242,4.49324569212165,128.804379064469));
#62205=CARTESIAN_POINT('Ctrl Pts',(39.8607275162051,4.43776919082428,128.679743139661));
#62206=CARTESIAN_POINT('Ctrl Pts',(39.852953182086,4.37701506704252,128.557219802717));
#62207=CARTESIAN_POINT('Ctrl Pts',(39.8451788479669,4.31116592882415,128.437288291538));
#62208=CARTESIAN_POINT('Ctrl Pts',(39.8374140950198,4.24539794378352,128.317504585229));
#62209=CARTESIAN_POINT('Ctrl Pts',(39.8296493420727,4.17454762430183,128.200306688608));
#62210=CARTESIAN_POINT('Ctrl Pts',(39.8218845891257,4.09884557530925,128.08615385349));
#62211=CARTESIAN_POINT('Ctrl Pts',(39.8141275482407,4.02321871465893,127.972114396578));
#62212=CARTESIAN_POINT('Ctrl Pts',(39.8063705073557,3.9427499288189,127.8611143062));
#62213=CARTESIAN_POINT('Ctrl Pts',(39.7986134664707,3.85771548726882,127.753587882375));
#62214=CARTESIAN_POINT('Ctrl Pts',(39.7908622752305,3.77274517085235,127.646142545062));
#62215=CARTESIAN_POINT('Ctrl Pts',(39.7831110839904,3.68321629333454,127.542165965727));
#62216=CARTESIAN_POINT('Ctrl Pts',(39.7753598927503,3.58944793614549,127.442062805622));
#62217=CARTESIAN_POINT('Ctrl Pts',(39.7676119959732,3.49571943300985,127.342002192032));
#62218=CARTESIAN_POINT('Ctrl Pts',(39.7598640991961,3.39775530074743,127.245812008031));
#62219=CARTESIAN_POINT('Ctrl Pts',(39.752116202419,3.29591419182915,127.153863020991));
#62220=CARTESIAN_POINT('Ctrl Pts',(39.744369926335,3.19409438587555,127.061933267698));
#62221=CARTESIAN_POINT('Ctrl Pts',(39.7366236502509,3.0883995063539,126.974243208577));
#62222=CARTESIAN_POINT('Ctrl Pts',(39.7288773741668,2.97922398351145,126.89112570019));
#62223=CARTESIAN_POINT('Ctrl Pts',(39.7211310409015,2.87004765476009,126.808007578249));
#62224=CARTESIAN_POINT('Ctrl Pts',(39.7133847076362,2.75739094249258,126.729462311221));
#62225=CARTESIAN_POINT('Ctrl Pts',(39.7056383743708,2.64167984689107,126.655781264459));
#62226=CARTESIAN_POINT('Ctrl Pts',(39.6978903063679,2.52594283859184,126.582083717337));
#62227=CARTESIAN_POINT('Ctrl Pts',(39.6901422383649,2.40715041558078,126.513252768033));
#62228=CARTESIAN_POINT('Ctrl Pts',(39.6823941703619,2.28575557549405,126.449535189194));
#62229=CARTESIAN_POINT('Ctrl Pts',(39.6746378676201,2.16423171552666,126.385749890553));
#62230=CARTESIAN_POINT('Ctrl Pts',(39.6668815648782,2.04010026006971,126.327089000469));
#62231=CARTESIAN_POINT('Ctrl Pts',(39.6591252621364,1.91383721504967,126.273752471104));
#62232=CARTESIAN_POINT('Ctrl Pts',(39.6513648196222,1.7875067796408,126.220387474427));
#62233=CARTESIAN_POINT('Ctrl Pts',(39.643604377108,1.65904285374134,126.172352637803));
#62234=CARTESIAN_POINT('Ctrl Pts',(39.6358439345939,1.52893828125394,126.129798521004));
#62235=CARTESIAN_POINT('Ctrl Pts',(39.6280710343285,1.39862485335665,126.087176092559));
#62236=CARTESIAN_POINT('Ctrl Pts',(39.6202981340631,1.26666589244829,126.050052071362));
#62237=CARTESIAN_POINT('Ctrl Pts',(39.6125252337977,1.13356703007465,126.018526432094));
#62238=CARTESIAN_POINT('Ctrl Pts',(39.6050348980356,1.00530664660302,125.988146829222));
#62239=CARTESIAN_POINT('Ctrl Pts',(39.5975445622735,0.8759881017261,125.962965703229));
#62240=CARTESIAN_POINT('Ctrl Pts',(39.5900542265114,0.746067927177802,125.943026879739));
#62241=CARTESIAN_POINT('Ctrl Pts',(39.5822798923923,0.611221789724072,125.922332069696));
#62242=CARTESIAN_POINT('Ctrl Pts',(39.5745055582732,0.475300348405679,125.907219378263));
#62243=CARTESIAN_POINT('Ctrl Pts',(39.5667312241541,0.33880550375241,125.897794211908));
#62244=CARTESIAN_POINT('Ctrl Pts',(39.558966471207,0.202478876796096,125.888380661229));
#62245=CARTESIAN_POINT('Ctrl Pts',(39.5512017182599,0.0655806388564525,
125.884640715753));
#62246=CARTESIAN_POINT('Ctrl Pts',(39.5434369653128,-0.0713781809104709,
125.886628597845));
#62247=CARTESIAN_POINT('Ctrl Pts',(39.5356799244278,-0.208200971246262,
125.888614505544));
#62248=CARTESIAN_POINT('Ctrl Pts',(39.5279228835428,-0.345083835272505,
125.896316913889));
#62249=CARTESIAN_POINT('Ctrl Pts',(39.5201658426578,-0.481512053682665,
125.909738139309));
#62250=CARTESIAN_POINT('Ctrl Pts',(39.5124146514177,-0.617837390513364,
125.923149243679));
#62251=CARTESIAN_POINT('Ctrl Pts',(39.5046634601775,-0.75370837664104,125.942270543025));
#62252=CARTESIAN_POINT('Ctrl Pts',(39.4969122689373,-0.888612087786601,
125.967052314394));
#62253=CARTESIAN_POINT('Ctrl Pts',(39.4891643721602,-1.02345846125552,125.991823552849));
#62254=CARTESIAN_POINT('Ctrl Pts',(39.4814164753831,-1.15733799369815,126.022250407781));
#62255=CARTESIAN_POINT('Ctrl Pts',(39.473668578606,-1.28974488760317,126.058231543531));
#62256=CARTESIAN_POINT('Ctrl Pts',(39.4659223025219,-1.42212408483981,126.094205152802));
#62257=CARTESIAN_POINT('Ctrl Pts',(39.4581760264378,-1.5530308792119,126.135730629475));
#62258=CARTESIAN_POINT('Ctrl Pts',(39.4504297503537,-1.68197202988457,126.182656045313));
#62259=CARTESIAN_POINT('Ctrl Pts',(39.4426834170884,-1.81091413237188,126.229581807544));
#62260=CARTESIAN_POINT('Ctrl Pts',(39.434937083823,-1.93789019481426,126.281907454775));
#62261=CARTESIAN_POINT('Ctrl Pts',(39.4271907505576,-2.06242481978431,126.339432071079));
#62262=CARTESIAN_POINT('Ctrl Pts',(39.4194426825546,-2.18698733342016,126.396969569621));
#62263=CARTESIAN_POINT('Ctrl Pts',(39.4116946145517,-2.30910696676692,126.459708190089));
#62264=CARTESIAN_POINT('Ctrl Pts',(39.4039465465487,-2.42833124672092,126.527400199384));
#62265=CARTESIAN_POINT('Ctrl Pts',(39.3961902438068,-2.54768223965844,126.595164152551));
#62266=CARTESIAN_POINT('Ctrl Pts',(39.388433941065,-2.66413139160323,126.66789181765));
#62267=CARTESIAN_POINT('Ctrl Pts',(39.3806776383231,-2.77725318430666,126.745290796442));
#62268=CARTESIAN_POINT('Ctrl Pts',(39.372917195809,-2.89043535351673,126.822731085399));
#62269=CARTESIAN_POINT('Ctrl Pts',(39.3651567532948,-3.00028631184022,126.904847422035));
#62270=CARTESIAN_POINT('Ctrl Pts',(39.3573963107806,-3.10641299490876,126.991306544049));
#62271=CARTESIAN_POINT('Ctrl Pts',(39.3496234105152,-3.21271004195058,127.077904457922));
#62272=CARTESIAN_POINT('Ctrl Pts',(39.3418505102498,-3.31527057403758,127.168858828746));
#62273=CARTESIAN_POINT('Ctrl Pts',(39.3340776099843,-3.41373717343956,127.263798293135));
#62274=CARTESIAN_POINT('Ctrl Pts',(39.3265872742224,-3.50862426392981,127.355286468856));
#62275=CARTESIAN_POINT('Ctrl Pts',(39.3190969384604,-3.59970969067984,127.450474809468));
#62276=CARTESIAN_POINT('Ctrl Pts',(39.3116066026985,-3.68670981539713,127.549002910715));
#62277=CARTESIAN_POINT('Ctrl Pts',(39.3039014951383,-3.77620451096235,127.650356126637));
#62278=CARTESIAN_POINT('Ctrl Pts',(39.2961963875781,-3.86167199230871,127.755578846841));
#62279=CARTESIAN_POINT('Ctrl Pts',(39.2884912800179,-3.94275437005546,127.864314522705));
#62280=CARTESIAN_POINT('Ctrl Pts',(39.2807954511361,-4.0237391064261,127.972919256417));
#62281=CARTESIAN_POINT('Ctrl Pts',(39.2730996222543,-4.10034900457173,128.085028217023));
#62282=CARTESIAN_POINT('Ctrl Pts',(39.2654037933725,-4.1722639134616,128.200249080222));
#62283=CARTESIAN_POINT('Ctrl Pts',(39.2577168462748,-4.24409582509387,128.315336966605));
#62284=CARTESIAN_POINT('Ctrl Pts',(39.250029899177,-4.31124332455259,128.433529270244));
#62285=CARTESIAN_POINT('Ctrl Pts',(39.2423429520793,-4.37342782573868,128.554402370052));
#62286=CARTESIAN_POINT('Ctrl Pts',(39.2346611715276,-4.43557053151691,128.675194228709));
#62287=CARTESIAN_POINT('Ctrl Pts',(39.2269793909759,-4.49275669100498,128.798662947593));
#62288=CARTESIAN_POINT('Ctrl Pts',(39.2192976104242,-4.54475224278082,128.924357927611));
#62289=CARTESIAN_POINT('Ctrl Pts',(39.211619031124,-4.59672612629417,129.050000526382));
#62290=CARTESIAN_POINT('Ctrl Pts',(39.2039404518238,-4.6435135511543,129.177867174037));
#62291=CARTESIAN_POINT('Ctrl Pts',(39.1962618725236,-4.68492764495315,129.307485197214));
#62292=CARTESIAN_POINT('Ctrl Pts',(39.1908790763459,-4.71395952924944,129.398349323564));
#62293=CARTESIAN_POINT('Ctrl Pts',(39.1854962801682,-4.74035182336093,129.490073632747));
#62294=CARTESIAN_POINT('Ctrl Pts',(39.1801134839905,-4.76405452823399,129.582490119308));
#62295=CARTESIAN_POINT('Origin',(213.235140564004,0.,130.804360617566));
#62296=CARTESIAN_POINT('',(37.0846781642943,-4.76405452823403,129.582490119308));
#62297=CARTESIAN_POINT('',(37.4302319972992,-4.76405452823409,129.582490119308));
#62298=CARTESIAN_POINT('',(213.235140564004,-4.76405452823405,129.582490119308));
#62299=CARTESIAN_POINT('',(38.7648594359501,-4.91824989201514,130.803329990072));
#62300=CARTESIAN_POINT('Ctrl Pts',(38.7648594359501,-4.91824989201514,130.803329990072));
#62301=CARTESIAN_POINT('Ctrl Pts',(38.7571284799429,-4.91827832612957,130.939020218589));
#62302=CARTESIAN_POINT('Ctrl Pts',(38.7493975239357,-4.91268714457348,131.074935898356));
#62303=CARTESIAN_POINT('Ctrl Pts',(38.7416665679285,-4.90144643826978,131.210569769694));
#62304=CARTESIAN_POINT('Ctrl Pts',(38.7339450451304,-4.89021944772569,131.346038142394));
#62305=CARTESIAN_POINT('Ctrl Pts',(38.7262235223324,-4.87335667787914,131.481225000161));
#62306=CARTESIAN_POINT('Ctrl Pts',(38.7185019995344,-4.8508801956055,131.615621605401));
#62307=CARTESIAN_POINT('Ctrl Pts',(38.7107879983121,-4.82842560779075,131.749887294204));
#62308=CARTESIAN_POINT('Ctrl Pts',(38.7030739970898,-4.80036825250335,131.883363874273));
#62309=CARTESIAN_POINT('Ctrl Pts',(38.6953599958675,-4.76678207865275,132.015546679711));
#62310=CARTESIAN_POINT('Ctrl Pts',(38.6876516116237,-4.73322036069873,132.147633235751));
#62311=CARTESIAN_POINT('Ctrl Pts',(38.6799432273799,-4.69413793299307,132.278427509872));
#62312=CARTESIAN_POINT('Ctrl Pts',(38.6722348431361,-4.6496599296308,132.407434415395));
#62313=CARTESIAN_POINT('Ctrl Pts',(38.664529411506,-4.6051989630897,132.53639190621));
#62314=CARTESIAN_POINT('Ctrl Pts',(38.656823979876,-4.55534665848608,132.663563016094));
#62315=CARTESIAN_POINT('Ctrl Pts',(38.6491185482459,-4.50027809824341,132.788467494972));
#62316=CARTESIAN_POINT('Ctrl Pts',(38.6414144491673,-4.44521906137262,132.91335037329));
#62317=CARTESIAN_POINT('Ctrl Pts',(38.6337103500887,-4.38494572239737,133.035967038157));
#62318=CARTESIAN_POINT('Ctrl Pts',(38.6260062510101,-4.31968124987413,133.15585736687));
#62319=CARTESIAN_POINT('Ctrl Pts',(38.6183017685783,-4.25441352981426,133.275753661282));
#62320=CARTESIAN_POINT('Ctrl Pts',(38.6105972861466,-4.18415437138044,133.392923002053));
#62321=CARTESIAN_POINT('Ctrl Pts',(38.6028928037148,-4.10917260174733,133.506930430087));
#62322=CARTESIAN_POINT('Ctrl Pts',(38.5951862220833,-4.03417040222643,133.620968921124));
#62323=CARTESIAN_POINT('Ctrl Pts',(38.5874796404517,-3.95444324922921,133.731843455126));
#62324=CARTESIAN_POINT('Ctrl Pts',(38.5797730588201,-3.87030266124698,133.839148974741));
#62325=CARTESIAN_POINT('Ctrl Pts',(38.5720581865016,-3.78607155540491,133.946569932888));
#62326=CARTESIAN_POINT('Ctrl Pts',(38.5643433141832,-3.69741777832495,134.05041389815));
#62327=CARTESIAN_POINT('Ctrl Pts',(38.5566284418647,-3.6046926910649,134.150309461389));
#62328=CARTESIAN_POINT('Ctrl Pts',(38.5489090297513,-3.51191303998919,134.250263807891));
#62329=CARTESIAN_POINT('Ctrl Pts',(38.5411896176381,-3.41505758782715,134.346264846846));
#62330=CARTESIAN_POINT('Ctrl Pts',(38.5334702055248,-3.31451291341551,134.437979641253));
#62331=CARTESIAN_POINT('Ctrl Pts',(38.5257391821786,-3.21381700370119,134.529832389409));
#62332=CARTESIAN_POINT('Ctrl Pts',(38.5180081588324,-3.10942109242567,134.617385763959));
#62333=CARTESIAN_POINT('Ctrl Pts',(38.5102771354862,-3.00174347226363,134.700348193165));
#62334=CARTESIAN_POINT('Ctrl Pts',(38.5054689994639,-2.93477579914787,134.751944809357));
#62335=CARTESIAN_POINT('Ctrl Pts',(38.5006608634416,-2.86653935663988,134.801766539492));
#62336=CARTESIAN_POINT('Ctrl Pts',(38.4958527274192,-2.79713972328847,134.849752122835));
#62337=CARTESIAN_POINT('Ctrl Pts',(38.4880783933002,-2.68492660475101,134.927340601212));
#62338=CARTESIAN_POINT('Ctrl Pts',(38.4803040591811,-2.56930501935536,135.000379499363));
#62339=CARTESIAN_POINT('Ctrl Pts',(38.472529725062,-2.45068021440031,135.068554509645));
#62340=CARTESIAN_POINT('Ctrl Pts',(38.4647649721149,-2.33220160391541,135.136645500321));
#62341=CARTESIAN_POINT('Ctrl Pts',(38.4570002191679,-2.21072747387373,135.199884337073));
#62342=CARTESIAN_POINT('Ctrl Pts',(38.4492354662208,-2.08669366730699,135.257998748501));
#62343=CARTESIAN_POINT('Ctrl Pts',(38.4414784253358,-1.962783052866,135.316055439877));
#62344=CARTESIAN_POINT('Ctrl Pts',(38.4337213844507,-1.83631817294624,135.368997669762));
#62345=CARTESIAN_POINT('Ctrl Pts',(38.4259643435658,-1.70776089130751,135.416598230766));
#62346=CARTESIAN_POINT('Ctrl Pts',(38.4182131523256,-1.57930055571454,135.464162895818));
#62347=CARTESIAN_POINT('Ctrl Pts',(38.4104619610856,-1.44875132426562,135.50639377466));
#62348=CARTESIAN_POINT('Ctrl Pts',(38.4027107698455,-1.31659620710292,135.543111242989));
#62349=CARTESIAN_POINT('Ctrl Pts',(38.3949628730684,-1.18449725939038,135.579813105414));
#62350=CARTESIAN_POINT('Ctrl Pts',(38.3872149762913,-1.05079415940023,135.611006113622));
#62351=CARTESIAN_POINT('Ctrl Pts',(38.3794670795142,-0.915986082312354,
135.636560174653));
#62352=CARTESIAN_POINT('Ctrl Pts',(38.3717208034301,-0.781206204167893,
135.662108890325));
#62353=CARTESIAN_POINT('Ctrl Pts',(38.363974527346,-0.645322192552095,135.682020932234));
#62354=CARTESIAN_POINT('Ctrl Pts',(38.3562282512619,-0.508844058494613,
135.696217196273));
#62355=CARTESIAN_POINT('Ctrl Pts',(38.3484819179966,-0.372364916987106,
135.710413565105));
#62356=CARTESIAN_POINT('Ctrl Pts',(38.3407355847312,-0.235292033153742,
135.718894031424));
#62357=CARTESIAN_POINT('Ctrl Pts',(38.3329892514659,-0.0981407976885719,
135.721631349011));
#62358=CARTESIAN_POINT('Ctrl Pts',(38.3252411834629,0.0390411518450279,
135.724369279601));
#62359=CARTESIAN_POINT('Ctrl Pts',(38.31749311546,0.176301097113004,135.721361494392));
#62360=CARTESIAN_POINT('Ctrl Pts',(38.309745047457,0.313123786251959,135.712632875396));
#62361=CARTESIAN_POINT('Ctrl Pts',(38.3019887447152,0.450091892173327,135.70389497952));
#62362=CARTESIAN_POINT('Ctrl Pts',(38.2942324419733,0.586621422841188,135.689424128992));
#62363=CARTESIAN_POINT('Ctrl Pts',(38.2864761392314,0.722201831039167,135.669297161627));
#62364=CARTESIAN_POINT('Ctrl Pts',(38.2787156967173,0.857854602583064,135.649159451894));
#62365=CARTESIAN_POINT('Ctrl Pts',(38.2709552542032,0.99255685846541,135.623359683539));
#62366=CARTESIAN_POINT('Ctrl Pts',(38.263194811689,1.12580936377113,135.592025637066));
#62367=CARTESIAN_POINT('Ctrl Pts',(38.2554219114236,1.25927577782815,135.5606412904));
#62368=CARTESIAN_POINT('Ctrl Pts',(38.2476490111581,1.39128741396276,135.523705017729));
#62369=CARTESIAN_POINT('Ctrl Pts',(38.2398761108927,1.52136042919586,135.481394453982));
#62370=CARTESIAN_POINT('Ctrl Pts',(38.2323857751306,1.64670496269283,135.4406219858));
#62371=CARTESIAN_POINT('Ctrl Pts',(38.2248954393685,1.77024908689878,135.394859287784));
#62372=CARTESIAN_POINT('Ctrl Pts',(38.2174051036063,1.89158010045018,135.344306408661));
#62373=CARTESIAN_POINT('Ctrl Pts',(38.2096307694872,2.01751141625654,135.291836801762));
#62374=CARTESIAN_POINT('Ctrl Pts',(38.2018564353682,2.14145740096002,135.234040395919));
#62375=CARTESIAN_POINT('Ctrl Pts',(38.1940821012491,2.26293457257786,135.171088246206));
#62376=CARTESIAN_POINT('Ctrl Pts',(38.186317348302,2.38426203443824,135.108213679392));
#62377=CARTESIAN_POINT('Ctrl Pts',(38.1785525953548,2.50312639327234,135.040196189421));
#62378=CARTESIAN_POINT('Ctrl Pts',(38.1707878424077,2.61906299563609,134.967255294037));
#62379=CARTESIAN_POINT('Ctrl Pts',(38.1630308015227,2.73488444813212,134.894386844578));
#62380=CARTESIAN_POINT('Ctrl Pts',(38.1552737606378,2.84778360220955,134.816604927869));
#62381=CARTESIAN_POINT('Ctrl Pts',(38.1475167197528,2.95731965321308,134.734175311826));
#62382=CARTESIAN_POINT('Ctrl Pts',(38.1397655285127,3.06677310222863,134.651807856597));
#62383=CARTESIAN_POINT('Ctrl Pts',(38.1320143372725,3.17286818507974,134.564799912393));
#62384=CARTESIAN_POINT('Ctrl Pts',(38.1242631460323,3.2751926999721,134.473460758002));
#62385=CARTESIAN_POINT('Ctrl Pts',(38.1165152492553,3.37747372421589,134.382160425188));
#62386=CARTESIAN_POINT('Ctrl Pts',(38.1087673524782,3.47598707687795,134.286532803366));
#62387=CARTESIAN_POINT('Ctrl Pts',(38.1010194557011,3.57035349068835,134.186927544329));
#62388=CARTESIAN_POINT('Ctrl Pts',(38.093273179617,3.66470016507914,134.087343120564));
#62389=CARTESIAN_POINT('Ctrl Pts',(38.085526903533,3.75490135730511,133.983782998187));
#62390=CARTESIAN_POINT('Ctrl Pts',(38.0777806274489,3.8406148414214,133.876633506219));
#62391=CARTESIAN_POINT('Ctrl Pts',(38.0700342941836,3.92632895825492,133.769483223298));
#62392=CARTESIAN_POINT('Ctrl Pts',(38.0622879609182,4.00755505665235,133.658743823216));
#62393=CARTESIAN_POINT('Ctrl Pts',(38.0545416276528,4.08399163233707,133.544834191513));
#62394=CARTESIAN_POINT('Ctrl Pts',(38.0467935596499,4.16044532546293,133.430899050537));
#62395=CARTESIAN_POINT('Ctrl Pts',(38.039045491647,4.23210714375918,133.313792589805));
#62396=CARTESIAN_POINT('Ctrl Pts',(38.031297423644,4.29871951494976,133.193961754637));
#62397=CARTESIAN_POINT('Ctrl Pts',(38.0235411209022,4.36540268256133,133.074003561831));
#62398=CARTESIAN_POINT('Ctrl Pts',(38.0157848181603,4.42702549242186,132.951315552782));
#62399=CARTESIAN_POINT('Ctrl Pts',(38.0080285154185,4.48337662711915,132.826368798039));
#62400=CARTESIAN_POINT('Ctrl Pts',(38.0002680729043,4.53975783811389,132.701355355451));
#62401=CARTESIAN_POINT('Ctrl Pts',(37.9925076303902,4.5908616218996,132.574081127621));
#62402=CARTESIAN_POINT('Ctrl Pts',(37.984747187876,4.63652563516663,132.445035203504));
#62403=CARTESIAN_POINT('Ctrl Pts',(37.9769742876105,4.68226295236154,132.315782123414));
#62404=CARTESIAN_POINT('Ctrl Pts',(37.9692013873451,4.72254293396779,132.184752037572));
#62405=CARTESIAN_POINT('Ctrl Pts',(37.9614284870797,4.75725350033361,132.052448032799));
#62406=CARTESIAN_POINT('Ctrl Pts',(37.9539381513176,4.79070225018148,131.924953611853));
#62407=CARTESIAN_POINT('Ctrl Pts',(37.9464478155556,4.81897941313919,131.796276585114));
#62408=CARTESIAN_POINT('Ctrl Pts',(37.9389574797935,4.84203022070033,131.666872301153));
#62409=CARTESIAN_POINT('Ctrl Pts',(37.9311831456744,4.86595500663622,131.532561614435));
#62410=CARTESIAN_POINT('Ctrl Pts',(37.9234088115554,4.88432508580291,131.397041978058));
#62411=CARTESIAN_POINT('Ctrl Pts',(37.9156344774363,4.89702303785638,131.260812618552));
#62412=CARTESIAN_POINT('Ctrl Pts',(37.9078697244892,4.90970534081879,131.124751149556));
#62413=CARTESIAN_POINT('Ctrl Pts',(37.9001049715421,4.91672938952374,130.987982083306));
#62414=CARTESIAN_POINT('Ctrl Pts',(37.892340218595,4.91802871393031,130.851015000607));
#62415=CARTESIAN_POINT('Ctrl Pts',(37.88458317771,4.91932674782958,130.714183955545));
#62416=CARTESIAN_POINT('Ctrl Pts',(37.8768261368249,4.91491136889733,130.577155673838));
#62417=CARTESIAN_POINT('Ctrl Pts',(37.8690690959399,4.90476790952643,130.44044467098));
#62418=CARTESIAN_POINT('Ctrl Pts',(37.8613179046998,4.89463209941722,130.303836762953));
#62419=CARTESIAN_POINT('Ctrl Pts',(37.8535667134597,4.87877683556304,130.167546045853));
#62420=CARTESIAN_POINT('Ctrl Pts',(37.8458155222196,4.85723951782926,130.032086489463));
#62421=CARTESIAN_POINT('Ctrl Pts',(37.8380676254425,4.83571135402995,129.896684506997));
#62422=CARTESIAN_POINT('Ctrl Pts',(37.8303197286654,4.8085060009122,129.76211336793));
#62423=CARTESIAN_POINT('Ctrl Pts',(37.8225718318884,4.77571262720884,129.628881155892));
#62424=CARTESIAN_POINT('Ctrl Pts',(37.8148255558042,4.74292611317228,129.49567681316));
#62425=CARTESIAN_POINT('Ctrl Pts',(37.8070792797201,4.70455399692611,129.363811219768));
#62426=CARTESIAN_POINT('Ctrl Pts',(37.799333003636,4.66073632653493,129.233781120368));
#62427=CARTESIAN_POINT('Ctrl Pts',(37.7915866703707,4.61691833269178,129.103750061116));
#62428=CARTESIAN_POINT('Ctrl Pts',(37.7838403371053,4.56765482934145,128.975554893387));
#62429=CARTESIAN_POINT('Ctrl Pts',(37.77609400384,4.51313526632565,128.849675699133));
#62430=CARTESIAN_POINT('Ctrl Pts',(37.768345935837,4.45860349403173,128.723768315107));
#62431=CARTESIAN_POINT('Ctrl Pts',(37.7605978678341,4.39881347521647,128.600178295296));
#62432=CARTESIAN_POINT('Ctrl Pts',(37.7528497998311,4.3340020135298,128.479363927414));
#62433=CARTESIAN_POINT('Ctrl Pts',(37.7450934970892,4.26912166945028,128.358421156583));
#62434=CARTESIAN_POINT('Ctrl Pts',(37.7373371943474,4.19920940668318,128.240260275687));
#62435=CARTESIAN_POINT('Ctrl Pts',(37.7295808916055,4.12454732799884,128.125313697186));
#62436=CARTESIAN_POINT('Ctrl Pts',(37.7218204490913,4.04984539991507,128.010305768235));
#62437=CARTESIAN_POINT('Ctrl Pts',(37.7140600065772,3.97038883086328,127.898515878614));
#62438=CARTESIAN_POINT('Ctrl Pts',(37.706299564063,3.88650135470987,127.790344976874));
#62439=CARTESIAN_POINT('Ctrl Pts',(37.6985266637975,3.80247921493244,127.682000429599));
#62440=CARTESIAN_POINT('Ctrl Pts',(37.6907537635321,3.71401220670041,127.5772867783));
#62441=CARTESIAN_POINT('Ctrl Pts',(37.6829808632666,3.62146300941391,127.476570249477));
#62442=CARTESIAN_POINT('Ctrl Pts',(37.6754905275045,3.53227820856576,127.379515020166));
#62443=CARTESIAN_POINT('Ctrl Pts',(37.6680001917425,3.43930307893425,127.286171566055));
#62444=CARTESIAN_POINT('Ctrl Pts',(37.6605098559805,3.34289111445189,127.196832092465));
#62445=CARTESIAN_POINT('Ctrl Pts',(37.6527355218614,3.24282366103296,127.10410528558));
#62446=CARTESIAN_POINT('Ctrl Pts',(37.6449611877423,3.13873662933688,127.015398343996));
#62447=CARTESIAN_POINT('Ctrl Pts',(37.6371868536232,3.03098656421825,126.931079900909));
#62448=CARTESIAN_POINT('Ctrl Pts',(37.6294221006761,2.92336929142483,126.846865372767));
#62449=CARTESIAN_POINT('Ctrl Pts',(37.621657347729,2.81209827238428,126.767028820582));
#62450=CARTESIAN_POINT('Ctrl Pts',(37.6138925947819,2.69756630317921,126.691901608354));
#62451=CARTESIAN_POINT('Ctrl Pts',(37.6061355538969,2.58314808874105,126.616849013532));
#62452=CARTESIAN_POINT('Ctrl Pts',(37.5983785130119,2.46547569433492,126.546496663514));
#62453=CARTESIAN_POINT('Ctrl Pts',(37.5906214721269,2.34497406821629,126.481135006764));
#62454=CARTESIAN_POINT('Ctrl Pts',(37.5828702808868,2.22456331331063,126.415822639748));
#62455=CARTESIAN_POINT('Ctrl Pts',(37.5751190896467,2.10132791566018,126.355493660594));
#62456=CARTESIAN_POINT('Ctrl Pts',(37.5673678984065,1.97572050814078,126.300394416959));
#62457=CARTESIAN_POINT('Ctrl Pts',(37.5596200016294,1.85016648712079,126.245318591973));
#62458=CARTESIAN_POINT('Ctrl Pts',(37.5518721048523,1.72224281868317,126.195468238298));
#62459=CARTESIAN_POINT('Ctrl Pts',(37.5441242080752,1.59242516585422,126.151042967367));
#62460=CARTESIAN_POINT('Ctrl Pts',(37.5363779319911,1.46263466807933,126.106626989245));
#62461=CARTESIAN_POINT('Ctrl Pts',(37.528631655907,1.33095134360888,126.067633963173));
#62462=CARTESIAN_POINT('Ctrl Pts',(37.5208853798229,1.19786881718728,126.034214565367));
#62463=CARTESIAN_POINT('Ctrl Pts',(37.5131390465576,1.06478530838106,126.000794920866));
#62464=CARTESIAN_POINT('Ctrl Pts',(37.5053927132922,0.930302956205765,125.972949081951));
#62465=CARTESIAN_POINT('Ctrl Pts',(37.4976463800269,0.794928069472048,125.950777155127));
#62466=CARTESIAN_POINT('Ctrl Pts',(37.4898983120239,0.659522866471439,125.928600263053));
#62467=CARTESIAN_POINT('Ctrl Pts',(37.4821502440209,0.523225116931304,125.912099874661));
#62468=CARTESIAN_POINT('Ctrl Pts',(37.474402176018,0.386548389441731,125.901324476039));
#62469=CARTESIAN_POINT('Ctrl Pts',(37.4666458732761,0.249726400299151,125.890537625195));
#62470=CARTESIAN_POINT('Ctrl Pts',(37.4588895705342,0.112525018983439,125.885487949514));
#62471=CARTESIAN_POINT('Ctrl Pts',(37.4511332677924,-0.0245394702169603,
125.886171837446));
#62472=CARTESIAN_POINT('Ctrl Pts',(37.4433728252782,-0.161677114861992,
125.886856090389));
#62473=CARTESIAN_POINT('Ctrl Pts',(37.4356123827641,-0.298677331461582,
125.893279986299));
#62474=CARTESIAN_POINT('Ctrl Pts',(37.4278519402499,-0.435027804581187,
125.905387881191));
#62475=CARTESIAN_POINT('Ctrl Pts',(37.4200790399845,-0.571597159585056,
125.917515212752));
#62476=CARTESIAN_POINT('Ctrl Pts',(37.412306139719,-0.70751429894357,125.935344725993));
#62477=CARTESIAN_POINT('Ctrl Pts',(37.4045332394536,-0.842275068855532,
125.958769242833));
#62478=CARTESIAN_POINT('Ctrl Pts',(37.3970429036916,-0.972136945338934,
125.981342219483));
#62479=CARTESIAN_POINT('Ctrl Pts',(37.3895525679296,-1.10092476551482,126.009110412247));
#62480=CARTESIAN_POINT('Ctrl Pts',(37.3820622321676,-1.22820161666663,126.041934360781));
#62481=CARTESIAN_POINT('Ctrl Pts',(37.3742878980485,-1.36030420831501,126.0760028393));
#62482=CARTESIAN_POINT('Ctrl Pts',(37.3665135639294,-1.49119745367912,126.11562593825));
#62483=CARTESIAN_POINT('Ctrl Pts',(37.3587392298104,-1.62037849000892,126.160702941594));
#62484=CARTESIAN_POINT('Ctrl Pts',(37.3509744768633,-1.74940032225669,126.205724391559));
#62485=CARTESIAN_POINT('Ctrl Pts',(37.3432097239161,-1.87671377843557,126.256186244665));
#62486=CARTESIAN_POINT('Ctrl Pts',(37.335444970969,-2.0018277567502,126.311937140777));
#62487=CARTESIAN_POINT('Ctrl Pts',(37.327687930084,-2.12681747009793,126.367632664314));
#62488=CARTESIAN_POINT('Ctrl Pts',(37.319930889199,-2.2496116981351,126.428606618747));
#62489=CARTESIAN_POINT('Ctrl Pts',(37.312173848314,-2.36973638343055,126.494658477563));
#62490=CARTESIAN_POINT('Ctrl Pts',(37.3044226570739,-2.4897704817672,126.56066052616));
#62491=CARTESIAN_POINT('Ctrl Pts',(37.2966714658337,-2.60713870315736,126.631732669561));
#62492=CARTESIAN_POINT('Ctrl Pts',(37.2889202745936,-2.72138912921527,126.707627251836));
#62493=CARTESIAN_POINT('Ctrl Pts',(37.2811723778165,-2.83559099579344,126.783489576887));
#62494=CARTESIAN_POINT('Ctrl Pts',(37.2734244810394,-2.94667737767535,126.864170048307));
#62495=CARTESIAN_POINT('Ctrl Pts',(37.2656765842623,-3.05422322862498,126.949376372173));
#62496=CARTESIAN_POINT('Ctrl Pts',(37.2579303081782,-3.16174658330117,127.034564872713));
#62497=CARTESIAN_POINT('Ctrl Pts',(37.2501840320941,-3.26573057389539,127.124277100006));
#62498=CARTESIAN_POINT('Ctrl Pts',(37.24243775601,-3.36578161600863,127.218179197749));
#62499=CARTESIAN_POINT('Ctrl Pts',(37.2346914227446,-3.46583339667552,127.312081988656));
#62500=CARTESIAN_POINT('Ctrl Pts',(37.2269450894793,-3.56195188585453,127.410174444173));
#62501=CARTESIAN_POINT('Ctrl Pts',(37.219198756214,-3.65377918882848,127.512084702369));
#62502=CARTESIAN_POINT('Ctrl Pts',(37.211450688211,-3.74562705589024,127.614017782662));
#62503=CARTESIAN_POINT('Ctrl Pts',(37.2037026202081,-3.83318156284325,127.719770076533));
#62504=CARTESIAN_POINT('Ctrl Pts',(37.1959545522052,-3.91612432060231,127.828935712097));
#62505=CARTESIAN_POINT('Ctrl Pts',(37.1881982494633,-3.99915523091157,127.938217370197));
#62506=CARTESIAN_POINT('Ctrl Pts',(37.1804419467215,-4.07756436400675,128.050919304993));
#62507=CARTESIAN_POINT('Ctrl Pts',(37.1726856439796,-4.1510756941205,128.166605199757));
#62508=CARTESIAN_POINT('Ctrl Pts',(37.1649252014654,-4.22462625944472,128.282352839566));
#62509=CARTESIAN_POINT('Ctrl Pts',(37.1571647589513,-4.29327361737003,128.401087274491));
#62510=CARTESIAN_POINT('Ctrl Pts',(37.1494043164371,-4.35678766375012,128.522347402115));
#62511=CARTESIAN_POINT('Ctrl Pts',(37.1416314161717,-4.42040366851579,128.643802187259));
#62512=CARTESIAN_POINT('Ctrl Pts',(37.1338585159063,-4.47886972785175,128.767790413392));
#62513=CARTESIAN_POINT('Ctrl Pts',(37.1260856156408,-4.53200350626976,128.89382998927));
#62514=CARTESIAN_POINT('Ctrl Pts',(37.1185952798788,-4.58320573800636,129.01528770909));
#62515=CARTESIAN_POINT('Ctrl Pts',(37.1111049441168,-4.62945653362067,129.138649936129));
#62516=CARTESIAN_POINT('Ctrl Pts',(37.1036146083548,-4.6706370630542,129.263473701623));
#62517=CARTESIAN_POINT('Ctrl Pts',(37.0973024603346,-4.70534012652036,129.368663389944));
#62518=CARTESIAN_POINT('Ctrl Pts',(37.0909903123145,-4.73650493527999,129.475074674504));
#62519=CARTESIAN_POINT('Ctrl Pts',(37.0846781642943,-4.76405452823403,129.582490119308));
#62520=CARTESIAN_POINT('Ctrl Pts',(38.8349537180509,-4.76405452823399,129.582490119308));
#62521=CARTESIAN_POINT('Ctrl Pts',(38.8271914067485,-4.79811247623972,129.715281541681));
#62522=CARTESIAN_POINT('Ctrl Pts',(38.819429095446,-4.82658390929227,129.849379955364));
#62523=CARTESIAN_POINT('Ctrl Pts',(38.8116667841435,-4.84939621256512,129.984275599986));
#62524=CARTESIAN_POINT('Ctrl Pts',(38.8038928211692,-4.87224275840619,130.119373730664));
#62525=CARTESIAN_POINT('Ctrl Pts',(38.7961188581948,-4.88941315961131,130.2552710952));
#62526=CARTESIAN_POINT('Ctrl Pts',(38.7883448952204,-4.90088673234273,130.391453486062));
#62527=CARTESIAN_POINT('Ctrl Pts',(38.7836633805576,-4.90779616825762,130.473463120238));
#62528=CARTESIAN_POINT('Ctrl Pts',(38.7789818658948,-4.91264065855441,130.555576104893));
#62529=CARTESIAN_POINT('Ctrl Pts',(38.7743003512321,-4.91542478919734,130.637680672029));
#62530=CARTESIAN_POINT('Ctrl Pts',(38.7711533794851,-4.91729631606509,130.692872372085));
#62531=CARTESIAN_POINT('Ctrl Pts',(38.7680064077382,-4.91823831758393,130.748095770571));
#62532=CARTESIAN_POINT('Ctrl Pts',(38.7648594359912,-4.91824989201499,130.80332998935));
#62533=CARTESIAN_POINT('',(39.1101405639799,-4.91824799303067,130.808803763948));
#62534=CARTESIAN_POINT('Ctrl Pts',(39.1801134839905,-4.76405452823399,129.582490119308));
#62535=CARTESIAN_POINT('Ctrl Pts',(39.1724358615329,-4.79786231385947,129.714306162357));
#62536=CARTESIAN_POINT('Ctrl Pts',(39.1647582390752,-4.82619617992312,129.847530671823));
#62537=CARTESIAN_POINT('Ctrl Pts',(39.1570806166175,-4.84895407859681,129.981665409023));
#62538=CARTESIAN_POINT('Ctrl Pts',(39.149257274516,-4.87214391735433,130.11834599505));
#62539=CARTESIAN_POINT('Ctrl Pts',(39.1414339324146,-4.8895438922101,130.255971290643));
#62540=CARTESIAN_POINT('Ctrl Pts',(39.1336105903131,-4.9011011506914,130.394006413016));
#62541=CARTESIAN_POINT('Ctrl Pts',(39.1257872482116,-4.91265840917271,130.53204153539));
#62542=CARTESIAN_POINT('Ctrl Pts',(39.1179639061101,-4.91837294927344,130.670486047647));
#62543=CARTESIAN_POINT('Ctrl Pts',(39.1101405640087,-4.91824799303113,130.808803763438));
#62544=CARTESIAN_POINT('Ctrl Pts',(39.1101405639799,-4.91824799303067,130.808803763948));
#62545=CARTESIAN_POINT('Ctrl Pts',(39.1005410273949,-4.91809466697877,130.978524831473));
#62546=CARTESIAN_POINT('Ctrl Pts',(39.09094149081,-4.90915251206192,131.147854560965));
#62547=CARTESIAN_POINT('Ctrl Pts',(39.0813419542251,-4.891564635173,131.316003542295));
#62548=CARTESIAN_POINT('Ctrl Pts',(39.0715821838055,-4.87368318442951,131.486959237868));
#62549=CARTESIAN_POINT('Ctrl Pts',(39.061822413386,-4.84686501379065,131.656694537834));
#62550=CARTESIAN_POINT('Ctrl Pts',(39.0520626429664,-4.81130913710586,131.824403484166));
#62551=CARTESIAN_POINT('Ctrl Pts',(39.0457614216062,-4.78835312072256,131.932681768337));
#62552=CARTESIAN_POINT('Ctrl Pts',(39.0394602002459,-4.76175584959625,132.040115861972));
#62553=CARTESIAN_POINT('Ctrl Pts',(39.0331589788857,-4.73158134341099,132.146493641221));
#62554=CARTESIAN_POINT('Ctrl Pts',(39.0253846447666,-4.6943525778192,132.27774064104));
#62555=CARTESIAN_POINT('Ctrl Pts',(39.0176103106475,-4.65159981236601,132.407645347261));
#62556=CARTESIAN_POINT('Ctrl Pts',(39.0098359765284,-4.60343580140505,132.535707458855));
#62557=CARTESIAN_POINT('Ctrl Pts',(39.0020712235814,-4.55533114828305,132.663611745342));
#62558=CARTESIAN_POINT('Ctrl Pts',(38.9943064706342,-4.50182865503804,132.789677593055));
#62559=CARTESIAN_POINT('Ctrl Pts',(38.9865417176871,-4.44309142330373,132.913417673851));
#62560=CARTESIAN_POINT('Ctrl Pts',(38.9787846768021,-4.38441253021619,133.037034854253));
#62561=CARTESIAN_POINT('Ctrl Pts',(38.9710276359172,-4.32050941188381,133.158330513804));
#62562=CARTESIAN_POINT('Ctrl Pts',(38.9632705950322,-4.25159391314395,133.276835543671));
#62563=CARTESIAN_POINT('Ctrl Pts',(38.9555194037921,-4.18273038411758,133.395251207973));
#62564=CARTESIAN_POINT('Ctrl Pts',(38.9477682125519,-4.10886219404433,133.510880094741));
#62565=CARTESIAN_POINT('Ctrl Pts',(38.9400170213118,-4.03024777233264,133.623276358788));
#62566=CARTESIAN_POINT('Ctrl Pts',(38.9322691245347,-3.9516667638474,133.735624851424));
#62567=CARTESIAN_POINT('Ctrl Pts',(38.9245212277576,-3.86834375954424,133.844743134319));
#62568=CARTESIAN_POINT('Ctrl Pts',(38.9167733309805,-3.78058116910775,133.950213297888));
#62569=CARTESIAN_POINT('Ctrl Pts',(38.9090270548964,-3.69283693671324,134.055661399372));
#62570=CARTESIAN_POINT('Ctrl Pts',(38.9012807788123,-3.60065521526645,134.157462599055));
#62571=CARTESIAN_POINT('Ctrl Pts',(38.8935345027282,-3.50437920986823,134.25523143751));
#62572=CARTESIAN_POINT('Ctrl Pts',(38.8857881694628,-3.40810249378241,134.353000997673));
#62573=CARTESIAN_POINT('Ctrl Pts',(38.8780418361975,-3.30773170775642,134.446737858641));
#62574=CARTESIAN_POINT('Ctrl Pts',(38.8702955029322,-3.20364719512028,134.536093152421));
#62575=CARTESIAN_POINT('Ctrl Pts',(38.8625474349292,-3.0995393734792,134.6254684567));
#62576=CARTESIAN_POINT('Ctrl Pts',(38.8547993669262,-2.99171646690314,134.710459986657));
#62577=CARTESIAN_POINT('Ctrl Pts',(38.8470512989232,-2.88059187085699,134.790759184701));
#62578=CARTESIAN_POINT('Ctrl Pts',(38.8392949961814,-2.76934917026777,134.871143725687));
#62579=CARTESIAN_POINT('Ctrl Pts',(38.8315386934395,-2.65479808784851,134.946825743208));
#62580=CARTESIAN_POINT('Ctrl Pts',(38.8237823906977,-2.53738143853433,135.017539761381));
#62581=CARTESIAN_POINT('Ctrl Pts',(38.8160219481835,-2.4199021204189,135.088291521756));
#62582=CARTESIAN_POINT('Ctrl Pts',(38.8082615056694,-2.29955453076905,135.154069811887));
#62583=CARTESIAN_POINT('Ctrl Pts',(38.8005010631552,-2.17680516108111,135.214655659079));
#62584=CARTESIAN_POINT('Ctrl Pts',(38.7927281628898,-2.05385874320777,135.275338764051));
#62585=CARTESIAN_POINT('Ctrl Pts',(38.7849552626243,-1.92850319840539,135.330812611052));
#62586=CARTESIAN_POINT('Ctrl Pts',(38.7771823623589,-1.80122485463524,135.380906485963));
#62587=CARTESIAN_POINT('Ctrl Pts',(38.7696920265968,-1.6785733992556,135.429179322342));
#62588=CARTESIAN_POINT('Ctrl Pts',(38.7622016908348,-1.55413680592188,135.472456445569));
#62589=CARTESIAN_POINT('Ctrl Pts',(38.7547113550727,-1.4283607674286,135.510629689832));
#62590=CARTESIAN_POINT('Ctrl Pts',(38.7469370209536,-1.29781589220743,135.550250284255));
#62591=CARTESIAN_POINT('Ctrl Pts',(38.7391626868345,-1.16541446974887,135.584497838669));
#62592=CARTESIAN_POINT('Ctrl Pts',(38.7313883527154,-1.03163836396168,135.61319679158));
#62593=CARTESIAN_POINT('Ctrl Pts',(38.7236235997683,-0.89802712526896,135.641860375595));
#62594=CARTESIAN_POINT('Ctrl Pts',(38.7158588468212,-0.763044952747463,
135.664988882778));
#62595=CARTESIAN_POINT('Ctrl Pts',(38.7080940938741,-0.627190009783876,
135.682456122384));
#62596=CARTESIAN_POINT('Ctrl Pts',(38.7003370529891,-0.491469999865044,
135.699906013282));
#62597=CARTESIAN_POINT('Ctrl Pts',(38.6925800121042,-0.354879329834526,
135.711705776797));
#62598=CARTESIAN_POINT('Ctrl Pts',(38.6848229712192,-0.217927181546811,
135.717780079208));
#62599=CARTESIAN_POINT('Ctrl Pts',(38.6770717799791,-0.0810783099396389,
135.723849800941));
#62600=CARTESIAN_POINT('Ctrl Pts',(38.6693205887389,0.0561311083429407,
135.724202638266));
#62601=CARTESIAN_POINT('Ctrl Pts',(38.6615693974988,0.193186283712091,135.718815024953));
#62602=CARTESIAN_POINT('Ctrl Pts',(38.6538215007217,0.330183206976016,135.713429701519));
#62603=CARTESIAN_POINT('Ctrl Pts',(38.6460736039447,0.467025627869497,135.702308795436));
#62604=CARTESIAN_POINT('Ctrl Pts',(38.6383257071676,0.603198487401534,135.685480842196));
#62605=CARTESIAN_POINT('Ctrl Pts',(38.6305794310835,0.739342862506905,135.668656409002));
#62606=CARTESIAN_POINT('Ctrl Pts',(38.6228331549993,0.874817567065649,135.646127351088));
#62607=CARTESIAN_POINT('Ctrl Pts',(38.6150868789152,1.00911279240587,135.61797406639));
#62608=CARTESIAN_POINT('Ctrl Pts',(38.6073405456498,1.14340900908293,135.589820573871));
#62609=CARTESIAN_POINT('Ctrl Pts',(38.5995942123845,1.27652534652062,135.556042851942));
#62610=CARTESIAN_POINT('Ctrl Pts',(38.5918478791192,1.40796270733709,135.516772322548));
#62611=CARTESIAN_POINT('Ctrl Pts',(38.5840998111162,1.5394295026392,135.47749299879));
#62612=CARTESIAN_POINT('Ctrl Pts',(38.5763517431132,1.66921619860237,135.432718531759));
#62613=CARTESIAN_POINT('Ctrl Pts',(38.5686036751102,1.79683974664007,135.382629939853));
#62614=CARTESIAN_POINT('Ctrl Pts',(38.5608473723684,1.92459893450336,135.332488113195));
#62615=CARTESIAN_POINT('Ctrl Pts',(38.5530910696266,2.05019001738285,135.277021022406));
#62616=CARTESIAN_POINT('Ctrl Pts',(38.5453347668847,2.17315029061294,135.216457724035));
#62617=CARTESIAN_POINT('Ctrl Pts',(38.5375743243705,2.29617619144311,135.155862101207));
#62618=CARTESIAN_POINT('Ctrl Pts',(38.5298138818563,2.41656814172715,135.090165038154));
#62619=CARTESIAN_POINT('Ctrl Pts',(38.5220534393422,2.53388976348633,135.019640647291));
#62620=CARTESIAN_POINT('Ctrl Pts',(38.5142805390767,2.65139972032808,134.949003044416));
#62621=CARTESIAN_POINT('Ctrl Pts',(38.5065076388113,2.76582917285638,134.873522843648));
#62622=CARTESIAN_POINT('Ctrl Pts',(38.4987347385458,2.87677162230528,134.793516931324));
#62623=CARTESIAN_POINT('Ctrl Pts',(38.4912444027838,2.98368103426908,134.716419435437));
#62624=CARTESIAN_POINT('Ctrl Pts',(38.4837540670219,3.08735232193994,134.635119747445));
#62625=CARTESIAN_POINT('Ctrl Pts',(38.4762637312599,3.18745357451689,134.549934375056));
#62626=CARTESIAN_POINT('Ctrl Pts',(38.4684893971408,3.29135019651085,134.461519173382));
#62627=CARTESIAN_POINT('Ctrl Pts',(38.4607150630217,3.3917298369044,134.368637746568));
#62628=CARTESIAN_POINT('Ctrl Pts',(38.4529407289026,3.48818433162545,134.271600605092));
#62629=CARTESIAN_POINT('Ctrl Pts',(38.4451759759555,3.58451995480214,134.174683053221));
#62630=CARTESIAN_POINT('Ctrl Pts',(38.4374112230084,3.67693978429857,134.073620251662));
#62631=CARTESIAN_POINT('Ctrl Pts',(38.4296464700613,3.76506838279081,133.968763110203));
#62632=CARTESIAN_POINT('Ctrl Pts',(38.4218894291763,3.85310945071664,133.864010114336));
#62633=CARTESIAN_POINT('Ctrl Pts',(38.4141323882913,3.93686751951246,133.755470575595));
#62634=CARTESIAN_POINT('Ctrl Pts',(38.4063753474063,4.01600398355601,133.64353216338));
#62635=CARTESIAN_POINT('Ctrl Pts',(38.3986241561662,4.09508077017642,133.531678164793));
#62636=CARTESIAN_POINT('Ctrl Pts',(38.3908729649261,4.16954266431975,133.416430712412));
#62637=CARTESIAN_POINT('Ctrl Pts',(38.383121773686,4.23909158270006,133.298210175174));
#62638=CARTESIAN_POINT('Ctrl Pts',(38.3753738769089,4.30861094093478,133.180039884818));
#62639=CARTESIAN_POINT('Ctrl Pts',(38.3676259801318,4.37322127874126,133.05889935916));
#62640=CARTESIAN_POINT('Ctrl Pts',(38.3598780833547,4.4326682018728,132.935237356048));
#62641=CARTESIAN_POINT('Ctrl Pts',(38.3521318072706,4.49210268998955,132.811601220362));
#62642=CARTESIAN_POINT('Ctrl Pts',(38.3443855311865,4.54637574247788,132.685445008469));
#62643=CARTESIAN_POINT('Ctrl Pts',(38.3366392551024,4.5952794363588,132.55724109389));
#62644=CARTESIAN_POINT('Ctrl Pts',(38.3288929218371,4.64418349123561,132.42903623294));
#62645=CARTESIAN_POINT('Ctrl Pts',(38.3211465885717,4.68771796907419,132.298784004433));
#62646=CARTESIAN_POINT('Ctrl Pts',(38.3134002553064,4.72572366455252,132.166975349905));
#62647=CARTESIAN_POINT('Ctrl Pts',(38.3056521873034,4.7637378711429,132.035137177743));
#62648=CARTESIAN_POINT('Ctrl Pts',(38.2979041193004,4.79622072333547,131.901742261572));
#62649=CARTESIAN_POINT('Ctrl Pts',(38.2901560512974,4.82306341747488,131.767294848713));
#62650=CARTESIAN_POINT('Ctrl Pts',(38.2823997485555,4.84993464034905,131.632704543545));
#62651=CARTESIAN_POINT('Ctrl Pts',(38.2746434458137,4.87115365398788,131.497059891164));
#62652=CARTESIAN_POINT('Ctrl Pts',(38.2668871430718,4.88666306697858,131.360873988769));
#62653=CARTESIAN_POINT('Ctrl Pts',(38.2591267005577,4.90218075780997,131.224615399857));
#62654=CARTESIAN_POINT('Ctrl Pts',(38.2513662580435,4.91198274789094,131.087815375086));
#62655=CARTESIAN_POINT('Ctrl Pts',(38.2436058155293,4.91606378280456,130.950989216063));
#62656=CARTESIAN_POINT('Ctrl Pts',(38.2358329152639,4.92015136895772,130.813943411544));
#62657=CARTESIAN_POINT('Ctrl Pts',(38.2280600149985,4.918499652528,130.6768717801));
#62658=CARTESIAN_POINT('Ctrl Pts',(38.2202871147331,4.91115551645211,130.540287605461));
#62659=CARTESIAN_POINT('Ctrl Pts',(38.212796778971,4.9040783582213,130.408668609605));
#62660=CARTESIAN_POINT('Ctrl Pts',(38.2053064432089,4.8917154914845,130.277502551947));
#62661=CARTESIAN_POINT('Ctrl Pts',(38.1978161074468,4.87415379724563,130.147239758594));
#62662=CARTESIAN_POINT('Ctrl Pts',(38.1900417733277,4.85592624603203,130.012038011839));
#62663=CARTESIAN_POINT('Ctrl Pts',(38.1822674392087,4.83204011865691,129.877381097529));
#62664=CARTESIAN_POINT('Ctrl Pts',(38.1744931050896,4.80253603372715,129.743780254155));
#62665=CARTESIAN_POINT('Ctrl Pts',(38.1667283521425,4.77306830994521,129.610344061881));
#62666=CARTESIAN_POINT('Ctrl Pts',(38.1589635991954,4.73799648806898,129.477961729021));
#62667=CARTESIAN_POINT('Ctrl Pts',(38.1511988462483,4.69741286539684,129.347138796941));
#62668=CARTESIAN_POINT('Ctrl Pts',(38.1434418053633,4.65686955095092,129.216445800042));
#62669=CARTESIAN_POINT('Ctrl Pts',(38.1356847644783,4.61082544509765,129.087309492698));
#62670=CARTESIAN_POINT('Ctrl Pts',(38.1279277235933,4.55942368047204,128.960224298188));
#62671=CARTESIAN_POINT('Ctrl Pts',(38.1201765323532,4.50806067831697,128.833234939611));
#62672=CARTESIAN_POINT('Ctrl Pts',(38.1124253411131,4.45134820526876,128.70829397611));
#62673=CARTESIAN_POINT('Ctrl Pts',(38.1046741498729,4.38947880832195,128.585879413275));
#62674=CARTESIAN_POINT('Ctrl Pts',(38.0969262530959,4.32763570751926,128.463516879894));
#62675=CARTESIAN_POINT('Ctrl Pts',(38.0891783563188,4.26064021818513,128.343678959698));
#62676=CARTESIAN_POINT('Ctrl Pts',(38.0814304595417,4.18873238670201,128.226822246349));
#62677=CARTESIAN_POINT('Ctrl Pts',(38.0736841834576,4.11683959678708,128.109989976906));
#62678=CARTESIAN_POINT('Ctrl Pts',(38.0659379073735,4.04003671335433,127.99613800669));
#62679=CARTESIAN_POINT('Ctrl Pts',(38.0581916312894,3.95860877017774,127.885696596619));
#62680=CARTESIAN_POINT('Ctrl Pts',(38.0504452980241,3.87718022591847,127.775254371294));
#62681=CARTESIAN_POINT('Ctrl Pts',(38.0426989647587,3.7911267858018,127.668223071033));
#62682=CARTESIAN_POINT('Ctrl Pts',(38.0349526314934,3.70077543847887,127.565002005672));
#62683=CARTESIAN_POINT('Ctrl Pts',(38.0272045634904,3.61040385759816,127.461757824669));
#62684=CARTESIAN_POINT('Ctrl Pts',(38.0194564954874,3.51573271173069,127.362325870615));
#62685=CARTESIAN_POINT('Ctrl Pts',(38.0117084274845,3.41712742739617,127.2670702411));
#62686=CARTESIAN_POINT('Ctrl Pts',(38.0039521247426,3.31841734419204,127.171713372769));
#62687=CARTESIAN_POINT('Ctrl Pts',(37.9961958220007,3.21576505166253,127.080541967724));
#62688=CARTESIAN_POINT('Ctrl Pts',(37.9884395192589,3.10957121155231,126.993881652556));
#62689=CARTESIAN_POINT('Ctrl Pts',(37.9806790767447,3.00332069259218,126.907175084168));
#62690=CARTESIAN_POINT('Ctrl Pts',(37.9729186342305,2.89352517243947,126.824984637391));
#62691=CARTESIAN_POINT('Ctrl Pts',(37.9651581917163,2.78061534879152,126.747593266021));
#62692=CARTESIAN_POINT('Ctrl Pts',(37.9573852914509,2.66752427227099,126.670077659151));
#62693=CARTESIAN_POINT('Ctrl Pts',(37.9496123911855,2.5513092335913,126.597376730006));
#62694=CARTESIAN_POINT('Ctrl Pts',(37.94183949092,2.43242741426335,126.529728477037));
#62695=CARTESIAN_POINT('Ctrl Pts',(37.934349155158,2.31786724851352,126.46453940846));
#62696=CARTESIAN_POINT('Ctrl Pts',(37.926858819396,2.20083109794056,126.404042180308));
#62697=CARTESIAN_POINT('Ctrl Pts',(37.919368483634,2.08174479595503,126.348407109391));
#62698=CARTESIAN_POINT('Ctrl Pts',(37.9115941495149,1.95814330063388,126.290662617851));
#62699=CARTESIAN_POINT('Ctrl Pts',(37.9038198153958,1.83194158964571,126.237973341939));
#62700=CARTESIAN_POINT('Ctrl Pts',(37.8960454812768,1.703591737761,126.190581444964));
#62701=CARTESIAN_POINT('Ctrl Pts',(37.8882807283297,1.57540006559778,126.143247954267));
#62702=CARTESIAN_POINT('Ctrl Pts',(37.8805159753826,1.44506588329948,126.101198986768));
#62703=CARTESIAN_POINT('Ctrl Pts',(37.8727512224355,1.31306440607854,126.064630147593));
#62704=CARTESIAN_POINT('Ctrl Pts',(37.8649941815505,1.18119403458568,126.028097629105));
#62705=CARTESIAN_POINT('Ctrl Pts',(37.8572371406654,1.04766003798285,125.997034510947));
#62706=CARTESIAN_POINT('Ctrl Pts',(37.8494800997804,0.912955755263201,125.971587619438));
#62707=CARTESIAN_POINT('Ctrl Pts',(37.8417289085403,0.778353054091366,125.946159917629));
#62708=CARTESIAN_POINT('Ctrl Pts',(37.8339777173003,0.642582206024923,125.92634008476));
#62709=CARTESIAN_POINT('Ctrl Pts',(37.8262265260601,0.506149447057368,125.91222449929));
#62710=CARTESIAN_POINT('Ctrl Pts',(37.8184786292831,0.369774675651652,125.898114913319));
#62711=CARTESIAN_POINT('Ctrl Pts',(37.810730732506,0.232738940963491,125.889704792837));
#62712=CARTESIAN_POINT('Ctrl Pts',(37.8029828357289,0.0955561391059442,
125.88703898005));
#62713=CARTESIAN_POINT('Ctrl Pts',(37.7952365596448,-0.0415979670667733,
125.884373724894));
#62714=CARTESIAN_POINT('Ctrl Pts',(37.7874902835607,-0.178898688575267,
125.887450395006));
#62715=CARTESIAN_POINT('Ctrl Pts',(37.7797440074766,-0.315829967006171,
125.896261749935));
#62716=CARTESIAN_POINT('Ctrl Pts',(37.7719976742112,-0.452762256232666,
125.905073169907));
#62717=CARTESIAN_POINT('Ctrl Pts',(37.7642513409459,-0.589324706781487,
125.919619334061));
#62718=CARTESIAN_POINT('Ctrl Pts',(37.7565050076805,-0.725004622624458,
125.939840974305));
#62719=CARTESIAN_POINT('Ctrl Pts',(37.7487569396776,-0.860714923043844,
125.960067143045));
#62720=CARTESIAN_POINT('Ctrl Pts',(37.7410088716746,-0.995541908861559,
125.985971259362));
#62721=CARTESIAN_POINT('Ctrl Pts',(37.7332608036716,-1.12898173250234,126.017442683219));
#62722=CARTESIAN_POINT('Ctrl Pts',(37.7255045009298,-1.26256337757564,126.048947555279));
#62723=CARTESIAN_POINT('Ctrl Pts',(37.7177481981879,-1.39475453428196,126.086031464836));
#62724=CARTESIAN_POINT('Ctrl Pts',(37.7099918954461,-1.52506467628915,126.128533332942));
#62725=CARTESIAN_POINT('Ctrl Pts',(37.7022314529319,-1.65544436874287,126.171057885575));
#62726=CARTESIAN_POINT('Ctrl Pts',(37.6944710104177,-1.78394067991828,126.219006022153));
#62727=CARTESIAN_POINT('Ctrl Pts',(37.6867105679035,-1.91008275014688,126.272168327946));
#62728=CARTESIAN_POINT('Ctrl Pts',(37.6789376676381,-2.03642731482499,126.325415974591));
#62729=CARTESIAN_POINT('Ctrl Pts',(37.6711647673726,-2.1604097326283,126.383894349992));
#62730=CARTESIAN_POINT('Ctrl Pts',(37.6633918671072,-2.2815826509457,126.44734745837));
#62731=CARTESIAN_POINT('Ctrl Pts',(37.6559015313451,-2.39835062846626,126.508493886431));
#62732=CARTESIAN_POINT('Ctrl Pts',(37.6484111955832,-2.51250955803329,126.574259485001));
#62733=CARTESIAN_POINT('Ctrl Pts',(37.6409208598211,-2.62368597393076,126.644378048769));
#62734=CARTESIAN_POINT('Ctrl Pts',(37.633145138272,-2.73909827056281,126.717168167209));
#62735=CARTESIAN_POINT('Ctrl Pts',(37.625369416723,-2.85166193403462,126.794880145919));
#62736=CARTESIAN_POINT('Ctrl Pts',(37.6175936951739,-2.96092863014544,126.877264399024));
#62737=CARTESIAN_POINT('Ctrl Pts',(37.6097869577625,-3.07063117015674,126.959977267119));
#62738=CARTESIAN_POINT('Ctrl Pts',(37.601980220351,-3.17701001363012,127.047399613342));
#62739=CARTESIAN_POINT('Ctrl Pts',(37.5941734829396,-3.27963693609872,127.139232430193));
#62740=CARTESIAN_POINT('Ctrl Pts',(37.5864171843116,-3.38160079321118,127.230471921648));
#62741=CARTESIAN_POINT('Ctrl Pts',(37.5786608856836,-3.47986075706443,127.326064815401));
#62742=CARTESIAN_POINT('Ctrl Pts',(37.5709045870557,-3.57402692832669,127.425675284763));
#62743=CARTESIAN_POINT('Ctrl Pts',(37.5631536839099,-3.66812759516169,127.525216462504));
#62744=CARTESIAN_POINT('Ctrl Pts',(37.5554027807641,-3.75813986802794,127.628769372447));
#62745=CARTESIAN_POINT('Ctrl Pts',(37.5476518776184,-3.84370926926902,127.735960038138));
#62746=CARTESIAN_POINT('Ctrl Pts',(37.5399046875389,-3.92923767853069,127.843099354194));
#62747=CARTESIAN_POINT('Ctrl Pts',(37.5321574974594,-4.01032720884455,127.953872652802));
#62748=CARTESIAN_POINT('Ctrl Pts',(37.52441030738,-4.08666266672071,128.06787175208));
#62749=CARTESIAN_POINT('Ctrl Pts',(37.5165621148733,-4.16399333272432,128.183357091609));
#62750=CARTESIAN_POINT('Ctrl Pts',(37.5087139223665,-4.23644482229462,128.302152628001));
#62751=CARTESIAN_POINT('Ctrl Pts',(37.5008657298598,-4.30373392387507,128.423802410971));
#62752=CARTESIAN_POINT('Ctrl Pts',(37.4931192925096,-4.37015059361115,128.543874952723));
#62753=CARTESIAN_POINT('Ctrl Pts',(37.4853728551594,-4.43153778052614,128.666727803173));
#62754=CARTESIAN_POINT('Ctrl Pts',(37.4776264178092,-4.48766908577469,128.791897142349));
#62755=CARTESIAN_POINT('Ctrl Pts',(37.4697273477242,-4.54490638003987,128.91953276863));
#62756=CARTESIAN_POINT('Ctrl Pts',(37.4618282776392,-4.59667831078346,129.04957674941));
#62757=CARTESIAN_POINT('Ctrl Pts',(37.4539292075542,-4.6427964119176,129.181516034747));
#62758=CARTESIAN_POINT('Ctrl Pts',(37.4460301374693,-4.68891451305174,129.313455320084));
#62759=CARTESIAN_POINT('Ctrl Pts',(37.4381310673843,-4.72937867507802,129.447289494132));
#62760=CARTESIAN_POINT('Ctrl Pts',(37.4302319972993,-4.76405452823409,129.582490119308));
#62761=CARTESIAN_POINT('Origin',(213.235140564004,0.,130.804360617566));
#62762=CARTESIAN_POINT('',(35.3346663362986,-4.76405452823403,129.582490119308));
#62763=CARTESIAN_POINT('',(35.6799972093173,-4.76405452823406,129.582490119308));
#62764=CARTESIAN_POINT('',(213.235140564004,-4.76405452823405,129.582490119308));
#62765=CARTESIAN_POINT('',(37.0148594360394,-4.91824833830055,130.800317684988));
#62766=CARTESIAN_POINT('Ctrl Pts',(37.0148594359912,-4.91824833830126,130.800317685842));
#62767=CARTESIAN_POINT('Ctrl Pts',(37.0069555838475,-4.91836336589627,130.940249378149));
#62768=CARTESIAN_POINT('Ctrl Pts',(36.9990517317038,-4.91250179003222,131.080267730569));
#62769=CARTESIAN_POINT('Ctrl Pts',(36.99114787956,-4.90067081885339,131.219822514422));
#62770=CARTESIAN_POINT('Ctrl Pts',(36.9834261315574,-4.88911243233405,131.356161966865));
#62771=CARTESIAN_POINT('Ctrl Pts',(36.9757043835548,-4.8718567741881,131.492058569711));
#62772=CARTESIAN_POINT('Ctrl Pts',(36.9679826355522,-4.84896321405377,131.62700198004));
#62773=CARTESIAN_POINT('Ctrl Pts',(36.9602609837571,-4.82606993915677,131.761943709071));
#62774=CARTESIAN_POINT('Ctrl Pts',(36.952539331962,-4.79753896740725,131.89593188133));
#62775=CARTESIAN_POINT('Ctrl Pts',(36.9448176801668,-4.76348108957116,132.028464768281));
#62776=CARTESIAN_POINT('Ctrl Pts',(36.9370944283567,-4.72941615455136,132.16102511757));
#62777=CARTESIAN_POINT('Ctrl Pts',(36.9293711765465,-4.68982213260539,132.292129200606));
#62778=CARTESIAN_POINT('Ctrl Pts',(36.9216479247363,-4.64486002074495,132.421289326627));
#62779=CARTESIAN_POINT('Ctrl Pts',(36.9136078463868,-4.59805345389917,132.555747914586));
#62780=CARTESIAN_POINT('Ctrl Pts',(36.9055677680373,-4.54542915690043,132.688099216945));
#62781=CARTESIAN_POINT('Ctrl Pts',(36.8975276896877,-4.48722413897979,132.817816002981));
#62782=CARTESIAN_POINT('Ctrl Pts',(36.8897917680836,-4.43122102109632,132.942625593621));
#62783=CARTESIAN_POINT('Ctrl Pts',(36.8820558464795,-4.37005195295995,133.064996035608));
#62784=CARTESIAN_POINT('Ctrl Pts',(36.8743199248753,-4.30397461236673,133.184483639303));
#62785=CARTESIAN_POINT('Ctrl Pts',(36.8665783727035,-4.23784917757628,133.304058211697));
#62786=CARTESIAN_POINT('Ctrl Pts',(36.8588368205316,-4.16680855978427,133.420745432725));
#62787=CARTESIAN_POINT('Ctrl Pts',(36.8510952683598,-4.09115340355658,133.534131100788));
#62788=CARTESIAN_POINT('Ctrl Pts',(36.8433427586412,-4.01539116351749,133.647677257178));
#62789=CARTESIAN_POINT('Ctrl Pts',(36.8355902489226,-3.93500158236551,133.757912220027));
#62790=CARTESIAN_POINT('Ctrl Pts',(36.827837739204,-3.85032529005803,133.864455097029));
#62791=CARTESIAN_POINT('Ctrl Pts',(36.8269474876499,-3.84060157431263,133.876689839747));
#62792=CARTESIAN_POINT('Ctrl Pts',(36.8260572360959,-3.83082136961932,133.888875936193));
#62793=CARTESIAN_POINT('Ctrl Pts',(36.8251669845419,-3.82098522180156,133.901012841706));
#62794=CARTESIAN_POINT('Ctrl Pts',(36.8173926504228,-3.73508871397414,134.007001265093));
#62795=CARTESIAN_POINT('Ctrl Pts',(36.8096183163038,-3.64464286930925,134.109580896771));
#62796=CARTESIAN_POINT('Ctrl Pts',(36.8018439821847,-3.54994831405154,134.208336238816));
#62797=CARTESIAN_POINT('Ctrl Pts',(36.7940792292376,-3.45537046137022,134.306969873727));
#62798=CARTESIAN_POINT('Ctrl Pts',(36.7863144762904,-3.35655458447976,134.401788317172));
#62799=CARTESIAN_POINT('Ctrl Pts',(36.7785497233434,-3.25384248265377,134.492407819078));
#62800=CARTESIAN_POINT('Ctrl Pts',(36.7707926824583,-3.15123239593516,134.582937316416));
#62801=CARTESIAN_POINT('Ctrl Pts',(36.7630356415734,-3.04473407660474,134.669275914611));
#62802=CARTESIAN_POINT('Ctrl Pts',(36.7552786006884,-2.934726956821,134.751075802553));
#62803=CARTESIAN_POINT('Ctrl Pts',(36.7475274094482,-2.82480279426218,134.832814004563));
#62804=CARTESIAN_POINT('Ctrl Pts',(36.7397762182081,-2.71137541044566,134.910020076606));
#62805=CARTESIAN_POINT('Ctrl Pts',(36.732025026968,-2.59485790007508,134.98238593354));
#62806=CARTESIAN_POINT('Ctrl Pts',(36.7242771301909,-2.47838991275446,135.054721033054));
#62807=CARTESIAN_POINT('Ctrl Pts',(36.7165292334138,-2.35883474253219,135.122219803274));
#62808=CARTESIAN_POINT('Ctrl Pts',(36.7087813366367,-2.23663491326429,135.184617154262));
#62809=CARTESIAN_POINT('Ctrl Pts',(36.7010350605526,-2.11446064556651,135.247001453069));
#62810=CARTESIAN_POINT('Ctrl Pts',(36.6932887844685,-1.98964316715752,135.304286277493));
#62811=CARTESIAN_POINT('Ctrl Pts',(36.6855425083844,-1.86264972594991,135.356252428771));
#62812=CARTESIAN_POINT('Ctrl Pts',(36.677796175119,-1.73565534730556,135.408218963652));
#62813=CARTESIAN_POINT('Ctrl Pts',(36.6700498418537,-1.60648533565349,135.454866598976));
#62814=CARTESIAN_POINT('Ctrl Pts',(36.6623035085884,-1.47562667065963,135.496024394025));
#62815=CARTESIAN_POINT('Ctrl Pts',(36.6545554405854,-1.34473870077469,135.537191406077));
#62816=CARTESIAN_POINT('Ctrl Pts',(36.6468073725823,-1.21216169793079,135.572866014189));
#62817=CARTESIAN_POINT('Ctrl Pts',(36.6390593045793,-1.07839715325156,135.602927345492));
#62818=CARTESIAN_POINT('Ctrl Pts',(36.6313030018375,-0.944490442022615,
135.633020626336));
#62819=CARTESIAN_POINT('Ctrl Pts',(36.6235466990957,-0.809394049770029,
135.657488627067));
#62820=CARTESIAN_POINT('Ctrl Pts',(36.6157903963538,-0.673619548697748,
135.676261659881));
#62821=CARTESIAN_POINT('Ctrl Pts',(36.6080299538397,-0.537772580686338,
135.695044712429));
#62822=CARTESIAN_POINT('Ctrl Pts',(36.6002695113255,-0.401247171677058,
135.708126703174));
#62823=CARTESIAN_POINT('Ctrl Pts',(36.5925090688113,-0.264558348793582,
135.715490013396));
#62824=CARTESIAN_POINT('Ctrl Pts',(36.5847361685459,-0.127650100876764,
135.722865143857));
#62825=CARTESIAN_POINT('Ctrl Pts',(36.5769632682804,0.0094216939638202,
135.724503244287));
#62826=CARTESIAN_POINT('Ctrl Pts',(36.569190368015,0.146142774750661,135.720438866728));
#62827=CARTESIAN_POINT('Ctrl Pts',(36.561700032253,0.277893699871095,135.716522239531));
#62828=CARTESIAN_POINT('Ctrl Pts',(36.554209696491,0.409318659657122,135.707310556714));
#62829=CARTESIAN_POINT('Ctrl Pts',(36.546719360729,0.539965372782319,135.692879867676));
#62830=CARTESIAN_POINT('Ctrl Pts',(36.5389450266099,0.675565595744873,135.677902034677));
#62831=CARTESIAN_POINT('Ctrl Pts',(36.5311706924908,0.810756933385873,135.65725418057));
#62832=CARTESIAN_POINT('Ctrl Pts',(36.5233963583717,0.94502731970406,135.630964643951));
#62833=CARTESIAN_POINT('Ctrl Pts',(36.5156316054246,1.07913222977138,135.604707506836));
#62834=CARTESIAN_POINT('Ctrl Pts',(36.5078668524776,1.21231806681136,135.572822595748));
#62835=CARTESIAN_POINT('Ctrl Pts',(36.5001020995305,1.34407722016159,135.535390049808));
#62836=CARTESIAN_POINT('Ctrl Pts',(36.4923450586455,1.47570550846288,135.497994682401));
#62837=CARTESIAN_POINT('Ctrl Pts',(36.4845880177604,1.60590955932414,135.455062751421));
#62838=CARTESIAN_POINT('Ctrl Pts',(36.4768309768754,1.73419165705913,135.406725483489));
#62839=CARTESIAN_POINT('Ctrl Pts',(36.4690797856353,1.86237701626686,135.358424667068));
#62840=CARTESIAN_POINT('Ctrl Pts',(36.4613285943952,1.9886429428368,135.304726764434));
#62841=CARTESIAN_POINT('Ctrl Pts',(36.4535774031551,2.11250694823694,135.245812796319));
#62842=CARTESIAN_POINT('Ctrl Pts',(36.445829506378,2.23631830813009,135.186923868212));
#62843=CARTESIAN_POINT('Ctrl Pts',(36.4380816096009,2.35772942498303,135.122823451579));
#62844=CARTESIAN_POINT('Ctrl Pts',(36.4303337128239,2.47627807616937,135.053740566686));
#62845=CARTESIAN_POINT('Ctrl Pts',(36.4225874367398,2.59480192953367,134.984672132443));
#62846=CARTESIAN_POINT('Ctrl Pts',(36.4148411606557,2.7104641706291,134.910623499704));
#62847=CARTESIAN_POINT('Ctrl Pts',(36.4070948845716,2.82282782241725,134.831869295085));
#62848=CARTESIAN_POINT('Ctrl Pts',(36.3993485513062,2.9351923036482,134.75311450912));
#62849=CARTESIAN_POINT('Ctrl Pts',(36.3916022180409,3.04425782682659,134.669654306356));
#62850=CARTESIAN_POINT('Ctrl Pts',(36.3838558847756,3.14961735028056,134.581805998946));
#62851=CARTESIAN_POINT('Ctrl Pts',(36.3761078167726,3.25500046826902,134.493938018517));
#62852=CARTESIAN_POINT('Ctrl Pts',(36.3683597487697,3.35667563484056,134.401680228335));
#62853=CARTESIAN_POINT('Ctrl Pts',(36.3606116807667,3.45427008802615,134.305389212346));
#62854=CARTESIAN_POINT('Ctrl Pts',(36.3528553780249,3.55196826575824,134.20899585712));
#62855=CARTESIAN_POINT('Ctrl Pts',(36.3450990752831,3.64557678766811,134.108560988248));
#62856=CARTESIAN_POINT('Ctrl Pts',(36.3373427725412,3.73476050616096,134.004477337956));
#62857=CARTESIAN_POINT('Ctrl Pts',(36.3295823300271,3.82399182468987,133.900338135085));
#62858=CARTESIAN_POINT('Ctrl Pts',(36.3218218875129,3.90879339239342,133.792546577429));
#62859=CARTESIAN_POINT('Ctrl Pts',(36.3140614449988,3.98887200140158,133.681526448542));
#62860=CARTESIAN_POINT('Ctrl Pts',(36.3062885447334,4.06907915970186,133.570328100288));
#62861=CARTESIAN_POINT('Ctrl Pts',(36.2985156444679,4.14454799326345,133.45589115051));
#62862=CARTESIAN_POINT('Ctrl Pts',(36.2907427442025,4.21502960107745,133.338666937753));
#62863=CARTESIAN_POINT('Ctrl Pts',(36.2832524084404,4.28294902491581,133.225704120399));
#62864=CARTESIAN_POINT('Ctrl Pts',(36.2757620726782,4.34623737627149,133.110153440011));
#62865=CARTESIAN_POINT('Ctrl Pts',(36.2682717369161,4.40471416855361,132.992436520236));
#62866=CARTESIAN_POINT('Ctrl Pts',(36.260497402797,4.46540812618805,132.870256327669));
#62867=CARTESIAN_POINT('Ctrl Pts',(36.252723068678,4.52111072197726,132.745355356997));
#62868=CARTESIAN_POINT('Ctrl Pts',(36.2449487345589,4.57156901380272,132.618179741552));
#62869=CARTESIAN_POINT('Ctrl Pts',(36.2371839816118,4.62196512029315,132.491160858687));
#62870=CARTESIAN_POINT('Ctrl Pts',(36.2294192286647,4.66712963973266,132.361873268692));
#62871=CARTESIAN_POINT('Ctrl Pts',(36.2216544757175,4.70685561947062,132.230787355943));
#62872=CARTESIAN_POINT('Ctrl Pts',(36.2138974348325,4.74654214280535,132.099831639572));
#62873=CARTESIAN_POINT('Ctrl Pts',(36.2061403939475,4.78080076327774,131.967081526647));
#62874=CARTESIAN_POINT('Ctrl Pts',(36.1983833530626,4.8094728580747,131.833026690664));
#62875=CARTESIAN_POINT('Ctrl Pts',(36.1906321618224,4.83812333102186,131.699072946476));
#62876=CARTESIAN_POINT('Ctrl Pts',(36.1828809705823,4.86119558226044,131.563816818399));
#62877=CARTESIAN_POINT('Ctrl Pts',(36.1751297793422,4.87858111282007,131.427762083826));
#62878=CARTESIAN_POINT('Ctrl Pts',(36.1673818825651,4.89595925406551,131.291765176144));
#62879=CARTESIAN_POINT('Ctrl Pts',(36.1596339857881,4.90765543242442,131.154970724064));
#62880=CARTESIAN_POINT('Ctrl Pts',(36.151886089011,4.91361248651288,131.01789139962));
#62881=CARTESIAN_POINT('Ctrl Pts',(36.1441398129269,4.91956829451405,130.880840749216));
#62882=CARTESIAN_POINT('Ctrl Pts',(36.1363935368428,4.91978734914383,130.743505735324));
#62883=CARTESIAN_POINT('Ctrl Pts',(36.1286472607587,4.91426450478877,130.606402441496));
#62884=CARTESIAN_POINT('Ctrl Pts',(36.1209009274934,4.90874161966532,130.469298135601));
#62885=CARTESIAN_POINT('Ctrl Pts',(36.113154594228,4.89747676671626,130.332425943833));
#62886=CARTESIAN_POINT('Ctrl Pts',(36.1054082609626,4.88051689367513,130.196299836845));
#62887=CARTESIAN_POINT('Ctrl Pts',(36.0976601929596,4.86355322258803,130.060143245359));
#62888=CARTESIAN_POINT('Ctrl Pts',(36.0899121249567,4.84089204191675,129.924733459015));
#62889=CARTESIAN_POINT('Ctrl Pts',(36.0821640569537,4.81263186888596,129.79057683535));
#62890=CARTESIAN_POINT('Ctrl Pts',(36.0744077542119,4.78434166060696,129.656277628429));
#62891=CARTESIAN_POINT('Ctrl Pts',(36.06665145147,4.7504406535697,129.523234627932));
#62892=CARTESIAN_POINT('Ctrl Pts',(36.0588951487282,4.71107810905525,129.391942084382));
#62893=CARTESIAN_POINT('Ctrl Pts',(36.051134706214,4.6716945555656,129.260579466049));
#62894=CARTESIAN_POINT('Ctrl Pts',(36.0433742636998,4.62684378403051,129.130969535566));
#62895=CARTESIAN_POINT('Ctrl Pts',(36.0356138211856,4.57672384954214,129.003588042383));
#62896=CARTESIAN_POINT('Ctrl Pts',(36.0278409209202,4.5265234580855,128.876002065118));
#62897=CARTESIAN_POINT('Ctrl Pts',(36.0200680206547,4.47103715918253,128.750652031421));
#62898=CARTESIAN_POINT('Ctrl Pts',(36.0122951203893,4.41051013966063,128.627991308269));
#62899=CARTESIAN_POINT('Ctrl Pts',(36.0048047846273,4.35218342975687,128.509789611367));
#62900=CARTESIAN_POINT('Ctrl Pts',(35.9973144488653,4.2891762695934,128.394085363722));
#62901=CARTESIAN_POINT('Ctrl Pts',(35.9898241131033,4.22174582567467,128.281258311694));
#62902=CARTESIAN_POINT('Ctrl Pts',(35.9820497789842,4.15175873597951,128.164153387694));
#62903=CARTESIAN_POINT('Ctrl Pts',(35.9742754448651,4.07678462560965,128.049777190753));
#62904=CARTESIAN_POINT('Ctrl Pts',(35.966501110746,3.99706211777929,127.938583674203));
#62905=CARTESIAN_POINT('Ctrl Pts',(35.9587363577989,3.91743786081483,127.827527193723));
#62906=CARTESIAN_POINT('Ctrl Pts',(35.9509716048519,3.83307707569843,127.719645903975));
#62907=CARTESIAN_POINT('Ctrl Pts',(35.9432068519048,3.74426364716699,127.615368174332));
#62908=CARTESIAN_POINT('Ctrl Pts',(35.9354498110197,3.6555384293847,127.5111940148));
#62909=CARTESIAN_POINT('Ctrl Pts',(35.9276927701347,3.56236962088044,127.410616588503));
#62910=CARTESIAN_POINT('Ctrl Pts',(35.9199357292497,3.46508345833033,127.314034029794));
#62911=CARTESIAN_POINT('Ctrl Pts',(35.9121845380096,3.36787066003257,127.217524304745));
#62912=CARTESIAN_POINT('Ctrl Pts',(35.9044333467695,3.26654696419431,127.125003725297));
#62913=CARTESIAN_POINT('Ctrl Pts',(35.8966821555294,3.16147756666012,127.036835878695));
#62914=CARTESIAN_POINT('Ctrl Pts',(35.8889342587523,3.05645282642241,126.948705505779));
#62915=CARTESIAN_POINT('Ctrl Pts',(35.8811863619752,2.94768584976528,126.864924436933));
#62916=CARTESIAN_POINT('Ctrl Pts',(35.8734384651981,2.83557706506659,126.785817875406));
#62917=CARTESIAN_POINT('Ctrl Pts',(35.865692189114,2.72349173110873,126.706727861265));
#62918=CARTESIAN_POINT('Ctrl Pts',(35.8579459130299,2.60806629876926,126.632310634798));
#62919=CARTESIAN_POINT('Ctrl Pts',(35.8501996369458,2.48973218242708,126.562849480921));
#62920=CARTESIAN_POINT('Ctrl Pts',(35.8424533036804,2.37139719256966,126.493387814297));
#62921=CARTESIAN_POINT('Ctrl Pts',(35.8347069704151,2.25015381303461,126.42888249118));
#62922=CARTESIAN_POINT('Ctrl Pts',(35.8269606371497,2.12645983828727,126.369571826806));
#62923=CARTESIAN_POINT('Ctrl Pts',(35.8192125691467,2.00273816313141,126.31024788022));
#62924=CARTESIAN_POINT('Ctrl Pts',(35.8114645011437,1.87656515319319,126.25612107623));
#62925=CARTESIAN_POINT('Ctrl Pts',(35.8037164331407,1.74842007237432,126.207382228122));
#62926=CARTESIAN_POINT('Ctrl Pts',(35.7959601303989,1.62013879743897,126.158591579786));
#62927=CARTESIAN_POINT('Ctrl Pts',(35.788203827657,1.48988163076539,126.115200465608));
#62928=CARTESIAN_POINT('Ctrl Pts',(35.7804475249151,1.35814507868509,126.077350462326));
#62929=CARTESIAN_POINT('Ctrl Pts',(35.772687082401,1.22633821484043,126.039480257357));
#62930=CARTESIAN_POINT('Ctrl Pts',(35.7649266398868,1.09305077202556,126.007157148365));
#62931=CARTESIAN_POINT('Ctrl Pts',(35.7571661973727,0.958790065340662,125.980471660189));
#62932=CARTESIAN_POINT('Ctrl Pts',(35.7493932971072,0.824313831450109,125.953743334098));
#62933=CARTESIAN_POINT('Ctrl Pts',(35.7416203968418,0.688861598117829,125.932670773761));
#62934=CARTESIAN_POINT('Ctrl Pts',(35.7338474965763,0.552947325291186,125.91729275248));
#62935=CARTESIAN_POINT('Ctrl Pts',(35.7263571608143,0.421973878629179,125.902473761008));
#62936=CARTESIAN_POINT('Ctrl Pts',(35.7188668250523,0.290571709066281,125.892942497224));
#62937=CARTESIAN_POINT('Ctrl Pts',(35.7113764892902,0.159199312747926,125.888687861847));
#62938=CARTESIAN_POINT('Ctrl Pts',(35.7036021551711,0.0228458920933872,
125.884271910676));
#62939=CARTESIAN_POINT('Ctrl Pts',(35.695827821052,-0.113907379694791,125.885526624867));
#62940=CARTESIAN_POINT('Ctrl Pts',(35.6880534869329,-0.250549597146119,
125.892496616815));
#62941=CARTESIAN_POINT('Ctrl Pts',(35.6802887339859,-0.387023415275948,
125.899458018871));
#62942=CARTESIAN_POINT('Ctrl Pts',(35.6725239810387,-0.523386064679369,
125.912120664356));
#62943=CARTESIAN_POINT('Ctrl Pts',(35.6647592280917,-0.659123699436644,
125.930477257109));
#62944=CARTESIAN_POINT('Ctrl Pts',(35.6570021872067,-0.794726517661697,
125.948815617835));
#62945=CARTESIAN_POINT('Ctrl Pts',(35.6492451463217,-0.929705171676313,
125.972836619454));
#62946=CARTESIAN_POINT('Ctrl Pts',(35.6414881054367,-1.06354836088296,126.002480991153));
#62947=CARTESIAN_POINT('Ctrl Pts',(35.6337369141966,-1.19729061789893,126.0321030078));
#62948=CARTESIAN_POINT('Ctrl Pts',(35.6259857229566,-1.32989873427611,126.067339869612));
#62949=CARTESIAN_POINT('Ctrl Pts',(35.6182345317165,-1.46086941649534,126.10808085477));
#62950=CARTESIAN_POINT('Ctrl Pts',(35.6104866349394,-1.5917844326814,126.148804523922));
#62951=CARTESIAN_POINT('Ctrl Pts',(35.6027387381623,-1.72106302636876,126.195027547647));
#62952=CARTESIAN_POINT('Ctrl Pts',(35.5949908413852,-1.84821515353499,126.246588814509));
#62953=CARTESIAN_POINT('Ctrl Pts',(35.5872445653011,-1.97534068321765,126.298139295865));
#62954=CARTESIAN_POINT('Ctrl Pts',(35.579498289217,-2.10034026905229,126.355025652463));
#62955=CARTESIAN_POINT('Ctrl Pts',(35.5717520131329,-2.2227423854061,126.417038045584));
#62956=CARTESIAN_POINT('Ctrl Pts',(35.5640056798676,-2.34514540530436,126.479050896467));
#62957=CARTESIAN_POINT('Ctrl Pts',(35.5562593466021,-2.46495056870129,126.546189682686));
#62958=CARTESIAN_POINT('Ctrl Pts',(35.5485130133368,-2.58170992514885,126.618198063999));
#62959=CARTESIAN_POINT('Ctrl Pts',(35.5407649453338,-2.69849542904522,126.69022257109));
#62960=CARTESIAN_POINT('Ctrl Pts',(35.5330168773308,-2.81223343601147,126.767118638079));
#62961=CARTESIAN_POINT('Ctrl Pts',(35.5252688093278,-2.92250435558116,126.848586185914));
#62962=CARTESIAN_POINT('Ctrl Pts',(35.5175125065859,-3.03289247239596,126.930140318429));
#62963=CARTESIAN_POINT('Ctrl Pts',(35.5097562038441,-3.13980582594915,127.016275404726));
#62964=CARTESIAN_POINT('Ctrl Pts',(35.5019999011022,-3.24285692992184,127.106650245652));
#62965=CARTESIAN_POINT('Ctrl Pts',(35.494239458588,-3.34596303537152,127.197073322353));
#62966=CARTESIAN_POINT('Ctrl Pts',(35.4864790160739,-3.44520250097287,127.291740392943));
#62967=CARTESIAN_POINT('Ctrl Pts',(35.4787185735597,-3.54022494941101,127.39027356975));
#62968=CARTESIAN_POINT('Ctrl Pts',(35.4709456732943,-3.63539993631909,127.488964920759));
#62969=CARTESIAN_POINT('Ctrl Pts',(35.4631727730288,-3.72634411885754,127.591534487279));
#62970=CARTESIAN_POINT('Ctrl Pts',(35.4553998727634,-3.81274706804235,127.697570818169));
#62971=CARTESIAN_POINT('Ctrl Pts',(35.4479095370014,-3.89600905238817,127.799752461342));
#62972=CARTESIAN_POINT('Ctrl Pts',(35.4404192012393,-3.97505405687443,127.905152947208));
#62973=CARTESIAN_POINT('Ctrl Pts',(35.4329288654773,-4.04964359127354,128.013380530543));
#62974=CARTESIAN_POINT('Ctrl Pts',(35.4247403213791,-4.13118595614205,128.131696500207));
#62975=CARTESIAN_POINT('Ctrl Pts',(35.4165517772809,-4.20766704647845,128.253774597608));
#62976=CARTESIAN_POINT('Ctrl Pts',(35.4083632331827,-4.2787288669236,128.379146741254));
#62977=CARTESIAN_POINT('Ctrl Pts',(35.4004930663826,-4.34702774561443,128.499644313319));
#62978=CARTESIAN_POINT('Ctrl Pts',(35.3926228995825,-4.41032059105628,128.623184240247));
#62979=CARTESIAN_POINT('Ctrl Pts',(35.3847527327825,-4.46833125497048,128.749318316699));
#62980=CARTESIAN_POINT('Ctrl Pts',(35.376890577065,-4.5262828695363,128.875324000636));
#62981=CARTESIAN_POINT('Ctrl Pts',(35.3690284213476,-4.5789628450409,129.003918239692));
#62982=CARTESIAN_POINT('Ctrl Pts',(35.3611662656302,-4.62614009302874,129.13462683574));
#62983=CARTESIAN_POINT('Ctrl Pts',(35.3533121480127,-4.67326910800649,129.265201798112));
#62984=CARTESIAN_POINT('Ctrl Pts',(35.3454580303952,-4.71490647440109,129.397886458584));
#62985=CARTESIAN_POINT('Ctrl Pts',(35.3376039127777,-4.7508687549419,129.532185654828));
#62986=CARTESIAN_POINT('Ctrl Pts',(35.336624720618,-4.75535226090213,129.548929065918));
#62987=CARTESIAN_POINT('Ctrl Pts',(35.3356455284583,-4.75974761945892,129.565697547361));
#62988=CARTESIAN_POINT('Ctrl Pts',(35.3346663362986,-4.76405452823404,129.582490119308));
#62989=CARTESIAN_POINT('Ctrl Pts',(37.0846781642943,-4.76405452823403,129.582490119308));
#62990=CARTESIAN_POINT('Ctrl Pts',(37.0754335152278,-4.80440312556933,129.739808687943));
#62991=CARTESIAN_POINT('Ctrl Pts',(37.0661888661614,-4.8369949620545,129.899282122246));
#62992=CARTESIAN_POINT('Ctrl Pts',(37.0569442170948,-4.86162747657715,130.060209193802));
#62993=CARTESIAN_POINT('Ctrl Pts',(37.0477930819962,-4.88601082164451,130.219508412435));
#62994=CARTESIAN_POINT('Ctrl Pts',(37.0386419468975,-4.90259499612365,130.380231947554));
#62995=CARTESIAN_POINT('Ctrl Pts',(37.0294908117989,-4.91123014170045,130.541679141719));
#62996=CARTESIAN_POINT('Ctrl Pts',(37.0246136865457,-4.91583226877033,130.627722914348));
#62997=CARTESIAN_POINT('Ctrl Pts',(37.0197365612925,-4.91817735973255,130.713971890829));
#62998=CARTESIAN_POINT('Ctrl Pts',(37.0148594360393,-4.91824833830055,130.800317684988));
#62999=CARTESIAN_POINT('',(37.3601405639635,-4.9182499932755,130.804103429838));
#63000=CARTESIAN_POINT('Ctrl Pts',(37.4302319972993,-4.76405452823409,129.582490119308));
#63001=CARTESIAN_POINT('Ctrl Pts',(37.4224712764234,-4.79812304700691,129.715322756942));
#63002=CARTESIAN_POINT('Ctrl Pts',(37.4147105555475,-4.82660434211345,129.849473974204));
#63003=CARTESIAN_POINT('Ctrl Pts',(37.4069498346715,-4.84942300612506,129.984434053681));
#63004=CARTESIAN_POINT('Ctrl Pts',(37.3991767847143,-4.87227792104283,130.119608537698));
#63005=CARTESIAN_POINT('Ctrl Pts',(37.391403734757,-4.88945218054426,130.255594063599));
#63006=CARTESIAN_POINT('Ctrl Pts',(37.3836306847998,-4.90092230039882,130.391875868813));
#63007=CARTESIAN_POINT('Ctrl Pts',(37.3765782018693,-4.91132913232845,130.515524257838));
#63008=CARTESIAN_POINT('Ctrl Pts',(37.3695257189387,-4.91704102316591,130.639416300982));
#63009=CARTESIAN_POINT('Ctrl Pts',(37.3624732360082,-4.91807750796032,130.763169742425));
#63010=CARTESIAN_POINT('Ctrl Pts',(37.3616956786751,-4.91819178350845,130.776813929422));
#63011=CARTESIAN_POINT('Ctrl Pts',(37.3609181213419,-4.91824927975026,130.790458592636));
#63012=CARTESIAN_POINT('Ctrl Pts',(37.3601405640087,-4.91824999327546,130.804103429044));
#63013=CARTESIAN_POINT('Ctrl Pts',(37.3601405639634,-4.9182499932755,130.804103429838));
#63014=CARTESIAN_POINT('Ctrl Pts',(37.3523778041444,-4.9182571167472,130.940326938106));
#63015=CARTESIAN_POINT('Ctrl Pts',(37.3446150443255,-4.91260036309792,131.076769552372));
#63016=CARTESIAN_POINT('Ctrl Pts',(37.3368522845065,-4.90125105140445,131.212920519669));
#63017=CARTESIAN_POINT('Ctrl Pts',(37.3290990918319,-4.88991572706942,131.348903688916));
#63018=CARTESIAN_POINT('Ctrl Pts',(37.3213458991574,-4.87290183538294,131.484595539201));
#63019=CARTESIAN_POINT('Ctrl Pts',(37.3135927064828,-4.85023267081422,131.619483983362));
#63020=CARTESIAN_POINT('Ctrl Pts',(37.3058471995574,-4.82758597821549,131.754238712446));
#63021=CARTESIAN_POINT('Ctrl Pts',(37.298101692632,-4.79929523305588,131.888191235892));
#63022=CARTESIAN_POINT('Ctrl Pts',(37.2903561857066,-4.7654356002907,132.020833634933));
#63023=CARTESIAN_POINT('Ctrl Pts',(37.2826164899166,-4.73160137101562,132.153376517836));
#63024=CARTESIAN_POINT('Ctrl Pts',(37.2748767941265,-4.69220666661304,132.284610854149));
#63025=CARTESIAN_POINT('Ctrl Pts',(37.2671370983365,-4.64737782508226,132.41403835346));
#63026=CARTESIAN_POINT('Ctrl Pts',(37.2594006351337,-4.60256770691539,132.54341179565));
#63027=CARTESIAN_POINT('Ctrl Pts',(37.2516641719308,-4.55232809347918,132.670979531734));
#63028=CARTESIAN_POINT('Ctrl Pts',(37.243927708728,-4.49683526483856,132.796258120804));
#63029=CARTESIAN_POINT('Ctrl Pts',(37.2361928087239,-4.44135364885621,132.921511396584));
#63030=CARTESIAN_POINT('Ctrl Pts',(37.2284579087198,-4.38062108760279,133.044476086857));
#63031=CARTESIAN_POINT('Ctrl Pts',(37.2207230087157,-4.31486196531586,133.164688832618));
#63032=CARTESIAN_POINT('Ctrl Pts',(37.2129879830845,-4.24910177499682,133.284903530824));
#63033=CARTESIAN_POINT('Ctrl Pts',(37.2052529574535,-4.17831504931166,133.402365851346));
#63034=CARTESIAN_POINT('Ctrl Pts',(37.1975179318223,-4.10277187954645,133.516637514732));
#63035=CARTESIAN_POINT('Ctrl Pts',(37.1897810920046,-4.02721099175189,133.630935979598));
#63036=CARTESIAN_POINT('Ctrl Pts',(37.1820442521868,-3.94689165646444,133.742041971183));
#63037=CARTESIAN_POINT('Ctrl Pts',(37.174307412369,-3.86212674368066,133.849546995811));
#63038=CARTESIAN_POINT('Ctrl Pts',(37.1665623311173,-3.77727153764473,133.957166536904));
#63039=CARTESIAN_POINT('Ctrl Pts',(37.1588172498655,-3.68796153855184,134.061177140821));
#63040=CARTESIAN_POINT('Ctrl Pts',(37.1510721686138,-3.59454962950483,134.161203780945));
#63041=CARTESIAN_POINT('Ctrl Pts',(37.1433228552727,-3.5010866780555,134.261285077912));
#63042=CARTESIAN_POINT('Ctrl Pts',(37.1355735419316,-3.40351763033354,134.357377798867));
#63043=CARTESIAN_POINT('Ctrl Pts',(37.1278242285904,-3.302230782838,134.449145236632));
#63044=CARTESIAN_POINT('Ctrl Pts',(37.1200626672136,-3.2007838482657,134.541057715744));
#63045=CARTESIAN_POINT('Ctrl Pts',(37.1123011058368,-3.09560767478678,134.628631001705));
#63046=CARTESIAN_POINT('Ctrl Pts',(37.10453954446,-2.9871226855163,134.711569483774));
#63047=CARTESIAN_POINT('Ctrl Pts',(37.0977015670384,-2.89154682504207,134.784638733662));
#63048=CARTESIAN_POINT('Ctrl Pts',(37.0908635896169,-2.79340335410348,134.854111132265));
#63049=CARTESIAN_POINT('Ctrl Pts',(37.0840256121953,-2.69299607361674,134.919813838049));
#63050=CARTESIAN_POINT('Ctrl Pts',(37.0762512780763,-2.57883954773673,134.994513527124));
#63051=CARTESIAN_POINT('Ctrl Pts',(37.0684769439571,-2.46139176392207,135.06457813823));
#63052=CARTESIAN_POINT('Ctrl Pts',(37.060702609838,-2.34106585819466,135.129703807429));
#63053=CARTESIAN_POINT('Ctrl Pts',(37.0529378568909,-2.22088824339222,135.194749215061));
#63054=CARTESIAN_POINT('Ctrl Pts',(37.0451731039439,-2.09783990473823,135.254867607402));
#63055=CARTESIAN_POINT('Ctrl Pts',(37.0374083509968,-1.97236349131766,135.309797923824));
#63056=CARTESIAN_POINT('Ctrl Pts',(37.0296513101118,-1.84701170283981,135.364673682681));
#63057=CARTESIAN_POINT('Ctrl Pts',(37.0218942692268,-1.71923699461641,135.41437146429));
#63058=CARTESIAN_POINT('Ctrl Pts',(37.0141372283418,-1.58950687801603,135.458675921372));
#63059=CARTESIAN_POINT('Ctrl Pts',(37.0063860371016,-1.45987459190555,135.502946968118));
#63060=CARTESIAN_POINT('Ctrl Pts',(36.9986348458615,-1.32829020098468,135.541832659905));
#63061=CARTESIAN_POINT('Ctrl Pts',(36.9908836546213,-1.19524114186396,135.575165756669));
#63062=CARTESIAN_POINT('Ctrl Pts',(36.9831357578443,-1.06224863214274,135.608484685979));
#63063=CARTESIAN_POINT('Ctrl Pts',(36.9753878610671,-0.92779307082301,135.636255619314));
#63064=CARTESIAN_POINT('Ctrl Pts',(36.96763996429,-0.792376790317983,135.658361244334));
#63065=CARTESIAN_POINT('Ctrl Pts',(36.9598936882059,-0.656988835979415,
135.680462245334));
#63066=CARTESIAN_POINT('Ctrl Pts',(36.9521474121218,-0.52064094779285,135.696900232221));
#63067=CARTESIAN_POINT('Ctrl Pts',(36.9444011360377,-0.383844989328075,
135.707609141419));
#63068=CARTESIAN_POINT('Ctrl Pts',(36.9366548027723,-0.247048021066796,
135.718318129668));
#63069=CARTESIAN_POINT('Ctrl Pts',(36.928908469507,-0.109803365700026,135.723297925327));
#63070=CARTESIAN_POINT('Ctrl Pts',(36.9211621362416,0.0273730586309466,
135.722534443099));
#63071=CARTESIAN_POINT('Ctrl Pts',(36.9134140682387,0.164580202671034,135.721770789896));
#63072=CARTESIAN_POINT('Ctrl Pts',(36.9056660002356,0.301718694385837,135.715261301658));
#63073=CARTESIAN_POINT('Ctrl Pts',(36.8979179322326,0.438274084659371,135.703044000804));
#63074=CARTESIAN_POINT('Ctrl Pts',(36.8901616294908,0.574974607626718,135.690813715258));
#63075=CARTESIAN_POINT('Ctrl Pts',(36.882405326749,0.711090401150329,135.672863533843));
#63076=CARTESIAN_POINT('Ctrl Pts',(36.8746490240071,0.846113045068823,135.649283297802));
#63077=CARTESIAN_POINT('Ctrl Pts',(36.8668885814929,0.981207754637829,135.625690476279));
#63078=CARTESIAN_POINT('Ctrl Pts',(36.8591281389788,1.11520777023767,135.596461695834));
#63079=CARTESIAN_POINT('Ctrl Pts',(36.8513676964646,1.24761728031085,135.561737435138));
#63080=CARTESIAN_POINT('Ctrl Pts',(36.8435947961992,1.38023934588435,135.526957431975));
#63081=CARTESIAN_POINT('Ctrl Pts',(36.8358218959337,1.51126542987309,135.486664434713));
#63082=CARTESIAN_POINT('Ctrl Pts',(36.8280489956683,1.64021637985857,135.441048367431));
#63083=CARTESIAN_POINT('Ctrl Pts',(36.8205586599063,1.76447963800284,135.397090559094));
#63084=CARTESIAN_POINT('Ctrl Pts',(36.8130683241444,1.88681572945309,135.348190089941));
#63085=CARTESIAN_POINT('Ctrl Pts',(36.8055779883824,2.00681719220789,135.294557475117));
#63086=CARTESIAN_POINT('Ctrl Pts',(36.7978036542634,2.13136854689776,135.2388913634));
#63087=CARTESIAN_POINT('Ctrl Pts',(36.7900293201443,2.25379928452739,135.177950850309));
#63088=CARTESIAN_POINT('Ctrl Pts',(36.7822549860253,2.37363044564825,135.111919272999));
#63089=CARTESIAN_POINT('Ctrl Pts',(36.7744902330782,2.49331392557281,135.045969073706));
#63090=CARTESIAN_POINT('Ctrl Pts',(36.7667254801311,2.6104038643552,134.97494048102));
#63091=CARTESIAN_POINT('Ctrl Pts',(36.758960727184,2.72444136165393,134.899064798506));
#63092=CARTESIAN_POINT('Ctrl Pts',(36.751203686299,2.83836559530254,134.82326447679));
#63093=CARTESIAN_POINT('Ctrl Pts',(36.743446645414,2.94924309734985,134.74262686089));
#63094=CARTESIAN_POINT('Ctrl Pts',(36.735689604529,3.05663998871665,134.657428880896));
#63095=CARTESIAN_POINT('Ctrl Pts',(36.7279384132889,3.1639558912524,134.572295149361));
#63096=CARTESIAN_POINT('Ctrl Pts',(36.7201872220488,3.2677961024728,134.482608140862));
#63097=CARTESIAN_POINT('Ctrl Pts',(36.7124360308087,3.36775644718183,134.388687552287));
#63098=CARTESIAN_POINT('Ctrl Pts',(36.7046881340316,3.46767430607783,134.294806882467));
#63099=CARTESIAN_POINT('Ctrl Pts',(36.6969402372545,3.56371529395929,134.19669647856));
#63100=CARTESIAN_POINT('Ctrl Pts',(36.6891923404774,3.65550918969215,134.094715556866));
#63101=CARTESIAN_POINT('Ctrl Pts',(36.6814460643933,3.74728388412075,133.992755967383));
#63102=CARTESIAN_POINT('Ctrl Pts',(36.6736997883093,3.83481299208366,133.886927760912));
#63103=CARTESIAN_POINT('Ctrl Pts',(36.6659535122252,3.91776425766106,133.777625873794));
#63104=CARTESIAN_POINT('Ctrl Pts',(36.6582071789599,4.00071613556585,133.668323179835));
#63105=CARTESIAN_POINT('Ctrl Pts',(36.6504608456946,4.07908986730144,133.555547065496));
#63106=CARTESIAN_POINT('Ctrl Pts',(36.6427145124293,4.1525947361521,133.439723973876));
#63107=CARTESIAN_POINT('Ctrl Pts',(36.6349664444263,4.22611606590828,133.323874944478));
#63108=CARTESIAN_POINT('Ctrl Pts',(36.6272183764233,4.29476615366091,133.204977910039));
#63109=CARTESIAN_POINT('Ctrl Pts',(36.6194703084204,4.35829891643479,133.083486243218));
#63110=CARTESIAN_POINT('Ctrl Pts',(36.6117140056786,4.42189920258526,132.961865453607));
#63111=CARTESIAN_POINT('Ctrl Pts',(36.6039577029367,4.48037111779735,132.837644870003));
#63112=CARTESIAN_POINT('Ctrl Pts',(36.5962014001948,4.53351543453886,132.711300802076));
#63113=CARTESIAN_POINT('Ctrl Pts',(36.5884409576807,4.58668811600236,132.584889300515));
#63114=CARTESIAN_POINT('Ctrl Pts',(36.5806805151665,4.63452739677627,132.45635242253));
#63115=CARTESIAN_POINT('Ctrl Pts',(36.5729200726524,4.67688346728702,132.32618324058));
#63116=CARTESIAN_POINT('Ctrl Pts',(36.5651471723869,4.71930753152241,132.195805099503));
#63117=CARTESIAN_POINT('Ctrl Pts',(36.5573742721215,4.7562306906546,132.06378979496));
#63118=CARTESIAN_POINT('Ctrl Pts',(36.5496013718561,4.78755373960541,131.930643110056));
#63119=CARTESIAN_POINT('Ctrl Pts',(36.542111036094,4.81773811682938,131.802336642523));
#63120=CARTESIAN_POINT('Ctrl Pts',(36.5346207003317,4.84272241285229,131.672979926006));
#63121=CARTESIAN_POINT('Ctrl Pts',(36.5271303645696,4.86246349686421,131.543029558407));
#63122=CARTESIAN_POINT('Ctrl Pts',(36.5193560304505,4.88295307007626,131.408152083125));
#63123=CARTESIAN_POINT('Ctrl Pts',(36.5115816963315,4.89785889471362,131.272207800258));
#63124=CARTESIAN_POINT('Ctrl Pts',(36.5038073622124,4.90707632823586,131.135698770164));
#63125=CARTESIAN_POINT('Ctrl Pts',(36.4960426092653,4.91628240209508,130.99935797525));
#63126=CARTESIAN_POINT('Ctrl Pts',(36.4882778563181,4.91981400742653,130.862454204276));
#63127=CARTESIAN_POINT('Ctrl Pts',(36.480513103371,4.91761769962746,130.725498568324));
#63128=CARTESIAN_POINT('Ctrl Pts',(36.472756062486,4.91542357323227,130.588678958639));
#63129=CARTESIAN_POINT('Ctrl Pts',(36.464999021601,4.90751286138939,130.451807974875));
#63130=CARTESIAN_POINT('Ctrl Pts',(36.457241980716,4.89388403098659,130.315400339267));
#63131=CARTESIAN_POINT('Ctrl Pts',(36.4494907894759,4.88026547819087,130.179095569718));
#63132=CARTESIAN_POINT('Ctrl Pts',(36.4417395982358,4.86093742847594,130.043253840291));
#63133=CARTESIAN_POINT('Ctrl Pts',(36.4339884069957,4.83595038532041,129.908387999));
#63134=CARTESIAN_POINT('Ctrl Pts',(36.4262405102186,4.8109739623247,129.77357947929));
#63135=CARTESIAN_POINT('Ctrl Pts',(36.4184926134416,4.78034340076808,129.639746406371));
#63136=CARTESIAN_POINT('Ctrl Pts',(36.4107447166645,4.74416080593153,129.507394422955));
#63137=CARTESIAN_POINT('Ctrl Pts',(36.4029984405804,4.70798577971382,129.375070124721));
#63138=CARTESIAN_POINT('Ctrl Pts',(36.3952521644963,4.66626113327027,129.244226676643));
#63139=CARTESIAN_POINT('Ctrl Pts',(36.3875058884122,4.61913954528972,129.115357087777));
#63140=CARTESIAN_POINT('Ctrl Pts',(36.3797595551468,4.57201760946825,128.986486547624));
#63141=CARTESIAN_POINT('Ctrl Pts',(36.3720132218815,4.51949878687747,128.859590262946));
#63142=CARTESIAN_POINT('Ctrl Pts',(36.3642668886161,4.46178471668666,128.735143324858));
#63143=CARTESIAN_POINT('Ctrl Pts',(36.3565188206131,4.40405772182991,128.610668517742));
#63144=CARTESIAN_POINT('Ctrl Pts',(36.3487707526101,4.34113332871914,128.488644503307));
#63145=CARTESIAN_POINT('Ctrl Pts',(36.3410226846071,4.2732599587523,128.369523377128));
#63146=CARTESIAN_POINT('Ctrl Pts',(36.3332663818653,4.20531445216025,128.250275647598));
#63147=CARTESIAN_POINT('Ctrl Pts',(36.3255100791234,4.13240965549268,128.133937309625));
#63148=CARTESIAN_POINT('Ctrl Pts',(36.3177537763816,4.05483861421586,128.020933435985));
#63149=CARTESIAN_POINT('Ctrl Pts',(36.3099933338674,3.97722617093868,127.907869248775));
#63150=CARTESIAN_POINT('Ctrl Pts',(36.3022328913532,3.89494275493409,127.798143384742));
#63151=CARTESIAN_POINT('Ctrl Pts',(36.294472448839,3.80832222629196,127.692148400632));
#63152=CARTESIAN_POINT('Ctrl Pts',(36.2866995485736,3.72156264668746,127.585983263964));
#63153=CARTESIAN_POINT('Ctrl Pts',(36.2789266483081,3.630452301517,127.48356126771));
#63154=CARTESIAN_POINT('Ctrl Pts',(36.2711537480427,3.53536309766314,127.385239264034));
#63155=CARTESIAN_POINT('Ctrl Pts',(36.2636634122807,3.443730625885,127.29049151285));
#63156=CARTESIAN_POINT('Ctrl Pts',(36.2561730765187,3.34840377898473,127.199551052025));
#63157=CARTESIAN_POINT('Ctrl Pts',(36.2486827407567,3.24974339245113,127.112700971049));
#63158=CARTESIAN_POINT('Ctrl Pts',(36.2409084066377,3.14734226737451,127.022557942856));
#63159=CARTESIAN_POINT('Ctrl Pts',(36.2331340725186,3.04102545436761,126.93653604492));
#63160=CARTESIAN_POINT('Ctrl Pts',(36.2253597383995,2.9311587891807,126.854994691862));
#63161=CARTESIAN_POINT('Ctrl Pts',(36.2175949854524,2.82142752483986,126.773553831235));
#63162=CARTESIAN_POINT('Ctrl Pts',(36.2098302325054,2.70815542394951,126.696582759378));
#63163=CARTESIAN_POINT('Ctrl Pts',(36.2020654795583,2.59174361062467,126.624402708772));
#63164=CARTESIAN_POINT('Ctrl Pts',(36.1943084386733,2.47544741915411,126.552294348411));
#63165=CARTESIAN_POINT('Ctrl Pts',(36.1865513977883,2.35601805114521,126.484967744343));
#63166=CARTESIAN_POINT('Ctrl Pts',(36.1787943569034,2.23388772830796,126.422702406362));
#63167=CARTESIAN_POINT('Ctrl Pts',(36.1710431656632,2.11184950489721,126.360484023156));
#63168=CARTESIAN_POINT('Ctrl Pts',(36.1632919744232,1.98711472770768,126.303319485905));
#63169=CARTESIAN_POINT('Ctrl Pts',(36.1555407831831,1.86014216866299,126.251443511483));
#63170=CARTESIAN_POINT('Ctrl Pts',(36.147792886406,1.73322357634265,126.199589585734));
#63171=CARTESIAN_POINT('Ctrl Pts',(36.1400449896289,1.60406945503248,126.153019899707));
#63172=CARTESIAN_POINT('Ctrl Pts',(36.1322970928518,1.47316040666341,126.111921861574));
#63173=CARTESIAN_POINT('Ctrl Pts',(36.1245508167677,1.34227874164482,126.070832420264));
#63174=CARTESIAN_POINT('Ctrl Pts',(36.1168045406836,1.20964325251376,126.035212467305));
#63175=CARTESIAN_POINT('Ctrl Pts',(36.1090582645995,1.07575124831147,126.005200033229));
#63176=CARTESIAN_POINT('Ctrl Pts',(36.1013119313341,0.941858255748634,125.975187377607));
#63177=CARTESIAN_POINT('Ctrl Pts',(36.0935655980687,0.806709111104827,125.95078240898));
#63178=CARTESIAN_POINT('Ctrl Pts',(36.0858192648033,0.670812512888385,125.932072280957));
#63179=CARTESIAN_POINT('Ctrl Pts',(36.0780711968004,0.534885481571384,125.913357962931));
#63180=CARTESIAN_POINT('Ctrl Pts',(36.0703231287974,0.398211050838375,125.900341076563));
#63181=CARTESIAN_POINT('Ctrl Pts',(36.0625750607944,0.261303859331813,125.893056986594));
#63182=CARTESIAN_POINT('Ctrl Pts',(36.0548187580526,0.124251161232901,125.885765155008));
#63183=CARTESIAN_POINT('Ctrl Pts',(36.0470624553108,-0.0130344007740541,
125.884218311819));
#63184=CARTESIAN_POINT('Ctrl Pts',(36.0393061525689,-0.150036802691739,
125.888399671796));
#63185=CARTESIAN_POINT('Ctrl Pts',(36.0315457100547,-0.287112326916577,
125.89258326349));
#63186=CARTESIAN_POINT('Ctrl Pts',(36.0237852675405,-0.423904000159855,
125.902501122049));
#63187=CARTESIAN_POINT('Ctrl Pts',(36.0160248250264,-0.559901093780867,
125.918084548034));
#63188=CARTESIAN_POINT('Ctrl Pts',(36.0082519247609,-0.696116502009629,
125.933692989917));
#63189=CARTESIAN_POINT('Ctrl Pts',(36.0004790244955,-0.831534395258706,
125.954985112916));
#63190=CARTESIAN_POINT('Ctrl Pts',(35.99270612423,-0.965653518941221,125.981840908549));
#63191=CARTESIAN_POINT('Ctrl Pts',(35.9852157884679,-1.09489707465365,126.007720428365));
#63192=CARTESIAN_POINT('Ctrl Pts',(35.9777254527058,-1.2229343491525,126.03876606404));
#63193=CARTESIAN_POINT('Ctrl Pts',(35.9702351169437,-1.34933213083662,126.07482725124));
#63194=CARTESIAN_POINT('Ctrl Pts',(35.9624607828246,-1.48052232282976,126.112255709313));
#63195=CARTESIAN_POINT('Ctrl Pts',(35.9546864487055,-1.61036181619281,126.155206118109));
#63196=CARTESIAN_POINT('Ctrl Pts',(35.9469121145864,-1.73835048206726,126.20356496203));
#63197=CARTESIAN_POINT('Ctrl Pts',(35.9391473616393,-1.86618141334934,126.251864207999));
#63198=CARTESIAN_POINT('Ctrl Pts',(35.9313826086923,-1.99216569339321,126.305558490049));
#63199=CARTESIAN_POINT('Ctrl Pts',(35.9236178557452,-2.11581624283175,126.364483965105));
#63200=CARTESIAN_POINT('Ctrl Pts',(35.9158608148602,-2.23934398080176,126.423350914549));
#63201=CARTESIAN_POINT('Ctrl Pts',(35.9081037739752,-2.36054225022622,126.487438550228));
#63202=CARTESIAN_POINT('Ctrl Pts',(35.9003467330901,-2.47894226520921,126.556534313648));
#63203=CARTESIAN_POINT('Ctrl Pts',(35.89259554185,-2.59725299381955,126.625577971414));
#63204=CARTESIAN_POINT('Ctrl Pts',(35.8848443506099,-2.71276933187949,126.699622043432));
#63205=CARTESIAN_POINT('Ctrl Pts',(35.8770931593698,-2.82504582800595,126.77840742209));
#63206=CARTESIAN_POINT('Ctrl Pts',(35.8693452625927,-2.93727460362663,126.85715931486));
#63207=CARTESIAN_POINT('Ctrl Pts',(35.8615973658156,-3.04626595673606,126.940648282128));
#63208=CARTESIAN_POINT('Ctrl Pts',(35.8538494690385,-3.15160243844918,127.028571278572));
#63209=CARTESIAN_POINT('Ctrl Pts',(35.8461031929544,-3.25691688604112,127.11647588342));
#63210=CARTESIAN_POINT('Ctrl Pts',(35.8383569168703,-3.35857768295184,127.208812422219));
#63211=CARTESIAN_POINT('Ctrl Pts',(35.8306106407862,-3.45619989250171,127.30523710366));
#63212=CARTESIAN_POINT('Ctrl Pts',(35.8228643075208,-3.55382282267643,127.401662496886));
#63213=CARTESIAN_POINT('Ctrl Pts',(35.8151179742555,-3.64740682784782,127.50217581823));
#63214=CARTESIAN_POINT('Ctrl Pts',(35.8073716409901,-3.73660361924633,127.606396193884));
#63215=CARTESIAN_POINT('Ctrl Pts',(35.7996235729872,-3.82582038564783,127.710639908969));
#63216=CARTESIAN_POINT('Ctrl Pts',(35.7918755049842,-3.91064772907651,127.818592033328));
#63217=CARTESIAN_POINT('Ctrl Pts',(35.7841274369812,-3.99077772141636,127.929838702404));
#63218=CARTESIAN_POINT('Ctrl Pts',(35.7763711342394,-4.07099287686562,128.041203605763));
#63219=CARTESIAN_POINT('Ctrl Pts',(35.7686148314975,-4.1465004795,128.155869730682));
#63220=CARTESIAN_POINT('Ctrl Pts',(35.7608585287557,-4.21703572763549,128.273393858727));
#63221=CARTESIAN_POINT('Ctrl Pts',(35.7530980862415,-4.28760862255669,128.390980712939));
#63222=CARTESIAN_POINT('Ctrl Pts',(35.7453376437273,-4.35320368797253,128.511428266588));
#63223=CARTESIAN_POINT('Ctrl Pts',(35.7375772012132,-4.4136026613618,128.63426969548));
#63224=CARTESIAN_POINT('Ctrl Pts',(35.7298043009478,-4.47409859254521,128.757308320339));
#63225=CARTESIAN_POINT('Ctrl Pts',(35.7220314006823,-4.52938160550884,128.882748141734));
#63226=CARTESIAN_POINT('Ctrl Pts',(35.7142585004169,-4.5792817264392,129.010102572468));
#63227=CARTESIAN_POINT('Ctrl Pts',(35.7067681646548,-4.62736785228278,129.132827348858));
#63228=CARTESIAN_POINT('Ctrl Pts',(35.6992778288928,-4.67045555408226,129.25732965851));
#63229=CARTESIAN_POINT('Ctrl Pts',(35.6917874931308,-4.70843734442204,129.383163644535));
#63230=CARTESIAN_POINT('Ctrl Pts',(35.6878573985263,-4.72836596097904,129.449187316271));
#63231=CARTESIAN_POINT('Ctrl Pts',(35.6839273039218,-4.74691073125618,129.515646715085));
#63232=CARTESIAN_POINT('Ctrl Pts',(35.6799972093173,-4.76405452823406,129.582490119308));
#63233=CARTESIAN_POINT('Origin',(213.235140564004,0.,130.804360617566));
#63234=CARTESIAN_POINT('',(33.584997801213,-4.7640545282341,129.582490119308));
#63235=CARTESIAN_POINT('',(33.9299189896066,-4.764054528234,129.582490119308));
#63236=CARTESIAN_POINT('',(213.235140564004,-4.76405452823405,129.582490119308));
#63237=CARTESIAN_POINT('',(35.2648594359407,-4.91824928377686,130.80701488364));
#63238=CARTESIAN_POINT('Ctrl Pts',(35.2648594359407,-4.91824928377686,130.80701488364));
#63239=CARTESIAN_POINT('Ctrl Pts',(35.2562894561528,-4.91816724259869,130.959033918108));
#63240=CARTESIAN_POINT('Ctrl Pts',(35.2477194763649,-4.91103296049634,131.110804385526));
#63241=CARTESIAN_POINT('Ctrl Pts',(35.2391494965771,-4.89693982404999,131.261704494898));
#63242=CARTESIAN_POINT('Ctrl Pts',(35.2305320272072,-4.88276859206837,131.413440800305));
#63243=CARTESIAN_POINT('Ctrl Pts',(35.2219145578374,-4.8615612559285,131.56429684572));
#63244=CARTESIAN_POINT('Ctrl Pts',(35.2132970884676,-4.83346292747159,131.713656604172));
#63245=CARTESIAN_POINT('Ctrl Pts',(35.2046550026758,-4.80528433411579,131.863443019531));
#63246=CARTESIAN_POINT('Ctrl Pts',(35.1960129168841,-4.77017544093273,132.011724373643));
#63247=CARTESIAN_POINT('Ctrl Pts',(35.1873708310923,-4.72833133818723,132.157898876655));
#63248=CARTESIAN_POINT('Ctrl Pts',(35.1786971614629,-4.68633430970349,132.304607596971));
#63249=CARTESIAN_POINT('Ctrl Pts',(35.1700234918334,-4.63755287123151,132.449193829812));
#63250=CARTESIAN_POINT('Ctrl Pts',(35.161349822204,-4.58223150063536,132.591071992435));
#63251=CARTESIAN_POINT('Ctrl Pts',(35.1590602953575,-4.5676287121297,132.628522561356));
#63252=CARTESIAN_POINT('Ctrl Pts',(35.156770768511,-4.55257049352782,132.665784574027));
#63253=CARTESIAN_POINT('Ctrl Pts',(35.1544812416645,-4.53706187100313,132.702847552256));
#63254=CARTESIAN_POINT('Ctrl Pts',(35.1467069075454,-4.48440067883743,132.828698872426));
#63255=CARTESIAN_POINT('Ctrl Pts',(35.1389325734263,-4.42641571523285,132.952556757311));
#63256=CARTESIAN_POINT('Ctrl Pts',(35.1311582393072,-4.36327877084152,133.073937985805));
#63257=CARTESIAN_POINT('Ctrl Pts',(35.1233934863601,-4.30021963709144,133.195169622783));
#63258=CARTESIAN_POINT('Ctrl Pts',(35.115628733413,-4.2320213345633,133.313930332933));
#63259=CARTESIAN_POINT('Ctrl Pts',(35.1078639804659,-4.15890408787074,133.429755797418));
#63260=CARTESIAN_POINT('Ctrl Pts',(35.1001069395809,-4.08585946225846,133.545466222419));
#63261=CARTESIAN_POINT('Ctrl Pts',(35.0923498986959,-4.00790582232535,133.658246874925));
#63262=CARTESIAN_POINT('Ctrl Pts',(35.0845928578109,-3.92530960651127,133.767657355244));
#63263=CARTESIAN_POINT('Ctrl Pts',(35.0768416665708,-3.84277567714615,133.876985328268));
#63264=CARTESIAN_POINT('Ctrl Pts',(35.0690904753307,-3.75560637504087,133.982947876983));
#63265=CARTESIAN_POINT('Ctrl Pts',(35.0613392840906,-3.66411160592648,134.08513327074));
#63266=CARTESIAN_POINT('Ctrl Pts',(35.0535913873135,-3.57265572452953,134.18727523298));
#63267=CARTESIAN_POINT('Ctrl Pts',(35.0458434905364,-3.47687829288984,134.285642942603));
#63268=CARTESIAN_POINT('Ctrl Pts',(35.0380955937594,-3.377129539576,134.37985766489));
#63269=CARTESIAN_POINT('Ctrl Pts',(35.0303493176753,-3.27740165155103,134.474052679488));
#63270=CARTESIAN_POINT('Ctrl Pts',(35.0226030415912,-3.17370437823536,134.564096166386));
#63271=CARTESIAN_POINT('Ctrl Pts',(35.0148567655071,-3.0664245690127,134.64964648796));
#63272=CARTESIAN_POINT('Ctrl Pts',(35.0071104322417,-2.95914396787486,134.735197441048));
#63273=CARTESIAN_POINT('Ctrl Pts',(34.9993640989764,-2.84828108373235,134.816254918872));
#63274=CARTESIAN_POINT('Ctrl Pts',(34.9916177657111,-2.73425526047784,134.892518054976));
#63275=CARTESIAN_POINT('Ctrl Pts',(34.9838696977081,-2.62020390193065,134.968798269681));
#63276=CARTESIAN_POINT('Ctrl Pts',(34.976121629705,-2.50298851971675,135.040281788896));
#63277=CARTESIAN_POINT('Ctrl Pts',(34.9683735617021,-2.38305645062066,135.106711720818));
#63278=CARTESIAN_POINT('Ctrl Pts',(34.9606172589602,-2.26299691629449,135.173212255263));
#63279=CARTESIAN_POINT('Ctrl Pts',(34.9528609562184,-2.1402152698902,135.2346482835));
#63280=CARTESIAN_POINT('Ctrl Pts',(34.9451046534766,-2.01518290299934,135.290809205253));
#63281=CARTESIAN_POINT('Ctrl Pts',(34.9373442109624,-1.89008380256962,135.347000101781));
#63282=CARTESIAN_POINT('Ctrl Pts',(34.9295837684482,-1.76273195086124,135.39791013668));
#63283=CARTESIAN_POINT('Ctrl Pts',(34.921823325934,-1.63361668332313,135.44337771114));
#63284=CARTESIAN_POINT('Ctrl Pts',(34.9140504256686,-1.50429414849508,135.488918274186));
#63285=CARTESIAN_POINT('Ctrl Pts',(34.9062775254032,-1.37320291510912,135.528998803664));
#63286=CARTESIAN_POINT('Ctrl Pts',(34.8985046251378,-1.24084623996858,135.563507985662));
#63287=CARTESIAN_POINT('Ctrl Pts',(34.8910142893758,-1.11330106335539,135.596762671972));
#63288=CARTESIAN_POINT('Ctrl Pts',(34.8835239536137,-0.984581152594259,
135.624843977655));
#63289=CARTESIAN_POINT('Ctrl Pts',(34.8760336178516,-0.855141939076149,
135.647697827232));
#63290=CARTESIAN_POINT('Ctrl Pts',(34.8682592837326,-0.720794998435681,
135.671418187462));
#63291=CARTESIAN_POINT('Ctrl Pts',(34.8604849496135,-0.585247562854529,
135.689582007539));
#63292=CARTESIAN_POINT('Ctrl Pts',(34.8527106154944,-0.44899903697857,135.702072626994));
#63293=CARTESIAN_POINT('Ctrl Pts',(34.8449458625473,-0.312918425234057,
135.714547852876));
#63294=CARTESIAN_POINT('Ctrl Pts',(34.8371811096002,-0.176138827954184,
135.721363754211));
#63295=CARTESIAN_POINT('Ctrl Pts',(34.8294163566532,-0.0391699265099815,
135.722454636529));
#63296=CARTESIAN_POINT('Ctrl Pts',(34.8216593157682,0.0976629354903832,
135.723544435367));
#63297=CARTESIAN_POINT('Ctrl Pts',(34.8139022748831,0.234684339064692,135.718920527829));
#63298=CARTESIAN_POINT('Ctrl Pts',(34.8061452339981,0.371379746995001,135.708569029331));
#63299=CARTESIAN_POINT('Ctrl Pts',(34.798394042758,0.507972071854669,135.698225336977));
#63300=CARTESIAN_POINT('Ctrl Pts',(34.7906428515179,0.64423850212011,135.682162680213));
#63301=CARTESIAN_POINT('Ctrl Pts',(34.7828916602778,0.779665125519412,135.660419241033));
#63302=CARTESIAN_POINT('Ctrl Pts',(34.7751437635007,0.91503418899133,135.638685043395));
#63303=CARTESIAN_POINT('Ctrl Pts',(34.7673958667237,1.04956377031092,135.611274927415));
#63304=CARTESIAN_POINT('Ctrl Pts',(34.7596479699466,1.18274592213557,135.57827883494));
#63305=CARTESIAN_POINT('Ctrl Pts',(34.7519016938625,1.31590021512531,135.545289644535));
#63306=CARTESIAN_POINT('Ctrl Pts',(34.7441554177784,1.44770725999012,135.506716895738));
#63307=CARTESIAN_POINT('Ctrl Pts',(34.7364091416943,1.5776705257821,135.46270139241));
#63308=CARTESIAN_POINT('Ctrl Pts',(34.7286628084289,1.7076347509332,135.418685564171));
#63309=CARTESIAN_POINT('Ctrl Pts',(34.7209164751636,1.83575479954868,135.369227026644));
#63310=CARTESIAN_POINT('Ctrl Pts',(34.7131701418982,1.96155087854192,135.314515960056));
#63311=CARTESIAN_POINT('Ctrl Pts',(34.7054220738953,2.08737512869485,135.259792641304));
#63312=CARTESIAN_POINT('Ctrl Pts',(34.6976740058923,2.21087401516037,135.199814608753));
#63313=CARTESIAN_POINT('Ctrl Pts',(34.6899259378893,2.33158961113015,135.134819363215));
#63314=CARTESIAN_POINT('Ctrl Pts',(34.6821696351475,2.45243350507186,135.069755039957));
#63315=CARTESIAN_POINT('Ctrl Pts',(34.6744133324057,2.57048785457699,134.999663037401));
#63316=CARTESIAN_POINT('Ctrl Pts',(34.6666570296638,2.68532067699727,134.924826116049));
#63317=CARTESIAN_POINT('Ctrl Pts',(34.6588965871496,2.80021478915258,134.849949251979));
#63318=CARTESIAN_POINT('Ctrl Pts',(34.6511361446354,2.911883629951,134.770322649755));
#63319=CARTESIAN_POINT('Ctrl Pts',(34.6433757021212,3.01992674397284,134.686270653043));
#63320=CARTESIAN_POINT('Ctrl Pts',(34.6356028018558,3.12814329839277,134.602083728605));
#63321=CARTESIAN_POINT('Ctrl Pts',(34.6278299015904,3.232722196708,134.513457466464));
#63322=CARTESIAN_POINT('Ctrl Pts',(34.620057001325,3.33329776477895,134.420755102937));
#63323=CARTESIAN_POINT('Ctrl Pts',(34.6125666655629,3.4302171576165,134.331422703826));
#63324=CARTESIAN_POINT('Ctrl Pts',(34.6050763298009,3.52341901131686,134.238305629011));
#63325=CARTESIAN_POINT('Ctrl Pts',(34.5975859940388,3.61261165885588,134.141757816702));
#63326=CARTESIAN_POINT('Ctrl Pts',(34.5898116599197,3.70518607273547,134.041549364744));
#63327=CARTESIAN_POINT('Ctrl Pts',(34.5820373258007,3.7937345088545,133.937327456715));
#63328=CARTESIAN_POINT('Ctrl Pts',(34.5742629916816,3.87788887704562,133.829449198052));
#63329=CARTESIAN_POINT('Ctrl Pts',(34.5664982387345,3.96193953249892,133.721703889702));
#63330=CARTESIAN_POINT('Ctrl Pts',(34.5587334857874,4.04160665668523,133.61031150187));
#63331=CARTESIAN_POINT('Ctrl Pts',(34.5509687328403,4.11655948375679,133.495665334463));
#63332=CARTESIAN_POINT('Ctrl Pts',(34.5432116919553,4.19143786662386,133.381133035246));
#63333=CARTESIAN_POINT('Ctrl Pts',(34.5354546510703,4.2616110578223,133.263353712802));
#63334=CARTESIAN_POINT('Ctrl Pts',(34.5276976101853,4.32678925592282,133.142752756907));
#63335=CARTESIAN_POINT('Ctrl Pts',(34.5199464189452,4.39191830263723,133.022242747131));
#63336=CARTESIAN_POINT('Ctrl Pts',(34.512195227705,4.45205966863424,132.898915681749));
#63337=CARTESIAN_POINT('Ctrl Pts',(34.5044440364649,4.50696769537298,132.773224568012));
#63338=CARTESIAN_POINT('Ctrl Pts',(34.4966961396878,4.56185238473563,132.647586876351));
#63339=CARTESIAN_POINT('Ctrl Pts',(34.4889482429108,4.61150800263786,132.519587492294));
#63340=CARTESIAN_POINT('Ctrl Pts',(34.4812003461337,4.6557356617563,132.389702382092));
#63341=CARTESIAN_POINT('Ctrl Pts',(34.4734540700496,4.69995406940184,132.259844441055));
#63342=CARTESIAN_POINT('Ctrl Pts',(34.4657077939654,4.73874665071692,132.128101928324));
#63343=CARTESIAN_POINT('Ctrl Pts',(34.4579615178813,4.77196348087364,131.994968697376));
#63344=CARTESIAN_POINT('Ctrl Pts',(34.450215184616,4.80518055622947,131.861834483668));
#63345=CARTESIAN_POINT('Ctrl Pts',(34.4424688513506,4.83282170365258,131.727309910595));
#63346=CARTESIAN_POINT('Ctrl Pts',(34.4347225180853,4.85478758726982,131.591901438724));
#63347=CARTESIAN_POINT('Ctrl Pts',(34.4269744500823,4.87675838999441,131.456462643066));
#63348=CARTESIAN_POINT('Ctrl Pts',(34.4192263820794,4.89305133730586,131.320139940574));
#63349=CARTESIAN_POINT('Ctrl Pts',(34.4114783140764,4.90361872473794,131.183446973031));
#63350=CARTESIAN_POINT('Ctrl Pts',(34.4037220113346,4.91419734331514,131.046608726575));
#63351=CARTESIAN_POINT('Ctrl Pts',(34.3959657085927,4.91903821600145,130.90939981939));
#63352=CARTESIAN_POINT('Ctrl Pts',(34.3882094058508,4.91814574004211,130.772336529669));
#63353=CARTESIAN_POINT('Ctrl Pts',(34.3804489633367,4.91725278774148,130.635200085143));
#63354=CARTESIAN_POINT('Ctrl Pts',(34.3726885208225,4.91062040826214,130.498209803263));
#63355=CARTESIAN_POINT('Ctrl Pts',(34.3649280783083,4.89830502518097,130.36187791419));
#63356=CARTESIAN_POINT('Ctrl Pts',(34.3571551780429,4.88596987235357,130.225327173065));
#63357=CARTESIAN_POINT('Ctrl Pts',(34.3493822777775,4.86793353700968,130.089437324581));
#63358=CARTESIAN_POINT('Ctrl Pts',(34.341609377512,4.84430396434359,129.954712358847));
#63359=CARTESIAN_POINT('Ctrl Pts',(34.33411904175,4.82153338616318,129.824884984968));
#63360=CARTESIAN_POINT('Ctrl Pts',(34.3266287059879,4.79356923241567,129.696139572388));
#63361=CARTESIAN_POINT('Ctrl Pts',(34.3191383702259,4.7605516281902,129.568912821083));
#63362=CARTESIAN_POINT('Ctrl Pts',(34.3113640361068,4.72628215146513,129.436862228832));
#63363=CARTESIAN_POINT('Ctrl Pts',(34.3035897019877,4.68645990116027,129.306029434651));
#63364=CARTESIAN_POINT('Ctrl Pts',(34.2958153678686,4.64118635846841,129.176917147437));
#63365=CARTESIAN_POINT('Ctrl Pts',(34.2880506149216,4.5959686113717,129.047963979577));
#63366=CARTESIAN_POINT('Ctrl Pts',(34.2802858619744,4.54531306729262,128.920727465175));
#63367=CARTESIAN_POINT('Ctrl Pts',(34.2725211090273,4.48937183356195,128.795698475114));
#63368=CARTESIAN_POINT('Ctrl Pts',(34.2647640681423,4.43348616145325,128.670793665608));
#63369=CARTESIAN_POINT('Ctrl Pts',(34.2570070272574,4.37232540571543,128.548092371744));
#63370=CARTESIAN_POINT('Ctrl Pts',(34.2492499863724,4.30609081406378,128.428068345236));
#63371=CARTESIAN_POINT('Ctrl Pts',(34.2414987951323,4.23990617043293,128.30813482978));
#63372=CARTESIAN_POINT('Ctrl Pts',(34.2337476038921,4.16865549487908,128.190874904005));
#63373=CARTESIAN_POINT('Ctrl Pts',(34.225996412652,4.09258713079035,128.076740108883));
#63374=CARTESIAN_POINT('Ctrl Pts',(34.2182485158749,4.01655109778554,127.962653824093));
#63375=CARTESIAN_POINT('Ctrl Pts',(34.2105006190979,3.93570166523003,127.851690352791));
#63376=CARTESIAN_POINT('Ctrl Pts',(34.2027527223208,3.85033177355368,127.744274295897));
#63377=CARTESIAN_POINT('Ctrl Pts',(34.1950064462367,3.7649797394183,127.636880708128));
#63378=CARTESIAN_POINT('Ctrl Pts',(34.1872601701526,3.67510937007827,127.533033364684));
#63379=CARTESIAN_POINT('Ctrl Pts',(34.1795138940685,3.58105512041832,127.433125341436));
#63380=CARTESIAN_POINT('Ctrl Pts',(34.1717675608031,3.48700017647126,127.333216580689));
#63381=CARTESIAN_POINT('Ctrl Pts',(34.1640212275378,3.38876155856534,127.237247482833));
#63382=CARTESIAN_POINT('Ctrl Pts',(34.1562748942724,3.28671167285548,127.145575376258));
#63383=CARTESIAN_POINT('Ctrl Pts',(34.1485268262695,3.18463893378127,127.05388274035));
#63384=CARTESIAN_POINT('Ctrl Pts',(34.1407787582665,3.07875351931422,126.966489271772));
#63385=CARTESIAN_POINT('Ctrl Pts',(34.1330306902635,2.96946178540415,126.883712741574));
#63386=CARTESIAN_POINT('Ctrl Pts',(34.1252743875216,2.8600538949387,126.800848235493));
#63387=CARTESIAN_POINT('Ctrl Pts',(34.1175180847798,2.74723276529731,126.722610706354));
#63388=CARTESIAN_POINT('Ctrl Pts',(34.1097617820379,2.63143513276518,126.649275515604));
#63389=CARTESIAN_POINT('Ctrl Pts',(34.1020013395238,2.51557569554997,126.575901183654));
#63390=CARTESIAN_POINT('Ctrl Pts',(34.0942408970096,2.39673692852486,126.507434598819));
#63391=CARTESIAN_POINT('Ctrl Pts',(34.0864804544955,2.27538028375261,126.444105163259));
#63392=CARTESIAN_POINT('Ctrl Pts',(34.07870755423,2.15382882652046,126.380674065668));
#63393=CARTESIAN_POINT('Ctrl Pts',(34.0709346539645,2.02975176857446,126.322396763008));
#63394=CARTESIAN_POINT('Ctrl Pts',(34.0631617536991,1.90363147808261,126.269454856897));
#63395=CARTESIAN_POINT('Ctrl Pts',(34.055671417937,1.78209597782729,126.218437522425));
#63396=CARTESIAN_POINT('Ctrl Pts',(34.048181082175,1.65866350780082,126.172374516677));
#63397=CARTESIAN_POINT('Ctrl Pts',(34.0406907464129,1.53377721709419,126.131383995452));
#63398=CARTESIAN_POINT('Ctrl Pts',(34.0329164122938,1.40415582471778,126.088839306156));
#63399=CARTESIAN_POINT('Ctrl Pts',(34.0251420781747,1.27255759059411,126.051624572139));
#63400=CARTESIAN_POINT('Ctrl Pts',(34.0173677440556,1.13946031101753,126.019926140837));
#63401=CARTESIAN_POINT('Ctrl Pts',(34.0096029911085,1.00652706194278,125.988266775018));
#63402=CARTESIAN_POINT('Ctrl Pts',(34.0018382381615,0.872098819945926,125.962110274932));
#63403=CARTESIAN_POINT('Ctrl Pts',(33.9940734852144,0.736670786330147,125.941593996077));
#63404=CARTESIAN_POINT('Ctrl Pts',(33.9863164443294,0.601377261746741,125.921098094279));
#63405=CARTESIAN_POINT('Ctrl Pts',(33.9785594034443,0.465086305726717,125.906231323765));
#63406=CARTESIAN_POINT('Ctrl Pts',(33.9708023625593,0.328305278311106,125.897080443505));
#63407=CARTESIAN_POINT('Ctrl Pts',(33.9630511713192,0.191627398532086,125.887936463995));
#63408=CARTESIAN_POINT('Ctrl Pts',(33.9552999800791,0.0544605714722569,
125.884499821148));
#63409=CARTESIAN_POINT('Ctrl Pts',(33.947548788839,-0.0826810729926777,
125.886805645563));
#63410=CARTESIAN_POINT('Ctrl Pts',(33.9398008920619,-0.219764428600342,
125.889110489941));
#63411=CARTESIAN_POINT('Ctrl Pts',(33.9320529952848,-0.356822232809559,
125.897152940653));
#63412=CARTESIAN_POINT('Ctrl Pts',(33.9243050985077,-0.493338915381331,
125.910916045787));
#63413=CARTESIAN_POINT('Ctrl Pts',(33.9165588224236,-0.629827041606068,
125.924676271977));
#63414=CARTESIAN_POINT('Ctrl Pts',(33.9088125463395,-0.76577388258952,125.94415473322));
#63415=CARTESIAN_POINT('Ctrl Pts',(33.9010662702554,-0.900667951434378,
125.969282510259));
#63416=CARTESIAN_POINT('Ctrl Pts',(33.8933199369901,-1.03556301603643,125.994410472786));
#63417=CARTESIAN_POINT('Ctrl Pts',(33.8855736037247,-1.16940490863912,126.025187762725));
#63418=CARTESIAN_POINT('Ctrl Pts',(33.8778272704594,-1.30169170412281,126.061494208956));
#63419=CARTESIAN_POINT('Ctrl Pts',(33.8700792024564,-1.43400812431731,126.097808785765));
#63420=CARTESIAN_POINT('Ctrl Pts',(33.8623311344534,-1.56476837745789,126.139654879316));
#63421=CARTESIAN_POINT('Ctrl Pts',(33.8545830664505,-1.69348546844494,126.186862373856));
#63422=CARTESIAN_POINT('Ctrl Pts',(33.8468267637086,-1.82233936148805,126.234120041083));
#63423=CARTESIAN_POINT('Ctrl Pts',(33.8390704609667,-1.94914538693545,126.286750357153));
#63424=CARTESIAN_POINT('Ctrl Pts',(33.8313141582249,-2.07343580877234,126.344534723049));
#63425=CARTESIAN_POINT('Ctrl Pts',(33.8235537157107,-2.19779256814968,126.402349930202));
#63426=CARTESIAN_POINT('Ctrl Pts',(33.8157932731965,-2.31963070142117,126.465324489097));
#63427=CARTESIAN_POINT('Ctrl Pts',(33.8080328306824,-2.43850777994066,126.533194164515));
#63428=CARTESIAN_POINT('Ctrl Pts',(33.8002599304169,-2.55757569050001,126.601172790361));
#63429=CARTESIAN_POINT('Ctrl Pts',(33.7924870301515,-2.673672716297,126.674062027667));
#63430=CARTESIAN_POINT('Ctrl Pts',(33.7847141298861,-2.78638533897131,126.751554206538));
#63431=CARTESIAN_POINT('Ctrl Pts',(33.7772237941241,-2.89500057390483,126.826229349517));
#63432=CARTESIAN_POINT('Ctrl Pts',(33.7697334583621,-3.00047295026603,126.905178402581));
#63433=CARTESIAN_POINT('Ctrl Pts',(33.7622431226001,-3.10246352732764,126.988092397943));
#63434=CARTESIAN_POINT('Ctrl Pts',(33.7545737356394,-3.20689211727199,127.072988393945));
#63435=CARTESIAN_POINT('Ctrl Pts',(33.7469043486787,-3.30802008847212,127.162325913931));
#63436=CARTESIAN_POINT('Ctrl Pts',(33.739234961718,-3.40543838223453,127.255815494941));
#63437=CARTESIAN_POINT('Ctrl Pts',(33.7315743594801,-3.50274509045334,127.349197990462));
#63438=CARTESIAN_POINT('Ctrl Pts',(33.7239137572423,-3.59635028099301,127.446722817711));
#63439=CARTESIAN_POINT('Ctrl Pts',(33.7162531550044,-3.68587607219211,127.548058935759));
#63440=CARTESIAN_POINT('Ctrl Pts',(33.708599562025,-3.77531994954259,127.649302333805));
#63441=CARTESIAN_POINT('Ctrl Pts',(33.7009459690456,-3.8606915845894,127.754349789671));
#63442=CARTESIAN_POINT('Ctrl Pts',(33.6932923760662,-3.94164865608082,127.862832284451));
#63443=CARTESIAN_POINT('Ctrl Pts',(33.6856440233496,-4.02255029787662,127.971240503427));
#63444=CARTESIAN_POINT('Ctrl Pts',(33.6779956706331,-4.09904314811599,128.083078762522));
#63445=CARTESIAN_POINT('Ctrl Pts',(33.6703473179165,-4.17082440111321,128.197944135578));
#63446=CARTESIAN_POINT('Ctrl Pts',(33.6627016087951,-4.24258084346383,128.312769806288));
#63447=CARTESIAN_POINT('Ctrl Pts',(33.6550558996738,-4.30962871074624,128.430620171986));
#63448=CARTESIAN_POINT('Ctrl Pts',(33.6474101905524,-4.37170810607383,128.551062746048));
#63449=CARTESIAN_POINT('Ctrl Pts',(33.639766171144,-4.4337737817638,128.671478702124));
#63450=CARTESIAN_POINT('Ctrl Pts',(33.6321221517355,-4.49087298879841,128.794485367841));
#63451=CARTESIAN_POINT('Ctrl Pts',(33.6244781323271,-4.54279179119425,128.919625674833));
#63452=CARTESIAN_POINT('Ctrl Pts',(33.6168317504326,-4.59472663978789,129.044804658105));
#63453=CARTESIAN_POINT('Ctrl Pts',(33.6091853685381,-4.64147772989695,129.172118228636));
#63454=CARTESIAN_POINT('Ctrl Pts',(33.6015389866436,-4.68287933659217,129.301089457257));
#63455=CARTESIAN_POINT('Ctrl Pts',(33.5960252581668,-4.71273361551444,129.394089302903));
#63456=CARTESIAN_POINT('Ctrl Pts',(33.5905115296898,-4.73980732912571,129.487950657987));
#63457=CARTESIAN_POINT('Ctrl Pts',(33.5849978012129,-4.7640545282341,129.582490119308));
#63458=CARTESIAN_POINT('Ctrl Pts',(35.3346663362986,-4.76405452823404,129.582490119308));
#63459=CARTESIAN_POINT('Ctrl Pts',(35.3268190006772,-4.79857048949325,129.717067328405));
#63460=CARTESIAN_POINT('Ctrl Pts',(35.3189716650557,-4.82740159557297,129.853192944721));
#63461=CARTESIAN_POINT('Ctrl Pts',(35.3111243294342,-4.85042023697192,129.990354114353));
#63462=CARTESIAN_POINT('Ctrl Pts',(35.3032799627014,-4.87343016971004,130.127463391691));
#63463=CARTESIAN_POINT('Ctrl Pts',(35.2954355959687,-4.89063195106467,130.265607071631));
#63464=CARTESIAN_POINT('Ctrl Pts',(35.2875912292359,-4.90194899773832,130.404261772189));
#63465=CARTESIAN_POINT('Ctrl Pts',(35.280013964821,-4.91288069662027,130.53819525137));
#63466=CARTESIAN_POINT('Ctrl Pts',(35.2724367004061,-4.91832182157851,130.672605181811));
#63467=CARTESIAN_POINT('Ctrl Pts',(35.2648594359912,-4.91824928377735,130.807014882743));
#63468=CARTESIAN_POINT('',(35.6101405640464,-4.91824810389018,130.800041927872));
#63469=CARTESIAN_POINT('Ctrl Pts',(35.6799972093173,-4.76405452823406,129.582490119308));
#63470=CARTESIAN_POINT('Ctrl Pts',(35.6704631326066,-4.80564392796807,129.744646557664));
#63471=CARTESIAN_POINT('Ctrl Pts',(35.6609290558958,-4.83898524524807,129.909064387513));
#63472=CARTESIAN_POINT('Ctrl Pts',(35.6513949791851,-4.86386696777967,130.074990216301));
#63473=CARTESIAN_POINT('Ctrl Pts',(35.641986490425,-4.88842093497294,130.238730381452));
#63474=CARTESIAN_POINT('Ctrl Pts',(35.6325780016649,-4.90473667682801,130.403939105789));
#63475=CARTESIAN_POINT('Ctrl Pts',(35.6231695129047,-4.91265689632296,130.5698712116));
#63476=CARTESIAN_POINT('Ctrl Pts',(35.618826529952,-4.9163128903009,130.646465904459));
#63477=CARTESIAN_POINT('Ctrl Pts',(35.6144835469992,-4.91818064204093,130.723214432572));
#63478=CARTESIAN_POINT('Ctrl Pts',(35.6101405640464,-4.91824810389018,130.800041927872));
#63479=CARTESIAN_POINT('Ctrl Pts',(35.6101405640087,-4.91824810389076,130.800041928539));
#63480=CARTESIAN_POINT('Ctrl Pts',(35.60244394154,-4.91836765957639,130.936195404843));
#63481=CARTESIAN_POINT('Ctrl Pts',(35.5947473190712,-4.91282919250016,131.072456023416));
#63482=CARTESIAN_POINT('Ctrl Pts',(35.5870506966025,-4.90163285999156,131.208314041058));
#63483=CARTESIAN_POINT('Ctrl Pts',(35.5793566006028,-4.8904402027558,131.344127462376));
#63484=CARTESIAN_POINT('Ctrl Pts',(35.5716625046031,-4.8735934032755,131.479538150618));
#63485=CARTESIAN_POINT('Ctrl Pts',(35.5639684086034,-4.85114468232059,131.614038537293));
#63486=CARTESIAN_POINT('Ctrl Pts',(35.5562753587172,-4.82869901356424,131.748520636873));
#63487=CARTESIAN_POINT('Ctrl Pts',(35.5485823088309,-4.80065300315192,131.882092289763));
#63488=CARTESIAN_POINT('Ctrl Pts',(35.5408892589447,-4.76711041607429,132.014253729976));
#63489=CARTESIAN_POINT('Ctrl Pts',(35.5331955327345,-4.733564880146,132.146426788981));
#63490=CARTESIAN_POINT('Ctrl Pts',(35.5255018065243,-4.69452190390324,132.277189004101));
#63491=CARTESIAN_POINT('Ctrl Pts',(35.517808080314,-4.65013566353249,132.406053900702));
#63492=CARTESIAN_POINT('Ctrl Pts',(35.5101119551761,-4.60573558339437,132.534958977778));
#63493=CARTESIAN_POINT('Ctrl Pts',(35.5024158300383,-4.55598905413414,132.661965184604));
#63494=CARTESIAN_POINT('Ctrl Pts',(35.4947197049004,-4.5010989311345,132.786604667788));
#63495=CARTESIAN_POINT('Ctrl Pts',(35.4870150064303,-4.44614766161606,132.911382996907));
#63496=CARTESIAN_POINT('Ctrl Pts',(35.4793103079601,-4.38604151849413,133.033788975197));
#63497=CARTESIAN_POINT('Ctrl Pts',(35.47160560949,-4.32103017225646,133.15337771264));
#63498=CARTESIAN_POINT('Ctrl Pts',(35.4638960953197,-4.25597819170293,133.273041197136));
#63499=CARTESIAN_POINT('Ctrl Pts',(35.4561865811494,-4.18601510605575,133.389883594735));
#63500=CARTESIAN_POINT('Ctrl Pts',(35.4484770669791,-4.11143407551822,133.503488792582));
#63501=CARTESIAN_POINT('Ctrl Pts',(35.4407559761704,-4.03674105379598,133.617264580466));
#63502=CARTESIAN_POINT('Ctrl Pts',(35.4330348853616,-3.9574164727118,133.727793141836));
#63503=CARTESIAN_POINT('Ctrl Pts',(35.4253137945529,-3.87379422963091,133.834690851877));
#63504=CARTESIAN_POINT('Ctrl Pts',(35.4213224861412,-3.83056689679963,133.889950107316));
#63505=CARTESIAN_POINT('Ctrl Pts',(35.4173311777296,-3.78619174998896,133.944239705668));
#63506=CARTESIAN_POINT('Ctrl Pts',(35.413339869318,-3.74071865843683,133.997510626714));
#63507=CARTESIAN_POINT('Ctrl Pts',(35.4055655351989,-3.6521454461734,134.101272575511));
#63508=CARTESIAN_POINT('Ctrl Pts',(35.3977912010798,-3.55911136619014,134.201510749947));
#63509=CARTESIAN_POINT('Ctrl Pts',(35.3900168669607,-3.46192754976004,134.297817458964));
#63510=CARTESIAN_POINT('Ctrl Pts',(35.3822521140136,-3.36486350369824,134.39400547857));
#63511=CARTESIAN_POINT('Ctrl Pts',(35.3744873610665,-3.26366017192064,134.486271400666));
#63512=CARTESIAN_POINT('Ctrl Pts',(35.3667226081194,-3.15866903516011,134.574240322387));
#63513=CARTESIAN_POINT('Ctrl Pts',(35.3589655672344,-3.05378217707659,134.662121872135));
#63514=CARTESIAN_POINT('Ctrl Pts',(35.3512085263495,-2.94511529850038,134.745714665239));
#63515=CARTESIAN_POINT('Ctrl Pts',(35.3434514854645,-2.83305658368171,134.824680686436));
#63516=CARTESIAN_POINT('Ctrl Pts',(35.3357002942244,-2.72108237321172,134.903587158742));
#63517=CARTESIAN_POINT('Ctrl Pts',(35.3279491029842,-2.60572173595831,134.977873579655));
#63518=CARTESIAN_POINT('Ctrl Pts',(35.3201979117441,-2.48739549400316,135.047242505966));
#63519=CARTESIAN_POINT('Ctrl Pts',(35.312450014967,-2.36911954385729,135.116581948633));
#63520=CARTESIAN_POINT('Ctrl Pts',(35.30470211819,-2.24788083254293,135.181007856363));
#63521=CARTESIAN_POINT('Ctrl Pts',(35.2969542214129,-2.12412850453284,135.240266518138));
#63522=CARTESIAN_POINT('Ctrl Pts',(35.2892079453288,-2.0004020628418,135.299512784279));
#63523=CARTESIAN_POINT('Ctrl Pts',(35.2814616692447,-1.87416340268791,135.353593785641));
#63524=CARTESIAN_POINT('Ctrl Pts',(35.2737153931606,-1.7458852134702,135.402302318358));
#63525=CARTESIAN_POINT('Ctrl Pts',(35.2659690598952,-1.61760607733222,135.451011210631));
#63526=CARTESIAN_POINT('Ctrl Pts',(35.2582227266299,-1.48728774759163,135.494347416339));
#63527=CARTESIAN_POINT('Ctrl Pts',(35.2504763933645,-1.35542140749701,135.532152477473));
#63528=CARTESIAN_POINT('Ctrl Pts',(35.2427283253615,-1.22352553684964,135.569966004788));
#63529=CARTESIAN_POINT('Ctrl Pts',(35.2349802573585,-1.09008134177591,135.602245815011));
#63530=CARTESIAN_POINT('Ctrl Pts',(35.2272321893556,-0.955593234594663,
135.628883871992));
#63531=CARTESIAN_POINT('Ctrl Pts',(35.2194758866137,-0.820962191852861,
135.655550240217));
#63532=CARTESIAN_POINT('Ctrl Pts',(35.2117195838719,-0.685285404819466,
135.676562801214));
#63533=CARTESIAN_POINT('Ctrl Pts',(35.20396328113,-0.549076057439199,135.691864944485));
#63534=CARTESIAN_POINT('Ctrl Pts',(35.1962028386159,-0.412794011028866,
135.70717525497));
#63535=CARTESIAN_POINT('Ctrl Pts',(35.1884423961017,-0.275979227709126,
135.71676904735));
#63536=CARTESIAN_POINT('Ctrl Pts',(35.1806819535875,-0.139147016488932,
135.720641851416));
#63537=CARTESIAN_POINT('Ctrl Pts',(35.1729090533221,-0.002095150055894,
135.72452087245));
#63538=CARTESIAN_POINT('Ctrl Pts',(35.1651361530567,0.134973809029991,135.722660558244));
#63539=CARTESIAN_POINT('Ctrl Pts',(35.1573632527912,0.271546648981629,135.715108572809));
#63540=CARTESIAN_POINT('Ctrl Pts',(35.1498729170292,0.403154722194802,135.707831121068));
#63541=CARTESIAN_POINT('Ctrl Pts',(35.1423825812672,0.534301813784657,135.695268656236));
#63542=CARTESIAN_POINT('Ctrl Pts',(35.1348922455051,0.66453773038607,135.677508744536));
#63543=CARTESIAN_POINT('Ctrl Pts',(35.1271179113861,0.799711581349775,135.659075460387));
#63544=CARTESIAN_POINT('Ctrl Pts',(35.119343577267,0.934331989109421,135.634984435771));
#63545=CARTESIAN_POINT('Ctrl Pts',(35.1115692431479,1.06788777758088,135.605277067265));
#63546=CARTESIAN_POINT('Ctrl Pts',(35.1038044902008,1.20127897047926,135.575606310437));
#63547=CARTESIAN_POINT('Ctrl Pts',(35.0960397372537,1.33360777669981,135.540333065798));
#63548=CARTESIAN_POINT('Ctrl Pts',(35.0882749843066,1.46436879592354,135.499550399888));
#63549=CARTESIAN_POINT('Ctrl Pts',(35.0805179434216,1.59499994145957,135.458808239898));
#63550=CARTESIAN_POINT('Ctrl Pts',(35.0727609025366,1.72406602797549,135.412567663886));
#63551=CARTESIAN_POINT('Ctrl Pts',(35.0650038616516,1.85107285058801,135.36097255675));
#63552=CARTESIAN_POINT('Ctrl Pts',(35.0572526704115,1.97798389636694,135.309416357887));
#63553=CARTESIAN_POINT('Ctrl Pts',(35.0495014791713,2.10283840845757,135.252513811633));
#63554=CARTESIAN_POINT('Ctrl Pts',(35.0417502879313,2.22515867484831,135.190458192204));
#63555=CARTESIAN_POINT('Ctrl Pts',(35.0340023911542,2.34742695186333,135.128428948069));
#63556=CARTESIAN_POINT('Ctrl Pts',(35.0262544943771,2.46716277755906,135.0612511634));
#63557=CARTESIAN_POINT('Ctrl Pts',(35.0185065976001,2.58390992411118,134.98916557916));
#63558=CARTESIAN_POINT('Ctrl Pts',(35.010760321516,2.70063264967702,134.91709507367));
#63559=CARTESIAN_POINT('Ctrl Pts',(35.0030140454319,2.81436760714029,134.840119015856));
#63560=CARTESIAN_POINT('Ctrl Pts',(34.9952677693478,2.92468496985382,134.758523093946));
#63561=CARTESIAN_POINT('Ctrl Pts',(34.9875214360825,3.03500314690477,134.676926569714));
#63562=CARTESIAN_POINT('Ctrl Pts',(34.9797751028171,3.14190336453829,134.590710345827));
#63563=CARTESIAN_POINT('Ctrl Pts',(34.9720287695517,3.24498681100062,134.500202018239));
#63564=CARTESIAN_POINT('Ctrl Pts',(34.9642807015488,3.3480933422862,134.40967342194));
#63565=CARTESIAN_POINT('Ctrl Pts',(34.9565326335458,3.4473811078317,134.314851067192));
#63566=CARTESIAN_POINT('Ctrl Pts',(34.9487845655429,3.54248656658443,134.216100934189));
#63567=CARTESIAN_POINT('Ctrl Pts',(34.941028262801,3.63769310455074,134.117245848368));
#63568=CARTESIAN_POINT('Ctrl Pts',(34.9332719600592,3.72870818470604,134.01445492735));
#63569=CARTESIAN_POINT('Ctrl Pts',(34.9255156573173,3.81520679057626,133.908129327963));
#63570=CARTESIAN_POINT('Ctrl Pts',(34.9177552148031,3.90175156335674,133.801746979403));
#63571=CARTESIAN_POINT('Ctrl Pts',(34.9099947722889,3.98377482486769,133.691826506523));
#63572=CARTESIAN_POINT('Ctrl Pts',(34.9022343297748,4.06099427708879,133.57879903713));
#63573=CARTESIAN_POINT('Ctrl Pts',(34.8944614295094,4.13833768882981,133.465590126009));
#63574=CARTESIAN_POINT('Ctrl Pts',(34.886688529244,4.21086167428251,133.349264583466));
#63575=CARTESIAN_POINT('Ctrl Pts',(34.8789156289786,4.27832893102401,133.230279952676));
#63576=CARTESIAN_POINT('Ctrl Pts',(34.8714252932165,4.34334358304393,133.115620712919));
#63577=CARTESIAN_POINT('Ctrl Pts',(34.8639349574543,4.40366263204399,132.998492631387));
#63578=CARTESIAN_POINT('Ctrl Pts',(34.8564446216922,4.45911640945718,132.879321800193));
#63579=CARTESIAN_POINT('Ctrl Pts',(34.8486702875731,4.51667273369515,132.755632570714));
#63580=CARTESIAN_POINT('Ctrl Pts',(34.8408959534541,4.56916989107253,132.629350821757));
#63581=CARTESIAN_POINT('Ctrl Pts',(34.833121619335,4.61636640654297,132.5009289961));
#63582=CARTESIAN_POINT('Ctrl Pts',(34.8253568663879,4.66350475652624,132.372665438865));
#63583=CARTESIAN_POINT('Ctrl Pts',(34.8175921134408,4.70535532889446,132.242267416121));
#63584=CARTESIAN_POINT('Ctrl Pts',(34.8098273604937,4.74172324194553,132.110210440208));
#63585=CARTESIAN_POINT('Ctrl Pts',(34.8020703196087,4.77805503387275,131.978284625144));
#63586=CARTESIAN_POINT('Ctrl Pts',(34.7943132787236,4.80891490004916,131.844703510393));
#63587=CARTESIAN_POINT('Ctrl Pts',(34.7865562378386,4.83415676510285,131.709960657821));
#63588=CARTESIAN_POINT('Ctrl Pts',(34.7788050465985,4.85937959506961,131.575319415884));
#63589=CARTESIAN_POINT('Ctrl Pts',(34.7710538553584,4.87899278486863,131.439518562626));
#63590=CARTESIAN_POINT('Ctrl Pts',(34.7633026641183,4.89290072655954,131.303064480127));
#63591=CARTESIAN_POINT('Ctrl Pts',(34.7555547673412,4.90680275700424,131.166668394253));
#63592=CARTESIAN_POINT('Ctrl Pts',(34.7478068705642,4.91500432268716,131.029620019478));
#63593=CARTESIAN_POINT('Ctrl Pts',(34.7400589737871,4.91746136351502,130.892433319563));
#63594=CARTESIAN_POINT('Ctrl Pts',(34.732312697703,4.9199178903829,130.755275316148));
#63595=CARTESIAN_POINT('Ctrl Pts',(34.7245664216189,4.91663227550848,130.6179794358));
#63596=CARTESIAN_POINT('Ctrl Pts',(34.7168201455348,4.90761254468703,130.481061725315));
#63597=CARTESIAN_POINT('Ctrl Pts',(34.7090738122694,4.89859274728394,130.344143004135));
#63598=CARTESIAN_POINT('Ctrl Pts',(34.7013274790041,4.88383877517136,130.207602848509));
#63599=CARTESIAN_POINT('Ctrl Pts',(34.6935811457387,4.86341067660904,130.071953863675));
#63600=CARTESIAN_POINT('Ctrl Pts',(34.6858330777357,4.84297800331568,129.936274501191));
#63601=CARTESIAN_POINT('Ctrl Pts',(34.6780850097328,4.81686873327383,129.801487093156));
#63602=CARTESIAN_POINT('Ctrl Pts',(34.6703369417298,4.78519427316441,129.668095318186));
#63603=CARTESIAN_POINT('Ctrl Pts',(34.6625806389879,4.75348614906189,129.534561772851));
#63604=CARTESIAN_POINT('Ctrl Pts',(34.6548243362461,4.71620111000998,129.402427204617));
#63605=CARTESIAN_POINT('Ctrl Pts',(34.6470680335042,4.67350098126703,129.272181894115));
#63606=CARTESIAN_POINT('Ctrl Pts',(34.6393075909901,4.63077806217969,129.141867067769));
#63607=CARTESIAN_POINT('Ctrl Pts',(34.6315471484759,4.58263443161248,129.013443874292));
#63608=CARTESIAN_POINT('Ctrl Pts',(34.6237867059617,4.52928022062335,128.887382854114));
#63609=CARTESIAN_POINT('Ctrl Pts',(34.6160138056963,4.47584036071818,128.761119469595));
#63610=CARTESIAN_POINT('Ctrl Pts',(34.6082409054309,4.41717337290042,128.637226189494));
#63611=CARTESIAN_POINT('Ctrl Pts',(34.6004680051655,4.35353593344518,128.516149976322));
#63612=CARTESIAN_POINT('Ctrl Pts',(34.5929776694034,4.292211875207,128.399475188472));
#63613=CARTESIAN_POINT('Ctrl Pts',(34.5854873336414,4.22627262233482,128.285416475144));
#63614=CARTESIAN_POINT('Ctrl Pts',(34.5779969978794,4.15598494818403,128.174346896505));
#63615=CARTESIAN_POINT('Ctrl Pts',(34.5702226637603,4.08303229550444,128.059066081033));
#63616=CARTESIAN_POINT('Ctrl Pts',(34.5624483296412,4.00516387949855,127.94664036582));
#63617=CARTESIAN_POINT('Ctrl Pts',(34.5546739955221,3.9226298299287,127.837517467035));
#63618=CARTESIAN_POINT('Ctrl Pts',(34.546909242575,3.84019749619866,127.72852905247));
#63619=CARTESIAN_POINT('Ctrl Pts',(34.5391444896279,3.75311120322232,127.622835664225));
#63620=CARTESIAN_POINT('Ctrl Pts',(34.5313797366808,3.66166567467816,127.52085828783));
#63621=CARTESIAN_POINT('Ctrl Pts',(34.5236226957958,3.57031097112198,127.418982196803));
#63622=CARTESIAN_POINT('Ctrl Pts',(34.5158656549108,3.47460590753085,127.320815061969));
#63623=CARTESIAN_POINT('Ctrl Pts',(34.5081086140258,3.37488677417489,127.22674656292));
#63624=CARTESIAN_POINT('Ctrl Pts',(34.5003574227857,3.27524283979377,127.132749001659));
#63625=CARTESIAN_POINT('Ctrl Pts',(34.4926062315456,3.17159114403351,127.042844191301));
#63626=CARTESIAN_POINT('Ctrl Pts',(34.4848550403055,3.06430604205144,126.957386281396));
#63627=CARTESIAN_POINT('Ctrl Pts',(34.4771071435284,2.95706653909905,126.871964693383));
#63628=CARTESIAN_POINT('Ctrl Pts',(34.4693592467513,2.84619700657529,126.790986489735));
#63629=CARTESIAN_POINT('Ctrl Pts',(34.4616113499742,2.73210604119116,126.714766549423));
#63630=CARTESIAN_POINT('Ctrl Pts',(34.4538650738901,2.61803894117763,126.638562552681));
#63631=CARTESIAN_POINT('Ctrl Pts',(34.4461187978061,2.500752073524,126.567115056561));
#63632=CARTESIAN_POINT('Ctrl Pts',(34.438372521722,2.38068394115421,126.500696244636));
#63633=CARTESIAN_POINT('Ctrl Pts',(34.4306261884566,2.26061492246842,126.434276942421));
#63634=CARTESIAN_POINT('Ctrl Pts',(34.4228798551912,2.13776494020911,126.372886587719));
#63635=CARTESIAN_POINT('Ctrl Pts',(34.4151335219258,2.01259772123235,126.31675173588));
#63636=CARTESIAN_POINT('Ctrl Pts',(34.4073854539228,1.88740247192457,126.26060431303));
#63637=CARTESIAN_POINT('Ctrl Pts',(34.3996373859199,1.7598893099546,126.20971489496));
#63638=CARTESIAN_POINT('Ctrl Pts',(34.3918893179168,1.63054221243973,126.164262002671));
#63639=CARTESIAN_POINT('Ctrl Pts',(34.384133015175,1.50105764329072,126.118760802507));
#63640=CARTESIAN_POINT('Ctrl Pts',(34.3763767124331,1.36973561444498,126.078707800132));
#63641=CARTESIAN_POINT('Ctrl Pts',(34.3686204096912,1.23707608338644,126.044231856029));
#63642=CARTESIAN_POINT('Ctrl Pts',(34.3608599671771,1.10434574794187,126.009737511076));
#63643=CARTESIAN_POINT('Ctrl Pts',(34.3530995246629,0.970276869840605,125.980826237986));
#63644=CARTESIAN_POINT('Ctrl Pts',(34.3453390821487,0.835378909042103,125.957575586143));
#63645=CARTESIAN_POINT('Ctrl Pts',(34.3375661818832,0.700264398061065,125.934287610289));
#63646=CARTESIAN_POINT('Ctrl Pts',(34.3297932816179,0.564318532735446,125.91667846452));
#63647=CARTESIAN_POINT('Ctrl Pts',(34.3220203813524,0.428056095080841,125.904773793969));
#63648=CARTESIAN_POINT('Ctrl Pts',(34.3145300455905,0.296747140260636,125.893301888179));
#63649=CARTESIAN_POINT('Ctrl Pts',(34.3070397098285,0.165144537596052,125.887126928525));
#63650=CARTESIAN_POINT('Ctrl Pts',(34.2995493740665,0.0337063506838879,
125.886226119159));
#63651=CARTESIAN_POINT('Ctrl Pts',(34.2917750399474,-0.102715355035972,
125.885291155331));
#63652=CARTESIAN_POINT('Ctrl Pts',(34.2840007058283,-0.239392074199353,
125.890035213842));
#63653=CARTESIAN_POINT('Ctrl Pts',(34.2762263717092,-0.375811929267305,
125.900489854962));
#63654=CARTESIAN_POINT('Ctrl Pts',(34.2684616187622,-0.512063659055707,
125.910931611672));
#63655=CARTESIAN_POINT('Ctrl Pts',(34.2606968658152,-0.648058768532885,
125.927069918314));
#63656=CARTESIAN_POINT('Ctrl Pts',(34.2529321128681,-0.783283765302231,
125.948884368472));
#63657=CARTESIAN_POINT('Ctrl Pts',(34.2451750719831,-0.918374454698078,
125.970677152211));
#63658=CARTESIAN_POINT('Ctrl Pts',(34.2374180310982,-1.05269617006782,125.998134798475));
#63659=CARTESIAN_POINT('Ctrl Pts',(34.2296609902132,-1.18573928982888,126.031185008073));
#63660=CARTESIAN_POINT('Ctrl Pts',(34.2219097989731,-1.31868208073877,126.064210294251));
#63661=CARTESIAN_POINT('Ctrl Pts',(34.214158607733,-1.45034781732185,126.102819655417));
#63662=CARTESIAN_POINT('Ctrl Pts',(34.2064074164929,-1.58023619542438,126.146889562458));
#63663=CARTESIAN_POINT('Ctrl Pts',(34.1986595197158,-1.71006936750168,126.190940738612));
#63664=CARTESIAN_POINT('Ctrl Pts',(34.1909116229387,-1.83812631412066,126.240447719238));
#63665=CARTESIAN_POINT('Ctrl Pts',(34.1831637261616,-1.96392126218237,126.295236940126));
#63666=CARTESIAN_POINT('Ctrl Pts',(34.1754174500775,-2.08968989665294,126.35001470029));
#63667=CARTESIAN_POINT('Ctrl Pts',(34.1676711739934,-2.21319711549453,126.410072346929));
#63668=CARTESIAN_POINT('Ctrl Pts',(34.1599248979092,-2.33397690141957,126.475188076983));
#63669=CARTESIAN_POINT('Ctrl Pts',(34.1521785646439,-2.45475757891338,126.540304287706));
#63670=CARTESIAN_POINT('Ctrl Pts',(34.1444322313786,-2.57281043917829,126.610478470813));
#63671=CARTESIAN_POINT('Ctrl Pts',(34.1366858981132,-2.68769421908834,126.685442938469));
#63672=CARTESIAN_POINT('Ctrl Pts',(34.1289378301103,-2.80260372642357,126.760424193897));
#63673=CARTESIAN_POINT('Ctrl Pts',(34.1211897621073,-2.91434241383451,126.840197654912));
#63674=CARTESIAN_POINT('Ctrl Pts',(34.1134416941044,-3.0224984850947,126.924452632819));
#63675=CARTESIAN_POINT('Ctrl Pts',(34.1056853913625,-3.13076950591523,127.008797157921));
#63676=CARTESIAN_POINT('Ctrl Pts',(34.0979290886207,-3.23544999548343,127.097632473889));
#63677=CARTESIAN_POINT('Ctrl Pts',(34.0901727858788,-3.33616130059324,127.190607604572));
#63678=CARTESIAN_POINT('Ctrl Pts',(34.0824123433647,-3.43692635835894,127.283632358882));
#63679=CARTESIAN_POINT('Ctrl Pts',(34.0746519008506,-3.53371773464809,127.380801053753));
#63680=CARTESIAN_POINT('Ctrl Pts',(34.0668914583364,-3.62619480941399,127.481726983432));
#63681=CARTESIAN_POINT('Ctrl Pts',(34.059118558071,-3.71882033659002,127.582814928372));
#63682=CARTESIAN_POINT('Ctrl Pts',(34.0513456578055,-3.80711747051388,127.687671861642));
#63683=CARTESIAN_POINT('Ctrl Pts',(34.0435727575401,-3.8907863829533,127.795878544373));
#63684=CARTESIAN_POINT('Ctrl Pts',(34.0360824217779,-3.97141371967799,127.900151641632));
#63685=CARTESIAN_POINT('Ctrl Pts',(34.0285920860157,-4.04774330943377,128.007534921912));
#63686=CARTESIAN_POINT('Ctrl Pts',(34.0211017502535,-4.11954673645024,128.117630681621));
#63687=CARTESIAN_POINT('Ctrl Pts',(34.0131632968525,-4.1956458830708,128.234313042179));
#63688=CARTESIAN_POINT('Ctrl Pts',(34.0052248434515,-4.26689421093774,128.354399816872));
#63689=CARTESIAN_POINT('Ctrl Pts',(33.9972863900504,-4.33297996118468,128.477459734745));
#63690=CARTESIAN_POINT('Ctrl Pts',(33.9893578838863,-4.39898290303297,128.600365453042));
#63691=CARTESIAN_POINT('Ctrl Pts',(33.9814293777222,-4.45983596784123,128.726236578905));
#63692=CARTESIAN_POINT('Ctrl Pts',(33.9735008715581,-4.51527021446301,128.854612440779));
#63693=CARTESIAN_POINT('Ctrl Pts',(33.9655838239637,-4.57062434546535,128.982802769119));
#63694=CARTESIAN_POINT('Ctrl Pts',(33.9576667763694,-4.62057511695177,129.113490284522));
#63695=CARTESIAN_POINT('Ctrl Pts',(33.9497497287751,-4.66489946646814,129.246189885507));
#63696=CARTESIAN_POINT('Ctrl Pts',(33.9431394823856,-4.70190756423015,129.356985866944));
#63697=CARTESIAN_POINT('Ctrl Pts',(33.9365292359961,-4.73499410125762,129.469183955581));
#63698=CARTESIAN_POINT('Ctrl Pts',(33.9299189896066,-4.764054528234,129.582490119308));
#63699=CARTESIAN_POINT('Origin',(213.235140564004,0.,130.804360617566));
#63700=CARTESIAN_POINT('',(31.8348922615591,-4.76405452823409,129.582490119308));
#63701=CARTESIAN_POINT('',(32.1802676473795,-4.76405452823406,129.582490119308));
#63702=CARTESIAN_POINT('',(213.235140564004,-4.76405452823405,129.582490119308));
#63703=CARTESIAN_POINT('',(33.5148594360289,-4.9182490365939,130.807439017015));
#63704=CARTESIAN_POINT('Ctrl Pts',(33.5148594359912,-4.91824903659349,130.807439017678));
#63705=CARTESIAN_POINT('Ctrl Pts',(33.5045047902566,-4.91813509922922,130.989472642819));
#63706=CARTESIAN_POINT('Ctrl Pts',(33.4941501445219,-4.90791567783689,131.171189313812));
#63707=CARTESIAN_POINT('Ctrl Pts',(33.4837954987872,-4.88769185390603,131.351764859202));
#63708=CARTESIAN_POINT('Ctrl Pts',(33.4760211646682,-4.87250767779513,131.487342131427));
#63709=CARTESIAN_POINT('Ctrl Pts',(33.4682468305493,-4.85165410939625,131.622501889997));
#63710=CARTESIAN_POINT('Ctrl Pts',(33.4604724964303,-4.82516026654944,131.756732112631));
#63711=CARTESIAN_POINT('Ctrl Pts',(33.4527077434833,-4.79869907499611,131.890796908512));
#63712=CARTESIAN_POINT('Ctrl Pts',(33.4449429905363,-4.76661151465987,132.023934067916));
#63713=CARTESIAN_POINT('Ctrl Pts',(33.4371782375894,-4.72897849706514,132.155636102726));
#63714=CARTESIAN_POINT('Ctrl Pts',(33.4294211967045,-4.69138285711401,132.287207329219));
#63715=CARTESIAN_POINT('Ctrl Pts',(33.4216641558196,-4.64825282744883,132.417345894214));
#63716=CARTESIAN_POINT('Ctrl Pts',(33.4139071149347,-4.59972039197709,132.545554282306));
#63717=CARTESIAN_POINT('Ctrl Pts',(33.4061559236947,-4.55122455519253,132.673665987455));
#63718=CARTESIAN_POINT('Ctrl Pts',(33.3984047324547,-4.49733455949609,132.799850048742));
#63719=CARTESIAN_POINT('Ctrl Pts',(33.3906535412146,-4.43823215967319,132.923624253677));
#63720=CARTESIAN_POINT('Ctrl Pts',(33.3829056444377,-4.37915487994675,133.047345851274));
#63721=CARTESIAN_POINT('Ctrl Pts',(33.3751577476607,-4.31486977049039,133.168659277611));
#63722=CARTESIAN_POINT('Ctrl Pts',(33.3674098508837,-4.24560655472915,133.287102659128));
#63723=CARTESIAN_POINT('Ctrl Pts',(33.3596635747997,-4.17635782733951,133.405521264843));
#63724=CARTESIAN_POINT('Ctrl Pts',(33.3519172987157,-4.10213326210762,133.521070682589));
#63725=CARTESIAN_POINT('Ctrl Pts',(33.3441710226317,-4.02320815033575,133.633314353768));
#63726=CARTESIAN_POINT('Ctrl Pts',(33.3364246893665,-3.94428245595663,133.745558853504));
#63727=CARTESIAN_POINT('Ctrl Pts',(33.3286783561012,-3.86065637068076,133.854497238165));
#63728=CARTESIAN_POINT('Ctrl Pts',(33.320932022836,-3.77264782574022,133.959722949444));
#63729=CARTESIAN_POINT('Ctrl Pts',(33.3131839548331,-3.68461957189626,134.064972225292));
#63730=CARTESIAN_POINT('Ctrl Pts',(33.3054358868302,-3.59220715625296,134.166506873474));
#63731=CARTESIAN_POINT('Ctrl Pts',(33.2976878188274,-3.49576772962533,134.263954675112));
#63732=CARTESIAN_POINT('Ctrl Pts',(33.2899315160856,-3.39922580602742,134.361506045434));
#63733=CARTESIAN_POINT('Ctrl Pts',(33.2821752133439,-3.2986485972248,134.454961614173));
#63734=CARTESIAN_POINT('Ctrl Pts',(33.2744189106021,-3.19442934502391,134.543986831795));
#63735=CARTESIAN_POINT('Ctrl Pts',(33.2666584680881,-3.09015446787014,134.633059564856));
#63736=CARTESIAN_POINT('Ctrl Pts',(33.258898025574,-2.9822339814863,134.71769699396));
#63737=CARTESIAN_POINT('Ctrl Pts',(33.2511375830599,-2.87109211515023,134.797606556501));
#63738=CARTESIAN_POINT('Ctrl Pts',(33.2433646827946,-2.7597718340236,134.877644396966));
#63739=CARTESIAN_POINT('Ctrl Pts',(33.2355917825293,-2.64522016604579,134.95293898958));
#63740=CARTESIAN_POINT('Ctrl Pts',(33.227818882264,-2.52788882802643,135.023242120481));
#63741=CARTESIAN_POINT('Ctrl Pts',(33.2203285465007,-2.41482277966371,135.090989555503));
#63742=CARTESIAN_POINT('Ctrl Pts',(33.2128382107374,-2.29917591896668,135.154101985117));
#63743=CARTESIAN_POINT('Ctrl Pts',(33.2053478749742,-2.18137014376445,135.21239956458));
#63744=CARTESIAN_POINT('Ctrl Pts',(33.1975735408551,-2.05909772680879,135.272907514478));
#63745=CARTESIAN_POINT('Ctrl Pts',(33.189799206736,-1.93411213090131,135.328419967749));
#63746=CARTESIAN_POINT('Ctrl Pts',(33.1820248726169,-1.80685987379269,135.378684661507));
#63747=CARTESIAN_POINT('Ctrl Pts',(33.1742601196698,-1.67976444371827,135.428887408522));
#63748=CARTESIAN_POINT('Ctrl Pts',(33.1664953667226,-1.55040827072505,135.473855121959));
#63749=CARTESIAN_POINT('Ctrl Pts',(33.1587306137755,-1.4192620535936,135.51338156525));
#63750=CARTESIAN_POINT('Ctrl Pts',(33.1509735728905,-1.28824609273366,135.552868750321));
#63751=CARTESIAN_POINT('Ctrl Pts',(33.1432165320055,-1.15544399774161,135.586925308049));
#63752=CARTESIAN_POINT('Ctrl Pts',(33.1354594911205,-1.0213456829442,135.615393361004));
#63753=CARTESIAN_POINT('Ctrl Pts',(33.1277082998803,-0.887348492729106,
135.643839945979));
#63754=CARTESIAN_POINT('Ctrl Pts',(33.1199571086401,-0.752057409236861,
135.666706333698));
#63755=CARTESIAN_POINT('Ctrl Pts',(33.1122059174,-0.615976374393877,135.68388479198));
#63756=CARTESIAN_POINT('Ctrl Pts',(33.1044580206229,-0.479953177620966,
135.701055948959));
#63757=CARTESIAN_POINT('Ctrl Pts',(33.0967101238458,-0.343141084353969,
135.712543935904));
#63758=CARTESIAN_POINT('Ctrl Pts',(33.0889622270687,-0.206052853023449,
135.718292371697));
#63759=CARTESIAN_POINT('Ctrl Pts',(33.0812159509846,-0.0689932975954562,
135.724039605042));
#63760=CARTESIAN_POINT('Ctrl Pts',(33.0734696749004,0.0683418906295579,
135.724049658905));
#63761=CARTESIAN_POINT('Ctrl Pts',(33.0657233988163,0.205436620866316,135.718318173071));
#63762=CARTESIAN_POINT('Ctrl Pts',(33.057977065551,0.342532363105043,135.712586644929));
#63763=CARTESIAN_POINT('Ctrl Pts',(33.0502307322857,0.479387253189631,135.701113508848));
#63764=CARTESIAN_POINT('Ctrl Pts',(33.0424843990203,0.615487392506522,135.683946494684));
#63765=CARTESIAN_POINT('Ctrl Pts',(33.0347363310173,0.751618010506147,135.666775636086));
#63766=CARTESIAN_POINT('Ctrl Pts',(33.0269882630143,0.886993153588004,135.643908411011));
#63767=CARTESIAN_POINT('Ctrl Pts',(33.0192401950113,1.02110661472941,135.615444107161));
#63768=CARTESIAN_POINT('Ctrl Pts',(33.0114838922694,1.15536261325329,135.58694955111));
#63769=CARTESIAN_POINT('Ctrl Pts',(33.0037275895275,1.28835386812738,135.552846114531));
#63770=CARTESIAN_POINT('Ctrl Pts',(32.9959712867856,1.41958635655096,135.513283810696));
#63771=CARTESIAN_POINT('Ctrl Pts',(32.9882108442715,1.55088888770496,135.473700391268));
#63772=CARTESIAN_POINT('Ctrl Pts',(32.9804504017573,1.68043041286254,135.428652427418));
#63773=CARTESIAN_POINT('Ctrl Pts',(32.9726899592431,1.80773548453207,135.378338698019));
#63774=CARTESIAN_POINT('Ctrl Pts',(32.9649170589776,1.93524491760425,135.327944200555));
#63775=CARTESIAN_POINT('Ctrl Pts',(32.9571441587122,2.06051036544685,135.27226720449));
#63776=CARTESIAN_POINT('Ctrl Pts',(32.9493712584467,2.18307883474006,135.211553586317));
#63777=CARTESIAN_POINT('Ctrl Pts',(32.9418809226849,2.3011916314388,135.153047061095));
#63778=CARTESIAN_POINT('Ctrl Pts',(32.9343905869232,2.41679985892478,135.089863891726));
#63779=CARTESIAN_POINT('Ctrl Pts',(32.9269002511614,2.5295241626408,135.022261822326));
#63780=CARTESIAN_POINT('Ctrl Pts',(32.9191259170424,2.64652244259797,134.952096599915));
#63781=CARTESIAN_POINT('Ctrl Pts',(32.9113515829233,2.76078440926004,134.876948515263));
#63782=CARTESIAN_POINT('Ctrl Pts',(32.9035772488042,2.87185647296498,134.797056882146));
#63783=CARTESIAN_POINT('Ctrl Pts',(32.8958124958571,2.9827916502782,134.717263708327));
#63784=CARTESIAN_POINT('Ctrl Pts',(32.88804774291,3.09054443234698,134.63273884394));
#63785=CARTESIAN_POINT('Ctrl Pts',(32.8802829899629,3.19468688231904,134.5437668253));
#63786=CARTESIAN_POINT('Ctrl Pts',(32.8725259490779,3.29872589654164,134.454883174923));
#63787=CARTESIAN_POINT('Ctrl Pts',(32.8647689081929,3.39916141930434,134.361561412585));
#63788=CARTESIAN_POINT('Ctrl Pts',(32.8570118673078,3.49559581319379,134.264128380478));
#63789=CARTESIAN_POINT('Ctrl Pts',(32.8492606760677,3.59195748515665,134.166768823378));
#63790=CARTESIAN_POINT('Ctrl Pts',(32.8415094848276,3.68432376005028,134.065304444298));
#63791=CARTESIAN_POINT('Ctrl Pts',(32.8337582935875,3.77233160681873,133.960100991978));
#63792=CARTESIAN_POINT('Ctrl Pts',(32.8260103968104,3.86030204790462,133.854942253932));
#63793=CARTESIAN_POINT('Ctrl Pts',(32.8182625000333,3.94391749491032,133.746047902701));
#63794=CARTESIAN_POINT('Ctrl Pts',(32.8105146032562,4.02285335434779,133.633818861102));
#63795=CARTESIAN_POINT('Ctrl Pts',(32.8027683271721,4.10177270210512,133.521613295399));
#63796=CARTESIAN_POINT('Ctrl Pts',(32.795022051088,4.1760141845391,133.40607474637));
#63797=CARTESIAN_POINT('Ctrl Pts',(32.7872757750039,4.24529517360068,133.287635059005));
#63798=CARTESIAN_POINT('Ctrl Pts',(32.7795294417385,4.31457667407878,133.169194497345));
#63799=CARTESIAN_POINT('Ctrl Pts',(32.7717831084732,4.37889741071513,133.047853092086));
#63800=CARTESIAN_POINT('Ctrl Pts',(32.7640367752078,4.43801976523524,132.92406899984));
#63801=CARTESIAN_POINT('Ctrl Pts',(32.7562887072048,4.49715535979672,132.800257187004));
#63802=CARTESIAN_POINT('Ctrl Pts',(32.7485406392018,4.55109008726569,132.67400195139));
#63803=CARTESIAN_POINT('Ctrl Pts',(32.7407925711988,4.59963386393606,132.545782846732));
#63804=CARTESIAN_POINT('Ctrl Pts',(32.733036268457,4.64822923350994,132.417427469283));
#63805=CARTESIAN_POINT('Ctrl Pts',(32.725279965715,4.69142206820747,132.287104419556));
#63806=CARTESIAN_POINT('Ctrl Pts',(32.7175236629732,4.72907154705318,132.155310418762));
#63807=CARTESIAN_POINT('Ctrl Pts',(32.709763220459,4.76674112055941,132.023446075542));
#63808=CARTESIAN_POINT('Ctrl Pts',(32.7020027779448,4.79886135132349,131.890109596802));
#63809=CARTESIAN_POINT('Ctrl Pts',(32.6942423354307,4.82534248665787,131.755808434818));
#63810=CARTESIAN_POINT('Ctrl Pts',(32.6864694351652,4.85186613186153,131.621291680687));
#63811=CARTESIAN_POINT('Ctrl Pts',(32.6786965348997,4.87273253255604,131.485807535357));
#63812=CARTESIAN_POINT('Ctrl Pts',(32.6709236346343,4.88790369764239,131.349870017186));
#63813=CARTESIAN_POINT('Ctrl Pts',(32.6634332988723,4.90252335266384,131.218874170208));
#63814=CARTESIAN_POINT('Ctrl Pts',(32.6559429631104,4.9118546336778,131.087457647847));
#63815=CARTESIAN_POINT('Ctrl Pts',(32.6484526273485,4.91590933770428,130.956078928827));
#63816=CARTESIAN_POINT('Ctrl Pts',(32.6406782932294,4.92011777706637,130.819718945742));
#63817=CARTESIAN_POINT('Ctrl Pts',(32.6329039591103,4.91865494912831,130.682967741773));
#63818=CARTESIAN_POINT('Ctrl Pts',(32.6251296249912,4.91147701905707,130.546336289693));
#63819=CARTESIAN_POINT('Ctrl Pts',(32.6173648720441,4.90430793514313,130.409873223667));
#63820=CARTESIAN_POINT('Ctrl Pts',(32.609600119097,4.89143778358255,130.27353000256));
#63821=CARTESIAN_POINT('Ctrl Pts',(32.60183536615,4.87287464251269,130.137820460594));
#63822=CARTESIAN_POINT('Ctrl Pts',(32.594078325265,4.85432993861621,130.002245707258));
#63823=CARTESIAN_POINT('Ctrl Pts',(32.58632128438,4.83010355027915,129.867303765421));
#63824=CARTESIAN_POINT('Ctrl Pts',(32.578564243495,4.80025552635874,129.73350584489));
#63825=CARTESIAN_POINT('Ctrl Pts',(32.5708130522549,4.77043001106535,129.599808822412));
#63826=CARTESIAN_POINT('Ctrl Pts',(32.5630618610147,4.73499138307699,129.467254484097));
#63827=CARTESIAN_POINT('Ctrl Pts',(32.5553106697746,4.69405113001353,129.336345954384));
#63828=CARTESIAN_POINT('Ctrl Pts',(32.5475627729976,4.6531282776498,129.205493064287));
#63829=CARTESIAN_POINT('Ctrl Pts',(32.5398148762205,4.60670856743803,129.076284963876));
#63830=CARTESIAN_POINT('Ctrl Pts',(32.5320669794434,4.55495385639095,128.949211451421));
#63831=CARTESIAN_POINT('Ctrl Pts',(32.5243207033594,4.50320997131365,128.822164520005));
#63832=CARTESIAN_POINT('Ctrl Pts',(32.5165744272753,4.44613345249836,128.697251650269));
#63833=CARTESIAN_POINT('Ctrl Pts',(32.5088281511912,4.38393485600219,128.574944047961));
#63834=CARTESIAN_POINT('Ctrl Pts',(32.5010818179258,4.32173580037011,128.452635542806));
#63835=CARTESIAN_POINT('Ctrl Pts',(32.4933354846604,4.25441476883246,128.332932691945));
#63836=CARTESIAN_POINT('Ctrl Pts',(32.4855891513951,4.18222878303977,128.216283055202));
#63837=CARTESIAN_POINT('Ctrl Pts',(32.4778410833921,4.11002663169616,128.099607295581));
#63838=CARTESIAN_POINT('Ctrl Pts',(32.4700930153892,4.03295756386686,127.985986443046));
#63839=CARTESIAN_POINT('Ctrl Pts',(32.4623449473862,3.95132229680212,127.875839630908));
#63840=CARTESIAN_POINT('Ctrl Pts',(32.4545886446444,3.86960026680397,127.765575753428));
#63841=CARTESIAN_POINT('Ctrl Pts',(32.4468323419026,3.78330257632576,127.658793606617));
#63842=CARTESIAN_POINT('Ctrl Pts',(32.4390760391607,3.69277101381425,127.555880157099));
#63843=CARTESIAN_POINT('Ctrl Pts',(32.4313155966466,3.60219113188197,127.452911779575));
#63844=CARTESIAN_POINT('Ctrl Pts',(32.4235551541324,3.50737314534137,127.353816496058));
#63845=CARTESIAN_POINT('Ctrl Pts',(32.4157947116182,3.40869547464421,127.258944108376));
#63846=CARTESIAN_POINT('Ctrl Pts',(32.4080218113528,3.30985939778986,127.163919423115));
#63847=CARTESIAN_POINT('Ctrl Pts',(32.4002489110874,3.20715154847891,127.073131439308));
#63848=CARTESIAN_POINT('Ctrl Pts',(32.392476010822,3.10098384979719,126.986889959421));
#63849=CARTESIAN_POINT('Ctrl Pts',(32.3849856750599,2.99867561438155,126.903783574557));
#63850=CARTESIAN_POINT('Ctrl Pts',(32.3774953392977,2.89315495752513,126.824899063199));
#63851=CARTESIAN_POINT('Ctrl Pts',(32.3700050035356,2.78481398694011,126.750474319131));
#63852=CARTESIAN_POINT('Ctrl Pts',(32.3622306694165,2.6723652355271,126.673227738271));
#63853=CARTESIAN_POINT('Ctrl Pts',(32.3544563352975,2.55652188040092,126.600541090766));
#63854=CARTESIAN_POINT('Ctrl Pts',(32.3466820011784,2.4376901236276,126.532727449366));
#63855=CARTESIAN_POINT('Ctrl Pts',(32.3389172482313,2.31900481637421,126.464997382218));
#63856=CARTESIAN_POINT('Ctrl Pts',(32.3311524952842,2.19733877172655,126.402128563851));
#63857=CARTESIAN_POINT('Ctrl Pts',(32.3233877423371,2.07312865939804,126.344391937846));
#63858=CARTESIAN_POINT('Ctrl Pts',(32.3156307014521,1.94904191430415,126.286712656672));
#63859=CARTESIAN_POINT('Ctrl Pts',(32.307873660567,1.82241648222416,126.234155587604));
#63860=CARTESIAN_POINT('Ctrl Pts',(32.300116619682,1.69371491631963,126.186946531225));
#63861=CARTESIAN_POINT('Ctrl Pts',(32.2923654284419,1.56511040526729,126.139773075563));
#63862=CARTESIAN_POINT('Ctrl Pts',(32.2846142372018,1.43443324224509,126.097939739285));
#63863=CARTESIAN_POINT('Ctrl Pts',(32.2768630459616,1.30216698187255,126.061624675747));
#63864=CARTESIAN_POINT('Ctrl Pts',(32.2691151491846,1.16995693818882,126.025325047079));
#63865=CARTESIAN_POINT('Ctrl Pts',(32.2613672524075,1.03615951671507,125.9945391296));
#63866=CARTESIAN_POINT('Ctrl Pts',(32.2536193556304,0.901274286277271,125.969395496348));
#63867=CARTESIAN_POINT('Ctrl Pts',(32.2458730795463,0.766417270921887,125.944257122602));
#63868=CARTESIAN_POINT('Ctrl Pts',(32.2381268034622,0.630473283305439,125.924758757114));
#63869=CARTESIAN_POINT('Ctrl Pts',(32.2303805273781,0.493952572860944,125.910977951325));
#63870=CARTESIAN_POINT('Ctrl Pts',(32.2226341941127,0.357430854651577,125.89719704381));
#63871=CARTESIAN_POINT('Ctrl Pts',(32.2148878608474,0.220332794107589,125.889133819478));
#63872=CARTESIAN_POINT('Ctrl Pts',(32.207141527582,0.0831738624639008,125.886813955754));
#63873=CARTESIAN_POINT('Ctrl Pts',(32.199393459579,-0.0540157849715361,
125.884493572511));
#63874=CARTESIAN_POINT('Ctrl Pts',(32.1916453915761,-0.191265939797621,
125.887919115847));
#63875=CARTESIAN_POINT('Ctrl Pts',(32.1838973235731,-0.328061428269853,
125.897064135614));
#63876=CARTESIAN_POINT('Ctrl Pts',(32.1761410208312,-0.46500230461512,125.906218874816));
#63877=CARTESIAN_POINT('Ctrl Pts',(32.1683847180894,-0.601487158596418,
125.921105207243));
#63878=CARTESIAN_POINT('Ctrl Pts',(32.1606284153475,-0.737005679230065,
125.941644741506));
#63879=CARTESIAN_POINT('Ctrl Pts',(32.1528679728333,-0.872596530178557,
125.962195238337));
#63880=CARTESIAN_POINT('Ctrl Pts',(32.1451075303191,-1.00721963650943,125.988404874521));
#63881=CARTESIAN_POINT('Ctrl Pts',(32.1373470878049,-1.14037615453993,126.020144350647));
#63882=CARTESIAN_POINT('Ctrl Pts',(32.1295741875395,-1.27374642723425,126.051934777797));
#63883=CARTESIAN_POINT('Ctrl Pts',(32.1218012872741,-1.4056450305916,126.089272677393));
#63884=CARTESIAN_POINT('Ctrl Pts',(32.1140283870087,-1.53558866453363,126.131978942675));
#63885=CARTESIAN_POINT('Ctrl Pts',(32.1065380512467,-1.66080852007273,126.173132727644));
#63886=CARTESIAN_POINT('Ctrl Pts',(32.0990477154847,-1.78421278611718,126.219271239507));
#63887=CARTESIAN_POINT('Ctrl Pts',(32.0915573797228,-1.90538937209461,126.27019317434));
#63888=CARTESIAN_POINT('Ctrl Pts',(32.0837826263318,-2.03116718802486,126.323048680168));
#63889=CARTESIAN_POINT('Ctrl Pts',(32.0760078729409,-2.15494325307723,126.381225491961));
#63890=CARTESIAN_POINT('Ctrl Pts',(32.06823311955,-2.27623453040337,126.444551054626));
#63891=CARTESIAN_POINT('Ctrl Pts',(32.0604680431041,-2.39737484100826,126.50779779833));
#63892=CARTESIAN_POINT('Ctrl Pts',(32.0527029666583,-2.51603617442874,126.576180362149));
#63893=CARTESIAN_POINT('Ctrl Pts',(32.0449378902125,-2.63175449102122,126.6494777839));
#63894=CARTESIAN_POINT('Ctrl Pts',(32.0371806211944,-2.74735645816118,126.72270150846));
#63895=CARTESIAN_POINT('Ctrl Pts',(32.0294233521763,-2.86002096928335,126.80083004836));
#63896=CARTESIAN_POINT('Ctrl Pts',(32.0216660831582,-2.96930799465667,126.883596266656));
#63897=CARTESIAN_POINT('Ctrl Pts',(32.0138838405916,-3.07894685581445,126.966628940345));
#63898=CARTESIAN_POINT('Ctrl Pts',(32.0061015980249,-3.1851860933382,127.054329023599));
#63899=CARTESIAN_POINT('Ctrl Pts',(31.9983193554583,-3.28760955243346,127.14638214671));
#63900=CARTESIAN_POINT('Ctrl Pts',(31.9905717987671,-3.38957650463929,127.238024984079));
#63901=CARTESIAN_POINT('Ctrl Pts',(31.982824242076,-3.48776132977043,127.333981874158));
#63902=CARTESIAN_POINT('Ctrl Pts',(31.9750766853848,-3.58178601945645,127.433901899034));
#63903=CARTESIAN_POINT('Ctrl Pts',(31.9673308780817,-3.67578947849214,127.533799362102));
#63904=CARTESIAN_POINT('Ctrl Pts',(31.9595850707785,-3.76563440369733,127.637657894713));
#63905=CARTESIAN_POINT('Ctrl Pts',(31.9518392634754,-3.85097996662846,127.745090057592));
#63906=CARTESIAN_POINT('Ctrl Pts',(31.9440935277672,-3.93632474070641,127.852521227469));
#63907=CARTESIAN_POINT('Ctrl Pts',(31.9363477920589,-4.01716999289573,127.963525655289));
#63908=CARTESIAN_POINT('Ctrl Pts',(31.9286020563507,-4.09321573473597,128.077683516879));
#63909=CARTESIAN_POINT('Ctrl Pts',(31.9207929067847,-4.16988405834689,128.1927759818));
#63910=CARTESIAN_POINT('Ctrl Pts',(31.9129837572187,-4.24167369234902,128.311073421181));
#63911=CARTESIAN_POINT('Ctrl Pts',(31.9051746076528,-4.30832268917191,128.432117234507));
#63912=CARTESIAN_POINT('Ctrl Pts',(31.8974207673178,-4.37449963654455,128.552303740623));
#63913=CARTESIAN_POINT('Ctrl Pts',(31.8896669269828,-4.43560839980911,128.675197467796));
#63914=CARTESIAN_POINT('Ctrl Pts',(31.8819130866478,-4.49143985946111,128.800326922404));
#63915=CARTESIAN_POINT('Ctrl Pts',(31.8740762824664,-4.54786869956544,128.926795225946));
#63916=CARTESIAN_POINT('Ctrl Pts',(31.8662394782849,-4.59890648942169,129.05554700006));
#63917=CARTESIAN_POINT('Ctrl Pts',(31.8584026741034,-4.64438842963329,129.186077831033));
#63918=CARTESIAN_POINT('Ctrl Pts',(31.850565869922,-4.68987036984483,129.316608662006));
#63919=CARTESIAN_POINT('Ctrl Pts',(31.8427290657405,-4.72979638684535,129.448918145974));
#63920=CARTESIAN_POINT('Ctrl Pts',(31.8348922615591,-4.76405452823408,129.582490119308));
#63921=CARTESIAN_POINT('Ctrl Pts',(33.5849978012129,-4.7640545282341,129.582490119308));
#63922=CARTESIAN_POINT('Ctrl Pts',(33.5773446850024,-4.79770990922239,129.71371193899));
#63923=CARTESIAN_POINT('Ctrl Pts',(33.5696915687919,-4.82591769789479,129.846240287322));
#63924=CARTESIAN_POINT('Ctrl Pts',(33.5620384525814,-4.8485992859329,129.979576993243));
#63925=CARTESIAN_POINT('Ctrl Pts',(33.554175283156,-4.87190340998842,130.116573359227));
#63926=CARTESIAN_POINT('Ctrl Pts',(33.5463121137306,-4.88937354778417,130.254422640192));
#63927=CARTESIAN_POINT('Ctrl Pts',(33.5384489443052,-4.90098157445576,130.392580737842));
#63928=CARTESIAN_POINT('Ctrl Pts',(33.5305857748798,-4.91258960112736,130.530738835493));
#63929=CARTESIAN_POINT('Ctrl Pts',(33.5227226054543,-4.91833555897516,130.669205293498));
#63930=CARTESIAN_POINT('Ctrl Pts',(33.5148594360289,-4.9182490365939,130.807439017015));
#63931=CARTESIAN_POINT('',(33.8601405639655,-4.91824957007167,130.806417068353));
#63932=CARTESIAN_POINT('Ctrl Pts',(33.9299189896066,-4.764054528234,129.582490119308));
#63933=CARTESIAN_POINT('Ctrl Pts',(33.9220152405073,-4.79880154218852,129.717968199357));
#63934=CARTESIAN_POINT('Ctrl Pts',(33.914111491408,-4.82779127781455,129.855030603445));
#63935=CARTESIAN_POINT('Ctrl Pts',(33.9062077423087,-4.85089013886288,129.993159087006));
#63936=CARTESIAN_POINT('Ctrl Pts',(33.8983092543243,-4.87397362420029,130.131195625616));
#63937=CARTESIAN_POINT('Ctrl Pts',(33.8904107663399,-4.89117398588149,130.270296467006));
#63938=CARTESIAN_POINT('Ctrl Pts',(33.8825122783555,-4.90240853659577,130.409932420282));
#63939=CARTESIAN_POINT('Ctrl Pts',(33.8750550402399,-4.91301546794307,130.54176759622));
#63940=CARTESIAN_POINT('Ctrl Pts',(33.8675978021243,-4.91830490393996,130.674079413037));
#63941=CARTESIAN_POINT('Ctrl Pts',(33.8601405640087,-4.91824957007199,130.806417067586));
#63942=CARTESIAN_POINT('Ctrl Pts',(33.8601405639655,-4.91824957007167,130.806417068353));
#63943=CARTESIAN_POINT('Ctrl Pts',(33.8517056390285,-4.91818698159191,130.956104950805));
#63944=CARTESIAN_POINT('Ctrl Pts',(33.8432707140914,-4.91128657896475,131.105575117));
#63945=CARTESIAN_POINT('Ctrl Pts',(33.8348357891543,-4.89763267691119,131.254224179718));
#63946=CARTESIAN_POINT('Ctrl Pts',(33.8263627532913,-4.88391708339587,131.403544873002));
#63947=CARTESIAN_POINT('Ctrl Pts',(33.8178897174284,-4.86338690985431,131.552036764359));
#63948=CARTESIAN_POINT('Ctrl Pts',(33.8094166815654,-4.83617815412594,131.699102996162));
#63949=CARTESIAN_POINT('Ctrl Pts',(33.8009242185549,-4.80890701361357,131.846506424388));
#63950=CARTESIAN_POINT('Ctrl Pts',(33.7924317555444,-4.77492675024485,131.992477400738));
#63951=CARTESIAN_POINT('Ctrl Pts',(33.7839392925339,-4.73442338032173,132.136433557897));
#63952=CARTESIAN_POINT('Ctrl Pts',(33.7754180739657,-4.69378286561634,132.280877151926));
#63953=CARTESIAN_POINT('Ctrl Pts',(33.7668968553975,-4.6465751220737,132.423292017553));
#63954=CARTESIAN_POINT('Ctrl Pts',(33.7583756368293,-4.59303557172602,132.563112248513));
#63955=CARTESIAN_POINT('Ctrl Pts',(33.7531351333664,-4.56010903701138,132.649100936476));
#63956=CARTESIAN_POINT('Ctrl Pts',(33.7478946299035,-4.52478862071199,132.734108740538));
#63957=CARTESIAN_POINT('Ctrl Pts',(33.7426541264407,-4.48713762383094,132.818008801162));
#63958=CARTESIAN_POINT('Ctrl Pts',(33.7348797923216,-4.43128203061448,132.942475297279));
#63959=CARTESIAN_POINT('Ctrl Pts',(33.7271054582025,-4.37015526934994,133.064813152049));
#63960=CARTESIAN_POINT('Ctrl Pts',(33.7193311240834,-4.30394140587459,133.184543685588));
#63961=CARTESIAN_POINT('Ctrl Pts',(33.7115663711363,-4.23780914506827,133.304126661945));
#63962=CARTESIAN_POINT('Ctrl Pts',(33.7038016181891,-4.16660244367708,133.421108371713));
#63963=CARTESIAN_POINT('Ctrl Pts',(33.696036865242,-4.09055330336761,133.535030267086));
#63964=CARTESIAN_POINT('Ctrl Pts',(33.688279824357,-4.01457969613639,133.648839013626));
#63965=CARTESIAN_POINT('Ctrl Pts',(33.680522783472,-3.93377343692912,133.759593670555));
#63966=CARTESIAN_POINT('Ctrl Pts',(33.6727657425869,-3.84841211580568,133.866860780737));
#63967=CARTESIAN_POINT('Ctrl Pts',(33.6650145513468,-3.76311516631873,133.974046999955));
#63968=CARTESIAN_POINT('Ctrl Pts',(33.6572633601067,-3.6732702345515,134.077750602571));
#63969=CARTESIAN_POINT('Ctrl Pts',(33.6495121688666,-3.57919763210577,134.17756790038));
#63970=CARTESIAN_POINT('Ctrl Pts',(33.6417642720895,-3.48516501302541,134.277342773175));
#63971=CARTESIAN_POINT('Ctrl Pts',(33.6340163753123,-3.38690856469369,134.373234342509));
#63972=CARTESIAN_POINT('Ctrl Pts',(33.6262684785352,-3.28478806640864,134.464872934343));
#63973=CARTESIAN_POINT('Ctrl Pts',(33.6185222024511,-3.18268892953023,134.55649235736));
#63974=CARTESIAN_POINT('Ctrl Pts',(33.610775926367,-3.07672764120346,134.643860311451));
#63975=CARTESIAN_POINT('Ctrl Pts',(33.6030296502828,-2.96729964294952,134.726645142107));
#63976=CARTESIAN_POINT('Ctrl Pts',(33.5952833170175,-2.85787083692296,134.809430583861));
#63977=CARTESIAN_POINT('Ctrl Pts',(33.587536983752,-2.74497558169847,134.887632598793));
#63978=CARTESIAN_POINT('Ctrl Pts',(33.5797906504866,-2.62904076230094,134.960961119498));
#63979=CARTESIAN_POINT('Ctrl Pts',(33.5720425824836,-2.51307998010459,135.034306061616));
#63980=CARTESIAN_POINT('Ctrl Pts',(33.5642945144807,-2.39407860959861,135.102775128827));
#63981=CARTESIAN_POINT('Ctrl Pts',(33.5565464464777,-2.27249039741194,135.166122928395));
#63982=CARTESIAN_POINT('Ctrl Pts',(33.5487901437358,-2.15077295982644,135.229538054759));
#63983=CARTESIAN_POINT('Ctrl Pts',(33.541033840994,-2.02646353576651,135.287820859679));
#63984=CARTESIAN_POINT('Ctrl Pts',(33.5332775382521,-1.90003873753938,135.340772840717));
#63985=CARTESIAN_POINT('Ctrl Pts',(33.5255170957379,-1.77354646259069,135.39375308382));
#63986=CARTESIAN_POINT('Ctrl Pts',(33.5177566532237,-1.64493693020729,135.44139669795));
#63987=CARTESIAN_POINT('Ctrl Pts',(33.5099962107095,-1.51470344026117,135.483554624076));
#63988=CARTESIAN_POINT('Ctrl Pts',(33.5022233104441,-1.38426088795541,135.525780225848));
#63989=CARTESIAN_POINT('Ctrl Pts',(33.4944504101786,-1.25218954552087,135.562502437403));
#63990=CARTESIAN_POINT('Ctrl Pts',(33.4866775099131,-1.11899534644983,135.593622823493));
#63991=CARTESIAN_POINT('Ctrl Pts',(33.4791871741513,-0.99064309201547,135.62361190516));
#63992=CARTESIAN_POINT('Ctrl Pts',(33.4716968383895,-0.86124850345266,135.648399313348));
#63993=CARTESIAN_POINT('Ctrl Pts',(33.4642065026277,-0.731268243770763,
135.667942612161));
#63994=CARTESIAN_POINT('Ctrl Pts',(33.4564321685087,-0.596359743032192,
135.68822690109));
#63995=CARTESIAN_POINT('Ctrl Pts',(33.4486578343896,-0.460392933458573,
135.70292582441));
#63996=CARTESIAN_POINT('Ctrl Pts',(33.4408835002705,-0.323870034075956,
135.711935503752));
#63997=CARTESIAN_POINT('Ctrl Pts',(33.4331187473235,-0.187515386965612,
135.720934079471));
#63998=CARTESIAN_POINT('Ctrl Pts',(33.4253539943764,-0.0506064000222067,
135.724257336478));
#63999=CARTESIAN_POINT('Ctrl Pts',(33.4175892414293,0.0863457349310442,
135.721852608059));
#64000=CARTESIAN_POINT('Ctrl Pts',(33.4098322005443,0.223161847093359,135.719450268049));
#64001=CARTESIAN_POINT('Ctrl Pts',(33.4020751596593,0.360020633606295,135.711331271029));
#64002=CARTESIAN_POINT('Ctrl Pts',(33.3943181187743,0.496407370497047,135.697494867208));
#64003=CARTESIAN_POINT('Ctrl Pts',(33.3865669275341,0.632691257088577,135.683668897526));
#64004=CARTESIAN_POINT('Ctrl Pts',(33.378815736294,0.768503415212321,135.664134142205));
#64005=CARTESIAN_POINT('Ctrl Pts',(33.3710645450539,0.903331074304611,135.638941885132));
#64006=CARTESIAN_POINT('Ctrl Pts',(33.3633166482768,1.03810142804496,135.61376033544));
#64007=CARTESIAN_POINT('Ctrl Pts',(33.3555687514997,1.17188773148628,135.582926138198));
#64008=CARTESIAN_POINT('Ctrl Pts',(33.3478208547227,1.30418449789093,135.546542168072));
#64009=CARTESIAN_POINT('Ctrl Pts',(33.3400745786386,1.43645359066405,135.510165808688));
#64010=CARTESIAN_POINT('Ctrl Pts',(33.3323283025546,1.56723338941808,135.468242089107));
#64011=CARTESIAN_POINT('Ctrl Pts',(33.3245820264705,1.69603111802011,135.420924438116));
#64012=CARTESIAN_POINT('Ctrl Pts',(33.3168356932051,1.82482979737771,135.373606437836));
#64013=CARTESIAN_POINT('Ctrl Pts',(33.3090893599397,1.95164601040449,135.320894561518));
#64014=CARTESIAN_POINT('Ctrl Pts',(33.3013430266744,2.07600497339404,135.262991171104));
#64015=CARTESIAN_POINT('Ctrl Pts',(33.2935949586714,2.20039178571112,135.205074813627));
#64016=CARTESIAN_POINT('Ctrl Pts',(33.2858468906685,2.32231989862834,135.141964793605));
#64017=CARTESIAN_POINT('Ctrl Pts',(33.2780988226656,2.44133759515221,135.073910220158));
#64018=CARTESIAN_POINT('Ctrl Pts',(33.2703425199237,2.56048178510027,135.005783317502));
#64019=CARTESIAN_POINT('Ctrl Pts',(33.2625862171819,2.67670903966507,134.932701558111));
#64020=CARTESIAN_POINT('Ctrl Pts',(33.2548299144401,2.78959473252861,134.854958634001));
#64021=CARTESIAN_POINT('Ctrl Pts',(33.2470694719259,2.90254067588566,134.777174216152));
#64022=CARTESIAN_POINT('Ctrl Pts',(33.2393090294117,3.01214119150543,134.694723911344));
#64023=CARTESIAN_POINT('Ctrl Pts',(33.2315485868975,3.11800423117598,134.607942176685));
#64024=CARTESIAN_POINT('Ctrl Pts',(33.2237756866321,3.22403721159574,134.521021132281));
#64025=CARTESIAN_POINT('Ctrl Pts',(33.2160027863666,3.32632043481156,134.429755023772));
#64026=CARTESIAN_POINT('Ctrl Pts',(33.2082298861012,3.42449761505119,134.334516300678));
#64027=CARTESIAN_POINT('Ctrl Pts',(33.2007395503391,3.51910580749719,134.242739745059));
#64028=CARTESIAN_POINT('Ctrl Pts',(33.193249214577,3.60990109178267,134.147274612643));
#64029=CARTESIAN_POINT('Ctrl Pts',(33.1857588788148,3.69660092787551,134.048482169316));
#64030=CARTESIAN_POINT('Ctrl Pts',(33.1779845446957,3.78658801460439,133.945943980474));
#64031=CARTESIAN_POINT('Ctrl Pts',(33.1702102105766,3.87244801683716,133.839496379896));
#64032=CARTESIAN_POINT('Ctrl Pts',(33.1624358764576,3.95382207710918,133.729505749874));
#64033=CARTESIAN_POINT('Ctrl Pts',(33.1546711235105,4.0350958511244,133.619650673474));
#64034=CARTESIAN_POINT('Ctrl Pts',(33.1469063705634,4.11189445299536,133.506261566882));
#64035=CARTESIAN_POINT('Ctrl Pts',(33.1391416176163,4.18389726105459,133.38974004261));
#64036=CARTESIAN_POINT('Ctrl Pts',(33.1313845767313,4.2558285549098,133.273334249158));
#64037=CARTESIAN_POINT('Ctrl Pts',(33.1236275358463,4.32297332984678,133.153802559816));
#64038=CARTESIAN_POINT('Ctrl Pts',(33.1158704949613,4.38505273416512,133.031577621158));
#64039=CARTESIAN_POINT('Ctrl Pts',(33.1081193037212,4.44708532392176,132.909444853278));
#64040=CARTESIAN_POINT('Ctrl Pts',(33.1003681124811,4.50405996987923,132.784623225834));
#64041=CARTESIAN_POINT('Ctrl Pts',(33.0926169212409,4.55574265360974,132.657571867419));
#64042=CARTESIAN_POINT('Ctrl Pts',(33.0848690244639,4.60740337082099,132.53057450922));
#64043=CARTESIAN_POINT('Ctrl Pts',(33.0771211276868,4.65377645233411,132.401349666334));
#64044=CARTESIAN_POINT('Ctrl Pts',(33.0693732309097,4.69467522158936,132.270378225337));
#64045=CARTESIAN_POINT('Ctrl Pts',(33.0616269548256,4.73556543570374,132.139434180743));
#64046=CARTESIAN_POINT('Ctrl Pts',(33.0538806787415,4.77098349877912,132.006744637697));
#64047=CARTESIAN_POINT('Ctrl Pts',(33.0461344026575,4.80079213726351,131.872807114724));
#64048=CARTESIAN_POINT('Ctrl Pts',(33.0383880693921,4.83060099578849,131.738868603055));
#64049=CARTESIAN_POINT('Ctrl Pts',(33.0306417361267,4.85480026216309,131.603682474704));
#64050=CARTESIAN_POINT('Ctrl Pts',(33.0228954028614,4.87330355703107,131.467757560224));
#64051=CARTESIAN_POINT('Ctrl Pts',(33.0151473348584,4.89181099558365,131.331802206302));
#64052=CARTESIAN_POINT('Ctrl Pts',(33.0073992668555,4.90461987166122,131.195108124351));
#64053=CARTESIAN_POINT('Ctrl Pts',(32.9996511988525,4.91169560375513,131.058190006236));
#64054=CARTESIAN_POINT('Ctrl Pts',(32.9918948961106,4.91877885602131,130.921126369916));
#64055=CARTESIAN_POINT('Ctrl Pts',(32.9841385933688,4.92011677216353,130.783838612851));
#64056=CARTESIAN_POINT('Ctrl Pts',(32.976382290627,4.91572692269514,130.646842732898));
#64057=CARTESIAN_POINT('Ctrl Pts',(32.9686218481128,4.91133473023189,130.509773734119));
#64058=CARTESIAN_POINT('Ctrl Pts',(32.9608614055987,4.90120870951671,130.372997312571));
#64059=CARTESIAN_POINT('Ctrl Pts',(32.9531009630845,4.88541833715185,130.237024091754));
#64060=CARTESIAN_POINT('Ctrl Pts',(32.9453280628191,4.86960261667947,130.100832594652));
#64061=CARTESIAN_POINT('Ctrl Pts',(32.9375551625536,4.84810443535503,129.965447261201));
#64062=CARTESIAN_POINT('Ctrl Pts',(32.9297822622882,4.82104456434546,129.831369162776));
#64063=CARTESIAN_POINT('Ctrl Pts',(32.9222919265261,4.79496838780672,129.70216514095));
#64064=CARTESIAN_POINT('Ctrl Pts',(32.9148015907641,4.76372793714712,129.57417526089));
#64065=CARTESIAN_POINT('Ctrl Pts',(32.907311255002,4.72747443579848,129.447832504561));
#64066=CARTESIAN_POINT('Ctrl Pts',(32.8995369208829,4.6898463719273,129.316699424226));
#64067=CARTESIAN_POINT('Ctrl Pts',(32.8917625867639,4.6466984192615,129.186925444426));
#64068=CARTESIAN_POINT('Ctrl Pts',(32.8839882526448,4.59814485437666,129.059010520689));
#64069=CARTESIAN_POINT('Ctrl Pts',(32.8762234996977,4.54965112742119,128.931253240663));
#64070=CARTESIAN_POINT('Ctrl Pts',(32.8684587467506,4.49576518092037,128.805350820063));
#64071=CARTESIAN_POINT('Ctrl Pts',(32.8606939938035,4.43665159901168,128.681790088352));
#64072=CARTESIAN_POINT('Ctrl Pts',(32.8529369529185,4.37759672954589,128.558352078901));
#64073=CARTESIAN_POINT('Ctrl Pts',(32.8451799120334,4.3133247249444,128.437251480295));
#64074=CARTESIAN_POINT('Ctrl Pts',(32.8374228711484,4.24404885686923,128.318956754407));
#64075=CARTESIAN_POINT('Ctrl Pts',(32.8296716799083,4.17482523026507,128.200751235492));
#64076=CARTESIAN_POINT('Ctrl Pts',(32.8219204886682,4.10060544778748,128.085347713671));
#64077=CARTESIAN_POINT('Ctrl Pts',(32.814169297428,4.02164929464727,127.973191245493));
#64078=CARTESIAN_POINT('Ctrl Pts',(32.8064214006509,3.94272669997837,127.861082446806));
#64079=CARTESIAN_POINT('Ctrl Pts',(32.7986735038739,3.85907196310345,127.752218275903));
#64080=CARTESIAN_POINT('Ctrl Pts',(32.7909256070968,3.77098876427939,127.647015720001));
#64081=CARTESIAN_POINT('Ctrl Pts',(32.7831793310127,3.68292399056167,127.541835170206));
#64082=CARTESIAN_POINT('Ctrl Pts',(32.7754330549286,3.59043284826041,127.440315011511));
#64083=CARTESIAN_POINT('Ctrl Pts',(32.7676867788445,3.49385971409267,127.342839656956));
#64084=CARTESIAN_POINT('Ctrl Pts',(32.7599404455792,3.397285867044,127.245363582861));
#64085=CARTESIAN_POINT('Ctrl Pts',(32.7521941123137,3.29663024316775,127.151932650223));
#64086=CARTESIAN_POINT('Ctrl Pts',(32.7444477790484,3.19227424586641,127.062894567783));
#64087=CARTESIAN_POINT('Ctrl Pts',(32.7366997110454,3.08789487876302,126.973836545882));
#64088=CARTESIAN_POINT('Ctrl Pts',(32.7289516430425,2.97981378663374,126.889173585438));
#64089=CARTESIAN_POINT('Ctrl Pts',(32.7212035750395,2.86844530217183,126.80921298438));
#64090=CARTESIAN_POINT('Ctrl Pts',(32.7134472722976,2.75695845395933,126.729167400244));
#64091=CARTESIAN_POINT('Ctrl Pts',(32.7056909695557,2.64217755210482,126.653834387369));
#64092=CARTESIAN_POINT('Ctrl Pts',(32.6979346668139,2.52454621750959,126.583478072629));
#64093=CARTESIAN_POINT('Ctrl Pts',(32.6901742242997,2.40685209952911,126.513084206605));
#64094=CARTESIAN_POINT('Ctrl Pts',(32.6824137817855,2.28630486083248,126.44767251782));
#64095=CARTESIAN_POINT('Ctrl Pts',(32.6746533392713,2.16337165723281,126.387460558115));
#64096=CARTESIAN_POINT('Ctrl Pts',(32.6668804390058,2.04024111034122,126.327151940827));
#64097=CARTESIAN_POINT('Ctrl Pts',(32.6591075387404,1.91471730286885,126.272059889934));
#64098=CARTESIAN_POINT('Ctrl Pts',(32.651334638475,1.78728708011941,126.222353638551));
#64099=CARTESIAN_POINT('Ctrl Pts',(32.643844302713,1.66448926694566,126.174454334609));
#64100=CARTESIAN_POINT('Ctrl Pts',(32.6363539669511,1.5399215293189,126.131556154026));
#64101=CARTESIAN_POINT('Ctrl Pts',(32.6288636311891,1.41402988718873,126.093765905575));
#64102=CARTESIAN_POINT('Ctrl Pts',(32.6210892970701,1.28336502518216,126.054542828367));
#64103=CARTESIAN_POINT('Ctrl Pts',(32.613314962951,1.15085997822314,126.020698416971));
#64104=CARTESIAN_POINT('Ctrl Pts',(32.6055406288319,1.01699714233727,125.992406765441));
#64105=CARTESIAN_POINT('Ctrl Pts',(32.5977758758848,0.883299280432971,125.964149980844));
#64106=CARTESIAN_POINT('Ctrl Pts',(32.5900111229377,0.748247337919862,125.941432420093));
#64107=CARTESIAN_POINT('Ctrl Pts',(32.5822463699906,0.612339859958383,125.924378757107));
#64108=CARTESIAN_POINT('Ctrl Pts',(32.5744893291056,0.476567367219976,125.907342032061));
#64109=CARTESIAN_POINT('Ctrl Pts',(32.5667322882206,0.339941415446912,125.895958058216));
#64110=CARTESIAN_POINT('Ctrl Pts',(32.5589752473356,0.202971413425118,125.89030061917));
#64111=CARTESIAN_POINT('Ctrl Pts',(32.5512240560955,0.0661047015473196,
125.884647446444));
#64112=CARTESIAN_POINT('Ctrl Pts',(32.5434728648554,-0.0711051551062505,
125.884712229023));
#64113=CARTESIAN_POINT('Ctrl Pts',(32.5357216736152,-0.208143297603718,
125.890516966191));
#64114=CARTESIAN_POINT('Ctrl Pts',(32.5279737768382,-0.345123195235013,
125.89631923619));
#64115=CARTESIAN_POINT('Ctrl Pts',(32.5202258800611,-0.481931134070877,
125.907856592019));
#64116=CARTESIAN_POINT('Ctrl Pts',(32.512477983284,-0.618052144358261,125.925098930655));
#64117=CARTESIAN_POINT('Ctrl Pts',(32.5047317071999,-0.754144681064723,
125.942337662566));
#64118=CARTESIAN_POINT('Ctrl Pts',(32.4969854311159,-0.889550187411085,
125.965278954526));
#64119=CARTESIAN_POINT('Ctrl Pts',(32.4892391550318,-1.02375910179051,125.993840857291));
#64120=CARTESIAN_POINT('Ctrl Pts',(32.4814928217665,-1.15796900686948,126.022402970892));
#64121=CARTESIAN_POINT('Ctrl Pts',(32.473746488501,-1.29098191995453,126.056585696706));
#64122=CARTESIAN_POINT('Ctrl Pts',(32.4660001552357,-1.42229914597879,126.096256094316));
#64123=CARTESIAN_POINT('Ctrl Pts',(32.4582520872327,-1.55364577958533,126.135935375836));
#64124=CARTESIAN_POINT('Ctrl Pts',(32.4505040192298,-1.68329559630917,126.181104661533));
#64125=CARTESIAN_POINT('Ctrl Pts',(32.4427559512268,-1.81076610075897,126.231581463611));
#64126=CARTESIAN_POINT('Ctrl Pts',(32.434999648485,-1.93837208237799,126.282111913036));
#64127=CARTESIAN_POINT('Ctrl Pts',(32.4272433457431,-2.06379376078352,126.33796100296));
#64128=CARTESIAN_POINT('Ctrl Pts',(32.4194870430013,-2.18656913062253,126.398898269582));
#64129=CARTESIAN_POINT('Ctrl Pts',(32.4117266004871,-2.30941002937312,126.459868060257));
#64130=CARTESIAN_POINT('Ctrl Pts',(32.403966157973,-2.42960146274863,126.52593125069));
#64131=CARTESIAN_POINT('Ctrl Pts',(32.3962057154588,-2.54670788909553,126.596812401548));
#64132=CARTESIAN_POINT('Ctrl Pts',(32.3884328151934,-2.66400230507421,126.667807337122));
#64133=CARTESIAN_POINT('Ctrl Pts',(32.380659914928,-2.77820149180594,126.743635472161));
#64134=CARTESIAN_POINT('Ctrl Pts',(32.3728870146626,-2.88889991690063,126.823978684556));
#64135=CARTESIAN_POINT('Ctrl Pts',(32.3653966789004,-2.99557417541182,126.901401218809));
#64136=CARTESIAN_POINT('Ctrl Pts',(32.3579063431383,-3.09899753460147,126.983016069966));
#64137=CARTESIAN_POINT('Ctrl Pts',(32.3504160073762,-3.19883904854657,127.068505721562));
#64138=CARTESIAN_POINT('Ctrl Pts',(32.3427555834548,-3.30094773179821,127.155936644945));
#64139=CARTESIAN_POINT('Ctrl Pts',(32.3350951595333,-3.39965344572871,127.247714920717));
#64140=CARTESIAN_POINT('Ctrl Pts',(32.3274347356118,-3.49455512505835,127.343541705743));
#64141=CARTESIAN_POINT('Ctrl Pts',(32.3197831159588,-3.58934773211337,127.439258355254));
#64142=CARTESIAN_POINT('Ctrl Pts',(32.3121314963058,-3.68034471478857,127.539013981536));
#64143=CARTESIAN_POINT('Ctrl Pts',(32.3044798766527,-3.76717720600479,127.6424689431));
#64144=CARTESIAN_POINT('Ctrl Pts',(32.2968352796751,-3.85393000214713,127.745828953446));
#64145=CARTESIAN_POINT('Ctrl Pts',(32.2891906826974,-3.93652564899884,127.852881241732));
#64146=CARTESIAN_POINT('Ctrl Pts',(32.2815460857197,-4.0146317797902,127.963249085929));
#64147=CARTESIAN_POINT('Ctrl Pts',(32.2739067365241,-4.09268429311149,128.073541165977));
#64148=CARTESIAN_POINT('Ctrl Pts',(32.2662673873284,-4.16625318802899,128.187143947303));
#64149=CARTESIAN_POINT('Ctrl Pts',(32.2586280381327,-4.23504645809728,128.303647807134));
#64150=CARTESIAN_POINT('Ctrl Pts',(32.2509915588414,-4.30381388432724,128.420107899502));
#64151=CARTESIAN_POINT('Ctrl Pts',(32.2433550795501,-4.36780904705292,128.539466557496));
#64152=CARTESIAN_POINT('Ctrl Pts',(32.2357186002588,-4.42678361026189,128.661285740102));
#64153=CARTESIAN_POINT('Ctrl Pts',(32.2280837877793,-4.48574530111247,128.783078333275));
#64154=CARTESIAN_POINT('Ctrl Pts',(32.2204489752998,-4.53968840018407,128.907330018292));
#64155=CARTESIAN_POINT('Ctrl Pts',(32.2128141628203,-4.58841114259887,129.033579363719));
#64156=CARTESIAN_POINT('Ctrl Pts',(32.2051776741029,-4.63714458218635,129.159856427436));
#64157=CARTESIAN_POINT('Ctrl Pts',(32.1975411853855,-4.68065523172521,129.288131650922));
#64158=CARTESIAN_POINT('Ctrl Pts',(32.1899046966682,-4.7187900697642,129.417925137641));
#64159=CARTESIAN_POINT('Ctrl Pts',(32.1866923469053,-4.73483179292596,129.472523800943));
#64160=CARTESIAN_POINT('Ctrl Pts',(32.1834799971424,-4.74992285459696,129.527390938275));
#64161=CARTESIAN_POINT('Ctrl Pts',(32.1802676473795,-4.76405452823406,129.582490119308));
#64162=CARTESIAN_POINT('Origin',(213.235140564004,0.,130.804360617566));
#64163=CARTESIAN_POINT('',(30.0845737196929,-4.764054528234,129.582490119308));
#64164=CARTESIAN_POINT('',(30.4301958372212,-4.76405452823406,129.582490119308));
#64165=CARTESIAN_POINT('',(213.235140564004,-4.76405452823405,129.582490119308));
#64166=CARTESIAN_POINT('',(31.7648594359428,-4.91824826067858,130.800224335163));
#64167=CARTESIAN_POINT('Ctrl Pts',(31.7648594359429,-4.91824826067858,130.800224335163));
#64168=CARTESIAN_POINT('Ctrl Pts',(31.757212549846,-4.91836154469456,130.934924740103));
#64169=CARTESIAN_POINT('Ctrl Pts',(31.7495656637491,-4.91293693387984,131.069821508205));
#64170=CARTESIAN_POINT('Ctrl Pts',(31.7419187776522,-4.90195272443736,131.204413801382));
#64171=CARTESIAN_POINT('Ctrl Pts',(31.7342789780509,-4.89097869424312,131.338881365658));
#64172=CARTESIAN_POINT('Ctrl Pts',(31.7266391784498,-4.87445534555453,131.473044616405));
#64173=CARTESIAN_POINT('Ctrl Pts',(31.7189993788485,-4.85241302391724,131.606402329585));
#64174=CARTESIAN_POINT('Ctrl Pts',(31.7113186602338,-4.83025264289347,131.740474310984));
#64175=CARTESIAN_POINT('Ctrl Pts',(31.7036379416192,-4.8025139878959,131.873731687635));
#64176=CARTESIAN_POINT('Ctrl Pts',(31.6959572230045,-4.76928087100165,132.005669502074));
#64177=CARTESIAN_POINT('Ctrl Pts',(31.6883248466186,-4.73625692241787,132.13677690359));
#64178=CARTESIAN_POINT('Ctrl Pts',(31.6806924702326,-4.69780758699693,132.26658091181));
#64179=CARTESIAN_POINT('Ctrl Pts',(31.6730600938466,-4.65406632644129,132.394596352162));
#64180=CARTESIAN_POINT('Ctrl Pts',(31.6654284959104,-4.61032952719301,132.522598735821));
#64181=CARTESIAN_POINT('Ctrl Pts',(31.6577968979742,-4.56130200649142,132.648812532375));
#64182=CARTESIAN_POINT('Ctrl Pts',(31.6501653000381,-4.50716674333285,132.772768860359));
#64183=CARTESIAN_POINT('Ctrl Pts',(31.6425327135101,-4.45302446753059,132.896741245558));
#64184=CARTESIAN_POINT('Ctrl Pts',(31.6349001269821,-4.39377329563917,133.018455210967));
#64185=CARTESIAN_POINT('Ctrl Pts',(31.6272675404542,-4.3296436464861,133.137463477909));
#64186=CARTESIAN_POINT('Ctrl Pts',(31.6195504230911,-4.26480376197823,133.257789760462));
#64187=CARTESIAN_POINT('Ctrl Pts',(31.611833305728,-4.19497688306446,133.375349675669));
#64188=CARTESIAN_POINT('Ctrl Pts',(31.6041161883649,-4.12044738007431,133.489709095983));
#64189=CARTESIAN_POINT('Ctrl Pts',(31.5964724350254,-4.04662640385107,133.602981339984));
#64190=CARTESIAN_POINT('Ctrl Pts',(31.5888286816858,-3.96819211872463,133.713113386612));
#64191=CARTESIAN_POINT('Ctrl Pts',(31.5811849283463,-3.88546220587877,133.819715739138));
#64192=CARTESIAN_POINT('Ctrl Pts',(31.5734311289714,-3.80154124218248,133.92785283065));
#64193=CARTESIAN_POINT('Ctrl Pts',(31.5656773295965,-3.71320029065335,134.032357481853));
#64194=CARTESIAN_POINT('Ctrl Pts',(31.5579235302216,-3.62080982167619,134.132861676264));
#64195=CARTESIAN_POINT('Ctrl Pts',(31.5501697308467,-3.52841935269891,134.233365870675));
#64196=CARTESIAN_POINT('Ctrl Pts',(31.5424159314718,-3.43197971543658,134.329869355433));
#64197=CARTESIAN_POINT('Ctrl Pts',(31.5346621320969,-3.33189555451496,134.422047043488));
#64198=CARTESIAN_POINT('Ctrl Pts',(31.5268877979779,-3.23154633609829,134.514468849963));
#64199=CARTESIAN_POINT('Ctrl Pts',(31.5191134638588,-3.12718979311009,134.602858575542));
#64200=CARTESIAN_POINT('Ctrl Pts',(31.5113391297397,-3.01918359074611,134.686848673938));
#64201=CARTESIAN_POINT('Ctrl Pts',(31.5035743767926,-2.91131049637376,134.770735262044));
#64202=CARTESIAN_POINT('Ctrl Pts',(31.4958096238455,-2.79979699773103,134.850232773725));
#64203=CARTESIAN_POINT('Ctrl Pts',(31.4880448708984,-2.6850368976392,134.925011042052));
#64204=CARTESIAN_POINT('Ctrl Pts',(31.4802878300134,-2.57039077889661,134.999715039548));
#64205=CARTESIAN_POINT('Ctrl Pts',(31.4725307891284,-2.45250480118755,135.069708909408));
#64206=CARTESIAN_POINT('Ctrl Pts',(31.4647737482434,-2.33180479482437,135.134703497909));
#64207=CARTESIAN_POINT('Ctrl Pts',(31.4570225570033,-2.21119580927489,135.199649073484));
#64208=CARTESIAN_POINT('Ctrl Pts',(31.4492713657632,-2.08777736178262,135.259602687039));
#64209=CARTESIAN_POINT('Ctrl Pts',(31.441520174523,-1.9620028329244,135.314319369716));
#64210=CARTESIAN_POINT('Ctrl Pts',(31.433772277746,-1.83628176159591,135.369012796344));
#64211=CARTESIAN_POINT('Ctrl Pts',(31.4260243809689,-1.70820695836303,135.418473563473));
#64212=CARTESIAN_POINT('Ctrl Pts',(31.4182764841918,-1.57825469159732,135.462503508349));
#64213=CARTESIAN_POINT('Ctrl Pts',(31.4105302081077,-1.44832960804454,135.50652424311));
#64214=CARTESIAN_POINT('Ctrl Pts',(31.4027839320236,-1.31652821216427,135.545116289826));
#64215=CARTESIAN_POINT('Ctrl Pts',(31.3950376559395,-1.18334458502106,135.578130475404));
#64216=CARTESIAN_POINT('Ctrl Pts',(31.3872913226741,-1.05015997474638,135.611144904685));
#64217=CARTESIAN_POINT('Ctrl Pts',(31.3795449894088,-0.915593492328854,
135.6385812966));
#64218=CARTESIAN_POINT('Ctrl Pts',(31.3717986561434,-0.780151748923722,
135.660341086138));
#64219=CARTESIAN_POINT('Ctrl Pts',(31.3640505881404,-0.644679674279241,
135.682105748629));
#64220=CARTESIAN_POINT('Ctrl Pts',(31.3563025201375,-0.508332334554018,
135.698191217127));
#64221=CARTESIAN_POINT('Ctrl Pts',(31.3485544521345,-0.371623443534293,
135.708550568895));
#64222=CARTESIAN_POINT('Ctrl Pts',(31.3407981493926,-0.234769256678522,
135.718920930705));
#64223=CARTESIAN_POINT('Ctrl Pts',(31.3330418466508,-0.0975531413946325,
135.723552989186));
#64224=CARTESIAN_POINT('Ctrl Pts',(31.3252855439089,0.0395086314126486,
135.722451927266));
#64225=CARTESIAN_POINT('Ctrl Pts',(31.3175251013948,0.176643558214927,135.721350277675));
#64226=CARTESIAN_POINT('Ctrl Pts',(31.3097646588806,0.313623588109476,135.714509429987));
#64227=CARTESIAN_POINT('Ctrl Pts',(31.3020042163665,0.449936577395924,135.70198658724));
#64228=CARTESIAN_POINT('Ctrl Pts',(31.294231316101,0.586468388394074,135.689443641713));
#64229=CARTESIAN_POINT('Ctrl Pts',(31.2864584158357,0.722330631288314,135.671200526038));
#64230=CARTESIAN_POINT('Ctrl Pts',(31.2786855155702,0.85701948082588,135.647365952271));
#64231=CARTESIAN_POINT('Ctrl Pts',(31.2711951798082,0.98681205142256,135.624397825296));
#64232=CARTESIAN_POINT('Ctrl Pts',(31.2637048440461,1.11551475823591,135.596237775329));
#64233=CARTESIAN_POINT('Ctrl Pts',(31.256214508284,1.24269111504239,135.56302659188));
#64234=CARTESIAN_POINT('Ctrl Pts',(31.2484401741649,1.37468940207106,135.528556196316));
#64235=CARTESIAN_POINT('Ctrl Pts',(31.2406658400458,1.50546144206318,135.488534886884));
#64236=CARTESIAN_POINT('Ctrl Pts',(31.2328915059268,1.63450468114292,135.443064909696));
#64237=CARTESIAN_POINT('Ctrl Pts',(31.2251267529797,1.76338888596324,135.397650970191));
#64238=CARTESIAN_POINT('Ctrl Pts',(31.2173620000326,1.89054816391202,135.346801852455));
#64239=CARTESIAN_POINT('Ctrl Pts',(31.2095972470856,2.01549187615683,135.290670410664));
#64240=CARTESIAN_POINT('Ctrl Pts',(31.2018402062006,2.14031149254523,135.234594719412));
#64241=CARTESIAN_POINT('Ctrl Pts',(31.1940831653156,2.26291956806447,135.173247304016));
#64242=CARTESIAN_POINT('Ctrl Pts',(31.1863261244306,2.38284265781293,135.106830132927));
#64243=CARTESIAN_POINT('Ctrl Pts',(31.1785749331905,2.50267531262654,135.040463047542));
#64244=CARTESIAN_POINT('Ctrl Pts',(31.1708237419504,2.61982667121735,134.96903400485));
#64245=CARTESIAN_POINT('Ctrl Pts',(31.1630725507103,2.73384557107229,134.892792035118));
#64246=CARTESIAN_POINT('Ctrl Pts',(31.1553246539332,2.84781600985339,134.816582470257));
#64247=CARTESIAN_POINT('Ctrl Pts',(31.1475767571561,2.95865631358876,134.73556426381));
#64248=CARTESIAN_POINT('Ctrl Pts',(31.139828860379,3.06594232765335,134.650031002038));
#64249=CARTESIAN_POINT('Ctrl Pts',(31.1320825842949,3.17320589979662,134.56451563198));
#64250=CARTESIAN_POINT('Ctrl Pts',(31.1243363082109,3.27691635558389,134.474487328729));
#64251=CARTESIAN_POINT('Ctrl Pts',(31.1165900321268,3.37668112858294,134.380281144979));
#64252=CARTESIAN_POINT('Ctrl Pts',(31.1088436988615,3.47644663802261,134.28607426582));
#64253=CARTESIAN_POINT('Ctrl Pts',(31.1010973655961,3.57226612229523,134.187689713043));
#64254=CARTESIAN_POINT('Ctrl Pts',(31.0933510323308,3.6637828201612,134.085500436164));
#64255=CARTESIAN_POINT('Ctrl Pts',(31.0856029643278,3.75532001255724,133.983288274706));
#64256=CARTESIAN_POINT('Ctrl Pts',(31.0778548963249,3.8425522403587,133.87726998487));
#64257=CARTESIAN_POINT('Ctrl Pts',(31.0701068283219,3.92516235128952,133.767852405731));
#64258=CARTESIAN_POINT('Ctrl Pts',(31.0623505255801,4.00786026122942,133.658318536286));
#64259=CARTESIAN_POINT('Ctrl Pts',(31.0545942228383,4.08592600521726,133.545378473088));
#64260=CARTESIAN_POINT('Ctrl Pts',(31.0468379200964,4.15908488676225,133.429469370971));
#64261=CARTESIAN_POINT('Ctrl Pts',(31.0390774775823,4.2322828154051,133.313498404677));
#64262=CARTESIAN_POINT('Ctrl Pts',(31.031317035068,4.30056846858348,133.194555580778));
#64263=CARTESIAN_POINT('Ctrl Pts',(31.0235565925539,4.36371314665402,133.073102699914));
#64264=CARTESIAN_POINT('Ctrl Pts',(31.0157836922884,4.42695919016753,132.951454852104));
#64265=CARTESIAN_POINT('Ctrl Pts',(31.0080107920231,4.48504760118261,132.827289249704));
#64266=CARTESIAN_POINT('Ctrl Pts',(31.0002378917576,4.53779751237551,132.701088536688));
#64267=CARTESIAN_POINT('Ctrl Pts',(30.9927475559955,4.5886298314284,132.57947553747));
#64268=CARTESIAN_POINT('Ctrl Pts',(30.9852572202334,4.63450494062869,132.455973110321));
#64269=CARTESIAN_POINT('Ctrl Pts',(30.9777668844712,4.67530535871284,132.331024583634));
#64270=CARTESIAN_POINT('Ctrl Pts',(30.9699925503521,4.717652737049,132.201338595582));
#64271=CARTESIAN_POINT('Ctrl Pts',(30.962218216233,4.7546671578616,132.069683879357));
#64272=CARTESIAN_POINT('Ctrl Pts',(30.9544438821139,4.78616300105551,131.936538514289));
#64273=CARTESIAN_POINT('Ctrl Pts',(30.9466791291668,4.81762002843762,131.803557238983));
#64274=CARTESIAN_POINT('Ctrl Pts',(30.9389143762197,4.84357192133382,131.669089346911));
#64275=CARTESIAN_POINT('Ctrl Pts',(30.9311496232725,4.86388207801844,131.533630247834));
#64276=CARTESIAN_POINT('Ctrl Pts',(30.9233925823875,4.88417206236906,131.398305688644));
#64277=CARTESIAN_POINT('Ctrl Pts',(30.9156355415026,4.89883140403384,131.261992265753));
#64278=CARTESIAN_POINT('Ctrl Pts',(30.9078785006176,4.90777411625741,131.125197470645));
#64279=CARTESIAN_POINT('Ctrl Pts',(30.9001273093775,4.91671008471207,130.988505833557));
#64280=CARTESIAN_POINT('Ctrl Pts',(30.8923761181374,4.91993797901853,130.85133393535));
#64281=CARTESIAN_POINT('Ctrl Pts',(30.8846249268973,4.91742345103647,130.714195958766));
#64282=CARTESIAN_POINT('Ctrl Pts',(30.8768770301202,4.91490999179586,130.577116269479));
#64283=CARTESIAN_POINT('Ctrl Pts',(30.8691291333431,4.90665897175083,130.440070863221));
#64284=CARTESIAN_POINT('Ctrl Pts',(30.861381236566,4.89268812740213,130.303575283837));
#64285=CARTESIAN_POINT('Ctrl Pts',(30.8536349604819,4.87872020545289,130.167108256385));
#64286=CARTESIAN_POINT('Ctrl Pts',(30.8458886843978,4.85903487881592,130.031191215728));
#64287=CARTESIAN_POINT('Ctrl Pts',(30.8381424083137,4.83370184506461,129.896335543287));
#64288=CARTESIAN_POINT('Ctrl Pts',(30.8303960750483,4.80836862431053,129.761478875372));
#64289=CARTESIAN_POINT('Ctrl Pts',(30.822649741783,4.77738768543392,129.627683975552));
#64290=CARTESIAN_POINT('Ctrl Pts',(30.8149034085176,4.74087996326124,129.495452585484));
#64291=CARTESIAN_POINT('Ctrl Pts',(30.8071553405146,4.70436406543749,129.363191583114));
#64292=CARTESIAN_POINT('Ctrl Pts',(30.7994072725117,4.66231902549706,129.232495164023));
#64293=CARTESIAN_POINT('Ctrl Pts',(30.7916592045087,4.614915700122,129.103850063859));
#64294=CARTESIAN_POINT('Ctrl Pts',(30.7839029017669,4.5674619939285,128.975068238152));
#64295=CARTESIAN_POINT('Ctrl Pts',(30.7761465990249,4.51463876161879,128.848342453926));
#64296=CARTESIAN_POINT('Ctrl Pts',(30.7683902962831,4.45666531377142,128.724140113983));
#64297=CARTESIAN_POINT('Ctrl Pts',(30.7606298537689,4.3986609237493,128.599871483512));
#64298=CARTESIAN_POINT('Ctrl Pts',(30.7528694112547,4.3355010208798,128.478129327885));
#64299=CARTESIAN_POINT('Ctrl Pts',(30.7451089687405,4.26745051337621,128.359355673116));
#64300=CARTESIAN_POINT('Ctrl Pts',(30.7373360684751,4.19929076515675,128.240391352332));
#64301=CARTESIAN_POINT('Ctrl Pts',(30.7295631682096,4.12622493234602,128.124405385984));
#64302=CARTESIAN_POINT('Ctrl Pts',(30.7217902679442,4.04856131378395,128.011810823734));
#64303=CARTESIAN_POINT('Ctrl Pts',(30.7142999321822,3.9737209633802,127.903309357431));
#64304=CARTESIAN_POINT('Ctrl Pts',(30.7068095964203,3.8946114907362,127.797957250225));
#64305=CARTESIAN_POINT('Ctrl Pts',(30.6993192606583,3.81154237909028,127.696092972253));
#64306=CARTESIAN_POINT('Ctrl Pts',(30.6915449265392,3.72532367682728,127.590366479221));
#64307=CARTESIAN_POINT('Ctrl Pts',(30.6837705924202,3.63456603398841,127.488062608723));
#64308=CARTESIAN_POINT('Ctrl Pts',(30.6759962583011,3.53957134005861,127.38959594176));
#64309=CARTESIAN_POINT('Ctrl Pts',(30.668231505354,3.44469371859928,127.291250626163));
#64310=CARTESIAN_POINT('Ctrl Pts',(30.6604667524068,3.34558970469151,127.196733383448));
#64311=CARTESIAN_POINT('Ctrl Pts',(30.6527019994597,3.24260226402893,127.106426921593));
#64312=CARTESIAN_POINT('Ctrl Pts',(30.6449449585747,3.13971711194414,127.016210153388));
#64313=CARTESIAN_POINT('Ctrl Pts',(30.6371879176898,3.03295650091295,126.930196099358));
#64314=CARTESIAN_POINT('Ctrl Pts',(30.6294308768048,2.92270091995374,126.848731414139));
#64315=CARTESIAN_POINT('Ctrl Pts',(30.6216796855647,2.8125284835864,126.767328162074));
#64316=CARTESIAN_POINT('Ctrl Pts',(30.6139284943246,2.69886663643271,126.690467681584));
#64317=CARTESIAN_POINT('Ctrl Pts',(30.6061773030845,2.58212940898807,126.618456799065));
#64318=CARTESIAN_POINT('Ctrl Pts',(30.5984294063074,2.46544179797868,126.546476523092));
#64319=CARTESIAN_POINT('Ctrl Pts',(30.5906815095303,2.34568173849001,126.479341950335));
#64320=CARTESIAN_POINT('Ctrl Pts',(30.5829336127532,2.22329255917093,126.417316822613));
#64321=CARTESIAN_POINT('Ctrl Pts',(30.5751873366691,2.1009289810296,126.355304669211));
#64322=CARTESIAN_POINT('Ctrl Pts',(30.5674410605851,1.97593772546609,126.298400011594));
#64323=CARTESIAN_POINT('Ctrl Pts',(30.5596947845009,1.84878670539437,126.246820625371));
#64324=CARTESIAN_POINT('Ctrl Pts',(30.5519484512356,1.72163474672271,126.1952408584));
#64325=CARTESIAN_POINT('Ctrl Pts',(30.5442021179702,1.59232335402133,126.148986588228));
#64326=CARTESIAN_POINT('Ctrl Pts',(30.5364557847048,1.46134002498524,126.108227272581));
#64327=CARTESIAN_POINT('Ctrl Pts',(30.5287077167018,1.33032736314044,126.067458829169));
#64328=CARTESIAN_POINT('Ctrl Pts',(30.5209596486988,1.19764239314845,126.032187905091));
#64329=CARTESIAN_POINT('Ctrl Pts',(30.5132115806958,1.06378697170545,126.002533846291));
#64330=CARTESIAN_POINT('Ctrl Pts',(30.505455277954,0.9297892871282,125.972848270805));
#64331=CARTESIAN_POINT('Ctrl Pts',(30.4976989752121,0.794619048455475,125.948791570355));
#64332=CARTESIAN_POINT('Ctrl Pts',(30.4899426724703,0.658788037627371,125.930431875373));
#64333=CARTESIAN_POINT('Ctrl Pts',(30.4821822299561,0.522884529698626,125.912062381268));
#64334=CARTESIAN_POINT('Ctrl Pts',(30.4744217874419,0.386319935985556,125.8993959875));
#64335=CARTESIAN_POINT('Ctrl Pts',(30.4666613449278,0.249609334851573,125.892448745143));
#64336=CARTESIAN_POINT('Ctrl Pts',(30.4588884446623,0.112679273724425,125.885490350455));
#64337=CARTESIAN_POINT('Ctrl Pts',(30.4511155443969,-0.0243968720229893,
125.884269457005));
#64338=CARTESIAN_POINT('Ctrl Pts',(30.4433426441315,-0.161104948959712,
125.888749947678));
#64339=CARTESIAN_POINT('Ctrl Pts',(30.4358523083695,-0.292843342953098,
125.893067561229));
#64340=CARTESIAN_POINT('Ctrl Pts',(30.4283619726074,-0.424239656794046,
125.902679213748));
#64341=CARTESIAN_POINT('Ctrl Pts',(30.4208716368454,-0.554841842719261,
125.917507479598));
#64342=CARTESIAN_POINT('Ctrl Pts',(30.4130973027263,-0.690395850219506,
125.932897963655));
#64343=CARTESIAN_POINT('Ctrl Pts',(30.4053229686072,-0.825523716698272,
125.953957198051));
#64344=CARTESIAN_POINT('Ctrl Pts',(30.3975486344881,-0.959713464779091,
125.980655285767));
#64345=CARTESIAN_POINT('Ctrl Pts',(30.389783881541,-1.09373783598828,126.007320470477));
#64346=CARTESIAN_POINT('Ctrl Pts',(30.3820191285939,-1.22682600941911,126.03961060575));
#64347=CARTESIAN_POINT('Ctrl Pts',(30.3742543756468,-1.35847062067631,126.077444007845));
#64348=CARTESIAN_POINT('Ctrl Pts',(30.3664973347618,-1.48998448064956,126.115239833271));
#64349=CARTESIAN_POINT('Ctrl Pts',(30.3587402938768,-1.62005725838474,126.158567861736));
#64350=CARTESIAN_POINT('Ctrl Pts',(30.3509832529918,-1.74819163990967,126.207295352351));
#64351=CARTESIAN_POINT('Ctrl Pts',(30.3432320617517,-1.87622939430109,126.255986097186));
#64352=CARTESIAN_POINT('Ctrl Pts',(30.3354808705116,-2.00233129807149,126.310068061141));
#64353=CARTESIAN_POINT('Ctrl Pts',(30.3277296792714,-2.12601541588856,126.369358755796));
#64354=CARTESIAN_POINT('Ctrl Pts',(30.3199817824944,-2.24964696465584,126.428624250324));
#64355=CARTESIAN_POINT('Ctrl Pts',(30.3122338857172,-2.37086241952226,126.493093903724));
#64356=CARTESIAN_POINT('Ctrl Pts',(30.3044859889402,-2.48920025706133,126.562537289945));
#64357=CARTESIAN_POINT('Ctrl Pts',(30.2967397128561,-2.60751334087601,126.631966150107));
#64358=CARTESIAN_POINT('Ctrl Pts',(30.288993436772,-2.72294966766552,126.706366475934));
#64359=CARTESIAN_POINT('Ctrl Pts',(30.2812471606879,-2.83507309828441,126.785462312074));
#64360=CARTESIAN_POINT('Ctrl Pts',(30.2735008274225,-2.94719735657299,126.864558732082));
#64361=CARTESIAN_POINT('Ctrl Pts',(30.2657544941571,-3.05600835041942,126.948350506199));
#64362=CARTESIAN_POINT('Ctrl Pts',(30.2580081608918,-3.16110000582624,127.036519084849));
#64363=CARTESIAN_POINT('Ctrl Pts',(30.2502600928888,-3.26621519578077,127.124707408241));
#64364=CARTESIAN_POINT('Ctrl Pts',(30.2425120248858,-3.36760909042246,127.217274235325));
#64365=CARTESIAN_POINT('Ctrl Pts',(30.2347639568828,-3.46491001482774,127.313861849246));
#64366=CARTESIAN_POINT('Ctrl Pts',(30.227007654141,-3.56231435181325,127.410552117631));
#64367=CARTESIAN_POINT('Ctrl Pts',(30.2192513513991,-3.65561675094221,127.511271433436));
#64368=CARTESIAN_POINT('Ctrl Pts',(30.2114950486572,-3.74448326151398,127.615626046182));
#64369=CARTESIAN_POINT('Ctrl Pts',(30.203734606143,-3.83339720281852,127.720036356127));
#64370=CARTESIAN_POINT('Ctrl Pts',(30.1959741636288,-3.91787029730434,127.828085521302));
#64371=CARTESIAN_POINT('Ctrl Pts',(30.1882137211146,-3.99761062831091,127.939348867692));
#64372=CARTESIAN_POINT('Ctrl Pts',(30.1804408208492,-4.07747896557551,128.050790823882));
#64373=CARTESIAN_POINT('Ctrl Pts',(30.1726679205837,-4.15259914285998,128.165456944766));
#64374=CARTESIAN_POINT('Ctrl Pts',(30.1648950203183,-4.22272363402761,128.282895136318));
#64375=CARTESIAN_POINT('Ctrl Pts',(30.1574046845564,-4.29029892330751,128.396064153797));
#64376=CARTESIAN_POINT('Ctrl Pts',(30.1499143487945,-4.35323528499088,128.51180692693));
#64377=CARTESIAN_POINT('Ctrl Pts',(30.1424240130325,-4.41135351660019,128.629701284687));
#64378=CARTESIAN_POINT('Ctrl Pts',(30.1340770920882,-4.47611807457019,128.761077889855));
#64379=CARTESIAN_POINT('Ctrl Pts',(30.1257301711438,-4.53508181396193,128.895495486326));
#64380=CARTESIAN_POINT('Ctrl Pts',(30.1173832501995,-4.58797003398941,129.03243679592));
#64381=CARTESIAN_POINT('Ctrl Pts',(30.1090570204088,-4.64072714959,129.169038642173));
#64382=CARTESIAN_POINT('Ctrl Pts',(30.100730790618,-4.68743866908584,129.308151446056));
#64383=CARTESIAN_POINT('Ctrl Pts',(30.0924045608273,-4.72787693153724,129.449235980222));
#64384=CARTESIAN_POINT('Ctrl Pts',(30.0897942804491,-4.74055436245833,129.493466106035));
#64385=CARTESIAN_POINT('Ctrl Pts',(30.087184000071,-4.75261558259996,129.537889843891));
#64386=CARTESIAN_POINT('Ctrl Pts',(30.0845737196928,-4.764054528234,129.582490119308));
#64387=CARTESIAN_POINT('Ctrl Pts',(31.8348922615591,-4.76405452823408,129.582490119308));
#64388=CARTESIAN_POINT('Ctrl Pts',(31.8276314263427,-4.79579485422486,129.70624516862));
#64389=CARTESIAN_POINT('Ctrl Pts',(31.8203705911263,-4.82267033838414,129.83108358097));
#64390=CARTESIAN_POINT('Ctrl Pts',(31.8131097559098,-4.84463298162091,129.95659040348));
#64391=CARTESIAN_POINT('Ctrl Pts',(31.8010364482278,-4.88115243722137,130.165282990379));
#64392=CARTESIAN_POINT('Ctrl Pts',(31.7889631405457,-4.90419455431079,130.376398608338));
#64393=CARTESIAN_POINT('Ctrl Pts',(31.7768898328637,-4.91351263397855,130.588544357212));
#64394=CARTESIAN_POINT('Ctrl Pts',(31.7728797005729,-4.91660762113103,130.659008271519));
#64395=CARTESIAN_POINT('Ctrl Pts',(31.7688695682821,-4.91818885296885,130.729585588476));
#64396=CARTESIAN_POINT('Ctrl Pts',(31.7648594359912,-4.91824826067786,130.800224334311));
#64397=CARTESIAN_POINT('',(32.1101405640431,-4.91824869043815,130.80794969871));
#64398=CARTESIAN_POINT('Ctrl Pts',(32.1802676473795,-4.76405452823406,129.582490119308));
#64399=CARTESIAN_POINT('Ctrl Pts',(32.1726250379345,-4.79767566864033,129.71357843548));
#64400=CARTESIAN_POINT('Ctrl Pts',(32.1649824284896,-4.82586285442501,129.845980649058));
#64401=CARTESIAN_POINT('Ctrl Pts',(32.1573398190446,-4.84853511858555,129.979199865747));
#64402=CARTESIAN_POINT('Ctrl Pts',(32.1494732765444,-4.87187169372778,130.116322485643));
#64403=CARTESIAN_POINT('Ctrl Pts',(32.1416067340441,-4.88936513831279,130.254310262019));
#64404=CARTESIAN_POINT('Ctrl Pts',(32.1337401915439,-4.90098462731627,130.392617074436));
#64405=CARTESIAN_POINT('Ctrl Pts',(32.1258736490436,-4.91260411631975,130.530923886852));
#64406=CARTESIAN_POINT('Ctrl Pts',(32.1180071065434,-4.91834968784368,130.669549273215));
#64407=CARTESIAN_POINT('Ctrl Pts',(32.1101405640432,-4.91824869043815,130.80794969871));
#64408=CARTESIAN_POINT('Ctrl Pts',(32.1101405640087,-4.9182486904377,130.807949699317));
#64409=CARTESIAN_POINT('Ctrl Pts',(32.0974165038603,-4.91808532803547,131.031811114739));
#64410=CARTESIAN_POINT('Ctrl Pts',(32.0846924437118,-4.90263711850592,131.255124154281));
#64411=CARTESIAN_POINT('Ctrl Pts',(32.0719683835633,-4.87213117064359,131.476313680319));
#64412=CARTESIAN_POINT('Ctrl Pts',(32.0641940494444,-4.85349219624961,131.611459322429));
#64413=CARTESIAN_POINT('Ctrl Pts',(32.0564197153255,-4.8291963301871,131.746042911859));
#64414=CARTESIAN_POINT('Ctrl Pts',(32.0486453812066,-4.79928574690886,131.879553336113));
#64415=CARTESIAN_POINT('Ctrl Pts',(32.0408806282597,-4.76941202575137,132.012899220702));
#64416=CARTESIAN_POINT('Ctrl Pts',(32.0331158753128,-4.73393744004321,132.145174193811));
#64417=CARTESIAN_POINT('Ctrl Pts',(32.0253511223659,-4.69295582534925,132.275872997337));
#64418=CARTESIAN_POINT('Ctrl Pts',(32.0175940814811,-4.65201491417275,132.40644198897));
#64419=CARTESIAN_POINT('Ctrl Pts',(32.0098370405962,-4.60557797509594,132.535437555741));
#64420=CARTESIAN_POINT('Ctrl Pts',(32.0020799997114,-4.55378964494523,132.662365712309));
#64421=CARTESIAN_POINT('Ctrl Pts',(31.9943288084715,-4.50204036877727,132.789198151366));
#64422=CARTESIAN_POINT('Ctrl Pts',(31.9865776172316,-4.44494788110479,132.913965922886));
#64423=CARTESIAN_POINT('Ctrl Pts',(31.9788264259917,-4.38270618291501,133.036191609541));
#64424=CARTESIAN_POINT('Ctrl Pts',(31.9710785292148,-4.32049093910715,133.158365347018));
#64425=CARTESIAN_POINT('Ctrl Pts',(31.9633306324379,-4.25313101468764,133.277998800907));
#64426=CARTESIAN_POINT('Ctrl Pts',(31.955582735661,-4.18086784464108,133.394636110278));
#64427=CARTESIAN_POINT('Ctrl Pts',(31.9478364595771,-4.10861979049199,133.511249021638));
#64428=CARTESIAN_POINT('Ctrl Pts',(31.9400901834931,-4.03147073657413,133.62486670294));
#64429=CARTESIAN_POINT('Ctrl Pts',(31.9323439074092,-3.94970702490744,133.735059762804));
#64430=CARTESIAN_POINT('Ctrl Pts',(31.924597574144,-3.8679427096796,133.845253636087));
#64431=CARTESIAN_POINT('Ctrl Pts',(31.9168512408789,-3.78156390169932,133.952022523515));
#64432=CARTESIAN_POINT('Ctrl Pts',(31.9091049076137,-3.69089880346489,134.05496811234));
#64433=CARTESIAN_POINT('Ctrl Pts',(31.901356839611,-3.60021340141046,134.157936755116));
#64434=CARTESIAN_POINT('Ctrl Pts',(31.8936087716082,-3.50524005739219,134.257080102205));
#64435=CARTESIAN_POINT('Ctrl Pts',(31.8858607036055,-3.40634530442495,134.352035169934));
#64436=CARTESIAN_POINT('Ctrl Pts',(31.8781044008638,-3.30734544493726,134.44709115704));
#64437=CARTESIAN_POINT('Ctrl Pts',(31.8703480981221,-3.20441613349485,134.537949701517));
#64438=CARTESIAN_POINT('Ctrl Pts',(31.8625917953804,-3.09795902108185,134.624286397761));
#64439=CARTESIAN_POINT('Ctrl Pts',(31.8548313528664,-2.99144508930259,134.710669174499));
#64440=CARTESIAN_POINT('Ctrl Pts',(31.8470709103525,-2.88139991827175,134.792525060781));
#64441=CARTESIAN_POINT('Ctrl Pts',(31.8393104678385,-2.76825506490569,134.869572415016));
#64442=CARTESIAN_POINT('Ctrl Pts',(31.8315375675733,-2.65492858137648,134.946743452504));
#64443=CARTESIAN_POINT('Ctrl Pts',(31.823764667308,-2.53849280438096,135.019090326302));
#64444=CARTESIAN_POINT('Ctrl Pts',(31.8159917670428,-2.41940563769781,135.086376430565));
#64445=CARTESIAN_POINT('Ctrl Pts',(31.8085014312786,-2.30464758945076,135.151216515475));
#64446=CARTESIAN_POINT('Ctrl Pts',(31.8010110955145,-2.187427848196,135.211357245643));
#64447=CARTESIAN_POINT('Ctrl Pts',(31.7935207597504,-2.06817276375785,135.266629601138));
#64448=CARTESIAN_POINT('Ctrl Pts',(31.7857464256313,-1.94439608658098,135.323997624775));
#64449=CARTESIAN_POINT('Ctrl Pts',(31.7779720915122,-1.81803459211856,135.376302542037));
#64450=CARTESIAN_POINT('Ctrl Pts',(31.770197757393,-1.6895410901089,135.423303566698));
#64451=CARTESIAN_POINT('Ctrl Pts',(31.7624330044459,-1.5612059448565,135.470246666796));
#64452=CARTESIAN_POINT('Ctrl Pts',(31.7546682514988,-1.43074438366379,135.511898747109));
#64453=CARTESIAN_POINT('Ctrl Pts',(31.7469034985517,-1.29863221489678,135.54806564981));
#64454=CARTESIAN_POINT('Ctrl Pts',(31.7391464576666,-1.16665126179825,135.584196631032));
#64455=CARTESIAN_POINT('Ctrl Pts',(31.7313894167816,-1.03302333826876,135.614853173756));
#64456=CARTESIAN_POINT('Ctrl Pts',(31.7236323758966,-0.898242227905167,
135.639889953896));
#64457=CARTESIAN_POINT('Ctrl Pts',(31.7158811846564,-0.763562757025524,
135.664907853605));
#64458=CARTESIAN_POINT('Ctrl Pts',(31.7081299934163,-0.627732213086083,
135.684314354911));
#64459=CARTESIAN_POINT('Ctrl Pts',(31.7003788021761,-0.491257123078367,
135.698014620612));
#64460=CARTESIAN_POINT('Ctrl Pts',(31.692630905399,-0.354840038624496,135.711709063334));
#64461=CARTESIAN_POINT('Ctrl Pts',(31.6848830086219,-0.21777934116214,135.719702055223));
#64462=CARTESIAN_POINT('Ctrl Pts',(31.6771351118448,-0.0805890609082852,
135.721950318401));
#64463=CARTESIAN_POINT('Ctrl Pts',(31.6693888357607,0.0565725220964206,
135.724198111292));
#64464=CARTESIAN_POINT('Ctrl Pts',(31.6616425596766,0.193863243312399,135.720703559264));
#64465=CARTESIAN_POINT('Ctrl Pts',(31.6538962835924,0.330767068754069,135.711475473439));
#64466=CARTESIAN_POINT('Ctrl Pts',(31.6461499503271,0.467671904788678,135.702247319494));
#64467=CARTESIAN_POINT('Ctrl Pts',(31.6384036170617,0.604189449270041,135.687285573593));
#64468=CARTESIAN_POINT('Ctrl Pts',(31.6306572837963,0.739807188936438,135.666651064022));
#64469=CARTESIAN_POINT('Ctrl Pts',(31.6229092157933,0.875455299255326,135.646011933496));
#64470=CARTESIAN_POINT('Ctrl Pts',(31.6151611477903,1.01020281734468,135.619697570198));
#64471=CARTESIAN_POINT('Ctrl Pts',(31.6074130797873,1.14354623471323,135.587820147192));
#64472=CARTESIAN_POINT('Ctrl Pts',(31.5996567770454,1.27703137105257,135.555908844482));
#64473=CARTESIAN_POINT('Ctrl Pts',(31.5919004743035,1.40910904479453,135.518422762286));
#64474=CARTESIAN_POINT('Ctrl Pts',(31.5841441715616,1.53928922214793,135.475524471798));
#64475=CARTESIAN_POINT('Ctrl Pts',(31.5763837290474,1.66953888058163,135.4326032852));
#64476=CARTESIAN_POINT('Ctrl Pts',(31.5686232865333,1.7978886589368,135.384264272143));
#64477=CARTESIAN_POINT('Ctrl Pts',(31.5608628440191,1.92386833711233,135.330718279523));
#64478=CARTESIAN_POINT('Ctrl Pts',(31.5530899437537,2.05005024905121,135.277086330122));
#64479=CARTESIAN_POINT('Ctrl Pts',(31.5453170434882,2.17385410451755,135.218230865757));
#64480=CARTESIAN_POINT('Ctrl Pts',(31.5375441432227,2.29483333213541,135.154409242607));
#64481=CARTESIAN_POINT('Ctrl Pts',(31.530053807461,2.41141466009582,135.092907696218));
#64482=CARTESIAN_POINT('Ctrl Pts',(31.5225634716993,2.52537289302176,135.026794941759));
#64483=CARTESIAN_POINT('Ctrl Pts',(31.5150731359376,2.63633537716449,134.956338320012));
#64484=CARTESIAN_POINT('Ctrl Pts',(31.5072988018185,2.751505037625,134.883210314034));
#64485=CARTESIAN_POINT('Ctrl Pts',(31.4995244676994,2.86381212017765,134.805170895397));
#64486=CARTESIAN_POINT('Ctrl Pts',(31.4917501335803,2.97280928982719,134.722470874924));
#64487=CARTESIAN_POINT('Ctrl Pts',(31.4839853806332,3.0816721302065,134.639872774836));
#64488=CARTESIAN_POINT('Ctrl Pts',(31.4762206276861,3.1872328655475,134.552625735359));
#64489=CARTESIAN_POINT('Ctrl Pts',(31.468455874739,3.28907095932687,134.461025120499));
#64490=CARTESIAN_POINT('Ctrl Pts',(31.4606988338539,3.39080790607584,134.369515484662));
#64491=CARTESIAN_POINT('Ctrl Pts',(31.452941792969,3.48882928041906,134.273661138227));
#64492=CARTESIAN_POINT('Ctrl Pts',(31.4451847520839,3.58274591499209,134.173798964102));
#64493=CARTESIAN_POINT('Ctrl Pts',(31.4374335608438,3.67659172630042,134.074012096819));
#64494=CARTESIAN_POINT('Ctrl Pts',(31.4296823696036,3.76633869231463,133.970223701268));
#64495=CARTESIAN_POINT('Ctrl Pts',(31.4219311783634,3.85163323359892,133.862808671128));
#64496=CARTESIAN_POINT('Ctrl Pts',(31.4141832815863,3.93689152242786,133.755439295241));
#64497=CARTESIAN_POINT('Ctrl Pts',(31.4064353848092,4.01770090774935,133.644446656061));
#64498=CARTESIAN_POINT('Ctrl Pts',(31.3986874880321,4.09374713277167,133.530239829018));
#64499=CARTESIAN_POINT('Ctrl Pts',(31.3909412119479,4.16977745056309,133.41605689158));
#64500=CARTESIAN_POINT('Ctrl Pts',(31.3831949358638,4.24104637330068,133.298661428816));
#64501=CARTESIAN_POINT('Ctrl Pts',(31.3754486597797,4.30728238505632,133.178492357357));
#64502=CARTESIAN_POINT('Ctrl Pts',(31.3677023265143,4.37351888575106,133.058322398838));
#64503=CARTESIAN_POINT('Ctrl Pts',(31.3599559932489,4.43472221260389,132.935379133167));
#64504=CARTESIAN_POINT('Ctrl Pts',(31.3522096599836,4.49066651623954,132.810126631443));
#64505=CARTESIAN_POINT('Ctrl Pts',(31.3444615919806,4.54662334821411,132.68484608029));
#64506=CARTESIAN_POINT('Ctrl Pts',(31.3367135239776,4.59731865402818,132.557255620947));
#64507=CARTESIAN_POINT('Ctrl Pts',(31.3289654559746,4.64257464941985,132.427839501649));
#64508=CARTESIAN_POINT('Ctrl Pts',(31.3212091532327,4.68787874342203,132.29828583736));
#64509=CARTESIAN_POINT('Ctrl Pts',(31.3134528504908,4.72773184964324,132.166903006731));
#64510=CARTESIAN_POINT('Ctrl Pts',(31.3056965477489,4.76200586859986,132.034191162772));
#64511=CARTESIAN_POINT('Ctrl Pts',(31.2979361052347,4.79629818063242,131.901408486505));
#64512=CARTESIAN_POINT('Ctrl Pts',(31.2901756627205,4.82500539023408,131.767295765616));
#64513=CARTESIAN_POINT('Ctrl Pts',(31.2824152202063,4.84805072342043,131.632362577493));
#64514=CARTESIAN_POINT('Ctrl Pts',(31.2746423199408,4.87113305102145,131.497212782637));
#64515=CARTESIAN_POINT('Ctrl Pts',(31.2668694196754,4.88853528993475,131.361240276612));
#64516=CARTESIAN_POINT('Ctrl Pts',(31.25909651941,4.90023257846541,131.224959879865));
#64517=CARTESIAN_POINT('Ctrl Pts',(31.2516061836482,4.91150464109385,131.093633618814));
#64518=CARTESIAN_POINT('Ctrl Pts',(31.2441158478864,4.91747931683862,130.962021771309));
#64519=CARTESIAN_POINT('Ctrl Pts',(31.2366255121246,4.9181800986161,130.830582365726));
#64520=CARTESIAN_POINT('Ctrl Pts',(31.2288511780056,4.91890745074769,130.694159395125));
#64521=CARTESIAN_POINT('Ctrl Pts',(31.2210768438865,4.91395539903072,130.557490053881));
#64522=CARTESIAN_POINT('Ctrl Pts',(31.2133025097675,4.90329316222011,130.421086266969));
#64523=CARTESIAN_POINT('Ctrl Pts',(31.2055377568204,4.89264406566346,130.284850585534));
#64524=CARTESIAN_POINT('Ctrl Pts',(31.1977730038733,4.87629881630337,130.148880193293));
#64525=CARTESIAN_POINT('Ctrl Pts',(31.1900082509262,4.8542786019798,130.013688550992));
#64526=CARTESIAN_POINT('Ctrl Pts',(31.1822512100413,4.83228025844352,129.878631182935));
#64527=CARTESIAN_POINT('Ctrl Pts',(31.1744941691563,4.80461822918996,129.744351408971));
#64528=CARTESIAN_POINT('Ctrl Pts',(31.1667371282713,4.77136558888309,129.611358740064));
#64529=CARTESIAN_POINT('Ctrl Pts',(31.1589859370312,4.73813802465096,129.478466361964));
#64530=CARTESIAN_POINT('Ctrl Pts',(31.1512347457912,4.69932833535641,129.346859534723));
#64531=CARTESIAN_POINT('Ctrl Pts',(31.1434835545511,4.65506081134759,129.217038373926));
#64532=CARTESIAN_POINT('Ctrl Pts',(31.135735657774,4.61081210221734,129.087272390585));
#64533=CARTESIAN_POINT('Ctrl Pts',(31.1279877609969,4.5611102980461,128.959290933451));
#64534=CARTESIAN_POINT('Ctrl Pts',(31.1202398642199,4.50612970210671,128.833579510925));
#64535=CARTESIAN_POINT('Ctrl Pts',(31.1124935881358,4.45116060692274,128.70789438452));
#64536=CARTESIAN_POINT('Ctrl Pts',(31.1047473120517,4.39091507286729,128.584478706212));
#64537=CARTESIAN_POINT('Ctrl Pts',(31.0970010359676,4.32561561194335,128.463798155205));
#64538=CARTESIAN_POINT('Ctrl Pts',(31.0892547027023,4.26031566899363,128.343116713362));
#64539=CARTESIAN_POINT('Ctrl Pts',(31.081508369437,4.18996191078986,128.225170782961));
#64540=CARTESIAN_POINT('Ctrl Pts',(31.0737620361716,4.11482269638577,128.110401219244));
#64541=CARTESIAN_POINT('Ctrl Pts',(31.0660139681687,4.0396666550756,127.995605953678));
#64542=CARTESIAN_POINT('Ctrl Pts',(31.0582659001658,3.95972323917565,127.883988797286));
#64543=CARTESIAN_POINT('Ctrl Pts',(31.0505178321628,3.87530376370483,127.775961073002));
#64544=CARTESIAN_POINT('Ctrl Pts',(31.042761529421,3.79079456621087,127.667818535567));
#64545=CARTESIAN_POINT('Ctrl Pts',(31.0350052266791,3.70180004722754,127.563273359446));
#64546=CARTESIAN_POINT('Ctrl Pts',(31.0272489239373,3.60867175874623,127.46270366328));
#64547=CARTESIAN_POINT('Ctrl Pts',(31.0194884814232,3.51549376489332,127.362080290039));
#64548=CARTESIAN_POINT('Ctrl Pts',(31.011728038909,3.41817788254379,127.265436900046));
#64549=CARTESIAN_POINT('Ctrl Pts',(31.0039675963948,3.31711133537094,127.173113524451));
#64550=CARTESIAN_POINT('Ctrl Pts',(30.9961946961294,3.21588254720417,127.080641943178));
#64551=CARTESIAN_POINT('Ctrl Pts',(30.9884217958641,3.11089136215078,126.992504485904));
#64552=CARTESIAN_POINT('Ctrl Pts',(30.9806488955987,3.00255747487995,126.909000342503));
#64553=CARTESIAN_POINT('Ctrl Pts',(30.9731585598364,2.89816179728389,126.828531785045));
#64554=CARTESIAN_POINT('Ctrl Pts',(30.965668224074,2.7906624807089,126.752365702749));
#64555=CARTESIAN_POINT('Ctrl Pts',(30.9581778883117,2.68045757589407,126.680729905883));
#64556=CARTESIAN_POINT('Ctrl Pts',(30.9504035541926,2.56607421862117,126.606378016009));
#64557=CARTESIAN_POINT('Ctrl Pts',(30.9426292200736,2.44841372624144,126.536671200091));
#64558=CARTESIAN_POINT('Ctrl Pts',(30.9348548859545,2.32789015772045,126.471912063216));
#64559=CARTESIAN_POINT('Ctrl Pts',(30.9270901330074,2.20751512372633,126.40723273619));
#64560=CARTESIAN_POINT('Ctrl Pts',(30.9193253800602,2.08428437531739,126.34748913913));
#64561=CARTESIAN_POINT('Ctrl Pts',(30.9115606271131,1.95864135410702,126.292940984182));
#64562=CARTESIAN_POINT('Ctrl Pts',(30.9038035862281,1.83312312331657,126.238447007231));
#64563=CARTESIAN_POINT('Ctrl Pts',(30.8960465453431,1.70519774398497,126.189138358077));
#64564=CARTESIAN_POINT('Ctrl Pts',(30.8882895044581,1.57533338075835,126.145228960061));
#64565=CARTESIAN_POINT('Ctrl Pts',(30.880538313218,1.44556694925841,126.101352674463));
#64566=CARTESIAN_POINT('Ctrl Pts',(30.8727871219779,1.3138648131581,126.062867660414));
#64567=CARTESIAN_POINT('Ctrl Pts',(30.8650359307378,1.18071491583145,126.029939673616));
#64568=CARTESIAN_POINT('Ctrl Pts',(30.8572880339607,1.04762161076286,125.997025682089));
#64569=CARTESIAN_POINT('Ctrl Pts',(30.8495401371836,0.913082147063845,125.969664113865));
#64570=CARTESIAN_POINT('Ctrl Pts',(30.8417922404065,0.777599211879236,125.947970751813));
#64571=CARTESIAN_POINT('Ctrl Pts',(30.8340459643224,0.642144616803992,125.926281927545));
#64572=CARTESIAN_POINT('Ctrl Pts',(30.8262996882383,0.505747328594069,125.910259012868));
#64573=CARTESIAN_POINT('Ctrl Pts',(30.8185534121542,0.368919409523134,125.899966513115));
#64574=CARTESIAN_POINT('Ctrl Pts',(30.8108070788889,0.232090480419583,125.889673937385));
#64575=CARTESIAN_POINT('Ctrl Pts',(30.8030607456235,0.0948313039756817,
125.885111890313));
#64576=CARTESIAN_POINT('Ctrl Pts',(30.7953144123581,-0.0423421611861836,
125.886292886852));
#64577=CARTESIAN_POINT('Ctrl Pts',(30.7875663443551,-0.179546345394478,
125.887474147868));
#64578=CARTESIAN_POINT('Ctrl Pts',(30.7798182763522,-0.316664389250117,
125.89440100835));
#64579=CARTESIAN_POINT('Ctrl Pts',(30.7720702083492,-0.453181961747182,
125.907033880248));
#64580=CARTESIAN_POINT('Ctrl Pts',(30.7643139056073,-0.589844626744877,
125.919680178513));
#64581=CARTESIAN_POINT('Ctrl Pts',(30.7565576028654,-0.7259051556118,125.938044566439));
#64582=CARTESIAN_POINT('Ctrl Pts',(30.7488013001236,-0.860855403987377,
125.96203565574));
#64583=CARTESIAN_POINT('Ctrl Pts',(30.7410408576094,-0.99587767937397,125.986039549807));
#64584=CARTESIAN_POINT('Ctrl Pts',(30.7332804150953,-1.12978811194168,126.01567604482));
#64585=CARTESIAN_POINT('Ctrl Pts',(30.7255199725811,-1.2620913199983,126.050803153678));
#64586=CARTESIAN_POINT('Ctrl Pts',(30.7177470723156,-1.39460691290965,126.085986651689));
#64587=CARTESIAN_POINT('Ctrl Pts',(30.7099741720502,-1.52550975197105,126.126678260646));
#64588=CARTESIAN_POINT('Ctrl Pts',(30.7022012717848,-1.65432126504699,126.172686598973));
#64589=CARTESIAN_POINT('Ctrl Pts',(30.6947109360228,-1.77845015516478,126.217022418312));
#64590=CARTESIAN_POINT('Ctrl Pts',(30.6872206002609,-1.90063684375572,126.266295009943));
#64591=CARTESIAN_POINT('Ctrl Pts',(30.6797302644989,-2.02047451144142,126.320292619518));
#64592=CARTESIAN_POINT('Ctrl Pts',(30.6719553683487,-2.14486485264301,126.37634161654));
#64593=CARTESIAN_POINT('Ctrl Pts',(30.6641804721984,-2.26711822400421,126.43765929837));
#64594=CARTESIAN_POINT('Ctrl Pts',(30.6564055760482,-2.38675612313621,126.504060829043));
#64595=CARTESIAN_POINT('Ctrl Pts',(30.6486403882002,-2.50624463366379,126.570379445923));
#64596=CARTESIAN_POINT('Ctrl Pts',(30.6408752003522,-2.62312383178251,126.641769092157));
#64597=CARTESIAN_POINT('Ctrl Pts',(30.6331100125042,-2.73693544843405,126.717997024638));
#64598=CARTESIAN_POINT('Ctrl Pts',(30.6253526633053,-2.85063217677376,126.794148008046));
#64599=CARTESIAN_POINT('Ctrl Pts',(30.6175953141063,-2.96126716367557,126.875127341253));
#64600=CARTESIAN_POINT('Ctrl Pts',(30.6098379649074,-3.0684073272435,126.960656735031));
#64601=CARTESIAN_POINT('Ctrl Pts',(30.6020870037687,-3.17545926250074,127.046115696641));
#64602=CARTESIAN_POINT('Ctrl Pts',(30.5943360426299,-3.27902180075424,127.136117014887));
#64603=CARTESIAN_POINT('Ctrl Pts',(30.5865850814912,-3.37869178243243,127.23033978637));
#64604=CARTESIAN_POINT('Ctrl Pts',(30.578837600197,-3.47831701662366,127.324520255926));
#64605=CARTESIAN_POINT('Ctrl Pts',(30.5710901189027,-3.57405288770035,127.422918140061));
#64606=CARTESIAN_POINT('Ctrl Pts',(30.5633426376084,-3.66553033294913,127.525173151023));
#64607=CARTESIAN_POINT('Ctrl Pts',(30.5555969568124,-3.75698651903374,127.627404398139));
#64608=CARTESIAN_POINT('Ctrl Pts',(30.5478512760163,-3.84418598852938,127.733490696938));
#64609=CARTESIAN_POINT('Ctrl Pts',(30.5401055952202,-3.92679776726853,127.843036191321));
#64610=CARTESIAN_POINT('Ctrl Pts',(30.5323600371418,-4.00940823715925,127.952579950136));
#64611=CARTESIAN_POINT('Ctrl Pts',(30.5246144790634,-4.08743092668292,128.06558248268));
#64612=CARTESIAN_POINT('Ctrl Pts',(30.5168689209849,-4.16057650347028,128.181616592452));
#64613=CARTESIAN_POINT('Ctrl Pts',(30.5091184097264,-4.23376885586907,128.297724904475));
#64614=CARTESIAN_POINT('Ctrl Pts',(30.5013678984679,-4.30207765539265,128.416868336089));
#64615=CARTESIAN_POINT('Ctrl Pts',(30.4936173872094,-4.36525797165065,128.53859233651));
#64616=CARTESIAN_POINT('Ctrl Pts',(30.485864316519,-4.42845915178563,128.660356533541));
#64617=CARTESIAN_POINT('Ctrl Pts',(30.4781112458286,-4.48652830534811,128.784702644735));
#64618=CARTESIAN_POINT('Ctrl Pts',(30.4703581751383,-4.53926790328042,128.911154351797));
#64619=CARTESIAN_POINT('Ctrl Pts',(30.4625962548564,-4.59206769979935,129.037750394696));
#64620=CARTESIAN_POINT('Ctrl Pts',(30.4548343345745,-4.63952564950778,129.166456468992));
#64621=CARTESIAN_POINT('Ctrl Pts',(30.4470724142927,-4.68149335458289,129.296778767882));
#64622=CARTESIAN_POINT('Ctrl Pts',(30.4414468886022,-4.71190984876183,129.391231095892));
#64623=CARTESIAN_POINT('Ctrl Pts',(30.4358213629117,-4.73944348570093,129.486532037996));
#64624=CARTESIAN_POINT('Ctrl Pts',(30.4301958372212,-4.76405452823406,129.582490119308));
#64625=CARTESIAN_POINT('Origin',(213.235140564004,0.,130.804360617566));
#64626=CARTESIAN_POINT('',(28.3348598006328,-4.76405452823408,129.582490119308));
#64627=CARTESIAN_POINT('',(28.6798592372483,-4.76405452823403,129.582490119308));
#64628=CARTESIAN_POINT('',(213.235140564004,-4.76405452823405,129.582490119308));
#64629=CARTESIAN_POINT('',(30.0148594360429,-4.91824986981998,130.803229018815));
#64630=CARTESIAN_POINT('Ctrl Pts',(30.0148594359913,-4.91824986982019,130.803229019732));
#64631=CARTESIAN_POINT('Ctrl Pts',(30.006871955308,-4.91828249669703,130.945034816734));
#64632=CARTESIAN_POINT('Ctrl Pts',(29.9988844746248,-4.91217783929229,131.086768889376));
#64633=CARTESIAN_POINT('Ctrl Pts',(29.9908969939415,-4.89998063896011,131.227884879346));
#64634=CARTESIAN_POINT('Ctrl Pts',(29.9829032257318,-4.88777383732535,131.369111951964));
#64635=CARTESIAN_POINT('Ctrl Pts',(29.9749094575221,-4.86946496135127,131.509719618149));
#64636=CARTESIAN_POINT('Ctrl Pts',(29.9669156893125,-4.84515038299053,131.649168778456));
#64637=CARTESIAN_POINT('Ctrl Pts',(29.9589144275633,-4.82081301159287,131.788748661567));
#64638=CARTESIAN_POINT('Ctrl Pts',(29.9509131658141,-4.79045877355497,131.927167524177));
#64639=CARTESIAN_POINT('Ctrl Pts',(29.9429119040649,-4.75423467615063,132.063898511631));
#64640=CARTESIAN_POINT('Ctrl Pts',(29.9348961969934,-4.71794518046554,132.200876350551));
#64641=CARTESIAN_POINT('Ctrl Pts',(29.9268804899219,-4.67576474248506,132.336159882206));
#64642=CARTESIAN_POINT('Ctrl Pts',(29.9188647828504,-4.62788995883001,132.469238268164));
#64643=CARTESIAN_POINT('Ctrl Pts',(29.9108407880352,-4.57996567561917,132.602454248915));
#64644=CARTESIAN_POINT('Ctrl Pts',(29.90281679322,-4.5263354379027,132.733460208831));
#64645=CARTESIAN_POINT('Ctrl Pts',(29.8947927984047,-4.46724301163168,132.861767465403));
#64646=CARTESIAN_POINT('Ctrl Pts',(29.8867542047405,-4.40804307265357,132.990308164083));
#64647=CARTESIAN_POINT('Ctrl Pts',(29.8787156110763,-4.34336125144675,133.116140034342));
#64648=CARTESIAN_POINT('Ctrl Pts',(29.8706770174121,-4.27348655801177,133.23880012205));
#64649=CARTESIAN_POINT('Ctrl Pts',(29.8684434746813,-4.2540717051022,133.272881524682));
#64650=CARTESIAN_POINT('Ctrl Pts',(29.8662099319505,-4.2342562022846,133.306718242284));
#64651=CARTESIAN_POINT('Ctrl Pts',(29.8639763892196,-4.21404681532671,133.340300778677));
#64652=CARTESIAN_POINT('Ctrl Pts',(29.8562020551005,-4.14370362270071,133.457192143628));
#64653=CARTESIAN_POINT('Ctrl Pts',(29.8484277209815,-4.06838173780606,133.571339615384));
#64654=CARTESIAN_POINT('Ctrl Pts',(29.8406533868624,-3.9883211644295,133.682289969003));
#64655=CARTESIAN_POINT('Ctrl Pts',(29.8328886339153,-3.90835925855429,133.793103586228));
#64656=CARTESIAN_POINT('Ctrl Pts',(29.8251238809683,-3.82367051065479,133.900727611066));
#64657=CARTESIAN_POINT('Ctrl Pts',(29.8173591280212,-3.73454010796197,134.004734540176));
#64658=CARTESIAN_POINT('Ctrl Pts',(29.8096020871362,-3.64549823084174,134.108638168138));
#64659=CARTESIAN_POINT('Ctrl Pts',(29.8018450462511,-3.55202373080071,134.208931554762));
#64660=CARTESIAN_POINT('Ctrl Pts',(29.7940880053661,-3.45444405478792,134.305217560493));
#64661=CARTESIAN_POINT('Ctrl Pts',(29.786336814126,-3.35693796436774,134.401430956198));
#64662=CARTESIAN_POINT('Ctrl Pts',(29.7785856228859,-3.25533313703544,134.493642712621));
#64663=CARTESIAN_POINT('Ctrl Pts',(29.7708344316457,-3.14999587357852,134.581490355732));
#64664=CARTESIAN_POINT('Ctrl Pts',(29.7630865348687,-3.04470338126868,134.669300661251));
#64665=CARTESIAN_POINT('Ctrl Pts',(29.7553386380916,-2.9356819076587,134.752750292766));
#64666=CARTESIAN_POINT('Ctrl Pts',(29.7475907413145,-2.82333286907851,134.831515267301));
#64667=CARTESIAN_POINT('Ctrl Pts',(29.7398444652304,-2.71100733149522,134.910263765901));
#64668=CARTESIAN_POINT('Ctrl Pts',(29.7320981891463,-2.59535593335977,134.984329332361));
#64669=CARTESIAN_POINT('Ctrl Pts',(29.7243519130622,-2.4768109492746,135.053429996154));
#64670=CARTESIAN_POINT('Ctrl Pts',(29.7166055797968,-2.35826509011744,135.122531170032));
#64671=CARTESIAN_POINT('Ctrl Pts',(29.7088592465315,-2.23682594015884,135.186667171224));
#64672=CARTESIAN_POINT('Ctrl Pts',(29.7011129132662,-2.11295201709328,135.245601078964));
#64673=CARTESIAN_POINT('Ctrl Pts',(29.6933648452632,-1.98905035332137,135.304548184545));
#64674=CARTESIAN_POINT('Ctrl Pts',(29.6856167772602,-1.86271318443584,135.358290710583));
#64675=CARTESIAN_POINT('Ctrl Pts',(29.6778687092572,-1.73442035288852,135.40663930339));
#64676=CARTESIAN_POINT('Ctrl Pts',(29.6701124065154,-1.60599117019312,135.455039281656));
#64677=CARTESIAN_POINT('Ctrl Pts',(29.6623561037736,-1.47560253923632,135.498033736841));
#64678=CARTESIAN_POINT('Ctrl Pts',(29.6545998010317,-1.34375139496071,135.535482604055));
#64679=CARTESIAN_POINT('Ctrl Pts',(29.6468393585175,-1.21182987775927,135.572951458858));
#64680=CARTESIAN_POINT('Ctrl Pts',(29.6390789160033,-1.07844467189758,135.604868737004));
#64681=CARTESIAN_POINT('Ctrl Pts',(29.6313184734891,-0.944103365652468,
135.631145458168));
#64682=CARTESIAN_POINT('Ctrl Pts',(29.6235455732237,-0.809546402816311,
135.657464361057));
#64683=CARTESIAN_POINT('Ctrl Pts',(29.6157726729584,-0.674030659264654,
135.678124553783));
#64684=CARTESIAN_POINT('Ctrl Pts',(29.6079997726929,-0.538070210576818,
135.693088827539));
#64685=CARTESIAN_POINT('Ctrl Pts',(29.6005094369309,-0.407052266662118,
135.707509112252));
#64686=CARTESIAN_POINT('Ctrl Pts',(29.5930191011688,-0.275621695856512,
135.716640388885));
#64687=CARTESIAN_POINT('Ctrl Pts',(29.5855287654067,-0.144236958399345,
135.720495152171));
#64688=CARTESIAN_POINT('Ctrl Pts',(29.5777544312876,-0.00787072868834712,
135.724496069978));
#64689=CARTESIAN_POINT('Ctrl Pts',(29.5699800971686,0.128878090749471,135.72282513168));
#64690=CARTESIAN_POINT('Ctrl Pts',(29.5622057630495,0.265498461025315,135.71543928011));
#64691=CARTESIAN_POINT('Ctrl Pts',(29.5544410101024,0.401950458904537,135.708062530941));
#64692=CARTESIAN_POINT('Ctrl Pts',(29.5466762571553,0.538273935948422,135.694984903111));
#64693=CARTESIAN_POINT('Ctrl Pts',(29.5389115042083,0.673955070824333,135.676215256716));
#64694=CARTESIAN_POINT('Ctrl Pts',(29.5311544633233,0.809501445284316,135.657464252599));
#64695=CARTESIAN_POINT('Ctrl Pts',(29.5233974224382,0.944406362420823,135.633032533651));
#64696=CARTESIAN_POINT('Ctrl Pts',(29.5156403815533,1.07815870440459,135.602980926636));
#64697=CARTESIAN_POINT('Ctrl Pts',(29.5078891903131,1.21181018270755,135.572951981771));
#64698=CARTESIAN_POINT('Ctrl Pts',(29.500137999073,1.34431043596769,135.537311669681));
#64699=CARTESIAN_POINT('Ctrl Pts',(29.4923868078328,1.47515650999621,135.496172243528));
#64700=CARTESIAN_POINT('Ctrl Pts',(29.4846389110557,1.60594697095248,135.455050302729));
#64701=CARTESIAN_POINT('Ctrl Pts',(29.4768910142787,1.7350842788462,135.408434013537));
#64702=CARTESIAN_POINT('Ctrl Pts',(29.4691431175016,1.86207888229262,135.356485978166));
#64703=CARTESIAN_POINT('Ctrl Pts',(29.4613968414175,1.9890469212055,135.304548809205));
#64704=CARTESIAN_POINT('Ctrl Pts',(29.4536505653334,2.11387278554884,135.24728226036));
#64705=CARTESIAN_POINT('Ctrl Pts',(29.4459042892493,2.23608559055076,135.184897604538));
#64706=CARTESIAN_POINT('Ctrl Pts',(29.438157955984,2.3582992977,135.122512488207));
#64707=CARTESIAN_POINT('Ctrl Pts',(29.4304116227186,2.47789955879707,135.055009367264));
#64708=CARTESIAN_POINT('Ctrl Pts',(29.4226652894533,2.59443920568036,134.982645944172));
#64709=CARTESIAN_POINT('Ctrl Pts',(29.4149172214503,2.71100495080923,134.910266315793));
#64710=CARTESIAN_POINT('Ctrl Pts',(29.4071691534473,2.82450838577123,134.833024425612));
#64711=CARTESIAN_POINT('Ctrl Pts',(29.3994210854444,2.93453083538086,134.751221628382));
#64712=CARTESIAN_POINT('Ctrl Pts',(29.3916647827025,3.04467021815951,134.669331890165));
#64713=CARTESIAN_POINT('Ctrl Pts',(29.3839084799606,3.1513209109239,134.582871795368));
#64714=CARTESIAN_POINT('Ctrl Pts',(29.3761521772187,3.25409646764277,134.492183720939));
#64715=CARTESIAN_POINT('Ctrl Pts',(29.3683917347046,3.35692687877077,134.401447243555));
#64716=CARTESIAN_POINT('Ctrl Pts',(29.3606312921904,3.45587775070292,134.306478560659));
#64717=CARTESIAN_POINT('Ctrl Pts',(29.3528708496763,3.55059985790736,134.207656624605));
#64718=CARTESIAN_POINT('Ctrl Pts',(29.3450979494108,3.64547402144733,134.108676050806));
#64719=CARTESIAN_POINT('Ctrl Pts',(29.3373250491454,3.73610559626051,134.005830156573));
#64720=CARTESIAN_POINT('Ctrl Pts',(29.3295521488799,3.8221854071165,133.89953133598));
#64721=CARTESIAN_POINT('Ctrl Pts',(29.3220618131179,3.90513600002592,133.797096745266));
#64722=CARTESIAN_POINT('Ctrl Pts',(29.314571477356,3.98385983555859,133.691456161804));
#64723=CARTESIAN_POINT('Ctrl Pts',(29.3070811415939,4.05811961692932,133.583002054886));
#64724=CARTESIAN_POINT('Ctrl Pts',(29.2993068074748,4.13519498048149,133.470435877541));
#64725=CARTESIAN_POINT('Ctrl Pts',(29.2915324733557,4.20770524995025,133.354482039855));
#64726=CARTESIAN_POINT('Ctrl Pts',(29.2837581392366,4.27533797111791,133.235547219869));
#64727=CARTESIAN_POINT('Ctrl Pts',(29.2759933862895,4.34288734100114,133.116758976419));
#64728=CARTESIAN_POINT('Ctrl Pts',(29.2682286333425,4.4055709315585,132.994997397019));
#64729=CARTESIAN_POINT('Ctrl Pts',(29.2604638803954,4.46311846405882,132.870699563208));
#64730=CARTESIAN_POINT('Ctrl Pts',(29.2527068395104,4.52060883953867,132.746525183757));
#64731=CARTESIAN_POINT('Ctrl Pts',(29.2449497986254,4.57297314539408,132.619819915395));
#64732=CARTESIAN_POINT('Ctrl Pts',(29.2371927577404,4.61998628523119,132.491046654378));
#64733=CARTESIAN_POINT('Ctrl Pts',(29.2294415665002,4.66696397209396,132.362370502278));
#64734=CARTESIAN_POINT('Ctrl Pts',(29.2216903752601,4.70859839153284,132.23162982736));
#64735=CARTESIAN_POINT('Ctrl Pts',(29.2139391840199,4.74471212628655,132.099308454805));
#64736=CARTESIAN_POINT('Ctrl Pts',(29.2061912872428,4.78081051173948,131.967043322363));
#64737=CARTESIAN_POINT('Ctrl Pts',(29.1984433904658,4.81139277667065,131.833199204899));
#64738=CARTESIAN_POINT('Ctrl Pts',(29.1906954936887,4.83633110844715,131.698275866326));
#64739=CARTESIAN_POINT('Ctrl Pts',(29.1829492176046,4.86126422366228,131.563380750808));
#64740=CARTESIAN_POINT('Ctrl Pts',(29.1752029415205,4.8805556829645,131.427407247419));
#64741=CARTESIAN_POINT('Ctrl Pts',(29.1674566654364,4.89412871151387,131.290865723023));
#64742=CARTESIAN_POINT('Ctrl Pts',(29.1597103321711,4.90770184025621,131.154323190709));
#64743=CARTESIAN_POINT('Ctrl Pts',(29.1519639989057,4.91555641534079,131.017213018067));
#64744=CARTESIAN_POINT('Ctrl Pts',(29.1442176656404,4.91766754383402,130.880050714814));
#64745=CARTESIAN_POINT('Ctrl Pts',(29.1364695976374,4.91977914509984,130.742857695014));
#64746=CARTESIAN_POINT('Ctrl Pts',(29.1287215296345,4.91614473435951,130.605612912215));
#64747=CARTESIAN_POINT('Ctrl Pts',(29.1209734616315,4.90679154573585,130.468831499314));
#64748=CARTESIAN_POINT('Ctrl Pts',(29.1132171588896,4.89742841643201,130.331904713499));
#64749=CARTESIAN_POINT('Ctrl Pts',(29.1054608561478,4.8823343945294,130.195442672028));
#64750=CARTESIAN_POINT('Ctrl Pts',(29.097704553406,4.86158864793186,130.059955565998));
#64751=CARTESIAN_POINT('Ctrl Pts',(29.0899441108918,4.84083182870469,129.924396146419));
#64752=CARTESIAN_POINT('Ctrl Pts',(29.0821836683776,4.81441734942052,129.789813082584));
#64753=CARTESIAN_POINT('Ctrl Pts',(29.0744232258635,4.78247526849565,129.656705020827));
#64754=CARTESIAN_POINT('Ctrl Pts',(29.066650325598,4.7504819113068,129.523383282191));
#64755=CARTESIAN_POINT('Ctrl Pts',(29.0588774253325,4.71294332772681,129.391541653497));
#64756=CARTESIAN_POINT('Ctrl Pts',(29.0511045250671,4.67003935980689,129.261663161694));
#64757=CARTESIAN_POINT('Ctrl Pts',(29.043614189305,4.62869505918903,129.13650608021));
#64758=CARTESIAN_POINT('Ctrl Pts',(29.036123853543,4.58236880046733,129.013172172025));
#64759=CARTESIAN_POINT('Ctrl Pts',(29.0286335177809,4.53126251446374,128.892073220882));
#64760=CARTESIAN_POINT('Ctrl Pts',(29.0208591836617,4.47821851809335,128.766382766201));
#64761=CARTESIAN_POINT('Ctrl Pts',(29.0130848495427,4.41985684227472,128.6427019413));
#64762=CARTESIAN_POINT('Ctrl Pts',(29.0053105154236,4.35635074762307,128.521513442176));
#64763=CARTESIAN_POINT('Ctrl Pts',(28.9975457624765,4.29292291855755,128.400474297047));
#64764=CARTESIAN_POINT('Ctrl Pts',(28.9897810095294,4.22436346516957,128.281921709163));
#64765=CARTESIAN_POINT('Ctrl Pts',(28.9820162565823,4.15089402427952,128.166319324921));
#64766=CARTESIAN_POINT('Ctrl Pts',(28.9742592156973,4.0774975542738,128.050831758597));
#64767=CARTESIAN_POINT('Ctrl Pts',(28.9665021748123,3.99920100990512,127.938288892549));
#64768=CARTESIAN_POINT('Ctrl Pts',(28.9587451339273,3.91627216880442,127.829130313481));
#64769=CARTESIAN_POINT('Ctrl Pts',(28.9509939426872,3.83340586498799,127.720054051746));
#64770=CARTESIAN_POINT('Ctrl Pts',(28.9432427514471,3.74591445309607,127.614357307214));
#64771=CARTESIAN_POINT('Ctrl Pts',(28.9354915602069,3.6541090905907,127.512450865376));
#64772=CARTESIAN_POINT('Ctrl Pts',(28.9277436634299,3.56234274781325,127.410587736495));
#64773=CARTESIAN_POINT('Ctrl Pts',(28.9199957666528,3.46626636233686,127.31251199606));
#64774=CARTESIAN_POINT('Ctrl Pts',(28.9122478698757,3.36623131384609,127.218601311062));
#64775=CARTESIAN_POINT('Ctrl Pts',(28.9045015937916,3.26621719053096,127.124710270155));
#64776=CARTESIAN_POINT('Ctrl Pts',(28.8967553177075,3.16224633613331,127.034982819162));
#64777=CARTESIAN_POINT('Ctrl Pts',(28.8890090416234,3.05470663807239,126.949759416687));
#64778=CARTESIAN_POINT('Ctrl Pts',(28.881262708358,2.94716614617769,126.864535385112));
#64779=CARTESIAN_POINT('Ctrl Pts',(28.8735163750926,2.83605706446422,126.783815711226));
#64780=CARTESIAN_POINT('Ctrl Pts',(28.8657700418273,2.72179965061627,126.70789998375));
#64781=CARTESIAN_POINT('Ctrl Pts',(28.8580219738243,2.60751664961301,126.631967255474));
#64782=CARTESIAN_POINT('Ctrl Pts',(28.8502739058213,2.49008423908966,126.560840830669));
#64783=CARTESIAN_POINT('Ctrl Pts',(28.8425258378184,2.369950535649,126.494776238409));
#64784=CARTESIAN_POINT('Ctrl Pts',(28.8347695350765,2.24968915267839,126.428641431914));
#64785=CARTESIAN_POINT('Ctrl Pts',(28.8270132323346,2.12672108485306,126.36757939334));
#64786=CARTESIAN_POINT('Ctrl Pts',(28.8192569295927,2.00151836257592,126.311799287237));
#64787=CARTESIAN_POINT('Ctrl Pts',(28.8114964870785,1.87624881583596,126.255989409611));
#64788=CARTESIAN_POINT('Ctrl Pts',(28.8037360445644,1.74874260137819,126.205467225753));
#64789=CARTESIAN_POINT('Ctrl Pts',(28.7959756020502,1.61948954423614,126.160392844356));
#64790=CARTESIAN_POINT('Ctrl Pts',(28.7882027017848,1.49002899861257,126.115246105562));
#64791=CARTESIAN_POINT('Ctrl Pts',(28.7804298015193,1.3588163810876,126.075564758356));
#64792=CARTESIAN_POINT('Ctrl Pts',(28.7726569012539,1.22635528493476,126.041458584392));
#64793=CARTESIAN_POINT('Ctrl Pts',(28.7651665654919,1.09870948327789,126.008592255761));
#64794=CARTESIAN_POINT('Ctrl Pts',(28.75767622973,0.969904698905462,125.980902859279));
#64795=CARTESIAN_POINT('Ctrl Pts',(28.750185893968,0.840396525686057,125.958443084001));
#64796=CARTESIAN_POINT('Ctrl Pts',(28.7424115598489,0.705978010714365,125.935131739516));
#64797=CARTESIAN_POINT('Ctrl Pts',(28.7346372257298,0.57037591855945,125.91738056334));
#64798=CARTESIAN_POINT('Ctrl Pts',(28.7268628916108,0.434090006628336,125.905304695386));
#64799=CARTESIAN_POINT('Ctrl Pts',(28.7190981386637,0.297972054903456,125.893243709861));
#64800=CARTESIAN_POINT('Ctrl Pts',(28.7113333857166,0.161172345918071,125.886844150141));
#64801=CARTESIAN_POINT('Ctrl Pts',(28.7035686327695,0.0242007586337614,
125.886170159096));
#64802=CARTESIAN_POINT('Ctrl Pts',(28.6958115918845,-0.112634786539282,
125.885496837469));
#64803=CARTESIAN_POINT('Ctrl Pts',(28.6880545509994,-0.249641481856184,
125.890537769609));
#64804=CARTESIAN_POINT('Ctrl Pts',(28.6802975101144,-0.386304750222389,
125.901305273961));
#64805=CARTESIAN_POINT('Ctrl Pts',(28.6725463188743,-0.522864959754461,
125.912064658454));
#64806=CARTESIAN_POINT('Ctrl Pts',(28.6647951276342,-0.659081869641387,
125.928541988958));
#64807=CARTESIAN_POINT('Ctrl Pts',(28.6570439363941,-0.79444168620454,125.95069751948));
#64808=CARTESIAN_POINT('Ctrl Pts',(28.649296039617,-0.929743971234814,125.972843633311));
#64809=CARTESIAN_POINT('Ctrl Pts',(28.6415481428399,-1.06418950245819,126.000663084099));
#64810=CARTESIAN_POINT('Ctrl Pts',(28.6338002460628,-1.19727060863685,126.034064384396));
#64811=CARTESIAN_POINT('Ctrl Pts',(28.6260539699787,-1.33032387711717,126.067458697862));
#64812=CARTESIAN_POINT('Ctrl Pts',(28.6183076938946,-1.46201290928184,126.106432443298));
#64813=CARTESIAN_POINT('Ctrl Pts',(28.6105614178105,-1.59184160504136,126.150843306224));
#64814=CARTESIAN_POINT('Ctrl Pts',(28.6028150845451,-1.72167125916683,126.195254496981));
#64815=CARTESIAN_POINT('Ctrl Pts',(28.5950687512798,-1.84964017956391,126.245102758776));
#64816=CARTESIAN_POINT('Ctrl Pts',(28.5873224180144,-1.97526915421154,126.300196451939));
#64817=CARTESIAN_POINT('Ctrl Pts',(28.5795743500114,-2.10092626259682,126.355302482952));
#64818=CARTESIAN_POINT('Ctrl Pts',(28.5718262820084,-2.22424202452435,126.415656125818));
#64819=CARTESIAN_POINT('Ctrl Pts',(28.5640782140055,-2.34475923817768,126.481018487052));
#64820=CARTESIAN_POINT('Ctrl Pts',(28.5563219112636,-2.46540453895984,126.546450316181));
#64821=CARTESIAN_POINT('Ctrl Pts',(28.5485656085218,-2.58324500570006,126.616901310907));
#64822=CARTESIAN_POINT('Ctrl Pts',(28.5408093057799,-2.69784951837669,126.69208739723));
#64823=CARTESIAN_POINT('Ctrl Pts',(28.5330488632658,-2.81251519893226,126.767313612631));
#64824=CARTESIAN_POINT('Ctrl Pts',(28.5252884207516,-2.9239411665011,126.847279727569));
#64825=CARTESIAN_POINT('Ctrl Pts',(28.5175279782374,-3.03172795470893,126.931660181031));
#64826=CARTESIAN_POINT('Ctrl Pts',(28.509755077972,-3.1396877718382,127.016176089488));
#64827=CARTESIAN_POINT('Ctrl Pts',(28.5019821777066,-3.24399643789525,127.105120243311));
#64828=CARTESIAN_POINT('Ctrl Pts',(28.4942092774412,-3.34428938600066,127.19812829488));
#64829=CARTESIAN_POINT('Ctrl Pts',(28.4867189416792,-3.44093643281988,127.287755269502));
#64830=CARTESIAN_POINT('Ctrl Pts',(28.4792286059171,-3.53385443847036,127.381155587387));
#64831=CARTESIAN_POINT('Ctrl Pts',(28.471738270155,-3.62275281454509,127.477974424232));
#64832=CARTESIAN_POINT('Ctrl Pts',(28.4640491790996,-3.71401009993794,127.57736233901));
#64833=CARTESIAN_POINT('Ctrl Pts',(28.456360088044,-3.80133502515556,127.680683630055));
#64834=CARTESIAN_POINT('Ctrl Pts',(28.4486709969885,-3.88436366672537,127.787590495876));
#64835=CARTESIAN_POINT('Ctrl Pts',(28.4409910655761,-3.96729340028223,127.894370008707));
#64836=CARTESIAN_POINT('Ctrl Pts',(28.4333111341636,-4.04593678375962,128.004726290477));
#64837=CARTESIAN_POINT('Ctrl Pts',(28.4256312027512,-4.11996687512301,128.118274987809));
#64838=CARTESIAN_POINT('Ctrl Pts',(28.4179598667928,-4.19391411128604,128.23169660033));
#64839=CARTESIAN_POINT('Ctrl Pts',(28.4102885308345,-4.26325811512867,128.348303183766));
#64840=CARTESIAN_POINT('Ctrl Pts',(28.4026171948762,-4.32771284263925,128.467678222769));
#64841=CARTESIAN_POINT('Ctrl Pts',(28.3949509219467,-4.39212503047414,128.586974475069));
#64842=CARTESIAN_POINT('Ctrl Pts',(28.3872846490172,-4.45165416910228,128.709035199073));
#64843=CARTESIAN_POINT('Ctrl Pts',(28.3796183760877,-4.5060581971628,128.833416025173));
#64844=CARTESIAN_POINT('Ctrl Pts',(28.3719547042758,-4.56044376628301,128.957754649652));
#64845=CARTESIAN_POINT('Ctrl Pts',(28.3642910324639,-4.60970751792294,129.084411446939));
#64846=CARTESIAN_POINT('Ctrl Pts',(28.356627360652,-4.65365410871967,129.212918975879));
#64847=CARTESIAN_POINT('Ctrl Pts',(28.3493715073123,-4.69526210361161,129.334588040777));
#64848=CARTESIAN_POINT('Ctrl Pts',(28.3421156539726,-4.73210404157072,129.457915656724));
#64849=CARTESIAN_POINT('Ctrl Pts',(28.3348598006328,-4.76405452823408,129.582490119308));
#64850=CARTESIAN_POINT('Ctrl Pts',(30.0845737196928,-4.764054528234,129.582490119308));
#64851=CARTESIAN_POINT('Ctrl Pts',(30.0762738315874,-4.80042685421111,129.724305266266));
#64852=CARTESIAN_POINT('Ctrl Pts',(30.0679739434819,-4.83050405968412,129.867906679042));
#64853=CARTESIAN_POINT('Ctrl Pts',(30.0596740553765,-4.85412279584103,130.01273258282));
#64854=CARTESIAN_POINT('Ctrl Pts',(30.0513972716616,-4.87767578454456,130.157155334867));
#64855=CARTESIAN_POINT('Ctrl Pts',(30.0431204879468,-4.89480610788418,130.302795483977));
#64856=CARTESIAN_POINT('Ctrl Pts',(30.034843704232,-4.90540096313198,130.449079808341));
#64857=CARTESIAN_POINT('Ctrl Pts',(30.0281822815023,-4.91392804466475,130.566814155025));
#64858=CARTESIAN_POINT('Ctrl Pts',(30.0215208587727,-4.91822265953884,130.684965401437));
#64859=CARTESIAN_POINT('Ctrl Pts',(30.014859436043,-4.91824986981998,130.803229018816));
#64860=CARTESIAN_POINT('',(30.3601405639767,-4.91824855297799,130.800587869246));
#64861=CARTESIAN_POINT('Ctrl Pts',(30.4301958372212,-4.76405452823406,129.582490119308));
#64862=CARTESIAN_POINT('Ctrl Pts',(30.4224205637759,-4.79807047554281,129.715117781601));
#64863=CARTESIAN_POINT('Ctrl Pts',(30.4146452903305,-4.82650126630627,129.849000753027));
#64864=CARTESIAN_POINT('Ctrl Pts',(30.4068700168851,-4.84928678182263,129.98362876724));
#64865=CARTESIAN_POINT('Ctrl Pts',(30.4050075581521,-4.85474473550842,130.015877037675));
#64866=CARTESIAN_POINT('Ctrl Pts',(30.4031450994191,-4.85987901195573,130.048168045123));
#64867=CARTESIAN_POINT('Ctrl Pts',(30.4012826406861,-4.86468922843001,130.080494764457));
#64868=CARTESIAN_POINT('Ctrl Pts',(30.3875686151269,-4.90010876847374,130.31852927622));
#64869=CARTESIAN_POINT('Ctrl Pts',(30.3738545895678,-4.91806340583222,130.559225480776));
#64870=CARTESIAN_POINT('Ctrl Pts',(30.3601405640087,-4.91824855297756,130.800587868682));
#64871=CARTESIAN_POINT('Ctrl Pts',(30.3601405639766,-4.91824855297799,130.800587869246));
#64872=CARTESIAN_POINT('Ctrl Pts',(30.3524894783402,-4.91835184697044,130.935244487123));
#64873=CARTESIAN_POINT('Ctrl Pts',(30.3448383927039,-4.91292084437805,131.070109760254));
#64874=CARTESIAN_POINT('Ctrl Pts',(30.3371873070675,-4.90193073887906,131.204683104734));
#64875=CARTESIAN_POINT('Ctrl Pts',(30.3295438958543,-4.89095165700789,131.339121465391));
#64876=CARTESIAN_POINT('Ctrl Pts',(30.3219004846411,-4.87442459481917,131.473268080537));
#64877=CARTESIAN_POINT('Ctrl Pts',(30.3142570734279,-4.85237677947207,131.606621580433));
#64878=CARTESIAN_POINT('Ctrl Pts',(30.3062811544048,-4.82936982813323,131.74577629643));
#64879=CARTESIAN_POINT('Ctrl Pts',(30.2983052353817,-4.80035094440838,131.884066891241));
#64880=CARTESIAN_POINT('Ctrl Pts',(30.2903293163586,-4.76541147807761,132.020928127861));
#64881=CARTESIAN_POINT('Ctrl Pts',(30.2826947511554,-4.73196735294386,132.151931969767));
#64882=CARTESIAN_POINT('Ctrl Pts',(30.2750601859522,-4.69309904374229,132.281625834324));
#64883=CARTESIAN_POINT('Ctrl Pts',(30.2674256207491,-4.64893892523314,132.409524139439));
#64884=CARTESIAN_POINT('Ctrl Pts',(30.2597922977726,-4.60478599205496,132.537401634111));
#64885=CARTESIAN_POINT('Ctrl Pts',(30.2521589747961,-4.55534309303943,132.663483768904));
#64886=CARTESIAN_POINT('Ctrl Pts',(30.2445256518197,-4.50079218013342,132.787301063911));
#64887=CARTESIAN_POINT('Ctrl Pts',(30.2368918049718,-4.44623752342343,132.911126856442));
#64888=CARTESIAN_POINT('Ctrl Pts',(30.2292579581239,-4.3865743188075,133.032687130993));
#64889=CARTESIAN_POINT('Ctrl Pts',(30.221624111276,-4.32203204386775,133.151533826829));
#64890=CARTESIAN_POINT('Ctrl Pts',(30.2139879742221,-4.25747040580612,133.270416177482));
#64891=CARTESIAN_POINT('Ctrl Pts',(30.2063518371682,-4.18802697972943,133.386582976516));
#64892=CARTESIAN_POINT('Ctrl Pts',(30.1987157001143,-4.11397613336882,133.499612634831));
#64893=CARTESIAN_POINT('Ctrl Pts',(30.1910714077416,-4.03984620143695,133.612763007703));
#64894=CARTESIAN_POINT('Ctrl Pts',(30.1834271153688,-3.96109924965702,133.722769215435));
#64895=CARTESIAN_POINT('Ctrl Pts',(30.1757828229961,-3.87805187000201,133.829240244274));
#64896=CARTESIAN_POINT('Ctrl Pts',(30.1681337229086,-3.79495225946831,133.935778235797));
#64897=CARTESIAN_POINT('Ctrl Pts',(30.1604846228212,-3.70754709806342,134.038776316573));
#64898=CARTESIAN_POINT('Ctrl Pts',(30.1528355227338,-3.61619092374368,134.137879218914));
#64899=CARTESIAN_POINT('Ctrl Pts',(30.1451756766574,-3.52470640590252,134.237121347921));
#64900=CARTESIAN_POINT('Ctrl Pts',(30.137515830581,-3.42926008346147,134.332457095685));
#64901=CARTESIAN_POINT('Ctrl Pts',(30.1298559845046,-3.33024088731945,134.423570295787));
#64902=CARTESIAN_POINT('Ctrl Pts',(30.1275156619608,-3.29998742599787,134.451408228052));
#64903=CARTESIAN_POINT('Ctrl Pts',(30.125175339417,-3.26940065230052,134.478852288305));
#64904=CARTESIAN_POINT('Ctrl Pts',(30.1228350168732,-3.23849219777335,134.505894265591));
#64905=CARTESIAN_POINT('Ctrl Pts',(30.1150606827541,-3.13581718264174,134.595725202448));
#64906=CARTESIAN_POINT('Ctrl Pts',(30.1072863486349,-3.02923904101996,134.681423110129));
#64907=CARTESIAN_POINT('Ctrl Pts',(30.0995120145159,-2.9191247008982,134.762629689156));
#64908=CARTESIAN_POINT('Ctrl Pts',(30.0917472615688,-2.80914606685958,134.843736188332));
#64909=CARTESIAN_POINT('Ctrl Pts',(30.0839825086217,-2.69564021717182,134.920362142353));
#64910=CARTESIAN_POINT('Ctrl Pts',(30.0762177556747,-2.57900925181315,134.99218754111));
#64911=CARTESIAN_POINT('Ctrl Pts',(30.0684607147897,-2.46249412597348,135.063941601868));
#64912=CARTESIAN_POINT('Ctrl Pts',(30.0607036739046,-2.34286039212943,135.13090439217));
#64913=CARTESIAN_POINT('Ctrl Pts',(30.0529466330196,-2.22054112072062,135.192797719051));
#64914=CARTESIAN_POINT('Ctrl Pts',(30.0451954417795,-2.09831409122572,135.254644371693));
#64915=CARTESIAN_POINT('Ctrl Pts',(30.0374442505394,-1.97340590261091,135.311428994406));
#64916=CARTESIAN_POINT('Ctrl Pts',(30.0296930592992,-1.84627603907225,135.36291826775));
#64917=CARTESIAN_POINT('Ctrl Pts',(30.0219451625222,-1.71920020911707,135.414385656778));
#64918=CARTESIAN_POINT('Ctrl Pts',(30.0141972657451,-1.5899049439349,135.460562026379));
#64919=CARTESIAN_POINT('Ctrl Pts',(30.006449368968,-1.45887141363654,135.501261432037));
#64920=CARTESIAN_POINT('Ctrl Pts',(29.9987030928839,-1.32786529272796,135.541952324256));
#64921=CARTESIAN_POINT('Ctrl Pts',(29.9909568167999,-1.19512200307163,135.577168415421));
#64922=CARTESIAN_POINT('Ctrl Pts',(29.9832105407158,-1.06113927152275,135.606773189277));
#64923=CARTESIAN_POINT('Ctrl Pts',(29.9754642074504,-0.927155550943786,
135.63637818167));
#64924=CARTESIAN_POINT('Ctrl Pts',(29.967717874185,-0.791932751972515,135.660371689748));
#64925=CARTESIAN_POINT('Ctrl Pts',(29.9599715409197,-0.655979836026633,
135.678668108608));
#64926=CARTESIAN_POINT('Ctrl Pts',(29.9522234729167,-0.519996474367857,
135.696968624824));
#64927=CARTESIAN_POINT('Ctrl Pts',(29.9444754049137,-0.383283057777108,
135.709569460946));
#64928=CARTESIAN_POINT('Ctrl Pts',(29.9367273369108,-0.246354330151193,
135.716436818778));
#64929=CARTESIAN_POINT('Ctrl Pts',(29.9289710341689,-0.109280073043898,
135.72331147532));
#64930=CARTESIAN_POINT('Ctrl Pts',(29.9212147314271,0.0280095611243244,
135.724440461317));
#64931=CARTESIAN_POINT('Ctrl Pts',(29.9134584286852,0.164998601834844,135.719842132524));
#64932=CARTESIAN_POINT('Ctrl Pts',(29.905697986171,0.302060757721051,135.715241349464));
#64933=CARTESIAN_POINT('Ctrl Pts',(29.8979375436569,0.438821610804647,135.704907190044));
#64934=CARTESIAN_POINT('Ctrl Pts',(29.8901771011427,0.574770643908035,135.688909907869));
#64935=CARTESIAN_POINT('Ctrl Pts',(29.8824042008773,0.710937914468348,135.672886945437));
#64936=CARTESIAN_POINT('Ctrl Pts',(29.8746313006118,0.846290374572785,135.651182755576));
#64937=CARTESIAN_POINT('Ctrl Pts',(29.8668584003463,0.980327137220798,135.62391887186));
#64938=CARTESIAN_POINT('Ctrl Pts',(29.8593680645843,1.10949132592833,135.59764609899));
#64939=CARTESIAN_POINT('Ctrl Pts',(29.8518777288223,1.23743351513012,135.566210905697));
#64940=CARTESIAN_POINT('Ctrl Pts',(29.8443873930603,1.36372095349765,135.529765174161));
#64941=CARTESIAN_POINT('Ctrl Pts',(29.8366130589412,1.49479661847512,135.491937591637));
#64942=CARTESIAN_POINT('Ctrl Pts',(29.8288387248222,1.62450478416031,135.44859219503));
#64943=CARTESIAN_POINT('Ctrl Pts',(29.8210643907031,1.75234566951372,135.399844021631));
#64944=CARTESIAN_POINT('Ctrl Pts',(29.813299637756,1.88002900240139,135.351155925998));
#64945=CARTESIAN_POINT('Ctrl Pts',(29.8055348848088,2.00584927197037,135.297078439845));
#64946=CARTESIAN_POINT('Ctrl Pts',(29.7977701318617,2.12931989979165,135.237776887989));
#64947=CARTESIAN_POINT('Ctrl Pts',(29.7900130909767,2.25266789484475,135.17853423527));
#64948=CARTESIAN_POINT('Ctrl Pts',(29.7822560500918,2.37367054216918,135.114078010599));
#64949=CARTESIAN_POINT('Ctrl Pts',(29.7744990092067,2.49185970499534,135.044622198308));
#64950=CARTESIAN_POINT('Ctrl Pts',(29.7667478179666,2.60995974045491,134.975218763186));
#64951=CARTESIAN_POINT('Ctrl Pts',(29.7589966267264,2.72525017876658,134.900823442139));
#64952=CARTESIAN_POINT('Ctrl Pts',(29.7512454354862,2.83728635924497,134.821696697376));
#64953=CARTESIAN_POINT('Ctrl Pts',(29.7434975387091,2.94927492135753,134.742603583591));
#64954=CARTESIAN_POINT('Ctrl Pts',(29.7357496419321,3.05801165792907,134.658783270851));
#64955=CARTESIAN_POINT('Ctrl Pts',(29.728001745155,3.16308004437384,134.570540073644));
#64956=CARTESIAN_POINT('Ctrl Pts',(29.7202554690709,3.26812645277718,134.482315335012));
#64957=CARTESIAN_POINT('Ctrl Pts',(29.7125091929868,3.36950573814034,134.389669803414));
#64958=CARTESIAN_POINT('Ctrl Pts',(29.7047629169027,3.46683401194917,134.29294844018));
#64959=CARTESIAN_POINT('Ctrl Pts',(29.6970165836373,3.56416300421321,134.196226362971));
#64960=CARTESIAN_POINT('Ctrl Pts',(29.689270250372,3.65744064793493,134.095428669678));
#64961=CARTESIAN_POINT('Ctrl Pts',(29.6815239171066,3.74631981520688,133.990937292414));
#64962=CARTESIAN_POINT('Ctrl Pts',(29.6737758491036,3.83521888635222,133.886422515032));
#64963=CARTESIAN_POINT('Ctrl Pts',(29.6660277811006,3.91971726773403,133.778212705445));
#64964=CARTESIAN_POINT('Ctrl Pts',(29.6582797130976,3.99950829232395,133.666722663522));
#64965=CARTESIAN_POINT('Ctrl Pts',(29.6505234103558,4.07938411976421,133.555114128657));
#64966=CARTESIAN_POINT('Ctrl Pts',(29.6427671076139,4.15454236841179,133.440218715695));
#64967=CARTESIAN_POINT('Ctrl Pts',(29.6350108048721,4.22471958681367,133.322480446981));
#64968=CARTESIAN_POINT('Ctrl Pts',(29.6272503623579,4.2949342609101,133.204679337807));
#64969=CARTESIAN_POINT('Ctrl Pts',(29.6194899198437,4.36016242157305,133.084032693247));
#64970=CARTESIAN_POINT('Ctrl Pts',(29.6117294773295,4.42018722814457,132.961007999649));
#64971=CARTESIAN_POINT('Ctrl Pts',(29.6039565770641,4.48030839186435,132.837785815892));
#64972=CARTESIAN_POINT('Ctrl Pts',(29.5961836767987,4.53520935309395,132.712178313051));
#64973=CARTESIAN_POINT('Ctrl Pts',(29.5884107765332,4.58472161981121,132.584672593411));
#64974=CARTESIAN_POINT('Ctrl Pts',(29.5809204407712,4.63243399091916,132.461802027847));
#64975=CARTESIAN_POINT('Ctrl Pts',(29.5734301050092,4.67514255093558,132.337169150739));
#64976=CARTESIAN_POINT('Ctrl Pts',(29.5659397692473,4.71274116997774,132.211220144064));
#64977=CARTESIAN_POINT('Ctrl Pts',(29.5581654351282,4.75176535208891,132.080495742518));
#64978=CARTESIAN_POINT('Ctrl Pts',(29.5503911010091,4.78540807416891,131.947939343565));
#64979=CARTESIAN_POINT('Ctrl Pts',(29.54261676689,4.81349597648854,131.814033607612));
#64980=CARTESIAN_POINT('Ctrl Pts',(29.5348520139429,4.84154926297886,131.680292898512));
#64981=CARTESIAN_POINT('Ctrl Pts',(29.5270872609958,4.86406127135682,131.545206540126));
#64982=CARTESIAN_POINT('Ctrl Pts',(29.5193225080487,4.88090808654822,131.409273266771));
#64983=CARTESIAN_POINT('Ctrl Pts',(29.5115654671637,4.89773816924527,131.273475004259));
#64984=CARTESIAN_POINT('Ctrl Pts',(29.5038084262787,4.90891420846665,131.136831886226));
#64985=CARTESIAN_POINT('Ctrl Pts',(29.4960513853937,4.91436319593427,130.999853433154));
#64986=CARTESIAN_POINT('Ctrl Pts',(29.4883001941536,4.91980807427803,130.8629782766));
#64987=CARTESIAN_POINT('Ctrl Pts',(29.4805490029135,4.91953448172863,130.725768677422));
#64988=CARTESIAN_POINT('Ctrl Pts',(29.4727978116734,4.91352120255837,130.588739527435));
#64989=CARTESIAN_POINT('Ctrl Pts',(29.4650499148963,4.90751047919213,130.451768618491));
#64990=CARTESIAN_POINT('Ctrl Pts',(29.4573020181192,4.89576493832854,130.314978395968));
#64991=CARTESIAN_POINT('Ctrl Pts',(29.4495541213421,4.87831546665287,130.178883783211));
#64992=CARTESIAN_POINT('Ctrl Pts',(29.441807845258,4.86086964503051,130.042817638512));
#64993=CARTESIAN_POINT('Ctrl Pts',(29.4340615691739,4.83772231550504,129.907447201704));
#64994=CARTESIAN_POINT('Ctrl Pts',(29.4263152930898,4.80895620269387,129.77328190909));
#64995=CARTESIAN_POINT('Ctrl Pts',(29.4185689598245,4.78018987753779,129.639115626099));
#64996=CARTESIAN_POINT('Ctrl Pts',(29.4108226265591,4.74580476829578,129.50615488733));
#64997=CARTESIAN_POINT('Ctrl Pts',(29.4030762932938,4.70593457415945,129.37489818496));
#64998=CARTESIAN_POINT('Ctrl Pts',(29.3953282252908,4.66605545136963,129.243612088563));
#64999=CARTESIAN_POINT('Ctrl Pts',(29.3875801572878,4.62068891302786,129.114031161935));
#65000=CARTESIAN_POINT('Ctrl Pts',(29.3798320892848,4.57001818099174,128.986637622194));
#65001=CARTESIAN_POINT('Ctrl Pts',(29.372075786543,4.51929359549856,128.859108687083));
#65002=CARTESIAN_POINT('Ctrl Pts',(29.3643194838012,4.46325369980301,128.733772146721));
#65003=CARTESIAN_POINT('Ctrl Pts',(29.3565631810593,4.40212966053271,128.6110896552));
#65004=CARTESIAN_POINT('Ctrl Pts',(29.3488027385451,4.34097299752225,128.48834168434));
#65005=CARTESIAN_POINT('Ctrl Pts',(29.3410422960309,4.2747269726881,128.368250927073));
#65006=CARTESIAN_POINT('Ctrl Pts',(29.3332818535168,4.20366768786337,128.251252505379));
#65007=CARTESIAN_POINT('Ctrl Pts',(29.3255089532513,4.13249433236628,128.134066267432));
#65008=CARTESIAN_POINT('Ctrl Pts',(29.3177360529859,4.05649249341213,128.019982610454));
#65009=CARTESIAN_POINT('Ctrl Pts',(29.3099631527205,3.97598090989422,127.909406582239));
#65010=CARTESIAN_POINT('Ctrl Pts',(29.3024728169585,3.89839612523374,127.802850271174));
#65011=CARTESIAN_POINT('Ctrl Pts',(29.2949824811964,3.81662397583925,127.699551235658));
#65012=CARTESIAN_POINT('Ctrl Pts',(29.2874921454344,3.73098248145132,127.599839938025));
#65013=CARTESIAN_POINT('Ctrl Pts',(29.2797178113153,3.64209386377338,127.496348056237));
#65014=CARTESIAN_POINT('Ctrl Pts',(29.2719434771962,3.54875512419509,127.396393509835));
#65015=CARTESIAN_POINT('Ctrl Pts',(29.2641691430771,3.4512786334196,127.300383041011));
#65016=CARTESIAN_POINT('Ctrl Pts',(29.2564043901301,3.35392227370753,127.204490896509));
#65017=CARTESIAN_POINT('Ctrl Pts',(29.248639637183,3.25243858496823,127.112533429913));
#65018=CARTESIAN_POINT('Ctrl Pts',(29.240874884236,3.14718018738191,127.024884472562));
#65019=CARTESIAN_POINT('Ctrl Pts',(29.233117843351,3.0420263339198,126.937322569392));
#65020=CARTESIAN_POINT('Ctrl Pts',(29.2253608024659,2.93310553097379,126.854060908083));
#65021=CARTESIAN_POINT('Ctrl Pts',(29.2176037615809,2.82080698979821,126.775436320833));
#65022=CARTESIAN_POINT('Ctrl Pts',(29.2098525703408,2.70859313382654,126.696871024996));
#65023=CARTESIAN_POINT('Ctrl Pts',(29.2021013791007,2.59300692860439,126.62293606627));
#65024=CARTESIAN_POINT('Ctrl Pts',(29.1943501878606,2.47447009957901,126.55392760565));
#65025=CARTESIAN_POINT('Ctrl Pts',(29.1866022910835,2.35598365186756,126.484948475466));
#65026=CARTESIAN_POINT('Ctrl Pts',(29.1788543943065,2.23454941182109,126.420891875084));
#65027=CARTESIAN_POINT('Ctrl Pts',(29.1711064975294,2.11061729404101,126.362010147309));
#65028=CARTESIAN_POINT('Ctrl Pts',(29.1633602214453,1.98671110018831,126.303140736321));
#65029=CARTESIAN_POINT('Ctrl Pts',(29.1556139453612,1.86030842079838,126.249444212516));
#65030=CARTESIAN_POINT('Ctrl Pts',(29.1478676692771,1.73188257373812,126.201126340095));
#65031=CARTESIAN_POINT('Ctrl Pts',(29.1401213360118,1.60345577866778,126.152808111003));
#65032=CARTESIAN_POINT('Ctrl Pts',(29.1323750027464,1.47300615205,126.109868750194));
#65033=CARTESIAN_POINT('Ctrl Pts',(29.1246286694811,1.34102535714994,126.07246521995));
#65034=CARTESIAN_POINT('Ctrl Pts',(29.1168806014782,1.2090150060656,126.035053313444));
#65035=CARTESIAN_POINT('Ctrl Pts',(29.1091325334752,1.07547318045794,126.003179810966));
#65036=CARTESIAN_POINT('Ctrl Pts',(29.1013844654722,0.940904619134276,125.976951212907));
#65037=CARTESIAN_POINT('Ctrl Pts',(29.0936281627304,0.806193036742072,125.950694738782));
#65038=CARTESIAN_POINT('Ctrl Pts',(29.0858718599885,0.670452923146452,125.930095228582));
#65039=CARTESIAN_POINT('Ctrl Pts',(29.0781155572466,0.534197632218005,125.915207730589));
#65040=CARTESIAN_POINT('Ctrl Pts',(29.0703551147325,0.397869617738221,125.900312286691));
#65041=CARTESIAN_POINT('Ctrl Pts',(29.0625946722183,0.261026267931343,125.891134955886));
#65042=CARTESIAN_POINT('Ctrl Pts',(29.0548342297042,0.124182903025224,125.887678639942));
#65043=CARTESIAN_POINT('Ctrl Pts',(29.0470613294387,-0.0128801349986252,
125.884216775612));
#65044=CARTESIAN_POINT('Ctrl Pts',(29.0392884291733,-0.149942797033939,
125.886494271963));
#65045=CARTESIAN_POINT('Ctrl Pts',(29.0315155289078,-0.28649201874362,125.894461903163));
#65046=CARTESIAN_POINT('Ctrl Pts',(29.0240251931457,-0.418077332298904,
125.9021398909));
#65047=CARTESIAN_POINT('Ctrl Pts',(29.0165348573836,-0.549185580604208,
125.915101464177));
#65048=CARTESIAN_POINT('Ctrl Pts',(29.0090445216215,-0.679366838901137,
125.933257686945));
#65049=CARTESIAN_POINT('Ctrl Pts',(29.0012701875024,-0.814483959172609,
125.952102308418));
#65050=CARTESIAN_POINT('Ctrl Pts',(28.9934958533833,-0.949030418587731,
125.97660295966));
#65051=CARTESIAN_POINT('Ctrl Pts',(28.9857215192642,-1.08249516942704,126.006716688441));
#65052=CARTESIAN_POINT('Ctrl Pts',(28.9779567663171,-1.21579543688921,126.036793304744));
#65053=CARTESIAN_POINT('Ctrl Pts',(28.97019201337,-1.34801627054872,126.072469149366));
#65054=CARTESIAN_POINT('Ctrl Pts',(28.9624272604229,-1.47865255569009,126.113649617936));
#65055=CARTESIAN_POINT('Ctrl Pts',(28.9546702195379,-1.60915909103123,126.154789185484));
#65056=CARTESIAN_POINT('Ctrl Pts',(28.9469131786529,-1.73808383931453,126.201422380083));
#65057=CARTESIAN_POINT('Ctrl Pts',(28.9391561377679,-1.86493303588192,126.253403813313));
#65058=CARTESIAN_POINT('Ctrl Pts',(28.9314049465277,-1.99168657448327,126.30534604694));
#65059=CARTESIAN_POINT('Ctrl Pts',(28.9236537552877,-2.11636731647962,126.362628343812));
#65060=CARTESIAN_POINT('Ctrl Pts',(28.9159025640475,-2.23849814033236,126.425055976618));
#65061=CARTESIAN_POINT('Ctrl Pts',(28.9081546672705,-2.36057705532702,126.487457076015));
#65062=CARTESIAN_POINT('Ctrl Pts',(28.9004067704934,-2.48010786034616,126.554998984187));
#65063=CARTESIAN_POINT('Ctrl Pts',(28.8926588737163,-2.59663506241136,126.627439572687));
#65064=CARTESIAN_POINT('Ctrl Pts',(28.8849125976322,-2.71313788949824,126.699865008177));
#65065=CARTESIAN_POINT('Ctrl Pts',(28.877166321548,-2.82663803150784,126.777186879531));
#65066=CARTESIAN_POINT('Ctrl Pts',(28.8694200454639,-2.9367065333206,126.859118191599));
#65067=CARTESIAN_POINT('Ctrl Pts',(28.8616737121986,-3.04677584763359,126.941050108465));
#65068=CARTESIAN_POINT('Ctrl Pts',(28.8539273789333,-3.15341315758425,127.027591300495));
#65069=CARTESIAN_POINT('Ctrl Pts',(28.8461810456679,-3.2562206503555,127.118412959406));
#65070=CARTESIAN_POINT('Ctrl Pts',(28.838432977665,-3.35905116615221,127.209254957198));
#65071=CARTESIAN_POINT('Ctrl Pts',(28.830684909662,-3.45804986517336,127.304379070539));
#65072=CARTESIAN_POINT('Ctrl Pts',(28.822936841659,-3.55285432196795,127.403418214441));
#65073=CARTESIAN_POINT('Ctrl Pts',(28.8151805389171,-3.64775953806741,127.502562618323));
#65074=CARTESIAN_POINT('Ctrl Pts',(28.8074242361753,-3.73846133644194,127.605630081817));
#65075=CARTESIAN_POINT('Ctrl Pts',(28.7996679334334,-3.8246359231063,127.712218460713));
#65076=CARTESIAN_POINT('Ctrl Pts',(28.7919074909192,-3.91085650374247,127.818863729037));
#65077=CARTESIAN_POINT('Ctrl Pts',(28.784147048405,-3.99254482521903,127.929033343366));
#65078=CARTESIAN_POINT('Ctrl Pts',(28.7763866058908,-4.06941990302799,128.042295318675));
#65079=CARTESIAN_POINT('Ctrl Pts',(28.7686137056254,-4.14641838753629,128.15573911216));
#65080=CARTESIAN_POINT('Ctrl Pts',(28.7608408053599,-4.21858798212553,128.272284853956));
#65081=CARTESIAN_POINT('Ctrl Pts',(28.7530679050945,-4.28569277807604,128.391474280739));
#65082=CARTESIAN_POINT('Ctrl Pts',(28.7455775693325,-4.35035814566643,128.506330871638));
#65083=CARTESIAN_POINT('Ctrl Pts',(28.7380872335705,-4.41032041768173,128.623642001074));
#65084=CARTESIAN_POINT('Ctrl Pts',(28.7305968978086,-4.46541122321864,128.742981062498));
#65085=CARTESIAN_POINT('Ctrl Pts',(28.7221355457944,-4.52764377369516,128.877790747917));
#65086=CARTESIAN_POINT('Ctrl Pts',(28.7136741937802,-4.58383185446041,129.015559555786));
#65087=CARTESIAN_POINT('Ctrl Pts',(28.705212841766,-4.63370916988232,129.155748355253));
#65088=CARTESIAN_POINT('Ctrl Pts',(28.69676164026,-4.68352665088257,129.295768979755));
#65089=CARTESIAN_POINT('Ctrl Pts',(28.6883104387542,-4.72704834146951,129.438203558761));
#65090=CARTESIAN_POINT('Ctrl Pts',(28.6798592372483,-4.76405452823403,129.582490119308));
#65091=CARTESIAN_POINT('Origin',(213.235140564004,0.,130.804360617566));
#65092=CARTESIAN_POINT('',(26.5849533738221,-4.764054528234,129.582490119308));
#65093=CARTESIAN_POINT('',(26.9301047320142,-4.76405452823399,129.582490119308));
#65094=CARTESIAN_POINT('',(213.235140564004,-4.76405452823405,129.582490119308));
#65095=CARTESIAN_POINT('',(28.2648594359576,-4.9182479151818,130.808889117301));
#65096=CARTESIAN_POINT('Ctrl Pts',(28.2648594359576,-4.9182479151818,130.808889117301));
#65097=CARTESIAN_POINT('Ctrl Pts',(28.2550046190053,-4.918087596155,130.983006102042));
#65098=CARTESIAN_POINT('Ctrl Pts',(28.2451498020529,-4.90867757925288,131.156709223396));
#65099=CARTESIAN_POINT('Ctrl Pts',(28.2352949851005,-4.89017053265966,131.329160792878));
#65100=CARTESIAN_POINT('Ctrl Pts',(28.2252357564318,-4.87127960707866,131.505189407114));
#65101=CARTESIAN_POINT('Ctrl Pts',(28.2151765277632,-4.84291035541841,131.679914228869));
#65102=CARTESIAN_POINT('Ctrl Pts',(28.2051172990946,-4.80527329238343,131.852469222629));
#65103=CARTESIAN_POINT('Ctrl Pts',(28.2011750815104,-4.79052330542128,131.920093625357));
#65104=CARTESIAN_POINT('Ctrl Pts',(28.1972328639263,-4.77435042589291,131.987385019867));
#65105=CARTESIAN_POINT('Ctrl Pts',(28.1932906463422,-4.75676929952319,132.054292173138));
#65106=CARTESIAN_POINT('Ctrl Pts',(28.1855163122231,-4.72209806495262,132.18623784924));
#65107=CARTESIAN_POINT('Ctrl Pts',(28.177741978104,-4.68187778908076,132.31694883218));
#65108=CARTESIAN_POINT('Ctrl Pts',(28.1699676439849,-4.63621148270328,132.445922724265));
#65109=CARTESIAN_POINT('Ctrl Pts',(28.1622028910378,-4.59060145596709,132.574737667555));
#65110=CARTESIAN_POINT('Ctrl Pts',(28.1544381380908,-4.53955888233867,132.701819414554));
#65111=CARTESIAN_POINT('Ctrl Pts',(28.1466733851437,-4.48323736248634,132.826677559617));
#65112=CARTESIAN_POINT('Ctrl Pts',(28.1389163442587,-4.42697178196153,132.95141169381));
#65113=CARTESIAN_POINT('Ctrl Pts',(28.1311593033737,-4.36543784898505,133.073926267028));
#65114=CARTESIAN_POINT('Ctrl Pts',(28.1234022624887,-4.29883825227731,133.19374814228));
#65115=CARTESIAN_POINT('Ctrl Pts',(28.1156510712486,-4.23228887884352,133.313479658923));
#65116=CARTESIAN_POINT('Ctrl Pts',(28.1078998800085,-4.16068163443954,133.430522179011));
#65117=CARTESIAN_POINT('Ctrl Pts',(28.1001486887683,-4.08426623563861,133.544424919535));
#65118=CARTESIAN_POINT('Ctrl Pts',(28.0924007919913,-4.00788331542061,133.658279248355));
#65119=CARTESIAN_POINT('Ctrl Pts',(28.0846528952142,-3.92669652271729,133.768996127821));
#65120=CARTESIAN_POINT('Ctrl Pts',(28.0769049984372,-3.8410000889408,133.876151850586));
#65121=CARTESIAN_POINT('Ctrl Pts',(28.0691587223531,-3.75532158101085,133.983285158684));
#65122=CARTESIAN_POINT('Ctrl Pts',(28.061412446269,-3.66513555235274,134.086858486624));
#65123=CARTESIAN_POINT('Ctrl Pts',(28.0536661701849,-3.57077765268976,134.186479778322));
#65124=CARTESIAN_POINT('Ctrl Pts',(28.0459198369196,-3.4764190564982,134.286101805402));
#65125=CARTESIAN_POINT('Ctrl Pts',(28.0381735036542,-3.37788879670492,134.381771454176));
#65126=CARTESIAN_POINT('Ctrl Pts',(28.0304271703889,-3.27556036532457,134.473132531383));
#65127=CARTESIAN_POINT('Ctrl Pts',(28.0226791023859,-3.17320901820138,134.564514068271));
#65128=CARTESIAN_POINT('Ctrl Pts',(28.0149310343829,-3.06705809853189,134.651584853269));
#65129=CARTESIAN_POINT('Ctrl Pts',(28.0071829663799,-2.95751492756948,134.73402835361));
#65130=CARTESIAN_POINT('Ctrl Pts',(27.9994266636381,-2.84785533282154,134.816559475883));
#65131=CARTESIAN_POINT('Ctrl Pts',(27.9916703608962,-2.73479659763375,134.894453253922));
#65132=CARTESIAN_POINT('Ctrl Pts',(27.9839140581544,-2.6187762943739,134.967435656828));
#65133=CARTESIAN_POINT('Ctrl Pts',(27.9761536156402,-2.50269406758489,135.04045701264));
#65134=CARTESIAN_POINT('Ctrl Pts',(27.968393173126,-2.38364746228006,135.108561576014));
#65135=CARTESIAN_POINT('Ctrl Pts',(27.9606327306118,-2.26209862660601,135.171521350354));
#65136=CARTESIAN_POINT('Ctrl Pts',(27.9528598303464,-2.14035466995034,135.234582193313));
#65137=CARTESIAN_POINT('Ctrl Pts',(27.945086930081,-2.01610081065817,135.292481578153));
#65138=CARTESIAN_POINT('Ctrl Pts',(27.9373140298156,-1.88981996739606,135.34503937226));
#65139=CARTESIAN_POINT('Ctrl Pts',(27.9298236940535,-1.76812975086793,135.395686558167));
#65140=CARTESIAN_POINT('Ctrl Pts',(27.9223333582914,-1.6445576526277,135.441373664574));
#65141=CARTESIAN_POINT('Ctrl Pts',(27.9148430225294,-1.51954717933933,135.481983885024));
#65142=CARTESIAN_POINT('Ctrl Pts',(27.9070686884103,-1.38979689596103,135.524133854325));
#65143=CARTESIAN_POINT('Ctrl Pts',(27.8992943542913,-1.2580860025425,135.560947876209));
#65144=CARTESIAN_POINT('Ctrl Pts',(27.8915200201722,-1.12489286034248,135.592241058351));
#65145=CARTESIAN_POINT('Ctrl Pts',(27.8837552672251,-0.991863866786592,
135.623495674443));
#65146=CARTESIAN_POINT('Ctrl Pts',(27.875990514278,-0.857356636063686,135.649242900046));
#65147=CARTESIAN_POINT('Ctrl Pts',(27.8682257613309,-0.721866785246101,
135.669346887522));
#65148=CARTESIAN_POINT('Ctrl Pts',(27.8604687204459,-0.586511504858237,
135.689430907434));
#65149=CARTESIAN_POINT('Ctrl Pts',(27.8527116795609,-0.450175930793075,
135.703882786299));
#65150=CARTESIAN_POINT('Ctrl Pts',(27.8449546386759,-0.313367684806054,
135.712617309776));
#65151=CARTESIAN_POINT('Ctrl Pts',(27.8372034474358,-0.176662606981544,
135.72134524648));
#65152=CARTESIAN_POINT('Ctrl Pts',(27.8294522561957,-0.0394859553105575,
135.72436438477));
#65153=CARTESIAN_POINT('Ctrl Pts',(27.8217010649556,0.0976480357871611,
135.721641159045));
#65154=CARTESIAN_POINT('Ctrl Pts',(27.8139531681785,0.234723741280308,135.718919090763));
#65155=CARTESIAN_POINT('Ctrl Pts',(27.8062052714014,0.371756432193335,135.710459520493));
#65156=CARTESIAN_POINT('Ctrl Pts',(27.7984573746243,0.508230592271119,135.696280969287));
#65157=CARTESIAN_POINT('Ctrl Pts',(27.7907110985402,0.644676204896843,135.682105383927));
#65158=CARTESIAN_POINT('Ctrl Pts',(27.7829648224562,0.780563130447971,135.662213237487));
#65159=CARTESIAN_POINT('Ctrl Pts',(27.7752185463721,0.915380094162875,135.636675005694));
#65160=CARTESIAN_POINT('Ctrl Pts',(27.7674722131067,1.05019805306598,135.611136585384));
#65161=CARTESIAN_POINT('Ctrl Pts',(27.7597258798414,1.1839456502386,135.579952069321));
#65162=CARTESIAN_POINT('Ctrl Pts',(27.7519795465761,1.3161213286455,135.543243155758));
#65163=CARTESIAN_POINT('Ctrl Pts',(27.7442314785731,1.44832660687915,135.506526021489));
#65164=CARTESIAN_POINT('Ctrl Pts',(27.7364834105701,1.57895888923273,135.464282132534));
#65165=CARTESIAN_POINT('Ctrl Pts',(27.7287353425671,1.70753170063621,135.416683086109));
#65166=CARTESIAN_POINT('Ctrl Pts',(27.7209790398253,1.83624116075369,135.36903345085));
#65167=CARTESIAN_POINT('Ctrl Pts',(27.7132227370835,1.96288641026609,135.316017424638));
#65168=CARTESIAN_POINT('Ctrl Pts',(27.7054664343416,2.08700038066533,135.257855029104));
#65169=CARTESIAN_POINT('Ctrl Pts',(27.6977059918274,2.21118059442774,135.199661590549));
#65170=CARTESIAN_POINT('Ctrl Pts',(27.6899455493133,2.33282649045845,135.136316489981));
#65171=CARTESIAN_POINT('Ctrl Pts',(27.6821851067991,2.45149644640171,135.068085307996));
#65172=CARTESIAN_POINT('Ctrl Pts',(27.6744122065337,2.57035690189312,134.99974459526));
#65173=CARTESIAN_POINT('Ctrl Pts',(27.6666393062682,2.68623154017101,134.926502336162));
#65174=CARTESIAN_POINT('Ctrl Pts',(27.6588664060028,2.79870778123177,134.848667457776));
#65175=CARTESIAN_POINT('Ctrl Pts',(27.6513760702407,2.90709522762048,134.773662073274));
#65176=CARTESIAN_POINT('Ctrl Pts',(27.6438857344786,3.01232682168215,134.694392364263));
#65177=CARTESIAN_POINT('Ctrl Pts',(27.6363953987165,3.11406456465109,134.611168328718));
#65178=CARTESIAN_POINT('Ctrl Pts',(27.6286210645974,3.21965972506633,134.52478882857));
#65179=CARTESIAN_POINT('Ctrl Pts',(27.6208467304783,3.32182535941488,134.433875601751));
#65180=CARTESIAN_POINT('Ctrl Pts',(27.6130723963593,3.42014734660246,134.338731168319));
#65181=CARTESIAN_POINT('Ctrl Pts',(27.6053076434122,3.51834816072812,134.243703991897));
#65182=CARTESIAN_POINT('Ctrl Pts',(27.597542890465,3.61271447455497,134.144456253596));
#65183=CARTESIAN_POINT('Ctrl Pts',(27.589778137518,3.70286410248391,134.041331501129));
#65184=CARTESIAN_POINT('Ctrl Pts',(27.5820210966329,3.79292419253151,133.93830917362));
#65185=CARTESIAN_POINT('Ctrl Pts',(27.5742640557479,3.87877567548259,133.831417787468));
#65186=CARTESIAN_POINT('Ctrl Pts',(27.5665070148629,3.96007247614123,133.7210383588));
#65187=CARTESIAN_POINT('Ctrl Pts',(27.5587558236228,4.0413079702501,133.610742168117));
#65188=CARTESIAN_POINT('Ctrl Pts',(27.5510046323827,4.11799538775448,133.496963484014));
#65189=CARTESIAN_POINT('Ctrl Pts',(27.5432534411426,4.18982853269809,133.380116803444));
#65190=CARTESIAN_POINT('Ctrl Pts',(27.5355055443655,4.26163114663889,133.26331978583));
#65191=CARTESIAN_POINT('Ctrl Pts',(27.5277576475883,4.32858338723187,133.14345769763));
#65192=CARTESIAN_POINT('Ctrl Pts',(27.5200097508112,4.39042218763301,133.02097426835));
#65193=CARTESIAN_POINT('Ctrl Pts',(27.5122634747271,4.4522480526902,132.898516459962));
#65194=CARTESIAN_POINT('Ctrl Pts',(27.5045171986431,4.50896242899818,132.773438749934));
#65195=CARTESIAN_POINT('Ctrl Pts',(27.496770922559,4.56034825328579,132.646209382056));
#65196=CARTESIAN_POINT('Ctrl Pts',(27.4890245892936,4.61173445689188,132.518979074999));
#65197=CARTESIAN_POINT('Ctrl Pts',(27.4812782560283,4.6577918835755,132.389597440913));
#65198=CARTESIAN_POINT('Ctrl Pts',(27.4735319227629,4.69835181769382,132.258552234814));
#65199=CARTESIAN_POINT('Ctrl Pts',(27.4657838547599,4.73892083492816,132.127477682049));
#65200=CARTESIAN_POINT('Ctrl Pts',(27.4580357867569,4.77398979422473,131.994739189362));
#65201=CARTESIAN_POINT('Ctrl Pts',(27.4502877187539,4.80344011352057,131.860838794492));
#65202=CARTESIAN_POINT('Ctrl Pts',(27.4425314160121,4.83292173296623,131.726796088689));
#65203=CARTESIAN_POINT('Ctrl Pts',(27.4347751132702,4.85677269946563,131.591589396339));
#65204=CARTESIAN_POINT('Ctrl Pts',(27.4270188105283,4.87492566151178,131.45573060247));
#65205=CARTESIAN_POINT('Ctrl Pts',(27.4192583680141,4.89308831234036,131.319799296673));
#65206=CARTESIAN_POINT('Ctrl Pts',(27.4114979255,4.90554686337682,131.183215585004));
#65207=CARTESIAN_POINT('Ctrl Pts',(27.4037374829858,4.91228604742679,131.046494569659));
#65208=CARTESIAN_POINT('Ctrl Pts',(27.3959645827204,4.91903604981327,130.909554077602));
#65209=CARTESIAN_POINT('Ctrl Pts',(27.388191682455,4.92004833529016,130.772476232594));
#65210=CARTESIAN_POINT('Ctrl Pts',(27.3804187821895,4.91535980338444,130.635775132507));
#65211=CARTESIAN_POINT('Ctrl Pts',(27.3729284464276,4.91084171142324,130.504043461739));
#65212=CARTESIAN_POINT('Ctrl Pts',(27.3654381106656,4.90103010721261,130.372661927353));
#65213=CARTESIAN_POINT('Ctrl Pts',(27.3579477749036,4.88600310423868,130.24208245876));
#65214=CARTESIAN_POINT('Ctrl Pts',(27.3501734407846,4.87040634787951,130.106552029926));
#65215=CARTESIAN_POINT('Ctrl Pts',(27.3423991066654,4.84914149626035,129.971456368493));
#65216=CARTESIAN_POINT('Ctrl Pts',(27.3346247725464,4.8222392255061,129.837307405747));
#65217=CARTESIAN_POINT('Ctrl Pts',(27.3268600195993,4.79537010939626,129.703323769607));
#65218=CARTESIAN_POINT('Ctrl Pts',(27.3190952666522,4.76287747397065,129.57028489038));
#65219=CARTESIAN_POINT('Ctrl Pts',(27.3113305137051,4.72484377499819,129.438698007563));
#65220=CARTESIAN_POINT('Ctrl Pts',(27.3035734728201,4.68684785163173,129.307241818693));
#65221=CARTESIAN_POINT('Ctrl Pts',(27.2958164319351,4.64332192471477,129.177235129463));
#65222=CARTESIAN_POINT('Ctrl Pts',(27.2880593910501,4.59439949180924,129.049175051262));
#65223=CARTESIAN_POINT('Ctrl Pts',(27.28030819981,4.54551395169086,128.921211544161));
#65224=CARTESIAN_POINT('Ctrl Pts',(27.2725570085698,4.49124014473066,128.795192089957));
#65225=CARTESIAN_POINT('Ctrl Pts',(27.2648058173297,4.43176129256114,128.671598345709));
#65226=CARTESIAN_POINT('Ctrl Pts',(27.2570579205526,4.37230772049045,128.548057132099));
#65227=CARTESIAN_POINT('Ctrl Pts',(27.2493100237755,4.30765367245697,128.426939929435));
#65228=CARTESIAN_POINT('Ctrl Pts',(27.2415621269984,4.23803027660593,128.308707909942));
#65229=CARTESIAN_POINT('Ctrl Pts',(27.2338158509143,4.1684214444684,128.190500622038));
#65230=CARTESIAN_POINT('Ctrl Pts',(27.2260695748303,4.09384553035747,128.075177653553));
#65231=CARTESIAN_POINT('Ctrl Pts',(27.2183232987462,4.0145791530345,127.963174723169));
#65232=CARTESIAN_POINT('Ctrl Pts',(27.2105769654808,3.93531219058525,127.851170966005));
#65233=CARTESIAN_POINT('Ctrl Pts',(27.2028306322155,3.8513549216881,127.742487614977));
#65234=CARTESIAN_POINT('Ctrl Pts',(27.1950842989501,3.76302651352613,127.637530258832));
#65235=CARTESIAN_POINT('Ctrl Pts',(27.1873362309472,3.67467832482958,127.532549398215));
#65236=CARTESIAN_POINT('Ctrl Pts',(27.1795881629443,3.58195730068962,127.431296491939));
#65237=CARTESIAN_POINT('Ctrl Pts',(27.1718400949413,3.48522172317316,127.334142670113));
#65238=CARTESIAN_POINT('Ctrl Pts',(27.1640837921995,3.38838333393362,127.236885592049));
#65239=CARTESIAN_POINT('Ctrl Pts',(27.1563274894576,3.28752214439158,127.143736578616));
#65240=CARTESIAN_POINT('Ctrl Pts',(27.1485711867157,3.18303241278574,127.055028980907));
#65241=CARTESIAN_POINT('Ctrl Pts',(27.1408107442015,3.07848691186388,126.966274037281));
#65242=CARTESIAN_POINT('Ctrl Pts',(27.1330503016873,2.97030931813767,126.88196547305));
#65243=CARTESIAN_POINT('Ctrl Pts',(27.1252898591732,2.85892474937989,126.802394558254));
#65244=CARTESIAN_POINT('Ctrl Pts',(27.1175169589077,2.74736137622423,126.722695909162));
#65245=CARTESIAN_POINT('Ctrl Pts',(27.1097440586423,2.63258106799976,126.647750321182));
#65246=CARTESIAN_POINT('Ctrl Pts',(27.1019711583768,2.51503629490142,126.577804632153));
#65247=CARTESIAN_POINT('Ctrl Pts',(27.0944808226147,2.40176457038167,126.510401645103));
#65248=CARTESIAN_POINT('Ctrl Pts',(27.0869904868527,2.2859261528447,126.447641497095));
#65249=CARTESIAN_POINT('Ctrl Pts',(27.0795001510906,2.16794348555073,126.389702747928));
#65250=CARTESIAN_POINT('Ctrl Pts',(27.0717258169715,2.04548746956728,126.329567233476));
#65251=CARTESIAN_POINT('Ctrl Pts',(27.0639514828524,1.92033349177264,126.274435450496));
#65252=CARTESIAN_POINT('Ctrl Pts',(27.0561771487333,1.7929288356507,126.224558301658));
#65253=CARTESIAN_POINT('Ctrl Pts',(27.0484123957862,1.66568119438094,126.174742621949));
#65254=CARTESIAN_POINT('Ctrl Pts',(27.0406476428391,1.53618875430544,126.130168832494));
#65255=CARTESIAN_POINT('Ctrl Pts',(27.0328828898921,1.40492283973767,126.091041736259));
#65256=CARTESIAN_POINT('Ctrl Pts',(27.025125849007,1.27378730032678,126.051953501608));
#65257=CARTESIAN_POINT('Ctrl Pts',(27.017368808122,1.1408821640186,126.018301305523));
#65258=CARTESIAN_POINT('Ctrl Pts',(27.009611767237,1.00669782339524,125.990241533572));
#65259=CARTESIAN_POINT('Ctrl Pts',(27.0018605759969,0.872614672226939,125.962202921714));
#65260=CARTESIAN_POINT('Ctrl Pts',(26.9941093847568,0.73725461797565,125.939748419431));
#65261=CARTESIAN_POINT('Ctrl Pts',(26.9863581935166,0.601121928133267,125.922984224578));
#65262=CARTESIAN_POINT('Ctrl Pts',(26.9786102967395,0.46504709831534,125.906227154956));
#65263=CARTESIAN_POINT('Ctrl Pts',(26.9708623999624,0.328200673272089,125.895155630173));
#65264=CARTESIAN_POINT('Ctrl Pts',(26.9631145031854,0.191095580663751,125.889824470425));
#65265=CARTESIAN_POINT('Ctrl Pts',(26.9553682271012,0.0540191674853299,
125.884494425842));
#65266=CARTESIAN_POINT('Ctrl Pts',(26.9476219510171,-0.0833154152125675,
125.884902373097));
#65267=CARTESIAN_POINT('Ctrl Pts',(26.939875674933,-0.220392065764167,125.891051101583));
#65268=CARTESIAN_POINT('Ctrl Pts',(26.9321293416677,-0.357469728184462,
125.897199875458));
#65269=CARTESIAN_POINT('Ctrl Pts',(26.9243830084023,-0.494289064086698,
125.909089497605));
#65270=CARTESIAN_POINT('Ctrl Pts',(26.9166366751369,-0.630336322510923,
125.926670674261));
#65271=CARTESIAN_POINT('Ctrl Pts',(26.908888607134,-0.766414047775387,125.944255788098));
#65272=CARTESIAN_POINT('Ctrl Pts',(26.901140539131,-0.901718963841309,125.967534942622));
#65273=CARTESIAN_POINT('Ctrl Pts',(26.893392471128,-1.03574516822834,125.996407309869));
#65274=CARTESIAN_POINT('Ctrl Pts',(26.8856361683862,-1.16991381726033,126.025310363013));
#65275=CARTESIAN_POINT('Ctrl Pts',(26.8778798656443,-1.30280065699779,126.05981842126));
#65276=CARTESIAN_POINT('Ctrl Pts',(26.8701235629024,-1.43391212351709,126.099779968397));
#65277=CARTESIAN_POINT('Ctrl Pts',(26.8623631203883,-1.56509356817394,126.139762844216));
#65278=CARTESIAN_POINT('Ctrl Pts',(26.8546026778741,-1.69449738279775,126.185204879249));
#65279=CARTESIAN_POINT('Ctrl Pts',(26.8468422353599,-1.82164872711363,126.235905848445));
#65280=CARTESIAN_POINT('Ctrl Pts',(26.8390693350945,-1.9490041860552,126.286688207338));
#65281=CARTESIAN_POINT('Ctrl Pts',(26.831296434829,-2.07409959205256,126.342746210443));
#65282=CARTESIAN_POINT('Ctrl Pts',(26.8235235345636,-2.19648270224759,126.403832603654));
#65283=CARTESIAN_POINT('Ctrl Pts',(26.8160331988016,-2.31441687812141,126.462698352603));
#65284=CARTESIAN_POINT('Ctrl Pts',(26.8085428630397,-2.42983226228726,126.52623310099));
#65285=CARTESIAN_POINT('Ctrl Pts',(26.8010525272777,-2.54235028642948,126.594177951269));
#65286=CARTESIAN_POINT('Ctrl Pts',(26.7932769255178,-2.65915350785349,126.66471044997));
#65287=CARTESIAN_POINT('Ctrl Pts',(26.7855013237579,-2.7732043645862,126.740219083085));
#65288=CARTESIAN_POINT('Ctrl Pts',(26.777725721998,-2.88404977769799,126.820463035767));
#65289=CARTESIAN_POINT('Ctrl Pts',(26.769693540824,-2.99855286927972,126.903354879506));
#65290=CARTESIAN_POINT('Ctrl Pts',(26.76166135965,-3.10963493645122,126.991299800931));
#65291=CARTESIAN_POINT('Ctrl Pts',(26.753629178476,-3.21682377204222,127.083980545299));
#65292=CARTESIAN_POINT('Ctrl Pts',(26.74587310756,-3.32032793762808,127.173475342576));
#65293=CARTESIAN_POINT('Ctrl Pts',(26.738117036644,-3.42020176294556,127.267385488728));
#65294=CARTESIAN_POINT('Ctrl Pts',(26.730360965728,-3.51604985092081,127.365381625432));
#65295=CARTESIAN_POINT('Ctrl Pts',(26.7226102075952,-3.61183228450382,127.463310636365));
#65296=CARTESIAN_POINT('Ctrl Pts',(26.7148594494626,-3.70359419500579,127.565319790991));
#65297=CARTESIAN_POINT('Ctrl Pts',(26.7071086913299,-3.79097497367265,127.671041002288));
#65298=CARTESIAN_POINT('Ctrl Pts',(26.6993615637294,-3.87831482231281,127.776712692716));
#65299=CARTESIAN_POINT('Ctrl Pts',(26.6916144361289,-3.96127737484887,127.886092678676));
#65300=CARTESIAN_POINT('Ctrl Pts',(26.6838673085285,-4.03954073810423,127.998778024289));
#65301=CARTESIAN_POINT('Ctrl Pts',(26.676122132029,-4.1177843908648,128.111434990291));
#65302=CARTESIAN_POINT('Ctrl Pts',(26.6683769555294,-4.19133098842976,128.227395337436));
#65303=CARTESIAN_POINT('Ctrl Pts',(26.6606317790299,-4.25990083556751,128.346225565615));
#65304=CARTESIAN_POINT('Ctrl Pts',(26.6528849935841,-4.32848492708036,128.465080479022));
#65305=CARTESIAN_POINT('Ctrl Pts',(26.6451382081383,-4.39209000396303,128.586806127822));
#65306=CARTESIAN_POINT('Ctrl Pts',(26.6373914226925,-4.45048139914605,128.710942747585));
#65307=CARTESIAN_POINT('Ctrl Pts',(26.629643615013,-4.50888049941597,128.835095747904));
#65308=CARTESIAN_POINT('Ctrl Pts',(26.6218958073334,-4.5620643888499,128.961659995719));
#65309=CARTESIAN_POINT('Ctrl Pts',(26.6141479996539,-4.60984614003261,129.090154787531));
#65310=CARTESIAN_POINT('Ctrl Pts',(26.606395229731,-4.65765849402371,129.218731876484));
#65311=CARTESIAN_POINT('Ctrl Pts',(26.5986424598082,-4.70006167527236,129.349241608434));
#65312=CARTESIAN_POINT('Ctrl Pts',(26.5908896898854,-4.73691828870304,129.481187088262));
#65313=CARTESIAN_POINT('Ctrl Pts',(26.5889109178643,-4.74632535690903,129.514864087115));
#65314=CARTESIAN_POINT('Ctrl Pts',(26.5869321458431,-4.75537135427362,129.548634555822));
#65315=CARTESIAN_POINT('Ctrl Pts',(26.584953373822,-4.764054528234,129.582490119308));
#65316=CARTESIAN_POINT('Ctrl Pts',(28.3348598006328,-4.76405452823408,129.582490119308));
#65317=CARTESIAN_POINT('Ctrl Pts',(28.3271967665533,-4.79779799805008,129.714055395992));
#65318=CARTESIAN_POINT('Ctrl Pts',(28.3195337324737,-4.82608509567171,129.847011134992));
#65319=CARTESIAN_POINT('Ctrl Pts',(28.3118706983942,-4.84881738849676,129.980860164918));
#65320=CARTESIAN_POINT('Ctrl Pts',(28.3040354879937,-4.8720604401812,130.117716571987));
#65321=CARTESIAN_POINT('Ctrl Pts',(28.2962002775933,-4.88949601255481,130.255506459426));
#65322=CARTESIAN_POINT('Ctrl Pts',(28.2883650671927,-4.90107474611519,130.393691169601));
#65323=CARTESIAN_POINT('Ctrl Pts',(28.2805298567922,-4.91265347967555,130.531875879776));
#65324=CARTESIAN_POINT('Ctrl Pts',(28.2726946463917,-4.91837537905588,130.670454966552));
#65325=CARTESIAN_POINT('Ctrl Pts',(28.2648594359912,-4.91824791518235,130.808889116708));
#65326=CARTESIAN_POINT('',(28.6101405640463,-4.91824967358338,130.802568747881));
#65327=CARTESIAN_POINT('Ctrl Pts',(28.6798592372483,-4.76405452823403,129.582490119308));
#65328=CARTESIAN_POINT('Ctrl Pts',(28.6714381530766,-4.80092883698196,129.726262489471));
#65329=CARTESIAN_POINT('Ctrl Pts',(28.6630170689048,-4.83133387643135,129.871873410875));
#65330=CARTESIAN_POINT('Ctrl Pts',(28.6545959847331,-4.85509965397195,130.018745945795));
#65331=CARTESIAN_POINT('Ctrl Pts',(28.6462045412791,-4.87878178020488,130.16510151553));
#65332=CARTESIAN_POINT('Ctrl Pts',(28.6378130978251,-4.89587119819743,130.312709571153));
#65333=CARTESIAN_POINT('Ctrl Pts',(28.6294216543711,-4.90624850217443,130.460982258593));
#65334=CARTESIAN_POINT('Ctrl Pts',(28.6229946242628,-4.91419650843435,130.574544726317));
#65335=CARTESIAN_POINT('Ctrl Pts',(28.6165675941545,-4.91820811362474,130.688496695248));
#65336=CARTESIAN_POINT('Ctrl Pts',(28.6101405640463,-4.91824967358338,130.802568747881));
#65337=CARTESIAN_POINT('Ctrl Pts',(28.6101405640087,-4.91824967358362,130.802568748549));
#65338=CARTESIAN_POINT('Ctrl Pts',(28.6022183214708,-4.91830090221393,130.943179023052));
#65339=CARTESIAN_POINT('Ctrl Pts',(28.594296078933,-4.91231781269187,131.083747826792));
#65340=CARTESIAN_POINT('Ctrl Pts',(28.5863738363952,-4.90033740463775,131.223736800972));
#65341=CARTESIAN_POINT('Ctrl Pts',(28.5784473695675,-4.88835060840305,131.363800419925));
#65342=CARTESIAN_POINT('Ctrl Pts',(28.5705209027398,-4.87036015166487,131.50328322899));
#65343=CARTESIAN_POINT('Ctrl Pts',(28.5625944359122,-4.84645477838846,131.641653364182));
#65344=CARTESIAN_POINT('Ctrl Pts',(28.5546623705243,-4.82253252045522,131.780121231889));
#65345=CARTESIAN_POINT('Ctrl Pts',(28.5467303051364,-4.7926870820956,131.917474499724));
#65346=CARTESIAN_POINT('Ctrl Pts',(28.5387982397485,-4.75705801439906,132.053192916212));
#65347=CARTESIAN_POINT('Ctrl Pts',(28.5308534277911,-4.72137169195654,132.189129427755));
#65348=CARTESIAN_POINT('Ctrl Pts',(28.5229086158336,-4.67988326406572,132.323425485124));
#65349=CARTESIAN_POINT('Ctrl Pts',(28.5149638038762,-4.63278206483875,132.455576352171));
#65350=CARTESIAN_POINT('Ctrl Pts',(28.5070120490144,-4.58563970427,132.58784270475));
#65351=CARTESIAN_POINT('Ctrl Pts',(28.4990602941526,-4.53287492916211,132.717959791013));
#65352=CARTESIAN_POINT('Ctrl Pts',(28.4911085392909,-4.47472447691595,132.845444623233));
#65353=CARTESIAN_POINT('Ctrl Pts',(28.4831421766297,-4.41646719917555,132.973163651916));
#65354=CARTESIAN_POINT('Ctrl Pts',(28.4751758139685,-4.35280463859669,133.09824043786));
#65355=CARTESIAN_POINT('Ctrl Pts',(28.4672094513074,-4.28401911945446,133.220217245483));
#65356=CARTESIAN_POINT('Ctrl Pts',(28.4621893922034,-4.24067344385904,133.297081783241));
#65357=CARTESIAN_POINT('Ctrl Pts',(28.4571693330995,-4.19529432823964,133.372715901334));
#65358=CARTESIAN_POINT('Ctrl Pts',(28.4521492739956,-4.14796084086393,133.447011545169));
#65359=CARTESIAN_POINT('Ctrl Pts',(28.4443749398765,-4.0746576509486,133.562069783888));
#65360=CARTESIAN_POINT('Ctrl Pts',(28.4366006057574,-3.99644741041953,133.67425797368));
#65361=CARTESIAN_POINT('Ctrl Pts',(28.4288262716383,-3.91358161057447,133.783129161759));
#65362=CARTESIAN_POINT('Ctrl Pts',(28.4210615186912,-3.8308179354218,133.891866175829));
#65363=CARTESIAN_POINT('Ctrl Pts',(28.4132967657442,-3.74341035150631,133.99729401379));
#65364=CARTESIAN_POINT('Ctrl Pts',(28.4055320127971,-3.6516548624765,134.0989925891));
#65365=CARTESIAN_POINT('Ctrl Pts',(28.3977749719121,-3.55999050629192,134.200590155951));
#65366=CARTESIAN_POINT('Ctrl Pts',(28.3900179310271,-3.46398709900981,134.298465542789));
#65367=CARTESIAN_POINT('Ctrl Pts',(28.382260890142,-3.36398211539322,134.392230095378));
#65368=CARTESIAN_POINT('Ctrl Pts',(28.3745096989019,-3.26405254631271,134.485923939389));
#65369=CARTESIAN_POINT('Ctrl Pts',(28.3667585076618,-3.16012769134259,134.575512853207));
#65370=CARTESIAN_POINT('Ctrl Pts',(28.3590073164217,-3.05258298181562,134.660643828331));
#65371=CARTESIAN_POINT('Ctrl Pts',(28.3512594196446,-2.94508398165919,134.74573862052));
#65372=CARTESIAN_POINT('Ctrl Pts',(28.3435115228675,-2.833968492879,134.826379000362));
#65373=CARTESIAN_POINT('Ctrl Pts',(28.3357636260904,-2.71964606867674,134.902251333975));
#65374=CARTESIAN_POINT('Ctrl Pts',(28.3280173500063,-2.60534755826111,134.978107796731));
#65375=CARTESIAN_POINT('Ctrl Pts',(28.3202710739223,-2.48784377227086,135.04919798103));
#65376=CARTESIAN_POINT('Ctrl Pts',(28.3125247978382,-2.36757404003198,135.115251039215));
#65377=CARTESIAN_POINT('Ctrl Pts',(28.3047784645728,-2.24730341998926,135.181304584989));
#65378=CARTESIAN_POINT('Ctrl Pts',(28.2970321313075,-2.1242671556406,135.242320742248));
#65379=CARTESIAN_POINT('Ctrl Pts',(28.2892857980421,-1.99892966125069,135.298074368115));
#65380=CARTESIAN_POINT('Ctrl Pts',(28.2815377300391,-1.8735640983976,135.35384047962));
#65381=CARTESIAN_POINT('Ctrl Pts',(28.2737896620362,-1.74589663717662,135.404341555771));
#65382=CARTESIAN_POINT('Ctrl Pts',(28.2660415940332,-1.61641179581979,135.449400549454));
#65383=CARTESIAN_POINT('Ctrl Pts',(28.2582852912913,-1.48678933643303,135.494507432372));
#65384=CARTESIAN_POINT('Ctrl Pts',(28.2505289885495,-1.35534600830051,135.534160550141));
#65385=CARTESIAN_POINT('Ctrl Pts',(28.2427726858077,-1.22258215879735,135.568232564574));
#65386=CARTESIAN_POINT('Ctrl Pts',(28.2350122432935,-1.08974744922992,135.602322764267));
#65387=CARTESIAN_POINT('Ctrl Pts',(28.2272518007793,-0.955591196156083,
135.630825843896));
#65388=CARTESIAN_POINT('Ctrl Pts',(28.2194913582651,-0.820623093209166,
135.653665805053));
#65389=CARTESIAN_POINT('Ctrl Pts',(28.2117184579997,-0.685438327481676,
135.676542430944));
#65390=CARTESIAN_POINT('Ctrl Pts',(28.2039455577342,-0.549439495665727,
135.693737722699));
#65391=CARTESIAN_POINT('Ctrl Pts',(28.1961726574688,-0.41314145544745,135.70522760212));
#65392=CARTESIAN_POINT('Ctrl Pts',(28.1886823217068,-0.281798192305892,
135.716299795483));
#65393=CARTESIAN_POINT('Ctrl Pts',(28.1811919859448,-0.150177404762075,
135.722074173482));
#65394=CARTESIAN_POINT('Ctrl Pts',(28.1737016501829,-0.0187370849083707,
135.722574926047));
#65395=CARTESIAN_POINT('Ctrl Pts',(28.1659273160638,0.117686834623777,135.723094664799));
#65396=CARTESIAN_POINT('Ctrl Pts',(28.1581529819447,0.254348481427725,135.717934631344));
#65397=CARTESIAN_POINT('Ctrl Pts',(28.1503786478256,0.390735884276925,135.707064823536));
#65398=CARTESIAN_POINT('Ctrl Pts',(28.1426138948785,0.526955201841035,135.696208411795));
#65399=CARTESIAN_POINT('Ctrl Pts',(28.1348491419315,0.662900561944117,135.679656257572));
#65400=CARTESIAN_POINT('Ctrl Pts',(28.1270843889844,0.798058536678102,135.657430330081));
#65401=CARTESIAN_POINT('Ctrl Pts',(28.1193273480994,0.933082270606188,135.635226477696));
#65402=CARTESIAN_POINT('Ctrl Pts',(28.1115703072144,1.0673197921771,135.607360129517));
#65403=CARTESIAN_POINT('Ctrl Pts',(28.1038132663294,1.20026170222267,135.573905135513));
#65404=CARTESIAN_POINT('Ctrl Pts',(28.0960620750893,1.33310335974009,135.54047537018));
#65405=CARTESIAN_POINT('Ctrl Pts',(28.0883108838492,1.46465097284247,135.501465442639));
#65406=CARTESIAN_POINT('Ctrl Pts',(28.0805596926091,1.59440461567362,135.457000404184));
#65407=CARTESIAN_POINT('Ctrl Pts',(28.072811795832,1.7241031097451,135.412554264556));
#65408=CARTESIAN_POINT('Ctrl Pts',(28.0650638990549,1.85200878099351,135.362657751947));
#65409=CARTESIAN_POINT('Ctrl Pts',(28.0573160022778,1.97763638683973,135.307485908289));
#65410=CARTESIAN_POINT('Ctrl Pts',(28.0495697261937,2.10323771409902,135.252325605391));
#65411=CARTESIAN_POINT('Ctrl Pts',(28.0418234501096,2.22656156604584,135.191892323445));
#65412=CARTESIAN_POINT('Ctrl Pts',(28.0340771740255,2.34714260264339,135.126409282882));
#65413=CARTESIAN_POINT('Ctrl Pts',(28.0263308407602,2.46772452934292,135.060925758937));
#65414=CARTESIAN_POINT('Ctrl Pts',(28.0185845074948,2.58556325672055,134.990392588573));
#65415=CARTESIAN_POINT('Ctrl Pts',(28.0108381742294,2.70021833844389,134.91507880144));
#65416=CARTESIAN_POINT('Ctrl Pts',(28.0030901062264,2.81489909637797,134.839748148306));
#65417=CARTESIAN_POINT('Ctrl Pts',(27.9953420382235,2.92639446324936,134.759634962667));
#65418=CARTESIAN_POINT('Ctrl Pts',(27.9875939702205,3.03429359036853,134.675051185145));
#65419=CARTESIAN_POINT('Ctrl Pts',(27.9798376674786,3.14230739396372,134.590377510978));
#65420=CARTESIAN_POINT('Ctrl Pts',(27.9720813647368,3.24671701451504,134.501223995088));
#65421=CARTESIAN_POINT('Ctrl Pts',(27.9643250619949,3.347144868821,134.407942764489));
#65422=CARTESIAN_POINT('Ctrl Pts',(27.9565646194808,3.44762632449677,134.31461174689));
#65423=CARTESIAN_POINT('Ctrl Pts',(27.9488041769666,3.54412150437218,134.217148902442));
#65424=CARTESIAN_POINT('Ctrl Pts',(27.9410437344524,3.63629096697756,134.11594197184));
#65425=CARTESIAN_POINT('Ctrl Pts',(27.933270834187,3.72860838818661,134.014572574889));
#65426=CARTESIAN_POINT('Ctrl Pts',(27.9254979339216,3.81658596468831,133.909447381207));
#65427=CARTESIAN_POINT('Ctrl Pts',(27.9177250336562,3.89992514565808,133.800986540294));
#65428=CARTESIAN_POINT('Ctrl Pts',(27.9102346978941,3.98023473748121,133.696468524143));
#65429=CARTESIAN_POINT('Ctrl Pts',(27.9027443621321,4.05623713591522,133.588853420243));
#65430=CARTESIAN_POINT('Ctrl Pts',(27.89525402637,4.12770513672061,133.478539625559));
#65431=CARTESIAN_POINT('Ctrl Pts',(27.8874796922509,4.20188286849857,133.364043249821));
#65432=CARTESIAN_POINT('Ctrl Pts',(27.8797053581318,4.27141054445722,133.246276811783));
#65433=CARTESIAN_POINT('Ctrl Pts',(27.8719310240127,4.33598618998724,133.125654830444));
#65434=CARTESIAN_POINT('Ctrl Pts',(27.8641662710656,4.40048225180552,133.005181504917));
#65435=CARTESIAN_POINT('Ctrl Pts',(27.8564015181186,4.46003824346202,132.881859979622));
#65436=CARTESIAN_POINT('Ctrl Pts',(27.8486367651714,4.51439512795429,132.756134090898));
#65437=CARTESIAN_POINT('Ctrl Pts',(27.8408797242864,4.56869802442259,132.630533074899));
#65438=CARTESIAN_POINT('Ctrl Pts',(27.8331226834014,4.61781193582661,132.502532804333));
#65439=CARTESIAN_POINT('Ctrl Pts',(27.8253656425164,4.66152365154309,132.372601768858));
#65440=CARTESIAN_POINT('Ctrl Pts',(27.8176144512763,4.70520240391442,132.242768715388));
#65441=CARTESIAN_POINT('Ctrl Pts',(27.8098632600362,4.74348694516597,132.111008164157));
#65442=CARTESIAN_POINT('Ctrl Pts',(27.8021120687961,4.7762122623572,131.977808310226));
#65443=CARTESIAN_POINT('Ctrl Pts',(27.7943641720191,4.80892367041582,131.844665069785));
#65444=CARTESIAN_POINT('Ctrl Pts',(27.7866162752419,4.83608046079466,131.710084122231));
#65445=CARTESIAN_POINT('Ctrl Pts',(27.7788683784649,4.85756761576195,131.57456833033));
#65446=CARTESIAN_POINT('Ctrl Pts',(27.7711221023808,4.87905027607967,131.43908088541));
#65447=CARTESIAN_POINT('Ctrl Pts',(27.7633758262966,4.89486559874909,131.302659370997));
#65448=CARTESIAN_POINT('Ctrl Pts',(27.7556295502125,4.90494985778331,131.165815946938));
#65449=CARTESIAN_POINT('Ctrl Pts',(27.7478832169472,4.91503419125721,131.028971512732));
#65450=CARTESIAN_POINT('Ctrl Pts',(27.7401368836819,4.91938734794547,130.891705552573));
#65451=CARTESIAN_POINT('Ctrl Pts',(27.7323905504165,4.91799759811043,130.754534043532));
#65452=CARTESIAN_POINT('Ctrl Pts',(27.7246424824135,4.91660753705056,130.617331815881));
#65453=CARTESIAN_POINT('Ctrl Pts',(27.7168944144105,4.90947201426901,130.480224472309));
#65454=CARTESIAN_POINT('Ctrl Pts',(27.7091463464075,4.89663140049338,130.343726282977));
#65455=CARTESIAN_POINT('Ctrl Pts',(27.7013900436656,4.88377713956064,130.207083021746));
#65456=CARTESIAN_POINT('Ctrl Pts',(27.6936337409238,4.86520571193757,130.071050597907));
#65457=CARTESIAN_POINT('Ctrl Pts',(27.685877438182,4.84100927911253,129.936137016155));
#65458=CARTESIAN_POINT('Ctrl Pts',(27.6781169956678,4.81679993192274,129.801151426963));
#65459=CARTESIAN_POINT('Ctrl Pts',(27.6703565531536,4.78695968234598,129.667286251162));
#65460=CARTESIAN_POINT('Ctrl Pts',(27.6625961106394,4.75163127120419,129.535036653791));
#65461=CARTESIAN_POINT('Ctrl Pts',(27.654823210374,4.71624614776048,129.402574757625));
#65462=CARTESIAN_POINT('Ctrl Pts',(27.6470503101086,4.67535537408643,129.271733995848));
#65463=CARTESIAN_POINT('Ctrl Pts',(27.6392774098431,4.62915105984179,129.142992648793));
#65464=CARTESIAN_POINT('Ctrl Pts',(27.6317870740811,4.58462638880153,129.018931373982));
#65465=CARTESIAN_POINT('Ctrl Pts',(27.624296738319,4.53516790688726,128.896819811377));
#65466=CARTESIAN_POINT('Ctrl Pts',(27.616806402557,4.48098798730894,128.77706445763));
#65467=CARTESIAN_POINT('Ctrl Pts',(27.6090320684379,4.42475381961234,128.652768543246));
#65468=CARTESIAN_POINT('Ctrl Pts',(27.6012577343187,4.36325498713541,128.530617303972));
#65469=CARTESIAN_POINT('Ctrl Pts',(27.5934834001997,4.29667701179976,128.411088857241));
#65470=CARTESIAN_POINT('Ctrl Pts',(27.5857186472526,4.23018108786846,128.291707718638));
#65471=CARTESIAN_POINT('Ctrl Pts',(27.5779538943055,4.15861866421749,128.174943279426));
#65472=CARTESIAN_POINT('Ctrl Pts',(27.5701891413584,4.0822231371006,128.061253379155));
#65473=CARTESIAN_POINT('Ctrl Pts',(27.5624321004734,4.00590348709822,127.947676397296));
#65474=CARTESIAN_POINT('Ctrl Pts',(27.5546750595884,3.92476050310255,127.837168199832));
#65475=CARTESIAN_POINT('Ctrl Pts',(27.5469180187034,3.8390730931821,127.730161397004));
#65476=CARTESIAN_POINT('Ctrl Pts',(27.5391668274633,3.75345030080436,127.623235288838));
#65477=CARTESIAN_POINT('Ctrl Pts',(27.5314156362232,3.66329014709929,127.519805623638));
#65478=CARTESIAN_POINT('Ctrl Pts',(27.5236644449831,3.56891417087302,127.420275112819));
#65479=CARTESIAN_POINT('Ctrl Pts',(27.515916548206,3.47457830695383,127.320786905121));
#65480=CARTESIAN_POINT('Ctrl Pts',(27.508168651429,3.37603045278773,127.22519483878));
#65481=CARTESIAN_POINT('Ctrl Pts',(27.5004207546519,3.27363151116684,127.133867491078));
#65482=CARTESIAN_POINT('Ctrl Pts',(27.4926744785678,3.17125398919736,127.042559247089));
#65483=CARTESIAN_POINT('Ctrl Pts',(27.4849282024837,3.06502727367775,126.955514207393));
#65484=CARTESIAN_POINT('Ctrl Pts',(27.4771819263996,2.95534781373978,126.873062821377));
#65485=CARTESIAN_POINT('Ctrl Pts',(27.4694355931343,2.84566754417265,126.790610826722));
#65486=CARTESIAN_POINT('Ctrl Pts',(27.4616892598689,2.73253479183859,126.712752788339));
#65487=CARTESIAN_POINT('Ctrl Pts',(27.4539429266035,2.61637732265057,126.639777472998));
#65488=CARTESIAN_POINT('Ctrl Pts',(27.4461948586006,2.50019384080285,126.566785815341));
#65489=CARTESIAN_POINT('Ctrl Pts',(27.4384467905975,2.3809846252153,126.498679264512));
#65490=CARTESIAN_POINT('Ctrl Pts',(27.4306987225946,2.25920416730621,126.435701831059));
#65491=CARTESIAN_POINT('Ctrl Pts',(27.4229424198527,2.13729427967708,126.37265746444));
#65492=CARTESIAN_POINT('Ctrl Pts',(27.4151861171109,2.01280803860045,126.314753284608));
#65493=CARTESIAN_POINT('Ctrl Pts',(27.407429814369,1.88622265834908,126.262186342438));
#65494=CARTESIAN_POINT('Ctrl Pts',(27.3996693718548,1.75956971566852,126.209591343709));
#65495=CARTESIAN_POINT('Ctrl Pts',(27.3919089293407,1.6308157682231,126.162339393438));
#65496=CARTESIAN_POINT('Ctrl Pts',(27.3841484868265,1.50045456728431,126.120578048529));
#65497=CARTESIAN_POINT('Ctrl Pts',(27.376375586561,1.36988409897321,126.078749664602));
#65498=CARTESIAN_POINT('Ctrl Pts',(27.3686026862956,1.23770159850452,126.042429602877));
#65499=CARTESIAN_POINT('Ctrl Pts',(27.3608297860301,1.1044132966301,126.01171475826));
#65500=CARTESIAN_POINT('Ctrl Pts',(27.3533394502681,0.975970360262141,125.98211647561));
#65501=CARTESIAN_POINT('Ctrl Pts',(27.3458491145061,0.84650092669847,125.957723014853));
#65502=CARTESIAN_POINT('Ctrl Pts',(27.3383587787441,0.716461785993515,125.938575421761));
#65503=CARTESIAN_POINT('Ctrl Pts',(27.330584444625,0.581492171743992,125.918701841858));
#65504=CARTESIAN_POINT('Ctrl Pts',(27.322810110506,0.445481253493059,125.904416822821));
#65505=CARTESIAN_POINT('Ctrl Pts',(27.3150357763869,0.308931564110554,125.895822713954));
#65506=CARTESIAN_POINT('Ctrl Pts',(27.3072710234398,0.172550160016417,125.887239196558));
#65507=CARTESIAN_POINT('Ctrl Pts',(27.2995062704927,0.0356316923748154,
125.884332658805));
#65508=CARTESIAN_POINT('Ctrl Pts',(27.2917415175457,-0.101312489059482,
125.887154211276));
#65509=CARTESIAN_POINT('Ctrl Pts',(27.2839844766607,-0.238120655601647,
125.889972961341));
#65510=CARTESIAN_POINT('Ctrl Pts',(27.2762274357757,-0.37495409675927,125.898508471823));
#65511=CARTESIAN_POINT('Ctrl Pts',(27.2684703948908,-0.511298088661625,
125.912759925867));
#65512=CARTESIAN_POINT('Ctrl Pts',(27.2607192036507,-0.647539262499085,
125.927000632779));
#65513=CARTESIAN_POINT('Ctrl Pts',(27.2529680124105,-0.783291334474043,
125.946948663108));
#65514=CARTESIAN_POINT('Ctrl Pts',(27.2452168211705,-0.918041692488448,
125.972551172508));
#65515=CARTESIAN_POINT('Ctrl Pts',(27.2374689243934,-1.05273477800685,125.998142800158));
#65516=CARTESIAN_POINT('Ctrl Pts',(27.2297210276163,-1.18642661306955,126.029384054065));
#65517=CARTESIAN_POINT('Ctrl Pts',(27.2219731308392,-1.31861202639542,126.066170521512));
#65518=CARTESIAN_POINT('Ctrl Pts',(27.2142268547551,-1.4507697893824,126.102949294023));
#65519=CARTESIAN_POINT('Ctrl Pts',(27.206480578671,-1.58142138099239,126.145270868138));
#65520=CARTESIAN_POINT('Ctrl Pts',(27.1987343025869,-1.7100744943594,126.192980315938));
#65521=CARTESIAN_POINT('Ctrl Pts',(27.1909879693215,-1.83872855741499,126.240690115919));
#65522=CARTESIAN_POINT('Ctrl Pts',(27.1832416360561,-1.96538374621911,126.29378773301));
#65523=CARTESIAN_POINT('Ctrl Pts',(27.1754953027908,-2.08956589518471,126.352069361125));
#65524=CARTESIAN_POINT('Ctrl Pts',(27.1677472347878,-2.2137758538802,126.410364041006));
#65525=CARTESIAN_POINT('Ctrl Pts',(27.1599991667849,-2.33551131684215,126.473844875942));
#65526=CARTESIAN_POINT('Ctrl Pts',(27.1522510987819,-2.45432132737185,126.542261383092));
#65527=CARTESIAN_POINT('Ctrl Pts',(27.1444947960401,-2.57325761059524,126.61075060412));
#65528=CARTESIAN_POINT('Ctrl Pts',(27.1367384932982,-2.68926189106693,126.684185780783));
#65529=CARTESIAN_POINT('Ctrl Pts',(27.1289821905564,-2.80191043833319,126.762271930011));
#65530=CARTESIAN_POINT('Ctrl Pts',(27.1212217480422,-2.91461910952122,126.840399756168));
#65531=CARTESIAN_POINT('Ctrl Pts',(27.1134613055281,-3.02396816711284,126.923183265341));
#65532=CARTESIAN_POINT('Ctrl Pts',(27.1057008630139,-3.12956658268446,127.01028680871));
#65533=CARTESIAN_POINT('Ctrl Pts',(27.0979279627485,-3.23533451420719,127.09753017842));
#65534=CARTESIAN_POINT('Ctrl Pts',(27.090155062483,-3.3373394810141,127.189107179139));
#65535=CARTESIAN_POINT('Ctrl Pts',(27.0823821622176,-3.43522633259145,127.284644278659));
#65536=CARTESIAN_POINT('Ctrl Pts',(27.0748918264555,-3.52955475055266,127.376708363969));
#65537=CARTESIAN_POINT('Ctrl Pts',(27.0674014906934,-3.62005905125558,127.472449403809));
#65538=CARTESIAN_POINT('Ctrl Pts',(27.0599111549313,-3.70645779554588,127.571505274013));
#65539=CARTESIAN_POINT('Ctrl Pts',(27.0522003402356,-3.79539969726117,127.673476865666));
#65540=CARTESIAN_POINT('Ctrl Pts',(27.0444895255398,-3.88028405432929,127.779298092409));
#65541=CARTESIAN_POINT('Ctrl Pts',(27.0367787108441,-3.96075487053853,127.88860961345));
#65542=CARTESIAN_POINT('Ctrl Pts',(27.0290772170675,-4.04112841272462,127.997788997501));
#65543=CARTESIAN_POINT('Ctrl Pts',(27.0213757232908,-4.11709879048239,128.110449968231));
#65544=CARTESIAN_POINT('Ctrl Pts',(27.0136742295142,-4.1883479812841,128.226197657206));
#65545=CARTESIAN_POINT('Ctrl Pts',(27.0059817100385,-4.25951414771428,128.341810469152));
#65546=CARTESIAN_POINT('Ctrl Pts',(26.9982891905628,-4.32596987231821,128.460502502148));
#65547=CARTESIAN_POINT('Ctrl Pts',(26.9905966710871,-4.38743890312703,128.581847865335));
#65548=CARTESIAN_POINT('Ctrl Pts',(26.9829093560516,-4.44886634653436,128.703111131274));
#65549=CARTESIAN_POINT('Ctrl Pts',(26.9752220410162,-4.50531362653266,128.827023804066));
#65550=CARTESIAN_POINT('Ctrl Pts',(26.9675347259807,-4.55654918213162,128.953133291354));
#65551=CARTESIAN_POINT('Ctrl Pts',(26.9598507877126,-4.60776223175137,129.079187383174));
#65552=CARTESIAN_POINT('Ctrl Pts',(26.9521668494444,-4.65376796085912,129.207436002332));
#65553=CARTESIAN_POINT('Ctrl Pts',(26.9444829111763,-4.69438213913888,129.337404791976));
#65554=CARTESIAN_POINT('Ctrl Pts',(26.9396901847889,-4.71971454514624,129.418470623835));
#65555=CARTESIAN_POINT('Ctrl Pts',(26.9348974584015,-4.74295035070058,129.500205251406));
#65556=CARTESIAN_POINT('Ctrl Pts',(26.9301047320141,-4.76405452823399,129.582490119308));
#65557=CARTESIAN_POINT('Origin',(213.235140564004,0.,130.804360617566));
#65558=CARTESIAN_POINT('',(24.8346867982621,-4.76405452823407,129.582490119308));
#65559=CARTESIAN_POINT('',(25.1802307898757,-4.7640545282341,129.582490119308));
#65560=CARTESIAN_POINT('',(213.235140564004,-4.76405452823405,129.582490119308));
#65561=CARTESIAN_POINT('',(26.5148594359565,-4.91824992681965,130.803512184618));
#65562=CARTESIAN_POINT('Ctrl Pts',(26.5148594359565,-4.91824992681965,130.803512184618));
#65563=CARTESIAN_POINT('Ctrl Pts',(26.5071213653779,-4.91827335442518,130.93931881427));
#65564=CARTESIAN_POINT('Ctrl Pts',(26.4993832947993,-4.91266751947957,131.075349760757));
#65565=CARTESIAN_POINT('Ctrl Pts',(26.4916452242207,-4.90140271489009,131.211097005129));
#65566=CARTESIAN_POINT('Ctrl Pts',(26.4839166302215,-4.89015170596362,131.346678003987));
#65567=CARTESIAN_POINT('Ctrl Pts',(26.4761880362222,-4.87325554665902,131.481975602133));
#65568=CARTESIAN_POINT('Ctrl Pts',(26.468459442223,-4.85073650515059,131.616480325552));
#65569=CARTESIAN_POINT('Ctrl Pts',(26.4607384194964,-4.82823952429199,131.750853282191));
#65570=CARTESIAN_POINT('Ctrl Pts',(26.4530173967699,-4.80013068620106,131.884434522536));
#65571=CARTESIAN_POINT('Ctrl Pts',(26.4452963740434,-4.76648413899611,132.01671865676));
#65572=CARTESIAN_POINT('Ctrl Pts',(26.4375810242629,-4.73286231326318,132.148905596508));
#65573=CARTESIAN_POINT('Ctrl Pts',(26.4298656744825,-4.69371097281804,132.279796945508));
#65574=CARTESIAN_POINT('Ctrl Pts',(26.422150324702,-4.64915544975939,132.408896895271));
#65575=CARTESIAN_POINT('Ctrl Pts',(26.4144380056585,-4.60461742896188,132.537946132107));
#65576=CARTESIAN_POINT('Ctrl Pts',(26.4067256866149,-4.55467957499654,132.665204996173));
#65577=CARTESIAN_POINT('Ctrl Pts',(26.3990133675713,-4.49951716911133,132.790192510595));
#65578=CARTESIAN_POINT('Ctrl Pts',(26.3913024431291,-4.44436473812009,132.915157423806));
#65579=CARTESIAN_POINT('Ctrl Pts',(26.3835915186868,-4.38398979346227,133.037851442993));
#65580=CARTESIAN_POINT('Ctrl Pts',(26.3758805942445,-4.31861570996299,133.1578137002));
#65581=CARTESIAN_POINT('Ctrl Pts',(26.3681693541893,-4.25323895066184,133.277780867537));
#65582=CARTESIAN_POINT('Ctrl Pts',(26.3604581141342,-4.18286283443898,133.39501570358));
#65583=CARTESIAN_POINT('Ctrl Pts',(26.352746874079,-4.10775640988115,133.509082477495));
#65584=CARTESIAN_POINT('Ctrl Pts',(26.3450336083111,-4.03263025515848,133.623179216308));
#65585=CARTESIAN_POINT('Ctrl Pts',(26.3373203425433,-3.95277153721105,133.734105907581));
#65586=CARTESIAN_POINT('Ctrl Pts',(26.3296070767754,-3.86849202061374,133.841456689301));
#65587=CARTESIAN_POINT('Ctrl Pts',(26.3218855356824,-3.78412208312014,133.948922644366));
#65588=CARTESIAN_POINT('Ctrl Pts',(26.3141639945894,-3.69532211974546,134.052804717578));
#65589=CARTESIAN_POINT('Ctrl Pts',(26.3064424534963,-3.60244378223147,134.15273064765));
#65590=CARTESIAN_POINT('Ctrl Pts',(26.298716449483,-3.50951176260749,134.252714333221));
#65591=CARTESIAN_POINT('Ctrl Pts',(26.2909904454696,-3.41249695400789,134.348737043806));
#65592=CARTESIAN_POINT('Ctrl Pts',(26.2832644414563,-3.31178627641337,134.440464950758));
#65593=CARTESIAN_POINT('Ctrl Pts',(26.2755266750374,-3.21092227249013,134.532332508278));
#65594=CARTESIAN_POINT('Ctrl Pts',(26.2677889086186,-3.10635146373076,134.61989194957));
#65595=CARTESIAN_POINT('Ctrl Pts',(26.2600511421997,-2.99849258607423,134.702850745007));
#65596=CARTESIAN_POINT('Ctrl Pts',(26.2547531880171,-2.92464292958739,134.759651619249));
#65597=CARTESIAN_POINT('Ctrl Pts',(26.2494552338345,-2.849252461346,134.81429661822));
#65598=CARTESIAN_POINT('Ctrl Pts',(26.244157279652,-2.77246245245571,134.866704154519));
#65599=CARTESIAN_POINT('Ctrl Pts',(26.2363829455329,-2.65977910987732,134.943608122259));
#65600=CARTESIAN_POINT('Ctrl Pts',(26.2286086114138,-2.54371505817791,135.01594184576));
#65601=CARTESIAN_POINT('Ctrl Pts',(26.2208342772947,-2.42467745042779,135.08339349006));
#65602=CARTESIAN_POINT('Ctrl Pts',(26.2130695243476,-2.30578654589053,135.150762006237));
#65603=CARTESIAN_POINT('Ctrl Pts',(26.2053047714005,-2.18392971373467,135.213260223812));
#65604=CARTESIAN_POINT('Ctrl Pts',(26.1975400184535,-2.05954444631006,135.270618529529));
#65605=CARTESIAN_POINT('Ctrl Pts',(26.1897829775685,-1.93528272008642,135.327919866169));
#65606=CARTESIAN_POINT('Ctrl Pts',(26.1820259366835,-1.80849790888738,135.380091287538));
#65607=CARTESIAN_POINT('Ctrl Pts',(26.1742688957985,-1.6796532509913,135.426908401952));
#65608=CARTESIAN_POINT('Ctrl Pts',(26.1665177045584,-1.55090575585419,135.473690211217));
#65609=CARTESIAN_POINT('Ctrl Pts',(26.1587665133182,-1.42010187183409,135.515125617392));
#65610=CARTESIAN_POINT('Ctrl Pts',(26.1510153220781,-1.28772569354826,135.551037939723));
#65611=CARTESIAN_POINT('Ctrl Pts',(26.143267425301,-1.15540577866928,135.586934998358));
#65612=CARTESIAN_POINT('Ctrl Pts',(26.1355195285239,-1.02151527519313,135.617313539913));
#65613=CARTESIAN_POINT('Ctrl Pts',(26.1277716317469,-0.886554140963911,
135.642046512458));
#65614=CARTESIAN_POINT('Ctrl Pts',(26.1200253556628,-0.751621237694911,
135.666774311399));
#65615=CARTESIAN_POINT('Ctrl Pts',(26.1122790795787,-0.615618533444684,
135.685858819836));
#65616=CARTESIAN_POINT('Ctrl Pts',(26.1045328034946,-0.479056511322725,
135.699224039712));
#65617=CARTESIAN_POINT('Ctrl Pts',(26.0967864702293,-0.342493481130756,
135.712589358246));
#65618=CARTESIAN_POINT('Ctrl Pts',(26.0890401369639,-0.205371513934557,
135.720235265893));
#65619=CARTESIAN_POINT('Ctrl Pts',(26.0812938036986,-0.0682061567346617,
135.722137654265));
#65620=CARTESIAN_POINT('Ctrl Pts',(26.0735457356956,0.0689899176957541,
135.724040468664));
#65621=CARTESIAN_POINT('Ctrl Pts',(26.0657976676927,0.206229010612564,135.720197198936));
#65622=CARTESIAN_POINT('Ctrl Pts',(26.0580495996897,0.34299603116267,135.710635863117));
#65623=CARTESIAN_POINT('Ctrl Pts',(26.0502932969479,0.479908409329951,135.701064365397));
#65624=CARTESIAN_POINT('Ctrl Pts',(26.042536994206,0.616347322247349,135.685762688976));
#65625=CARTESIAN_POINT('Ctrl Pts',(26.0347806914642,0.751802699891313,135.66481077809));
#65626=CARTESIAN_POINT('Ctrl Pts',(26.02702024895,0.887330374148809,135.643847684538));
#65627=CARTESIAN_POINT('Ctrl Pts',(26.0192598064359,1.02187308379769,135.617228423329));
#65628=CARTESIAN_POINT('Ctrl Pts',(26.0114993639217,1.15493238100874,135.585083811581));
#65629=CARTESIAN_POINT('Ctrl Pts',(26.0037264636563,1.2882052768163,135.55288759845));
#65630=CARTESIAN_POINT('Ctrl Pts',(25.9959535633908,1.41998962550569,135.515148417823));
#65631=CARTESIAN_POINT('Ctrl Pts',(25.9881806631254,1.54980267437654,135.47204684663));
#65632=CARTESIAN_POINT('Ctrl Pts',(25.9806903273633,1.67489669194231,135.430512126116));
#65633=CARTESIAN_POINT('Ctrl Pts',(25.9731999916013,1.79815995662908,135.383998227827));
#65634=CARTESIAN_POINT('Ctrl Pts',(25.9657096558392,1.91918099247313,135.332707709014));
#65635=CARTESIAN_POINT('Ctrl Pts',(25.9579353217201,2.04479057767405,135.279472494593));
#65636=CARTESIAN_POINT('Ctrl Pts',(25.950160987601,2.16838244281859,135.220922665195));
#65637=CARTESIAN_POINT('Ctrl Pts',(25.9423866534819,2.28947415614256,135.157232215816));
#65638=CARTESIAN_POINT('Ctrl Pts',(25.9346219005349,2.41041663475197,135.093620259225));
#65639=CARTESIAN_POINT('Ctrl Pts',(25.9268571475877,2.5288647495377,135.02488046837));
#65640=CARTESIAN_POINT('Ctrl Pts',(25.9190923946406,2.64435519193146,134.951235185407));
#65641=CARTESIAN_POINT('Ctrl Pts',(25.9113353537556,2.75973092759032,134.877663047976));
#65642=CARTESIAN_POINT('Ctrl Pts',(25.9035783128706,2.87215450930422,134.79919532319));
#65643=CARTESIAN_POINT('Ctrl Pts',(25.8958212719855,2.98118675838969,134.716100457343));
#65644=CARTESIAN_POINT('Ctrl Pts',(25.8880700807454,3.09013678540752,134.633068253982));
#65645=CARTESIAN_POINT('Ctrl Pts',(25.8803188895053,3.19570026051014,134.545416090952));
#65646=CARTESIAN_POINT('Ctrl Pts',(25.8725676982652,3.29746687220816,134.453455750498));
#65647=CARTESIAN_POINT('Ctrl Pts',(25.8648198014881,3.39919023038121,134.361534495643));
#65648=CARTESIAN_POINT('Ctrl Pts',(25.857071904711,3.49711964534237,134.26530896684));
#65649=CARTESIAN_POINT('Ctrl Pts',(25.8493240079339,3.59087798527832,134.165131118112));
#65650=CARTESIAN_POINT('Ctrl Pts',(25.8415777318498,3.68461671299101,134.064974224431));
#65651=CARTESIAN_POINT('Ctrl Pts',(25.8338314557658,3.77418583413915,133.960866940524));
#65652=CARTESIAN_POINT('Ctrl Pts',(25.8260851796817,3.85924548081293,133.853197671481));
#65653=CARTESIAN_POINT('Ctrl Pts',(25.8183388464164,3.94430575537748,133.745527607648));
#65654=CARTESIAN_POINT('Ctrl Pts',(25.810592513151,4.02485624668364,133.634295812995));
#65655=CARTESIAN_POINT('Ctrl Pts',(25.8028461798856,4.10059800591613,133.519923000642));
#65656=CARTESIAN_POINT('Ctrl Pts',(25.7950981118826,4.17635672699065,133.40552457529));
#65657=CARTESIAN_POINT('Ctrl Pts',(25.7873500438797,4.24730435729436,133.28798405844));
#65658=CARTESIAN_POINT('Ctrl Pts',(25.7796019758767,4.31318605000646,133.167749955049));
#65659=CARTESIAN_POINT('Ctrl Pts',(25.7718456731348,4.37913776256549,133.047388065422));
#65660=CARTESIAN_POINT('Ctrl Pts',(25.764089370393,4.4400125939639,132.924327213964));
#65661=CARTESIAN_POINT('Ctrl Pts',(25.7563330676512,4.49560209824486,132.799039748844));
#65662=CARTESIAN_POINT('Ctrl Pts',(25.748572625137,4.55122127231809,132.673685414031));
#65663=CARTESIAN_POINT('Ctrl Pts',(25.7408121826228,4.60154935491937,132.546102461061));
#65664=CARTESIAN_POINT('Ctrl Pts',(25.7330517401086,4.64642698297014,132.416780958056));
#65665=CARTESIAN_POINT('Ctrl Pts',(25.7252788398432,4.69137665257352,132.287251856695));
#65666=CARTESIAN_POINT('Ctrl Pts',(25.7175059395777,4.73085827056162,132.155979002856));
#65667=CARTESIAN_POINT('Ctrl Pts',(25.7097330393123,4.76476282179153,132.023466156301));
#65668=CARTESIAN_POINT('Ctrl Pts',(25.7022427035503,4.79743485718374,131.895770485497));
#65669=CARTESIAN_POINT('Ctrl Pts',(25.6947523677883,4.82492820264624,131.766923711729));
#65670=CARTESIAN_POINT('Ctrl Pts',(25.6872620320263,4.84719086252336,131.637381508523));
#65671=CARTESIAN_POINT('Ctrl Pts',(25.6794876979072,4.87029761791637,131.502927673307));
#65672=CARTESIAN_POINT('Ctrl Pts',(25.6717133637881,4.88784241023631,131.367298723909));
#65673=CARTESIAN_POINT('Ctrl Pts',(25.663939029669,4.89971086024828,131.230994592379));
#65674=CARTESIAN_POINT('Ctrl Pts',(25.6561742767219,4.91156468345633,131.09485844351));
#65675=CARTESIAN_POINT('Ctrl Pts',(25.6484095237748,4.91775604989592,130.958049153896));
#65676=CARTESIAN_POINT('Ctrl Pts',(25.6406447708277,4.91822159272069,130.821076699523));
#65677=CARTESIAN_POINT('Ctrl Pts',(25.6328877299427,4.91868667316176,130.684240288123));
#65678=CARTESIAN_POINT('Ctrl Pts',(25.6251306890577,4.91343724599223,130.547241422898));
#65679=CARTESIAN_POINT('Ctrl Pts',(25.6173736481727,4.90246177587857,130.410594699095));
#65680=CARTESIAN_POINT('Ctrl Pts',(25.6096224569325,4.89149458245229,130.274051021649));
#65681=CARTESIAN_POINT('Ctrl Pts',(25.6018712656924,4.87480997208041,130.13785934519));
#65682=CARTESIAN_POINT('Ctrl Pts',(25.5941200744523,4.85244847261533,130.002533402318));
#65683=CARTESIAN_POINT('Ctrl Pts',(25.5863721776752,4.83009647738406,129.86726497658));
#65684=CARTESIAN_POINT('Ctrl Pts',(25.5786242808982,4.80207245559914,129.732861937511));
#65685=CARTESIAN_POINT('Ctrl Pts',(25.5708763841211,4.76846866719055,129.599831816531));
#65686=CARTESIAN_POINT('Ctrl Pts',(25.563130108037,4.73487190797012,129.466829522585));
#65687=CARTESIAN_POINT('Ctrl Pts',(25.5553838319529,4.69569779937562,129.335199954321));
#65688=CARTESIAN_POINT('Ctrl Pts',(25.5476375558688,4.65108941070256,129.205438994674));
#65689=CARTESIAN_POINT('Ctrl Pts',(25.5398912226034,4.60648069274045,129.075677077162));
#65690=CARTESIAN_POINT('Ctrl Pts',(25.5321448893381,4.55643774175662,128.94778416552));
#65691=CARTESIAN_POINT('Ctrl Pts',(25.5243985560727,4.50115292647783,128.822239179571));
#65692=CARTESIAN_POINT('Ctrl Pts',(25.5166504880698,4.44585573054797,128.696666078693));
#65693=CARTESIAN_POINT('Ctrl Pts',(25.5089024200668,4.38531449197364,128.573442307533));
#65694=CARTESIAN_POINT('Ctrl Pts',(25.5011543520638,4.3197687997447,128.453024703824));
#65695=CARTESIAN_POINT('Ctrl Pts',(25.493398049322,4.25415344477406,128.332479118853));
#65696=CARTESIAN_POINT('Ctrl Pts',(25.4856417465801,4.18352319849925,128.214746002991));
#65697=CARTESIAN_POINT('Ctrl Pts',(25.4778854438382,4.10816279068132,128.100256043449));
#65698=CARTESIAN_POINT('Ctrl Pts',(25.4701250013241,4.03276216074458,127.985704977168));
#65699=CARTESIAN_POINT('Ctrl Pts',(25.4623645588099,3.95262656705109,127.874400833443));
#65700=CARTESIAN_POINT('Ctrl Pts',(25.4546041162958,3.86808217815684,127.766742582736));
#65701=CARTESIAN_POINT('Ctrl Pts',(25.4468312160303,3.78340207110404,127.658911509448));
#65702=CARTESIAN_POINT('Ctrl Pts',(25.4390583157649,3.69429928024414,127.554738322039));
#65703=CARTESIAN_POINT('Ctrl Pts',(25.4312854154995,3.60113870758233,127.454587032493));
#65704=CARTESIAN_POINT('Ctrl Pts',(25.4237950797374,3.51136475639397,127.358076494588));
#65705=CARTESIAN_POINT('Ctrl Pts',(25.4163047439754,3.41782314127747,127.265300735919));
#65706=CARTESIAN_POINT('Ctrl Pts',(25.4088144082133,3.32086912835263,127.176549804575));
#65707=CARTESIAN_POINT('Ctrl Pts',(25.4010400740942,3.22023907455935,127.084433854694));
#65708=CARTESIAN_POINT('Ctrl Pts',(25.3932657399751,3.11561398702345,126.99636216395));
#65709=CARTESIAN_POINT('Ctrl Pts',(25.385491405856,3.00735264796848,126.912701188318));
#65710=CARTESIAN_POINT('Ctrl Pts',(25.3777266529089,2.89922473133816,126.829143317361));
#65711=CARTESIAN_POINT('Ctrl Pts',(25.3699618999619,2.78746978613843,126.749985582637));
#65712=CARTESIAN_POINT('Ctrl Pts',(25.3621971470148,2.67248261828102,126.675556950947));
#65713=CARTESIAN_POINT('Ctrl Pts',(25.3544401061298,2.55760965729992,126.601202242823));
#65714=CARTESIAN_POINT('Ctrl Pts',(25.3466830652447,2.43951118836747,126.531567501535));
#65715=CARTESIAN_POINT('Ctrl Pts',(25.3389260243597,2.31861391990805,126.466940583386));
#65716=CARTESIAN_POINT('Ctrl Pts',(25.3311748331196,2.19780782101939,126.402362400898));
#65717=CARTESIAN_POINT('Ctrl Pts',(25.3234236418795,2.07420746701642,126.342784708344));
#65718=CARTESIAN_POINT('Ctrl Pts',(25.3156724506394,1.94826698197686,126.288451093512));
#65719=CARTESIAN_POINT('Ctrl Pts',(25.3079245538623,1.82238002500284,126.234140571916));
#65720=CARTESIAN_POINT('Ctrl Pts',(25.3001766570852,1.69415527344232,126.185069849531));
#65721=CARTESIAN_POINT('Ctrl Pts',(25.2924287603081,1.56406959660007,126.141435638597));
#65722=CARTESIAN_POINT('Ctrl Pts',(25.284682484224,1.43401113087709,126.097810554999));
#65723=CARTESIAN_POINT('Ctrl Pts',(25.27693620814,1.30209288457659,126.05961984515));
#65724=CARTESIAN_POINT('Ctrl Pts',(25.2691899320559,1.16880939050615,126.02701117764));
#65725=CARTESIAN_POINT('Ctrl Pts',(25.2614435987905,1.03552491256723,125.994402269419));
#65726=CARTESIAN_POINT('Ctrl Pts',(25.2536972655251,0.900875546513192,125.967375578671));
#65727=CARTESIAN_POINT('Ctrl Pts',(25.2459509322598,0.765368201150668,125.946028128001));
#65728=CARTESIAN_POINT('Ctrl Pts',(25.2382028642568,0.62983050985806,125.924675896716));
#65729=CARTESIAN_POINT('Ctrl Pts',(25.2304547962539,0.493434843051849,125.909005497126));
#65730=CARTESIAN_POINT('Ctrl Pts',(25.2227067282509,0.356695054955446,125.899062288181));
#65731=CARTESIAN_POINT('Ctrl Pts',(25.214950425509,0.219809938184657,125.889108511474));
#65732=CARTESIAN_POINT('Ctrl Pts',(25.2071941227671,0.0825803600836163,
125.884894113103));
#65733=CARTESIAN_POINT('Ctrl Pts',(25.1994378200253,-0.0544774266093184,
125.886412338813));
#65734=CARTESIAN_POINT('Ctrl Pts',(25.1916773775111,-0.191608365169928,
125.887931374845));
#65735=CARTESIAN_POINT('Ctrl Pts',(25.1839169349969,-0.328566939395477,
125.895189110939));
#65736=CARTESIAN_POINT('Ctrl Pts',(25.1761564924828,-0.464841182064157,
125.908126785532));
#65737=CARTESIAN_POINT('Ctrl Pts',(25.1683835922173,-0.601334184245027,
125.921085228828));
#65738=CARTESIAN_POINT('Ctrl Pts',(25.1606106919519,-0.737140272066211,
125.939741777935));
#65739=CARTESIAN_POINT('Ctrl Pts',(25.1528377916865,-0.871755953490742,
125.963986187829));
#65740=CARTESIAN_POINT('Ctrl Pts',(25.1453474559245,-1.00147801581778,125.987349252355));
#65741=CARTESIAN_POINT('Ctrl Pts',(25.1378571201625,-1.13009441698203,126.015900898654));
#65742=CARTESIAN_POINT('Ctrl Pts',(25.1303667844006,-1.25716910129661,126.049499009354));
#65743=CARTESIAN_POINT('Ctrl Pts',(25.1225924502815,-1.38906186089178,126.084371002634));
#65744=CARTESIAN_POINT('Ctrl Pts',(25.1148181161623,-1.5197114840579,126.124790151797));
#65745=CARTESIAN_POINT('Ctrl Pts',(25.1070437820432,-1.64861573044893,126.170652681602));
#65746=CARTESIAN_POINT('Ctrl Pts',(25.0992790290961,-1.77736111387661,126.216458689938));
#65747=CARTESIAN_POINT('Ctrl Pts',(25.0915142761491,-1.90436503560955,126.267694601246));
#65748=CARTESIAN_POINT('Ctrl Pts',(25.083749523202,-2.02913732432348,126.324206068721));
#65749=CARTESIAN_POINT('Ctrl Pts',(25.075992482317,-2.15378568744161,126.38066140821));
#65750=CARTESIAN_POINT('Ctrl Pts',(25.0682354414319,-2.27620647461936,126.442381716256));
#65751=CARTESIAN_POINT('Ctrl Pts',(25.0604784005469,-2.39592685787054,126.50916358434));
#65752=CARTESIAN_POINT('Ctrl Pts',(25.0527272093068,-2.51555695904878,126.575895091697));
#65753=CARTESIAN_POINT('Ctrl Pts',(25.0449760180666,-2.63249036956697,126.647680371972));
#65754=CARTESIAN_POINT('Ctrl Pts',(25.0372248268265,-2.74627668696429,126.724269022867));
#65755=CARTESIAN_POINT('Ctrl Pts',(25.0294769300494,-2.86001464214169,126.800825121542));
#65756=CARTESIAN_POINT('Ctrl Pts',(25.0217290332724,-2.97060784092103,126.882180312475));
#65757=CARTESIAN_POINT('Ctrl Pts',(25.0139811364953,-3.0776330242175,126.968039719786));
#65758=CARTESIAN_POINT('Ctrl Pts',(25.0062348604112,-3.18463582015282,127.053881167159));
#65759=CARTESIAN_POINT('Ctrl Pts',(24.9984885843271,-3.28807178037368,127.144224712357));
#65760=CARTESIAN_POINT('Ctrl Pts',(24.9907423082429,-3.38754936005132,127.238734109403));
#65761=CARTESIAN_POINT('Ctrl Pts',(24.9829959749776,-3.48702767404986,127.333244204095));
#65762=CARTESIAN_POINT('Ctrl Pts',(24.9752496417122,-3.5825472657576,127.431919942712));
#65763=CARTESIAN_POINT('Ctrl Pts',(24.9675033084469,-3.67375251071746,127.534387291605));
#65764=CARTESIAN_POINT('Ctrl Pts',(24.9597552404439,-3.76497818045956,127.63687758735));
#65765=CARTESIAN_POINT('Ctrl Pts',(24.9520071724409,-3.85188732100181,127.743160891011));
#65766=CARTESIAN_POINT('Ctrl Pts',(24.9442591044379,-3.93416401981541,127.852829400098));
#65767=CARTESIAN_POINT('Ctrl Pts',(24.9365028016961,-4.0165281632836,127.962614466181));
#65768=CARTESIAN_POINT('Ctrl Pts',(24.9287464989542,-4.0942497949735,128.075791611519));
#65769=CARTESIAN_POINT('Ctrl Pts',(24.9209901962124,-4.16705555021563,128.191922847223));
#65770=CARTESIAN_POINT('Ctrl Pts',(24.9132297536982,-4.23990016408146,128.308116065664));
#65771=CARTESIAN_POINT('Ctrl Pts',(24.905469311184,-4.30782347992387,128.427266176667));
#65772=CARTESIAN_POINT('Ctrl Pts',(24.8977088686698,-4.37059820472111,128.548910685648));
#65773=CARTESIAN_POINT('Ctrl Pts',(24.8899359684044,-4.43347370107946,128.670750469195));
#65774=CARTESIAN_POINT('Ctrl Pts',(24.882163068139,-4.49118392565028,128.79509229761));
#65775=CARTESIAN_POINT('Ctrl Pts',(24.8743901678735,-4.54354948094981,128.921452978657));
#65776=CARTESIAN_POINT('Ctrl Pts',(24.8668998321115,-4.59401141641347,129.043220130665));
#65777=CARTESIAN_POINT('Ctrl Pts',(24.8594094963494,-4.63951041421743,129.166861613809));
#65778=CARTESIAN_POINT('Ctrl Pts',(24.8519191605873,-4.67993034298145,129.29193374418));
#65779=CARTESIAN_POINT('Ctrl Pts',(24.8461750398123,-4.71092721146841,129.387847925501));
#65780=CARTESIAN_POINT('Ctrl Pts',(24.8404309190372,-4.73898758443333,129.484754485873));
#65781=CARTESIAN_POINT('Ctrl Pts',(24.8346867982621,-4.76405452823407,129.582490119308));
#65782=CARTESIAN_POINT('Ctrl Pts',(26.584953373822,-4.764054528234,129.582490119308));
#65783=CARTESIAN_POINT('Ctrl Pts',(26.5771914547002,-4.79811509371724,129.715291747186));
#65784=CARTESIAN_POINT('Ctrl Pts',(26.5694295355783,-4.82658894433892,129.849403140099));
#65785=CARTESIAN_POINT('Ctrl Pts',(26.5616676164564,-4.84940279828725,129.984314544187));
#65786=CARTESIAN_POINT('Ctrl Pts',(26.5538938870113,-4.87225136517013,130.119431225769));
#65787=CARTESIAN_POINT('Ctrl Pts',(26.5461201575662,-4.88942268405172,130.255349962639));
#65788=CARTESIAN_POINT('Ctrl Pts',(26.5383464281211,-4.90089540289503,130.391556411698));
#65789=CARTESIAN_POINT('Ctrl Pts',(26.5330992532357,-4.90863935161451,130.48349414426));
#65790=CARTESIAN_POINT('Ctrl Pts',(26.5278520783502,-4.9137880539663,130.575562919708));
#65791=CARTESIAN_POINT('Ctrl Pts',(26.5226049034648,-4.91634834589865,130.667605346079));
#65792=CARTESIAN_POINT('Ctrl Pts',(26.5200230809736,-4.91760811319045,130.712893946466));
#65793=CARTESIAN_POINT('Ctrl Pts',(26.5174412584824,-4.91824211014721,130.758200034511));
#65794=CARTESIAN_POINT('Ctrl Pts',(26.5148594359912,-4.91824992681955,130.803512184009));
#65795=CARTESIAN_POINT('',(26.8601405639764,-4.91824802889422,130.808763886588));
#65796=CARTESIAN_POINT('Ctrl Pts',(26.9301047320141,-4.76405452823399,129.582490119308));
#65797=CARTESIAN_POINT('Ctrl Pts',(26.9224218544244,-4.79788512892272,129.714395117942));
#65798=CARTESIAN_POINT('Ctrl Pts',(26.9147389768347,-4.82623545671776,129.847714506907));
#65799=CARTESIAN_POINT('Ctrl Pts',(26.9070560992449,-4.84900229538889,129.981949648638));
#65800=CARTESIAN_POINT('Ctrl Pts',(26.8992368433722,-4.87217326679926,130.118567590032));
#65801=CARTESIAN_POINT('Ctrl Pts',(26.8914175874995,-4.88956054893843,130.256133687399));
#65802=CARTESIAN_POINT('Ctrl Pts',(26.8835983316268,-4.90111018938166,130.394114381704));
#65803=CARTESIAN_POINT('Ctrl Pts',(26.8757790757541,-4.91265982982489,130.532095076008));
#65804=CARTESIAN_POINT('Ctrl Pts',(26.8679598198814,-4.91837182446762,130.670489933609));
#65805=CARTESIAN_POINT('Ctrl Pts',(26.8601405640087,-4.91824802889473,130.808763886018));
#65806=CARTESIAN_POINT('Ctrl Pts',(26.8601405639765,-4.91824802889422,130.808763886588));
#65807=CARTESIAN_POINT('Ctrl Pts',(26.850613514715,-4.91809719527359,130.977238071039));
#65808=CARTESIAN_POINT('Ctrl Pts',(26.8410864654536,-4.90928611020261,131.145327951723));
#65809=CARTESIAN_POINT('Ctrl Pts',(26.8315594161922,-4.89195503112132,131.312257296022));
#65810=CARTESIAN_POINT('Ctrl Pts',(26.8218831116281,-4.87435243507981,131.481801835136));
#65811=CARTESIAN_POINT('Ctrl Pts',(26.8122068070639,-4.84796084158413,131.650149258514));
#65812=CARTESIAN_POINT('Ctrl Pts',(26.8025305024998,-4.81297596357176,131.816509537726));
#65813=CARTESIAN_POINT('Ctrl Pts',(26.795508178706,-4.78758660757745,131.937241139269));
#65814=CARTESIAN_POINT('Ctrl Pts',(26.7884858549122,-4.7576723990162,132.056926656006));
#65815=CARTESIAN_POINT('Ctrl Pts',(26.7814635311184,-4.7233237335095,132.175271253226));
#65816=CARTESIAN_POINT('Ctrl Pts',(26.7736891969994,-4.68529671994025,132.306289199279));
#65817=CARTESIAN_POINT('Ctrl Pts',(26.7659148628803,-4.64175397977864,132.435931250449));
#65818=CARTESIAN_POINT('Ctrl Pts',(26.7581405287612,-4.59281131076359,132.563697801343));
#65819=CARTESIAN_POINT('Ctrl Pts',(26.7503757758141,-4.54392895921404,132.691306891382));
#65820=CARTESIAN_POINT('Ctrl Pts',(26.742611022867,-4.48966005864959,132.817044718525));
#65821=CARTESIAN_POINT('Ctrl Pts',(26.7348462699199,-4.4301706741868,132.940424956502));
#65822=CARTESIAN_POINT('Ctrl Pts',(26.7270892290349,-4.37074037541939,133.063682651488));
#65823=CARTESIAN_POINT('Ctrl Pts',(26.7193321881499,-4.30610007995629,133.184587067291));
#65824=CARTESIAN_POINT('Ctrl Pts',(26.7115751472649,-4.23646448430847,133.302670393333));
#65825=CARTESIAN_POINT('Ctrl Pts',(26.7038239560248,-4.16688140140482,133.420664671821));
#65826=CARTESIAN_POINT('Ctrl Pts',(26.6960727647846,-4.0923107140849,133.535841759613));
#65827=CARTESIAN_POINT('Ctrl Pts',(26.6883215735445,-4.01301356095525,133.647757392919));
#65828=CARTESIAN_POINT('Ctrl Pts',(26.6805736767674,-3.9337501112311,133.759625459096));
#65829=CARTESIAN_POINT('Ctrl Pts',(26.6728257799903,-3.84976441675079,133.868234509505));
#65830=CARTESIAN_POINT('Ctrl Pts',(26.6650778832133,-3.76136142553019,133.973168483157));
#65831=CARTESIAN_POINT('Ctrl Pts',(26.6573316071292,-3.6729769263096,134.078080506885));
#65832=CARTESIAN_POINT('Ctrl Pts',(26.6495853310451,-3.58017721997951,134.179318684124));
#65833=CARTESIAN_POINT('Ctrl Pts',(26.641839054961,-3.4833078516829,134.276499651779));
#65834=CARTESIAN_POINT('Ctrl Pts',(26.6340927216956,-3.38643776831875,134.373681336801));
#65835=CARTESIAN_POINT('Ctrl Pts',(26.6263463884303,-3.28549823905269,134.466805475578));
#65836=CARTESIAN_POINT('Ctrl Pts',(26.618600055165,-3.18087172382634,134.555525521841));
#65837=CARTESIAN_POINT('Ctrl Pts',(26.610851987162,-3.07622177821734,134.644265436343));
#65838=CARTESIAN_POINT('Ctrl Pts',(26.6031039191591,-2.96788350178384,134.728599042967));
#65839=CARTESIAN_POINT('Ctrl Pts',(26.5953558511561,-2.85627216060912,134.808220306295));
#65840=CARTESIAN_POINT('Ctrl Pts',(26.5875995484142,-2.74454219757266,134.88792619205));
#65841=CARTESIAN_POINT('Ctrl Pts',(26.5798432456725,-2.62953253959788,134.962909502405));
#65842=CARTESIAN_POINT('Ctrl Pts',(26.5720869429306,-2.51168760944261,135.032907461941));
#65843=CARTESIAN_POINT('Ctrl Pts',(26.5643265004165,-2.39377978189987,135.102942781495));
#65844=CARTESIAN_POINT('Ctrl Pts',(26.5565660579022,-2.27303401089016,135.167987262969));
#65845=CARTESIAN_POINT('Ctrl Pts',(26.5488056153881,-2.14991811221573,135.227824777392));
#65846=CARTESIAN_POINT('Ctrl Pts',(26.5410327151227,-2.02660457697104,135.287758348305));
#65847=CARTESIAN_POINT('Ctrl Pts',(26.5332598148572,-1.90091366966469,135.342468092723));
#65848=CARTESIAN_POINT('Ctrl Pts',(26.5254869145918,-1.77333274843271,135.391786260106));
#65849=CARTESIAN_POINT('Ctrl Pts',(26.5179965788297,-1.65038971504309,135.43931158788));
#65850=CARTESIAN_POINT('Ctrl Pts',(26.5105062430676,-1.52569198709775,135.481830428419));
#65851=CARTESIAN_POINT('Ctrl Pts',(26.5030159073055,-1.39968590756955,135.519237330975));
#65852=CARTESIAN_POINT('Ctrl Pts',(26.4952415731864,-1.26890226923879,135.558062527611));
#65853=CARTESIAN_POINT('Ctrl Pts',(26.4874672390674,-1.13629482528775,135.59150348246));
#65854=CARTESIAN_POINT('Ctrl Pts',(26.4796929049483,-1.00234649939001,135.619387570519));
#65855=CARTESIAN_POINT('Ctrl Pts',(26.4719281520012,-0.868563252832645,
135.647237293931));
#65856=CARTESIAN_POINT('Ctrl Pts',(26.4641633990541,-0.73344279143046,135.669543697799));
#65857=CARTESIAN_POINT('Ctrl Pts',(26.456398646107,-0.597484037499191,135.68618362618));
#65858=CARTESIAN_POINT('Ctrl Pts',(26.448641605222,-0.461660319719009,135.70280702755));
#65859=CARTESIAN_POINT('Ctrl Pts',(26.440884564337,-0.325000351887533,135.713775106265));
#65860=CARTESIAN_POINT('Ctrl Pts',(26.433127523452,-0.188013765003033,135.719015629535));
#65861=CARTESIAN_POINT('Ctrl Pts',(26.4253763322119,-0.0511304807694892,
135.724252200886));
#65862=CARTESIAN_POINT('Ctrl Pts',(26.4176251409718,0.0860785431613368,
135.723769799));
#65863=CARTESIAN_POINT('Ctrl Pts',(26.4098739497317,0.223098383284125,135.717547991754));
#65864=CARTESIAN_POINT('Ctrl Pts',(26.4021260529546,0.36005998632011,135.711328828941));
#65865=CARTESIAN_POINT('Ctrl Pts',(26.3943781561775,0.496832175728681,135.699375130246));
#65866=CARTESIAN_POINT('Ctrl Pts',(26.3866302594004,0.632900075765341,135.681718565943));
#65867=CARTESIAN_POINT('Ctrl Pts',(26.3788839833163,0.768939513330597,135.664065695013));
#65868=CARTESIAN_POINT('Ctrl Pts',(26.3711377072322,0.904274567086835,135.640712381531));
#65869=CARTESIAN_POINT('Ctrl Pts',(26.3633914311481,1.03839592721278,135.611742125294));
#65870=CARTESIAN_POINT('Ctrl Pts',(26.3556450978827,1.17251827739196,135.582771655206));
#65871=CARTESIAN_POINT('Ctrl Pts',(26.3478987646174,1.30542653391143,135.548184242171));
#65872=CARTESIAN_POINT('Ctrl Pts',(26.340152431352,1.43662240863915,135.508114343846));
#65873=CARTESIAN_POINT('Ctrl Pts',(26.3324043633491,1.56784766377337,135.468035472146));
#65874=CARTESIAN_POINT('Ctrl Pts',(26.3246562953461,1.69735940020019,135.422471786226));
#65875=CARTESIAN_POINT('Ctrl Pts',(26.3169082273431,1.82467568019322,135.371607241585));
#65876=CARTESIAN_POINT('Ctrl Pts',(26.3091519246013,1.95212727344371,135.3206886375));
#65877=CARTESIAN_POINT('Ctrl Pts',(26.3013956218594,2.07737838548611,135.26445806582));
#65878=CARTESIAN_POINT('Ctrl Pts',(26.2936393191176,2.19996771455989,135.203147395462));
#65879=CARTESIAN_POINT('Ctrl Pts',(26.2858788766034,2.32262247324987,135.141804001754));
#65880=CARTESIAN_POINT('Ctrl Pts',(26.2781184340892,2.44261227628008,135.075375295942));
#65881=CARTESIAN_POINT('Ctrl Pts',(26.2703579915751,2.55950242235699,135.004138041722));
#65882=CARTESIAN_POINT('Ctrl Pts',(26.2625850913096,2.67658021087339,134.932786431137));
#65883=CARTESIAN_POINT('Ctrl Pts',(26.2548121910442,2.7905480738831,134.856611064286));
#65884=CARTESIAN_POINT('Ctrl Pts',(26.2470392907788,2.90100144912869,134.775931296108));
#65885=CARTESIAN_POINT('Ctrl Pts',(26.2395489550168,3.00743956596915,134.698184440723));
#65886=CARTESIAN_POINT('Ctrl Pts',(26.2320586192546,3.11061403857548,134.616255182471));
#65887=CARTESIAN_POINT('Ctrl Pts',(26.2245682834926,3.21019488896853,134.530462043633));
#65888=CARTESIAN_POINT('Ctrl Pts',(26.2167939493735,3.31355137757088,134.44141603186));
#65889=CARTESIAN_POINT('Ctrl Pts',(26.2090196152544,3.41336376255425,134.347925286562));
#65890=CARTESIAN_POINT('Ctrl Pts',(26.2012452811353,3.5092257775743,134.250302797073));
#65891=CARTESIAN_POINT('Ctrl Pts',(26.1934805281882,3.60496965122826,134.152800618578));
#65892=CARTESIAN_POINT('Ctrl Pts',(26.1857157752411,3.69677257044115,134.051177103745));
#65893=CARTESIAN_POINT('Ctrl Pts',(26.177951022294,3.78426124093248,133.945785441253));
#65894=CARTESIAN_POINT('Ctrl Pts',(26.170193981409,3.8716630164428,133.840498455246));
#65895=CARTESIAN_POINT('Ctrl Pts',(26.1624369405241,3.95475882241595,133.731451068354));
#65896=CARTESIAN_POINT('Ctrl Pts',(26.1546798996391,4.03321241935692,133.619033003981));
#65897=CARTESIAN_POINT('Ctrl Pts',(26.1469287083989,4.11160685383015,133.506699714944));
#65898=CARTESIAN_POINT('Ctrl Pts',(26.1391775171588,4.18536582441316,133.391001127147));
#65899=CARTESIAN_POINT('Ctrl Pts',(26.1314263259187,4.25419381224783,133.272359416255));
#65900=CARTESIAN_POINT('Ctrl Pts',(26.1236784291416,4.32299254635162,133.153768131255));
#65901=CARTESIAN_POINT('Ctrl Pts',(26.1159305323645,4.38686427031463,133.032236548586));
#65902=CARTESIAN_POINT('Ctrl Pts',(26.1081826355875,4.44555732631989,132.908214966351));
#65903=CARTESIAN_POINT('Ctrl Pts',(26.1004363595034,4.50423810500311,132.784219326758));
#65904=CARTESIAN_POINT('Ctrl Pts',(26.0926900834193,4.55774220326821,132.657735076772));
#65905=CARTESIAN_POINT('Ctrl Pts',(26.0849438073352,4.60586457746024,132.52923584685));
#65906=CARTESIAN_POINT('Ctrl Pts',(26.0771974740699,4.65398730688071,132.400735668376));
#65907=CARTESIAN_POINT('Ctrl Pts',(26.0694511408045,4.69672809584134,132.270220846419));
#65908=CARTESIAN_POINT('Ctrl Pts',(26.0617048075391,4.7339307304703,132.138183282544));
#65909=CARTESIAN_POINT('Ctrl Pts',(26.0539567395361,4.77114169637134,132.006116149772));
#65910=CARTESIAN_POINT('Ctrl Pts',(26.0462086715332,4.80281193401514,131.872525972759));
#65911=CARTESIAN_POINT('Ctrl Pts',(26.0384606035302,4.82883571125878,131.737917651802));
#65912=CARTESIAN_POINT('Ctrl Pts',(26.0307043007884,4.85488714688257,131.60316626752));
#65913=CARTESIAN_POINT('Ctrl Pts',(26.0229479980465,4.87528005988263,131.467394962162));
#65914=CARTESIAN_POINT('Ctrl Pts',(26.0151916953047,4.8899601832778,131.331117172777));
#65915=CARTESIAN_POINT('Ctrl Pts',(26.0074312527905,4.90464814189684,131.194766647833));
#65916=CARTESIAN_POINT('Ctrl Pts',(25.9996708102763,4.91361720979041,131.057909490153));
#65917=CARTESIAN_POINT('Ctrl Pts',(25.9919103677622,4.91686526942607,130.921061023785));
#65918=CARTESIAN_POINT('Ctrl Pts',(25.9841374674967,4.92011854313541,130.78399287611));
#65919=CARTESIAN_POINT('Ctrl Pts',(25.9763645672314,4.91763246338203,130.646933838752));
#65920=CARTESIAN_POINT('Ctrl Pts',(25.9685916669659,4.90945703673777,130.510396900543));
#65921=CARTESIAN_POINT('Ctrl Pts',(25.9611013312039,4.90157880744467,130.378823423953));
#65922=CARTESIAN_POINT('Ctrl Pts',(25.9536109954418,4.88841772474093,130.247735052778));
#65923=CARTESIAN_POINT('Ctrl Pts',(25.9461206596798,4.8700634092836,130.117581575911));
#65924=CARTESIAN_POINT('Ctrl Pts',(25.9383463255607,4.85101318437705,129.982493290409));
#65925=CARTESIAN_POINT('Ctrl Pts',(25.9305719914415,4.82630780469903,129.847984272616));
#65926=CARTESIAN_POINT('Ctrl Pts',(25.9227976573225,4.79599100015764,129.714565504296));
#65927=CARTESIAN_POINT('Ctrl Pts',(25.9150329043754,4.76571155836837,129.581311162684));
#65928=CARTESIAN_POINT('Ctrl Pts',(25.9072681514283,4.72983453745714,129.449144774696));
#65929=CARTESIAN_POINT('Ctrl Pts',(25.8995033984812,4.68845531038606,129.318571310493));
#65930=CARTESIAN_POINT('Ctrl Pts',(25.8917463575962,4.64711718174665,129.188127533695));
#65931=CARTESIAN_POINT('Ctrl Pts',(25.8839893167113,4.60028783962797,129.059273902488));
#65932=CARTESIAN_POINT('Ctrl Pts',(25.8762322758263,4.54811342370792,128.932503959703));
#65933=CARTESIAN_POINT('Ctrl Pts',(25.8684810845861,4.49597835292078,128.805829615117));
#65934=CARTESIAN_POINT('Ctrl Pts',(25.860729893346,4.43850637951602,128.681236191403));
#65935=CARTESIAN_POINT('Ctrl Pts',(25.8529787021059,4.37589295667642,128.559200513206));
#65936=CARTESIAN_POINT('Ctrl Pts',(25.8452308053288,4.3133061462118,128.437216703427));
#65937=CARTESIAN_POINT('Ctrl Pts',(25.8374829085517,4.24558241071458,128.317788824109));
#65938=CARTESIAN_POINT('Ctrl Pts',(25.8297350117746,4.17296457153491,128.201371999225));
#65939=CARTESIAN_POINT('Ctrl Pts',(25.8219887356905,4.10036192244175,128.08497952623));
#65940=CARTESIAN_POINT('Ctrl Pts',(25.8142424596063,4.02286741273072,127.971597186378));
#65941=CARTESIAN_POINT('Ctrl Pts',(25.8064961835222,3.94076869001512,127.861653497532));
#65942=CARTESIAN_POINT('Ctrl Pts',(25.7987498502569,3.8586693612654,127.751708997108));
#65943=CARTESIAN_POINT('Ctrl Pts',(25.7910035169916,3.7719659856159,127.645203511603));
#65944=CARTESIAN_POINT('Ctrl Pts',(25.7832571837262,3.68098797637171,127.542534352986));
#65945=CARTESIAN_POINT('Ctrl Pts',(25.7755091157233,3.58998959323315,127.439842202321));
#65946=CARTESIAN_POINT('Ctrl Pts',(25.7677610477202,3.49471493087628,127.340988380647));
#65947=CARTESIAN_POINT('Ctrl Pts',(25.7600129797173,3.39553162541569,127.246334754352));
#65948=CARTESIAN_POINT('Ctrl Pts',(25.7522566769754,3.29624290675776,127.151580529056));
#65949=CARTESIAN_POINT('Ctrl Pts',(25.7445003742336,3.19303752991747,127.061035686847));
#65950=CARTESIAN_POINT('Ctrl Pts',(25.7367440714917,3.0863181313976,126.97502340934));
#65951=CARTESIAN_POINT('Ctrl Pts',(25.7289836289776,2.97954177352148,126.88896522449));
#65952=CARTESIAN_POINT('Ctrl Pts',(25.7212231864633,2.86924797104752,126.807444657006));
#65953=CARTESIAN_POINT('Ctrl Pts',(25.7134627439492,2.75586913611329,126.730742033663));
#65954=CARTESIAN_POINT('Ctrl Pts',(25.7056898436837,2.64230829540793,126.65391628046));
#65955=CARTESIAN_POINT('Ctrl Pts',(25.6979169434184,2.52565285873307,126.581924132221));
#65956=CARTESIAN_POINT('Ctrl Pts',(25.690144043153,2.40636144789321,126.515000799995));
#65957=CARTESIAN_POINT('Ctrl Pts',(25.6826537073909,2.29140658031384,126.450510299464));
#65958=CARTESIAN_POINT('Ctrl Pts',(25.6751633716288,2.17400433434992,126.390726624453));
#65959=CARTESIAN_POINT('Ctrl Pts',(25.6676730358667,2.05458157228911,126.335817496446));
#65960=CARTESIAN_POINT('Ctrl Pts',(25.6598987017476,1.93063085990736,126.278826472161));
#65961=CARTESIAN_POINT('Ctrl Pts',(25.6521243676285,1.80411075256694,126.226906398095));
#65962=CARTESIAN_POINT('Ctrl Pts',(25.6443500335095,1.67547479077921,126.180296681161));
#65963=CARTESIAN_POINT('Ctrl Pts',(25.6365852805624,1.54699736131804,126.133744406537));
#65964=CARTESIAN_POINT('Ctrl Pts',(25.6288205276153,1.41640962981017,126.092489599269));
#65965=CARTESIAN_POINT('Ctrl Pts',(25.6210557746682,1.28418799336735,126.056724968088));
#65966=CARTESIAN_POINT('Ctrl Pts',(25.6132987337832,1.15209768131784,126.020995858844));
#65967=CARTESIAN_POINT('Ctrl Pts',(25.6055416928981,1.01837706877371,125.990746175552));
#65968=CARTESIAN_POINT('Ctrl Pts',(25.5977846520131,0.883520379361143,125.966119738718));
#65969=CARTESIAN_POINT('Ctrl Pts',(25.590033460773,0.748765386427281,125.941511872872));
#65970=CARTESIAN_POINT('Ctrl Pts',(25.5822822695329,0.612876404931816,125.922518882908));
#65971=CARTESIAN_POINT('Ctrl Pts',(25.5745310782928,0.476360248171889,125.909234063894));
#65972=CARTESIAN_POINT('Ctrl Pts',(25.5667831815157,0.339902114419901,125.895954891283));
#65973=CARTESIAN_POINT('Ctrl Pts',(25.5590352847386,0.202817723895715,125.888379102034));
#65974=CARTESIAN_POINT('Ctrl Pts',(25.5512873879615,0.0656212361583364,
125.88654840929));
#65975=CARTESIAN_POINT('Ctrl Pts',(25.5435411118774,-0.071546553031422,
125.884718099489));
#65976=CARTESIAN_POINT('Ctrl Pts',(25.5357948357933,-0.20882600211165,125.888630501059));
#65977=CARTESIAN_POINT('Ctrl Pts',(25.5280485597092,-0.345701106305024,
125.898275232292));
#65978=CARTESIAN_POINT('Ctrl Pts',(25.5203022264438,-0.482577220879138,
125.90792003472));
#65979=CARTESIAN_POINT('Ctrl Pts',(25.5125558931785,-0.619048594612275,
125.923297223765));
#65980=CARTESIAN_POINT('Ctrl Pts',(25.5048095599131,-0.75460290175703,125.944344411507));
#65981=CARTESIAN_POINT('Ctrl Pts',(25.4970614919101,-0.890187565349003,
125.96539631262));
#65982=CARTESIAN_POINT('Ctrl Pts',(25.4893134239071,-1.02485436742657,125.992120679126));
#65983=CARTESIAN_POINT('Ctrl Pts',(25.4815653559041,-1.15810014324691,126.024403805971));
#65984=CARTESIAN_POINT('Ctrl Pts',(25.4738090531623,-1.29148753426344,126.056721243708));
#65985=CARTESIAN_POINT('Ctrl Pts',(25.4660527504204,-1.42345050149076,126.094609151277));
#65986=CARTESIAN_POINT('Ctrl Pts',(25.4582964476785,-1.55349950821828,126.137903466743));
#65987=CARTESIAN_POINT('Ctrl Pts',(25.4505360051644,-1.68361792601657,126.181220889689));
#65988=CARTESIAN_POINT('Ctrl Pts',(25.4427755626502,-1.81181998253636,126.229950331418));
#65989=CARTESIAN_POINT('Ctrl Pts',(25.435015120136,-1.93763610160001,126.283879514821));
#65990=CARTESIAN_POINT('Ctrl Pts',(25.4272422198705,-2.06365419186741,126.337895270137));
#65991=CARTESIAN_POINT('Ctrl Pts',(25.4194693196051,-2.18727833809453,126.397127278236));
#65992=CARTESIAN_POINT('Ctrl Pts',(25.4116964193397,-2.3080627542776,126.461316824923));
#65993=CARTESIAN_POINT('Ctrl Pts',(25.4042060835778,-2.42445635269303,126.523172919903));
#65994=CARTESIAN_POINT('Ctrl Pts',(25.3967157478158,-2.53821283329266,126.589632217794));
#65995=CARTESIAN_POINT('Ctrl Pts',(25.3892254120539,-2.64896035774722,126.660426244825));
#65996=CARTESIAN_POINT('Ctrl Pts',(25.3814496526714,-2.763927981328,126.733917919619));
#65997=CARTESIAN_POINT('Ctrl Pts',(25.3736738932888,-2.87601703573611,126.812314070818));
#65998=CARTESIAN_POINT('Ctrl Pts',(25.3658981339063,-2.98478070791217,126.895362384236));
#65999=CARTESIAN_POINT('Ctrl Pts',(25.3581346820708,-3.09337222789739,126.978279247982));
#66000=CARTESIAN_POINT('Ctrl Pts',(25.3503712302353,-3.19864854090535,127.065833372998));
#66001=CARTESIAN_POINT('Ctrl Pts',(25.3426077783998,-3.30019022499862,127.157728261361));
#66002=CARTESIAN_POINT('Ctrl Pts',(25.3348514285176,-3.40163901944636,127.249539084902));
#66003=CARTESIAN_POINT('Ctrl Pts',(25.3270950786352,-3.49935969320959,127.345682512303));
#66004=CARTESIAN_POINT('Ctrl Pts',(25.319338728753,-3.59296420884819,127.445820569206));
#66005=CARTESIAN_POINT('Ctrl Pts',(25.3115877943238,-3.68650337018103,127.545888710111));
#66006=CARTESIAN_POINT('Ctrl Pts',(25.3038368598946,-3.7759318256622,127.649945646897));
#66007=CARTESIAN_POINT('Ctrl Pts',(25.2960859254653,-3.86089717024458,127.757615452099));
#66008=CARTESIAN_POINT('Ctrl Pts',(25.2883387240328,-3.94582159390907,127.865233401485));
#66009=CARTESIAN_POINT('Ctrl Pts',(25.2805915226004,-4.02628694324508,127.976460449943));
#66010=CARTESIAN_POINT('Ctrl Pts',(25.2728443211679,-4.1019802860687,128.090886682699));
#66011=CARTESIAN_POINT('Ctrl Pts',(25.2650974390395,-4.17767050915993,128.205308199331));
#66012=CARTESIAN_POINT('Ctrl Pts',(25.2573505569111,-4.24858889158202,128.322928318665));
#66013=CARTESIAN_POINT('Ctrl Pts',(25.2496036747827,-4.31446518421511,128.443307200827));
#66014=CARTESIAN_POINT('Ctrl Pts',(25.2418573440181,-4.38033678827769,128.56367751534));
#66015=CARTESIAN_POINT('Ctrl Pts',(25.2341110132535,-4.44116683329889,128.686805856572));
#66016=CARTESIAN_POINT('Ctrl Pts',(25.2263646824889,-4.49673087808077,128.812227471259));
#66017=CARTESIAN_POINT('Ctrl Pts',(25.218613615461,-4.5523288958436,128.937725771259));
#66018=CARTESIAN_POINT('Ctrl Pts',(25.210862548433,-4.60265432247078,129.065519787961));
#66019=CARTESIAN_POINT('Ctrl Pts',(25.2031114814051,-4.64753064735533,129.195124169932));
#66020=CARTESIAN_POINT('Ctrl Pts',(25.1954845842286,-4.69168806649772,129.322652327198));
#66021=CARTESIAN_POINT('Ctrl Pts',(25.1878576870521,-4.7305696063685,129.451932917159));
#66022=CARTESIAN_POINT('Ctrl Pts',(25.1802307898757,-4.7640545282341,129.582490119308));
#66023=CARTESIAN_POINT('Origin',(213.235140564004,0.,130.804360617566));
#66024=CARTESIAN_POINT('',(23.0846591878033,-4.76405452823398,129.582490119308));
#66025=CARTESIAN_POINT('',(23.4300068676217,-4.76405452823403,129.582490119308));
#66026=CARTESIAN_POINT('',(213.235140564004,-4.76405452823405,129.582490119308));
#66027=CARTESIAN_POINT('',(24.7648594360374,-4.91824827617447,130.800242801777));
#66028=CARTESIAN_POINT('Ctrl Pts',(24.7648594359913,-4.91824827617515,130.800242802593));
#66029=CARTESIAN_POINT('Ctrl Pts',(24.7568849401906,-4.91836645954758,130.941399015684));
#66030=CARTESIAN_POINT('Ctrl Pts',(24.7489104443899,-4.91240288179963,131.082649968674));
#66031=CARTESIAN_POINT('Ctrl Pts',(24.7409359485892,-4.90036364732372,131.223430046764));
#66032=CARTESIAN_POINT('Ctrl Pts',(24.7332213675798,-4.88871681071159,131.359621643583));
#66033=CARTESIAN_POINT('Ctrl Pts',(24.7255067865705,-4.87138422612501,131.495372160377));
#66034=CARTESIAN_POINT('Ctrl Pts',(24.7177922055612,-4.8484243349185,131.630172055529));
#66035=CARTESIAN_POINT('Ctrl Pts',(24.7100779293296,-4.82546535078202,131.764966625179));
#66036=CARTESIAN_POINT('Ctrl Pts',(24.7023636530981,-4.79687956809056,131.898810259205));
#66037=CARTESIAN_POINT('Ctrl Pts',(24.6946493768665,-4.76277686638179,132.031201920897));
#66038=CARTESIAN_POINT('Ctrl Pts',(24.6869337021269,-4.72866798225196,132.163617583648));
#66039=CARTESIAN_POINT('Ctrl Pts',(24.6792180273873,-4.68904028752408,132.294580368594));
#66040=CARTESIAN_POINT('Ctrl Pts',(24.6715023526477,-4.64405389505115,132.423603181965));
#66041=CARTESIAN_POINT('Ctrl Pts',(24.6637835755001,-4.59904941392792,132.552677874324));
#66042=CARTESIAN_POINT('Ctrl Pts',(24.6560647983525,-4.54868207766955,132.679810671195));
#66043=CARTESIAN_POINT('Ctrl Pts',(24.6483460212049,-4.49316043851339,132.804533694147));
#66044=CARTESIAN_POINT('Ctrl Pts',(24.6406182047815,-4.43757377928982,132.929402777256));
#66045=CARTESIAN_POINT('Ctrl Pts',(24.6328903883581,-4.37682092878727,133.051856093216));
#66046=CARTESIAN_POINT('Ctrl Pts',(24.6251625719347,-4.31115694857983,133.171449299304));
#66047=CARTESIAN_POINT('Ctrl Pts',(24.6174293470803,-4.24544701242726,133.291126204534));
#66048=CARTESIAN_POINT('Ctrl Pts',(24.6096961222258,-4.17481930515338,133.407938677641));
#66049=CARTESIAN_POINT('Ctrl Pts',(24.6019628973714,-4.09957202948641,133.521471626994));
#66050=CARTESIAN_POINT('Ctrl Pts',(24.5942185416995,-4.02421644665088,133.635167990001));
#66051=CARTESIAN_POINT('Ctrl Pts',(24.5864741860276,-3.94422825541909,133.745575091));
#66052=CARTESIAN_POINT('Ctrl Pts',(24.5787298303558,-3.85994588593471,133.852310882934));
#66053=CARTESIAN_POINT('Ctrl Pts',(24.5769770658287,-3.84087042585147,133.876468181203));
#66054=CARTESIAN_POINT('Ctrl Pts',(24.5752243013017,-3.82157514713822,133.900437569811));
#66055=CARTESIAN_POINT('Ctrl Pts',(24.5734715367746,-3.80206422677062,133.924214889485));
#66056=CARTESIAN_POINT('Ctrl Pts',(24.5656972026555,-3.7155241287903,134.029678472728));
#66057=CARTESIAN_POINT('Ctrl Pts',(24.5579228685364,-3.62445552854384,134.131705634315));
#66058=CARTESIAN_POINT('Ctrl Pts',(24.5501485344174,-3.5291615759598,134.229882714016));
#66059=CARTESIAN_POINT('Ctrl Pts',(24.5423837814703,-3.43398506465566,134.327938799241));
#66060=CARTESIAN_POINT('Ctrl Pts',(24.5346190285231,-3.33459383181647,134.42215396563));
#66061=CARTESIAN_POINT('Ctrl Pts',(24.526854275576,-3.23133200637872,134.512146550849));
#66062=CARTESIAN_POINT('Ctrl Pts',(24.519097234691,-3.1281727420416,134.602049754164));
#66063=CARTESIAN_POINT('Ctrl Pts',(24.5113401938061,-3.02115082832521,134.687738467207));
#66064=CARTESIAN_POINT('Ctrl Pts',(24.503583152921,-2.91064780758299,134.768867195025));
#66065=CARTESIAN_POINT('Ctrl Pts',(24.4958319616809,-2.80022811802831,134.849934743038));
#66066=CARTESIAN_POINT('Ctrl Pts',(24.4880807704408,-2.68633286048399,134.926448919951));
#66067=CARTESIAN_POINT('Ctrl Pts',(24.4803295792006,-2.56937699740166,134.998104160956));
#66068=CARTESIAN_POINT('Ctrl Pts',(24.4725816824235,-2.45247084368119,135.069728946572));
#66069=CARTESIAN_POINT('Ctrl Pts',(24.4648337856464,-2.33250700436656,135.136498699941));
#66070=CARTESIAN_POINT('Ctrl Pts',(24.4570858888693,-2.20992960879253,135.198151029805));
#66071=CARTESIAN_POINT('Ctrl Pts',(24.4493396127852,-2.08737785376737,135.25979046333));
#66072=CARTESIAN_POINT('Ctrl Pts',(24.4415933367011,-1.96221397895153,135.316314426981));
#66073=CARTESIAN_POINT('Ctrl Pts',(24.433847060617,-1.83490655792569,135.367506570325));
#66074=CARTESIAN_POINT('Ctrl Pts',(24.4261007273517,-1.70759819714538,135.418699091558));
#66075=CARTESIAN_POINT('Ctrl Pts',(24.4183543940863,-1.57814662131808,135.464559568085));
#66076=CARTESIAN_POINT('Ctrl Pts',(24.4106080608209,-1.44703984165177,135.50492002674));
#66077=CARTESIAN_POINT('Ctrl Pts',(24.402859992818,-1.31590370153101,135.545289523839));
#66078=CARTESIAN_POINT('Ctrl Pts',(24.3951119248151,-1.18311199356689,135.580156437137));
#66079=CARTESIAN_POINT('Ctrl Pts',(24.3873638568121,-1.04916693537901,135.609402948723));
#66080=CARTESIAN_POINT('Ctrl Pts',(24.3796075540703,-0.915079518789317,
135.638680543849));
#66081=CARTESIAN_POINT('Ctrl Pts',(24.3718512513283,-0.77983668589471,135.66232572116));
#66082=CARTESIAN_POINT('Ctrl Pts',(24.3640949485865,-0.643950423630331,
135.680271908228));
#66083=CARTESIAN_POINT('Ctrl Pts',(24.3563345060723,-0.507991634776325,
135.698227673717));
#66084=CARTESIAN_POINT('Ctrl Pts',(24.3485740635582,-0.371389121475727,
135.710478353168));
#66085=CARTESIAN_POINT('Ctrl Pts',(24.340813621044,-0.234658008560122,135.717009463303));
#66086=CARTESIAN_POINT('Ctrl Pts',(24.3330407207786,-0.0977074027236458,
135.723551057755));
#66087=CARTESIAN_POINT('Ctrl Pts',(24.3252678205131,0.039371824076289,135.724354732915));
#66088=CARTESIAN_POINT('Ctrl Pts',(24.3174949202477,0.176065630718323,135.719458170634));
#66089=CARTESIAN_POINT('Ctrl Pts',(24.3100045844857,0.30779027317707,135.714739610727));
#66090=CARTESIAN_POINT('Ctrl Pts',(24.3025142487238,0.439156723834318,135.704728077548));
#66091=CARTESIAN_POINT('Ctrl Pts',(24.2950239129618,0.56971317267766,135.689502372252));
#66092=CARTESIAN_POINT('Ctrl Pts',(24.2872495788427,0.705219708961442,135.673699379712));
#66093=CARTESIAN_POINT('Ctrl Pts',(24.2794752447236,0.84028285247154,135.652228960118));
#66094=CARTESIAN_POINT('Ctrl Pts',(24.2717009106046,0.974390719199168,135.625122568631));
#66095=CARTESIAN_POINT('Ctrl Pts',(24.2639361576575,1.10833330996662,135.598049583349));
#66096=CARTESIAN_POINT('Ctrl Pts',(24.2561714047104,1.24132258687751,135.565354523023));
#66097=CARTESIAN_POINT('Ctrl Pts',(24.2484066517633,1.37285143650384,135.527120615257));
#66098=CARTESIAN_POINT('Ctrl Pts',(24.2406496108783,1.50424964982285,135.488924681947));
#66099=CARTESIAN_POINT('Ctrl Pts',(24.2328925699932,1.63418994945571,135.445200957383));
#66100=CARTESIAN_POINT('Ctrl Pts',(24.2251355291082,1.76217542775139,135.396083695489));
#66101=CARTESIAN_POINT('Ctrl Pts',(24.217384337868,1.89006439120212,135.347003473304));
#66102=CARTESIAN_POINT('Ctrl Pts',(24.209633146628,2.01600110398207,135.292537949035));
#66103=CARTESIAN_POINT('Ctrl Pts',(24.2018819553878,2.13950418842319,135.232871077102));
#66104=CARTESIAN_POINT('Ctrl Pts',(24.1941340586107,2.26295478075869,135.173229565181));
#66105=CARTESIAN_POINT('Ctrl Pts',(24.1863861618337,2.38397345071505,135.108391272251));
#66106=CARTESIAN_POINT('Ctrl Pts',(24.1786382650566,2.50209937834119,135.038588028016));
#66107=CARTESIAN_POINT('Ctrl Pts',(24.1708919889725,2.6202005965696,134.968799385115));
#66108=CARTESIAN_POINT('Ctrl Pts',(24.1631457128884,2.73540993966643,134.894048055435));
#66109=CARTESIAN_POINT('Ctrl Pts',(24.1553994368043,2.84729211041955,134.814611320507));
#66110=CARTESIAN_POINT('Ctrl Pts',(24.147653103539,2.9591751070616,134.735173999196));
#66111=CARTESIAN_POINT('Ctrl Pts',(24.1399067702737,3.06773056356553,134.651051429961));
#66112=CARTESIAN_POINT('Ctrl Pts',(24.1321604370083,3.17255337737015,134.562563396853));
#66113=CARTESIAN_POINT('Ctrl Pts',(24.1244123690053,3.27739966551712,134.474055547463));
#66114=CARTESIAN_POINT('Ctrl Pts',(24.1166643010024,3.37851134892897,134.381180541005));
#66115=CARTESIAN_POINT('Ctrl Pts',(24.1089162329994,3.47551784317074,134.284297223929));
#66116=CARTESIAN_POINT('Ctrl Pts',(24.1011599302575,3.57262743706899,134.18731093811));
#66117=CARTESIAN_POINT('Ctrl Pts',(24.0934036275156,3.66562284907619,134.086308108422));
#66118=CARTESIAN_POINT('Ctrl Pts',(24.0856473247738,3.75417132847954,133.98168349995));
#66119=CARTESIAN_POINT('Ctrl Pts',(24.0778868822596,3.84276706887262,133.877003050175));
#66120=CARTESIAN_POINT('Ctrl Pts',(24.0701264397455,3.9269109075931,133.768697278434));
#66121=CARTESIAN_POINT('Ctrl Pts',(24.0623659972313,4.00631222189423,133.657191745271));
#66122=CARTESIAN_POINT('Ctrl Pts',(24.0545930969659,4.08584099823399,133.545507213527));
#66123=CARTESIAN_POINT('Ctrl Pts',(24.0468201967005,4.16061182333853,133.430612983789));
#66124=CARTESIAN_POINT('Ctrl Pts',(24.039047296435,4.23037854823634,133.312961901374));
#66125=CARTESIAN_POINT('Ctrl Pts',(24.031556960673,4.29760907695243,133.199587732149));
#66126=CARTESIAN_POINT('Ctrl Pts',(24.0240666249109,4.36019286593216,133.08365393849));
#66127=CARTESIAN_POINT('Ctrl Pts',(24.0165762891489,4.41795199847147,132.965583234906));
#66128=CARTESIAN_POINT('Ctrl Pts',(24.0088019550298,4.47790108607643,132.843035844708));
#66129=CARTESIAN_POINT('Ctrl Pts',(24.0010276209107,4.53284234216597,132.717798110651));
#66130=CARTESIAN_POINT('Ctrl Pts',(23.9932532867916,4.58252554504819,132.590317697532));
#66131=CARTESIAN_POINT('Ctrl Pts',(23.9854885338445,4.63214751782318,132.462994392629));
#66132=CARTESIAN_POINT('Ctrl Pts',(23.9777237808974,4.6765241902122,132.333434268783));
#66133=CARTESIAN_POINT('Ctrl Pts',(23.9699590279503,4.71545147676222,132.202108961439));
#66134=CARTESIAN_POINT('Ctrl Pts',(23.9622019870653,4.75434010018245,132.070914088242));
#66135=CARTESIAN_POINT('Ctrl Pts',(23.9544449461803,4.78778999830565,131.937957892922));
#66136=CARTESIAN_POINT('Ctrl Pts',(23.9466879052953,4.81564553203922,131.803731005486));
#66137=CARTESIAN_POINT('Ctrl Pts',(23.9389367140552,4.84348005969796,131.66960533959));
#66138=CARTESIAN_POINT('Ctrl Pts',(23.9311855228151,4.86572854101926,131.534211270154));
#66139=CARTESIAN_POINT('Ctrl Pts',(23.923434331575,4.88228554567899,131.398053225701));
#66140=CARTESIAN_POINT('Ctrl Pts',(23.9156864347979,4.89883551317014,131.261953052048));
#66141=CARTESIAN_POINT('Ctrl Pts',(23.9079385380209,4.90969876816926,131.125089936495));
#66142=CARTESIAN_POINT('Ctrl Pts',(23.9001906412438,4.91482127113167,130.987976889535));
#66143=CARTESIAN_POINT('Ctrl Pts',(23.8924443651597,4.91994270257689,130.850892523668));
#66144=CARTESIAN_POINT('Ctrl Pts',(23.8846980890756,4.91932575593822,130.713558720828));
#66145=CARTESIAN_POINT('Ctrl Pts',(23.8769518129915,4.91296842724458,130.576491586327));
#66146=CARTESIAN_POINT('Ctrl Pts',(23.8692054797262,4.90661105162259,130.439423440027));
#66147=CARTESIAN_POINT('Ctrl Pts',(23.8614591464608,4.89451322750493,130.302622356541));
#66148=CARTESIAN_POINT('Ctrl Pts',(23.8537128131954,4.87672503044056,130.166602011215));
#66149=CARTESIAN_POINT('Ctrl Pts',(23.8459647451925,4.85893284983277,130.030551205076));
#66150=CARTESIAN_POINT('Ctrl Pts',(23.8382166771894,4.83544781121733,129.895281872601));
#66151=CARTESIAN_POINT('Ctrl Pts',(23.8304686091865,4.80637151233564,129.761299762242));
#66152=CARTESIAN_POINT('Ctrl Pts',(23.8227123064446,4.7772643108175,129.627175254102));
#66153=CARTESIAN_POINT('Ctrl Pts',(23.8149560037028,4.74255406138123,129.494341083636));
#66154=CARTESIAN_POINT('Ctrl Pts',(23.8071997009609,4.70239303118569,129.363290583613));
#66155=CARTESIAN_POINT('Ctrl Pts',(23.7994392584467,4.66221056583905,129.232170137993));
#66156=CARTESIAN_POINT('Ctrl Pts',(23.7916788159326,4.61657165285026,129.102835628258));
#66157=CARTESIAN_POINT('Ctrl Pts',(23.7839183734184,4.5656772396639,128.975761589426));
#66158=CARTESIAN_POINT('Ctrl Pts',(23.776145473153,4.51470112624745,128.848483560065));
#66159=CARTESIAN_POINT('Ctrl Pts',(23.7683725728875,4.45845281414343,128.723473609665));
#66160=CARTESIAN_POINT('Ctrl Pts',(23.7605996726221,4.39718024540997,128.601183604279));
#66161=CARTESIAN_POINT('Ctrl Pts',(23.75310933686,4.33813508888617,128.483339148619));
#66162=CARTESIAN_POINT('Ctrl Pts',(23.745619001098,4.27442477150302,128.368020587173));
#66163=CARTESIAN_POINT('Ctrl Pts',(23.738128665336,4.20630876662415,128.255606093819));
#66164=CARTESIAN_POINT('Ctrl Pts',(23.7303543312169,4.13561012271688,128.138929370782));
#66165=CARTESIAN_POINT('Ctrl Pts',(23.7225799970978,4.05994116106895,128.025011681657));
#66166=CARTESIAN_POINT('Ctrl Pts',(23.7148056629787,3.97954326381621,127.914305518798));
#66167=CARTESIAN_POINT('Ctrl Pts',(23.7070409100316,3.89924444978648,127.80373579139));
#66168=CARTESIAN_POINT('Ctrl Pts',(23.6992761570846,3.81422852364892,127.696370028476));
#66169=CARTESIAN_POINT('Ctrl Pts',(23.6915114041375,3.72478197248664,127.592634863405));
#66170=CARTESIAN_POINT('Ctrl Pts',(23.6837543632525,3.63542426089996,127.489002729563));
#66171=CARTESIAN_POINT('Ctrl Pts',(23.6759973223674,3.54164493525683,127.388994311715));
#66172=CARTESIAN_POINT('Ctrl Pts',(23.6682402814824,3.44377264974579,127.293005750942));
#66173=CARTESIAN_POINT('Ctrl Pts',(23.6604890902423,3.34597417048686,127.19708957589));
#66174=CARTESIAN_POINT('Ctrl Pts',(23.6527378990022,3.24408915291436,127.10518749673));
#66175=CARTESIAN_POINT('Ctrl Pts',(23.6449867077621,3.1384849993654,127.017660870919));
#66176=CARTESIAN_POINT('Ctrl Pts',(23.637238810985,3.03292573039863,126.930171446258));
#66177=CARTESIAN_POINT('Ctrl Pts',(23.629490914208,2.92365076979577,126.84705402514));
#66178=CARTESIAN_POINT('Ctrl Pts',(23.6217430174309,2.81106251812016,126.768631367267));
#66179=CARTESIAN_POINT('Ctrl Pts',(23.6139967413468,2.69849781747983,126.690225113723));
#66180=CARTESIAN_POINT('Ctrl Pts',(23.6062504652627,2.58262152492707,126.616511893403));
#66181=CARTESIAN_POINT('Ctrl Pts',(23.5985041891786,2.46386677128336,126.547772359834));
#66182=CARTESIAN_POINT('Ctrl Pts',(23.5907578559133,2.34511114101887,126.479032318844));
#66183=CARTESIAN_POINT('Ctrl Pts',(23.5830115226479,2.22347734563218,126.415266233726));
#66184=CARTESIAN_POINT('Ctrl Pts',(23.5752651893826,2.09942462179924,126.356709628574));
#66185=CARTESIAN_POINT('Ctrl Pts',(23.5675171213796,1.97534411721892,126.298139910076));
#66186=CARTESIAN_POINT('Ctrl Pts',(23.5597690533766,1.84884395975591,126.244782159854));
#66187=CARTESIAN_POINT('Ctrl Pts',(23.5520209853736,1.72040456596692,126.196824270243));
#66188=CARTESIAN_POINT('Ctrl Pts',(23.5442646826318,1.59182866526177,126.148815410416));
#66189=CARTESIAN_POINT('Ctrl Pts',(23.53650837989,1.46130977792409,126.10621801252));
#66190=CARTESIAN_POINT('Ctrl Pts',(23.5287520771481,1.32934526290405,126.069170628295));
#66191=CARTESIAN_POINT('Ctrl Pts',(23.520991634634,1.19731031444896,126.032103470765));
#66192=CARTESIAN_POINT('Ctrl Pts',(23.5132311921198,1.06382858120302,126.000592319141));
#66193=CARTESIAN_POINT('Ctrl Pts',(23.5054707496056,0.929407919917445,125.974724608414));
#66194=CARTESIAN_POINT('Ctrl Pts',(23.4976978493402,0.794771474652884,125.948815372542));
#66195=CARTESIAN_POINT('Ctrl Pts',(23.4899249490748,0.659193476281055,125.928567738821));
#66196=CARTESIAN_POINT('Ctrl Pts',(23.4821520488094,0.52318811125092,125.914017351215));
#66197=CARTESIAN_POINT('Ctrl Pts',(23.4746617130473,0.392126883815917,125.899995906849));
#66198=CARTESIAN_POINT('Ctrl Pts',(23.4671713772852,0.260669129322521,125.891264701959));
#66199=CARTESIAN_POINT('Ctrl Pts',(23.4596810415231,0.129273267856855,125.887809846475));
#66200=CARTESIAN_POINT('Ctrl Pts',(23.4519067074041,-0.00710450763261369,
125.884223999095));
#66201=CARTESIAN_POINT('Ctrl Pts',(23.444132373285,-0.143847607897832,125.886311146019));
#66202=CARTESIAN_POINT('Ctrl Pts',(23.4363580391659,-0.280444865365881,
125.894112788791));
#66203=CARTESIAN_POINT('Ctrl Pts',(23.4285932862188,-0.416873778922149,
125.901904816735));
#66204=CARTESIAN_POINT('Ctrl Pts',(23.4208285332716,-0.553156820724757,
125.915397305761));
#66205=CARTESIAN_POINT('Ctrl Pts',(23.4130637803245,-0.688780198788125,
125.934579831919));
#66206=CARTESIAN_POINT('Ctrl Pts',(23.4053067394395,-0.824268873800814,
125.953743305721));
#66207=CARTESIAN_POINT('Ctrl Pts',(23.3975496985545,-0.959098804319341,
125.978585515665));
#66208=CARTESIAN_POINT('Ctrl Pts',(23.3897926576695,-1.09275906001764,126.009044079604));
#66209=CARTESIAN_POINT('Ctrl Pts',(23.3820414664293,-1.22631852147721,126.039479674503));
#66210=CARTESIAN_POINT('Ctrl Pts',(23.3742902751892,-1.35870968415475,126.075523106702));
#66211=CARTESIAN_POINT('Ctrl Pts',(23.3665390839491,-1.48942993785113,126.11706059274));
#66212=CARTESIAN_POINT('Ctrl Pts',(23.358791187172,-1.62009463195226,126.158580424239));
#66213=CARTESIAN_POINT('Ctrl Pts',(23.3510432903949,-1.7490894577416,126.205589547052));
#66214=CARTESIAN_POINT('Ctrl Pts',(23.3432953936178,-1.87592536100717,126.257923869691));
#66215=CARTESIAN_POINT('Ctrl Pts',(23.3355491175337,-2.00273473293604,126.310247245118));
#66216=CARTESIAN_POINT('Ctrl Pts',(23.3278028414496,-2.12738571941861,126.367893455701));
#66217=CARTESIAN_POINT('Ctrl Pts',(23.3200565653655,-2.2494080809062,126.430649796301));
#66218=CARTESIAN_POINT('Ctrl Pts',(23.3123102321002,-2.37143134313498,126.493406600153));
#66219=CARTESIAN_POINT('Ctrl Pts',(23.3045638988349,-2.49082559397138,126.56127343048));
#66220=CARTESIAN_POINT('Ctrl Pts',(23.2968175655695,-2.60714445168269,126.633991224987));
#66221=CARTESIAN_POINT('Ctrl Pts',(23.2890694975665,-2.72348935819601,126.70672530414));
#66222=CARTESIAN_POINT('Ctrl Pts',(23.2813214295635,-2.83675716967449,126.784312301954));
#66223=CARTESIAN_POINT('Ctrl Pts',(23.2735733615606,-2.94653013009208,126.86644959077));
#66224=CARTESIAN_POINT('Ctrl Pts',(23.2658170588187,-3.05641975851831,126.948674176074));
#66225=CARTESIAN_POINT('Ctrl Pts',(23.2580607560769,-3.16280680249636,127.035458478417));
#66226=CARTESIAN_POINT('Ctrl Pts',(23.250304453335,-3.26530585986261,127.126458946226));
#66227=CARTESIAN_POINT('Ctrl Pts',(23.2425440108208,-3.36785962406225,127.217507983725));
#66228=CARTESIAN_POINT('Ctrl Pts',(23.2347835683066,-3.466520985658,127.312777399149));
#66229=CARTESIAN_POINT('Ctrl Pts',(23.2270231257924,-3.56094187413623,127.411887178978));
#66230=CARTESIAN_POINT('Ctrl Pts',(23.219250225527,-3.65551433540667,127.511156058624));
#66231=CARTESIAN_POINT('Ctrl Pts',(23.2114773252616,-3.74583246289593,127.614277327821));
#66232=CARTESIAN_POINT('Ctrl Pts',(23.2037044249961,-3.83158833799136,127.720837653379));
#66233=CARTESIAN_POINT('Ctrl Pts',(23.1962140892342,-3.91422677102037,127.823524242693));
#66234=CARTESIAN_POINT('Ctrl Pts',(23.1887237534722,-3.99262870831164,127.92940394511));
#66235=CARTESIAN_POINT('Ctrl Pts',(23.1812334177102,-4.06655804872064,128.038083570905));
#66236=CARTESIAN_POINT('Ctrl Pts',(23.173185565218,-4.1459900588959,128.154852381424));
#66237=CARTESIAN_POINT('Ctrl Pts',(23.1651377127257,-4.22050995647638,128.275223161469));
#66238=CARTESIAN_POINT('Ctrl Pts',(23.1570898602335,-4.2897812136878,128.398750466026));
#66239=CARTESIAN_POINT('Ctrl Pts',(23.1492064240141,-4.35763727076484,128.519754128526));
#66240=CARTESIAN_POINT('Ctrl Pts',(23.1413229877948,-4.42045684504684,128.643786255033));
#66241=CARTESIAN_POINT('Ctrl Pts',(23.1334395515754,-4.47796506753759,128.770396036652));
#66242=CARTESIAN_POINT('Ctrl Pts',(23.1253094909467,-4.53727236989769,128.900966662468));
#66243=CARTESIAN_POINT('Ctrl Pts',(23.117179430318,-4.59093031649128,129.034278550125));
#66244=CARTESIAN_POINT('Ctrl Pts',(23.1090493696893,-4.63868701110859,129.169806893924));
#66245=CARTESIAN_POINT('Ctrl Pts',(23.1009193090606,-4.68644370572583,129.305335237722));
#66246=CARTESIAN_POINT('Ctrl Pts',(23.0927892484319,-4.72829894556715,129.443079645157));
#66247=CARTESIAN_POINT('Ctrl Pts',(23.0846591878033,-4.76405452823398,129.582490119308));
#66248=CARTESIAN_POINT('Ctrl Pts',(24.8346867982621,-4.76405452823407,129.582490119308));
#66249=CARTESIAN_POINT('Ctrl Pts',(24.8253782229543,-4.80467650385836,129.740874585743));
#66250=CARTESIAN_POINT('Ctrl Pts',(24.8160696476464,-4.83743482907301,129.901437429581));
#66251=CARTESIAN_POINT('Ctrl Pts',(24.8067610723386,-4.86212490932803,130.063466273822));
#66252=CARTESIAN_POINT('Ctrl Pts',(24.7975526181693,-4.88654942811261,130.223752368842));
#66253=CARTESIAN_POINT('Ctrl Pts',(24.788344164,-4.90307827616601,130.385473055383));
#66254=CARTESIAN_POINT('Ctrl Pts',(24.7791357098307,-4.91155986073502,130.547918037411));
#66255=CARTESIAN_POINT('Ctrl Pts',(24.7743769518996,-4.91594298596908,130.631866584299));
#66256=CARTESIAN_POINT('Ctrl Pts',(24.7696181939684,-4.91817775056553,130.716008228789));
#66257=CARTESIAN_POINT('Ctrl Pts',(24.7648594360373,-4.91824827617447,130.800242801777));
#66258=CARTESIAN_POINT('',(25.1101405639584,-4.91824999949758,130.804290318038));
#66259=CARTESIAN_POINT('Ctrl Pts',(25.1802307898757,-4.7640545282341,129.582490119308));
#66260=CARTESIAN_POINT('Ctrl Pts',(25.1724704274842,-4.79812541214831,129.715331978592));
#66261=CARTESIAN_POINT('Ctrl Pts',(25.1647100650928,-4.82660895352866,129.849495165861));
#66262=CARTESIAN_POINT('Ctrl Pts',(25.1569497027014,-4.84942908031038,129.984469980017));
#66263=CARTESIAN_POINT('Ctrl Pts',(25.1491768448978,-4.87228595110947,130.119662124996));
#66264=CARTESIAN_POINT('Ctrl Pts',(25.1414039870941,-4.88946113521461,130.255668120271));
#66265=CARTESIAN_POINT('Ctrl Pts',(25.1336311292905,-4.90093048084847,130.391973076059));
#66266=CARTESIAN_POINT('Ctrl Pts',(25.1260133489406,-4.9121709998446,130.525558591197));
#66267=CARTESIAN_POINT('Ctrl Pts',(25.1183955685907,-4.91793128908067,130.65943090316));
#66268=CARTESIAN_POINT('Ctrl Pts',(25.1107777882409,-4.91823712792333,130.793108239306));
#66269=CARTESIAN_POINT('Ctrl Pts',(25.1105653801635,-4.91824565568831,130.79683559093));
#66270=CARTESIAN_POINT('Ctrl Pts',(25.1103529720861,-4.91824994621942,130.800562952252));
#66271=CARTESIAN_POINT('Ctrl Pts',(25.1101405640087,-4.91824999949757,130.804290317156));
#66272=CARTESIAN_POINT('Ctrl Pts',(25.1101405639584,-4.91824999949758,130.804290318038));
#66273=CARTESIAN_POINT('Ctrl Pts',(25.1023694478026,-4.91825194869619,130.940658887285));
#66274=CARTESIAN_POINT('Ctrl Pts',(25.0945983316468,-4.91257795198346,131.07724441592));
#66275=CARTESIAN_POINT('Ctrl Pts',(25.086827215491,-4.9011997743606,131.213535194376));
#66276=CARTESIAN_POINT('Ctrl Pts',(25.0790656782968,-4.88983562189504,131.349657975841));
#66277=CARTESIAN_POINT('Ctrl Pts',(25.0713041411026,-4.87278131048978,131.485486343794));
#66278=CARTESIAN_POINT('Ctrl Pts',(25.0635426039084,-4.8500605813044,131.620507307921));
#66279=CARTESIAN_POINT('Ctrl Pts',(25.0557887730794,-4.82736241134048,131.755394210865));
#66280=CARTESIAN_POINT('Ctrl Pts',(25.0480349422505,-4.79900908420948,131.889474921901));
#66281=CARTESIAN_POINT('Ctrl Pts',(25.0402811114215,-4.76507620767709,132.022240659906));
#66282=CARTESIAN_POINT('Ctrl Pts',(25.0325331210781,-4.73116889070126,132.154906393616));
#66283=CARTESIAN_POINT('Ctrl Pts',(25.0247851307347,-4.69169048599964,132.286258748163));
#66284=CARTESIAN_POINT('Ctrl Pts',(25.0170371403913,-4.64676776865121,132.415798598602));
#66285=CARTESIAN_POINT('Ctrl Pts',(25.0092924292492,-4.6018640640566,132.545283623566));
#66286=CARTESIAN_POINT('Ctrl Pts',(25.0015477181072,-4.55152075755507,132.672957301151));
#66287=CARTESIAN_POINT('Ctrl Pts',(24.9938030069651,-4.49591456095806,132.798335372438));
#66288=CARTESIAN_POINT('Ctrl Pts',(24.9860599017827,-4.44031989497931,132.923687445063));
#66289=CARTESIAN_POINT('Ctrl Pts',(24.9783167966002,-4.37946466813168,133.046744500704));
#66290=CARTESIAN_POINT('Ctrl Pts',(24.9705736914178,-4.31357369545086,133.167042364314));
#66291=CARTESIAN_POINT('Ctrl Pts',(24.9628305112143,-4.24768208436868,133.28734139346));
#66292=CARTESIAN_POINT('Ctrl Pts',(24.9550873310108,-4.17675481816997,133.404880834054));
#66293=CARTESIAN_POINT('Ctrl Pts',(24.9473441508074,-4.10106242447939,133.519221581414));
#66294=CARTESIAN_POINT('Ctrl Pts',(24.9395992149067,-4.0253528682118,133.63358825452));
#66295=CARTESIAN_POINT('Ctrl Pts',(24.931854279006,-3.94487625050408,133.744754464969));
#66296=CARTESIAN_POINT('Ctrl Pts',(24.9241093431053,-3.85994589212343,133.852310875096));
#66297=CARTESIAN_POINT('Ctrl Pts',(24.9163561711497,-3.77492521781236,133.959981661961));
#66298=CARTESIAN_POINT('Ctrl Pts',(24.9086029991941,-3.68544158497976,134.064034672876));
#66299=CARTESIAN_POINT('Ctrl Pts',(24.9008498272385,-3.59184836161745,134.164094001281));
#66300=CARTESIAN_POINT('Ctrl Pts',(24.8930924907353,-3.49820486548413,134.264207075667));
#66301=CARTESIAN_POINT('Ctrl Pts',(24.8853351542321,-3.40044765936741,134.360321919051));
#66302=CARTESIAN_POINT('Ctrl Pts',(24.8775778177288,-3.29896556490838,134.452100913153));
#66303=CARTESIAN_POINT('Ctrl Pts',(24.8698080807413,-3.19732124632465,134.544026620496));
#66304=CARTESIAN_POINT('Ctrl Pts',(24.8620383437537,-3.09194044214155,134.631602378409));
#66305=CARTESIAN_POINT('Ctrl Pts',(24.8542686067661,-2.98324419280498,134.714531604696));
#66306=CARTESIAN_POINT('Ctrl Pts',(24.8469557926535,-2.88094015504777,134.7925839271));
#66307=CARTESIAN_POINT('Ctrl Pts',(24.8396429785408,-2.7756996540835,134.866520397982));
#66308=CARTESIAN_POINT('Ctrl Pts',(24.8323301644281,-2.66789424677801,134.936130619697));
#66309=CARTESIAN_POINT('Ctrl Pts',(24.8245558303091,-2.55328511774448,135.010134021585));
#66310=CARTESIAN_POINT('Ctrl Pts',(24.8167814961899,-2.43541300679089,135.07948239656));
#66311=CARTESIAN_POINT('Ctrl Pts',(24.8090071620709,-2.3146928919907,135.143874401191));
#66312=CARTESIAN_POINT('Ctrl Pts',(24.8012424091238,-2.19412155394278,135.20818704843));
#66313=CARTESIAN_POINT('Ctrl Pts',(24.7934776561767,-2.07070953737171,135.267555296753));
#66314=CARTESIAN_POINT('Ctrl Pts',(24.7857129032296,-1.94490107231132,135.321720784901));
#66315=CARTESIAN_POINT('Ctrl Pts',(24.7779558623446,-1.81921756199236,135.375832475122));
#66316=CARTESIAN_POINT('Ctrl Pts',(24.7701988214596,-1.69114269663616,135.42475153503));
#66317=CARTESIAN_POINT('Ctrl Pts',(24.7624417805746,-1.56114528982937,135.468265467211));
#66318=CARTESIAN_POINT('Ctrl Pts',(24.7546905893345,-1.43124591507793,135.511746585198));
#66319=CARTESIAN_POINT('Ctrl Pts',(24.7469393980943,-1.29942725386825,135.549830564987));
#66320=CARTESIAN_POINT('Ctrl Pts',(24.7391882068542,-1.16617775181755,135.58235313678));
#66321=CARTESIAN_POINT('Ctrl Pts',(24.7314403100771,-1.03298488435996,135.614861885612));
#66322=CARTESIAN_POINT('Ctrl Pts',(24.7236924133001,-0.898362764637024,
135.641813835252));
#66323=CARTESIAN_POINT('Ctrl Pts',(24.715944516523,-0.762814429868399,135.663094733371));
#66324=CARTESIAN_POINT('Ctrl Pts',(24.7081982404389,-0.627294448889324,
135.684371179985));
#66325=CARTESIAN_POINT('Ctrl Pts',(24.7004519643548,-0.490849024221865,
135.699978874018));
#66326=CARTESIAN_POINT('Ctrl Pts',(24.6927056882707,-0.353990412099897,
135.709854868979));
#66327=CARTESIAN_POINT('Ctrl Pts',(24.6849593550054,-0.21713078971893,135.719730936841));
#66328=CARTESIAN_POINT('Ctrl Pts',(24.67721302174,-0.0798583637485085,135.723875193064));
#66329=CARTESIAN_POINT('Ctrl Pts',(24.6694666884747,0.0573108714876579,
135.722276693152));
#66330=CARTESIAN_POINT('Ctrl Pts',(24.6617186204717,0.194510824822804,135.720677835268));
#66331=CARTESIAN_POINT('Ctrl Pts',(24.6539705524688,0.331607150575921,135.713333666712));
#66332=CARTESIAN_POINT('Ctrl Pts',(24.6462224844659,0.468085640615847,135.700285340797));
#66333=CARTESIAN_POINT('Ctrl Pts',(24.638466181724,0.604709181619474,135.687223146967));
#66334=CARTESIAN_POINT('Ctrl Pts',(24.6307098789822,0.740713185383398,135.668444722657));
#66335=CARTESIAN_POINT('Ctrl Pts',(24.6229535762403,0.875589788055244,135.644043002346));
#66336=CARTESIAN_POINT('Ctrl Pts',(24.6151931337262,1.01053837843099,135.619628258103));
#66337=CARTESIAN_POINT('Ctrl Pts',(24.6074326912119,1.14435798743811,135.589584323071));
#66338=CARTESIAN_POINT('Ctrl Pts',(24.5996722486978,1.27655366783885,135.554054691465));
#66339=CARTESIAN_POINT('Ctrl Pts',(24.5918993484323,1.40896156048173,135.518468024539));
#66340=CARTESIAN_POINT('Ctrl Pts',(24.5841264481669,1.53973994194982,135.47737818085));
#66341=CARTESIAN_POINT('Ctrl Pts',(24.5763535479015,1.66841082482402,135.430977997695));
#66342=CARTESIAN_POINT('Ctrl Pts',(24.5688632121394,1.79240419700439,135.386264578072));
#66343=CARTESIAN_POINT('Ctrl Pts',(24.5613728763773,1.91444035081732,135.336620320418));
#66344=CARTESIAN_POINT('Ctrl Pts',(24.5538825406152,2.03411311327613,135.282258216317));
#66345=CARTESIAN_POINT('Ctrl Pts',(24.5461082064961,2.15832330489626,135.225834956516));
#66346=CARTESIAN_POINT('Ctrl Pts',(24.538333872377,2.28038081196803,135.164150301861));
#66347=CARTESIAN_POINT('Ctrl Pts',(24.5305595382579,2.39980779994224,135.097390501673));
#66348=CARTESIAN_POINT('Ctrl Pts',(24.5227947853108,2.51908760482727,135.030712976972));
#66349=CARTESIAN_POINT('Ctrl Pts',(24.5150300323637,2.63574300300044,134.95897294059));
#66350=CARTESIAN_POINT('Ctrl Pts',(24.5072652794166,2.74931651063303,134.882404485263));
#66351=CARTESIAN_POINT('Ctrl Pts',(24.4995082385316,2.86277721545675,134.805912078805));
#66352=CARTESIAN_POINT('Ctrl Pts',(24.4917511976466,2.97316179914533,134.724601014107));
#66353=CARTESIAN_POINT('Ctrl Pts',(24.4839941567616,3.08003807641042,134.638750857273));
#66354=CARTESIAN_POINT('Ctrl Pts',(24.4762429655215,3.18683375744329,134.55296544071));
#66355=CARTESIAN_POINT('Ctrl Pts',(24.4684917742814,3.29012609446808,134.462647989066));
#66356=CARTESIAN_POINT('Ctrl Pts',(24.4607405830413,3.38951286586288,134.36812065363));
#66357=CARTESIAN_POINT('Ctrl Pts',(24.4529926862642,3.4888573952286,134.273633494835));
#66358=CARTESIAN_POINT('Ctrl Pts',(24.4452447894871,3.58429937781728,134.174940279933));
#66359=CARTESIAN_POINT('Ctrl Pts',(24.4374968927101,3.6754707860058,134.072402472212));
#66360=CARTESIAN_POINT('Ctrl Pts',(24.429750616626,3.76662312310115,133.96988611319));
#66361=CARTESIAN_POINT('Ctrl Pts',(24.4220043405419,3.85350640302204,133.863527052946));
#66362=CARTESIAN_POINT('Ctrl Pts',(24.4142580644578,3.93579078009416,133.753722243041));
#66363=CARTESIAN_POINT('Ctrl Pts',(24.4065117311924,4.01807576457098,133.643916622582));
#66364=CARTESIAN_POINT('Ctrl Pts',(24.398765397927,4.09576154400529,133.530665514573));
#66365=CARTESIAN_POINT('Ctrl Pts',(24.3910190646617,4.16856000294783,133.414397123886));
#66366=CARTESIAN_POINT('Ctrl Pts',(24.3832709966587,4.2413747646005,133.298102695699));
#66367=CARTESIAN_POINT('Ctrl Pts',(24.3755229286557,4.30929982043058,133.178789971577));
#66368=CARTESIAN_POINT('Ctrl Pts',(24.3677748606528,4.37209185183028,133.056913813755));
#66369=CARTESIAN_POINT('Ctrl Pts',(24.3600185579109,4.4349506193481,132.934908124501));
#66370=CARTESIAN_POINT('Ctrl Pts',(24.3522622551691,4.49266528526042,132.810333907273));
#66371=CARTESIAN_POINT('Ctrl Pts',(24.3445059524272,4.54503952515843,132.683668675668));
#66372=CARTESIAN_POINT('Ctrl Pts',(24.3367455099131,4.59744171876523,132.556935839015));
#66373=CARTESIAN_POINT('Ctrl Pts',(24.3289850673989,4.64449767272845,132.428110131241));
#66374=CARTESIAN_POINT('Ctrl Pts',(24.3212246248848,4.68606058172216,132.297685527601));
#66375=CARTESIAN_POINT('Ctrl Pts',(24.3134517246193,4.72769021118716,132.167051554808));
#66376=CARTESIAN_POINT('Ctrl Pts',(24.3056788243539,4.76380907158931,132.034813934454));
#66377=CARTESIAN_POINT('Ctrl Pts',(24.2979059240885,4.79432103853378,131.90147904416));
#66378=CARTESIAN_POINT('Ctrl Pts',(24.2904155883265,4.82372381862486,131.772991212979));
#66379=CARTESIAN_POINT('Ctrl Pts',(24.2829252525644,4.84792022069687,131.643484806644));
#66380=CARTESIAN_POINT('Ctrl Pts',(24.2754349168024,4.86686989417998,131.513416677144));
#66381=CARTESIAN_POINT('Ctrl Pts',(24.2676605826833,4.88653805029281,131.378416974982));
#66382=CARTESIAN_POINT('Ctrl Pts',(24.2598862485643,4.90061606732433,131.242384474862));
#66383=CARTESIAN_POINT('Ctrl Pts',(24.2521119144452,4.90900236085679,131.105821864831));
#66384=CARTESIAN_POINT('Ctrl Pts',(24.2443471614981,4.91737831903197,130.969427556012));
#66385=CARTESIAN_POINT('Ctrl Pts',(24.236582408551,4.9200764868191,130.832504823664));
#66386=CARTESIAN_POINT('Ctrl Pts',(24.2288176556039,4.91704653188386,130.695565094731));
#66387=CARTESIAN_POINT('Ctrl Pts',(24.2210606147189,4.91401958634258,130.558761376268));
#66388=CARTESIAN_POINT('Ctrl Pts',(24.2133035738339,4.9052758485401,130.421941083154));
#66389=CARTESIAN_POINT('Ctrl Pts',(24.2055465329489,4.89081691865295,130.285618937423));
#66390=CARTESIAN_POINT('Ctrl Pts',(24.1977953417088,4.87636889235729,130.149399593281));
#66391=CARTESIAN_POINT('Ctrl Pts',(24.1900441504686,4.85621429358276,130.013678036011));
#66392=CARTESIAN_POINT('Ctrl Pts',(24.1822929592285,4.8304067467237,129.878966796695));
#66393=CARTESIAN_POINT('Ctrl Pts',(24.1745450624514,4.80461016876053,129.74431281325));
#66394=CARTESIAN_POINT('Ctrl Pts',(24.1667971656743,4.77316549481603,129.610668676871));
#66395=CARTESIAN_POINT('Ctrl Pts',(24.1590492688973,4.7361779062701,129.478539399355));
#66396=CARTESIAN_POINT('Ctrl Pts',(24.1513029928132,4.69919805473034,129.346437760435));
#66397=CARTESIAN_POINT('Ctrl Pts',(24.1435567167291,4.65667770014155,129.215850726349));
#66398=CARTESIAN_POINT('Ctrl Pts',(24.135810440645,4.60877251944987,129.087270367619));
#66399=CARTESIAN_POINT('Ctrl Pts',(24.1280641073797,4.56086698513295,128.958689059737));
#66400=CARTESIAN_POINT('Ctrl Pts',(24.1203177741143,4.50757668189198,128.832114823132));
#66401=CARTESIAN_POINT('Ctrl Pts',(24.112571440849,4.44910613717478,128.708021512685));
#66402=CARTESIAN_POINT('Ctrl Pts',(24.104823372846,4.39062249838434,128.583900412401));
#66403=CARTESIAN_POINT('Ctrl Pts',(24.0970753048429,4.32695647630629,128.46226169743));
#66404=CARTESIAN_POINT('Ctrl Pts',(24.0893272368399,4.25835923976998,128.343555942756));
#66405=CARTESIAN_POINT('Ctrl Pts',(24.0815709340981,4.18968909727455,128.224724026195));
#66406=CARTESIAN_POINT('Ctrl Pts',(24.0738146313562,4.11607746687996,128.108831635892));
#66407=CARTESIAN_POINT('Ctrl Pts',(24.0660583286144,4.03781997616164,127.996302052897));
#66408=CARTESIAN_POINT('Ctrl Pts',(24.0582978861002,3.95952071706434,127.883712409476));
#66409=CARTESIAN_POINT('Ctrl Pts',(24.050537443586,3.87657089310265,127.774489460918));
#66410=CARTESIAN_POINT('Ctrl Pts',(24.0427770010718,3.78930674778514,127.669023724393));
#66411=CARTESIAN_POINT('Ctrl Pts',(24.0350041008064,3.70190251831451,127.563388684905));
#66412=CARTESIAN_POINT('Ctrl Pts',(24.027231200541,3.61017038944566,127.461523200825));
#66413=CARTESIAN_POINT('Ctrl Pts',(24.0194583002756,3.514484433431,127.363781853801));
#66414=CARTESIAN_POINT('Ctrl Pts',(24.0119679645136,3.42227690293597,127.269593650937));
#66415=CARTESIAN_POINT('Ctrl Pts',(24.0044776287515,3.32639824182405,127.179235156602));
#66416=CARTESIAN_POINT('Ctrl Pts',(23.9969872929895,3.2272110021447,127.092987258533));
#66417=CARTESIAN_POINT('Ctrl Pts',(23.9892129588704,3.12426304812545,127.003469245195));
#66418=CARTESIAN_POINT('Ctrl Pts',(23.9814386247513,3.01742456521416,126.918096121663));
#66419=CARTESIAN_POINT('Ctrl Pts',(23.9736642906322,2.9070635702418,126.837225068952));
#66420=CARTESIAN_POINT('Ctrl Pts',(23.9658995376851,2.7968385853322,126.756453682587));
#66421=CARTESIAN_POINT('Ctrl Pts',(23.958134784738,2.68310003834946,126.680173556254));
#66422=CARTESIAN_POINT('Ctrl Pts',(23.9503700317909,2.56625100141003,126.608703474726));
#66423=CARTESIAN_POINT('Ctrl Pts',(23.9426129909059,2.44951802058136,126.537304378291));
#66424=CARTESIAN_POINT('Ctrl Pts',(23.9348559500208,2.32968102917263,126.470706022091));
#66425=CARTESIAN_POINT('Ctrl Pts',(23.9270989091358,2.20717394234117,126.409185279681));
#66426=CARTESIAN_POINT('Ctrl Pts',(23.9193477178957,2.08475923905703,126.347710930542));
#66427=CARTESIAN_POINT('Ctrl Pts',(23.9115965266555,1.95967879614976,126.291306748411));
#66428=CARTESIAN_POINT('Ctrl Pts',(23.9038453354154,1.83239280583126,126.240204653136));
#66429=CARTESIAN_POINT('Ctrl Pts',(23.8960974386383,1.7051609154541,126.189124277615));
#66430=CARTESIAN_POINT('Ctrl Pts',(23.8883495418612,1.57572570417334,126.143341652212));
#66431=CARTESIAN_POINT('Ctrl Pts',(23.8806016450841,1.44456890582217,126.103041256064));
#66432=CARTESIAN_POINT('Ctrl Pts',(23.872855369,1.31343954264597,126.062749289891));
#66433=CARTESIAN_POINT('Ctrl Pts',(23.8651090929159,1.18058968217964,126.027937386756));
#66434=CARTESIAN_POINT('Ctrl Pts',(23.8573628168318,1.04651746448144,125.998740547374));
#66435=CARTESIAN_POINT('Ctrl Pts',(23.8496164835664,0.912444257092589,125.969543492467));
#66436=CARTESIAN_POINT('Ctrl Pts',(23.8418701503011,0.777149056478749,125.945961667211));
#66437=CARTESIAN_POINT('Ctrl Pts',(23.8341238170357,0.641141082252026,125.928079127009));
#66438=CARTESIAN_POINT('Ctrl Pts',(23.8263757490328,0.505102649982488,125.910192582136));
#66439=CARTESIAN_POINT('Ctrl Pts',(23.8186276810298,0.36835151402817,125.898007912993));
#66440=CARTESIAN_POINT('Ctrl Pts',(23.8108796130268,0.231402518771666,125.891557350916));
#66441=CARTESIAN_POINT('Ctrl Pts',(23.8031233102849,0.0943079724932895,
125.885099933105));
#66442=CARTESIAN_POINT('Ctrl Pts',(23.7953670075431,-0.0429844620036973,
125.884388814758));
#66443=CARTESIAN_POINT('Ctrl Pts',(23.7876107048012,-0.179958872459176,
125.88940406977));
#66444=CARTESIAN_POINT('Ctrl Pts',(23.779850262287,-0.317006390281922,125.894422001575));
#66445=CARTESIAN_POINT('Ctrl Pts',(23.7720898197728,-0.453735156272228,
125.905172366121));
#66446=CARTESIAN_POINT('Ctrl Pts',(23.7643293772587,-0.589634869444966,
125.92158335629));
#66447=CARTESIAN_POINT('Ctrl Pts',(23.7565564769932,-0.725752740901897,
125.938020690838));
#66448=CARTESIAN_POINT('Ctrl Pts',(23.7487835767278,-0.861038513975048,
125.960136746496));
#66449=CARTESIAN_POINT('Ctrl Pts',(23.7410106764623,-0.99499167389035,125.987808465727));
#66450=CARTESIAN_POINT('Ctrl Pts',(23.7335203407004,-1.12407529903236,126.014474248262));
#66451=CARTESIAN_POINT('Ctrl Pts',(23.7260300049386,-1.25192121769692,126.046298707963));
#66452=CARTESIAN_POINT('Ctrl Pts',(23.7185396691767,-1.37809714283713,126.083128646205));
#66453=CARTESIAN_POINT('Ctrl Pts',(23.7107653350576,-1.50905706653195,126.12135500275));
#66454=CARTESIAN_POINT('Ctrl Pts',(23.7029910009386,-1.63863270294063,126.165094985623));
#66455=CARTESIAN_POINT('Ctrl Pts',(23.6952166668195,-1.76632462347257,126.214232036904));
#66456=CARTESIAN_POINT('Ctrl Pts',(23.6874519138724,-1.89385917512443,126.26330853116));
#66457=CARTESIAN_POINT('Ctrl Pts',(23.6796871609253,-2.01951426863631,126.317768720451));
#66458=CARTESIAN_POINT('Ctrl Pts',(23.6719224079782,-2.14280383102489,126.377445799745));
#66459=CARTESIAN_POINT('Ctrl Pts',(23.6641653670932,-2.26597094048202,126.437063606922));
#66460=CARTESIAN_POINT('Ctrl Pts',(23.6564083262082,-2.38677684475436,126.501887823473));
#66461=CARTESIAN_POINT('Ctrl Pts',(23.6486512853232,-2.50475406053538,126.571703041204));
#66462=CARTESIAN_POINT('Ctrl Pts',(23.640900094083,-2.62264230878137,126.641465610738));
#66463=CARTESIAN_POINT('Ctrl Pts',(23.6331489028428,-2.73770577930966,126.716211491628));
#66464=CARTESIAN_POINT('Ctrl Pts',(23.6253977116026,-2.84950060625191,126.795678869476));
#66465=CARTESIAN_POINT('Ctrl Pts',(23.6176498148255,-2.96124791740973,126.875112471568));
#66466=CARTESIAN_POINT('Ctrl Pts',(23.6099019180484,-3.06972903012121,126.959263353281));
#66467=CARTESIAN_POINT('Ctrl Pts',(23.6021540212713,-3.17452834795856,127.047825933777));
#66468=CARTESIAN_POINT('Ctrl Pts',(23.5944077451872,-3.27930574403782,127.136369988891));
#66469=CARTESIAN_POINT('Ctrl Pts',(23.5866614691031,-3.38040257868966,127.229323655033));
#66470=CARTESIAN_POINT('Ctrl Pts',(23.578915193019,-3.4774360151217,127.326340804046));
#66471=CARTESIAN_POINT('Ctrl Pts',(23.5711688597536,-3.57447016783252,127.423358669218));
#66472=CARTESIAN_POINT('Ctrl Pts',(23.5634225264883,-3.66744058599315,127.524439800685));
#66473=CARTESIAN_POINT('Ctrl Pts',(23.5556761932229,-3.75600130577403,127.629201211564));
#66474=CARTESIAN_POINT('Ctrl Pts',(23.5479281252199,-3.84458185811382,127.733986083034));
#66475=CARTESIAN_POINT('Ctrl Pts',(23.5401800572169,-3.92875049466683,127.842452575407));
#66476=CARTESIAN_POINT('Ctrl Pts',(23.532431989214,-4.00820181233323,127.954184957346));
#66477=CARTESIAN_POINT('Ctrl Pts',(23.5246756864721,-4.08773757180564,128.066036089791));
#66478=CARTESIAN_POINT('Ctrl Pts',(23.5169193837303,-4.16254577021058,128.181159726421));
#66479=CARTESIAN_POINT('Ctrl Pts',(23.5091630809884,-4.23236430876659,128.299111045093));
#66480=CARTESIAN_POINT('Ctrl Pts',(23.5014026384742,-4.30222011157883,128.417125317934));
#66481=CARTESIAN_POINT('Ctrl Pts',(23.49364219596,-4.3670807632239,128.537969935751));
#66482=CARTESIAN_POINT('Ctrl Pts',(23.4858817534459,-4.42673084691588,128.66117675437));
#66483=CARTESIAN_POINT('Ctrl Pts',(23.4781088531804,-4.48647668621777,128.784581355513));
#66484=CARTESIAN_POINT('Ctrl Pts',(23.470335952915,-4.54099508711831,128.910355376189));
#66485=CARTESIAN_POINT('Ctrl Pts',(23.4625630526495,-4.59011904094761,129.03801120354));
#66486=CARTESIAN_POINT('Ctrl Pts',(23.4550727168875,-4.63745721531911,129.16102642002));
#66487=CARTESIAN_POINT('Ctrl Pts',(23.4475823811255,-4.67978623790627,129.285788710003));
#66488=CARTESIAN_POINT('Ctrl Pts',(23.4400920453635,-4.71700133734242,129.411851570554));
#66489=CARTESIAN_POINT('Ctrl Pts',(23.4367303194496,-4.73370378809248,129.468429646434));
#66490=CARTESIAN_POINT('Ctrl Pts',(23.4333685935357,-4.74939168437933,129.525319913658));
#66491=CARTESIAN_POINT('Ctrl Pts',(23.4300068676217,-4.76405452823403,129.582490119308));
#66492=CARTESIAN_POINT('Origin',(213.235140564004,0.,130.804360617566));
#66493=CARTESIAN_POINT('',(21.3349957656066,-4.76405452823399,129.582490119308));
#66494=CARTESIAN_POINT('',(21.6799128182693,-4.76405452823405,129.582490119308));
#66495=CARTESIAN_POINT('',(213.235140564004,-4.76405452823405,129.582490119308));
#66496=CARTESIAN_POINT('',(23.0148594359424,-4.91824935608045,130.80687734446));
#66497=CARTESIAN_POINT('Ctrl Pts',(23.0148594359423,-4.91824935608045,130.80687734446));
#66498=CARTESIAN_POINT('Ctrl Pts',(23.0063233041041,-4.91817186460964,130.958313075279));
#66499=CARTESIAN_POINT('Ctrl Pts',(22.9977871722658,-4.91109609712324,131.109507565572));
#66500=CARTESIAN_POINT('Ctrl Pts',(22.9892510404275,-4.89711325436575,131.259843697839));
#66501=CARTESIAN_POINT('Ctrl Pts',(22.9806698930086,-4.88305667261293,131.410972632797));
#66502=CARTESIAN_POINT('Ctrl Pts',(22.9720887455896,-4.86202006107709,131.561233895066));
#66503=CARTESIAN_POINT('Ctrl Pts',(22.9635075981707,-4.83414632790528,131.710016370543));
#66504=CARTESIAN_POINT('Ctrl Pts',(22.9549031950898,-4.80619705447221,131.859202059575));
#66505=CARTESIAN_POINT('Ctrl Pts',(22.9462987920088,-4.77137366953818,132.006900713411));
#66506=CARTESIAN_POINT('Ctrl Pts',(22.9376943889279,-4.72986906089499,132.15251555276));
#66507=CARTESIAN_POINT('Ctrl Pts',(22.9290591231688,-4.688215581567,132.298652690272));
#66508=CARTESIAN_POINT('Ctrl Pts',(22.9204238574096,-4.63983298507327,132.442690820695));
#66509=CARTESIAN_POINT('Ctrl Pts',(22.9117885916505,-4.58496354168943,132.584049462246));
#66510=CARTESIAN_POINT('Ctrl Pts',(22.9087876590661,-4.56589528077753,132.633174499662));
#66511=CARTESIAN_POINT('Ctrl Pts',(22.9057867264817,-4.54604400850942,132.681976149457));
#66512=CARTESIAN_POINT('Ctrl Pts',(22.9027857938973,-4.52542118092908,132.73043076107));
#66513=CARTESIAN_POINT('Ctrl Pts',(22.8950114597781,-4.4719948717462,132.855959185884));
#66514=CARTESIAN_POINT('Ctrl Pts',(22.887237125659,-4.41325702436792,132.979461805039));
#66515=CARTESIAN_POINT('Ctrl Pts',(22.8794627915399,-4.3493823677675,133.100456452119));
#66516=CARTESIAN_POINT('Ctrl Pts',(22.8716980385927,-4.28558643097271,133.221301984111));
#66517=CARTESIAN_POINT('Ctrl Pts',(22.8639332856456,-4.21666646184963,133.339645351477));
#66518=CARTESIAN_POINT('Ctrl Pts',(22.8561685326984,-4.1428455073722,133.455023584551));
#66519=CARTESIAN_POINT('Ctrl Pts',(22.8484114918134,-4.06909787290755,133.570287222338));
#66520=CARTESIAN_POINT('Ctrl Pts',(22.8406544509283,-3.99045914943143,133.682591259347));
#66521=CARTESIAN_POINT('Ctrl Pts',(22.8328974100433,-3.90719845128515,133.791496925935));
#66522=CARTESIAN_POINT('Ctrl Pts',(22.8251462188031,-3.8240005406789,133.900320465912));
#66523=CARTESIAN_POINT('Ctrl Pts',(22.817395027563,-3.73618782950813,134.005750427103));
#66524=CARTESIAN_POINT('Ctrl Pts',(22.8096438363228,-3.64407272408339,134.107376972974));
#66525=CARTESIAN_POINT('Ctrl Pts',(22.8018959395456,-3.55199677003571,134.208960324851));
#66526=CARTESIAN_POINT('Ctrl Pts',(22.7941480427685,-3.45562232076047,134.306743187538));
#66527=CARTESIAN_POINT('Ctrl Pts',(22.7864001459914,-3.35530190380313,134.400348965272));
#66528=CARTESIAN_POINT('Ctrl Pts',(22.7786538699072,-3.25500247171422,134.493935162694));
#66529=CARTESIAN_POINT('Ctrl Pts',(22.7709075938231,-3.15075899940555,134.583345746559));
#66530=CARTESIAN_POINT('Ctrl Pts',(22.7631613177389,-3.04296040873856,134.668241440437));
#66531=CARTESIAN_POINT('Ctrl Pts',(22.7554149844735,-2.93516102232701,134.753137760995));
#66532=CARTESIAN_POINT('Ctrl Pts',(22.7476686512081,-2.82380677234151,134.833518883169));
#66533=CARTESIAN_POINT('Ctrl Pts',(22.7399223179427,-2.70931882636476,134.909086498743));
#66534=CARTESIAN_POINT('Ctrl Pts',(22.7321742499397,-2.59480524160632,134.984671037161));
#66535=CARTESIAN_POINT('Ctrl Pts',(22.7244261819366,-2.47715689065008,135.055439708651));
#66536=CARTESIAN_POINT('Ctrl Pts',(22.7166781139336,-2.35682266576578,135.121138349235));
#66537=CARTESIAN_POINT('Ctrl Pts',(22.7089218111917,-2.23636054823513,135.186906815116));
#66538=CARTESIAN_POINT('Ctrl Pts',(22.7011655084498,-2.11320719814752,135.247594298355));
#66539=CARTESIAN_POINT('Ctrl Pts',(22.6934092057078,-1.98783528034439,135.30299307207));
#66540=CARTESIAN_POINT('Ctrl Pts',(22.6856487631936,-1.86239644777402,135.358421413779));
#66541=CARTESIAN_POINT('Ctrl Pts',(22.6778883206794,-1.73473705176687,135.408555278564));
#66542=CARTESIAN_POINT('Ctrl Pts',(22.6701278781652,-1.60534740240345,135.453236049334));
#66543=CARTESIAN_POINT('Ctrl Pts',(22.6623549778997,-1.47575004528803,135.497988545644));
#66544=CARTESIAN_POINT('Ctrl Pts',(22.6545820776342,-1.34441725915866,135.537270342975));
#66545=CARTESIAN_POINT('Ctrl Pts',(22.6468091773687,-1.21185296909385,135.570973192949));
#66546=CARTESIAN_POINT('Ctrl Pts',(22.6393188416073,-1.08410772489296,135.603450859431));
#66547=CARTESIAN_POINT('Ctrl Pts',(22.6318285058459,-0.955219260145688,
135.630748090198));
#66548=CARTESIAN_POINT('Ctrl Pts',(22.6243381700844,-0.825643326977589,
135.652813583113));
#66549=CARTESIAN_POINT('Ctrl Pts',(22.6165638359653,-0.691154482909617,
135.675715695899));
#66550=CARTESIAN_POINT('Ctrl Pts',(22.6087895018463,-0.555498990380398,
135.69305406373));
#66551=CARTESIAN_POINT('Ctrl Pts',(22.6010151677272,-0.419176954928391,
135.704715068313));
#66552=CARTESIAN_POINT('Ctrl Pts',(22.5932504147801,-0.283022924201629,
135.716361701751));
#66553=CARTESIAN_POINT('Ctrl Pts',(22.585485661833,-0.146204370804925,135.722344860571));
#66554=CARTESIAN_POINT('Ctrl Pts',(22.5777209088859,-0.00923136656696278,
135.722601954098));
#66555=CARTESIAN_POINT('Ctrl Pts',(22.5699638680009,0.127605594152209,135.722858792276));
#66556=CARTESIAN_POINT('Ctrl Pts',(22.5622068271159,0.264596311999639,135.717400882234));
#66557=CARTESIAN_POINT('Ctrl Pts',(22.5544497862309,0.401226174771141,135.706217471777));
#66558=CARTESIAN_POINT('Ctrl Pts',(22.5466985949908,0.537753003900302,135.695042494818));
#66559=CARTESIAN_POINT('Ctrl Pts',(22.5389474037507,0.673919131513696,135.678150643219));
#66560=CARTESIAN_POINT('Ctrl Pts',(22.5311962125106,0.80921088728567,135.6555832266));
#66561=CARTESIAN_POINT('Ctrl Pts',(22.5234483157335,0.944445140452415,135.633025401734));
#66562=CARTESIAN_POINT('Ctrl Pts',(22.5157004189564,1.07880537609453,135.604796873855));
#66563=CARTESIAN_POINT('Ctrl Pts',(22.5079525221793,1.21178420378202,135.570990675161));
#66564=CARTESIAN_POINT('Ctrl Pts',(22.5002062460952,1.34473521516545,135.537191547994));
#66565=CARTESIAN_POINT('Ctrl Pts',(22.4924599700112,1.47630501468061,135.497817166967));
#66566=CARTESIAN_POINT('Ctrl Pts',(22.4847136939271,1.60599793769223,135.453011355859));
#66567=CARTESIAN_POINT('Ctrl Pts',(22.4769673606617,1.73569181806755,135.408205214004));
#66568=CARTESIAN_POINT('Ctrl Pts',(22.4692210273963,1.8635084247593,135.357967689728));
#66569=CARTESIAN_POINT('Ctrl Pts',(22.461474694131,1.98896913125135,135.302491880372));
#66570=CARTESIAN_POINT('Ctrl Pts',(22.453726626128,2.11445793379874,135.247003647592));
#66571=CARTESIAN_POINT('Ctrl Pts',(22.445978558125,2.23758942880797,135.18627495352));
#66572=CARTESIAN_POINT('Ctrl Pts',(22.438230490122,2.35790714368988,135.120546082098));
#66573=CARTESIAN_POINT('Ctrl Pts',(22.4304741873802,2.47835273367096,135.054747353249));
#66574=CARTESIAN_POINT('Ctrl Pts',(22.4227178846384,2.59597822598835,134.983938019002));
#66575=CARTESIAN_POINT('Ctrl Pts',(22.4149615818965,2.71035336724085,134.908403464222));
#66576=CARTESIAN_POINT('Ctrl Pts',(22.4072011393823,2.82478955395015,134.832828594375));
#66577=CARTESIAN_POINT('Ctrl Pts',(22.3994406968681,2.9359716160551,134.752523707518));
#66578=CARTESIAN_POINT('Ctrl Pts',(22.391680254354,3.04350107992747,134.667815578994));
#66579=CARTESIAN_POINT('Ctrl Pts',(22.3839073540885,3.15120315964111,134.582971469462));
#66580=CARTESIAN_POINT('Ctrl Pts',(22.3761344538231,3.25524062713876,134.493710247924));
#66581=CARTESIAN_POINT('Ctrl Pts',(22.3683615535577,3.3552500261785,134.400397369927));
#66582=CARTESIAN_POINT('Ctrl Pts',(22.3608712177957,3.45162383165535,134.310476650085));
#66583=CARTESIAN_POINT('Ctrl Pts',(22.3533808820336,3.54425712847715,134.216793954376));
#66584=CARTESIAN_POINT('Ctrl Pts',(22.3458905462715,3.63286040954603,134.119704989913));
#66585=CARTESIAN_POINT('Ctrl Pts',(22.3381162121525,3.72482311094637,134.018934867853));
#66586=CARTESIAN_POINT('Ctrl Pts',(22.3303418780333,3.81273547813195,133.914175871351));
#66587=CARTESIAN_POINT('Ctrl Pts',(22.3225675439143,3.89623160155745,133.805787339897));
#66588=CARTESIAN_POINT('Ctrl Pts',(22.3148027909672,3.97962482347297,133.697532387622));
#66589=CARTESIAN_POINT('Ctrl Pts',(22.3070380380201,4.05861239453024,133.585657107236));
#66590=CARTESIAN_POINT('Ctrl Pts',(22.2992732850731,4.13286594913798,133.470556804825));
#66591=CARTESIAN_POINT('Ctrl Pts',(22.2915162441881,4.2070457540686,133.355570821657));
#66592=CARTESIAN_POINT('Ctrl Pts',(22.283759203303,4.2765006889549,133.237366517259));
#66593=CARTESIAN_POINT('Ctrl Pts',(22.2760021624181,4.34094354720525,133.116371037628));
#66594=CARTESIAN_POINT('Ctrl Pts',(22.2682509711779,4.4053378085949,132.995466801631));
#66595=CARTESIAN_POINT('Ctrl Pts',(22.2604997799379,4.4647273334603,132.871775923649));
#66596=CARTESIAN_POINT('Ctrl Pts',(22.2527485886978,4.51886922539576,132.745752897934));
#66597=CARTESIAN_POINT('Ctrl Pts',(22.2450006919207,4.5729881055828,132.619783435366));
#66598=CARTESIAN_POINT('Ctrl Pts',(22.2372527951435,4.62186363490008,132.491484155002));
#66599=CARTESIAN_POINT('Ctrl Pts',(22.2295048983665,4.66529982705084,132.361332224956));
#66600=CARTESIAN_POINT('Ctrl Pts',(22.2217586222824,4.70872693328657,132.231207519888));
#66601=CARTESIAN_POINT('Ctrl Pts',(22.2140123461983,4.74671684179706,132.099231306588));
#66602=CARTESIAN_POINT('Ctrl Pts',(22.2062660701143,4.77912263675844,131.965898342017));
#66603=CARTESIAN_POINT('Ctrl Pts',(22.1985197368489,4.81152867093203,131.832564393213));
#66604=CARTESIAN_POINT('Ctrl Pts',(22.1907734035836,4.83835041696987,131.697874053058));
#66605=CARTESIAN_POINT('Ctrl Pts',(22.1830270703183,4.8594916238085,131.562334377425));
#66606=CARTESIAN_POINT('Ctrl Pts',(22.1752790023153,4.88063756507382,131.426764348622));
#66607=CARTESIAN_POINT('Ctrl Pts',(22.1675309343124,4.89610037553176,131.290344992079));
#66608=CARTESIAN_POINT('Ctrl Pts',(22.1597828663094,4.90583547828324,131.153590230453));
#66609=CARTESIAN_POINT('Ctrl Pts',(22.1520265635676,4.91558092761777,131.01669012424));
#66610=CARTESIAN_POINT('Ctrl Pts',(22.1442702608258,4.9195864810515,130.879454291452));
#66611=CARTESIAN_POINT('Ctrl Pts',(22.1365139580839,4.91785967848011,130.742398973951));
#66612=CARTESIAN_POINT('Ctrl Pts',(22.1287535155698,4.9161319542622,130.6052705059));
#66613=CARTESIAN_POINT('Ctrl Pts',(22.1209930730556,4.90866579893738,130.46832313531));
#66614=CARTESIAN_POINT('Ctrl Pts',(22.1132326305414,4.89552075312753,130.332068739383));
#66615=CARTESIAN_POINT('Ctrl Pts',(22.105459730276,4.88235460572318,130.195595615804));
#66616=CARTESIAN_POINT('Ctrl Pts',(22.0976868300106,4.86349140447315,130.059818077336));
#66617=CARTESIAN_POINT('Ctrl Pts',(22.0899139297452,4.83904216050259,129.925239447659));
#66618=CARTESIAN_POINT('Ctrl Pts',(22.082423593983,4.81548170813386,129.795553090152));
#66619=CARTESIAN_POINT('Ctrl Pts',(22.0749332582209,4.78673436262831,129.666980288665));
#66620=CARTESIAN_POINT('Ctrl Pts',(22.0674429224587,4.7529429047956,129.539956882103));
#66621=CARTESIAN_POINT('Ctrl Pts',(22.0596685883396,4.71787023356905,129.408117344475));
#66622=CARTESIAN_POINT('Ctrl Pts',(22.0518942542205,4.67725230472525,129.277529383664));
#66623=CARTESIAN_POINT('Ctrl Pts',(22.0441199201015,4.63119365770849,129.148695081505));
#66624=CARTESIAN_POINT('Ctrl Pts',(22.0363551671544,4.58519177385779,129.020019556109));
#66625=CARTESIAN_POINT('Ctrl Pts',(22.0285904142072,4.53376264353133,128.89309375378));
#66626=CARTESIAN_POINT('Ctrl Pts',(22.0208256612601,4.47706135931208,128.768407610384));
#66627=CARTESIAN_POINT('Ctrl Pts',(22.0130686203751,4.42041639160767,128.643845307023));
#66628=CARTESIAN_POINT('Ctrl Pts',(22.0053115794901,4.35850985143435,128.521518589409));
#66629=CARTESIAN_POINT('Ctrl Pts',(21.9975545386051,4.29154586663991,128.401899975427));
#66630=CARTESIAN_POINT('Ctrl Pts',(21.989803347365,4.22463237990732,128.282371566773));
#66631=CARTESIAN_POINT('Ctrl Pts',(21.9820521561249,4.15266923001278,128.165547536638));
#66632=CARTESIAN_POINT('Ctrl Pts',(21.9743009648848,4.07590750440126,128.051877905892));
#66633=CARTESIAN_POINT('Ctrl Pts',(21.9665530681077,3.99917840457082,127.938256587771));
#66634=CARTESIAN_POINT('Ctrl Pts',(21.9588051713305,3.91765500382286,127.827787325808));
#66635=CARTESIAN_POINT('Ctrl Pts',(21.9510572745534,3.83163282182608,127.720892929847));
#66636=CARTESIAN_POINT('Ctrl Pts',(21.9433109984693,3.74562863381534,127.61402089389));
#66637=CARTESIAN_POINT('Ctrl Pts',(21.9355647223852,3.65512778130999,127.510722540942));
#66638=CARTESIAN_POINT('Ctrl Pts',(21.9278184463011,3.56046710576245,127.411388903672));
#66639=CARTESIAN_POINT('Ctrl Pts',(21.9200721130358,3.46580573145132,127.312054533144));
#66640=CARTESIAN_POINT('Ctrl Pts',(21.9123257797705,3.36698474254132,127.216685219723));
#66641=CARTESIAN_POINT('Ctrl Pts',(21.9045794465051,3.26437871344689,127.125636018239));
#66642=CARTESIAN_POINT('Ctrl Pts',(21.8968313785021,3.16174970644381,127.034566426918));
#66643=CARTESIAN_POINT('Ctrl Pts',(21.8890833104992,3.05533426493972,126.947819132111));
#66644=CARTESIAN_POINT('Ctrl Pts',(21.8813352424962,2.94554067171819,126.865709425374));
#66645=CARTESIAN_POINT('Ctrl Pts',(21.8735789397544,2.83563038855907,126.783512451464));
#66646=CARTESIAN_POINT('Ctrl Pts',(21.8658226370124,2.72233509518536,126.705963146124));
#66647=CARTESIAN_POINT('Ctrl Pts',(21.8580663342706,2.60609319599383,126.633334207161));
#66648=CARTESIAN_POINT('Ctrl Pts',(21.8503058917564,2.48978925500072,126.560666503947));
#66649=CARTESIAN_POINT('Ctrl Pts',(21.8425454492422,2.37053591424746,126.492924592945));
#66650=CARTESIAN_POINT('Ctrl Pts',(21.834785006728,2.24879601368324,126.430335063075));
#66651=CARTESIAN_POINT('Ctrl Pts',(21.8270121064626,2.12686068542307,126.367645058935));
#66652=CARTESIAN_POINT('Ctrl Pts',(21.8192392061972,2.00243117585515,126.310124128288));
#66653=CARTESIAN_POINT('Ctrl Pts',(21.8114663059318,1.8759909496709,126.257950933073));
#66654=CARTESIAN_POINT('Ctrl Pts',(21.8039759701698,1.75414714419302,126.207674364921));
#66655=CARTESIAN_POINT('Ctrl Pts',(21.7964856344078,1.63043656249565,126.162363581094));
#66656=CARTESIAN_POINT('Ctrl Pts',(21.7889952986458,1.50530306470711,126.122134037627));
#66657=CARTESIAN_POINT('Ctrl Pts',(21.7812209645267,1.37542509231568,126.080379178792));
#66658=CARTESIAN_POINT('Ctrl Pts',(21.7734466304077,1.24360275975388,126.043966210081));
#66659=CARTESIAN_POINT('Ctrl Pts',(21.7656722962886,1.11031498881336,126.013078566996));
#66660=CARTESIAN_POINT('Ctrl Pts',(21.7579075433415,0.977191483138436,125.98222899017));
#66661=CARTESIAN_POINT('Ctrl Pts',(21.7501427903944,0.842606509745777,125.956891277568));
#66662=CARTESIAN_POINT('Ctrl Pts',(21.7423780374473,0.707056096885537,125.937199767711));
#66663=CARTESIAN_POINT('Ctrl Pts',(21.7346209965623,0.571640314606091,125.91752781574));
#66664=CARTESIAN_POINT('Ctrl Pts',(21.7268639556773,0.435261385489979,125.903490962406));
#66665=CARTESIAN_POINT('Ctrl Pts',(21.7191069147923,0.29842718830451,125.895172876628));
#66666=CARTESIAN_POINT('Ctrl Pts',(21.7113557235522,0.161696178851553,125.886861063583));
#66667=CARTESIAN_POINT('Ctrl Pts',(21.7036045323121,0.0245109733550467,
125.884259457818));
#66668=CARTESIAN_POINT('Ctrl Pts',(21.695853341072,-0.112614093985012,125.887400059626));
#66669=CARTESIAN_POINT('Ctrl Pts',(21.6881054442949,-0.24968087951352,125.890539326595));
#66670=CARTESIAN_POINT('Ctrl Pts',(21.6803575475178,-0.386687187678713,
125.899415938054));
#66671=CARTESIAN_POINT('Ctrl Pts',(21.6726096507407,-0.523117560985009,
125.914009803985));
#66672=CARTESIAN_POINT('Ctrl Pts',(21.6648633746566,-0.659519395998308,
125.928600617194));
#66673=CARTESIAN_POINT('Ctrl Pts',(21.6571170985726,-0.795345147279287,
125.948906264554));
#66674=CARTESIAN_POINT('Ctrl Pts',(21.6493708224885,-0.930083756938391,
125.974854714518));
#66675=CARTESIAN_POINT('Ctrl Pts',(21.6416244892231,-1.06482336120712,126.000803356027));
#66676=CARTESIAN_POINT('Ctrl Pts',(21.6338781559577,-1.19847542392991,126.032394809324));
#66677=CARTESIAN_POINT('Ctrl Pts',(21.6261318226924,-1.33053876080233,126.069505850152));
#66678=CARTESIAN_POINT('Ctrl Pts',(21.6183837546894,-1.46263167234339,126.106625201741));
#66679=CARTESIAN_POINT('Ctrl Pts',(21.6106356866865,-1.59313477375025,126.149266494756));
#66680=CARTESIAN_POINT('Ctrl Pts',(21.6028876186836,-1.7215621144891,126.197256652117));
#66681=CARTESIAN_POINT('Ctrl Pts',(21.5951313159417,-1.85012594933417,126.245297813988));
#66682=CARTESIAN_POINT('Ctrl Pts',(21.5873750131999,-1.97660924968733,126.298699059209));
#66683=CARTESIAN_POINT('Ctrl Pts',(21.579618710458,-2.10054561887412,126.357238945571));
#66684=CARTESIAN_POINT('Ctrl Pts',(21.5718582679439,-2.22454813663279,126.415810076432));
#66685=CARTESIAN_POINT('Ctrl Pts',(21.5640978254297,-2.34600066851148,126.479525131853));
#66686=CARTESIAN_POINT('Ctrl Pts',(21.5563373829155,-2.46446240253599,126.548117188322));
#66687=CARTESIAN_POINT('Ctrl Pts',(21.5485644826501,-2.5831143018525,126.616819354848));
#66688=CARTESIAN_POINT('Ctrl Pts',(21.5407915823847,-2.69876547916453,126.690413957233));
#66689=CARTESIAN_POINT('Ctrl Pts',(21.5330186821193,-2.81100429664725,126.76859081408));
#66690=CARTESIAN_POINT('Ctrl Pts',(21.5255283463571,-2.91916295040333,126.843925745266));
#66691=CARTESIAN_POINT('Ctrl Pts',(21.518038010595,-3.02415278731309,126.923515375879));
#66692=CARTESIAN_POINT('Ctrl Pts',(21.5105476748329,-3.12563675370366,127.00704868063));
#66693=CARTESIAN_POINT('Ctrl Pts',(21.5028809039019,-3.22951117912261,127.092549615831));
#66694=CARTESIAN_POINT('Ctrl Pts',(21.4952141329709,-3.33006085910876,127.182469365699));
#66695=CARTESIAN_POINT('Ctrl Pts',(21.4875473620399,-3.4268786485251,127.276516262895));
#66696=CARTESIAN_POINT('Ctrl Pts',(21.4798893792858,-3.52358545877347,127.37045535711));
#66697=CARTESIAN_POINT('Ctrl Pts',(21.4722313965317,-3.6165685964263,127.468511917343));
#66698=CARTESIAN_POINT('Ctrl Pts',(21.4645734137776,-3.70545233636739,127.57035288019));
#66699=CARTESIAN_POINT('Ctrl Pts',(21.4569224419515,-3.79425470272478,127.67210060704));
#66700=CARTESIAN_POINT('Ctrl Pts',(21.4492714701254,-3.87896487069117,127.777625546692));
#66701=CARTESIAN_POINT('Ctrl Pts',(21.4416204982993,-3.95924290016274,127.886556868166));
#66702=CARTESIAN_POINT('Ctrl Pts',(21.4339747666824,-4.03946594659654,127.995413581743));
#66703=CARTESIAN_POINT('Ctrl Pts',(21.4263290350655,-4.11526265422054,128.10767171418));
#66704=CARTESIAN_POINT('Ctrl Pts',(21.4186833034487,-4.18633280130811,128.222926764222));
#66705=CARTESIAN_POINT('Ctrl Pts',(21.4110402676312,-4.25737788985743,128.338141176623));
#66706=CARTESIAN_POINT('Ctrl Pts',(21.4033972318137,-4.32369951793267,128.456350065217));
#66707=CARTESIAN_POINT('Ctrl Pts',(21.3957541959962,-4.38504055658446,128.577119638325));
#66708=CARTESIAN_POINT('Ctrl Pts',(21.3881128424118,-4.44636809406644,128.697862630036));
#66709=CARTESIAN_POINT('Ctrl Pts',(21.3804714888275,-4.50271704387422,128.821164824662));
#66710=CARTESIAN_POINT('Ctrl Pts',(21.3728301352431,-4.5538763862623,128.946568131538));
#66711=CARTESIAN_POINT('Ctrl Pts',(21.3651865881523,-4.60505041431342,129.07200743635));
#66712=CARTESIAN_POINT('Ctrl Pts',(21.3575430410616,-4.65103170633734,129.199548685551));
#66713=CARTESIAN_POINT('Ctrl Pts',(21.3498994939708,-4.69165758490788,129.328714261396));
#66714=CARTESIAN_POINT('Ctrl Pts',(21.3449315845161,-4.71806230039657,129.412665191226));
#66715=CARTESIAN_POINT('Ctrl Pts',(21.3399636750613,-4.74220571102834,129.497301912625));
#66716=CARTESIAN_POINT('Ctrl Pts',(21.3349957656066,-4.76405452823399,129.582490119308));
#66717=CARTESIAN_POINT('Ctrl Pts',(23.0846591878033,-4.76405452823398,129.582490119308));
#66718=CARTESIAN_POINT('Ctrl Pts',(23.0767991264479,-4.79862266817693,129.717270772301));
#66719=CARTESIAN_POINT('Ctrl Pts',(23.0689390650927,-4.82748971154215,129.853608202476));
#66720=CARTESIAN_POINT('Ctrl Pts',(23.0610790037373,-4.85052663452102,129.990988359432));
#66721=CARTESIAN_POINT('Ctrl Pts',(23.0532224290515,-4.87355333847808,130.128307575488));
#66722=CARTESIAN_POINT('Ctrl Pts',(23.0453658543657,-4.8907550081303,130.266668228245));
#66723=CARTESIAN_POINT('Ctrl Pts',(23.0375092796799,-4.90205361781031,130.405545634632));
#66724=CARTESIAN_POINT('Ctrl Pts',(23.0299593317837,-4.91291126478697,130.53900292666));
#66725=CARTESIAN_POINT('Ctrl Pts',(23.0224093838875,-4.91831789489641,130.672937064906));
#66726=CARTESIAN_POINT('Ctrl Pts',(23.0148594359913,-4.91824935608089,130.806877343592));
#66727=CARTESIAN_POINT('',(23.3601405640434,-4.91824805923248,130.79999136638));
#66728=CARTESIAN_POINT('Ctrl Pts',(23.4300068676217,-4.76405452823403,129.582490119308));
#66729=CARTESIAN_POINT('Ctrl Pts',(23.4203944872076,-4.80598085913958,129.745960247188));
#66730=CARTESIAN_POINT('Ctrl Pts',(23.4107821067936,-4.83952298414148,129.911720709109));
#66731=CARTESIAN_POINT('Ctrl Pts',(23.4011697263795,-4.86446705838591,130.079003257103));
#66732=CARTESIAN_POINT('Ctrl Pts',(23.3916925947081,-4.8890601628878,130.243932095264));
#66733=CARTESIAN_POINT('Ctrl Pts',(23.3822154630367,-4.90529544518096,130.410340540976));
#66734=CARTESIAN_POINT('Ctrl Pts',(23.3727383313653,-4.913013755741,130.577471000352));
#66735=CARTESIAN_POINT('Ctrl Pts',(23.3685390755913,-4.91643368925132,130.651525426403));
#66736=CARTESIAN_POINT('Ctrl Pts',(23.3643398198173,-4.91818207954048,130.725721319109));
#66737=CARTESIAN_POINT('Ctrl Pts',(23.3601405640433,-4.91824805923248,130.79999136638));
#66738=CARTESIAN_POINT('Ctrl Pts',(23.3601405640087,-4.91824805923302,130.799991366992));
#66739=CARTESIAN_POINT('Ctrl Pts',(23.3524493576804,-4.91836890525452,130.936021722922));
#66740=CARTESIAN_POINT('Ctrl Pts',(23.3447581513522,-4.91284195572749,131.072164803608));
#66741=CARTESIAN_POINT('Ctrl Pts',(23.3370669450239,-4.90166600722439,131.207911625644));
#66742=CARTESIAN_POINT('Ctrl Pts',(23.3293785715744,-4.89049417512461,131.343608448464));
#66743=CARTESIAN_POINT('Ctrl Pts',(23.321690198125,-4.87367751226833,131.478908907352));
#66744=CARTESIAN_POINT('Ctrl Pts',(23.3140018246755,-4.85126688212405,131.613306042738));
#66745=CARTESIAN_POINT('Ctrl Pts',(23.3063147009714,-4.82885989482867,131.747681331863));
#66746=CARTESIAN_POINT('Ctrl Pts',(23.2986275772674,-4.8008608136778,131.88115319757));
#66747=CARTESIAN_POINT('Ctrl Pts',(23.2909404535633,-4.7673720683186,132.013222323766));
#66748=CARTESIAN_POINT('Ctrl Pts',(23.2832528521044,-4.73388124163343,132.145299658059));
#66749=CARTESIAN_POINT('Ctrl Pts',(23.2755652506455,-4.69490016976641,132.275973694137));
#66750=CARTESIAN_POINT('Ctrl Pts',(23.2678776491866,-4.65058173179877,132.404758261391));
#66751=CARTESIAN_POINT('Ctrl Pts',(23.2601878424331,-4.60625058047556,132.533579772275));
#66752=CARTESIAN_POINT('Ctrl Pts',(23.2524980356797,-4.55657914682727,132.660510360545));
#66753=CARTESIAN_POINT('Ctrl Pts',(23.2448082289262,-4.50176904100897,132.785082345602));
#66754=CARTESIAN_POINT('Ctrl Pts',(23.2371099815117,-4.44689877327234,132.909791066202));
#66755=CARTESIAN_POINT('Ctrl Pts',(23.2294117340971,-4.38687873152101,133.032135650302));
#66756=CARTESIAN_POINT('Ctrl Pts',(23.2217134866826,-4.32195740773694,133.151671254914));
#66757=CARTESIAN_POINT('Ctrl Pts',(23.2140105872283,-4.25699685209071,133.27127909472));
#66758=CARTESIAN_POINT('Ctrl Pts',(23.2063076877739,-4.1871293199716,133.388074234461));
#66759=CARTESIAN_POINT('Ctrl Pts',(23.1986047883196,-4.11264686820347,133.501640506631));
#66760=CARTESIAN_POINT('Ctrl Pts',(23.1908901871356,-4.03805126767569,133.615379301087));
#66761=CARTESIAN_POINT('Ctrl Pts',(23.1831755859515,-3.9588269793492,133.725879111192));
#66762=CARTESIAN_POINT('Ctrl Pts',(23.1754609847674,-3.87530691427489,133.832756130486));
#66763=CARTESIAN_POINT('Ctrl Pts',(23.1708554636952,-3.82544647295366,133.896560383324));
#66764=CARTESIAN_POINT('Ctrl Pts',(23.166249942623,-3.77405578018836,133.959074172579));
#66765=CARTESIAN_POINT('Ctrl Pts',(23.1616444215508,-3.72121174115413,134.020222281257));
#66766=CARTESIAN_POINT('Ctrl Pts',(23.1538700874317,-3.63200854151381,134.123443137302));
#66767=CARTESIAN_POINT('Ctrl Pts',(23.1460957533127,-3.53836600701794,134.223113129705));
#66768=CARTESIAN_POINT('Ctrl Pts',(23.1383214191936,-3.44059774490611,134.318826468908));
#66769=CARTESIAN_POINT('Ctrl Pts',(23.1305566662465,-3.34294997343953,134.414421849974));
#66770=CARTESIAN_POINT('Ctrl Pts',(23.1227919132994,-3.24118686786929,134.50607000919));
#66771=CARTESIAN_POINT('Ctrl Pts',(23.1150271603523,-3.13566218455629,134.593398190202));
#66772=CARTESIAN_POINT('Ctrl Pts',(23.1072701194673,-3.03024230984653,134.680639635632));
#66773=CARTESIAN_POINT('Ctrl Pts',(23.0995130785823,-2.92106859155812,134.763569393822));
#66774=CARTESIAN_POINT('Ctrl Pts',(23.0917560376973,-2.80853126434396,134.841851818758));
#66775=CARTESIAN_POINT('Ctrl Pts',(23.0840048464572,-2.69607880240321,134.920075210309));
#66776=CARTESIAN_POINT('Ctrl Pts',(23.0762536552171,-2.58026809998581,134.993658021925));
#66777=CARTESIAN_POINT('Ctrl Pts',(23.068502463977,-2.46152178199783,135.062305377571));
#66778=CARTESIAN_POINT('Ctrl Pts',(23.0607545671999,-2.34282593436282,135.130923556259));
#66779=CARTESIAN_POINT('Ctrl Pts',(23.0530066704227,-2.2211972905342,135.194610255879));
#66780=CARTESIAN_POINT('Ctrl Pts',(23.0452587736456,-2.0970865310741,135.253114504183));
#66781=CARTESIAN_POINT('Ctrl Pts',(23.0375124975615,-1.97300173290936,135.311606514659));
#66782=CARTESIAN_POINT('Ctrl Pts',(23.0297662214774,-1.84643620526013,135.36491806347));
#66783=CARTESIAN_POINT('Ctrl Pts',(23.0220199453933,-1.71786389007637,135.412844827984));
#66784=CARTESIAN_POINT('Ctrl Pts',(23.014273612128,-1.58929062580134,135.460771946282));
#66785=CARTESIAN_POINT('Ctrl Pts',(23.0065272788626,-1.4587109107733,135.503314064408));
#66786=CARTESIAN_POINT('Ctrl Pts',(22.9987809455973,-1.32661688371923,135.540315717261));
#66787=CARTESIAN_POINT('Ctrl Pts',(22.9910328775943,-1.19449327512332,135.577325656379));
#66788=CARTESIAN_POINT('Ctrl Pts',(22.9832848095914,-1.06085505609451,135.60879255584));
#66789=CARTESIAN_POINT('Ctrl Pts',(22.9755367415884,-0.926207287252766,
135.634611451999));
#66790=CARTESIAN_POINT('Ctrl Pts',(22.9677804388465,-0.791416413160151,
135.660457788787));
#66791=CARTESIAN_POINT('Ctrl Pts',(22.9600241361046,-0.655614230480491,
135.680644057358));
#66792=CARTESIAN_POINT('Ctrl Pts',(22.9522678333628,-0.519314258254587,
135.695116772157));
#66793=CARTESIAN_POINT('Ctrl Pts',(22.9445073908486,-0.382941538629593,
135.70959721148));
#66794=CARTESIAN_POINT('Ctrl Pts',(22.9367469483345,-0.246070890033827,
135.718357995691));
#66795=CARTESIAN_POINT('Ctrl Pts',(22.9289865058203,-0.10921763914018,135.721397791495));
#66796=CARTESIAN_POINT('Ctrl Pts',(22.9212136055549,0.0278553007410634,
135.72444246705));
#66797=CARTESIAN_POINT('Ctrl Pts',(22.9134407052895,0.16491039599584,135.721747809652));
#66798=CARTESIAN_POINT('Ctrl Pts',(22.9056678050241,0.301434734490052,135.713364606497));
#66799=CARTESIAN_POINT('Ctrl Pts',(22.898177469262,0.432996069396678,135.705286153893));
#66800=CARTESIAN_POINT('Ctrl Pts',(22.8906871334999,0.56406425984617,135.691925592244));
#66801=CARTESIAN_POINT('Ctrl Pts',(22.8831967977378,0.694189653854869,135.673373226605));
#66802=CARTESIAN_POINT('Ctrl Pts',(22.8754224636188,0.829248791727227,135.654117442384));
#66803=CARTESIAN_POINT('Ctrl Pts',(22.8676481294997,0.963720056377465,135.629207391487));
#66804=CARTESIAN_POINT('Ctrl Pts',(22.8598737953807,1.0970925331851,135.598687581398));
#66805=CARTESIAN_POINT('Ctrl Pts',(22.8521090424336,1.23030064033491,135.568205384248));
#66806=CARTESIAN_POINT('Ctrl Pts',(22.8443442894865,1.36241227655698,135.532127270138));
#66807=CARTESIAN_POINT('Ctrl Pts',(22.8365795365395,1.49292261741866,135.490549380399));
#66808=CARTESIAN_POINT('Ctrl Pts',(22.8288224956545,1.62330333356975,135.449012786406));
#66809=CARTESIAN_POINT('Ctrl Pts',(22.8210654547694,1.75208554927871,135.401987405223));
#66810=CARTESIAN_POINT('Ctrl Pts',(22.8133084138845,1.87877594468694,135.349620127447));
#66811=CARTESIAN_POINT('Ctrl Pts',(22.8055572226444,2.00537080188213,135.297292340243));
#66812=CARTESIAN_POINT('Ctrl Pts',(22.7978060314044,2.1298766187578,135.239630823409));
#66813=CARTESIAN_POINT('Ctrl Pts',(22.7900548401643,2.25181686866827,135.176831755547));
#66814=CARTESIAN_POINT('Ctrl Pts',(22.7823069433872,2.37370529072016,135.114059378964));
#66815=CARTESIAN_POINT('Ctrl Pts',(22.7745590466101,2.49302996774566,135.046153972988));
#66816=CARTESIAN_POINT('Ctrl Pts',(22.7668111498331,2.60933614583188,134.973359051309));
#66817=CARTESIAN_POINT('Ctrl Pts',(22.759064873749,2.72561799517307,134.900579356759));
#66818=CARTESIAN_POINT('Ctrl Pts',(22.7513185976649,2.83888227027877,134.822912388165));
#66819=CARTESIAN_POINT('Ctrl Pts',(22.7435723215808,2.94870089153081,134.74064644494));
#66820=CARTESIAN_POINT('Ctrl Pts',(22.7358259883155,3.05852032343868,134.658379894447));
#66821=CARTESIAN_POINT('Ctrl Pts',(22.7280796550501,3.16489373783297,134.57151453598));
#66822=CARTESIAN_POINT('Ctrl Pts',(22.7203333217848,3.26742432451853,134.480380387105));
#66823=CARTESIAN_POINT('Ctrl Pts',(22.7125852537818,3.36997787221837,134.38922582937));
#66824=CARTESIAN_POINT('Ctrl Pts',(22.7048371857788,3.46868658760461,134.293800838651));
#66825=CARTESIAN_POINT('Ctrl Pts',(22.6970891177759,3.56318916418544,134.194473601337));
#66826=CARTESIAN_POINT('Ctrl Pts',(22.689332815034,3.65779217922913,134.095040797853));
#66827=CARTESIAN_POINT('Ctrl Pts',(22.6815765122922,3.74817985557386,133.991697746687));
#66828=CARTESIAN_POINT('Ctrl Pts',(22.6738202095504,3.83402962472286,133.884847575702));
#66829=CARTESIAN_POINT('Ctrl Pts',(22.6660597670362,3.91992521447854,133.777940375564));
#66830=CARTESIAN_POINT('Ctrl Pts',(22.6582993245221,4.00127783917086,133.667522640383));
#66831=CARTESIAN_POINT('Ctrl Pts',(22.650538882008,4.07780783040716,133.554027208404));
#66832=CARTESIAN_POINT('Ctrl Pts',(22.6427659817426,4.1544606743794,133.440349583482));
#66833=CARTESIAN_POINT('Ctrl Pts',(22.6349930814771,4.22627520953607,133.323584722098));
#66834=CARTESIAN_POINT('Ctrl Pts',(22.6272201812117,4.29301692304613,133.204191603477));
#66835=CARTESIAN_POINT('Ctrl Pts',(22.6197298454494,4.35733240715977,133.089138725448));
#66836=CARTESIAN_POINT('Ctrl Pts',(22.6122395096872,4.41693734671143,132.971645634855));
#66837=CARTESIAN_POINT('Ctrl Pts',(22.604749173925,4.47166467002125,132.852139448735));
#66838=CARTESIAN_POINT('Ctrl Pts',(22.5969748398059,4.52846699642694,132.728102149249));
#66839=CARTESIAN_POINT('Ctrl Pts',(22.5892005056868,4.58019446830472,132.601503174902));
#66840=CARTESIAN_POINT('Ctrl Pts',(22.5814261715677,4.62660836922988,132.472796430018));
#66841=CARTESIAN_POINT('Ctrl Pts',(22.5736614186206,4.67296506917014,132.344248304694));
#66842=CARTESIAN_POINT('Ctrl Pts',(22.5658966656736,4.71402109636827,132.213597941611));
#66843=CARTESIAN_POINT('Ctrl Pts',(22.5581319127265,4.74958446731142,132.081322030599));
#66844=CARTESIAN_POINT('Ctrl Pts',(22.5503748718415,4.78511251621329,131.949177497885));
#66845=CARTESIAN_POINT('Ctrl Pts',(22.5426178309564,4.81515866446744,131.815411005319));
#66846=CARTESIAN_POINT('Ctrl Pts',(22.5348607900714,4.83957984385959,131.680516994823));
#66847=CARTESIAN_POINT('Ctrl Pts',(22.5271095988313,4.86398260705025,131.545724708951));
#66848=CARTESIAN_POINT('Ctrl Pts',(22.5193584075912,4.8827687751236,131.409806980715));
#66849=CARTESIAN_POINT('Ctrl Pts',(22.5116072163511,4.89584582440208,131.273270764806));
#66850=CARTESIAN_POINT('Ctrl Pts',(22.503859319574,4.90891731558585,131.13679258043));
#66851=CARTESIAN_POINT('Ctrl Pts',(22.4961114227969,4.91628447695654,130.999696819586));
#66852=CARTESIAN_POINT('Ctrl Pts',(22.4883635260198,4.91790637788049,130.862497704717));
#66853=CARTESIAN_POINT('Ctrl Pts',(22.4806172499357,4.91952793953773,130.725327288945));
#66854=CARTESIAN_POINT('Ctrl Pts',(22.4728709738516,4.91540662654518,130.588053952842));
#66855=CARTESIAN_POINT('Ctrl Pts',(22.4651246977675,4.90555360587275,130.451193684786));
#66856=CARTESIAN_POINT('Ctrl Pts',(22.4573783645021,4.89570051246756,130.31433240646));
#66857=CARTESIAN_POINT('Ctrl Pts',(22.4496320312368,4.88011565502983,130.177884592223));
#66858=CARTESIAN_POINT('Ctrl Pts',(22.4418856979714,4.85886220108035,130.042362472284));
#66859=CARTESIAN_POINT('Ctrl Pts',(22.4341376299685,4.83760398756724,129.906810003107));
#66860=CARTESIAN_POINT('Ctrl Pts',(22.4263895619654,4.81067471205974,129.772184026908));
#66861=CARTESIAN_POINT('Ctrl Pts',(22.4186414939625,4.77818884520936,129.638987534808));
#66862=CARTESIAN_POINT('Ctrl Pts',(22.4108851912206,4.74566845199301,129.505649479891));
#66863=CARTESIAN_POINT('Ctrl Pts',(22.4031288884787,4.70757976312526,129.37374432442));
#66864=CARTESIAN_POINT('Ctrl Pts',(22.3953725857368,4.66408758534354,129.243761354865));
#66865=CARTESIAN_POINT('Ctrl Pts',(22.3876121432226,4.62057219447691,129.113709009485));
#66866=CARTESIAN_POINT('Ctrl Pts',(22.3798517007084,4.57164770746976,128.985581259335));
#66867=CARTESIAN_POINT('Ctrl Pts',(22.3720912581942,4.51752711579995,128.859847357001));
#66868=CARTESIAN_POINT('Ctrl Pts',(22.3643183579287,4.46331964495186,128.733911615445));
#66869=CARTESIAN_POINT('Ctrl Pts',(22.3565454576633,4.40389957053603,128.610377753406));
#66870=CARTESIAN_POINT('Ctrl Pts',(22.3487725573979,4.3395262848596,128.489691162652));
#66871=CARTESIAN_POINT('Ctrl Pts',(22.341282221636,4.27749313026517,128.373391833465));
#66872=CARTESIAN_POINT('Ctrl Pts',(22.333791885874,4.2108607913339,128.259736624332));
#66873=CARTESIAN_POINT('Ctrl Pts',(22.3263015501121,4.1398983074016,128.149096964579));
#66874=CARTESIAN_POINT('Ctrl Pts',(22.3185272159931,4.06624525932138,128.034262368497));
#66875=CARTESIAN_POINT('Ctrl Pts',(22.310752881874,3.98769391879824,127.922312743422));
#66876=CARTESIAN_POINT('Ctrl Pts',(22.3029785477549,3.90449713633556,127.813694274617));
#66877=CARTESIAN_POINT('Ctrl Pts',(22.2952137948078,3.82140288647188,127.705209668368));
#66878=CARTESIAN_POINT('Ctrl Pts',(22.2874490418607,3.73367482134943,127.60004835736));
#66879=CARTESIAN_POINT('Ctrl Pts',(22.2796842889136,3.64161022184459,127.498629525257));
#66880=CARTESIAN_POINT('Ctrl Pts',(22.2719272480287,3.54963706219798,127.397311423769));
#66881=CARTESIAN_POINT('Ctrl Pts',(22.2641702071437,3.45333620058764,127.299728691631));
#66882=CARTESIAN_POINT('Ctrl Pts',(22.2564131662588,3.35304629314327,127.206268954123));
#66883=CARTESIAN_POINT('Ctrl Pts',(22.2486619750187,3.25283201509825,127.11287969533));
#66884=CARTESIAN_POINT('Ctrl Pts',(22.2409107837785,3.14863496366501,127.023607507991));
#66885=CARTESIAN_POINT('Ctrl Pts',(22.2331595925384,3.04083164287378,126.93880425629));
#66886=CARTESIAN_POINT('Ctrl Pts',(22.2254116957613,2.93307414136934,126.854037048234));
#66887=CARTESIAN_POINT('Ctrl Pts',(22.2176637989843,2.8217137256914,126.773735239237));
#66888=CARTESIAN_POINT('Ctrl Pts',(22.2099159022072,2.70716090173826,126.698211215194));
#66889=CARTESIAN_POINT('Ctrl Pts',(22.2021696261231,2.59263203976657,126.622702989149));
#66890=CARTESIAN_POINT('Ctrl Pts',(22.194423350039,2.47491242397898,126.551970775239));
#66891=CARTESIAN_POINT('Ctrl Pts',(22.1866770739549,2.35444220603363,126.486284082701));
#66892=CARTESIAN_POINT('Ctrl Pts',(22.1789307406896,2.23397109880465,126.420596905279));
#66893=CARTESIAN_POINT('Ctrl Pts',(22.1711844074243,2.1107496921579,126.359955510709));
#66894=CARTESIAN_POINT('Ctrl Pts',(22.1634380741589,1.98524308346435,126.304583627308));
#66895=CARTESIAN_POINT('Ctrl Pts',(22.155690006156,1.85970836843616,126.249199343757));
#66896=CARTESIAN_POINT('Ctrl Pts',(22.1479419381531,1.73188779065886,126.19908707736));
#66897=CARTESIAN_POINT('Ctrl Pts',(22.1401938701501,1.60226640499075,126.154422399704));
#66898=CARTESIAN_POINT('Ctrl Pts',(22.1324375674083,1.47250725617108,126.109710251896));
#66899=CARTESIAN_POINT('Ctrl Pts',(22.1246812646664,1.34094384642488,126.070457386073));
#66900=CARTESIAN_POINT('Ctrl Pts',(22.1169249619246,1.20807690838336,126.036789616948));
#66901=CARTESIAN_POINT('Ctrl Pts',(22.1091645194104,1.07513905525627,126.003103878321));
#66902=CARTESIAN_POINT('Ctrl Pts',(22.1014040768963,0.940896670015681,125.975009256204));
#66903=CARTESIAN_POINT('Ctrl Pts',(22.0936436343821,0.805859675247033,125.952580197317));
#66904=CARTESIAN_POINT('Ctrl Pts',(22.0858707341167,0.67060590710636,125.930115133314));
#66905=CARTESIAN_POINT('Ctrl Pts',(22.0780978338512,0.534555368674742,125.913333854869));
#66906=CARTESIAN_POINT('Ctrl Pts',(22.0703249335858,0.398222988539267,125.902258873018));
#66907=CARTESIAN_POINT('Ctrl Pts',(22.0628345978236,0.266846633818932,125.891586494653));
#66908=CARTESIAN_POINT('Ctrl Pts',(22.0553442620614,0.135208880709391,125.886212751802));
#66909=CARTESIAN_POINT('Ctrl Pts',(22.0478539262992,0.00376764555583718,
125.886112060676));
#66910=CARTESIAN_POINT('Ctrl Pts',(22.0400795921801,-0.13265722397581,125.886007551816));
#66911=CARTESIAN_POINT('Ctrl Pts',(22.032305258061,-0.269302532405295,125.891583512413));
#66912=CARTESIAN_POINT('Ctrl Pts',(22.0245309239419,-0.405656219561243,
125.902868386211));
#66913=CARTESIAN_POINT('Ctrl Pts',(22.0167661709948,-0.541841862984792,
125.914139352411));
#66914=CARTESIAN_POINT('Ctrl Pts',(22.0090014180477,-0.677736214335374,
125.931105200879));
#66915=CARTESIAN_POINT('Ctrl Pts',(22.0012366651005,-0.812825914949846,
125.953742399804));
#66916=CARTESIAN_POINT('Ctrl Pts',(21.9934796242156,-0.947781442568135,
125.976357115143));
#66917=CARTESIAN_POINT('Ctrl Pts',(21.9857225833306,-1.08193352678154,126.004631907087));
#66918=CARTESIAN_POINT('Ctrl Pts',(21.9779655424457,-1.21477299555531,126.038491375574));
#66919=CARTESIAN_POINT('Ctrl Pts',(21.9702143512055,-1.3475122890527,126.072325310372));
#66920=CARTESIAN_POINT('Ctrl Pts',(21.9624631599654,-1.47894056003473,126.111735442906));
#66921=CARTESIAN_POINT('Ctrl Pts',(21.9547119687253,-1.6085582655739,126.156595200857));
#66922=CARTESIAN_POINT('Ctrl Pts',(21.9469640719482,-1.73812088013073,126.201435892215));
#66923=CARTESIAN_POINT('Ctrl Pts',(21.9392161751711,-1.8658740911082,126.251721474573));
#66924=CARTESIAN_POINT('Ctrl Pts',(21.931468278394,-1.99133319094225,126.307275429897));
#66925=CARTESIAN_POINT('Ctrl Pts',(21.92372200231,-2.11676604743703,126.362817764531));
#66926=CARTESIAN_POINT('Ctrl Pts',(21.9159757262259,-2.23990539003404,126.423626121938));
#66927=CARTESIAN_POINT('Ctrl Pts',(21.9082294501418,-2.36028656025812,126.489475866386));
#66928=CARTESIAN_POINT('Ctrl Pts',(21.9004831168765,-2.48066861910864,126.555326096922));
#66929=CARTESIAN_POINT('Ctrl Pts',(21.8927367836111,-2.59829212195689,126.626217601132));
#66930=CARTESIAN_POINT('Ctrl Pts',(21.8849904503458,-2.71271744334429,126.701880010046));
#66931=CARTESIAN_POINT('Ctrl Pts',(21.8772423823428,-2.8271683894892,126.777559363032));
#66932=CARTESIAN_POINT('Ctrl Pts',(21.8694943143397,-2.93841940294213,126.858011531136));
#66933=CARTESIAN_POINT('Ctrl Pts',(21.8617462463367,-3.04606058635649,126.942923324699));
#66934=CARTESIAN_POINT('Ctrl Pts',(21.8539899435949,-3.15381617210139,127.027925363526));
#66935=CARTESIAN_POINT('Ctrl Pts',(21.8462336408531,-3.25795395639954,127.117396253433));
#66936=CARTESIAN_POINT('Ctrl Pts',(21.8384773381113,-3.3580974295519,127.210982719802));
#66937=CARTESIAN_POINT('Ctrl Pts',(21.8307168955971,-3.45829435229115,127.304619136086));
#66938=CARTESIAN_POINT('Ctrl Pts',(21.8229564530829,-3.55449244183456,127.402375227227));
#66939=CARTESIAN_POINT('Ctrl Pts',(21.8151960105688,-3.64635343843405,127.503862221184));
#66940=CARTESIAN_POINT('Ctrl Pts',(21.8074231103034,-3.73836189846031,127.605512131073));
#66941=CARTESIAN_POINT('Ctrl Pts',(21.7996502100379,-3.82601910252778,127.710904611302));
#66942=CARTESIAN_POINT('Ctrl Pts',(21.7918773097725,-3.9090277799853,127.819618605632));
#66943=CARTESIAN_POINT('Ctrl Pts',(21.7843869740105,-3.98901888293133,127.924380572434));
#66944=CARTESIAN_POINT('Ctrl Pts',(21.7768966382484,-4.0646933859691,128.032226503026));
#66945=CARTESIAN_POINT('Ctrl Pts',(21.7694063024863,-4.13582529849485,128.142757310754));
#66946=CARTESIAN_POINT('Ctrl Pts',(21.7614526540249,-4.21135705629471,128.260124971799));
#66947=CARTESIAN_POINT('Ctrl Pts',(21.7534990055635,-4.28199732470296,128.380878229055));
#66948=CARTESIAN_POINT('Ctrl Pts',(21.7455453571021,-4.34743626146344,128.50458214671));
#66949=CARTESIAN_POINT('Ctrl Pts',(21.7376017899302,-4.41279225404161,128.628129269026));
#66950=CARTESIAN_POINT('Ctrl Pts',(21.7296582227582,-4.47295986578013,128.754619287473));
#66951=CARTESIAN_POINT('Ctrl Pts',(21.7217146555863,-4.52767227611354,128.883588162898));
#66952=CARTESIAN_POINT('Ctrl Pts',(21.713782789,-4.58230409705596,129.012367071859));
#66953=CARTESIAN_POINT('Ctrl Pts',(21.7058509224138,-4.63149658517907,129.143617227038));
#66954=CARTESIAN_POINT('Ctrl Pts',(21.6979190558275,-4.6750289639352,129.276850470671));
#66955=CARTESIAN_POINT('Ctrl Pts',(21.6919169766414,-4.7079701110927,129.377668666465));
#66956=CARTESIAN_POINT('Ctrl Pts',(21.6859148974553,-4.73767117147266,129.479621811719));
#66957=CARTESIAN_POINT('Ctrl Pts',(21.6799128182693,-4.76405452823405,129.582490119308));
#66958=CARTESIAN_POINT('Origin',(213.235140564004,0.,130.804360617566));
#66959=CARTESIAN_POINT('',(19.584898128716,-4.76405452823411,129.582490119308));
#66960=CARTESIAN_POINT('',(19.9302639333258,-4.76405452823407,129.582490119308));
#66961=CARTESIAN_POINT('',(213.235140564004,-4.76405452823405,129.582490119308));
#66962=CARTESIAN_POINT('',(21.2648594360286,-4.91824895315572,130.807569555502));
#66963=CARTESIAN_POINT('Ctrl Pts',(21.2648594359913,-4.91824895315529,130.807569556159));
#66964=CARTESIAN_POINT('Ctrl Pts',(21.2539396410009,-4.91812367982727,130.99957242459));
#66965=CARTESIAN_POINT('Ctrl Pts',(21.2430198460104,-4.90675553107628,131.191209609033));
#66966=CARTESIAN_POINT('Ctrl Pts',(21.2321000510199,-4.88426909130594,131.381507484675));
#66967=CARTESIAN_POINT('Ctrl Pts',(21.2243257169006,-4.8682598991846,131.516989814583));
#66968=CARTESIAN_POINT('Ctrl Pts',(21.2165513827813,-4.84658396133967,131.652020127371));
#66969=CARTESIAN_POINT('Ctrl Pts',(21.2087770486621,-4.81927351189672,131.786086587494));
#66970=CARTESIAN_POINT('Ctrl Pts',(21.2010122957148,-4.7919967201419,131.919987822686));
#66971=CARTESIAN_POINT('Ctrl Pts',(21.1932475427675,-4.75909931063389,132.052927189284));
#66972=CARTESIAN_POINT('Ctrl Pts',(21.1854827898202,-4.72066528262224,132.184397701106));
#66973=CARTESIAN_POINT('Ctrl Pts',(21.1777257489351,-4.68226942782904,132.315737634562));
#66974=CARTESIAN_POINT('Ctrl Pts',(21.1699687080499,-4.63834800687803,132.445611243662));
#66975=CARTESIAN_POINT('Ctrl Pts',(21.1622116671647,-4.58903602974887,132.573521825644));
#66976=CARTESIAN_POINT('Ctrl Pts',(21.1544604759244,-4.53976123916531,132.70133594926));
#66977=CARTESIAN_POINT('Ctrl Pts',(21.1467092846841,-4.48510412372615,132.827189628953));
#66978=CARTESIAN_POINT('Ctrl Pts',(21.1389580934439,-4.42524937021364,132.950601767559));
#66979=CARTESIAN_POINT('Ctrl Pts',(21.1312101966667,-4.36542005656797,133.073961452715));
#66980=CARTESIAN_POINT('Ctrl Pts',(21.1234622998895,-4.30039766890311,133.194881309691));
#66981=CARTESIAN_POINT('Ctrl Pts',(21.1157144031123,-4.23041473794333,133.312900871876));
#66982=CARTESIAN_POINT('Ctrl Pts',(21.1079681270281,-4.16044644590405,133.430895746912));
#66983=CARTESIAN_POINT('Ctrl Pts',(21.1002218509438,-4.08551987377458,133.545991197801));
#66984=CARTESIAN_POINT('Ctrl Pts',(21.0924755748595,-4.00591296521278,133.65775234981));
#66985=CARTESIAN_POINT('Ctrl Pts',(21.0847292415941,-3.92630546901098,133.769514326814));
#66986=CARTESIAN_POINT('Ctrl Pts',(21.0769829083287,-3.84201779426044,133.877941637384));
#66987=CARTESIAN_POINT('Ctrl Pts',(21.0692365750632,-3.75337034113855,133.982629666083));
#66988=CARTESIAN_POINT('Ctrl Pts',(21.0614885070601,-3.66470303603405,134.087341138941));
#66989=CARTESIAN_POINT('Ctrl Pts',(21.053740439057,-3.57167426235135,134.188311365318));
#66990=CARTESIAN_POINT('Ctrl Pts',(21.0459923710539,-3.47464343009023,134.285170307312));
#66991=CARTESIAN_POINT('Ctrl Pts',(21.038236068312,-3.37750947230591,134.382132192143));
#66992=CARTESIAN_POINT('Ctrl Pts',(21.03047976557,-3.27636523638796,134.47497378735));
#66993=CARTESIAN_POINT('Ctrl Pts',(21.0227234628281,-3.17160599335499,134.563362943372));
#66994=CARTESIAN_POINT('Ctrl Pts',(21.0149630203138,-3.06679083715964,134.651799275348));
#66995=CARTESIAN_POINT('Ctrl Pts',(21.0072025777995,-2.95835713823287,134.735778193684));
#66996=CARTESIAN_POINT('Ctrl Pts',(20.9994421352852,-2.84673089890415,134.815009723599));
#66997=CARTESIAN_POINT('Ctrl Pts',(20.9916692350196,-2.73492546722636,134.894368443));
#66998=CARTESIAN_POINT('Ctrl Pts',(20.9838963347541,-2.61991758206336,134.968964332062));
#66999=CARTESIAN_POINT('Ctrl Pts',(20.9761234344885,-2.50216046280378,135.038551931251));
#67000=CARTESIAN_POINT('Ctrl Pts',(20.9686330987281,-2.38868411146803,135.105609845913));
#67001=CARTESIAN_POINT('Ctrl Pts',(20.9611427629677,-2.27265521020997,135.168017130908));
#67002=CARTESIAN_POINT('Ctrl Pts',(20.9536524272073,-2.15449674380741,135.22559651304));
#67003=CARTESIAN_POINT('Ctrl Pts',(20.9458780930882,-2.03185826321195,135.285359034958));
#67004=CARTESIAN_POINT('Ctrl Pts',(20.9381037589692,-1.90653706293946,135.340109636914));
#67005=CARTESIAN_POINT('Ctrl Pts',(20.9303294248502,-1.77898118806346,135.389598778776));
#67006=CARTESIAN_POINT('Ctrl Pts',(20.9225646719031,-1.65158251440343,135.439026929694));
#67007=CARTESIAN_POINT('Ctrl Pts',(20.914799918956,-1.52195500684621,135.483206382242));
#67008=CARTESIAN_POINT('Ctrl Pts',(20.907035166009,-1.39057061087192,135.521933768952));
#67009=CARTESIAN_POINT('Ctrl Pts',(20.899278125124,-1.25931670773173,135.560622691076));
#67010=CARTESIAN_POINT('Ctrl Pts',(20.891521084239,-1.12630976132239,135.593870213769));
#67011=CARTESIAN_POINT('Ctrl Pts',(20.883764043354,-0.992040637938393,135.621521444773));
#67012=CARTESIAN_POINT('Ctrl Pts',(20.8760128521139,-0.857872767944983,
135.649151823769));
#67013=CARTESIAN_POINT('Ctrl Pts',(20.8682616608739,-0.722444996891805,
135.671194232601));
#67014=CARTESIAN_POINT('Ctrl Pts',(20.8605104696337,-0.586261913164761,
135.687544008723));
#67015=CARTESIAN_POINT('Ctrl Pts',(20.8527625728567,-0.450136710881104,
135.703886835754));
#67016=CARTESIAN_POINT('Ctrl Pts',(20.8450146760796,-0.313257221788848,
135.71454179581));
#67017=CARTESIAN_POINT('Ctrl Pts',(20.8372667793025,-0.17613653802619,135.719455630124));
#67018=CARTESIAN_POINT('Ctrl Pts',(20.8295205032184,-0.0390445369545952,
135.72436843657));
#67019=CARTESIAN_POINT('Ctrl Pts',(20.8217742271344,0.0982881679672947,
135.723542491976));
#67020=CARTESIAN_POINT('Ctrl Pts',(20.8140279510503,0.235345468974294,135.716976577799));
#67021=CARTESIAN_POINT('Ctrl Pts',(20.8062816177849,0.372403781707155,135.710410615153));
#67022=CARTESIAN_POINT('Ctrl Pts',(20.7985352845196,0.509186295951143,135.698104617083));
#67023=CARTESIAN_POINT('Ctrl Pts',(20.7907889512542,0.645179413159238,135.680109440807));
#67024=CARTESIAN_POINT('Ctrl Pts',(20.7830408832513,0.781202985083022,135.662110234636));
#67025=CARTESIAN_POINT('Ctrl Pts',(20.7752928152483,0.916436420686703,135.638419366319));
#67026=CARTESIAN_POINT('Ctrl Pts',(20.7675447472453,1.05037412671886,135.609139203143));
#67027=CARTESIAN_POINT('Ctrl Pts',(20.7597884445035,1.18445418333906,135.579827920662));
#67028=CARTESIAN_POINT('Ctrl Pts',(20.7520321417616,1.31723537689449,135.544915560424));
#67029=CARTESIAN_POINT('Ctrl Pts',(20.7442758390197,1.44822460691093,135.504555140183));
#67030=CARTESIAN_POINT('Ctrl Pts',(20.7365153965055,1.57928374982344,135.46417317837));
#67031=CARTESIAN_POINT('Ctrl Pts',(20.7287549539914,1.70854865513402,135.418337493123));
#67032=CARTESIAN_POINT('Ctrl Pts',(20.7209945114772,1.83554509418338,135.367249753817));
#67033=CARTESIAN_POINT('Ctrl Pts',(20.7132216112118,1.96274539919092,135.316080003937));
#67034=CARTESIAN_POINT('Ctrl Pts',(20.7054487109463,2.08766960447644,135.259641513104));
#67035=CARTESIAN_POINT('Ctrl Pts',(20.6976758106809,2.20986622183303,135.198182910752));
#67036=CARTESIAN_POINT('Ctrl Pts',(20.6901854749186,2.32762068435814,135.138958483399));
#67037=CARTESIAN_POINT('Ctrl Pts',(20.6826951391563,2.44284215601372,135.07507274457));
#67038=CARTESIAN_POINT('Ctrl Pts',(20.6752048033941,2.55515285823264,135.006785742844));
#67039=CARTESIAN_POINT('Ctrl Pts',(20.667430469275,2.67172185485804,134.935909618694));
#67040=CARTESIAN_POINT('Ctrl Pts',(20.6596561351559,2.78552425678915,134.860067381339));
#67041=CARTESIAN_POINT('Ctrl Pts',(20.6518818010368,2.89610793953882,134.779501101252));
#67042=CARTESIAN_POINT('Ctrl Pts',(20.6441170480897,3.00655533778249,134.699034111905));
#67043=CARTESIAN_POINT('Ctrl Pts',(20.6363522951427,3.1137915966007,134.613854891801));
#67044=CARTESIAN_POINT('Ctrl Pts',(20.6285875421956,3.21739051912314,134.524250576954));
#67045=CARTESIAN_POINT('Ctrl Pts',(20.6208305013107,3.32088654573525,134.434735258376));
#67046=CARTESIAN_POINT('Ctrl Pts',(20.6130734604258,3.42075213160468,134.340803845541));
#67047=CARTESIAN_POINT('Ctrl Pts',(20.6053164195408,3.51659163626656,134.242785595116));
#67048=CARTESIAN_POINT('Ctrl Pts',(20.5975652283007,3.61235886761257,134.144841261016));
#67049=CARTESIAN_POINT('Ctrl Pts',(20.5898140370606,3.70410578869839,134.042816502105));
#67050=CARTESIAN_POINT('Ctrl Pts',(20.5820628458205,3.79147160161056,133.937079270219));
#67051=CARTESIAN_POINT('Ctrl Pts',(20.5743149490435,3.87880028172168,133.831386979478));
#67052=CARTESIAN_POINT('Ctrl Pts',(20.5665670522664,3.96175130870287,133.721985654848));
#67053=CARTESIAN_POINT('Ctrl Pts',(20.5588191554894,4.04000253561102,133.609278187613));
#67054=CARTESIAN_POINT('Ctrl Pts',(20.5510728794053,4.11823739404941,133.49659429635));
#67055=CARTESIAN_POINT('Ctrl Pts',(20.5433266033212,4.19177418501898,133.380605959007));
#67056=CARTESIAN_POINT('Ctrl Pts',(20.5355803272371,4.26033291447015,133.261746733011));
#67057=CARTESIAN_POINT('Ctrl Pts',(20.5278339939718,4.32889215000629,133.142886629623));
#67058=CARTESIAN_POINT('Ctrl Pts',(20.5200876607065,4.39247305535386,133.02115593396));
#67059=CARTESIAN_POINT('Ctrl Pts',(20.5123413274412,4.45084080557019,132.897014240594));
#67060=CARTESIAN_POINT('Ctrl Pts',(20.5045932594382,4.50922162683949,132.772844746556));
#67061=CARTESIAN_POINT('Ctrl Pts',(20.4968451914353,4.56238680356838,132.646263534166));
#67062=CARTESIAN_POINT('Ctrl Pts',(20.4890971234323,4.61014917475224,132.517751305364));
#67063=CARTESIAN_POINT('Ctrl Pts',(20.4813408206905,4.65796230835257,132.389102492235));
#67064=CARTESIAN_POINT('Ctrl Pts',(20.4735845179487,4.70036102939339,132.258518930049));
#67065=CARTESIAN_POINT('Ctrl Pts',(20.4658282152069,4.73720754319135,132.126498188029));
#67066=CARTESIAN_POINT('Ctrl Pts',(20.4580677726928,4.77407372308315,131.994406982565));
#67067=CARTESIAN_POINT('Ctrl Pts',(20.4503073301787,4.80538170174257,131.860877449281));
#67068=CARTESIAN_POINT('Ctrl Pts',(20.4425468876646,4.831044817151,131.7264175774));
#67069=CARTESIAN_POINT('Ctrl Pts',(20.4347739873992,4.85674912927056,131.591741858596));
#67070=CARTESIAN_POINT('Ctrl Pts',(20.4270010871338,4.87679041291184,131.45613320377));
#67071=CARTESIAN_POINT('Ctrl Pts',(20.4192281868684,4.89113380665535,131.32010585302));
#67072=CARTESIAN_POINT('Ctrl Pts',(20.411737851106,4.90495578190807,131.189023439095));
#67073=CARTESIAN_POINT('Ctrl Pts',(20.4042475153437,4.91348692036363,131.057552549415));
#67074=CARTESIAN_POINT('Ctrl Pts',(20.3967571795814,4.91674180971358,130.926151582397));
#67075=CARTESIAN_POINT('Ctrl Pts',(20.3889828454623,4.92012010918239,130.789768507781));
#67076=CARTESIAN_POINT('Ctrl Pts',(20.3812085113432,4.91782486495393,130.653028742144));
#67077=CARTESIAN_POINT('Ctrl Pts',(20.3734341772241,4.90981535344358,130.516443515626));
#67078=CARTESIAN_POINT('Ctrl Pts',(20.365669424277,4.90181571294033,130.380026618192));
#67079=CARTESIAN_POINT('Ctrl Pts',(20.3579046713298,4.888115839948,130.243764267474));
#67080=CARTESIAN_POINT('Ctrl Pts',(20.3501399183827,4.86872694030906,130.108170238999));
#67081=CARTESIAN_POINT('Ctrl Pts',(20.3423828774977,4.8493572979986,129.972710884426));
#67082=CARTESIAN_POINT('Ctrl Pts',(20.3346258366128,4.8243099286192,129.837918915653));
#67083=CARTESIAN_POINT('Ctrl Pts',(20.3268687957278,4.79364799179473,129.704305167481));
#67084=CARTESIAN_POINT('Ctrl Pts',(20.3191176044876,4.76300917737529,129.570792178475));
#67085=CARTESIAN_POINT('Ctrl Pts',(20.3113664132474,4.72676431010166,129.438456021073));
#67086=CARTESIAN_POINT('Ctrl Pts',(20.3036152220073,4.68502793818937,129.307799131731));
#67087=CARTESIAN_POINT('Ctrl Pts',(20.2958673252302,4.6433093053485,129.177197775053));
#67088=CARTESIAN_POINT('Ctrl Pts',(20.2881194284531,4.59610392880527,129.048274638519));
#67089=CARTESIAN_POINT('Ctrl Pts',(20.280371531676,4.54357664411465,128.921518526058));
#67090=CARTESIAN_POINT('Ctrl Pts',(20.2726252555918,4.49106034699962,128.794788928242));
#67091=CARTESIAN_POINT('Ctrl Pts',(20.2648789795077,4.43322450558711,128.670225813822));
#67092=CARTESIAN_POINT('Ctrl Pts',(20.2571327034235,4.37028254039623,128.548299098102));
#67093=CARTESIAN_POINT('Ctrl Pts',(20.2493863701582,4.30734011058206,128.426371482346));
#67094=CARTESIAN_POINT('Ctrl Pts',(20.2416400368929,4.23929166111792,128.307080651528));
#67095=CARTESIAN_POINT('Ctrl Pts',(20.2338937036275,4.16639693331599,128.190872592616));
#67096=CARTESIAN_POINT('Ctrl Pts',(20.2261456356245,4.09348588124518,128.074638509715));
#67097=CARTESIAN_POINT('Ctrl Pts',(20.2183975676215,4.01572659894786,127.961488903602));
#67098=CARTESIAN_POINT('Ctrl Pts',(20.2106494996185,3.93342234948612,127.851841069271));
#67099=CARTESIAN_POINT('Ctrl Pts',(20.2028931968766,3.85103062608863,127.742076699917));
#67100=CARTESIAN_POINT('Ctrl Pts',(20.1951368941347,3.76408452127027,127.635821850068));
#67101=CARTESIAN_POINT('Ctrl Pts',(20.1873805913928,3.67292817272093,127.533461398615));
#67102=CARTESIAN_POINT('Ctrl Pts',(20.1796201488786,3.58172317128358,127.431046314307));
#67103=CARTESIAN_POINT('Ctrl Pts',(20.1718597063645,3.48630372038269,127.332530050792));
#67104=CARTESIAN_POINT('Ctrl Pts',(20.1640992638503,3.38705036280178,127.238260099865));
#67105=CARTESIAN_POINT('Ctrl Pts',(20.1563263635848,3.28763767492011,127.143838818445));
#67106=CARTESIAN_POINT('Ctrl Pts',(20.1485534633193,3.18437907632109,127.05367772856));
#67107=CARTESIAN_POINT('Ctrl Pts',(20.1407805630539,3.07768836831409,126.968084119444));
#67108=CARTESIAN_POINT('Ctrl Pts',(20.133290227292,2.97487613628343,126.885602053619));
#67109=CARTESIAN_POINT('Ctrl Pts',(20.1257998915302,2.86887724207329,126.807361338));
#67110=CARTESIAN_POINT('Ctrl Pts',(20.1183095557683,2.76008523425795,126.733597475091));
#67111=CARTESIAN_POINT('Ctrl Pts',(20.1105352216493,2.64716834439697,126.657036832898));
#67112=CARTESIAN_POINT('Ctrl Pts',(20.1027608875302,2.53088467132556,126.585056703491));
#67113=CARTESIAN_POINT('Ctrl Pts',(20.0949865534111,2.41164231534645,126.517967681153));
#67114=CARTESIAN_POINT('Ctrl Pts',(20.087221800464,2.2925469149141,126.450961340039));
#67115=CARTESIAN_POINT('Ctrl Pts',(20.0794570475169,2.17050042411475,126.388834302232));
#67116=CARTESIAN_POINT('Ctrl Pts',(20.0716922945698,2.04594115388183,126.331854848162));
#67117=CARTESIAN_POINT('Ctrl Pts',(20.0639352536848,1.92150559767225,126.274931986889));
#67118=CARTESIAN_POINT('Ctrl Pts',(20.0561782127998,1.7945625818715,126.223146696527));
#67119=CARTESIAN_POINT('Ctrl Pts',(20.0484211719148,1.66557602558337,126.176721957785));
#67120=CARTESIAN_POINT('Ctrl Pts',(20.0406699806747,1.53668673906053,126.130332228299));
#67121=CARTESIAN_POINT('Ctrl Pts',(20.0329187894345,1.40575734579168,126.089295136077));
#67122=CARTESIAN_POINT('Ctrl Pts',(20.0251675981944,1.27327247590721,126.053785887642));
#67123=CARTESIAN_POINT('Ctrl Pts',(20.0174197014173,1.14084391562659,126.018291731583));
#67124=CARTESIAN_POINT('Ctrl Pts',(20.0096718046402,1.00686157049138,125.988320847376));
#67125=CARTESIAN_POINT('Ctrl Pts',(20.0019239078631,0.871825782732259,125.96399876466));
#67126=CARTESIAN_POINT('Ctrl Pts',(19.994177631779,0.736818241548902,125.9396817696));
#67127=CARTESIAN_POINT('Ctrl Pts',(19.986431355695,0.600758080574644,125.92101129501));
#67128=CARTESIAN_POINT('Ctrl Pts',(19.9786850796108,0.464156011866409,125.908061784861));
#67129=CARTESIAN_POINT('Ctrl Pts',(19.9709387463455,0.327552934792919,125.895112179122));
#67130=CARTESIAN_POINT('Ctrl Pts',(19.9631924130801,0.190408331223513,125.887883658991));
#67131=CARTESIAN_POINT('Ctrl Pts',(19.9554460798148,0.0532378191483778,
125.886398763595));
#67132=CARTESIAN_POINT('Ctrl Pts',(19.9476980118118,-0.0839634113118627,
125.884913535667));
#67133=CARTESIAN_POINT('Ctrl Pts',(19.9399499438089,-0.221190170955723,
125.889174496184));
#67134=CARTESIAN_POINT('Ctrl Pts',(19.9322018758059,-0.357927456593226,
125.89915205948));
#67135=CARTESIAN_POINT('Ctrl Pts',(19.9244455730641,-0.4948100682451,125.90914022705));
#67136=CARTESIAN_POINT('Ctrl Pts',(19.9166892703222,-0.631201776147267,
125.924857105712));
#67137=CARTESIAN_POINT('Ctrl Pts',(19.9089329675803,-0.766592755961558,
125.946221199125));
#67138=CARTESIAN_POINT('Ctrl Pts',(19.9011725250662,-0.902055998018503,
125.967596695198));
#67139=CARTESIAN_POINT('Ctrl Pts',(19.893412082552,-1.0365170646004,125.994625334837));
#67140=CARTESIAN_POINT('Ctrl Pts',(19.8856516400378,-1.16947790834913,126.027174784423));
#67141=CARTESIAN_POINT('Ctrl Pts',(19.8778787397724,-1.30265219264795,126.059776485275));
#67142=CARTESIAN_POINT('Ctrl Pts',(19.870105839507,-1.43432106583708,126.097916597322));
#67143=CARTESIAN_POINT('Ctrl Pts',(19.8623329392416,-1.5640023270663,126.141413075138));
#67144=CARTESIAN_POINT('Ctrl Pts',(19.8548426034795,-1.68896934780209,126.183328346425));
#67145=CARTESIAN_POINT('Ctrl Pts',(19.8473522677175,-1.81209046923445,126.230217200242));
#67146=CARTESIAN_POINT('Ctrl Pts',(19.8398619319555,-1.93295483382021,126.281875827883));
#67147=CARTESIAN_POINT('Ctrl Pts',(19.8320871447504,-2.05840911854133,126.335496232894));
#67148=CARTESIAN_POINT('Ctrl Pts',(19.8243123575451,-2.18182927946781,126.394425706269));
#67149=CARTESIAN_POINT('Ctrl Pts',(19.81653757034,-2.30273333283727,126.458488753332));
#67150=CARTESIAN_POINT('Ctrl Pts',(19.8087724675611,-2.42348678576311,126.522472002216));
#67151=CARTESIAN_POINT('Ctrl Pts',(19.8010073647823,-2.54173002514391,126.591575919711));
#67152=CARTESIAN_POINT('Ctrl Pts',(19.7932422620035,-2.65700036040956,126.665576720419));
#67153=CARTESIAN_POINT('Ctrl Pts',(19.7854849741014,-2.77215468646279,126.739503045985));
#67154=CARTESIAN_POINT('Ctrl Pts',(19.7777276861993,-2.88434173596447,126.818316236782));
#67155=CARTESIAN_POINT('Ctrl Pts',(19.7699703982972,-2.99312311050278,126.901746479853));
#67156=CARTESIAN_POINT('Ctrl Pts',(19.7622194065634,-3.10181619312028,126.985109007137));
#67157=CARTESIAN_POINT('Ctrl Pts',(19.7544684148297,-3.20710879562608,127.073080888195));
#67158=CARTESIAN_POINT('Ctrl Pts',(19.746717423096,-3.30859159272759,127.165349112359));
#67159=CARTESIAN_POINT('Ctrl Pts',(19.7389698774254,-3.41002927094018,127.257576314399));
#67160=CARTESIAN_POINT('Ctrl Pts',(19.7312223317549,-3.50766022489781,127.354095797025));
#67161=CARTESIAN_POINT('Ctrl Pts',(19.7234747860844,-3.60110844992599,127.454554504614));
#67162=CARTESIAN_POINT('Ctrl Pts',(19.7157290071483,-3.69453536521233,127.554990303805));
#67163=CARTESIAN_POINT('Ctrl Pts',(19.7079832282122,-3.78378118368068,127.659363254309));
#67164=CARTESIAN_POINT('Ctrl Pts',(19.7002374492761,-3.86850728762713,127.767283992244));
#67165=CARTESIAN_POINT('Ctrl Pts',(19.6924917592817,-3.95323241869766,127.875203490968));
#67166=CARTESIAN_POINT('Ctrl Pts',(19.6847460692873,-4.03343769799112,127.986670388027));
#67167=CARTESIAN_POINT('Ctrl Pts',(19.6770003792929,-4.10882553095543,128.101263168588));
#67168=CARTESIAN_POINT('Ctrl Pts',(19.6692493289486,-4.184265535536,128.215935252273));
#67169=CARTESIAN_POINT('Ctrl Pts',(19.6614982786043,-4.25488121633397,128.333737215375));
#67170=CARTESIAN_POINT('Ctrl Pts',(19.6537472282599,-4.32041880507549,128.454219257722));
#67171=CARTESIAN_POINT('Ctrl Pts',(19.6459936047494,-4.38597815075279,128.574741297269));
#67172=CARTESIAN_POINT('Ctrl Pts',(19.6382399812389,-4.44645586956471,128.697944839499));
#67173=CARTESIAN_POINT('Ctrl Pts',(19.6304863577284,-4.50164517484358,128.823357391343));
#67174=CARTESIAN_POINT('Ctrl Pts',(19.6227229073165,-4.55690442675623,128.948928890392));
#67175=CARTESIAN_POINT('Ctrl Pts',(19.6149594569045,-4.60686172565171,129.07671463039));
#67176=CARTESIAN_POINT('Ctrl Pts',(19.6071960064926,-4.65135902473962,129.20622348782));
#67177=CARTESIAN_POINT('Ctrl Pts',(19.5997633805671,-4.69396015713153,129.330213574732));
#67178=CARTESIAN_POINT('Ctrl Pts',(19.5923307546415,-4.73155697456111,129.455782650757));
#67179=CARTESIAN_POINT('Ctrl Pts',(19.584898128716,-4.76405452823411,129.582490119308));
#67180=CARTESIAN_POINT('Ctrl Pts',(21.3349957656066,-4.76405452823399,129.582490119308));
#67181=CARTESIAN_POINT('Ctrl Pts',(21.3273456225782,-4.79769978247013,129.713672454937));
#67182=CARTESIAN_POINT('Ctrl Pts',(21.3196954795498,-4.82590128757831,129.846162751177));
#67183=CARTESIAN_POINT('Ctrl Pts',(21.3120453365213,-4.84857992481995,129.979463184467));
#67184=CARTESIAN_POINT('Ctrl Pts',(21.3041810197725,-4.8718934741269,130.116495502196));
#67185=CARTESIAN_POINT('Ctrl Pts',(21.2963167030238,-4.88937031344629,130.254383527775));
#67186=CARTESIAN_POINT('Ctrl Pts',(21.288452386275,-4.90098172796321,130.392582564884));
#67187=CARTESIAN_POINT('Ctrl Pts',(21.2805880695262,-4.91259314248012,130.530781601993));
#67188=CARTESIAN_POINT('Ctrl Pts',(21.2727237527774,-4.918339173616,130.669291192643));
#67189=CARTESIAN_POINT('Ctrl Pts',(21.2648594360286,-4.91824895315572,130.807569555502));
#67190=CARTESIAN_POINT('',(21.610140563968,-4.91824963054304,130.806266965701));
#67191=CARTESIAN_POINT('Ctrl Pts',(21.6799128182693,-4.76405452823405,129.582490119308));
#67192=CARTESIAN_POINT('Ctrl Pts',(21.6719943898972,-4.79886158663048,129.718202311725));
#67193=CARTESIAN_POINT('Ctrl Pts',(21.6640759615251,-4.82789234323369,129.855507719247));
#67194=CARTESIAN_POINT('Ctrl Pts',(21.6561575331531,-4.85101175268147,129.993886658795));
#67195=CARTESIAN_POINT('Ctrl Pts',(21.6482449636327,-4.87411405605911,130.132163211651));
#67196=CARTESIAN_POINT('Ctrl Pts',(21.6403323941123,-4.8913136665669,130.271511353085));
#67197=CARTESIAN_POINT('Ctrl Pts',(21.6324198245919,-4.90252642019679,130.411400362868));
#67198=CARTESIAN_POINT('Ctrl Pts',(21.6249934043975,-4.91305026074918,130.542694573245));
#67199=CARTESIAN_POINT('Ctrl Pts',(21.6175669842031,-4.9183007179387,130.674464880059));
#67200=CARTESIAN_POINT('Ctrl Pts',(21.6101405640087,-4.91824963054332,130.806266964978));
#67201=CARTESIAN_POINT('Ctrl Pts',(21.610140563968,-4.91824963054304,130.8062669657));
#67202=CARTESIAN_POINT('Ctrl Pts',(21.6017353324186,-4.91819180974393,130.955440728217));
#67203=CARTESIAN_POINT('Ctrl Pts',(21.593330100869,-4.91134301940546,131.104404178229));
#67204=CARTESIAN_POINT('Ctrl Pts',(21.5849248693196,-4.89778544524941,131.252557889761));
#67205=CARTESIAN_POINT('Ctrl Pts',(21.5764834188236,-4.88416945020985,131.401350009804));
#67206=CARTESIAN_POINT('Ctrl Pts',(21.5680419683276,-4.86378681331425,131.549325129188));
#67207=CARTESIAN_POINT('Ctrl Pts',(21.5596005178316,-4.83677140407179,131.695890452879));
#67208=CARTESIAN_POINT('Ctrl Pts',(21.5511406982542,-4.80969720774602,131.842774711139));
#67209=CARTESIAN_POINT('Ctrl Pts',(21.5426808786767,-4.77596146114176,131.988242777102));
#67210=CARTESIAN_POINT('Ctrl Pts',(21.5342210590993,-4.73574807339157,132.131716352804));
#67211=CARTESIAN_POINT('Ctrl Pts',(21.5257330831344,-4.69540084546728,132.275667444313));
#67212=CARTESIAN_POINT('Ctrl Pts',(21.5172451071696,-4.64853291458363,132.417610498472));
#67213=CARTESIAN_POINT('Ctrl Pts',(21.5087571312047,-4.59537761380565,132.556983694281));
#67214=CARTESIAN_POINT('Ctrl Pts',(21.5028243136943,-4.5582237975681,132.654400998477));
#67215=CARTESIAN_POINT('Ctrl Pts',(21.4968914961838,-4.51799925047187,132.750563247881));
#67216=CARTESIAN_POINT('Ctrl Pts',(21.4909586786734,-4.47479683952839,132.845285973243));
#67217=CARTESIAN_POINT('Ctrl Pts',(21.4831843445544,-4.4181846182973,132.969410154433));
#67218=CARTESIAN_POINT('Ctrl Pts',(21.4754100104353,-4.35631428432474,133.091373646621));
#67219=CARTESIAN_POINT('Ctrl Pts',(21.4676356763162,-4.28937281389802,133.210698899249));
#67220=CARTESIAN_POINT('Ctrl Pts',(21.4598709233691,-4.22251384285087,133.329877094168));
#67221=CARTESIAN_POINT('Ctrl Pts',(21.452106170422,-4.15059635988457,133.446423181133));
#67222=CARTESIAN_POINT('Ctrl Pts',(21.4443414174749,-4.0738551536779,133.559880033094));
#67223=CARTESIAN_POINT('Ctrl Pts',(21.4365843765899,-3.9971901679192,133.673224198111));
#67224=CARTESIAN_POINT('Ctrl Pts',(21.428827335705,-3.91571121083265,133.783484912376));
#67225=CARTESIAN_POINT('Ctrl Pts',(21.42107029482,-3.82969850591166,133.890230416556));
#67226=CARTESIAN_POINT('Ctrl Pts',(21.4133191035799,-3.74375066384029,133.996895423121));
#67227=CARTESIAN_POINT('Ctrl Pts',(21.4055679123397,-3.65327612342795,134.100050192748));
#67228=CARTESIAN_POINT('Ctrl Pts',(21.3978167210996,-3.55859764770646,134.199292994542));
#67229=CARTESIAN_POINT('Ctrl Pts',(21.3900688243225,-3.46395941286292,134.298493615497));
#67230=CARTESIAN_POINT('Ctrl Pts',(21.3823209275455,-3.36512106579618,134.393785293293));
#67231=CARTESIAN_POINT('Ctrl Pts',(21.3745730307684,-3.26244462944918,134.484800550818));
#67232=CARTESIAN_POINT('Ctrl Pts',(21.3668267546843,-3.15978967079923,134.575796769914));
#67233=CARTESIAN_POINT('Ctrl Pts',(21.3590804786002,-3.05329851215573,134.662518088841));
#67234=CARTESIAN_POINT('Ctrl Pts',(21.3513342025161,-2.94336860658837,134.744635266401));
#67235=CARTESIAN_POINT('Ctrl Pts',(21.3435878692507,-2.83343788954342,134.826753050131));
#67236=CARTESIAN_POINT('Ctrl Pts',(21.3358415359854,-2.72006868814584,134.904266390699));
#67237=CARTESIAN_POINT('Ctrl Pts',(21.3280952027201,-2.60368964523393,134.976887824643));
#67238=CARTESIAN_POINT('Ctrl Pts',(21.3203471347171,-2.48728454004212,135.049525521655));
#67239=CARTESIAN_POINT('Ctrl Pts',(21.312599066714,-2.36786858371024,135.117268925174));
#67240=CARTESIAN_POINT('Ctrl Pts',(21.304850998711,-2.24589700823557,135.179875409096));
#67241=CARTESIAN_POINT('Ctrl Pts',(21.2970946959692,-2.12379579991917,135.242548431935));
#67242=CARTESIAN_POINT('Ctrl Pts',(21.2893383932273,-1.9991338950492,135.300073450262));
#67243=CARTESIAN_POINT('Ctrl Pts',(21.2815820904855,-1.87238910544307,135.352254866591));
#67244=CARTESIAN_POINT('Ctrl Pts',(21.2738216479713,-1.74557666832651,135.404464133714));
#67245=CARTESIAN_POINT('Ctrl Pts',(21.2660612054571,-1.61667949857841,135.45132398239));
#67246=CARTESIAN_POINT('Ctrl Pts',(21.258300762943,-1.48619179429567,135.49268835921));
#67247=CARTESIAN_POINT('Ctrl Pts',(21.2505278626775,-1.35549461956586,135.5341191378));
#67248=CARTESIAN_POINT('Ctrl Pts',(21.2427549624122,-1.22320218558329,135.57003671323));
#67249=CARTESIAN_POINT('Ctrl Pts',(21.2349820621467,-1.08982101566974,135.600345731837));
#67250=CARTESIAN_POINT('Ctrl Pts',(21.2274917263847,-0.961288587248536,
135.629552941273));
#67251=CARTESIAN_POINT('Ctrl Pts',(21.2200013906225,-0.831745508073716,
135.653552228622));
#67252=CARTESIAN_POINT('Ctrl Pts',(21.2125110548605,-0.701648691013128,
135.67230393861));
#67253=CARTESIAN_POINT('Ctrl Pts',(21.2047367207414,-0.56661921359256,135.691766625382));
#67254=CARTESIAN_POINT('Ctrl Pts',(21.1969623866224,-0.43056544665073,135.705637607803));
#67255=CARTESIAN_POINT('Ctrl Pts',(21.1891880525033,-0.293990232245845,
135.713816066579));
#67256=CARTESIAN_POINT('Ctrl Pts',(21.1814232995562,-0.157583334586822,
135.721984446135));
#67257=CARTESIAN_POINT('Ctrl Pts',(21.1736585466091,-0.0206566546412068,
135.724474237708));
#67258=CARTESIAN_POINT('Ctrl Pts',(21.165893793662,0.116278304641728,135.721235887325));
#67259=CARTESIAN_POINT('Ctrl Pts',(21.158136752777,0.253077258192844,135.718000753318));
#67260=CARTESIAN_POINT('Ctrl Pts',(21.150379711892,0.38988408639012,135.709048808445));
#67261=CARTESIAN_POINT('Ctrl Pts',(21.142622671007,0.52618407023321,135.694382436202));
#67262=CARTESIAN_POINT('Ctrl Pts',(21.1348714797669,0.662381269198224,135.679727123983));
#67263=CARTESIAN_POINT('Ctrl Pts',(21.1271202885268,0.798071997436957,135.659366003441));
#67264=CARTESIAN_POINT('Ctrl Pts',(21.1193690972867,0.932743806065768,135.633353478893));
#67265=CARTESIAN_POINT('Ctrl Pts',(21.1116212005096,1.06735837558342,135.607352010361));
#67266=CARTESIAN_POINT('Ctrl Pts',(21.1038733037326,1.20095450376418,135.575703989204));
#67267=CARTESIAN_POINT('Ctrl Pts',(21.0961254069555,1.33302733946318,135.538515365221));
#67268=CARTESIAN_POINT('Ctrl Pts',(21.0883791308714,1.46507254837211,135.501334520297));
#67269=CARTESIAN_POINT('Ctrl Pts',(21.0806328547873,1.59559472249907,135.45861548371));
#67270=CARTESIAN_POINT('Ctrl Pts',(21.0728865787032,1.72410202880573,135.410514681074));
#67271=CARTESIAN_POINT('Ctrl Pts',(21.0651402454379,1.85261028372413,135.362413523368));
#67272=CARTESIAN_POINT('Ctrl Pts',(21.0573939121725,1.97910327498779,135.308930657396));
#67273=CARTESIAN_POINT('Ctrl Pts',(21.0496475789072,2.10310745952155,135.250271331492));
#67274=CARTESIAN_POINT('Ctrl Pts',(21.0418995109042,2.22713941393265,135.19159886924));
#67275=CARTESIAN_POINT('Ctrl Pts',(21.0341514429013,2.34868109919985,135.127747807469));
#67276=CARTESIAN_POINT('Ctrl Pts',(21.0264033748983,2.46728232309684,135.058970000416));
#67277=CARTESIAN_POINT('Ctrl Pts',(21.0186470721565,2.58600959778595,134.990119095491));
#67278=CARTESIAN_POINT('Ctrl Pts',(21.0108907694145,2.70178982951656,134.916331181848));
#67279=CARTESIAN_POINT('Ctrl Pts',(21.0031344666727,2.81420018762465,134.837902530882));
#67280=CARTESIAN_POINT('Ctrl Pts',(20.9953740241585,2.92667054252564,134.759432020182));
#67281=CARTESIAN_POINT('Ctrl Pts',(20.9876135816444,3.03576712909411,134.67631607354));
#67282=CARTESIAN_POINT('Ctrl Pts',(20.9798531391302,3.14109994231722,134.588891528376));
#67283=CARTESIAN_POINT('Ctrl Pts',(20.9720802388648,3.24660184512298,134.50132664157));
#67284=CARTESIAN_POINT('Ctrl Pts',(20.9643073385994,3.34832761056063,134.409439597));
#67285=CARTESIAN_POINT('Ctrl Pts',(20.956534438334,3.44592322666501,134.313605006096));
#67286=CARTESIAN_POINT('Ctrl Pts',(20.9490441025719,3.53997099629627,134.221254243964));
#67287=CARTESIAN_POINT('Ctrl Pts',(20.9415537668098,3.63018347499754,134.125238183631));
#67288=CARTESIAN_POINT('Ctrl Pts',(20.9340634310477,3.71628032709946,134.025919804189));
#67289=CARTESIAN_POINT('Ctrl Pts',(20.9262890969286,3.80564156751676,133.922835738204));
#67290=CARTESIAN_POINT('Ctrl Pts',(20.9185147628095,3.89085200220441,133.815867455649));
#67291=CARTESIAN_POINT('Ctrl Pts',(20.9107404286904,3.97155501061956,133.705383516497));
#67292=CARTESIAN_POINT('Ctrl Pts',(20.9029756757433,4.05215855978947,133.595035738926));
#67293=CARTESIAN_POINT('Ctrl Pts',(20.8952109227963,4.12826550708481,133.481181238284));
#67294=CARTESIAN_POINT('Ctrl Pts',(20.8874461698492,4.19955768150787,133.364223571356));
#67295=CARTESIAN_POINT('Ctrl Pts',(20.8796891289642,4.27077904753815,133.247382068433));
#67296=CARTESIAN_POINT('Ctrl Pts',(20.8719320880791,4.33719495511777,133.127443864432));
#67297=CARTESIAN_POINT('Ctrl Pts',(20.8641750471941,4.39852919135532,133.004843295365));
#67298=CARTESIAN_POINT('Ctrl Pts',(20.856423855954,4.45981717496822,132.882335180341));
#67299=CARTESIAN_POINT('Ctrl Pts',(20.8486726647139,4.51603094064258,132.757169044712));
#67300=CARTESIAN_POINT('Ctrl Pts',(20.8409214734738,4.56693926913249,132.629805433099));
#67301=CARTESIAN_POINT('Ctrl Pts',(20.8331735766967,4.61782596022483,132.502495954418));
#67302=CARTESIAN_POINT('Ctrl Pts',(20.8254256799196,4.66341155425515,132.372991219659));
#67303=CARTESIAN_POINT('Ctrl Pts',(20.8176777831425,4.70351230541546,132.241773242843));
#67304=CARTESIAN_POINT('Ctrl Pts',(20.8099315070584,4.74360466836304,132.110582713999));
#67305=CARTESIAN_POINT('Ctrl Pts',(20.8021852309742,4.77821435631338,131.97768002958));
#67306=CARTESIAN_POINT('Ctrl Pts',(20.7944389548901,4.80720712679434,131.843563534516));
#67307=CARTESIAN_POINT('Ctrl Pts',(20.7866926216248,4.83620011129336,131.709446049435));
#67308=CARTESIAN_POINT('Ctrl Pts',(20.7789462883595,4.85957601297787,131.574115117967));
#67309=CARTESIAN_POINT('Ctrl Pts',(20.7711999550941,4.87725155148807,131.438080087053));
#67310=CARTESIAN_POINT('Ctrl Pts',(20.7634518870911,4.89493104831257,131.302014592038));
#67311=CARTESIAN_POINT('Ctrl Pts',(20.7557038190881,4.90690759139603,131.165245071447));
#67312=CARTESIAN_POINT('Ctrl Pts',(20.7479557510852,4.91314973294599,131.028286418118));
#67313=CARTESIAN_POINT('Ctrl Pts',(20.7401994483433,4.91939850871827,130.891182203502));
#67314=CARTESIAN_POINT('Ctrl Pts',(20.7324431456015,4.91990069052779,130.753888845786));
#67315=CARTESIAN_POINT('Ctrl Pts',(20.7246868428596,4.91467698958774,130.61692222631));
#67316=CARTESIAN_POINT('Ctrl Pts',(20.7169264003455,4.90945050060121,130.479882503624));
#67317=CARTESIAN_POINT('Ctrl Pts',(20.7091659578313,4.89849207059793,130.343170256188));
#67318=CARTESIAN_POINT('Ctrl Pts',(20.7014055153171,4.88187428320314,130.207295675118));
#67319=CARTESIAN_POINT('Ctrl Pts',(20.6936326150516,4.86522981946075,130.071202976109));
#67320=CARTESIAN_POINT('Ctrl Pts',(20.6858597147862,4.84290790749611,129.935951016566));
#67321=CARTESIAN_POINT('Ctrl Pts',(20.6780868145208,4.8150323664022,129.802040123413));
#67322=CARTESIAN_POINT('Ctrl Pts',(20.6705964787587,4.78817017144131,129.672997228527));
#67323=CARTESIAN_POINT('Ctrl Pts',(20.6631061429967,4.75615118886716,129.545199889313));
#67324=CARTESIAN_POINT('Ctrl Pts',(20.6556158072347,4.7191292749939,129.419080159177));
#67325=CARTESIAN_POINT('Ctrl Pts',(20.6478414731156,4.68070366400356,129.288178561139));
#67326=CARTESIAN_POINT('Ctrl Pts',(20.6400671389966,4.63676653972007,129.158669639584));
#67327=CARTESIAN_POINT('Ctrl Pts',(20.6322928048775,4.58743521997294,129.031052645145));
#67328=CARTESIAN_POINT('Ctrl Pts',(20.6245280519304,4.53816469666853,128.903592927246));
#67329=CARTESIAN_POINT('Ctrl Pts',(20.6167632989832,4.48351334477991,128.778020858378));
#67330=CARTESIAN_POINT('Ctrl Pts',(20.6089985460361,4.4236487088643,128.654822257112));
#67331=CARTESIAN_POINT('Ctrl Pts',(20.6012415051511,4.36384353134911,128.531746018434));
#67332=CARTESIAN_POINT('Ctrl Pts',(20.5934844642662,4.29883554384291,128.411038905476));
#67333=CARTESIAN_POINT('Ctrl Pts',(20.5857274233812,4.22884086571668,128.293168073187));
#67334=CARTESIAN_POINT('Ctrl Pts',(20.5779762321411,4.15889897112161,128.17538612821));
#67335=CARTESIAN_POINT('Ctrl Pts',(20.5702250409009,4.08397806977192,128.060436541431));
#67336=CARTESIAN_POINT('Ctrl Pts',(20.5624738496608,4.00434065125074,127.948762779767));
#67337=CARTESIAN_POINT('Ctrl Pts',(20.5547259528837,3.92473708075683,127.837136482432));
#67338=CARTESIAN_POINT('Ctrl Pts',(20.5469780561066,3.84042120670279,127.728783558656));
#67339=CARTESIAN_POINT('Ctrl Pts',(20.5392301593295,3.75169924203856,127.624119139347));
#67340=CARTESIAN_POINT('Ctrl Pts',(20.5314838832454,3.66299583609671,127.519476613577));
#67341=CARTESIAN_POINT('Ctrl Pts',(20.5237376071613,3.56988842542124,127.41852135565));
#67342=CARTESIAN_POINT('Ctrl Pts',(20.5159913310772,3.47272372038001,127.321635675167));
#67343=CARTESIAN_POINT('Ctrl Pts',(20.5082449978119,3.37555829809113,127.224749279496));
#67344=CARTESIAN_POINT('Ctrl Pts',(20.5004986645465,3.27433579852477,127.131932797268));
#67345=CARTESIAN_POINT('Ctrl Pts',(20.4927523312812,3.16943973461865,127.043531609073));
#67346=CARTESIAN_POINT('Ctrl Pts',(20.4850042632782,3.06452017996618,126.955110624045));
#67347=CARTESIAN_POINT('Ctrl Pts',(20.4772561952752,2.95592572285877,126.871107152495));
#67348=CARTESIAN_POINT('Ctrl Pts',(20.4695081272723,2.84407255892277,126.791825964497));
#67349=CARTESIAN_POINT('Ctrl Pts',(20.4617518245304,2.73210051611321,126.712460515509));
#67350=CARTESIAN_POINT('Ctrl Pts',(20.4539955217886,2.6168631674517,126.637827602308));
#67351=CARTESIAN_POINT('Ctrl Pts',(20.4462392190467,2.49880573343549,126.568188646429));
#67352=CARTESIAN_POINT('Ctrl Pts',(20.4384787765326,2.38068528861194,126.498512522142));
#67353=CARTESIAN_POINT('Ctrl Pts',(20.4307183340184,2.25974210386092,126.433835850541));
#67354=CARTESIAN_POINT('Ctrl Pts',(20.4229578915042,2.13644465064005,126.374373335727));
#67355=CARTESIAN_POINT('Ctrl Pts',(20.4151849912388,2.01294926940144,126.314815366406));
#67356=CARTESIAN_POINT('Ctrl Pts',(20.4074120909734,1.88709242664392,126.260488435286));
#67357=CARTESIAN_POINT('Ctrl Pts',(20.399639190708,1.75936198882108,126.21155880878));
#67358=CARTESIAN_POINT('Ctrl Pts',(20.392148854946,1.636274874147,126.164407897443));
#67359=CARTESIAN_POINT('Ctrl Pts',(20.3846585191839,1.51144831106987,126.122268790839));
#67360=CARTESIAN_POINT('Ctrl Pts',(20.3771681834219,1.3853289614509,126.085245580712));
#67361=CARTESIAN_POINT('Ctrl Pts',(20.3693938493029,1.25442775835778,126.046818624319));
#67362=CARTESIAN_POINT('Ctrl Pts',(20.3616195151838,1.12171914587204,126.013781435811));
#67363=CARTESIAN_POINT('Ctrl Pts',(20.3538451810647,0.987686570841499,125.986305169537));
#67364=CARTESIAN_POINT('Ctrl Pts',(20.3460804281176,0.853819178980851,125.958862765306));
#67365=CARTESIAN_POINT('Ctrl Pts',(20.3383156751706,0.718631450427147,125.936967724965));
#67366=CARTESIAN_POINT('Ctrl Pts',(20.3305509222235,0.58262268002947,125.920741685338));
#67367=CARTESIAN_POINT('Ctrl Pts',(20.3227938813385,0.446748995459941,125.904531761643));
#67368=CARTESIAN_POINT('Ctrl Pts',(20.3150368404535,0.310056277569384,125.893979679664));
#67369=CARTESIAN_POINT('Ctrl Pts',(20.3072797995685,0.173054374847257,125.889156120717));
#67370=CARTESIAN_POINT('Ctrl Pts',(20.2995286083284,0.0361557863255061,
125.884336199253));
#67371=CARTESIAN_POINT('Ctrl Pts',(20.2917774170882,-0.10105113379744,125.885236215975));
#67372=CARTESIAN_POINT('Ctrl Pts',(20.2840262258481,-0.23805140221298,125.891875035663));
#67373=CARTESIAN_POINT('Ctrl Pts',(20.276278329071,-0.374993441859656,125.898511033676));
#67374=CARTESIAN_POINT('Ctrl Pts',(20.2685304322939,-0.511728614801637,
125.910880964499));
#67375=CARTESIAN_POINT('Ctrl Pts',(20.2607825355168,-0.647742144072723,
125.9289515909));
#67376=CARTESIAN_POINT('Ctrl Pts',(20.2530362594327,-0.783727222245598,
125.947018437316));
#67377=CARTESIAN_POINT('Ctrl Pts',(20.2452899833486,-0.918990569685856,
125.970783555977));
#67378=CARTESIAN_POINT('Ctrl Pts',(20.2375437072645,-1.05302313307597,126.00016189731));
#67379=CARTESIAN_POINT('Ctrl Pts',(20.2297973739992,-1.18705668586403,126.029540455508));
#67380=CARTESIAN_POINT('Ctrl Pts',(20.2220510407339,-1.31985905457379,126.06453223535));
#67381=CARTESIAN_POINT('Ctrl Pts',(20.2143047074685,-1.45093236262411,126.105001263187));
#67382=CARTESIAN_POINT('Ctrl Pts',(20.2065566394656,-1.58203502363297,126.145479353782));
#67383=CARTESIAN_POINT('Ctrl Pts',(20.1988085714625,-1.71140747998354,126.191437017829));
#67384=CARTESIAN_POINT('Ctrl Pts',(20.1910605034595,-1.838568356079,126.242688833831));
#67385=CARTESIAN_POINT('Ctrl Pts',(20.1833042007177,-1.96586438026681,126.293995120873));
#67386=CARTESIAN_POINT('Ctrl Pts',(20.1755478979759,-2.09094376563688,126.350606653398));
#67387=CARTESIAN_POINT('Ctrl Pts',(20.167791595234,-2.21334591829464,126.412290159517));
#67388=CARTESIAN_POINT('Ctrl Pts',(20.1600311527199,-2.33581340066673,126.474006587981));
#67389=CARTESIAN_POINT('Ctrl Pts',(20.1522707102057,-2.45560046178221,126.540800193785));
#67390=CARTESIAN_POINT('Ctrl Pts',(20.1445102676915,-2.57227324473449,126.612392891435));
#67391=CARTESIAN_POINT('Ctrl Pts',(20.1367373674261,-2.68913332119584,126.684100516039));
#67392=CARTESIAN_POINT('Ctrl Pts',(20.1289644671607,-2.80286880470068,126.760622409023));
#67393=CARTESIAN_POINT('Ctrl Pts',(20.1211915668953,-2.91307610687209,126.841637985578));
#67394=CARTESIAN_POINT('Ctrl Pts',(20.1137012311332,-3.01927709601458,126.91970844186));
#67395=CARTESIAN_POINT('Ctrl Pts',(20.1062108953711,-3.12220172624427,127.001951348225));
#67396=CARTESIAN_POINT('Ctrl Pts',(20.098720559609,-3.22152099058269,127.088047179529));
#67397=CARTESIAN_POINT('Ctrl Pts',(20.0910614977135,-3.32307750515688,127.176082392082));
#67398=CARTESIAN_POINT('Ctrl Pts',(20.083402435818,-3.42120616241053,127.268442879405));
#67399=CARTESIAN_POINT('Ctrl Pts',(20.0757433739224,-3.51550779383497,127.364827507682));
#67400=CARTESIAN_POINT('Ctrl Pts',(20.0680931230708,-3.60970093993493,127.46110125434));
#67401=CARTESIAN_POINT('Ctrl Pts',(20.0604428722193,-3.70007553284389,127.561389654635));
#67402=CARTESIAN_POINT('Ctrl Pts',(20.0527926213676,-3.78626484654163,127.665350968912));
#67403=CARTESIAN_POINT('Ctrl Pts',(20.0451493990129,-3.87237497573554,127.769216771057));
#67404=CARTESIAN_POINT('Ctrl Pts',(20.0375061766581,-3.9543072152907,127.876748469623));
#67405=CARTESIAN_POINT('Ctrl Pts',(20.0298629543033,-4.03173156280554,127.987567464355));
#67406=CARTESIAN_POINT('Ctrl Pts',(20.0222249846418,-4.1091027015647,128.098310300345));
#67407=CARTESIAN_POINT('Ctrl Pts',(20.0145870149802,-4.18197187982267,128.212335609902));
#67408=CARTESIAN_POINT('Ctrl Pts',(20.0069490453187,-4.25004965468716,128.329232137023));
#67409=CARTESIAN_POINT('Ctrl Pts',(19.9993140021762,-4.31810134527726,128.446083874768));
#67410=CARTESIAN_POINT('Ctrl Pts',(19.9916789590337,-4.38136507934984,128.565804295163));
#67411=CARTESIAN_POINT('Ctrl Pts',(19.9840439158911,-4.43959526219746,128.687954000119));
#67412=CARTESIAN_POINT('Ctrl Pts',(19.97641053745,-4.49781274886634,128.810077072246));
#67413=CARTESIAN_POINT('Ctrl Pts',(19.9687771590089,-4.55099869748895,128.934628009698));
#67414=CARTESIAN_POINT('Ctrl Pts',(19.9611437805678,-4.59895422551359,129.061144310239));
#67415=CARTESIAN_POINT('Ctrl Pts',(19.9535088799648,-4.64691931628697,129.187685839229));
#67416=CARTESIAN_POINT('Ctrl Pts',(19.9458739793618,-4.68965176189308,129.316193136262));
#67417=CARTESIAN_POINT('Ctrl Pts',(19.9382390787587,-4.72700154321437,129.446185565171));
#67418=CARTESIAN_POINT('Ctrl Pts',(19.9355806969477,-4.74000629395983,129.491447386712));
#67419=CARTESIAN_POINT('Ctrl Pts',(19.9329223151368,-4.7523589215535,129.536889126366));
#67420=CARTESIAN_POINT('Ctrl Pts',(19.9302639333258,-4.76405452823407,129.582490119308));
#67421=CARTESIAN_POINT('Origin',(213.235140564004,0.,130.804360617566));
#67422=CARTESIAN_POINT('',(17.8345741463799,-4.76405452823412,129.582490119309));
#67423=CARTESIAN_POINT('',(18.1802003750168,-4.76405452823408,129.582490119308));
#67424=CARTESIAN_POINT('',(213.235140564004,-4.76405452823405,129.582490119308));
#67425=CARTESIAN_POINT('',(19.5148594359387,-4.91824832460085,130.800301053439));
#67426=CARTESIAN_POINT('Ctrl Pts',(19.5148594359387,-4.91824832460085,130.800301053439));
#67427=CARTESIAN_POINT('Ctrl Pts',(19.5072120057733,-4.9183594917055,130.934982366288));
#67428=CARTESIAN_POINT('Ctrl Pts',(19.499564575608,-4.91293433359908,131.069863219504));
#67429=CARTESIAN_POINT('Ctrl Pts',(19.4919171454426,-4.90195035046161,131.204442889242));
#67430=CARTESIAN_POINT('Ctrl Pts',(19.4842769476887,-4.8909767552171,131.338895282819));
#67431=CARTESIAN_POINT('Ctrl Pts',(19.4766367499348,-4.87445482369759,131.47304665972));
#67432=CARTESIAN_POINT('Ctrl Pts',(19.468996552181,-4.85241410186351,131.606395807901));
#67433=CARTESIAN_POINT('Ctrl Pts',(19.4612453076872,-4.83005302833382,131.741683124263));
#67434=CARTESIAN_POINT('Ctrl Pts',(19.4534940631934,-4.80201146538665,131.876144287265));
#67435=CARTESIAN_POINT('Ctrl Pts',(19.4457428186996,-4.76837496711769,132.009260296156));
#67436=CARTESIAN_POINT('Ctrl Pts',(19.4381103908622,-4.73525407331205,132.14033580702));
#67437=CARTESIAN_POINT('Ctrl Pts',(19.4304779630248,-4.69670866418405,132.270106707331));
#67438=CARTESIAN_POINT('Ctrl Pts',(19.4228455351874,-4.65287189227426,132.398087763781));
#67439=CARTESIAN_POINT('Ctrl Pts',(19.4152140006218,-4.6090402508622,132.526053841791));
#67440=CARTESIAN_POINT('Ctrl Pts',(19.4075824660562,-4.55991860874222,132.652230110592));
#67441=CARTESIAN_POINT('Ctrl Pts',(19.3999509314906,-4.50568965152999,132.776147580348));
#67442=CARTESIAN_POINT('Ctrl Pts',(19.3923185231087,-4.4514544850618,132.900079238745));
#67443=CARTESIAN_POINT('Ctrl Pts',(19.3846861147267,-4.3921110029713,133.02175121418));
#67444=CARTESIAN_POINT('Ctrl Pts',(19.3770537063447,-4.32788935284373,133.140716072552));
#67445=CARTESIAN_POINT('Ctrl Pts',(19.3692131211768,-4.2619160332504,133.262925741817));
#67446=CARTESIAN_POINT('Ctrl Pts',(19.3613725360089,-4.19079482862168,133.382278098069));
#67447=CARTESIAN_POINT('Ctrl Pts',(19.353531950841,-4.1148241224104,133.49831783774));
#67448=CARTESIAN_POINT('Ctrl Pts',(19.3458884728877,-4.04076327037145,133.611440413783));
#67449=CARTESIAN_POINT('Ctrl Pts',(19.3382449949344,-3.96209412539492,133.72141464901));
#67450=CARTESIAN_POINT('Ctrl Pts',(19.3306015169811,-3.87913481056252,133.827851345844));
#67451=CARTESIAN_POINT('Ctrl Pts',(19.3226623782059,-3.79296650901433,133.938405168608));
#67452=CARTESIAN_POINT('Ctrl Pts',(19.3147232394306,-3.70216979308598,134.045141910077));
#67453=CARTESIAN_POINT('Ctrl Pts',(19.3067841006554,-3.60714332747181,134.147667375489));
#67454=CARTESIAN_POINT('Ctrl Pts',(19.2988449618802,-3.51211686185776,134.250192840902));
#67455=CARTESIAN_POINT('Ctrl Pts',(19.2909058231049,-3.41286104041815,134.348506746843));
#67456=CARTESIAN_POINT('Ctrl Pts',(19.2829666843296,-3.30981193811156,134.442262210083));
#67457=CARTESIAN_POINT('Ctrl Pts',(19.2751923502106,-3.208901981165,134.53407145002));
#67458=CARTESIAN_POINT('Ctrl Pts',(19.2674180160915,-3.10400931831421,134.621824290045));
#67459=CARTESIAN_POINT('Ctrl Pts',(19.2596436819724,-2.9954938454868,134.705155367889));
#67460=CARTESIAN_POINT('Ctrl Pts',(19.2518789290254,-2.8871121082812,134.788383747628));
#67461=CARTESIAN_POINT('Ctrl Pts',(19.2441141760783,-2.77511675180746,134.867200972087));
#67462=CARTESIAN_POINT('Ctrl Pts',(19.2363494231312,-2.65990358141037,134.941279277644));
#67463=CARTESIAN_POINT('Ctrl Pts',(19.2285923822462,-2.5448048423585,135.015284007583));
#67464=CARTESIAN_POINT('Ctrl Pts',(19.2208353413611,-2.42649497625105,135.084558975212));
#67465=CARTESIAN_POINT('Ctrl Pts',(19.2130783004762,-2.30540156567152,135.148817624316));
#67466=CARTESIAN_POINT('Ctrl Pts',(19.205327109236,-2.18439947257454,135.213027815473));
#67467=CARTESIAN_POINT('Ctrl Pts',(19.1975759179959,-2.06061835707731,135.272229035106));
#67468=CARTESIAN_POINT('Ctrl Pts',(19.1898247267557,-1.93451308255149,135.326179078754));
#67469=CARTESIAN_POINT('Ctrl Pts',(19.1820768299787,-1.80846140613166,135.380106192194));
#67470=CARTESIAN_POINT('Ctrl Pts',(19.1743289332016,-1.68008789410022,135.42878641525));
#67471=CARTESIAN_POINT('Ctrl Pts',(19.1665810364245,-1.54987001227751,135.47202448802));
#67472=CARTESIAN_POINT('Ctrl Pts',(19.1588347603404,-1.41967936922851,135.515253516318));
#67473=CARTESIAN_POINT('Ctrl Pts',(19.1510884842563,-1.2876454945807,135.553042535506));
#67474=CARTESIAN_POINT('Ctrl Pts',(19.1433422081722,-1.15426336830343,135.585245382868));
#67475=CARTESIAN_POINT('Ctrl Pts',(19.1355958749068,-1.0208802574296,135.617448467943));
#67476=CARTESIAN_POINT('Ctrl Pts',(19.1278495416415,-0.886149255112507,
135.644065207152));
#67477=CARTESIAN_POINT('Ctrl Pts',(19.1201032083762,-0.750577563114254,
135.665000121196));
#67478=CARTESIAN_POINT('Ctrl Pts',(19.1123551403732,-0.614975510775381,
135.685939723469));
#67479=CARTESIAN_POINT('Ctrl Pts',(19.1046070723703,-0.478532780438202,
135.701194908983));
#67480=CARTESIAN_POINT('Ctrl Pts',(19.0968590043673,-0.34176336200302,135.710721882994));
#67481=CARTESIAN_POINT('Ctrl Pts',(19.0891027016254,-0.204848583402535,
135.720258982386));
#67482=CARTESIAN_POINT('Ctrl Pts',(19.0813463988835,-0.0676068137607187,
135.724055681606));
#67483=CARTESIAN_POINT('Ctrl Pts',(19.0735900961417,0.069445717132957,135.722120306171));
#67484=CARTESIAN_POINT('Ctrl Pts',(19.0658296536275,0.206571397089129,135.720183897769));
#67485=CARTESIAN_POINT('Ctrl Pts',(19.0580692111134,0.34350724687965,135.712509340504));
#67486=CARTESIAN_POINT('Ctrl Pts',(19.0503087685992,0.479741480504115,135.69915695392));
#67487=CARTESIAN_POINT('Ctrl Pts',(19.0425358683338,0.616194409414515,135.685783132899));
#67488=CARTESIAN_POINT('Ctrl Pts',(19.0347629680683,0.75194308407296,135.666713323192));
#67489=CARTESIAN_POINT('Ctrl Pts',(19.0269900678029,0.886484350322532,135.642059301768));
#67490=CARTESIAN_POINT('Ctrl Pts',(19.0194997320409,1.01613470265511,135.618301516123));
#67491=CARTESIAN_POINT('Ctrl Pts',(19.0120093962789,1.14466360668811,135.58935853799));
#67492=CARTESIAN_POINT('Ctrl Pts',(19.0045190605169,1.2716354413108,135.555373811286));
#67493=CARTESIAN_POINT('Ctrl Pts',(18.9967447263978,1.40342145163528,135.52010054334));
#67494=CARTESIAN_POINT('Ctrl Pts',(18.9889703922787,1.53394744765447,135.479283928885));
#67495=CARTESIAN_POINT('Ctrl Pts',(18.9811960581596,1.66271150720481,135.433029271327));
#67496=CARTESIAN_POINT('Ctrl Pts',(18.9734313052125,1.7913168765599,135.3868316185));
#67497=CARTESIAN_POINT('Ctrl Pts',(18.9656665522655,1.91816426552975,135.335209388264));
#67498=CARTESIAN_POINT('Ctrl Pts',(18.9579017993184,2.04276397483909,135.278318418619));
#67499=CARTESIAN_POINT('Ctrl Pts',(18.9501447584334,2.16723992995991,135.221483953887));
#67500=CARTESIAN_POINT('Ctrl Pts',(18.9423877175484,2.28947229470515,135.15939132496));
#67501=CARTESIAN_POINT('Ctrl Pts',(18.9346306766635,2.4089888623843,135.092245378542));
#67502=CARTESIAN_POINT('Ctrl Pts',(18.9268794854233,2.5284153016904,135.025150067404));
#67503=CARTESIAN_POINT('Ctrl Pts',(18.9191282941832,2.64512968088099,134.953009214555));
#67504=CARTESIAN_POINT('Ctrl Pts',(18.9113771029431,2.75868236171997,134.876074592004));
#67505=CARTESIAN_POINT('Ctrl Pts',(18.903629206166,2.87218677964077,134.79917266872));
#67506=CARTESIAN_POINT('Ctrl Pts',(18.8958813093888,2.98253184894381,134.717481246964));
#67507=CARTESIAN_POINT('Ctrl Pts',(18.8881334126118,3.08929521000551,134.631296489505));
#67508=CARTESIAN_POINT('Ctrl Pts',(18.8803871365277,3.19603623847348,134.545129760041));
#67509=CARTESIAN_POINT('Ctrl Pts',(18.8726408604436,3.29919674491121,134.454471809825));
#67510=CARTESIAN_POINT('Ctrl Pts',(18.8648945843595,3.39838620972065,134.359660075007));
#67511=CARTESIAN_POINT('Ctrl Pts',(18.8571482510942,3.49757640672432,134.26484764031));
#67512=CARTESIAN_POINT('Ctrl Pts',(18.8494019178289,3.59279522098654,134.165881629973));
#67513=CARTESIAN_POINT('Ctrl Pts',(18.8416555845635,3.68368816812722,134.063137158309));
#67514=CARTESIAN_POINT('Ctrl Pts',(18.8339075165606,3.77460147011271,133.960369677734));
#67515=CARTESIAN_POINT('Ctrl Pts',(18.8261594485576,3.86118671828092,133.853822344842));
#67516=CARTESIAN_POINT('Ctrl Pts',(18.8184113805547,3.94312924277681,133.743903921765));
#67517=CARTESIAN_POINT('Ctrl Pts',(18.8106550778128,4.02515885676319,133.633868676078));
#67518=CARTESIAN_POINT('Ctrl Pts',(18.802898775071,4.10253565615266,133.520455497057));
#67519=CARTESIAN_POINT('Ctrl Pts',(18.7951424723291,4.17498761062946,133.404103203591));
#67520=CARTESIAN_POINT('Ctrl Pts',(18.787382029815,4.24747823489596,133.287688809402));
#67521=CARTESIAN_POINT('Ctrl Pts',(18.7796215873008,4.31503858417031,133.168332515085));
#67522=CARTESIAN_POINT('Ctrl Pts',(18.7718611447866,4.37744277415799,133.046497504884));
#67523=CARTESIAN_POINT('Ctrl Pts',(18.7640882445212,4.43994714089134,132.924466914309));
#67524=CARTESIAN_POINT('Ctrl Pts',(18.7563153442557,4.49727864439844,132.799950011764));
#67525=CARTESIAN_POINT('Ctrl Pts',(18.7485424439903,4.54925935869746,132.673430533274));
#67526=CARTESIAN_POINT('Ctrl Pts',(18.7410521082282,4.59935044310082,132.551510356509));
#67527=CARTESIAN_POINT('Ctrl Pts',(18.7335617724661,4.64447290801315,132.427730962764));
#67528=CARTESIAN_POINT('Ctrl Pts',(18.726071436704,4.68451197301331,132.302536387359));
#67529=CARTESIAN_POINT('Ctrl Pts',(18.7182971025849,4.72606913133215,132.172595021577));
#67530=CARTESIAN_POINT('Ctrl Pts',(18.7105227684658,4.76228144672758,132.040717427323));
#67531=CARTESIAN_POINT('Ctrl Pts',(18.7027484343467,4.79296621274816,131.907382804992));
#67532=CARTESIAN_POINT('Ctrl Pts',(18.6949836813996,4.82361316253692,131.774212505668));
#67533=CARTESIAN_POINT('Ctrl Pts',(18.6872189284525,4.84874603037898,131.639589128437));
#67534=CARTESIAN_POINT('Ctrl Pts',(18.6794541755054,4.86823123277945,131.504008905415));
#67535=CARTESIAN_POINT('Ctrl Pts',(18.6716971346204,4.88769708220229,131.368563342583));
#67536=CARTESIAN_POINT('Ctrl Pts',(18.6639400937354,4.90152637376799,131.232163209689));
#67537=CARTESIAN_POINT('Ctrl Pts',(18.6561830528503,4.90963621155905,131.095316512244));
#67538=CARTESIAN_POINT('Ctrl Pts',(18.6484318616102,4.91773993365834,130.958573011959));
#67539=CARTESIAN_POINT('Ctrl Pts',(18.6406806703701,4.92013276388098,130.821384006119));
#67540=CARTESIAN_POINT('Ctrl Pts',(18.6329294791299,4.91678348469934,130.684263877028));
#67541=CARTESIAN_POINT('Ctrl Pts',(18.6251815823528,4.91343562905071,130.547202027651));
#67542=CARTESIAN_POINT('Ctrl Pts',(18.6174336855758,4.90435052759191,130.410209386828));
#67543=CARTESIAN_POINT('Ctrl Pts',(18.6096857887987,4.8895490547568,130.273801380886));
#67544=CARTESIAN_POINT('Ctrl Pts',(18.6019395127146,4.87475067807071,130.137421908557));
#67545=CARTESIAN_POINT('Ctrl Pts',(18.5941932366305,4.85423835055292,130.001627216299));
#67546=CARTESIAN_POINT('Ctrl Pts',(18.5864469605464,4.82808488140931,129.866928251789));
#67547=CARTESIAN_POINT('Ctrl Pts',(18.578700627281,4.80193121920673,129.732228292961));
#67548=CARTESIAN_POINT('Ctrl Pts',(18.5709542940157,4.77013640680457,129.598624461819));
#67549=CARTESIAN_POINT('Ctrl Pts',(18.5632079607503,4.73282443103251,129.466617754561));
#67550=CARTESIAN_POINT('Ctrl Pts',(18.5554598927473,4.69550409950208,129.334581485315));
#67551=CARTESIAN_POINT('Ctrl Pts',(18.5477118247444,4.6526642523596,129.204143427817));
#67552=CARTESIAN_POINT('Ctrl Pts',(18.5399637567414,4.60447870601963,129.075789268645));
#67553=CARTESIAN_POINT('Ctrl Pts',(18.5322074539995,4.55624194750766,128.947298693145));
#67554=CARTESIAN_POINT('Ctrl Pts',(18.5244511512577,4.50264827807244,128.820896806862));
#67555=CARTESIAN_POINT('Ctrl Pts',(18.5166948485158,4.44391984944271,128.697049668933));
#67556=CARTESIAN_POINT('Ctrl Pts',(18.5089344060016,4.38516007568227,128.573136430057));
#67557=CARTESIAN_POINT('Ctrl Pts',(18.5011739634874,4.32126026396362,128.451781002287));
#67558=CARTESIAN_POINT('Ctrl Pts',(18.4934135209733,4.25248800832976,128.333423790872));
#67559=CARTESIAN_POINT('Ctrl Pts',(18.4856406207078,4.18360535336593,128.214876581955));
#67560=CARTESIAN_POINT('Ctrl Pts',(18.4778677204424,4.10983483479806,128.099337537022));
#67561=CARTESIAN_POINT('Ctrl Pts',(18.4700948201769,4.03148726010452,127.987217821378));
#67562=CARTESIAN_POINT('Ctrl Pts',(18.462604484415,3.95598781709757,127.879173939811));
#67563=CARTESIAN_POINT('Ctrl Pts',(18.4551141486531,3.87623850199006,127.77430534635));
#67564=CARTESIAN_POINT('Ctrl Pts',(18.4476238128911,3.79255085265012,127.672948620948));
#67565=CARTESIAN_POINT('Ctrl Pts',(18.439849478772,3.70569016064817,127.567748924495));
#67566=CARTESIAN_POINT('Ctrl Pts',(18.4320751446529,3.61431144664124,127.465999416983));
#67567=CARTESIAN_POINT('Ctrl Pts',(18.4243008105339,3.51871911819316,127.368112834044));
#67568=CARTESIAN_POINT('Ctrl Pts',(18.4165360575868,3.42324459874682,127.270346887569));
#67569=CARTESIAN_POINT('Ctrl Pts',(18.4087713046398,3.32356706772349,127.176434670302));
#67570=CARTESIAN_POINT('Ctrl Pts',(18.4010065516927,3.22003181411451,127.086756795399));
#67571=CARTESIAN_POINT('Ctrl Pts',(18.3932495108077,3.11659939317901,126.997167989826));
#67572=CARTESIAN_POINT('Ctrl Pts',(18.3854924699227,3.00931716821446,126.911805411579));
#67573=CARTESIAN_POINT('Ctrl Pts',(18.3777354290377,2.89856773137483,126.831013392727));
#67574=CARTESIAN_POINT('Ctrl Pts',(18.3699842377976,2.78790181154732,126.750282299766));
#67575=CARTESIAN_POINT('Ctrl Pts',(18.3622330465575,2.67377419872415,126.674115135248));
#67576=CARTESIAN_POINT('Ctrl Pts',(18.3544818553175,2.55660078346902,126.602816199561));
#67577=CARTESIAN_POINT('Ctrl Pts',(18.3467339585404,2.43947717004044,126.531547567824));
#67578=CARTESIAN_POINT('Ctrl Pts',(18.3389860617633,2.31931066222879,126.465143252389));
#67579=CARTESIAN_POINT('Ctrl Pts',(18.3312381649862,2.19654618594038,126.403864291522));
#67580=CARTESIAN_POINT('Ctrl Pts',(18.3234918889021,2.07380738933391,126.342598148892));
#67581=CARTESIAN_POINT('Ctrl Pts',(18.315745612818,1.94847205476656,126.286455402836));
#67582=CARTESIAN_POINT('Ctrl Pts',(18.3079993367339,1.82100941214491,126.235650976608));
#67583=CARTESIAN_POINT('Ctrl Pts',(18.3002530034685,1.69354582862264,126.184846175354));
#67584=CARTESIAN_POINT('Ctrl Pts',(18.2925066702032,1.56395526889053,126.139379917316));
#67585=CARTESIAN_POINT('Ctrl Pts',(18.2847603369378,1.43272625314865,126.099418689546));
#67586=CARTESIAN_POINT('Ctrl Pts',(18.2770122689348,1.30146784957912,126.059448512737));
#67587=CARTESIAN_POINT('Ctrl Pts',(18.2692642009318,1.16857063380698,126.024985933221));
#67588=CARTESIAN_POINT('Ctrl Pts',(18.2615161329288,1.0345371797228,125.996147239785));
#67589=CARTESIAN_POINT('Ctrl Pts',(18.253759830187,0.900361273288428,125.967277896242));
#67590=CARTESIAN_POINT('Ctrl Pts',(18.2460035274452,0.765047099043303,125.944044461116));
#67591=CARTESIAN_POINT('Ctrl Pts',(18.2382472247033,0.629106844174649,125.926511948213));
#67592=CARTESIAN_POINT('Ctrl Pts',(18.2304867821891,0.493094033898705,125.908970077679));
#67593=CARTESIAN_POINT('Ctrl Pts',(18.2227263396749,0.356454866477291,125.897135226033));
#67594=CARTESIAN_POINT('Ctrl Pts',(18.2149658971608,0.219704508438073,125.891020308624));
#67595=CARTESIAN_POINT('Ctrl Pts',(18.2071929968953,0.0827346265840056,
125.884895575007));
#67596=CARTESIAN_POINT('Ctrl Pts',(18.1994200966299,-0.0543464113851937,
125.884509125583));
#67597=CARTESIAN_POINT('Ctrl Pts',(18.1916471963644,-0.191024681419766,
125.889821714109));
#67598=CARTESIAN_POINT('Ctrl Pts',(18.1841568606023,-0.322734352068102,
125.894941176661));
#67599=CARTESIAN_POINT('Ctrl Pts',(18.1766665248402,-0.454069722584113,
125.905352497755));
#67600=CARTESIAN_POINT('Ctrl Pts',(18.1691761890781,-0.584579224891734,
125.920975501448));
#67601=CARTESIAN_POINT('Ctrl Pts',(18.161401854959,-0.720037034645514,125.937190856073));
#67602=CARTESIAN_POINT('Ctrl Pts',(18.1536275208399,-0.855034203980925,
125.959072261967));
#67603=CARTESIAN_POINT('Ctrl Pts',(18.1458531867208,-0.989058946998879,
125.986586706115));
#67604=CARTESIAN_POINT('Ctrl Pts',(18.1380884337737,-1.12291851649902,126.014067241169));
#67605=CARTESIAN_POINT('Ctrl Pts',(18.1303236808266,-1.25580766489575,126.047166923667));
#67606=CARTESIAN_POINT('Ctrl Pts',(18.1225589278795,-1.38721953442619,126.08580098291));
#67607=CARTESIAN_POINT('Ctrl Pts',(18.1148018869945,-1.51850088383524,126.124396670261));
#67608=CARTESIAN_POINT('Ctrl Pts',(18.1070448461095,-1.64830750161597,126.168515685875));
#67609=CARTESIAN_POINT('Ctrl Pts',(18.0992878052245,-1.77614289104181,126.218022264031));
#67610=CARTESIAN_POINT('Ctrl Pts',(18.0915366139844,-1.90388187880537,126.267491508892));
#67611=CARTESIAN_POINT('Ctrl Pts',(18.0837854227443,-2.02965223393379,126.322340088914));
#67612=CARTESIAN_POINT('Ctrl Pts',(18.0760342315042,-2.15297314088268,126.38238258538));
#67613=CARTESIAN_POINT('Ctrl Pts',(18.0682863347271,-2.27624163315727,126.442399562183));
#67614=CARTESIAN_POINT('Ctrl Pts',(18.0605384379501,-2.39706239710342,126.50760589399));
#67615=CARTESIAN_POINT('Ctrl Pts',(18.052790541173,-2.51497532051442,126.577768349591));
#67616=CARTESIAN_POINT('Ctrl Pts',(18.0450442650889,-2.63286357908359,126.64791612872));
#67617=CARTESIAN_POINT('Ctrl Pts',(18.0372979890047,-2.74784487120467,126.723017769767));
#67618=CARTESIAN_POINT('Ctrl Pts',(18.0295517129206,-2.8594847456314,126.802794667591));
#67619=CARTESIAN_POINT('Ctrl Pts',(18.0218053796552,-2.97112544415847,126.88257215431));
#67620=CARTESIAN_POINT('Ctrl Pts',(18.0140590463899,-3.07942435767732,126.967024739363));
#67621=CARTESIAN_POINT('Ctrl Pts',(18.0063127131245,-3.18397735881582,127.055831407189));
#67622=CARTESIAN_POINT('Ctrl Pts',(17.9985646451215,-3.28855377387414,127.144657962653));
#67623=CARTESIAN_POINT('Ctrl Pts',(17.9908165771185,-3.38938230937185,127.237840288103));
#67624=CARTESIAN_POINT('Ctrl Pts',(17.9830685091155,-3.4860934747957,127.335018410823));
#67625=CARTESIAN_POINT('Ctrl Pts',(17.9753122063736,-3.58290742599678,127.432299815608));
#67626=CARTESIAN_POINT('Ctrl Pts',(17.9675559036318,-3.67559498938548,127.533585223503));
#67627=CARTESIAN_POINT('Ctrl Pts',(17.9597996008899,-3.76382461731946,127.638478858473));
#67628=CARTESIAN_POINT('Ctrl Pts',(17.9520391583757,-3.8521013360624,127.743428478333));
#67629=CARTESIAN_POINT('Ctrl Pts',(17.9442787158616,-3.93591513952066,127.85198985331));
#67630=CARTESIAN_POINT('Ctrl Pts',(17.9365182733474,-4.0149767015535,127.963736540275));
#67631=CARTESIAN_POINT('Ctrl Pts',(17.928745373082,-4.09416518022448,128.075662612943));
#67632=CARTESIAN_POINT('Ctrl Pts',(17.9209724728166,-4.16858596048213,128.19078388717));
#67633=CARTESIAN_POINT('Ctrl Pts',(17.9131995725511,-4.23799427280047,128.308646770545));
#67634=CARTESIAN_POINT('Ctrl Pts',(17.9057092367892,-4.3048794181364,128.42222504123));
#67635=CARTESIAN_POINT('Ctrl Pts',(17.8982189010272,-4.36711005464315,128.538348781416));
#67636=CARTESIAN_POINT('Ctrl Pts',(17.8907285652652,-4.42450955303831,128.656594737035));
#67637=CARTESIAN_POINT('Ctrl Pts',(17.8823534369874,-4.48868934115728,128.78880844255));
#67638=CARTESIAN_POINT('Ctrl Pts',(17.8739783087096,-4.54700911824314,128.924045188624));
#67639=CARTESIAN_POINT('Ctrl Pts',(17.8656031804317,-4.59919598865022,129.061782263378));
#67640=CARTESIAN_POINT('Ctrl Pts',(17.8572491334189,-4.65125149805542,129.199172636367));
#67641=CARTESIAN_POINT('Ctrl Pts',(17.848895086406,-4.69720477936736,129.339050511504));
#67642=CARTESIAN_POINT('Ctrl Pts',(17.8405410393931,-4.73683014450314,129.48087157544));
#67643=CARTESIAN_POINT('Ctrl Pts',(17.8385520750553,-4.7462643071315,129.514636891589));
#67644=CARTESIAN_POINT('Ctrl Pts',(17.8365631107176,-4.75533998593173,129.548512251133));
#67645=CARTESIAN_POINT('Ctrl Pts',(17.8345741463799,-4.76405452823412,129.582490119309));
#67646=CARTESIAN_POINT('Ctrl Pts',(19.584898128716,-4.76405452823411,129.582490119308));
#67647=CARTESIAN_POINT('Ctrl Pts',(19.5770701885249,-4.79828050826579,129.715936696));
#67648=CARTESIAN_POINT('Ctrl Pts',(19.5692422483337,-4.8268499179298,129.850645650192));
#67649=CARTESIAN_POINT('Ctrl Pts',(19.5614143081426,-4.84970383971167,129.986096766729));
#67650=CARTESIAN_POINT('Ctrl Pts',(19.549079713458,-4.88571508344255,130.199528982776));
#67651=CARTESIAN_POINT('Ctrl Pts',(19.5367451187733,-4.90764377638311,130.415400463251));
#67652=CARTESIAN_POINT('Ctrl Pts',(19.5244105240887,-4.91523706832655,130.632233848443));
#67653=CARTESIAN_POINT('Ctrl Pts',(19.5212268280562,-4.9171969814045,130.688200956062));
#67654=CARTESIAN_POINT('Ctrl Pts',(19.5180431320238,-4.91820204469388,130.744231974131));
#67655=CARTESIAN_POINT('Ctrl Pts',(19.5148594359913,-4.91824832460009,130.800301052513));
#67656=CARTESIAN_POINT('',(19.8601405640419,-4.9182486111303,130.808056779749));
#67657=CARTESIAN_POINT('Ctrl Pts',(19.9302639333258,-4.76405452823407,129.582490119308));
#67658=CARTESIAN_POINT('Ctrl Pts',(19.9226230702679,-4.79767066593726,129.713558930017));
#67659=CARTESIAN_POINT('Ctrl Pts',(19.9149822072099,-4.82585514710882,129.845943911475));
#67660=CARTESIAN_POINT('Ctrl Pts',(19.907341344152,-4.84852636025179,129.979148404591));
#67661=CARTESIAN_POINT('Ctrl Pts',(19.8994745474669,-4.87186794130703,130.116291637879));
#67662=CARTESIAN_POINT('Ctrl Pts',(19.891607750782,-4.88936509178852,130.254303138695));
#67663=CARTESIAN_POINT('Ctrl Pts',(19.8837409540969,-4.90098625865664,130.392636492746));
#67664=CARTESIAN_POINT('Ctrl Pts',(19.8758741574119,-4.91260742552476,130.530969846797));
#67665=CARTESIAN_POINT('Ctrl Pts',(19.8680073607269,-4.91835264568835,130.669624591082));
#67666=CARTESIAN_POINT('Ctrl Pts',(19.8601405640419,-4.9182486111303,130.808056779749));
#67667=CARTESIAN_POINT('Ctrl Pts',(19.8601405640087,-4.91824861112986,130.808056780332));
#67668=CARTESIAN_POINT('Ctrl Pts',(19.8468513546045,-4.9180728677745,131.041907281002));
#67669=CARTESIAN_POINT('Ctrl Pts',(19.8335621452003,-4.90121708260459,131.275143667519));
#67670=CARTESIAN_POINT('Ctrl Pts',(19.8202729357961,-4.86795053232145,131.505959275897));
#67671=CARTESIAN_POINT('Ctrl Pts',(19.812498601677,-4.84848923338151,131.640988953347));
#67672=CARTESIAN_POINT('Ctrl Pts',(19.8047242675579,-4.82337456895603,131.775422153426));
#67673=CARTESIAN_POINT('Ctrl Pts',(19.7969499334388,-4.79265182400327,131.908748029835));
#67674=CARTESIAN_POINT('Ctrl Pts',(19.7891851804917,-4.7619669420879,132.041909594017));
#67675=CARTESIAN_POINT('Ctrl Pts',(19.7814204275447,-4.72568781833477,132.173966172509));
#67676=CARTESIAN_POINT('Ctrl Pts',(19.7736556745976,-4.68391136221968,132.304413087771));
#67677=CARTESIAN_POINT('Ctrl Pts',(19.7658986337126,-4.64217639906987,132.434730441319));
#67678=CARTESIAN_POINT('Ctrl Pts',(19.7581415928275,-4.59495508773192,132.563440943275));
#67679=CARTESIAN_POINT('Ctrl Pts',(19.7503845519425,-4.54239506938144,132.690051497896));
#67680=CARTESIAN_POINT('Ctrl Pts',(19.7426333607024,-4.48987468694967,132.816566574512));
#67681=CARTESIAN_POINT('Ctrl Pts',(19.7348821694623,-4.43202376022778,132.9409844962));
#67682=CARTESIAN_POINT('Ctrl Pts',(19.7271309782222,-4.36903919278346,133.062829035415));
#67683=CARTESIAN_POINT('Ctrl Pts',(19.7193830814451,-4.3060813954603,133.184621787451));
#67684=CARTESIAN_POINT('Ctrl Pts',(19.711635184668,-4.23799447627153,133.303842985833));
#67685=CARTESIAN_POINT('Ctrl Pts',(19.703887287891,-4.16502264068342,133.420038247759));
#67686=CARTESIAN_POINT('Ctrl Pts',(19.6961410118068,-4.09206606923021,133.536209204142));
#67687=CARTESIAN_POINT('Ctrl Pts',(19.6883947357228,-4.01422682162775,133.649355152185));
#67688=CARTESIAN_POINT('Ctrl Pts',(19.6806484596387,-3.93179384841794,133.759048451508));
#67689=CARTESIAN_POINT('Ctrl Pts',(19.6729021263734,-3.84936026670676,133.868742560561));
#67690=CARTESIAN_POINT('Ctrl Pts',(19.6651557931079,-3.76233312659987,133.974983657488));
#67691=CARTESIAN_POINT('Ctrl Pts',(19.6574094598426,-3.67104304915753,134.077375434785));
#67692=CARTESIAN_POINT('Ctrl Pts',(19.6496613918396,-3.57973252793531,134.179790142009));
#67693=CARTESIAN_POINT('Ctrl Pts',(19.6419133238367,-3.48415742985533,134.278353522501));
#67694=CARTESIAN_POINT('Ctrl Pts',(19.6341652558337,-3.38468649072615,134.372704830502));
#67695=CARTESIAN_POINT('Ctrl Pts',(19.6264089530918,-3.28510983269901,134.467156416197));
#67696=CARTESIAN_POINT('Ctrl Pts',(19.61865265035,-3.18162934654533,134.557386717343));
#67697=CARTESIAN_POINT('Ctrl Pts',(19.6108963476081,-3.07464865055661,134.643073779308));
#67698=CARTESIAN_POINT('Ctrl Pts',(19.6031359050939,-2.96761085574931,134.728806575038));
#67699=CARTESIAN_POINT('Ctrl Pts',(19.5953754625798,-2.85706944358312,134.809991068529));
#67700=CARTESIAN_POINT('Ctrl Pts',(19.5876150200656,-2.74345767741099,134.886348250418));
#67701=CARTESIAN_POINT('Ctrl Pts',(19.5798421198002,-2.62966353154581,134.962828007634));
#67702=CARTESIAN_POINT('Ctrl Pts',(19.5720692195348,-2.51278951587592,135.034464763388));
#67703=CARTESIAN_POINT('Ctrl Pts',(19.5642963192693,-2.39329496598304,135.10102470361));
#67704=CARTESIAN_POINT('Ctrl Pts',(19.5568059835073,-2.27814434396737,135.165165022351));
#67705=CARTESIAN_POINT('Ctrl Pts',(19.5493156477453,-2.16056068086108,135.224591088396));
#67706=CARTESIAN_POINT('Ctrl Pts',(19.5418253119832,-2.04097134746111,135.279136480259));
#67707=CARTESIAN_POINT('Ctrl Pts',(19.5340509778642,-1.91684774813689,135.335749977234));
#67708=CARTESIAN_POINT('Ctrl Pts',(19.5262766437451,-1.7901701999834,135.387284727124));
#67709=CARTESIAN_POINT('Ctrl Pts',(19.518502309626,-1.66139297008352,135.433502704547));
#67710=CARTESIAN_POINT('Ctrl Pts',(19.5107375566789,-1.53277444661052,135.479663722443));
#67711=CARTESIAN_POINT('Ctrl Pts',(19.5029728037318,-1.40206175453398,135.520520874487));
#67712=CARTESIAN_POINT('Ctrl Pts',(19.4952080507848,-1.2697318752981,135.555882902829));
#67713=CARTESIAN_POINT('Ctrl Pts',(19.4874510098998,-1.1375334279638,135.591209809106));
#67714=CARTESIAN_POINT('Ctrl Pts',(19.4796939690148,-1.00372136517407,135.621052352737));
#67715=CARTESIAN_POINT('Ctrl Pts',(19.4719369281298,-0.868790346006051,
135.645268218129));
#67716=CARTESIAN_POINT('Ctrl Pts',(19.4641857368896,-0.733961079369011,
135.669465822148));
#67717=CARTESIAN_POINT('Ctrl Pts',(19.4564345456495,-0.598014919173669,
135.688045124823));
#67718=CARTESIAN_POINT('Ctrl Pts',(19.4486833544094,-0.461458960327743,
135.70091437408));
#67719=CARTESIAN_POINT('Ctrl Pts',(19.4409354576323,-0.324961041407075,
135.713778153564));
#67720=CARTESIAN_POINT('Ctrl Pts',(19.4331875608552,-0.187854227752063,
135.720936669993));
#67721=CARTESIAN_POINT('Ctrl Pts',(19.4254396640781,-0.0506528035006185,
135.722349775342));
#67722=CARTESIAN_POINT('Ctrl Pts',(19.417693387994,0.0865199211705932,135.723762585099));
#67723=CARTESIAN_POINT('Ctrl Pts',(19.4099471119099,0.223786826377065,135.719432370229));
#67724=CARTESIAN_POINT('Ctrl Pts',(19.4022008358258,0.36063194132993,135.709371082936));
#67725=CARTESIAN_POINT('Ctrl Pts',(19.3944545025604,0.497478066442161,135.699309721373));
#67726=CARTESIAN_POINT('Ctrl Pts',(19.3867081692951,0.633902005175143,135.683517231637));
#67727=CARTESIAN_POINT('Ctrl Pts',(19.3789618360298,0.769391624041899,135.662057560702));
#67728=CARTESIAN_POINT('Ctrl Pts',(19.3712137680268,0.904911584869381,135.640593084023));
#67729=CARTESIAN_POINT('Ctrl Pts',(19.3634657000238,1.03949642340052,135.613458961881));
#67730=CARTESIAN_POINT('Ctrl Pts',(19.3557176320208,1.1726433233022,135.580770430262));
#67731=CARTESIAN_POINT('Ctrl Pts',(19.3479613292789,1.30593173331356,135.548047156882));
#67732=CARTESIAN_POINT('Ctrl Pts',(19.3402050265371,1.43777877153954,135.509757774928));
#67733=CARTESIAN_POINT('Ctrl Pts',(19.3324487237952,1.56769540288516,135.466067835557));
#67734=CARTESIAN_POINT('Ctrl Pts',(19.3246882812811,1.69768137464881,135.42235457755));
#67735=CARTESIAN_POINT('Ctrl Pts',(19.316927838767,1.8257345216869,135.373235158573));
#67736=CARTESIAN_POINT('Ctrl Pts',(19.3091673962528,1.95138591609533,135.318923283978));
#67737=CARTESIAN_POINT('Ctrl Pts',(19.3013944959874,2.07723901727688,135.264524223141));
#67738=CARTESIAN_POINT('Ctrl Pts',(19.2936215957219,2.20068230902758,135.204916220025));
#67739=CARTESIAN_POINT('Ctrl Pts',(19.2858486954565,2.32127079484554,135.140359344445));
#67740=CARTESIAN_POINT('Ctrl Pts',(19.2783583596944,2.43747558545995,135.078149273902));
#67741=CARTESIAN_POINT('Ctrl Pts',(19.2708680239325,2.5510292599072,135.011344048248));
#67742=CARTESIAN_POINT('Ctrl Pts',(19.2633776881704,2.66156079872216,134.94021327176));
#67743=CARTESIAN_POINT('Ctrl Pts',(19.2556033540513,2.77628317442661,134.866385550262));
#67744=CARTESIAN_POINT('Ctrl Pts',(19.2478290199323,2.88811312809731,134.787663932428));
#67745=CARTESIAN_POINT('Ctrl Pts',(19.2400546858132,2.99660485978374,134.704301947486));
#67746=CARTESIAN_POINT('Ctrl Pts',(19.2322899328661,3.10496288510706,134.621042698741));
#67747=CARTESIAN_POINT('Ctrl Pts',(19.2245251799189,3.20999056715886,134.533154697592));
#67748=CARTESIAN_POINT('Ctrl Pts',(19.2167604269718,3.31126917517196,134.440935862499));
#67749=CARTESIAN_POINT('Ctrl Pts',(19.2090033860868,3.41244719184381,134.348808620452));
#67750=CARTESIAN_POINT('Ctrl Pts',(19.2012463452018,3.50988325746431,134.252359366049));
#67751=CARTESIAN_POINT('Ctrl Pts',(19.1934893043168,3.60319026258126,134.151927344928));
#67752=CARTESIAN_POINT('Ctrl Pts',(19.1857381130767,3.69642690415983,134.051571060375));
#67753=CARTESIAN_POINT('Ctrl Pts',(19.1779869218366,3.78554041794808,133.947238272527));
#67754=CARTESIAN_POINT('Ctrl Pts',(19.1702357305965,3.87017951314547,133.839306020457));
#67755=CARTESIAN_POINT('Ctrl Pts',(19.1624878338194,3.95478263446958,133.731419642473));
#67756=CARTESIAN_POINT('Ctrl Pts',(19.1547399370423,4.03491487888207,133.619937150065));
#67757=CARTESIAN_POINT('Ctrl Pts',(19.1469920402652,4.11026448557195,133.505269524054));
#67758=CARTESIAN_POINT('Ctrl Pts',(19.1392457641811,4.18559833074846,133.390625884038));
#67759=CARTESIAN_POINT('Ctrl Pts',(19.1314994880969,4.2561513135353,133.272798762179));
#67760=CARTESIAN_POINT('Ctrl Pts',(19.1237532120128,4.32165459484505,133.152228719772));
#67761=CARTESIAN_POINT('Ctrl Pts',(19.1160068787475,4.38715835968523,133.031657787344));
#67762=CARTESIAN_POINT('Ctrl Pts',(19.1082605454821,4.44761216202877,132.908344237505));
#67763=CARTESIAN_POINT('Ctrl Pts',(19.1005142122168,4.50279298161737,132.782753507565));
#67764=CARTESIAN_POINT('Ctrl Pts',(19.0927661442138,4.55798615856785,132.657134652451));
#67765=CARTESIAN_POINT('Ctrl Pts',(19.0850180762108,4.60790384577495,132.529237960349));
#67766=CARTESIAN_POINT('Ctrl Pts',(19.0772700082078,4.65237121002717,132.399548752743));
#67767=CARTESIAN_POINT('Ctrl Pts',(19.069513705466,4.69688583472329,132.269721709905));
#67768=CARTESIAN_POINT('Ctrl Pts',(19.0617574027241,4.73593843797796,132.138098716327));
#67769=CARTESIAN_POINT('Ctrl Pts',(19.0540010999823,4.76940396725428,132.005180695529));
#67770=CARTESIAN_POINT('Ctrl Pts',(19.0462406574681,4.80288735809124,131.872191732382));
#67771=CARTESIAN_POINT('Ctrl Pts',(19.0384802149539,4.83077765361724,131.737906747359));
#67772=CARTESIAN_POINT('Ctrl Pts',(19.0307197724397,4.85300118321247,131.602835775751));
#67773=CARTESIAN_POINT('Ctrl Pts',(19.0229468721743,4.87526038799032,131.467547976228));
#67774=CARTESIAN_POINT('Ctrl Pts',(19.0151739719089,4.89183460124296,131.331472057091));
#67775=CARTESIAN_POINT('Ctrl Pts',(19.0074010716434,4.90270209559428,131.195122980589));
#67776=CARTESIAN_POINT('Ctrl Pts',(18.9999107358814,4.91317452915234,131.063730536461));
#67777=CARTESIAN_POINT('Ctrl Pts',(18.9924204001193,4.91834793552886,130.932084757867));
#67778=CARTESIAN_POINT('Ctrl Pts',(18.9849300643573,4.91824859535366,130.800643521688));
#67779=CARTESIAN_POINT('Ctrl Pts',(18.9771557302382,4.91814548866552,130.66421865109));
#67780=CARTESIAN_POINT('Ctrl Pts',(18.9693813961192,4.91236158362694,130.527581986556));
#67781=CARTESIAN_POINT('Ctrl Pts',(18.9616070620001,4.90086921579578,130.391245630952));
#67782=CARTESIAN_POINT('Ctrl Pts',(18.953842309053,4.88939101128088,130.255077297721));
#67783=CARTESIAN_POINT('Ctrl Pts',(18.9460775561058,4.87221837438962,130.119208922868));
#67784=CARTESIAN_POINT('Ctrl Pts',(18.9383128031587,4.84937561815072,129.984153828649));
#67785=CARTESIAN_POINT('Ctrl Pts',(18.9305557622737,4.82655554965938,129.849232873054));
#67786=CARTESIAN_POINT('Ctrl Pts',(18.9227987213888,4.79807663382164,129.715123973606));
#67787=CARTESIAN_POINT('Ctrl Pts',(18.9150416805038,4.76401504548548,129.582336187005));
#67788=CARTESIAN_POINT('Ctrl Pts',(18.9072904892636,4.72997914325799,129.449648536707));
#67789=CARTESIAN_POINT('Ctrl Pts',(18.8995392980235,4.69036904490487,129.318280393429));
#67790=CARTESIAN_POINT('Ctrl Pts',(18.8917881067834,4.64531208281695,129.1887311069));
#67791=CARTESIAN_POINT('Ctrl Pts',(18.8840402100063,4.60027427113991,129.059236882274));
#67792=CARTESIAN_POINT('Ctrl Pts',(18.8762923132292,4.5497943283726,128.931560345329));
#67793=CARTESIAN_POINT('Ctrl Pts',(18.8685444164522,4.49404950998589,128.806185934438));
#67794=CARTESIAN_POINT('Ctrl Pts',(18.860798140368,4.4383163522134,128.68083774917));
#67795=CARTESIAN_POINT('Ctrl Pts',(18.8530518642839,4.37732066810429,128.557791089135));
#67796=CARTESIAN_POINT('Ctrl Pts',(18.8453055881998,4.31128780026043,128.437510270411));
#67797=CARTESIAN_POINT('Ctrl Pts',(18.8375592549345,4.24525444497703,128.317228563803));
#67798=CARTESIAN_POINT('Ctrl Pts',(18.8298129216691,4.17418401990964,128.199713081962));
#67799=CARTESIAN_POINT('Ctrl Pts',(18.8220665884038,4.0983475627509,128.085403038384));
#67800=CARTESIAN_POINT('Ctrl Pts',(18.8143185204008,4.02249412254329,127.971067395863));
#67801=CARTESIAN_POINT('Ctrl Pts',(18.8065704523978,3.94187274249744,127.859938945742));
#67802=CARTESIAN_POINT('Ctrl Pts',(18.7988223843948,3.85679723570375,127.752427108269));
#67803=CARTESIAN_POINT('Ctrl Pts',(18.791066081653,3.77163130964914,127.644801005937));
#67804=CARTESIAN_POINT('Ctrl Pts',(18.7833097789112,3.68200204336714,127.540799501692));
#67805=CARTESIAN_POINT('Ctrl Pts',(18.7755534761693,3.58826328405119,127.440798567175));
#67806=CARTESIAN_POINT('Ctrl Pts',(18.7677930336552,3.49447449353685,127.340744259148));
#67807=CARTESIAN_POINT('Ctrl Pts',(18.7600325911409,3.39657211847902,127.24469504913));
#67808=CARTESIAN_POINT('Ctrl Pts',(18.7522721486268,3.29494544524281,127.152988604832));
#67809=CARTESIAN_POINT('Ctrl Pts',(18.7444992483613,3.19315563184874,127.061134945209));
#67810=CARTESIAN_POINT('Ctrl Pts',(18.7367263480959,3.08762987431949,126.973638232061));
#67811=CARTESIAN_POINT('Ctrl Pts',(18.7289534478305,2.97878968080195,126.890795094919));
#67812=CARTESIAN_POINT('Ctrl Pts',(18.7214631120685,2.87390610247098,126.810963514482));
#67813=CARTESIAN_POINT('Ctrl Pts',(18.7139727763065,2.76594513305206,126.735453222222));
#67814=CARTESIAN_POINT('Ctrl Pts',(18.7064824405445,2.65530620265505,126.66448960114));
#67815=CARTESIAN_POINT('Ctrl Pts',(18.6987081064254,2.54047236358374,126.590835372796));
#67816=CARTESIAN_POINT('Ctrl Pts',(18.6909337723063,2.42238972600694,126.521846081197));
#67817=CARTESIAN_POINT('Ctrl Pts',(18.6831594381872,2.30147418326171,126.457821805329));
#67818=CARTESIAN_POINT('Ctrl Pts',(18.6753946852401,2.18070765811654,126.39387643366));
#67819=CARTESIAN_POINT('Ctrl Pts',(18.6676299322931,2.05711551665556,126.334884084053));
#67820=CARTESIAN_POINT('Ctrl Pts',(18.659865179346,1.93114277321776,126.281101764488));
#67821=CARTESIAN_POINT('Ctrl Pts',(18.652108138461,1.80529514768465,126.227372862281));
#67822=CARTESIAN_POINT('Ctrl Pts',(18.644351097576,1.67707198277137,126.178843844796));
#67823=CARTESIAN_POINT('Ctrl Pts',(18.636594056691,1.5469427366621,126.135725781558));
#67824=CARTESIAN_POINT('Ctrl Pts',(18.6288428654508,1.41691162202958,126.092640233986));
#67825=CARTESIAN_POINT('Ctrl Pts',(18.6210916742107,1.28497765686095,126.05495764126));
#67826=CARTESIAN_POINT('Ctrl Pts',(18.6133404829706,1.15162978449178,126.022840785758));
#67827=CARTESIAN_POINT('Ctrl Pts',(18.6055925861935,1.01833858852554,125.990737580776));
#67828=CARTESIAN_POINT('Ctrl Pts',(18.5978446894165,0.883635059899439,125.964195499401));
#67829=CARTESIAN_POINT('Ctrl Pts',(18.5900967926394,0.748022581247887,125.943327262358));
#67830=CARTESIAN_POINT('Ctrl Pts',(18.5823505165553,0.612438469803402,125.9224633905));
#67831=CARTESIAN_POINT('Ctrl Pts',(18.5746042404711,0.475946172690013,125.907271061698));
#67832=CARTESIAN_POINT('Ctrl Pts',(18.5668579643871,0.339058135356334,125.897811663021));
#67833=CARTESIAN_POINT('Ctrl Pts',(18.5591116311217,0.202169087546445,125.888352194516));
#67834=CARTESIAN_POINT('Ctrl Pts',(18.5513652978564,0.0648846837221543,
125.884625767534));
#67835=CARTESIAN_POINT('Ctrl Pts',(18.5436189645911,-0.0722790508716011,
125.88664175601));
#67836=CARTESIAN_POINT('Ctrl Pts',(18.5358708965881,-0.209473502332692,
125.888658195952));
#67837=CARTESIAN_POINT('Ctrl Pts',(18.5281228285852,-0.346546839942367,
125.896419604547));
#67838=CARTESIAN_POINT('Ctrl Pts',(18.5203747605823,-0.482984983207766,
125.909883263599));
#67839=CARTESIAN_POINT('Ctrl Pts',(18.5126184578404,-0.619568134555649,
125.923361231989));
#67840=CARTESIAN_POINT('Ctrl Pts',(18.5048621550985,-0.755514353294202,
125.942553518722));
#67841=CARTESIAN_POINT('Ctrl Pts',(18.4971058523566,-0.890316060784019,
125.967365643989));
#67842=CARTESIAN_POINT('Ctrl Pts',(18.4893454098425,-1.02518971600411,125.992191012234));
#67843=CARTESIAN_POINT('Ctrl Pts',(18.4815849673283,-1.15891726176452,126.022642108962));
#67844=CARTESIAN_POINT('Ctrl Pts',(18.4738245248142,-1.2910041898671,126.058573934176));
#67845=CARTESIAN_POINT('Ctrl Pts',(18.4660516245487,-1.4233031556328,126.094563440345));
#67846=CARTESIAN_POINT('Ctrl Pts',(18.4582787242832,-1.55395586799444,126.136051138116));
#67847=CARTESIAN_POINT('Ctrl Pts',(18.4505058240178,-1.68248492867731,126.182842736255));
#67848=CARTESIAN_POINT('Ctrl Pts',(18.4430154882557,-1.80634163425989,126.227933341942));
#67849=CARTESIAN_POINT('Ctrl Pts',(18.4355251524937,-1.9282261227659,126.27794880572));
#67850=CARTESIAN_POINT('Ctrl Pts',(18.4280348167316,-2.04773287136316,126.332674900743));
#67851=CARTESIAN_POINT('Ctrl Pts',(18.420259886146,-2.1717802711554,126.389480310212));
#67852=CARTESIAN_POINT('Ctrl Pts',(18.4124849555604,-2.293658649495,126.451541345122));
#67853=CARTESIAN_POINT('Ctrl Pts',(18.4047100249748,-2.41289063170151,126.518670257548));
#67854=CARTESIAN_POINT('Ctrl Pts',(18.3969448101675,-2.5319736181719,126.585715283743));
#67855=CARTESIAN_POINT('Ctrl Pts',(18.3891795953601,-2.64841645136489,126.6578153959));
#67856=CARTESIAN_POINT('Ctrl Pts',(18.3814143805528,-2.76176228286144,126.734735062866));
#67857=CARTESIAN_POINT('Ctrl Pts',(18.3736570118381,-2.8749935879856,126.811577009018));
#67858=CARTESIAN_POINT('Ctrl Pts',(18.3658996431232,-2.98513379777967,126.893228599994));
#67859=CARTESIAN_POINT('Ctrl Pts',(18.3581422744085,-3.09175152938691,126.979408912899));
#67860=CARTESIAN_POINT('Ctrl Pts',(18.3503913215521,-3.19828108105846,127.06551794897));
#67861=CARTESIAN_POINT('Ctrl Pts',(18.3426403686959,-3.30129365293273,127.15614800374));
#67862=CARTESIAN_POINT('Ctrl Pts',(18.3348894158395,-3.40038804793612,127.250975726233));
#67863=CARTESIAN_POINT('Ctrl Pts',(18.3271419534053,-3.49943781858518,127.345760745747));
#67864=CARTESIAN_POINT('Ctrl Pts',(18.3193944909712,-3.59457264104929,127.44473940239));
#67865=CARTESIAN_POINT('Ctrl Pts',(18.311647028537,-3.68542565559922,127.547549170836));
#67866=CARTESIAN_POINT('Ctrl Pts',(18.3039013771726,-3.77625743207812,127.650334906165));
#67867=CARTESIAN_POINT('Ctrl Pts',(18.2961557258082,-3.8628091341744,127.756949678145));
#67868=CARTESIAN_POINT('Ctrl Pts',(18.2884100744438,-3.94475220748754,127.866995627644));
#67869=CARTESIAN_POINT('Ctrl Pts',(18.2806645563721,-4.02669387066683,127.977039683394));
#67870=CARTESIAN_POINT('Ctrl Pts',(18.2729190383004,-4.10402683062057,128.090514484904));
#67871=CARTESIAN_POINT('Ctrl Pts',(18.2651735202287,-4.17646436527294,128.206991088965));
#67872=CARTESIAN_POINT('Ctrl Pts',(18.257423172576,-4.24894706707074,128.323540319956));
#67873=CARTESIAN_POINT('Ctrl Pts',(18.2496728249232,-4.31652803848912,128.44309476067));
#67874=CARTESIAN_POINT('Ctrl Pts',(18.2419224772704,-4.37896513540232,128.565198406954));
#67875=CARTESIAN_POINT('Ctrl Pts',(18.2341695744863,-4.44142281655195,128.687342308319));
#67876=CARTESIAN_POINT('Ctrl Pts',(18.2264166717022,-4.4987330775707,128.812036736195));
#67877=CARTESIAN_POINT('Ctrl Pts',(18.218663768918,-4.55070130352922,128.938804210336));
#67878=CARTESIAN_POINT('Ctrl Pts',(18.2109023070429,-4.60272690164677,129.065711633908));
#67879=CARTESIAN_POINT('Ctrl Pts',(18.2031408451677,-4.6493985481491,129.194696308785));
#67880=CARTESIAN_POINT('Ctrl Pts',(18.1953793832926,-4.69057087589728,129.325263622544));
#67881=CARTESIAN_POINT('Ctrl Pts',(18.1903197138673,-4.71741097009964,129.410379990568));
#67882=CARTESIAN_POINT('Ctrl Pts',(18.185260044442,-4.74191504912875,129.49616862629));
#67883=CARTESIAN_POINT('Ctrl Pts',(18.1802003750167,-4.76405452823408,129.582490119308));
#67884=CARTESIAN_POINT('Origin',(213.235140564004,0.,130.804360617566));
#67885=CARTESIAN_POINT('',(16.0848513025106,-4.76405452823409,129.582490119308));
#67886=CARTESIAN_POINT('',(16.4298612965399,-4.76405452823409,129.582490119308));
#67887=CARTESIAN_POINT('',(213.235140564004,-4.76405452823405,129.582490119308));
#67888=CARTESIAN_POINT('',(17.7648594360204,-4.9182498302975,130.803068611917));
#67889=CARTESIAN_POINT('Ctrl Pts',(17.7648594359913,-4.91824983029764,130.803068612434));
#67890=CARTESIAN_POINT('Ctrl Pts',(17.7568883079903,-4.91828700392096,130.944576693201));
#67891=CARTESIAN_POINT('Ctrl Pts',(17.7489171799893,-4.91221261508659,131.086020317408));
#67892=CARTESIAN_POINT('Ctrl Pts',(17.7409460519883,-4.9000695348613,131.226855133535));
#67893=CARTESIAN_POINT('Ctrl Pts',(17.7329691638686,-4.88791767976969,131.367791720108));
#67894=CARTESIAN_POINT('Ctrl Pts',(17.724992275749,-4.86968842145711,131.508118265165));
#67895=CARTESIAN_POINT('Ctrl Pts',(17.7170153876293,-4.84547629013657,131.647297497898));
#67896=CARTESIAN_POINT('Ctrl Pts',(17.7090314877391,-4.82124287609155,131.786599070678));
#67897=CARTESIAN_POINT('Ctrl Pts',(17.7010475878487,-4.79101616576517,131.924750968601));
#67898=CARTESIAN_POINT('Ctrl Pts',(17.6930636879584,-4.75494136603763,132.061228020296));
#67899=CARTESIAN_POINT('Ctrl Pts',(17.685065771649,-4.71880323391348,132.197944669128));
#67900=CARTESIAN_POINT('Ctrl Pts',(17.6770678553396,-4.67679659075788,132.332980250728));
#67901=CARTESIAN_POINT('Ctrl Pts',(17.6690699390301,-4.62911627812375,132.465825497156));
#67902=CARTESIAN_POINT('Ctrl Pts',(17.6610640711306,-4.58138856135538,132.598802819351));
#67903=CARTESIAN_POINT('Ctrl Pts',(17.6530582032311,-4.52797606011424,132.72958513304));
#67904=CARTESIAN_POINT('Ctrl Pts',(17.6450523353316,-4.46912083899419,132.857685236073));
#67905=CARTESIAN_POINT('Ctrl Pts',(17.637031874495,-4.41015833774535,132.986018837431));
#67906=CARTESIAN_POINT('Ctrl Pts',(17.6290114136584,-4.34573345708694,133.111660141843));
#67907=CARTESIAN_POINT('Ctrl Pts',(17.6209909528218,-4.27613358421434,133.234147569637));
#67908=CARTESIAN_POINT('Ctrl Pts',(17.6180876156986,-4.2509390350735,133.278486954054));
#67909=CARTESIAN_POINT('Ctrl Pts',(17.6151842785755,-4.22506676861061,133.322413351635));
#67910=CARTESIAN_POINT('Ctrl Pts',(17.6122809414523,-4.19853175125283,133.365905892634));
#67911=CARTESIAN_POINT('Ctrl Pts',(17.6045066073332,-4.12747831100699,133.482366892879));
#67912=CARTESIAN_POINT('Ctrl Pts',(17.5967322732141,-4.05146297359281,133.596053744055));
#67913=CARTESIAN_POINT('Ctrl Pts',(17.5889579390951,-3.97072849725918,133.706514690587));
#67914=CARTESIAN_POINT('Ctrl Pts',(17.581193186148,-3.89009351895228,133.816839503875));
#67915=CARTESIAN_POINT('Ctrl Pts',(17.5734284332009,-3.80475120215271,133.923946010243));
#67916=CARTESIAN_POINT('Ctrl Pts',(17.5656636802538,-3.71498933114176,134.027408450286));
#67917=CARTESIAN_POINT('Ctrl Pts',(17.5579066393688,-3.62531661288664,134.130768129975));
#67918=CARTESIAN_POINT('Ctrl Pts',(17.5501495984839,-3.53123333040069,134.230490652582));
#67919=CARTESIAN_POINT('Ctrl Pts',(17.5423925575989,-3.43306934206733,134.326180879172));
#67920=CARTESIAN_POINT('Ctrl Pts',(17.5346413663587,-3.3349793799609,134.421798945018));
#67921=CARTESIAN_POINT('Ctrl Pts',(17.5268901751186,-3.23281511599657,134.513390495547));
#67922=CARTESIAN_POINT('Ctrl Pts',(17.5191389838785,-3.12694505065742,134.600595293224));
#67923=CARTESIAN_POINT('Ctrl Pts',(17.5113910871014,-3.02111998292037,134.687763026536));
#67924=CARTESIAN_POINT('Ctrl Pts',(17.5036431903243,-2.91159254763293,134.770547467268));
#67925=CARTESIAN_POINT('Ctrl Pts',(17.4958952935472,-2.79876612586406,134.848627081984));
#67926=CARTESIAN_POINT('Ctrl Pts',(17.4881490174631,-2.68596330495037,134.926690364127));
#67927=CARTESIAN_POINT('Ctrl Pts',(17.480402741379,-2.56986319144211,135.000050555438));
#67928=CARTESIAN_POINT('Ctrl Pts',(17.4726564652949,-2.45089976836731,135.068428321991));
#67929=CARTESIAN_POINT('Ctrl Pts',(17.4649101320296,-2.33193546713171,135.136806593292));
#67930=CARTESIAN_POINT('Ctrl Pts',(17.4571637987643,-2.21010815311608,135.200202171618));
#67931=CARTESIAN_POINT('Ctrl Pts',(17.449417465499,-2.08587777772356,135.25838093172));
#67932=CARTESIAN_POINT('Ctrl Pts',(17.441669397496,-1.96161958180016,135.316572720553));
#67933=CARTESIAN_POINT('Ctrl Pts',(17.433921329493,-1.83495760764034,135.36954520066));
#67934=CARTESIAN_POINT('Ctrl Pts',(17.4261732614901,-1.7063728414552,135.4171119428));
#67935=CARTESIAN_POINT('Ctrl Pts',(17.4184169587483,-1.57765141384985,135.464729239439));
#67936=CARTESIAN_POINT('Ctrl Pts',(17.4106606560064,-1.4470034792404,135.506929185431));
#67937=CARTESIAN_POINT('Ctrl Pts',(17.4029043532646,-1.31492681597713,135.543574743465));
#67938=CARTESIAN_POINT('Ctrl Pts',(17.3951439107504,-1.18277965942175,135.580239860338));
#67939=CARTESIAN_POINT('Ctrl Pts',(17.3873834682363,-1.0492026353477,135.611344593524));
#67940=CARTESIAN_POINT('Ctrl Pts',(17.3796230257221,-0.914703864275895,
135.636803054179));
#67941=CARTESIAN_POINT('Ctrl Pts',(17.3718501254566,-0.779989183836526,
135.662302383015));
#67942=CARTESIAN_POINT('Ctrl Pts',(17.3640772251912,-0.644350186620545,
135.682137270161));
#67943=CARTESIAN_POINT('Ctrl Pts',(17.3563043249258,-0.508301165183191,
135.696273636823));
#67944=CARTESIAN_POINT('Ctrl Pts',(17.3488139891637,-0.37719786836078,135.709896110949));
#67945=CARTESIAN_POINT('Ctrl Pts',(17.3413236534016,-0.245714147985853,
135.718227163212));
#67946=CARTESIAN_POINT('Ctrl Pts',(17.3338333176395,-0.114308379744584,
135.721282078889));
#67947=CARTESIAN_POINT('Ctrl Pts',(17.3260589835204,0.0220796781381341,
135.724452822623));
#67948=CARTESIAN_POINT('Ctrl Pts',(17.3182846494013,0.158815792461206,135.721949486406));
#67949=CARTESIAN_POINT('Ctrl Pts',(17.3105103152822,0.295388671702986,135.713732124707));
#67950=CARTESIAN_POINT('Ctrl Pts',(17.3027455623352,0.431793237076968,135.705524890172));
#67951=CARTESIAN_POINT('Ctrl Pts',(17.2949808093881,0.568034581130291,135.691617664942));
#67952=CARTESIAN_POINT('Ctrl Pts',(17.287216056441,0.703598945984164,135.672022436726));
#67953=CARTESIAN_POINT('Ctrl Pts',(17.279459015556,0.839028666399557,135.652446670767));
#67954=CARTESIAN_POINT('Ctrl Pts',(17.271701974671,0.973782361252646,135.627194199962));
#67955=CARTESIAN_POINT('Ctrl Pts',(17.263944933786,1.10734929245375,135.596328961264));
#67956=CARTESIAN_POINT('Ctrl Pts',(17.2561937425459,1.24081549979359,135.565486998282));
#67957=CARTESIAN_POINT('Ctrl Pts',(17.2484425513058,1.37309634543516,135.529040779876));
#67958=CARTESIAN_POINT('Ctrl Pts',(17.2406913600656,1.50368956782508,135.48710561875));
#67959=CARTESIAN_POINT('Ctrl Pts',(17.2329434632885,1.63422728461162,135.445188281186));
#67960=CARTESIAN_POINT('Ctrl Pts',(17.2251955665115,1.76307843330656,135.397786760239));
#67961=CARTESIAN_POINT('Ctrl Pts',(17.2174476697344,1.88975446140122,135.345066635149));
#67962=CARTESIAN_POINT('Ctrl Pts',(17.2097013936503,2.01640399160146,135.292357537973));
#67963=CARTESIAN_POINT('Ctrl Pts',(17.2019551175661,2.14087894547366,135.234332199678));
#67964=CARTESIAN_POINT('Ctrl Pts',(17.194208841482,2.26270973304852,135.171204755667));
#67965=CARTESIAN_POINT('Ctrl Pts',(17.1864625082166,2.38454141995092,135.108076845664));
#67966=CARTESIAN_POINT('Ctrl Pts',(17.1787161749513,2.50372855447549,135.039846934661));
#67967=CARTESIAN_POINT('Ctrl Pts',(17.170969841686,2.61982554545366,134.966775442387));
#67968=CARTESIAN_POINT('Ctrl Pts',(17.163221773683,2.73594853554753,134.893687586259));
#67969=CARTESIAN_POINT('Ctrl Pts',(17.15547370568,2.84897967424441,134.815756199567));
#67970=CARTESIAN_POINT('Ctrl Pts',(17.1477256376771,2.95850212854773,134.733285180074));
#67971=CARTESIAN_POINT('Ctrl Pts',(17.1399693349352,3.06814098461898,134.6507265094));
#67972=CARTESIAN_POINT('Ctrl Pts',(17.1322130321934,3.17426339425559,134.563618803471));
#67973=CARTESIAN_POINT('Ctrl Pts',(17.1244567294515,3.27648500273192,134.472306785297));
#67974=CARTESIAN_POINT('Ctrl Pts',(17.1166962869373,3.37876116995867,134.38094603115));
#67975=CARTESIAN_POINT('Ctrl Pts',(17.1089358444232,3.47713210723224,134.285376765761));
#67976=CARTESIAN_POINT('Ctrl Pts',(17.101175401909,3.57125090228166,134.185980060296));
#67977=CARTESIAN_POINT('Ctrl Pts',(17.0934025016436,3.66552078517624,134.086423794416));
#67978=CARTESIAN_POINT('Ctrl Pts',(17.0856296013781,3.75552462864681,133.983028105559));
#67979=CARTESIAN_POINT('Ctrl Pts',(17.0778567011127,3.84095577355102,133.876207262196));
#67980=CARTESIAN_POINT('Ctrl Pts',(17.0703663653507,3.92328128115025,133.773269625554));
#67981=CARTESIAN_POINT('Ctrl Pts',(17.0628760295886,4.00136059389691,133.667151785036));
#67982=CARTESIAN_POINT('Ctrl Pts',(17.0553856938266,4.07495880847432,133.558247647155));
#67983=CARTESIAN_POINT('Ctrl Pts',(17.0476113597075,4.1513475217268,133.445214375785));
#67984=CARTESIAN_POINT('Ctrl Pts',(17.0398370255884,4.22315060382649,133.328821295865));
#67985=CARTESIAN_POINT('Ctrl Pts',(17.0320626914693,4.29005808190938,133.209476979895));
#67986=CARTESIAN_POINT('Ctrl Pts',(17.0242979385222,4.35688310250523,133.090279745129));
#67987=CARTESIAN_POINT('Ctrl Pts',(17.0165331855752,4.41882433438697,132.968138848882));
#67988=CARTESIAN_POINT('Ctrl Pts',(17.0087684326281,4.47561416447044,132.843493009857));
#67989=CARTESIAN_POINT('Ctrl Pts',(17.0010113917431,4.53234759009423,132.718970970837));
#67990=CARTESIAN_POINT('Ctrl Pts',(16.993254350858,4.58393963482862,132.591949293637));
#67991=CARTESIAN_POINT('Ctrl Pts',(16.985497309973,4.63016802423113,132.462892236163));
#67992=CARTESIAN_POINT('Ctrl Pts',(16.9777461187329,4.67636155244552,132.333932501621));
#67993=CARTESIAN_POINT('Ctrl Pts',(16.9699949274927,4.71719934489805,132.202940808498));
#67994=CARTESIAN_POINT('Ctrl Pts',(16.9622437362526,4.75250693279576,132.070402052997));
#67995=CARTESIAN_POINT('Ctrl Pts',(16.9544958394755,4.7877995140267,131.937919630003));
#67996=CARTESIAN_POINT('Ctrl Pts',(16.9467479426985,4.81756646520682,131.803891829434));
#67997=CARTESIAN_POINT('Ctrl Pts',(16.9390000459214,4.84168301827607,131.668819183975));
#67998=CARTESIAN_POINT('Ctrl Pts',(16.9312537698373,4.8657945266823,131.533774792801));
#67999=CARTESIAN_POINT('Ctrl Pts',(16.9235074937532,4.88425791924941,131.397686376098));
#68000=CARTESIAN_POINT('Ctrl Pts',(16.9157612176691,4.89699952930785,131.261064758623));
#68001=CARTESIAN_POINT('Ctrl Pts',(16.9080148844038,4.90974123342197,131.124442132638));
#68002=CARTESIAN_POINT('Ctrl Pts',(16.9002685511384,4.91676103444208,130.987286687303));
#68003=CARTESIAN_POINT('Ctrl Pts',(16.8925222178731,4.91803717794974,130.850114074311));
#68004=CARTESIAN_POINT('Ctrl Pts',(16.8847741498701,4.9193136072409,130.712910742463));
#68005=CARTESIAN_POINT('Ctrl Pts',(16.8770260818671,4.91484381589012,130.575690626182));
#68006=CARTESIAN_POINT('Ctrl Pts',(16.8692780138641,4.90465817327578,130.438968683037));
#68007=CARTESIAN_POINT('Ctrl Pts',(16.8615217111223,4.89446170523928,130.302101430183));
#68008=CARTESIAN_POINT('Ctrl Pts',(16.8537654083804,4.87853727981489,130.165733798634));
#68009=CARTESIAN_POINT('Ctrl Pts',(16.8460091056386,4.85696716911769,130.030375488114));
#68010=CARTESIAN_POINT('Ctrl Pts',(16.8382486631244,4.83538554580289,129.894944932787));
#68011=CARTESIAN_POINT('Ctrl Pts',(16.8304882206102,4.80815231060895,129.760525154897));
#68012=CARTESIAN_POINT('Ctrl Pts',(16.822727778096,4.77540055494424,129.627613999836));
#68013=CARTESIAN_POINT('Ctrl Pts',(16.8149548778305,4.74259622325382,129.49448948399));
#68014=CARTESIAN_POINT('Ctrl Pts',(16.8071819775651,4.70425577776178,129.362878806029));
#68015=CARTESIAN_POINT('Ctrl Pts',(16.7994090772997,4.66056199750942,129.233263889204));
#68016=CARTESIAN_POINT('Ctrl Pts',(16.7919187415377,4.61845659622734,129.108360801085));
#68017=CARTESIAN_POINT('Ctrl Pts',(16.7844284057757,4.57138042731904,128.985311179079));
#68018=CARTESIAN_POINT('Ctrl Pts',(16.7769380700137,4.51953792450967,128.864525570089));
#68019=CARTESIAN_POINT('Ctrl Pts',(16.7691637358946,4.46572979744902,128.739160338023));
#68020=CARTESIAN_POINT('Ctrl Pts',(16.7613894017756,4.40661632265131,128.615837068728));
#68021=CARTESIAN_POINT('Ctrl Pts',(16.7536150676565,4.34237369582919,128.49503739457));
#68022=CARTESIAN_POINT('Ctrl Pts',(16.7458503147094,4.27821024230318,128.374386595214));
#68023=CARTESIAN_POINT('Ctrl Pts',(16.7380855617624,4.20893039591155,128.256253544686));
#68024=CARTESIAN_POINT('Ctrl Pts',(16.7303208088153,4.1347586117155,128.141100531629));
#68025=CARTESIAN_POINT('Ctrl Pts',(16.7225637679303,4.06066049598095,128.026061890167));
#68026=CARTESIAN_POINT('Ctrl Pts',(16.7148067270453,3.98168032189687,127.913997722567));
#68027=CARTESIAN_POINT('Ctrl Pts',(16.7070496861603,3.8980885380219,127.805345977348));
#68028=CARTESIAN_POINT('Ctrl Pts',(16.6992984949201,3.81455979136117,127.696776167255));
#68029=CARTESIAN_POINT('Ctrl Pts',(16.69154730368,3.72642659439786,127.591613966095));
#68030=CARTESIAN_POINT('Ctrl Pts',(16.6837961124398,3.63400259939691,127.490268257647));
#68031=CARTESIAN_POINT('Ctrl Pts',(16.6760482156627,3.54161788705958,127.388965623828));
#68032=CARTESIAN_POINT('Ctrl Pts',(16.6683003188856,3.44494626678687,127.291476544737));
#68033=CARTESIAN_POINT('Ctrl Pts',(16.6605524221085,3.34434141071926,127.19817654142));
#68034=CARTESIAN_POINT('Ctrl Pts',(16.6528061460244,3.24375759901876,127.104896054452));
#68035=CARTESIAN_POINT('Ctrl Pts',(16.6450598699404,3.13924247449838,127.015803166003));
#68036=CARTESIAN_POINT('Ctrl Pts',(16.6373135938562,3.03118598985885,126.931235967186));
#68037=CARTESIAN_POINT('Ctrl Pts',(16.6295672605909,2.92312870757075,126.846668144112));
#68038=CARTESIAN_POINT('Ctrl Pts',(16.6218209273255,2.81153032088532,126.766626318291));
#68039=CARTESIAN_POINT('Ctrl Pts',(16.6140745940602,2.69681290338204,126.691407514666));
#68040=CARTESIAN_POINT('Ctrl Pts',(16.6063265260572,2.58206979570897,126.616171866312));
#68041=CARTESIAN_POINT('Ctrl Pts',(16.5985784580542,2.46420659420051,126.545761603729));
#68042=CARTESIAN_POINT('Ctrl Pts',(16.5908303900513,2.34367296263487,126.480429523444));
#68043=CARTESIAN_POINT('Ctrl Pts',(16.5830740873094,2.22301122649107,126.415028007446));
#68044=CARTESIAN_POINT('Ctrl Pts',(16.5753177845676,2.09967373501934,126.354715641742));
#68045=CARTESIAN_POINT('Ctrl Pts',(16.5675614818258,1.97413378312091,126.299698713622));
#68046=CARTESIAN_POINT('Ctrl Pts',(16.5598010393116,1.84852682677004,126.244652421311));
#68047=CARTESIAN_POINT('Ctrl Pts',(16.5520405967974,1.72071543183442,126.19490734003));
#68048=CARTESIAN_POINT('Ctrl Pts',(16.5442801542832,1.59119038889936,126.150620593803));
#68049=CARTESIAN_POINT('Ctrl Pts',(16.5365072540178,1.46145742086669,126.106262754559));
#68050=CARTESIAN_POINT('Ctrl Pts',(16.5287343537524,1.3300056827843,126.067380871002));
#68051=CARTESIAN_POINT('Ctrl Pts',(16.520961453487,1.19733942686742,126.034081657236));
#68052=CARTESIAN_POINT('Ctrl Pts',(16.513471117725,1.06949592351978,126.001992953766));
#68053=CARTESIAN_POINT('Ctrl Pts',(16.505980781963,0.940524972385241,125.975088141586));
#68054=CARTESIAN_POINT('Ctrl Pts',(16.498490446201,0.810882479624476,125.953417135444));
#68055=CARTESIAN_POINT('Ctrl Pts',(16.4907161120819,0.676324552346135,125.930924466518));
#68056=CARTESIAN_POINT('Ctrl Pts',(16.4829417779627,0.540616916136176,125.913999067653));
#68057=CARTESIAN_POINT('Ctrl Pts',(16.4751674438436,0.404260020031606,125.902753034466));
#68058=CARTESIAN_POINT('Ctrl Pts',(16.4674026908966,0.268071171615288,125.891520861009));
#68059=CARTESIAN_POINT('Ctrl Pts',(16.4596379379496,0.131235041275635,125.885954158516));
#68060=CARTESIAN_POINT('Ctrl Pts',(16.4518731850025,-0.00573811101679774,
125.886113964888));
#68061=CARTESIAN_POINT('Ctrl Pts',(16.4441161441175,-0.14257521964339,125.886273612538));
#68062=CARTESIAN_POINT('Ctrl Pts',(16.4363591032325,-0.279548690958253,
125.892148449922));
#68063=CARTESIAN_POINT('Ctrl Pts',(16.4286020623475,-0.416143882414879,
125.903747662881));
#68064=CARTESIAN_POINT('Ctrl Pts',(16.4208508711074,-0.552636066374886,
125.915338128783));
#68065=CARTESIAN_POINT('Ctrl Pts',(16.4130996798673,-0.688750150289997,
125.932644344993));
#68066=CARTESIAN_POINT('Ctrl Pts',(16.4053484886272,-0.823972591946111,
125.955623438648));
#68067=CARTESIAN_POINT('Ctrl Pts',(16.3976005918501,-0.959137560457898,
125.978592765575));
#68068=CARTESIAN_POINT('Ctrl Pts',(16.3898526950731,-1.0934112558241,126.007230109041));
#68069=CARTESIAN_POINT('Ctrl Pts',(16.382104798296,-1.22628657312295,126.041440892956));
#68070=CARTESIAN_POINT('Ctrl Pts',(16.3743585222119,-1.3591340957697,126.075644520713));
#68071=CARTESIAN_POINT('Ctrl Pts',(16.3666122461277,-1.49058344379092,126.115419172572));
#68072=CARTESIAN_POINT('Ctrl Pts',(16.3588659700436,-1.62013939259733,126.160619516788));
#68073=CARTESIAN_POINT('Ctrl Pts',(16.3511196367782,-1.74969629775649,126.205820194663));
#68074=CARTESIAN_POINT('Ctrl Pts',(16.3433733035129,-1.87735940666773,126.256446516025));
#68075=CARTESIAN_POINT('Ctrl Pts',(16.3356269702476,-2.00265068275373,126.312303927656));
#68076=CARTESIAN_POINT('Ctrl Pts',(16.3278789022447,-2.12797001695128,126.368173848166));
#68077=CARTESIAN_POINT('Ctrl Pts',(16.3201308342417,-2.25091610436807,126.429277030862));
#68078=CARTESIAN_POINT('Ctrl Pts',(16.3123827662388,-2.37103320587095,126.495371803568));
#68079=CARTESIAN_POINT('Ctrl Pts',(16.3046264634969,-2.49127796925954,126.561536822586));
#68080=CARTESIAN_POINT('Ctrl Pts',(16.2968701607551,-2.60868739748767,126.632703840386));
#68081=CARTESIAN_POINT('Ctrl Pts',(16.2891138580132,-2.72283210776043,126.708586163882));
#68082=CARTESIAN_POINT('Ctrl Pts',(16.2813534154991,-2.83703774050189,126.784508988059));
#68083=CARTESIAN_POINT('Ctrl Pts',(16.2735929729849,-2.94797486716718,126.865151902901));
#68084=CARTESIAN_POINT('Ctrl Pts',(16.2658325304708,-3.05524601056549,126.950186921762));
#68085=CARTESIAN_POINT('Ctrl Pts',(16.2580596302054,-3.16268935512641,127.035358446385));
#68086=CARTESIAN_POINT('Ctrl Pts',(16.2502867299399,-3.26645466027605,127.124935908735));
#68087=CARTESIAN_POINT('Ctrl Pts',(16.2425138296744,-3.36617958377696,127.218552748722));
#68088=CARTESIAN_POINT('Ctrl Pts',(16.2350234939122,-3.46227925511926,127.308766380772));
#68089=CARTESIAN_POINT('Ctrl Pts',(16.22753315815,-3.55462698497167,127.402730586441));
#68090=CARTESIAN_POINT('Ctrl Pts',(16.2200428223877,-3.64293435022734,127.500088779107));
#68091=CARTESIAN_POINT('Ctrl Pts',(16.2123490717802,-3.73363987620862,127.600090925573));
#68092=CARTESIAN_POINT('Ctrl Pts',(16.2046553211726,-3.8203836463713,127.70400636712));
#68093=CARTESIAN_POINT('Ctrl Pts',(16.196961570565,-3.90280362575176,127.811484589175));
#68094=CARTESIAN_POINT('Ctrl Pts',(16.1892770144218,-3.98512510862497,127.918834368714));
#68095=CARTESIAN_POINT('Ctrl Pts',(16.1815924582786,-4.06313283469464,128.029738148571));
#68096=CARTESIAN_POINT('Ctrl Pts',(16.1739079021353,-4.13650198839578,128.143809102842));
#68097=CARTESIAN_POINT('Ctrl Pts',(16.166232029742,-4.20978823303011,128.257751153945));
#68098=CARTESIAN_POINT('Ctrl Pts',(16.1585561573487,-4.278446124117,128.374852921575));
#68099=CARTESIAN_POINT('Ctrl Pts',(16.1508802849553,-4.34219195467867,128.494695687057));
#68100=CARTESIAN_POINT('Ctrl Pts',(16.1432095053106,-4.40589549148183,128.614458939872));
#68101=CARTESIAN_POINT('Ctrl Pts',(16.1355387256659,-4.46469326139856,128.736959222908));
#68102=CARTESIAN_POINT('Ctrl Pts',(16.1278679460212,-4.51834571167189,128.86175023658));
#68103=CARTESIAN_POINT('Ctrl Pts',(16.1201999619047,-4.57197860892104,128.986495771589));
#68104=CARTESIAN_POINT('Ctrl Pts',(16.1125319777883,-4.62046975447682,129.113530012034));
#68105=CARTESIAN_POINT('Ctrl Pts',(16.1048639936718,-4.66362646419048,129.242383900389));
#68106=CARTESIAN_POINT('Ctrl Pts',(16.0981930966181,-4.70117139950928,129.354482596883));
#68107=CARTESIAN_POINT('Ctrl Pts',(16.0915221995643,-4.73467966531899,129.467957974628));
#68108=CARTESIAN_POINT('Ctrl Pts',(16.0848513025106,-4.7640545282341,129.582490119308));
#68109=CARTESIAN_POINT('Ctrl Pts',(17.8345741463799,-4.76405452823412,129.582490119309));
#68110=CARTESIAN_POINT('Ctrl Pts',(17.826246821477,-4.8005402629227,129.724747445111));
#68111=CARTESIAN_POINT('Ctrl Pts',(17.8179194965742,-4.83069182849782,129.868803123946));
#68112=CARTESIAN_POINT('Ctrl Pts',(17.8095921716714,-4.8543443026394,130.014092021497));
#68113=CARTESIAN_POINT('Ctrl Pts',(17.8012893778004,-4.87792710019173,130.158952920068));
#68114=CARTESIAN_POINT('Ctrl Pts',(17.7929865839295,-4.89504893771605,130.305039501495));
#68115=CARTESIAN_POINT('Ctrl Pts',(17.7846837900586,-4.90559544208159,130.451775278778));
#68116=CARTESIAN_POINT('Ctrl Pts',(17.7780756720458,-4.91398930883925,130.568560947318));
#68117=CARTESIAN_POINT('Ctrl Pts',(17.7714675540331,-4.91821901310473,130.685757473852));
#68118=CARTESIAN_POINT('Ctrl Pts',(17.7648594360204,-4.9182498302975,130.803068611917));
#68119=CARTESIAN_POINT('',(18.1101405639752,-4.91824863063063,130.80069049496));
#68120=CARTESIAN_POINT('Ctrl Pts',(18.1802003750167,-4.76405452823408,129.582490119308));
#68121=CARTESIAN_POINT('Ctrl Pts',(18.1724253847387,-4.79807537432806,129.71513688189));
#68122=CARTESIAN_POINT('Ctrl Pts',(18.1646503944607,-4.82651012511269,129.849041933792));
#68123=CARTESIAN_POINT('Ctrl Pts',(18.1568754041827,-4.84929797755833,129.983694919886));
#68124=CARTESIAN_POINT('Ctrl Pts',(18.1544460004281,-4.85641835871787,130.025769116546));
#68125=CARTESIAN_POINT('Ctrl Pts',(18.1520165966734,-4.86298779495552,130.067916315731));
#68126=CARTESIAN_POINT('Ctrl Pts',(18.1495871929188,-4.86900547391144,130.110120920112));
#68127=CARTESIAN_POINT('Ctrl Pts',(18.1364383166155,-4.90157548870386,130.338548624393));
#68128=CARTESIAN_POINT('Ctrl Pts',(18.1232894403121,-4.91807597667301,130.569320852748));
#68129=CARTESIAN_POINT('Ctrl Pts',(18.1101405640087,-4.91824863063019,130.80069049437));
#68130=CARTESIAN_POINT('Ctrl Pts',(18.1101405639752,-4.91824863063063,130.80069049496));
#68131=CARTESIAN_POINT('Ctrl Pts',(18.1024877344152,-4.91834911762773,130.935350856185));
#68132=CARTESIAN_POINT('Ctrl Pts',(18.0948349048551,-4.91291499953517,131.070222394372));
#68133=CARTESIAN_POINT('Ctrl Pts',(18.087182075295,-4.90192082362746,131.204804498013));
#68134=CARTESIAN_POINT('Ctrl Pts',(18.0795370510837,-4.89093786100716,131.339249337359));
#68135=CARTESIAN_POINT('Ctrl Pts',(18.0718920268724,-4.87440615162998,131.473404930247));
#68136=CARTESIAN_POINT('Ctrl Pts',(18.0642470026611,-4.85235227221648,131.606769795489));
#68137=CARTESIAN_POINT('Ctrl Pts',(18.0566078217135,-4.83031524907821,131.740032726971));
#68138=CARTESIAN_POINT('Ctrl Pts',(18.0489686407659,-4.80276451771623,131.872505736876));
#68139=CARTESIAN_POINT('Ctrl Pts',(18.0413294598183,-4.76977850556778,132.003692127335));
#68140=CARTESIAN_POINT('Ctrl Pts',(18.0336934871889,-4.73680634694948,132.134823421876));
#68141=CARTESIAN_POINT('Ctrl Pts',(18.0260575145595,-4.69840354306254,132.26466878065));
#68142=CARTESIAN_POINT('Ctrl Pts',(18.0184215419301,-4.65469960475385,132.392741759485));
#68143=CARTESIAN_POINT('Ctrl Pts',(18.0107870094105,-4.61100390880987,132.520790584337));
#68144=CARTESIAN_POINT('Ctrl Pts',(18.0031524768908,-4.56200919624942,132.647067312195));
#68145=CARTESIAN_POINT('Ctrl Pts',(17.9955179443712,-4.50789465898002,132.771101273077));
#68146=CARTESIAN_POINT('Ctrl Pts',(17.9878830865016,-4.45377781558775,132.895140519739));
#68147=CARTESIAN_POINT('Ctrl Pts',(17.9802482286319,-4.39454087526188,133.016936439758));
#68148=CARTESIAN_POINT('Ctrl Pts',(17.9726133707622,-4.33041069719544,133.136039466832));
#68149=CARTESIAN_POINT('Ctrl Pts',(17.9649764220151,-4.26626295647827,133.255175111387));
#68150=CARTESIAN_POINT('Ctrl Pts',(17.957339473268,-4.19721950497333,133.371616041812));
#68151=CARTESIAN_POINT('Ctrl Pts',(17.9497025245208,-4.12355226990168,133.484938864864));
#68152=CARTESIAN_POINT('Ctrl Pts',(17.942057511435,-4.04980724492238,133.598381352676));
#68153=CARTESIAN_POINT('Ctrl Pts',(17.9344124983492,-3.97142891044997,133.708698822479));
#68154=CARTESIAN_POINT('Ctrl Pts',(17.9267674852633,-3.88873164018912,133.815498158943));
#68155=CARTESIAN_POINT('Ctrl Pts',(17.9191178451733,-3.80598431892015,133.922362133749));
#68156=CARTESIAN_POINT('Ctrl Pts',(17.9114682050834,-3.71891311803668,134.025703429375));
#68157=CARTESIAN_POINT('Ctrl Pts',(17.9038185649934,-3.62787060720634,134.125164423856));
#68158=CARTESIAN_POINT('Ctrl Pts',(17.8961579427078,-3.53669739131641,134.22476820938));
#68159=CARTESIAN_POINT('Ctrl Pts',(17.8884973204221,-3.44154176957863,134.32048029062));
#68160=CARTESIAN_POINT('Ctrl Pts',(17.8808366981365,-3.34279104476289,134.411981868966));
#68161=CARTESIAN_POINT('Ctrl Pts',(17.8776043217929,-3.30112347587621,134.450590682482));
#68162=CARTESIAN_POINT('Ctrl Pts',(17.8743719454494,-3.25881621449291,134.488450374975));
#68163=CARTESIAN_POINT('Ctrl Pts',(17.8711395691059,-3.21589991007689,134.525539305948));
#68164=CARTESIAN_POINT('Ctrl Pts',(17.8633652349868,-3.11267997086588,134.614743566486));
#68165=CARTESIAN_POINT('Ctrl Pts',(17.8555909008677,-3.0055821364023,134.699791114984));
#68166=CARTESIAN_POINT('Ctrl Pts',(17.8478165667486,-2.89497550894862,134.780325892199));
#68167=CARTESIAN_POINT('Ctrl Pts',(17.8400518138015,-2.78450519427823,134.860761417498));
#68168=CARTESIAN_POINT('Ctrl Pts',(17.8322870608545,-2.67053500365993,134.936695009494));
#68169=CARTESIAN_POINT('Ctrl Pts',(17.8245223079074,-2.55346897761433,135.007809111703));
#68170=CARTESIAN_POINT('Ctrl Pts',(17.8167652670224,-2.43651922319598,135.078852582383));
#68171=CARTESIAN_POINT('Ctrl Pts',(17.8090082261374,-2.31648008437703,135.145085887524));
#68172=CARTESIAN_POINT('Ctrl Pts',(17.8012511852524,-2.19378631701284,135.206233475542));
#68173=CARTESIAN_POINT('Ctrl Pts',(17.7934999940123,-2.07118507397319,135.267334951688));
#68174=CARTESIAN_POINT('Ctrl Pts',(17.7857488027722,-1.94593353550228,135.323358170717));
#68175=CARTESIAN_POINT('Ctrl Pts',(17.7779976115321,-1.81849259756462,135.37407261452));
#68176=CARTESIAN_POINT('Ctrl Pts',(17.770249714755,-1.69110582542519,135.424765503331));
#68177=CARTESIAN_POINT('Ctrl Pts',(17.762501817978,-1.56153186711679,135.470153960414));
#68178=CARTESIAN_POINT('Ctrl Pts',(17.7547539212009,-1.43025301573231,135.510054973715));
#68179=CARTESIAN_POINT('Ctrl Pts',(17.7470076451168,-1.29900162505332,135.549947640584));
#68180=CARTESIAN_POINT('Ctrl Pts',(17.7392613690326,-1.16604642448024,135.584355033195));
#68181=CARTESIAN_POINT('Ctrl Pts',(17.7315150929485,-1.03188596265973,135.613143667628));
#68182=CARTESIAN_POINT('Ctrl Pts',(17.7237687596832,-0.897724510497346,
135.641932514572));
#68183=CARTESIAN_POINT('Ctrl Pts',(17.7160224264178,-0.762358161597664,
135.665102438548));
#68184=CARTESIAN_POINT('Ctrl Pts',(17.7082760931525,-0.626296389049847,
135.68257093443));
#68185=CARTESIAN_POINT('Ctrl Pts',(17.7005280251495,-0.490204146411083,
135.700043342262));
#68186=CARTESIAN_POINT('Ctrl Pts',(17.6927799571466,-0.353416557937074,
135.711811731549));
#68187=CARTESIAN_POINT('Ctrl Pts',(17.6850318891436,-0.216448563726812,
135.717845438115));
#68188=CARTESIAN_POINT('Ctrl Pts',(17.6772755864018,-0.079334998302549,
135.723885557376));
#68189=CARTESIAN_POINT('Ctrl Pts',(17.6695192836599,0.0579589646647878,
135.724178801485));
#68190=CARTESIAN_POINT('Ctrl Pts',(17.6617629809181,0.194917475952982,135.718746666715));
#68191=CARTESIAN_POINT('Ctrl Pts',(17.6540025384039,0.331949086122393,135.713311632651));
#68192=CARTESIAN_POINT('Ctrl Pts',(17.6462420958897,0.468644498382405,135.702145162569));
#68193=CARTESIAN_POINT('Ctrl Pts',(17.6384816533755,0.604493632667761,135.685320616435));
#68194=CARTESIAN_POINT('Ctrl Pts',(17.6307087531101,0.740560844043591,135.668469062046));
#68195=CARTESIAN_POINT('Ctrl Pts',(17.6229358528448,0.875778676816222,135.645941345472));
#68196=CARTESIAN_POINT('Ctrl Pts',(17.6151629525793,1.00964699307473,135.617862047074));
#68197=CARTESIAN_POINT('Ctrl Pts',(17.6076726168172,1.13864885884493,135.5908035019));
#68198=CARTESIAN_POINT('Ctrl Pts',(17.6001822810551,1.26639732263179,135.558590070608));
#68199=CARTESIAN_POINT('Ctrl Pts',(17.592691945293,1.39246056567462,135.521376266845));
#68200=CARTESIAN_POINT('Ctrl Pts',(17.5849176111739,1.52330353489222,135.482751490402));
#68201=CARTESIAN_POINT('Ctrl Pts',(17.5771432770548,1.65274544165364,135.438617326465));
#68202=CARTESIAN_POINT('Ctrl Pts',(17.5693689429357,1.78028721444383,135.389091852501));
#68203=CARTESIAN_POINT('Ctrl Pts',(17.5616041899886,1.90767180339761,135.339627414258));
#68204=CARTESIAN_POINT('Ctrl Pts',(17.5538394370415,2.03316055680117,135.284785026342));
#68205=CARTESIAN_POINT('Ctrl Pts',(17.5460746840944,2.15626791161973,135.22473297245));
#68206=CARTESIAN_POINT('Ctrl Pts',(17.5383176432094,2.27925299447797,135.164740563104));
#68207=CARTESIAN_POINT('Ctrl Pts',(17.5305606023244,2.39986103656915,135.099548955198));
#68208=CARTESIAN_POINT('Ctrl Pts',(17.5228035614394,2.51762521238051,135.029374978783));
#68209=CARTESIAN_POINT('Ctrl Pts',(17.5150523701992,2.63530058131066,134.959253921109));
#68210=CARTESIAN_POINT('Ctrl Pts',(17.5073011789592,2.75013601812175,134.884158172813));
#68211=CARTESIAN_POINT('Ctrl Pts',(17.499549987719,2.86168845587438,134.804350898056));
#68212=CARTESIAN_POINT('Ctrl Pts',(17.4918020909419,2.97319348086536,134.724577543519));
#68213=CARTESIAN_POINT('Ctrl Pts',(17.4840541941648,3.08141796476232,134.640096872397));
#68214=CARTESIAN_POINT('Ctrl Pts',(17.4763062973877,3.18594724314544,134.551215729042));
#68215=CARTESIAN_POINT('Ctrl Pts',(17.4685600213036,3.29045465625706,134.462353177706));
#68216=CARTESIAN_POINT('Ctrl Pts',(17.4608137452195,3.39126810365021,134.369092238131));
#68217=CARTESIAN_POINT('Ctrl Pts',(17.4530674691354,3.48800580380087,134.271780202092));
#68218=CARTESIAN_POINT('Ctrl Pts',(17.4453211358701,3.58474421804698,134.174467447717));
#68219=CARTESIAN_POINT('Ctrl Pts',(17.4375748026047,3.67740654938099,134.073103814479));
#68220=CARTESIAN_POINT('Ctrl Pts',(17.4298284693394,3.76564800125611,133.968073340481));
#68221=CARTESIAN_POINT('Ctrl Pts',(17.4220804013364,3.85390921419255,133.863019345637));
#68222=CARTESIAN_POINT('Ctrl Pts',(17.4143323333335,3.93774732619028,133.754297175296));
#68223=CARTESIAN_POINT('Ctrl Pts',(17.4065842653305,4.01685820090729,133.642323488413));
#68224=CARTESIAN_POINT('Ctrl Pts',(17.3988279625886,4.09605315560337,133.530230794562));
#68225=CARTESIAN_POINT('Ctrl Pts',(17.3910716598467,4.1705106107527,133.414880000754));
#68226=CARTESIAN_POINT('Ctrl Pts',(17.3833153571049,4.23996982267342,133.29671672481));
#68227=CARTESIAN_POINT('Ctrl Pts',(17.3755549145907,4.3094661070672,133.178490381568));
#68228=CARTESIAN_POINT('Ctrl Pts',(17.3677944720766,4.37395864883448,133.057448909983));
#68229=CARTESIAN_POINT('Ctrl Pts',(17.3600340295624,4.43323345705695,132.934061107713));
#68230=CARTESIAN_POINT('Ctrl Pts',(17.3522611292969,4.49260341846359,132.810475232389));
#68231=CARTESIAN_POINT('Ctrl Pts',(17.3444882290315,4.54673875398404,132.684535859031));
#68232=CARTESIAN_POINT('Ctrl Pts',(17.336715328766,4.59547393984774,132.556731106555));
#68233=CARTESIAN_POINT('Ctrl Pts',(17.3292249930041,4.64243747894838,132.433572378754));
#68234=CARTESIAN_POINT('Ctrl Pts',(17.3217346572422,4.68438657197599,132.308681831678));
#68235=CARTESIAN_POINT('Ctrl Pts',(17.3142443214802,4.72121780705052,132.182506285081));
#68236=CARTESIAN_POINT('Ctrl Pts',(17.3064699873611,4.75944550959783,132.051546754283));
#68237=CARTESIAN_POINT('Ctrl Pts',(17.298695653242,4.79228069993176,131.918788018494));
#68238=CARTESIAN_POINT('Ctrl Pts',(17.2909213191229,4.81955295962598,131.784713784471));
#68239=CARTESIAN_POINT('Ctrl Pts',(17.2831565661759,4.84679160869744,131.650804784959));
#68240=CARTESIAN_POINT('Ctrl Pts',(17.2753918132288,4.86848089097449,131.515583892426));
#68241=CARTESIAN_POINT('Ctrl Pts',(17.2676270602817,4.88449992961611,131.379550586255));
#68242=CARTESIAN_POINT('Ctrl Pts',(17.2598700193967,4.90050305792272,131.243652390281));
#68243=CARTESIAN_POINT('Ctrl Pts',(17.2521129785118,4.91084710463466,131.106943772206));
#68244=CARTESIAN_POINT('Ctrl Pts',(17.2443559376268,4.91546216442233,130.969934687494));
#68245=CARTESIAN_POINT('Ctrl Pts',(17.2366047463867,4.9200737439575,130.833028922399));
#68246=CARTESIAN_POINT('Ctrl Pts',(17.2288535551466,4.91896492270234,130.695823530833));
#68247=CARTESIAN_POINT('Ctrl Pts',(17.2211023639065,4.91211761961487,130.558833524216));
#68248=CARTESIAN_POINT('Ctrl Pts',(17.2133544671294,4.90527322681385,130.421901742005));
#68249=CARTESIAN_POINT('Ctrl Pts',(17.2056065703523,4.8926952226579,130.285185552329));
#68250=CARTESIAN_POINT('Ctrl Pts',(17.1978586735752,4.8744176277446,130.149199680977));
#68251=CARTESIAN_POINT('Ctrl Pts',(17.1901123974911,4.85614385611008,130.013242254937));
#68252=CARTESIAN_POINT('Ctrl Pts',(17.182366121407,4.83217291717957,129.878015230594));
#68253=CARTESIAN_POINT('Ctrl Pts',(17.1746198453229,4.80259063512115,129.744027531245));
#68254=CARTESIAN_POINT('Ctrl Pts',(17.1668735120575,4.77300813469308,129.61003884283));
#68255=CARTESIAN_POINT('Ctrl Pts',(17.1591271787923,4.737814292772,129.477289879435));
#68256=CARTESIAN_POINT('Ctrl Pts',(17.1513808455269,4.69714584053573,129.346278310137));
#68257=CARTESIAN_POINT('Ctrl Pts',(17.143632777524,4.65646828088173,129.215237401706));
#68258=CARTESIAN_POINT('Ctrl Pts',(17.135884709521,4.61031378719728,129.085935034909));
#68259=CARTESIAN_POINT('Ctrl Pts',(17.128136641518,4.55886851333777,128.958852302603));
#68260=CARTESIAN_POINT('Ctrl Pts',(17.1203803387762,4.50736856282885,128.831634505257));
#68261=CARTESIAN_POINT('Ctrl Pts',(17.1126240360344,4.45056674632708,128.706641417842));
#68262=CARTESIAN_POINT('Ctrl Pts',(17.1048677332925,4.38869703639658,128.58433327872));
#68263=CARTESIAN_POINT('Ctrl Pts',(17.0971072907783,4.32679430473895,128.461959860061));
#68264=CARTESIAN_POINT('Ctrl Pts',(17.0893468482642,4.25981848076507,128.342274586155));
#68265=CARTESIAN_POINT('Ctrl Pts',(17.08158640575,4.1880483099035,128.225710890206));
#68266=CARTESIAN_POINT('Ctrl Pts',(17.0738135054846,4.1161629271922,128.108960075864));
#68267=CARTESIAN_POINT('Ctrl Pts',(17.0660406052191,4.03946803677542,127.995341177358));
#68268=CARTESIAN_POINT('Ctrl Pts',(17.0582677049537,3.95828483728186,127.885257294721));
#68269=CARTESIAN_POINT('Ctrl Pts',(17.0507773691915,3.88005285157638,127.7791752385));
#68270=CARTESIAN_POINT('Ctrl Pts',(17.0432870334293,3.79765340667968,127.676375887157));
#68271=CARTESIAN_POINT('Ctrl Pts',(17.0357966976671,3.71140652805818,127.577187761026));
#68272=CARTESIAN_POINT('Ctrl Pts',(17.028022363548,3.62188957282146,127.474238886948));
#68273=CARTESIAN_POINT('Ctrl Pts',(17.020248029429,3.52794411089937,127.374854371873));
#68274=CARTESIAN_POINT('Ctrl Pts',(17.0124736953099,3.4298849831627,127.279439048967));
#68275=CARTESIAN_POINT('Ctrl Pts',(17.0047089423628,3.33194670453718,127.184141316919));
#68276=CARTESIAN_POINT('Ctrl Pts',(16.9969441894157,3.22990512485546,127.092803314099));
#68277=CARTESIAN_POINT('Ctrl Pts',(16.9891794364686,3.12411513338199,127.005796718423));
#68278=CARTESIAN_POINT('Ctrl Pts',(16.9814223955835,3.01843021401929,126.918876538924));
#68279=CARTESIAN_POINT('Ctrl Pts',(16.9736653546985,2.90900459175828,126.836279452103));
#68280=CARTESIAN_POINT('Ctrl Pts',(16.9659083138135,2.79622952103531,126.758339914679));
#68281=CARTESIAN_POINT('Ctrl Pts',(16.9581571225733,2.68353949486998,126.680459152066));
#68282=CARTESIAN_POINT('Ctrl Pts',(16.9504059313332,2.56750536811216,126.607229169221));
#68283=CARTESIAN_POINT('Ctrl Pts',(16.942654740093,2.44855066121156,126.53894355449));
#68284=CARTESIAN_POINT('Ctrl Pts',(16.9349068433159,2.3296465132351,126.470686962967));
#68285=CARTESIAN_POINT('Ctrl Pts',(16.9271589465388,2.20782459237548,126.407370754093));
#68286=CARTESIAN_POINT('Ctrl Pts',(16.9194110497617,2.08353634098049,126.349244527236));
#68287=CARTESIAN_POINT('Ctrl Pts',(16.9116647736776,1.95927408800835,126.291130459134));
#68288=CARTESIAN_POINT('Ctrl Pts',(16.9039184975935,1.8325468845856,126.238204379187));
#68289=CARTESIAN_POINT('Ctrl Pts',(16.8961722215094,1.70382929235474,126.190669166568));
#68290=CARTESIAN_POINT('Ctrl Pts',(16.8884258882441,1.57511074996057,126.143133603054));
#68291=CARTESIAN_POINT('Ctrl Pts',(16.8806795549787,1.4444021561953,126.100989121716));
#68292=CARTESIAN_POINT('Ctrl Pts',(16.8729332217134,1.31219612068867,126.064389689032));
#68293=CARTESIAN_POINT('Ctrl Pts',(16.8651851537104,1.17996047855685,126.027782060158));
#68294=CARTESIAN_POINT('Ctrl Pts',(16.8574370857075,1.0462271041137,125.996722055219));
#68295=CARTESIAN_POINT('Ctrl Pts',(16.8496890177045,0.911501375113033,125.971313100143));
#68296=CARTESIAN_POINT('Ctrl Pts',(16.8419327149626,0.776632458003775,125.945877140128));
#68297=CARTESIAN_POINT('Ctrl Pts',(16.8341764122207,0.640769464292466,125.926104300189));
#68298=CARTESIAN_POINT('Ctrl Pts',(16.8264201094789,0.504426073432944,125.912046502657));
#68299=CARTESIAN_POINT('Ctrl Pts',(16.8186596669647,0.368009912000501,125.897981202055));
#68300=CARTESIAN_POINT('Ctrl Pts',(16.8108992244505,0.23111323256635,125.889637045597));
#68301=CARTESIAN_POINT('Ctrl Pts',(16.8031387819363,0.0942513634745103,
125.887013798093));
#68302=CARTESIAN_POINT('Ctrl Pts',(16.7953658816709,-0.042830208439435,
125.884386339519));
#68303=CARTESIAN_POINT('Ctrl Pts',(16.7875929814055,-0.179876467254304,
125.887498133001));
#68304=CARTESIAN_POINT('Ctrl Pts',(16.77982008114,-0.316374657790517,125.896296830449));
#68305=CARTESIAN_POINT('Ctrl Pts',(16.7723297453781,-0.447910795280879,
125.904775673083));
#68306=CARTESIAN_POINT('Ctrl Pts',(16.7648394096162,-0.578937713675355,
125.918535099333));
#68307=CARTESIAN_POINT('Ctrl Pts',(16.7573490738542,-0.709006037930606,
125.937483435976));
#68308=CARTESIAN_POINT('Ctrl Pts',(16.7495747397352,-0.844005942235119,
125.957150204563));
#68309=CARTESIAN_POINT('Ctrl Pts',(16.7418004056161,-0.978400766397726,
125.982469424352));
#68310=CARTESIAN_POINT('Ctrl Pts',(16.734026071497,-1.11167973362992,126.013395033017));
#68311=CARTESIAN_POINT('Ctrl Pts',(16.7262613185499,-1.24479444644594,126.044282528632));
#68312=CARTESIAN_POINT('Ctrl Pts',(16.7184965656028,-1.37679566136668,126.080762578007));
#68313=CARTESIAN_POINT('Ctrl Pts',(16.7107318126558,-1.50717884891897,126.122737503744));
#68314=CARTESIAN_POINT('Ctrl Pts',(16.7029747717708,-1.63743253805147,126.164670739394));
#68315=CARTESIAN_POINT('Ctrl Pts',(16.6952177308858,-1.76607102816584,126.212087871524));
#68316=CARTESIAN_POINT('Ctrl Pts',(16.6874606900008,-1.89260144877294,126.264840508722));
#68317=CARTESIAN_POINT('Ctrl Pts',(16.6797094987607,-2.01903645180526,126.317553364745));
#68318=CARTESIAN_POINT('Ctrl Pts',(16.6719583075206,-2.14336619015607,126.375593567374));
#68319=CARTESIAN_POINT('Ctrl Pts',(16.6642071162805,-2.26511473648712,126.43876348853));
#68320=CARTESIAN_POINT('Ctrl Pts',(16.6564592195034,-2.38681153643872,126.501906560785));
#68321=CARTESIAN_POINT('Ctrl Pts',(16.6487113227264,-2.50592898006322,126.570174835499));
#68322=CARTESIAN_POINT('Ctrl Pts',(16.6409634259493,-2.62201305672604,126.643323415995));
#68323=CARTESIAN_POINT('Ctrl Pts',(16.6332171498652,-2.73807285110251,126.716456695385));
#68324=CARTESIAN_POINT('Ctrl Pts',(16.6254708737811,-2.85110021003967,126.794468041723));
#68325=CARTESIAN_POINT('Ctrl Pts',(16.617724597697,-2.96066793338639,126.877067854005));
#68326=CARTESIAN_POINT('Ctrl Pts',(16.6099782644316,-3.0702364655376,126.959668276021));
#68327=CARTESIAN_POINT('Ctrl Pts',(16.6022319311663,-3.17634499894735,127.046856996216));
#68328=CARTESIAN_POINT('Ctrl Pts',(16.5944855979009,-3.27859772971845,127.138302790801));
#68329=CARTESIAN_POINT('Ctrl Pts',(16.5867375298979,-3.38087335927908,127.229769064037));
#68330=CARTESIAN_POINT('Ctrl Pts',(16.578989461895,-3.47929117660609,127.325494048129));
#68331=CARTESIAN_POINT('Ctrl Pts',(16.571241393892,-3.57349099751393,127.425108458702));
#68332=CARTESIAN_POINT('Ctrl Pts',(16.5634850911501,-3.66779093511267,127.524828740656));
#68333=CARTESIAN_POINT('Ctrl Pts',(16.5557287884083,-3.75786365208871,127.628446422139));
#68334=CARTESIAN_POINT('Ctrl Pts',(16.5479724856665,-3.84338780842195,127.735557395368));
#68335=CARTESIAN_POINT('Ctrl Pts',(16.5402120431523,-3.92895761157227,127.842725536948));
#68336=CARTESIAN_POINT('Ctrl Pts',(16.5324516006381,-4.00997378584083,127.953390370087));
#68337=CARTESIAN_POINT('Ctrl Pts',(16.524691158124,-4.0861579815411,128.067118207331));
#68338=CARTESIAN_POINT('Ctrl Pts',(16.5169182578585,-4.16246447487574,128.181028610596));
#68339=CARTESIAN_POINT('Ctrl Pts',(16.5091453575931,-4.23392328531967,128.298011509875));
#68340=CARTESIAN_POINT('Ctrl Pts',(16.5013724573277,-4.300301298103,128.417607214293));
#68341=CARTESIAN_POINT('Ctrl Pts',(16.4938821215656,-4.36426630292633,128.532855313614));
#68342=CARTESIAN_POINT('Ctrl Pts',(16.4863917858034,-4.42351335783911,128.650529276918));
#68343=CARTESIAN_POINT('Ctrl Pts',(16.4789014500413,-4.47787669193268,128.770201480638));
#68344=CARTESIAN_POINT('Ctrl Pts',(16.4704079154249,-4.5395210393493,128.905901673153));
#68345=CARTESIAN_POINT('Ctrl Pts',(16.4619143808085,-4.59505545712627,129.044543350627));
#68346=CARTESIAN_POINT('Ctrl Pts',(16.4534208461921,-4.64421539216793,129.185581307823));
#68347=CARTESIAN_POINT('Ctrl Pts',(16.4455676629748,-4.68966902181364,129.315986017817));
#68348=CARTESIAN_POINT('Ctrl Pts',(16.4377144797573,-4.72967346533817,129.448438876883));
#68349=CARTESIAN_POINT('Ctrl Pts',(16.4298612965399,-4.76405452823409,129.582490119308));
#68350=CARTESIAN_POINT('Origin',(213.235140564004,0.,130.804360617566));
#68351=CARTESIAN_POINT('',(14.334952816073,-4.76405452823406,129.582490119308));
#68352=CARTESIAN_POINT('',(14.6800959310997,-4.76405452823407,129.582490119308));
#68353=CARTESIAN_POINT('',(213.235140564004,-4.76405452823405,129.582490119308));
#68354=CARTESIAN_POINT('',(16.0148594359499,-4.91824793335368,130.808869338258));
#68355=CARTESIAN_POINT('Ctrl Pts',(16.0148594359499,-4.91824793335368,130.808869338258));
#68356=CARTESIAN_POINT('Ctrl Pts',(16.0050887965409,-4.91808964415007,130.981535955167));
#68357=CARTESIAN_POINT('Ctrl Pts',(15.9953181571318,-4.90883501695725,131.153795784248));
#68358=CARTESIAN_POINT('Ctrl Pts',(15.9855475177229,-4.89063364109632,131.324827380267));
#68359=CARTESIAN_POINT('Ctrl Pts',(15.9755880421458,-4.87208048906916,131.499164486794));
#68360=CARTESIAN_POINT('Ctrl Pts',(15.9656285665686,-4.84423143683517,131.672225602518));
#68361=CARTESIAN_POINT('Ctrl Pts',(15.9556690909914,-4.80729321664908,131.843165215005));
#68362=CARTESIAN_POINT('Ctrl Pts',(15.9509777935192,-4.78989388897932,131.923684371434));
#68363=CARTESIAN_POINT('Ctrl Pts',(15.9462864960471,-4.77047856592294,132.003733145737));
#68364=CARTESIAN_POINT('Ctrl Pts',(15.9415951985749,-4.74907247945354,132.08322481966));
#68365=CARTESIAN_POINT('Ctrl Pts',(15.9338208644558,-4.71359869647948,132.214956997469));
#68366=CARTESIAN_POINT('Ctrl Pts',(15.9260465303367,-4.67258349094273,132.345420726402));
#68367=CARTESIAN_POINT('Ctrl Pts',(15.9182721962176,-4.62613292996776,132.474114245131));
#68368=CARTESIAN_POINT('Ctrl Pts',(15.9105074432705,-4.57973961515778,132.6026491606));
#68369=CARTESIAN_POINT('Ctrl Pts',(15.9027426903235,-4.52792440456582,132.729417842436));
#68370=CARTESIAN_POINT('Ctrl Pts',(15.8949779373764,-4.47084388125271,132.85393082909));
#68371=CARTESIAN_POINT('Ctrl Pts',(15.8872208964914,-4.41382005112021,132.978320147689));
#68372=CARTESIAN_POINT('Ctrl Pts',(15.8794638556063,-4.35154147724408,133.100457876481));
#68373=CARTESIAN_POINT('Ctrl Pts',(15.8717068147214,-4.28421372470851,133.219872121062));
#68374=CARTESIAN_POINT('Ctrl Pts',(15.8639556234813,-4.21693674455496,133.339196314432));
#68375=CARTESIAN_POINT('Ctrl Pts',(15.8562044322412,-4.14461835582714,133.455800772371));
#68376=CARTESIAN_POINT('Ctrl Pts',(15.8484532410011,-4.06751101451575,133.569236240319));
#68377=CARTESIAN_POINT('Ctrl Pts',(15.840705344224,-3.9904364458811,133.682623495167));
#68378=CARTESIAN_POINT('Ctrl Pts',(15.832957447447,-3.90857719231051,133.792844116254));
#68379=CARTESIAN_POINT('Ctrl Pts',(15.8252095506699,-3.82223005899156,133.899476195156));
#68380=CARTESIAN_POINT('Ctrl Pts',(15.8174632745858,-3.73590098763136,134.006085968926));
#68381=CARTESIAN_POINT('Ctrl Pts',(15.8097169985016,-3.64508614966657,134.109108389938));
#68382=CARTESIAN_POINT('Ctrl Pts',(15.8019707224175,-3.55012357515833,134.208153452567));
#68383=CARTESIAN_POINT('Ctrl Pts',(15.7942243891522,-3.45516029965794,134.307199246324));
#68384=CARTESIAN_POINT('Ctrl Pts',(15.7864780558868,-3.35604949709565,134.402267340904));
#68385=CARTESIAN_POINT('Ctrl Pts',(15.7787317226215,-3.25316682081566,134.493003823197));
#68386=CARTESIAN_POINT('Ctrl Pts',(15.7709836546185,-3.15026110467366,134.583760625295));
#68387=CARTESIAN_POINT('Ctrl Pts',(15.7632355866155,-3.04358212715293,134.670183626296));
#68388=CARTESIAN_POINT('Ctrl Pts',(15.7554875186125,-2.93353912878493,134.751958778776));
#68389=CARTESIAN_POINT('Ctrl Pts',(15.7477312158707,-2.82337917540874,134.833820842861));
#68390=CARTESIAN_POINT('Ctrl Pts',(15.7399749131288,-2.70984837340149,134.911024957097));
#68391=CARTESIAN_POINT('Ctrl Pts',(15.732218610387,-2.59338595512761,134.983299759292));
#68392=CARTESIAN_POINT('Ctrl Pts',(15.7244581678728,-2.47686137735449,135.055613136724));
#68393=CARTESIAN_POINT('Ctrl Pts',(15.7166977253586,-2.35740240589971,135.122991767803));
#68394=CARTESIAN_POINT('Ctrl Pts',(15.7089372828445,-2.23547256822738,135.185210473382));
#68395=CARTESIAN_POINT('Ctrl Pts',(15.701164382579,-2.11334699795519,135.247529057951));
#68396=CARTESIAN_POINT('Ctrl Pts',(15.6933914823136,-1.98874299080975,135.30467100154));
#68397=CARTESIAN_POINT('Ctrl Pts',(15.6856185820482,-1.8621445530286,135.356459114537));
#68398=CARTESIAN_POINT('Ctrl Pts',(15.6781282462862,-1.74014828734301,135.406364599181));
#68399=CARTESIAN_POINT('Ctrl Pts',(15.6706379105241,-1.61630036822402,135.451298640675));
#68400=CARTESIAN_POINT('Ctrl Pts',(15.6631475747621,-1.49104500515247,135.491147134478));
#68401=CARTESIAN_POINT('Ctrl Pts',(15.655373240643,-1.3610405469197,135.532506496036));
#68402=CARTESIAN_POINT('Ctrl Pts',(15.647598906524,-1.22910799639871,135.568518074249));
#68403=CARTESIAN_POINT('Ctrl Pts',(15.6398245724049,-1.09572683147738,135.598999892139));
#68404=CARTESIAN_POINT('Ctrl Pts',(15.6320598194578,-0.962510046921385,
135.629444143913));
#68405=CARTESIAN_POINT('Ctrl Pts',(15.6242950665107,-0.827848577635766,
135.654372108789));
#68406=CARTESIAN_POINT('Ctrl Pts',(15.6165303135637,-0.692238858453363,
135.673650958606));
#68407=CARTESIAN_POINT('Ctrl Pts',(15.6087732726787,-0.55676382875563,135.692910660398));
#68408=CARTESIAN_POINT('Ctrl Pts',(15.6010162317937,-0.42034280798432,135.706532358167));
#68409=CARTESIAN_POINT('Ctrl Pts',(15.5932591909087,-0.283483927213691,
135.714433929189));
#68410=CARTESIAN_POINT('Ctrl Pts',(15.5855079996685,-0.146728252789657,
135.722329541575));
#68411=CARTESIAN_POINT('Ctrl Pts',(15.5777568084284,-0.0095357643326108,
135.724513590713));
#68412=CARTESIAN_POINT('Ctrl Pts',(15.5700056171883,0.127579108941926,135.720955641916));
#68413=CARTESIAN_POINT('Ctrl Pts',(15.5622577204112,0.264635704737663,135.717399205341));
#68414=CARTESIAN_POINT('Ctrl Pts',(15.5545098236341,0.401614360947145,135.708105634924));
#68415=CARTESIAN_POINT('Ctrl Pts',(15.5467619268571,0.537999683609464,135.693096589465));
#68416=CARTESIAN_POINT('Ctrl Pts',(15.539015650773,0.674356477402409,135.678090683574));
#68417=CARTESIAN_POINT('Ctrl Pts',(15.5312693746889,0.810119796142087,135.657371723404));
#68418=CARTESIAN_POINT('Ctrl Pts',(15.5235230986048,0.944778803545363,135.631013295652));
#68419=CARTESIAN_POINT('Ctrl Pts',(15.5157767653395,1.07943880497084,135.604654673327));
#68420=CARTESIAN_POINT('Ctrl Pts',(15.5080304320742,1.21299409510976,135.572656575456));
#68421=CARTESIAN_POINT('Ctrl Pts',(15.5002840988088,1.34494386703139,135.535143751153));
#68422=CARTESIAN_POINT('Ctrl Pts',(15.4925360308058,1.47692318818957,135.497622526114));
#68423=CARTESIAN_POINT('Ctrl Pts',(15.4847879628029,1.60729589968721,135.454584224061));
#68424=CARTESIAN_POINT('Ctrl Pts',(15.4770398947999,1.73557658002847,135.406203400339));
#68425=CARTESIAN_POINT('Ctrl Pts',(15.4692835920581,1.86399359860336,135.357771156901));
#68426=CARTESIAN_POINT('Ctrl Pts',(15.4615272893162,1.99031377807332,135.303985187373));
#68427=CARTESIAN_POINT('Ctrl Pts',(15.4537709865743,2.11407139791809,135.245068352489));
#68428=CARTESIAN_POINT('Ctrl Pts',(15.4460105440602,2.23789507093084,135.186120071916));
#68429=CARTESIAN_POINT('Ctrl Pts',(15.438250101546,2.35915311353804,135.12203565189));
#68430=CARTESIAN_POINT('Ctrl Pts',(15.4304896590318,2.47740552823067,135.053083356366));
#68431=CARTESIAN_POINT('Ctrl Pts',(15.4227167587664,2.59584777219731,134.984020372495));
#68432=CARTESIAN_POINT('Ctrl Pts',(15.414943858501,2.71127441716679,134.910074108594));
#68433=CARTESIAN_POINT('Ctrl Pts',(15.4071709582356,2.82327477130643,134.831555997505));
#68434=CARTESIAN_POINT('Ctrl Pts',(15.3996806224735,2.93120363046228,134.755892217529));
#68435=CARTESIAN_POINT('Ctrl Pts',(15.3921902867114,3.03595073760808,134.675983402621));
#68436=CARTESIAN_POINT('Ctrl Pts',(15.3846999509493,3.13717998728614,134.592141602506));
#68437=CARTESIAN_POINT('Ctrl Pts',(15.3769256168302,3.24224737473282,134.505120915057));
#68438=CARTESIAN_POINT('Ctrl Pts',(15.3691512827111,3.34385770157291,134.413587461436));
#68439=CARTESIAN_POINT('Ctrl Pts',(15.361376948592,3.4415986959103,134.317846276966));
#68440=CARTESIAN_POINT('Ctrl Pts',(15.3536121956449,3.53921923320752,134.222223084949));
#68441=CARTESIAN_POINT('Ctrl Pts',(15.3458474426978,3.63297964949225,134.122402750943));
#68442=CARTESIAN_POINT('Ctrl Pts',(15.3380826897507,3.72249985751884,134.018731142766));
#68443=CARTESIAN_POINT('Ctrl Pts',(15.3303256488657,3.81193115281268,133.915162502692));
#68444=CARTESIAN_POINT('Ctrl Pts',(15.3225686079807,3.89713036692762,133.807750494645));
#68445=CARTESIAN_POINT('Ctrl Pts',(15.3148115670957,3.97775375043304,133.696878234352));
#68446=CARTESIAN_POINT('Ctrl Pts',(15.3070603758556,4.05831633521779,133.586089583692));
#68447=CARTESIAN_POINT('Ctrl Pts',(15.2993091846155,4.13430972873748,133.471846189568));
#68448=CARTESIAN_POINT('Ctrl Pts',(15.2915579933754,4.20543026386955,133.354564405154));
#68449=CARTESIAN_POINT('Ctrl Pts',(15.2838100965983,4.27652057087708,133.237332468627));
#68450=CARTESIAN_POINT('Ctrl Pts',(15.2760621998212,4.34274193644835,133.117065043902));
#68451=CARTESIAN_POINT('Ctrl Pts',(15.2683143030441,4.40383399972079,132.994207453626));
#68452=CARTESIAN_POINT('Ctrl Pts',(15.26056802696,4.4649132838506,132.871375562509));
#68453=CARTESIAN_POINT('Ctrl Pts',(15.2528217508759,4.52086522585035,132.745954933376));
#68454=CARTESIAN_POINT('Ctrl Pts',(15.2450754747918,4.57147561680339,132.618415122666));
#68455=CARTESIAN_POINT('Ctrl Pts',(15.2373291415264,4.62208638135077,132.490874370485));
#68456=CARTESIAN_POINT('Ctrl Pts',(15.229582808261,4.66735537196735,132.361214768913));
#68457=CARTESIAN_POINT('Ctrl Pts',(15.2218364749957,4.70711684523941,132.229925090946));
#68458=CARTESIAN_POINT('Ctrl Pts',(15.2140884069927,4.74688722281772,132.098606011567));
#68459=CARTESIAN_POINT('Ctrl Pts',(15.2063403389898,4.78114751548703,131.965656503508));
#68460=CARTESIAN_POINT('Ctrl Pts',(15.1985922709868,4.80978219942763,131.83157931705));
#68461=CARTESIAN_POINT('Ctrl Pts',(15.190835968245,4.83844731665112,131.697359631762));
#68462=CARTESIAN_POINT('Ctrl Pts',(15.1830796655031,4.86147479973481,131.562010256876));
#68463=CARTESIAN_POINT('Ctrl Pts',(15.1753233627613,4.87880041440905,131.426043477923));
#68464=CARTESIAN_POINT('Ctrl Pts',(15.1675629202471,4.89613527628551,131.290004129407));
#68465=CARTESIAN_POINT('Ctrl Pts',(15.1598024777329,4.9077621726739,131.153347109582));
#68466=CARTESIAN_POINT('Ctrl Pts',(15.1520420352187,4.91366897223597,131.016587604035));
#68467=CARTESIAN_POINT('Ctrl Pts',(15.1442691349533,4.91958525391707,130.879608559988));
#68468=CARTESIAN_POINT('Ctrl Pts',(15.1364962346879,4.91976308888877,130.742527092646));
#68469=CARTESIAN_POINT('Ctrl Pts',(15.1287233344224,4.91424250545409,130.605857065738));
#68470=CARTESIAN_POINT('Ctrl Pts',(15.1212329986604,4.90892260913278,130.47415533856));
#68471=CARTESIAN_POINT('Ctrl Pts',(15.1137426628984,4.89831143001804,130.342835964388));
#68472=CARTESIAN_POINT('Ctrl Pts',(15.1062523271364,4.88248983117134,130.212350388762));
#68473=CARTESIAN_POINT('Ctrl Pts',(15.0984779930173,4.86606835159545,130.076917412876));
#68474=CARTESIAN_POINT('Ctrl Pts',(15.0907036588982,4.84398152832882,129.94195369964));
#68475=CARTESIAN_POINT('Ctrl Pts',(15.0829293247791,4.81626315319903,129.807970984121));
#68476=CARTESIAN_POINT('Ctrl Pts',(15.075164571832,4.78857893848932,129.674153390324));
#68477=CARTESIAN_POINT('Ctrl Pts',(15.0673998188849,4.75527705965809,129.541314767893));
#68478=CARTESIAN_POINT('Ctrl Pts',(15.0596350659378,4.71644305865732,129.409961844997));
#68479=CARTESIAN_POINT('Ctrl Pts',(15.0518780250528,4.67764762813387,129.278739383675));
#68480=CARTESIAN_POINT('Ctrl Pts',(15.0441209841679,4.63333112003381,129.14900005784));
#68481=CARTESIAN_POINT('Ctrl Pts',(15.0363639432829,4.58363005550378,129.02124015703));
#68482=CARTESIAN_POINT('Ctrl Pts',(15.0286127520428,4.53396647093312,128.893576600955));
#68483=CARTESIAN_POINT('Ctrl Pts',(15.0208615608026,4.47892655335453,128.767889861668));
#68484=CARTESIAN_POINT('Ctrl Pts',(15.0131103695625,4.41869645298907,128.644660471981));
#68485=CARTESIAN_POINT('Ctrl Pts',(15.0053624727854,4.35849195202295,128.521483458071));
#68486=CARTESIAN_POINT('Ctrl Pts',(14.9976145760083,4.29310182708948,128.400762066971));
#68487=CARTESIAN_POINT('Ctrl Pts',(14.9898666792312,4.22276000933783,128.282956055415));
#68488=CARTESIAN_POINT('Ctrl Pts',(14.9821204031471,4.15243290557807,128.165174686337));
#68489=CARTESIAN_POINT('Ctrl Pts',(14.974374127063,4.07715636954441,128.050307819276));
#68490=CARTESIAN_POINT('Ctrl Pts',(14.9666278509789,3.99720966721641,127.938789480984));
#68491=CARTESIAN_POINT('Ctrl Pts',(14.9588815177135,3.91726237474002,127.82727031949));
#68492=CARTESIAN_POINT('Ctrl Pts',(14.9511351844482,3.83264507497081,127.719100053837));
#68493=CARTESIAN_POINT('Ctrl Pts',(14.9433888511829,3.74367939811231,127.614682322401));
#68494=CARTESIAN_POINT('Ctrl Pts',(14.9356407831799,3.65469379800732,127.510241207337));
#68495=CARTESIAN_POINT('Ctrl Pts',(14.927892715177,3.56135813659362,127.409554596234));
#68496=CARTESIAN_POINT('Ctrl Pts',(14.920144647174,3.4640329484743,127.312991431361));
#68497=CARTESIAN_POINT('Ctrl Pts',(14.9123883444322,3.36660432198686,127.216325638006));
#68498=CARTESIAN_POINT('Ctrl Pts',(14.9046320416903,3.26517797668552,127.123792321097));
#68499=CARTESIAN_POINT('Ctrl Pts',(14.8968757389485,3.16015019270701,127.035722425588));
#68500=CARTESIAN_POINT('Ctrl Pts',(14.8891152964343,3.05506635223773,126.947605524524));
#68501=CARTESIAN_POINT('Ctrl Pts',(14.8813548539201,2.94637755263178,126.863957030053));
#68502=CARTESIAN_POINT('Ctrl Pts',(14.8735944114059,2.8345106768289,126.785065619007));
#68503=CARTESIAN_POINT('Ctrl Pts',(14.8658215111405,2.72246422238591,126.706047564464));
#68504=CARTESIAN_POINT('Ctrl Pts',(14.8580486108751,2.60722982570853,126.631802065367));
#68505=CARTESIAN_POINT('Ctrl Pts',(14.8502757106096,2.48926145118047,126.562573200667));
#68506=CARTESIAN_POINT('Ctrl Pts',(14.8427853748476,2.3755815242106,126.495860979575));
#68507=CARTESIAN_POINT('Ctrl Pts',(14.8352950390855,2.25936321405745,126.433807135694));
#68508=CARTESIAN_POINT('Ctrl Pts',(14.8278047033235,2.14103004309853,126.376587653982));
#68509=CARTESIAN_POINT('Ctrl Pts',(14.8200303692044,2.01821023399662,126.317198678228));
#68510=CARTESIAN_POINT('Ctrl Pts',(14.8122560350853,1.8927229722042,126.262829764498));
#68511=CARTESIAN_POINT('Ctrl Pts',(14.8044817009662,1.7650170602338,126.213729088072));
#68512=CARTESIAN_POINT('Ctrl Pts',(14.7967169480191,1.63746853438632,126.164688923842));
#68513=CARTESIAN_POINT('Ctrl Pts',(14.788952195072,1.50770716019783,126.120904217473));
#68514=CARTESIAN_POINT('Ctrl Pts',(14.7811874421249,1.37620549994302,126.082576899052));
#68515=CARTESIAN_POINT('Ctrl Pts',(14.7734304012399,1.24483444899121,126.044287647864));
#68516=CARTESIAN_POINT('Ctrl Pts',(14.7656733603549,1.11172692463833,126.011445106564));
#68517=CARTESIAN_POINT('Ctrl Pts',(14.7579163194699,0.977374262343983,125.984202672663));
#68518=CARTESIAN_POINT('Ctrl Pts',(14.7501651282298,0.8431229164372,125.956980782494));
#68519=CARTESIAN_POINT('Ctrl Pts',(14.7424139369897,0.707628683165423,125.935350671311));
#68520=CARTESIAN_POINT('Ctrl Pts',(14.7346627457496,0.571396467134131,125.919415465382));
#68521=CARTESIAN_POINT('Ctrl Pts',(14.7269148489725,0.435222153428951,125.903487032341));
#68522=CARTESIAN_POINT('Ctrl Pts',(14.7191669521954,0.29831086831951,125.893248735718));
#68523=CARTESIAN_POINT('Ctrl Pts',(14.7114190554183,0.161175863668773,125.888752272359));
#68524=CARTESIAN_POINT('Ctrl Pts',(14.7036727793342,0.0240695447047199,
125.884256749563));
#68525=CARTESIAN_POINT('Ctrl Pts',(14.6959265032501,-0.113260010210574,
125.885500683844));
#68526=CARTESIAN_POINT('Ctrl Pts',(14.688180227166,-0.250296691993672,125.892483722887));
#68527=CARTESIAN_POINT('Ctrl Pts',(14.6804338939007,-0.387334385350425,
125.899466813478));
#68528=CARTESIAN_POINT('Ctrl Pts',(14.6726875606354,-0.524078810802432,
125.91218907347));
#68529=CARTESIAN_POINT('Ctrl Pts',(14.66494122737,-0.660016526973496,125.930598082663));
#68530=CARTESIAN_POINT('Ctrl Pts',(14.657193159367,-0.79598468545357,125.949011214427));
#68531=CARTESIAN_POINT('Ctrl Pts',(14.649445091364,-0.931145387811661,125.973113577069));
#68532=CARTESIAN_POINT('Ctrl Pts',(14.641697023361,-1.06499335470903,126.002801264926));
#68533=CARTESIAN_POINT('Ctrl Pts',(14.6339407206192,-1.19898357681844,126.032520505211));
#68534=CARTESIAN_POINT('Ctrl Pts',(14.6261844178773,-1.33165789412531,126.067836844015));
#68535=CARTESIAN_POINT('Ctrl Pts',(14.6184281151355,-1.46252367417283,126.108595763468));
#68536=CARTESIAN_POINT('Ctrl Pts',(14.6106676726213,-1.59345930122745,126.149376437183));
#68537=CARTESIAN_POINT('Ctrl Pts',(14.6029072301072,-1.72258409973279,126.195605348029));
#68538=CARTESIAN_POINT('Ctrl Pts',(14.5951467875931,-1.84942445703835,126.247079384176));
#68539=CARTESIAN_POINT('Ctrl Pts',(14.5873738873276,-1.97646842974598,126.298636051016));
#68540=CARTESIAN_POINT('Ctrl Pts',(14.5796009870622,-2.10122027703923,126.355454506739));
#68541=CARTESIAN_POINT('Ctrl Pts',(14.5718280867967,-2.22322926954491,126.417284748888));
#68542=CARTESIAN_POINT('Ctrl Pts',(14.5643377510347,-2.34080292785123,126.476867305994));
#68543=CARTESIAN_POINT('Ctrl Pts',(14.5568474152726,-2.4558294195921,126.541103443432));
#68544=CARTESIAN_POINT('Ctrl Pts',(14.5493570795106,-2.56793175944869,126.609731964));
#68545=CARTESIAN_POINT('Ctrl Pts',(14.5415814403922,-2.68430402455614,126.680974512547));
#68546=CARTESIAN_POINT('Ctrl Pts',(14.5338058012739,-2.79789365806825,126.757176396579));
#68547=CARTESIAN_POINT('Ctrl Pts',(14.5260301621556,-2.90824904890265,126.838094044067));
#68548=CARTESIAN_POINT('Ctrl Pts',(14.5180686060688,-3.02124305752823,126.920946447461));
#68549=CARTESIAN_POINT('Ctrl Pts',(14.510107049982,-3.13084582219223,127.008742832104));
#68550=CARTESIAN_POINT('Ctrl Pts',(14.5021454938952,-3.23659923655579,127.101171661487));
#68551=CARTESIAN_POINT('Ctrl Pts',(14.4943893526811,-3.33962412349214,127.191215748991));
#68552=CARTESIAN_POINT('Ctrl Pts',(14.486633211467,-3.43899551995466,127.285655914357));
#68553=CARTESIAN_POINT('Ctrl Pts',(14.4788770702529,-3.53431973952729,127.384160763568));
#68554=CARTESIAN_POINT('Ctrl Pts',(14.4711262677283,-3.62957834575012,127.482597810146));
#68555=CARTESIAN_POINT('Ctrl Pts',(14.4633754652037,-3.72079504694466,127.585093694297));
#68556=CARTESIAN_POINT('Ctrl Pts',(14.455624662679,-3.80761114440574,127.691278473533));
#68557=CARTESIAN_POINT('Ctrl Pts',(14.4478775165418,-3.89438628697464,127.797413160835));
#68558=CARTESIAN_POINT('Ctrl Pts',(14.4401303704045,-3.97676471054156,127.907232977849));
#68559=CARTESIAN_POINT('Ctrl Pts',(14.4323832242672,-4.05442661119648,128.02033333377));
#68560=CARTESIAN_POINT('Ctrl Pts',(14.4242640235843,-4.13581820310089,128.13886530293));
#68561=CARTESIAN_POINT('Ctrl Pts',(14.4161448229015,-4.21202872068971,128.261000375865));
#68562=CARTESIAN_POINT('Ctrl Pts',(14.4080256222186,-4.28273977518678,128.38623674139));
#68563=CARTESIAN_POINT('Ctrl Pts',(14.4002789357348,-4.35020656059208,128.50572718115));
#68564=CARTESIAN_POINT('Ctrl Pts',(14.3925322492509,-4.41266711117819,128.628040287164));
#68565=CARTESIAN_POINT('Ctrl Pts',(14.3847855627671,-4.46989140568988,128.752713990137));
#68566=CARTESIAN_POINT('Ctrl Pts',(14.3770377993638,-4.52712365533874,128.877405024847));
#68567=CARTESIAN_POINT('Ctrl Pts',(14.3692900359605,-4.57911804373872,129.004456951509));
#68568=CARTESIAN_POINT('Ctrl Pts',(14.3615422725572,-4.62569249797559,129.133387255518));
#68569=CARTESIAN_POINT('Ctrl Pts',(14.3537897751549,-4.67229540989897,129.262396337868));
#68570=CARTESIAN_POINT('Ctrl Pts',(14.3460372777525,-4.71347165420832,129.393285717809));
#68571=CARTESIAN_POINT('Ctrl Pts',(14.3382847803502,-4.749088862512,129.525557255643));
#68572=CARTESIAN_POINT('Ctrl Pts',(14.3371741255911,-4.75419153070459,129.544507021811));
#68573=CARTESIAN_POINT('Ctrl Pts',(14.336063470832,-4.75918018708975,129.563485137165));
#68574=CARTESIAN_POINT('Ctrl Pts',(14.334952816073,-4.76405452823406,129.582490119308));
#68575=CARTESIAN_POINT('Ctrl Pts',(16.0848513025106,-4.7640545282341,129.582490119308));
#68576=CARTESIAN_POINT('Ctrl Pts',(16.0771840538337,-4.79781676096018,129.714128552294));
#68577=CARTESIAN_POINT('Ctrl Pts',(16.0695168051568,-4.82611756725086,129.847162936191));
#68578=CARTESIAN_POINT('Ctrl Pts',(16.0618495564799,-4.84885740150383,129.981095798458));
#68579=CARTESIAN_POINT('Ctrl Pts',(16.0540178697318,-4.87208493279666,130.11790109417));
#68580=CARTESIAN_POINT('Ctrl Pts',(16.0461861829837,-4.88951015732492,130.255643418976));
#68581=CARTESIAN_POINT('Ctrl Pts',(16.0383544962356,-4.90108262611967,130.393785223213));
#68582=CARTESIAN_POINT('Ctrl Pts',(16.0305228094875,-4.91265509491442,130.53192702745));
#68583=CARTESIAN_POINT('Ctrl Pts',(16.0226911227394,-4.91837481054274,130.670467867685));
#68584=CARTESIAN_POINT('Ctrl Pts',(16.0148594359913,-4.91824793335435,130.808869337526));
#68585=CARTESIAN_POINT('',(16.360140564049,-4.91824961586008,130.802416757441));
#68586=CARTESIAN_POINT('Ctrl Pts',(16.4298612965399,-4.76405452823409,129.582490119308));
#68587=CARTESIAN_POINT('Ctrl Pts',(16.4214087741111,-4.80105948497718,129.726771884021));
#68588=CARTESIAN_POINT('Ctrl Pts',(16.4129562516822,-4.83154930639298,129.872905341603));
#68589=CARTESIAN_POINT('Ctrl Pts',(16.4045037292534,-4.85535239555172,130.020309485617));
#68590=CARTESIAN_POINT('Ctrl Pts',(16.3960826455574,-4.87906695031521,130.167165367317));
#68591=CARTESIAN_POINT('Ctrl Pts',(16.3876615618615,-4.89614432061384,130.31528224506));
#68592=CARTESIAN_POINT('Ctrl Pts',(16.3792404781655,-4.90646351831546,130.464068381481));
#68593=CARTESIAN_POINT('Ctrl Pts',(16.3728738401267,-4.91426519788417,130.576555979276));
#68594=CARTESIAN_POINT('Ctrl Pts',(16.3665072020878,-4.91820495795325,130.689425740071));
#68595=CARTESIAN_POINT('Ctrl Pts',(16.3601405640489,-4.91824961586008,130.802416757442));
#68596=CARTESIAN_POINT('Ctrl Pts',(16.3601405640087,-4.91824961586036,130.802416758157));
#68597=CARTESIAN_POINT('Ctrl Pts',(16.3522326324733,-4.91830508493801,130.942761666103));
#68598=CARTESIAN_POINT('Ctrl Pts',(16.3443247009378,-4.91234897419799,131.083072226503));
#68599=CARTESIAN_POINT('Ctrl Pts',(16.3364167694024,-4.90041647627177,131.222811835254));
#68600=CARTESIAN_POINT('Ctrl Pts',(16.3285050531866,-4.88847826753609,131.362618322396));
#68601=CARTESIAN_POINT('Ctrl Pts',(16.3205933369708,-4.87055800315575,131.501852946995));
#68602=CARTESIAN_POINT('Ctrl Pts',(16.3126816207551,-4.84674264482889,131.639985412134));
#68603=CARTESIAN_POINT('Ctrl Pts',(16.3047647134023,-4.82291166046301,131.778208510521));
#68604=CARTESIAN_POINT('Ctrl Pts',(16.2968478060496,-4.79317793675304,131.915327646397));
#68605=CARTESIAN_POINT('Ctrl Pts',(16.2889308986969,-4.75767928262551,132.050823976906));
#68606=CARTESIAN_POINT('Ctrl Pts',(16.2810016138169,-4.72212512885164,132.186532146387));
#68607=CARTESIAN_POINT('Ctrl Pts',(16.273072328937,-4.68078813042954,132.320612085298));
#68608=CARTESIAN_POINT('Ctrl Pts',(16.2651430440571,-4.63385592650999,132.452560336911));
#68609=CARTESIAN_POINT('Ctrl Pts',(16.2572071134798,-4.58688438774137,132.584619177078));
#68610=CARTESIAN_POINT('Ctrl Pts',(16.2492711829025,-4.53430843109388,132.714542427513));
#68611=CARTESIAN_POINT('Ctrl Pts',(16.2413352523251,-4.47636315764902,132.841848272337));
#68612=CARTESIAN_POINT('Ctrl Pts',(16.2333846977217,-4.41831110489378,132.969388711451));
#68613=CARTESIAN_POINT('Ctrl Pts',(16.2254341431182,-4.3548701281287,133.094301778135));
#68614=CARTESIAN_POINT('Ctrl Pts',(16.2174835885147,-4.28632100174241,133.216130783341));
#68615=CARTESIAN_POINT('Ctrl Pts',(16.2118070010859,-4.2373778614832,133.303115029585));
#68616=CARTESIAN_POINT('Ctrl Pts',(16.2061304136572,-4.18583164427882,133.388527667036));
#68617=CARTESIAN_POINT('Ctrl Pts',(16.2004538262285,-4.13179742248621,133.472212397938));
#68618=CARTESIAN_POINT('Ctrl Pts',(16.1926794921094,-4.05779519855281,133.586822287572));
#68619=CARTESIAN_POINT('Ctrl Pts',(16.1849051579903,-3.97890348572438,133.698532310843));
#68620=CARTESIAN_POINT('Ctrl Pts',(16.1771308238712,-3.89537649136763,133.806897054148));
#68621=CARTESIAN_POINT('Ctrl Pts',(16.1693660709242,-3.8119524365664,133.915128247591));
#68622=CARTESIAN_POINT('Ctrl Pts',(16.161601317977,-3.72390470293747,134.020022057445));
#68623=CARTESIAN_POINT('Ctrl Pts',(16.1538365650299,-3.6315318458311,134.121160206811));
#68624=CARTESIAN_POINT('Ctrl Pts',(16.1460795241449,-3.53925073474864,134.222197904341));
#68625=CARTESIAN_POINT('Ctrl Pts',(16.13832248326,-3.44265331092744,134.319487077785));
#68626=CARTESIAN_POINT('Ctrl Pts',(16.130565442375,-3.34207940872658,134.412641134414));
#68627=CARTESIAN_POINT('Ctrl Pts',(16.1228142511349,-3.24158135008772,134.505724942845));
#68628=CARTESIAN_POINT('Ctrl Pts',(16.1150630598947,-3.13711306745785,134.594679576698));
#68629=CARTESIAN_POINT('Ctrl Pts',(16.1073118686546,-3.02905213407681,134.679154319371));
#68630=CARTESIAN_POINT('Ctrl Pts',(16.0995639718775,-2.92103712947493,134.763593158024));
#68631=CARTESIAN_POINT('Ctrl Pts',(16.0918160751005,-2.8094328185267,134.843555652269));
#68632=CARTESIAN_POINT('Ctrl Pts',(16.0840681783234,-2.6946506560242,134.918730667098));
#68633=CARTESIAN_POINT('Ctrl Pts',(16.0763219022393,-2.57989250347584,134.993889956935));
#68634=CARTESIAN_POINT('Ctrl Pts',(16.0685756261552,-2.46195814842898,135.064263545201));
#68635=CARTESIAN_POINT('Ctrl Pts',(16.0608293500711,-2.34128856079642,135.129583263579));
#68636=CARTESIAN_POINT('Ctrl Pts',(16.0530830168058,-2.22061808240855,135.194903464132));
#68637=CARTESIAN_POINT('Ctrl Pts',(16.0453366835404,-2.09721267496941,135.25516953424));
#68638=CARTESIAN_POINT('Ctrl Pts',(16.0375903502751,-1.97153811464774,135.310159162218));
#68639=CARTESIAN_POINT('Ctrl Pts',(16.0298422822721,-1.84583541038,135.365161104742));
#68640=CARTESIAN_POINT('Ctrl Pts',(16.0220942142692,-1.71786290015782,135.414884097152));
#68641=CARTESIAN_POINT('Ctrl Pts',(16.0143461462662,-1.58810617097229,135.459154045015));
#68642=CARTESIAN_POINT('Ctrl Pts',(16.0065898435243,-1.45821153479016,135.503471043505));
#68643=CARTESIAN_POINT('Ctrl Pts',(15.9988335407825,-1.32652926221515,135.542323293748));
#68644=CARTESIAN_POINT('Ctrl Pts',(15.9910772380407,-1.19356046649581,135.57558650567));
#68645=CARTESIAN_POINT('Ctrl Pts',(15.9833167955265,-1.06052070132659,135.608867471171));
#68646=CARTESIAN_POINT('Ctrl Pts',(15.9755563530123,-0.92619342752175,135.636553375513));
#68647=CARTESIAN_POINT('Ctrl Pts',(15.9677959104981,-0.791088791895037,
135.658571324348));
#68648=CARTESIAN_POINT('Ctrl Pts',(15.9600230102327,-0.65576727431319,135.680624618349));
#68649=CARTESIAN_POINT('Ctrl Pts',(15.9522501099673,-0.519666289619082,
135.696991728025));
#68650=CARTESIAN_POINT('Ctrl Pts',(15.9444772097018,-0.383300832530537,
135.707651709708));
#68651=CARTESIAN_POINT('Ctrl Pts',(15.9369868739397,-0.251892603290093,
135.717924174207));
#68652=CARTESIAN_POINT('Ctrl Pts',(15.9294965381777,-0.120239104095079,
135.722897232128));
#68653=CARTESIAN_POINT('Ctrl Pts',(15.9220062024156,0.0112018286986203,
135.722597860881));
#68654=CARTESIAN_POINT('Ctrl Pts',(15.9142318682965,0.147626384408839,135.722287138883));
#68655=CARTESIAN_POINT('Ctrl Pts',(15.9064575341774,0.284254088600799,135.716295302799));
#68656=CARTESIAN_POINT('Ctrl Pts',(15.8986832000583,0.420572796901996,135.704595467551));
#68657=CARTESIAN_POINT('Ctrl Pts',(15.8909184471112,0.556723504578179,135.692910051304));
#68658=CARTESIAN_POINT('Ctrl Pts',(15.8831536941642,0.692565588267988,135.675530665761));
#68659=CARTESIAN_POINT('Ctrl Pts',(15.8753889412171,0.827585763308846,135.652482405111));
#68660=CARTESIAN_POINT('Ctrl Pts',(15.8676319003321,0.962471834408769,135.629457036318));
#68661=CARTESIAN_POINT('Ctrl Pts',(15.859874859447,1.0965372384991,135.600774062543));
#68662=CARTESIAN_POINT('Ctrl Pts',(15.852117818562,1.22927303539538,135.566510433243));
#68663=CARTESIAN_POINT('Ctrl Pts',(15.8443666273218,1.36190873519467,135.532272642412));
#68664=CARTESIAN_POINT('Ctrl Pts',(15.8366154360817,1.49321644652337,135.492462669975));
#68665=CARTESIAN_POINT('Ctrl Pts',(15.8288642448416,1.62269701401046,135.447208608102));
#68666=CARTESIAN_POINT('Ctrl Pts',(15.8211163480645,1.752122548802,135.401973780412));
#68667=CARTESIAN_POINT('Ctrl Pts',(15.8133684512874,1.87972211601999,135.351299594145));
#68668=CARTESIAN_POINT('Ctrl Pts',(15.8056205545103,2.00501154760564,135.295364041799));
#68669=CARTESIAN_POINT('Ctrl Pts',(15.7978742784262,2.13027477134314,135.239440189964));
#68670=CARTESIAN_POINT('Ctrl Pts',(15.7901280023422,2.25322846384438,135.178257320417));
#68671=CARTESIAN_POINT('Ctrl Pts',(15.7823817262581,2.37340865250036,135.112041482107));
#68672=CARTESIAN_POINT('Ctrl Pts',(15.7746353929927,2.49358972829903,135.045825155008));
#68673=CARTESIAN_POINT('Ctrl Pts',(15.7668890597274,2.61099691696992,134.97457597368));
#68674=CARTESIAN_POINT('Ctrl Pts',(15.7591427264621,2.72519141800093,134.898565643912));
#68675=CARTESIAN_POINT('Ctrl Pts',(15.7513946584591,2.83941149209853,134.822538292157));
#68676=CARTESIAN_POINT('Ctrl Pts',(15.7436465904561,2.95041712151859,134.741747886886));
#68677=CARTESIAN_POINT('Ctrl Pts',(15.7358985224532,3.05779936405475,134.656508863894));
#68678=CARTESIAN_POINT('Ctrl Pts',(15.7281422197114,3.16529573371629,134.571179247854));
#68679=CARTESIAN_POINT('Ctrl Pts',(15.7203859169695,3.26916071704303,134.481391812776));
#68680=CARTESIAN_POINT('Ctrl Pts',(15.7126296142276,3.36901888132632,134.387500977609));
#68681=CARTESIAN_POINT('Ctrl Pts',(15.7048691717135,3.46893034291883,134.293560030076));
#68682=CARTESIAN_POINT('Ctrl Pts',(15.6971087291993,3.56483045096466,134.19551159784));
#68683=CARTESIAN_POINT('Ctrl Pts',(15.6893482866851,3.65638213057086,134.093745480689));
#68684=CARTESIAN_POINT('Ctrl Pts',(15.6815753864197,3.74808077706075,133.991815999532));
#68685=CARTESIAN_POINT('Ctrl Pts',(15.6738024861543,3.83541679664981,133.886157209097));
#68686=CARTESIAN_POINT('Ctrl Pts',(15.6660295858888,3.91809420161419,133.777191068462));
#68687=CARTESIAN_POINT('Ctrl Pts',(15.6585392501268,3.99776607465664,133.672186121509));
#68688=CARTESIAN_POINT('Ctrl Pts',(15.6510489143647,4.07311198126007,133.564110363295));
#68689=CARTESIAN_POINT('Ctrl Pts',(15.6435585786027,4.14390714654999,133.453363566464));
#68690=CARTESIAN_POINT('Ctrl Pts',(15.6357842444836,4.21738653204919,133.338417771171));
#68691=CARTESIAN_POINT('Ctrl Pts',(15.6280099103645,4.28619604208648,133.220230280375));
#68692=CARTESIAN_POINT('Ctrl Pts',(15.6202355762454,4.35003623094224,133.099217443599));
#68693=CARTESIAN_POINT('Ctrl Pts',(15.6124708232983,4.4137977424708,132.978353744329));
#68694=CARTESIAN_POINT('Ctrl Pts',(15.6047060703512,4.47260193756526,132.854671969672));
#68695=CARTESIAN_POINT('Ctrl Pts',(15.5969413174041,4.52619248578029,132.728617524574));
#68696=CARTESIAN_POINT('Ctrl Pts',(15.5891842765191,4.57972980710733,132.602688278527));
#68697=CARTESIAN_POINT('Ctrl Pts',(15.5814272356342,4.62806363456646,132.47439140919));
#68698=CARTESIAN_POINT('Ctrl Pts',(15.5736701947492,4.67098361331424,132.344196695416));
#68699=CARTESIAN_POINT('Ctrl Pts',(15.565919003509,4.71387122577234,132.214100162488));
#68700=CARTESIAN_POINT('Ctrl Pts',(15.5581678122689,4.75135299382685,132.082109003605));
#68701=CARTESIAN_POINT('Ctrl Pts',(15.5504166210287,4.78326687937643,131.948712409263));
#68702=CARTESIAN_POINT('Ctrl Pts',(15.5426687242516,4.81516720067318,131.815372512033));
#68703=CARTESIAN_POINT('Ctrl Pts',(15.5349208274745,4.84150425547309,131.680628746862));
#68704=CARTESIAN_POINT('Ctrl Pts',(15.5271729306975,4.86216608924381,131.544984667343));
#68705=CARTESIAN_POINT('Ctrl Pts',(15.5194266546134,4.88282360100431,131.409368961641));
#68706=CARTESIAN_POINT('Ctrl Pts',(15.5116803785293,4.89780819417306,131.272853702445));
#68707=CARTESIAN_POINT('Ctrl Pts',(15.5039341024452,4.90705926160619,131.135951428031));
#68708=CARTESIAN_POINT('Ctrl Pts',(15.4961877691798,4.91631039732861,130.999048143035));
#68709=CARTESIAN_POINT('Ctrl Pts',(15.4884414359145,4.91982789650269,130.861758227196));
#68710=CARTESIAN_POINT('Ctrl Pts',(15.4806951026491,4.91760317050699,130.724597719427));
#68711=CARTESIAN_POINT('Ctrl Pts',(15.4729470346461,4.91537794629932,130.587406495512));
#68712=CARTESIAN_POINT('Ctrl Pts',(15.4651989666432,4.90740794440638,130.450345128173));
#68713=CARTESIAN_POINT('Ctrl Pts',(15.4574508986402,4.89373666531621,130.313927632297));
#68714=CARTESIAN_POINT('Ctrl Pts',(15.4496945958983,4.88005085622802,130.177365150284));
#68715=CARTESIAN_POINT('Ctrl Pts',(15.4419382931565,4.86065170471596,130.041448296362));
#68716=CARTESIAN_POINT('Ctrl Pts',(15.4341819904146,4.83563446292962,129.906684504802));
#68717=CARTESIAN_POINT('Ctrl Pts',(15.4264215479005,4.81060386868809,129.771848785748));
#68718=CARTESIAN_POINT('Ctrl Pts',(15.4186611053863,4.77994929666152,129.638167736228));
#68719=CARTESIAN_POINT('Ctrl Pts',(15.4109006628722,4.74381649923732,129.506135643201));
#68720=CARTESIAN_POINT('Ctrl Pts',(15.4031277626068,4.70762569823893,129.373891600538));
#68721=CARTESIAN_POINT('Ctrl Pts',(15.3953548623413,4.66593921732234,129.243302176684));
#68722=CARTESIAN_POINT('Ctrl Pts',(15.3875819620759,4.61895207401608,129.114844473683));
#68723=CARTESIAN_POINT('Ctrl Pts',(15.3800916263139,4.57367303172241,128.991056531751));
#68724=CARTESIAN_POINT('Ctrl Pts',(15.3726012905519,4.52347213841844,128.869248299408));
#68725=CARTESIAN_POINT('Ctrl Pts',(15.3651109547898,4.46856423783985,128.749824972998));
#68726=CARTESIAN_POINT('Ctrl Pts',(15.3573366206708,4.41157448752199,128.625873674871));
#68727=CARTESIAN_POINT('Ctrl Pts',(15.3495622865517,4.34933322521199,128.504099059624));
#68728=CARTESIAN_POINT('Ctrl Pts',(15.3417879524326,4.28202887983068,128.384978106512));
#68729=CARTESIAN_POINT('Ctrl Pts',(15.3340231994855,4.21480748103971,128.266003959327));
#68730=CARTESIAN_POINT('Ctrl Pts',(15.3262584465384,4.14253560499146,128.149677304275));
#68731=CARTESIAN_POINT('Ctrl Pts',(15.3184936935913,4.06544943061467,128.036454551672));
#68732=CARTESIAN_POINT('Ctrl Pts',(15.3107366527063,3.988439819313,127.923344253502));
#68733=CARTESIAN_POINT('Ctrl Pts',(15.3029796118212,3.90662564394487,127.813332043874));
#68734=CARTESIAN_POINT('Ctrl Pts',(15.2952225709362,3.82028844083258,127.706848827219));
#68735=CARTESIAN_POINT('Ctrl Pts',(15.2874713796961,3.73401634527724,127.600445910386));
#68736=CARTESIAN_POINT('Ctrl Pts',(15.2797201884561,3.6432282563021,127.497566991944));
#68737=CARTESIAN_POINT('Ctrl Pts',(15.271968997216,3.54824815817462,127.398612818549));
#68738=CARTESIAN_POINT('Ctrl Pts',(15.2642211004389,3.45330842912226,127.299700703317));
#68739=CARTESIAN_POINT('Ctrl Pts',(15.2564732036618,3.35418050477971,127.204710296835));
#68740=CARTESIAN_POINT('Ctrl Pts',(15.2487253068848,3.25122752488696,127.114007972639));
#68741=CARTESIAN_POINT('Ctrl Pts',(15.2409790308007,3.1482960805382,127.023324621415));
#68742=CARTESIAN_POINT('Ctrl Pts',(15.2332327547166,3.04154146529052,126.93692782663));
#68743=CARTESIAN_POINT('Ctrl Pts',(15.2254864786325,2.93136213246959,126.85514561825));
#68744=CARTESIAN_POINT('Ctrl Pts',(15.2177401453671,2.82118198632957,126.773362806172));
#68745=CARTESIAN_POINT('Ctrl Pts',(15.2099938121017,2.70757738610485,126.696194881492));
#68746=CARTESIAN_POINT('Ctrl Pts',(15.2022474788363,2.5909778475882,126.623928001699));
#68747=CARTESIAN_POINT('Ctrl Pts',(15.1944994108333,2.47435219741349,126.551644938239));
#68748=CARTESIAN_POINT('Ctrl Pts',(15.1867513428304,2.35473060659061,126.484265309597));
#68749=CARTESIAN_POINT('Ctrl Pts',(15.1790032748274,2.23256904347863,126.422030355183));
#68750=CARTESIAN_POINT('Ctrl Pts',(15.1712469720855,2.11027764560363,126.359729256718));
#68751=CARTESIAN_POINT('Ctrl Pts',(15.1634906693437,1.98544123179093,126.3025839328));
#68752=CARTESIAN_POINT('Ctrl Pts',(15.1557343666019,1.85853820697621,126.250788525712));
#68753=CARTESIAN_POINT('Ctrl Pts',(15.1479739240877,1.73156745019634,126.198965473857));
#68754=CARTESIAN_POINT('Ctrl Pts',(15.1402134815735,1.60252825223089,126.152498160878));
#68755=CARTESIAN_POINT('Ctrl Pts',(15.1324530390594,1.47191525342404,126.111531135341));
#68756=CARTESIAN_POINT('Ctrl Pts',(15.1246801387939,1.34109258303586,126.070498345898));
#68757=CARTESIAN_POINT('Ctrl Pts',(15.1169072385284,1.20869144107801,126.034983589498));
#68758=CARTESIAN_POINT('Ctrl Pts',(15.109134338263,1.07521863874984,126.005080677681));
#68759=CARTESIAN_POINT('Ctrl Pts',(15.101644002501,0.946597908984719,125.976264812029));
#68760=CARTESIAN_POINT('Ctrl Pts',(15.094153666739,0.816982384270664,125.952659920416));
#68761=CARTESIAN_POINT('Ctrl Pts',(15.086663330977,0.686829096056115,125.934304267244));
#68762=CARTESIAN_POINT('Ctrl Pts',(15.078888996858,0.551741006359105,125.915252653903));
#68763=CARTESIAN_POINT('Ctrl Pts',(15.0711146627388,0.415645651109847,125.901795836598));
#68764=CARTESIAN_POINT('Ctrl Pts',(15.0633403286197,0.279046176896683,125.894033103677));
#68765=CARTESIAN_POINT('Ctrl Pts',(15.0555755756726,0.142615049327056,125.88627993763));
#68766=CARTESIAN_POINT('Ctrl Pts',(15.0478108227256,0.0056814255469059,
125.884206915303));
#68767=CARTESIAN_POINT('Ctrl Pts',(15.0400460697785,-0.131243043038496,
125.887862033599));
#68768=CARTESIAN_POINT('Ctrl Pts',(15.0322890288935,-0.268031516311589,
125.891513521579));
#68769=CARTESIAN_POINT('Ctrl Pts',(15.0245319880084,-0.404810464188582,
125.900881817912));
#68770=CARTESIAN_POINT('Ctrl Pts',(15.0167749471234,-0.541065177307815,
125.915962972488));
#68771=CARTESIAN_POINT('Ctrl Pts',(15.0090237558833,-0.677217139686495,
125.931032754247));
#68772=CARTESIAN_POINT('Ctrl Pts',(15.0012725646433,-0.812845267167011,
125.951806776379));
#68773=CARTESIAN_POINT('Ctrl Pts',(14.9935213734032,-0.947437278827389,
125.9782290751));
#68774=CARTESIAN_POINT('Ctrl Pts',(14.9857734766262,-1.08197208529355,126.004640143639));
#68775=CARTESIAN_POINT('Ctrl Pts',(14.978025579849,-1.21547126897631,126.036694638864));
#68776=CARTESIAN_POINT('Ctrl Pts',(14.9702776830719,-1.34743030354397,126.074285074872));
#68777=CARTESIAN_POINT('Ctrl Pts',(14.9625314069878,-1.47936173512649,126.111867647772));
#68778=CARTESIAN_POINT('Ctrl Pts',(14.9547851309037,-1.60975328263125,126.154983751087));
#68779=CARTESIAN_POINT('Ctrl Pts',(14.9470388548196,-1.73811359140382,126.20347546296));
#68780=CARTESIAN_POINT('Ctrl Pts',(14.9392925215543,-1.86647484770234,126.251967532786));
#68781=CARTESIAN_POINT('Ctrl Pts',(14.9315461882889,-1.99280446961197,126.305835152184));
#68782=CARTESIAN_POINT('Ctrl Pts',(14.9237998550236,-2.11662954095628,126.364871632463));
#68783=CARTESIAN_POINT('Ctrl Pts',(14.9160517870206,-2.24048234206729,126.423921333553));
#68784=CARTESIAN_POINT('Ctrl Pts',(14.9083037190177,-2.36182912369358,126.488142030652));
#68785=CARTESIAN_POINT('Ctrl Pts',(14.9005556510147,-2.48022046225175,126.557280500459));
#68786=CARTESIAN_POINT('Ctrl Pts',(14.8927993482729,-2.59873762853342,126.626492451454));
#68787=CARTESIAN_POINT('Ctrl Pts',(14.885043045531,-2.71429273895081,126.700632418516));
#68788=CARTESIAN_POINT('Ctrl Pts',(14.8772867427891,-2.82646386654663,126.779402844669));
#68789=CARTESIAN_POINT('Ctrl Pts',(14.8695263002749,-2.93869486325066,126.85821531297));
#68790=CARTESIAN_POINT('Ctrl Pts',(14.8617658577607,-3.0475379681402,126.941662927106));
#68791=CARTESIAN_POINT('Ctrl Pts',(14.8540054152466,-3.15260420322612,127.029407664177));
#68792=CARTESIAN_POINT('Ctrl Pts',(14.8462325149811,-3.25783909995994,127.117293256889));
#68793=CARTESIAN_POINT('Ctrl Pts',(14.8384596147157,-3.35928472165498,127.209489494083));
#68794=CARTESIAN_POINT('Ctrl Pts',(14.8306867144503,-3.45658819817418,127.305620688571));
#68795=CARTESIAN_POINT('Ctrl Pts',(14.8231963786882,-3.5503544482303,127.398257272001));
#68796=CARTESIAN_POINT('Ctrl Pts',(14.8157060429261,-3.64027426921428,127.494547463348));
#68797=CARTESIAN_POINT('Ctrl Pts',(14.808215707164,-3.72606843153878,127.594127431956));
#68798=CARTESIAN_POINT('Ctrl Pts',(14.8004988501849,-3.81445716354266,127.696718877805));
#68799=CARTESIAN_POINT('Ctrl Pts',(14.7927819932059,-3.8987577119728,127.803140151212));
#68800=CARTESIAN_POINT('Ctrl Pts',(14.7850651362268,-3.97861597536864,127.91302909333));
#68801=CARTESIAN_POINT('Ctrl Pts',(14.777357644971,-4.05837731712915,128.022784666458));
#68802=CARTESIAN_POINT('Ctrl Pts',(14.7696501537153,-4.13370686506258,128.135999220308));
#68803=CARTESIAN_POINT('Ctrl Pts',(14.7619426624595,-4.20428872582697,128.25227531876));
#68804=CARTESIAN_POINT('Ctrl Pts',(14.7542442395176,-4.27478754290774,128.368414611586));
#68805=CARTESIAN_POINT('Ctrl Pts',(14.7465458165756,-4.34054958910387,128.487607940334));
#68806=CARTESIAN_POINT('Ctrl Pts',(14.7388473936337,-4.40130094564209,128.609427122357));
#68807=CARTESIAN_POINT('Ctrl Pts',(14.731154215882,-4.46201091027164,128.731163304942));
#68808=CARTESIAN_POINT('Ctrl Pts',(14.7234610381303,-4.51771679823394,128.855521428867));
#68809=CARTESIAN_POINT('Ctrl Pts',(14.7157678603785,-4.56818954633877,128.982046887381));
#68810=CARTESIAN_POINT('Ctrl Pts',(14.7080782288489,-4.61863902869028,129.108514023132));
#68811=CARTESIAN_POINT('Ctrl Pts',(14.7003885973193,-4.66386002327873,129.237146137795));
#68812=CARTESIAN_POINT('Ctrl Pts',(14.6926989657897,-4.70367093645055,129.367467168458));
#68813=CARTESIAN_POINT('Ctrl Pts',(14.6884979542264,-4.72542049700328,129.43866435842));
#68814=CARTESIAN_POINT('Ctrl Pts',(14.6842969426631,-4.7455561645854,129.510365280194));
#68815=CARTESIAN_POINT('Ctrl Pts',(14.6800959310998,-4.76405452823407,129.582490119308));
#68816=CARTESIAN_POINT('Origin',(213.235140564004,0.,130.804360617566));
#68817=CARTESIAN_POINT('',(12.5846956991378,-4.76405452823411,129.582490119308));
#68818=CARTESIAN_POINT('',(12.9302349012324,-4.7640545282341,129.582490119308));
#68819=CARTESIAN_POINT('',(213.235140564004,-4.76405452823405,129.582490119308));
#68820=CARTESIAN_POINT('',(14.2648594359355,-4.91824995510319,130.803696067003));
#68821=CARTESIAN_POINT('Ctrl Pts',(14.2648594359355,-4.91824995510319,130.803696067003));
#68822=CARTESIAN_POINT('Ctrl Pts',(14.2571139563985,-4.91826832183562,130.939625800473));
#68823=CARTESIAN_POINT('Ctrl Pts',(14.2493684768615,-4.91264721499648,131.0757784822));
#68824=CARTESIAN_POINT('Ctrl Pts',(14.2416229973244,-4.90135718546593,131.211645288259));
#68825=CARTESIAN_POINT('Ctrl Pts',(14.2338870308702,-4.8900810224733,131.347345221218));
#68826=CARTESIAN_POINT('Ctrl Pts',(14.226151064416,-4.8731498207027,131.482759588039));
#68827=CARTESIAN_POINT('Ctrl Pts',(14.2184150979618,-4.85058610595946,131.617378139624));
#68828=CARTESIAN_POINT('Ctrl Pts',(14.2106867461381,-4.82804460102725,131.7518641841));
#68829=CARTESIAN_POINT('Ctrl Pts',(14.2029583943145,-4.79988167951563,131.885555585763));
#68830=CARTESIAN_POINT('Ctrl Pts',(14.1952300424909,-4.76617174467524,132.017946198709));
#68831=CARTESIAN_POINT('Ctrl Pts',(14.1875074137658,-4.73248677314925,132.150238772057));
#68832=CARTESIAN_POINT('Ctrl Pts',(14.1797847850407,-4.69326306038384,132.281232093317));
#68833=CARTESIAN_POINT('Ctrl Pts',(14.1720621563155,-4.64862619136131,132.410429605963));
#68834=CARTESIAN_POINT('Ctrl Pts',(14.1643426296658,-4.60400725236479,132.539575221717));
#68835=CARTESIAN_POINT('Ctrl Pts',(14.156623103016,-4.55397960920367,132.666926091366));
#68836=CARTESIAN_POINT('Ctrl Pts',(14.1489035763663,-4.49871879539489,132.792000489993));
#68837=CARTESIAN_POINT('Ctrl Pts',(14.1411855021117,-4.44346837866608,132.91705135642));
#68838=CARTESIAN_POINT('Ctrl Pts',(14.1334674278571,-4.38298690867677,133.039826243258));
#68839=CARTESIAN_POINT('Ctrl Pts',(14.1257493536025,-4.31749801802492,133.159863520738));
#68840=CARTESIAN_POINT('Ctrl Pts',(14.118031027675,-4.25200699189477,133.279904712423));
#68841=CARTESIAN_POINT('Ctrl Pts',(14.1103127017474,-4.1815084089773,133.397207771056));
#68842=CARTESIAN_POINT('Ctrl Pts',(14.1025943758199,-4.10627158855874,133.511336181456));
#68843=CARTESIAN_POINT('Ctrl Pts',(14.094874094318,-4.0310157055618,133.625493508306));
#68844=CARTESIAN_POINT('Ctrl Pts',(14.0871538128162,-3.95101941357975,133.736474257679));
#68845=CARTESIAN_POINT('Ctrl Pts',(14.0794335313144,-3.86659477019901,133.843871753517));
#68846=CARTESIAN_POINT('Ctrl Pts',(14.0717049876774,-3.78207977676924,133.951384184623));
#68847=CARTESIAN_POINT('Ctrl Pts',(14.0639764440405,-3.69312721127982,134.055305393542));
#68848=CARTESIAN_POINT('Ctrl Pts',(14.0562479004035,-3.60008906066226,134.15526226008));
#68849=CARTESIAN_POINT('Ctrl Pts',(14.0485149685762,-3.50699808390658,134.255275881134));
#68850=CARTESIAN_POINT('Ctrl Pts',(14.0407820367489,-3.40981718115627,134.351320399342));
#68851=CARTESIAN_POINT('Ctrl Pts',(14.0330491049216,-3.30893365570468,134.443061089526));
#68852=CARTESIAN_POINT('Ctrl Pts',(14.0253042589508,-3.20789469880424,134.534943124775));
#68853=CARTESIAN_POINT('Ctrl Pts',(14.01755941298,-3.10314202617667,134.622507834068));
#68854=CARTESIAN_POINT('Ctrl Pts',(14.0098145670092,-2.99509485695859,134.705461726269));
#68855=CARTESIAN_POINT('Ctrl Pts',(14.0040303219677,-2.91439973336894,134.767415913794));
#68856=CARTESIAN_POINT('Ctrl Pts',(13.9982460769262,-2.83186763822481,134.826799121679));
#68857=CARTESIAN_POINT('Ctrl Pts',(13.9924618318848,-2.74768244700801,134.883505654569));
#68858=CARTESIAN_POINT('Ctrl Pts',(13.9846874977657,-2.63453305591139,134.959722261967));
#68859=CARTESIAN_POINT('Ctrl Pts',(13.9769131636466,-2.51803083870433,135.031348130466));
#68860=CARTESIAN_POINT('Ctrl Pts',(13.9691388295275,-2.39858483914146,135.098073909338));
#68861=CARTESIAN_POINT('Ctrl Pts',(13.9613740765804,-2.27928604609785,135.164717454651));
#68862=CARTESIAN_POINT('Ctrl Pts',(13.9536093236333,-2.15705102727736,135.226472737154));
#68863=CARTESIAN_POINT('Ctrl Pts',(13.9458445706862,-2.03231890813653,135.283072811727));
#68864=CARTESIAN_POINT('Ctrl Pts',(13.9380875298012,-1.90771067469467,135.339616670309));
#68865=CARTESIAN_POINT('Ctrl Pts',(13.9303304889162,-1.78061063027463,135.391015349931));
#68866=CARTESIAN_POINT('Ctrl Pts',(13.9225734480312,-1.65148337050791,135.437047282929));
#68867=CARTESIAN_POINT('Ctrl Pts',(13.9148222567911,-1.52245348661242,135.483044502889));
#68868=CARTESIAN_POINT('Ctrl Pts',(13.907071065551,-1.39139979700716,135.523682900994));
#68869=CARTESIAN_POINT('Ctrl Pts',(13.8993198743108,-1.25880746284614,135.558788746582));
#68870=CARTESIAN_POINT('Ctrl Pts',(13.8915719775338,-1.12627148396433,135.59387967125));
#68871=CARTESIAN_POINT('Ctrl Pts',(13.8838240807567,-0.992198538364546,
135.623442620463));
#68872=CARTESIAN_POINT('Ctrl Pts',(13.8760761839796,-0.857089348028968,
135.647353588033));
#68873=CARTESIAN_POINT('Ctrl Pts',(13.8683299078956,-0.722008419623206,
135.671259553944));
#68874=CARTESIAN_POINT('Ctrl Pts',(13.8605836318115,-0.585892062368198,
135.689515821727));
#68875=CARTESIAN_POINT('Ctrl Pts',(13.8528373557274,-0.449251212537125,
135.702049502186));
#68876=CARTESIAN_POINT('Ctrl Pts',(13.8450910224621,-0.312609354054525,
135.714583275166));
#68877=CARTESIAN_POINT('Ctrl Pts',(13.8373446891967,-0.175443384600942,
135.721394340818));
#68878=CARTESIAN_POINT('Ctrl Pts',(13.8295983559314,-0.0382689883796058,
135.722461729482));
#68879=CARTESIAN_POINT('Ctrl Pts',(13.8218502879285,0.0989361270964765,
135.72352935718));
#68880=CARTESIAN_POINT('Ctrl Pts',(13.8141022199255,0.236149282216913,135.718850745347));
#68881=CARTESIAN_POINT('Ctrl Pts',(13.8063541519226,0.372855566225771,135.708457047005));
#68882=CARTESIAN_POINT('Ctrl Pts',(13.7985978491807,0.509707143300472,135.698052302116));
#68883=CARTESIAN_POINT('Ctrl Pts',(13.7908415464389,0.646050382673326,135.681920366811));
#68884=CARTESIAN_POINT('Ctrl Pts',(13.783085243697,0.781375710414469,135.660144288785));
#68885=CARTESIAN_POINT('Ctrl Pts',(13.7753248011829,0.916773265357595,135.63835658821));
#68886=CARTESIAN_POINT('Ctrl Pts',(13.7675643586687,1.05115144324327,135.610918820533));
#68887=CARTESIAN_POINT('Ctrl Pts',(13.7598039161545,1.1840126017983,135.577964834642));
#68888=CARTESIAN_POINT('Ctrl Pts',(13.7520310158891,1.31708704087991,135.544957948087));
#68889=CARTESIAN_POINT('Ctrl Pts',(13.7442581156237,1.44863921880625,135.506417257945));
#68890=CARTESIAN_POINT('Ctrl Pts',(13.7364852153583,1.57818749104427,135.462526276451));
#68891=CARTESIAN_POINT('Ctrl Pts',(13.7289948795962,1.70302635727561,135.420230842688));
#68892=CARTESIAN_POINT('Ctrl Pts',(13.7215045438341,1.82600419487917,135.372967467714));
#68893=CARTESIAN_POINT('Ctrl Pts',(13.7140142080719,1.9467107685384,135.320941209801));
#68894=CARTESIAN_POINT('Ctrl Pts',(13.7062398739529,2.0719939686243,135.266942360507));
#68895=CARTESIAN_POINT('Ctrl Pts',(13.6984655398337,2.19522713446769,135.20764127714));
#68896=CARTESIAN_POINT('Ctrl Pts',(13.6906912057147,2.31592890239964,135.143214888169));
#68897=CARTESIAN_POINT('Ctrl Pts',(13.6829264527676,2.43648191619019,135.078867898965));
#68898=CARTESIAN_POINT('Ctrl Pts',(13.6751616998205,2.55450939778924,135.009408354405));
#68899=CARTESIAN_POINT('Ctrl Pts',(13.6673969468734,2.66954940067231,134.935061412815));
#68900=CARTESIAN_POINT('Ctrl Pts',(13.6596399059884,2.78447514420273,134.860788313656));
#68901=CARTESIAN_POINT('Ctrl Pts',(13.6518828651034,2.89641898765502,134.781637688443));
#68902=CARTESIAN_POINT('Ctrl Pts',(13.6441258242184,3.00494339459148,134.697880651905));
#68903=CARTESIAN_POINT('Ctrl Pts',(13.6363746329783,3.11338596242833,134.614186777201));
#68904=CARTESIAN_POINT('Ctrl Pts',(13.6286234417381,3.21841391808913,134.525893643326));
#68905=CARTESIAN_POINT('Ctrl Pts',(13.620872250498,3.31961885559364,134.433315524435));
#68906=CARTESIAN_POINT('Ctrl Pts',(13.6131243537209,3.42078077829998,134.340776753714));
#68907=CARTESIAN_POINT('Ctrl Pts',(13.6053764569439,3.51812262675017,134.243956883602));
#68908=CARTESIAN_POINT('Ctrl Pts',(13.5976285601668,3.61126941856233,134.143210157311));
#68909=CARTESIAN_POINT('Ctrl Pts',(13.5898822840827,3.70439672607366,134.042484505063));
#68910=CARTESIAN_POINT('Ctrl Pts',(13.5821360079986,3.79333045712705,133.93783391736));
#68911=CARTESIAN_POINT('Ctrl Pts',(13.5743897319145,3.87773311444168,133.829648860967));
#68912=CARTESIAN_POINT('Ctrl Pts',(13.5666433986491,3.96213639479755,133.721463005977));
#68913=CARTESIAN_POINT('Ctrl Pts',(13.5588970653838,4.04200829418442,133.609742938488));
#68914=CARTESIAN_POINT('Ctrl Pts',(13.5511507321184,4.11705243032601,133.494911183611));
#68915=CARTESIAN_POINT('Ctrl Pts',(13.5434026641154,4.19211337208167,133.380053712959));
#68916=CARTESIAN_POINT('Ctrl Pts',(13.5356545961125,4.26234418540212,133.2620834955));
#68917=CARTESIAN_POINT('Ctrl Pts',(13.5279065281095,4.32749275836524,133.141450579206));
#68918=CARTESIAN_POINT('Ctrl Pts',(13.5201502253676,4.3927105720068,133.020689452812));
#68919=CARTESIAN_POINT('Ctrl Pts',(13.5123939226258,4.45283516920389,132.89726031901));
#68920=CARTESIAN_POINT('Ctrl Pts',(13.504637619884,4.50766098317906,132.771636786086));
#68921=CARTESIAN_POINT('Ctrl Pts',(13.4968771773698,4.56251605934192,132.6459462041));
#68922=CARTESIAN_POINT('Ctrl Pts',(13.4891167348557,4.61206657583323,132.518059253622));
#68923=CARTESIAN_POINT('Ctrl Pts',(13.4813562923415,4.65615615571087,132.388466963786));
#68924=CARTESIAN_POINT('Ctrl Pts',(13.4735833920761,4.70031651209633,132.258666640902));
#68925=CARTESIAN_POINT('Ctrl Pts',(13.4658104918106,4.73899830346059,132.127155883431));
#68926=CARTESIAN_POINT('Ctrl Pts',(13.4580375915452,4.77209558320917,131.994439105404));
#68927=CARTESIAN_POINT('Ctrl Pts',(13.4505472557831,4.80398969347205,131.866546916552));
#68928=CARTESIAN_POINT('Ctrl Pts',(13.4430569200211,4.83069820266381,131.737535170218));
#68929=CARTESIAN_POINT('Ctrl Pts',(13.435566584259,4.85217188990619,131.607859847998));
#68930=CARTESIAN_POINT('Ctrl Pts',(13.4277922501399,4.87445975852701,131.473267846522));
#68931=CARTESIAN_POINT('Ctrl Pts',(13.4200179160209,4.89117861387149,131.337534609884));
#68932=CARTESIAN_POINT('Ctrl Pts',(13.4122435819018,4.90221712205221,131.20116075713));
#68933=CARTESIAN_POINT('Ctrl Pts',(13.4044788289547,4.91324202625818,131.064954972962));
#68934=CARTESIAN_POINT('Ctrl Pts',(13.3967140760076,4.91860048100911,130.928110529502));
#68935=CARTESIAN_POINT('Ctrl Pts',(13.3889493230604,4.91823222500125,130.79113777902));
#68936=CARTESIAN_POINT('Ctrl Pts',(13.3811922821754,4.91786433475046,130.654301071804));
#68937=CARTESIAN_POINT('Ctrl Pts',(13.3734352412904,4.91178105386311,130.517336699605));
#68938=CARTESIAN_POINT('Ctrl Pts',(13.3656782004054,4.89997397970673,130.380759318351));
#68939=CARTESIAN_POINT('Ctrl Pts',(13.3579270091653,4.88817580935676,130.244284931161));
#68940=CARTESIAN_POINT('Ctrl Pts',(13.3501758179252,4.8706624707216,130.108197341978));
#68941=CARTESIAN_POINT('Ctrl Pts',(13.342424626685,4.84747761813886,129.973010027175));
#68942=CARTESIAN_POINT('Ctrl Pts',(13.3346767299079,4.824302619737,129.837880170588));
#68943=CARTESIAN_POINT('Ctrl Pts',(13.3269288331308,4.79546096772526,129.70365021187));
#68944=CARTESIAN_POINT('Ctrl Pts',(13.3191809363537,4.76104800981208,129.570827111428));
#68945=CARTESIAN_POINT('Ctrl Pts',(13.3114346602696,4.72664225034779,129.438031794715));
#68946=CARTESIAN_POINT('Ctrl Pts',(13.3036883841855,4.6866676010156,129.306643129159));
#68947=CARTESIAN_POINT('Ctrl Pts',(13.2959421081013,4.64127014704047,129.177156117606));
#68948=CARTESIAN_POINT('Ctrl Pts',(13.288195774836,4.59587235795176,129.047668150209));
#68949=CARTESIAN_POINT('Ctrl Pts',(13.2804494415707,4.54505181369432,128.920082233773));
#68950=CARTESIAN_POINT('Ctrl Pts',(13.2727031083054,4.48900379475163,128.794876108244));
#68951=CARTESIAN_POINT('Ctrl Pts',(13.2649550403024,4.43294322424386,128.669641943672));
#68952=CARTESIAN_POINT('Ctrl Pts',(13.2572069722994,4.37165300928843,128.546788987267));
#68953=CARTESIAN_POINT('Ctrl Pts',(13.2494589042965,4.30537551533711,128.42677260985));
#68954=CARTESIAN_POINT('Ctrl Pts',(13.2417026015546,4.23902758087623,128.306628677598));
#68955=CARTESIAN_POINT('Ctrl Pts',(13.2339462988128,4.16768196832323,128.189327689415));
#68956=CARTESIAN_POINT('Ctrl Pts',(13.2261899960709,4.09162602387908,128.075298591298));
#68957=CARTESIAN_POINT('Ctrl Pts',(13.2184295535567,4.01552948608718,127.961208632419));
#68958=CARTESIAN_POINT('Ctrl Pts',(13.2106691110425,3.93471783720559,127.850394359005));
#68959=CARTESIAN_POINT('Ctrl Pts',(13.2029086685283,3.84951966839361,127.743252748648));
#68960=CARTESIAN_POINT('Ctrl Pts',(13.1951357682629,3.76418473191775,127.635939145067));
#68961=CARTESIAN_POINT('Ctrl Pts',(13.1873628679975,3.67444946016647,127.532310281725));
#68962=CARTESIAN_POINT('Ctrl Pts',(13.179589967732,3.58068096422841,127.432727942598));
#68963=CARTESIAN_POINT('Ctrl Pts',(13.1720996319701,3.49032118930705,127.336765672332));
#68964=CARTESIAN_POINT('Ctrl Pts',(13.1646092962081,3.39621655492498,127.244561046946));
#68965=CARTESIAN_POINT('Ctrl Pts',(13.1571189604461,3.29872408622477,127.156401946547));
#68966=CARTESIAN_POINT('Ctrl Pts',(13.149344626327,3.19753516094088,127.064900267061));
#68967=CARTESIAN_POINT('Ctrl Pts',(13.141570292208,3.09237589448637,126.977467090686));
#68968=CARTESIAN_POINT('Ctrl Pts',(13.1337959580889,2.9836072931589,126.894466682597));
#68969=CARTESIAN_POINT('Ctrl Pts',(13.1260312051418,2.8749727394115,126.811568565093));
#68970=CARTESIAN_POINT('Ctrl Pts',(13.1182664521946,2.76273800917329,126.73309258105));
#68971=CARTESIAN_POINT('Ctrl Pts',(13.1105016992475,2.64729990355545,126.659365287878));
#68972=CARTESIAN_POINT('Ctrl Pts',(13.1027446583625,2.53197645269135,126.585711221693));
#68973=CARTESIAN_POINT('Ctrl Pts',(13.0949876174775,2.41345628541489,126.516796669476));
#68974=CARTESIAN_POINT('Ctrl Pts',(13.0872305765925,2.29216785450756,126.452906884701));
#68975=CARTESIAN_POINT('Ctrl Pts',(13.0794793853524,2.1709708881503,126.389065279711));
#68976=CARTESIAN_POINT('Ctrl Pts',(13.0717281941123,2.04701015785136,126.330241081431));
#68977=CARTESIAN_POINT('Ctrl Pts',(13.0639770028722,1.92074126206259,126.276675108754));
#68978=CARTESIAN_POINT('Ctrl Pts',(13.0562291060951,1.79452603392217,126.223131903043));
#68979=CARTESIAN_POINT('Ctrl Pts',(13.048481209318,1.66600495065421,126.174842630283));
#68980=CARTESIAN_POINT('Ctrl Pts',(13.040733312541,1.53565607017141,126.132001096227));
#68981=CARTESIAN_POINT('Ctrl Pts',(13.0329870364569,1.40533445586477,126.089168523697));
#68982=CARTESIAN_POINT('Ctrl Pts',(13.0252407603729,1.2731861760135,126.051781545242));
#68983=CARTESIAN_POINT('Ctrl Pts',(13.0174944842888,1.13970665316326,126.019984816353));
#68984=CARTESIAN_POINT('Ctrl Pts',(13.0097481510234,1.00622614499769,125.988187852748));
#68985=CARTESIAN_POINT('Ctrl Pts',(13.002001817758,0.871414754547387,125.961981311651));
#68986=CARTESIAN_POINT('Ctrl Pts',(12.9942554844927,0.735779971831289,125.941459128172));
#68987=CARTESIAN_POINT('Ctrl Pts',(12.9865074164897,0.600114814645843,125.920932348892));
#68988=CARTESIAN_POINT('Ctrl Pts',(12.9787593484868,0.463626284765305,125.906092518776));
#68989=CARTESIAN_POINT('Ctrl Pts',(12.9710112804839,0.326828503005363,125.896981867956));
#68990=CARTESIAN_POINT('Ctrl Pts',(12.963254977742,0.189885330934866,125.887861534228));
#68991=CARTESIAN_POINT('Ctrl Pts',(12.9554986750001,0.0526326411411423,
125.884482569333));
#68992=CARTESIAN_POINT('Ctrl Pts',(12.9477423722583,-0.0844133643174855,
125.886835076562));
#68993=CARTESIAN_POINT('Ctrl Pts',(12.9399819297441,-0.221532515355789,
125.889188839396));
#68994=CARTESIAN_POINT('Ctrl Pts',(12.9322214872299,-0.358444372156434,
125.897280146735));
#68995=CARTESIAN_POINT('Ctrl Pts',(12.9244610447157,-0.494637334681499,
125.911047121617));
#68996=CARTESIAN_POINT('Ctrl Pts',(12.9166881444503,-0.631048926240653,
125.924836196468));
#68997=CARTESIAN_POINT('Ctrl Pts',(12.9089152441849,-0.766738930179669,
125.944319090115));
#68998=CARTESIAN_POINT('Ctrl Pts',(12.9011423439194,-0.901204534882882,
125.969382494678));
#68999=CARTESIAN_POINT('Ctrl Pts',(12.8936520081573,-1.03078197615781,125.993534781354));
#69000=CARTESIAN_POINT('Ctrl Pts',(12.8861616723953,-1.15922219238532,126.022868823197));
#69001=CARTESIAN_POINT('Ctrl Pts',(12.8786713366332,-1.28609000106636,126.057239851074));
#69002=CARTESIAN_POINT('Ctrl Pts',(12.8708970025141,-1.41776804127254,126.09291406692));
#69003=CARTESIAN_POINT('Ctrl Pts',(12.863122668395,-1.54816920096978,126.134127768548));
#69004=CARTESIAN_POINT('Ctrl Pts',(12.855348334276,-1.67679188082675,126.180774125362));
#69005=CARTESIAN_POINT('Ctrl Pts',(12.8475835813289,-1.80525604472684,126.22736299471));
#69006=CARTESIAN_POINT('Ctrl Pts',(12.8398188283817,-1.93194572583687,126.279371065655));
#69007=CARTESIAN_POINT('Ctrl Pts',(12.8320540754346,-2.05637170146708,126.336641010439));
#69008=CARTESIAN_POINT('Ctrl Pts',(12.8242970345496,-2.18067409546403,126.393854073907));
#69009=CARTESIAN_POINT('Ctrl Pts',(12.8165399936646,-2.30271690543444,126.456318448498));
#69010=CARTESIAN_POINT('Ctrl Pts',(12.8087829527796,-2.42202855035795,126.523827851221));
#69011=CARTESIAN_POINT('Ctrl Pts',(12.8010317615395,-2.54125022144256,126.59128634458));
#69012=CARTESIAN_POINT('Ctrl Pts',(12.7932805702993,-2.65774448808031,126.6637821017));
#69013=CARTESIAN_POINT('Ctrl Pts',(12.7855293790591,-2.77106248042518,126.741061983195));
#69014=CARTESIAN_POINT('Ctrl Pts',(12.777781482282,-2.88433230959951,126.818309018679));
#69015=CARTESIAN_POINT('Ctrl Pts',(12.7700335855049,-2.99442822720415,126.90033591448));
#69016=CARTESIAN_POINT('Ctrl Pts',(12.7622856887279,-3.10092877698945,126.986845223682));
#69017=CARTESIAN_POINT('Ctrl Pts',(12.7545394126438,-3.20740704915576,127.073336437002));
#69018=CARTESIAN_POINT('Ctrl Pts',(12.7467931365598,-3.3102911461455,127.164307952392));
#69019=CARTESIAN_POINT('Ctrl Pts',(12.7390468604757,-3.40919157720906,127.25942114666));
#69020=CARTESIAN_POINT('Ctrl Pts',(12.7313005272103,-3.50809273833326,127.354535043032));
#69021=CARTESIAN_POINT('Ctrl Pts',(12.723554193945,-3.6030098930557,127.453790408282));
#69022=CARTESIAN_POINT('Ctrl Pts',(12.7158078606796,-3.69358970035717,127.556811050906));
#69023=CARTESIAN_POINT('Ctrl Pts',(12.7080597926766,-3.78418979237833,127.659854764288));
#69024=CARTESIAN_POINT('Ctrl Pts',(12.7003117246737,-3.87045034605917,127.766665139372));
#69025=CARTESIAN_POINT('Ctrl Pts',(12.6925636566707,-3.95205793713351,127.876832458173));
#69026=CARTESIAN_POINT('Ctrl Pts',(12.6848073539289,-4.03375226172667,127.987116864111));
#69027=CARTESIAN_POINT('Ctrl Pts',(12.6770510511871,-4.11078351200734,128.100765026171));
#69028=CARTESIAN_POINT('Ctrl Pts',(12.6692947484452,-4.18288099453353,128.217337299528));
#69029=CARTESIAN_POINT('Ctrl Pts',(12.6615343059311,-4.25501695765696,128.333971791018));
#69030=CARTESIAN_POINT('Ctrl Pts',(12.6537738634169,-4.32221371449295,128.453533162948));
#69031=CARTESIAN_POINT('Ctrl Pts',(12.6460134209027,-4.38424679156678,128.575557545705));
#69032=CARTESIAN_POINT('Ctrl Pts',(12.6382405206373,-4.44637944964296,128.697777812835));
#69033=CARTESIAN_POINT('Ctrl Pts',(12.630467620372,-4.50333170097486,128.822468636001));
#69034=CARTESIAN_POINT('Ctrl Pts',(12.6226947201066,-4.55492709273088,128.949145739875));
#69035=CARTESIAN_POINT('Ctrl Pts',(12.6152043843445,-4.60464686203589,129.071217811943));
#69036=CARTESIAN_POINT('Ctrl Pts',(12.6077140485824,-4.64939237604732,129.195133969611));
#69037=CARTESIAN_POINT('Ctrl Pts',(12.6002237128204,-4.68905020636647,129.320449830263));
#69038=CARTESIAN_POINT('Ctrl Pts',(12.5950477082595,-4.71645473363021,129.407046144085));
#69039=CARTESIAN_POINT('Ctrl Pts',(12.5898717036987,-4.74146979795504,129.494432598722));
#69040=CARTESIAN_POINT('Ctrl Pts',(12.5846956991378,-4.76405452823411,129.582490119308));
#69041=CARTESIAN_POINT('Ctrl Pts',(14.334952816073,-4.76405452823406,129.582490119308));
#69042=CARTESIAN_POINT('Ctrl Pts',(14.3271912810888,-4.7981176509159,129.715301717665));
#69043=CARTESIAN_POINT('Ctrl Pts',(14.3194297461047,-4.82659387817116,129.849425848687));
#69044=CARTESIAN_POINT('Ctrl Pts',(14.3116682111206,-4.84940926176714,129.984352767368));
#69045=CARTESIAN_POINT('Ctrl Pts',(14.3038947053308,-4.87225983408868,130.119487787143));
#69046=CARTESIAN_POINT('Ctrl Pts',(14.296121199541,-4.88943207225405,130.255427680485));
#69047=CARTESIAN_POINT('Ctrl Pts',(14.2883476937511,-4.90090395618872,130.39165797072));
#69048=CARTESIAN_POINT('Ctrl Pts',(14.2825349477333,-4.90948221540155,130.493526046524));
#69049=CARTESIAN_POINT('Ctrl Pts',(14.2767222017155,-4.91487420243906,130.595556415439));
#69050=CARTESIAN_POINT('Ctrl Pts',(14.2709094556978,-4.91708972550395,130.697535087642));
#69051=CARTESIAN_POINT('Ctrl Pts',(14.2688927824623,-4.91785837874528,130.73291555295));
#69052=CARTESIAN_POINT('Ctrl Pts',(14.2668761092268,-4.91824517299084,130.768304344428));
#69053=CARTESIAN_POINT('Ctrl Pts',(14.2648594359913,-4.91824995510306,130.803696066023));
#69054=CARTESIAN_POINT('',(14.6101405639733,-4.91824806987161,130.808717876352));
#69055=CARTESIAN_POINT('Ctrl Pts',(14.6800959310998,-4.76405452823407,129.582490119308));
#69056=CARTESIAN_POINT('Ctrl Pts',(14.6724074655865,-4.79790923889645,129.714489122364));
#69057=CARTESIAN_POINT('Ctrl Pts',(14.6647190000732,-4.8262769048776,129.847908572509));
#69058=CARTESIAN_POINT('Ctrl Pts',(14.6570305345599,-4.84905312519189,129.982249401509));
#69059=CARTESIAN_POINT('Ctrl Pts',(14.649215539468,-4.87220417524972,130.118801086295));
#69060=CARTESIAN_POINT('Ctrl Pts',(14.6414005443761,-4.88957802181369,130.256304331193));
#69061=CARTESIAN_POINT('Ctrl Pts',(14.6335855492843,-4.90111961205373,130.39422696759));
#69062=CARTESIAN_POINT('Ctrl Pts',(14.6257705541924,-4.91266120229374,130.532149603987));
#69063=CARTESIAN_POINT('Ctrl Pts',(14.6179555591006,-4.91837053000324,130.670491201671));
#69064=CARTESIAN_POINT('Ctrl Pts',(14.6101405640088,-4.91824806987217,130.808717875725));
#69065=CARTESIAN_POINT('Ctrl Pts',(14.6101405639733,-4.91824806987162,130.808717876352));
#69066=CARTESIAN_POINT('Ctrl Pts',(14.6006828491783,-4.91809986847844,130.9759999341));
#69067=CARTESIAN_POINT('Ctrl Pts',(14.5912251343833,-4.90941345961392,131.142904723301));
#69068=CARTESIAN_POINT('Ctrl Pts',(14.5817674195883,-4.89232631017948,131.308668397821));
#69069=CARTESIAN_POINT('Ctrl Pts',(14.5721703630257,-4.87498741350398,131.476874290564));
#69070=CARTESIAN_POINT('Ctrl Pts',(14.5625733064631,-4.84899846510879,131.643905236848));
#69071=CARTESIAN_POINT('Ctrl Pts',(14.5529762499004,-4.81455199274701,131.808986006274));
#69072=CARTESIAN_POINT('Ctrl Pts',(14.545240194384,-4.78678516436619,131.942055347757));
#69073=CARTESIAN_POINT('Ctrl Pts',(14.5375041388675,-4.7535237939816,132.073857971543));
#69074=CARTESIAN_POINT('Ctrl Pts',(14.5297680833511,-4.71489109911027,132.203998065633));
#69075=CARTESIAN_POINT('Ctrl Pts',(14.5219937492321,-4.67606724666873,132.334782103001));
#69076=CARTESIAN_POINT('Ctrl Pts',(14.514219415113,-4.63173614529118,132.464156695185));
#69077=CARTESIAN_POINT('Ctrl Pts',(14.506445080994,-4.58201663181093,132.591622950943));
#69078=CARTESIAN_POINT('Ctrl Pts',(14.4986803280469,-4.53235839318747,132.718932115932));
#69079=CARTESIAN_POINT('Ctrl Pts',(14.4909155750999,-4.47732509625781,132.844337263243));
#69080=CARTESIAN_POINT('Ctrl Pts',(14.4831508221528,-4.41708576346771,132.967353086501));
#69081=CARTESIAN_POINT('Ctrl Pts',(14.4753937812678,-4.35690626123224,133.09024672871));
#69082=CARTESIAN_POINT('Ctrl Pts',(14.4676367403828,-4.29153118390861,133.210755420609));
#69083=CARTESIAN_POINT('Ctrl Pts',(14.4598796994979,-4.22117807172571,133.328412667204));
#69084=CARTESIAN_POINT('Ctrl Pts',(14.4521285082578,-4.15087801337197,133.445981187555));
#69085=CARTESIAN_POINT('Ctrl Pts',(14.4443773170177,-4.07560759205015,133.560702208443));
#69086=CARTESIAN_POINT('Ctrl Pts',(14.4366261257776,-3.99563064588826,133.672133063932));
#69087=CARTESIAN_POINT('Ctrl Pts',(14.4288782290005,-3.91568769206196,133.783516558336));
#69088=CARTESIAN_POINT('Ctrl Pts',(14.4211303322236,-3.83104241952575,133.89161235171));
#69089=CARTESIAN_POINT('Ctrl Pts',(14.4133824354465,-3.74200230332689,133.99600624708));
#69090=CARTESIAN_POINT('Ctrl Pts',(14.4056361593625,-3.65298081240086,134.100378305497));
#69091=CARTESIAN_POINT('Ctrl Pts',(14.3978898832784,-3.55956655991525,134.201049708876));
#69092=CARTESIAN_POINT('Ctrl Pts',(14.3901436071943,-3.46210741825086,134.297639204652));
#69093=CARTESIAN_POINT('Ctrl Pts',(14.382397273929,-3.36464755716523,134.39422941343));
#69094=CARTESIAN_POINT('Ctrl Pts',(14.3746509406637,-3.26314302501076,134.486737379268));
#69095=CARTESIAN_POINT('Ctrl Pts',(14.3669046073984,-3.1579783841685,134.574818890459));
#69096=CARTESIAN_POINT('Ctrl Pts',(14.3591565393954,-3.05279019243393,134.662920126893));
#69097=CARTESIAN_POINT('Ctrl Pts',(14.3514084713925,-2.9439405606578,134.746592685173));
#69098=CARTESIAN_POINT('Ctrl Pts',(14.3436604033895,-2.83184661015392,134.825533063391));
#69099=CARTESIAN_POINT('Ctrl Pts',(14.3359041006477,-2.71963352486567,134.904557340382));
#69100=CARTESIAN_POINT('Ctrl Pts',(14.3281477979059,-2.60416955306115,134.978839165039));
#69101=CARTESIAN_POINT('Ctrl Pts',(14.3203914951641,-2.48590070885261,135.048118472136));
#69102=CARTESIAN_POINT('Ctrl Pts',(14.31263105265,-2.36756874100076,135.117434755686));
#69103=CARTESIAN_POINT('Ctrl Pts',(14.3048706101358,-2.24642926291042,135.181743018257));
#69104=CARTESIAN_POINT('Ctrl Pts',(14.2971101676216,-2.1229513973547,135.24082998261));
#69105=CARTESIAN_POINT('Ctrl Pts',(14.2893372673562,-1.99927531416751,135.300011798603));
#69106=CARTESIAN_POINT('Ctrl Pts',(14.2815643670909,-1.87325370188042,135.353955413148));
#69107=CARTESIAN_POINT('Ctrl Pts',(14.2737914668255,-1.74537493074503,135.402496045501));
#69108=CARTESIAN_POINT('Ctrl Pts',(14.2663011310631,-1.62214487504086,135.449272103603));
#69109=CARTESIAN_POINT('Ctrl Pts',(14.2588107953007,-1.49719063320006,135.491031085904));
#69110=CARTESIAN_POINT('Ctrl Pts',(14.2513204595383,-1.37095918183447,135.527670260628));
#69111=CARTESIAN_POINT('Ctrl Pts',(14.2435461254192,-1.2399416266296,135.565698620796));
#69112=CARTESIAN_POINT('Ctrl Pts',(14.2357717913002,-1.10713307500333,135.598331736911));
#69113=CARTESIAN_POINT('Ctrl Pts',(14.2279974571811,-0.973017492499181,
135.625399926863));
#69114=CARTESIAN_POINT('Ctrl Pts',(14.220232704234,-0.839067195464393,135.652434757691));
#69115=CARTESIAN_POINT('Ctrl Pts',(14.2124679512869,-0.703813452119732,
135.673918231672));
#69116=CARTESIAN_POINT('Ctrl Pts',(14.2047031983398,-0.567755925222235,
135.689730232229));
#69117=CARTESIAN_POINT('Ctrl Pts',(14.1969461574548,-0.431833532578712,
135.705526528084));
#69118=CARTESIAN_POINT('Ctrl Pts',(14.1891891165698,-0.295109330931846,
135.715662515573));
#69119=CARTESIAN_POINT('Ctrl Pts',(14.1814320756848,-0.158093381539117,
135.720069065513));
#69120=CARTESIAN_POINT('Ctrl Pts',(14.1736808844447,-0.021180756939468,
135.724472292439));
#69121=CARTESIAN_POINT('Ctrl Pts',(14.1659296932045,0.116022788308936,135.723154669218));
#69122=CARTESIAN_POINT('Ctrl Pts',(14.1581785019644,0.253002215864965,135.716098898589));
#69123=CARTESIAN_POINT('Ctrl Pts',(14.1504306051873,0.389923423510236,135.709046126851));
#69124=CARTESIAN_POINT('Ctrl Pts',(14.1426827084102,0.526620313289917,135.696260078493));
#69125=CARTESIAN_POINT('Ctrl Pts',(14.1349348116331,0.66257821178492,135.677775557397));
#69126=CARTESIAN_POINT('Ctrl Pts',(14.127188535549,0.798507670818471,135.659294902865));
#69127=CARTESIAN_POINT('Ctrl Pts',(14.119442259465,0.933698058881814,135.635118199181));
#69128=CARTESIAN_POINT('Ctrl Pts',(14.1116959833809,1.06764058387698,135.605332044908));
#69129=CARTESIAN_POINT('Ctrl Pts',(14.1039496501156,1.20158409760543,135.575545670762));
#69130=CARTESIAN_POINT('Ctrl Pts',(14.0962033168502,1.33427934824253,135.54014984827));
#69131=CARTESIAN_POINT('Ctrl Pts',(14.0884569835848,1.46522887537027,135.499282065821));
#69132=CARTESIAN_POINT('Ctrl Pts',(14.0807089155818,1.59620772773667,135.458405131315));
#69133=CARTESIAN_POINT('Ctrl Pts',(14.0729608475789,1.72543970552228,135.412053914885));
#69134=CARTESIAN_POINT('Ctrl Pts',(14.0652127795759,1.85244399971922,135.360415302313));
#69135=CARTESIAN_POINT('Ctrl Pts',(14.057456476834,1.9795832755914,135.308721807609));
#69136=CARTESIAN_POINT('Ctrl Pts',(14.0497001740922,2.10448977557084,135.251729838681));
#69137=CARTESIAN_POINT('Ctrl Pts',(14.0419438713504,2.22670361789578,135.189674068227));
#69138=CARTESIAN_POINT('Ctrl Pts',(14.0341834288362,2.34898268942833,135.12758517674));
#69139=CARTESIAN_POINT('Ctrl Pts',(14.026422986322,2.46856589893843,135.06042728971));
#69140=CARTESIAN_POINT('Ctrl Pts',(14.0186625438078,2.58502023792568,134.988479811855));
#69141=CARTESIAN_POINT('Ctrl Pts',(14.0108896435423,2.70166151975621,134.91641683752));
#69142=CARTESIAN_POINT('Ctrl Pts',(14.003116743277,2.81516357012621,134.839549127293));
#69143=CARTESIAN_POINT('Ctrl Pts',(13.9953438430115,2.92512377827804,134.758198492878));
#69144=CARTESIAN_POINT('Ctrl Pts',(13.9878535072495,3.03108665589094,134.679805158934));
#69145=CARTESIAN_POINT('Ctrl Pts',(13.9803631714874,3.13376049026414,134.597249366343));
#69146=CARTESIAN_POINT('Ctrl Pts',(13.9728728357253,3.23281724846769,134.510851640152));
#69147=CARTESIAN_POINT('Ctrl Pts',(13.9650985016062,3.33562977376589,134.421178117913));
#69148=CARTESIAN_POINT('Ctrl Pts',(13.9573241674871,3.4348712047546,134.327081518464));
#69149=CARTESIAN_POINT('Ctrl Pts',(13.949549833368,3.53013718787154,134.228877298399));
#69150=CARTESIAN_POINT('Ctrl Pts',(13.9417850804209,3.62528576417846,134.130794106259));
#69151=CARTESIAN_POINT('Ctrl Pts',(13.9340203274738,3.71646837131698,134.028613643848));
#69152=CARTESIAN_POINT('Ctrl Pts',(13.9262555745267,3.80331387188264,133.92269136565));
#69153=CARTESIAN_POINT('Ctrl Pts',(13.9184985336417,3.89007311627284,133.816874290952));
#69154=CARTESIAN_POINT('Ctrl Pts',(13.9107414927567,3.97250358027798,133.707323096698));
#69155=CARTESIAN_POINT('Ctrl Pts',(13.9029844518717,4.05027140298973,133.594429545859));
#69156=CARTESIAN_POINT('Ctrl Pts',(13.8952332606315,4.12798058038143,133.481621128924));
#69157=CARTESIAN_POINT('Ctrl Pts',(13.8874820693913,4.20103389423856,133.365475692964));
#69158=CARTESIAN_POINT('Ctrl Pts',(13.8797308781512,4.26913840108136,133.24641720473));
#69159=CARTESIAN_POINT('Ctrl Pts',(13.8719829813741,4.33721396169201,133.12740931953));
#69160=CARTESIAN_POINT('Ctrl Pts',(13.8642350845971,4.40034470502147,133.005491183247));
#69161=CARTESIAN_POINT('Ctrl Pts',(13.85648718782,4.45828171900775,132.881114617553));
#69162=CARTESIAN_POINT('Ctrl Pts',(13.8487409117359,4.51620661381969,132.756764068755));
#69163=CARTESIAN_POINT('Ctrl Pts',(13.8409946356517,4.56893977524758,132.629956467597));
#69164=CARTESIAN_POINT('Ctrl Pts',(13.8332483595676,4.61627904655845,132.501166683917));
#69165=CARTESIAN_POINT('Ctrl Pts',(13.8255020263022,4.663618667317,132.372375949541));
#69166=CARTESIAN_POINT('Ctrl Pts',(13.8177556930369,4.70556418362389,132.241603370407));
#69167=CARTESIAN_POINT('Ctrl Pts',(13.8100093597715,4.74196237884601,132.109341789886));
#69168=CARTESIAN_POINT('Ctrl Pts',(13.8022612917685,4.77836872519158,131.977050590301));
#69169=CARTESIAN_POINT('Ctrl Pts',(13.7945132237656,4.80922517473416,131.843270102678));
#69170=CARTESIAN_POINT('Ctrl Pts',(13.7867651557626,4.83442907076123,131.708505861583));
#69171=CARTESIAN_POINT('Ctrl Pts',(13.7790088530207,4.85965975378897,131.573598391449));
#69172=CARTESIAN_POINT('Ctrl Pts',(13.7712525502789,4.87922581048319,131.437705464168));
#69173=CARTESIAN_POINT('Ctrl Pts',(13.763496247537,4.89307610030521,131.301340837617));
#69174=CARTESIAN_POINT('Ctrl Pts',(13.7557358050229,4.90693378244394,131.164903429159));
#69175=CARTESIAN_POINT('Ctrl Pts',(13.7479753625086,4.91506959579771,131.027994209863));
#69176=CARTESIAN_POINT('Ctrl Pts',(13.7402149199945,4.91748455979706,130.891128507119));
#69177=CARTESIAN_POINT('Ctrl Pts',(13.732442019729,4.91990340051102,130.754043095398));
#69178=CARTESIAN_POINT('Ctrl Pts',(13.7246691194636,4.91658304955627,130.617001730901));
#69179=CARTESIAN_POINT('Ctrl Pts',(13.7168962191981,4.90757663528673,130.480517088546));
#69180=CARTESIAN_POINT('Ctrl Pts',(13.7094058834363,4.89889762686187,130.348994006729));
#69181=CARTESIAN_POINT('Ctrl Pts',(13.7019155476744,4.88493881588,130.217988179567));
#69182=CARTESIAN_POINT('Ctrl Pts',(13.6944252119125,4.86579255933035,130.087948842073));
#69183=CARTESIAN_POINT('Ctrl Pts',(13.6866508777935,4.84592036664384,129.95297902357));
#69184=CARTESIAN_POINT('Ctrl Pts',(13.6788765436744,4.82039665012975,129.818622886577));
#69185=CARTESIAN_POINT('Ctrl Pts',(13.6711022095553,4.789268249377,129.685391137192));
#69186=CARTESIAN_POINT('Ctrl Pts',(13.6633374566082,4.75817821159616,129.55232358403));
#69187=CARTESIAN_POINT('Ctrl Pts',(13.6555727036611,4.72149732108605,129.420378038389));
#69188=CARTESIAN_POINT('Ctrl Pts',(13.6478079507141,4.67932402293845,129.29005888051));
#69189=CARTESIAN_POINT('Ctrl Pts',(13.6400509098291,4.63719261190517,129.159869157455));
#69190=CARTESIAN_POINT('Ctrl Pts',(13.6322938689441,4.58957976879964,129.031302977105));
#69191=CARTESIAN_POINT('Ctrl Pts',(13.6245368280591,4.53663463492747,128.904852983552));
#69192=CARTESIAN_POINT('Ctrl Pts',(13.6167856368189,4.48372942739252,128.778498346923));
#69193=CARTESIAN_POINT('Ctrl Pts',(13.6090344455789,4.42550008327639,128.654257079851));
#69194=CARTESIAN_POINT('Ctrl Pts',(13.6012832543387,4.36214495470752,128.532604808369));
#69195=CARTESIAN_POINT('Ctrl Pts',(13.5935353575617,4.29881675375834,128.411004242348));
#69196=CARTESIAN_POINT('Ctrl Pts',(13.5857874607845,4.23036728162606,128.291990829352));
#69197=CARTESIAN_POINT('Ctrl Pts',(13.5780395640075,4.15704212563074,128.1760182068));
#69198=CARTESIAN_POINT('Ctrl Pts',(13.5702932879234,4.08373230767745,128.060069843221));
#69199=CARTESIAN_POINT('Ctrl Pts',(13.5625470118393,4.00554904327596,127.947161335157));
#69200=CARTESIAN_POINT('Ctrl Pts',(13.5548007357552,3.92278258322002,127.837719441541));
#69201=CARTESIAN_POINT('Ctrl Pts',(13.5470544024899,3.84001551220088,127.72827674005));
#69202=CARTESIAN_POINT('Ctrl Pts',(13.5393080692245,3.75266541384422,127.622301015903));
#69203=CARTESIAN_POINT('Ctrl Pts',(13.5315617359591,3.6610641139026,127.520187568472));
#69204=CARTESIAN_POINT('Ctrl Pts',(13.5238136679562,3.56944230048484,127.418051253442));
#69205=CARTESIAN_POINT('Ctrl Pts',(13.5160655999532,3.47356765207634,127.319779227212));
#69206=CARTESIAN_POINT('Ctrl Pts',(13.5083175319503,3.37381000076367,127.225731111561));
#69207=CARTESIAN_POINT('Ctrl Pts',(13.5005612292084,3.27394632583218,127.131583040454));
#69208=CARTESIAN_POINT('Ctrl Pts',(13.4928049264665,3.17019168899456,127.041668116254));
#69209=CARTESIAN_POINT('Ctrl Pts',(13.4850486237247,3.0629506865919,126.956307063624));
#69210=CARTESIAN_POINT('Ctrl Pts',(13.4772881812105,2.95565244643715,126.87090045123));
#69211=CARTESIAN_POINT('Ctrl Pts',(13.4695277386964,2.8448644486195,126.790052783814));
#69212=CARTESIAN_POINT('Ctrl Pts',(13.4617672961822,2.73102080369358,126.714041750742));
#69213=CARTESIAN_POINT('Ctrl Pts',(13.4539943959168,2.61699440684225,126.637908698012));
#69214=CARTESIAN_POINT('Ctrl Pts',(13.4462214956514,2.49990289488248,126.566627998375));
#69215=CARTESIAN_POINT('Ctrl Pts',(13.4384485953859,2.380206312918,126.50043206676));
#69216=CARTESIAN_POINT('Ctrl Pts',(13.4309582596238,2.26486100320381,126.436642523995));
#69217=CARTESIAN_POINT('Ctrl Pts',(13.4234679238617,2.14709701223217,126.37757461743));
#69218=CARTESIAN_POINT('Ctrl Pts',(13.4159775880996,2.02734221535028,126.32339346701));
#69219=CARTESIAN_POINT('Ctrl Pts',(13.4082032539805,1.9030468789475,126.267158021805));
#69220=CARTESIAN_POINT('Ctrl Pts',(13.4004289198614,1.77621306350427,126.216009073502));
#69221=CARTESIAN_POINT('Ctrl Pts',(13.3926545857423,1.64729575846675,126.170183263748));
#69222=CARTESIAN_POINT('Ctrl Pts',(13.3848898327953,1.51853733248636,126.12441393021));
#69223=CARTESIAN_POINT('Ctrl Pts',(13.3771250798482,1.38770089074569,126.083954811885));
#69224=CARTESIAN_POINT('Ctrl Pts',(13.3693603269011,1.25526399460268,126.04899571397));
#69225=CARTESIAN_POINT('Ctrl Pts',(13.3616032860161,1.12295863665178,126.014071337924));
#69226=CARTESIAN_POINT('Ctrl Pts',(13.3538462451311,0.989056363232963,125.984636210412));
#69227=CARTESIAN_POINT('Ctrl Pts',(13.3460892042461,0.854052264291844,125.960831140794));
#69228=CARTESIAN_POINT('Ctrl Pts',(13.338338013006,0.719149972991915,125.937044022765));
#69229=CARTESIAN_POINT('Ctrl Pts',(13.3305868217659,0.583147893483745,125.918878579497));
#69230=CARTESIAN_POINT('Ctrl Pts',(13.3228356305258,0.446553397587962,125.906425019214));
#69231=CARTESIAN_POINT('Ctrl Pts',(13.3150877337487,0.310016957996711,125.893976752027));
#69232=CARTESIAN_POINT('Ctrl Pts',(13.3073398369715,0.172888991349683,125.887235574733));
#69233=CARTESIAN_POINT('Ctrl Pts',(13.2995919401945,0.0356839015994468,
125.88624006987));
#69234=CARTESIAN_POINT('Ctrl Pts',(13.2918456641104,-0.101492487804,125.885244773246));
#69235=CARTESIAN_POINT('Ctrl Pts',(13.2840993880262,-0.238745577515022,
125.889992761299));
#69236=CARTESIAN_POINT('Ctrl Pts',(13.2763531119421,-0.37555943551309,125.900470511446));
#69237=CARTESIAN_POINT('Ctrl Pts',(13.2686067786768,-0.512374303439792,
125.910948338938));
#69238=CARTESIAN_POINT('Ctrl Pts',(13.2608604454115,-0.648749543360048,
125.927155983066));
#69239=CARTESIAN_POINT('Ctrl Pts',(13.2531141121461,-0.784173218791643,
125.949027938395));
#69240=CARTESIAN_POINT('Ctrl Pts',(13.2453660441432,-0.91962722141639,125.970904791796));
#69241=CARTESIAN_POINT('Ctrl Pts',(13.2376179761402,-1.05412884962571,125.998448418208));
#69242=CARTESIAN_POINT('Ctrl Pts',(13.2298699081372,-1.18717564015418,126.031542051779));
#69243=CARTESIAN_POINT('Ctrl Pts',(13.2221136053954,-1.3203638343949,126.064670857657));
#69244=CARTESIAN_POINT('Ctrl Pts',(13.2143573026535,-1.45209372220673,126.103361359288));
#69245=CARTESIAN_POINT('Ctrl Pts',(13.2066009999117,-1.58187677464065,126.147446517827));
#69246=CARTESIAN_POINT('Ctrl Pts',(13.1988405573975,-1.71172909619735,126.191555205941));
#69247=CARTESIAN_POINT('Ctrl Pts',(13.1910801148834,-1.83963214748684,126.241064147132));
#69248=CARTESIAN_POINT('Ctrl Pts',(13.1833196723692,-1.96511765322266,126.29575820978));
#69249=CARTESIAN_POINT('Ctrl Pts',(13.1755467721038,-2.09080459943255,126.350540072193));
#69250=CARTESIAN_POINT('Ctrl Pts',(13.1677738718383,-2.21406589314516,126.410523518127));
#69251=CARTESIAN_POINT('Ctrl Pts',(13.1600009715729,-2.33445733148285,126.475447124553));
#69252=CARTESIAN_POINT('Ctrl Pts',(13.1525106358108,-2.4504722377899,126.538010594354));
#69253=CARTESIAN_POINT('Ctrl Pts',(13.1450203000487,-2.56382205413805,126.605161128895));
#69254=CARTESIAN_POINT('Ctrl Pts',(13.1375299642867,-2.67413658336338,126.676627995894));
#69255=CARTESIAN_POINT('Ctrl Pts',(13.1297595003965,-2.7885767223821,126.750767624209));
#69256=CARTESIAN_POINT('Ctrl Pts',(13.1219890365063,-2.90011380735081,126.829788347022));
#69257=CARTESIAN_POINT('Ctrl Pts',(13.1142185726161,-3.00830292214689,126.91343571581));
#69258=CARTESIAN_POINT('Ctrl Pts',(13.1064604100668,-3.11632076387646,126.996950663316));
#69259=CARTESIAN_POINT('Ctrl Pts',(13.0987022475175,-3.22100088449626,127.085077431815));
#69260=CARTESIAN_POINT('Ctrl Pts',(13.0909440849681,-3.32192599673668,127.177517536496));
#69261=CARTESIAN_POINT('Ctrl Pts',(13.0831930221195,-3.42275874972563,127.269873046781));
#69262=CARTESIAN_POINT('Ctrl Pts',(13.0754419592708,-3.51984304309827,127.366533778881));
#69263=CARTESIAN_POINT('Ctrl Pts',(13.0676908964221,-3.61279320540572,127.467159946723));
#69264=CARTESIAN_POINT('Ctrl Pts',(13.0599452416455,-3.70567851452026,127.567715905669));
#69265=CARTESIAN_POINT('Ctrl Pts',(13.0521995868689,-3.79443516705613,127.672231509142));
#69266=CARTESIAN_POINT('Ctrl Pts',(13.0444539320923,-3.87871334140427,127.780329222605));
#69267=CARTESIAN_POINT('Ctrl Pts',(13.0367119978187,-3.96295103406133,127.888375013036));
#69268=CARTESIAN_POINT('Ctrl Pts',(13.0289700635451,-4.04271428975083,127.999999180904));
#69269=CARTESIAN_POINT('Ctrl Pts',(13.0212281292715,-4.11769295949528,128.11479043744));
#69270=CARTESIAN_POINT('Ctrl Pts',(13.0134865487772,-4.19266820297759,128.229576448419));
#69271=CARTESIAN_POINT('Ctrl Pts',(13.0057449682828,-4.26285907196028,128.347528938801));
#69272=CARTESIAN_POINT('Ctrl Pts',(12.9980033877885,-4.32799828600891,128.468206962773));
#69273=CARTESIAN_POINT('Ctrl Pts',(12.9902623349182,-4.39313306052229,128.588876761985));
#69274=CARTESIAN_POINT('Ctrl Pts',(12.982521282048,-4.4532166836464,128.712271378145));
#69275=CARTESIAN_POINT('Ctrl Pts',(12.9747802291778,-4.50802783479095,128.837925237684));
#69276=CARTESIAN_POINT('Ctrl Pts',(12.9670346006886,-4.56287138397525,128.963653369313));
#69277=CARTESIAN_POINT('Ctrl Pts',(12.9592889721994,-4.61243607931077,129.09164305243));
#69278=CARTESIAN_POINT('Ctrl Pts',(12.9515433437103,-4.65654867068509,129.221408457821));
#69279=CARTESIAN_POINT('Ctrl Pts',(12.944440529551,-4.69700033178115,129.340404554794));
#69280=CARTESIAN_POINT('Ctrl Pts',(12.9373377153916,-4.73286777220424,129.460893430873));
#69281=CARTESIAN_POINT('Ctrl Pts',(12.9302349012323,-4.7640545282341,129.582490119308));
#69282=CARTESIAN_POINT('Origin',(213.235140564004,0.,130.804360617566));
#69283=CARTESIAN_POINT('',(10.8346522545384,-4.76405452823402,129.582490119308));
#69284=CARTESIAN_POINT('',(11.1800167307073,-4.76405452823405,129.582490119308));
#69285=CARTESIAN_POINT('',(213.235140564004,-4.76405452823405,129.582490119308));
#69286=CARTESIAN_POINT('',(12.5148594360351,-4.91824821769922,130.800173542404));
#69287=CARTESIAN_POINT('Ctrl Pts',(12.5148594359913,-4.91824821769988,130.800173543179));
#69288=CARTESIAN_POINT('Ctrl Pts',(12.5068142965337,-4.91836943045601,130.942553249534));
#69289=CARTESIAN_POINT('Ctrl Pts',(12.498769157076,-4.91230289435018,131.085035942718));
#69290=CARTESIAN_POINT('Ctrl Pts',(12.4907240176183,-4.90005356047322,131.227040362756));
#69291=CARTESIAN_POINT('Ctrl Pts',(12.4830162607711,-4.88831791716201,131.363089656449));
#69292=CARTESIAN_POINT('Ctrl Pts',(12.4753085039239,-4.87090757015808,131.498699546133));
#69293=CARTESIAN_POINT('Ctrl Pts',(12.4676007470767,-4.84788005281825,131.63336125447));
#69294=CARTESIAN_POINT('Ctrl Pts',(12.459893497827,-4.82485405196521,131.768014094603));
#69295=CARTESIAN_POINT('Ctrl Pts',(12.4521862485774,-4.79621168283912,131.901718488149));
#69296=CARTESIAN_POINT('Ctrl Pts',(12.4444789993277,-4.76206193345132,132.033974054575));
#69297=CARTESIAN_POINT('Ctrl Pts',(12.4367705478664,-4.7279068572309,132.166250250824));
#69298=CARTESIAN_POINT('Ctrl Pts',(12.429062096405,-4.68824279042093,132.297076787814));
#69299=CARTESIAN_POINT('Ctrl Pts',(12.4213536449437,-4.64322898087268,132.425967133859));
#69300=CARTESIAN_POINT('Ctrl Pts',(12.4136422809646,-4.59819816356065,132.554906179105));
#69301=CARTESIAN_POINT('Ctrl Pts',(12.4059309169855,-4.54781371223153,132.681907205291));
#69302=CARTESIAN_POINT('Ctrl Pts',(12.3982195530064,-4.49228334782613,132.806502816648));
#69303=CARTESIAN_POINT('Ctrl Pts',(12.3904992836522,-4.43668885485341,132.931242315734));
#69304=CARTESIAN_POINT('Ctrl Pts',(12.3827790142979,-4.37593674684958,133.053570493914));
#69305=CARTESIAN_POINT('Ctrl Pts',(12.3750587449437,-4.31028129629677,133.173043418047));
#69306=CARTESIAN_POINT('Ctrl Pts',(12.3673332242949,-4.24458118718358,133.292597607159));
#69307=CARTESIAN_POINT('Ctrl Pts',(12.359607703646,-4.17397129776218,133.409292337912));
#69308=CARTESIAN_POINT('Ctrl Pts',(12.3518821829972,-4.09874908507779,133.522712875842));
#69309=CARTESIAN_POINT('Ctrl Pts',(12.3441454390979,-4.02341759332118,133.636298185463));
#69310=CARTESIAN_POINT('Ctrl Pts',(12.3364086951987,-3.94346063515098,133.746599490057));
#69311=CARTESIAN_POINT('Ctrl Pts',(12.3286719512995,-3.85921596973571,133.853235026497));
#69312=CARTESIAN_POINT('Ctrl Pts',(12.3263733305355,-3.83418650776852,133.884916915084));
#69313=CARTESIAN_POINT('Ctrl Pts',(12.3240747097715,-3.80877881157106,133.916275471344));
#69314=CARTESIAN_POINT('Ctrl Pts',(12.3217760890076,-3.78300234485484,133.947301329912));
#69315=CARTESIAN_POINT('Ctrl Pts',(12.3140017548885,-3.69582186349672,134.05223616502));
#69316=CARTESIAN_POINT('Ctrl Pts',(12.3062274207694,-3.60413388224911,134.153707075862));
#69317=CARTESIAN_POINT('Ctrl Pts',(12.2984530866503,-3.50824406349114,134.251302255233));
#69318=CARTESIAN_POINT('Ctrl Pts',(12.2906883337032,-3.41247242036487,134.348777157267));
#69319=CARTESIAN_POINT('Ctrl Pts',(12.2829235807562,-3.31250951455571,134.442385555422));
#69320=CARTESIAN_POINT('Ctrl Pts',(12.2751588278091,-3.20870179191121,134.531747889247));
#69321=CARTESIAN_POINT('Ctrl Pts',(12.2674017869241,-3.10499717256027,134.621021467141));
#69322=CARTESIAN_POINT('Ctrl Pts',(12.259644746039,-2.99745563019451,134.706057119805));
#69323=CARTESIAN_POINT('Ctrl Pts',(12.251887705154,-2.88646080322414,134.786511681244));
#69324=CARTESIAN_POINT('Ctrl Pts',(12.2441365139139,-2.77554967831635,134.866905571272));
#69325=CARTESIAN_POINT('Ctrl Pts',(12.2363853226737,-2.66119076747546,134.942725017794));
#69326=CARTESIAN_POINT('Ctrl Pts',(12.2286341314336,-2.5438008855245,135.013666987659));
#69327=CARTESIAN_POINT('Ctrl Pts',(12.2208862346565,-2.42646089740469,135.084578805294));
#69328=CARTESIAN_POINT('Ctrl Pts',(12.2131383378794,-2.30609283430186,135.150617067635));
#69329=CARTESIAN_POINT('Ctrl Pts',(12.2053904411023,-2.18314241457215,135.211522091825));
#69330=CARTESIAN_POINT('Ctrl Pts',(12.1976441650182,-2.06021771341975,135.272414375998));
#69331=CARTESIAN_POINT('Ctrl Pts',(12.1898978889341,-1.93471208019027,135.328175384359));
#69332=CARTESIAN_POINT('Ctrl Pts',(12.18215161285,-1.80709539676928,135.378591622825));
#69333=CARTESIAN_POINT('Ctrl Pts',(12.1744052795846,-1.67947777131093,135.429008233453));
#69334=CARTESIAN_POINT('Ctrl Pts',(12.1666589463192,-1.54974942818394,135.474079851807));
#69335=CARTESIAN_POINT('Ctrl Pts',(12.1589126130539,-1.4183993920549,135.513641478496));
#69336=CARTESIAN_POINT('Ctrl Pts',(12.1511645450509,-1.28701994099618,135.553211964736));
#69337=CARTESIAN_POINT('Ctrl Pts',(12.143416477048,-1.15401844855735,135.587269891213));
#69338=CARTESIAN_POINT('Ctrl Pts',(12.135668409045,-1.01989784024417,135.615700499342));
#69339=CARTESIAN_POINT('Ctrl Pts',(12.1279121063031,-0.88563468695223,135.644161323859));
#69340=CARTESIAN_POINT('Ctrl Pts',(12.1201558035612,-0.750250424888485,
135.666982801569));
#69341=CARTESIAN_POINT('Ctrl Pts',(12.1123995008194,-0.614257436747398,
135.684101477888));
#69342=CARTESIAN_POINT('Ctrl Pts',(12.1046390583052,-0.478191865053869,
135.701229290961));
#69343=CARTESIAN_POINT('Ctrl Pts',(12.0968786157911,-0.341517309318485,
135.712648205165));
#69344=CARTESIAN_POINT('Ctrl Pts',(12.0891181732769,-0.204748972992584,
135.7183468732));
#69345=CARTESIAN_POINT('Ctrl Pts',(12.0813452730115,-0.0677610839914891,
135.724054689243));
#69346=CARTESIAN_POINT('Ctrl Pts',(12.073572372746,0.0693204952466555,135.724023909351));
#69347=CARTESIAN_POINT('Ctrl Pts',(12.0657994724806,0.205981962504627,135.718295343793));
#69348=CARTESIAN_POINT('Ctrl Pts',(12.0583091367186,0.337675441197567,135.712775026023));
#69349=CARTESIAN_POINT('Ctrl Pts',(12.0508188009566,0.468978514894847,135.701964013463));
#69350=CARTESIAN_POINT('Ctrl Pts',(12.0433284651946,0.599439861640033,135.685943856104));
#69351=CARTESIAN_POINT('Ctrl Pts',(12.0355541310755,0.73484769000088,135.66931628961));
#69352=CARTESIAN_POINT('Ctrl Pts',(12.0277797969564,0.869777634565994,135.647024100123));
#69353=CARTESIAN_POINT('Ctrl Pts',(12.0200054628373,1.00371801228709,135.619101858205));
#69354=CARTESIAN_POINT('Ctrl Pts',(12.0122407098902,1.13749332046325,135.591214027955));
#69355=CARTESIAN_POINT('Ctrl Pts',(12.0044759569431,1.27028110927898,135.557710029917));
#69356=CARTESIAN_POINT('Ctrl Pts',(11.996711203996,1.40157478133202,135.518676177097));
#69357=CARTESIAN_POINT('Ctrl Pts',(11.988954163111,1.53273805065924,135.47968109325));
#69358=CARTESIAN_POINT('Ctrl Pts',(11.981197122226,1.66240978407772,135.435167195299));
#69359=CARTESIAN_POINT('Ctrl Pts',(11.973440081341,1.79009390038473,135.385271759501));
#69360=CARTESIAN_POINT('Ctrl Pts',(11.9656888901008,1.91768172910639,135.33541395024));
#69361=CARTESIAN_POINT('Ctrl Pts',(11.9579376988606,2.04328456146562,135.280182822575));
#69362=CARTESIAN_POINT('Ctrl Pts',(11.9501865076205,2.16642214849594,135.219765257801));
#69363=CARTESIAN_POINT('Ctrl Pts',(11.9424386108434,2.28950739876697,135.159373372103));
#69364=CARTESIAN_POINT('Ctrl Pts',(11.9346907140663,2.41012913743569,135.093799605484));
#69365=CARTESIAN_POINT('Ctrl Pts',(11.9269428172892,2.52782796430217,135.023278588491));
#69366=CARTESIAN_POINT('Ctrl Pts',(11.9191965412051,2.6455021711112,134.952772322975));
#69367=CARTESIAN_POINT('Ctrl Pts',(11.911450265121,2.76025434708535,134.877321066292));
#69368=CARTESIAN_POINT('Ctrl Pts',(11.9037039890369,2.87165089096896,134.797204744613));
#69369=CARTESIAN_POINT('Ctrl Pts',(11.8959576557715,2.9830482571564,134.717087831535));
#69370=CARTESIAN_POINT('Ctrl Pts',(11.8882113225061,3.09108962442339,134.63230601302));
#69371=CARTESIAN_POINT('Ctrl Pts',(11.8804649892408,3.19537184433061,134.54318153317));
#69372=CARTESIAN_POINT('Ctrl Pts',(11.8727169212378,3.29967741751793,134.454037094511));
#69373=CARTESIAN_POINT('Ctrl Pts',(11.8649688532349,3.40022187103907,134.360548313296));
#69374=CARTESIAN_POINT('Ctrl Pts',(11.8572207852319,3.49663681172535,134.263076285178));
#69375=CARTESIAN_POINT('Ctrl Pts',(11.84946448249,3.59315422335808,134.165500662629));
#69376=CARTESIAN_POINT('Ctrl Pts',(11.8417081797482,3.68553307948342,134.063933614821));
#69377=CARTESIAN_POINT('Ctrl Pts',(11.8339518770063,3.77344303860083,133.958771925074));
#69378=CARTESIAN_POINT('Ctrl Pts',(11.8261914344921,3.86139991791058,133.853554107366));
#69379=CARTESIAN_POINT('Ctrl Pts',(11.8184309919779,3.94488290966734,133.744738134851));
#69380=CARTESIAN_POINT('Ctrl Pts',(11.8106705494637,4.02360398701671,133.632751329289));
#69381=CARTESIAN_POINT('Ctrl Pts',(11.8028976491983,4.10245143442787,133.520584752566));
#69382=CARTESIAN_POINT('Ctrl Pts',(11.7951247489328,4.17652148041489,133.405237500317));
#69383=CARTESIAN_POINT('Ctrl Pts',(11.7873518486673,4.24557073716481,133.287163907847));
#69384=CARTESIAN_POINT('Ctrl Pts',(11.7798615129054,4.31210987950598,133.173382587875));
#69385=CARTESIAN_POINT('Ctrl Pts',(11.7723711771436,4.37398678704385,133.057069976916));
#69386=CARTESIAN_POINT('Ctrl Pts',(11.7648808413817,4.43102611955394,132.938649864676));
#69387=CARTESIAN_POINT('Ctrl Pts',(11.7571065072626,4.4902281156938,132.815739817886));
#69388=CARTESIAN_POINT('Ctrl Pts',(11.7493321731435,4.54440599621508,132.690169961175));
#69389=CARTESIAN_POINT('Ctrl Pts',(11.7415578390244,4.59331226912462,132.562389474215));
#69390=CARTESIAN_POINT('Ctrl Pts',(11.7337930860773,4.64215826942374,132.434766465284));
#69391=CARTESIAN_POINT('Ctrl Pts',(11.7260283331303,4.68574545036839,132.304938608488));
#69392=CARTESIAN_POINT('Ctrl Pts',(11.7182635801832,4.72387260126554,132.173378772856));
#69393=CARTESIAN_POINT('Ctrl Pts',(11.7105065392982,4.76196188373883,132.041949604307));
#69394=CARTESIAN_POINT('Ctrl Pts',(11.7027494984132,4.79460182001442,131.908792253334));
#69395=CARTESIAN_POINT('Ctrl Pts',(11.6949924575282,4.82163976048743,131.774398288271));
#69396=CARTESIAN_POINT('Ctrl Pts',(11.6872412662881,4.84865731143925,131.640105670742));
#69397=CARTESIAN_POINT('Ctrl Pts',(11.6794900750479,4.87008119841774,131.504578677024));
#69398=CARTESIAN_POINT('Ctrl Pts',(11.6717388838078,4.88580906365169,131.368322368077));
#69399=CARTESIAN_POINT('Ctrl Pts',(11.6639909870307,4.90153024412339,131.232123971695));
#69400=CARTESIAN_POINT('Ctrl Pts',(11.6562430902537,4.91156017322077,131.095197264182));
#69401=CARTESIAN_POINT('Ctrl Pts',(11.6484951934766,4.91584793524088,130.958055575479));
#69402=CARTESIAN_POINT('Ctrl Pts',(11.6407489173925,4.9201348003536,130.820942573862));
#69403=CARTESIAN_POINT('Ctrl Pts',(11.6330026413083,4.91868187530762,130.683615071028));
#69404=CARTESIAN_POINT('Ctrl Pts',(11.6252563652242,4.91149029784851,130.546589174927));
#69405=CARTESIAN_POINT('Ctrl Pts',(11.6175100319589,4.90429866730282,130.409562267333));
#69406=CARTESIAN_POINT('Ctrl Pts',(11.6097636986935,4.89136832030583,130.272837361343));
#69407=CARTESIAN_POINT('Ctrl Pts',(11.6020173654282,4.87275245836635,130.136927817964));
#69408=CARTESIAN_POINT('Ctrl Pts',(11.5942692974252,4.85413242753369,130.000987838585));
#69409=CARTESIAN_POINT('Ctrl Pts',(11.5865212294223,4.82982440122089,129.865863972434));
#69410=CARTESIAN_POINT('Ctrl Pts',(11.5787731614193,4.79993305392135,129.732061340138));
#69411=CARTESIAN_POINT('Ctrl Pts',(11.5710168586775,4.77000993774212,129.598116500811));
#69412=CARTESIAN_POINT('Ctrl Pts',(11.5632605559356,4.73449173210793,129.465496082595));
#69413=CARTESIAN_POINT('Ctrl Pts',(11.5555042531937,4.69353370441307,129.334692482224));
#69414=CARTESIAN_POINT('Ctrl Pts',(11.5477438106795,4.6525538161856,129.203819068034));
#69415=CARTESIAN_POINT('Ctrl Pts',(11.5399833681654,4.60612845290998,129.074764771586));
#69416=CARTESIAN_POINT('Ctrl Pts',(11.5322229256512,4.55446144693704,128.94800289588));
#69417=CARTESIAN_POINT('Ctrl Pts',(11.5244500253858,4.50271150049933,128.821037530757));
#69418=CARTESIAN_POINT('Ctrl Pts',(11.5166771251204,4.44570325949606,128.696372295942));
#69419=CARTESIAN_POINT('Ctrl Pts',(11.5089042248549,4.38368741202849,128.574457539824));
#69420=CARTESIAN_POINT('Ctrl Pts',(11.5014138890929,4.32392599682478,128.456974692175));
#69421=CARTESIAN_POINT('Ctrl Pts',(11.4939235533308,4.25951488303135,128.3420460901));
#69422=CARTESIAN_POINT('Ctrl Pts',(11.4864332175688,4.19071584125612,128.230048320982));
#69423=CARTESIAN_POINT('Ctrl Pts',(11.4786588834497,4.11930826290116,128.113804122407));
#69424=CARTESIAN_POINT('Ctrl Pts',(11.4708845493307,4.04294725391655,128.00034916236));
#69425=CARTESIAN_POINT('Ctrl Pts',(11.4631102152116,3.96187694641529,127.89013445545));
#69426=CARTESIAN_POINT('Ctrl Pts',(11.4553454622645,3.88090655082245,127.780055578315));
#69427=CARTESIAN_POINT('Ctrl Pts',(11.4475807093174,3.79523863396022,127.673209320713));
#69428=CARTESIAN_POINT('Ctrl Pts',(11.4398159563703,3.70516227464205,127.57002056416));
#69429=CARTESIAN_POINT('Ctrl Pts',(11.4320589154853,3.61517538043418,127.466934296134));
#69430=CARTESIAN_POINT('Ctrl Pts',(11.4243018746003,3.52078901267995,127.367498592584));
#69431=CARTESIAN_POINT('Ctrl Pts',(11.4165448337153,3.42233423090189,127.272107586638));
#69432=CARTESIAN_POINT('Ctrl Pts',(11.4087936424752,3.32395369464051,127.176788515792));
#69433=CARTESIAN_POINT('Ctrl Pts',(11.4010424512351,3.22151113072069,127.085508342385));
#69434=CARTESIAN_POINT('Ctrl Pts',(11.393291259995,3.1153761343578,126.998626180697));
#69435=CARTESIAN_POINT('Ctrl Pts',(11.3855433632179,3.0092862481996,126.911780946244));
#69436=CARTESIAN_POINT('Ctrl Pts',(11.3777954664409,2.89950735287498,126.829330252801));
#69437=CARTESIAN_POINT('Ctrl Pts',(11.3700475696638,2.7864438062216,126.751594404562));
#69438=CARTESIAN_POINT('Ctrl Pts',(11.3623012935797,2.67340391002482,126.673874816986));
#69439=CARTESIAN_POINT('Ctrl Pts',(11.3545550174956,2.55708105109701,126.600868334284));
#69440=CARTESIAN_POINT('Ctrl Pts',(11.3468087414115,2.4379100606524,126.532852968191));
#69441=CARTESIAN_POINT('Ctrl Pts',(11.3390624081462,2.3187381905143,126.464837100023));
#69442=CARTESIAN_POINT('Ctrl Pts',(11.3313160748808,2.19671848646086,126.401812615779));
#69443=CARTESIAN_POINT('Ctrl Pts',(11.3235697416154,2.0723116103615,126.344012239686));
#69444=CARTESIAN_POINT('Ctrl Pts',(11.3158216736124,1.94787687420431,126.286198919598));
#69445=CARTESIAN_POINT('Ctrl Pts',(11.3080736056094,1.8210542567252,126.233612200335));
#69446=CARTESIAN_POINT('Ctrl Pts',(11.3003255376064,1.69232530933384,126.186437046318));
#69447=CARTESIAN_POINT('Ctrl Pts',(11.2925692348646,1.56345954728617,126.139211753986));
#69448=CARTESIAN_POINT('Ctrl Pts',(11.2848129321227,1.43268377570976,126.097409650834));
#69449=CARTESIAN_POINT('Ctrl Pts',(11.2770566293809,1.30049618774361,126.06116625847));
#69450=CARTESIAN_POINT('Ctrl Pts',(11.2692961868667,1.16823804728131,126.024903521915));
#69451=CARTESIAN_POINT('Ctrl Pts',(11.2615357443525,1.03456696981866,125.994205495317));
#69452=CARTESIAN_POINT('Ctrl Pts',(11.2537753018383,0.899991334939068,125.969156520577));
#69453=CARTESIAN_POINT('Ctrl Pts',(11.2460024015729,0.765199667303492,125.944067335));
#69454=CARTESIAN_POINT('Ctrl Pts',(11.2382295013076,0.629500927784692,125.924645378178));
#69455=CARTESIAN_POINT('Ctrl Pts',(11.2304566010421,0.493409510279886,125.910923163417));
#69456=CARTESIAN_POINT('Ctrl Pts',(11.2229662652801,0.362265358594056,125.897699785727));
#69457=CARTESIAN_POINT('Ctrl Pts',(11.215475929518,0.230756890385802,125.88976896327));
#69458=CARTESIAN_POINT('Ctrl Pts',(11.2079855937559,0.0993424326949853,
125.8871140157));
#69459=CARTESIAN_POINT('Ctrl Pts',(11.2002112596368,-0.0370546441009691,
125.884358404985));
#69460=CARTESIAN_POINT('Ctrl Pts',(11.1924369255177,-0.173782505777523,
125.887277907303));
#69461=CARTESIAN_POINT('Ctrl Pts',(11.1846625913986,-0.310329741600855,
125.895910911806));
#69462=CARTESIAN_POINT('Ctrl Pts',(11.1768978384515,-0.446708695159241,
125.904533276902));
#69463=CARTESIAN_POINT('Ctrl Pts',(11.1691330855045,-0.582907079342031,
125.9188551095));
#69464=CARTESIAN_POINT('Ctrl Pts',(11.1613683325574,-0.718411175136592,
125.938862858247));
#69465=CARTESIAN_POINT('Ctrl Pts',(11.1536112916725,-0.853780686352752,
125.958850735015));
#69466=CARTESIAN_POINT('Ctrl Pts',(11.1458542507874,-0.988456897201061,
125.984513232747));
#69467=CARTESIAN_POINT('Ctrl Pts',(11.1380972099025,-1.12192926655965,126.015784860273));
#69468=CARTESIAN_POINT('Ctrl Pts',(11.1303460186623,-1.25530098336678,126.047032905621));
#69469=CARTESIAN_POINT('Ctrl Pts',(11.1225948274222,-1.38747028654043,126.083881572602));
#69470=CARTESIAN_POINT('Ctrl Pts',(11.1148436361821,-1.51793526782587,126.126214020334));
#69471=CARTESIAN_POINT('Ctrl Pts',(11.107095739405,-1.64834479801399,126.168528475647));
#69472=CARTESIAN_POINT('Ctrl Pts',(11.0993478426279,-1.77705107595486,126.216321955607));
#69473=CARTESIAN_POINT('Ctrl Pts',(11.0915999458508,-1.90356605536896,126.269427394756));
#69474=CARTESIAN_POINT('Ctrl Pts',(11.0838536697667,-2.03005457057688,126.322521725392));
#69475=CARTESIAN_POINT('Ctrl Pts',(11.0761073936825,-2.15435233872,126.38092565386));
#69476=CARTESIAN_POINT('Ctrl Pts',(11.0683611175984,-2.27599042375861,126.444423616478));
#69477=CARTESIAN_POINT('Ctrl Pts',(11.060614784333,-2.39762940670193,126.507922047823));
#69478=CARTESIAN_POINT('Ctrl Pts',(11.0528684510678,-2.51660832078079,126.576514407428));
#69479=CARTESIAN_POINT('Ctrl Pts',(11.0451221178024,-2.63248236951863,126.649938920546));
#69480=CARTESIAN_POINT('Ctrl Pts',(11.0373740497994,-2.74838236744611,126.723379876573));
#69481=CARTESIAN_POINT('Ctrl Pts',(11.0296259817964,-2.86117578625689,126.801654930198));
#69482=CARTESIAN_POINT('Ctrl Pts',(11.0218779137934,-2.97044671984541,126.884458916367));
#69483=CARTESIAN_POINT('Ctrl Pts',(11.0141216110516,-3.07983378788249,126.967350907599));
#69484=CARTESIAN_POINT('Ctrl Pts',(11.0063653083097,-3.18569058007435,127.054781210162));
#69485=CARTESIAN_POINT('Ctrl Pts',(10.9986090055679,-3.28763379269392,127.146403932798));
#69486=CARTESIAN_POINT('Ctrl Pts',(10.9908485630537,-3.38963141547551,127.23807555724));
#69487=CARTESIAN_POINT('Ctrl Pts',(10.9830881205395,-3.48771101713213,127.333943787254));
#69488=CARTESIAN_POINT('Ctrl Pts',(10.9753276780253,-3.58152684684924,127.433626497556));
#69489=CARTESIAN_POINT('Ctrl Pts',(10.9675547777599,-3.67549327806491,127.533469227395));
#69490=CARTESIAN_POINT('Ctrl Pts',(10.9597818774944,-3.76518200373369,127.63713837807));
#69491=CARTESIAN_POINT('Ctrl Pts',(10.952008977229,-3.85028762702443,127.744218749665));
#69492=CARTESIAN_POINT('Ctrl Pts',(10.944518641467,-3.93229944653996,127.847406480032));
#69493=CARTESIAN_POINT('Ctrl Pts',(10.937028305705,-4.01005541142441,127.953761475589));
#69494=CARTESIAN_POINT('Ctrl Pts',(10.929537969943,-4.08332181836509,128.062889116681));
#69495=CARTESIAN_POINT('Ctrl Pts',(10.9216308269926,-4.16066520743983,128.178089273974));
#69496=CARTESIAN_POINT('Ctrl Pts',(10.9137236840423,-4.2332444689001,128.296735493713));
#69497=CARTESIAN_POINT('Ctrl Pts',(10.9058165410919,-4.30074360286296,128.418404305113));
#69498=CARTESIAN_POINT('Ctrl Pts',(10.8979193786894,-4.36815753812039,128.539919543799));
#69499=CARTESIAN_POINT('Ctrl Pts',(10.8900222162869,-4.43050392698758,128.664449458864));
#69500=CARTESIAN_POINT('Ctrl Pts',(10.8821250538845,-4.48750917204769,128.791540582568));
#69501=CARTESIAN_POINT('Ctrl Pts',(10.8742129206602,-4.54462248318634,128.91887263567));
#69502=CARTESIAN_POINT('Ctrl Pts',(10.8663007874359,-4.5963741548825,129.0487753131));
#69503=CARTESIAN_POINT('Ctrl Pts',(10.8583886542115,-4.64253391849751,129.180765262159));
#69504=CARTESIAN_POINT('Ctrl Pts',(10.8504765209872,-4.68869368211251,129.312755211218));
#69505=CARTESIAN_POINT('Ctrl Pts',(10.8425643877628,-4.7292613624623,129.446832094024));
#69506=CARTESIAN_POINT('Ctrl Pts',(10.8346522545385,-4.76405452823403,129.582490119308));
#69507=CARTESIAN_POINT('Ctrl Pts',(12.5846956991378,-4.76405452823411,129.582490119308));
#69508=CARTESIAN_POINT('Ctrl Pts',(12.5753201746923,-4.80496324234701,129.741992574758));
#69509=CARTESIAN_POINT('Ctrl Pts',(12.5659446502468,-4.83789536222626,129.903698025889));
#69510=CARTESIAN_POINT('Ctrl Pts',(12.5565691258012,-4.86264420202425,130.066882192783));
#69511=CARTESIAN_POINT('Ctrl Pts',(12.5473009272211,-4.8871097306683,130.228198316771));
#69512=CARTESIAN_POINT('Ctrl Pts',(12.5380327286411,-4.9035782152433,130.390959472741));
#69513=CARTESIAN_POINT('Ctrl Pts',(12.528764530061,-4.9118963060295,130.55444514923));
#69514=CARTESIAN_POINT('Ctrl Pts',(12.5241294987191,-4.91605618792739,130.636204428332));
#69515=CARTESIAN_POINT('Ctrl Pts',(12.519494467377,-4.91817838360492,130.718144585058));
#69516=CARTESIAN_POINT('Ctrl Pts',(12.514859436035,-4.91824821769922,130.800173542404));
#69517=CARTESIAN_POINT('',(12.8601405640505,-4.91824999861463,130.804477352914));
#69518=CARTESIAN_POINT('Ctrl Pts',(12.9302349012323,-4.7640545282341,129.582490119308));
#69519=CARTESIAN_POINT('Ctrl Pts',(12.9224800024765,-4.79810443156944,129.715250175634));
#69520=CARTESIAN_POINT('Ctrl Pts',(12.9147251037206,-4.82657402661124,129.849330561244));
#69521=CARTESIAN_POINT('Ctrl Pts',(12.9069702049648,-4.84938717326976,129.984222149851));
#69522=CARTESIAN_POINT('Ctrl Pts',(12.8991652648124,-4.87234753032454,130.119984177091));
#69523=CARTESIAN_POINT('Ctrl Pts',(12.89136032466,-4.88957814010849,130.256567512834));
#69524=CARTESIAN_POINT('Ctrl Pts',(12.8835553845076,-4.90105455902557,130.393450320841));
#69525=CARTESIAN_POINT('Ctrl Pts',(12.8757504443553,-4.91253097794264,130.530333128848));
#69526=CARTESIAN_POINT('Ctrl Pts',(12.8679455042029,-4.91825324943492,130.667515009186));
#69527=CARTESIAN_POINT('Ctrl Pts',(12.8601405640505,-4.91824999861463,130.804477352914));
#69528=CARTESIAN_POINT('Ctrl Pts',(12.8601405640088,-4.91824999861462,130.804477353645));
#69529=CARTESIAN_POINT('Ctrl Pts',(12.8597878228304,-4.91824985169416,130.810667312513));
#69530=CARTESIAN_POINT('Ctrl Pts',(12.8594350816521,-4.91823801904131,130.816857255042));
#69531=CARTESIAN_POINT('Ctrl Pts',(12.8590823404737,-4.91821450080088,130.823047153146));
#69532=CARTESIAN_POINT('Ctrl Pts',(12.8513080063546,-4.91769616421236,130.959471078012));
#69533=CARTESIAN_POINT('Ctrl Pts',(12.8435336722355,-4.91149641095859,131.096089505437));
#69534=CARTESIAN_POINT('Ctrl Pts',(12.8357593381164,-4.89958913539054,131.232390250726));
#69535=CARTESIAN_POINT('Ctrl Pts',(12.8279945851693,-4.88769653447546,131.368523017527));
#69536=CARTESIAN_POINT('Ctrl Pts',(12.8202298322223,-4.87011044053039,131.504338495448));
#69537=CARTESIAN_POINT('Ctrl Pts',(12.8124650792752,-4.84685672884779,131.639323438608));
#69538=CARTESIAN_POINT('Ctrl Pts',(12.8047080383902,-4.8236261130795,131.77417431282));
#69539=CARTESIAN_POINT('Ctrl Pts',(12.7969509975053,-4.7947391477958,131.908195911061));
#69540=CARTESIAN_POINT('Ctrl Pts',(12.7891939566203,-4.7602735568853,132.04087941084));
#69541=CARTESIAN_POINT('Ctrl Pts',(12.7814427653802,-4.72583395674501,132.173462852959));
#69542=CARTESIAN_POINT('Ctrl Pts',(12.77369157414,-4.6858242024239,132.304709828234));
#69543=CARTESIAN_POINT('Ctrl Pts',(12.7659403828999,-4.64037314557179,132.434121376805));
#69544=CARTESIAN_POINT('Ctrl Pts',(12.7581924861228,-4.59494140663123,132.563477922017));
#69545=CARTESIAN_POINT('Ctrl Pts',(12.7504445893458,-4.54407309422403,132.691000223991));
#69546=CARTESIAN_POINT('Ctrl Pts',(12.7426966925687,-4.48794693746378,132.816204386105));
#69547=CARTESIAN_POINT('Ctrl Pts',(12.7349504164846,-4.43183252108565,132.941382358207));
#69548=CARTESIAN_POINT('Ctrl Pts',(12.7272041404005,-4.37046260779772,133.064242798418));
#69549=CARTESIAN_POINT('Ctrl Pts',(12.7194578643164,-4.3040639523765,133.184322078673));
#69550=CARTESIAN_POINT('Ctrl Pts',(12.7117115310511,-4.23766480681539,133.304402245326));
#69551=CARTESIAN_POINT('Ctrl Pts',(12.7039651977858,-4.16623703423832,133.421700868916));
#69552=CARTESIAN_POINT('Ctrl Pts',(12.6962188645204,-4.09005300789726,133.535779562929));
#69553=CARTESIAN_POINT('Ctrl Pts',(12.6884707965174,-4.01385192067183,133.649883804075));
#69554=CARTESIAN_POINT('Ctrl Pts',(12.6807227285145,-3.93289267728338,133.760766355709));
#69555=CARTESIAN_POINT('Ctrl Pts',(12.6729746605115,-3.84749033550317,133.868018754616));
#69556=CARTESIAN_POINT('Ctrl Pts',(12.6652183577697,-3.76199722709781,133.975385142648));
#69557=CARTESIAN_POINT('Ctrl Pts',(12.6574620550279,-3.67205183116872,134.079113364509));
#69558=CARTESIAN_POINT('Ctrl Pts',(12.649705752286,-3.57800913759869,134.17882852729));
#69559=CARTESIAN_POINT('Ctrl Pts',(12.6419453097719,-3.4839162506114,134.278596911057));
#69560=CARTESIAN_POINT('Ctrl Pts',(12.6341848672577,-3.38572198827512,134.374347695028));
#69561=CARTESIAN_POINT('Ctrl Pts',(12.6264244247436,-3.28381666289617,134.465744397913));
#69562=CARTESIAN_POINT('Ctrl Pts',(12.6186515244781,-3.18174775004218,134.557287818898));
#69563=CARTESIAN_POINT('Ctrl Pts',(12.6108786242127,-3.07595617140401,134.644462942661));
#69564=CARTESIAN_POINT('Ctrl Pts',(12.6031057239473,-2.96686433601439,134.726974423969));
#69565=CARTESIAN_POINT('Ctrl Pts',(12.5956153881851,-2.86173826362546,134.8064864051));
#69566=CARTESIAN_POINT('Ctrl Pts',(12.588125052423,-2.7535479669175,134.881667751548));
#69567=CARTESIAN_POINT('Ctrl Pts',(12.5806347166609,-2.64269356013857,134.952294297087));
#69568=CARTESIAN_POINT('Ctrl Pts',(12.5728603825418,-2.52763607483477,135.025598669565));
#69569=CARTESIAN_POINT('Ctrl Pts',(12.5650860484227,-2.40934400453649,135.09422823868));
#69570=CARTESIAN_POINT('Ctrl Pts',(12.5573117143037,-2.28823415399159,135.157884192672));
#69571=CARTESIAN_POINT('Ctrl Pts',(12.5495469613566,-2.1672735605136,135.22146169639));
#69572=CARTESIAN_POINT('Ctrl Pts',(12.5417822084094,-2.04350243910324,135.280077600784));
#69573=CARTESIAN_POINT('Ctrl Pts',(12.5340174554623,-1.91736658428213,135.333476253535));
#69574=CARTESIAN_POINT('Ctrl Pts',(12.5262604145773,-1.79135600937023,135.386821869991));
#69575=CARTESIAN_POINT('Ctrl Pts',(12.5185033736924,-1.6629857327419,135.434960395485));
#69576=CARTESIAN_POINT('Ctrl Pts',(12.5107463328074,-1.53272585282985,135.477682190341));
#69577=CARTESIAN_POINT('Ctrl Pts',(12.5029951415673,-1.4025642029067,135.520371768359));
#69578=CARTESIAN_POINT('Ctrl Pts',(12.4952439503272,-1.27051615599734,135.557652624935));
#69579=CARTESIAN_POINT('Ctrl Pts',(12.487492759087,-1.13707114862613,135.589363466621));
#69580=CARTESIAN_POINT('Ctrl Pts',(12.47974486231,-1.00368285894246,135.621060830352));
#69581=CARTESIAN_POINT('Ctrl Pts',(12.4719969655329,-0.868899169288064,
135.647192797582));
#69582=CARTESIAN_POINT('Ctrl Pts',(12.4642490687558,-0.733223803048837,
135.667648180228));
#69583=CARTESIAN_POINT('Ctrl Pts',(12.4565027926717,-0.597576817171404,
135.688099284049));
#69584=CARTESIAN_POINT('Ctrl Pts',(12.4487565165876,-0.461038912057853,
135.702876106881));
#69585=CARTESIAN_POINT('Ctrl Pts',(12.4410102405035,-0.324122717624308,
135.711918821645));
#69586=CARTESIAN_POINT('Ctrl Pts',(12.4332639072381,-0.187205512506706,
135.72096160316));
#69587=CARTESIAN_POINT('Ctrl Pts',(12.4255175739728,-0.0499104026122739,
135.72427016638));
#69588=CARTESIAN_POINT('Ctrl Pts',(12.4177712407074,0.087246560673206,135.721836708016));
#69589=CARTESIAN_POINT('Ctrl Pts',(12.4100231727045,0.224434239309634,135.719402704697));
#69590=CARTESIAN_POINT('Ctrl Pts',(12.4022751047015,0.361483318947243,135.711224127964));
#69591=CARTESIAN_POINT('Ctrl Pts',(12.3945270366985,0.497879851493844,135.697345260499));
#69592=CARTESIAN_POINT('Ctrl Pts',(12.3867707339567,0.634421347898376,135.683451642408));
#69593=CARTESIAN_POINT('Ctrl Pts',(12.3790144312148,0.770308522224405,135.663845671046));
#69594=CARTESIAN_POINT('Ctrl Pts',(12.371258128473,0.905034085747642,135.638623370679));
#69595=CARTESIAN_POINT('Ctrl Pts',(12.3634976859588,1.03983155636082,135.613387608411));
#69596=CARTESIAN_POINT('Ctrl Pts',(12.3557372434446,1.17346580004069,135.582529632081));
#69597=CARTESIAN_POINT('Ctrl Pts',(12.3479768009304,1.30544275220973,135.546195946128));
#69598=CARTESIAN_POINT('Ctrl Pts',(12.340203900665,1.43763156549876,135.509803934117));
#69599=CARTESIAN_POINT('Ctrl Pts',(12.3324310003996,1.56815739840512,135.4679187666));
#69600=CARTESIAN_POINT('Ctrl Pts',(12.3246581001342,1.69654344622106,135.420736186948));
#69601=CARTESIAN_POINT('Ctrl Pts',(12.3171677643721,1.82026233781431,135.375268812911));
#69602=CARTESIAN_POINT('Ctrl Pts',(12.30967742861,1.94199403189221,135.324882606345));
#69603=CARTESIAN_POINT('Ctrl Pts',(12.302187092848,2.06133365953379,135.269793027375));
#69604=CARTESIAN_POINT('Ctrl Pts',(12.2944127587289,2.18519808542954,135.212614710275));
#69605=CARTESIAN_POINT('Ctrl Pts',(12.2866384246098,2.30687783905734,135.150188199804));
#69606=CARTESIAN_POINT('Ctrl Pts',(12.2788640904907,2.42589622847365,135.082702650548));
#69607=CARTESIAN_POINT('Ctrl Pts',(12.2710993375436,2.54476793836198,135.015300271199));
#69608=CARTESIAN_POINT('Ctrl Pts',(12.2633345845965,2.6609844732171,134.942851449474));
#69609=CARTESIAN_POINT('Ctrl Pts',(12.2555698316494,2.77408978267536,134.865593058606));
#69610=CARTESIAN_POINT('Ctrl Pts',(12.2478127907644,2.88708275434562,134.788411401861));
#69611=CARTESIAN_POINT('Ctrl Pts',(12.2400557498794,2.99697032933374,134.706429901377));
#69612=CARTESIAN_POINT('Ctrl Pts',(12.2322987089944,3.10332203215698,134.619930748913));
#69613=CARTESIAN_POINT('Ctrl Pts',(12.2245475177543,3.20959353433398,134.533496826133));
#69614=CARTESIAN_POINT('Ctrl Pts',(12.2167963265141,3.31233416962784,134.442552278088));
#69615=CARTESIAN_POINT('Ctrl Pts',(12.209045135274,3.41114368489523,134.347421698538));
#69616=CARTESIAN_POINT('Ctrl Pts',(12.2012972384969,3.50991120348281,134.252331552023));
#69617=CARTESIAN_POINT('Ctrl Pts',(12.1935493417199,3.60475064414116,134.15305918324));
#69618=CARTESIAN_POINT('Ctrl Pts',(12.1858014449428,3.69529618639546,134.049968289068));
#69619=CARTESIAN_POINT('Ctrl Pts',(12.1780551688587,3.78582278847425,133.946898959288));
#69620=CARTESIAN_POINT('Ctrl Pts',(12.1703088927746,3.87205702086128,133.840012986446));
#69621=CARTESIAN_POINT('Ctrl Pts',(12.1625626166905,3.95367146035036,133.729709322611));
#69622=CARTESIAN_POINT('Ctrl Pts',(12.1548162834251,4.03528650229868,133.61940484454));
#69623=CARTESIAN_POINT('Ctrl Pts',(12.1470699501597,4.11228145075645,133.505682939423));
#69624=CARTESIAN_POINT('Ctrl Pts',(12.1393236168944,4.18437080221711,133.388973558038));
#69625=CARTESIAN_POINT('Ctrl Pts',(12.1315755488914,4.2564762975882,133.272238040396));
#69626=CARTESIAN_POINT('Ctrl Pts',(12.1238274808884,4.32367380450758,133.152514047768));
#69627=CARTESIAN_POINT('Ctrl Pts',(12.1160794128855,4.38572277775109,133.03025791511));
#69628=CARTESIAN_POINT('Ctrl Pts',(12.1083231101436,4.44783769738176,132.90787184718));
#69629=CARTESIAN_POINT('Ctrl Pts',(12.1005668074017,4.5047929753564,132.782948612471));
#69630=CARTESIAN_POINT('Ctrl Pts',(12.0928105046599,4.55639519766442,132.655966910815));
#69631=CARTESIAN_POINT('Ctrl Pts',(12.0850500621457,4.60802496163226,132.528917435202));
#69632=CARTESIAN_POINT('Ctrl Pts',(12.0772896196315,4.65429584510939,132.399807671321));
#69633=CARTESIAN_POINT('Ctrl Pts',(12.0695291771173,4.69506405245742,132.269132478923));
#69634=CARTESIAN_POINT('Ctrl Pts',(12.0617562768519,4.73589770455106,132.138247515105));
#69635=CARTESIAN_POINT('Ctrl Pts',(12.0539833765864,4.77121092782574,132.005792479052));
#69636=CARTESIAN_POINT('Ctrl Pts',(12.046210476321,4.80091068213192,131.872274324141));
#69637=CARTESIAN_POINT('Ctrl Pts',(12.038720140559,4.82953077555965,131.743609890475));
#69638=CARTESIAN_POINT('Ctrl Pts',(12.031229804797,4.85293838707447,131.613958593228));
#69639=CARTESIAN_POINT('Ctrl Pts',(12.0237394690351,4.87109594784187,131.483777521549));
#69640=CARTESIAN_POINT('Ctrl Pts',(12.015965134916,4.88994195804478,131.34866059497));
#69641=CARTESIAN_POINT('Ctrl Pts',(12.008190800797,4.90319164580439,131.212544918332));
#69642=CARTESIAN_POINT('Ctrl Pts',(12.0004164666779,4.91074648858991,131.075933788741));
#69643=CARTESIAN_POINT('Ctrl Pts',(11.9926517137308,4.91829202070688,130.939491020158));
#69644=CARTESIAN_POINT('Ctrl Pts',(11.9848869607837,4.92015665096811,130.802554400158));
#69645=CARTESIAN_POINT('Ctrl Pts',(11.9771222078367,4.91629316117279,130.665635652597));
#69646=CARTESIAN_POINT('Ctrl Pts',(11.9693651669517,4.91243350865,130.528852894666));
#69647=CARTESIAN_POINT('Ctrl Pts',(11.9616081260666,4.90285706889034,130.39208836213));
#69648=CARTESIAN_POINT('Ctrl Pts',(11.9538510851816,4.88756857529978,130.255856757742));
#69649=CARTESIAN_POINT('Ctrl Pts',(11.9460998939415,4.87229161088117,130.119727886666));
#69650=CARTESIAN_POINT('Ctrl Pts',(11.9383487027014,4.85131120988324,129.984131530765));
#69651=CARTESIAN_POINT('Ctrl Pts',(11.9305975114613,4.82468411562899,129.8495798852));
#69652=CARTESIAN_POINT('Ctrl Pts',(11.9228496146842,4.7980683386001,129.715085427673));
#69653=CARTESIAN_POINT('Ctrl Pts',(11.9151017179071,4.76581071746173,129.581635180066));
#69654=CARTESIAN_POINT('Ctrl Pts',(11.90735382113,4.72801950579517,129.449733504549));
#69655=CARTESIAN_POINT('Ctrl Pts',(11.8996075450459,4.69023619923541,129.31785942002));
#69656=CARTESIAN_POINT('Ctrl Pts',(11.8918612689619,4.64692171210883,129.187533638876));
#69657=CARTESIAN_POINT('Ctrl Pts',(11.8841149928778,4.59823471385015,129.059247274874));
#69658=CARTESIAN_POINT('Ctrl Pts',(11.8763686596124,4.54954735619512,128.93095996389));
#69659=CARTESIAN_POINT('Ctrl Pts',(11.868622326347,4.49548754699586,128.804712465615));
#69660=CARTESIAN_POINT('Ctrl Pts',(11.8608759930817,4.43626269439996,128.680977381131));
#69661=CARTESIAN_POINT('Ctrl Pts',(11.8531279250787,4.37702457880896,128.557214587032));
#69662=CARTESIAN_POINT('Ctrl Pts',(11.8453798570758,4.31261928693193,128.435965678892));
#69663=CARTESIAN_POINT('Ctrl Pts',(11.8376317890728,4.24330072572247,128.317679694411));
#69664=CARTESIAN_POINT('Ctrl Pts',(11.8298754863309,4.17390849192125,128.199267994178));
#69665=CARTESIAN_POINT('Ctrl Pts',(11.8221191835891,4.09959275550587,128.08382584598));
#69666=CARTESIAN_POINT('Ctrl Pts',(11.8143628808473,4.02065171520637,127.971774723457));
#69667=CARTESIAN_POINT('Ctrl Pts',(11.8066024383331,3.94166854169669,127.859663795875));
#69668=CARTESIAN_POINT('Ctrl Pts',(11.7988419958189,3.85805538351401,127.750947810087));
#69669=CARTESIAN_POINT('Ctrl Pts',(11.7910815533047,3.77015085512594,127.646015229219));
#69670=CARTESIAN_POINT('Ctrl Pts',(11.7833086530393,3.68210521458523,127.540914201257));
#69671=CARTESIAN_POINT('Ctrl Pts',(11.7755357527739,3.58975470118596,127.439609004013));
#69672=CARTESIAN_POINT('Ctrl Pts',(11.7677628525084,3.49347553868896,127.342451935483));
#69673=CARTESIAN_POINT('Ctrl Pts',(11.7602725167463,3.40069636626039,127.248826771117));
#69674=CARTESIAN_POINT('Ctrl Pts',(11.7527821809843,3.30426944375523,127.159053591539));
#69675=CARTESIAN_POINT('Ctrl Pts',(11.7452918452222,3.20455902634905,127.073411072324));
#69676=CARTESIAN_POINT('Ctrl Pts',(11.7375175111031,3.10106805816147,126.984521390962));
#69677=CARTESIAN_POINT('Ctrl Pts',(11.729743176984,2.99371186428505,126.899800205366));
#69678=CARTESIAN_POINT('Ctrl Pts',(11.7219688428649,2.88286062899448,126.81960244971));
#69679=CARTESIAN_POINT('Ctrl Pts',(11.7142040899178,2.77214600794435,126.73950353062));
#69680=CARTESIAN_POINT('Ctrl Pts',(11.7064393369708,2.65794522949385,126.6639171764));
#69681=CARTESIAN_POINT('Ctrl Pts',(11.6986745840237,2.54066329882483,126.593159712301));
#69682=CARTESIAN_POINT('Ctrl Pts',(11.6909175431387,2.4234978542229,126.522472525513));
#69683=CARTESIAN_POINT('Ctrl Pts',(11.6831605022536,2.30325768001945,126.456604885007));
#69684=CARTESIAN_POINT('Ctrl Pts',(11.6754034613686,2.18037836874034,126.395831017844));
#69685=CARTESIAN_POINT('Ctrl Pts',(11.6676522701284,2.05759172170556,126.335102980726));
#69686=CARTESIAN_POINT('Ctrl Pts',(11.6599010788884,1.93217024798331,126.279461243792));
#69687=CARTESIAN_POINT('Ctrl Pts',(11.6521498876482,1.8045755430211,126.229134921272));
#69688=CARTESIAN_POINT('Ctrl Pts',(11.6444019908711,1.67703506921221,126.178829988781));
#69689=CARTESIAN_POINT('Ctrl Pts',(11.636654094094,1.54732356423078,126.133836120493));
#69690=CARTESIAN_POINT('Ctrl Pts',(11.628906197317,1.41592387596149,126.094334859677));
#69691=CARTESIAN_POINT('Ctrl Pts',(11.6211599212328,1.28455167367433,126.054841861672));
#69692=CARTESIAN_POINT('Ctrl Pts',(11.6134136451487,1.15149236467301,126.02083929833));
#69693=CARTESIAN_POINT('Ctrl Pts',(11.6056673690646,1.01724490157407,125.99245913554));
#69694=CARTESIAN_POINT('Ctrl Pts',(11.5979210357993,0.882996447491034,125.964078763255));
#69695=CARTESIAN_POINT('Ctrl Pts',(11.590174702534,0.747560204320396,125.941320955203));
#69696=CARTESIAN_POINT('Ctrl Pts',(11.5824283692686,0.611445893908689,125.924266665466));
#69697=CARTESIAN_POINT('Ctrl Pts',(11.5746803012656,0.475301101640729,125.907208556539));
#69698=CARTESIAN_POINT('Ctrl Pts',(11.5669322332626,0.338478327828677,125.895856556129));
#69699=CARTESIAN_POINT('Ctrl Pts',(11.5591841652597,0.201492603517559,125.89023976097));
#69700=CARTESIAN_POINT('Ctrl Pts',(11.5514278625178,0.0643612891484933,
125.884616996215));
#69701=CARTESIAN_POINT('Ctrl Pts',(11.5436715597759,-0.0729329304169342,
125.884741629061));
#69702=CARTESIAN_POINT('Ctrl Pts',(11.5359152570341,-0.209874273773137,
125.890590593266));
#69703=CARTESIAN_POINT('Ctrl Pts',(11.5281548145199,-0.346888706847513,
125.89644267924));
#69704=CARTESIAN_POINT('Ctrl Pts',(11.5203943720057,-0.483549499050023,
125.908025151413));
#69705=CARTESIAN_POINT('Ctrl Pts',(11.5126339294916,-0.61934679596056,125.925263097652));
#69706=CARTESIAN_POINT('Ctrl Pts',(11.5048610292261,-0.755362086747616,
125.942528715772));
#69707=CARTESIAN_POINT('Ctrl Pts',(11.4970881289607,-0.890510726580555,
125.96546788457));
#69708=CARTESIAN_POINT('Ctrl Pts',(11.4893152286953,-1.02429295904482,125.993954502013));
#69709=CARTESIAN_POINT('Ctrl Pts',(11.4818248929333,-1.15321187038117,126.021405559158));
#69710=CARTESIAN_POINT('Ctrl Pts',(11.4743345571713,-1.28086169583977,126.05400766362));
#69711=CARTESIAN_POINT('Ctrl Pts',(11.4668442214093,-1.40681108894646,126.091604988158));
#69712=CARTESIAN_POINT('Ctrl Pts',(11.4590698872902,-1.53753589157485,126.130627826684));
#69713=CARTESIAN_POINT('Ctrl Pts',(11.4512955531711,-1.66684286955632,126.175155762833));
#69714=CARTESIAN_POINT('Ctrl Pts',(11.443521219052,-1.79423331307467,126.225069200681));
#69715=CARTESIAN_POINT('Ctrl Pts',(11.4357564661049,-1.92146675925659,126.274921124679));
#69716=CARTESIAN_POINT('Ctrl Pts',(11.4279917131579,-2.04678801004079,126.330145203168));
#69717=CARTESIAN_POINT('Ctrl Pts',(11.4202269602108,-2.16971201683931,126.390571675344));
#69718=CARTESIAN_POINT('Ctrl Pts',(11.4124699193258,-2.29251393378151,126.450938131096));
#69719=CARTESIAN_POINT('Ctrl Pts',(11.4047128784407,-2.41292299639496,126.516496526432));
#69720=CARTESIAN_POINT('Ctrl Pts',(11.3969558375557,-2.53047304128532,126.587028611448));
#69721=CARTESIAN_POINT('Ctrl Pts',(11.3892046463156,-2.64793444077242,126.65750750767));
#69722=CARTESIAN_POINT('Ctrl Pts',(11.3814534550755,-2.7625407800478,126.732952427695));
#69723=CARTESIAN_POINT('Ctrl Pts',(11.3737022638354,-2.87384979520548,126.813098860039));
#69724=CARTESIAN_POINT('Ctrl Pts',(11.3659543670583,-2.98511150106229,126.893211228011));
#69725=CARTESIAN_POINT('Ctrl Pts',(11.3582064702812,-3.0930783535679,126.978020905926));
#69726=CARTESIAN_POINT('Ctrl Pts',(11.3504585735042,-3.19733662415185,127.067219788756));
#69727=CARTESIAN_POINT('Ctrl Pts',(11.3427122974201,-3.30157308615313,127.156400013103));
#69728=CARTESIAN_POINT('Ctrl Pts',(11.334966021336,-3.40210221236536,127.249967362156));
#69729=CARTESIAN_POINT('Ctrl Pts',(11.3272197452519,-3.49854328006957,127.347573383735));
#69730=CARTESIAN_POINT('Ctrl Pts',(11.3194734119865,-3.59498505967983,127.445180125819));
#69731=CARTESIAN_POINT('Ctrl Pts',(11.3117270787212,-3.6873384457763,127.54682532181));
#69732=CARTESIAN_POINT('Ctrl Pts',(11.3039807454558,-3.77525981228915,127.65212388594));
#69733=CARTESIAN_POINT('Ctrl Pts',(11.2962326774528,-3.86320086818244,127.757446030953));
#69734=CARTESIAN_POINT('Ctrl Pts',(11.2884846094499,-3.9467076789601,127.866422872073));
#69735=CARTESIAN_POINT('Ctrl Pts',(11.2807365414469,-4.0254773778554,127.978636826592));
#69736=CARTESIAN_POINT('Ctrl Pts',(11.2729802387051,-4.10433079412415,128.090970043438));
#69737=CARTESIAN_POINT('Ctrl Pts',(11.2652239359632,-4.17843681625437,128.20654692583));
#69738=CARTESIAN_POINT('Ctrl Pts',(11.2574676332213,-4.24753605807933,128.324921064398));
#69739=CARTESIAN_POINT('Ctrl Pts',(11.2497071907071,-4.31667218025019,128.443358382807));
#69740=CARTESIAN_POINT('Ctrl Pts',(11.241946748193,-4.38079601468925,128.564595586849));
#69741=CARTESIAN_POINT('Ctrl Pts',(11.2341863056788,-4.43969499832822,128.688163229722));
#69742=CARTESIAN_POINT('Ctrl Pts',(11.2264134054134,-4.49868853184453,128.811929234344));
#69743=CARTESIAN_POINT('Ctrl Pts',(11.2186405051479,-4.55244030048262,128.9380327937));
#69744=CARTESIAN_POINT('Ctrl Pts',(11.2108676048825,-4.60078626690473,129.065985287334));
#69745=CARTESIAN_POINT('Ctrl Pts',(11.2033772691205,-4.64737473567126,129.189286385531));
#69746=CARTESIAN_POINT('Ctrl Pts',(11.1958869333585,-4.68894351052908,129.314304032733));
#69747=CARTESIAN_POINT('Ctrl Pts',(11.1883965975965,-4.72539054004279,129.440591096505));
#69748=CARTESIAN_POINT('Ctrl Pts',(11.1856033086334,-4.73898233198792,129.487685949476));
#69749=CARTESIAN_POINT('Ctrl Pts',(11.1828100196703,-4.75187229284884,129.534991768433));
#69750=CARTESIAN_POINT('Ctrl Pts',(11.1800167307073,-4.76405452823405,129.582490119308));
#69751=CARTESIAN_POINT('Origin',(213.235140564004,0.,130.804360617566));
#69752=CARTESIAN_POINT('',(9.08499331100838,-4.76405452823401,129.582490119308));
#69753=CARTESIAN_POINT('',(9.4299069079559,-4.76405452823399,129.582490119308));
#69754=CARTESIAN_POINT('',(213.235140564004,-4.76405452823405,129.582490119308));
#69755=CARTESIAN_POINT('',(10.7648594359442,-4.91824942613488,130.806736501389));
#69756=CARTESIAN_POINT('Ctrl Pts',(10.7648594359442,-4.91824942613488,130.80673650139));
#69757=CARTESIAN_POINT('Ctrl Pts',(10.7563560984096,-4.91817654457573,130.957606540948));
#69758=CARTESIAN_POINT('Ctrl Pts',(10.747852760875,-4.91115752432135,131.108242687845));
#69759=CARTESIAN_POINT('Ctrl Pts',(10.7393494233403,-4.89728139431641,131.258032313159));
#69760=CARTESIAN_POINT('Ctrl Pts',(10.7308033869406,-4.88333558637619,131.408574095725));
#69761=CARTESIAN_POINT('Ctrl Pts',(10.7222573505409,-4.86246371736281,131.558260588257));
#69762=CARTESIAN_POINT('Ctrl Pts',(10.7137113141411,-4.83480651108763,131.706485366614));
#69763=CARTESIAN_POINT('Ctrl Pts',(10.705143301354,-4.80707818348182,131.855091309408));
#69764=CARTESIAN_POINT('Ctrl Pts',(10.6965752885669,-4.77252969569435,132.002227780159));
#69765=CARTESIAN_POINT('Ctrl Pts',(10.6880072757797,-4.73135175804063,132.147302762331));
#69766=CARTESIAN_POINT('Ctrl Pts',(10.679409092323,-4.69002881990874,132.292888599174));
#69767=CARTESIAN_POINT('Ctrl Pts',(10.6708109088663,-4.64202978451954,132.436398178318));
#69768=CARTESIAN_POINT('Ctrl Pts',(10.6622127254095,-4.58759474578353,132.577255851628));
#69769=CARTESIAN_POINT('Ctrl Pts',(10.6585052656497,-4.56412284422976,132.637992419798));
#69770=CARTESIAN_POINT('Ctrl Pts',(10.6547978058899,-4.53945490902743,132.698236235402));
#69771=CARTESIAN_POINT('Ctrl Pts',(10.6510903461301,-4.51361279970871,132.757942598647));
#69772=CARTESIAN_POINT('Ctrl Pts',(10.643316012011,-4.45942335324091,132.883143476601));
#69773=CARTESIAN_POINT('Ctrl Pts',(10.6355416778919,-4.39993479864231,133.006286253589));
#69774=CARTESIAN_POINT('Ctrl Pts',(10.6277673437729,-4.33532479673268,133.126889835754));
#69775=CARTESIAN_POINT('Ctrl Pts',(10.6200025908258,-4.27079442087604,133.247344784782));
#69776=CARTESIAN_POINT('Ctrl Pts',(10.6122378378787,-4.2011553390139,133.365266424104));
#69777=CARTESIAN_POINT('Ctrl Pts',(10.6044730849316,-4.1266334122154,133.480193150384));
#69778=CARTESIAN_POINT('Ctrl Pts',(10.5967160440466,-4.05218550164527,133.595005729819));
#69779=CARTESIAN_POINT('Ctrl Pts',(10.5889590031616,-3.97286460861424,133.706828989864));
#69780=CARTESIAN_POINT('Ctrl Pts',(10.5812019622766,-3.8889425133929,133.815225807179));
#69781=CARTESIAN_POINT('Ctrl Pts',(10.5734507710364,-3.80508370447638,133.923540881611));
#69782=CARTESIAN_POINT('Ctrl Pts',(10.5656995797963,-3.71663083817425,134.028434348532));
#69783=CARTESIAN_POINT('Ctrl Pts',(10.5579483885562,-3.62389880980018,134.129498280706));
#69784=CARTESIAN_POINT('Ctrl Pts',(10.5502004917791,-3.53120619501176,134.230519258012));
#69785=CARTESIAN_POINT('Ctrl Pts',(10.542452595002,-3.43423829929339,134.327713650381));
#69786=CARTESIAN_POINT('Ctrl Pts',(10.5347046982249,-3.33334993610429,134.420707014964));
#69787=CARTESIAN_POINT('Ctrl Pts',(10.5269584221408,-3.23248267658601,134.513680927339));
#69788=CARTESIAN_POINT('Ctrl Pts',(10.5192121460567,-3.12769686806685,134.602455295029));
#69789=CARTESIAN_POINT('Ctrl Pts',(10.5114658699726,-3.01938349047435,134.686693215367));
#69790=CARTESIAN_POINT('Ctrl Pts',(10.5037195367072,-2.91106931333711,134.770931757531));
#69791=CARTESIAN_POINT('Ctrl Pts',(10.4959732034419,-2.79922782378346,134.850633545503));
#69792=CARTESIAN_POINT('Ctrl Pts',(10.4882268701766,-2.68428199747963,134.925502840361));
#69793=CARTESIAN_POINT('Ctrl Pts',(10.4804788021736,-2.56931042985481,135.00038890168));
#69794=CARTESIAN_POINT('Ctrl Pts',(10.4727307341707,-2.45123346966108,135.070440103085));
#69795=CARTESIAN_POINT('Ctrl Pts',(10.4649826661677,-2.3305015480195,135.135405017844));
#69796=CARTESIAN_POINT('Ctrl Pts',(10.4572263634258,-2.20964131105503,135.200438978087));
#69797=CARTESIAN_POINT('Ctrl Pts',(10.4494700606839,-2.08612082077943,135.260375667531));
#69798=CARTESIAN_POINT('Ctrl Pts',(10.4417137579421,-1.96041399776924,135.315010240386));
#69799=CARTESIAN_POINT('Ctrl Pts',(10.4339533154279,-1.83464008124248,135.369673973359));
#69800=CARTESIAN_POINT('Ctrl Pts',(10.4261928729138,-1.70667787140462,135.419029810303));
#69801=CARTESIAN_POINT('Ctrl Pts',(10.4184324303996,-1.57701863479912,135.462922121721));
#69802=CARTESIAN_POINT('Ctrl Pts',(10.4106595301341,-1.44715125767642,135.506884892974));
#69803=CARTESIAN_POINT('Ctrl Pts',(10.4028866298687,-1.3155817853907,135.54536650256));
#69804=CARTESIAN_POINT('Ctrl Pts',(10.3951137296033,-1.18281479262253,135.578261771638));
#69805=CARTESIAN_POINT('Ctrl Pts',(10.3876233938413,-1.05487421446154,135.609961214828));
#69806=CARTESIAN_POINT('Ctrl Pts',(10.3801330580792,-0.925821971717786,
135.636473359175));
#69807=CARTESIAN_POINT('Ctrl Pts',(10.3726427223172,-0.796114120363577,
135.657749677785));
#69808=CARTESIAN_POINT('Ctrl Pts',(10.3648683881981,-0.661488356401419,
135.679832694483));
#69809=CARTESIAN_POINT('Ctrl Pts',(10.3570940540791,-0.525729833688034,
135.696344967587));
#69810=CARTESIAN_POINT('Ctrl Pts',(10.34931971996,-0.389339340122872,135.707175925196));
#69811=CARTESIAN_POINT('Ctrl Pts',(10.3415549670129,-0.253116935651461,
135.717993534618));
#69812=CARTESIAN_POINT('Ctrl Pts',(10.3337902140658,-0.116264495999656,
135.723143729216));
#69813=CARTESIAN_POINT('Ctrl Pts',(10.3260254611187,0.0207075354470989,
135.722567024426));
#69814=CARTESIAN_POINT('Ctrl Pts',(10.3182684202337,0.157543524341253,135.721990892426));
#69815=CARTESIAN_POINT('Ctrl Pts',(10.3105113793487,0.294498480220442,135.715699182124));
#69816=CARTESIAN_POINT('Ctrl Pts',(10.3027543384637,0.431057734963402,135.703684274116));
#69817=CARTESIAN_POINT('Ctrl Pts',(10.2950031472236,0.567514009310084,135.691678426643));
#69818=CARTESIAN_POINT('Ctrl Pts',(10.2872519559834,0.703574788585392,135.673958006143));
#69819=CARTESIAN_POINT('Ctrl Pts',(10.2795007647433,0.838726663444165,135.650567448328));
#69820=CARTESIAN_POINT('Ctrl Pts',(10.2717528679662,0.973821095150829,135.627186832124));
#69821=CARTESIAN_POINT('Ctrl Pts',(10.2640049711892,1.10800700634759,135.598140938364));
#69822=CARTESIAN_POINT('Ctrl Pts',(10.2562570744121,1.24077758231864,135.563525886152));
#69823=CARTESIAN_POINT('Ctrl Pts',(10.248510798328,1.37352038554759,135.528918074663));
#69824=CARTESIAN_POINT('Ctrl Pts',(10.2407645222439,1.50484806434621,135.488743520438));
#69825=CARTESIAN_POINT('Ctrl Pts',(10.2330182461598,1.63426583875893,135.443149061844));
#69826=CARTESIAN_POINT('Ctrl Pts',(10.2252719128944,1.76368456850426,135.397554266681));
#69827=CARTESIAN_POINT('Ctrl Pts',(10.2175255796291,1.89119299698116,135.346539617228));
#69828=CARTESIAN_POINT('Ctrl Pts',(10.2097792463637,2.01631368197962,135.290301120778));
#69829=CARTESIAN_POINT('Ctrl Pts',(10.2020311783608,2.1414623868878,135.234050030108));
#69830=CARTESIAN_POINT('Ctrl Pts',(10.1942831103577,2.26422192775795,135.172572924839));
#69831=CARTESIAN_POINT('Ctrl Pts',(10.1865350423548,2.38413730313486,135.10611286314));
#69832=CARTESIAN_POINT('Ctrl Pts',(10.1787787396129,2.50418012599973,135.039582166896));
#69833=CARTESIAN_POINT('Ctrl Pts',(10.1710224368711,2.62137240247355,134.968058124825));
#69834=CARTESIAN_POINT('Ctrl Pts',(10.1632661341292,2.73528562434537,134.891828735576));
#69835=CARTESIAN_POINT('Ctrl Pts',(10.155505691615,2.84925964513373,134.815558660407));
#69836=CARTESIAN_POINT('Ctrl Pts',(10.1477452491009,2.95995080865304,134.734578464644));
#69837=CARTESIAN_POINT('Ctrl Pts',(10.1399848065868,3.06696263783213,134.649217343199));
#69838=CARTESIAN_POINT('Ctrl Pts',(10.1322119063213,3.17414625189949,134.563719192503));
#69839=CARTESIAN_POINT('Ctrl Pts',(10.1244390060559,3.2776384334331,134.473826319174));
#69840=CARTESIAN_POINT('Ctrl Pts',(10.1166661057904,3.37707795755671,134.37990638445));
#69841=CARTESIAN_POINT('Ctrl Pts',(10.1091757700284,3.47290260450552,134.289400675924));
#69842=CARTESIAN_POINT('Ctrl Pts',(10.1016854342664,3.5649639118874,134.195155830769));
#69843=CARTESIAN_POINT('Ctrl Pts',(10.0941950985043,3.65297454325851,134.097529311819));
#69844=CARTESIAN_POINT('Ctrl Pts',(10.0864207643853,3.74432212446818,133.99620125373));
#69845=CARTESIAN_POINT('Ctrl Pts',(10.0786464302662,3.83159516509547,133.890909050637));
#69846=CARTESIAN_POINT('Ctrl Pts',(10.0708720961471,3.91442994977599,133.78201426277));
#69847=CARTESIAN_POINT('Ctrl Pts',(10.0631073432,3.99716264798756,133.673253677997));
#69848=CARTESIAN_POINT('Ctrl Pts',(10.0553425902529,4.07546773900256,133.560899650636));
#69849=CARTESIAN_POINT('Ctrl Pts',(10.0475778373058,4.14901926965393,133.445349478304));
#69850=CARTESIAN_POINT('Ctrl Pts',(10.0398207964208,4.22249774788806,133.329914072032));
#69851=CARTESIAN_POINT('Ctrl Pts',(10.0320637555358,4.29123185278397,133.211289165783));
#69852=CARTESIAN_POINT('Ctrl Pts',(10.0243067146508,4.35493698323023,133.08990364595));
#69853=CARTESIAN_POINT('Ctrl Pts',(10.0165555234107,4.41859407314216,132.968609663881));
#69854=CARTESIAN_POINT('Ctrl Pts',(10.0088043321705,4.4772295561753,132.84455955671));
#69855=CARTESIAN_POINT('Ctrl Pts',(10.0010531409304,4.53060330705976,132.718209288846));
#69856=CARTESIAN_POINT('Ctrl Pts',(9.99330524415329,4.58395437267624,132.591912723216));
#69857=CARTESIAN_POINT('Ctrl Pts',(9.98555734737628,4.63204800230789,132.463318300721));
#69858=CARTESIAN_POINT('Ctrl Pts',(9.97780945059921,4.67469111794686,132.332904373658));
#69859=CARTESIAN_POINT('Ctrl Pts',(9.97006317451511,4.71732531356538,132.202517726378));
#69860=CARTESIAN_POINT('Ctrl Pts',(9.96231689843095,4.75451114154116,132.070312702935));
#69861=CARTESIAN_POINT('Ctrl Pts',(9.95457062234684,4.78610470049843,131.936784945443));
#69862=CARTESIAN_POINT('Ctrl Pts',(9.94682428908149,4.81769849267213,131.803256202279));
#69863=CARTESIAN_POINT('Ctrl Pts',(9.93907795581623,4.84369984343484,131.668405086043));
#69864=CARTESIAN_POINT('Ctrl Pts',(9.93133162255089,4.86401559009945,131.53273922912));
#69865=CARTESIAN_POINT('Ctrl Pts',(9.92358355454792,4.88433588633465,131.397042990769));
#69866=CARTESIAN_POINT('Ctrl Pts',(9.91583548654487,4.8989679869587,131.260532035244));
#69867=CARTESIAN_POINT('Ctrl Pts',(9.9080874185419,4.9078704442915,131.123720547034));
#69868=CARTESIAN_POINT('Ctrl Pts',(9.90033111580004,4.91678236326191,130.986763653946));
#69869=CARTESIAN_POINT('Ctrl Pts',(9.89257481305825,4.91995244901552,130.849505980879));
#69870=CARTESIAN_POINT('Ctrl Pts',(9.88481851031639,4.91739138381905,130.712463714233));
#69871=CARTESIAN_POINT('Ctrl Pts',(9.87705806780222,4.91482895170497,130.575348304003));
#69872=CARTESIAN_POINT('Ctrl Pts',(9.86929762528801,4.90652929719546,130.438448919336));
#69873=CARTESIAN_POINT('Ctrl Pts',(9.86153718277384,4.89255507575106,130.302277065513));
#69874=CARTESIAN_POINT('Ctrl Pts',(9.85376428250841,4.87855842164584,130.165886616541));
#69875=CARTESIAN_POINT('Ctrl Pts',(9.84599138224295,4.85886905347212,130.030226419376));
#69876=CARTESIAN_POINT('Ctrl Pts',(9.83821848197752,4.83360104417242,129.895799112617));
#69877=CARTESIAN_POINT('Ctrl Pts',(9.8307281462155,4.80925159065707,129.766258577061));
#69878=CARTESIAN_POINT('Ctrl Pts',(9.82323781045352,4.77972211863777,129.637863150984));
#69879=CARTESIAN_POINT('Ctrl Pts',(9.81574747469151,4.74515805935389,129.511047796069));
#69880=CARTESIAN_POINT('Ctrl Pts',(9.80797314057242,4.70928349325669,129.379424198427));
#69881=CARTESIAN_POINT('Ctrl Pts',(9.80019880645332,4.66787139098634,129.24908590997));
#69882=CARTESIAN_POINT('Ctrl Pts',(9.79242447233423,4.6210293463649,129.12053436687));
#69883=CARTESIAN_POINT('Ctrl Pts',(9.78465971938714,4.57424503037706,128.992141252057));
#69884=CARTESIAN_POINT('Ctrl Pts',(9.77689496644005,4.52204421952871,128.865530865083));
#69885=CARTESIAN_POINT('Ctrl Pts',(9.76913021349296,4.464584985908,128.741192188643));
#69886=CARTESIAN_POINT('Ctrl Pts',(9.76137317260795,4.40718282160814,128.616977007129));
#69887=CARTESIAN_POINT('Ctrl Pts',(9.75361613172297,4.3445327909691,128.495029398627));
#69888=CARTESIAN_POINT('Ctrl Pts',(9.74585909083797,4.27684189440716,128.375820629684));
#69889=CARTESIAN_POINT('Ctrl Pts',(9.73810789959784,4.20920204407687,128.256701757));
#69890=CARTESIAN_POINT('Ctrl Pts',(9.73035670835775,4.13652908646285,128.140317951463));
#69891=CARTESIAN_POINT('Ctrl Pts',(9.72260551711761,4.05907684376275,128.027117697163));
#69892=CARTESIAN_POINT('Ctrl Pts',(9.71485762034053,3.98165752033191,127.913965555991));
#69893=CARTESIAN_POINT('Ctrl Pts',(9.7071097235634,3.89946317227134,127.803994596847));
#69894=CARTESIAN_POINT('Ctrl Pts',(9.69936182678632,3.81279188753796,127.69762582283));
#69895=CARTESIAN_POINT('Ctrl Pts',(9.69161555070221,3.72613873256894,127.591279298867));
#69896=CARTESIAN_POINT('Ctrl Pts',(9.6838692746181,3.63501075044088,127.488533764175));
#69897=CARTESIAN_POINT('Ctrl Pts',(9.676122998534,3.53974715669219,127.389778193727));
#69898=CARTESIAN_POINT('Ctrl Pts',(9.66837666526864,3.44448285972928,127.291021894288));
#69899=CARTESIAN_POINT('Ctrl Pts',(9.66063033200331,3.34508316166357,127.196255899248));
#69900=CARTESIAN_POINT('Ctrl Pts',(9.65288399873796,3.24192479128902,127.105832976717));
#69901=CARTESIAN_POINT('Ctrl Pts',(9.64513593073498,3.13874331931268,127.0153898046));
#69902=CARTESIAN_POINT('Ctrl Pts',(9.63738786273201,3.03180179403487,126.929291898015));
#69903=CARTESIAN_POINT('Ctrl Pts',(9.62963979472903,2.92151040994382,126.847852057347));
#69904=CARTESIAN_POINT('Ctrl Pts',(9.62188349198717,2.81110180685728,126.766325661446));
#69905=CARTESIAN_POINT('Ctrl Pts',(9.61412718924527,2.69733654795029,126.689467453522));
#69906=CARTESIAN_POINT('Ctrl Pts',(9.60637088650341,2.58065468948598,126.617547457639));
#69907=CARTESIAN_POINT('Ctrl Pts',(9.59861044398924,2.46391055440042,126.545589075889));
#69908=CARTESIAN_POINT('Ctrl Pts',(9.59085000147507,2.34424705889555,126.478574348921));
#69909=CARTESIAN_POINT('Ctrl Pts',(9.58308955896089,2.22212841365627,126.416727044018));
#69910=CARTESIAN_POINT('Ctrl Pts',(9.57531665869545,2.09981373272648,126.354780456332));
#69911=CARTESIAN_POINT('Ctrl Pts',(9.56754375842999,1.97503638231783,126.298018029156));
#69912=CARTESIAN_POINT('Ctrl Pts',(9.55977085816454,1.84828090573022,126.246615478134));
#69913=CARTESIAN_POINT('Ctrl Pts',(9.5522805224025,1.72613330999434,126.197081539317));
#69914=CARTESIAN_POINT('Ctrl Pts',(9.54479018664053,1.60214920076463,126.152524656418));
#69915=CARTESIAN_POINT('Ctrl Pts',(9.5372998508785,1.47677313275936,126.11305758143));
#69916=CARTESIAN_POINT('Ctrl Pts',(9.52952551675939,1.34664339302863,126.072094100297));
#69917=CARTESIAN_POINT('Ctrl Pts',(9.52175118264028,1.21460184675343,126.036484246188));
#69918=CARTESIAN_POINT('Ctrl Pts',(9.5139768485212,1.08112852347603,126.006408535873));
#69919=CARTESIAN_POINT('Ctrl Pts',(9.5062120955741,0.947819694140715,125.976369891182));
#69920=CARTESIAN_POINT('Ctrl Pts',(9.49844734262707,0.813082976447265,125.951851904962));
#69921=CARTESIAN_POINT('Ctrl Pts',(9.49068258967998,0.677415207212283,125.93298589378));
#69922=CARTESIAN_POINT('Ctrl Pts',(9.48292554879497,0.541882185118286,125.914138620587));
#69923=CARTESIAN_POINT('Ctrl Pts',(9.47516850790994,0.40542033647734,125.900932204574));
#69924=CARTESIAN_POINT('Ctrl Pts',(9.46741146702493,0.268538039963397,125.893447221507));
#69925=CARTESIAN_POINT('Ctrl Pts',(9.45966027578481,0.131758967454229,125.885967882924));
#69926=CARTESIAN_POINT('Ctrl Pts',(9.45190908454467,-0.00543953303081873,
125.884201410645));
#69927=CARTESIAN_POINT('Ctrl Pts',(9.44415789330455,-0.142542942026305,
125.888176673471));
#69928=CARTESIAN_POINT('Ctrl Pts',(9.43640999652746,-0.279588078415802,
125.892150246704));
#69929=CARTESIAN_POINT('Ctrl Pts',(9.4286620997504,-0.416537813718125,125.901860689986));
#69930=CARTESIAN_POINT('Ctrl Pts',(9.42091420297331,-0.552876822281564,
125.917284775932));
#69931=CARTESIAN_POINT('Ctrl Pts',(9.4131679268892,-0.689187311663541,125.932705635492));
#69932=CARTESIAN_POINT('Ctrl Pts',(9.40542165080507,-0.824886940169155,
125.953837716535));
#69933=CARTESIAN_POINT('Ctrl Pts',(9.39767537472096,-0.959465097854031,
125.980605877895));
#69934=CARTESIAN_POINT('Ctrl Pts',(9.3899290414556,-1.09404424896429,126.007374236851));
#69935=CARTESIAN_POINT('Ctrl Pts',(9.38218270819028,-1.22750152928127,126.039778682872));
#69936=CARTESIAN_POINT('Ctrl Pts',(9.37443637492493,-1.35933651388733,126.077692943135));
#69937=CARTESIAN_POINT('Ctrl Pts',(9.36668830692195,-1.4912010220241,126.115615694033));
#69938=CARTESIAN_POINT('Ctrl Pts',(9.35894023891897,-1.62144213585741,126.159050606424));
#69939=CARTESIAN_POINT('Ctrl Pts',(9.35119217091599,-1.74957496742626,126.207821648314));
#69940=CARTESIAN_POINT('Ctrl Pts',(9.34343586817414,-1.8778439800933,126.256644524647));
#69941=CARTESIAN_POINT('Ctrl Pts',(9.33567956543229,-2.00399986846719,126.310814720217));
#69942=CARTESIAN_POINT('Ctrl Pts',(9.32792326269043,-2.12757759249629,126.370107957826));
#69943=CARTESIAN_POINT('Ctrl Pts',(9.32016282017626,-2.25122127367756,126.429432842022));
#69944=CARTESIAN_POINT('Ctrl Pts',(9.31240237766206,-2.37228370369536,126.493886032985));
#69945=CARTESIAN_POINT('Ctrl Pts',(9.30464193514788,-2.49032570358189,126.5631979288));
#69946=CARTESIAN_POINT('Ctrl Pts',(9.29686903488245,-2.60855719496591,126.632621090224));
#69947=CARTESIAN_POINT('Ctrl Pts',(9.28909613461702,-2.72375823829617,126.706918330613));
#69948=CARTESIAN_POINT('Ctrl Pts',(9.28132323435159,-2.83551909153673,126.785776968563));
#69949=CARTESIAN_POINT('Ctrl Pts',(9.27383289858961,-2.94321715625263,126.861768896391));
#69950=CARTESIAN_POINT('Ctrl Pts',(9.26634256282764,-3.04772056327013,126.941996155328));
#69951=CARTESIAN_POINT('Ctrl Pts',(9.25885222706566,-3.14869415846041,127.026145674107));
#69952=CARTESIAN_POINT('Ctrl Pts',(9.25118777213279,-3.25201497001521,127.112251319407));
#69953=CARTESIAN_POINT('Ctrl Pts',(9.24352331719991,-3.35198673246377,127.202753229069));
#69954=CARTESIAN_POINT('Ctrl Pts',(9.23585886226704,-3.44820420953052,127.297357510656));
#69955=CARTESIAN_POINT('Ctrl Pts',(9.2282031996922,-3.54431130973226,127.391853265972));
#69956=CARTESIAN_POINT('Ctrl Pts',(9.22054753711735,-3.63667240165821,127.490441759251));
#69957=CARTESIAN_POINT('Ctrl Pts',(9.21289187454252,-3.72491391245029,127.592787886437));
#69958=CARTESIAN_POINT('Ctrl Pts',(9.20524322549842,-3.81307458313985,127.695040251952));
#69959=CARTESIAN_POINT('Ctrl Pts',(9.19759457645428,-3.89712291543507,127.801043103937));
#69960=CARTESIAN_POINT('Ctrl Pts',(9.18994592741018,-3.97672134586974,127.910423783459));
#69961=CARTESIAN_POINT('Ctrl Pts',(9.18230251965738,-4.0562652309123,128.019729509089));
#69962=CARTESIAN_POINT('Ctrl Pts',(9.17465911190463,-4.13136504286035,128.13240813422));
#69963=CARTESIAN_POINT('Ctrl Pts',(9.16701570415182,-4.20172313864092,128.248053568577));
#69964=CARTESIAN_POINT('Ctrl Pts',(9.15937504556866,-4.27205592812527,128.363657407756));
#69965=CARTESIAN_POINT('Ctrl Pts',(9.15173438698547,-4.33765018133567,128.482225592273));
#69966=CARTESIAN_POINT('Ctrl Pts',(9.14409372840231,-4.39825153053533,128.603323013016));
#69967=CARTESIAN_POINT('Ctrl Pts',(9.13645474582435,-4.45883958661697,128.724393870616));
#69968=CARTESIAN_POINT('Ctrl Pts',(9.12881576324646,-4.5144367404964,128.847992499081));
#69969=CARTESIAN_POINT('Ctrl Pts',(9.12117678066849,-4.5648348802313,128.973659773975));
#69970=CARTESIAN_POINT('Ctrl Pts',(9.11353577045341,-4.61524639728936,129.099360405096));
#69971=CARTESIAN_POINT('Ctrl Pts',(9.10589476023829,-4.66045599357105,129.227130405468));
#69972=CARTESIAN_POINT('Ctrl Pts',(9.09825375002322,-4.70030402803673,129.356491456861));
#69973=CARTESIAN_POINT('Ctrl Pts',(9.09383360368492,-4.72335518733032,129.431323810376));
#69974=CARTESIAN_POINT('Ctrl Pts',(9.08941345734662,-4.74461309477974,129.506688265335));
#69975=CARTESIAN_POINT('Ctrl Pts',(9.08499331100833,-4.76405452823402,129.582490119308));
#69976=CARTESIAN_POINT('Ctrl Pts',(10.8346522545385,-4.76405452823403,129.582490119308));
#69977=CARTESIAN_POINT('Ctrl Pts',(10.8267790172283,-4.79867665138673,129.717481252017));
#69978=CARTESIAN_POINT('Ctrl Pts',(10.818905779918,-4.82758080289594,129.854037654495));
#69979=CARTESIAN_POINT('Ctrl Pts',(10.8110325426078,-4.85063653588562,129.991644025369));
#69980=CARTESIAN_POINT('Ctrl Pts',(10.8031633271452,-4.87368049142725,130.12918010345));
#69981=CARTESIAN_POINT('Ctrl Pts',(10.7952941116825,-4.89088191557338,130.267764714496));
#69982=CARTESIAN_POINT('Ctrl Pts',(10.7874248962198,-4.9021613315402,130.40687182269));
#69983=CARTESIAN_POINT('Ctrl Pts',(10.7799030761437,-4.91294280497544,130.539837890797));
#69984=CARTESIAN_POINT('Ctrl Pts',(10.7723812560675,-4.91831389514874,130.673280985255));
#69985=CARTESIAN_POINT('Ctrl Pts',(10.7648594359913,-4.91824942613528,130.806736500554));
#69986=CARTESIAN_POINT('',(11.1101405640401,-4.91824801950251,130.799946870896));
#69987=CARTESIAN_POINT('Ctrl Pts',(11.1800167307073,-4.76405452823405,129.582490119308));
#69988=CARTESIAN_POINT('Ctrl Pts',(11.1703218396064,-4.8063363855668,129.747346439332));
#69989=CARTESIAN_POINT('Ctrl Pts',(11.1606269485055,-4.840089161629,129.914523699574));
#69990=CARTESIAN_POINT('Ctrl Pts',(11.1509320574046,-4.86509658065642,130.083237657603));
#69991=CARTESIAN_POINT('Ctrl Pts',(11.1413830686639,-4.88972765286176,130.249412570645));
#69992=CARTESIAN_POINT('Ctrl Pts',(11.1318340799231,-4.9058745984055,130.417078356921));
#69993=CARTESIAN_POINT('Ctrl Pts',(11.1222850911824,-4.91337637600288,130.585464180325));
#69994=CARTESIAN_POINT('Ctrl Pts',(11.1182369154683,-4.91655666186421,130.656849268255));
#69995=CARTESIAN_POINT('Ctrl Pts',(11.1141887397541,-4.91818377896244,130.728363490022));
#69996=CARTESIAN_POINT('Ctrl Pts',(11.11014056404,-4.91824801950251,130.799946870896));
#69997=CARTESIAN_POINT('Ctrl Pts',(11.1101405640087,-4.918248019503,130.799946871451));
#69998=CARTESIAN_POINT('Ctrl Pts',(11.1024544495004,-4.91836999051411,130.935859465454));
#69999=CARTESIAN_POINT('Ctrl Pts',(11.0947683349922,-4.91285393968429,131.071890269725));
#70000=CARTESIAN_POINT('Ctrl Pts',(11.0870822204839,-4.90169732681665,131.207531026672));
#70001=CARTESIAN_POINT('Ctrl Pts',(11.0793992390307,-4.89054526166714,131.343116493009));
#70002=CARTESIAN_POINT('Ctrl Pts',(11.0717162575775,-4.87375723796405,131.478311832142));
#70003=CARTESIAN_POINT('Ctrl Pts',(11.0640332761243,-4.85138278522514,131.612610661625));
#70004=CARTESIAN_POINT('Ctrl Pts',(11.0563517432926,-4.82901255117571,131.746884169145));
#70005=CARTESIAN_POINT('Ctrl Pts',(11.0486702104609,-4.80105804789083,131.880261110623));
#70006=CARTESIAN_POINT('Ctrl Pts',(11.0409886776292,-4.76762039214223,132.012242589834));
#70007=CARTESIAN_POINT('Ctrl Pts',(11.0333068612482,-4.73418150210544,132.144228940893));
#70008=CARTESIAN_POINT('Ctrl Pts',(11.0256250448671,-4.69525915478474,132.274819341283));
#70009=CARTESIAN_POINT('Ctrl Pts',(11.0179432284861,-4.65100495372822,132.403527895525));
#70010=CARTESIAN_POINT('Ctrl Pts',(11.0102593964723,-4.60673914080644,132.532270221621));
#70011=CARTESIAN_POINT('Ctrl Pts',(11.0025755644586,-4.55713882092296,132.659129343108));
#70012=CARTESIAN_POINT('Ctrl Pts',(10.9948917324448,-4.50240437979523,132.78363772381));
#70013=CARTESIAN_POINT('Ctrl Pts',(10.9871995896671,-4.44761073838575,132.908280771662));
#70014=CARTESIAN_POINT('Ctrl Pts',(10.9795074468893,-4.38767204782599,133.03056763695));
#70015=CARTESIAN_POINT('Ctrl Pts',(10.9718153041116,-4.32283564172309,133.150053495406));
#70016=CARTESIAN_POINT('Ctrl Pts',(10.9641186702404,-4.25796138058213,133.269609116238));
#70017=CARTESIAN_POINT('Ctrl Pts',(10.9564220363693,-4.18818391336705,133.386360132513));
#70018=CARTESIAN_POINT('Ctrl Pts',(10.9487254024982,-4.11379421335629,133.49989029328));
#70019=CARTESIAN_POINT('Ctrl Pts',(10.9410169382095,-4.03929016969578,133.613594960101));
#70020=CARTESIAN_POINT('Ctrl Pts',(10.9333084739209,-3.96015996659395,133.724068561489));
#70021=CARTESIAN_POINT('Ctrl Pts',(10.9256000096322,-3.87673554877064,133.830927079317));
#70022=CARTESIAN_POINT('Ctrl Pts',(10.9203829976827,-3.82027473266398,133.903247861193));
#70023=CARTESIAN_POINT('Ctrl Pts',(10.9151659857332,-3.7618477954338,133.973913487563));
#70024=CARTESIAN_POINT('Ctrl Pts',(10.9099489737837,-3.70156693300311,134.042814770862));
#70025=CARTESIAN_POINT('Ctrl Pts',(10.9021746396646,-3.61173705144308,134.145490709269));
#70026=CARTESIAN_POINT('Ctrl Pts',(10.8944003055455,-3.51748953239293,134.244588826331));
#70027=CARTESIAN_POINT('Ctrl Pts',(10.8866259714264,-3.41914044743804,134.339705249026));
#70028=CARTESIAN_POINT('Ctrl Pts',(10.8788612184793,-3.32091256894066,134.434704449231));
#70029=CARTESIAN_POINT('Ctrl Pts',(10.8710964655323,-3.21859346044696,134.525731449512));
#70030=CARTESIAN_POINT('Ctrl Pts',(10.8633317125852,-3.1125391408373,134.612415653835));
#70031=CARTESIAN_POINT('Ctrl Pts',(10.8555746717002,-3.00659015587313,134.699013762185));
#70032=CARTESIAN_POINT('Ctrl Pts',(10.8478176308151,-2.89691364334437,134.781277412468));
#70033=CARTESIAN_POINT('Ctrl Pts',(10.8400605899301,-2.78390187384632,134.85887334036));
#70034=CARTESIAN_POINT('Ctrl Pts',(10.83230939869,-2.67097532740261,134.936410752558));
#70035=CARTESIAN_POINT('Ctrl Pts',(10.8245582074499,-2.55471885122989,135.009287228239));
#70036=CARTESIAN_POINT('Ctrl Pts',(10.8168070162097,-2.4355568573981,135.077210469466));
#70037=CARTESIAN_POINT('Ctrl Pts',(10.8090591194327,-2.31644551059244,135.145104841504));
#70038=CARTESIAN_POINT('Ctrl Pts',(10.8013112226556,-2.19443144124389,135.20804997308));
#70039=CARTESIAN_POINT('Ctrl Pts',(10.7935633258785,-2.06996684930385,135.265797640016));
#70040=CARTESIAN_POINT('Ctrl Pts',(10.7858170497944,-1.94552829267329,135.323533227384));
#70041=CARTESIAN_POINT('Ctrl Pts',(10.7780707737103,-1.81864058746095,135.376073348166));
#70042=CARTESIAN_POINT('Ctrl Pts',(10.7703244976262,-1.68977891060562,135.423216568532));
#70043=CARTESIAN_POINT('Ctrl Pts',(10.7625781643609,-1.56091628252266,135.470360136898));
#70044=CARTESIAN_POINT('Ctrl Pts',(10.7548318310955,-1.43008002088606,135.512106591029));
#70045=CARTESIAN_POINT('Ctrl Pts',(10.7470854978302,-1.29776320166481,135.548303464492));
#70046=CARTESIAN_POINT('Ctrl Pts',(10.7393374298272,-1.16541675100968,135.584508443994));
#70047=CARTESIAN_POINT('Ctrl Pts',(10.7315893618243,-1.03158946003955,135.615161266677));
#70048=CARTESIAN_POINT('Ctrl Pts',(10.7238412938213,-0.896787018960324,
135.640160045285));
#70049=CARTESIAN_POINT('Ctrl Pts',(10.7160849910794,-0.76184130824218,135.665185392892));
#70050=CARTESIAN_POINT('Ctrl Pts',(10.7083286883375,-0.625918762115954,
135.684544621027));
#70051=CARTESIAN_POINT('Ctrl Pts',(10.7005723855956,-0.489533215689875,
135.698187371062));
#70052=CARTESIAN_POINT('Ctrl Pts',(10.6928119430815,-0.353074876191179,
135.711837402644));
#70053=CARTESIAN_POINT('Ctrl Pts',(10.6850515005674,-0.216153434111273,
135.719764854052));
#70054=CARTESIAN_POINT('Ctrl Pts',(10.6772910580532,-0.0792842146913874,
135.721971528954));
#70055=CARTESIAN_POINT('Ctrl Pts',(10.6695181577878,0.0578047193501897,
135.724181746207));
#70056=CARTESIAN_POINT('Ctrl Pts',(10.6617452575223,0.194840872147232,135.720652845469));
#70057=CARTESIAN_POINT('Ctrl Pts',(10.6539723572569,0.331311650224775,135.711438735237));
#70058=CARTESIAN_POINT('Ctrl Pts',(10.6464820214948,0.462821371771351,135.702559581121));
#70059=CARTESIAN_POINT('Ctrl Pts',(10.6389916857327,0.593805804300594,135.688401417735));
#70060=CARTESIAN_POINT('Ctrl Pts',(10.6315013499706,0.723815853872389,135.669057285621));
#70061=CARTESIAN_POINT('Ctrl Pts',(10.6237270158515,0.858755273988071,135.648979714858));
#70062=CARTESIAN_POINT('Ctrl Pts',(10.6159526817324,0.993072412647427,135.623251560731));
#70063=CARTESIAN_POINT('Ctrl Pts',(10.6081783476133,1.12625663562571,135.591920439982));
#70064=CARTESIAN_POINT('Ctrl Pts',(10.6004135946663,1.25927672095201,135.560627932039));
#70065=CARTESIAN_POINT('Ctrl Pts',(10.5926488417192,1.39116629173078,135.523746285345));
#70066=CARTESIAN_POINT('Ctrl Pts',(10.5848840887721,1.52142111812217,135.481374712459));
#70067=CARTESIAN_POINT('Ctrl Pts',(10.5771270478871,1.65154657358389,135.439045223617));
#70068=CARTESIAN_POINT('Ctrl Pts',(10.5693700070021,1.78004014641446,135.391236779806));
#70069=CARTESIAN_POINT('Ctrl Pts',(10.5616129661171,1.90640942006008,135.338099271878));
#70070=CARTESIAN_POINT('Ctrl Pts',(10.5538617748769,2.03268339765342,135.285001835359));
#70071=CARTESIAN_POINT('Ctrl Pts',(10.5461105836368,2.15683590570613,135.226583484613));
#70072=CARTESIAN_POINT('Ctrl Pts',(10.5383593923967,2.2783916205963,135.163043295359));
#70073=CARTESIAN_POINT('Ctrl Pts',(10.5306114956196,2.39989567106504,135.099530112382));
#70074=CARTESIAN_POINT('Ctrl Pts',(10.5228635988425,2.51880477780077,135.030899601358));
#70075=CARTESIAN_POINT('Ctrl Pts',(10.5151157020654,2.63466567765311,134.957398039682));
#70076=CARTESIAN_POINT('Ctrl Pts',(10.5073694259813,2.75050234190286,134.883911852949));
#70077=CARTESIAN_POINT('Ctrl Pts',(10.4996231498972,2.86329173760149,134.805556851553));
#70078=CARTESIAN_POINT('Ctrl Pts',(10.4918768738131,2.97260754802252,134.722623935407));
#70079=CARTESIAN_POINT('Ctrl Pts',(10.4841305405477,3.08192416538788,134.639690407069));
#70080=CARTESIAN_POINT('Ctrl Pts',(10.4763842072824,3.18776683483693,134.552179132851));
#70081=CARTESIAN_POINT('Ctrl Pts',(10.468637874017,3.28974076243709,134.460422539698));
#70082=CARTESIAN_POINT('Ctrl Pts',(10.4608898060141,3.39173752639143,134.368645398291));
#70083=CARTESIAN_POINT('Ctrl Pts',(10.4531417380112,3.48986353393035,134.272621307609));
#70084=CARTESIAN_POINT('Ctrl Pts',(10.4453936700082,3.58375972651124,134.172720646591));
#70085=CARTESIAN_POINT('Ctrl Pts',(10.4376373672663,3.67775571308298,134.072713809963));
#70086=CARTESIAN_POINT('Ctrl Pts',(10.4298810645244,3.76751263626869,133.968822458062));
#70087=CARTESIAN_POINT('Ctrl Pts',(10.4221247617825,3.85271038750178,133.861451674852));
#70088=CARTESIAN_POINT('Ctrl Pts',(10.4143643192683,3.93795361134007,133.754023584621));
#70089=CARTESIAN_POINT('Ctrl Pts',(10.4066038767542,4.01863258466237,133.643112678706));
#70090=CARTESIAN_POINT('Ctrl Pts',(10.39884343424,4.09447027906687,133.529153489756));
#70091=CARTESIAN_POINT('Ctrl Pts',(10.3910705339746,4.17042971487088,133.415011363399));
#70092=CARTESIAN_POINT('Ctrl Pts',(10.3832976337091,4.24153213861732,133.297811509938));
#70093=CARTESIAN_POINT('Ctrl Pts',(10.3755247334437,4.30754583575698,133.178014327641));
#70094=CARTESIAN_POINT('Ctrl Pts',(10.3680343976817,4.3711597687267,133.062572074672));
#70095=CARTESIAN_POINT('Ctrl Pts',(10.3605440619197,4.43004839014375,132.944718328772));
#70096=CARTESIAN_POINT('Ctrl Pts',(10.3530537261578,4.48404723140638,132.824881216079));
#70097=CARTESIAN_POINT('Ctrl Pts',(10.3452793920387,4.54009345514839,132.700500442834));
#70098=CARTESIAN_POINT('Ctrl Pts',(10.3375050579196,4.59104932474587,132.57358893427));
#70099=CARTESIAN_POINT('Ctrl Pts',(10.3297307238005,4.6366788912414,132.444602039435));
#70100=CARTESIAN_POINT('Ctrl Pts',(10.3219659708534,4.6822522233743,132.315774109421));
#70101=CARTESIAN_POINT('Ctrl Pts',(10.3142012179064,4.72251218405631,132.184876247295));
#70102=CARTESIAN_POINT('Ctrl Pts',(10.3064364649593,4.75726969507791,132.052386302716));
#70103=CARTESIAN_POINT('Ctrl Pts',(10.2986794240743,4.79199268444946,131.920027949017));
#70104=CARTESIAN_POINT('Ctrl Pts',(10.2909223831893,4.82122400141028,131.786081035402));
#70105=CARTESIAN_POINT('Ctrl Pts',(10.2831653423043,4.84482359020511,131.65104086553));
#70106=CARTESIAN_POINT('Ctrl Pts',(10.2754141510642,4.86840538236648,131.5161025305));
#70107=CARTESIAN_POINT('Ctrl Pts',(10.267662959824,4.8863638325859,131.380072963768));
#70108=CARTESIAN_POINT('Ctrl Pts',(10.2599117685838,4.89860950487715,131.243459673847));
#70109=CARTESIAN_POINT('Ctrl Pts',(10.2521638718067,4.91084997243103,131.106904448219));
#70110=CARTESIAN_POINT('Ctrl Pts',(10.2444159750297,4.91738245649662,130.96976638144));
#70111=CARTESIAN_POINT('Ctrl Pts',(10.2366680782526,4.91816915741655,130.832559935582));
#70112=CARTESIAN_POINT('Ctrl Pts',(10.2289218021686,4.91895569377562,130.695382190354));
#70113=CARTESIAN_POINT('Ctrl Pts',(10.2211755260845,4.91399883538182,130.55813648521));
#70114=CARTESIAN_POINT('Ctrl Pts',(10.2134292500004,4.90331288996588,130.421338730992));
#70115=CARTESIAN_POINT('Ctrl Pts',(10.205682916735,4.89262686566873,130.284539966965));
#70116=CARTESIAN_POINT('Ctrl Pts',(10.1979365834697,4.87621170040865,130.148189550241));
#70117=CARTESIAN_POINT('Ctrl Pts',(10.1901902502044,4.85413367862674,130.01279931702));
#70118=CARTESIAN_POINT('Ctrl Pts',(10.1824421822014,4.83205071262496,129.877378764096));
#70119=CARTESIAN_POINT('Ctrl Pts',(10.1746941141985,4.80430242952618,129.742919208349));
#70120=CARTESIAN_POINT('Ctrl Pts',(10.1669460461955,4.77100635971077,129.609922934763));
#70121=CARTESIAN_POINT('Ctrl Pts',(10.1591897434537,4.73767490243609,129.476785311155));
#70122=CARTESIAN_POINT('Ctrl Pts',(10.1514334407118,4.6987839751433,129.345114456242));
#70123=CARTESIAN_POINT('Ctrl Pts',(10.14367713797,4.65450135994198,129.215398644202));
#70124=CARTESIAN_POINT('Ctrl Pts',(10.1359166954558,4.61019510977554,129.085613598926));
#70125=CARTESIAN_POINT('Ctrl Pts',(10.1281562529416,4.5604915792441,128.957786039927));
#70126=CARTESIAN_POINT('Ctrl Pts',(10.1203958104275,4.50560661235295,128.832383914554));
#70127=CARTESIAN_POINT('Ctrl Pts',(10.112622910162,4.45063353924048,128.706780482557));
#70128=CARTESIAN_POINT('Ctrl Pts',(10.1048500098967,4.39046258006013,128.583610616173));
#70129=CARTESIAN_POINT('Ctrl Pts',(10.0970771096312,4.32535583353923,128.463318119924));
#70130=CARTESIAN_POINT('Ctrl Pts',(10.0895867738691,4.26261588124758,128.34739855891));
#70131=CARTESIAN_POINT('Ctrl Pts',(10.082096438107,4.19529292534033,128.234151065501));
#70132=CARTESIAN_POINT('Ctrl Pts',(10.0746061023449,4.12365826116438,128.123945424423));
#70133=CARTESIAN_POINT('Ctrl Pts',(10.0668317682258,4.04930754692415,128.009561302969));
#70134=CARTESIAN_POINT('Ctrl Pts',(10.0590574341066,3.97007619263236,127.898091916367));
#70135=CARTESIAN_POINT('Ctrl Pts',(10.0512830999876,3.88621976016404,127.789981902439));
#70136=CARTESIAN_POINT('Ctrl Pts',(10.0435183470405,3.80246667325427,127.682005124442));
#70137=CARTESIAN_POINT('Ctrl Pts',(10.0357535940935,3.71410008678098,127.577379787462));
#70138=CARTESIAN_POINT('Ctrl Pts',(10.0279888411464,3.62141982780256,127.476523257763));
#70139=CARTESIAN_POINT('Ctrl Pts',(10.0202318002614,3.52883162016379,127.375766900192));
#70140=CARTESIAN_POINT('Ctrl Pts',(10.0124747593763,3.43193852899701,127.278772186714));
#70141=CARTESIAN_POINT('Ctrl Pts',(10.0047177184913,3.3310815637425,127.18592467393));
#70142=CARTESIAN_POINT('Ctrl Pts',(9.99696652725117,3.23030065551072,127.093147178179));
#70143=CARTESIAN_POINT('Ctrl Pts',(9.98921533601106,3.12556210946481,127.004510921874));
#70144=CARTESIAN_POINT('Ctrl Pts',(9.98146414477097,3.01724456455642,126.920365470793));
#70145=CARTESIAN_POINT('Ctrl Pts',(9.97371624799389,2.90897305749364,126.836255783773));
#70146=CARTESIAN_POINT('Ctrl Pts',(9.96596835121683,2.79712588516252,126.756633345042));
#70147=CARTESIAN_POINT('Ctrl Pts',(9.95822045443975,2.68211544743726,126.681808035837));
#70148=CARTESIAN_POINT('Ctrl Pts',(9.95047417835566,2.56712906741623,126.606998378474));
#70149=CARTESIAN_POINT('Ctrl Pts',(9.94272790227159,2.44898106563803,126.536984067783));
#70150=CARTESIAN_POINT('Ctrl Pts',(9.93498162618749,2.32811322618503,126.472031928678));
#70151=CARTESIAN_POINT('Ctrl Pts',(9.92723529292215,2.2072444945131,126.407079310111));
#70152=CARTESIAN_POINT('Ctrl Pts',(9.91948895965675,2.08365622949244,126.347189122762));
#70153=CARTESIAN_POINT('Ctrl Pts',(9.9117426263914,1.95781488177463,126.292582259623));
#70154=CARTESIAN_POINT('Ctrl Pts',(9.90399455838842,1.83194535275952,126.237963167656));
#70155=CARTESIAN_POINT('Ctrl Pts',(9.8962464903855,1.70382209561181,126.18862990986));
#70156=CARTESIAN_POINT('Ctrl Pts',(9.88849842238253,1.57393122495696,126.144755101902));
#70157=CARTESIAN_POINT('Ctrl Pts',(9.88074211964067,1.44390230473888,126.100833663276));
#70158=CARTESIAN_POINT('Ctrl Pts',(9.87298581689877,1.31210238922202,126.062382388535));
#70159=CARTESIAN_POINT('Ctrl Pts',(9.86522951415691,1.17903296763002,126.02952404196));
#70160=CARTESIAN_POINT('Ctrl Pts',(9.85746907164274,1.04589252288108,125.996648157896));
#70161=CARTESIAN_POINT('Ctrl Pts',(9.84970862912859,0.911481604901739,125.969371227809));
#70162=CARTESIAN_POINT('Ctrl Pts',(9.84194818661442,0.776310580008076,125.947764592996));
#70163=CARTESIAN_POINT('Ctrl Pts',(9.83417528634898,0.640922566585333,125.926123273295));
#70164=CARTESIAN_POINT('Ctrl Pts',(9.82640238608358,0.504772396449882,125.910170484012));
#70165=CARTESIAN_POINT('Ctrl Pts',(9.81862948581815,0.368375125679472,125.899925601249));
#70166=CARTESIAN_POINT('Ctrl Pts',(9.81113915005611,0.236936239265373,125.890053145779));
#70167=CARTESIAN_POINT('Ctrl Pts',(9.80364881429403,0.105268213603494,125.885480818858));
#70168=CARTESIAN_POINT('Ctrl Pts',(9.79615847853199,-0.0261711991809226,
125.886180249703));
#70169=CARTESIAN_POINT('Ctrl Pts',(9.78838414441291,-0.162594177251013,
125.886906199681));
#70170=CARTESIAN_POINT('Ctrl Pts',(9.78060981029386,-0.299203011504808,
125.893313855746));
#70171=CARTESIAN_POINT('Ctrl Pts',(9.77283547617478,-0.435485478113105,
125.905428544057));
#70172=CARTESIAN_POINT('Ctrl Pts',(9.76507072322768,-0.57159998876122,125.917528302098));
#70173=CARTESIAN_POINT('Ctrl Pts',(9.75730597028051,-0.707388546368588,
125.935321063716));
#70174=CARTESIAN_POINT('Ctrl Pts',(9.74954121733342,-0.842337945028206,
125.958780172576));
#70175=CARTESIAN_POINT('Ctrl Pts',(9.7417841764484,-0.977153310042805,125.982215981519));
#70176=CARTESIAN_POINT('Ctrl Pts',(9.73402713556341,-1.11113079204565,126.01130687141));
#70177=CARTESIAN_POINT('Ctrl Pts',(9.7262700946784,-1.24376168741733,126.04597434411));
#70178=CARTESIAN_POINT('Ctrl Pts',(9.71851890343822,-1.37629256479963,126.080615673799));
#70179=CARTESIAN_POINT('Ctrl Pts',(9.71076771219805,-1.50747850005841,126.120825117345));
#70180=CARTESIAN_POINT('Ctrl Pts',(9.70301652095787,-1.6368207300032,126.166473063913));
#70181=CARTESIAN_POINT('Ctrl Pts',(9.69526862418079,-1.76610798604925,126.212101608886));
#70182=CARTESIAN_POINT('Ctrl Pts',(9.68752072740372,-1.89355272744303,126.263163929624));
#70183=CARTESIAN_POINT('Ctrl Pts',(9.67977283062663,-2.01867133011636,126.319480560812));
#70184=CARTESIAN_POINT('Ctrl Pts',(9.67202655454253,-2.14376376067508,126.375785411776));
#70185=CARTESIAN_POINT('Ctrl Pts',(9.66428027845839,-2.26653066405425,126.437342226674));
#70186=CARTESIAN_POINT('Ctrl Pts',(9.65653400237429,-2.38650875780919,126.50392354543));
#70187=CARTESIAN_POINT('Ctrl Pts',(9.64878766910891,-2.50648773721548,126.570505355675));
#70188=CARTESIAN_POINT('Ctrl Pts',(9.64104133584361,-2.62367752406538,126.642111554077));
#70189=CARTESIAN_POINT('Ctrl Pts',(9.63329500257825,-2.73764014685824,126.718469100552));
#70190=CARTESIAN_POINT('Ctrl Pts',(9.62554693457525,-2.85162829079047,126.794843746769));
#70191=CARTESIAN_POINT('Ctrl Pts',(9.61779886657223,-2.9623875078377,126.875971640777));
#70192=CARTESIAN_POINT('Ctrl Pts',(9.61005079856923,-3.06950981472219,126.961537103557));
#70193=CARTESIAN_POINT('Ctrl Pts',(9.60229449582738,-3.17674597246892,127.047193506328));
#70194=CARTESIAN_POINT('Ctrl Pts',(9.59453819308545,-3.28033719263344,127.137296654798));
#70195=CARTESIAN_POINT('Ctrl Pts',(9.58678189034359,-3.37990912297542,127.231490988972));
#70196=CARTESIAN_POINT('Ctrl Pts',(9.57902144782944,-3.4795341978544,127.325735597498));
#70197=CARTESIAN_POINT('Ctrl Pts',(9.5712610053153,-3.57513543599653,127.424075462521));
#70198=CARTESIAN_POINT('Ctrl Pts',(9.56350056280115,-3.66637695048661,127.526119760118));
#70199=CARTESIAN_POINT('Ctrl Pts',(9.55572766253572,-3.75776493395605,127.628327868282));
#70200=CARTESIAN_POINT('Ctrl Pts',(9.54795476227035,-3.84477895999743,127.734251990114));
#70201=CARTESIAN_POINT('Ctrl Pts',(9.54018186200491,-3.92712432655619,127.843469267606));
#70202=CARTESIAN_POINT('Ctrl Pts',(9.53269152624299,-4.00647623162396,127.948716221957));
#70203=CARTESIAN_POINT('Ctrl Pts',(9.52520119048102,-4.08149284379729,128.057020806591));
#70204=CARTESIAN_POINT('Ctrl Pts',(9.5177108547191,-4.15195060601324,128.167982566579));
#70205=CARTESIAN_POINT('Ctrl Pts',(9.50974150827459,-4.22691417702676,128.286040386087));
#70206=CARTESIAN_POINT('Ctrl Pts',(9.50177216183008,-4.29694495240893,128.40746501991));
#70207=CARTESIAN_POINT('Ctrl Pts',(9.49380281538558,-4.36173500513333,128.53181781104));
#70208=CARTESIAN_POINT('Ctrl Pts',(9.48584369238272,-4.42644194221854,128.656011076728));
#70209=CARTESIAN_POINT('Ctrl Pts',(9.47788456937984,-4.48592137079548,128.783124703114));
#70210=CARTESIAN_POINT('Ctrl Pts',(9.46992544637698,-4.5399085880573,128.912691229279));
#70211=CARTESIAN_POINT('Ctrl Pts',(9.46197826351917,-4.59381481458623,129.042063381878));
#70212=CARTESIAN_POINT('Ctrl Pts',(9.45403108066137,-4.642245108635,129.173880767391));
#70213=CARTESIAN_POINT('Ctrl Pts',(9.44608389780356,-4.68498097380139,129.307652116348));
#70214=CARTESIAN_POINT('Ctrl Pts',(9.44069156785431,-4.71397815302414,129.398418777219));
#70215=CARTESIAN_POINT('Ctrl Pts',(9.4352992379051,-4.74035460762676,129.490084488557));
#70216=CARTESIAN_POINT('Ctrl Pts',(9.42990690795585,-4.76405452823399,129.582490119308));
#70217=CARTESIAN_POINT('Origin',(213.235140564004,0.,130.804360617566));
#70218=CARTESIAN_POINT('',(7.33490367089153,-4.76405452823399,129.582490119308));
#70219=CARTESIAN_POINT('',(7.68025985017537,-4.76405452823403,129.582490119308));
#70220=CARTESIAN_POINT('',(213.235140564004,-4.76405452823405,129.582490119308));
#70221=CARTESIAN_POINT('',(9.01485943602795,-4.91824886988786,130.807694736162));
#70222=CARTESIAN_POINT('Ctrl Pts',(9.0148594359913,-4.91824886988742,130.807694736807));
#70223=CARTESIAN_POINT('Ctrl Pts',(9.00337449174511,-4.91811194828998,131.009671463859));
#70224=CARTESIAN_POINT('Ctrl Pts',(8.99188954749892,-4.90553346737286,131.211229737893));
#70225=CARTESIAN_POINT('Ctrl Pts',(8.98040460325277,-4.88066534031835,131.41122872376));
#70226=CARTESIAN_POINT('Ctrl Pts',(8.97263026913369,-4.86383172541402,131.546611090995));
#70227=CARTESIAN_POINT('Ctrl Pts',(8.96485593501466,-4.84133422133454,131.681506954395));
#70228=CARTESIAN_POINT('Ctrl Pts',(8.95708160089558,-4.81320817729648,131.815404684116));
#70229=CARTESIAN_POINT('Ctrl Pts',(8.9493168479485,-4.78511679609403,131.949137396852));
#70230=CARTESIAN_POINT('Ctrl Pts',(8.94155209500138,-4.7514107564428,132.08187404452));
#70231=CARTESIAN_POINT('Ctrl Pts',(8.9337873420543,-4.71217714220482,132.213108161657));
#70232=CARTESIAN_POINT('Ctrl Pts',(8.9260303011693,-4.67298249534548,132.34421193522));
#70233=CARTESIAN_POINT('Ctrl Pts',(8.91827326028429,-4.62827131063702,132.473815775905));
#70234=CARTESIAN_POINT('Ctrl Pts',(8.91051621939928,-4.57818161912834,132.601423811996));
#70235=CARTESIAN_POINT('Ctrl Pts',(8.90276502815916,-4.52812970064574,132.728935617874));
#70236=CARTESIAN_POINT('Ctrl Pts',(8.89501383691906,-4.47270749080831,132.854454252413));
#70237=CARTESIAN_POINT('Ctrl Pts',(8.88726264567893,-4.41210260155147,132.977499751603));
#70238=CARTESIAN_POINT('Ctrl Pts',(8.87951474890185,-4.35152347098925,133.100492953173));
#70239=CARTESIAN_POINT('Ctrl Pts',(8.87176685212476,-4.28576621455026,133.221014760054));
#70240=CARTESIAN_POINT('Ctrl Pts',(8.86401895534769,-4.21506616164149,133.338606129643));
#70241=CARTESIAN_POINT('Ctrl Pts',(8.8562726792636,-4.14438089765976,133.456172901654));
#70242=CARTESIAN_POINT('Ctrl Pts',(8.84852640317951,-4.06875509507117,133.570810120778));
#70243=CARTESIAN_POINT('Ctrl Pts',(8.84078012709543,-3.98846933958987,133.682084612262));
#70244=CARTESIAN_POINT('Ctrl Pts',(8.83303379383008,-3.90818299145725,133.79335992515));
#70245=CARTESIAN_POINT('Ctrl Pts',(8.82528746056474,-3.82323685054995,133.901272143812));
#70246=CARTESIAN_POINT('Ctrl Pts',(8.81754112729939,-3.73395377411807,134.005418610675));
#70247=CARTESIAN_POINT('Ctrl Pts',(8.80979305929643,-3.64465070336038,134.109588400418));
#70248=CARTESIAN_POINT('Ctrl Pts',(8.80204499129345,-3.55100901886174,134.2099904635));
#70249=CARTESIAN_POINT('Ctrl Pts',(8.79429692329049,-3.45339037648862,134.306256956705));
#70250=CARTESIAN_POINT('Ctrl Pts',(8.78654062054865,-3.35566798386071,134.402625763085));
#70251=CARTESIAN_POINT('Ctrl Pts',(8.77878431780682,-3.25396046877286,134.49484994448));
#70252=CARTESIAN_POINT('Ctrl Pts',(8.77102801506499,-3.14866511680885,134.582599763609));
#70253=CARTESIAN_POINT('Ctrl Pts',(8.76326757255081,-3.04331356554482,134.670396417459));
#70254=CARTESIAN_POINT('Ctrl Pts',(8.75550713003664,-2.93437067213466,134.753713713157));
#70255=CARTESIAN_POINT('Ctrl Pts',(8.74774668752246,-2.82226419617377,134.832264274494));
#70256=CARTESIAN_POINT('Ctrl Pts',(8.73997378725704,-2.70997775694548,134.910940932166));
#70257=CARTESIAN_POINT('Ctrl Pts',(8.73220088699162,-2.59451791626622,134.984835353499));
#70258=CARTESIAN_POINT('Ctrl Pts',(8.7244279867262,-2.47633937930935,135.053704842383));
#70259=CARTESIAN_POINT('Ctrl Pts',(8.71693765096409,-2.36245692984319,135.120070751875));
#70260=CARTESIAN_POINT('Ctrl Pts',(8.70944731520199,-2.24605028744914,135.181770579768));
#70261=CARTESIAN_POINT('Ctrl Pts',(8.70195697943987,-2.12754350818067,135.238629630977));
#70262=CARTESIAN_POINT('Ctrl Pts',(8.69418264532078,-2.00454350835826,135.297644510394));
#70263=CARTESIAN_POINT('Ctrl Pts',(8.68640831120169,-1.87889134754276,135.351631232232));
#70264=CARTESIAN_POINT('Ctrl Pts',(8.6786339770826,-1.75103658152808,135.40034298836));
#70265=CARTESIAN_POINT('Ctrl Pts',(8.6708692241355,-1.62333938508579,135.448994711602));
#70266=CARTESIAN_POINT('Ctrl Pts',(8.66310447118845,-1.49344534635818,135.492384266176));
#70267=CARTESIAN_POINT('Ctrl Pts',(8.65533971824135,-1.3618276400368,135.530311161248));
#70268=CARTESIAN_POINT('Ctrl Pts',(8.64758267735635,-1.23034065827701,135.568200386794));
#70269=CARTESIAN_POINT('Ctrl Pts',(8.6398256364713,-1.09713378907069,135.600637642452));
#70270=CARTESIAN_POINT('Ctrl Pts',(8.6320685955863,-0.962698832490867,135.627471026879));
#70271=CARTESIAN_POINT('Ctrl Pts',(8.62431740434618,-0.82836525435755,135.654284176041));
#70272=CARTESIAN_POINT('Ctrl Pts',(8.61656621310607,-0.692805814067956,
135.675501789198));
#70273=CARTESIAN_POINT('Ctrl Pts',(8.60881502186595,-0.556525727769769,
135.691022277312));
#70274=CARTESIAN_POINT('Ctrl Pts',(8.60106712508886,-0.420303564143464,
135.706536168805));
#70275=CARTESIAN_POINT('Ctrl Pts',(8.5933192283118,-0.28336175134443,135.716357707148));
#70276=CARTESIAN_POINT('Ctrl Pts',(8.58557133153471,-0.146213696205706,
135.720436757898));
#70277=CARTESIAN_POINT('Ctrl Pts',(8.5778250554506,-0.00909432948354663,
135.724514955399));
#70278=CARTESIAN_POINT('Ctrl Pts',(8.57007877936647,0.128230803222779,135.722853042953));
#70279=CARTESIAN_POINT('Ctrl Pts',(8.56233250328236,0.265245596292749,135.715452943734));
#70280=CARTESIAN_POINT('Ctrl Pts',(8.55458617001701,0.402261400774609,135.708052789889));
#70281=CARTESIAN_POINT('Ctrl Pts',(8.54683983675167,0.538966470652652,135.694914385833));
#70282=CARTESIAN_POINT('Ctrl Pts',(8.53909350348633,0.674847526477958,135.676091714261));
#70283=CARTESIAN_POINT('Ctrl Pts',(8.53134543548336,0.810759011923582,135.657264827483));
#70284=CARTESIAN_POINT('Ctrl Pts',(8.5235973674804,0.94584572892552,135.632751193796));
#70285=CARTESIAN_POINT('Ctrl Pts',(8.51584929947742,1.07960271673855,135.602656256281));
#70286=CARTESIAN_POINT('Ctrl Pts',(8.50809299673556,1.21350186307015,135.572529333508));
#70287=CARTESIAN_POINT('Ctrl Pts',(8.50033669399372,1.34606807505181,135.536809343303));
#70288=CARTESIAN_POINT('Ctrl Pts',(8.49258039125186,1.47680919280781,135.495652302224));
#70289=CARTESIAN_POINT('Ctrl Pts',(8.48481994873769,1.60762009103489,135.454473294392));
#70290=CARTESIAN_POINT('Ctrl Pts',(8.47705950622351,1.7366035865406,135.407851586206));
#70291=CARTESIAN_POINT('Ctrl Pts',(8.46929906370934,1.86328668707073,135.355991730067));
#70292=CARTESIAN_POINT('Ctrl Pts',(8.46152616344391,1.99017315056022,135.304048623882));
#70293=CARTESIAN_POINT('Ctrl Pts',(8.4537532631784,2.1147514841769,135.246850729628));
#70294=CARTESIAN_POINT('Ctrl Pts',(8.44598036291296,2.23657172155684,135.184649420468));
#70295=CARTESIAN_POINT('Ctrl Pts',(8.43849002715095,2.35396348646102,135.124709285573));
#70296=CARTESIAN_POINT('Ctrl Pts',(8.43099969138902,2.4687939327003,135.060123344598));
#70297=CARTESIAN_POINT('Ctrl Pts',(8.423509355627,2.58068687169647,134.991153940952));
#70298=CARTESIAN_POINT('Ctrl Pts',(8.41573502150793,2.69682226548398,134.919569541404));
#70299=CARTESIAN_POINT('Ctrl Pts',(8.40796068738887,2.81016088569513,134.843035961709));
#70300=CARTESIAN_POINT('Ctrl Pts',(8.40018635326979,2.92025208977126,134.761798020064));
#70301=CARTESIAN_POINT('Ctrl Pts',(8.3924216003227,3.0302076162775,134.680660196921));
#70302=CARTESIAN_POINT('Ctrl Pts',(8.38465684737557,3.13692337816709,134.594829777445));
#70303=CARTESIAN_POINT('Ctrl Pts',(8.37689209442848,3.23997493434462,134.504596486713));
#70304=CARTESIAN_POINT('Ctrl Pts',(8.36913505354349,3.34292413826377,134.414452816956));
#70305=CARTESIAN_POINT('Ctrl Pts',(8.36137801265849,3.44221608668468,134.319915234286));
#70306=CARTESIAN_POINT('Ctrl Pts',(8.35362097177349,3.53745715075157,134.221315397644));
#70307=CARTESIAN_POINT('Ctrl Pts',(8.34586978053337,3.63262639279117,134.122789915906));
#70308=CARTESIAN_POINT('Ctrl Pts',(8.33811858929324,3.72375056035358,134.020208557727));
#70309=CARTESIAN_POINT('Ctrl Pts',(8.33036739805311,3.81047110203739,133.913941464407));
#70310=CARTESIAN_POINT('Ctrl Pts',(8.32261950127603,3.89715478517763,133.807719537435));
#70311=CARTESIAN_POINT('Ctrl Pts',(8.31487160449895,3.97943831835365,133.697815293313));
#70312=CARTESIAN_POINT('Ctrl Pts',(8.30712370772187,4.05700201310458,133.584633576857));
#70313=CARTESIAN_POINT('Ctrl Pts',(8.29937743163777,4.13454948320265,133.471475535576));
#70314=CARTESIAN_POINT('Ctrl Pts',(8.29163115555376,4.20737885777497,133.35504170791));
#70315=CARTESIAN_POINT('Ctrl Pts',(8.28388487946967,4.27521278714674,133.235767347654));
#70316=CARTESIAN_POINT('Ctrl Pts',(8.27613854620433,4.34304721725306,133.116492106942));
#70317=CARTESIAN_POINT('Ctrl Pts',(8.26839221293897,4.40588593529777,132.99437663165));
#70318=CARTESIAN_POINT('Ctrl Pts',(8.26064587967363,4.46349691837158,132.869881937279));
#70319=CARTESIAN_POINT('Ctrl Pts',(8.25289781167067,4.5211208030256,132.745359363184));
#70320=CARTESIAN_POINT('Ctrl Pts',(8.24514974366772,4.57351445895888,132.618456864529));
#70321=CARTESIAN_POINT('Ctrl Pts',(8.23740167566476,4.62049365480359,132.489656273651));
#70322=CARTESIAN_POINT('Ctrl Pts',(8.22964537292291,4.66752278069678,132.360718791972));
#70323=CARTESIAN_POINT('Ctrl Pts',(8.22188907018102,4.70912581698028,132.229879556147));
#70324=CARTESIAN_POINT('Ctrl Pts',(8.21413276743917,4.74516800036887,132.097636964978));
#70325=CARTESIAN_POINT('Ctrl Pts',(8.20637232492501,4.78122942055595,131.965323791957));
#70326=CARTESIAN_POINT('Ctrl Pts',(8.19861188241084,4.81172398698152,131.831606152112));
#70327=CARTESIAN_POINT('Ctrl Pts',(8.19085143989668,4.83656813150723,131.696992552794));
#70328=CARTESIAN_POINT('Ctrl Pts',(8.18307853963125,4.8614521580593,131.562162859775));
#70329=CARTESIAN_POINT('Ctrl Pts',(8.17530563936583,4.8806675820095,131.426434720481));
#70330=CARTESIAN_POINT('Ctrl Pts',(8.16753273910041,4.89418267290967,131.290322577693));
#70331=CARTESIAN_POINT('Ctrl Pts',(8.16004240333831,4.90720645621331,131.15915845414));
#70332=CARTESIAN_POINT('Ctrl Pts',(8.15255206757619,4.91493713598488,131.027638068854));
#70333=CARTESIAN_POINT('Ctrl Pts',(8.14506173181408,4.91739209004694,130.89621972296));
#70334=CARTESIAN_POINT('Ctrl Pts',(8.13728739769499,4.9199401244384,130.759818610539));
#70335=CARTESIAN_POINT('Ctrl Pts',(8.12951306357587,4.91681254897074,130.623095350177));
#70336=CARTESIAN_POINT('Ctrl Pts',(8.12173872945678,4.90797175281682,130.486561410436));
#70337=CARTESIAN_POINT('Ctrl Pts',(8.11397397650968,4.89914185215404,130.350195736574));
#70338=CARTESIAN_POINT('Ctrl Pts',(8.10620922356266,4.88461276538403,130.214019305498));
#70339=CARTESIAN_POINT('Ctrl Pts',(8.09844447061556,4.86439882563909,130.078545815002));
#70340=CARTESIAN_POINT('Ctrl Pts',(8.09068742973055,4.84420496266407,129.943206878687));
#70341=CARTESIAN_POINT('Ctrl Pts',(8.08293038884552,4.81833754038205,129.808569877744));
#70342=CARTESIAN_POINT('Ctrl Pts',(8.07517334796052,4.7868628268431,129.675145253037));
#70343=CARTESIAN_POINT('Ctrl Pts',(8.06742215672038,4.75541184863047,129.541821244878));
#70344=CARTESIAN_POINT('Ctrl Pts',(8.05967096548027,4.71836208513883,129.409708172153));
#70345=CARTESIAN_POINT('Ctrl Pts',(8.05191977424013,4.67583114093473,129.279307764723));
#70346=CARTESIAN_POINT('Ctrl Pts',(8.04417187746305,4.63331827351647,129.148962780945));
#70347=CARTESIAN_POINT('Ctrl Pts',(8.03642398068592,4.58532897985487,129.020329385584));
#70348=CARTESIAN_POINT('Ctrl Pts',(8.02867608390883,4.53203106793912,128.893895370111));
#70349=CARTESIAN_POINT('Ctrl Pts',(8.02092980782473,4.47874430479757,128.767487801908));
#70350=CARTESIAN_POINT('Ctrl Pts',(8.01318353174065,4.42015128391673,128.643279058536));
#70351=CARTESIAN_POINT('Ctrl Pts',(8.00543725565655,4.35646828236937,128.521737747443));
#70352=CARTESIAN_POINT('Ctrl Pts',(7.99769092239119,4.29278481072855,128.400195539159));
#70353=CARTESIAN_POINT('Ctrl Pts',(7.98994458912586,4.22401146489882,128.281321148751));
#70354=CARTESIAN_POINT('Ctrl Pts',(7.98219825586051,4.15041069622921,128.165558973803));
#70355=CARTESIAN_POINT('Ctrl Pts',(7.97445018785754,4.07679344517786,128.049770874719));
#70356=CARTESIAN_POINT('Ctrl Pts',(7.96670211985455,3.99834682981219,127.937096707828));
#70357=CARTESIAN_POINT('Ctrl Pts',(7.95895405185158,3.91537664776859,127.827951914345));
#70358=CARTESIAN_POINT('Ctrl Pts',(7.95119774910972,3.83231828402806,127.718691120477));
#70359=CARTESIAN_POINT('Ctrl Pts',(7.94344144636785,3.74472698669015,127.612967504902));
#70360=CARTESIAN_POINT('Ctrl Pts',(7.93568514362599,3.65294922993573,127.511163844518));
#70361=CARTESIAN_POINT('Ctrl Pts',(7.92792470111181,3.56112248862904,127.409305848455));
#70362=CARTESIAN_POINT('Ctrl Pts',(7.92016425859764,3.46510510917158,127.3113722555));
#70363=CARTESIAN_POINT('Ctrl Pts',(7.91240381608347,3.36527974257748,127.217708234536));
#70364=CARTESIAN_POINT('Ctrl Pts',(7.90463091581804,3.26529412744299,127.12389385577));
#70365=CARTESIAN_POINT('Ctrl Pts',(7.89685801555258,3.16148860584203,127.034363000759));
#70366=CARTESIAN_POINT('Ctrl Pts',(7.88908511528714,3.05427884197399,126.949420434117));
#70367=CARTESIAN_POINT('Ctrl Pts',(7.88159477952518,2.95096642306852,126.86756574373));
#70368=CARTESIAN_POINT('Ctrl Pts',(7.87410444376324,2.84449321932749,126.789971723085));
#70369=CARTESIAN_POINT('Ctrl Pts',(7.86661410800127,2.73525420560422,126.716871474678));
#70370=CARTESIAN_POINT('Ctrl Pts',(7.85883977388218,2.62187336147205,126.640999608135));
#70371=CARTESIAN_POINT('Ctrl Pts',(7.85106543976306,2.50515367938956,126.569728664076));
#70372=CARTESIAN_POINT('Ctrl Pts',(7.84329110564397,2.38550514277391,126.503366746808));
#70373=CARTESIAN_POINT('Ctrl Pts',(7.83552635269688,2.26600406228651,126.437086614672));
#70374=CARTESIAN_POINT('Ctrl Pts',(7.82776159974985,2.14358164781312,126.375703659566));
#70375=CARTESIAN_POINT('Ctrl Pts',(7.81999684680275,2.01867783526541,126.319483488825));
#70376=CARTESIAN_POINT('Ctrl Pts',(7.81223980591775,1.89389807894516,126.26331915675));
#70377=CARTESIAN_POINT('Ctrl Pts',(7.80448276503274,1.76664218334352,126.212307564018));
#70378=CARTESIAN_POINT('Ctrl Pts',(7.79672572414773,1.63737541631576,126.166668863197));
#70379=CARTESIAN_POINT('Ctrl Pts',(7.7889745329076,1.50820613036257,126.121064578875));
#70380=CARTESIAN_POINT('Ctrl Pts',(7.78122334166745,1.37702935848411,126.080825251355));
#70381=CARTESIAN_POINT('Ctrl Pts',(7.77347215042732,1.24433078836353,126.04612313383));
#70382=CARTESIAN_POINT('Ctrl Pts',(7.76572425365024,1.1116886186751,126.011435765631));
#70383=CARTESIAN_POINT('Ctrl Pts',(7.75797635687314,0.977526314643554,125.982281025278));
#70384=CARTESIAN_POINT('Ctrl Pts',(7.75022846009605,0.842344973363954,125.958781394362));
#70385=CARTESIAN_POINT('Ctrl Pts',(7.74248218401195,0.707191909106776,125.935286679062));
#70386=CARTESIAN_POINT('Ctrl Pts',(7.73473590792787,0.571020616534077,125.91744478721));
#70387=CARTESIAN_POINT('Ctrl Pts',(7.72698963184376,0.434342251402056,125.905327052551));
#70388=CARTESIAN_POINT('Ctrl Pts',(7.71924329857841,0.297662877341392,125.893209228441));
#70389=CARTESIAN_POINT('Ctrl Pts',(7.71149696531305,0.16047681268997,125.886815680366));
#70390=CARTESIAN_POINT('Ctrl Pts',(7.7037506320477,0.0232998030868416,125.886165808322));
#70391=CARTESIAN_POINT('Ctrl Pts',(7.69600256404473,-0.113907926356282,
125.885515790744));
#70392=CARTESIAN_POINT('Ctrl Pts',(7.68825449604176,-0.251106205830005,
125.890612010551));
#70393=CARTESIAN_POINT('Ctrl Pts',(7.6805064280388,-0.387780221782509,125.901421747654));
#70394=CARTESIAN_POINT('Ctrl Pts',(7.67275012529694,-0.524599496505796,
125.912242973475));
#70395=CARTESIAN_POINT('Ctrl Pts',(7.66499382255506,-0.660893004284258,
125.928789815979));
#70396=CARTESIAN_POINT('Ctrl Pts',(7.65723751981321,-0.796151426316966,
125.950977676887));
#70397=CARTESIAN_POINT('Ctrl Pts',(7.64947707729904,-0.931482039842065,
125.973177380125));
#70398=CARTESIAN_POINT('Ctrl Pts',(7.64171663478488,-1.06577608417067,126.001024021662));
#70399=CARTESIAN_POINT('Ctrl Pts',(7.63395619227072,-1.19853632672462,126.034382238577));
#70400=CARTESIAN_POINT('Ctrl Pts',(7.62618329200527,-1.331509687806,126.067794005063));
#70401=CARTESIAN_POINT('Ctrl Pts',(7.61841039173986,-1.46294395178855,126.106734916265));
#70402=CARTESIAN_POINT('Ctrl Pts',(7.61063749147442,-1.59235803491825,126.151019994838));
#70403=CARTESIAN_POINT('Ctrl Pts',(7.60314715571237,-1.71706759015198,126.193695199257));
#70404=CARTESIAN_POINT('Ctrl Pts',(7.59565681995031,-1.83990100467396,126.241332657545));
#70405=CARTESIAN_POINT('Ctrl Pts',(7.58816648418826,-1.9604486691947,126.293726063764));
#70406=CARTESIAN_POINT('Ctrl Pts',(7.58039166302064,-2.0855747734972,126.348109388712));
#70407=CARTESIAN_POINT('Ctrl Pts',(7.57261684185302,-2.20863445582198,126.407789347682));
#70408=CARTESIAN_POINT('Ctrl Pts',(7.5648420206854,-2.32914680335446,126.472587512829));
#70409=CARTESIAN_POINT('Ctrl Pts',(7.55707689142416,-2.4495089230728,126.537304902131));
#70410=CARTESIAN_POINT('Ctrl Pts',(7.5493117621629,-2.56732968538282,126.607127618751));
#70411=CARTESIAN_POINT('Ctrl Pts',(7.54154663290166,-2.68214776593824,126.681829062299));
#70412=CARTESIAN_POINT('Ctrl Pts',(7.53378932596478,-2.79685018270511,126.75645525418));
#70413=CARTESIAN_POINT('Ctrl Pts',(7.52603201902788,-2.90855561193974,126.835950180062));
#70414=CARTESIAN_POINT('Ctrl Pts',(7.518274712091,-3.01682730279926,126.920041360916));
#70415=CARTESIAN_POINT('Ctrl Pts',(7.51052373062126,-3.12501070670188,127.004063972096));
#70416=CARTESIAN_POINT('Ctrl Pts',(7.50277274915155,-3.22976563980371,127.092675136782));
#70417=CARTESIAN_POINT('Ctrl Pts',(7.49502176768181,-3.33068469169375,127.185559359274));
#70418=CARTESIAN_POINT('Ctrl Pts',(7.48727424285852,-3.43155873747922,127.278402158893));
#70419=CARTESIAN_POINT('Ctrl Pts',(7.4795267180353,-3.52860001835509,127.375513960967));
#70420=CARTESIAN_POINT('Ctrl Pts',(7.471779193212,-3.62143468904814,127.476539430143));
#70421=CARTESIAN_POINT('Ctrl Pts',(7.46403344570116,-3.71424806310507,127.577541723682));
#70422=CARTESIAN_POINT('Ctrl Pts',(7.4562876981903,-3.80285648317711,127.682455609967));
#70423=CARTESIAN_POINT('Ctrl Pts',(7.44854195067947,-3.88692371226027,127.790889675684));
#70424=CARTESIAN_POINT('Ctrl Pts',(7.44079630269244,-3.97098986117785,127.899322348149));
#70425=CARTESIAN_POINT('Ctrl Pts',(7.43305065470545,-4.05051469664554,128.011274800506));
#70426=CARTESIAN_POINT('Ctrl Pts',(7.42530500671842,-4.12520320028202,128.126323721091));
#70427=CARTESIAN_POINT('Ctrl Pts',(7.41755412798041,-4.19994214217289,128.241450335918));
#70428=CARTESIAN_POINT('Ctrl Pts',(7.40980324924236,-4.26983801271335,128.359677269191));
#70429=CARTESIAN_POINT('Ctrl Pts',(7.40205237050435,-4.33463980240314,128.480553214634));
#70430=CARTESIAN_POINT('Ctrl Pts',(7.39429892290299,-4.39946306926325,128.601469221829));
#70431=CARTESIAN_POINT('Ctrl Pts',(7.38654547530157,-4.45918871762214,128.725035640154));
#70432=CARTESIAN_POINT('Ctrl Pts',(7.3787920277002,-4.51361285293805,128.850778759467));
#70433=CARTESIAN_POINT('Ctrl Pts',(7.37102906749447,-4.56810376052012,128.976676151384));
#70434=CARTESIAN_POINT('Ctrl Pts',(7.36326610728878,-4.61728001501608,129.104755216337));
#70435=CARTESIAN_POINT('Ctrl Pts',(7.35550314708306,-4.66098658752424,129.234523972109));
#70436=CARTESIAN_POINT('Ctrl Pts',(7.34863665501921,-4.69964591660902,129.349307006935));
#70437=CARTESIAN_POINT('Ctrl Pts',(7.34177016295534,-4.73402658012365,129.465411605364));
#70438=CARTESIAN_POINT('Ctrl Pts',(7.33490367089149,-4.76405452823399,129.582490119308));
#70439=CARTESIAN_POINT('Ctrl Pts',(9.08499331100833,-4.76405452823402,129.582490119308));
#70440=CARTESIAN_POINT('Ctrl Pts',(9.07734584844658,-4.79769088846045,129.713637777328));
#70441=CARTESIAN_POINT('Ctrl Pts',(9.06969838588486,-4.82588697168254,129.846095034761));
#70442=CARTESIAN_POINT('Ctrl Pts',(9.06205092332311,-4.8485631154531,129.979364388503));
#70443=CARTESIAN_POINT('Ctrl Pts',(9.0541856754406,-4.87188503306103,130.11642900227));
#70444=CARTESIAN_POINT('Ctrl Pts',(9.04632042755805,-4.88936785715086,130.254352199333));
#70445=CARTESIAN_POINT('Ctrl Pts',(9.03845517967554,-4.90098224828163,130.39258875776));
#70446=CARTESIAN_POINT('Ctrl Pts',(9.03058993179303,-4.91259663941239,130.530825316186));
#70447=CARTESIAN_POINT('Ctrl Pts',(9.02272468391051,-4.91834263804842,130.669374776506));
#70448=CARTESIAN_POINT('Ctrl Pts',(9.01485943602799,-4.91824886988786,130.807694736162));
#70449=CARTESIAN_POINT('',(9.3601405639707,-4.91824968732061,130.806114376595));
#70450=CARTESIAN_POINT('Ctrl Pts',(9.42990690795585,-4.76405452823399,129.582490119308));
#70451=CARTESIAN_POINT('Ctrl Pts',(9.42197330691278,-4.79892363242829,129.718444227349));
#70452=CARTESIAN_POINT('Ctrl Pts',(9.41403970586967,-4.82799669543438,129.856000569293));
#70453=CARTESIAN_POINT('Ctrl Pts',(9.40610610482659,-4.85113721517965,129.994637960109));
#70454=CARTESIAN_POINT('Ctrl Pts',(9.39817898243846,-4.87425883815384,130.133162138298));
#70455=CARTESIAN_POINT('Ctrl Pts',(9.39025186005033,-4.89145751185162,130.272765247639));
#70456=CARTESIAN_POINT('Ctrl Pts',(9.3823247376622,-4.90264758826632,130.412914979238));
#70457=CARTESIAN_POINT('Ctrl Pts',(9.37493001311104,-4.91308612178979,130.543652037447));
#70458=CARTESIAN_POINT('Ctrl Pts',(9.36753528855989,-4.91829648867104,130.674864409002));
#70459=CARTESIAN_POINT('Ctrl Pts',(9.36014056400873,-4.91824968732085,130.80611437592));
#70460=CARTESIAN_POINT('Ctrl Pts',(9.36014056397079,-4.91824968732061,130.806114376595));
#70461=CARTESIAN_POINT('Ctrl Pts',(9.3517641285291,-4.9181966726834,130.95478886298));
#70462=CARTESIAN_POINT('Ctrl Pts',(9.3433876930874,-4.91139802649659,131.103260454074));
#70463=CARTESIAN_POINT('Ctrl Pts',(9.33501125764573,-4.89793381843472,131.250933537405));
#70464=CARTESIAN_POINT('Ctrl Pts',(9.32660038269188,-4.8844142526063,131.399213775055));
#70465=CARTESIAN_POINT('Ctrl Pts',(9.31818950773799,-4.86417428476807,131.54668865016));
#70466=CARTESIAN_POINT('Ctrl Pts',(9.30977863278414,-4.83734567219708,131.69276925675));
#70467=CARTESIAN_POINT('Ctrl Pts',(9.30135038794373,-4.81046165398046,131.839151544624));
#70468=CARTESIAN_POINT('Ctrl Pts',(9.29292214310327,-4.77696186955486,131.984133538149));
#70469=CARTESIAN_POINT('Ctrl Pts',(9.28449389826284,-4.73702814048069,132.127140818051));
#70470=CARTESIAN_POINT('Ctrl Pts',(9.27603806763434,-4.6969637076351,132.2706161632));
#70471=CARTESIAN_POINT('Ctrl Pts',(9.2675822370059,-4.65042327378475,132.412103591709));
#70472=CARTESIAN_POINT('Ctrl Pts',(9.25912640637742,-4.59763810719735,132.551045161995));
#70473=CARTESIAN_POINT('Ctrl Pts',(9.25250534788704,-4.55630642841202,132.659838763005));
#70474=CARTESIAN_POINT('Ctrl Pts',(9.24588428939664,-4.51114697948034,132.767071863098));
#70475=CARTESIAN_POINT('Ctrl Pts',(9.23926323090626,-4.46229023998372,132.872487518084));
#70476=CARTESIAN_POINT('Ctrl Pts',(9.23148889678717,-4.40492348852432,132.996264784882));
#70477=CARTESIAN_POINT('Ctrl Pts',(9.22371456266808,-4.34231187447133,133.117849395084));
#70478=CARTESIAN_POINT('Ctrl Pts',(9.21594022854899,-4.27464527763359,133.236764945161));
#70479=CARTESIAN_POINT('Ctrl Pts',(9.2081754756019,-4.207062073829,133.355533942451));
#70480=CARTESIAN_POINT('Ctrl Pts',(9.20041072265486,-4.13443647421598,133.471640087955));
#70481=CARTESIAN_POINT('Ctrl Pts',(9.19264596970777,-4.05700604578529,133.58462769232));
#70482=CARTESIAN_POINT('Ctrl Pts',(9.18488892882277,-3.9796525223477,133.697503075803));
#70483=CARTESIAN_POINT('Ctrl Pts',(9.17713188793769,-3.8975038866139,133.807265761656));
#70484=CARTESIAN_POINT('Ctrl Pts',(9.16937484705269,-3.81084298512702,133.91348570434));
#70485=CARTESIAN_POINT('Ctrl Pts',(9.16162365581257,-3.72424743530007,134.01962554574));
#70486=CARTESIAN_POINT('Ctrl Pts',(9.15387246457247,-3.63314663880996,134.122227659941));
#70487=CARTESIAN_POINT('Ctrl Pts',(9.14612127333234,-3.53786579815845,134.22089228824));
#70488=CARTESIAN_POINT('Ctrl Pts',(9.13837337655525,-3.44262545440579,134.319514981441));
#70489=CARTESIAN_POINT('Ctrl Pts',(9.13062547977819,-3.34320887109478,134.414203236631));
#70490=CARTESIAN_POINT('Ctrl Pts',(9.1228775830011,-3.23998030139839,134.504591787243));
#70491=CARTESIAN_POINT('Ctrl Pts',(9.11513130691699,-3.13677332489344,134.594961430519));
#70492=CARTESIAN_POINT('Ctrl Pts',(9.10738503083286,-3.02975624200152,134.681032900793));
#70493=CARTESIAN_POINT('Ctrl Pts',(9.09963875474875,-2.91932850261307,134.762479382375));
#70494=CARTESIAN_POINT('Ctrl Pts',(9.0918924214834,-2.80889994807228,134.843926465176));
#70495=CARTESIAN_POINT('Ctrl Pts',(9.08414608821806,-2.69506100143844,134.920748259094));
#70496=CARTESIAN_POINT('Ctrl Pts',(9.07639975495272,-2.57824204747977,134.992659915265));
#70497=CARTESIAN_POINT('Ctrl Pts',(9.06865168694975,-2.46139693272634,135.064587675553));
#70498=CARTESIAN_POINT('Ctrl Pts',(9.06090361894673,-2.34157081557059,135.131602905123));
#70499=CARTESIAN_POINT('Ctrl Pts',(9.05315555094376,-2.21922039650939,135.193465753493));
#70500=CARTESIAN_POINT('Ctrl Pts',(9.0453992482019,-2.09673994196665,135.255394350434));
#70501=CARTESIAN_POINT('Ctrl Pts',(9.03764294546011,-1.97173017567875,135.312159450558));
#70502=CARTESIAN_POINT('Ctrl Pts',(9.02988664271825,-1.84467009126778,135.363568368577));
#70503=CARTESIAN_POINT('Ctrl Pts',(9.02212620020407,-1.71754219106388,135.415004725085));
#70504=CARTESIAN_POINT('Ctrl Pts',(9.01436575768981,-1.58836216028212,135.461079071899));
#70505=CARTESIAN_POINT('Ctrl Pts',(9.00660531517562,-1.45762507693163,135.50164836664));
#70506=CARTESIAN_POINT('Ctrl Pts',(8.99883241491018,-1.32667812280883,135.542282786815));
#70507=CARTESIAN_POINT('Ctrl Pts',(8.99105951464476,-1.1941694994222,135.57739439518));
#70508=CARTESIAN_POINT('Ctrl Pts',(8.98328661437932,-1.06060630115362,135.606890923192));
#70509=CARTESIAN_POINT('Ctrl Pts',(8.97579627861731,-0.931898461567866,
135.635315178113));
#70510=CARTESIAN_POINT('Ctrl Pts',(8.96830594285535,-0.802211692053463,
135.658525455318));
#70511=CARTESIAN_POINT('Ctrl Pts',(8.96081560709334,-0.672003138405616,
135.676484881629));
#70512=CARTESIAN_POINT('Ctrl Pts',(8.95304127297425,-0.536857687869795,
135.695125245047));
#70513=CARTESIAN_POINT('Ctrl Pts',(8.94526693885518,-0.400722005081922,
135.708167772575));
#70514=CARTESIAN_POINT('Ctrl Pts',(8.93749260473609,-0.264099536499374,
135.715514707729));
#70515=CARTESIAN_POINT('Ctrl Pts',(8.92972785178899,-0.127645442899052,
135.722852588441));
#70516=CARTESIAN_POINT('Ctrl Pts',(8.92196309884195,0.00929385618066372,
135.724508822318));
#70517=CARTESIAN_POINT('Ctrl Pts',(8.91419834589485,0.146206565618375,135.72043696997));
#70518=CARTESIAN_POINT('Ctrl Pts',(8.90644130500985,0.282983291422756,135.716369161844));
#70519=CARTESIAN_POINT('Ctrl Pts',(8.89868426412476,0.419733091877031,135.706584600837));
#70520=CARTESIAN_POINT('Ctrl Pts',(8.89092722323977,0.555941272026413,135.691088803639));
#70521=CARTESIAN_POINT('Ctrl Pts',(8.88317603199965,0.692046736527599,135.675604691942));
#70522=CARTESIAN_POINT('Ctrl Pts',(8.87542484075957,0.82761100681146,135.654417960668));
#70523=CARTESIAN_POINT('Ctrl Pts',(8.86767364951945,0.962121974663368,135.627586132548));
#70524=CARTESIAN_POINT('Ctrl Pts',(8.85992575274236,1.09657577176592,135.60076570867));
#70525=CARTESIAN_POINT('Ctrl Pts',(8.8521778559653,1.22997677423242,135.568305036326));
#70526=CARTESIAN_POINT('Ctrl Pts',(8.8444299591882,1.36182078521822,135.530313136524));
#70527=CARTESIAN_POINT('Ctrl Pts',(8.83668368310409,1.49363721727915,135.492329183809));
#70528=CARTESIAN_POINT('Ctrl Pts',(8.82893740701994,1.62389693023184,135.448816413186));
#70529=CARTESIAN_POINT('Ctrl Pts',(8.82119113093583,1.75210905235757,135.399934241299));
#70530=CARTESIAN_POINT('Ctrl Pts',(8.81344479767048,1.8803221209159,135.351051708574));
#70531=CARTESIAN_POINT('Ctrl Pts',(8.80569846440514,2.00648720317191,135.296799834774));
#70532=CARTESIAN_POINT('Ctrl Pts',(8.79795213113979,2.13013201422899,135.237386747024));
#70533=CARTESIAN_POINT('Ctrl Pts',(8.79020406313683,2.25380451468422,135.177960354125));
#70534=CARTESIAN_POINT('Ctrl Pts',(8.78245599513389,2.37495526852933,135.11337061663));
#70535=CARTESIAN_POINT('Ctrl Pts',(8.77470792713092,2.49313562498726,135.043872124558));
#70536=CARTESIAN_POINT('Ctrl Pts',(8.76695162438906,2.61144158493456,134.974299768661));
#70537=CARTESIAN_POINT('Ctrl Pts',(8.75919532164722,2.72677050355186,134.899808435005));
#70538=CARTESIAN_POINT('Ctrl Pts',(8.75143901890536,2.8387013614973,134.820696963383));
#70539=CARTESIAN_POINT('Ctrl Pts',(8.74367857639119,2.95069196031181,134.741543267588));
#70540=CARTESIAN_POINT('Ctrl Pts',(8.73591813387695,3.0592805752148,134.657764759004));
#70541=CARTESIAN_POINT('Ctrl Pts',(8.72815769136278,3.1640792588443,134.569700642883));
#70542=CARTESIAN_POINT('Ctrl Pts',(8.72038479109735,3.26904617462435,134.481495158424));
#70543=CARTESIAN_POINT('Ctrl Pts',(8.71261189083194,3.37021071279827,134.3889905827));
#70544=CARTESIAN_POINT('Ctrl Pts',(8.70483899056651,3.46722114832605,134.292563675173));
#70545=CARTESIAN_POINT('Ctrl Pts',(8.69734865480451,3.56070501016758,134.19964212862));
#70546=CARTESIAN_POINT('Ctrl Pts',(8.68985831904251,3.65033134042777,134.10307869828));
#70547=CARTESIAN_POINT('Ctrl Pts',(8.6823679832805,3.735822018188,134.003238063002));
#70548=CARTESIAN_POINT('Ctrl Pts',(8.67459364916144,3.82455410098009,133.899611939692));
#70549=CARTESIAN_POINT('Ctrl Pts',(8.66681931504231,3.90911181061861,133.79212693891));
#70550=CARTESIAN_POINT('Ctrl Pts',(8.65904498092323,3.98914077669724,133.681153784652));
#70551=CARTESIAN_POINT('Ctrl Pts',(8.65128022797613,4.06907111422757,133.570317394888));
#70552=CARTESIAN_POINT('Ctrl Pts',(8.64351547502905,4.14448358677629,133.456001719116));
#70553=CARTESIAN_POINT('Ctrl Pts',(8.63575072208195,4.21506248580536,133.338612243442));
#70554=CARTESIAN_POINT('Ctrl Pts',(8.62799368119695,4.28557128487692,133.221339360651));
#70555=CARTESIAN_POINT('Ctrl Pts',(8.62023664031196,4.35125586403343,133.100999086347));
#70556=CARTESIAN_POINT('Ctrl Pts',(8.61247959942696,4.41184265942764,132.97802742988));
#70557=CARTESIAN_POINT('Ctrl Pts',(8.60472840818683,4.47238376584814,132.855148507295));
#70558=CARTESIAN_POINT('Ctrl Pts',(8.59697721694674,4.52783456821774,132.729642501557));
#70559=CARTESIAN_POINT('Ctrl Pts',(8.58922602570661,4.57796665504031,132.601971356252));
#70560=CARTESIAN_POINT('Ctrl Pts',(8.58147812892952,4.62807743438866,132.474354474589));
#70561=CARTESIAN_POINT('Ctrl Pts',(8.57373023215236,4.67287385174521,132.344574646803));
#70562=CARTESIAN_POINT('Ctrl Pts',(8.56598233537528,4.7121750988625,132.213114996498));
#70563=CARTESIAN_POINT('Ctrl Pts',(8.55823605929118,4.75146812500614,132.081682844718));
#70564=CARTESIAN_POINT('Ctrl Pts',(8.55048978320709,4.78526815535684,131.948571943684));
#70565=CARTESIAN_POINT('Ctrl Pts',(8.54274350712299,4.81344398349671,131.814281446265));
#70566=CARTESIAN_POINT('Ctrl Pts',(8.53499717385765,4.8416200196241,131.679989957544));
#70567=CARTESIAN_POINT('Ctrl Pts',(8.52725084059236,4.86417169041596,131.544519237696));
#70568=CARTESIAN_POINT('Ctrl Pts',(8.51950450732701,4.88101881759487,131.408379131177));
#70569=CARTESIAN_POINT('Ctrl Pts',(8.51175643932403,4.89786971757112,131.272208537024));
#70570=CARTESIAN_POINT('Ctrl Pts',(8.504008371321,4.90901348386535,131.135368645839));
#70571=CARTESIAN_POINT('Ctrl Pts',(8.49626030331802,4.91442180356658,130.998374532349));
#70572=CARTESIAN_POINT('Ctrl Pts',(8.48850400057617,4.91983587129435,130.861234819885));
#70573=CARTESIAN_POINT('Ctrl Pts',(8.48074769783432,4.91950230016269,130.723940948974));
#70574=CARTESIAN_POINT('Ctrl Pts',(8.47299139509246,4.91344494131719,130.587008665321));
#70575=CARTESIAN_POINT('Ctrl Pts',(8.4652309525783,4.90738434947689,130.450003296786));
#70576=CARTESIAN_POINT('Ctrl Pts',(8.45747051006412,4.89559391625424,130.313360289386));
#70577=CARTESIAN_POINT('Ctrl Pts',(8.44971006754994,4.87814932960778,130.177589382946));
#70578=CARTESIAN_POINT('Ctrl Pts',(8.44193716728451,4.86067673936218,130.041600524994));
#70579=CARTESIAN_POINT('Ctrl Pts',(8.43416426701909,4.83753192390406,129.906486951171));
#70580=CARTESIAN_POINT('Ctrl Pts',(8.42639136675365,4.80884174566431,129.772748225407));
#70581=CARTESIAN_POINT('Ctrl Pts',(8.41890103099157,4.78119452766961,129.643871239191));
#70582=CARTESIAN_POINT('Ctrl Pts',(8.41141069522956,4.74839819965585,129.516271176401));
#70583=CARTESIAN_POINT('Ctrl Pts',(8.40392035946749,4.71060924511826,129.390379145868));
#70584=CARTESIAN_POINT('Ctrl Pts',(8.39614602534841,4.6713875108839,129.259713880734));
#70585=CARTESIAN_POINT('Ctrl Pts',(8.38837169122933,4.62666284308901,129.130474816426));
#70586=CARTESIAN_POINT('Ctrl Pts',(8.38059735711025,4.57655559646977,129.003160480179));
#70587=CARTESIAN_POINT('Ctrl Pts',(8.37283260416315,4.52651010255378,128.876003047474));
#70588=CARTESIAN_POINT('Ctrl Pts',(8.36506785121598,4.4710953704033,128.750765983456));
#70589=CARTESIAN_POINT('Ctrl Pts',(8.35730309826889,4.41048189878688,128.627934077806));
#70590=CARTESIAN_POINT('Ctrl Pts',(8.34954605738388,4.34992862932497,128.505224170536));
#70591=CARTESIAN_POINT('Ctrl Pts',(8.3417890164989,4.28418706780876,128.384915016072));
#70592=CARTESIAN_POINT('Ctrl Pts',(8.3340319756139,4.2134761733098,128.267472445129));
#70593=CARTESIAN_POINT('Ctrl Pts',(8.32628078437376,4.14281860244644,128.150118438543));
#70594=CARTESIAN_POINT('Ctrl Pts',(8.31852959313362,4.06719935844619,128.035627046305));
#70595=CARTESIAN_POINT('Ctrl Pts',(8.31077840189349,3.98688362553787,127.924440129268));
#70596=CARTESIAN_POINT('Ctrl Pts',(8.3030305051164,3.90660202895852,127.813300469637));
#70597=CARTESIAN_POINT('Ctrl Pts',(8.29528260833936,3.82162814208108,127.705462808048));
#70598=CARTESIAN_POINT('Ctrl Pts',(8.28753471156227,3.73227069920171,127.601340403708));
#70599=CARTESIAN_POINT('Ctrl Pts',(8.27978843547817,3.64293194797306,127.497239779531));
#70600=CARTESIAN_POINT('Ctrl Pts',(8.27204215939406,3.54921171905273,127.396853163308));
#70601=CARTESIAN_POINT('Ctrl Pts',(8.26429588330996,3.4514590436119,127.30056074703));
#70602=CARTESIAN_POINT('Ctrl Pts',(8.2565495500446,3.35370564658301,127.204267619943));
#70603=CARTESIAN_POINT('Ctrl Pts',(8.24880321677919,3.2519200221632,127.112069027476));
#70604=CARTESIAN_POINT('Ctrl Pts',(8.24105688351383,3.14648777861424,127.024308009264));
#70605=CARTESIAN_POINT('Ctrl Pts',(8.23330881551085,3.04103192424536,126.936527337581));
#70606=CARTESIAN_POINT('Ctrl Pts',(8.22556074750791,2.93192812616736,126.853186467704));
#70607=CARTESIAN_POINT('Ctrl Pts',(8.21781267950493,2.81959442751738,126.774587630559));
#70608=CARTESIAN_POINT('Ctrl Pts',(8.21005637676307,2.70714133927568,126.695905257635));
#70609=CARTESIAN_POINT('Ctrl Pts',(8.20230007402117,2.59145181396916,126.621975209658));
#70610=CARTESIAN_POINT('Ctrl Pts',(8.19454377127931,2.47297265519326,126.553056193137));
#70611=CARTESIAN_POINT('Ctrl Pts',(8.18678332876513,2.35443026052283,126.484100392462));
#70612=CARTESIAN_POINT('Ctrl Pts',(8.179022886251,2.23309561131126,126.420161134664));
#70613=CARTESIAN_POINT('Ctrl Pts',(8.17126244373682,2.1094384773013,126.361450268146));
#70614=CARTESIAN_POINT('Ctrl Pts',(8.16348954347139,1.98558283788222,126.302645153734));
#70615=CARTESIAN_POINT('Ctrl Pts',(8.15571664320593,1.85939762351093,126.24908535549));
#70616=CARTESIAN_POINT('Ctrl Pts',(8.1479437429405,1.73137170371282,126.200934166966));
#70617=CARTESIAN_POINT('Ctrl Pts',(8.14045340717853,1.60799984857824,126.154533395431));
#70618=CARTESIAN_POINT('Ctrl Pts',(8.13296307141654,1.48291908554651,126.113154924286));
#70619=CARTESIAN_POINT('Ctrl Pts',(8.12547273565457,1.3565767018392,126.076900124391));
#70620=CARTESIAN_POINT('Ctrl Pts',(8.11769840153549,1.22544400825176,126.039270712739));
#70621=CARTESIAN_POINT('Ctrl Pts',(8.10992406741637,1.09253674780571,126.007041971325));
#70622=CARTESIAN_POINT('Ctrl Pts',(8.1021497332973,0.958339400256849,125.98038210845));
#70623=CARTESIAN_POINT('Ctrl Pts',(8.0943849803502,0.824307438945096,125.953755101473));
#70624=CARTESIAN_POINT('Ctrl Pts',(8.08662022740324,0.688988933781597,125.932683392871));
#70625=CARTESIAN_POINT('Ctrl Pts',(8.07885547445613,0.552883910802526,125.917285577864));
#70626=CARTESIAN_POINT('Ctrl Pts',(8.07109843357113,0.416914069251208,125.901903056185));
#70627=CARTESIAN_POINT('Ctrl Pts',(8.063341392686,0.280159650442069,125.892183257084));
#70628=CARTESIAN_POINT('Ctrl Pts',(8.055584351801,0.143130923675482,125.888193756974));
#70629=CARTESIAN_POINT('Ctrl Pts',(8.04783316056088,0.00620553133767746,
125.884207265376));
#70630=CARTESIAN_POINT('Ctrl Pts',(8.0400819693208,-0.1309933680014,125.88594248289));
#70631=CARTESIAN_POINT('Ctrl Pts',(8.03233077808068,-0.267950685739329,
125.893415139095));
#70632=CARTESIAN_POINT('Ctrl Pts',(8.0245828813036,-0.404849792963763,125.900884619223));
#70633=CARTESIAN_POINT('Ctrl Pts',(8.01683498452654,-0.541507133239762,
125.914086666668));
#70634=CARTESIAN_POINT('Ctrl Pts',(8.00908708774946,-0.67740814146322,125.93298491122));
#70635=CARTESIAN_POINT('Ctrl Pts',(8.00134081166537,-0.813280722125444,
125.951879202667));
#70636=CARTESIAN_POINT('Ctrl Pts',(7.99359453558127,-0.948396898426527,
125.976467267404));
#70637=CARTESIAN_POINT('Ctrl Pts',(7.98584825949717,-1.08224814420142,126.00666095868));
#70638=CARTESIAN_POINT('Ctrl Pts',(7.97810192623183,-1.21610037803581,126.03685487284));
#70639=CARTESIAN_POINT('Ctrl Pts',(7.97035559296646,-1.34868728132952,126.072654410078));
#70640=CARTESIAN_POINT('Ctrl Pts',(7.96260925970111,-1.4795118144361,126.113920568547));
#70641=CARTESIAN_POINT('Ctrl Pts',(7.95486119169814,-1.61036564478981,126.155195968285));
#70642=CARTESIAN_POINT('Ctrl Pts',(7.94711312369521,-1.73945594682301,126.201940307706));
#70643=CARTESIAN_POINT('Ctrl Pts',(7.93936505569224,-1.86630248257096,126.253965238475));
#70644=CARTESIAN_POINT('Ctrl Pts',(7.93160875295039,-1.99328383232659,126.306045461961));
#70645=CARTESIAN_POINT('Ctrl Pts',(7.92385245020855,-2.11801628979861,126.363417339325));
#70646=CARTESIAN_POINT('Ctrl Pts',(7.9160961474667,-2.24004068961837,126.425844799237));
#70647=CARTESIAN_POINT('Ctrl Pts',(7.90833570495254,-2.3621302175344,126.488305578564));
#70648=CARTESIAN_POINT('Ctrl Pts',(7.90057526243834,-2.48150846763626,126.555827124678));
#70649=CARTESIAN_POINT('Ctrl Pts',(7.89281481992418,-2.59774328384107,126.628128716227));
#70650=CARTESIAN_POINT('Ctrl Pts',(7.88504191965875,-2.71416469049186,126.70054637271));
#70651=CARTESIAN_POINT('Ctrl Pts',(7.87726901939337,-2.82743225625953,126.77775918809));
#70652=CARTESIAN_POINT('Ctrl Pts',(7.86949611912794,-2.93714435173543,126.859444126743));
#70653=CARTESIAN_POINT('Ctrl Pts',(7.86200578336589,-3.04286813619313,126.938159612124));
#70654=CARTESIAN_POINT('Ctrl Pts',(7.85451544760377,-3.14529022355345,127.021027526156));
#70655=CARTESIAN_POINT('Ctrl Pts',(7.8470251118417,-3.24408355797388,127.107726346857));
#70656=CARTESIAN_POINT('Ctrl Pts',(7.83936711384137,-3.34508826343304,127.196365817321));
#70657=CARTESIAN_POINT('Ctrl Pts',(7.83170911584105,-3.44264003407282,127.289308622642));
#70658=CARTESIAN_POINT('Ctrl Pts',(7.82405111784072,-3.53634159520523,127.386251317891));
#70659=CARTESIAN_POINT('Ctrl Pts',(7.81640193856051,-3.62993525243869,127.48308237685));
#70660=CARTESIAN_POINT('Ctrl Pts',(7.80875275928028,-3.7196872363694,127.583903882855));
#70661=CARTESIAN_POINT('Ctrl Pts',(7.80110358000007,-3.80523295924066,127.688371980166));
#70662=CARTESIAN_POINT('Ctrl Pts',(7.79346143612713,-3.89070000059879,127.792743991925));
#70663=CARTESIAN_POINT('Ctrl Pts',(7.78581929225413,-3.9719682192457,127.900755616373));
#70664=CARTESIAN_POINT('Ctrl Pts',(7.77817714838119,-4.04870997390888,128.012026359339));
#70665=CARTESIAN_POINT('Ctrl Pts',(7.77054026338514,-4.12539891938049,128.12322053228));
#70666=CARTESIAN_POINT('Ctrl Pts',(7.76290337838913,-4.19756736791663,128.237669032266));
#70667=CARTESIAN_POINT('Ctrl Pts',(7.75526649339307,-4.26492843596357,128.354958956219));
#70668=CARTESIAN_POINT('Ctrl Pts',(7.74763259241966,-4.33226318346841,128.472203050519));
#70669=CARTESIAN_POINT('Ctrl Pts',(7.73999869144624,-4.39479408454358,128.592286012124));
#70670=CARTESIAN_POINT('Ctrl Pts',(7.73236479047284,-4.45227827998498,128.714767073339));
#70671=CARTESIAN_POINT('Ctrl Pts',(7.72473255343253,-4.50974994580944,128.837221437812));
#70672=CARTESIAN_POINT('Ctrl Pts',(7.71710031639215,-4.56217692640189,128.962072495382));
#70673=CARTESIAN_POINT('Ctrl Pts',(7.70946807935184,-4.60936321395806,129.088856661199));
#70674=CARTESIAN_POINT('Ctrl Pts',(7.70183446999593,-4.65655798585214,129.215663623464));
#70675=CARTESIAN_POINT('Ctrl Pts',(7.69420086064008,-4.69851004404001,129.344404009283));
#70676=CARTESIAN_POINT('Ctrl Pts',(7.68656725128417,-4.7350723614769,129.474596430171));
#70677=CARTESIAN_POINT('Ctrl Pts',(7.68446478424792,-4.74514244282322,129.510454339651));
#70678=CARTESIAN_POINT('Ctrl Pts',(7.68236231721161,-4.75480396485171,129.546422313077));
#70679=CARTESIAN_POINT('Ctrl Pts',(7.68025985017536,-4.76405452823403,129.582490119308));
#70680=CARTESIAN_POINT('Origin',(213.235140564004,0.,130.804360617566));
#70681=CARTESIAN_POINT('',(5.58457496064637,-4.76405452823403,129.582490119308));
#70682=CARTESIAN_POINT('',(5.9302046085579,-4.76405452823401,129.582490119308));
#70683=CARTESIAN_POINT('',(213.235140564004,-4.76405452823405,129.582490119308));
#70684=CARTESIAN_POINT('',(7.26485943593479,-4.91824839244092,130.800384092418));
#70685=CARTESIAN_POINT('Ctrl Pts',(7.26485943593477,-4.91824839244093,130.800384092418));
#70686=CARTESIAN_POINT('Ctrl Pts',(7.2572111745685,-4.91835727452995,130.935051707829));
#70687=CARTESIAN_POINT('Ctrl Pts',(7.2495629132022,-4.91293095719067,131.069921889364));
#70688=CARTESIAN_POINT('Ctrl Pts',(7.24191465183594,-4.90194617917634,131.204493994027));
#70689=CARTESIAN_POINT('Ctrl Pts',(7.23427376524274,-4.89097199314379,131.338936338647));
#70690=CARTESIAN_POINT('Ctrl Pts',(7.22663287864958,-4.87445003899003,131.473080778438));
#70691=CARTESIAN_POINT('Ctrl Pts',(7.21899199205637,-4.85240909752608,131.606426084187));
#70692=CARTESIAN_POINT('Ctrl Pts',(7.21117029391079,-4.82984658611166,131.742926831578));
#70693=CARTESIAN_POINT('Ctrl Pts',(7.20334859576518,-4.80150060326161,131.878589721244));
#70694=CARTESIAN_POINT('Ctrl Pts',(7.1955268976196,-4.7674584782635,132.012881498864));
#70695=CARTESIAN_POINT('Ctrl Pts',(7.18789412315048,-4.73423859969954,132.143929620711));
#70696=CARTESIAN_POINT('Ctrl Pts',(7.18026134868138,-4.69559471079806,132.273671696196));
#70697=CARTESIAN_POINT('Ctrl Pts',(7.17262857421227,-4.65165968572856,132.401622409092));
#70698=CARTESIAN_POINT('Ctrl Pts',(7.16499680520051,-4.60773044817374,132.529556267175));
#70699=CARTESIAN_POINT('Ctrl Pts',(7.15736503618873,-4.55851159127469,132.655698850132));
#70700=CARTESIAN_POINT('Ctrl Pts',(7.14973326717697,-4.50418553713212,132.779581038074));
#70701=CARTESIAN_POINT('Ctrl Pts',(7.14210073665751,-4.44985406226613,132.903475587138));
#70702=CARTESIAN_POINT('Ctrl Pts',(7.13446820613806,-4.39041453938712,133.025108923194));
#70703=CARTESIAN_POINT('Ctrl Pts',(7.12683567561859,-4.32609687367602,133.144033437015));
#70704=CARTESIAN_POINT('Ctrl Pts',(7.11887197236391,-4.25898848774158,133.268118042425));
#70705=CARTESIAN_POINT('Ctrl Pts',(7.11090826910921,-4.1865693442687,133.38925304212));
#70706=CARTESIAN_POINT('Ctrl Pts',(7.10294456585453,-4.10915224902535,133.506961375508));
#70707=CARTESIAN_POINT('Ctrl Pts',(7.09530106243412,-4.03484789420867,133.61993696238));
#70708=CARTESIAN_POINT('Ctrl Pts',(7.08765755901373,-3.95593998433738,133.729755794599));
#70709=CARTESIAN_POINT('Ctrl Pts',(7.08001405559332,-3.87274710804022,133.836028953593));
#70710=CARTESIAN_POINT('Ctrl Pts',(7.07236545936534,-3.78949880096902,133.942372921575));
#70711=CARTESIAN_POINT('Ctrl Pts',(7.06471686313732,-3.70196010609965,134.045166208678));
#70712=CARTESIAN_POINT('Ctrl Pts',(7.05706826690934,-3.61048729867891,134.144055892374));
#70713=CARTESIAN_POINT('Ctrl Pts',(7.04940928413935,-3.5188902741955,134.243079865007));
#70714=CARTESIAN_POINT('Ctrl Pts',(7.04175030136939,-3.42334876518385,134.338189377904));
#70715=CARTESIAN_POINT('Ctrl Pts',(7.03409131859939,-3.32425305306113,134.429070909674));
#70716=CARTESIAN_POINT('Ctrl Pts',(7.03315129125375,-3.3120905137228,134.440225279339));
#70717=CARTESIAN_POINT('Ctrl Pts',(7.03221126390809,-3.29987447066042,134.451316011969));
#70718=CARTESIAN_POINT('Ctrl Pts',(7.03127123656245,-3.28760567540848,134.462342572896));
#70719=CARTESIAN_POINT('Ctrl Pts',(7.02349690244336,-3.18613871918751,134.553535844272));
#70720=CARTESIAN_POINT('Ctrl Pts',(7.01572256832429,-3.08071382331022,134.640648547029));
#70721=CARTESIAN_POINT('Ctrl Pts',(7.0079482342052,-2.97169310110002,134.723317516458));
#70722=CARTESIAN_POINT('Ctrl Pts',(7.00018348125811,-2.86280673718648,134.805884603771));
#70723=CARTESIAN_POINT('Ctrl Pts',(6.99241872831108,-2.75033367291102,134.884018620406));
#70724=CARTESIAN_POINT('Ctrl Pts',(6.98465397536398,-2.63467170147528,134.957394218194));
#70725=CARTESIAN_POINT('Ctrl Pts',(6.97689693447898,-2.51912460714011,135.030696938304));
#70726=CARTESIAN_POINT('Ctrl Pts',(6.96913989359391,-2.40039523664977,135.099250436693));
#70727=CARTESIAN_POINT('Ctrl Pts',(6.96138285270891,-2.27891290901463,135.162770765272));
#70728=CARTESIAN_POINT('Ctrl Pts',(6.95363166146881,-2.15752219214824,135.226243192677));
#70729=CARTESIAN_POINT('Ctrl Pts',(6.94588047022871,-2.03338299540185,135.284689824665));
#70730=CARTESIAN_POINT('Ctrl Pts',(6.93812927898861,-1.90695164808688,135.337871230144));
#70731=CARTESIAN_POINT('Ctrl Pts',(6.93038138221154,-1.78057403746684,135.391030032108));
#70732=CARTESIAN_POINT('Ctrl Pts',(6.92263348543447,-1.65190657356444,135.438927907227));
#70733=CARTESIAN_POINT('Ctrl Pts',(6.9148855886574,-1.52142790195612,135.48137250569));
#70734=CARTESIAN_POINT('Ctrl Pts',(6.90713931257332,-1.39097652367328,135.523808225657));
#70735=CARTESIAN_POINT('Ctrl Pts',(6.89939303648919,-1.25871506282197,135.560792817032));
#70736=CARTESIAN_POINT('Ctrl Pts',(6.89164676040511,-1.12513937993463,135.592183132888));
#70737=CARTESIAN_POINT('Ctrl Pts',(6.88390042713978,-0.99156271102194,135.62357368046));
#70738=CARTESIAN_POINT('Ctrl Pts',(6.87615409387449,-0.856672181312171,
135.64936978067));
#70739=CARTESIAN_POINT('Ctrl Pts',(6.86840776060916,-0.720975564379753,
135.66947904347));
#70740=CARTESIAN_POINT('Ctrl Pts',(6.86065969260619,-0.585248559130641,
135.689592809599));
#70741=CARTESIAN_POINT('Ctrl Pts',(6.8529116246032,-0.448715494117277,135.704017146844));
#70742=CARTESIAN_POINT('Ctrl Pts',(6.84516355660023,-0.311890616307963,
135.712711390072));
#70743=CARTESIAN_POINT('Ctrl Pts',(6.83740725385838,-0.174920319390276,
135.721414873645));
#70744=CARTESIAN_POINT('Ctrl Pts',(6.82965095111652,-0.0376579809348041,
135.724376072915));
#70745=CARTESIAN_POINT('Ctrl Pts',(6.82189464837467,0.0993802295133067,
135.721606455683));
#70746=CARTESIAN_POINT('Ctrl Pts',(6.8141342058605,0.236491581380661,135.718835360223));
#70747=CARTESIAN_POINT('Ctrl Pts',(6.80637376334631,0.373378176858677,135.710327377766));
#70748=CARTESIAN_POINT('Ctrl Pts',(6.79861332083215,0.509528606611335,135.696145942122));
#70749=CARTESIAN_POINT('Ctrl Pts',(6.79084042056672,0.645897597120513,135.68194174118));
#70750=CARTESIAN_POINT('Ctrl Pts',(6.78306752030125,0.781527673326089,135.662045944079));
#70751=CARTESIAN_POINT('Ctrl Pts',(6.77529462003582,0.915916370811572,135.636573388562));
#70752=CARTESIAN_POINT('Ctrl Pts',(6.76780428427374,1.04541970063984,135.6120268246));
#70753=CARTESIAN_POINT('Ctrl Pts',(6.76031394851172,1.17377003920796,135.582301990793));
#70754=CARTESIAN_POINT('Ctrl Pts',(6.75282361274964,1.30053264666007,135.547544980151));
#70755=CARTESIAN_POINT('Ctrl Pts',(6.74504927863056,1.43210149690128,135.511470146887));
#70756=CARTESIAN_POINT('Ctrl Pts',(6.73727494451147,1.56237661225875,135.469859739883));
#70757=CARTESIAN_POINT('Ctrl Pts',(6.72950061039239,1.6908567208801,135.422822115939));
#70758=CARTESIAN_POINT('Ctrl Pts',(6.7217358574453,1.81917848925018,135.375842461662));
#70759=CARTESIAN_POINT('Ctrl Pts',(6.71397110449823,1.94570928886396,135.323449031806));
#70760=CARTESIAN_POINT('Ctrl Pts',(6.70620635155115,2.0699603781493,135.265800642423));
#70761=CARTESIAN_POINT('Ctrl Pts',(6.69844931066616,2.19408805950096,135.208209510233));
#70762=CARTESIAN_POINT('Ctrl Pts',(6.69069226978117,2.31594018410765,135.14537396864));
#70763=CARTESIAN_POINT('Ctrl Pts',(6.68293522889618,2.4350458009878,135.07750173501));
#70764=CARTESIAN_POINT('Ctrl Pts',(6.67518403765605,2.55406159939608,135.009680684359));
#70765=CARTESIAN_POINT('Ctrl Pts',(6.66743284641591,2.67033467429255,134.936830694559));
#70766=CARTESIAN_POINT('Ctrl Pts',(6.65968165517577,2.78341692837952,134.859206270031));
#70767=CARTESIAN_POINT('Ctrl Pts',(6.65193375839868,2.89645111949194,134.781614837953));
#70768=CARTESIAN_POINT('Ctrl Pts',(6.64418586162162,3.00629686548536,134.699253227993));
#70769=CARTESIAN_POINT('Ctrl Pts',(6.63643796484453,3.11253361738844,134.612420168456));
#70770=CARTESIAN_POINT('Ctrl Pts',(6.62869168876044,3.21874814685306,134.525605272524));
#70771=CARTESIAN_POINT('Ctrl Pts',(6.62094541267632,3.32135488129076,134.434321034708));
#70772=CARTESIAN_POINT('Ctrl Pts',(6.61319913659221,3.41996536240851,134.338907262106));
#70773=CARTESIAN_POINT('Ctrl Pts',(6.60545280332685,3.51857657144656,134.243492785181));
#70774=CARTESIAN_POINT('Ctrl Pts',(6.59770647006154,3.61319118732984,134.143948984506));
#70775=CARTESIAN_POINT('Ctrl Pts',(6.58996013679618,3.70345701567332,134.040653125291));
#70776=CARTESIAN_POINT('Ctrl Pts',(6.58221206879322,3.79374305842295,133.937334133686));
#70777=CARTESIAN_POINT('Ctrl Pts',(6.57446400079024,3.87967811851019,133.830261705888));
#70778=CARTESIAN_POINT('Ctrl Pts',(6.56671593278728,3.96095002016121,133.719846511938));
#70779=CARTESIAN_POINT('Ctrl Pts',(6.55895963004543,4.04230829855656,133.609313967407));
#70780=CARTESIAN_POINT('Ctrl Pts',(6.55120332730362,4.11899328612188,133.49543187513));
#70781=CARTESIAN_POINT('Ctrl Pts',(6.54344702456177,4.19073562879666,133.37864070179));
#70782=CARTESIAN_POINT('Ctrl Pts',(6.53568658204762,4.26251626251975,133.261787193486));
#70783=CARTESIAN_POINT('Ctrl Pts',(6.52792613953346,4.3293488044162,133.142021851543));
#70784=CARTESIAN_POINT('Ctrl Pts',(6.52016569701931,4.39101019391058,133.019809226646));
#70785=CARTESIAN_POINT('Ctrl Pts',(6.51239279675388,4.45277056774158,132.897400415193));
#70786=CARTESIAN_POINT('Ctrl Pts',(6.5046198964884,4.50934303930082,132.772536826523));
#70787=CARTESIAN_POINT('Ctrl Pts',(6.49684699622296,4.56055263054152,132.645703270784));
#70788=CARTESIAN_POINT('Ctrl Pts',(6.48935666046088,4.60990062415172,132.52348043427));
#70789=CARTESIAN_POINT('Ctrl Pts',(6.48186632469884,4.6542687727465,132.39942866062));
#70790=CARTESIAN_POINT('Ctrl Pts',(6.47437598893677,4.69354500100034,132.273992675628));
#70791=CARTESIAN_POINT('Ctrl Pts',(6.46660165481768,4.73431039938595,132.143800747141));
#70792=CARTESIAN_POINT('Ctrl Pts',(6.45882732069861,4.76971926750344,132.011705161631));
#70793=CARTESIAN_POINT('Ctrl Pts',(6.45105298657953,4.79959181931533,131.878186222802));
#70794=CARTESIAN_POINT('Ctrl Pts',(6.44328823363245,4.82942755587681,131.744831834133));
#70795=CARTESIAN_POINT('Ctrl Pts',(6.43552348068539,4.85374046735714,131.610057960262));
#70796=CARTESIAN_POINT('Ctrl Pts',(6.42775872773831,4.87239999344214,131.474361637271));
#70797=CARTESIAN_POINT('Ctrl Pts',(6.42000168685332,4.89104098662277,131.33880008978));
#70798=CARTESIAN_POINT('Ctrl Pts',(6.41224464596833,4.90403971563981,131.202318301243));
#70799=CARTESIAN_POINT('Ctrl Pts',(6.40448760508335,4.9113163784853,131.065424772367));
#70800=CARTESIAN_POINT('Ctrl Pts',(6.3967364138432,4.91858755394277,130.928634475965));
#70801=CARTESIAN_POINT('Ctrl Pts',(6.38898522260302,4.92014523141444,130.791433446083));
#70802=CARTESIAN_POINT('Ctrl Pts',(6.38123403136288,4.91596132514216,130.654336245524));
#70803=CARTESIAN_POINT('Ctrl Pts',(6.37348613458579,4.91177919714166,130.517297314933));
#70804=CARTESIAN_POINT('Ctrl Pts',(6.36573823780875,4.90186035092097,130.380362515858));
#70805=CARTESIAN_POINT('Ctrl Pts',(6.35799034103167,4.88622879807351,130.244047138006));
#70806=CARTESIAN_POINT('Ctrl Pts',(6.35024406494757,4.87060051500995,130.107760274392));
#70807=CARTESIAN_POINT('Ctrl Pts',(6.34249778886339,4.84926194670322,129.972092962455));
#70808=CARTESIAN_POINT('Ctrl Pts',(6.33475151277929,4.82228901129376,129.837555697194));
#70809=CARTESIAN_POINT('Ctrl Pts',(6.3270051795139,4.79531587677608,129.703017438809));
#70810=CARTESIAN_POINT('Ctrl Pts',(6.31925884624859,4.76270836901654,129.569609627084));
#70811=CARTESIAN_POINT('Ctrl Pts',(6.3115125129832,4.72459352225369,129.43783249419));
#70812=CARTESIAN_POINT('Ctrl Pts',(6.30376444498021,4.68647013993534,129.306025850721));
#70813=CARTESIAN_POINT('Ctrl Pts',(6.29601637697722,4.64283707303733,129.175850988248));
#70814=CARTESIAN_POINT('Ctrl Pts',(6.28826830897424,4.59387109126585,129.047792526278));
#70815=CARTESIAN_POINT('Ctrl Pts',(6.28051200623239,4.5448530678663,128.919597962251));
#70816=CARTESIAN_POINT('Ctrl Pts',(6.27275570349055,4.49049094723878,128.79352465778));
#70817=CARTESIAN_POINT('Ctrl Pts',(6.26499940074871,4.43100971403031,128.670037311066));
#70818=CARTESIAN_POINT('Ctrl Pts',(6.25723895823452,4.3714967338965,128.546484055437));
#70819=CARTESIAN_POINT('Ctrl Pts',(6.24947851572029,4.30685938115965,128.425519852392));
#70820=CARTESIAN_POINT('Ctrl Pts',(6.2417180732061,4.23736792577663,128.307583470102));
#70821=CARTESIAN_POINT('Ctrl Pts',(6.23394517294067,4.16776491654045,128.189457765862));
#70822=CARTESIAN_POINT('Ctrl Pts',(6.22617227267524,4.093292445809,128.074369923685));
#70823=CARTESIAN_POINT('Ctrl Pts',(6.21839937240981,4.01426381818204,127.962729209284));
#70824=CARTESIAN_POINT('Ctrl Pts',(6.21090903664783,3.93810808023096,127.855146916059));
#70825=CARTESIAN_POINT('Ctrl Pts',(6.20341870088583,3.85772187779952,127.750765722285));
#70826=CARTESIAN_POINT('Ctrl Pts',(6.19592836512385,3.77341879184149,127.649920305264));
#70827=CARTESIAN_POINT('Ctrl Pts',(6.18815403100476,3.68591932875538,127.545251303604));
#70828=CARTESIAN_POINT('Ctrl Pts',(6.1803796968857,3.59392292965214,127.444059929443));
#70829=CARTESIAN_POINT('Ctrl Pts',(6.1726053627666,3.49773650889457,127.346757057751));
#70830=CARTESIAN_POINT('Ctrl Pts',(6.1648406098195,3.40166862930415,127.249574103152));
#70831=CARTESIAN_POINT('Ctrl Pts',(6.15707585687246,3.30142127475228,127.156270391283));
#70832=CARTESIAN_POINT('Ctrl Pts',(6.14931110392536,3.19734204473323,127.067224426379));
#70833=CARTESIAN_POINT('Ctrl Pts',(6.14155406304033,3.09336618767242,126.978266903182));
#70834=CARTESIAN_POINT('Ctrl Pts',(6.13379702215528,2.98556632415576,126.893558963859));
#70835=CARTESIAN_POINT('Ctrl Pts',(6.12603998127025,2.8743271352957,126.813442605153));
#70836=CARTESIAN_POINT('Ctrl Pts',(6.11828879003016,2.76317183277417,126.733386662817));
#70837=CARTESIAN_POINT('Ctrl Pts',(6.11053759879005,2.64858268332197,126.657915636672));
#70838=CARTESIAN_POINT('Ctrl Pts',(6.10278640754996,2.53097742216015,126.587331289826));
#70839=CARTESIAN_POINT('Ctrl Pts',(6.09503851077288,2.41342214637107,126.516776943211));
#70840=CARTESIAN_POINT('Ctrl Pts',(6.08729061399582,2.29285364305069,126.451105345734));
#70841=CARTESIAN_POINT('Ctrl Pts',(6.07954271721874,2.16971841887591,126.390574822436));
#70842=CARTESIAN_POINT('Ctrl Pts',(6.07179644113467,2.04660895193588,126.330056960819));
#70843=CARTESIAN_POINT('Ctrl Pts',(6.06405016505058,1.92093418271198,126.274678206715));
#70844=CARTESIAN_POINT('Ctrl Pts',(6.05630388896651,1.79316464071586,126.224650623059));
#70845=CARTESIAN_POINT('Ctrl Pts',(6.04855755570119,1.66539415555401,126.174622670111));
#70846=CARTESIAN_POINT('Ctrl Pts',(6.04081122243583,1.53552923081809,126.129946108978));
#70847=CARTESIAN_POINT('Ctrl Pts',(6.0330648891705,1.404059391111,126.090784449864));
#70848=CARTESIAN_POINT('Ctrl Pts',(6.02531682116754,1.27256010964468,126.051614020767));
#70849=CARTESIAN_POINT('Ctrl Pts',(6.01756875316456,1.13945557264713,126.017961062836));
#70850=CARTESIAN_POINT('Ctrl Pts',(6.0098206851616,1.00524905258022,125.989938803393));
#70851=CARTESIAN_POINT('Ctrl Pts',(6.00206438241975,0.87089989622652,125.961886761558));
#70852=CARTESIAN_POINT('Ctrl Pts',(5.99430807967794,0.735446800525724,125.939477452679));
#70853=CARTESIAN_POINT('Ctrl Pts',(5.9865517769361,0.599402338932921,125.922772771528));
#70854=CARTESIAN_POINT('Ctrl Pts',(5.97879133442193,0.463285266314561,125.906059174586));
#70855=CARTESIAN_POINT('Ctrl Pts',(5.97103089190775,0.326576588399491,125.895056303608));
#70856=CARTESIAN_POINT('Ctrl Pts',(5.96327044939358,0.189791540789937,125.889773937738));
#70857=CARTESIAN_POINT('Ctrl Pts',(5.95549754912814,0.052786913678754,125.884483092145));
#70858=CARTESIAN_POINT('Ctrl Pts',(5.94772464886272,-0.0842939369234755,
125.884931101068));
#70859=CARTESIAN_POINT('Ctrl Pts',(5.93995174859728,-0.220937335391866,
125.891075590588));
#70860=CARTESIAN_POINT('Ctrl Pts',(5.93246141283519,-0.352613402143094,
125.896996712436));
#70861=CARTESIAN_POINT('Ctrl Pts',(5.92497107707308,-0.483882962651974,
125.908207316311));
#70862=CARTESIAN_POINT('Ctrl Pts',(5.91748074131098,-0.61429494526265,125.924624478929));
#70863=CARTESIAN_POINT('Ctrl Pts',(5.90970640719189,-0.749651537830731,
125.941664103257));
#70864=CARTESIAN_POINT('Ctrl Pts',(5.9019320730728,-0.884513007652761,125.964366869825));
#70865=CARTESIAN_POINT('Ctrl Pts',(5.89415773895371,-1.01836777927145,125.992696650845));
#70866=CARTESIAN_POINT('Ctrl Pts',(5.8863929860066,-1.15205758684725,126.020991517942));
#70867=CARTESIAN_POINT('Ctrl Pts',(5.87862823305954,-1.28474278595388,126.054899521144));
#70868=CARTESIAN_POINT('Ctrl Pts',(5.87086348011243,-1.4159170442427,126.094332805937));
#70869=CARTESIAN_POINT('Ctrl Pts',(5.86310643922744,-1.54696101840859,126.133726925035));
#70870=CARTESIAN_POINT('Ctrl Pts',(5.85534939834241,-1.67649666620272,126.178635292951));
#70871=CARTESIAN_POINT('Ctrl Pts',(5.84759235745742,-1.80402832654186,126.228919124165));
#70872=CARTESIAN_POINT('Ctrl Pts',(5.83984116621732,-1.93146381426336,126.27916503595));
#70873=CARTESIAN_POINT('Ctrl Pts',(5.83208997497718,-2.05689796028396,126.334778199604));
#70874=CARTESIAN_POINT('Ctrl Pts',(5.82433878373709,-2.17985108666403,126.395570272985));
#70875=CARTESIAN_POINT('Ctrl Pts',(5.81659088696,-2.30275195468635,126.456336508113));
#70876=CARTESIAN_POINT('Ctrl Pts',(5.80884299018301,-2.42317355065415,126.52227710208));
#70877=CARTESIAN_POINT('Ctrl Pts',(5.80109509340591,-2.54065719063008,126.593156027167));
#70878=CARTESIAN_POINT('Ctrl Pts',(5.79334881732182,-2.65811625556071,126.66402012591));
#70879=CARTESIAN_POINT('Ctrl Pts',(5.7856025412377,-2.77263825233905,126.739820299258));
#70880=CARTESIAN_POINT('Ctrl Pts',(5.77785626515362,-2.88379043371678,126.820275302603));
#70881=CARTESIAN_POINT('Ctrl Pts',(5.77010993188827,-2.99494343559482,126.900730899849));
#70882=CARTESIAN_POINT('Ctrl Pts',(5.7623635986229,-3.10272625572969,126.985841166417));
#70883=CARTESIAN_POINT('Ctrl Pts',(5.75461726535755,-3.20673672834962,127.075282632654));
#70884=CARTESIAN_POINT('Ctrl Pts',(5.74686919735461,-3.31077049339332,127.164744128687));
#70885=CARTESIAN_POINT('Ctrl Pts',(5.7391211293517,-3.41102993350776,127.258538499599));
#70886=CARTESIAN_POINT('Ctrl Pts',(5.73137306134876,-3.50714775628163,127.356303530146));
#70887=CARTESIAN_POINT('Ctrl Pts',(5.72361675860691,-3.60336773422175,127.454172466531));
#70888=CARTESIAN_POINT('Ctrl Pts',(5.7158604558651,-3.69543702729854,127.556020213348));
#70889=CARTESIAN_POINT('Ctrl Pts',(5.70810415312326,-3.78302650321348,127.661448983669));
#70890=CARTESIAN_POINT('Ctrl Pts',(5.70034371060909,-3.87066272826922,127.766934024499));
#70891=CARTESIAN_POINT('Ctrl Pts',(5.69258326809486,-3.95381413494921,127.876003586496));
#70892=CARTESIAN_POINT('Ctrl Pts',(5.68482282558068,-4.03219399835365,127.988229473223));
#70893=CARTESIAN_POINT('Ctrl Pts',(5.67704992531526,-4.11069968407284,128.100635514905));
#70894=CARTESIAN_POINT('Ctrl Pts',(5.66927702504981,-4.18441830961435,128.216207676614));
#70895=CARTESIAN_POINT('Ctrl Pts',(5.66150412478439,-4.25310787113293,128.33449088436));
#70896=CARTESIAN_POINT('Ctrl Pts',(5.65401378902231,-4.31930039407231,128.448474199568));
#70897=CARTESIAN_POINT('Ctrl Pts',(5.64652345326028,-4.38082299942428,128.5649746038));
#70898=CARTESIAN_POINT('Ctrl Pts',(5.6390331174982,-4.4375016376466,128.683567775635));
#70899=CARTESIAN_POINT('Ctrl Pts',(5.63062887149623,-4.50109574528171,128.816630727941));
#70900=CARTESIAN_POINT('Ctrl Pts',(5.62222462549418,-4.55876921861174,128.952698836224));
#70901=CARTESIAN_POINT('Ctrl Pts',(5.61382037949224,-4.61025095434813,129.091243808813));
#70902=CARTESIAN_POINT('Ctrl Pts',(5.60543761451511,-4.66160110416448,129.22943466421));
#70903=CARTESIAN_POINT('Ctrl Pts',(5.59705484953792,-4.70679097399697,129.370089487592));
#70904=CARTESIAN_POINT('Ctrl Pts',(5.58867208456076,-4.74559683346664,129.512658733735));
#70905=CARTESIAN_POINT('Ctrl Pts',(5.58730637658928,-4.75191902808408,129.535885909551));
#70906=CARTESIAN_POINT('Ctrl Pts',(5.58594066861784,-4.75807187600522,129.559163849067));
#70907=CARTESIAN_POINT('Ctrl Pts',(5.58457496064636,-4.76405452823403,129.582490119308));
#70908=CARTESIAN_POINT('Ctrl Pts',(7.33490367089149,-4.76405452823399,129.582490119308));
#70909=CARTESIAN_POINT('Ctrl Pts',(7.32712774182063,-4.79805954746054,129.715075173174));
#70910=CARTESIAN_POINT('Ctrl Pts',(7.31935181274974,-4.82648152751553,129.848908982077));
#70911=CARTESIAN_POINT('Ctrl Pts',(7.31157588367887,-4.8492618516729,129.983481481268));
#70912=CARTESIAN_POINT('Ctrl Pts',(7.31095687591102,-4.85107529383255,129.994194210458));
#70913=CARTESIAN_POINT('Ctrl Pts',(7.31033786814316,-4.85285301182095,130.004911619619));
#70914=CARTESIAN_POINT('Ctrl Pts',(7.30971886037531,-4.85459499024321,130.015633451047));
#70915=CARTESIAN_POINT('Ctrl Pts',(7.29709861902769,-4.89011019579174,130.234228608222));
#70916=CARTESIAN_POINT('Ctrl Pts',(7.28447837768005,-4.91086740907761,130.455283374741));
#70917=CARTESIAN_POINT('Ctrl Pts',(7.27185813633238,-4.91660648592595,130.677223978273));
#70918=CARTESIAN_POINT('Ctrl Pts',(7.26952523621868,-4.9176673763371,130.718250551771));
#70919=CARTESIAN_POINT('Ctrl Pts',(7.26719233610501,-4.91821518082649,130.759307292362));
#70920=CARTESIAN_POINT('Ctrl Pts',(7.2648594359913,-4.91824839244012,130.800384091423));
#70921=CARTESIAN_POINT('',(7.6101405640404,-4.91824853408196,130.808157919327));
#70922=CARTESIAN_POINT('Ctrl Pts',(7.68025985017536,-4.76405452823403,129.582490119308));
#70923=CARTESIAN_POINT('Ctrl Pts',(7.67262044065622,-4.79766687065929,129.713544132286));
#70924=CARTESIAN_POINT('Ctrl Pts',(7.66498103113705,-4.82584948931522,129.845916780401));
#70925=CARTESIAN_POINT('Ctrl Pts',(7.65734162161792,-4.84852009828473,129.979111613308));
#70926=CARTESIAN_POINT('Ctrl Pts',(7.64947477868833,-4.87186563558502,130.116271799169));
#70927=CARTESIAN_POINT('Ctrl Pts',(7.64160793575874,-4.8893657805543,130.25430342844));
#70928=CARTESIAN_POINT('Ctrl Pts',(7.63374109282915,-4.90098822212115,130.392659865648));
#70929=CARTESIAN_POINT('Ctrl Pts',(7.62587424989955,-4.91261066368802,130.531016302857));
#70930=CARTESIAN_POINT('Ctrl Pts',(7.61800740696999,-4.91835543749873,130.669697084274));
#70931=CARTESIAN_POINT('Ctrl Pts',(7.61014056404039,-4.91824853408196,130.808157919327));
#70932=CARTESIAN_POINT('Ctrl Pts',(7.61014056400873,-4.91824853408153,130.808157919885));
#70933=CARTESIAN_POINT('Ctrl Pts',(7.59628620534876,-4.91806026560986,131.05200238028));
#70934=CARTESIAN_POINT('Ctrl Pts',(7.58243184668884,-4.8997349343828,131.295162959375));
#70935=CARTESIAN_POINT('Ctrl Pts',(7.56857748802884,-4.86358951030189,131.53557887348));
#70936=CARTESIAN_POINT('Ctrl Pts',(7.56080315390975,-4.84330660796207,131.670487582693));
#70937=CARTESIAN_POINT('Ctrl Pts',(7.55302881979068,-4.81737407580755,131.804765411944));
#70938=CARTESIAN_POINT('Ctrl Pts',(7.54525448567159,-4.78584030762398,131.937901800065));
#70939=CARTESIAN_POINT('Ctrl Pts',(7.5374897327245,-4.75434540199149,132.070874109486));
#70940=CARTESIAN_POINT('Ctrl Pts',(7.52972497977747,-4.71726308453112,132.202707399951));
#70941=CARTESIAN_POINT('Ctrl Pts',(7.52196022683037,-4.67469333503861,132.332897593189));
#70942=CARTESIAN_POINT('Ctrl Pts',(7.51420318594536,-4.63216586642137,132.462958479691));
#70943=CARTESIAN_POINT('Ctrl Pts',(7.50644614506031,-4.584161932627,132.591379147415));
#70944=CARTESIAN_POINT('Ctrl Pts',(7.4986891041753,-4.53083217370943,132.717667408486));
#70945=CARTESIAN_POINT('Ctrl Pts',(7.49093791293519,-4.47754263117812,132.843860434596));
#70946=CARTESIAN_POINT('Ctrl Pts',(7.48318672169511,-4.41893540909666,132.967923896096));
#70947=CARTESIAN_POINT('Ctrl Pts',(7.475435530455,-4.35521030631677,133.089382772875));
#70948=CARTESIAN_POINT('Ctrl Pts',(7.46768763367792,-4.2915122884053,133.210790026391));
#70949=CARTESIAN_POINT('Ctrl Pts',(7.45993973690087,-4.22270089743599,133.329594551477));
#70950=CARTESIAN_POINT('Ctrl Pts',(7.45219184012379,-4.14902310030759,133.4453434603));
#70951=CARTESIAN_POINT('Ctrl Pts',(7.44444556403969,-4.07536071498604,133.561068156946));
#70952=CARTESIAN_POINT('Ctrl Pts',(7.43669928795559,-3.99683415806429,133.673738179062));
#70953=CARTESIAN_POINT('Ctrl Pts',(7.4289530118715,-3.91373497789903,133.782927653117));
#70954=CARTESIAN_POINT('Ctrl Pts',(7.42120667860616,-3.83063518431451,133.892117933183));
#70955=CARTESIAN_POINT('Ctrl Pts',(7.41346034534081,-3.74296293690717,133.997827302806));
#70956=CARTESIAN_POINT('Ctrl Pts',(7.40571401207546,-3.65105126304789,134.099661474407));
#70957=CARTESIAN_POINT('Ctrl Pts',(7.39796594407249,-3.55911900620652,134.201518451065));
#70958=CARTESIAN_POINT('Ctrl Pts',(7.39021787606948,-3.46294569563908,134.299498212655));
#70959=CARTESIAN_POINT('Ctrl Pts',(7.3824698080665,-3.36290225628413,134.393242264706));
#70960=CARTESIAN_POINT('Ctrl Pts',(7.37471350532465,-3.26275248957129,134.487085949051));
#70961=CARTESIAN_POINT('Ctrl Pts',(7.36695720258282,-3.15872466321802,134.576684663347));
#70962=CARTESIAN_POINT('Ctrl Pts',(7.35920089984097,-3.0512243478669,134.661718915869));
#70963=CARTESIAN_POINT('Ctrl Pts',(7.3514404573268,-2.94366665636056,134.746798553731));
#70964=CARTESIAN_POINT('Ctrl Pts',(7.34368001481259,-2.83263309921594,134.82730864611));
#70965=CARTESIAN_POINT('Ctrl Pts',(7.33591957229842,-2.71855863016779,134.902972826209));
#70966=CARTESIAN_POINT('Ctrl Pts',(7.328146672033,-2.60430103865502,134.978758469168));
#70967=CARTESIAN_POINT('Ctrl Pts',(7.32037377176758,-2.48699311512489,135.049682452353));
#70968=CARTESIAN_POINT('Ctrl Pts',(7.31260087150216,-2.36709560994132,135.115513762131));
#70969=CARTESIAN_POINT('Ctrl Pts',(7.30511053574008,-2.25155668107396,135.178951937981));
#70970=CARTESIAN_POINT('Ctrl Pts',(7.29762019997802,-2.13361345318878,135.237661137868));
#70971=CARTESIAN_POINT('Ctrl Pts',(7.29012986421594,-2.01369430221937,135.291477544916));
#70972=CARTESIAN_POINT('Ctrl Pts',(7.28235553009686,-1.88922838019302,135.347334417394));
#70973=CARTESIAN_POINT('Ctrl Pts',(7.27458119597784,-1.76223947243117,135.398097090274));
#70974=CARTESIAN_POINT('Ctrl Pts',(7.26680686185875,-1.63318328652827,135.443530307834));
#70975=CARTESIAN_POINT('Ctrl Pts',(7.25904210891167,-1.50428615084059,135.488907533015));
#70976=CARTESIAN_POINT('Ctrl Pts',(7.25127735596448,-1.37332717148633,135.528968242813));
#70977=CARTESIAN_POINT('Ctrl Pts',(7.24351260301739,-1.24078448531313,135.563524086444));
#70978=CARTESIAN_POINT('Ctrl Pts',(7.2357555621324,-1.10837344240436,135.598045608724));
#70979=CARTESIAN_POINT('Ctrl Pts',(7.22799852124746,-0.974382198808795,
135.627073047435));
#70980=CARTESIAN_POINT('Ctrl Pts',(7.22024148036246,-0.83930627075409,135.650467100752));
#70981=CARTESIAN_POINT('Ctrl Pts',(7.21249028912233,-0.704332204507285,
135.67384351243));
#70982=CARTESIAN_POINT('Ctrl Pts',(7.20473909788218,-0.568275465590584,
135.69159492801));
#70983=CARTESIAN_POINT('Ctrl Pts',(7.19698790664205,-0.431643698037308,
135.703632683949));
#70984=CARTESIAN_POINT('Ctrl Pts',(7.18924000986497,-0.2950700026302,135.715665323521));
#70985=CARTESIAN_POINT('Ctrl Pts',(7.18149211308789,-0.157922153325711,
135.72198909923));
#70986=CARTESIAN_POINT('Ctrl Pts',(7.17374421631081,-0.0207146691257019,
135.722566994385));
#70987=CARTESIAN_POINT('Ctrl Pts',(7.16599794022671,0.116464114226464,135.723144768657));
#70988=CARTESIAN_POINT('Ctrl Pts',(7.15825166414256,0.253702116947971,135.717979051403));
#70989=CARTESIAN_POINT('Ctrl Pts',(7.15050538805846,0.390483450566157,135.707084935467));
#70990=CARTESIAN_POINT('Ctrl Pts',(7.14275905479311,0.527265793873075,135.696190739112));
#70991=CARTESIAN_POINT('Ctrl Pts',(7.13501272152783,0.663591071619001,135.679568090737));
#70992=CARTESIAN_POINT('Ctrl Pts',(7.12726638826248,0.79894754906899,135.657284053634));
#70993=CARTESIAN_POINT('Ctrl Pts',(7.11951832025951,0.934334338663608,135.634995026175));
#70994=CARTESIAN_POINT('Ctrl Pts',(7.11177025225655,1.06875151054637,135.607042150653));
#70995=CARTESIAN_POINT('Ctrl Pts',(7.10402218425358,1.20169695917431,135.573543721706));
#70996=CARTESIAN_POINT('Ctrl Pts',(7.09626588151172,1.33478370380732,135.540009690229));
#70997=CARTESIAN_POINT('Ctrl Pts',(7.08850957876982,1.46639522087747,135.500918427344));
#70998=CARTESIAN_POINT('Ctrl Pts',(7.08075327602796,1.59604349210736,135.456438458037));
#70999=CARTESIAN_POINT('Ctrl Pts',(7.07299283351379,1.72576096052324,135.411934748431));
#71000=CARTESIAN_POINT('Ctrl Pts',(7.06523239099967,1.85351273118804,135.36203674367));
#71001=CARTESIAN_POINT('Ctrl Pts',(7.0574719484855,1.97883118577096,135.306960999647));
#71002=CARTESIAN_POINT('Ctrl Pts',(7.04969904822006,2.10435081266243,135.251796843151));
#71003=CARTESIAN_POINT('Ctrl Pts',(7.04192614795461,2.2274289664611,135.191438510078));
#71004=CARTESIAN_POINT('Ctrl Pts',(7.03415324768918,2.34762224202864,135.126148774247));
#71005=CARTESIAN_POINT('Ctrl Pts',(7.02666291192713,2.46344618928086,135.063232484769));
#71006=CARTESIAN_POINT('Ctrl Pts',(7.01917257616506,2.57659109747155,134.995737263415));
#71007=CARTESIAN_POINT('Ctrl Pts',(7.01168224040302,2.68668759516743,134.923934967966));
#71008=CARTESIAN_POINT('Ctrl Pts',(7.00390790628395,2.80095843503624,134.849410266662));
#71009=CARTESIAN_POINT('Ctrl Pts',(6.99613357216491,2.91230711592514,134.770009366688));
#71010=CARTESIAN_POINT('Ctrl Pts',(6.98835923804583,3.02028938944762,134.685988506286));
#71011=CARTESIAN_POINT('Ctrl Pts',(6.98059448509874,3.12813858446863,134.602071194086));
#71012=CARTESIAN_POINT('Ctrl Pts',(6.97282973215161,3.23262932139203,134.513545487987));
#71013=CARTESIAN_POINT('Ctrl Pts',(6.96506497920453,3.33334469072293,134.420711849862));
#71014=CARTESIAN_POINT('Ctrl Pts',(6.95730793831954,3.43396002812917,134.327970415415));
#71015=CARTESIAN_POINT('Ctrl Pts',(6.94955089743459,3.53080717449782,134.230929827006));
#71016=CARTESIAN_POINT('Ctrl Pts',(6.94179385654959,3.62350109263339,134.129931680434));
#71017=CARTESIAN_POINT('Ctrl Pts',(6.93404266530948,3.71612510956425,134.029009697349));
#71018=CARTESIAN_POINT('Ctrl Pts',(6.92629147406933,3.80460186899259,133.924136383295));
#71019=CARTESIAN_POINT('Ctrl Pts',(6.91854028282921,3.88858238177032,133.815690908764));
#71020=CARTESIAN_POINT('Ctrl Pts',(6.91079238605214,3.97252720058986,133.707291526452));
#71021=CARTESIAN_POINT('Ctrl Pts',(6.9030444892751,4.05197933476359,133.595323311841));
#71022=CARTESIAN_POINT('Ctrl Pts',(6.89529659249803,4.12662953101364,133.480199135912));
#71023=CARTESIAN_POINT('Ctrl Pts',(6.88755031641393,4.20126411205189,133.36509904148));
#71024=CARTESIAN_POINT('Ctrl Pts',(6.87980404032983,4.27109854052124,133.246844626653));
#71025=CARTESIAN_POINT('Ctrl Pts',(6.87205776424574,4.33586666413687,133.125878081064));
#71026=CARTESIAN_POINT('Ctrl Pts',(6.8643114309804,4.40063526585608,133.004910642528));
#71027=CARTESIAN_POINT('Ctrl Pts',(6.85656509771505,4.46033730355215,132.88123137795));
#71028=CARTESIAN_POINT('Ctrl Pts',(6.8488187644497,4.51475259434785,132.755307073605));
#71029=CARTESIAN_POINT('Ctrl Pts',(6.84107069644674,4.56918007107063,132.629354569384));
#71030=CARTESIAN_POINT('Ctrl Pts',(6.83332262844376,4.61831828995238,132.501156383781));
#71031=CARTESIAN_POINT('Ctrl Pts',(6.8255745604408,4.66199537531048,132.371198893548));
#71032=CARTESIAN_POINT('Ctrl Pts',(6.81781825769896,4.70571888119466,132.241103282949));
#71033=CARTESIAN_POINT('Ctrl Pts',(6.81006195495711,4.7439695343741,132.10924500376));
#71034=CARTESIAN_POINT('Ctrl Pts',(6.80230565221527,4.77662533389249,131.97612573145));
#71035=CARTESIAN_POINT('Ctrl Pts',(6.79454520970111,4.80929856279434,131.842935409377));
#71036=CARTESIAN_POINT('Ctrl Pts',(6.78678476718693,4.83637091075933,131.708483136199));
#71037=CARTESIAN_POINT('Ctrl Pts',(6.77902432467278,4.8577718132622,131.573279386211));
#71038=CARTESIAN_POINT('Ctrl Pts',(6.77125142440736,4.87920707039365,131.437858595161));
#71039=CARTESIAN_POINT('Ctrl Pts',(6.76347852414195,4.89495264382186,131.301684305256));
#71040=CARTESIAN_POINT('Ctrl Pts',(6.75570562387654,4.90498994129464,131.165271601464));
#71041=CARTESIAN_POINT('Ctrl Pts',(6.74821528811446,4.91466235772195,131.033817843057));
#71042=CARTESIAN_POINT('Ctrl Pts',(6.74072495235235,4.91903430302753,130.90214301156));
#71043=CARTESIAN_POINT('Ctrl Pts',(6.73323461659027,4.91813484458084,130.770704815395));
#71044=CARTESIAN_POINT('Ctrl Pts',(6.72546028247117,4.91720128289376,130.634283100072));
#71045=CARTESIAN_POINT('Ctrl Pts',(6.71768594835209,4.91058573885847,130.497684175371));
#71046=CARTESIAN_POINT('Ctrl Pts',(6.70991161423299,4.89826366586087,130.361420303068));
#71047=CARTESIAN_POINT('Ctrl Pts',(6.70214686128589,4.88595677871698,130.225324363811));
#71048=CARTESIAN_POINT('Ctrl Pts',(6.69438210833877,4.86795739063315,130.089563040998));
#71049=CARTESIAN_POINT('Ctrl Pts',(6.68661735539166,4.84429293892591,129.954649499378));
#71050=CARTESIAN_POINT('Ctrl Pts',(6.67886031450665,4.82065199108574,129.819869955789));
#71051=CARTESIAN_POINT('Ctrl Pts',(6.67110327362168,4.79135724396076,129.685936900312));
#71052=CARTESIAN_POINT('Ctrl Pts',(6.66334623273667,4.7564879697602,129.553358916517));
#71053=CARTESIAN_POINT('Ctrl Pts',(6.65559504149654,4.72164499075055,129.420880910811));
#71054=CARTESIAN_POINT('Ctrl Pts',(6.64784385025639,4.68123595110599,129.289756319393));
#71055=CARTESIAN_POINT('Ctrl Pts',(6.64009265901626,4.63539122054166,129.160483707629));
#71056=CARTESIAN_POINT('Ctrl Pts',(6.63234476223918,4.58956597521078,129.031266040173));
#71057=CARTESIAN_POINT('Ctrl Pts',(6.62459686546214,4.53830976440054,128.903899154518));
#71058=CARTESIAN_POINT('Ctrl Pts',(6.61684896868505,4.48180278921155,128.778866401056));
#71059=CARTESIAN_POINT('Ctrl Pts',(6.60910269260094,4.42530763406361,128.65385980175));
#71060=CARTESIAN_POINT('Ctrl Pts',(6.6013564165168,4.36356406011884,128.531186719527));
#71061=CARTESIAN_POINT('Ctrl Pts',(6.5936101404327,4.29680023222776,128.411310090137));
#71062=CARTESIAN_POINT('Ctrl Pts',(6.58586380716735,4.23003591150127,128.291432575846));
#71063=CARTESIAN_POINT('Ctrl Pts',(6.57811747390196,4.15825145311134,128.174351897144));
#71064=CARTESIAN_POINT('Ctrl Pts',(6.57037114063661,4.0817205633461,128.060505609506));
#71065=CARTESIAN_POINT('Ctrl Pts',(6.56262307263363,4.00517253501872,127.94663382678));
#71066=CARTESIAN_POINT('Ctrl Pts',(6.55487500463068,3.92387617828241,127.835998200835));
#71067=CARTESIAN_POINT('Ctrl Pts',(6.54712693662771,3.83814779267064,127.729006234065));
#71068=CARTESIAN_POINT('Ctrl Pts',(6.53937063388585,3.75232829391047,127.62190055496));
#71069=CARTESIAN_POINT('Ctrl Pts',(6.53161433114397,3.66206760157558,127.518446576406));
#71070=CARTESIAN_POINT('Ctrl Pts',(6.52385802840212,3.56772184494956,127.419018109108));
#71071=CARTESIAN_POINT('Ctrl Pts',(6.51609758588795,3.47332573315253,127.319536573844));
#71072=CARTESIAN_POINT('Ctrl Pts',(6.50833714337374,3.37484049319558,127.224085102941));
#71073=CARTESIAN_POINT('Ctrl Pts',(6.50057670085957,3.27265745971043,127.132998988156));
#71074=CARTESIAN_POINT('Ctrl Pts',(6.49280380059412,3.17031039294841,127.041766653854));
#71075=CARTESIAN_POINT('Ctrl Pts',(6.48503090032871,3.06425397323944,126.954913927055));
#71076=CARTESIAN_POINT('Ctrl Pts',(6.47725800006327,2.954911506589,126.872734865955));
#71077=CARTESIAN_POINT('Ctrl Pts',(6.46976766430125,2.84954391401849,126.793543220723));
#71078=CARTESIAN_POINT('Ctrl Pts',(6.46227732853923,2.74112529228462,126.718691516558));
#71079=CARTESIAN_POINT('Ctrl Pts',(6.4547869927772,2.63005643606702,126.648402700839));
#71080=CARTESIAN_POINT('Ctrl Pts',(6.44701265865812,2.51477637040727,126.575448863309));
#71081=CARTESIAN_POINT('Ctrl Pts',(6.43923832453901,2.39627596322879,126.507179652453));
#71082=CARTESIAN_POINT('Ctrl Pts',(6.43146399041993,2.27497292682905,126.443892610036));
#71083=CARTESIAN_POINT('Ctrl Pts',(6.42369923747284,2.15381938558051,126.380683563242));
#71084=CARTESIAN_POINT('Ctrl Pts',(6.41593448452578,2.02987043081941,126.322444647072));
#71085=CARTESIAN_POINT('Ctrl Pts',(6.40816973157868,1.90357263312018,126.269430155813));
#71086=CARTESIAN_POINT('Ctrl Pts',(6.40041269069367,1.77740027617411,126.216468319294));
#71087=CARTESIAN_POINT('Ctrl Pts',(6.39265564980867,1.64888407703531,126.168720731739));
#71088=CARTESIAN_POINT('Ctrl Pts',(6.38489860892366,1.5184947700301,126.126395601035));
#71089=CARTESIAN_POINT('Ctrl Pts',(6.37714741768353,1.38820379061559,126.084102388041));
#71090=CARTESIAN_POINT('Ctrl Pts',(6.36939622644341,1.25604288524007,126.047223612979));
#71091=CARTESIAN_POINT('Ctrl Pts',(6.36164503520328,1.12250197908266,126.015919078876));
#71092=CARTESIAN_POINT('Ctrl Pts',(6.3538971384262,0.989017831372682,125.984627850034));
#71093=CARTESIAN_POINT('Ctrl Pts',(6.3461492416491,0.854155229307928,125.958906239035));
#71094=CARTESIAN_POINT('Ctrl Pts',(6.33840134487201,0.718418232359344,125.938863900281));
#71095=CARTESIAN_POINT('Ctrl Pts',(6.33065506878791,0.582709628664371,125.918825753952));
#71096=CARTESIAN_POINT('Ctrl Pts',(6.32290879270382,0.446127380419428,125.904464573982));
#71097=CARTESIAN_POINT('Ctrl Pts',(6.31516251661972,0.309184297259216,125.895838626902));
#71098=CARTESIAN_POINT('Ctrl Pts',(6.30741618335437,0.172240203216272,125.887212616148));
#71099=CARTESIAN_POINT('Ctrl Pts',(6.29966985008901,0.0349356591349389,
125.88432194734));
#71100=CARTESIAN_POINT('Ctrl Pts',(6.29192351682366,-0.102213262238794,
125.887172853048));
#71101=CARTESIAN_POINT('Ctrl Pts',(6.28417544882069,-0.239392897162357,
125.890024397197));
#71102=CARTESIAN_POINT('Ctrl Pts',(6.27642738081769,-0.376416449223656,
125.898620066303));
#71103=CARTESIAN_POINT('Ctrl Pts',(6.26867931281473,-0.512770107492321,
125.912914013609));
#71104=CARTESIAN_POINT('Ctrl Pts',(6.26092301007287,-0.649268684051809,
125.927223152692));
#71105=CARTESIAN_POINT('Ctrl Pts',(6.25316670733099,-0.78509555512517,125.947242627057));
#71106=CARTESIAN_POINT('Ctrl Pts',(6.24541040458914,-0.919743726602677,
125.972874868868));
#71107=CARTESIAN_POINT('Ctrl Pts',(6.23764996207496,-1.05446376386366,125.998520791378));
#71108=CARTESIAN_POINT('Ctrl Pts',(6.22988951956077,-1.18800346749367,126.029785361445));
#71109=CARTESIAN_POINT('Ctrl Pts',(6.22212907704659,-1.31986922111277,126.066520571547));
#71110=CARTESIAN_POINT('Ctrl Pts',(6.21435617678116,-1.4519466573459,126.10331475227));
#71111=CARTESIAN_POINT('Ctrl Pts',(6.20658327651567,-1.58234440162337,126.145597001514));
#71112=CARTESIAN_POINT('Ctrl Pts',(6.19881037625024,-1.71058624722145,126.193170125587));
#71113=CARTESIAN_POINT('Ctrl Pts',(6.19132004048827,-1.83416617870927,126.23901384677));
#71114=CARTESIAN_POINT('Ctrl Pts',(6.18382970472636,-1.95574395065215,126.289770329353));
#71115=CARTESIAN_POINT('Ctrl Pts',(6.17633936896439,-2.07491535179094,126.345222881927));
#71116=CARTESIAN_POINT('Ctrl Pts',(6.16856440379526,-2.19861521284597,126.402782606684));
#71117=CARTESIAN_POINT('Ctrl Pts',(6.16078943862611,-2.32011408055876,126.465584702731));
#71118=CARTESIAN_POINT('Ctrl Pts',(6.15301447345698,-2.43893572565106,126.533438517054));
#71119=CARTESIAN_POINT('Ctrl Pts',(6.14524923154099,-2.55760877420193,126.601207474429));
#71120=CARTESIAN_POINT('Ctrl Pts',(6.13748398962503,-2.67361092591063,126.674015386999));
#71121=CARTESIAN_POINT('Ctrl Pts',(6.12971874770903,-2.78648676993388,126.75162394422));
#71122=CARTESIAN_POINT('Ctrl Pts',(6.1219613593278,-2.89924845468501,126.829154010454));
#71123=CARTESIAN_POINT('Ctrl Pts',(6.1142039709465,-3.0088898043473,126.911474838259));
#71124=CARTESIAN_POINT('Ctrl Pts',(6.10644658256527,-3.1149811510953,126.998302881427));
#71125=CARTESIAN_POINT('Ctrl Pts',(6.09869563737146,-3.22098437972965,127.085058806335));
#71126=CARTESIAN_POINT('Ctrl Pts',(6.09094469217766,-3.32344317566096,127.176314245219));
#71127=CARTESIAN_POINT('Ctrl Pts',(6.08319374698385,-3.42195831907986,127.271743411445));
#71128=CARTESIAN_POINT('Ctrl Pts',(6.0754463027881,-3.52042896452899,127.367129473597));
#71129=CARTESIAN_POINT('Ctrl Pts',(6.06769885859239,-3.61495922139504,127.46668524084));
#71130=CARTESIAN_POINT('Ctrl Pts',(6.05995141439664,-3.70518444641721,127.570045963651));
#71131=CARTESIAN_POINT('Ctrl Pts',(6.05220579184048,-3.79538845697965,127.673382383482));
#71132=CARTESIAN_POINT('Ctrl Pts',(6.04446016928433,-3.88128919358331,127.780521683941));
#71133=CARTESIAN_POINT('Ctrl Pts',(6.03671454672818,-3.96256053364781,127.891064017548));
#71134=CARTESIAN_POINT('Ctrl Pts',(6.02896906803743,-4.04383036419728,128.001604297968));
#71135=CARTESIAN_POINT('Ctrl Pts',(6.02122358934664,-4.1204707390474,128.115547170041));
#71136=CARTESIAN_POINT('Ctrl Pts',(6.01347811065588,-4.19219755690558,128.232461959692));
#71137=CARTESIAN_POINT('Ctrl Pts',(6.00572792410674,-4.26396797177231,128.349447812514));
#71138=CARTESIAN_POINT('Ctrl Pts',(5.99797773755759,-4.33081865864229,128.469408858115));
#71139=CARTESIAN_POINT('Ctrl Pts',(5.99022755100845,-4.39251026806489,128.591887655597));
#71140=CARTESIAN_POINT('Ctrl Pts',(5.98247481362753,-4.45422218214933,128.714406764728));
#71141=CARTESIAN_POINT('Ctrl Pts',(5.97472207624662,-4.51077147100497,128.839444922287));
#71142=CARTESIAN_POINT('Ctrl Pts',(5.96696933886571,-4.56196644051339,128.966523503421));
#71143=CARTESIAN_POINT('Ctrl Pts',(5.95920832544955,-4.61321606057314,129.093737740745));
#71144=CARTESIAN_POINT('Ctrl Pts',(5.95144731203336,-4.65909981135122,129.222996384858));
#71145=CARTESIAN_POINT('Ctrl Pts',(5.94368629861719,-4.69947536023651,129.353804034378));
#71146=CARTESIAN_POINT('Ctrl Pts',(5.93919240193076,-4.72285420725288,129.429546212779));
#71147=CARTESIAN_POINT('Ctrl Pts',(5.93469850524435,-4.74438719609991,129.505807489811));
#71148=CARTESIAN_POINT('Ctrl Pts',(5.93020460855791,-4.76405452823401,129.582490119308));
#71149=CARTESIAN_POINT('Origin',(213.235140564004,0.,130.804360617566));
#71150=CARTESIAN_POINT('',(3.83484270885905,-4.76405452823401,129.582490119308));
#71151=CARTESIAN_POINT('',(4.17986374616532,-4.76405452823409,129.582490119308));
#71152=CARTESIAN_POINT('',(213.235140564004,-4.76405452823405,129.582490119308));
#71153=CARTESIAN_POINT('',(5.51485943602369,-4.91824978603851,130.802909882532));
#71154=CARTESIAN_POINT('Ctrl Pts',(5.51485943599135,-4.91824978603868,130.802909883106));
#71155=CARTESIAN_POINT('Ctrl Pts',(5.50690415626822,-4.91829144117287,130.944128252468));
#71156=CARTESIAN_POINT('Ctrl Pts',(5.49894887654507,-4.91224651275032,131.085289402386));
#71157=CARTESIAN_POINT('Ctrl Pts',(5.49099359682194,-4.90015601623778,131.225850924725));
#71158=CARTESIAN_POINT('Ctrl Pts',(5.4830330612392,-4.8880575318286,131.366505312638));
#71159=CARTESIAN_POINT('Ctrl Pts',(5.47507252565646,-4.8699055484061,131.506558924337));
#71160=CARTESIAN_POINT('Ctrl Pts',(5.46711199007373,-4.84579276826709,131.645476251418));
#71161=CARTESIAN_POINT('Ctrl Pts',(5.45914490500839,-4.82166014948372,131.784507871891));
#71162=CARTESIAN_POINT('Ctrl Pts',(5.45117781994306,-4.79155701944537,131.922400989644));
#71163=CARTESIAN_POINT('Ctrl Pts',(5.44321073487771,-4.75562679829129,132.058632046673));
#71164=CARTESIAN_POINT('Ctrl Pts',(5.43523004692704,-4.71963523039948,132.19509570263));
#71165=CARTESIAN_POINT('Ctrl Pts',(5.42724935897631,-4.67779678537567,132.329891279319));
#71166=CARTESIAN_POINT('Ctrl Pts',(5.41926867102563,-4.63030456398885,132.462511004957));
#71167=CARTESIAN_POINT('Ctrl Pts',(5.41128035769744,-4.58276696479505,132.59525744592));
#71168=CARTESIAN_POINT('Ctrl Pts',(5.4032920443693,-4.52956495186786,132.725823557045));
#71169=CARTESIAN_POINT('Ctrl Pts',(5.39530373104111,-4.47093890415826,132.853723537545));
#71170=CARTESIAN_POINT('Ctrl Pts',(5.38730082587285,-4.41220576727016,132.981857146344));
#71171=CARTESIAN_POINT('Ctrl Pts',(5.37929792070464,-4.3480289622186,133.107314573205));
#71172=CARTESIAN_POINT('Ctrl Pts',(5.37129501553639,-4.2786942712433,133.229635528938));
#71173=CARTESIAN_POINT('Ctrl Pts',(5.36772517491932,-4.2477662781193,133.28419900394));
#71174=CARTESIAN_POINT('Ctrl Pts',(5.36415533430224,-4.21581255218363,133.338138795468));
#71175=CARTESIAN_POINT('Ctrl Pts',(5.36058549368516,-4.18286110904065,133.391416087589));
#71176=CARTESIAN_POINT('Ctrl Pts',(5.35281115956605,-4.1111000540864,133.507442407623));
#71177=CARTESIAN_POINT('Ctrl Pts',(5.34503682544701,-4.03439408092906,133.62066442551));
#71178=CARTESIAN_POINT('Ctrl Pts',(5.33726249132792,-3.95298869328417,133.730631871785));
#71179=CARTESIAN_POINT('Ctrl Pts',(5.32949773838082,-3.87168363050414,133.84046379301));
#71180=CARTESIAN_POINT('Ctrl Pts',(5.32173298543377,-3.78569090719519,133.947048812037));
#71181=CARTESIAN_POINT('Ctrl Pts',(5.31396823248667,-3.69530089402499,134.049962929174));
#71182=CARTESIAN_POINT('Ctrl Pts',(5.30621119160166,-3.60500065749014,134.15277483056));
#71183=CARTESIAN_POINT('Ctrl Pts',(5.29845415071655,-3.5103120788495,134.251922793895));
#71184=CARTESIAN_POINT('Ctrl Pts',(5.29069710983154,-3.4115674156978,134.347013695508));
#71185=CARTESIAN_POINT('Ctrl Pts',(5.28294591859142,-3.31289721666484,134.442032888332));
#71186=CARTESIAN_POINT('Ctrl Pts',(5.27519472735137,-3.21017730180296,134.533000839009));
#71187=CARTESIAN_POINT('Ctrl Pts',(5.26744353611124,-3.10377835763593,134.619559559846));
#71188=CARTESIAN_POINT('Ctrl Pts',(5.25969563933416,-2.9974246358583,134.706081490917));
#71189=CARTESIAN_POINT('Ctrl Pts',(5.25194774255703,-2.88739529747263,134.788197673259));
#71190=CARTESIAN_POINT('Ctrl Pts',(5.24419984577995,-2.77409567333946,134.865589034887));
#71191=CARTESIAN_POINT('Ctrl Pts',(5.23645356969584,-2.6608197490452,134.942964207911));
#71192=CARTESIAN_POINT('Ctrl Pts',(5.22870729361176,-2.54427522229636,135.015616305683));
#71193=CARTESIAN_POINT('Ctrl Pts',(5.22096101752766,-2.42489776846515,135.083268641232));
#71194=CARTESIAN_POINT('Ctrl Pts',(5.21321468426229,-2.30551943341654,135.150921476175));
#71195=CARTESIAN_POINT('Ctrl Pts',(5.2054683509969,-2.18330846969928,135.213574282488));
#71196=CARTESIAN_POINT('Ctrl Pts',(5.19772201773154,-2.0587262453815,135.270995739117));
#71197=CARTESIAN_POINT('Ctrl Pts',(5.18997394972856,-1.93411612173872,135.328430054884));
#71198=CARTESIAN_POINT('Ctrl Pts',(5.1822258817256,-1.80713403580959,135.380630526146));
#71199=CARTESIAN_POINT('Ctrl Pts',(5.17447781372263,-1.67826209974133,135.427413655016));
#71200=CARTESIAN_POINT('Ctrl Pts',(5.16672151098077,-1.54925319704565,135.474246505552));
#71201=CARTESIAN_POINT('Ctrl Pts',(5.15896520823893,-1.41835079999062,135.515650378615));
#71202=CARTESIAN_POINT('Ctrl Pts',(5.15120890549707,-1.2860535118888,135.551491269556));
#71203=CARTESIAN_POINT('Ctrl Pts',(5.14344846298289,-1.15368561274076,135.587351289858));
#71204=CARTESIAN_POINT('Ctrl Pts',(5.1356880204687,-1.01992172019991,135.617642325487));
#71205=CARTESIAN_POINT('Ctrl Pts',(5.12792757795452,-0.885270468202647,
135.64228158226));
#71206=CARTESIAN_POINT('Ctrl Pts',(5.12015467768909,-0.750403062062084,
135.666960392156));
#71207=CARTESIAN_POINT('Ctrl Pts',(5.11238177742363,-0.614645837334676,
135.685969238732));
#71208=CARTESIAN_POINT('Ctrl Pts',(5.1046088771582,-0.478513284494333,135.699277174471));
#71209=CARTESIAN_POINT('Ctrl Pts',(5.09711854139623,-0.347329492848052,
135.712101333225));
#71210=CARTESIAN_POINT('Ctrl Pts',(5.08962820563424,-0.215797495084421,
135.719631852407));
#71211=CARTESIAN_POINT('Ctrl Pts',(5.08213786987227,-0.084375565351097,
135.721886807275));
#71212=CARTESIAN_POINT('Ctrl Pts',(5.07436353575318,0.0520292667940507,
135.724227259442));
#71213=CARTESIAN_POINT('Ctrl Pts',(5.06658920163414,0.188747609195711,135.720891618068));
#71214=CARTESIAN_POINT('Ctrl Pts',(5.05881486751505,0.325267936645508,135.711843050738));
#71215=CARTESIAN_POINT('Ctrl Pts',(5.05105011456797,0.461620014992709,135.702805634958));
#71216=CARTESIAN_POINT('Ctrl Pts',(5.0432853616209,0.597774177582164,135.688069327666));
#71217=CARTESIAN_POINT('Ctrl Pts',(5.03552060867381,0.73321674902639,135.667649243737));
#71218=CARTESIAN_POINT('Ctrl Pts',(5.02776356778882,0.868524796999067,135.647249441324));
#71219=CARTESIAN_POINT('Ctrl Pts',(5.02000652690377,1.00312227622098,135.6211771544));
#71220=CARTESIAN_POINT('Ctrl Pts',(5.01224948601879,1.13649884726764,135.589499427743));
#71221=CARTESIAN_POINT('Ctrl Pts',(5.00449829477867,1.26977483800474,135.557845589505));
#71222=CARTESIAN_POINT('Ctrl Pts',(4.99674710353862,1.40183137431215,135.52059481531));
#71223=CARTESIAN_POINT('Ctrl Pts',(4.98899591229849,1.53216690588338,135.477865473134));
#71224=CARTESIAN_POINT('Ctrl Pts',(4.98124801552141,1.66244704137687,135.435154292068));
#71225=CARTESIAN_POINT('Ctrl Pts',(4.97350011874427,1.79100725624612,135.386969295847));
#71226=CARTESIAN_POINT('Ctrl Pts',(4.96575222196719,1.91736001496204,135.333479034601));
#71227=CARTESIAN_POINT('Ctrl Pts',(4.95800594588309,2.04368634340485,135.279999962364));
#71228=CARTESIAN_POINT('Ctrl Pts',(4.95025966979898,2.16780577434087,135.22121798477));
#71229=CARTESIAN_POINT('Ctrl Pts',(4.94251339371488,2.28925003000418,135.157350091781));
#71230=CARTESIAN_POINT('Ctrl Pts',(4.93476706044952,2.4106951821414,135.093481727334));
#71231=CARTESIAN_POINT('Ctrl Pts',(4.9270207271842,2.52946477357003,135.024527554556));
#71232=CARTESIAN_POINT('Ctrl Pts',(4.91927439391884,2.64511480662607,134.950750700791));
#71233=CARTESIAN_POINT('Ctrl Pts',(4.91152632591586,2.76079073870515,134.876957325211));
#71234=CARTESIAN_POINT('Ctrl Pts',(4.90377825791289,2.87334539272677,134.798339329784));
#71235=CARTESIAN_POINT('Ctrl Pts',(4.89603018990991,2.98236379332925,134.715203144022));
#71236=CARTESIAN_POINT('Ctrl Pts',(4.88827388716806,3.09149805998509,134.631978600133));
#71237=CARTESIAN_POINT('Ctrl Pts',(4.88051758442617,3.19708825408913,134.544226510879));
#71238=CARTESIAN_POINT('Ctrl Pts',(4.87276128168432,3.29875212646374,134.452293932561));
#71239=CARTESIAN_POINT('Ctrl Pts',(4.86500083917015,3.40047025990822,134.360312287058));
#71240=CARTESIAN_POINT('Ctrl Pts',(4.85724039665602,3.49825761735194,134.26414598053));
#71241=CARTESIAN_POINT('Ctrl Pts',(4.84947995414186,3.59176961263977,134.164178188836));
#71242=CARTESIAN_POINT('Ctrl Pts',(4.84170705387644,3.68543172168391,134.064049919969));
#71243=CARTESIAN_POINT('Ctrl Pts',(4.83393415361098,3.77480449868644,133.960108267853));
#71244=CARTESIAN_POINT('Ctrl Pts',(4.82616125334556,3.85958381195648,133.852769360006));
#71245=CARTESIAN_POINT('Ctrl Pts',(4.81867091758351,3.94128118364331,133.749332491829));
#71246=CARTESIAN_POINT('Ctrl Pts',(4.81118058182146,4.01871308034606,133.64274132649));
#71247=CARTESIAN_POINT('Ctrl Pts',(4.8036902460594,4.09164700092106,133.533391193128));
#71248=CARTESIAN_POINT('Ctrl Pts',(4.79591591194033,4.16734623326212,133.419895016224));
#71249=CARTESIAN_POINT('Ctrl Pts',(4.78814157782123,4.23843946730323,133.303067007057));
#71250=CARTESIAN_POINT('Ctrl Pts',(4.78036724370216,4.30461922302025,133.183317617452));
#71251=CARTESIAN_POINT('Ctrl Pts',(4.77260249075509,4.37071741810292,133.063715808266));
#71252=CARTESIAN_POINT('Ctrl Pts',(4.76483773780799,4.43191399605386,132.941200121148));
#71253=CARTESIAN_POINT('Ctrl Pts',(4.75707298486091,4.4879440193524,132.816210895708));
#71254=CARTESIAN_POINT('Ctrl Pts',(4.74931594397591,4.54391839284207,132.691345811328));
#71255=CARTESIAN_POINT('Ctrl Pts',(4.7415589030909,4.59473626469316,132.564012432126));
#71256=CARTESIAN_POINT('Ctrl Pts',(4.73380186220589,4.64017819065105,132.434676360453));
#71257=CARTESIAN_POINT('Ctrl Pts',(4.72605067096575,4.68558584849916,132.305437822118));
#71258=CARTESIAN_POINT('Ctrl Pts',(4.71829947972566,4.72562550070614,132.174199964734));
#71259=CARTESIAN_POINT('Ctrl Pts',(4.71054828848551,4.76012563341238,132.04144873756));
#71260=CARTESIAN_POINT('Ctrl Pts',(4.70280039170845,4.79461110264175,131.9087539332));
#71261=CARTESIAN_POINT('Ctrl Pts',(4.69505249493136,4.82356163704551,131.774547415974));
#71262=CARTESIAN_POINT('Ctrl Pts',(4.6873045981543,4.84685551775979,131.639330468795));
#71263=CARTESIAN_POINT('Ctrl Pts',(4.67955832207022,4.87014452589638,131.504141806086));
#71264=CARTESIAN_POINT('Ctrl Pts',(4.67181204598612,4.88777916756064,131.367943518876));
#71265=CARTESIAN_POINT('Ctrl Pts',(4.66406576990204,4.89968888698319,131.231246870886));
#71266=CARTESIAN_POINT('Ctrl Pts',(4.65631943663671,4.91159869432056,131.094549213833));
#71267=CARTESIAN_POINT('Ctrl Pts',(4.64857310337144,4.91778346115495,130.957353578149));
#71268=CARTESIAN_POINT('Ctrl Pts',(4.64082677010612,4.91822457238921,130.820175738401));
#71269=CARTESIAN_POINT('Ctrl Pts',(4.63307870210316,4.91866578240726,130.682967178626));
#71270=CARTESIAN_POINT('Ctrl Pts',(4.62533063410015,4.91336077607595,130.545776813605));
#71271=CARTESIAN_POINT('Ctrl Pts',(4.61758256609718,4.90234305690388,130.409119406498));
#71272=CARTESIAN_POINT('Ctrl Pts',(4.60982626335533,4.89131362796874,130.272316758273));
#71273=CARTESIAN_POINT('Ctrl Pts',(4.60206996061352,4.8745593891082,130.136048589798));
#71274=CARTESIAN_POINT('Ctrl Pts',(4.59431365787168,4.85216571359989,130.00082409054));
#71275=CARTESIAN_POINT('Ctrl Pts',(4.58655321535754,4.82976008591273,129.865527417895));
#71276=CARTESIAN_POINT('Ctrl Pts',(4.57879277284337,4.8017091039469,129.731275906925));
#71277=CARTESIAN_POINT('Ctrl Pts',(4.57103233032922,4.76814888717111,129.598566583633));
#71278=CARTESIAN_POINT('Ctrl Pts',(4.56325943006379,4.73453479655596,129.465644223554));
#71279=CARTESIAN_POINT('Ctrl Pts',(4.55548652979832,4.69539390987147,129.334269373208));
#71280=CARTESIAN_POINT('Ctrl Pts',(4.54771362953289,4.65091193637605,129.204922834289));
#71281=CARTESIAN_POINT('Ctrl Pts',(4.54022329377076,4.60804699465992,129.080278367862));
#71282=CARTESIAN_POINT('Ctrl Pts',(4.53273295800869,4.56022265998851,128.95751759168));
#71283=CARTESIAN_POINT('Ctrl Pts',(4.52524262224657,4.50764586141486,128.837049800595));
#71284=CARTESIAN_POINT('Ctrl Pts',(4.51746828812748,4.45307559754362,128.712014436598));
#71285=CARTESIAN_POINT('Ctrl Pts',(4.50969395400838,4.39321251423806,128.589053292697));
#71286=CARTESIAN_POINT('Ctrl Pts',(4.50191961988929,4.32823573577927,128.46864691978));
#71287=CARTESIAN_POINT('Ctrl Pts',(4.4941548669422,4.26333903539278,128.348388936958));
#71288=CARTESIAN_POINT('Ctrl Pts',(4.48639011399515,4.1933413631873,128.230679801251));
#71289=CARTESIAN_POINT('Ctrl Pts',(4.47862536104805,4.11846998414756,128.115980426415));
#71290=CARTESIAN_POINT('Ctrl Pts',(4.47086832016304,4.04367296841699,128.001394972614));
#71291=CARTESIAN_POINT('Ctrl Pts',(4.46311127927798,3.96401209125675,127.88981365604));
#71292=CARTESIAN_POINT('Ctrl Pts',(4.45535423839297,3.87976046213168,127.781672770801));
#71293=CARTESIAN_POINT('Ctrl Pts',(4.44760304715284,3.79557236781552,127.673613435445));
#71294=CARTESIAN_POINT('Ctrl Pts',(4.43985185591273,3.70680065158938,127.568989674482));
#71295=CARTESIAN_POINT('Ctrl Pts',(4.43210066467259,3.61376144889855,127.468208454826));
#71296=CARTESIAN_POINT('Ctrl Pts',(4.4243527678955,3.52076179035076,127.367470069876));
#71297=CARTESIAN_POINT('Ctrl Pts',(4.41660487111835,3.4234985174841,127.270571264624));
#71298=CARTESIAN_POINT('Ctrl Pts',(4.40885697434126,3.32232758178954,127.177885400254));
#71299=CARTESIAN_POINT('Ctrl Pts',(4.40111069825715,3.22117780887359,127.085218923768));
#71300=CARTESIAN_POINT('Ctrl Pts',(4.39336442217312,3.11612228707666,126.996763899231));
#71301=CARTESIAN_POINT('Ctrl Pts',(4.385618146089,3.00755301993109,126.91285603774));
#71302=CARTESIAN_POINT('Ctrl Pts',(4.37787181282366,2.89898295135216,126.828947556861));
#71303=CARTESIAN_POINT('Ctrl Pts',(4.37012547955831,2.78689939501427,126.749586545085));
#71304=CARTESIAN_POINT('Ctrl Pts',(4.36237914629297,2.67172622475201,126.675067452571));
#71305=CARTESIAN_POINT('Ctrl Pts',(4.35463107829,2.55652726225698,126.600531672024));
#71306=CARTESIAN_POINT('Ctrl Pts',(4.346883010287,2.43823763722746,126.530840180741));
#71307=CARTESIAN_POINT('Ctrl Pts',(4.33913494228403,2.31730854395466,126.466243033335));
#71308=CARTESIAN_POINT('Ctrl Pts',(4.33137863954217,2.19625092580212,126.401577231312));
#71309=CARTESIAN_POINT('Ctrl Pts',(4.32362233680031,2.07254858099949,126.342016773374));
#71310=CARTESIAN_POINT('Ctrl Pts',(4.31586603405844,1.94667605140826,126.28776506191));
#71311=CARTESIAN_POINT('Ctrl Pts',(4.30810559154425,1.82073633985768,126.233484394674));
#71312=CARTESIAN_POINT('Ctrl Pts',(4.30034514903001,1.6926245005417,126.184518259292));
#71313=CARTESIAN_POINT('Ctrl Pts',(4.29258470651581,1.56283227141091,126.141020789295));
#71314=CARTESIAN_POINT('Ctrl Pts',(4.28481180625037,1.43283168827187,126.097453493298));
#71315=CARTESIAN_POINT('Ctrl Pts',(4.27703890598492,1.30114570062448,126.059372514173));
#71316=CARTESIAN_POINT('Ctrl Pts',(4.26926600571949,1.16827920094035,126.026881494519));
#71317=CARTESIAN_POINT('Ctrl Pts',(4.26177566995752,1.04024273319134,125.99557160527));
#71318=CARTESIAN_POINT('Ctrl Pts',(4.25428533419559,0.911110394362069,125.96945237436));
#71319=CARTESIAN_POINT('Ctrl Pts',(4.24679499843361,0.781338386011577,125.948570940382));
#71320=CARTESIAN_POINT('Ctrl Pts',(4.23902066431451,0.646646032519807,125.926897780488));
#71321=CARTESIAN_POINT('Ctrl Pts',(4.23124633019544,0.510837880950911,125.910798786112));
#71322=CARTESIAN_POINT('Ctrl Pts',(4.22347199607634,0.374415053427558,125.900383004417));
#71323=CARTESIAN_POINT('Ctrl Pts',(4.21570724312925,0.238160354847039,125.889980059242));
#71324=CARTESIAN_POINT('Ctrl Pts',(4.20794249018212,0.101292873665626,125.88524642025));
#71325=CARTESIAN_POINT('Ctrl Pts',(4.20017773723504,-0.035676768045025,
125.886240018117));
#71326=CARTESIAN_POINT('Ctrl Pts',(4.19242069635003,-0.172510369576782,
125.887232629129));
#71327=CARTESIAN_POINT('Ctrl Pts',(4.18466365546503,-0.309445541288254,
125.893941154063));
#71328=CARTESIAN_POINT('Ctrl Pts',(4.17690661458002,-0.445967594251223,
125.906371645817));
#71329=CARTESIAN_POINT('Ctrl Pts',(4.16915542333994,-0.582386694871138,
125.91879276364));
#71330=CARTESIAN_POINT('Ctrl Pts',(4.16140423209989,-0.718392909057021,
125.936927224268));
#71331=CARTESIAN_POINT('Ctrl Pts',(4.15365304085981,-0.85347296508882,125.960729029557));
#71332=CARTESIAN_POINT('Ctrl Pts',(4.14590514408274,-0.988495608493979,
125.984520718443));
#71333=CARTESIAN_POINT('Ctrl Pts',(4.1381572473056,-1.12259249244134,126.01397489342));
#71334=CARTESIAN_POINT('Ctrl Pts',(4.13040935052854,-1.25525709711611,126.04899389326));
#71335=CARTESIAN_POINT('Ctrl Pts',(4.12266307444444,-1.38789395121568,126.084005567879));
#71336=CARTESIAN_POINT('Ctrl Pts',(4.1149167983604,-1.51909874418968,126.124579652297));
#71337=CARTESIAN_POINT('Ctrl Pts',(4.10717052227631,-1.6483771452998,126.170567802889));
#71338=CARTESIAN_POINT('Ctrl Pts',(4.09942418901096,-1.77765650071371,126.216556292954));
#71339=CARTESIAN_POINT('Ctrl Pts',(4.09167785574562,-1.90500906753548,126.267958797907));
#71340=CARTESIAN_POINT('Ctrl Pts',(4.08393152248027,-2.02995800234534,126.324577858189));
#71341=CARTESIAN_POINT('Ctrl Pts',(4.07618345447731,-2.15493491860266,126.381209597916));
#71342=CARTESIAN_POINT('Ctrl Pts',(4.0684353864743,-2.27750677569764,126.443060056242));
#71343=CARTESIAN_POINT('Ctrl Pts',(4.06068731847134,-2.39721931406806,126.509884791256));
#71344=CARTESIAN_POINT('Ctrl Pts',(4.05293101572949,-2.51705908434902,126.576780548394));
#71345=CARTESIAN_POINT('Ctrl Pts',(4.04517471298766,-2.6340331234154,126.648660952148));
#71346=CARTESIAN_POINT('Ctrl Pts',(4.03741841024581,-2.74771380160992,126.72523670097));
#71347=CARTESIAN_POINT('Ctrl Pts',(4.02965796773162,-2.86145515460555,126.801853320575));
#71348=CARTESIAN_POINT('Ctrl Pts',(4.02189752521747,-2.97189932955123,126.883170047069));
#71349=CARTESIAN_POINT('Ctrl Pts',(4.01413708270329,-3.0786508531683,126.968856480326));
#71350=CARTESIAN_POINT('Ctrl Pts',(4.00636418243785,-3.18557374380789,127.054680465052));
#71351=CARTESIAN_POINT('Ctrl Pts',(3.99859128217245,-3.28879184298823,127.144887916603));
#71352=CARTESIAN_POINT('Ctrl Pts',(3.99081838190702,-3.38794504654056,127.239110076002));
#71353=CARTESIAN_POINT('Ctrl Pts',(3.98332804614494,-3.48349378139259,127.329907022576));
#71354=CARTESIAN_POINT('Ctrl Pts',(3.9758377103828,-3.5752678134635,127.424431634148));
#71355=CARTESIAN_POINT('Ctrl Pts',(3.96834737462072,-3.66298089563425,127.522325574987));
#71356=CARTESIAN_POINT('Ctrl Pts',(3.96064863976751,-3.75313436595113,127.622943159858));
#71357=CARTESIAN_POINT('Ctrl Pts',(3.95294990491429,-3.83929639987039,127.727454027614));
#71358=CARTESIAN_POINT('Ctrl Pts',(3.94525117006108,-3.92110685231847,127.835504926361));
#71359=CARTESIAN_POINT('Ctrl Pts',(3.9375616666992,-4.00281920650799,127.94342626214));
#71360=CARTESIAN_POINT('Ctrl Pts',(3.92987216333736,-4.08019011675992,128.054878873016));
#71361=CARTESIAN_POINT('Ctrl Pts',(3.92218265997548,-4.15289689457832,128.169473438672));
#71362=CARTESIAN_POINT('Ctrl Pts',(3.91450192989967,-4.22552071809771,128.283937258444));
#71363=CARTESIAN_POINT('Ctrl Pts',(3.90682119982385,-4.29349078972434,128.401535562331));
#71364=CARTESIAN_POINT('Ctrl Pts',(3.89914046974803,-4.35652573860561,128.521847408104));
#71365=CARTESIAN_POINT('Ctrl Pts',(3.89146486455688,-4.41951862809418,128.642078977091));
#71366=CARTESIAN_POINT('Ctrl Pts',(3.88378925936576,-4.47758275848176,128.765020135462));
#71367=CARTESIAN_POINT('Ctrl Pts',(3.87611365417462,-4.53048108308191,128.890222634468));
#71368=CARTESIAN_POINT('Ctrl Pts',(3.86844103308747,-4.58335884199401,129.015376457538));
#71369=CARTESIAN_POINT('Ctrl Pts',(3.86076841200032,-4.63107463184753,129.142789506805));
#71370=CARTESIAN_POINT('Ctrl Pts',(3.85309579091319,-4.6734384223704,129.271991088108));
#71371=CARTESIAN_POINT('Ctrl Pts',(3.84701143022851,-4.70703275455286,129.374447473319));
#71372=CARTESIAN_POINT('Ctrl Pts',(3.84092706954373,-4.73726240782115,129.478028048446));
#71373=CARTESIAN_POINT('Ctrl Pts',(3.83484270885904,-4.76405452823401,129.582490119308));
#71374=CARTESIAN_POINT('Ctrl Pts',(5.58457496064636,-4.76405452823403,129.582490119308));
#71375=CARTESIAN_POINT('Ctrl Pts',(5.57621930409528,-4.80065751242433,129.725204599138));
#71376=CARTESIAN_POINT('Ctrl Pts',(5.56786364754414,-4.83088577288846,129.869729750966));
#71377=CARTESIAN_POINT('Ctrl Pts',(5.55950799099307,-4.85457280706801,130.015496926314));
#71378=CARTESIAN_POINT('Ctrl Pts',(5.55117837062054,-4.87818603258305,130.160809891968));
#71379=CARTESIAN_POINT('Ctrl Pts',(5.542848750248,-4.89529863039668,130.307356877737));
#71380=CARTESIAN_POINT('Ctrl Pts',(5.53451912987546,-4.90579465410995,130.454557995783));
#71381=CARTESIAN_POINT('Ctrl Pts',(5.52796589859152,-4.9140522778525,130.570366751605));
#71382=CARTESIAN_POINT('Ctrl Pts',(5.52141266730759,-4.91821547224366,130.686580015051));
#71383=CARTESIAN_POINT('Ctrl Pts',(5.51485943602364,-4.91824978603851,130.802909882533));
#71384=CARTESIAN_POINT('',(5.86014056397397,-4.91824871042674,130.800799032843));
#71385=CARTESIAN_POINT('Ctrl Pts',(5.93020460855791,-4.76405452823401,129.582490119308));
#71386=CARTESIAN_POINT('Ctrl Pts',(5.92242989152009,-4.79808021972201,129.715155774008));
#71387=CARTESIAN_POINT('Ctrl Pts',(5.9146551744823,-4.82651889400264,129.849082692573));
#71388=CARTESIAN_POINT('Ctrl Pts',(5.90688045744446,-4.84930906415737,129.983760433078));
#71389=CARTESIAN_POINT('Ctrl Pts',(5.90388422001347,-4.85809198970231,130.035662834833));
#71390=CARTESIAN_POINT('Ctrl Pts',(5.90088798258247,-4.86603655196502,130.08767671438));
#71391=CARTESIAN_POINT('Ctrl Pts',(5.8978917451515,-4.87314129660454,130.139772801076));
#71392=CARTESIAN_POINT('Ctrl Pts',(5.88530801810389,-4.9029801092307,130.358568190401));
#71393=CARTESIAN_POINT('Ctrl Pts',(5.87272429105628,-4.91808839522474,130.579417271214));
#71394=CARTESIAN_POINT('Ctrl Pts',(5.8601405640087,-4.91824871042629,130.800799032232));
#71395=CARTESIAN_POINT('Ctrl Pts',(5.86014056397391,-4.91824871042674,130.800799032843));
#71396=CARTESIAN_POINT('Ctrl Pts',(5.85248570547013,-4.91834623240639,130.935468677974));
#71397=CARTESIAN_POINT('Ctrl Pts',(5.84483084696644,-4.91290838515486,131.070351857313));
#71398=CARTESIAN_POINT('Ctrl Pts',(5.83717598846266,-4.90190910706921,131.204947897109));
#71399=CARTESIAN_POINT('Ctrl Pts',(5.82952906258834,-4.89092122739117,131.339404456795));
#71400=CARTESIAN_POINT('Ctrl Pts',(5.82188213671392,-4.8743834115758,131.47357406995));
#71401=CARTESIAN_POINT('Ctrl Pts',(5.8142352108396,-4.85232162339504,131.606955113954));
#71402=CARTESIAN_POINT('Ctrl Pts',(5.806594256031,-4.83027706205674,131.740232008004));
#71403=CARTESIAN_POINT('Ctrl Pts',(5.79895330122243,-4.80271717437201,131.872721161818));
#71404=CARTESIAN_POINT('Ctrl Pts',(5.79131234641383,-4.76971978040956,132.003925654932));
#71405=CARTESIAN_POINT('Ctrl Pts',(5.78367476668045,-4.73673696167879,132.135072193896));
#71406=CARTESIAN_POINT('Ctrl Pts',(5.77603718694707,-4.69832150930007,132.264934809998));
#71407=CARTESIAN_POINT('Ctrl Pts',(5.76839960721369,-4.6546023401456,132.393026761729));
#71408=CARTESIAN_POINT('Ctrl Pts',(5.76076358446485,-4.61089208350954,132.521092600845));
#71409=CARTESIAN_POINT('Ctrl Pts',(5.75312756171603,-4.5618803897466,132.647388111796));
#71410=CARTESIAN_POINT('Ctrl Pts',(5.74549153896717,-4.5077458825195,132.771442243002));
#71411=CARTESIAN_POINT('Ctrl Pts',(5.7378553085799,-4.45360990326912,132.895499747483));
#71412=CARTESIAN_POINT('Ctrl Pts',(5.73021907819258,-4.39435099511473,133.01731538155));
#71413=CARTESIAN_POINT('Ctrl Pts',(5.72258284780531,-4.33019548578804,133.136439114821));
#71414=CARTESIAN_POINT('Ctrl Pts',(5.71494464519093,-4.26602340686762,133.255593614458));
#71415=CARTESIAN_POINT('Ctrl Pts',(5.70730644257658,-4.19695240360804,133.372054476202));
#71416=CARTESIAN_POINT('Ctrl Pts',(5.69966823996219,-4.12325391951159,133.485397763473));
#71417=CARTESIAN_POINT('Ctrl Pts',(5.6920220253493,-4.04947813029839,133.598859940788));
#71418=CARTESIAN_POINT('Ctrl Pts',(5.68437581073642,-3.97106539061897,133.7091976774));
#71419=CARTESIAN_POINT('Ctrl Pts',(5.67672959612352,-3.88832965658374,133.81601722884));
#71420=CARTESIAN_POINT('Ctrl Pts',(5.66907886296699,-3.80554502972464,133.922899905477));
#71421=CARTESIAN_POINT('Ctrl Pts',(5.66142812981041,-3.71843258245316,134.026259950901));
#71422=CARTESIAN_POINT('Ctrl Pts',(5.65377739665388,-3.62734453879843,134.125739045169));
#71423=CARTESIAN_POINT('Ctrl Pts',(5.64611553015503,-3.53612394387705,134.225362901356));
#71424=CARTESIAN_POINT('Ctrl Pts',(5.63845366365625,-3.44091648774859,134.321094248362));
#71425=CARTESIAN_POINT('Ctrl Pts',(5.6307917971574,-3.34210924864982,134.412613495704));
#71426=CARTESIAN_POINT('Ctrl Pts',(5.62700923855114,-3.293329467291,134.457795295298));
#71427=CARTESIAN_POINT('Ctrl Pts',(5.62322667994486,-3.24367280657356,134.501951138766));
#71428=CARTESIAN_POINT('Ctrl Pts',(5.6194441213386,-3.19318845602654,134.54504645666));
#71429=CARTESIAN_POINT('Ctrl Pts',(5.61166978721953,-3.08942741758886,134.633620735382));
#71430=CARTESIAN_POINT('Ctrl Pts',(5.60389545310043,-2.98181385883301,134.71801477323));
#71431=CARTESIAN_POINT('Ctrl Pts',(5.59612111898136,-2.87071904261656,134.797874764387));
#71432=CARTESIAN_POINT('Ctrl Pts',(5.58835636603427,-2.75976114083226,134.877636335242));
#71433=CARTESIAN_POINT('Ctrl Pts',(5.58059161308717,-2.64533083249046,134.952874751465));
#71434=CARTESIAN_POINT('Ctrl Pts',(5.57282686014008,-2.52783408368228,135.023274921966));
#71435=CARTESIAN_POINT('Ctrl Pts',(5.56506981925508,-2.41045403430128,135.093605170026));
#71436=CARTESIAN_POINT('Ctrl Pts',(5.55731277837004,-2.29001393860172,135.159106535709));
#71437=CARTESIAN_POINT('Ctrl Pts',(5.54955573748504,-2.16695022174466,135.219506119017));
#71438=CARTESIAN_POINT('Ctrl Pts',(5.54180454624488,-2.04397930819344,135.279860154529));
#71439=CARTESIAN_POINT('Ctrl Pts',(5.53405335500481,-1.91838906110722,135.335119893912));
#71440=CARTESIAN_POINT('Ctrl Pts',(5.52630216376465,-1.79064177114034,135.385057628933));
#71441=CARTESIAN_POINT('Ctrl Pts',(5.51855426698758,-1.66294877717999,135.434974139084));
#71442=CARTESIAN_POINT('Ctrl Pts',(5.5108063702105,-1.53310092715568,135.479573001762));
#71443=CARTESIAN_POINT('Ctrl Pts',(5.50305847343341,-1.40158161927083,135.518674144159));
#71444=CARTESIAN_POINT('Ctrl Pts',(5.49531219734931,-1.27008982238996,135.557767107441));
#71445=CARTESIAN_POINT('Ctrl Pts',(5.48756592126517,-1.13692763760397,135.59136452652));
#71446=CARTESIAN_POINT('Ctrl Pts',(5.47981964518107,-1.00259441687707,135.619335954756));
#71447=CARTESIAN_POINT('Ctrl Pts',(5.47207331191571,-0.868260204532673,
135.647307589471));
#71448=CARTESIAN_POINT('Ctrl Pts',(5.46432697865039,-0.732755321753876,
135.669653070774));
#71449=CARTESIAN_POINT('Ctrl Pts',(5.45658064538503,-0.59658973442259,135.686292996377));
#71450=CARTESIAN_POINT('Ctrl Pts',(5.44883257738204,-0.460393653752126,
135.702936648376));
#71451=CARTESIAN_POINT('Ctrl Pts',(5.44108450937911,-0.323536962109448,
135.713872154746));
#71452=CARTESIAN_POINT('Ctrl Pts',(5.43333644137613,-0.186534776714436,
135.719071986464));
#71453=CARTESIAN_POINT('Ctrl Pts',(5.42558013863428,-0.0493869837666271,
135.724277344625));
#71454=CARTESIAN_POINT('Ctrl Pts',(5.41782383589241,0.0879062205216979,
135.72373483598));
#71455=CARTESIAN_POINT('Ctrl Pts',(5.41006753315057,0.224829127339722,135.717469096523));
#71456=CARTESIAN_POINT('Ctrl Pts',(5.40230709063641,0.361825114035785,135.711200012852));
#71457=CARTESIAN_POINT('Ctrl Pts',(5.39454664812223,0.498450020173607,135.699201645886));
#71458=CARTESIAN_POINT('Ctrl Pts',(5.38678620560808,0.634194221701444,135.681550459233));
#71459=CARTESIAN_POINT('Ctrl Pts',(5.37901330534265,0.770156331872563,135.663870937328));
#71460=CARTESIAN_POINT('Ctrl Pts',(5.37124040507721,0.905234526767185,135.640520528812));
#71461=CARTESIAN_POINT('Ctrl Pts',(5.36346750481178,1.0389294360968,135.611626856221));
#71462=CARTESIAN_POINT('Ctrl Pts',(5.35597716904977,1.16776419871477,135.583783541407));
#71463=CARTESIAN_POINT('Ctrl Pts',(5.34848683328775,1.29531420331714,135.550793065797));
#71464=CARTESIAN_POINT('Ctrl Pts',(5.34099649752574,1.42114857971225,135.512812568779));
#71465=CARTESIAN_POINT('Ctrl Pts',(5.33322216340665,1.55175400473529,135.473392029672));
#71466=CARTESIAN_POINT('Ctrl Pts',(5.32544782928758,1.68092485605517,135.428470733813));
#71467=CARTESIAN_POINT('Ctrl Pts',(5.31767349516849,1.80816279017454,135.37816979447));
#71468=CARTESIAN_POINT('Ctrl Pts',(5.3099087422214,1.93524391491152,135.327930846539));
#71469=CARTESIAN_POINT('Ctrl Pts',(5.30214398927434,2.0603965021176,135.272325589066));
#71470=CARTESIAN_POINT('Ctrl Pts',(5.29437923632725,2.18313602214503,135.211525258388));
#71471=CARTESIAN_POINT('Ctrl Pts',(5.28662219544225,2.30575363555067,135.150785315456));
#71472=CARTESIAN_POINT('Ctrl Pts',(5.27886515455721,2.42596260323298,135.084860740015));
#71473=CARTESIAN_POINT('Ctrl Pts',(5.27110811367223,2.54329742823446,135.013971199798));
#71474=CARTESIAN_POINT('Ctrl Pts',(5.26335692243209,2.660543770132,134.943135117934));
#71475=CARTESIAN_POINT('Ctrl Pts',(5.25560573119195,2.77491995017405,134.86734172509));
#71476=CARTESIAN_POINT('Ctrl Pts',(5.24785453995182,2.88598451158511,134.786856877626));
#71477=CARTESIAN_POINT('Ctrl Pts',(5.24010664317474,2.99700186759469,134.706406238369));
#71478=CARTESIAN_POINT('Ctrl Pts',(5.23235874639765,3.10471008851892,134.621268339326));
#71479=CARTESIAN_POINT('Ctrl Pts',(5.22461084962057,3.20869638546944,134.531752543347));
#71480=CARTESIAN_POINT('Ctrl Pts',(5.21686457353648,3.31266093072833,134.442255472142));
#71481=CARTESIAN_POINT('Ctrl Pts',(5.20911829745239,3.41290480447179,134.348382580407));
#71482=CARTESIAN_POINT('Ctrl Pts',(5.20137202136829,3.50904834631291,134.250483477497));
#71483=CARTESIAN_POINT('Ctrl Pts',(5.19362568810293,3.60519259786381,134.152583651918));
#71484=CARTESIAN_POINT('Ctrl Pts',(5.18587935483762,3.69723618317356,134.050657834801));
#71485=CARTESIAN_POINT('Ctrl Pts',(5.17813302157228,3.78483664983259,133.945092156011));
#71486=CARTESIAN_POINT('Ctrl Pts',(5.17038495356932,3.87245673400862,133.839502836519));
#71487=CARTESIAN_POINT('Ctrl Pts',(5.16263688556637,3.95563146997038,133.730272334165));
#71488=CARTESIAN_POINT('Ctrl Pts',(5.1548888175634,4.0340592633321,133.617819151546));
#71489=CARTESIAN_POINT('Ctrl Pts',(5.14713251482155,4.11257041068601,133.505246452346));
#71490=CARTESIAN_POINT('Ctrl Pts',(5.13937621207964,4.18632431328884,133.389444552058));
#71491=CARTESIAN_POINT('Ctrl Pts',(5.13161990933779,4.2550629448919,133.270860647468));
#71492=CARTESIAN_POINT('Ctrl Pts',(5.12385946682361,4.32383826437243,133.152213451078));
#71493=CARTESIAN_POINT('Ctrl Pts',(5.11609902430944,4.38759279744898,133.030781637704));
#71494=CARTESIAN_POINT('Ctrl Pts',(5.10833858179527,4.44611541087243,132.907035298943));
#71495=CARTESIAN_POINT('Ctrl Pts',(5.10056568152983,4.50473196999033,132.783090311573));
#71496=CARTESIAN_POINT('Ctrl Pts',(5.09279278126444,4.55809967379698,132.656823734426));
#71497=CARTESIAN_POINT('Ctrl Pts',(5.085019880999,4.60605597290703,132.528724684968));
#71498=CARTESIAN_POINT('Ctrl Pts',(5.07752954523693,4.65226893974999,132.405282358619));
#71499=CARTESIAN_POINT('Ctrl Pts',(5.07003920947488,4.69345701135038,132.280138769438));
#71500=CARTESIAN_POINT('Ctrl Pts',(5.06254887371281,4.7295194976628,132.153741358398));
#71501=CARTESIAN_POINT('Ctrl Pts',(5.05477453959374,4.7669493041045,132.022551551101));
#71502=CARTESIAN_POINT('Ctrl Pts',(5.04700020547465,4.79897574597213,131.889595397901));
#71503=CARTESIAN_POINT('Ctrl Pts',(5.03922587135557,4.82543135245714,131.755357633978));
#71504=CARTESIAN_POINT('Ctrl Pts',(5.03146111840848,4.85185435477157,131.621285306101));
#71505=CARTESIAN_POINT('Ctrl Pts',(5.02369636546141,4.8727201072433,131.485934890081));
#71506=CARTESIAN_POINT('Ctrl Pts',(5.01593161251432,4.88791077574366,131.349806591856));
#71507=CARTESIAN_POINT('Ctrl Pts',(5.00817457162931,4.90308635665793,131.213813498176));
#71508=CARTESIAN_POINT('Ctrl Pts',(5.00041753074428,4.91259802755782,131.077044445846));
#71509=CARTESIAN_POINT('Ctrl Pts',(4.99266048985928,4.91637898865255,130.940009806416));
#71510=CARTESIAN_POINT('Ctrl Pts',(4.98490929861917,4.9201570984951,130.803078505874));
#71511=CARTESIAN_POINT('Ctrl Pts',(4.97715810737907,4.91821308962169,130.665882406115));
#71512=CARTESIAN_POINT('Ctrl Pts',(4.96940691613895,4.91053201634603,130.528936619083));
#71513=CARTESIAN_POINT('Ctrl Pts',(4.96165901936186,4.90285420773139,130.392049037662));
#71514=CARTESIAN_POINT('Ctrl Pts',(4.95391112258479,4.8894442063653,130.255411946902));
#71515=CARTESIAN_POINT('Ctrl Pts',(4.94616322580771,4.87033916549697,130.11953985596));
#71516=CARTESIAN_POINT('Ctrl Pts',(4.93841694972362,4.85123812099136,129.983696186531));
#71517=CARTESIAN_POINT('Ctrl Pts',(4.9306706736395,4.82644446090755,129.848617585542));
#71518=CARTESIAN_POINT('Ctrl Pts',(4.92292439755539,4.79604710578405,129.714812444422));
#71519=CARTESIAN_POINT('Ctrl Pts',(4.91517806429004,4.76564952627418,129.581006315584));
#71520=CARTESIAN_POINT('Ctrl Pts',(4.90743173102474,4.72964825579454,129.448474046625));
#71521=CARTESIAN_POINT('Ctrl Pts',(4.89968539775938,4.68818305244258,129.31771246508));
#71522=CARTESIAN_POINT('Ctrl Pts',(4.89193732975641,4.64670856324583,129.186921600385));
#71523=CARTESIAN_POINT('Ctrl Pts',(4.88418926175342,4.59976782448988,129.057902584763));
#71524=CARTESIAN_POINT('Ctrl Pts',(4.87644119375045,4.5475499151299,128.93113536899));
#71525=CARTESIAN_POINT('Ctrl Pts',(4.8686848910086,4.49527650795445,128.804233423511));
#71526=CARTESIAN_POINT('Ctrl Pts',(4.86092858826677,4.43771487545824,128.679588420708));
#71527=CARTESIAN_POINT('Ctrl Pts',(4.85317228552492,4.37510178747198,128.557659166158));
#71528=CARTESIAN_POINT('Ctrl Pts',(4.84541184301076,4.31245528099541,128.435664834293));
#71529=CARTESIAN_POINT('Ctrl Pts',(4.83765140049659,4.24475213969536,128.316389478728));
#71530=CARTESIAN_POINT('Ctrl Pts',(4.82989095798243,4.17227374226681,128.200264827836));
#71531=CARTESIAN_POINT('Ctrl Pts',(4.82211805771699,4.09967899608028,128.083953763345));
#71532=CARTESIAN_POINT('Ctrl Pts',(4.81434515745157,4.02229389615795,127.9708038335));
#71533=CARTESIAN_POINT('Ctrl Pts',(4.80657225718613,3.94044208896177,127.86121617564));
#71534=CARTESIAN_POINT('Ctrl Pts',(4.79908192142407,3.86156580112909,127.755612305178));
#71535=CARTESIAN_POINT('Ctrl Pts',(4.79159158566201,3.77854211407504,127.653316447279));
#71536=CARTESIAN_POINT('Ctrl Pts',(4.78410124989995,3.69169304713321,127.554655168106));
#71537=CARTESIAN_POINT('Ctrl Pts',(4.77632691578087,3.60155107142158,127.452253116547));
#71538=CARTESIAN_POINT('Ctrl Pts',(4.76855258166181,3.50700236833949,127.353442315528));
#71539=CARTESIAN_POINT('Ctrl Pts',(4.76077824754273,3.40836423725886,127.25862567419));
#71540=CARTESIAN_POINT('Ctrl Pts',(4.75301349459563,3.30984766885912,127.163925885889));
#71541=CARTESIAN_POINT('Ctrl Pts',(4.74524874164859,3.20725197942357,127.073210731409));
#71542=CARTESIAN_POINT('Ctrl Pts',(4.73748398870148,3.10093431415033,126.986849721468));
#71543=CARTESIAN_POINT('Ctrl Pts',(4.72972694781647,2.99472224508107,126.9005744865));
#71544=CARTESIAN_POINT('Ctrl Pts',(4.72196990693145,2.88479585831222,126.818645034834));
#71545=CARTESIAN_POINT('Ctrl Pts',(4.71421286604644,2.77154843696411,126.741393435313));
#71546=CARTESIAN_POINT('Ctrl Pts',(4.70646167480635,2.65838641637798,126.664200091826));
#71547=CARTESIAN_POINT('Ctrl Pts',(4.69871048356626,2.54190866777437,126.591677798427));
#71548=CARTESIAN_POINT('Ctrl Pts',(4.69095929232617,2.42254049091172,126.524117559936));
#71549=CARTESIAN_POINT('Ctrl Pts',(4.68321139554909,2.303223048708,126.456586036347));
#71550=CARTESIAN_POINT('Ctrl Pts',(4.67546349877192,2.18101796119212,126.394012565185));
#71551=CARTESIAN_POINT('Ctrl Pts',(4.66771560199484,2.05637818172992,126.336643993136));
#71552=CARTESIAN_POINT('Ctrl Pts',(4.65996932591073,1.93176447422232,126.279287421356));
#71553=CARTESIAN_POINT('Ctrl Pts',(4.65222304982664,1.80471744269036,126.227133746464));
#71554=CARTESIAN_POINT('Ctrl Pts',(4.64447677374253,1.67571287496711,126.18038295508));
#71555=CARTESIAN_POINT('Ctrl Pts',(4.63673044047714,1.54670735496128,126.133631818592));
#71556=CARTESIAN_POINT('Ctrl Pts',(4.62898410721181,1.41574463750276,126.092283778403));
#71557=CARTESIAN_POINT('Ctrl Pts',(4.62123777394643,1.283318260332,126.056489799484));
#71558=CARTESIAN_POINT('Ctrl Pts',(4.61348970594347,1.15086222719296,126.020687804751));
#71559=CARTESIAN_POINT('Ctrl Pts',(4.60574163794052,1.01694225945359,125.99044244829));
#71560=CARTESIAN_POINT('Ctrl Pts',(4.59799356993756,0.882064355087217,125.965854077735));
#71561=CARTESIAN_POINT('Ctrl Pts',(4.59023726719571,0.747043100878831,125.941239574368));
#71562=CARTESIAN_POINT('Ctrl Pts',(4.58248096445379,0.61106226150561,125.922294137379));
#71563=CARTESIAN_POINT('Ctrl Pts',(4.57472466171194,0.474635822970092,125.909066561224));
#71564=CARTESIAN_POINT('Ctrl Pts',(4.56696421919776,0.338136569536235,125.895831925114));
#71565=CARTESIAN_POINT('Ctrl Pts',(4.55920377668363,0.20119163323181,125.888321252197));
#71566=CARTESIAN_POINT('Ctrl Pts',(4.55144333416945,0.0643163314213354,
125.886531170339));
#71567=CARTESIAN_POINT('Ctrl Pts',(4.54367043390401,-0.0727786947746378,
125.884738214883));
#71568=CARTESIAN_POINT('Ctrl Pts',(4.53589753363858,-0.209803472069553,
125.888684190186));
#71569=CARTESIAN_POINT('Ctrl Pts',(4.52812463337315,-0.346245573441667,
125.898313627843));
#71570=CARTESIAN_POINT('Ctrl Pts',(4.52063429761112,-0.477727660751992,
125.907593011186));
#71571=CARTESIAN_POINT('Ctrl Pts',(4.51314396184914,-0.608668393989772,
125.922149780548));
#71572=CARTESIAN_POINT('Ctrl Pts',(4.50565362608711,-0.738618964478486,
125.941889528931));
#71573=CARTESIAN_POINT('Ctrl Pts',(4.497879291968,-0.873496650345266,125.962377715873));
#71574=CARTESIAN_POINT('Ctrl Pts',(4.49010495784889,-1.00773485920604,125.988514565996));
#71575=CARTESIAN_POINT('Ctrl Pts',(4.48233062372978,-1.14082310413027,126.020250908583));
#71576=CARTESIAN_POINT('Ctrl Pts',(4.47456587078265,-1.27374732968725,126.051948138964));
#71577=CARTESIAN_POINT('Ctrl Pts',(4.46680111783557,-1.40552403451739,126.08923104131));
#71578=CARTESIAN_POINT('Ctrl Pts',(4.45903636488845,-1.53564929308527,126.13199886882));
#71579=CARTESIAN_POINT('Ctrl Pts',(4.45127932400344,-1.66564530941155,126.17472421872));
#71580=CARTESIAN_POINT('Ctrl Pts',(4.44352228311836,-1.79399277461118,126.222923531322));
#71581=CARTESIAN_POINT('Ctrl Pts',(4.43576524223334,-1.92019973062742,126.27644541772));
#71582=CARTESIAN_POINT('Ctrl Pts',(4.42801405099323,-2.04631151299604,126.329926942847));
#71583=CARTESIAN_POINT('Ctrl Pts',(4.42026285975314,-2.17028564061794,126.388722900531));
#71584=CARTESIAN_POINT('Ctrl Pts',(4.41251166851302,-2.2916473979909,126.452632769253));
#71585=CARTESIAN_POINT('Ctrl Pts',(4.40476377173592,-2.41295757338004,126.516515474576));
#71586=CARTESIAN_POINT('Ctrl Pts',(4.39701587495879,-2.53165724166949,126.585507586127));
#71587=CARTESIAN_POINT('Ctrl Pts',(4.38926797818169,-2.647293891392,126.659361448073));
#71588=CARTESIAN_POINT('Ctrl Pts',(4.38152170209758,-2.76290635242006,126.733199861383));
#71589=CARTESIAN_POINT('Ctrl Pts',(4.37377542601346,-2.8754567400147,126.811897791967));
#71590=CARTESIAN_POINT('Ctrl Pts',(4.36602914992935,-2.98451962482338,126.895163043697));
#71591=CARTESIAN_POINT('Ctrl Pts',(4.35828281666399,-3.09358331470935,126.978428910072));
#71592=CARTESIAN_POINT('Ctrl Pts',(4.35053648339867,-3.19915913968632,127.066261927622));
#71593=CARTESIAN_POINT('Ctrl Pts',(4.34279015013331,-3.30085331944363,127.158328469323));
#71594=CARTESIAN_POINT('Ctrl Pts',(4.3350420821303,-3.40257027290781,127.250415628689));
#71595=CARTESIAN_POINT('Ctrl Pts',(4.32729401412733,-3.50040356163289,127.346737936408));
#71596=CARTESIAN_POINT('Ctrl Pts',(4.31954594612432,-3.59399525604552,127.446923922404));
#71597=CARTESIAN_POINT('Ctrl Pts',(4.31178964338246,-3.68768642082447,127.547216387258));
#71598=CARTESIAN_POINT('Ctrl Pts',(4.3040333406406,-3.77712671872418,127.65138044714));
#71599=CARTESIAN_POINT('Ctrl Pts',(4.29627703789873,-3.86199727559698,127.759010045664));
#71600=CARTESIAN_POINT('Ctrl Pts',(4.28851659538457,-3.94691313044127,127.866697089346));
#71601=CARTESIAN_POINT('Ctrl Pts',(4.28075615287032,-4.02725415541798,127.977853040572));
#71602=CARTESIAN_POINT('Ctrl Pts',(4.27299571035616,-4.10274464597638,128.092042525525));
#71603=CARTESIAN_POINT('Ctrl Pts',(4.26522281009071,-4.17835632057217,128.206415317578));
#71604=CARTESIAN_POINT('Ctrl Pts',(4.25744990982529,-4.24910169893824,128.323831039497));
#71605=CARTESIAN_POINT('Ctrl Pts',(4.24967700955983,-4.31475046889258,128.443828589889));
#71606=CARTESIAN_POINT('Ctrl Pts',(4.24218667379792,-4.37801274069866,128.559463927066));
#71607=CARTESIAN_POINT('Ctrl Pts',(4.23469633803604,-4.4365423830845,128.67749636378));
#71608=CARTESIAN_POINT('Ctrl Pts',(4.22720600227413,-4.49017623127887,128.797497275293));
#71609=CARTESIAN_POINT('Ctrl Pts',(4.21867919408695,-4.55123164326934,128.934103268305));
#71610=CARTESIAN_POINT('Ctrl Pts',(4.21015238589982,-4.60610988282734,129.073633207333));
#71611=CARTESIAN_POINT('Ctrl Pts',(4.20162557771272,-4.65454812012595,129.215535624078));
#71612=CARTESIAN_POINT('Ctrl Pts',(4.1943716338636,-4.69575559727382,129.336255140752));
#71613=CARTESIAN_POINT('Ctrl Pts',(4.18711769001443,-4.73230293808678,129.458691151222));
#71614=CARTESIAN_POINT('Ctrl Pts',(4.1798637461653,-4.76405452823409,129.582490119308));
#71615=CARTESIAN_POINT('Origin',(213.235140564004,0.,130.804360617566));
#71616=CARTESIAN_POINT('',(2.08495204958918,-4.764054528234,129.582490119308));
#71617=CARTESIAN_POINT('',(2.43008709577655,-4.76405452823407,129.582490119308));
#71618=CARTESIAN_POINT('',(213.235140564004,-4.76405452823405,129.582490119308));
#71619=CARTESIAN_POINT('',(3.76485943594234,-4.91824795725753,130.808843187376));
#71620=CARTESIAN_POINT('Ctrl Pts',(3.76485943594241,-4.91824795725753,130.808843187376));
#71621=CARTESIAN_POINT('Ctrl Pts',(3.75516901773868,-4.91809184520243,130.980128371696));
#71622=CARTESIAN_POINT('Ctrl Pts',(3.74547859953493,-4.90898427284577,131.151013822307));
#71623=CARTESIAN_POINT('Ctrl Pts',(3.7357881813312,-4.8910718301247,131.320693276867));
#71624=CARTESIAN_POINT('Ctrl Pts',(3.7259228264609,-4.8728360223069,131.493435876643));
#71625=CARTESIAN_POINT('Ctrl Pts',(3.71605747159059,-4.84547460045101,131.664928684303));
#71626=CARTESIAN_POINT('Ctrl Pts',(3.70619211672027,-4.80919068690557,131.834345083216));
#71627=CARTESIAN_POINT('Ctrl Pts',(3.7007613280828,-4.78921672063713,131.927607278679));
#71628=CARTESIAN_POINT('Ctrl Pts',(3.69533053944535,-4.76653972229635,132.020240647857));
#71629=CARTESIAN_POINT('Ctrl Pts',(3.68989975080788,-4.74119968075756,132.112110077395));
#71630=CARTESIAN_POINT('Ctrl Pts',(3.68212541668877,-4.70492466387409,132.243623875528));
#71631=CARTESIAN_POINT('Ctrl Pts',(3.67435108256961,-4.66311604850594,132.373835516073));
#71632=CARTESIAN_POINT('Ctrl Pts',(3.6665767484505,-4.61588295417604,132.502243892661));
#71633=CARTESIAN_POINT('Ctrl Pts',(3.65881199550337,-4.56870807041356,132.630494017401));
#71634=CARTESIAN_POINT('Ctrl Pts',(3.65104724255629,-4.51612214288966,132.756944936613));
#71635=CARTESIAN_POINT('Ctrl Pts',(3.64328248960916,-4.45828473125545,132.881108150983));
#71636=CARTESIAN_POINT('Ctrl Pts',(3.63552544872412,-4.40050476455383,133.005148044698));
#71637=CARTESIAN_POINT('Ctrl Pts',(3.62776840783913,-4.33748385753299,133.126904403205));
#71638=CARTESIAN_POINT('Ctrl Pts',(3.62001136695409,-4.26943044402365,133.245906592178));
#71639=CARTESIAN_POINT('Ctrl Pts',(3.61226017571392,-4.20142835012282,133.364819040674));
#71640=CARTESIAN_POINT('Ctrl Pts',(3.6045089844737,-4.1284014968548,133.480981115646));
#71641=CARTESIAN_POINT('Ctrl Pts',(3.59675779323354,-4.05060507027287,133.593945107625));
#71642=CARTESIAN_POINT('Ctrl Pts',(3.58900989645643,-3.97284170924763,133.706861086895));
#71643=CARTESIAN_POINT('Ctrl Pts',(3.58126199967937,-3.89031302813405,133.816581365339));
#71644=CARTESIAN_POINT('Ctrl Pts',(3.57351410290227,-3.80331839489694,133.922685849087));
#71645=CARTESIAN_POINT('Ctrl Pts',(3.56576782681814,-3.71634195906172,134.028768138064));
#71646=CARTESIAN_POINT('Ctrl Pts',(3.55802155073404,-3.6249016769672,134.131235834614));
#71647=CARTESIAN_POINT('Ctrl Pts',(3.55027527464992,-3.52933794648657,134.229700998023));
#71648=CARTESIAN_POINT('Ctrl Pts',(3.54252894138455,-3.43377351057619,134.32816688828));
#71649=CARTESIAN_POINT('Ctrl Pts',(3.53478260811909,-3.33408583783187,134.422629905881));
#71650=CARTESIAN_POINT('Ctrl Pts',(3.52703627485371,-3.23065272900738,134.512738430985));
#71651=CARTESIAN_POINT('Ctrl Pts',(3.51928820685072,-3.12719645705546,134.602867135268));
#71652=CARTESIAN_POINT('Ctrl Pts',(3.51154013884777,-3.01999337471197,134.688639149835));
#71653=CARTESIAN_POINT('Ctrl Pts',(3.50379207084478,-2.9094546266219,134.769742924246));
#71654=CARTESIAN_POINT('Ctrl Pts',(3.4960357681029,-2.79879839663478,134.850932896713));
#71655=CARTESIAN_POINT('Ctrl Pts',(3.48827946536104,-2.68479973473342,134.92744448632));
#71656=CARTESIAN_POINT('Ctrl Pts',(3.48052316261916,-2.56789951700299,134.999009009634));
#71657=CARTESIAN_POINT('Ctrl Pts',(3.47276272010497,-2.45093690610641,135.070611729088));
#71658=CARTESIAN_POINT('Ctrl Pts',(3.46500227759081,-2.33106999509739,135.137261931131));
#71659=CARTESIAN_POINT('Ctrl Pts',(3.45724183507662,-2.20876367358131,135.198737262412));
#71660=CARTESIAN_POINT('Ctrl Pts',(3.44946893481116,-2.08626101510008,135.260311279352));
#71661=CARTESIAN_POINT('Ctrl Pts',(3.44169603454567,-1.96131147734824,135.316693664275));
#71662=CARTESIAN_POINT('Ctrl Pts',(3.43392313428021,-1.83440013619927,135.367710177134));
#71663=CARTESIAN_POINT('Ctrl Pts',(3.42643279851843,-1.71210234197607,135.416872111247));
#71664=CARTESIAN_POINT('Ctrl Pts',(3.41894246275668,-1.58798319121196,135.46105142278));
#71665=CARTESIAN_POINT('Ctrl Pts',(3.4114521269949,-1.46248757974431,135.500136713335));
#71666=CARTESIAN_POINT('Ctrl Pts',(3.40367779287583,-1.33223376402007,135.540703934562));
#71667=CARTESIAN_POINT('Ctrl Pts',(3.3959034587567,-1.2000844452058,135.575911734682));
#71668=CARTESIAN_POINT('Ctrl Pts',(3.38812912463763,-1.06652020005127,135.605581058806));
#71669=CARTESIAN_POINT('Ctrl Pts',(3.38036437169055,-0.933120560891917,
135.63521381814));
#71670=CARTESIAN_POINT('Ctrl Pts',(3.37259961874353,-0.798309842973666,
135.659321598573));
#71671=CARTESIAN_POINT('Ctrl Pts',(3.36483486579644,-0.662585280494269,
135.677774596346));
#71672=CARTESIAN_POINT('Ctrl Pts',(3.35707782491145,-0.526995521563893,
135.696209266342));
#71673=CARTESIAN_POINT('Ctrl Pts',(3.3493207840264,-0.390494109217712,135.709000278258));
#71674=CARTESIAN_POINT('Ctrl Pts',(3.34156374314142,-0.253589665019819,
135.71606860403));
#71675=CARTESIAN_POINT('Ctrl Pts',(3.3338125519013,-0.116788461528071,135.723131599522));
#71676=CARTESIAN_POINT('Ctrl Pts',(3.32606136066122,0.0204147799969158,
135.724480478579));
#71677=CARTESIAN_POINT('Ctrl Pts',(3.3183101694211,0.157505454606213,135.72008793855));
#71678=CARTESIAN_POINT('Ctrl Pts',(3.31056227264402,0.294537862021787,135.715697265468));
#71679=CARTESIAN_POINT('Ctrl Pts',(3.30281437586693,0.431457407733053,135.70557003928));
#71680=CARTESIAN_POINT('Ctrl Pts',(3.29506647908985,0.567748839171424,135.689731055733));
#71681=CARTESIAN_POINT('Ctrl Pts',(3.28732020300576,0.704011761380442,135.673895385361));
#71682=CARTESIAN_POINT('Ctrl Pts',(3.27957392692169,0.839646442548953,135.65235037921));
#71683=CARTESIAN_POINT('Ctrl Pts',(3.27182765083759,0.974142503801548,135.625172732219));
#71684=CARTESIAN_POINT('Ctrl Pts',(3.26408131757225,1.10863955787352,135.597994884609));
#71685=CARTESIAN_POINT('Ctrl Pts',(3.25633498430693,1.24199759203833,135.56518439063));
#71686=CARTESIAN_POINT('Ctrl Pts',(3.24858865104159,1.37371656802735,135.52686904564));
#71687=CARTESIAN_POINT('Ctrl Pts',(3.24084058303862,1.50546504156776,135.488545120194));
#71688=CARTESIAN_POINT('Ctrl Pts',(3.23309251503565,1.63557335120067,135.444713999841));
#71689=CARTESIAN_POINT('Ctrl Pts',(3.22534444703268,1.76355714699191,135.395553191592));
#71690=CARTESIAN_POINT('Ctrl Pts',(3.21758814429084,1.89167696548434,135.346340134651));
#71691=CARTESIAN_POINT('Ctrl Pts',(3.20983184154892,2.01766739407113,135.291786214866));
#71692=CARTESIAN_POINT('Ctrl Pts',(3.20207553880707,2.14106407747729,135.232117123816));
#71693=CARTESIAN_POINT('Ctrl Pts',(3.1943150962929,2.26452662140879,135.172416185575));
#71694=CARTESIAN_POINT('Ctrl Pts',(3.18655465377879,2.38539231733127,135.107594820762));
#71695=CARTESIAN_POINT('Ctrl Pts',(3.17879421126463,2.50322280888666,135.037923966752));
#71696=CARTESIAN_POINT('Ctrl Pts',(3.17102131099921,2.6212424524076,134.968141270902));
#71697=CARTESIAN_POINT('Ctrl Pts',(3.16324841073373,2.73621682689186,134.893493742304));
#71698=CARTESIAN_POINT('Ctrl Pts',(3.15547551046831,2.84773714389602,134.814295308029));
#71699=CARTESIAN_POINT('Ctrl Pts',(3.14798517470621,2.95520341647541,134.737975936327));
#71700=CARTESIAN_POINT('Ctrl Pts',(3.14049483894416,3.05946215526273,134.657430976572));
#71701=CARTESIAN_POINT('Ctrl Pts',(3.13300450318206,3.1601791605628,134.572974518677));
#71702=CARTESIAN_POINT('Ctrl Pts',(3.12523016906299,3.26471488173007,134.485315868511));
#71703=CARTESIAN_POINT('Ctrl Pts',(3.11745583494393,3.36576613585352,134.393165579892));
#71704=CARTESIAN_POINT('Ctrl Pts',(3.10968150082485,3.46292251551207,134.296831192111));
#71705=CARTESIAN_POINT('Ctrl Pts',(3.10191674787777,3.55995915861568,134.200615527852));
#71706=CARTESIAN_POINT('Ctrl Pts',(3.09415199493068,3.65311020303134,134.100226297019));
#71707=CARTESIAN_POINT('Ctrl Pts',(3.0863872419836,3.74199767395112,133.996011674722));
#71708=CARTESIAN_POINT('Ctrl Pts',(3.07863020109861,3.83079686058169,133.891900559857));
#71709=CARTESIAN_POINT('Ctrl Pts',(3.07087316021368,3.91534064877232,133.783971910108));
#71710=CARTESIAN_POINT('Ctrl Pts',(3.0631161193287,3.99528762759541,133.672610926602));
#71711=CARTESIAN_POINT('Ctrl Pts',(3.05536492808856,4.07517431778009,133.561333921279));
#71712=CARTESIAN_POINT('Ctrl Pts',(3.04761373684839,4.15047087135219,133.446630050465));
#71713=CARTESIAN_POINT('Ctrl Pts',(3.03986254560826,4.22087616127534,133.328917508127));
#71714=CARTESIAN_POINT('Ctrl Pts',(3.03211464883119,4.29125152707197,133.21125499676));
#71715=CARTESIAN_POINT('Ctrl Pts',(3.02436675205405,4.35673956376432,133.090586692064));
#71716=CARTESIAN_POINT('Ctrl Pts',(3.01661885527699,4.4170826261191,132.967359493325));
#71717=CARTESIAN_POINT('Ctrl Pts',(3.0088725791929,4.47741306600616,132.84415807106));
#71718=CARTESIAN_POINT('Ctrl Pts',(3.00112630310885,4.53260050037787,132.718399170329));
#71719=CARTESIAN_POINT('Ctrl Pts',(2.99338002702476,4.5824335826097,132.590553642821));
#71720=CARTESIAN_POINT('Ctrl Pts',(2.98563369375941,4.63226703269803,132.462707171587));
#71721=CARTESIAN_POINT('Ctrl Pts',(2.97788736049404,4.6767459097886,132.332774407112));
#71722=CARTESIAN_POINT('Ctrl Pts',(2.97014102722869,4.71570744883851,132.201245122265));
#71723=CARTESIAN_POINT('Ctrl Pts',(2.96239295922573,4.7546777130549,132.069686382348));
#71724=CARTESIAN_POINT('Ctrl Pts',(2.95464489122278,4.78812806956927,131.93653078541));
#71725=CARTESIAN_POINT('Ctrl Pts',(2.94689682321982,4.81594605708595,131.802281775643));
#71726=CARTESIAN_POINT('Ctrl Pts',(2.93914052047796,4.84379360989085,131.667890084431));
#71727=CARTESIAN_POINT('Ctrl Pts',(2.93138421773616,4.86599675626703,131.53240304243));
#71728=CARTESIAN_POINT('Ctrl Pts',(2.92362791499431,4.8824943815624,131.396333316693));
#71729=CARTESIAN_POINT('Ctrl Pts',(2.91586747248016,4.89900081213713,131.260190966447));
#71730=CARTESIAN_POINT('Ctrl Pts',(2.90810702996598,4.90979562303861,131.123465702341));
#71731=CARTESIAN_POINT('Ctrl Pts',(2.90034658745182,4.91486981923424,130.986672774265));
#71732=CARTESIAN_POINT('Ctrl Pts',(2.8925736871864,4.91995216098007,130.849660254037));
#71733=CARTESIAN_POINT('Ctrl Pts',(2.88480078692092,4.91929553885698,130.712580243966));
#71734=CARTESIAN_POINT('Ctrl Pts',(2.8770278866555,4.91294310846071,130.575946354595));
#71735=CARTESIAN_POINT('Ctrl Pts',(2.86953755089338,4.90682160491007,130.444279451262));
#71736=CARTESIAN_POINT('Ctrl Pts',(2.86204721513129,4.89541124409234,130.313027103391));
#71737=CARTESIAN_POINT('Ctrl Pts',(2.85455687936917,4.87879563564792,130.182640255922));
#71738=CARTESIAN_POINT('Ctrl Pts',(2.84678254525008,4.86155004135932,130.047309751502));
#71739=CARTESIAN_POINT('Ctrl Pts',(2.83900821113101,4.83864206488063,129.912482987593));
#71740=CARTESIAN_POINT('Ctrl Pts',(2.83123387701193,4.81010861248993,129.77867148408));
#71741=CARTESIAN_POINT('Ctrl Pts',(2.82346912406483,4.78161032502918,129.645024891287));
#71742=CARTESIAN_POINT('Ctrl Pts',(2.81570437111772,4.74750043680579,129.512391448036));
#71743=CARTESIAN_POINT('Ctrl Pts',(2.80793961817062,4.70786757278504,129.381277352392));
#71744=CARTESIAN_POINT('Ctrl Pts',(2.80018257728562,4.66827407268356,129.250293481116));
#71745=CARTESIAN_POINT('Ctrl Pts',(2.79242553640064,4.62316862556491,129.120826326213));
#71746=CARTESIAN_POINT('Ctrl Pts',(2.78466849551563,4.57269077110158,128.993371336984));
#71747=CARTESIAN_POINT('Ctrl Pts',(2.7769173042755,4.52225098238097,128.866012462554));
#71748=CARTESIAN_POINT('Ctrl Pts',(2.76916611303533,4.46644699370828,128.740663095552));
#71749=CARTESIAN_POINT('Ctrl Pts',(2.76141492179519,4.40546787699527,128.617802626736));
#71750=CARTESIAN_POINT('Ctrl Pts',(2.7536670250181,4.34451467803353,128.494994376897));
#71751=CARTESIAN_POINT('Ctrl Pts',(2.74591912824104,4.27839089925505,128.374673270734));
#71752=CARTESIAN_POINT('Ctrl Pts',(2.73817123146395,4.20733326614456,128.257297632461));
#71753=CARTESIAN_POINT('Ctrl Pts',(2.73042495537984,4.13629049675909,128.139946546641));
#71754=CARTESIAN_POINT('Ctrl Pts',(2.72267867929577,4.06031612820225,128.025540037437));
#71755=CARTESIAN_POINT('Ctrl Pts',(2.71493240321166,3.97969206332346,127.91451042359));
#71756=CARTESIAN_POINT('Ctrl Pts',(2.70718606994631,3.89906740329614,127.803479990149));
#71757=CARTESIAN_POINT('Ctrl Pts',(2.69943973668084,3.81379320817995,127.695826818162));
#71758=CARTESIAN_POINT('Ctrl Pts',(2.69169340341548,3.72419355928067,127.59195258067));
#71759=CARTESIAN_POINT('Ctrl Pts',(2.68394533541251,3.63457384516137,127.488055081263));
#71760=CARTESIAN_POINT('Ctrl Pts',(2.67619726740958,3.5406270050612,127.387938496313));
#71761=CARTESIAN_POINT('Ctrl Pts',(2.66844919940661,3.44271581275968,127.291969566576));
#71762=CARTESIAN_POINT('Ctrl Pts',(2.66069289666475,3.34470055927768,127.195898639918));
#71763=CARTESIAN_POINT('Ctrl Pts',(2.65293659392291,3.24271281660731,127.103984448389));
#71764=CARTESIAN_POINT('Ctrl Pts',(2.64518029118105,3.13715087209901,127.016555518543));
#71765=CARTESIAN_POINT('Ctrl Pts',(2.63741984866688,3.03153258600251,126.929079925244));
#71766=CARTESIAN_POINT('Ctrl Pts',(2.6296594061527,2.92233660802012,126.846094600158));
#71767=CARTESIAN_POINT('Ctrl Pts',(2.62189896363853,2.80999157044021,126.767885616212));
#71768=CARTESIAN_POINT('Ctrl Pts',(2.6141260633731,2.69746618663247,126.689551084262));
#71769=CARTESIAN_POINT('Ctrl Pts',(2.60635316310764,2.58178197155513,126.616008425242));
#71770=CARTESIAN_POINT('Ctrl Pts',(2.59858026284221,2.46339436695886,126.547498950171));
#71771=CARTESIAN_POINT('Ctrl Pts',(2.59108992708022,2.34931044999069,126.481479967085));
#71772=CARTESIAN_POINT('Ctrl Pts',(2.58359959131826,2.23271655373394,126.420134726759));
#71773=CARTESIAN_POINT('Ctrl Pts',(2.57610925555628,2.1140372639896,126.36363663279));
#71774=CARTESIAN_POINT('Ctrl Pts',(2.56833492143719,1.99085821290211,126.304996396416));
#71775=CARTESIAN_POINT('Ctrl Pts',(2.56056058731809,1.86504231708822,126.251392366595));
#71776=CARTESIAN_POINT('Ctrl Pts',(2.552786253199,1.73703988145857,126.203069982024));
#71777=CARTESIAN_POINT('Ctrl Pts',(2.5450215002519,1.60919519739092,126.154807150474));
#71778=CARTESIAN_POINT('Ctrl Pts',(2.5372567473048,1.47916969744489,126.11181314965));
#71779=CARTESIAN_POINT('Ctrl Pts',(2.5294919943577,1.34743716434546,126.074287029276));
#71780=CARTESIAN_POINT('Ctrl Pts',(2.5217349534727,1.21583546985517,126.036798180374));
#71781=CARTESIAN_POINT('Ctrl Pts',(2.51397791258765,1.08253048980571,126.004766510851));
#71782=CARTESIAN_POINT('Ctrl Pts',(2.50622087170265,0.948014484327536,125.978342424479));
#71783=CARTESIAN_POINT('Ctrl Pts',(2.49846968046252,0.813599918415293,125.951938264716));
#71784=CARTESIAN_POINT('Ctrl Pts',(2.49071848922249,0.677976526911703,125.931133346144));
#71785=CARTESIAN_POINT('Ctrl Pts',(2.48296729798236,0.541649832826402,125.916027719624));
#71786=CARTESIAN_POINT('Ctrl Pts',(2.47521940120528,0.405381081222907,125.900928513399));
#71787=CARTESIAN_POINT('Ctrl Pts',(2.46747150442819,0.268410009344956,125.891523824321));
#71788=CARTESIAN_POINT('Ctrl Pts',(2.45972360765111,0.131250174239513,125.887862223967));
#71789=CARTESIAN_POINT('Ctrl Pts',(2.45197733156701,-0.00588096998543594,
125.884201389541));
#71790=CARTESIAN_POINT('Ctrl Pts',(2.44423105548288,-0.143200408321297,
125.886281264755));
#71791=CARTESIAN_POINT('Ctrl Pts',(2.43648477939877,-0.280192043391584,
125.894098355597));
#71792=CARTESIAN_POINT('Ctrl Pts',(2.42873844613342,-0.417184689702813,
125.901915504142));
#71793=CARTESIAN_POINT('Ctrl Pts',(2.42099211286805,-0.553849137589757,
125.91546993055));
#71794=CARTESIAN_POINT('Ctrl Pts',(2.4132457796027,-0.689672274285727,125.93470609013));
#71795=CARTESIAN_POINT('Ctrl Pts',(2.40549771159972,-0.825525827631614,
125.953946557514));
#71796=CARTESIAN_POINT('Ctrl Pts',(2.39774964359676,-0.96053730785265,125.978871235153));
#71797=CARTESIAN_POINT('Ctrl Pts',(2.39000157559377,-1.09420207747503,126.009373143531));
#71798=CARTESIAN_POINT('Ctrl Pts',(2.38224527285192,-1.22800890760501,126.0399074697));
#71799=CARTESIAN_POINT('Ctrl Pts',(2.37448897011011,-1.36046578618579,126.076030780401));
#71800=CARTESIAN_POINT('Ctrl Pts',(2.36673266736827,-1.49108103048203,126.117585561833));
#71801=CARTESIAN_POINT('Ctrl Pts',(2.3589722248541,-1.62176598806707,126.159162522304));
#71802=CARTESIAN_POINT('Ctrl Pts',(2.35121178233986,-1.75060698568748,126.206176595933));
#71803=CARTESIAN_POINT('Ctrl Pts',(2.34345133982569,-1.87713165586705,126.258421791642));
#71804=CARTESIAN_POINT('Ctrl Pts',(2.33567843956026,-2.00385943467953,126.310750855978));
#71805=CARTESIAN_POINT('Ctrl Pts',(2.3279055392948,-2.12826310054298,126.36832765889));
#71806=CARTESIAN_POINT('Ctrl Pts',(2.32013263902937,-2.24989345427112,126.430899458835));
#71807=CARTESIAN_POINT('Ctrl Pts',(2.31264230326736,-2.36710223827254,126.491196616244));
#71808=CARTESIAN_POINT('Ctrl Pts',(2.30515196750539,-2.4817355752373,126.556131762438));
#71809=CARTESIAN_POINT('Ctrl Pts',(2.29766163174338,-2.59341807681275,126.62544141024));
#71810=CARTESIAN_POINT('Ctrl Pts',(2.28988595511789,-2.70935507143737,126.697391376897));
#71811=CARTESIAN_POINT('Ctrl Pts',(2.2821102784924,-2.82247926998559,126.774283696204));
#71812=CARTESIAN_POINT('Ctrl Pts',(2.27433460186691,-2.93234054597536,126.855872047882));
#71813=CARTESIAN_POINT('Ctrl Pts',(2.26644366218868,-3.04383035497371,126.938669827746));
#71814=CARTESIAN_POINT('Ctrl Pts',(2.25855272251043,-3.15195935181584,127.026303834178));
#71815=CARTESIAN_POINT('Ctrl Pts',(2.2506617828322,-3.2562832339872,127.118468247657));
#71816=CARTESIAN_POINT('Ctrl Pts',(2.24290557038219,-3.35882592557094,127.209059077193));
#71817=CARTESIAN_POINT('Ctrl Pts',(2.23514935793222,-3.45769207768353,127.304026592513));
#71818=CARTESIAN_POINT('Ctrl Pts',(2.22739314548221,-3.55248972498134,127.403037372651));
#71819=CARTESIAN_POINT('Ctrl Pts',(2.21964229762557,-3.64722180537598,127.501979671866));
#71820=CARTESIAN_POINT('Ctrl Pts',(2.2118914497689,-3.73789071055311,127.604959390666));
#71821=CARTESIAN_POINT('Ctrl Pts',(2.20414060191226,-3.82413966135607,127.711604740853));
#71822=CARTESIAN_POINT('Ctrl Pts',(2.19639343629534,-3.91034763737561,127.818199426422));
#71823=CARTESIAN_POINT('Ctrl Pts',(2.18864627067844,-3.99213959289988,127.92845597419));
#71824=CARTESIAN_POINT('Ctrl Pts',(2.18089910506151,-4.06919782176642,128.041968149101));
#71825=CARTESIAN_POINT('Ctrl Pts',(2.17290351710548,-4.14872701697201,128.159120230709));
#71826=CARTESIAN_POINT('Ctrl Pts',(2.16490792914947,-4.2232135296843,128.279739901928));
#71827=CARTESIAN_POINT('Ctrl Pts',(2.15691234119345,-4.29235538605496,128.403346602133));
#71828=CARTESIAN_POINT('Ctrl Pts',(2.14916577050034,-4.35934386534797,128.523103653966));
#71829=CARTESIAN_POINT('Ctrl Pts',(2.14141919980721,-4.42131546369412,128.645664077464));
#71830=CARTESIAN_POINT('Ctrl Pts',(2.1336726291141,-4.47804181031442,128.770565001587));
#71831=CARTESIAN_POINT('Ctrl Pts',(2.12555253252662,-4.53750340072136,128.901488426664));
#71832=CARTESIAN_POINT('Ctrl Pts',(2.11743243593913,-4.59120110308603,129.034983256854));
#71833=CARTESIAN_POINT('Ctrl Pts',(2.10931233935165,-4.63892864520064,129.17049278716));
#71834=CARTESIAN_POINT('Ctrl Pts',(2.10119224276415,-4.68665618731532,129.306002317466));
#71835=CARTESIAN_POINT('Ctrl Pts',(2.09307214617668,-4.72841344343846,129.443526070619));
#71836=CARTESIAN_POINT('Ctrl Pts',(2.08495204958919,-4.764054528234,129.582490119308));
#71837=CARTESIAN_POINT('Ctrl Pts',(3.83484270885904,-4.76405452823401,129.582490119308));
#71838=CARTESIAN_POINT('Ctrl Pts',(3.82717092304017,-4.79783678081443,129.714206609402));
#71839=CARTESIAN_POINT('Ctrl Pts',(3.81949913722131,-4.82615215141464,129.847324677294));
#71840=CARTESIAN_POINT('Ctrl Pts',(3.81182735140243,-4.8488999635451,129.981346519247));
#71841=CARTESIAN_POINT('Ctrl Pts',(3.80399936550057,-4.87211092861365,130.11809708999));
#71842=CARTESIAN_POINT('Ctrl Pts',(3.79617137959876,-4.88952507481256,130.255788211832));
#71843=CARTESIAN_POINT('Ctrl Pts',(3.78834339369692,-4.90109085894145,130.393883511139));
#71844=CARTESIAN_POINT('Ctrl Pts',(3.78051540779509,-4.91265664307031,130.531978810446));
#71845=CARTESIAN_POINT('Ctrl Pts',(3.77268742189319,-4.91837406561657,130.670477846659));
#71846=CARTESIAN_POINT('Ctrl Pts',(3.76485943599135,-4.91824795725832,130.80884318651));
#71847=CARTESIAN_POINT('',(4.11014056405159,-4.91824955451988,130.80226730321));
#71848=CARTESIAN_POINT('Ctrl Pts',(4.1798637461653,-4.76405452823409,129.582490119308));
#71849=CARTESIAN_POINT('Ctrl Pts',(4.17137872466698,-4.80119472818719,129.727299195244));
#71850=CARTESIAN_POINT('Ctrl Pts',(4.16289370316864,-4.8317720853013,129.873973393409));
#71851=CARTESIAN_POINT('Ctrl Pts',(4.15440868167033,-4.85561338970576,130.021927443288));
#71852=CARTESIAN_POINT('Ctrl Pts',(4.1459570040762,-4.87936100405068,130.169300072642));
#71853=CARTESIAN_POINT('Ctrl Pts',(4.13750532648211,-4.89642530248433,130.317942265847));
#71854=CARTESIAN_POINT('Ctrl Pts',(4.12905364888798,-4.90668371155702,130.467258233651));
#71855=CARTESIAN_POINT('Ctrl Pts',(4.12274928727587,-4.91433576875379,130.578637524332));
#71856=CARTESIAN_POINT('Ctrl Pts',(4.11644492566373,-4.91820193766441,130.69039133125));
#71857=CARTESIAN_POINT('Ctrl Pts',(4.11014056405165,-4.91824955451988,130.80226730321));
#71858=CARTESIAN_POINT('Ctrl Pts',(4.11014056400876,-4.9182495545202,130.80226730397));
#71859=CARTESIAN_POINT('Ctrl Pts',(4.10224648305787,-4.91830917850728,130.942354125357));
#71860=CARTESIAN_POINT('Ctrl Pts',(4.09435240210698,-4.91237929659228,131.082413681721));
#71861=CARTESIAN_POINT('Ctrl Pts',(4.0864583211561,-4.90049331021611,131.221911068442));
#71862=CARTESIAN_POINT('Ctrl Pts',(4.07856087743446,-4.88860226057195,131.361467879147));
#71863=CARTESIAN_POINT('Ctrl Pts',(4.07066343371281,-4.87075008229045,131.500461674559));
#71864=CARTESIAN_POINT('Ctrl Pts',(4.06276598999116,-4.84702196962627,131.638363668196));
#71865=CARTESIAN_POINT('Ctrl Pts',(4.05486374740559,-4.82327943862775,131.776349457669));
#71866=CARTESIAN_POINT('Ctrl Pts',(4.04696150482002,-4.79365392157798,131.913241759357));
#71867=CARTESIAN_POINT('Ctrl Pts',(4.03905926223445,-4.75828149958854,132.048523080098));
#71868=CARTESIAN_POINT('Ctrl Pts',(4.03114499854317,-4.72285526811161,132.184010194453));
#71869=CARTESIAN_POINT('Ctrl Pts',(4.02323073485189,-4.68166475859979,132.317881073285));
#71870=CARTESIAN_POINT('Ctrl Pts',(4.01531647116062,-4.63489592976505,132.44963347723));
#71871=CARTESIAN_POINT('Ctrl Pts',(4.00739585069181,-4.5880895359651,132.581491705387));
#71872=CARTESIAN_POINT('Ctrl Pts',(3.999475230223,-4.5356960280495,132.711227723832));
#71873=CARTESIAN_POINT('Ctrl Pts',(3.99155460975419,-4.47794888609887,132.838360823069));
#71874=CARTESIAN_POINT('Ctrl Pts',(3.98361934313438,-4.42009496294793,132.965729006233));
#71875=CARTESIAN_POINT('Ctrl Pts',(3.97568407651458,-4.35686778787975,133.090484320939));
#71876=CARTESIAN_POINT('Ctrl Pts',(3.96774880989477,-4.28854660220437,133.212171055126));
#71877=CARTESIAN_POINT('Ctrl Pts',(3.96141866608358,-4.23404522860254,133.309243348247));
#71878=CARTESIAN_POINT('Ctrl Pts',(3.9550885222724,-4.17630313004901,133.404363398253));
#71879=CARTESIAN_POINT('Ctrl Pts',(3.94875837846121,-4.11548089883579,133.497314392479));
#71880=CARTESIAN_POINT('Ctrl Pts',(3.94098404434212,-4.04078238306371,133.611471686115));
#71881=CARTESIAN_POINT('Ctrl Pts',(3.93320971022298,-3.96121212129713,133.722699403411));
#71882=CARTESIAN_POINT('Ctrl Pts',(3.92543537610391,-3.8770270275519,133.830553686445));
#71883=CARTESIAN_POINT('Ctrl Pts',(3.91767062315682,-3.79294568441088,133.938275048715));
#71884=CARTESIAN_POINT('Ctrl Pts',(3.90990587020978,-3.70426106370937,134.042630943585));
#71885=CARTESIAN_POINT('Ctrl Pts',(3.90214111726269,-3.61127426143631,134.143204919295));
#71886=CARTESIAN_POINT('Ctrl Pts',(3.89438407637769,-3.51837981496627,134.243679003514));
#71887=CARTESIAN_POINT('Ctrl Pts',(3.88662703549263,-3.42119195405883,134.340378358479));
#71888=CARTESIAN_POINT('Ctrl Pts',(3.87886999460764,-3.32005286007642,134.432918467291));
#71889=CARTESIAN_POINT('Ctrl Pts',(3.87111880336752,-3.21899003587152,134.525388790886));
#71890=CARTESIAN_POINT('Ctrl Pts',(3.86336761212747,-3.11398219669232,134.613705848528));
#71891=CARTESIAN_POINT('Ctrl Pts',(3.85561642088734,-3.00540904369461,134.697521228507));
#71892=CARTESIAN_POINT('Ctrl Pts',(3.84786852411027,-2.89688203718321,134.781300984712));
#71893=CARTESIAN_POINT('Ctrl Pts',(3.84012062733318,-2.78479303960595,134.860582630319));
#71894=CARTESIAN_POINT('Ctrl Pts',(3.8323727305561,-2.66955539209871,134.935057540728));
#71895=CARTESIAN_POINT('Ctrl Pts',(3.82462645447201,-2.55434184982325,135.00951687259));
#71896=CARTESIAN_POINT('Ctrl Pts',(3.81688017838791,-2.43598129582079,135.079171257103));
#71897=CARTESIAN_POINT('Ctrl Pts',(3.80913390230381,-2.31491632425063,135.143755215228));
#71898=CARTESIAN_POINT('Ctrl Pts',(3.80138756903846,-2.19385045900619,135.208339650097));
#71899=CARTESIAN_POINT('Ctrl Pts',(3.79364123577312,-2.07008048130893,135.267853399872));
#71900=CARTESIAN_POINT('Ctrl Pts',(3.78589490250778,-1.94407351197216,135.322076992301));
#71901=CARTESIAN_POINT('Ctrl Pts',(3.77814683450482,-1.81803832424844,135.376312727727));
#71902=CARTESIAN_POINT('Ctrl Pts',(3.77039876650186,-1.68976550709223,135.425255793892));
#71903=CARTESIAN_POINT('Ctrl Pts',(3.7626506984989,-1.55974169826002,135.468735055495));
#71904=CARTESIAN_POINT('Ctrl Pts',(3.75489439575706,-1.42957969857648,135.512260527375));
#71905=CARTESIAN_POINT('Ctrl Pts',(3.74713809301523,-1.2976633610945,135.550310470406));
#71906=CARTESIAN_POINT('Ctrl Pts',(3.7393817902734,-1.16449454636711,135.582763647238));
#71907=CARTESIAN_POINT('Ctrl Pts',(3.73162134775923,-1.0312546554333,135.615234145308));
#71908=CARTESIAN_POINT('Ctrl Pts',(3.72386090524503,-0.896761338443784,
135.642101848452));
#71909=CARTESIAN_POINT('Ctrl Pts',(3.71610046273085,-0.761525176489029,
135.663296969081));
#71910=CARTESIAN_POINT('Ctrl Pts',(3.70832756246542,-0.626071921441587,
135.684526113999));
#71911=CARTESIAN_POINT('Ctrl Pts',(3.70055466219995,-0.489873827141526,
135.700064435106));
#71912=CARTESIAN_POINT('Ctrl Pts',(3.69278176193453,-0.353446006255062,
135.709894124042));
#71913=CARTESIAN_POINT('Ctrl Pts',(3.68529142617244,-0.221977680297659,
135.719366479026));
#71914=CARTESIAN_POINT('Ctrl Pts',(3.67780109041043,-0.0902963479219616,
135.723538032591));
#71915=CARTESIAN_POINT('Ctrl Pts',(3.67031075464834,0.0411403272179479,
135.722438548626));
#71916=CARTESIAN_POINT('Ctrl Pts',(3.66253642052925,0.177560463844138,135.721297377392));
#71917=CARTESIAN_POINT('Ctrl Pts',(3.65476208641021,0.31414916263425,135.714473960707));
#71918=CARTESIAN_POINT('Ctrl Pts',(3.64698775229112,0.45039412504755,135.701944531561));
#71919=CARTESIAN_POINT('Ctrl Pts',(3.63922299934403,0.586471177721238,135.689430543816));
#71920=CARTESIAN_POINT('Ctrl Pts',(3.63145824639686,0.722204951319387,135.671224570953));
#71921=CARTESIAN_POINT('Ctrl Pts',(3.62369349344976,0.857082323444843,135.647354831205));
#71922=CARTESIAN_POINT('Ctrl Pts',(3.61593645256475,0.991825733463049,135.623508799219));
#71923=CARTESIAN_POINT('Ctrl Pts',(3.60817941167973,1.12571405222937,135.594010262705));
#71924=CARTESIAN_POINT('Ctrl Pts',(3.60042237079472,1.25823881740201,135.55893926776));
#71925=CARTESIAN_POINT('Ctrl Pts',(3.59267117955457,1.39066364461834,135.523894720125));
#71926=CARTESIAN_POINT('Ctrl Pts',(3.58491998831445,1.52172658851761,135.483286177967));
#71927=CARTESIAN_POINT('Ctrl Pts',(3.57716879707431,1.65092928271038,135.437244769581));
#71928=CARTESIAN_POINT('Ctrl Pts',(3.56942090029723,1.78007706231118,135.391222930022));
#71929=CARTESIAN_POINT('Ctrl Pts',(3.56167300352011,1.90736579724985,135.339772947847));
#71930=CARTESIAN_POINT('Ctrl Pts',(3.55392510674304,2.03231241192895,135.283075759526));
#71931=CARTESIAN_POINT('Ctrl Pts',(3.54617883065893,2.15723289046998,135.226390431034));
#71932=CARTESIAN_POINT('Ctrl Pts',(3.53843255457485,2.27981186743149,135.164460241039));
#71933=CARTESIAN_POINT('Ctrl Pts',(3.53068627849075,2.39958675482496,135.097514058636));
#71934=CARTESIAN_POINT('Ctrl Pts',(3.52293994522539,2.51936252636945,135.030567382051));
#71935=CARTESIAN_POINT('Ctrl Pts',(3.51519361196002,2.63633382576766,134.958604829924));
#71936=CARTESIAN_POINT('Ctrl Pts',(3.50744727869466,2.7500635145877,134.881900774111));
#71937=CARTESIAN_POINT('Ctrl Pts',(3.49969921069166,2.86381867238316,134.805179540956));
#71938=CARTESIAN_POINT('Ctrl Pts',(3.49195114268869,2.97433045099858,134.72371490977));
#71939=CARTESIAN_POINT('Ctrl Pts',(3.48420307468569,3.0811918298643,134.63782379987));
#71940=CARTESIAN_POINT('Ctrl Pts',(3.47644677194383,3.188166782275,134.551841403876));
#71941=CARTESIAN_POINT('Ctrl Pts',(3.468690469202,3.29148327962229,134.461423376717));
#71942=CARTESIAN_POINT('Ctrl Pts',(3.46093416646013,3.39076805360215,134.36692641614));
#71943=CARTESIAN_POINT('Ctrl Pts',(3.45317372394595,3.49010581885543,134.27237901969));
#71944=CARTESIAN_POINT('Ctrl Pts',(3.44541328143177,3.58540730145787,134.173748632887));
#71945=CARTESIAN_POINT('Ctrl Pts',(3.43765283891759,3.6763378055837,134.071427100167));
#71946=CARTESIAN_POINT('Ctrl Pts',(3.42987993865215,3.76741427942705,133.968941311839));
#71947=CARTESIAN_POINT('Ctrl Pts',(3.4221070383867,3.85410550583488,133.862752839877));
#71948=CARTESIAN_POINT('Ctrl Pts',(3.41433413812126,3.93611807115195,133.753285437301));
#71949=CARTESIAN_POINT('Ctrl Pts',(3.40684380235932,4.01514927314168,133.647797450543));
#71950=CARTESIAN_POINT('Ctrl Pts',(3.39935346659739,4.08983589594292,133.539265042805));
#71951=CARTESIAN_POINT('Ctrl Pts',(3.39186313083545,4.15995560237529,133.428089347593));
#71952=CARTESIAN_POINT('Ctrl Pts',(3.38408879671637,4.23273391879019,133.312698392104));
#71953=CARTESIAN_POINT('Ctrl Pts',(3.37631446259734,4.30082271314453,133.194094228029));
#71954=CARTESIAN_POINT('Ctrl Pts',(3.36854012847826,4.36392507970444,133.072695019991));
#71955=CARTESIAN_POINT('Ctrl Pts',(3.36077537553116,4.42694967823727,132.951445425628));
#71956=CARTESIAN_POINT('Ctrl Pts',(3.35301062258409,4.48499989775883,132.827407984681));
#71957=CARTESIAN_POINT('Ctrl Pts',(3.34524586963698,4.53782212387933,132.701029654201));
#71958=CARTESIAN_POINT('Ctrl Pts',(3.33748882875198,4.59059188622012,132.574776844461));
#71959=CARTESIAN_POINT('Ctrl Pts',(3.32973178786687,4.6381438387067,132.446188130442));
#71960=CARTESIAN_POINT('Ctrl Pts',(3.32197474698188,4.68027049007024,132.315734562782));
#71961=CARTESIAN_POINT('Ctrl Pts',(3.31422355574176,4.72236537339829,132.185379371172));
#71962=CARTESIAN_POINT('Ctrl Pts',(3.30647236450168,4.75904297935461,132.053162495619));
#71963=CARTESIAN_POINT('Ctrl Pts',(3.29872117326155,4.79014425068146,131.919574103928));
#71964=CARTESIAN_POINT('Ctrl Pts',(3.29097327648448,4.82123230313835,131.786042490867));
#71965=CARTESIAN_POINT('Ctrl Pts',(3.28322537970742,4.84674864643022,131.651140901058));
#71966=CARTESIAN_POINT('Ctrl Pts',(3.27547748293034,4.86658439337261,131.515373560263));
#71967=CARTESIAN_POINT('Ctrl Pts',(3.26773120684624,4.88641599110435,131.379634619069));
#71968=CARTESIAN_POINT('Ctrl Pts',(3.25998493076212,4.90056929951295,131.243030673713));
#71969=CARTESIAN_POINT('Ctrl Pts',(3.25223865467802,4.90898683254339,131.106074621907));
#71970=CARTESIAN_POINT('Ctrl Pts',(3.24449232141269,4.91740442771014,130.969117559124));
#71971=CARTESIAN_POINT('Ctrl Pts',(3.23674598814735,4.92008613902789,130.831808774933));
#71972=CARTESIAN_POINT('Ctrl Pts',(3.22899965488202,4.91702651930969,130.694664350969));
#71973=CARTESIAN_POINT('Ctrl Pts',(3.22125158687905,4.91396621441086,130.557489214462));
#71974=CARTESIAN_POINT('Ctrl Pts',(3.21350351887613,4.90516202873807,130.420478902217));
#71975=CARTESIAN_POINT('Ctrl Pts',(3.20575545087317,4.89066059092794,130.284147154799));
#71976=CARTESIAN_POINT('Ctrl Pts',(3.19799914813132,4.87614374081711,130.147670512376));
#71977=CARTESIAN_POINT('Ctrl Pts',(3.19024284538943,4.85591758425885,130.01187426482));
#71978=CARTESIAN_POINT('Ctrl Pts',(3.18248654264758,4.83008046053437,129.877265257172));
#71979=CARTESIAN_POINT('Ctrl Pts',(3.1747261001334,4.80422954675894,129.742584404643));
#71980=CARTESIAN_POINT('Ctrl Pts',(3.16696565761921,4.7727617881989,129.609092435003));
#71981=CARTESIAN_POINT('Ctrl Pts',(3.15920521510503,4.73582594340621,129.477282738819));
#71982=CARTESIAN_POINT('Ctrl Pts',(3.1514323148396,4.69883080591651,129.345261450009));
#71983=CARTESIAN_POINT('Ctrl Pts',(3.1436594145742,4.65635016246514,129.214928203115));
#71984=CARTESIAN_POINT('Ctrl Pts',(3.13588651430877,4.60858193122296,129.086758904215));
#71985=CARTESIAN_POINT('Ctrl Pts',(3.1283961785467,4.56255019550716,128.963248882169));
#71986=CARTESIAN_POINT('Ctrl Pts',(3.12090584278461,4.51160875102569,128.841748493736));
#71987=CARTESIAN_POINT('Ctrl Pts',(3.11341550702255,4.45597490407882,128.722661619939));
#71988=CARTESIAN_POINT('Ctrl Pts',(3.10564117290348,4.39823168291575,128.599059531128));
#71989=CARTESIAN_POINT('Ctrl Pts',(3.09786683878435,4.33525029714539,128.477666052313));
#71990=CARTESIAN_POINT('Ctrl Pts',(3.09009250466528,4.26722207570553,128.358957006889));
#71991=CARTESIAN_POINT('Ctrl Pts',(3.0823277517182,4.19927769296874,128.240394259755));
#71992=CARTESIAN_POINT('Ctrl Pts',(3.07456299877111,4.1262990425844,128.124509699389));
#71993=CARTESIAN_POINT('Ctrl Pts',(3.06679824582403,4.04852507740453,128.011758289964));
#71994=CARTESIAN_POINT('Ctrl Pts',(3.05904120493902,3.9708283584231,127.899118866829));
#71995=CARTESIAN_POINT('Ctrl Pts',(3.05128416405397,3.88834602333693,127.789606721579));
#71996=CARTESIAN_POINT('Ctrl Pts',(3.04352712316896,3.80136222628971,127.683651036872));
#71997=CARTESIAN_POINT('Ctrl Pts',(3.03577593192882,3.71444402440048,127.577775254171));
#71998=CARTESIAN_POINT('Ctrl Pts',(3.02802474068875,3.62303136434073,127.475450894702));
#71999=CARTESIAN_POINT('Ctrl Pts',(3.0202735494486,3.52745066383389,127.377076725514));
#72000=CARTESIAN_POINT('Ctrl Pts',(3.01252565267152,3.43191058767473,127.278744367972));
#72001=CARTESIAN_POINT('Ctrl Pts',(3.00477775589443,3.3322062663772,127.184359141254));
#72002=CARTESIAN_POINT('Ctrl Pts',(2.99702985911736,3.22870306317286,127.094285201573));
#72003=CARTESIAN_POINT('Ctrl Pts',(2.98928358303327,3.12522151060737,127.004230103418));
#72004=CARTESIAN_POINT('Ctrl Pts',(2.98153730694914,3.01794295146319,126.918484755009));
#72005=CARTESIAN_POINT('Ctrl Pts',(2.97379103086504,2.90726782849507,126.837374754735));
#72006=CARTESIAN_POINT('Ctrl Pts',(2.96604469759967,2.79659188854803,126.756264155726));
#72007=CARTESIAN_POINT('Ctrl Pts',(2.95829836433435,2.68251965009295,126.679789204236));
#72008=CARTESIAN_POINT('Ctrl Pts',(2.95055203106898,2.56548236288651,126.608233437866));
#72009=CARTESIAN_POINT('Ctrl Pts',(2.94280396306597,2.44841886599092,126.536661647078));
#72010=CARTESIAN_POINT('Ctrl Pts',(2.93505589506296,2.32838933255448,126.470011437401));
#72011=CARTESIAN_POINT('Ctrl Pts',(2.92730782705996,2.20585119098098,126.408521268164));
#72012=CARTESIAN_POINT('Ctrl Pts',(2.91955152431812,2.0831828144129,126.346965746445));
#72013=CARTESIAN_POINT('Ctrl Pts',(2.91179522157622,1.95800085372341,126.29058139598));
#72014=CARTESIAN_POINT('Ctrl Pts',(2.90403891883437,1.83078488678367,126.239559443273));
#72015=CARTESIAN_POINT('Ctrl Pts',(2.89627847632019,1.70350102085163,126.188510258614));
#72016=CARTESIAN_POINT('Ctrl Pts',(2.88851803380606,1.57418135396013,126.142829304791));
#72017=CARTESIAN_POINT('Ctrl Pts',(2.88075759129188,1.4433213971969,126.102658116674));
#72018=CARTESIAN_POINT('Ctrl Pts',(2.87298469102646,1.31225137241423,126.0624224422));
#72019=CARTESIAN_POINT('Ctrl Pts',(2.86521179076101,1.17963649514066,126.027714307138));
#72020=CARTESIAN_POINT('Ctrl Pts',(2.85743889049559,1.04598413824297,125.998624436184));
#72021=CARTESIAN_POINT('Ctrl Pts',(2.84994855473362,0.917190381169401,125.970592055313));
#72022=CARTESIAN_POINT('Ctrl Pts',(2.84245821897168,0.787433568256173,125.947776607532));
#72023=CARTESIAN_POINT('Ctrl Pts',(2.83496788320971,0.657170955410278,125.930213574455));
#72024=CARTESIAN_POINT('Ctrl Pts',(2.82719354909065,0.521969396005091,125.911984633641));
#72025=CARTESIAN_POINT('Ctrl Pts',(2.81941921497166,0.385794646821428,125.899356516715));
#72026=CARTESIAN_POINT('Ctrl Pts',(2.81164488085258,0.249150449521832,125.892425447391));
#72027=CARTESIAN_POINT('Ctrl Pts',(2.80388012790551,0.11267465398335,125.88550291999));
#72028=CARTESIAN_POINT('Ctrl Pts',(2.79611537495831,-0.0242690518085328,
125.884263489906));
#72029=CARTESIAN_POINT('Ctrl Pts',(2.78835062201125,-0.161168733757474,
125.888752038584));
#72030=CARTESIAN_POINT('Ctrl Pts',(2.78059358112626,-0.297932445012727,
125.893236129173));
#72031=CARTESIAN_POINT('Ctrl Pts',(2.77283654024134,-0.434651831213299,
125.903436864212));
#72032=CARTESIAN_POINT('Ctrl Pts',(2.76507949935635,-0.570812216579347,
125.919347160481));
#72033=CARTESIAN_POINT('Ctrl Pts',(2.75732830811624,-0.706869922339248,
125.935245458672));
#72034=CARTESIAN_POINT('Ctrl Pts',(2.74957711687613,-0.842369079576227,
125.956844702817));
#72035=CARTESIAN_POINT('Ctrl Pts',(2.74182592563602,-0.976797757527117,
125.98408581177));
#72036=CARTESIAN_POINT('Ctrl Pts',(2.73407802885894,-1.11116929970424,126.011315342526));
#72037=CARTESIAN_POINT('Ctrl Pts',(2.72633013208189,-1.2444708851456,126.044181891278));
#72038=CARTESIAN_POINT('Ctrl Pts',(2.71858223530481,-1.37619865116445,126.08257490292));
#72039=CARTESIAN_POINT('Ctrl Pts',(2.71083595922072,-1.50789886257419,126.120959883572));
#72040=CARTESIAN_POINT('Ctrl Pts',(2.7030896831366,-1.63802553426643,126.164868918405));
#72041=CARTESIAN_POINT('Ctrl Pts',(2.69534340705252,-1.76608828200558,126.214141097471));
#72042=CARTESIAN_POINT('Ctrl Pts',(2.68759707378719,-1.89415197507484,126.263413640252));
#72043=CARTESIAN_POINT('Ctrl Pts',(2.67985074052184,-2.02015134890067,126.318049265873));
#72044=CARTESIAN_POINT('Ctrl Pts',(2.67210440725651,-2.14361475424143,126.377838410698));
#72045=CARTESIAN_POINT('Ctrl Pts',(2.66435633925359,-2.26710580835527,126.437640944887));
#72046=CARTESIAN_POINT('Ctrl Pts',(2.65660827125068,-2.38805941209476,126.502599124426));
#72047=CARTESIAN_POINT('Ctrl Pts',(2.64886020324775,-2.50602769164538,126.572456994939));
#72048=CARTESIAN_POINT('Ctrl Pts',(2.6411039005059,-2.624121349288,126.642389111227));
#72049=CARTESIAN_POINT('Ctrl Pts',(2.63334759776401,-2.73922300771383,126.717231121402));
#72050=CARTESIAN_POINT('Ctrl Pts',(2.62559129502216,-2.8509125590967,126.796682905613));
#72051=CARTESIAN_POINT('Ctrl Pts',(2.61783085250802,-2.96266172255591,126.876177095633));
#72052=CARTESIAN_POINT('Ctrl Pts',(2.61007040999388,-3.07099484152213,126.960285722551));
#72053=CARTESIAN_POINT('Ctrl Pts',(2.60230996747973,-3.17552500285442,127.048668401909));
#72054=CARTESIAN_POINT('Ctrl Pts',(2.59453706721429,-3.28022296528172,127.13719296099));
#72055=CARTESIAN_POINT('Ctrl Pts',(2.58676416694883,-3.38110548276027,127.230005018294));
#72056=CARTESIAN_POINT('Ctrl Pts',(2.5789912666834,-3.4778219786054,127.326726745574));
#72057=CARTESIAN_POINT('Ctrl Pts',(2.5715009309212,-3.57102258621452,127.419932394441));
#72058=CARTESIAN_POINT('Ctrl Pts',(2.56401059515899,-3.66035459546841,127.516768169228));
#72059=CARTESIAN_POINT('Ctrl Pts',(2.55652025939679,-3.74554099669369,127.616868546268));
#72060=CARTESIAN_POINT('Ctrl Pts',(2.54879702129302,-3.83337615932911,127.720081415585));
#72061=CARTESIAN_POINT('Ctrl Pts',(2.54107378318923,-3.91709218294665,127.827104364471));
#72062=CARTESIAN_POINT('Ctrl Pts',(2.53335054508545,-3.99633686245575,127.937572389552));
#72063=CARTESIAN_POINT('Ctrl Pts',(2.52563672019846,-4.07548495717279,128.047905774286));
#72064=CARTESIAN_POINT('Ctrl Pts',(2.51792289531153,-4.15017231769003,128.161675565284));
#72065=CARTESIAN_POINT('Ctrl Pts',(2.51020907042454,-4.22008518053593,128.278481734579));
#72066=CARTESIAN_POINT('Ctrl Pts',(2.50250440945722,-4.28991498784599,128.395149139724));
#72067=CARTESIAN_POINT('Ctrl Pts',(2.49479974848987,-4.35498138818687,128.514845403344));
#72068=CARTESIAN_POINT('Ctrl Pts',(2.48709508752256,-4.41501279501639,128.637140028345));
#72069=CARTESIAN_POINT('Ctrl Pts',(2.47939571550868,-4.47500299259391,128.759350702791));
#72070=CARTESIAN_POINT('Ctrl Pts',(2.47169634349475,-4.5299648967112,128.88415583685));
#72071=CARTESIAN_POINT('Ctrl Pts',(2.46399697148087,-4.57967193929555,129.011098787568));
#72072=CARTESIAN_POINT('Ctrl Pts',(2.45630130902744,-4.62935503300729,129.137980577122));
#72073=CARTESIAN_POINT('Ctrl Pts',(2.44860564657397,-4.67378815871689,129.266997765422));
#72074=CARTESIAN_POINT('Ctrl Pts',(2.44090998412054,-4.71279235395851,129.397672560117));
#72075=CARTESIAN_POINT('Ctrl Pts',(2.43730235467253,-4.73107702850097,129.458931254908));
#72076=CARTESIAN_POINT('Ctrl Pts',(2.43369472522455,-4.74816932413074,129.520553949601));
#72077=CARTESIAN_POINT('Ctrl Pts',(2.43008709577654,-4.76405452823407,129.582490119308));
#72078=CARTESIAN_POINT('Origin',(213.235140564004,0.,130.804360617566));
#72079=CARTESIAN_POINT('',(0.334704853334813,-4.76405452823404,129.582490119308));
#72080=CARTESIAN_POINT('',(0.68024183266882,-4.76405452823404,129.582490119308));
#72081=CARTESIAN_POINT('',(213.235140564004,-4.76405452823405,129.582490119308));
#72082=CARTESIAN_POINT('',(2.01485943595022,-4.9182499766426,130.803881289891));
#72083=CARTESIAN_POINT('Ctrl Pts',(2.01485943595023,-4.9182499766426,130.803881289891));
#72084=CARTESIAN_POINT('Ctrl Pts',(2.00710625195527,-4.91826323687598,130.939940912275));
#72085=CARTESIAN_POINT('Ctrl Pts',(1.99935306796029,-4.91262624006787,131.0762218757));
#72086=CARTESIAN_POINT('Ctrl Pts',(1.99159988396534,-4.90130985239998,131.21221450472));
#72087=CARTESIAN_POINT('Ctrl Pts',(1.98385624230379,-4.8900073925254,131.34803975902));
#72088=CARTESIAN_POINT('Ctrl Pts',(1.97611260064231,-4.87303948061168,131.483576996769));
#72089=CARTESIAN_POINT('Ctrl Pts',(1.96836895898076,-4.85042895777124,131.61831515445));
#72090=CARTESIAN_POINT('Ctrl Pts',(1.96063296861848,-4.82784077582469,131.752920180717));
#72091=CARTESIAN_POINT('Ctrl Pts',(1.95289697825616,-4.79962114165776,131.886727312609));
#72092=CARTESIAN_POINT('Ctrl Pts',(1.94516098789387,-4.76584477091121,132.019229615474));
#72093=CARTESIAN_POINT('Ctrl Pts',(1.93743076465436,-4.73209358019562,132.151633138867));
#72094=CARTESIAN_POINT('Ctrl Pts',(1.92970054141488,-4.69279399432024,132.282733389611));
#72095=CARTESIAN_POINT('Ctrl Pts',(1.92197031817537,-4.64807190734446,132.412033036517));
#72096=CARTESIAN_POINT('Ctrl Pts',(1.91424326113583,-4.60336813796008,132.541279723951));
#72097=CARTESIAN_POINT('Ctrl Pts',(1.90651620409623,-4.55324641239797,132.668726903142));
#72098=CARTESIAN_POINT('Ctrl Pts',(1.8987891470567,-4.49788257118241,132.793892079583));
#72099=CARTESIAN_POINT('Ctrl Pts',(1.89106359574771,-4.44252951842434,132.91903286575));
#72100=CARTESIAN_POINT('Ctrl Pts',(1.88333804443871,-4.38193654066813,133.041892174051));
#72101=CARTESIAN_POINT('Ctrl Pts',(1.87561249312972,-4.31632758104529,133.162007596146));
#72102=CARTESIAN_POINT('Ctrl Pts',(1.86788675011931,-4.25071699340516,133.282125998779));
#72103=CARTESIAN_POINT('Ctrl Pts',(1.86016100710894,-4.18009036471323,133.399500034469));
#72104=CARTESIAN_POINT('Ctrl Pts',(1.85243526409852,-4.10471733545377,133.513692390997));
#72105=CARTESIAN_POINT('Ctrl Pts',(1.8447076321693,-4.02932587773619,133.627912667183));
#72106=CARTESIAN_POINT('Ctrl Pts',(1.83698000024012,-3.94918592721915,133.738949388305));
#72107=CARTESIAN_POINT('Ctrl Pts',(1.8292523683109,-3.86460988258845,133.846395054896));
#72108=CARTESIAN_POINT('Ctrl Pts',(1.82151648514175,-3.77994353121904,133.953955447444));
#72109=CARTESIAN_POINT('Ctrl Pts',(1.81378060197253,-3.69083186904937,134.05791681778));
#72110=CARTESIAN_POINT('Ctrl Pts',(1.80604471880338,-3.59762726381741,134.157905180135));
#72111=CARTESIAN_POINT('Ctrl Pts',(1.79830451998079,-3.5043706620951,134.257949323467));
#72112=CARTESIAN_POINT('Ctrl Pts',(1.79056432115822,-3.40701684825682,134.354015767394));
#72113=CARTESIAN_POINT('Ctrl Pts',(1.78282412233563,-3.30595355212749,134.445768885486));
#72114=CARTESIAN_POINT('Ctrl Pts',(1.77507185722264,-3.20473270719266,134.537665038634));
#72115=CARTESIAN_POINT('Ctrl Pts',(1.76731959210972,-3.09979112926588,134.625234181002));
#72116=CARTESIAN_POINT('Ctrl Pts',(1.75956732699674,-2.99154856158227,134.708181856582));
#72117=CARTESIAN_POINT('Ctrl Pts',(1.75330034603704,-2.90404457393256,134.775237290825));
#72118=CARTESIAN_POINT('Ctrl Pts',(1.7470333650773,-2.81438396977513,134.839273274428));
#72119=CARTESIAN_POINT('Ctrl Pts',(1.74076638411759,-2.72280062517734,134.900156000399));
#72120=CARTESIAN_POINT('Ctrl Pts',(1.73299204999852,-2.60918937835477,134.975682423221));
#72121=CARTESIAN_POINT('Ctrl Pts',(1.72521771587948,-2.49225331267256,135.046597782595));
#72122=CARTESIAN_POINT('Ctrl Pts',(1.7174433817604,-2.37240334741237,135.112595223491));
#72123=CARTESIAN_POINT('Ctrl Pts',(1.70967862881333,-2.25270108652323,135.178511328439));
#72124=CARTESIAN_POINT('Ctrl Pts',(1.70191387586626,-2.13009241050186,135.239521387505));
#72125=CARTESIAN_POINT('Ctrl Pts',(1.69414912291919,-2.00501806163953,135.295361133598));
#72126=CARTESIAN_POINT('Ctrl Pts',(1.68639208203421,-1.88006793838389,135.351145418867));
#72127=CARTESIAN_POINT('Ctrl Pts',(1.67863504114923,-1.75265737048228,135.401769452145));
#72128=CARTESIAN_POINT('Ctrl Pts',(1.67087800026425,-1.62325229370357,135.447014497998));
#72129=CARTESIAN_POINT('Ctrl Pts',(1.66312680902413,-1.49394480229954,135.492225424209));
#72130=CARTESIAN_POINT('Ctrl Pts',(1.65537561778396,-1.36264616335181,135.532065308373));
#72131=CARTESIAN_POINT('Ctrl Pts',(1.64762442654384,-1.22984258657333,135.566363376359));
#72132=CARTESIAN_POINT('Ctrl Pts',(1.63987652976678,-1.09709545485781,135.600646866751));
#72133=CARTESIAN_POINT('Ctrl Pts',(1.63212863298972,-0.962845035256375,
135.629393128158));
#72134=CARTESIAN_POINT('Ctrl Pts',(1.62438073621266,-0.827592795334841,
135.652481204722));
#72135=CARTESIAN_POINT('Ctrl Pts',(1.61663446012857,-0.692368847266199,
135.675564451759));
#72136=CARTESIAN_POINT('Ctrl Pts',(1.60888818404446,-0.556143880848485,
135.692991802395));
#72137=CARTESIAN_POINT('Ctrl Pts',(1.60114190796037,-0.419429266585645,
135.704693478998));
#72138=CARTESIAN_POINT('Ctrl Pts',(1.59339557469502,-0.282713643126394,
135.71639524198));
#72139=CARTESIAN_POINT('Ctrl Pts',(1.58564924142971,-0.145508754150531,
135.72237121325));
#72140=CARTESIAN_POINT('Ctrl Pts',(1.57790290816436,-0.00833040195511292,
135.722603562654));
#72141=CARTESIAN_POINT('Ctrl Pts',(1.5701548401614,0.128878670380965,135.72283596409));
#72142=CARTESIAN_POINT('Ctrl Pts',(1.5624067721585,0.266060803221432,135.71732218352));
#72143=CARTESIAN_POINT('Ctrl Pts',(1.55465870415554,0.402701284987753,135.706096507796));
#72144=CARTESIAN_POINT('Ctrl Pts',(1.5469024014137,0.539486989884324,135.69485890129));
#72145=CARTESIAN_POINT('Ctrl Pts',(1.5391460986718,0.675729503463738,135.677897304875));
#72146=CARTESIAN_POINT('Ctrl Pts',(1.53138979592995,0.810919766772243,135.65529786663));
#72147=CARTESIAN_POINT('Ctrl Pts',(1.5236293534158,0.946182185194777,135.632686366384));
#72148=CARTESIAN_POINT('Ctrl Pts',(1.51586891090162,1.08039085188442,135.604431108955));
#72149=CARTESIAN_POINT('Ctrl Pts',(1.50810846838746,1.21304894856432,135.570668970042));
#72150=CARTESIAN_POINT('Ctrl Pts',(1.50033556812204,1.34591999979785,135.536852633147));
#72151=CARTESIAN_POINT('Ctrl Pts',(1.4925626678567,1.47723513224696,135.497511861629));
#72152=CARTESIAN_POINT('Ctrl Pts',(1.48478976759128,1.60651382739343,135.45283309623));
#72153=CARTESIAN_POINT('Ctrl Pts',(1.47729943182913,1.73109291634022,135.409778516491));
#72154=CARTESIAN_POINT('Ctrl Pts',(1.46980909606688,1.85378076987155,135.361767416195));
#72155=CARTESIAN_POINT('Ctrl Pts',(1.46231876030473,1.97416840851945,135.309007347034));
#72156=CARTESIAN_POINT('Ctrl Pts',(1.45454442618565,2.09912058107595,135.254246863815));
#72157=CARTESIAN_POINT('Ctrl Pts',(1.44677009206656,2.22199048116853,135.1941967239));
#72158=CARTESIAN_POINT('Ctrl Pts',(1.43899575794745,2.34229783106064,135.12903678268));
#72159=CARTESIAN_POINT('Ctrl Pts',(1.43123100500034,2.46245691289618,135.063957145265));
#72160=CARTESIAN_POINT('Ctrl Pts',(1.42346625205327,2.58005938775689,134.993780420848));
#72161=CARTESIAN_POINT('Ctrl Pts',(1.41570149910615,2.69464468827973,134.918734575585));
#72162=CARTESIAN_POINT('Ctrl Pts',(1.40794445822112,2.80911618106672,134.843763266913));
#72163=CARTESIAN_POINT('Ctrl Pts',(1.40018741733604,2.92057613813777,134.76393267423));
#72164=CARTESIAN_POINT('Ctrl Pts',(1.39243037645102,3.02858868151402,134.679516570648));
#72165=CARTESIAN_POINT('Ctrl Pts',(1.38467918521086,3.13651977179123,134.595164125906));
#72166=CARTESIAN_POINT('Ctrl Pts',(1.37692799397074,3.24100831616122,134.506233292922));
#72167=CARTESIAN_POINT('Ctrl Pts',(1.36917680273058,3.34164782928653,134.413040826108));
#72168=CARTESIAN_POINT('Ctrl Pts',(1.36142890595346,3.44224456793411,134.319887968579));
#72169=CARTESIAN_POINT('Ctrl Pts',(1.35368100917628,3.53899524283554,134.222477344855));
#72170=CARTESIAN_POINT('Ctrl Pts',(1.34593311239917,3.63152703493542,134.121165474206));
#72171=CARTESIAN_POINT('Ctrl Pts',(1.33818683631503,3.72403947137914,134.019874795817));
#72172=CARTESIAN_POINT('Ctrl Pts',(1.3304405602309,3.81233451686599,133.914684782183));
#72173=CARTESIAN_POINT('Ctrl Pts',(1.32269428414676,3.89607705725023,133.805987947277));
#72174=CARTESIAN_POINT('Ctrl Pts',(1.31494795088138,3.97982021580288,133.697290309996));
#72175=CARTESIAN_POINT('Ctrl Pts',(1.30720161761605,4.05901056358786,133.585086109498));
#72176=CARTESIAN_POINT('Ctrl Pts',(1.29945528435067,4.13335429585045,133.46979966723));
#72177=CARTESIAN_POINT('Ctrl Pts',(1.29170721634764,4.20771467687662,133.354487407363));
#72178=CARTESIAN_POINT('Ctrl Pts',(1.2839591483446,4.27722607078529,133.236091860723));
#72179=CARTESIAN_POINT('Ctrl Pts',(1.27621108034157,4.34163910989512,133.115064601621));
#72180=CARTESIAN_POINT('Ctrl Pts',(1.26845477759969,4.40612060794919,132.993908713309));
#72181=CARTESIAN_POINT('Ctrl Pts',(1.2606984748578,4.46549274300586,132.870115870873));
#72182=CARTESIAN_POINT('Ctrl Pts',(1.25294217211592,4.51955283508444,132.74416092517));
#72183=CARTESIAN_POINT('Ctrl Pts',(1.24518172960173,4.57364178066188,132.61813875352));
#72184=CARTESIAN_POINT('Ctrl Pts',(1.23742128708753,4.62241289493052,132.489952544433));
#72185=CARTESIAN_POINT('Ctrl Pts',(1.22966084457335,4.66571279287922,132.360094269855));
#72186=CARTESIAN_POINT('Ctrl Pts',(1.22188794430788,4.70908219966814,132.230027535246));
#72187=CARTESIAN_POINT('Ctrl Pts',(1.21411504404248,4.74696273104014,132.09828374732));
#72188=CARTESIAN_POINT('Ctrl Pts',(1.20634214377702,4.77925151287505,131.965367955692));
#72189=CARTESIAN_POINT('Ctrl Pts',(1.19885180801528,4.81036651615842,131.837283987889));
#72190=CARTESIAN_POINT('Ctrl Pts',(1.19136147225349,4.83628919938415,131.708112049573));
#72191=CARTESIAN_POINT('Ctrl Pts',(1.18387113649175,4.85697311827532,131.578308413513));
#72192=CARTESIAN_POINT('Ctrl Pts',(1.17609680237268,4.87844127423875,131.443583233133));
#72193=CARTESIAN_POINT('Ctrl Pts',(1.16832246825362,4.89433357308443,131.3077507389));
#72194=CARTESIAN_POINT('Ctrl Pts',(1.16054813413456,4.90454173039793,131.171312218306));
#72195=CARTESIAN_POINT('Ctrl Pts',(1.1527833811875,4.91473730706985,131.035041845994));
#72196=CARTESIAN_POINT('Ctrl Pts',(1.14501862824037,4.91926265157261,130.898167319511));
#72197=CARTESIAN_POINT('Ctrl Pts',(1.13725387529331,4.91806061037807,130.761199348496));
#72198=CARTESIAN_POINT('Ctrl Pts',(1.12949683440831,4.91685976306778,130.624367416));
#72199=CARTESIAN_POINT('Ctrl Pts',(1.12173979352335,4.90994285388088,130.487442612091));
#72200=CARTESIAN_POINT('Ctrl Pts',(1.11398275263835,4.89730461319729,130.35093963431));
#72201=CARTESIAN_POINT('Ctrl Pts',(1.10623156139825,4.88467590310936,130.214539594488));
#72202=CARTESIAN_POINT('Ctrl Pts',(1.09848037015815,4.86633448517438,130.078561135357));
#72203=CARTESIAN_POINT('Ctrl Pts',(1.09072917891805,4.84232713859761,129.943517458041));
#72204=CARTESIAN_POINT('Ctrl Pts',(1.08298128214098,4.81832999578348,129.80853117789));
#72205=CARTESIAN_POINT('Ctrl Pts',(1.07523338536392,4.7886717822832,129.674479273465));
#72206=CARTESIAN_POINT('Ctrl Pts',(1.06748548858684,4.75345093005052,129.54186811537));
#72207=CARTESIAN_POINT('Ctrl Pts',(1.05973921250273,4.71823744526082,129.40928469667));
#72208=CARTESIAN_POINT('Ctrl Pts',(1.0519929364186,4.67746373646669,129.278141802478));
#72209=CARTESIAN_POINT('Ctrl Pts',(1.04424666033449,4.63127889940931,129.148933537207));
#72210=CARTESIAN_POINT('Ctrl Pts',(1.03650032706913,4.58509372142596,129.01972431815));
#72211=CARTESIAN_POINT('Ctrl Pts',(1.02875399380379,4.533497467069,128.892450124662));
#72212=CARTESIAN_POINT('Ctrl Pts',(1.02100766053843,4.4766883213425,128.767587499112));
#72213=CARTESIAN_POINT('Ctrl Pts',(1.01325959253549,4.41986645360201,128.642696911444));
#72214=CARTESIAN_POINT('Ctrl Pts',(1.00551152453253,4.35782953339704,128.520219322154));
#72215=CARTESIAN_POINT('Ctrl Pts',(0.997763456529583,4.29082269366034,128.40060861828));
#72216=CARTESIAN_POINT('Ctrl Pts',(0.99000715378772,4.22374463825661,128.280870790726));
#72217=CARTESIAN_POINT('Ctrl Pts',(0.982250851045878,4.15168630316364,128.164006276852));
#72218=CARTESIAN_POINT('Ctrl Pts',(0.974494548304023,4.07493764037456,128.050442265552));
#72219=CARTESIAN_POINT('Ctrl Pts',(0.966734105789877,3.99814801451349,127.93681764172));
#72220=CARTESIAN_POINT('Ctrl Pts',(0.958973663275737,3.91666330495005,127.826497344883));
#72221=CARTESIAN_POINT('Ctrl Pts',(0.951213220761588,3.83081451327079,127.719876345048));
#72222=CARTESIAN_POINT('Ctrl Pts',(0.943440320496165,3.7448279094897,127.613084187718));
#72223=CARTESIAN_POINT('Ctrl Pts',(0.935667420230746,3.65446348202092,127.510003488448));
#72224=CARTESIAN_POINT('Ctrl Pts',(0.927894519965321,3.5600905374331,127.410993789801));
#72225=CARTESIAN_POINT('Ctrl Pts',(0.920404184203183,3.46914828709074,127.315583343088));
#72226=CARTESIAN_POINT('Ctrl Pts',(0.912913848441045,3.374484120522,127.223953267657));
#72227=CARTESIAN_POINT('Ctrl Pts',(0.905423512678908,3.27645680866257,127.136389264969));
#72228=CARTESIAN_POINT('Ctrl Pts',(0.897649178559821,3.17471276148065,127.045505246507));
#72229=CARTESIAN_POINT('Ctrl Pts',(0.889874844440721,3.06902321282255,126.958713824368));
#72230=CARTESIAN_POINT('Ctrl Pts',(0.882100510321635,2.95975137968282,126.876377059433));
#72231=CARTESIAN_POINT('Ctrl Pts',(0.874335757374518,2.85061421431125,126.794141767201));
#72232=CARTESIAN_POINT('Ctrl Pts',(0.866571004427363,2.73790385793331,126.716350441796));
#72233=CARTESIAN_POINT('Ctrl Pts',(0.858806251480246,2.62201909215602,126.643327219134));
#72234=CARTESIAN_POINT('Ctrl Pts',(0.851049210595241,2.5062494247621,126.570376524166));
#72235=CARTESIAN_POINT('Ctrl Pts',(0.843292169710317,2.38731195095036,126.502184714675));
#72236=CARTESIAN_POINT('Ctrl Pts',(0.835535128825313,2.26563685198288,126.439034430734));
#72237=CARTESIAN_POINT('Ctrl Pts',(0.827783937585192,2.1440535091542,126.375931768915));
#72238=CARTESIAN_POINT('Ctrl Pts',(0.820032746345022,2.01973699596873,126.317863244661));
#72239=CARTESIAN_POINT('Ctrl Pts',(0.812281555104903,1.89314436837007,126.265066899045));
#72240=CARTESIAN_POINT('Ctrl Pts',(0.804533658327831,1.76660554601511,126.212292993284));
#72241=CARTESIAN_POINT('Ctrl Pts',(0.79678576155074,1.63779289343586,126.164786959524));
#72242=CARTESIAN_POINT('Ctrl Pts',(0.789037864773661,1.5071856394384,126.122739689856));
#72243=CARTESIAN_POINT('Ctrl Pts',(0.781291588689562,1.3766057056629,126.08070121557));
#72244=CARTESIAN_POINT('Ctrl Pts',(0.773545312605469,1.24423228906344,126.044119353897));
#72245=CARTESIAN_POINT('Ctrl Pts',(0.765799036521372,1.11056168356567,126.013135741869));
#72246=CARTESIAN_POINT('Ctrl Pts',(0.758052703256014,0.976890091341672,
125.982151901128));
#72247=CARTESIAN_POINT('Ctrl Pts',(0.750306369990696,0.841921671979665,
125.956766480775));
#72248=CARTESIAN_POINT('Ctrl Pts',(0.742560036725337,0.706164477905643,
125.937070324945));
#72249=CARTESIAN_POINT('Ctrl Pts',(0.734811968722331,0.570376881948912,
125.917369758297));
#72250=CARTESIAN_POINT('Ctrl Pts',(0.727063900719244,0.433800546625983,
125.90336104755));
#72251=CARTESIAN_POINT('Ctrl Pts',(0.719315832716234,0.296949840293891,
125.895083292455));
#72252=CARTESIAN_POINT('Ctrl Pts',(0.711559529974378,0.159953687403126,
125.886796739664));
#72253=CARTESIAN_POINT('Ctrl Pts',(0.703803227232551,0.0226829718654649,
125.884253333452));
#72254=CARTESIAN_POINT('Ctrl Pts',(0.696046924490702,-0.114346174068859,
125.887440035029));
#72255=CARTESIAN_POINT('Ctrl Pts',(0.68828648197651,-0.251448456584796,
125.890628437444));
#72256=CARTESIAN_POINT('Ctrl Pts',(0.680526039462401,-0.388308522641809,
125.899553016204));
#72257=CARTESIAN_POINT('Ctrl Pts',(0.67276559694821,-0.524415158343417,
125.914148781234));
#72258=CARTESIAN_POINT('Ctrl Pts',(0.664992696682787,-0.660740284499077,
125.928767976683));
#72259=CARTESIAN_POINT('Ctrl Pts',(0.657219796417314,-0.796309176512856,
125.949076492924));
#72260=CARTESIAN_POINT('Ctrl Pts',(0.649446896151886,-0.930619721822204,
125.974957963422));
#72261=CARTESIAN_POINT('Ctrl Pts',(0.641956560389925,-1.06004774050061,
125.999898577275));
#72262=CARTESIAN_POINT('Ctrl Pts',(0.634466224627999,-1.1883070123873,126.030013927678));
#72263=CARTESIAN_POINT('Ctrl Pts',(0.626975888866042,-1.31496324429701,
126.0651565991));
#72264=CARTESIAN_POINT('Ctrl Pts',(0.619201554746944,-1.44642168573738,
126.10163171559));
#72265=CARTESIAN_POINT('Ctrl Pts',(0.611427220627866,-1.57656954990418,
126.143638442496));
#72266=CARTESIAN_POINT('Ctrl Pts',(0.603652886508769,-1.70490589706772,
126.19106689782));
#72267=CARTESIAN_POINT('Ctrl Pts',(0.595888133561661,-1.83308408115312,
126.238436901813));
#72268=CARTESIAN_POINT('Ctrl Pts',(0.588123380614518,-1.95945482710724,
126.291215205216));
#72269=CARTESIAN_POINT('Ctrl Pts',(0.580358627667408,-2.08352987900321,
126.349241505152));
#72270=CARTESIAN_POINT('Ctrl Pts',(0.572601586782389,-2.20748169780848,
126.407210172548));
#72271=CARTESIAN_POINT('Ctrl Pts',(0.564844545897377,-2.32914200823075,
126.470416299042));
#72272=CARTESIAN_POINT('Ctrl Pts',(0.557087505012362,-2.44804049369009,
126.53865073482));
#72273=CARTESIAN_POINT('Ctrl Pts',(0.549336313772261,-2.566849316876,126.606833714479));
#72274=CARTESIAN_POINT('Ctrl Pts',(0.541585122532171,-2.68290012289334,
126.680037262087));
#72275=CARTESIAN_POINT('Ctrl Pts',(0.533833931292065,-2.79574559114389,
126.758005510547));
#72276=CARTESIAN_POINT('Ctrl Pts',(0.526086034514964,-2.9085430970608,126.835940620422));
#72277=CARTESIAN_POINT('Ctrl Pts',(0.518338137737806,-3.01813765384677,
126.918636181555));
#72278=CARTESIAN_POINT('Ctrl Pts',(0.51059024096071,-3.12410962370458,127.005792187015));
#72279=CARTESIAN_POINT('Ctrl Pts',(0.502843964876572,-3.23005942651108,
127.092929961319));
#72280=CARTESIAN_POINT('Ctrl Pts',(0.495097688792449,-3.33238784786237,
127.184526075918));
#72281=CARTESIAN_POINT('Ctrl Pts',(0.487351412708307,-3.43070746552064,
127.280239542954));
#72282=CARTESIAN_POINT('Ctrl Pts',(0.479605079442925,-3.52902780895186,
127.375953716526));
#72283=CARTESIAN_POINT('Ctrl Pts',(0.471858746177595,-3.62333900949916,
127.475785030466));
#72284=CARTESIAN_POINT('Ctrl Pts',(0.464112412912215,-3.71329002267438,
127.579355149353));
#72285=CARTESIAN_POINT('Ctrl Pts',(0.456364344909199,-3.80326117975546,
127.682948462049));
#72286=CARTESIAN_POINT('Ctrl Pts',(0.448616276906127,-3.88886995015889,
127.790281950659));
#72287=CARTESIAN_POINT('Ctrl Pts',(0.440868208903112,-3.96980540949516,
127.900943996886));
#72288=CARTESIAN_POINT('Ctrl Pts',(0.433111906161231,-4.05082688800065,
128.011723656052));
#72289=CARTESIAN_POINT('Ctrl Pts',(0.425355603419435,-4.12716490245128,
128.125838623559));
#72290=CARTESIAN_POINT('Ctrl Pts',(0.417599300677551,-4.19855144066325,
128.242847614943));
#72291=CARTESIAN_POINT('Ctrl Pts',(0.409838858163378,-4.26997608001989,
128.359919057549));
#72292=CARTESIAN_POINT('Ctrl Pts',(0.402078415649149,-4.33644378784913,
128.479887260015));
#72293=CARTESIAN_POINT('Ctrl Pts',(0.394317973134974,-4.39773291854118,
128.602286994891));
#72294=CARTESIAN_POINT('Ctrl Pts',(0.386545072869516,-4.45912043598699,
128.724883216689));
#72295=CARTESIAN_POINT('Ctrl Pts',(0.378772172604079,-4.51531260369357,
128.849918414143));
#72296=CARTESIAN_POINT('Ctrl Pts',(0.370999272338622,-4.56613592001995,
128.976907246778));
#72297=CARTESIAN_POINT('Ctrl Pts',(0.363508936576789,-4.61511168078021,
129.099279715478));
#72298=CARTESIAN_POINT('Ctrl Pts',(0.35601860081495,-4.65910205293616,129.223465955907));
#72299=CARTESIAN_POINT('Ctrl Pts',(0.348528265053119,-4.69799631527375,
129.349020903213));
#72300=CARTESIAN_POINT('Ctrl Pts',(0.343920461147,-4.72192276391672,129.426258105258));
#72301=CARTESIAN_POINT('Ctrl Pts',(0.339312657240903,-4.74395159348324,
129.504109081819));
#72302=CARTESIAN_POINT('Ctrl Pts',(0.334704853334813,-4.76405452823404,
129.582490119308));
#72303=CARTESIAN_POINT('Ctrl Pts',(2.08495204958919,-4.764054528234,129.582490119308));
#72304=CARTESIAN_POINT('Ctrl Pts',(2.07719089070358,-4.79812014789423,129.715311453345));
#72305=CARTESIAN_POINT('Ctrl Pts',(2.06942973181799,-4.82659871089745,129.849448081613));
#72306=CARTESIAN_POINT('Ctrl Pts',(2.06166857293238,-4.84941560315185,129.984390270293));
#72307=CARTESIAN_POINT('Ctrl Pts',(2.05389528092719,-4.87226816534756,130.119543415833));
#72308=CARTESIAN_POINT('Ctrl Pts',(2.04612198892198,-4.88944132443237,130.255504250095));
#72309=CARTESIAN_POINT('Ctrl Pts',(2.03834869691681,-4.90091239245207,130.391758164823));
#72310=CARTESIAN_POINT('Ctrl Pts',(2.03197046725472,-4.91032476320187,130.503558771298));
#72311=CARTESIAN_POINT('Ctrl Pts',(2.0255922375926,-4.9158990529586,130.615556559118));
#72312=CARTESIAN_POINT('Ctrl Pts',(2.01921400793049,-4.91764890054129,130.727468787668));
#72313=CARTESIAN_POINT('Ctrl Pts',(2.01776248395077,-4.9180471216562,130.752937184382));
#72314=CARTESIAN_POINT('Ctrl Pts',(2.01631095997105,-4.9182474941043,130.77840868273));
#72315=CARTESIAN_POINT('Ctrl Pts',(2.01485943599133,-4.91824997664253,130.80388128917));
#72316=CARTESIAN_POINT('',(2.36014056397027,-4.91824811571211,130.808665823057));
#72317=CARTESIAN_POINT('Ctrl Pts',(2.43008709577654,-4.76405452823407,129.582490119308));
#72318=CARTESIAN_POINT('Ctrl Pts',(2.42239270595295,-4.79793465770959,129.714588229931));
#72319=CARTESIAN_POINT('Ctrl Pts',(2.41469831612934,-4.82632054610165,129.848112975725));
#72320=CARTESIAN_POINT('Ctrl Pts',(2.40700392630575,-4.84910659177793,129.982564825367));
#72321=CARTESIAN_POINT('Ctrl Pts',(2.39919336592291,-4.87223666313133,130.119046640598));
#72322=CARTESIAN_POINT('Ctrl Pts',(2.3913828055401,-4.8895963266762,130.25648337292));
#72323=CARTESIAN_POINT('Ctrl Pts',(2.38357224515727,-4.90112943007293,130.394344310362));
#72324=CARTESIAN_POINT('Ctrl Pts',(2.37576168477445,-4.91266253346964,130.532205247804));
#72325=CARTESIAN_POINT('Ctrl Pts',(2.36795112439161,-4.91836906840909,130.670489963754));
#72326=CARTESIAN_POINT('Ctrl Pts',(2.36014056400879,-4.9182481157127,130.808665822376));
#72327=CARTESIAN_POINT('Ctrl Pts',(2.3601405639703,-4.91824811571211,130.808665823057));
#72328=CARTESIAN_POINT('Ctrl Pts',(2.35074923592333,-4.91810268355692,130.974806887574));
#72329=CARTESIAN_POINT('Ctrl Pts',(2.34135790787636,-4.90953504095496,131.140577724705));
#72330=CARTESIAN_POINT('Ctrl Pts',(2.33196657982938,-4.89267991813134,131.305226149635));
#72331=CARTESIAN_POINT('Ctrl Pts',(2.32244488961019,-4.87559082728814,131.472160079471));
#72332=CARTESIAN_POINT('Ctrl Pts',(2.31292319939097,-4.84998263677548,131.637940234447));
#72333=CARTESIAN_POINT('Ctrl Pts',(2.30340150917178,-4.81604479222058,131.801805163305));
#72334=CARTESIAN_POINT('Ctrl Pts',(2.29495855130915,-4.78595183761593,131.947105488948));
#72335=CARTESIAN_POINT('Ctrl Pts',(2.28651559344653,-4.74931041912839,132.090900316533));
#72336=CARTESIAN_POINT('Ctrl Pts',(2.2780726355839,-4.70628375268726,132.23267301396));
#72337=CARTESIAN_POINT('Ctrl Pts',(2.27029830146482,-4.66666450000524,132.363218296394));
#72338=CARTESIAN_POINT('Ctrl Pts',(2.26252396734575,-4.62154668011665,132.49232063557));
#72339=CARTESIAN_POINT('Ctrl Pts',(2.25474963322668,-4.57105216454559,132.619481872883));
#72340=CARTESIAN_POINT('Ctrl Pts',(2.24698488027961,-4.52061987895223,132.746486395335));
#72341=CARTESIAN_POINT('Ctrl Pts',(2.23922012733254,-4.46482422493605,132.87155421588));
#72342=CARTESIAN_POINT('Ctrl Pts',(2.23145537438546,-4.4038371760089,132.994201066024));
#72343=CARTESIAN_POINT('Ctrl Pts',(2.22369833350046,-4.34291070027834,133.116726101587));
#72344=CARTESIAN_POINT('Ctrl Pts',(2.21594129261542,-4.276803263591,133.236834604088));
#72345=CARTESIAN_POINT('Ctrl Pts',(2.20818425173042,-4.2057352418327,133.354061411406));
#72346=CARTESIAN_POINT('Ctrl Pts',(2.20043306049029,-4.13472081302254,133.471199817076));
#72347=CARTESIAN_POINT('Ctrl Pts',(2.19268186925021,-4.05875344687101,133.58546052003));
#72348=CARTESIAN_POINT('Ctrl Pts',(2.18493067801009,-3.97809967125104,133.696402468593));
#72349=CARTESIAN_POINT('Ctrl Pts',(2.17718278123302,-3.89748017563722,133.807297263869));
#72350=CARTESIAN_POINT('Ctrl Pts',(2.16943488445592,-3.81217846160588,133.914875794679));
#72351=CARTESIAN_POINT('Ctrl Pts',(2.16168698767885,-3.72250451984202,134.018725743412));
#72352=CARTESIAN_POINT('Ctrl Pts',(2.15394071159476,-3.63284933593374,134.122553968974));
#72353=CARTESIAN_POINT('Ctrl Pts',(2.14619443551064,-3.53882399879116,134.222654868076));
#72354=CARTESIAN_POINT('Ctrl Pts',(2.13844815942656,-3.44077869514239,134.318649312815));
#72355=CARTESIAN_POINT('Ctrl Pts',(2.13070182616122,-3.34273266774545,134.414644466163));
#72356=CARTESIAN_POINT('Ctrl Pts',(2.12295549289591,-3.24066689398952,134.506532831145));
#72357=CARTESIAN_POINT('Ctrl Pts',(2.11520915963058,-3.13496802444492,134.593972543372));
#72358=CARTESIAN_POINT('Ctrl Pts',(2.10746109162761,-3.02924548437122,134.681431837115));
#72359=CARTESIAN_POINT('Ctrl Pts',(2.09971302362462,-2.91988853071488,134.764440246532));
#72360=CARTESIAN_POINT('Ctrl Pts',(2.09196495562165,-2.80731612456369,134.842696814475));
#72361=CARTESIAN_POINT('Ctrl Pts',(2.08420865287981,-2.69462407511977,134.921036554429));
#72362=CARTESIAN_POINT('Ctrl Pts',(2.07645235013801,-2.5787100680444,134.994614140847));
#72363=CARTESIAN_POINT('Ctrl Pts',(2.06869604739617,-2.46002169227708,135.063172228336));
#72364=CARTESIAN_POINT('Ctrl Pts',(2.06093560488201,-2.34126996894981,135.13176690734));
#72365=CARTESIAN_POINT('Ctrl Pts',(2.05317516236787,-2.21974127264585,135.195336568041));
#72366=CARTESIAN_POINT('Ctrl Pts',(2.04541471985371,-2.09590601572565,135.253670792834));
#72367=CARTESIAN_POINT('Ctrl Pts',(2.0376418195883,-1.97187196745764,135.312098660903));
#72368=CARTESIAN_POINT('Ctrl Pts',(2.02986891932286,-1.84552431996595,135.365274146675));
#72369=CARTESIAN_POINT('Ctrl Pts',(2.02209601905744,-1.71735243752097,135.413035445306));
#72370=CARTESIAN_POINT('Ctrl Pts',(2.01460568329531,-1.59383992584627,135.459060500428));
#72371=CARTESIAN_POINT('Ctrl Pts',(2.00711534753319,-1.46863380034468,135.500058077094));
#72372=CARTESIAN_POINT('Ctrl Pts',(1.99962501177106,-1.34218165470401,135.535928166305));
#72373=CARTESIAN_POINT('Ctrl Pts',(1.99185067765198,-1.21093503752911,135.573158280849));
#72374=CARTESIAN_POINT('Ctrl Pts',(1.98407634353283,-1.07793029949773,135.604982348999));
#72375=CARTESIAN_POINT('Ctrl Pts',(1.97630200941376,-0.943652430089781,
135.631233637823));
#72376=CARTESIAN_POINT('Ctrl Pts',(1.96853725646667,-0.809540046155123,
135.65745257428));
#72377=CARTESIAN_POINT('Ctrl Pts',(1.96077250351963,-0.674158032745218,
135.678112322297));
#72378=CARTESIAN_POINT('Ctrl Pts',(1.95300775057254,-0.53800677454321,135.693095809111));
#72379=CARTESIAN_POINT('Ctrl Pts',(1.94525070968754,-0.401990743690245,
135.708064414113));
#72380=CARTESIAN_POINT('Ctrl Pts',(1.93749366880255,-0.265207374593207,
135.717367934783));
#72381=CARTESIAN_POINT('Ctrl Pts',(1.92973662791755,-0.128167139868283,
135.720940348106));
#72382=CARTESIAN_POINT('Ctrl Pts',(1.92198543667743,0.00876975174943034,
135.724510067444));
#72383=CARTESIAN_POINT('Ctrl Pts',(1.91423424543737,0.145962734187203,135.722357271713));
#72384=CARTESIAN_POINT('Ctrl Pts',(1.90648305419725,0.28289667335303,135.714467799156));
#72385=CARTESIAN_POINT('Ctrl Pts',(1.89873515742017,0.419772411942066,135.706581679836));
#72386=CARTESIAN_POINT('Ctrl Pts',(1.89098726064303,0.556388936739516,135.692963755606));
#72387=CARTESIAN_POINT('Ctrl Pts',(1.88323936386595,0.69223179572312,135.673651962668));
#72388=CARTESIAN_POINT('Ctrl Pts',(1.87549308778186,0.828046239309058,135.654344209341));
#72389=CARTESIAN_POINT('Ctrl Pts',(1.86774681169782,0.963086952150149,135.629345011332));
#72390=CARTESIAN_POINT('Ctrl Pts',(1.86000053561372,1.09684567872519,135.598744062761));
#72391=CARTESIAN_POINT('Ctrl Pts',(1.85225420234838,1.23060539267676,135.568142888301));
#72392=CARTESIAN_POINT('Ctrl Pts',(1.84450786908304,1.36308272036018,135.531939967958));
#72393=CARTESIAN_POINT('Ctrl Pts',(1.83676153581769,1.49378104750507,135.490275815755));
#72394=CARTESIAN_POINT('Ctrl Pts',(1.82901346781471,1.62450864363412,135.448602333153));
#72395=CARTESIAN_POINT('Ctrl Pts',(1.8212653998117,1.75345607404007,135.401465303775));
#72396=CARTESIAN_POINT('Ctrl Pts',(1.81351733180873,1.8801436762501,135.34905453676));
#72397=CARTESIAN_POINT('Ctrl Pts',(1.80576102906687,2.00696592355136,135.296588066958));
#72398=CARTESIAN_POINT('Ctrl Pts',(1.79800472632501,2.13152318301157,135.238836812641));
#72399=CARTESIAN_POINT('Ctrl Pts',(1.79024842358317,2.25335700990883,135.17603824159));
#72400=CARTESIAN_POINT('Ctrl Pts',(1.78248798106899,2.37525586318801,135.113206153051));
#72401=CARTESIAN_POINT('Ctrl Pts',(1.77472753855485,2.4944280479782,135.045321573363));
#72402=CARTESIAN_POINT('Ctrl Pts',(1.76696709604067,2.61044226461746,134.972666537913));
#72403=CARTESIAN_POINT('Ctrl Pts',(1.75919419577525,2.72664271757638,134.899894870149));
#72404=CARTESIAN_POINT('Ctrl Pts',(1.75142129550978,2.83967474944634,134.822337664906));
#72405=CARTESIAN_POINT('Ctrl Pts',(1.74364839524435,2.94913771588834,134.740319178733));
#72406=CARTESIAN_POINT('Ctrl Pts',(1.73615805948226,3.05462142778048,134.661282271124));
#72407=CARTESIAN_POINT('Ctrl Pts',(1.72866772372022,3.15679081930401,134.578103003328));
#72408=CARTESIAN_POINT('Ctrl Pts',(1.72117738795814,3.25531981473364,134.491103891284));
#72409=CARTESIAN_POINT('Ctrl Pts',(1.71340305383905,3.35758456697151,134.400806181464));
#72410=CARTESIAN_POINT('Ctrl Pts',(1.70562871971992,3.45625136653761,134.306107214649));
#72411=CARTESIAN_POINT('Ctrl Pts',(1.69785438560083,3.55091778763522,134.207324903002));
#72412=CARTESIAN_POINT('Ctrl Pts',(1.69008963265374,3.64546754082941,134.108664331726));
#72413=CARTESIAN_POINT('Ctrl Pts',(1.68232487970668,3.73602645708835,134.005930708072));
#72414=CARTESIAN_POINT('Ctrl Pts',(1.67456012675959,3.82222556963625,133.899481739157));
#72415=CARTESIAN_POINT('Ctrl Pts',(1.66680308587459,3.90833906801025,133.793138496859));
#72416=CARTESIAN_POINT('Ctrl Pts',(1.65904604498957,3.99010113555588,133.683087554704));
#72417=CARTESIAN_POINT('Ctrl Pts',(1.65128900410457,4.06718030232289,133.569722700711));
#72418=CARTESIAN_POINT('Ctrl Pts',(1.64353781286444,4.14420134309065,133.456443336036));
#72419=CARTESIAN_POINT('Ctrl Pts',(1.63578662162434,4.21654629320427,133.339855355726));
#72420=CARTESIAN_POINT('Ctrl Pts',(1.62803543038422,4.2839247954175,133.220384501907));
#72421=CARTESIAN_POINT('Ctrl Pts',(1.62028753360714,4.35127465996991,133.100964426388));
#72422=CARTESIAN_POINT('Ctrl Pts',(1.61253963683011,4.4136620833328,132.978664254212));
#72423=CARTESIAN_POINT('Ctrl Pts',(1.60479174005303,4.47084090842272,132.85393731388));
#72424=CARTESIAN_POINT('Ctrl Pts',(1.59704546396892,4.52800777293514,132.729236463735));
#72425=CARTESIAN_POINT('Ctrl Pts',(1.58929918788476,4.57996804347919,132.602110210306));
#72426=CARTESIAN_POINT('Ctrl Pts',(1.58155291180066,4.62652245773492,132.473034645222));
#72427=CARTESIAN_POINT('Ctrl Pts',(1.57380657853531,4.6730772156447,132.343958127332));
#72428=CARTESIAN_POINT('Ctrl Pts',(1.56606024526992,4.71422590499153,132.212932636848));
#72429=CARTESIAN_POINT('Ctrl Pts',(1.55831391200456,4.74981831205854,132.080451940683));
#72430=CARTESIAN_POINT('Ctrl Pts',(1.55056584400159,4.78541868979834,131.947941576384));
#72431=CARTESIAN_POINT('Ctrl Pts',(1.54281777599861,4.8154602078429,131.813975735437));
#72432=CARTESIAN_POINT('Ctrl Pts',(1.53506970799563,4.83984328871408,131.679060567943));
#72433=CARTESIAN_POINT('Ctrl Pts',(1.52731340525377,4.8642522842138,131.544002011003));
#72434=CARTESIAN_POINT('Ctrl Pts',(1.51955710251191,4.88299075957508,131.407992497363));
#72435=CARTESIAN_POINT('Ctrl Pts',(1.51180079977004,4.89601070259675,131.271546086687));
#72436=CARTESIAN_POINT('Ctrl Pts',(1.50404035725587,4.90903759475403,131.135026850454));
#72437=CARTESIAN_POINT('Ctrl Pts',(1.49627991474181,4.91633985209286,130.998070642764));
#72438=CARTESIAN_POINT('Ctrl Pts',(1.48851947222764,4.91792163096898,130.861192775253));
#72439=CARTESIAN_POINT('Ctrl Pts',(1.4807465719622,4.91950594905698,130.724095179238));
#72440=CARTESIAN_POINT('Ctrl Pts',(1.47297367169672,4.91535144993815,130.587076565718));
#72441=CARTESIAN_POINT('Ctrl Pts',(1.46520077143128,4.90551438177984,130.450649276709));
#72442=CARTESIAN_POINT('Ctrl Pts',(1.45771043566926,4.89603491582718,130.319181463294));
#72443=CARTESIAN_POINT('Ctrl Pts',(1.45022009990723,4.88127889381572,130.188263034609));
#72444=CARTESIAN_POINT('Ctrl Pts',(1.44272976414521,4.86134140564454,130.058342655138));
#72445=CARTESIAN_POINT('Ctrl Pts',(1.43495543002614,4.84064798154949,129.92349630499));
#72446=CARTESIAN_POINT('Ctrl Pts',(1.42718109590707,4.81430687399003,129.789298027412));
#72447=CARTESIAN_POINT('Ctrl Pts',(1.419406761788,4.78236803050024,129.656258233913));
#72448=CARTESIAN_POINT('Ctrl Pts',(1.4116420088409,4.75046854878055,129.52338240007));
#72449=CARTESIAN_POINT('Ctrl Pts',(1.40387725589379,4.71298514789539,129.391662586066));
#72450=CARTESIAN_POINT('Ctrl Pts',(1.39611250294669,4.67001934141824,129.261602563534));
#72451=CARTESIAN_POINT('Ctrl Pts',(1.3883554620617,4.62709620918584,129.131671718451));
#72452=CARTESIAN_POINT('Ctrl Pts',(1.3805984211767,4.5787016294047,129.003397753025));
#72453=CARTESIAN_POINT('Ctrl Pts',(1.3728413802917,4.52498773948156,128.877272394354));
#72454=CARTESIAN_POINT('Ctrl Pts',(1.36509018905158,4.47131435562065,128.751242147798));
#72455=CARTESIAN_POINT('Ctrl Pts',(1.35733899781144,4.41232979850282,128.627357641175));
#72456=CARTESIAN_POINT('Ctrl Pts',(1.34958780657132,4.34823531185216,128.506093284277));
#72457=CARTESIAN_POINT('Ctrl Pts',(1.34183990979425,4.2841680670681,128.384880467966));
#72458=CARTESIAN_POINT('Ctrl Pts',(1.33409201301719,4.21499539472103,128.266285931379));
#72459=CARTESIAN_POINT('Ctrl Pts',(1.32634411624011,4.14096563900055,128.150761808568));
#72460=CARTESIAN_POINT('Ctrl Pts',(1.31859784015601,4.06695136870908,128.035261850913));
#72461=CARTESIAN_POINT('Ctrl Pts',(1.31085156407191,3.98808224672641,127.922831358503));
#72462=CARTESIAN_POINT('Ctrl Pts',(1.30310528798782,3.90465111627138,127.813895315527));
#72463=CARTESIAN_POINT('Ctrl Pts',(1.29535895472248,3.82121936994669,127.704958468409));
#72464=CARTESIAN_POINT('Ctrl Pts',(1.28761262145711,3.73322578567249,127.599516432588));
#72465=CARTESIAN_POINT('Ctrl Pts',(1.27986628819176,3.64100458935285,127.497962480195));
#72466=CARTESIAN_POINT('Ctrl Pts',(1.27211822018878,3.54876274073572,127.396385785498));
#72467=CARTESIAN_POINT('Ctrl Pts',(1.26437015218585,3.45229165894575,127.298699196218));
#72468=CARTESIAN_POINT('Ctrl Pts',(1.25662208418288,3.35196335833726,127.2052600762));
#72469=CARTESIAN_POINT('Ctrl Pts',(1.24886578144103,3.25152842761696,127.111721647972));
#72470=CARTESIAN_POINT('Ctrl Pts',(1.24110947869914,3.14722837544775,127.02243997361));
#72471=CARTESIAN_POINT('Ctrl Pts',(1.23335317595729,3.03946974301657,126.937733308943));
#72472=CARTESIAN_POINT('Ctrl Pts',(1.22559273344312,2.93165359655857,126.852981433779));
#72473=CARTESIAN_POINT('Ctrl Pts',(1.21783229092897,2.82037550868685,126.772809662271));
#72474=CARTESIAN_POINT('Ctrl Pts',(1.2100718484148,2.70607127228697,126.697493036087));
#72475=CARTESIAN_POINT('Ctrl Pts',(1.20229894814937,2.59158354457936,126.622055504968));
#72476=CARTESIAN_POINT('Ctrl Pts',(1.19452604788397,2.47406029620333,126.551488895265));
#72477=CARTESIAN_POINT('Ctrl Pts',(1.18675314761853,2.35396297851468,126.486022817175));
#72478=CARTESIAN_POINT('Ctrl Pts',(1.17926281185648,2.23823150083056,126.422936595923));
#72479=CARTESIAN_POINT('Ctrl Pts',(1.1717724760944,2.12011012864133,126.364586646589));
#72480=CARTESIAN_POINT('Ctrl Pts',(1.16428214033235,2.00002773449857,126.31113548146));
#72481=CARTESIAN_POINT('Ctrl Pts',(1.15650780621326,1.875392379884,126.255657699159));
#72482=CARTESIAN_POINT('Ctrl Pts',(1.14873347209425,1.74824955621147,126.205281771962));
#72483=CARTESIAN_POINT('Ctrl Pts',(1.14095913797516,1.61905568500213,126.160241567481));
#72484=CARTESIAN_POINT('Ctrl Pts',(1.13319438502807,1.49002103369284,126.115256871027));
#72485=CARTESIAN_POINT('Ctrl Pts',(1.12542963208091,1.35894072991131,126.075594940872));
#72486=CARTESIAN_POINT('Ctrl Pts',(1.11766487913383,1.22629348156548,126.041442671646));
#72487=CARTESIAN_POINT('Ctrl Pts',(1.10990783824882,1.09377798033653,126.007324322934));
#72488=CARTESIAN_POINT('Ctrl Pts',(1.10215079736381,0.959699007840664,125.978704841931));
#72489=CARTESIAN_POINT('Ctrl Pts',(1.09439375647881,0.824552501997182,125.955722021635));
#72490=CARTESIAN_POINT('Ctrl Pts',(1.08664256523868,0.689507911185042,125.932756532863));
#72491=CARTESIAN_POINT('Ctrl Pts',(1.0788913739985,0.553397773271081,125.915419309418));
#72492=CARTESIAN_POINT('Ctrl Pts',(1.07114018275837,0.416729999798574,125.903797469338));
#72493=CARTESIAN_POINT('Ctrl Pts',(1.06339228598128,0.280120313775526,125.89218056885));
#72494=CARTESIAN_POINT('Ctrl Pts',(1.05564438920424,0.142953852332378,125.886274253309));
#72495=CARTESIAN_POINT('Ctrl Pts',(1.04789649242716,0.00574524475383868,
125.886113973216));
#72496=CARTESIAN_POINT('Ctrl Pts',(1.04015021634305,-0.131434661741871,
125.885953726649));
#72497=CARTESIAN_POINT('Ctrl Pts',(1.03240394025895,-0.268656306120095,
125.891537125248));
#72498=CARTESIAN_POINT('Ctrl Pts',(1.02465766417484,-0.405403848235146,
125.902847506053));
#72499=CARTESIAN_POINT('Ctrl Pts',(1.01691133090949,-0.542152399789303,
125.914157970348));
#72500=CARTESIAN_POINT('Ctrl Pts',(1.00916499764412,-0.678426452462115,
125.93119546898));
#72501=CARTESIAN_POINT('Ctrl Pts',(1.00141866437878,-0.813714478006551,
125.953891381422));
#72502=CARTESIAN_POINT('Ctrl Pts',(0.993670596375804,-0.949032800366286,
125.976592376456));
#72503=CARTESIAN_POINT('Ctrl Pts',(0.98592252837279,-1.08336427070014,126.004954242135));
#72504=CARTESIAN_POINT('Ctrl Pts',(0.978174460369814,-1.21620714583907,
126.038857156135));
#72505=CARTESIAN_POINT('Ctrl Pts',(0.970418157627952,-1.34919120796672,
126.072796102555));
#72506=CARTESIAN_POINT('Ctrl Pts',(0.96266185488617,-1.48068313506388,126.112287764557));
#72507=CARTESIAN_POINT('Ctrl Pts',(0.954905552144311,-1.61019542404568,
126.157162132577));
#72508=CARTESIAN_POINT('Ctrl Pts',(0.94714510963014,-1.73977683763565,126.202060451398));
#72509=CARTESIAN_POINT('Ctrl Pts',(0.939384667115962,-1.86737614420063,
126.25234705748));
#72510=CARTESIAN_POINT('Ctrl Pts',(0.931624224601791,-1.99252638669743,
126.307803972664));
#72511=CARTESIAN_POINT('Ctrl Pts',(0.923851324336356,-2.1178775314738,126.363349912211));
#72512=CARTESIAN_POINT('Ctrl Pts',(0.916078424070928,-2.24077140517934,
126.424082573272));
#72513=CARTESIAN_POINT('Ctrl Pts',(0.908305523805495,-2.36076540452264,
126.489737833671));
#72514=CARTESIAN_POINT('Ctrl Pts',(0.900815188043487,-2.47639731974284,
126.553006359978));
#72515=CARTESIAN_POINT('Ctrl Pts',(0.893324852281462,-2.58933627161709,
126.62084564288));
#72516=CARTESIAN_POINT('Ctrl Pts',(0.885834516519452,-2.69921371786463,
126.692982701612));
#72517=CARTESIAN_POINT('Ctrl Pts',(0.878072281176324,-2.81307972117533,
126.767738339361));
#72518=CARTESIAN_POINT('Ctrl Pts',(0.870310045833136,-2.92402130880819,
126.847348396706));
#72519=CARTESIAN_POINT('Ctrl Pts',(0.862547810490014,-3.03159566656667,
126.931556623435));
#72520=CARTESIAN_POINT('Ctrl Pts',(0.854797860068331,-3.13899977149519,
127.015631577801));
#72521=CARTESIAN_POINT('Ctrl Pts',(0.847047909646632,-3.243046953757,127.10428996848));
#72522=CARTESIAN_POINT('Ctrl Pts',(0.83929795922495,-3.34332224722529,127.197231646527));
#72523=CARTESIAN_POINT('Ctrl Pts',(0.831555098781407,-3.4435058046695,127.290088297647));
#72524=CARTESIAN_POINT('Ctrl Pts',(0.823812238337883,-3.53992405127584,
127.387220176904));
#72525=CARTESIAN_POINT('Ctrl Pts',(0.816069377894337,-3.63219385504037,
127.48828600111));
#72526=CARTESIAN_POINT('Ctrl Pts',(0.808331908080964,-3.72439941996296,
127.589281462626));
#72527=CARTESIAN_POINT('Ctrl Pts',(0.800594438267576,-3.81246202473909,
127.694205131415));
#72528=CARTESIAN_POINT('Ctrl Pts',(0.792856968454203,-3.89603459572387,
127.802678174098));
#72529=CARTESIAN_POINT('Ctrl Pts',(0.785123194005817,-3.97956725299522,
127.911099410765));
#72530=CARTESIAN_POINT('Ctrl Pts',(0.777389419557418,-4.05861390533243,
128.023066337404));
#72531=CARTESIAN_POINT('Ctrl Pts',(0.769655645109026,-4.13286734607665,
128.1381665957));
#72532=CARTESIAN_POINT('Ctrl Pts',(0.761922227772828,-4.20711735811871,
128.253261539166));
#72533=CARTESIAN_POINT('Ctrl Pts',(0.754188810436655,-4.27657437691257,
128.371489202907));
#72534=CARTESIAN_POINT('Ctrl Pts',(0.746455393100462,-4.34097424555394,
128.492407836487));
#72535=CARTESIAN_POINT('Ctrl Pts',(0.738722464723643,-4.40537004239649,
128.613318824767));
#72536=CARTESIAN_POINT('Ctrl Pts',(0.730989536346873,-4.46470914538319,
128.736920095446));
#72537=CARTESIAN_POINT('Ctrl Pts',(0.723256607970058,-4.51877350937329,
128.862745559557));
#72538=CARTESIAN_POINT('Ctrl Pts',(0.715519219511834,-4.57286905578911,
128.988643595376));
#72539=CARTESIAN_POINT('Ctrl Pts',(0.707781831053554,-4.62168363215477,
129.116768025651));
#72540=CARTESIAN_POINT('Ctrl Pts',(0.700044442595328,-4.66504740260424,
129.246632851249));
#72541=CARTESIAN_POINT('Ctrl Pts',(0.693443572619805,-4.7020416173746,129.357422277526));
#72542=CARTESIAN_POINT('Ctrl Pts',(0.686842702644294,-4.73506949653453,
129.469477920621));
#72543=CARTESIAN_POINT('Ctrl Pts',(0.68024183266877,-4.76405452823404,129.582490119308));
#72544=CARTESIAN_POINT('Origin',(213.235140564004,0.,130.804360617566));
#72545=CARTESIAN_POINT('',(-1.41535445211275,-4.764054528234,129.582490119308));
#72546=CARTESIAN_POINT('',(-1.06997321827187,-4.76405452823403,129.582490119308));
#72547=CARTESIAN_POINT('',(213.235140564004,-4.76405452823405,129.582490119308));
#72548=CARTESIAN_POINT('',(0.264859436032587,-4.91824816321245,130.80011002262));
#72549=CARTESIAN_POINT('Ctrl Pts',(0.264859435991383,-4.91824816321308,
130.800110023348));
#72550=CARTESIAN_POINT('Ctrl Pts',(0.257155925891214,-4.91836596679253,
130.936417374421));
#72551=CARTESIAN_POINT('Ctrl Pts',(0.249452415791054,-4.91281295310806,
131.07282508718));
#72552=CARTESIAN_POINT('Ctrl Pts',(0.241748905690883,-4.9015909330034,131.208822467434));
#72553=CARTESIAN_POINT('Ctrl Pts',(0.234047548106026,-4.89037204855636,
131.344781847292));
#72554=CARTESIAN_POINT('Ctrl Pts',(0.226346190521118,-4.87348733670645,
131.480330728431));
#72555=CARTESIAN_POINT('Ctrl Pts',(0.218644832936263,-4.85099066675386,
131.614960773973));
#72556=CARTESIAN_POINT('Ctrl Pts',(0.210944272133467,-4.82849632430558,
131.749576890697));
#72557=CARTESIAN_POINT('Ctrl Pts',(0.203243711330728,-4.80039124349492,
131.883273970466));
#72558=CARTESIAN_POINT('Ctrl Pts',(0.195543150527925,-4.76678081049386,
132.015551670706));
#72559=CARTESIAN_POINT('Ctrl Pts',(0.187841670661972,-4.7331663660823,132.147845158312));
#72560=CARTESIAN_POINT('Ctrl Pts',(0.18014019079599,-4.69404535981923,132.278718545692));
#72561=CARTESIAN_POINT('Ctrl Pts',(0.172438710930038,-4.6495735423203,132.407684956886));
#72562=CARTESIAN_POINT('Ctrl Pts',(0.164734595837766,-4.60508650783633,
132.5366954967));
#72563=CARTESIAN_POINT('Ctrl Pts',(0.157030480745469,-4.55524514874875,
132.663797388243));
#72564=CARTESIAN_POINT('Ctrl Pts',(0.149326365653195,-4.50025383203119,
132.788522533789));
#72565=CARTESIAN_POINT('Ctrl Pts',(0.141613515289472,-4.44520016369075,
132.913389098302));
#72566=CARTESIAN_POINT('Ctrl Pts',(0.13390066492578,-4.38498504005876,133.035873174433));
#72567=CARTESIAN_POINT('Ctrl Pts',(0.126187814562059,-4.31985956285699,
133.155529777727));
#72568=CARTESIAN_POINT('Ctrl Pts',(0.118469949690756,-4.2546917443438,133.27526417573));
#72569=CARTESIAN_POINT('Ctrl Pts',(0.110752084819423,-4.18460741789559,
133.392167101679));
#72570=CARTESIAN_POINT('Ctrl Pts',(0.103034219948114,-4.1099010850809,133.50582246874));
#72571=CARTESIAN_POINT('Ctrl Pts',(0.0953049229631315,-4.03508409325585,
133.619646188202));
#72572=CARTESIAN_POINT('Ctrl Pts',(0.0875756259781753,-3.95563165761873,
133.730212425312));
#72573=CARTESIAN_POINT('Ctrl Pts',(0.0798463289931988,-3.87187887761787,
133.837137730965));
#72574=CARTESIAN_POINT('Ctrl Pts',(0.0765910997421861,-3.83660600612097,
133.882169819046));
#72575=CARTESIAN_POINT('Ctrl Pts',(0.0733358704911794,-3.80057083114038,
133.926556555174));
#72576=CARTESIAN_POINT('Ctrl Pts',(0.0700806412401676,-3.76380028239309,
133.970271307519));
#72577=CARTESIAN_POINT('Ctrl Pts',(0.0623063071210835,-3.67598264816203,
134.074673506092));
#72578=CARTESIAN_POINT('Ctrl Pts',(0.0545319730019769,-3.58367868344521,
134.175584406148));
#72579=CARTESIAN_POINT('Ctrl Pts',(0.0467576388828945,-3.48719655174587,
134.272594068762));
#72580=CARTESIAN_POINT('Ctrl Pts',(0.0389928859358018,-3.39083332565099,
134.369484175636));
#72581=CARTESIAN_POINT('Ctrl Pts',(0.0312281329887449,-3.29030245103418,
134.462482336865));
#72582=CARTESIAN_POINT('Ctrl Pts',(0.0234633800416475,-3.18595267781633,
134.55121110794));
#72583=CARTESIAN_POINT('Ctrl Pts',(0.015706339156641,-3.08170654626431,
134.639851752349));
#72584=CARTESIAN_POINT('Ctrl Pts',(0.00794929827169961,-2.97364936024052,
134.724231193607));
#72585=CARTESIAN_POINT('Ctrl Pts',(0.000192257386686379,-2.86216683999603,
134.804008607393));
#72586=CARTESIAN_POINT('Ctrl Pts',(-0.00755893385344394,-2.75076838958742,
134.883725860411));
#72587=CARTESIAN_POINT('Ctrl Pts',(-0.0153101250936031,-2.63595006306119,
134.958847767025));
#72588=CARTESIAN_POINT('Ctrl Pts',(-0.0230613163337239,-2.51813051216657,
135.029073836969));
#72589=CARTESIAN_POINT('Ctrl Pts',(-0.0308092131108083,-2.40036103772387,
135.099270058959));
#72590=CARTESIAN_POINT('Ctrl Pts',(-0.0385571098879394,-2.27959321111571,
135.164574383199));
#72591=CARTESIAN_POINT('Ctrl Pts',(-0.0463050066650226,-2.15627432320337,
135.224729844858));
#72592=CARTESIAN_POINT('Ctrl Pts',(-0.0540512827491253,-2.03298123094393,
135.284872723292));
#72593=CARTESIAN_POINT('Ctrl Pts',(-0.0617975588331814,-1.90713848995841,
135.339868710118));
#72594=CARTESIAN_POINT('Ctrl Pts',(-0.0695438349172832,-1.77921727302561,
135.389507175515));
#72595=CARTESIAN_POINT('Ctrl Pts',(-0.0772901681826248,-1.65129511180763,
135.439146007331));
#72596=CARTESIAN_POINT('Ctrl Pts',(-0.0850365014479683,-1.52129480851277,
135.483427097366));
#72597=CARTESIAN_POINT('Ctrl Pts',(-0.0927828347133186,-1.38970638314527,
135.522188426118));
#72598=CARTESIAN_POINT('Ctrl Pts',(-0.100530902716305,-1.25808848946211,
135.5609584352));
#72599=CARTESIAN_POINT('Ctrl Pts',(-0.108278970719271,-1.12488214096745,
135.594206112828));
#72600=CARTESIAN_POINT('Ctrl Pts',(-0.116027038722251,-0.990590952417051,
135.621819763993));
#72601=CARTESIAN_POINT('Ctrl Pts',(-0.123783341464108,-0.856157037593378,
135.649462763274));
#72602=CARTESIAN_POINT('Ctrl Pts',(-0.131539644205981,-0.720636363074086,
135.671459695725));
#72603=CARTESIAN_POINT('Ctrl Pts',(-0.13929594694784,-0.58454168832645,
135.687750226957));
#72604=CARTESIAN_POINT('Ctrl Pts',(-0.14705638946202,-0.448374375752984,
135.704049452936));
#72605=CARTESIAN_POINT('Ctrl Pts',(-0.154816831976237,-0.311632842108518,
135.71463617876));
#72606=CARTESIAN_POINT('Ctrl Pts',(-0.162577274490417,-0.17483235037309,
135.719502193529));
#72607=CARTESIAN_POINT('Ctrl Pts',(-0.17035017475585,-0.0378122543439376,
135.724376019658));
#72608=CARTESIAN_POINT('Ctrl Pts',(-0.178123075021275,0.099266597724136,
135.723510785855));
#72609=CARTESIAN_POINT('Ctrl Pts',(-0.185895975286712,0.235890661557176,
135.716950429294));
#72610=CARTESIAN_POINT('Ctrl Pts',(-0.193386311048693,0.367548096533708,
135.710628558218));
#72611=CARTESIAN_POINT('Ctrl Pts',(-0.200876646810635,0.498782927787022,
135.699018466883));
#72612=CARTESIAN_POINT('Ctrl Pts',(-0.208366982572613,0.629144338140574,
135.682204451094));
#72613=CARTESIAN_POINT('Ctrl Pts',(-0.2161413166917,0.764448440991128,135.664752926785));
#72614=CARTESIAN_POINT('Ctrl Pts',(-0.223915650810826,0.899240186732062,
135.64163979345));
#72615=CARTESIAN_POINT('Ctrl Pts',(-0.231689984929915,1.03300811223624,
135.612902735771));
#72616=CARTESIAN_POINT('Ctrl Pts',(-0.239454737877014,1.16661118072741,
135.584201093948));
#72617=CARTESIAN_POINT('Ctrl Pts',(-0.247219490824093,1.29919256094725,
135.5498893997));
#72618=CARTESIAN_POINT('Ctrl Pts',(-0.25498424377119,1.43024619029129,135.51005704824));
#72619=CARTESIAN_POINT('Ctrl Pts',(-0.262741284656176,1.56116965532278,
135.470264258833));
#72620=CARTESIAN_POINT('Ctrl Pts',(-0.270498325541162,1.69056801749238,
135.424961836975));
#72621=CARTESIAN_POINT('Ctrl Pts',(-0.278255366426151,1.81794604042814,
135.374290076167));
#72622=CARTESIAN_POINT('Ctrl Pts',(-0.286006557666269,1.94522800660595,
135.323656527329));
#72623=CARTESIAN_POINT('Ctrl Pts',(-0.29375774890639,2.07049230428448,135.267661842878));
#72624=CARTESIAN_POINT('Ctrl Pts',(-0.301508940146505,2.19325983099465,
135.206495824059));
#72625=CARTESIAN_POINT('Ctrl Pts',(-0.309256836923583,2.3159751782312,135.14535580243));
#72626=CARTESIAN_POINT('Ctrl Pts',(-0.317004733700642,2.43619551592867,
135.07904899198));
#72627=CARTESIAN_POINT('Ctrl Pts',(-0.324752630477718,2.55346288066148,
135.007812815413));
#72628=CARTESIAN_POINT('Ctrl Pts',(-0.332498906561814,2.67070571558959,
134.936591539918));
#72629=CARTESIAN_POINT('Ctrl Pts',(-0.340245182645885,2.78499647225651,
134.860443152107));
#72630=CARTESIAN_POINT('Ctrl Pts',(-0.347991458729979,2.89590326143027,
134.779650212418));
#72631=CARTESIAN_POINT('Ctrl Pts',(-0.355737791995302,3.00681086929244,
134.698856676334));
#72632=CARTESIAN_POINT('Ctrl Pts',(-0.363484125260661,3.11433414380964,
134.613418750162));
#72633=CARTESIAN_POINT('Ctrl Pts',(-0.371230458525986,3.21807190560325,
134.523661126112));
#72634=CARTESIAN_POINT('Ctrl Pts',(-0.378978526528957,3.32183289874962,
134.433883401463));
#72635=CARTESIAN_POINT('Ctrl Pts',(-0.386726594531866,3.42180639666844,
134.339784309752));
#72636=CARTESIAN_POINT('Ctrl Pts',(-0.394474662534833,3.51762621110825,
134.241727182456));
#72637=CARTESIAN_POINT('Ctrl Pts',(-0.402230965276666,3.61354786398699,
134.143565838878));
#72638=CARTESIAN_POINT('Ctrl Pts',(-0.409987268018584,3.70530674109778,
134.041438336555));
#72639=CARTESIAN_POINT('Ctrl Pts',(-0.417743570760422,3.7925749223932,133.935743462338));
#72640=CARTESIAN_POINT('Ctrl Pts',(-0.42550401327457,3.87988968134458,133.829992175584));
#72641=CARTESIAN_POINT('Ctrl Pts',(-0.433264455788733,3.96270873264421,
133.720670034511));
#72642=CARTESIAN_POINT('Ctrl Pts',(-0.441024898302885,4.04074665600303,
133.608206106265));
#72643=CARTESIAN_POINT('Ctrl Pts',(-0.448797798568311,4.11890985276441,
133.495561640938));
#72644=CARTESIAN_POINT('Ctrl Pts',(-0.456570698833782,4.19227637494115,
133.379765640413));
#72645=CARTESIAN_POINT('Ctrl Pts',(-0.464343599099209,4.26060560489768,
133.261273913149));
#72646=CARTESIAN_POINT('Ctrl Pts',(-0.471833934861339,4.32645089523526,
133.147089658633));
#72647=CARTESIAN_POINT('Ctrl Pts',(-0.47932427062341,4.38761862846298,133.030402540375));
#72648=CARTESIAN_POINT('Ctrl Pts',(-0.486814606385536,4.44393604733321,
132.911637407575));
#72649=CARTESIAN_POINT('Ctrl Pts',(-0.494588940504623,4.50238875825648,
132.78836925867));
#72650=CARTESIAN_POINT('Ctrl Pts',(-0.502363274623689,4.55580125562843,
132.66247193234));
#72651=CARTESIAN_POINT('Ctrl Pts',(-0.510137608742781,4.60392878632553,
132.534396106492));
#72652=CARTESIAN_POINT('Ctrl Pts',(-0.517902361689883,4.65199700414232,
132.406478122652));
#72653=CARTESIAN_POINT('Ctrl Pts',(-0.525667114636987,4.6947930785036,132.276387343723));
#72654=CARTESIAN_POINT('Ctrl Pts',(-0.533431867584085,4.73211868093234,
132.144597854801));
#72655=CARTESIAN_POINT('Ctrl Pts',(-0.541188908469091,4.76940721104654,
132.012939261057));
#72656=CARTESIAN_POINT('Ctrl Pts',(-0.548945949354093,4.80123597598984,
131.879585688624));
#72657=CARTESIAN_POINT('Ctrl Pts',(-0.556702990239103,4.82745532130159,
131.745029625952));
#72658=CARTESIAN_POINT('Ctrl Pts',(-0.564454181479197,4.85365489440094,
131.610575033053));
#72659=CARTESIAN_POINT('Ctrl Pts',(-0.57220537271931,4.8742533931664,131.474920137056));
#72660=CARTESIAN_POINT('Ctrl Pts',(-0.579956563959399,4.88915153617268,
131.338570612643));
#72661=CARTESIAN_POINT('Ctrl Pts',(-0.587704460736484,4.90404334707083,
131.202279040415));
#72662=CARTESIAN_POINT('Ctrl Pts',(-0.595452357513553,4.91323957860379,
131.065293814811));
#72663=CARTESIAN_POINT('Ctrl Pts',(-0.603200254290641,4.91669244079701,
130.928128566202));
#72664=CARTESIAN_POINT('Ctrl Pts',(-0.610946530374749,4.92014458072589,
130.790992009606));
#72665=CARTESIAN_POINT('Ctrl Pts',(-0.618692806458852,4.9178557311113,130.6536758955));
#72666=CARTESIAN_POINT('Ctrl Pts',(-0.626439082542959,4.90983017137331,
130.516696315345));
#72667=CARTESIAN_POINT('Ctrl Pts',(-0.634185415808306,4.90180455239248,
130.379715724038));
#72668=CARTESIAN_POINT('Ctrl Pts',(-0.641931749073644,4.88804216165495,
130.243072061936));
#72669=CARTESIAN_POINT('Ctrl Pts',(-0.649678082338994,4.86859932465799,
130.107278356682));
#72670=CARTESIAN_POINT('Ctrl Pts',(-0.65742615034198,4.84915213357247,129.971454241368));
#72671=CARTESIAN_POINT('Ctrl Pts',(-0.665174218344999,4.82402202030502,
129.836480848604));
#72672=CARTESIAN_POINT('Ctrl Pts',(-0.672922286347983,4.79331673222229,
129.702862652476));
#72673=CARTESIAN_POINT('Ctrl Pts',(-0.680678589089834,4.76257881019404,
129.569102445339));
#72674=CARTESIAN_POINT('Ctrl Pts',(-0.688434891831638,4.72625396450211,
129.43670069367));
#72675=CARTESIAN_POINT('Ctrl Pts',(-0.696191194573487,4.68450045702273,
129.306148839928));
#72676=CARTESIAN_POINT('Ctrl Pts',(-0.703951637087657,4.64272466443918,
129.17552730673));
#72677=CARTESIAN_POINT('Ctrl Pts',(-0.711712079601864,4.59551457118554,
129.046758005722));
#72678=CARTESIAN_POINT('Ctrl Pts',(-0.719472522116035,4.5430768869658,128.92031299035));
#72679=CARTESIAN_POINT('Ctrl Pts',(-0.72724542238147,4.49055502512016,128.793664994214));
#72680=CARTESIAN_POINT('Ctrl Pts',(-0.735018322646873,4.43278896767901,
128.669349094501));
#72681=CARTESIAN_POINT('Ctrl Pts',(-0.742791222912302,4.37003213949743,
128.547814105247));
#72682=CARTESIAN_POINT('Ctrl Pts',(-0.750281558674329,4.30955668009515,
128.43069721898));
#72683=CARTESIAN_POINT('Ctrl Pts',(-0.757771894436371,4.24444715666911,
128.316162834997));
#72684=CARTESIAN_POINT('Ctrl Pts',(-0.765262230198402,4.1749676273715,128.204585940233));
#72685=CARTESIAN_POINT('Ctrl Pts',(-0.773036564317499,4.10285376060263,
128.088778573591));
#72686=CARTESIAN_POINT('Ctrl Pts',(-0.780810898436576,4.02580353386628,
127.975790546737));
#72687=CARTESIAN_POINT('Ctrl Pts',(-0.788585232555675,3.9440638202062,127.866071379822));
#72688=CARTESIAN_POINT('Ctrl Pts',(-0.796349985502775,3.86242484343802,
127.756487431975));
#72689=CARTESIAN_POINT('Ctrl Pts',(-0.80411473844991,3.77610811030726,127.650164638912));
#72690=CARTESIAN_POINT('Ctrl Pts',(-0.811879491397008,3.6854052806458,127.547526114573));
#72691=CARTESIAN_POINT('Ctrl Pts',(-0.819636532282004,3.59479253831357,
127.444989532263));
#72692=CARTESIAN_POINT('Ctrl Pts',(-0.827393573166975,3.49980262596916,
127.346130227637));
#72693=CARTESIAN_POINT('Ctrl Pts',(-0.835150614051969,3.40076899620152,
127.251340311267));
#72694=CARTESIAN_POINT('Ctrl Pts',(-0.842901805292132,3.30181004846391,
127.15662187671));
#72695=CARTESIAN_POINT('Ctrl Pts',(-0.850652996532273,3.19881373424288,
127.065966991476));
#72696=CARTESIAN_POINT('Ctrl Pts',(-0.858404187772436,3.09215182793659,
126.979732513359));
#72697=CARTESIAN_POINT('Ctrl Pts',(-0.86615208454952,2.98553525578622,126.893534687197));
#72698=CARTESIAN_POINT('Ctrl Pts',(-0.873899981326623,2.87525649363664,
126.811753776668));
#72699=CARTESIAN_POINT('Ctrl Pts',(-0.881647878103706,2.76172184161628,
126.734707618594));
#72700=CARTESIAN_POINT('Ctrl Pts',(-0.889394154187809,2.6482109385976,126.657677576916));
#72701=CARTESIAN_POINT('Ctrl Pts',(-0.897140430271968,2.53144582368067,
126.585380537113));
#72702=CARTESIAN_POINT('Ctrl Pts',(-0.904886706356081,2.41186301235968,
126.518091858831));
#72703=CARTESIAN_POINT('Ctrl Pts',(-0.912633039621454,2.29227931830538,
126.450802683838));
#72704=CARTESIAN_POINT('Ctrl Pts',(-0.920379372886749,2.1698782270702,126.388522135864));
#72705=CARTESIAN_POINT('Ctrl Pts',(-0.928125706152116,2.04512180864695,
126.331480130643));
#72706=CARTESIAN_POINT('Ctrl Pts',(-0.935873774155067,1.92033745188947,
126.274425351261));
#72707=CARTESIAN_POINT('Ctrl Pts',(-0.94362184215799,1.79319707385472,126.222611611578));
#72708=CARTESIAN_POINT('Ctrl Pts',(-0.951369910160935,1.66418334296127,
126.176220941248));
#72709=CARTESIAN_POINT('Ctrl Pts',(-0.959126212902788,1.53503249473883,
126.129780966361));
#72710=CARTESIAN_POINT('Ctrl Pts',(-0.966882515644722,1.4040046848675,126.088775706945));
#72711=CARTESIAN_POINT('Ctrl Pts',(-0.97463881838658,1.27159892221444,126.053337649455));
#72712=CARTESIAN_POINT('Ctrl Pts',(-0.982399260900771,1.13912249061884,
126.017880677605));
#72713=CARTESIAN_POINT('Ctrl Pts',(-0.990159703414939,1.00526702217028,
125.987996913559));
#72714=CARTESIAN_POINT('Ctrl Pts',(-0.997920145929129,0.870541400446195,
125.963767603006));
#72715=CARTESIAN_POINT('Ctrl Pts',(-1.00569304619457,0.735599505193924,
125.939499397412));
#72716=CARTESIAN_POINT('Ctrl Pts',(-1.01346594646001,0.599785052894364,
125.920903837178));
#72717=CARTESIAN_POINT('Ctrl Pts',(-1.02123884672545,0.46361262583191,125.908010303744));
#72718=CARTESIAN_POINT('Ctrl Pts',(-1.02872918248739,0.332390409492662,
125.895585482727));
#72719=CARTESIAN_POINT('Ctrl Pts',(-1.0362195182493,0.200836100666851,125.888455336582));
#72720=CARTESIAN_POINT('Ctrl Pts',(-1.04370985401124,0.0694079163645821,
125.886600395306));
#72721=CARTESIAN_POINT('Ctrl Pts',(-1.0514841881303,-0.0670034074939693,
125.884675123367));
#72722=CARTESIAN_POINT('Ctrl Pts',(-1.0592585222494,-0.203710964080631,
125.888426872895));
#72723=CARTESIAN_POINT('Ctrl Pts',(-1.06703285636848,-0.340203118451164,
125.897890919229));
#72724=CARTESIAN_POINT('Ctrl Pts',(-1.07479760931557,-0.476527058439906,
125.907343301972));
#72725=CARTESIAN_POINT('Ctrl Pts',(-1.08256236226268,-0.612635738122209,
125.922493947443));
#72726=CARTESIAN_POINT('Ctrl Pts',(-1.09032711520976,-0.748015530494374,
125.943326177384));
#72727=CARTESIAN_POINT('Ctrl Pts',(-1.09808415609477,-0.883260861748602,
125.96413771646));
#72728=CARTESIAN_POINT('Ctrl Pts',(-1.10584119697979,-1.01777836245176,
125.990619551047));
#72729=CARTESIAN_POINT('Ctrl Pts',(-1.11359823786481,-1.15105789960446,
126.022703083378));
#72730=CARTESIAN_POINT('Ctrl Pts',(-1.12134942910496,-1.28423692962162,
126.054762421268));
#72731=CARTESIAN_POINT('Ctrl Pts',(-1.12910062034512,-1.41617947570971,
126.092414957592));
#72732=CARTESIAN_POINT('Ctrl Pts',(-1.13685181158527,-1.5463843501568,126.135540798373));
#72733=CARTESIAN_POINT('Ctrl Pts',(-1.14459970836237,-1.67653388405874,
126.178648309521));
#72734=CARTESIAN_POINT('Ctrl Pts',(-1.15234760513948,-1.80494684489254,
126.227224375624));
#72735=CARTESIAN_POINT('Ctrl Pts',(-1.16009550191657,-1.93113621239599,
126.281098963442));
#72736=CARTESIAN_POINT('Ctrl Pts',(-1.16784177800068,-2.05729918380391,
126.334962281856));
#72737=CARTESIAN_POINT('Ctrl Pts',(-1.17558805408473,-2.18123912770745,
126.394121764029));
#72738=CARTESIAN_POINT('Ctrl Pts',(-1.18333433016883,-2.30248842895252,
126.458358995726));
#72739=CARTESIAN_POINT('Ctrl Pts',(-1.1910806634342,-2.42373862523256,126.522596701607));
#72740=CARTESIAN_POINT('Ctrl Pts',(-1.19882699669964,-2.54229779374591,
126.591912048775));
#72741=CARTESIAN_POINT('Ctrl Pts',(-1.20657332996501,-2.65772273975424,
126.666040559729));
#72742=CARTESIAN_POINT('Ctrl Pts',(-1.214321397968,-2.77317353437893,126.74018567125));
#72743=CARTESIAN_POINT('Ctrl Pts',(-1.22206946597092,-2.88548838092046,
126.819145880174));
#72744=CARTESIAN_POINT('Ctrl Pts',(-1.22981753397391,-2.99425323860536,
126.902613495365));
#72745=CARTESIAN_POINT('Ctrl Pts',(-1.23757383671577,-3.10313369287517,
126.986169820931));
#72746=CARTESIAN_POINT('Ctrl Pts',(-1.24533013945765,-3.20845631071841,
127.074242883953));
#72747=CARTESIAN_POINT('Ctrl Pts',(-1.2530864421995,-3.30983990104797,127.166484466303));
#72748=CARTESIAN_POINT('Ctrl Pts',(-1.2608468847137,-3.41127760285271,127.258775280762));
#72749=CARTESIAN_POINT('Ctrl Pts',(-1.26860732722794,-3.50877181019504,
127.355238772934));
#72750=CARTESIAN_POINT('Ctrl Pts',(-1.27636776974214,-3.60197910477145,
127.45549071993));
#72751=CARTESIAN_POINT('Ctrl Pts',(-1.28414067000757,-3.69533602397128,
127.555903600252));
#72752=CARTESIAN_POINT('Ctrl Pts',(-1.29191357027294,-3.78439202437051,
127.660116790908));
#72753=CARTESIAN_POINT('Ctrl Pts',(-1.29968647053838,-3.86884424223603,
127.767713240636));
#72754=CARTESIAN_POINT('Ctrl Pts',(-1.30717680630035,-3.95022640925926,
127.871398288396));
#72755=CARTESIAN_POINT('Ctrl Pts',(-1.31466714206236,-4.02733352046038,
127.978224636069));
#72756=CARTESIAN_POINT('Ctrl Pts',(-1.32215747782433,-4.09993427901852,
128.087796248693));
#72757=CARTESIAN_POINT('Ctrl Pts',(-1.33007845192884,-4.1767090387597,128.203667410383));
#72758=CARTESIAN_POINT('Ctrl Pts',(-1.33799942603336,-4.24868068094989,
128.322965474712));
#72759=CARTESIAN_POINT('Ctrl Pts',(-1.34592040013786,-4.31553515966779,
128.445263470738));
#72760=CARTESIAN_POINT('Ctrl Pts',(-1.3538315769244,-4.38230694721971,128.567410198456));
#72761=CARTESIAN_POINT('Ctrl Pts',(-1.36174275371097,-4.44397398948351,
128.692549151836));
#72762=CARTESIAN_POINT('Ctrl Pts',(-1.36965393049752,-4.50026481313829,
128.820223607647));
#72763=CARTESIAN_POINT('Ctrl Pts',(-1.37755394090117,-4.55647618402545,
128.947717854888));
#72764=CARTESIAN_POINT('Ctrl Pts',(-1.38545395130488,-4.60732630606783,
129.077740137057));
#72765=CARTESIAN_POINT('Ctrl Pts',(-1.39335396170856,-4.65258938362391,
129.209808928253));
#72766=CARTESIAN_POINT('Ctrl Pts',(-1.40068745851,-4.69460662379444,129.332407001967));
#72767=CARTESIAN_POINT('Ctrl Pts',(-1.40802095531133,-4.73180972531184,
129.456768122098));
#72768=CARTESIAN_POINT('Ctrl Pts',(-1.41535445211275,-4.764054528234,129.582490119308));
#72769=CARTESIAN_POINT('Ctrl Pts',(0.334704853334813,-4.76405452823404,
129.582490119308));
#72770=CARTESIAN_POINT('Ctrl Pts',(0.325259123083958,-4.80526437630398,
129.743166691486));
#72771=CARTESIAN_POINT('Ctrl Pts',(0.315813392833079,-4.83837810705644,
129.906072091631));
#72772=CARTESIAN_POINT('Ctrl Pts',(0.306367662582232,-4.86318687792424,
130.070469308934));
#72773=CARTESIAN_POINT('Ctrl Pts',(0.297037133478273,-4.8876930783416,130.232861520009));
#72774=CARTESIAN_POINT('Ctrl Pts',(0.287706604374324,-4.9040956196616,130.396709380425));
#72775=CARTESIAN_POINT('Ctrl Pts',(0.27837607527033,-4.91223936948906,130.561281537138));
#72776=CARTESIAN_POINT('Ctrl Pts',(0.273870528857723,-4.91617184131476,
130.640750502084));
#72777=CARTESIAN_POINT('Ctrl Pts',(0.269364982445099,-4.91817926350584,
130.720388040219));
#72778=CARTESIAN_POINT('Ctrl Pts',(0.264859436032481,-4.91824816321245,
130.80011002262));
#72779=CARTESIAN_POINT('',(0.610140564062025,-4.91824999063408,130.80466414335));
#72780=CARTESIAN_POINT('Ctrl Pts',(0.68024183266877,-4.76405452823404,129.582490119308));
#72781=CARTESIAN_POINT('Ctrl Pts',(0.672495220846975,-4.79807061854507,
129.715118339165));
#72782=CARTESIAN_POINT('Ctrl Pts',(0.664748609025191,-4.82651737018263,
129.849063881117));
#72783=CARTESIAN_POINT('Ctrl Pts',(0.657001997203395,-4.84931889002808,
129.983818500843));
#72784=CARTESIAN_POINT('Ctrl Pts',(0.649191758346509,-4.87230769085994,
130.119679931793));
#72785=CARTESIAN_POINT('Ctrl Pts',(0.641381519489651,-4.88955806601628,
130.256363385809));
#72786=CARTESIAN_POINT('Ctrl Pts',(0.633571280632765,-4.90104574451915,
130.393345201029));
#72787=CARTESIAN_POINT('Ctrl Pts',(0.625761041775879,-4.91253342302202,
130.53032701625));
#72788=CARTESIAN_POINT('Ctrl Pts',(0.617950802918943,-4.91825844901687,
130.66760678831));
#72789=CARTESIAN_POINT('Ctrl Pts',(0.610140564062078,-4.91824999063408,
130.80466414335));
#72790=CARTESIAN_POINT('Ctrl Pts',(0.610140564008816,-4.91824999063402,
130.804664144283));
#72791=CARTESIAN_POINT('Ctrl Pts',(0.609222673574721,-4.91824899656807,
130.820771671519));
#72792=CARTESIAN_POINT('Ctrl Pts',(0.608304783140653,-4.91816887329494,
130.836878914827));
#72793=CARTESIAN_POINT('Ctrl Pts',(0.607386892706558,-4.91800962743144,
130.852985374549));
#72794=CARTESIAN_POINT('Ctrl Pts',(0.599612558587471,-4.91666084929413,
130.989403616534));
#72795=CARTESIAN_POINT('Ctrl Pts',(0.591838224468402,-4.90962957576278,
131.125981773078));
#72796=CARTESIAN_POINT('Ctrl Pts',(0.584063890349313,-4.89689281948563,
131.262207510064));
#72797=CARTESIAN_POINT('Ctrl Pts',(0.576299137402214,-4.88417176012228,
131.398265361004));
#72798=CARTESIAN_POINT('Ctrl Pts',(0.568534384455138,-4.86575924464363,
131.533971271033));
#72799=CARTESIAN_POINT('Ctrl Pts',(0.560769631508037,-4.84168427213609,
131.668812161292));
#72800=CARTESIAN_POINT('Ctrl Pts',(0.553012590623038,-4.81763321123067,
131.803519125678));
#72801=CARTESIAN_POINT('Ctrl Pts',(0.545255549737985,-4.7879309536471,131.937362397652));
#72802=CARTESIAN_POINT('Ctrl Pts',(0.537498508852991,-4.75265831918086,
132.069833637279));
#72803=CARTESIAN_POINT('Ctrl Pts',(0.52974731761287,-4.71741228408266,132.202204979313));
#72804=CARTESIAN_POINT('Ctrl Pts',(0.521996126372786,-4.67660433345869,
132.333205972155));
#72805=CARTESIAN_POINT('Ctrl Pts',(0.514244935132666,-4.63036635388174,
132.462338449547));
#72806=CARTESIAN_POINT('Ctrl Pts',(0.506497038355583,-4.58414802667949,
132.591416042191));
#72807=CARTESIAN_POINT('Ctrl Pts',(0.498749141578544,-4.5325043922969,132.718626331617));
#72808=CARTESIAN_POINT('Ctrl Pts',(0.491001244801453,-4.47561712215223,
132.843486518142));
#72809=CARTESIAN_POINT('Ctrl Pts',(0.483254968717341,-4.41874175159812,
132.968320586606));
#72810=CARTESIAN_POINT('Ctrl Pts',(0.47550869263321,-4.35662508898079,133.090805174417));
#72811=CARTESIAN_POINT('Ctrl Pts',(0.467762416549107,-4.28949670711112,
133.210478042419));
#72812=CARTESIAN_POINT('Ctrl Pts',(0.460016083283763,-4.22236782971507,
133.33015179382));
#72813=CARTESIAN_POINT('Ctrl Pts',(0.452269750018361,-4.15022735051399,
133.447013443013));
#72814=CARTESIAN_POINT('Ctrl Pts',(0.444523416753015,-4.07335030629657,
133.56062626962));
#72815=CARTESIAN_POINT('Ctrl Pts',(0.436775348750042,-3.99645604599812,
133.674264539032));
#72816=CARTESIAN_POINT('Ctrl Pts',(0.429027280747135,-3.91482332903275,
133.784652214376));
#72817=CARTESIAN_POINT('Ctrl Pts',(0.421279212744167,-3.82876969376594,
133.891382757849));
#72818=CARTESIAN_POINT('Ctrl Pts',(0.413522910002312,-3.7426245996714,133.998226735815));
#72819=CARTESIAN_POINT('Ctrl Pts',(0.405766607260464,-3.6520494470938,134.101405512678));
#72820=CARTESIAN_POINT('Ctrl Pts',(0.398010304518607,-3.55740150141835,
134.2005463634));
#72821=CARTESIAN_POINT('Ctrl Pts',(0.390249862004428,-3.46270303928437,
134.299740128579));
#72822=CARTESIAN_POINT('Ctrl Pts',(0.382489419490209,-3.36392773406066,
134.394891402165));
#72823=CARTESIAN_POINT('Ctrl Pts',(0.37472897697603,-3.26146793907907,134.485666085041));
#72824=CARTESIAN_POINT('Ctrl Pts',(0.366956076710598,-3.15884366653876,
134.576586487495));
#72825=CARTESIAN_POINT('Ctrl Pts',(0.359183176445221,-3.05252338825171,
134.663116012738));
#72826=CARTESIAN_POINT('Ctrl Pts',(0.351410276179791,-2.94293130327465,
134.744961892334));
#72827=CARTESIAN_POINT('Ctrl Pts',(0.343919940417796,-2.83732316663275,
134.823832468049));
#72828=CARTESIAN_POINT('Ctrl Pts',(0.336429604655745,-2.7286772242474,134.898353836516));
#72829=CARTESIAN_POINT('Ctrl Pts',(0.328939268893748,-2.61739494751692,
134.968304271269));
#72830=CARTESIAN_POINT('Ctrl Pts',(0.321164934774717,-2.50189336944019,
135.040906898017));
#72831=CARTESIAN_POINT('Ctrl Pts',(0.313390600655622,-2.38318572315328,
135.108815118178));
#72832=CARTESIAN_POINT('Ctrl Pts',(0.305616266536532,-2.26169062463364,
135.171732662737));
#72833=CARTESIAN_POINT('Ctrl Pts',(0.297851513589432,-2.14034525796458,
135.234572667047));
#72834=CARTESIAN_POINT('Ctrl Pts',(0.290086760642295,-2.0162196180991,135.292434055477));
#72835=CARTESIAN_POINT('Ctrl Pts',(0.2823220076952,-1.88976104752747,135.345063894124));
#72836=CARTESIAN_POINT('Ctrl Pts',(0.274564966810206,-1.76342807739106,
135.397641460074));
#72837=CARTESIAN_POINT('Ctrl Pts',(0.26680792592523,-1.63476714629866,135.444997667363));
#72838=CARTESIAN_POINT('Ctrl Pts',(0.259050885040239,-1.50424962010937,
135.486925741822));
#72839=CARTESIAN_POINT('Ctrl Pts',(0.25129969380011,-1.37383051820168,135.528822197994));
#72840=CARTESIAN_POINT('Ctrl Pts',(0.243548502559989,-1.24155797868094,
135.565298549901));
#72841=CARTESIAN_POINT('Ctrl Pts',(0.235797311319857,-1.10792241084239,
135.596196486422));
#72842=CARTESIAN_POINT('Ctrl Pts',(0.228049414542771,-0.974343641685012,
135.627081290495));
#72843=CARTESIAN_POINT('Ctrl Pts',(0.220301517765705,-0.839403376558608,
135.652392306984));
#72844=CARTESIAN_POINT('Ctrl Pts',(0.212553620988615,-0.703606006349638,
135.672021416176));
#72845=CARTESIAN_POINT('Ctrl Pts',(0.204807344904506,-0.567837042023063,
135.691646419382));
#72846=CARTESIAN_POINT('Ctrl Pts',(0.197061068820377,-0.43121171592598,
135.705591823451));
#72847=CARTESIAN_POINT('Ctrl Pts',(0.189314792736269,-0.29424301266107,
135.713800922937));
#72848=CARTESIAN_POINT('Ctrl Pts',(0.181568459470911,-0.157273298324307,
135.722010083021));
#72849=CARTESIAN_POINT('Ctrl Pts',(0.173822126205588,-0.0199605920267424,
135.724482830638));
#72850=CARTESIAN_POINT('Ctrl Pts',(0.166075792940234,0.117179016906247,
135.721214503995));
#72851=CARTESIAN_POINT('Ctrl Pts',(0.158327724937254,0.254349337303797,
135.717945445434));
#72852=CARTESIAN_POINT('Ctrl Pts',(0.150579656934228,0.391346092421572,
135.708932763584));
#72853=CARTESIAN_POINT('Ctrl Pts',(0.142831588931244,0.527655613250902,
135.694223868855));
#72854=CARTESIAN_POINT('Ctrl Pts',(0.135075286189384,0.664110005461073,
135.679499341337));
#72855=CARTESIAN_POINT('Ctrl Pts',(0.127318983447537,0.799875315000086,
135.659066549428));
#72856=CARTESIAN_POINT('Ctrl Pts',(0.119562680705684,0.93444484706951,135.633024603627));
#72857=CARTESIAN_POINT('Ctrl Pts',(0.11180223819152,1.06908620295001,135.606968758456));
#72858=CARTESIAN_POINT('Ctrl Pts',(0.104041795677362,1.20253012943633,135.575297884282));
#72859=CARTESIAN_POINT('Ctrl Pts',(0.0962813531631923,1.33428346291893,
135.538161490341));
#72860=CARTESIAN_POINT('Ctrl Pts',(0.0885084528977593,1.46624829854894,
135.500965481763));
#72861=CARTESIAN_POINT('Ctrl Pts',(0.0807355526322801,1.59651674621076,
135.458286542488));
#72862=CARTESIAN_POINT('Ctrl Pts',(0.0729626523668401,1.72461320157617,
135.410323314706));
#72863=CARTESIAN_POINT('Ctrl Pts',(0.0654723166047607,1.84805302813424,
135.364103671066));
#72864=CARTESIAN_POINT('Ctrl Pts',(0.0579819808427547,1.9694757516654,135.312977382666));
#72865=CARTESIAN_POINT('Ctrl Pts',(0.0504916450806832,2.08847782231686,
135.257162370192));
#72866=CARTESIAN_POINT('Ctrl Pts',(0.0427173109615991,2.21199189264627,
135.199231114556));
#72867=CARTESIAN_POINT('Ctrl Pts',(0.0349429768424324,2.333289383942,135.136065061507));
#72868=CARTESIAN_POINT('Ctrl Pts',(0.0271686427233533,2.45189476453013,
135.067856263884));
#72869=CARTESIAN_POINT('Ctrl Pts',(0.0194038897762637,2.57035397458675,
134.999731527507));
#72870=CARTESIAN_POINT('Ctrl Pts',(0.0116391368293173,2.68612733967731,
134.926576605057));
#72871=CARTESIAN_POINT('Ctrl Pts',(0.00387438388221995,2.79876025980233,
134.848631141486));
#72872=CARTESIAN_POINT('Ctrl Pts',(-0.00388265700278655,2.91128131132324,
134.770763094449));
#72873=CARTESIAN_POINT('Ctrl Pts',(-0.0116396978878533,3.02066780568661,
134.688114196033));
#72874=CARTESIAN_POINT('Ctrl Pts',(-0.0193967387728549,3.12649099316675,
134.600969253197));
#72875=CARTESIAN_POINT('Ctrl Pts',(-0.0271479300129735,3.2322343785579,
134.51389002704));
#72876=CARTESIAN_POINT('Ctrl Pts',(-0.034899121253116,3.33441950502844,
134.422321752578));
#72877=CARTESIAN_POINT('Ctrl Pts',(-0.0426503124932367,3.43264810274518,
134.326591454013));
#72878=CARTESIAN_POINT('Ctrl Pts',(-0.0503982092703211,3.53083495068769,
134.230901843379));
#72879=CARTESIAN_POINT('Ctrl Pts',(-0.0581461060473619,3.62506833510517,
134.131053999289));
#72880=CARTESIAN_POINT('Ctrl Pts',(-0.0658940028244501,3.71498465622671,
134.027413838737));
#72881=CARTESIAN_POINT('Ctrl Pts',(-0.0736402789085579,3.80488216879225,
133.923795357472));
#72882=CARTESIAN_POINT('Ctrl Pts',(-0.0813865549926884,3.89046415820408,
133.816386432731));
#72883=CARTESIAN_POINT('Ctrl Pts',(-0.089132831076796,3.97140563585688,
133.705588002309));
#72884=CARTESIAN_POINT('Ctrl Pts',(-0.096879164342154,4.05234771100129,
133.594788753999));
#72885=CARTESIAN_POINT('Ctrl Pts',(-0.104625497607482,4.12864897540637,
133.48060026578));
#72886=CARTESIAN_POINT('Ctrl Pts',(-0.112371830872831,4.2000265480877,133.363454218406));
#72887=CARTESIAN_POINT('Ctrl Pts',(-0.120119898875796,4.27142010528143,
133.246281936986));
#72888=CARTESIAN_POINT('Ctrl Pts',(-0.127867966878742,4.33788757326167,
133.126151112269));
#72889=CARTESIAN_POINT('Ctrl Pts',(-0.135616034881707,4.39919118910139,
133.003519535023));
#72890=CARTESIAN_POINT('Ctrl Pts',(-0.14337233762356,4.46055995915363,132.880757623478));
#72891=CARTESIAN_POINT('Ctrl Pts',(-0.151128640365466,4.51675373869174,
132.755490000364));
#72892=CARTESIAN_POINT('Ctrl Pts',(-0.158884943107324,4.56758203127038,
132.628196534011));
#72893=CARTESIAN_POINT('Ctrl Pts',(-0.166645385621494,4.61843745243918,
132.500835127303));
#72894=CARTESIAN_POINT('Ctrl Pts',(-0.174405828135649,4.66392155084546,
132.371446091527));
#72895=CARTESIAN_POINT('Ctrl Pts',(-0.182166270649816,4.7038935458668,132.240525152587));
#72896=CARTESIAN_POINT('Ctrl Pts',(-0.189939170915246,4.74392970748309,
132.109394047734));
#72897=CARTESIAN_POINT('Ctrl Pts',(-0.197712071180702,4.77843598508584,
131.976726504153));
#72898=CARTESIAN_POINT('Ctrl Pts',(-0.20548497144614,4.80732242621845,131.843030032191));
#72899=CARTESIAN_POINT('Ctrl Pts',(-0.212975307208133,4.83515877245517,
131.714193763746));
#72900=CARTESIAN_POINT('Ctrl Pts',(-0.220465642970109,4.85777672603543,
131.584402379861));
#72901=CARTESIAN_POINT('Ctrl Pts',(-0.227955978732098,4.87514150125221,
131.454113189911));
#72902=CARTESIAN_POINT('Ctrl Pts',(-0.235730312851184,4.89316466719935,
131.318884045721));
#72903=CARTESIAN_POINT('Ctrl Pts',(-0.243504646970255,4.90558553471498,
131.182690236381));
#72904=CARTESIAN_POINT('Ctrl Pts',(-0.251278981089342,4.91230864680604,
131.046035649405));
#72905=CARTESIAN_POINT('Ctrl Pts',(-0.25904373403643,4.91902347326231,130.909549476995));
#72906=CARTESIAN_POINT('Ctrl Pts',(-0.26680848698353,4.92005449690303,130.77260404358));
#72907=CARTESIAN_POINT('Ctrl Pts',(-0.274573239930618,4.9153576154106,130.635711350965));
#72908=CARTESIAN_POINT('Ctrl Pts',(-0.282330280815615,4.91066539892708,
130.498954622103));
#72909=CARTESIAN_POINT('Ctrl Pts',(-0.290087321700616,4.90025661206867,
130.362250918003));
#72910=CARTESIAN_POINT('Ctrl Pts',(-0.297844362585607,4.88413912129539,
130.226114903071));
#72911=CARTESIAN_POINT('Ctrl Pts',(-0.305595553825726,4.86803378484729,
130.090081549367));
#72912=CARTESIAN_POINT('Ctrl Pts',(-0.313346745065835,4.84622835906235,
129.954615419408));
#72913=CARTESIAN_POINT('Ctrl Pts',(-0.321097936305961,4.81878270408958,
129.820228353454));
#72914=CARTESIAN_POINT('Ctrl Pts',(-0.32884583308305,4.79134871425227,129.685898405587));
#72915=CARTESIAN_POINT('Ctrl Pts',(-0.336593729860114,4.75827934123794,
129.552646991799));
#72916=CARTESIAN_POINT('Ctrl Pts',(-0.344341626637203,4.71968590681787,
129.420977805946));
#72917=CARTESIAN_POINT('Ctrl Pts',(-0.3520879027213,4.68110054531236,129.289336162449));
#72918=CARTESIAN_POINT('Ctrl Pts',(-0.359834178805475,4.63699353068218,
129.159276463518));
#72919=CARTESIAN_POINT('Ctrl Pts',(-0.367580454889577,4.58752651897107,
129.031288847942));
#72920=CARTESIAN_POINT('Ctrl Pts',(-0.37532678815494,4.53805914210566,128.903300287591));
#72921=CARTESIAN_POINT('Ctrl Pts',(-0.38307312142022,4.48323183015402,128.777384205791));
#72922=CARTESIAN_POINT('Ctrl Pts',(-0.390819454685584,4.42325486427788,
128.654011932319));
#72923=CARTESIAN_POINT('Ctrl Pts',(-0.398567522688563,4.36326446697616,
128.530612030482));
#72924=CARTESIAN_POINT('Ctrl Pts',(-0.406315590691543,4.29812229186158,
128.409757422096));
#72925=CARTESIAN_POINT('Ctrl Pts',(-0.414063658694516,4.22808497460335,
128.291895590937));
#72926=CARTESIAN_POINT('Ctrl Pts',(-0.421819961436367,4.15797322085088,
128.173908494822));
#72927=CARTESIAN_POINT('Ctrl Pts',(-0.4295762641782,4.08295613221147,128.058920866481));
#72928=CARTESIAN_POINT('Ctrl Pts',(-0.437332566920048,4.00333446751986,
127.947352356523));
#72929=CARTESIAN_POINT('Ctrl Pts',(-0.445093009434219,3.92367030634834,
127.835724299092));
#72930=CARTESIAN_POINT('Ctrl Pts',(-0.452853451948422,3.83939691226101,
127.727519304586));
#72931=CARTESIAN_POINT('Ctrl Pts',(-0.460613894462597,3.75085525813705,
127.623123767691));
#72932=CARTESIAN_POINT('Ctrl Pts',(-0.468386794728035,3.66217146908954,
127.518560645811));
#72933=CARTESIAN_POINT('Ctrl Pts',(-0.476159694993406,3.56920599324174,
127.417819489305));
#72934=CARTESIAN_POINT('Ctrl Pts',(-0.483932595258835,3.47233719192184,
127.32125029946));
#72935=CARTESIAN_POINT('Ctrl Pts',(-0.491422931020872,3.37898981552757,
127.228191642909));
#72936=CARTESIAN_POINT('Ctrl Pts',(-0.498913266782951,3.28201820476584,
127.139007104667));
#72937=CARTESIAN_POINT('Ctrl Pts',(-0.506403602544992,3.18178830444075,
127.053973137822));
#72938=CARTESIAN_POINT('Ctrl Pts',(-0.514177936664069,3.0777581569809,126.965715082278));
#72939=CARTESIAN_POINT('Ctrl Pts',(-0.521952270783131,2.96988823026279,
126.881648973993));
#72940=CARTESIAN_POINT('Ctrl Pts',(-0.529726604902208,2.8585508622875,126.802127487148));
#72941=CARTESIAN_POINT('Ctrl Pts',(-0.537491357849296,2.74735070766773,
126.722704003429));
#72942=CARTESIAN_POINT('Ctrl Pts',(-0.545256110796364,2.6326919295012,126.6478142222));
#72943=CARTESIAN_POINT('Ctrl Pts',(-0.553020863743455,2.51498145102755,
126.577771997474));
#72944=CARTESIAN_POINT('Ctrl Pts',(-0.560777904628456,2.39738788426055,
126.507799339673));
#72945=CARTESIAN_POINT('Ctrl Pts',(-0.568534945513503,2.27674898280582,
126.44266485561));
#72946=CARTESIAN_POINT('Ctrl Pts',(-0.576291986398502,2.15350200041664,
126.382640115691));
#72947=CARTESIAN_POINT('Ctrl Pts',(-0.584043177638639,2.03034795953544,
126.322660640895));
#72948=CARTESIAN_POINT('Ctrl Pts',(-0.591794368878808,1.90459010253687,
126.267783410983));
#72949=CARTESIAN_POINT('Ctrl Pts',(-0.599545560118941,1.77669141099953,
126.218234726078));
#72950=CARTESIAN_POINT('Ctrl Pts',(-0.607293456896016,1.64884707981808,
126.168707100685));
#72951=CARTESIAN_POINT('Ctrl Pts',(-0.615041353673047,1.51886408764353,
126.124503656776));
#72952=CARTESIAN_POINT('Ctrl Pts',(-0.622789250450126,1.38722637851992,
126.085802995025));
#72953=CARTESIAN_POINT('Ctrl Pts',(-0.630535526534223,1.25561620516728,
126.047110428618));
#72954=CARTESIAN_POINT('Ctrl Pts',(-0.638281802618316,1.12235237819281,
126.013918465045));
#72955=CARTESIAN_POINT('Ctrl Pts',(-0.646028078702415,0.987934644282463,
125.986356030486));
#72956=CARTESIAN_POINT('Ctrl Pts',(-0.653774411967763,0.853515918130939,
125.958793392467));
#72957=CARTESIAN_POINT('Ctrl Pts',(-0.661520745233132,0.717943651043157,
125.936860444918));
#72958=CARTESIAN_POINT('Ctrl Pts',(-0.669267078498478,0.58172804821215,
125.920635037599));
#72959=CARTESIAN_POINT('Ctrl Pts',(-0.67701514650145,0.445481940841341,
125.904405996712));
#72960=CARTESIAN_POINT('Ctrl Pts',(-0.684763214504406,0.308592599189997,
125.893887085688));
#72961=CARTESIAN_POINT('Ctrl Pts',(-0.692511282507382,0.171575221880894,
125.88910426558));
#72962=CARTESIAN_POINT('Ctrl Pts',(-0.700267585249236,0.0344122208726595,
125.884316362235));
#72963=CARTESIAN_POINT('Ctrl Pts',(-0.708023887991096,-0.102878696273177,
125.885276741654));
#72964=CARTESIAN_POINT('Ctrl Pts',(-0.715780190732943,-0.239781898118024,
125.891959198317));
#72965=CARTESIAN_POINT('Ctrl Pts',(-0.723540633247101,-0.376758169323772,
125.898645221609));
#72966=CARTESIAN_POINT('Ctrl Pts',(-0.731301075761299,-0.513345923722532,
125.911059372217));
#72967=CARTESIAN_POINT('Ctrl Pts',(-0.739061518275463,-0.649035772352037,
125.929123635766));
#72968=CARTESIAN_POINT('Ctrl Pts',(-0.746834418540901,-0.784943442372726,
125.947216897675));
#72969=CARTESIAN_POINT('Ctrl Pts',(-0.754607318806317,-0.91994994098301,
125.970978329594));
#72970=CARTESIAN_POINT('Ctrl Pts',(-0.762380219071758,-1.05355628864653,
126.000278789667));
#72971=CARTESIAN_POINT('Ctrl Pts',(-0.769870554833828,-1.18230570903895,
126.028514104212));
#72972=CARTESIAN_POINT('Ctrl Pts',(-0.777360890595852,-1.30975471117975,
126.061892645352));
#72973=CARTESIAN_POINT('Ctrl Pts',(-0.784851226357915,-1.43547290515126,
126.100255963004));
#72974=CARTESIAN_POINT('Ctrl Pts',(-0.792625560477002,-1.56595774265788,
126.140073837504));
#72975=CARTESIAN_POINT('Ctrl Pts',(-0.800399894596131,-1.69499127069482,
126.18538807693));
#72976=CARTESIAN_POINT('Ctrl Pts',(-0.808174228715217,-1.82207551670014,
126.236076051786));
#72977=CARTESIAN_POINT('Ctrl Pts',(-0.815938981662313,-1.94900314273009,
126.286701558243));
#72978=CARTESIAN_POINT('Ctrl Pts',(-0.823703734609309,-2.0739859069617,
126.342687479582));
#72979=CARTESIAN_POINT('Ctrl Pts',(-0.831468487556407,-2.19653980317599,
126.403861105515));
#72980=CARTESIAN_POINT('Ctrl Pts',(-0.839225528441424,-2.31897197713303,
126.46497397294));
#72981=CARTESIAN_POINT('Ctrl Pts',(-0.846982569326493,-2.43897973628546,
126.531264117771));
#72982=CARTESIAN_POINT('Ctrl Pts',(-0.85473961021151,-2.55609825442499,
126.602510456479));
#72983=CARTESIAN_POINT('Ctrl Pts',(-0.862490801451634,-2.67312845257861,
126.673703067769));
#72984=CARTESIAN_POINT('Ctrl Pts',(-0.870241992691742,-2.78727341382176,
126.749844231291));
#72985=CARTESIAN_POINT('Ctrl Pts',(-0.877993183931864,-2.89809249259907,
126.830666748275));
#72986=CARTESIAN_POINT('Ctrl Pts',(-0.885741080708949,-3.00886447031184,
126.911454913534));
#72987=CARTESIAN_POINT('Ctrl Pts',(-0.893488977486078,-3.11631306186053,
126.996920244998));
#72988=CARTESIAN_POINT('Ctrl Pts',(-0.901236874263162,-3.22002642186285,
127.086752124865));
#72989=CARTESIAN_POINT('Ctrl Pts',(-0.908983150347267,-3.32371808726606,
127.176565213839));
#72990=CARTESIAN_POINT('Ctrl Pts',(-0.916729426431294,-3.42367577989525,
127.27074277863));
#72991=CARTESIAN_POINT('Ctrl Pts',(-0.924475702515394,-3.51952090521268,
127.368934055948));
#72992=CARTESIAN_POINT('Ctrl Pts',(-0.932222035780745,-3.61536673803706,
127.467126058092));
#72993=CARTESIAN_POINT('Ctrl Pts',(-0.939968369046134,-3.70709966988091,
127.569331552107));
#72994=CARTESIAN_POINT('Ctrl Pts',(-0.947714702311487,-3.79437842516739,
127.675163367611));
#72995=CARTESIAN_POINT('Ctrl Pts',(-0.955462770314454,-3.88167672592585,
127.781018883417));
#72996=CARTESIAN_POINT('Ctrl Pts',(-0.963210838317446,-3.96451861655245,
127.890502035108));
#72997=CARTESIAN_POINT('Ctrl Pts',(-0.970958906320419,-4.04260377783632,
128.003193404077));
#72998=CARTESIAN_POINT('Ctrl Pts',(-0.978715209062279,-4.12077192895895,
128.116004542775));
#72999=CARTESIAN_POINT('Ctrl Pts',(-0.986471511804122,-4.1941730287884,
128.232030388185));
#73000=CARTESIAN_POINT('Ctrl Pts',(-0.99422781454598,-4.26255041338435,
128.350822960252));
#73001=CARTESIAN_POINT('Ctrl Pts',(-1.00198825706015,-4.33096429304925,
128.469678935492));
#73002=CARTESIAN_POINT('Ctrl Pts',(-1.00974869957436,-4.39434893414989,
128.59130423327));
#73003=CARTESIAN_POINT('Ctrl Pts',(-1.01750914208853,-4.4524946352122,128.715228121551));
#73004=CARTESIAN_POINT('Ctrl Pts',(-1.02528204235397,-4.51073367691587,
128.839350943459));
#73005=CARTESIAN_POINT('Ctrl Pts',(-1.03305494261941,-4.56371682149993,
128.96577936868));
#73006=CARTESIAN_POINT('Ctrl Pts',(-1.04082784288485,-4.61128300903725,
129.094023787271));
#73007=CARTESIAN_POINT('Ctrl Pts',(-1.04831817864682,-4.65712004584514,
129.217606198216));
#73008=CARTESIAN_POINT('Ctrl Pts',(-1.05580851440876,-4.6979270326267,129.342874570061));
#73009=CARTESIAN_POINT('Ctrl Pts',(-1.06329885017072,-4.73360464165935,
129.469381157439));
#73010=CARTESIAN_POINT('Ctrl Pts',(-1.06552363953777,-4.74420165195899,
129.506956310196));
#73011=CARTESIAN_POINT('Ctrl Pts',(-1.0677484289048,-4.75435258515985,129.544662390509));
#73012=CARTESIAN_POINT('Ctrl Pts',(-1.06997321827188,-4.76405452823403,
129.582490119308));
#73013=CARTESIAN_POINT('Origin',(213.235140564004,0.,130.804360617566));
#73014=CARTESIAN_POINT('',(-3.16500955108754,-4.76405452823408,129.582490119308));
#73015=CARTESIAN_POINT('',(-2.82009873120266,-4.76405452823402,129.582490119308));
#73016=CARTESIAN_POINT('',(213.235140564004,-4.76405452823405,129.582490119308));
#73017=CARTESIAN_POINT('',(-1.48514056405364,-4.91824949356997,130.806592544705));
#73018=CARTESIAN_POINT('Ctrl Pts',(-1.48514056405364,-4.91824949356997,
130.806592544705));
#73019=CARTESIAN_POINT('Ctrl Pts',(-1.49361211986651,-4.91818127701446,
130.956913777718));
#73020=CARTESIAN_POINT('Ctrl Pts',(-1.50208367567946,-4.91121731645437,
131.107008485491));
#73021=CARTESIAN_POINT('Ctrl Pts',(-1.51055523149233,-4.89744448273245,
131.256268352677));
#73022=CARTESIAN_POINT('Ctrl Pts',(-1.51906731434727,-4.88360576120622,
131.406242263547));
#73023=CARTESIAN_POINT('Ctrl Pts',(-1.52757939720221,-4.86289295069057,
131.55537307392));
#73024=CARTESIAN_POINT('Ctrl Pts',(-1.53609148005714,-4.83544460907228,
131.703058840049));
#73025=CARTESIAN_POINT('Ctrl Pts',(-1.54462433530355,-4.80792928411897,
131.851105009924));
#73026=CARTESIAN_POINT('Ctrl Pts',(-1.55315719054997,-4.77364563370778,
131.997698835767));
#73027=CARTESIAN_POINT('Ctrl Pts',(-1.56169004579638,-4.73278221413539,
132.142252831484));
#73028=CARTESIAN_POINT('Ctrl Pts',(-1.5702524089246,-4.691777482784,132.287306716406));
#73029=CARTESIAN_POINT('Ctrl Pts',(-1.57881477205279,-4.64414752127059,
132.430306405755));
#73030=CARTESIAN_POINT('Ctrl Pts',(-1.58737713518101,-4.59013027638844,
132.570680834368));
#73031=CARTESIAN_POINT('Ctrl Pts',(-1.59178645733306,-4.56231325544641,
132.64296883108));
#73032=CARTESIAN_POINT('Ctrl Pts',(-1.5961957794851,-4.53280315123714,132.714561023417));
#73033=CARTESIAN_POINT('Ctrl Pts',(-1.60060510163714,-4.50163716490563,
132.785382045527));
#73034=CARTESIAN_POINT('Ctrl Pts',(-1.6083794357562,-4.4466865891624,132.910250737257));
#73035=CARTESIAN_POINT('Ctrl Pts',(-1.6161537698753,-4.38644953171332,133.033029108977));
#73036=CARTESIAN_POINT('Ctrl Pts',(-1.62392810399439,-4.32110657864136,
133.153237157217));
#73037=CARTESIAN_POINT('Ctrl Pts',(-1.63169285694149,-4.25584415491919,
133.27329705978));
#73038=CARTESIAN_POINT('Ctrl Pts',(-1.63945760988856,-4.18548854081923,
133.390792601431));
#73039=CARTESIAN_POINT('Ctrl Pts',(-1.64722236283566,-4.11026840313648,
133.505263562264));
#73040=CARTESIAN_POINT('Ctrl Pts',(-1.65497940372067,-4.03512297515488,
133.619620828925));
#73041=CARTESIAN_POINT('Ctrl Pts',(-1.6627364446057,-3.95512285183305,133.730959168355));
#73042=CARTESIAN_POINT('Ctrl Pts',(-1.67049348549071,-3.87054246929996,
133.838843119715));
#73043=CARTESIAN_POINT('Ctrl Pts',(-1.67824467673084,-3.78602586949127,
133.946645714947));
#73044=CARTESIAN_POINT('Ctrl Pts',(-1.68599586797096,-3.69693612571028,
134.050998800732));
#73045=CARTESIAN_POINT('Ctrl Pts',(-1.69374705921109,-3.60359061060528,
134.151496374248));
#73046=CARTESIAN_POINT('Ctrl Pts',(-1.70149495598818,-3.51028476983427,
134.251951233614));
#73047=CARTESIAN_POINT('Ctrl Pts',(-1.70924285276531,-3.412727020853,134.348553554092));
#73048=CARTESIAN_POINT('Ctrl Pts',(-1.71699074954239,-3.31127444988671,
134.440931059621));
#73049=CARTESIAN_POINT('Ctrl Pts',(-1.72473702562649,-3.20984310061121,
134.533289241767));
#73050=CARTESIAN_POINT('Ctrl Pts',(-1.73248330171057,-3.10451883875693,
134.621424103715));
#73051=CARTESIAN_POINT('Ctrl Pts',(-1.74022957779468,-2.99569468782962,
134.705001129047));
#73052=CARTESIAN_POINT('Ctrl Pts',(-1.74797591106004,-2.88686973358715,
134.788578771326));
#73053=CARTESIAN_POINT('Ctrl Pts',(-1.75572224432536,-2.77454514879164,
134.867598271717));
#73054=CARTESIAN_POINT('Ctrl Pts',(-1.76346857759071,-2.65914570151932,
134.941766471551));
#73055=CARTESIAN_POINT('Ctrl Pts',(-1.77121664559369,-2.54372041134091,
135.015951280839));
#73056=CARTESIAN_POINT('Ctrl Pts',(-1.77896471359672,-2.42521921729389,
135.085282416387));
#73057=CARTESIAN_POINT('Ctrl Pts',(-1.7867127815997,-2.30409407265979,135.149511198022));
#73058=CARTESIAN_POINT('Ctrl Pts',(-1.79446908434156,-2.18284019478057,
135.21380824277));
#73059=CARTESIAN_POINT('Ctrl Pts',(-1.80222538708341,-2.05895714141268,
135.272991917442));
#73060=CARTESIAN_POINT('Ctrl Pts',(-1.80998168982526,-1.93292007130647,
135.326860264934));
#73061=CARTESIAN_POINT('Ctrl Pts',(-1.81774213233943,-1.80681573142104,
135.380757363585));
#73062=CARTESIAN_POINT('Ctrl Pts',(-1.82550257485362,-1.67855544943819,
135.429333343788));
#73063=CARTESIAN_POINT('Ctrl Pts',(-1.83326301736778,-1.54863143016031,
135.472435569409));
#73064=CARTESIAN_POINT('Ctrl Pts',(-1.84103591763322,-1.41849884531257,
135.515606986548));
#73065=CARTESIAN_POINT('Ctrl Pts',(-1.84880881789865,-1.2866975622245,135.553286982436));
#73066=CARTESIAN_POINT('Ctrl Pts',(-1.85658171816408,-1.15373278648152,
135.585373451673));
#73067=CARTESIAN_POINT('Ctrl Pts',(-1.86407205392605,-1.02560161525594,
135.616293496932));
#73068=CARTESIAN_POINT('Ctrl Pts',(-1.87156238968801,-0.896390376604573,
135.642019572439));
#73069=CARTESIAN_POINT('Ctrl Pts',(-1.87905272544998,-0.766555413447032,
135.662505928342));
#73070=CARTESIAN_POINT('Ctrl Pts',(-1.88682705956907,-0.63179771819775,
135.683769030656));
#73071=CARTESIAN_POINT('Ctrl Pts',(-1.89460139368816,-0.49594119588205,
135.699454597165));
#73072=CARTESIAN_POINT('Ctrl Pts',(-1.90237572780725,-0.359487298203495,
135.709455106455));
#73073=CARTESIAN_POINT('Ctrl Pts',(-1.91014048075434,-0.223201567758778,
135.719443291011));
#73074=CARTESIAN_POINT('Ctrl Pts',(-1.91790523370135,-0.0863203129693952,
135.723760330545));
#73075=CARTESIAN_POINT('Ctrl Pts',(-1.92566998664844,0.0506456701371081,
135.722349848806));
#73076=CARTESIAN_POINT('Ctrl Pts',(-1.93342702753344,0.187475616698308,
135.720940767978));
#73077=CARTESIAN_POINT('Ctrl Pts',(-1.94118406841856,0.324389735692955,
135.713815490558));
#73078=CARTESIAN_POINT('Ctrl Pts',(-1.94894110930355,0.460873322153924,
135.700969530214));
#73079=CARTESIAN_POINT('Ctrl Pts',(-1.95669230054366,0.597253985280655,
135.688133257109));
#73080=CARTESIAN_POINT('Ctrl Pts',(-1.96444349178378,0.733204374435617,
135.669584924346));
#73081=CARTESIAN_POINT('Ctrl Pts',(-1.9721946830239,0.868211360278723,135.645372092081));
#73082=CARTESIAN_POINT('Ctrl Pts',(-1.97994257980098,1.00316096455142,135.621169550915));
#73083=CARTESIAN_POINT('Ctrl Pts',(-1.98769047657804,1.13716757899451,135.59130736758));
#73084=CARTESIAN_POINT('Ctrl Pts',(-1.99543837335511,1.26972498338656,135.555884744524));
#73085=CARTESIAN_POINT('Ctrl Pts',(-2.00318464943921,1.40225465962722,135.520469531117));
#73086=CARTESIAN_POINT('Ctrl Pts',(-2.01093092552328,1.53333535131349,135.479496292378));
#73087=CARTESIAN_POINT('Ctrl Pts',(-2.01867720160737,1.66247318150371,135.433114875817));
#73088=CARTESIAN_POINT('Ctrl Pts',(-2.02642353487273,1.79161196496023,135.38673311688));
#73089=CARTESIAN_POINT('Ctrl Pts',(-2.03416986813814,1.91880749035037,135.334943232614));
#73090=CARTESIAN_POINT('Ctrl Pts',(-2.0419162014035,2.04358351746206,135.277944133011));
#73091=CARTESIAN_POINT('Ctrl Pts',(-2.04966426940647,2.16838748729972,135.220932268854));
#73092=CARTESIAN_POINT('Ctrl Pts',(-2.05741233740945,2.29077052513087,135.158709030445));
#73093=CARTESIAN_POINT('Ctrl Pts',(-2.06516040541243,2.41027911749444,135.091520241171));
#73094=CARTESIAN_POINT('Ctrl Pts',(-2.07291670815428,2.52991472501214,135.024260042852));
#73095=CARTESIAN_POINT('Ctrl Pts',(-2.08067301089608,2.64666944303948,134.952023943305));
#73096=CARTESIAN_POINT('Ctrl Pts',(-2.08842931363793,2.76011652443431,134.875102544297));
#73097=CARTESIAN_POINT('Ctrl Pts',(-2.0961897561521,2.87362415595247,134.798140090022));
#73098=CARTESIAN_POINT('Ctrl Pts',(-2.10395019866628,2.98382031918437,134.716487586104));
#73099=CARTESIAN_POINT('Ctrl Pts',(-2.11171064118045,3.09031054830751,134.630476634824));
#73100=CARTESIAN_POINT('Ctrl Pts',(-2.11948354144589,3.1969717250002,134.54432761113));
#73101=CARTESIAN_POINT('Ctrl Pts',(-2.12725644171136,3.29991478562881,134.453806417024));
#73102=CARTESIAN_POINT('Ctrl Pts',(-2.1350293419768,3.39878075006804,134.359282905812));
#73103=CARTESIAN_POINT('Ctrl Pts',(-2.14251967773885,3.4940526876717,134.268195562322));
#73104=CARTESIAN_POINT('Ctrl Pts',(-2.15001001350078,3.58553859424845,134.173392059997));
#73105=CARTESIAN_POINT('Ctrl Pts',(-2.15750034926282,3.67295331465585,134.075231604147));
#73106=CARTESIAN_POINT('Ctrl Pts',(-2.16527468338191,3.7636823907565,133.973349364778));
#73107=CARTESIAN_POINT('Ctrl Pts',(-2.173049017501,3.85031287089078,133.867527856737));
#73108=CARTESIAN_POINT('Ctrl Pts',(-2.18082335162009,3.93248324735283,133.758130847592));
#73109=CARTESIAN_POINT('Ctrl Pts',(-2.18858810456719,4.01455235616967,133.648868660484));
#73110=CARTESIAN_POINT('Ctrl Pts',(-2.19635285751436,4.09217206551828,133.536040049468));
#73111=CARTESIAN_POINT('Ctrl Pts',(-2.20411761046145,4.1650188467341,133.42004428897));
#73112=CARTESIAN_POINT('Ctrl Pts',(-2.21187465134644,4.23779327549977,133.304163737096));
#73113=CARTESIAN_POINT('Ctrl Pts',(-2.21963169223139,4.30580400343781,133.185122624687));
#73114=CARTESIAN_POINT('Ctrl Pts',(-2.22738873311638,4.36876904546301,133.063351562635));
#73115=CARTESIAN_POINT('Ctrl Pts',(-2.23513992435652,4.43168660506031,132.941672329089));
#73116=CARTESIAN_POINT('Ctrl Pts',(-2.24289111559669,4.48956587350178,132.81726758945));
#73117=CARTESIAN_POINT('Ctrl Pts',(-2.25064230683682,4.54216950555128,132.690594761393));
#73118=CARTESIAN_POINT('Ctrl Pts',(-2.2583902036139,4.59475077965385,132.563975772667));
#73119=CARTESIAN_POINT('Ctrl Pts',(-2.26613810039093,4.64206072747275,132.435090973155));
#73120=CARTESIAN_POINT('Ctrl Pts',(-2.27388599716801,4.68390918644363,132.304419881612));
#73121=CARTESIAN_POINT('Ctrl Pts',(-2.28163227325211,4.72574889161904,132.173776123644));
#73122=CARTESIAN_POINT('Ctrl Pts',(-2.2893785493362,4.76212926112554,132.041347188965));
#73123=CARTESIAN_POINT('Ctrl Pts',(-2.2971248254203,4.79290941336774,131.907629586472));
#73124=CARTESIAN_POINT('Ctrl Pts',(-2.30487115868564,4.82368979282204,131.773910996906));
#73125=CARTESIAN_POINT('Ctrl Pts',(-2.31261749195099,4.84886978482011,131.638904101547));
#73126=CARTESIAN_POINT('Ctrl Pts',(-2.32036382521633,4.86835931850332,131.503117090482));
#73127=CARTESIAN_POINT('Ctrl Pts',(-2.3281118932193,4.88785321673246,131.367299670857));
#73128=CARTESIAN_POINT('Ctrl Pts',(-2.33585996122227,4.90165406532486,131.230702174814));
#73129=CARTESIAN_POINT('Ctrl Pts',(-2.34360802922524,4.90972354735527,131.09383902962));
#73130=CARTESIAN_POINT('Ctrl Pts',(-2.35136433196708,4.91780160572721,130.956830424646));
#73131=CARTESIAN_POINT('Ctrl Pts',(-2.35912063470901,4.92013610633213,130.819555997434));
#73132=CARTESIAN_POINT('Ctrl Pts',(-2.36687693745085,4.91674087341196,130.682531859794));
#73133=CARTESIAN_POINT('Ctrl Pts',(-2.37463737996501,4.91334382835375,130.545434588247));
#73134=CARTESIAN_POINT('Ctrl Pts',(-2.3823978224791,4.90421098220649,130.408588262362));
#73135=CARTESIAN_POINT('Ctrl Pts',(-2.39015826499326,4.88940810294767,130.27250399654));
#73136=CARTESIAN_POINT('Ctrl Pts',(-2.39793116525869,4.87458146079291,130.136201276173));
#73137=CARTESIAN_POINT('Ctrl Pts',(-2.40570406552415,4.85406665529249,130.00066344725));
#73138=CARTESIAN_POINT('Ctrl Pts',(-2.41347696578958,4.82798081697922,129.866392444662));
#73139=CARTESIAN_POINT('Ctrl Pts',(-2.42096730155164,4.80284326459482,129.737002531226));
#73140=CARTESIAN_POINT('Ctrl Pts',(-2.42845763731369,4.7725327602866,129.608789238297));
#73141=CARTESIAN_POINT('Ctrl Pts',(-2.43594797307574,4.73719738033461,129.482186634215));
#73142=CARTESIAN_POINT('Ctrl Pts',(-2.44372230719482,4.70052224871195,129.35078385392));
#73143=CARTESIAN_POINT('Ctrl Pts',(-2.45149664131394,4.65831750755569,129.22070006755));
#73144=CARTESIAN_POINT('Ctrl Pts',(-2.45927097543301,4.61069380107874,129.092436047033));
#73145=CARTESIAN_POINT('Ctrl Pts',(-2.4670357283801,4.56312878656376,128.964330100459));
#73146=CARTESIAN_POINT('Ctrl Pts',(-2.47480048132721,4.51015822951373,128.838039820433));
#73147=CARTESIAN_POINT('Ctrl Pts',(-2.48256523427429,4.45194317566456,128.714053218365));
#73148=CARTESIAN_POINT('Ctrl Pts',(-2.49032227515928,4.39378594182755,128.590189761538));
#73149=CARTESIAN_POINT('Ctrl Pts',(-2.49807931604422,4.33039474224271,128.468625780962));
#73150=CARTESIAN_POINT('Ctrl Pts',(-2.50583635692922,4.26197944222431,128.349831274381));
#73151=CARTESIAN_POINT('Ctrl Pts',(-2.51358754816935,4.19361573471585,128.231126351661));
#73152=CARTESIAN_POINT('Ctrl Pts',(-2.52133873940951,4.12023566230551,128.115187083367));
#73153=CARTESIAN_POINT('Ctrl Pts',(-2.52908993064963,4.04209577253818,128.00246040019));
#73154=CARTESIAN_POINT('Ctrl Pts',(-2.53683782742671,3.96398909430844,127.889781628862));
#73155=CARTESIAN_POINT('Ctrl Pts',(-2.54458572420377,3.88112684467706,127.780313047552));
#73156=CARTESIAN_POINT('Ctrl Pts',(-2.55233362098085,3.79380966884344,127.674473837011));
#73157=CARTESIAN_POINT('Ctrl Pts',(-2.56007989706494,3.70651075788066,127.568656765753));
#73158=CARTESIAN_POINT('Ctrl Pts',(-2.56782617314904,3.61475902291083,127.46646785659));
#73159=CARTESIAN_POINT('Ctrl Pts',(-2.57557244923314,3.5188960409885,127.368294012389));
#73160=CARTESIAN_POINT('Ctrl Pts',(-2.58331878249848,3.42303235142755,127.27011944349));
#73161=CARTESIAN_POINT('Ctrl Pts',(-2.59106511576381,3.32305762749868,127.175960278419));
#73162=CARTESIAN_POINT('Ctrl Pts',(-2.59881144902914,3.21935073841554,127.086166985496));
#73163=CARTESIAN_POINT('Ctrl Pts',(-2.6065595170321,3.11562062489366,126.996353583988));
#73164=CARTESIAN_POINT('Ctrl Pts',(-2.61430758503506,3.00815697860004,126.910908256017));
#73165=CARTESIAN_POINT('Ctrl Pts',(-2.62205565303802,2.89737189052766,126.830141299199));
#73166=CARTESIAN_POINT('Ctrl Pts',(-2.62981195577987,2.78646905874518,126.749288502299));
#73167=CARTESIAN_POINT('Ctrl Pts',(-2.6375682585217,2.67223804991851,126.673124239801));
#73168=CARTESIAN_POINT('Ctrl Pts',(-2.64532456126355,2.55512055587069,126.60191585202));
#73169=CARTESIAN_POINT('Ctrl Pts',(-2.65308500377771,2.43794055268995,126.530669458178));
#73170=CARTESIAN_POINT('Ctrl Pts',(-2.66084544629194,2.31787133660872,126.464384398499));
#73171=CARTESIAN_POINT('Ctrl Pts',(-2.6686058888061,2.19537847184615,126.403281610339));
#73172=CARTESIAN_POINT('Ctrl Pts',(-2.67637878907153,2.07268897066249,126.342080734559));
#73173=CARTESIAN_POINT('Ctrl Pts',(-2.68415168933696,1.94756840308402,126.286078914207));
#73174=CARTESIAN_POINT('Ctrl Pts',(-2.69192458960239,1.82050237306414,126.235448912119));
#73175=CARTESIAN_POINT('Ctrl Pts',(-2.69941492536449,1.69805551329447,126.186659438136));
#73176=CARTESIAN_POINT('Ctrl Pts',(-2.70690526112654,1.5738024708093,126.142858107236));
#73177=CARTESIAN_POINT('Ctrl Pts',(-2.71439559688864,1.44818847844375,126.104154963193));
#73178=CARTESIAN_POINT('Ctrl Pts',(-2.72216993100772,1.31781179337922,126.06398437768));
#73179=CARTESIAN_POINT('Ctrl Pts',(-2.72994426512682,1.18555592623878,126.029178957709));
#73180=CARTESIAN_POINT('Ctrl Pts',(-2.73771859924591,1.05190199652772,125.999916294629));
#73181=CARTESIAN_POINT('Ctrl Pts',(-2.74548335219301,0.918412783340025,
125.970689695166));
#73182=CARTESIAN_POINT('Ctrl Pts',(-2.75324810514009,0.783529314064722,
125.946992343851));
#73183=CARTESIAN_POINT('Ctrl Pts',(-2.76101285808718,0.647749215674395,
125.928952530432));
#73184=CARTESIAN_POINT('Ctrl Pts',(-2.76876989897218,0.512103975992138,
125.910930634409));
#73185=CARTESIAN_POINT('Ctrl Pts',(-2.77652693985721,0.375564264470655,
125.898555145085));
#73186=CARTESIAN_POINT('Ctrl Pts',(-2.7842839807422,0.238638940852387,125.891903542089));
#73187=CARTESIAN_POINT('Ctrl Pts',(-2.79203517198233,0.101816873685596,
125.885256955117));
#73188=CARTESIAN_POINT('Ctrl Pts',(-2.79978636322245,-0.0353898378473538,
125.88432568178));
#73189=CARTESIAN_POINT('Ctrl Pts',(-2.80753755446258,-0.172466508081281,
125.889135458319));
#73190=CARTESIAN_POINT('Ctrl Pts',(-2.81528545123967,-0.309484917073719,
125.893943190575));
#73191=CARTESIAN_POINT('Ctrl Pts',(-2.82303334801674,-0.446373004790244,
125.904487105854));
#73192=CARTESIAN_POINT('Ctrl Pts',(-2.83078124479383,-0.582615596518611,
125.92074084027));
#73193=CARTESIAN_POINT('Ctrl Pts',(-2.83852752087793,-0.718829689233839,
125.936991174756));
#73194=CARTESIAN_POINT('Ctrl Pts',(-2.84627379696204,-0.854398166564337,
125.958948906425));
#73195=CARTESIAN_POINT('Ctrl Pts',(-2.85402007304614,-0.988810885431754,
125.986535787277));
#73196=CARTESIAN_POINT('Ctrl Pts',(-2.8617664063115,-1.12322459650333,126.014122871768));
#73197=CARTESIAN_POINT('Ctrl Pts',(-2.86951273957685,-1.2564821491056,126.047339109755));
#73198=CARTESIAN_POINT('Ctrl Pts',(-2.87725907284221,-1.38808389625118,
126.086055184525));
#73199=CARTESIAN_POINT('Ctrl Pts',(-2.88500714084518,-1.5197151146954,126.124779929491));
#73200=CARTESIAN_POINT('Ctrl Pts',(-2.89275520884814,-1.64968941482233,
126.16900685176));
#73201=CARTESIAN_POINT('Ctrl Pts',(-2.90050327685111,-1.77752298921157,
126.218556970949));
#73202=CARTESIAN_POINT('Ctrl Pts',(-2.90825957959297,-1.90549242664508,
126.268159752595));
#73203=CARTESIAN_POINT('Ctrl Pts',(-2.91601588233487,-2.03131622828681,
126.323096891216));
#73204=CARTESIAN_POINT('Ctrl Pts',(-2.92377218507673,-2.15453072794016,
126.383141282941));
#73205=CARTESIAN_POINT('Ctrl Pts',(-2.93153262759091,-2.27781099088207,
126.443217722166));
#73206=CARTESIAN_POINT('Ctrl Pts',(-2.93929307010507,-2.39847883302623,
126.508406660333));
#73207=CARTESIAN_POINT('Ctrl Pts',(-2.94705351261925,-2.51609672468518,
126.578435827117));
#73208=CARTESIAN_POINT('Ctrl Pts',(-2.95482641288468,-2.63390342702529,
126.648577410937));
#73209=CARTESIAN_POINT('Ctrl Pts',(-2.96259931315011,-2.74865006755672,
126.723574536219));
#73210=CARTESIAN_POINT('Ctrl Pts',(-2.97037221341554,-2.85992881521558,
126.803112033136));
#73211=CARTESIAN_POINT('Ctrl Pts',(-2.97786254917752,-2.96716230010203,
126.879758141698));
#73212=CARTESIAN_POINT('Ctrl Pts',(-2.9853528849395,-3.07117540481709,126.96062005611));
#73213=CARTESIAN_POINT('Ctrl Pts',(-2.99284322070147,-3.17163488719524,
127.045382670726));
#73214=CARTESIAN_POINT('Ctrl Pts',(-3.00050565897731,-3.27440258779098,
127.132092842772));
#73215=CARTESIAN_POINT('Ctrl Pts',(-3.00816809725319,-3.37379675582324,
127.223176882538));
#73216=CARTESIAN_POINT('Ctrl Pts',(-3.01583053552906,-3.46941405963075,
127.318338651867));
#73217=CARTESIAN_POINT('Ctrl Pts',(-3.02348417649824,-3.56492158444669,
127.413391165207));
#73218=CARTESIAN_POINT('Ctrl Pts',(-3.03113781746743,-3.6566605822443,127.512511820838));
#73219=CARTESIAN_POINT('Ctrl Pts',(-3.03879145843661,-3.74425962852201,
127.615363455962));
#73220=CARTESIAN_POINT('Ctrl Pts',(-3.04643808230441,-3.83177836120907,
127.718120793436));
#73221=CARTESIAN_POINT('Ctrl Pts',(-3.0540847061722,-3.91516442972166,127.824602004542));
#73222=CARTESIAN_POINT('Ctrl Pts',(-3.06173133004,-3.99408264305215,127.934432586592));
#73223=CARTESIAN_POINT('Ctrl Pts',(-3.06937271037017,-4.07294673960785,
128.044187854255));
#73224=CARTESIAN_POINT('Ctrl Pts',(-3.07701409070032,-4.14734884027291,
128.157287598844));
#73225=CARTESIAN_POINT('Ctrl Pts',(-3.08465547103049,-4.21699387560951,
128.273324127198));
#73226=CARTESIAN_POINT('Ctrl Pts',(-3.09229404773085,-4.28661335811553,
128.389318081639));
#73227=CARTESIAN_POINT('Ctrl Pts',(-3.09993262443121,-4.35147903688056,
128.508246333531));
#73228=CARTESIAN_POINT('Ctrl Pts',(-3.10757120113158,-4.41133929890028,
128.629672443947));
#73229=CARTESIAN_POINT('Ctrl Pts',(-3.11520810678753,-4.4711864656589,128.75107199072));
#73230=CARTESIAN_POINT('Ctrl Pts',(-3.12284501244348,-4.52603021918189,
128.874967946026));
#73231=CARTESIAN_POINT('Ctrl Pts',(-3.13048191809943,-4.57566534712315,
129.00090014014));
#73232=CARTESIAN_POINT('Ctrl Pts',(-3.13812068892218,-4.62531259748629,
129.126863090762));
#73233=CARTESIAN_POINT('Ctrl Pts',(-3.1457594597449,-4.66974853392853,129.254862898307));
#73234=CARTESIAN_POINT('Ctrl Pts',(-3.15339823056763,-4.70881654090428,
129.384420531997));
#73235=CARTESIAN_POINT('Ctrl Pts',(-3.15726867074093,-4.72861166072115,
129.450065264877));
#73236=CARTESIAN_POINT('Ctrl Pts',(-3.16113911091424,-4.74702947019134,
129.516109676391));
#73237=CARTESIAN_POINT('Ctrl Pts',(-3.16500955108754,-4.76405452823408,
129.582490119308));
#73238=CARTESIAN_POINT('Ctrl Pts',(-1.41535445211275,-4.764054528234,129.582490119308));
#73239=CARTESIAN_POINT('Ctrl Pts',(-1.42324132509898,-4.79873248228505,
129.717698935842));
#73240=CARTESIAN_POINT('Ctrl Pts',(-1.43112819808529,-4.82767493793869,
129.854481638264));
#73241=CARTESIAN_POINT('Ctrl Pts',(-1.43901507107151,-4.85075001678642,
129.992321617797));
#73242=CARTESIAN_POINT('Ctrl Pts',(-1.44689736863845,-4.87381170906626,
130.130081632088));
#73243=CARTESIAN_POINT('Ctrl Pts',(-1.45477966620536,-4.89101274268046,
130.2688973364));
#73244=CARTESIAN_POINT('Ctrl Pts',(-1.46266196377232,-4.90227218133672,
130.408241288838));
#73245=CARTESIAN_POINT('Ctrl Pts',(-1.47015483051776,-4.91297533898373,
130.540700848824));
#73246=CARTESIAN_POINT('Ctrl Pts',(-1.47764769726323,-4.91830982928536,
130.673637394598));
#73247=CARTESIAN_POINT('Ctrl Pts',(-1.48514056400867,-4.91824949357033,
130.806592543907));
#73248=CARTESIAN_POINT('',(-1.13985943593539,-4.91824798494418,130.799908529016));
#73249=CARTESIAN_POINT('Ctrl Pts',(-1.06997321827188,-4.76405452823403,
129.582490119308));
#73250=CARTESIAN_POINT('Ctrl Pts',(-1.0797552074402,-4.80671218538992,129.748811677139));
#73251=CARTESIAN_POINT('Ctrl Pts',(-1.08953719660859,-4.8406862486606,129.917486629869));
#73252=CARTESIAN_POINT('Ctrl Pts',(-1.09931918577689,-4.86575789899625,
130.087713472274));
#73253=CARTESIAN_POINT('Ctrl Pts',(-1.10894348654133,-4.89042538730968,
130.255196210324));
#73254=CARTESIAN_POINT('Ctrl Pts',(-1.11856778730584,-4.9064751643602,130.424181317926));
#73255=CARTESIAN_POINT('Ctrl Pts',(-1.12819208807031,-4.91374425224563,
130.593883811188));
#73256=CARTESIAN_POINT('Ctrl Pts',(-1.13208120402536,-4.9166816423341,130.662459460506));
#73257=CARTESIAN_POINT('Ctrl Pts',(-1.13597031998038,-4.9181857452644,130.731151994587));
#73258=CARTESIAN_POINT('Ctrl Pts',(-1.13985943593545,-4.91824798494418,
130.799908529016));
#73259=CARTESIAN_POINT('Ctrl Pts',(-1.13985943599124,-4.91824798494508,
130.799908530003));
#73260=CARTESIAN_POINT('Ctrl Pts',(-1.14754077984185,-4.91837091372404,
130.935708693595));
#73261=CARTESIAN_POINT('Ctrl Pts',(-1.15522212369246,-4.91286514421883,
131.0716324534));
#73262=CARTESIAN_POINT('Ctrl Pts',(-1.16290346754306,-4.90172682389837,
131.207172243981));
#73263=CARTESIAN_POINT('Ctrl Pts',(-1.17058138413356,-4.89059347327091,
131.342651559452));
#73264=CARTESIAN_POINT('Ctrl Pts',(-1.1782593007241,-4.87383260126212,131.477746849842));
#73265=CARTESIAN_POINT('Ctrl Pts',(-1.1859372173146,-4.85149242725984,131.611952278457));
#73266=CARTESIAN_POINT('Ctrl Pts',(-1.19361349098168,-4.82915703361624,
131.746128989745));
#73267=CARTESIAN_POINT('Ctrl Pts',(-1.20128976464877,-4.80124477720653,
131.879415824793));
#73268=CARTESIAN_POINT('Ctrl Pts',(-1.20896603831585,-4.76785548487302,
132.011314277764));
#73269=CARTESIAN_POINT('Ctrl Pts',(-1.21664240553569,-4.73446578561544,
132.143214338217));
#73270=CARTESIAN_POINT('Ctrl Pts',(-1.22431877275549,-4.69559901550001,
132.273725596381));
#73271=CARTESIAN_POINT('Ctrl Pts',(-1.23199513997534,-4.65140552457929,
132.402362403677));
#73272=CARTESIAN_POINT('Ctrl Pts',(-1.23967333700939,-4.60720149926447,
132.531029874105));
#73273=CARTESIAN_POINT('Ctrl Pts',(-1.24735153404347,-4.5576683573535,132.657821628027));
#73274=CARTESIAN_POINT('Ctrl Pts',(-1.25502973107751,-4.50300528134762,
132.782270246102));
#73275=CARTESIAN_POINT('Ctrl Pts',(-1.2627161116868,-4.44828394434724,132.906851503992));
#73276=CARTESIAN_POINT('Ctrl Pts',(-1.27040249229602,-4.3884219153172,133.029084273436));
#73277=CARTESIAN_POINT('Ctrl Pts',(-1.2780888729053,-4.32366539000178,133.14852372149));
#73278=CARTESIAN_POINT('Ctrl Pts',(-1.28577958631668,-4.25887236152274,
133.268030497397));
#73279=CARTESIAN_POINT('Ctrl Pts',(-1.29347029972814,-4.18917954660631,
133.384740474492));
#73280=CARTESIAN_POINT('Ctrl Pts',(-1.30116101313953,-4.11487685512454,
133.498237290627));
#73281=CARTESIAN_POINT('Ctrl Pts',(-1.30886368927773,-4.04045858752501,
133.611910648433));
#73282=CARTESIAN_POINT('Ctrl Pts',(-1.31656636541592,-3.96141635337207,
133.722360539057));
#73283=CARTESIAN_POINT('Ctrl Pts',(-1.32426904155412,-3.87808115125348,
133.829202703823));
#73284=CARTESIAN_POINT('Ctrl Pts',(-1.33009485236395,-3.81505174269055,
133.910011273114));
#73285=CARTESIAN_POINT('Ctrl Pts',(-1.33592066317378,-3.7495674144181,133.988756737511));
#73286=CARTESIAN_POINT('Ctrl Pts',(-1.34174647398362,-3.68178496192597,
134.065287258359));
#73287=CARTESIAN_POINT('Ctrl Pts',(-1.34952080810276,-3.59133172712553,
134.167414474433));
#73288=CARTESIAN_POINT('Ctrl Pts',(-1.35729514222178,-3.49648271589758,
134.265937044038));
#73289=CARTESIAN_POINT('Ctrl Pts',(-1.36506947634086,-3.39755645246117,
134.360453025651));
#73290=CARTESIAN_POINT('Ctrl Pts',(-1.37283422928794,-3.29875210680341,
134.454852524763));
#73291=CARTESIAN_POINT('Ctrl Pts',(-1.38059898223503,-3.19588078685877,
134.54525499307));
#73292=CARTESIAN_POINT('Ctrl Pts',(-1.38836373518211,-3.08930076083462,
134.63129200859));
#73293=CARTESIAN_POINT('Ctrl Pts',(-1.39612077606711,-2.98282659159468,
134.717243570934));
#73294=CARTESIAN_POINT('Ctrl Pts',(-1.4038778169521,-2.87265134892913,134.798838065001));
#73295=CARTESIAN_POINT('Ctrl Pts',(-1.4116348578371,-2.75916932483993,134.875744620502));
#73296=CARTESIAN_POINT('Ctrl Pts',(-1.41938604907723,-2.64577287842785,
134.952593180171));
#73297=CARTESIAN_POINT('Ctrl Pts',(-1.42713724031735,-2.52907493642619,
135.024760619451));
#73298=CARTESIAN_POINT('Ctrl Pts',(-1.43488843155748,-2.40950168234198,
135.091957229339));
#73299=CARTESIAN_POINT('Ctrl Pts',(-1.44263632833456,-2.28997925008049,
135.159125278876));
#73300=CARTESIAN_POINT('Ctrl Pts',(-1.45038422511167,-2.1675842764883,135.221326509952));
#73301=CARTESIAN_POINT('Ctrl Pts',(-1.45813212188875,-2.04277046414959,
135.278315455659));
#73302=CARTESIAN_POINT('Ctrl Pts',(-1.46587839797285,-1.91798276016975,
135.335292480507));
#73303=CARTESIAN_POINT('Ctrl Pts',(-1.47362467405697,-1.79077757926496,
135.387059226365));
#73304=CARTESIAN_POINT('Ctrl Pts',(-1.48137095014107,-1.66163131575496,
135.433417155674));
#73305=CARTESIAN_POINT('Ctrl Pts',(-1.48911728340643,-1.5324840989164,135.479775427187));
#73306=CARTESIAN_POINT('Ctrl Pts',(-1.49686361667177,-1.40139613885729,
135.520724670392));
#73307=CARTESIAN_POINT('Ctrl Pts',(-1.50460994993713,-1.26886143051752,
135.556115423177));
#73308=CARTESIAN_POINT('Ctrl Pts',(-1.51235801794012,-1.13629704194875,
135.591514101475));
#73309=CARTESIAN_POINT('Ctrl Pts',(-1.52010608594308,-1.00228563805597,
135.621351711527));
#73310=CARTESIAN_POINT('Ctrl Pts',(-1.52785415394607,-0.867333519892452,
135.645529446245));
#73311=CARTESIAN_POINT('Ctrl Pts',(-1.53561045668791,-0.732237973012169,
135.669732877347));
#73312=CARTESIAN_POINT('Ctrl Pts',(-1.54336675942976,-0.596200100099769,
135.688264347682));
#73313=CARTESIAN_POINT('Ctrl Pts',(-1.5511230621716,-0.45973403329057,135.701076627417));
#73314=CARTESIAN_POINT('Ctrl Pts',(-1.55888350468578,-0.323195130432044,
135.713895745452));
#73315=CARTESIAN_POINT('Ctrl Pts',(-1.56664394719994,-0.186227968542318,
135.720989570301));
#73316=CARTESIAN_POINT('Ctrl Pts',(-1.57440438971412,-0.0493478523353866,
135.722363042532));
#73317=CARTESIAN_POINT('Ctrl Pts',(-1.58217728997954,0.0877519959853531,
135.723738719582));
#73318=CARTESIAN_POINT('Ctrl Pts',(-1.58995019024499,0.224764128399301,
135.719375706269));
#73319=CARTESIAN_POINT('Ctrl Pts',(-1.59772309051041,0.361176289084986,
135.709331030392));
#73320=CARTESIAN_POINT('Ctrl Pts',(-1.60521342627248,0.492629524128983,
135.699651503785));
#73321=CARTESIAN_POINT('Ctrl Pts',(-1.61270376203451,0.623525345060253,
135.684696263298));
#73322=CARTESIAN_POINT('Ctrl Pts',(-1.62019409779657,0.753415232623536,
135.664561081513));
#73323=CARTESIAN_POINT('Ctrl Pts',(-1.62796843191566,0.888229934752388,
135.643662468191));
#73324=CARTESIAN_POINT('Ctrl Pts',(-1.63574276603476,1.02238797024958,135.6171171642));
#73325=CARTESIAN_POINT('Ctrl Pts',(-1.64351710015384,1.15537900420787,135.584975893776));
#73326=CARTESIAN_POINT('Ctrl Pts',(-1.65128185310095,1.28820613860273,135.552874234596));
#73327=CARTESIAN_POINT('Ctrl Pts',(-1.65904660604807,1.41986875672192,135.515190421982));
#73328=CARTESIAN_POINT('Ctrl Pts',(-1.66681135899518,1.54986324200278,135.472026736044));
#73329=CARTESIAN_POINT('Ctrl Pts',(-1.67456839988019,1.67972861492825,135.428905920888));
#73330=CARTESIAN_POINT('Ctrl Pts',(-1.68232544076515,1.80792878350356,135.380316186007));
#73331=CARTESIAN_POINT('Ctrl Pts',(-1.69008248165017,1.93397225272641,135.326410416958));
#73332=CARTESIAN_POINT('Ctrl Pts',(-1.69783367289029,2.0599206715883,135.272545298669));
#73333=CARTESIAN_POINT('Ctrl Pts',(-1.7055848641304,2.18371527030032,135.213372278724));
#73334=CARTESIAN_POINT('Ctrl Pts',(-1.71333605537052,2.30488194587762,135.149093322586));
#73335=CARTESIAN_POINT('Ctrl Pts',(-1.72108395214761,2.42599712238574,135.084841686718));
#73336=CARTESIAN_POINT('Ctrl Pts',(-1.72883184892476,2.54448625261087,135.015488613775));
#73337=CARTESIAN_POINT('Ctrl Pts',(-1.73657974570185,2.65989758096093,134.941283135731));
#73338=CARTESIAN_POINT('Ctrl Pts',(-1.74432602178596,2.77528476774922,134.867093179872));
#73339=CARTESIAN_POINT('Ctrl Pts',(-1.75207229787005,2.88759510458844,134.788053049148));
#73340=CARTESIAN_POINT('Ctrl Pts',(-1.75981857395416,2.99640405344108,134.704456233192));
#73341=CARTESIAN_POINT('Ctrl Pts',(-1.76756490721952,3.10521380549651,134.620858800142));
#73342=CARTESIAN_POINT('Ctrl Pts',(-1.77531124048487,3.21052180796133,134.532704852934));
#73343=CARTESIAN_POINT('Ctrl Pts',(-1.78305757375023,3.31193529779476,134.440329215577));
#73344=CARTESIAN_POINT('Ctrl Pts',(-1.79080564175319,3.41337149847581,134.347932891336));
#73345=CARTESIAN_POINT('Ctrl Pts',(-1.79855370975612,3.51091116207193,134.251313258899));
#73346=CARTESIAN_POINT('Ctrl Pts',(-1.80630177775907,3.60419749129478,134.150842876034));
#73347=CARTESIAN_POINT('Ctrl Pts',(-1.81405808050093,3.69758296633871,134.050265712051));
#73348=CARTESIAN_POINT('Ctrl Pts',(-1.82181438324286,3.78670581038964,133.94582990915));
#73349=CARTESIAN_POINT('Ctrl Pts',(-1.82957068598472,3.87124838667286,133.837942492377));
#73350=CARTESIAN_POINT('Ctrl Pts',(-1.83733112849891,3.9558360858748,133.729997492841));
#73351=CARTESIAN_POINT('Ctrl Pts',(-1.845091571013,4.03583841823812,133.618597526039));
#73352=CARTESIAN_POINT('Ctrl Pts',(-1.85285201352718,4.11098100561726,133.504178802917));
#73353=CARTESIAN_POINT('Ctrl Pts',(-1.86062491379261,4.18624421854832,133.389576404704));
#73354=CARTESIAN_POINT('Ctrl Pts',(-1.8683978140581,4.25663189615823,133.271945902051));
#73355=CARTESIAN_POINT('Ctrl Pts',(-1.87617071432354,4.32191513076584,133.151749095206));
#73356=CARTESIAN_POINT('Ctrl Pts',(-1.88366105008548,4.3848251553562,133.035921745049));
#73357=CARTESIAN_POINT('Ctrl Pts',(-1.89115138584741,4.44299527650109,132.917711710954));
#73358=CARTESIAN_POINT('Ctrl Pts',(-1.89864172160935,4.49626363477128,132.797548112292));
#73359=CARTESIAN_POINT('Ctrl Pts',(-1.90641605572843,4.5515516790364,132.672828474263));
#73360=CARTESIAN_POINT('Ctrl Pts',(-1.91419038984752,4.60173405816527,132.545609134234));
#73361=CARTESIAN_POINT('Ctrl Pts',(-1.9219647239666,4.64657759941095,132.416346869105));
#73362=CARTESIAN_POINT('Ctrl Pts',(-1.92972947691367,4.69136587499977,132.287243908166));
#73363=CARTESIAN_POINT('Ctrl Pts',(-1.93749422986068,4.73082827731791,132.156103397468));
#73364=CARTESIAN_POINT('Ctrl Pts',(-1.94525898280776,4.76477864046553,132.023404328785));
#73365=CARTESIAN_POINT('Ctrl Pts',(-1.95301602369273,4.79869528363381,131.890837058689));
#73366=CARTESIAN_POINT('Ctrl Pts',(-1.96077306457775,4.82711068612423,131.756714687477));
#73367=CARTESIAN_POINT('Ctrl Pts',(-1.96853010546272,4.84988780983042,131.621533362191));
#73368=CARTESIAN_POINT('Ctrl Pts',(-1.9762812967028,4.87264775713039,131.486453978195));
#73369=CARTESIAN_POINT('Ctrl Pts',(-1.98403248794285,4.88977782403887,131.350317613592));
#73370=CARTESIAN_POINT('Ctrl Pts',(-1.99178367918293,4.90119166557506,131.213632311918));
#73371=CARTESIAN_POINT('Ctrl Pts',(-1.99953157596002,4.91260065592421,131.077005105141));
#73372=CARTESIAN_POINT('Ctrl Pts',(-2.00727947273708,4.91829822062125,130.939829814128));
#73373=CARTESIAN_POINT('Ctrl Pts',(-2.01502736951417,4.91824969238585,130.802621121516));
#73374=CARTESIAN_POINT('Ctrl Pts',(-2.02277364559828,4.9182011743015,130.665441130004));
#73375=CARTESIAN_POINT('Ctrl Pts',(-2.03051992168244,4.91240895418478,130.528228141509));
#73376=CARTESIAN_POINT('Ctrl Pts',(-2.03826619776655,4.90089047999705,130.391497970219));
#73377=CARTESIAN_POINT('Ctrl Pts',(-2.0460125310319,4.88937192078256,130.254766789619));
#73378=CARTESIAN_POINT('Ctrl Pts',(-2.05375886429728,4.87212705597011,130.118518822921));
#73379=CARTESIAN_POINT('Ctrl Pts',(-2.06150519756264,4.84922528446493,129.983265493353));
#73380=CARTESIAN_POINT('Ctrl Pts',(-2.06925326556563,4.82631838426679,129.84798187474));
#73381=CARTESIAN_POINT('Ctrl Pts',(-2.07700133356858,4.79775212179937,129.71369372189));
#73382=CARTESIAN_POINT('Ctrl Pts',(-2.08474940157157,4.76364708281675,129.580902595045));
#73383=CARTESIAN_POINT('Ctrl Pts',(-2.09250570431343,4.72950579659288,129.447970336209));
#73384=CARTESIAN_POINT('Ctrl Pts',(-2.1002620070553,4.68981407199235,129.316538660965));
#73385=CARTESIAN_POINT('Ctrl Pts',(-2.10801830979716,4.64474266027962,129.187094813105));
#73386=CARTESIAN_POINT('Ctrl Pts',(-2.11577875231133,4.59964719259739,129.057581877166));
#73387=CARTESIAN_POINT('Ctrl Pts',(-2.12353919482551,4.5491664603238,128.930059246013));
#73388=CARTESIAN_POINT('Ctrl Pts',(-2.13129963733968,4.49351915199342,128.804993544423));
#73389=CARTESIAN_POINT('Ctrl Pts',(-2.13907253760511,4.43778251366356,128.679727076266));
#73390=CARTESIAN_POINT('Ctrl Pts',(-2.14684543787049,4.37686289937521,128.556925769641));
#73391=CARTESIAN_POINT('Ctrl Pts',(-2.15461833813592,4.31102510456372,128.437031825378));
#73392=CARTESIAN_POINT('Ctrl Pts',(-2.16210867389809,4.24758067942785,128.321496327982));
#73393=CARTESIAN_POINT('Ctrl Pts',(-2.16959900966031,4.17956960122271,128.208660746727));
#73394=CARTESIAN_POINT('Ctrl Pts',(-2.17708934542247,4.10726541125329,128.098893208037));
#73395=CARTESIAN_POINT('Ctrl Pts',(-2.18486367954157,4.03221978594608,127.984963799757));
#73396=CARTESIAN_POINT('Ctrl Pts',(-2.19263801366062,3.9523113538326,127.873978782166));
#73397=CARTESIAN_POINT('Ctrl Pts',(-2.20041234777972,3.86779837868953,127.766381229172));
#73398=CARTESIAN_POINT('Ctrl Pts',(-2.20817710072681,3.78338955823542,127.658916280546));
#73399=CARTESIAN_POINT('Ctrl Pts',(-2.21594185367394,3.69438772486799,127.554830794525));
#73400=CARTESIAN_POINT('Ctrl Pts',(-2.22370660662102,3.60109524071745,127.454540304507));
#73401=CARTESIAN_POINT('Ctrl Pts',(-2.23146364750606,3.50789541597685,127.354349424417));
#73402=CARTESIAN_POINT('Ctrl Pts',(-2.23922068839106,3.41041368566301,127.257946323774));
#73403=CARTESIAN_POINT('Ctrl Pts',(-2.2469777292761,3.30899339989057,127.165714476213));
#73404=CARTESIAN_POINT('Ctrl Pts',(-2.2547289205162,3.2076495959454,127.073552181407));
#73405=CARTESIAN_POINT('Ctrl Pts',(-2.26248011175626,3.10237343641189,126.985555140585));
#73406=CARTESIAN_POINT('Ctrl Pts',(-2.27023130299636,2.99354568113249,126.902070608165));
#73407=CARTESIAN_POINT('Ctrl Pts',(-2.27797919977346,2.88476418055157,126.818621558897));
#73408=CARTESIAN_POINT('Ctrl Pts',(-2.28572709655065,2.77243439610505,126.739681440869));
#73409=CARTESIAN_POINT('Ctrl Pts',(-2.29347499332775,2.65697060636137,126.665557619182));
#73410=CARTESIAN_POINT('Ctrl Pts',(-2.30122126941187,2.5415309691534,126.591449302601));
#73411=CARTESIAN_POINT('Ctrl Pts',(-2.30896754549594,2.42295895940206,126.522155489534));
#73412=CARTESIAN_POINT('Ctrl Pts',(-2.31671382158007,2.30169797724346,126.457940310687));
#73413=CARTESIAN_POINT('Ctrl Pts',(-2.32446015484543,2.18043609996399,126.393724657817));
#73414=CARTESIAN_POINT('Ctrl Pts',(-2.33220648811075,2.05648555617816,126.334587896943));
#73415=CARTESIAN_POINT('Ctrl Pts',(-2.3399528213761,1.93031413253364,126.280748077544));
#73416=CARTESIAN_POINT('Ctrl Pts',(-2.34770088937908,1.80411445367361,126.226896201092));
#73417=CARTESIAN_POINT('Ctrl Pts',(-2.35544895738211,1.67569326481025,126.178343779959));
#73418=CARTESIAN_POINT('Ctrl Pts',(-2.36319702538509,1.54553772232298,126.135260467497));
#73419=CARTESIAN_POINT('Ctrl Pts',(-2.37095332812695,1.41524384897629,126.092131365577));
#73420=CARTESIAN_POINT('Ctrl Pts',(-2.37870963086884,1.28321231158345,126.054483106745));
#73421=CARTESIAN_POINT('Ctrl Pts',(-2.38646593361071,1.14994533737769,126.022435400298));
#73422=CARTESIAN_POINT('Ctrl Pts',(-2.39422637612488,1.01660723457521,125.990370589025));
#73423=CARTESIAN_POINT('Ctrl Pts',(-2.40198681863897,0.882032764503286,
125.963912361724));
#73424=CARTESIAN_POINT('Ctrl Pts',(-2.40974726115314,0.746732718296827,
125.943128951627));
#73425=CARTESIAN_POINT('Ctrl Pts',(-2.41752016141858,0.611215476444824,
125.922312178155));
#73426=CARTESIAN_POINT('Ctrl Pts',(-2.42529306168403,0.474970719700355,
125.90718846917));
#73427=CARTESIAN_POINT('Ctrl Pts',(-2.43306596194947,0.338513612546228,
125.897774065122));
#73428=CARTESIAN_POINT('Ctrl Pts',(-2.44055629771141,0.207017064953346,
125.888701898375));
#73429=CARTESIAN_POINT('Ctrl Pts',(-2.44804663347336,0.0753236457449448,
125.884931156813));
#73430=CARTESIAN_POINT('Ctrl Pts',(-2.45553696923531,-0.0561090741358449,
125.886430683712));
#73431=CARTESIAN_POINT('Ctrl Pts',(-2.4633113033544,-0.192525105540563,
125.887987065629));
#73432=CARTESIAN_POINT('Ctrl Pts',(-2.4710856374735,-0.329092403527903,
125.895226179723));
#73433=CARTESIAN_POINT('Ctrl Pts',(-2.47885997159258,-0.465298599591438,
125.908170233633));
#73434=CARTESIAN_POINT('Ctrl Pts',(-2.48662472453968,-0.601336933691422,
125.921098335154));
#73435=CARTESIAN_POINT('Ctrl Pts',(-2.49438947748676,-0.737014665861168,
125.939717350605));
#73436=CARTESIAN_POINT('Ctrl Pts',(-2.50215423043386,-0.871818761966877,
125.963997500115));
#73437=CARTESIAN_POINT('Ctrl Pts',(-2.50991127131886,-1.00648896874375,
125.988253534238));
#73438=CARTESIAN_POINT('Ctrl Pts',(-2.51766831220388,-1.14028688395007,
126.018159444103));
#73439=CARTESIAN_POINT('Ctrl Pts',(-2.52542535308888,-1.27270429123198,
126.0536336364));
#73440=CARTESIAN_POINT('Ctrl Pts',(-2.53317654432907,-1.40502184151826,
126.089081077333));
#73441=CARTESIAN_POINT('Ctrl Pts',(-2.54092773556929,-1.53596057991021,
126.130088341913));
#73442=CARTESIAN_POINT('Ctrl Pts',(-2.54867892680949,-1.66502254143622,
126.176522785596));
#73443=CARTESIAN_POINT('Ctrl Pts',(-2.55642682358656,-1.79402964818452,
126.222937493402));
#73444=CARTESIAN_POINT('Ctrl Pts',(-2.56417472036356,-1.92116119748271,
126.274774660387));
#73445=CARTESIAN_POINT('Ctrl Pts',(-2.57192261714064,-2.04593466667936,
126.331851880606));
#73446=CARTESIAN_POINT('Ctrl Pts',(-2.57966889322474,-2.17068203595605,
126.388917161502));
#73447=CARTESIAN_POINT('Ctrl Pts',(-2.58741516930889,-2.29307195094467,
126.451220152881));
#73448=CARTESIAN_POINT('Ctrl Pts',(-2.59516144539299,-2.41264252239813,
126.51853057875));
#73449=CARTESIAN_POINT('Ctrl Pts',(-2.60290777865834,-2.53221397649438,
126.58584150149));
#73450=CARTESIAN_POINT('Ctrl Pts',(-2.61065411192368,-2.64896570483473,
126.65815974069));
#73451=CARTESIAN_POINT('Ctrl Pts',(-2.61840044518902,-2.76246140610562,
126.735209595267));
#73452=CARTESIAN_POINT('Ctrl Pts',(-2.626148513192,-2.87598252395188,126.812276704625));
#73453=CARTESIAN_POINT('Ctrl Pts',(-2.63389658119496,-2.9862458403693,126.894077318311));
#73454=CARTESIAN_POINT('Ctrl Pts',(-2.64164464919793,-3.09284530126687,
126.980293279648));
#73455=CARTESIAN_POINT('Ctrl Pts',(-2.6494009519398,-3.19955805734032,127.066600872335));
#73456=CARTESIAN_POINT('Ctrl Pts',(-2.65715725468168,-3.30259887476059,
127.157332940562));
#73457=CARTESIAN_POINT('Ctrl Pts',(-2.66491355742355,-3.40159557261785,
127.252131652135));
#73458=CARTESIAN_POINT('Ctrl Pts',(-2.67267399993771,-3.50064510799336,
127.346980960635));
#73459=CARTESIAN_POINT('Ctrl Pts',(-2.68043444245186,-3.59564595219568,
127.445900955519));
#73460=CARTESIAN_POINT('Ctrl Pts',(-2.68819488496604,-3.686264603589,127.548498775468));
#73461=CARTESIAN_POINT('Ctrl Pts',(-2.69596778523146,-3.77702872408616,
127.651261294547));
#73462=CARTESIAN_POINT('Ctrl Pts',(-2.70374068549691,-3.86339634776465,
127.757713132924));
#73463=CARTESIAN_POINT('Ctrl Pts',(-2.71151358576233,-3.94507535208676,
127.867429646491));
#73464=CARTESIAN_POINT('Ctrl Pts',(-2.71900392152429,-4.0237851188641,127.97315768843));
#73465=CARTESIAN_POINT('Ctrl Pts',(-2.7264942572863,-4.09814106040651,128.081916913842));
#73466=CARTESIAN_POINT('Ctrl Pts',(-2.73398459304826,-4.16792206147586,
128.193305514363));
#73467=CARTESIAN_POINT('Ctrl Pts',(-2.74197015249147,-4.24231663466434,
128.312058574176));
#73468=CARTESIAN_POINT('Ctrl Pts',(-2.74995571193477,-4.31173644726357,
128.434159702435));
#73469=CARTESIAN_POINT('Ctrl Pts',(-2.75794127137803,-4.37587548579146,
128.559166462187));
#73470=CARTESIAN_POINT('Ctrl Pts',(-2.76591645663073,-4.43993120008732,
128.684010823304));
#73471=CARTESIAN_POINT('Ctrl Pts',(-2.77389164188335,-4.49871963179323,
128.811752983107));
#73472=CARTESIAN_POINT('Ctrl Pts',(-2.78186682713604,-4.55197819272829,
128.941922002356));
#73473=CARTESIAN_POINT('Ctrl Pts',(-2.789829834859,-4.60515543170167,129.071892262948));
#73474=CARTESIAN_POINT('Ctrl Pts',(-2.79779284258203,-4.65281948972259,
129.204281665528));
#73475=CARTESIAN_POINT('Ctrl Pts',(-2.80575585030499,-4.69475414447413,
129.338595770995));
#73476=CARTESIAN_POINT('Ctrl Pts',(-2.81053681060419,-4.71993155563622,
129.419237461698));
#73477=CARTESIAN_POINT('Ctrl Pts',(-2.81531777090342,-4.74304453855751,
129.500572488431));
#73478=CARTESIAN_POINT('Ctrl Pts',(-2.82009873120262,-4.76405452823401,
129.582490119308));
#73479=CARTESIAN_POINT('Origin',(213.235140564004,0.,130.804360617566));
#73480=CARTESIAN_POINT('',(-4.91509110695617,-4.76405452823401,129.582490119308));
#73481=CARTESIAN_POINT('',(-4.56974458955163,-4.76405452823408,129.582490119308));
#73482=CARTESIAN_POINT('',(213.235140564004,-4.76405452823405,129.582490119308));
#73483=CARTESIAN_POINT('',(-3.2351405639729,-4.91824878730941,130.80781440238));
#73484=CARTESIAN_POINT('Ctrl Pts',(-3.23514056400865,-4.91824878730896,
130.80781440301));
#73485=CARTESIAN_POINT('Ctrl Pts',(-3.24719065751056,-4.91809994407063,
131.019769687541));
#73486=CARTESIAN_POINT('Ctrl Pts',(-3.25924075101248,-4.90424944354162,
131.231249688169));
#73487=CARTESIAN_POINT('Ctrl Pts',(-3.27129084451443,-4.87688073448147,
131.440927475126));
#73488=CARTESIAN_POINT('Ctrl Pts',(-3.27906517863354,-4.85922332056942,
131.576204863048));
#73489=CARTESIAN_POINT('Ctrl Pts',(-3.28683951275261,-4.83590508390784,
131.710961278448));
#73490=CARTESIAN_POINT('Ctrl Pts',(-3.29461384687173,-4.80696448749442,
131.844685316142));
#73491=CARTESIAN_POINT('Ctrl Pts',(-3.30237859981885,-4.77805955777962,
131.978244550911));
#73492=CARTESIAN_POINT('Ctrl Pts',(-3.310143352766,-4.7435461369734,132.110773561046));
#73493=CARTESIAN_POINT('Ctrl Pts',(-3.31790810571312,-4.70351439032332,
132.241766420574));
#73494=CARTESIAN_POINT('Ctrl Pts',(-3.32566514659814,-4.66352240376836,
132.372629176148));
#73495=CARTESIAN_POINT('Ctrl Pts',(-3.33342218748322,-4.61802311209007,
132.501958445902));
#73496=CARTESIAN_POINT('Ctrl Pts',(-3.34117922836825,-4.56715756229186,
132.629259207543));
#73497=CARTESIAN_POINT('Ctrl Pts',(-3.3489304196084,-4.51633037060043,132.756463970689));
#73498=CARTESIAN_POINT('Ctrl Pts',(-3.3566816108485,-4.46014512005288,132.881642908936));
#73499=CARTESIAN_POINT('Ctrl Pts',(-3.36443280208866,-4.39879234078576,
133.004317209216));
#73500=CARTESIAN_POINT('Ctrl Pts',(-3.37218069886577,-4.33746563808646,
133.126939369646));
#73501=CARTESIAN_POINT('Ctrl Pts',(-3.3799285956429,-4.27097594952999,133.247058660452));
#73502=CARTESIAN_POINT('Ctrl Pts',(-3.38767649242001,-4.19956139448581,
133.364217480057));
#73503=CARTESIAN_POINT('Ctrl Pts',(-3.39542276850415,-4.12816177782704,
133.481351792563));
#73504=CARTESIAN_POINT('Ctrl Pts',(-3.40316904458825,-4.05183954711802,
133.595526532));
#73505=CARTESIAN_POINT('Ctrl Pts',(-3.41091532067239,-3.97087791973199,
133.706310239645));
#73506=CARTESIAN_POINT('Ctrl Pts',(-3.41866165393777,-3.88991569470562,
133.81709476507));
#73507=CARTESIAN_POINT('Ctrl Pts',(-3.42640798720316,-3.80431423534883,
133.924487893098));
#73508=CARTESIAN_POINT('Ctrl Pts',(-3.43415432046854,-3.71439884402085,
134.028088938941));
#73509=CARTESIAN_POINT('Ctrl Pts',(-3.44190238847154,-3.6244633167644,134.13171318552));
#73510=CARTESIAN_POINT('Ctrl Pts',(-3.44965045647455,-3.53021219137304,
134.231543364872));
#73511=CARTESIAN_POINT('Ctrl Pts',(-3.45739852447755,-3.43200935617864,
134.327213842099));
#73512=CARTESIAN_POINT('Ctrl Pts',(-3.46515482721944,-3.33370214984237,
134.422985999047));
#73513=CARTESIAN_POINT('Ctrl Pts',(-3.47291112996132,-3.23143512438988,
134.51458934923));
#73514=CARTESIAN_POINT('Ctrl Pts',(-3.4806674327032,-3.12560756524862,134.601696579864));
#73515=CARTESIAN_POINT('Ctrl Pts',(-3.48842787521739,-3.01972352275263,
134.68885030225));
#73516=CARTESIAN_POINT('Ctrl Pts',(-3.49618831773161,-2.91027547177423,
134.771502887958));
#73517=CARTESIAN_POINT('Ctrl Pts',(-3.50394876024581,-2.79769291332397,
134.849369569996));
#73518=CARTESIAN_POINT('Ctrl Pts',(-3.51172166051126,-2.68492962735628,
134.927361250545));
#73519=CARTESIAN_POINT('Ctrl Pts',(-3.5194945607767,-2.56902210956334,135.000551465963));
#73520=CARTESIAN_POINT('Ctrl Pts',(-3.52726746104216,-2.450426534054,135.068700292557));
#73521=CARTESIAN_POINT('Ctrl Pts',(-3.53475779680389,-2.33614220644363,
135.134371737645));
#73522=CARTESIAN_POINT('Ctrl Pts',(-3.54224813256557,-2.21936213643618,
135.195361822108));
#73523=CARTESIAN_POINT('Ctrl Pts',(-3.54973846832729,-2.10051143564684,
135.251498435446));
#73524=CARTESIAN_POINT('Ctrl Pts',(-3.55751280244637,-1.97715447440831,
135.309763485543));
#73525=CARTESIAN_POINT('Ctrl Pts',(-3.56528713656548,-1.85117600913743,
135.362984326765));
#73526=CARTESIAN_POINT('Ctrl Pts',(-3.57306147068456,-1.72302708969003,
135.410916892127));
#73527=CARTESIAN_POINT('Ctrl Pts',(-3.58082622363164,-1.59503610233302,
135.458790384885));
#73528=CARTESIAN_POINT('Ctrl Pts',(-3.58859097657867,-1.46488034570736,
135.501388433669));
#73529=CARTESIAN_POINT('Ctrl Pts',(-3.59635572952575,-1.33303420618238,
135.538513431708));
#73530=CARTESIAN_POINT('Ctrl Pts',(-3.60411277041076,-1.2013190181017,135.575601556675));
#73531=CARTESIAN_POINT('Ctrl Pts',(-3.6118698112958,-1.06791716212818,135.607227343325));
#73532=CARTESIAN_POINT('Ctrl Pts',(-3.6196268521808,-0.933321353889516,
135.633241886853));
#73533=CARTESIAN_POINT('Ctrl Pts',(-3.62737804342092,-0.798827045397031,
135.659236812612));
#73534=CARTESIAN_POINT('Ctrl Pts',(-3.63512923466104,-0.663140959076525,
135.679628843866));
#73535=CARTESIAN_POINT('Ctrl Pts',(-3.64288042590115,-0.526768920116495,
135.694319468855));
#73536=CARTESIAN_POINT('Ctrl Pts',(-3.65062832267823,-0.390454842910681,
135.709003849937));
#73537=CARTESIAN_POINT('Ctrl Pts',(-3.65837621945535,-0.253455780834875,
135.717991602626));
#73538=CARTESIAN_POINT('Ctrl Pts',(-3.66612411623242,-0.116285436392451,
135.721235718663));
#73539=CARTESIAN_POINT('Ctrl Pts',(-3.67387039231652,0.0208562149709664,
135.7244791561));
#73540=CARTESIAN_POINT('Ctrl Pts',(-3.68161666840053,0.158168686827711,
135.721981337385));
#73541=CARTESIAN_POINT('Ctrl Pts',(-3.68936294448463,0.295135894826391,
135.713747327338));
#73542=CARTESIAN_POINT('Ctrl Pts',(-3.69710927774999,0.432104113886074,
135.705513256509));
#73543=CARTESIAN_POINT('Ctrl Pts',(-3.70485561101539,0.56872667374139,135.691542933315));
#73544=CARTESIAN_POINT('Ctrl Pts',(-3.71260194428075,0.704490633061288,
135.67189346393));
#73545=CARTESIAN_POINT('Ctrl Pts',(-3.72035001228372,0.84028499577837,135.652239594182));
#73546=CARTESIAN_POINT('Ctrl Pts',(-3.72809808028665,0.975219988490295,
135.626904103487));
#73547=CARTESIAN_POINT('Ctrl Pts',(-3.73584614828962,1.10879130166956,135.595995506812));
#73548=CARTESIAN_POINT('Ctrl Pts',(-3.74360245103147,1.24250457602998,135.565054060113));
#73549=CARTESIAN_POINT('Ctrl Pts',(-3.75135875377329,1.37485089414771,135.528527763557));
#73550=CARTESIAN_POINT('Ctrl Pts',(-3.75911505651513,1.50533905498266,135.48657562673));
#73551=CARTESIAN_POINT('Ctrl Pts',(-3.76687549902928,1.63589686127797,135.444601098785));
#73552=CARTESIAN_POINT('Ctrl Pts',(-3.77463594154354,1.76459416744757,135.397195095244));
#73553=CARTESIAN_POINT('Ctrl Pts',(-3.78239638405771,1.89095923516923,135.344565043958));
#73554=CARTESIAN_POINT('Ctrl Pts',(-3.79016928432313,2.01752715531576,135.291850506241));
#73555=CARTESIAN_POINT('Ctrl Pts',(-3.79794218458852,2.14175500096732,135.233895328055));
#73556=CARTESIAN_POINT('Ctrl Pts',(-3.80571508485394,2.26319434427661,135.17095361698));
#73557=CARTESIAN_POINT('Ctrl Pts',(-3.81320542061605,2.38021906157068,135.110299995643));
#73558=CARTESIAN_POINT('Ctrl Pts',(-3.82069575637814,2.49465422731484,135.045016245777));
#73559=CARTESIAN_POINT('Ctrl Pts',(-3.82818609214024,2.60612525685957,134.975366995895));
#73560=CARTESIAN_POINT('Ctrl Pts',(-3.83596042625933,2.72182274436923,134.903076973534));
#73561=CARTESIAN_POINT('Ctrl Pts',(-3.8437347603784,2.83469338305596,134.825854887478));
#73562=CARTESIAN_POINT('Ctrl Pts',(-3.85150909449749,2.94428802898831,134.743948294577));
#73563=CARTESIAN_POINT('Ctrl Pts',(-3.85927384744459,3.0537476093143,134.662142644231));
#73564=CARTESIAN_POINT('Ctrl Pts',(-3.86703860039166,3.15993891988318,134.575664205862));
#73565=CARTESIAN_POINT('Ctrl Pts',(-3.87480335333876,3.26243929110219,134.484805282871));
#73566=CARTESIAN_POINT('Ctrl Pts',(-3.88256039422377,3.36483785750751,134.394036602243));
#73567=CARTESIAN_POINT('Ctrl Pts',(-3.89031743510878,3.46355248917999,134.298896352863));
#73568=CARTESIAN_POINT('Ctrl Pts',(-3.89807447599378,3.55819158345901,134.199718583658));
#73569=CARTESIAN_POINT('Ctrl Pts',(-3.90582566723391,3.65275930966084,134.10061560518));
#73570=CARTESIAN_POINT('Ctrl Pts',(-3.91357685847406,3.74325734706025,133.997481448924));
#73571=CARTESIAN_POINT('Ctrl Pts',(-3.92132804971419,3.82932940405408,133.890688431935));
#73572=CARTESIAN_POINT('Ctrl Pts',(-3.92907594649128,3.91536487812764,133.783940804827));
#73573=CARTESIAN_POINT('Ctrl Pts',(-3.93682384326838,3.99697786845188,133.673537713754));
#73574=CARTESIAN_POINT('Ctrl Pts',(-3.94457174004546,4.07385115689435,133.559885942068));
#73575=CARTESIAN_POINT('Ctrl Pts',(-3.95231801612957,4.15070836510207,133.446257943882));
#73576=CARTESIAN_POINT('Ctrl Pts',(-3.96006429221365,4.2228276245579,133.32938294039));
#73577=CARTESIAN_POINT('Ctrl Pts',(-3.96781056829775,4.28993424023908,133.20969786563));
#73578=CARTESIAN_POINT('Ctrl Pts',(-3.9755569015631,4.35704135128605,133.090011907382));
#73579=CARTESIAN_POINT('Ctrl Pts',(-3.98330323482846,4.4191355535163,132.967516177494));
#73580=CARTESIAN_POINT('Ctrl Pts',(-3.99104956809381,4.47598763465161,132.842673095315));
#73581=CARTESIAN_POINT('Ctrl Pts',(-3.99879763609679,4.53285244741631,132.717802055393));
#73582=CARTESIAN_POINT('Ctrl Pts',(-4.00654570409979,4.58447264108795,132.590582972893));
#73583=CARTESIAN_POINT('Ctrl Pts',(-4.01429377210277,4.6306669207623,132.461498792691));
#73584=CARTESIAN_POINT('Ctrl Pts',(-4.02205007484463,4.67691029626681,132.332277420287));
#73585=CARTESIAN_POINT('Ctrl Pts',(-4.02980637758658,4.71771610617723,132.201187359119));
#73586=CARTESIAN_POINT('Ctrl Pts',(-4.03756268032845,4.75295262360015,132.068727819099));
#73587=CARTESIAN_POINT('Ctrl Pts',(-4.04532312284262,4.78820794781337,131.936197581434));
#73588=CARTESIAN_POINT('Ctrl Pts',(-4.05308356535672,4.81788797201779,131.802296789986));
#73589=CARTESIAN_POINT('Ctrl Pts',(-4.06084400787088,4.84191222505194,131.667534451387));
#73590=CARTESIAN_POINT('Ctrl Pts',(-4.06861690813632,4.86597504394984,131.532555780317));
#73591=CARTESIAN_POINT('Ctrl Pts',(-4.0763898084018,4.88436389617445,131.396713186012));
#73592=CARTESIAN_POINT('Ctrl Pts',(-4.08416270866724,4.89705018342472,131.260521294872));
#73593=CARTESIAN_POINT('Ctrl Pts',(-4.09165304442921,4.90927529217851,131.129280322022));
#73594=CARTESIAN_POINT('Ctrl Pts',(-4.09914338019111,4.91620522680309,130.997715314665));
#73595=CARTESIAN_POINT('Ctrl Pts',(-4.10663371595308,4.91786015460807,130.866284459649));
#73596=CARTESIAN_POINT('Ctrl Pts',(-4.11440805007216,4.91957782950379,130.729870363817));
#73597=CARTESIAN_POINT('Ctrl Pts',(-4.12218238419122,4.91561803869035,130.593168675059));
#73598=CARTESIAN_POINT('Ctrl Pts',(-4.1299567183103,4.90594628549177,130.456691081412));
#73599=CARTESIAN_POINT('Ctrl Pts',(-4.13772147125738,4.89628645186462,130.320381684202));
#73600=CARTESIAN_POINT('Ctrl Pts',(-4.14548622420451,4.88092868969752,130.184296218834));
#73601=CARTESIAN_POINT('Ctrl Pts',(-4.1532509771516,4.85989045888151,130.048948286337));
#73602=CARTESIAN_POINT('Ctrl Pts',(-4.1610080180366,4.83887312353292,129.913734783315));
#73603=CARTESIAN_POINT('Ctrl Pts',(-4.16876505892156,4.8121866068751,129.779257739225));
#73604=CARTESIAN_POINT('Ctrl Pts',(-4.17652209980656,4.77990028292875,129.646027182083));
#73605=CARTESIAN_POINT('Ctrl Pts',(-4.18427329104669,4.74763830635043,129.51289709514));
#73606=CARTESIAN_POINT('Ctrl Pts',(-4.19202448228685,4.70978501953334,129.381012002591));
#73607=CARTESIAN_POINT('Ctrl Pts',(-4.19977567352697,4.66646107903714,129.250872909108));
#73608=CARTESIAN_POINT('Ctrl Pts',(-4.20752357030405,4.62315555237136,129.120789128211));
#73609=CARTESIAN_POINT('Ctrl Pts',(-4.21527146708113,4.57438411985224,128.992450240581));
#73610=CARTESIAN_POINT('Ctrl Pts',(-4.22301936385821,4.52031755568503,128.866343007154));
#73611=CARTESIAN_POINT('Ctrl Pts',(-4.23076563994232,4.46626230107749,128.740262152643));
#73612=CARTESIAN_POINT('Ctrl Pts',(-4.23851191602635,4.40691427191419,128.616412382921));
#73613=CARTESIAN_POINT('Ctrl Pts',(-4.24625819211045,4.34249259380731,128.495260980212));
#73614=CARTESIAN_POINT('Ctrl Pts',(-4.25400452537579,4.27807044015423,128.374108683191));
#73615=CARTESIAN_POINT('Ctrl Pts',(-4.26175085864116,4.20857474638045,128.255655138126));
#73616=CARTESIAN_POINT('Ctrl Pts',(-4.26949719190651,4.13427066414663,128.140343136753));
#73617=CARTESIAN_POINT('Ctrl Pts',(-4.27724525990948,4.05994994202888,128.025005312057));
#73618=CARTESIAN_POINT('Ctrl Pts',(-4.28499332791247,3.98081890046283,127.912810759571));
#73619=CARTESIAN_POINT('Ctrl Pts',(-4.29274139591544,3.89718586032778,127.804173051336));
#73620=CARTESIAN_POINT('Ctrl Pts',(-4.3004976986573,3.81346393400231,127.695419881652));
#73621=CARTESIAN_POINT('Ctrl Pts',(-4.30825400139915,3.72523068987249,127.59023141798));
#73622=CARTESIAN_POINT('Ctrl Pts',(-4.316010304141,3.63283492577143,127.488988321037));
#73623=CARTESIAN_POINT('Ctrl Pts',(-4.32377074665518,3.54038984726895,127.387691187604));
#73624=CARTESIAN_POINT('Ctrl Pts',(-4.33153118916932,3.44377809721412,127.290343894173));
#73625=CARTESIAN_POINT('Ctrl Pts',(-4.33929163168349,3.34338442067241,127.197289273927));
#73626=CARTESIAN_POINT('Ctrl Pts',(-4.34706453194892,3.24282958328872,127.104085274143));
#73627=CARTESIAN_POINT('Ctrl Pts',(-4.35483743221439,3.13848098523749,127.015187971605));
#73628=CARTESIAN_POINT('Ctrl Pts',(-4.36261033247982,3.03075613820552,126.930899595014));
#73629=CARTESIAN_POINT('Ctrl Pts',(-4.37010066824191,2.9269473607048,126.849675313221));
#73630=CARTESIAN_POINT('Ctrl Pts',(-4.37759100400395,2.82000379283648,126.772730862824));
#73631=CARTESIAN_POINT('Ctrl Pts',(-4.38508133976603,2.710321821097,126.700296937677));
#73632=CARTESIAN_POINT('Ctrl Pts',(-4.39285567388512,2.5964812240627,126.625116658243));
#73633=CARTESIAN_POINT('Ctrl Pts',(-4.40063000800419,2.47932985806009,126.554557540504));
#73634=CARTESIAN_POINT('Ctrl Pts',(-4.40840434212328,2.35927957442864,126.488925187371));
#73635=CARTESIAN_POINT('Ctrl Pts',(-4.41616909507036,2.23937724204273,126.423373720248));
#73636=CARTESIAN_POINT('Ctrl Pts',(-4.42393384801746,2.11658344030295,126.36273712241));
#73637=CARTESIAN_POINT('Ctrl Pts',(-4.43169860096455,1.99133971379722,126.307278318257));
#73638=CARTESIAN_POINT('Ctrl Pts',(-4.43945564184955,1.86622038112628,126.251874596571));
#73639=CARTESIAN_POINT('Ctrl Pts',(-4.44721268273454,1.73865632123798,126.201638591722));
#73640=CARTESIAN_POINT('Ctrl Pts',(-4.45496972361954,1.60911413349843,126.156787619982));
#73641=CARTESIAN_POINT('Ctrl Pts',(-4.46272091485966,1.47966963453053,126.111970470708));
#73642=CARTESIAN_POINT('Ctrl Pts',(-4.47047210609975,1.34825034484623,126.072530398973));
#73643=CARTESIAN_POINT('Ctrl Pts',(-4.47822329733987,1.2153429916841,126.038636698258));
#73644=CARTESIAN_POINT('Ctrl Pts',(-4.48597119411694,1.08249212769231,126.00475740327));
#73645=CARTESIAN_POINT('Ctrl Pts',(-4.49371909089409,0.948154836198017,
125.976419887112));
#73646=CARTESIAN_POINT('Ctrl Pts',(-4.50146698767117,0.812832950592326,
125.953743578783));
#73647=CARTESIAN_POINT('Ctrl Pts',(-4.50921326375526,0.6775393714079,125.931072013849));
#73648=CARTESIAN_POINT('Ctrl Pts',(-4.51695953983933,0.541261993114158,
125.914059365874));
#73649=CARTESIAN_POINT('Ctrl Pts',(-4.52470581592343,0.40451239622551,125.902773855731));
#73650=CARTESIAN_POINT('Ctrl Pts',(-4.53245214918877,0.267761789882404,
125.89148826228));
#73651=CARTESIAN_POINT('Ctrl Pts',(-4.54019848245411,0.130539347629309,
125.885929923176));
#73652=CARTESIAN_POINT('Ctrl Pts',(-4.54794481571946,-0.00663907635700782,
125.886115098566));
#73653=CARTESIAN_POINT('Ctrl Pts',(-4.55569288372243,-0.143848220500248,
125.886300315424));
#73654=CARTESIAN_POINT('Ctrl Pts',(-4.5634409517254,-0.281012935871234,
125.892231605679));
#73655=CARTESIAN_POINT('Ctrl Pts',(-4.57118901972837,-0.417618617632918,
125.90387311603));
#73656=CARTESIAN_POINT('Ctrl Pts',(-4.57894532247021,-0.554369485538806,
125.915526999118));
#73657=CARTESIAN_POINT('Ctrl Pts',(-4.58670162521208,-0.690559742787245,
125.932903192314));
#73658=CARTESIAN_POINT('Ctrl Pts',(-4.59445792795393,-0.825680594987528,
125.955913998538));
#73659=CARTESIAN_POINT('Ctrl Pts',(-4.6022183704681,-0.960873565255225,
125.978937086323));
#73660=CARTESIAN_POINT('Ctrl Pts',(-4.6099788129823,-1.09499561101543,126.007600697892));
#73661=CARTESIAN_POINT('Ctrl Pts',(-4.61773925549647,-1.22755033289508,
126.041766446034));
#73662=CARTESIAN_POINT('Ctrl Pts',(-4.62551215576191,-1.36031784338194,
126.075987040069));
#73663=CARTESIAN_POINT('Ctrl Pts',(-4.63328505602736,-1.49151262781264,
126.115727307456));
#73664=CARTESIAN_POINT('Ctrl Pts',(-4.6410579562928,-1.62065473735613,126.160799345785));
#73665=CARTESIAN_POINT('Ctrl Pts',(-4.64854829205488,-1.74510220592907,
126.204232901991));
#73666=CARTESIAN_POINT('Ctrl Pts',(-4.65603862781688,-1.86764336190305,
126.252617199525));
#73667=CARTESIAN_POINT('Ctrl Pts',(-4.66352896357895,-1.98786985942046,
126.305743442866));
#73668=CARTESIAN_POINT('Ctrl Pts',(-4.67130381885714,-2.11266314619595,
126.360887680263));
#73669=CARTESIAN_POINT('Ctrl Pts',(-4.67907867413534,-2.23535778873874,
126.421315921051));
#73670=CARTESIAN_POINT('Ctrl Pts',(-4.68685352941353,-2.35547396300495,
126.486846810743));
#73671=CARTESIAN_POINT('Ctrl Pts',(-4.69461868530658,-2.47544028843246,
126.552295948517));
#73672=CARTESIAN_POINT('Ctrl Pts',(-4.70238384119963,-2.59283420623772,
126.622834883091));
#73673=CARTESIAN_POINT('Ctrl Pts',(-4.71014899709269,-2.7071957753986,126.698234207412));
#73674=CARTESIAN_POINT('Ctrl Pts',(-4.71790632321508,-2.82144203137434,
126.773557505002));
#73675=CARTESIAN_POINT('Ctrl Pts',(-4.72566364933747,-2.93266169948924,
126.853731224905));
#73676=CARTESIAN_POINT('Ctrl Pts',(-4.73342097545986,-3.04041969265861,
126.938480232066));
#73677=CARTESIAN_POINT('Ctrl Pts',(-4.7411719472867,-3.14808941750899,127.023159818368));
#73678=CARTESIAN_POINT('Ctrl Pts',(-4.74892291911353,-3.25230280751886,
127.112406988649));
#73679=CARTESIAN_POINT('Ctrl Pts',(-4.75667389094036,-3.35265438215081,
127.205903773814));
#73680=CARTESIAN_POINT('Ctrl Pts',(-4.76442139553933,-3.4529610666987,127.299358735235));
#73681=CARTESIAN_POINT('Ctrl Pts',(-4.7721689001383,-3.54940908734863,127.397059263635));
#73682=CARTESIAN_POINT('Ctrl Pts',(-4.77991640473726,-3.64162677196687,
127.498647757048));
#73683=CARTESIAN_POINT('Ctrl Pts',(-4.78766212144777,-3.73382317554775,
127.600212806925));
#73684=CARTESIAN_POINT('Ctrl Pts',(-4.79540783815827,-3.82179092344786,
127.705663746969));
#73685=CARTESIAN_POINT('Ctrl Pts',(-4.80315355486877,-3.90519617169571,
127.814607128886));
#73686=CARTESIAN_POINT('Ctrl Pts',(-4.81089916147566,-3.98860023435679,
127.923548962198));
#73687=CARTESIAN_POINT('Ctrl Pts',(-4.81864476808254,-4.0674416898175,128.035982827566));
#73688=CARTESIAN_POINT('Ctrl Pts',(-4.82639037468942,-4.1414281066588,128.151483632126));
#73689=CARTESIAN_POINT('Ctrl Pts',(-4.83414108432917,-4.21546326792204,
128.267060532005));
#73690=CARTESIAN_POINT('Ctrl Pts',(-4.84189179396892,-4.2846367881272,128.385708078921));
#73691=CARTESIAN_POINT('Ctrl Pts',(-4.84964250360866,-4.34870042526321,
128.506973476961));
#73692=CARTESIAN_POINT('Ctrl Pts',(-4.85739577780969,-4.41278525982903,
128.628278999398));
#73693=CARTESIAN_POINT('Ctrl Pts',(-4.86514905201066,-4.47175667099767,
128.752203747457));
#73694=CARTESIAN_POINT('Ctrl Pts',(-4.87290232621169,-4.52541366335418,
128.878272811149));
#73695=CARTESIAN_POINT('Ctrl Pts',(-4.88066480617851,-4.57913436475701,
129.004491561574));
#73696=CARTESIAN_POINT('Ctrl Pts',(-4.88842728614534,-4.62752789909615,
129.132859349595));
#73697=CARTESIAN_POINT('Ctrl Pts',(-4.89618976611217,-4.6704422594521,129.262883350908));
#73698=CARTESIAN_POINT('Ctrl Pts',(-4.90249021306015,-4.70527386634634,
129.368417835472));
#73699=CARTESIAN_POINT('Ctrl Pts',(-4.90879066000816,-4.73649681451379,
129.47504301176));
#73700=CARTESIAN_POINT('Ctrl Pts',(-4.91509110695614,-4.76405452823401,
129.582490119308));
#73701=CARTESIAN_POINT('Ctrl Pts',(-3.16500955108754,-4.76405452823408,
129.582490119308));
#73702=CARTESIAN_POINT('Ctrl Pts',(-3.17265462575404,-4.79768322009091,
129.713607878472));
#73703=CARTESIAN_POINT('Ctrl Pts',(-3.18029970042054,-4.82587473776987,
129.846037078759));
#73704=CARTESIAN_POINT('Ctrl Pts',(-3.18794477508703,-4.84854884266275,
129.979280510659));
#73705=CARTESIAN_POINT('Ctrl Pts',(-3.19581073990133,-4.87187807345036,
130.116373762561));
#73706=CARTESIAN_POINT('Ctrl Pts',(-3.20367670471566,-4.88936616706746,
130.254328551633));
#73707=CARTESIAN_POINT('Ctrl Pts',(-3.21154266952996,-4.90098312584827,
130.392599202848));
#73708=CARTESIAN_POINT('Ctrl Pts',(-3.21940863434426,-4.91260008462908,
130.530869854064));
#73709=CARTESIAN_POINT('Ctrl Pts',(-3.22727459915858,-4.91834594800464,
130.66945590665));
#73710=CARTESIAN_POINT('Ctrl Pts',(-3.23514056397289,-4.91824878730941,
130.80781440238));
#73711=CARTESIAN_POINT('',(-2.8898594360264,-4.91824974010731,130.805959502914));
#73712=CARTESIAN_POINT('Ctrl Pts',(-2.82009873120262,-4.76405452823401,
129.582490119308));
#73713=CARTESIAN_POINT('Ctrl Pts',(-2.82804801001931,-4.7989877331598,129.718694155128));
#73714=CARTESIAN_POINT('Ctrl Pts',(-2.83599728883601,-4.82810441912981,
129.856509573153));
#73715=CARTESIAN_POINT('Ctrl Pts',(-2.84394656765269,-4.8512666200099,129.99541362049));
#73716=CARTESIAN_POINT('Ctrl Pts',(-2.85188872461985,-4.87440806961014,
130.134193222108));
#73717=CARTESIAN_POINT('Ctrl Pts',(-2.85983088158702,-4.89160560644795,
130.274059153101));
#73718=CARTESIAN_POINT('Ctrl Pts',(-2.86777303855419,-4.90277209154466,
130.414477454464));
#73719=CARTESIAN_POINT('Ctrl Pts',(-2.87513517103323,-4.91312307591163,
130.544640852315));
#73720=CARTESIAN_POINT('Ctrl Pts',(-2.88249730351221,-4.91829222347275,
130.675278536417));
#73721=CARTESIAN_POINT('Ctrl Pts',(-2.88985943599124,-4.91824974010752,
130.80595950229));
#73722=CARTESIAN_POINT('Ctrl Pts',(-2.88985943602637,-4.91824974010731,
130.805959502914));
#73723=CARTESIAN_POINT('Ctrl Pts',(-2.89820794086171,-4.91820156483749,
130.954148995372));
#73724=CARTESIAN_POINT('Ctrl Pts',(-2.90655644569702,-4.91145165372105,
131.102143021204));
#73725=CARTESIAN_POINT('Ctrl Pts',(-2.91490495053236,-4.89807797319362,
131.249349641043));
#73726=CARTESIAN_POINT('Ctrl Pts',(-2.92328621970895,-4.88465180664131,
131.397133984442));
#73727=CARTESIAN_POINT('Ctrl Pts',(-2.93166748888556,-4.86454985974308,
131.544124447829));
#73728=CARTESIAN_POINT('Ctrl Pts',(-2.94004875806212,-4.83790179310411,
131.689735850323));
#73729=CARTESIAN_POINT('Ctrl Pts',(-2.94844645255313,-4.81120150252806,
131.835632616886));
#73730=CARTESIAN_POINT('Ctrl Pts',(-2.9568441470441,-4.77792952909772,131.980144644462));
#73731=CARTESIAN_POINT('Ctrl Pts',(-2.96524184153512,-4.73826562546462,
132.122701212799));
#73732=CARTESIAN_POINT('Ctrl Pts',(-2.97366657939604,-4.69847399086689,
132.265716860711));
#73733=CARTESIAN_POINT('Ctrl Pts',(-2.982091317257,-4.65224932172985,132.406764172971));
#73734=CARTESIAN_POINT('Ctrl Pts',(-2.99051605511792,-4.5998208444264,132.545288893424));
#73735=CARTESIAN_POINT('Ctrl Pts',(-2.99782144236563,-4.55435826317674,
132.665408562783));
#73736=CARTESIAN_POINT('Ctrl Pts',(-3.00512682961338,-4.50423170428375,
132.783631688841));
#73737=CARTESIAN_POINT('Ctrl Pts',(-3.0124322168611,-4.44961828863167,132.899612427725));
#73738=CARTESIAN_POINT('Ctrl Pts',(-3.02020655098013,-4.39149913269009,
133.023038193518));
#73739=CARTESIAN_POINT('Ctrl Pts',(-3.02798088509929,-4.32814855865314,
133.144239416373));
#73740=CARTESIAN_POINT('Ctrl Pts',(-3.03575521921837,-4.25975934281512,
133.262740857439));
#73741=CARTESIAN_POINT('Ctrl Pts',(-3.04351997216547,-4.19145441057349,
133.38109625607));
#73742=CARTESIAN_POINT('Ctrl Pts',(-3.05128472511256,-4.11812338548197,
133.496758157758));
#73743=CARTESIAN_POINT('Ctrl Pts',(-3.05904947805965,-4.04000660404017,
133.609272327729));
#73744=CARTESIAN_POINT('Ctrl Pts',(-3.06680651894463,-3.96196740928718,
133.72167474704));
#73745=CARTESIAN_POINT('Ctrl Pts',(-3.0745635598296,-3.87915213895429,133.830935337182));
#73746=CARTESIAN_POINT('Ctrl Pts',(-3.08232060071458,-3.79184625215337,
133.936625782352));
#73747=CARTESIAN_POINT('Ctrl Pts',(-3.09007179195469,-3.70460620340083,
134.042236525535));
#73748=CARTESIAN_POINT('Ctrl Pts',(-3.09782298319482,-3.61288252660651,
134.144282182351));
#73749=CARTESIAN_POINT('Ctrl Pts',(-3.10557417443493,-3.51700285169162,
134.242364981102));
#73750=CARTESIAN_POINT('Ctrl Pts',(-3.11332207121201,-3.42116392819611,
134.340406092048));
#73751=CARTESIAN_POINT('Ctrl Pts',(-3.1210699679891,-3.32117279255921,134.434487415923));
#73752=CARTESIAN_POINT('Ctrl Pts',(-3.12881786476618,-3.21739591468639,
134.524245910241));
#73753=CARTESIAN_POINT('Ctrl Pts',(-3.13656414085027,-3.11364074469925,
134.613985629017));
#73754=CARTESIAN_POINT('Ctrl Pts',(-3.14431041693429,-3.00610170311664,
134.699404061227));
#73755=CARTESIAN_POINT('Ctrl Pts',(-3.15205669301838,-2.89518022184796,
134.780176828801));
#73756=CARTESIAN_POINT('Ctrl Pts',(-3.15980302628374,-2.78425792178195,
134.860950192622));
#73757=CARTESIAN_POINT('Ctrl Pts',(-3.16754935954914,-2.6699534482558,134.93707759323));
#73758=CARTESIAN_POINT('Ctrl Pts',(-3.1752956928145,-2.55269891201957,135.008276806915));
#73759=CARTESIAN_POINT('Ctrl Pts',(-3.18304376081748,-2.43541811744293,
135.079491965171));
#73760=CARTESIAN_POINT('Ctrl Pts',(-3.19079182882045,-2.31518627966388,
135.145776537518));
#73761=CARTESIAN_POINT('Ctrl Pts',(-3.19853989682343,-2.19246155075561,
135.206893457984));
#73762=CARTESIAN_POINT('Ctrl Pts',(-3.20629619956528,-2.06960638854518,
135.268075334241));
#73763=CARTESIAN_POINT('Ctrl Pts',(-3.2140525023072,-1.94425339312259,135.324078412709));
#73764=CARTESIAN_POINT('Ctrl Pts',(-3.22180880504905,-1.81688272216531,
135.374712927443));
#73765=CARTESIAN_POINT('Ctrl Pts',(-3.22956924756322,-1.68944406964588,
135.425374467342));
#73766=CARTESIAN_POINT('Ctrl Pts',(-3.23732969007735,-1.55998596464474,
135.470661604992));
#73767=CARTESIAN_POINT('Ctrl Pts',(-3.24509013259151,-1.42900434673795,
135.510434314344));
#73768=CARTESIAN_POINT('Ctrl Pts',(-3.25286303285694,-1.29781246551009,
135.55027087038));
#73769=CARTESIAN_POINT('Ctrl Pts',(-3.26063593312233,-1.16509256287556,
135.584575210608));
#73770=CARTESIAN_POINT('Ctrl Pts',(-3.26840883338775,-1.03135228548577,
135.613258155019));
#73771=CARTESIAN_POINT('Ctrl Pts',(-3.27589916914981,-0.902473804049821,
135.640898402154));
#73772=CARTESIAN_POINT('Ctrl Pts',(-3.2833895049119,-0.772648149784768,
135.663318809151));
#73773=CARTESIAN_POINT('Ctrl Pts',(-3.29087984067397,-0.642332684473476,
135.680485286292));
#73774=CARTESIAN_POINT('Ctrl Pts',(-3.29865417479303,-0.507076268687317,
135.698302635631));
#73775=CARTESIAN_POINT('Ctrl Pts',(-3.30642850891206,-0.370863714611736,
135.71051622497));
#73776=CARTESIAN_POINT('Ctrl Pts',(-3.31420284303113,-0.234199054447876,
135.717031364257));
#73777=CARTESIAN_POINT('Ctrl Pts',(-3.32196759597819,-0.0977028212637813,
135.723538474218));
#73778=CARTESIAN_POINT('Ctrl Pts',(-3.32973234892537,0.039244022613044,
135.724361089027));
#73779=CARTESIAN_POINT('Ctrl Pts',(-3.33749710187243,0.176129408853844,
135.719455885599));
#73780=CARTESIAN_POINT('Ctrl Pts',(-3.34525414275741,0.31287883859947,135.714555554087));
#73781=CARTESIAN_POINT('Ctrl Pts',(-3.35301118364226,0.449566543996468,
135.703938739516));
#73782=CARTESIAN_POINT('Ctrl Pts',(-3.36076822452725,0.585677873207814,
135.687614091566));
#73783=CARTESIAN_POINT('Ctrl Pts',(-3.36851941576737,0.721686559807009,
135.671301754161));
#73784=CARTESIAN_POINT('Ctrl Pts',(-3.37627060700752,0.857119348751999,
135.649290197237));
#73785=CARTESIAN_POINT('Ctrl Pts',(-3.38402179824763,0.991464491473524,
135.621640059808));
#73786=CARTESIAN_POINT('Ctrl Pts',(-3.3917696950247,1.12575253392562,135.594001674425));
#73787=CARTESIAN_POINT('Ctrl Pts',(-3.39951759180175,1.25895346745419,135.560729553737));
#73788=CARTESIAN_POINT('Ctrl Pts',(-3.40726548857882,1.39056376819806,135.52193578592));
#73789=CARTESIAN_POINT('Ctrl Pts',(-3.4150117646629,1.5221465389042,135.483150132924));
#73790=CARTESIAN_POINT('Ctrl Pts',(-3.42275804074694,1.65213896386063,135.438845240648));
#73791=CARTESIAN_POINT('Ctrl Pts',(-3.43050431683102,1.78005115085772,135.389183510855));
#73792=CARTESIAN_POINT('Ctrl Pts',(-3.43825065009635,1.90796428207352,135.339521414471));
#73793=CARTESIAN_POINT('Ctrl Pts',(-3.44599698336172,2.03379678022834,135.284502543167));
#73794=CARTESIAN_POINT('Ctrl Pts',(-3.45374331662705,2.15707763610479,135.224337895145));
#73795=CARTESIAN_POINT('Ctrl Pts',(-3.46149138463001,2.28038609987415,135.164159773667));
#73796=CARTESIAN_POINT('Ctrl Pts',(-3.46923945263297,2.40114143301143,135.098833753846));
#73797=CARTESIAN_POINT('Ctrl Pts',(-3.47698752063593,2.51889654281374,135.028617152046));
#73798=CARTESIAN_POINT('Ctrl Pts',(-3.48474382337776,2.63677680414805,134.958325923207));
#73799=CARTESIAN_POINT('Ctrl Pts',(-3.49250012611962,2.75165013609627,134.883133929841));
#73800=CARTESIAN_POINT('Ctrl Pts',(-3.50025642886146,2.86309734623971,134.80334256907));
#73801=CARTESIAN_POINT('Ctrl Pts',(-3.50801687137561,2.97460403911481,134.723508621248));
#73802=CARTESIAN_POINT('Ctrl Pts',(-3.51577731388975,3.08268065856118,134.639070655166));
#73803=CARTESIAN_POINT('Ctrl Pts',(-3.5235377564039,3.18694132924324,134.550370231337));
#73804=CARTESIAN_POINT('Ctrl Pts',(-3.53131065666931,3.29136936840972,134.461527417712));
#73805=CARTESIAN_POINT('Ctrl Pts',(-3.53908355693467,3.39196893063057,134.368408738626));
#73806=CARTESIAN_POINT('Ctrl Pts',(-3.54685645720008,3.48839059082423,134.271393087611));
#73807=CARTESIAN_POINT('Ctrl Pts',(-3.55434679296228,3.58130708080083,134.177904199876));
#73808=CARTESIAN_POINT('Ctrl Pts',(-3.56183712872454,3.67034394148668,134.080796977719));
#73809=CARTESIAN_POINT('Ctrl Pts',(-3.56932746448675,3.7552252770198,133.980437786234));
#73810=CARTESIAN_POINT('Ctrl Pts',(-3.57710179860585,3.8433249141869,133.876273445502));
#73811=CARTESIAN_POINT('Ctrl Pts',(-3.58487613272495,3.92722676545942,133.768275709389));
#73812=CARTESIAN_POINT('Ctrl Pts',(-3.59265046684405,4.00657872369888,133.656817452174));
#73813=CARTESIAN_POINT('Ctrl Pts',(-3.60041521979116,4.0858328877417,133.5454965573));
#73814=CARTESIAN_POINT('Ctrl Pts',(-3.6081799727383,4.16054809110699,133.430723942408));
#73815=CARTESIAN_POINT('Ctrl Pts',(-3.61594472568541,4.23041109941507,133.312907007898));
#73816=CARTESIAN_POINT('Ctrl Pts',(-3.62370176657043,4.3002047187984,133.195207090828));
#73817=CARTESIAN_POINT('Ctrl Pts',(-3.63145880745549,4.36515553556552,133.074469205474));
#73818=CARTESIAN_POINT('Ctrl Pts',(-3.63921584834051,4.42499264505032,132.951131018366));
#73819=CARTESIAN_POINT('Ctrl Pts',(-3.64696703958066,4.48478463090539,132.827885841544));
#73820=CARTESIAN_POINT('Ctrl Pts',(-3.65471823082077,4.53947041522027,132.702044616369));
#73821=CARTESIAN_POINT('Ctrl Pts',(-3.66246942206092,4.58882440271248,132.574070668272));
#73822=CARTESIAN_POINT('Ctrl Pts',(-3.67021731883803,4.63815741344345,132.446151112517));
#73823=CARTESIAN_POINT('Ctrl Pts',(-3.67796521561518,4.68216299417844,132.316101000743));
#73824=CARTESIAN_POINT('Ctrl Pts',(-3.68571311239228,4.72066328093046,132.184404548234));
#73825=CARTESIAN_POINT('Ctrl Pts',(-3.69345938847638,4.75915551425241,132.052735643785));
#73826=CARTESIAN_POINT('Ctrl Pts',(-3.70120566456046,4.79214463453071,131.919421458609));
#73827=CARTESIAN_POINT('Ctrl Pts',(-3.70895194064457,4.8195024762636,131.784961935018));
#73828=CARTESIAN_POINT('Ctrl Pts',(-3.71669827390993,4.84686051994587,131.650501418878));
#73829=CARTESIAN_POINT('Ctrl Pts',(-3.7244446071753,4.86858712418446,131.514895930568));
#73830=CARTESIAN_POINT('Ctrl Pts',(-3.73219094044066,4.88460521575539,131.378655793164));
#73831=CARTESIAN_POINT('Ctrl Pts',(-3.73993900844365,4.90062689446686,131.242385145726));
#73832=CARTESIAN_POINT('Ctrl Pts',(-3.74768707644666,4.91093747103526,131.105479954598));
#73833=CARTESIAN_POINT('Ctrl Pts',(-3.75543514444965,4.91551176848025,130.968455457315));
#73834=CARTESIAN_POINT('Ctrl Pts',(-3.76319144719153,4.92009092754301,130.831285328765));
#73835=CARTESIAN_POINT('Ctrl Pts',(-3.77094774993344,4.91892161583052,130.693996032133));
#73836=CARTESIAN_POINT('Ctrl Pts',(-3.77870405267532,4.91203082353697,130.557103158381));
#73837=CARTESIAN_POINT('Ctrl Pts',(-3.78646449518951,4.90513635342009,130.42013722078));
#73838=CARTESIAN_POINT('Ctrl Pts',(-3.79422493770368,4.8925143538766,130.283568516771));
#73839=CARTESIAN_POINT('Ctrl Pts',(-3.80198538021787,4.87424361439373,130.147906316002));
#73840=CARTESIAN_POINT('Ctrl Pts',(-3.80975828048332,4.85594354509784,130.012026338224));
#73841=CARTESIAN_POINT('Ctrl Pts',(-3.81753118074872,4.83197668378551,129.877056156804));
#73842=CARTESIAN_POINT('Ctrl Pts',(-3.82530408101417,4.80247293152463,129.743494554166));
#73843=CARTESIAN_POINT('Ctrl Pts',(-3.83279441677603,4.77404171497462,129.614788252209));
#73844=CARTESIAN_POINT('Ctrl Pts',(-3.8402847525379,4.74046925680224,129.487390194114));
#73845=CARTESIAN_POINT('Ctrl Pts',(-3.84777508829976,4.70191466188526,129.361730528164));
#73846=CARTESIAN_POINT('Ctrl Pts',(-3.85554942241884,4.66189825778269,129.231306437783));
#73847=CARTESIAN_POINT('Ctrl Pts',(-3.86332375653792,4.61638770376544,129.102342019724));
#73848=CARTESIAN_POINT('Ctrl Pts',(-3.871098090657,4.56550638701657,128.975335059349));
#73849=CARTESIAN_POINT('Ctrl Pts',(-3.87886284360409,4.5146877769432,128.848484623702));
#73850=CARTESIAN_POINT('Ctrl Pts',(-3.88662759655121,4.45851171794416,128.72358720524));
#73851=CARTESIAN_POINT('Ctrl Pts',(-3.8943923494983,4.39715165668143,128.601126546786));
#73852=CARTESIAN_POINT('Ctrl Pts',(-3.90214939038331,4.33585253909658,128.478787517985));
#73853=CARTESIAN_POINT('Ctrl Pts',(-3.90990643126832,4.26937983964819,128.358880780116));
#73854=CARTESIAN_POINT('Ctrl Pts',(-3.91766347215332,4.19795534899483,128.241870822397));
#73855=CARTESIAN_POINT('Ctrl Pts',(-3.92541466339345,4.12658472010546,128.124949102797));
#73856=CARTESIAN_POINT('Ctrl Pts',(-3.9331658546336,4.05026993555358,128.010920147622));
#73857=CARTESIAN_POINT('Ctrl Pts',(-3.94091704587373,3.96927886438715,127.900224195283));
#73858=CARTESIAN_POINT('Ctrl Pts',(-3.94866494265082,3.88832221658647,127.789575291678));
#73859=CARTESIAN_POINT('Ctrl Pts',(-3.95641283942789,3.80269346562427,127.682256888238));
#73860=CARTESIAN_POINT('Ctrl Pts',(-3.96416073620497,3.71270385570266,127.578680357163));
#73861=CARTESIAN_POINT('Ctrl Pts',(-3.97190701228908,3.6227330696675,127.475125492066));
#73862=CARTESIAN_POINT('Ctrl Pts',(-3.97965328837316,3.52840349533988,127.375311237408));
#73863=CARTESIAN_POINT('Ctrl Pts',(-3.98739956445726,3.43006647176078,127.279615653487));
#73864=CARTESIAN_POINT('Ctrl Pts',(-3.99514589772262,3.33172872228011,127.183919363162));
#73865=CARTESIAN_POINT('Ctrl Pts',(-4.002892230988,3.22938374471073,127.092342076907));
#73866=CARTESIAN_POINT('Ctrl Pts',(-4.01063856425336,3.12341922834965,127.005224480695));
#73867=CARTESIAN_POINT('Ctrl Pts',(-4.01838663225634,3.01743098196984,126.918087375102));
#73868=CARTESIAN_POINT('Ctrl Pts',(-4.02613470025925,2.90782188580262,126.835412195125));
#73869=CARTESIAN_POINT('Ctrl Pts',(-4.03388276826223,2.79501181500518,126.757498621342));
#73870=CARTESIAN_POINT('Ctrl Pts',(-4.04163907100409,2.68208184832205,126.679502240086));
#73871=CARTESIAN_POINT('Ctrl Pts',(-4.04939537374599,2.5659444332886,126.60627779684));
#73872=CARTESIAN_POINT('Ctrl Pts',(-4.05715167648785,2.447047940042,126.538081273496));
#73873=CARTESIAN_POINT('Ctrl Pts',(-4.06491211900203,2.32808798815688,126.469848351615));
#73874=CARTESIAN_POINT('Ctrl Pts',(-4.07267256151614,2.206366370585,126.406648876912));
#73875=CARTESIAN_POINT('Ctrl Pts',(-4.08043300403031,2.0823541379467,126.348691834243));
#73876=CARTESIAN_POINT('Ctrl Pts',(-4.08820590429574,1.95814282986346,126.290641753785));
#73877=CARTESIAN_POINT('Ctrl Pts',(-4.09597880456126,1.83163391971795,126.237851073096));
#73878=CARTESIAN_POINT('Ctrl Pts',(-4.10375170482669,1.70331726199213,126.190480106814));
#73879=CARTESIAN_POINT('Ctrl Pts',(-4.11124204058866,1.57966523798585,126.144831194476));
#73880=CARTESIAN_POINT('Ctrl Pts',(-4.11873237635065,1.4543349099125,126.104214892086));
#73881=CARTESIAN_POINT('Ctrl Pts',(-4.12622271211262,1.32777417377965,126.068729845858));
#73882=CARTESIAN_POINT('Ctrl Pts',(-4.13399704623169,1.19641484886808,126.031899373317));
#73883=CARTESIAN_POINT('Ctrl Pts',(-4.14177138035076,1.06331386538916,126.000480273246));
#73884=CARTESIAN_POINT('Ctrl Pts',(-4.14954571446984,0.928956718054041,
125.97463780166));
#73885=CARTESIAN_POINT('Ctrl Pts',(-4.15731046741691,0.79476515389535,125.948827178611));
#73886=CARTESIAN_POINT('Ctrl Pts',(-4.16507522036401,0.659320886399582,
125.928579582568));
#73887=CARTESIAN_POINT('Ctrl Pts',(-4.17283997331108,0.523124654261355,
125.914010562754));
#73888=CARTESIAN_POINT('Ctrl Pts',(-4.18059701419607,0.387063694140919,
125.899456013095));
#73889=CARTESIAN_POINT('Ctrl Pts',(-4.18835405508103,0.250252641898669,
125.890568857042));
#73890=CARTESIAN_POINT('Ctrl Pts',(-4.19611109596602,0.113202168737664,
125.887413563601));
#73891=CARTESIAN_POINT('Ctrl Pts',(-4.20386228720612,-0.0237449535952466,
125.884260649592));
#73892=CARTESIAN_POINT('Ctrl Pts',(-4.21161347844621,-0.160930748194613,
125.886831003597));
#73893=CARTESIAN_POINT('Ctrl Pts',(-4.21936466968631,-0.297840040250985,
125.895137219418));
#73894=CARTESIAN_POINT('Ctrl Pts',(-4.22711256646339,-0.434691142206245,
125.903439904875));
#73895=CARTESIAN_POINT('Ctrl Pts',(-4.23486046324046,-0.571265585928096,
125.917473579735));
#73896=CARTESIAN_POINT('Ctrl Pts',(-4.24260836001753,-0.707049037241934,
125.937198742157));
#73897=CARTESIAN_POINT('Ctrl Pts',(-4.25035463610162,-0.842804085584909,
125.9569197785));
#73898=CARTESIAN_POINT('Ctrl Pts',(-4.2581009121857,-0.977768083967068,
125.982329878192));
#73899=CARTESIAN_POINT('Ctrl Pts',(-4.26584718826979,-1.11143305221947,
126.013337800574));
#73900=CARTESIAN_POINT('Ctrl Pts',(-4.27359352153513,-1.2450990071563,126.04434595185));
#73901=CARTESIAN_POINT('Ctrl Pts',(-4.28133985480043,-1.37746553197736,
126.080951919919));
#73902=CARTESIAN_POINT('Ctrl Pts',(-4.28908618806577,-1.5080364423889,126.123013679886));
#73903=CARTESIAN_POINT('Ctrl Pts',(-4.29683425606873,-1.63863659325052,
126.165084859293));
#73904=CARTESIAN_POINT('Ctrl Pts',(-4.30458232407171,-1.76743995747763,
126.212614141957));
#73905=CARTESIAN_POINT('Ctrl Pts',(-4.31233039207467,-1.89396745253293,
126.265410259692));
#73906=CARTESIAN_POINT('Ctrl Pts',(-4.32008669481651,-2.02062942251567,
126.318262489769));
#73907=CARTESIAN_POINT('Ctrl Pts',(-4.32784299755834,-2.14501033008246,
126.376392586037));
#73908=CARTESIAN_POINT('Ctrl Pts',(-4.33559930030017,-2.26665245540512,
126.439561686469));
#73909=CARTESIAN_POINT('Ctrl Pts',(-4.34335974281432,-2.38835950479265,
126.502764502152));
#73910=CARTESIAN_POINT('Ctrl Pts',(-4.35112018532849,-2.50732452027586,
126.57101148654));
#73911=CARTESIAN_POINT('Ctrl Pts',(-4.35888062784264,-2.62311706260929,
126.644019292825));
#73912=CARTESIAN_POINT('Ctrl Pts',(-4.36665352810805,-2.73909548541125,
126.717144297722));
#73913=CARTESIAN_POINT('Ctrl Pts',(-4.37442642837349,-2.85189093627025,
126.795045174349));
#73914=CARTESIAN_POINT('Ctrl Pts',(-4.3821993286389,-2.96110375962843,126.877396448234));
#73915=CARTESIAN_POINT('Ctrl Pts',(-4.3896896644011,-3.06634642176969,126.956754045885));
#73916=CARTESIAN_POINT('Ctrl Pts',(-4.39718000016326,-3.16826217097445,
127.040243896885));
#73917=CARTESIAN_POINT('Ctrl Pts',(-4.40467033592546,-3.26652591465533,
127.127542494326));
#73918=CARTESIAN_POINT('Ctrl Pts',(-4.41232756809087,-3.36697912832878,
127.216786241141));
#73919=CARTESIAN_POINT('Ctrl Pts',(-4.41998480025625,-3.46395413688269,
127.310311515935));
#73920=CARTESIAN_POINT('Ctrl Pts',(-4.42764203242166,-3.55705555686598,
127.407812542259));
#73921=CARTESIAN_POINT('Ctrl Pts',(-4.43529043724618,-3.65004964851532,
127.505201168336));
#73922=CARTESIAN_POINT('Ctrl Pts',(-4.44293884207073,-3.73917875257566,
127.606556146739));
#73923=CARTESIAN_POINT('Ctrl Pts',(-4.45058724689525,-3.82408041706777,
127.71153148774));
#73924=CARTESIAN_POINT('Ctrl Pts',(-4.4582286082714,-3.90890389525773,127.816410156505));
#73925=CARTESIAN_POINT('Ctrl Pts',(-4.46586996964758,-3.98950742243945,
127.924902247342));
#73926=CARTESIAN_POINT('Ctrl Pts',(-4.47351133102373,-4.06556571548979,
128.036625356466));
#73927=CARTESIAN_POINT('Ctrl Pts',(-4.48153076923438,-4.1453871964407,128.153876265856));
#73928=CARTESIAN_POINT('Ctrl Pts',(-4.48955020744505,-4.22020185263817,
128.274685773025));
#73929=CARTESIAN_POINT('Ctrl Pts',(-4.49756964565572,-4.28968158809207,
128.398572818261));
#73930=CARTESIAN_POINT('Ctrl Pts',(-4.50520257694934,-4.35581266025541,
128.516488971441));
#73931=CARTESIAN_POINT('Ctrl Pts',(-4.51283550824294,-4.41711080757548,
128.637192555279));
#73932=CARTESIAN_POINT('Ctrl Pts',(-4.52046843953656,-4.47333819900914,
128.760240166177));
#73933=CARTESIAN_POINT('Ctrl Pts',(-4.52809978580013,-4.5295539144429,128.883262225403));
#73934=CARTESIAN_POINT('Ctrl Pts',(-4.53573113206374,-4.58070080474959,
129.00862697483));
#73935=CARTESIAN_POINT('Ctrl Pts',(-4.54336247832731,-4.62658815136065,
129.135868741593));
#73936=CARTESIAN_POINT('Ctrl Pts',(-4.55099506589904,-4.67248296196763,
129.263131205391));
#73937=CARTESIAN_POINT('Ctrl Pts',(-4.5586276534707,-4.71311638671098,129.392270915542));
#73938=CARTESIAN_POINT('Ctrl Pts',(-4.56626024104241,-4.74834690030874,
129.522805009397));
#73939=CARTESIAN_POINT('Ctrl Pts',(-4.56742169054548,-4.7537079213421,129.54266835941));
#73940=CARTESIAN_POINT('Ctrl Pts',(-4.56858314004855,-4.7589439293273,129.562563971735));
#73941=CARTESIAN_POINT('Ctrl Pts',(-4.56974458955162,-4.76405452823407,
129.582490119308));
#73942=CARTESIAN_POINT('Origin',(213.235140564004,0.,130.804360617566));
#73943=CARTESIAN_POINT('',(-6.66542383595775,-4.76405452823408,129.582490119308));
#73944=CARTESIAN_POINT('',(-6.31979145723438,-4.76405452823404,129.582490119308));
#73945=CARTESIAN_POINT('',(213.235140564004,-4.76405452823405,129.582490119308));
#73946=CARTESIAN_POINT('',(-4.98514056403867,-4.91824846381416,130.800473370515));
#73947=CARTESIAN_POINT('Ctrl Pts',(-4.98514056403869,-4.91824846381416,
130.800473370515));
#73948=CARTESIAN_POINT('Ctrl Pts',(-4.99278994307129,-4.91835489482087,
130.935132713854));
#73949=CARTESIAN_POINT('Ctrl Pts',(-5.00043932210384,-4.9129268059493,131.069997494585));
#73950=CARTESIAN_POINT('Ctrl Pts',(-5.00808870113644,-4.9019402097927,131.20456711691));
#73951=CARTESIAN_POINT('Ctrl Pts',(-5.01573056659492,-4.89096440517935,
131.339004558724));
#73952=CARTESIAN_POINT('Ctrl Pts',(-5.02337243205339,-4.87444098482965,
131.47314701929));
#73953=CARTESIAN_POINT('Ctrl Pts',(-5.03101429751186,-4.85239799954162,
131.606493222903));
#73954=CARTESIAN_POINT('Ctrl Pts',(-5.03890637724906,-4.82963327036855,
131.744205523294));
#73955=CARTESIAN_POINT('Ctrl Pts',(-5.04679845698631,-4.80098132423921,
131.88106809453));
#73956=CARTESIAN_POINT('Ctrl Pts',(-5.05469053672351,-4.76653130125415,
132.016533219411));
#73957=CARTESIAN_POINT('Ctrl Pts',(-5.06232395247998,-4.73321038243154,
132.147558456504));
#73958=CARTESIAN_POINT('Ctrl Pts',(-5.06995736823651,-4.69446559218237,
132.277275989228));
#73959=CARTESIAN_POINT('Ctrl Pts',(-5.07759078399297,-4.65042955773849,
132.405200394374));
#73960=CARTESIAN_POINT('Ctrl Pts',(-5.08522308473622,-4.60639995563924,
132.5331061136));
#73961=CARTESIAN_POINT('Ctrl Pts',(-5.09285538547939,-4.55708077729923,
132.659218844464));
#73962=CARTESIAN_POINT('Ctrl Pts',(-5.10048768622264,-4.50265421179631,
132.783069315554));
#73963=CARTESIAN_POINT('Ctrl Pts',(-5.10812063862446,-4.44822299926237,
132.906930361204));
#73964=CARTESIAN_POINT('Ctrl Pts',(-5.11575359102633,-4.38868369523615,
133.028528393651));
#73965=CARTESIAN_POINT('Ctrl Pts',(-5.12338654342815,-4.3242659919312,133.147415609137));
#73966=CARTESIAN_POINT('Ctrl Pts',(-5.13102191450769,-4.25982787638538,
133.266340496791));
#73967=CARTESIAN_POINT('Ctrl Pts',(-5.13865728558717,-4.19050848036941,
133.382552505079));
#73968=CARTESIAN_POINT('Ctrl Pts',(-5.1462926566667,-4.11658235665875,133.495630348259));
#73969=CARTESIAN_POINT('Ctrl Pts',(-5.15393623945735,-4.04257672666535,
133.608829804728));
#73970=CARTESIAN_POINT('Ctrl Pts',(-5.16157982224803,-3.96395470252006,
133.718888031474));
#73971=CARTESIAN_POINT('Ctrl Pts',(-5.16922340503868,-3.8810330157953,133.825414372931));
#73972=CARTESIAN_POINT('Ctrl Pts',(-5.17687191233893,-3.79805790534855,
133.932009345815));
#73973=CARTESIAN_POINT('Ctrl Pts',(-5.18452041963917,-3.71077787892187,
134.035067597811));
#73974=CARTESIAN_POINT('Ctrl Pts',(-5.19216892693942,-3.61954756763109,
134.134234259036));
#73975=CARTESIAN_POINT('Ctrl Pts',(-5.19982802808361,-3.52819089447081,
134.233538274662));
#73976=CARTESIAN_POINT('Ctrl Pts',(-5.20748712922783,-3.43287330403267,
134.328939661867));
#73977=CARTESIAN_POINT('Ctrl Pts',(-5.21514623037203,-3.33398372617403,
134.420122719268));
#73978=CARTESIAN_POINT('Ctrl Pts',(-5.21690555731626,-3.31126838457515,
134.441067841512));
#73979=CARTESIAN_POINT('Ctrl Pts',(-5.21866488426048,-3.28836469566599,
134.461790565631));
#73980=CARTESIAN_POINT('Ctrl Pts',(-5.22042421120472,-3.26527758926873,
134.482287387843));
#73981=CARTESIAN_POINT('Ctrl Pts',(-5.22819854532379,-3.16325739366898,
134.572861311456));
#73982=CARTESIAN_POINT('Ctrl Pts',(-5.23597287944286,-3.05730417132377,
134.659330648952));
#73983=CARTESIAN_POINT('Ctrl Pts',(-5.24374721356193,-2.94778223953403,
134.741334446637));
#73984=CARTESIAN_POINT('Ctrl Pts',(-5.25151196650902,-2.83839528373696,
134.82323718197));
#73985=CARTESIAN_POINT('Ctrl Pts',(-5.25927671945615,-2.72544867939069,
134.900685095497));
#73986=CARTESIAN_POINT('Ctrl Pts',(-5.26704147240324,-2.60934219281335,
134.973355266556));
#73987=CARTESIAN_POINT('Ctrl Pts',(-5.27479851328823,-2.49335102483528,
135.045953260576));
#73988=CARTESIAN_POINT('Ctrl Pts',(-5.2825555541732,-2.37420654952286,135.11378274945));
#73989=CARTESIAN_POINT('Ctrl Pts',(-5.2903125950582,-2.25233980640477,135.176562403736));
#73990=CARTESIAN_POINT('Ctrl Pts',(-5.29806378629832,-2.13056496394566,
135.239294715395));
#73991=CARTESIAN_POINT('Ctrl Pts',(-5.30581497753849,-2.00607228597268,
135.296984593977));
#73992=CARTESIAN_POINT('Ctrl Pts',(-5.31356616877861,-1.87931955082755,
135.349395390632));
#73993=CARTESIAN_POINT('Ctrl Pts',(-5.32131406555568,-1.75262068897609,
135.4017839113));
#73994=CARTESIAN_POINT('Ctrl Pts',(-5.32906196233272,-1.62366404102289,
135.44889766361));
#73995=CARTESIAN_POINT('Ctrl Pts',(-5.33680985910979,-1.49292941456408,
135.490547214964));
#73996=CARTESIAN_POINT('Ctrl Pts',(-5.34455613519389,-1.36222213497082,
135.532188054129));
#73997=CARTESIAN_POINT('Ctrl Pts',(-5.35230241127793,-1.22973798891268,
135.568366847213));
#73998=CARTESIAN_POINT('Ctrl Pts',(-5.36004868736202,-1.09597369911091,
135.598943468384));
#73999=CARTESIAN_POINT('Ctrl Pts',(-5.36779502062734,-0.9622084218921,135.629520315265));
#74000=CARTESIAN_POINT('Ctrl Pts',(-5.37554135389274,-0.827163363207984,
135.654494820592));
#74001=CARTESIAN_POINT('Ctrl Pts',(-5.38328768715806,-0.691346849629597,
135.673777686991));
#74002=CARTESIAN_POINT('Ctrl Pts',(-5.39103575516105,-0.555499920883754,
135.693064871654));
#74003=CARTESIAN_POINT('Ctrl Pts',(-5.39878382316402,-0.418881580476551,
135.70665782613));
#74004=CARTESIAN_POINT('Ctrl Pts',(-5.40653189116702,-0.282006313388684,
135.714519016407));
#74005=CARTESIAN_POINT('Ctrl Pts',(-5.41428819390887,-0.144985573638679,
135.722388561651));
#74006=CARTESIAN_POINT('Ctrl Pts',(-5.42204449665068,-0.00770775267616375,
135.724514151243));
#74007=CARTESIAN_POINT('Ctrl Pts',(-5.42980079939252,0.129311059324924,
135.720910394842));
#74008=CARTESIAN_POINT('Ctrl Pts',(-5.43756124190669,0.26640300239172,135.717304715009));
#74009=CARTESIAN_POINT('Ctrl Pts',(-5.44532168442086,0.403235271173919,
135.707963622625));
#74010=CARTESIAN_POINT('Ctrl Pts',(-5.45308212693502,0.539296851950341,
135.69295366342));
#74011=CARTESIAN_POINT('Ctrl Pts',(-5.46085502720044,0.675576850855206,
135.677919608897));
#74012=CARTESIAN_POINT('Ctrl Pts',(-5.46862792746586,0.811083302785558,
135.65719856165));
#74013=CARTESIAN_POINT('Ctrl Pts',(-5.47640082773128,0.945314451684333,
135.630908415935));
#74014=CARTESIAN_POINT('Ctrl Pts',(-5.48389116349339,1.07466596021423,135.605573983237));
#74015=CARTESIAN_POINT('Ctrl Pts',(-5.49138149925551,1.2028329772479,135.575068395221));
#74016=CARTESIAN_POINT('Ctrl Pts',(-5.49887183501761,1.32938166029384,135.539540388575));
#74017=CARTESIAN_POINT('Ctrl Pts',(-5.5066461691367,1.46072847511981,135.502665326759));
#74018=CARTESIAN_POINT('Ctrl Pts',(-5.51442050325583,1.59074788242342,135.460262669096));
#74019=CARTESIAN_POINT('Ctrl Pts',(-5.52219483737491,1.71893927923828,135.412443821762));
#74020=CARTESIAN_POINT('Ctrl Pts',(-5.52995959032199,1.84697269161318,135.364683906883));
#74021=CARTESIAN_POINT('Ctrl Pts',(-5.53772434326902,1.97318221322571,135.311521218864));
#74022=CARTESIAN_POINT('Ctrl Pts',(-5.5454890962161,2.09708007831739,135.253117545925));
#74023=CARTESIAN_POINT('Ctrl Pts',(-5.55324613710109,2.22085488630264,135.194771880337));
#74024=CARTESIAN_POINT('Ctrl Pts',(-5.56100317798608,2.34232225549514,135.131195754474));
#74025=CARTESIAN_POINT('Ctrl Pts',(-5.56876021887106,2.46101250807352,135.062599748663));
#74026=CARTESIAN_POINT('Ctrl Pts',(-5.5765114101112,2.57961325540947,134.994055471633));
#74027=CARTESIAN_POINT('Ctrl Pts',(-5.58426260135137,2.69544071746994,134.920499044366));
#74028=CARTESIAN_POINT('Ctrl Pts',(-5.5920137925915,2.8080483545001,134.842187694261));
#74029=CARTESIAN_POINT('Ctrl Pts',(-5.59976168936857,2.92060813028045,134.763909628569));
#74030=CARTESIAN_POINT('Ctrl Pts',(-5.60750958614558,3.02995048258962,134.680880882344));
#74031=CARTESIAN_POINT('Ctrl Pts',(-5.61525748292266,3.13565668869202,134.593402738361));
#74032=CARTESIAN_POINT('Ctrl Pts',(-5.62300375900676,3.24134078333488,134.50594289292));
#74033=CARTESIAN_POINT('Ctrl Pts',(-5.63075003509086,3.34338994364228,134.414035750073));
#74034=CARTESIAN_POINT('Ctrl Pts',(-5.63849631117495,3.44141778702071,134.31802347528));
#74035=CARTESIAN_POINT('Ctrl Pts',(-5.64624264444027,3.53944635401828,134.222010491746));
#74036=CARTESIAN_POINT('Ctrl Pts',(-5.65398897770562,3.63345326554301,134.121892589366));
#74037=CARTESIAN_POINT('Ctrl Pts',(-5.66173531097095,3.72308863025564,134.018049170267));
#74038=CARTESIAN_POINT('Ctrl Pts',(-5.6694833789739,3.81274406818646,133.914182496155));
#74039=CARTESIAN_POINT('Ctrl Pts',(-5.67723144697684,3.89802575583708,133.806588941059));
#74040=CARTESIAN_POINT('Ctrl Pts',(-5.68497951497977,3.97862402308269,133.695681067715));
#74041=CARTESIAN_POINT('Ctrl Pts',(-5.69273581772162,4.05930795112618,133.584655320163));
#74042=CARTESIAN_POINT('Ctrl Pts',(-5.70049212046346,4.13529828527706,133.470308534572));
#74043=CARTESIAN_POINT('Ctrl Pts',(-5.7082484232053,4.20632835771104,133.3530828091));
#74044=CARTESIAN_POINT('Ctrl Pts',(-5.71600886571946,4.27739634103336,133.235794516728));
#74045=CARTESIAN_POINT('Ctrl Pts',(-5.72376930823356,4.34349859904788,133.115624565108));
#74046=CARTESIAN_POINT('Ctrl Pts',(-5.73152975074771,4.40441490316382,132.993038854148));
#74047=CARTESIAN_POINT('Ctrl Pts',(-5.73930265101313,4.46542899553902,132.870256357722));
#74048=CARTESIAN_POINT('Ctrl Pts',(-5.74707555127867,4.52124033883662,132.745050709794));
#74049=CARTESIAN_POINT('Ctrl Pts',(-5.75484845154409,4.57167690942875,132.61790777667));
#74050=CARTESIAN_POINT('Ctrl Pts',(-5.76233878730621,4.62027998363842,132.495386809418));
#74051=CARTESIAN_POINT('Ctrl Pts',(-5.7698291230683,4.66389217183814,132.371067252646));
#74052=CARTESIAN_POINT('Ctrl Pts',(-5.77731945883042,4.70240410795104,132.245394506142));
#74053=CARTESIAN_POINT('Ctrl Pts',(-5.78509379294951,4.74237623582665,132.114956839259));
#74054=CARTESIAN_POINT('Ctrl Pts',(-5.79286812706855,4.77698034457764,131.982648157344));
#74055=CARTESIAN_POINT('Ctrl Pts',(-5.80064246118764,4.80603957524248,131.84894984961));
#74056=CARTESIAN_POINT('Ctrl Pts',(-5.80840721413473,4.83506299300263,131.715416313092));
#74057=CARTESIAN_POINT('Ctrl Pts',(-5.81617196708187,4.85855504719743,131.580496936675));
#74058=CARTESIAN_POINT('Ctrl Pts',(-5.82393672002897,4.87638820553139,131.44468954199));
#74059=CARTESIAN_POINT('Ctrl Pts',(-5.831693760914,4.89420365172113,131.309017033125));
#74060=CARTESIAN_POINT('Ctrl Pts',(-5.83945080179904,4.90637133651686,131.172458646325));
#74061=CARTESIAN_POINT('Ctrl Pts',(-5.84720784268407,4.9128145547773,131.035523358656));
#74062=CARTESIAN_POINT('Ctrl Pts',(-5.85495903392422,4.91925291415673,130.898691334953));
#74063=CARTESIAN_POINT('Ctrl Pts',(-5.86271022516431,4.91997538115697,130.761483365063));
#74064=CARTESIAN_POINT('Ctrl Pts',(-5.87046141640445,4.91495700283006,130.624414173223));
#74065=CARTESIAN_POINT('Ctrl Pts',(-5.87820931318154,4.90994075744782,130.487403239446));
#74066=CARTESIAN_POINT('Ctrl Pts',(-5.88595720995869,4.89918853401159,130.350531356287));
#74067=CARTESIAN_POINT('Ctrl Pts',(-5.89370510673578,4.88272748038461,130.214313657743));
#74068=CARTESIAN_POINT('Ctrl Pts',(-5.90145138281988,4.86626987005522,130.078124453004));
#74069=CARTESIAN_POINT('Ctrl Pts',(-5.90919765890394,4.84410585166792,129.942589548589));
#74070=CARTESIAN_POINT('Ctrl Pts',(-5.91694393498804,4.81631444948453,129.808218967906));
#74071=CARTESIAN_POINT('Ctrl Pts',(-5.92469026825341,4.78852284215129,129.67384739533));
#74072=CARTESIAN_POINT('Ctrl Pts',(-5.9324366015188,4.7551038473178,129.540640546498));
#74073=CARTESIAN_POINT('Ctrl Pts',(-5.94018293478416,4.71618754192418,129.40909787102));
#74074=CARTESIAN_POINT('Ctrl Pts',(-5.94793100278713,4.6772625214939,129.277525737472));
#74075=CARTESIAN_POINT('Ctrl Pts',(-5.95567907079004,4.63283785167975,129.147618893701));
#74076=CARTESIAN_POINT('Ctrl Pts',(-5.96342713879301,4.58309324892931,129.019860874187));
#74077=CARTESIAN_POINT('Ctrl Pts',(-5.97118344153487,4.53329577702295,128.89196707193));
#74078=CARTESIAN_POINT('Ctrl Pts',(-5.97893974427676,4.47816721961135,128.766227020963));
#74079=CARTESIAN_POINT('Ctrl Pts',(-5.98669604701863,4.41793538592294,128.643104041333));
#74080=CARTESIAN_POINT('Ctrl Pts',(-5.99445648953279,4.35767140469143,128.519915347262));
#74081=CARTESIAN_POINT('Ctrl Pts',(-6.00221693204695,4.29229890609762,128.399346851316));
#74082=CARTESIAN_POINT('Ctrl Pts',(-6.00997737456112,4.22209082599729,128.281835668328));
#74083=CARTESIAN_POINT('Ctrl Pts',(-6.01775027482656,4.15177004165382,128.164135845956));
#74084=CARTESIAN_POINT('Ctrl Pts',(-6.02552317509197,4.07659837836353,128.049503471157));
#74085=CARTESIAN_POINT('Ctrl Pts',(-6.03329607535741,3.99689162623794,127.938345894888));
#74086=CARTESIAN_POINT('Ctrl Pts',(-6.04078641111939,3.92008241532195,127.831229176506));
#74087=CARTESIAN_POINT('Ctrl Pts',(-6.04827674688136,3.83906230430724,127.727339250305));
#74088=CARTESIAN_POINT('Ctrl Pts',(-6.05576708264334,3.7541469056134,127.627008878527));
#74089=CARTESIAN_POINT('Ctrl Pts',(-6.06354141676242,3.66601191376809,127.522874450208));
#74090=CARTESIAN_POINT('Ctrl Pts',(-6.07131575088151,3.57340123852914,127.422244959083));
#74091=CARTESIAN_POINT('Ctrl Pts',(-6.07909008500059,3.47662428968547,127.325529404232));
#74092=CARTESIAN_POINT('Ctrl Pts',(-6.08685483794767,3.37996660978204,127.228933042658));
#74093=CARTESIAN_POINT('Ctrl Pts',(-6.09461959089471,3.27915314640472,127.136241293592));
#74094=CARTESIAN_POINT('Ctrl Pts',(-6.10238434384181,3.17453379667028,127.047830538318));
#74095=CARTESIAN_POINT('Ctrl Pts',(-6.11014138472682,3.07001835634872,126.959507593851));
#74096=CARTESIAN_POINT('Ctrl Pts',(-6.11789842561193,2.96170484884454,126.875457432337));
#74097=CARTESIAN_POINT('Ctrl Pts',(-6.12565546649694,2.84998002997416,126.796019702518));
#74098=CARTESIAN_POINT('Ctrl Pts',(-6.13340665773708,2.73833946365863,126.716641877309));
#74099=CARTESIAN_POINT('Ctrl Pts',(-6.14115784897715,2.62329302371982,126.641869786144));
#74100=CARTESIAN_POINT('Ctrl Pts',(-6.14890904021729,2.5052602745568,126.572002643667));
#74101=CARTESIAN_POINT('Ctrl Pts',(-6.15665693699436,2.38727769246112,126.50216519659));
#74102=CARTESIAN_POINT('Ctrl Pts',(-6.16440483377139,2.26631166134219,126.437228750557));
#74103=CARTESIAN_POINT('Ctrl Pts',(-6.17215273054848,2.14281025210197,126.377448907809));
#74104=CARTESIAN_POINT('Ctrl Pts',(-6.17989900663257,2.01933467669435,126.317681569715));
#74105=CARTESIAN_POINT('Ctrl Pts',(-6.18764528271668,1.89332512973804,126.263068859642));
#74106=CARTESIAN_POINT('Ctrl Pts',(-6.19539155880076,1.76525342291417,126.213819972349));
#74107=CARTESIAN_POINT('Ctrl Pts',(-6.20313789206611,1.63718077069388,126.164570721512));
#74108=CARTESIAN_POINT('Ctrl Pts',(-6.21088422533151,1.50704629314551,126.120685512788));
#74109=CARTESIAN_POINT('Ctrl Pts',(-6.21863055859686,1.37534050113522,126.082324873479));
#74110=CARTESIAN_POINT('Ctrl Pts',(-6.22637862659983,1.243605214526,126.04395564357));
#74111=CARTESIAN_POINT('Ctrl Pts',(-6.23412669460284,1.11029828854022,126.011113554247));
#74112=CARTESIAN_POINT('Ctrl Pts',(-6.24187476260582,0.975923675562169,
125.983908767171));
#74113=CARTESIAN_POINT('Ctrl Pts',(-6.24963106534768,0.84140624764618,125.956675066524));
#74114=CARTESIAN_POINT('Ctrl Pts',(-6.25738736808949,0.705819249753642,
125.935090714277));
#74115=CARTESIAN_POINT('Ctrl Pts',(-6.26514367083135,0.569675622613875,
125.919214483877));
#74116=CARTESIAN_POINT('Ctrl Pts',(-6.27290411334552,0.433459331521099,
125.903329779855));
#74117=CARTESIAN_POINT('Ctrl Pts',(-6.28066455585962,0.296686208902539,
125.893159297259));
#74118=CARTESIAN_POINT('Ctrl Pts',(-6.28842499837378,0.159871540342711,
125.888709678668));
#74119=CARTESIAN_POINT('Ctrl Pts',(-6.29619789863921,0.0228372447312607,
125.884252917154));
#74120=CARTESIAN_POINT('Ctrl Pts',(-6.30397079890471,-0.114238338922688,
125.885535367822));
#74121=CARTESIAN_POINT('Ctrl Pts',(-6.31174369917014,-0.250841802453506,
125.89251153065));
#74122=CARTESIAN_POINT('Ctrl Pts',(-6.31923403493218,-0.382479386001982,
125.899234092386));
#74123=CARTESIAN_POINT('Ctrl Pts',(-6.32672437069419,-0.513678272261304,
125.911243563628));
#74124=CARTESIAN_POINT('Ctrl Pts',(-6.33421470645624,-0.643987902710506,
125.928454276827));
#74125=CARTESIAN_POINT('Ctrl Pts',(-6.34198904057531,-0.779238262404569,
125.946317539448));
#74126=CARTESIAN_POINT('Ctrl Pts',(-6.34976337469434,-0.913959035371852,
125.969840825432));
#74127=CARTESIAN_POINT('Ctrl Pts',(-6.35753770881342,-1.04763887555349,
125.998984893553));
#74128=CARTESIAN_POINT('Ctrl Pts',(-6.36530246176052,-1.18115396727941,
126.028093044216));
#74129=CARTESIAN_POINT('Ctrl Pts',(-6.3730672147077,-1.31363030039658,126.062808111649));
#74130=CARTESIAN_POINT('Ctrl Pts',(-6.38083196765479,-1.44456208673287,
126.103039160776));
#74131=CARTESIAN_POINT('Ctrl Pts',(-6.3885890085398,-1.5753638297735,126.143230251858));
#74132=CARTESIAN_POINT('Ctrl Pts',(-6.39634604942478,-1.70462370759048,
126.188926307981));
#74133=CARTESIAN_POINT('Ctrl Pts',(-6.4041030903098,-1.83184691311086,126.239985528967));
#74134=CARTESIAN_POINT('Ctrl Pts',(-6.41185428154995,-1.95897417862231,
126.291006245796));
#74135=CARTESIAN_POINT('Ctrl Pts',(-6.41960547279004,-2.08406746752751,
126.347381932317));
#74136=CARTESIAN_POINT('Ctrl Pts',(-6.42735666403019,-2.20664825726625,
126.40892132994));
#74137=CARTESIAN_POINT('Ctrl Pts',(-6.43510456080726,-2.32917694689906,
126.470434571678));
#74138=CARTESIAN_POINT('Ctrl Pts',(-6.44285245758438,-2.44919491262162,
126.537106984353));
#74139=CARTESIAN_POINT('Ctrl Pts',(-6.45060035436146,-2.56624491576267,
126.608699752479));
#74140=CARTESIAN_POINT('Ctrl Pts',(-6.45834663044554,-2.68327043456621,
126.680277544942));
#74141=CARTESIAN_POINT('Ctrl Pts',(-6.46609290652965,-2.79732889234739,
126.756773441787));
#74142=CARTESIAN_POINT('Ctrl Pts',(-6.47383918261374,-2.90798926189143,
126.837903569365));
#74143=CARTESIAN_POINT('Ctrl Pts',(-6.48158551587913,-3.01865044830578,
126.919034295827));
#74144=CARTESIAN_POINT('Ctrl Pts',(-6.48933184914446,-3.12591318112526,
127.004799090118));
#74145=CARTESIAN_POINT('Ctrl Pts',(-6.49707818240984,-3.22937727108092,
127.094872040481));
#74146=CARTESIAN_POINT('Ctrl Pts',(-6.50482625041282,-3.33286453110187,
127.184965162056));
#74147=CARTESIAN_POINT('Ctrl Pts',(-6.51257431841579,-3.43255116068381,
127.279368102845));
#74148=CARTESIAN_POINT('Ctrl Pts',(-6.52032238641877,-3.5280720791275,127.377716418502));
#74149=CARTESIAN_POINT('Ctrl Pts',(-6.52807868916061,-3.62369451833976,
127.476169259919));
#74150=CARTESIAN_POINT('Ctrl Pts',(-6.53583499190238,-3.71514212944284,
127.578575571652));
#74151=CARTESIAN_POINT('Ctrl Pts',(-6.54359129464422,-3.80208820767823,
127.684535570623));
#74152=CARTESIAN_POINT('Ctrl Pts',(-6.55135173715836,-3.88908069165347,
127.790552123635));
#74153=CARTESIAN_POINT('Ctrl Pts',(-6.55911217967256,-3.97156662034854,
127.900125831039));
#74154=CARTESIAN_POINT('Ctrl Pts',(-6.56687262218671,-4.04926188072924,
128.012826758955));
#74155=CARTESIAN_POINT('Ctrl Pts',(-6.57464552245213,-4.12708186443946,
128.125708604405));
#74156=CARTESIAN_POINT('Ctrl Pts',(-6.58241842271761,-4.20009560359387,
128.241727371027));
#74157=CARTESIAN_POINT('Ctrl Pts',(-6.59019132298303,-4.26806386899554,
128.360426520117));
#74158=CARTESIAN_POINT('Ctrl Pts',(-6.59768165874506,-4.33356131674822,
128.474810656152));
#74159=CARTESIAN_POINT('Ctrl Pts',(-6.60517199450702,-4.39437361120099,
128.591683407461));
#74160=CARTESIAN_POINT('Ctrl Pts',(-6.61266233026905,-4.45032928900128,
128.710619400998));
#74161=CARTESIAN_POINT('Ctrl Pts',(-6.62145591455051,-4.5160207325354,128.850249147445));
#74162=CARTESIAN_POINT('Ctrl Pts',(-6.63024949883198,-4.57520851447709,
128.993126368615));
#74163=CARTESIAN_POINT('Ctrl Pts',(-6.63904308311345,-4.62758848881774,
129.138645203499));
#74164=CARTESIAN_POINT('Ctrl Pts',(-6.64783666739492,-4.6799684631584,129.284164038383));
#74165=CARTESIAN_POINT('Ctrl Pts',(-6.65663025167633,-4.72554041934122,
129.432324193268));
#74166=CARTESIAN_POINT('Ctrl Pts',(-6.66542383595777,-4.76405452823408,
129.582490119308));
#74167=CARTESIAN_POINT('Ctrl Pts',(-4.91509110695614,-4.76405452823401,
129.582490119308));
#74168=CARTESIAN_POINT('Ctrl Pts',(-4.92286673107686,-4.79806456359889,
129.715094731021));
#74169=CARTESIAN_POINT('Ctrl Pts',(-4.93064235519757,-4.82649058400499,
129.848951090438));
#74170=CARTESIAN_POINT('Ctrl Pts',(-4.93841797931836,-4.84927328742245,
129.98354903968));
#74171=CARTESIAN_POINT('Ctrl Pts',(-4.93960418200949,-4.85274888033759,
130.004082497462));
#74172=CARTESIAN_POINT('Ctrl Pts',(-4.94079038470059,-4.856093236529,130.024633209604));
#74173=CARTESIAN_POINT('Ctrl Pts',(-4.94197658739171,-4.85930625197158,
130.045199361936));
#74174=CARTESIAN_POINT('Ctrl Pts',(-4.95490804744516,-4.89433313326069,
130.269402509782));
#74175=CARTESIAN_POINT('Ctrl Pts',(-4.96783950749871,-4.91384944124733,
130.496089496467));
#74176=CARTESIAN_POINT('Ctrl Pts',(-4.98077096755208,-4.91758650221471,
130.723576610884));
#74177=CARTESIAN_POINT('Ctrl Pts',(-4.98222749970424,-4.91800742525288,
130.749199571863));
#74178=CARTESIAN_POINT('Ctrl Pts',(-4.98368403185642,-4.91822819808973,
130.774832639892));
#74179=CARTESIAN_POINT('Ctrl Pts',(-4.98514056400859,-4.91824846381374,
130.800473369986));
#74180=CARTESIAN_POINT('',(-4.63985943596118,-4.91824845974782,130.808253006061));
#74181=CARTESIAN_POINT('Ctrl Pts',(-4.56974458955162,-4.76405452823407,
129.582490119308));
#74182=CARTESIAN_POINT('Ctrl Pts',(-4.57738283870254,-4.79766427851359,
129.713534025549));
#74183=CARTESIAN_POINT('Ctrl Pts',(-4.58502108785347,-4.82584587317406,
129.845899218852));
#74184=CARTESIAN_POINT('Ctrl Pts',(-4.59265933700439,-4.84851632270241,
129.979089431235));
#74185=CARTESIAN_POINT('Ctrl Pts',(-4.60052602016385,-4.87186476813776,
130.11626290909));
#74186=CARTESIAN_POINT('Ctrl Pts',(-4.60839270332329,-4.88936719706201,
130.254311066717));
#74187=CARTESIAN_POINT('Ctrl Pts',(-4.61625938648274,-4.90099051151931,
130.392687120122));
#74188=CARTESIAN_POINT('Ctrl Pts',(-4.6241260696422,-4.91261382597663,130.531063173527));
#74189=CARTESIAN_POINT('Ctrl Pts',(-4.6319927528017,-4.9183580602836,130.669766658435));
#74190=CARTESIAN_POINT('Ctrl Pts',(-4.63985943596117,-4.91824845974782,
130.808253006061));
#74191=CARTESIAN_POINT('Ctrl Pts',(-4.63985943599116,-4.9182484597474,130.808253006589));
#74192=CARTESIAN_POINT('Ctrl Pts',(-4.65277286871676,-4.91806854664951,
131.03558314017));
#74193=CARTESIAN_POINT('Ctrl Pts',(-4.66568630144235,-4.90212487107249,
131.262306380489));
#74194=CARTESIAN_POINT('Ctrl Pts',(-4.67859973416799,-4.87068170378865,
131.486740865579));
#74195=CARTESIAN_POINT('Ctrl Pts',(-4.68010580935812,-4.86701453215803,
131.512916338591));
#74196=CARTESIAN_POINT('Ctrl Pts',(-4.68161188454825,-4.86313657009037,
131.539060722098));
#74197=CARTESIAN_POINT('Ctrl Pts',(-4.68311795973838,-4.85904826618473,
131.565171375499));
#74198=CARTESIAN_POINT('Ctrl Pts',(-4.69089229385748,-4.83794451203547,
131.699954117383));
#74199=CARTESIAN_POINT('Ctrl Pts',(-4.69866662797662,-4.81119507309146,
131.834071600094));
#74200=CARTESIAN_POINT('Ctrl Pts',(-4.70644096209571,-4.77885145017247,
131.967013566508));
#74201=CARTESIAN_POINT('Ctrl Pts',(-4.71420571504281,-4.74654768787809,
132.099791693831));
#74202=CARTESIAN_POINT('Ctrl Pts',(-4.72197046798986,-4.70866355080931,
132.231396811139));
#74203=CARTESIAN_POINT('Ctrl Pts',(-4.72973522093696,-4.66530208537696,
132.361325458106));
#74204=CARTESIAN_POINT('Ctrl Pts',(-4.73749226182196,-4.62198368716343,
132.491125058109));
#74205=CARTESIAN_POINT('Ctrl Pts',(-4.74524930270701,-4.57319890971626,
132.619251132925));
#74206=CARTESIAN_POINT('Ctrl Pts',(-4.75300634359201,-4.51910138638564,
132.745212420787));
#74207=CARTESIAN_POINT('Ctrl Pts',(-4.76075753483213,-4.46504465841819,
132.871078720262));
#74208=CARTESIAN_POINT('Ctrl Pts',(-4.76850872607221,-4.40568331268907,
132.994783124359));
#74209=CARTESIAN_POINT('Ctrl Pts',(-4.77625991731233,-4.34122003593043,
133.115851837998));
#74210=CARTESIAN_POINT('Ctrl Pts',(-4.78400781408942,-4.27678415778394,
133.236869094205));
#74211=CARTESIAN_POINT('Ctrl Pts',(-4.79175571086649,-4.20725084486524,
133.355252543651));
#74212=CARTESIAN_POINT('Ctrl Pts',(-4.79950360764357,-4.13286981635417,
133.470550810251));
#74213=CARTESIAN_POINT('Ctrl Pts',(-4.80724988372768,-4.05850434675079,
133.585824958939));
#74214=CARTESIAN_POINT('Ctrl Pts',(-4.81499615981182,-3.97929339033991,
133.698014880101));
#74215=CARTESIAN_POINT('Ctrl Pts',(-4.82274243589592,-3.89553108248959,
133.806696482831));
#74216=CARTESIAN_POINT('Ctrl Pts',(-4.83048876916126,-3.81176815632505,
133.915378887824));
#74217=CARTESIAN_POINT('Ctrl Pts',(-4.83823510242661,-3.72345405034454,
134.020552613043));
#74218=CARTESIAN_POINT('Ctrl Pts',(-4.84598143569195,-3.63092418588913,
134.121825405446));
#74219=CARTESIAN_POINT('Ctrl Pts',(-4.85372950369494,-3.53837360001199,
134.223120877189));
#74220=CARTESIAN_POINT('Ctrl Pts',(-4.86147757169793,-3.44160564069429,
134.320513389204));
#74221=CARTESIAN_POINT('Ctrl Pts',(-4.86922563970091,-3.34099340825978,
134.413646711583));
#74222=CARTESIAN_POINT('Ctrl Pts',(-4.87698194244276,-3.24027424394748,
134.506879017166));
#74223=CARTESIAN_POINT('Ctrl Pts',(-4.88473824518457,-3.13570293218376,
134.5958428245));
#74224=CARTESIAN_POINT('Ctrl Pts',(-4.89249454792642,-3.02768698093375,
134.680221116602));
#74225=CARTESIAN_POINT('Ctrl Pts',(-4.90025499044059,-2.91961337831811,
134.764644443938));
#74226=CARTESIAN_POINT('Ctrl Pts',(-4.90801543295482,-2.80809179058428,
134.844477151874));
#74227=CARTESIAN_POINT('Ctrl Pts',(-4.915775875469,-2.69355884573146,134.91944552642));
#74228=CARTESIAN_POINT('Ctrl Pts',(-4.92354877573443,-2.5788420424278,134.994534246857));
#74229=CARTESIAN_POINT('Ctrl Pts',(-4.93132167599983,-2.46110455792531,
135.064742829358));
#74230=CARTESIAN_POINT('Ctrl Pts',(-4.93909457626526,-2.34080854029682,
135.12984306929));
#74231=CARTESIAN_POINT('Ctrl Pts',(-4.94658491202727,-2.22488558591684,
135.192576751523));
#74232=CARTESIAN_POINT('Ctrl Pts',(-4.95407524778924,-2.10658716368409,
135.250566909759));
#74233=CARTESIAN_POINT('Ctrl Pts',(-4.96156558355125,-1.98634263879519,
135.303652337804));
#74234=CARTESIAN_POINT('Ctrl Pts',(-4.96933991767032,-1.8615390061974,135.358750515989));
#74235=CARTESIAN_POINT('Ctrl Pts',(-4.97711425178939,-1.73424344444807,
135.408739230828));
#74236=CARTESIAN_POINT('Ctrl Pts',(-4.98488858590846,-1.60491308476677,
135.453386004983));
#74237=CARTESIAN_POINT('Ctrl Pts',(-4.99265333885555,-1.47574211319519,
135.497977755978));
#74238=CARTESIAN_POINT('Ctrl Pts',(-5.00041809180266,-1.34454169929636,
135.537240539066));
#74239=CARTESIAN_POINT('Ctrl Pts',(-5.00818284474974,-1.21179111760383,
135.570988917507));
#74240=CARTESIAN_POINT('Ctrl Pts',(-5.01593988563473,-1.07917238566049,
135.604703776582));
#74241=CARTESIAN_POINT('Ctrl Pts',(-5.02369692651973,-0.945006926353916,
135.632915034751));
#74242=CARTESIAN_POINT('Ctrl Pts',(-5.03145396740473,-0.809791094700726,
135.655486409116));
#74243=CARTESIAN_POINT('Ctrl Pts',(-5.03920515864486,-0.674677230358012,
135.678040762233));
#74244=CARTESIAN_POINT('Ctrl Pts',(-5.04695634988493,-0.538514954352634,
135.694963632932));
#74245=CARTESIAN_POINT('Ctrl Pts',(-5.05470754112505,-0.401812441032595,
135.70616944949));
#74246=CARTESIAN_POINT('Ctrl Pts',(-5.06245543790213,-0.265168029927377,
135.717370503277));
#74247=CARTESIAN_POINT('Ctrl Pts',(-5.07020333467922,-0.127984227037229,
135.722859303935));
#74248=CARTESIAN_POINT('Ctrl Pts',(-5.0779512314563,0.00922423283774606,
135.722601967483));
#74249=CARTESIAN_POINT('Ctrl Pts',(-5.08569750754041,0.146403991660974,
135.722344684859));
#74250=CARTESIAN_POINT('Ctrl Pts',(-5.09344378362461,0.283608006493235,
135.716343656639));
#74251=CARTESIAN_POINT('Ctrl Pts',(-5.10119005970873,0.420320490294498,
135.704617115744));
#74252=CARTESIAN_POINT('Ctrl Pts',(-5.10893639297407,0.557033983275887,
135.692890488287));
#74253=CARTESIAN_POINT('Ctrl Pts',(-5.11668272623931,0.693255548451275,
135.675438297232));
#74254=CARTESIAN_POINT('Ctrl Pts',(-5.12442905950465,0.828473868800271,
135.652330719703));
#74255=CARTESIAN_POINT('Ctrl Pts',(-5.13217712750761,0.963722470354572,
135.629217967393));
#74256=CARTESIAN_POINT('Ctrl Pts',(-5.13992519551062,1.09796699471104,135.600447374296));
#74257=CARTESIAN_POINT('Ctrl Pts',(-5.14767326351358,1.23070606572261,135.566140289316));
#74258=CARTESIAN_POINT('Ctrl Pts',(-5.15542956625543,1.36358621339864,135.531796742359));
#74259=CARTESIAN_POINT('Ctrl Pts',(-5.16318586899724,1.49495733239947,135.491905047084));
#74260=CARTESIAN_POINT('Ctrl Pts',(-5.17094217173909,1.62433243934895,135.446636696062));
#74261=CARTESIAN_POINT('Ctrl Pts',(-5.17870261425326,1.75377659768859,135.401344183958));
#74262=CARTESIAN_POINT('Ctrl Pts',(-5.18646305676743,1.8812222580913,135.350669442404));
#74263=CARTESIAN_POINT('Ctrl Pts',(-5.19422349928161,2.00620312912733,135.294831869804));
#74264=CARTESIAN_POINT('Ctrl Pts',(-5.20199639954704,2.13138463055282,135.238904661776));
#74265=CARTESIAN_POINT('Ctrl Pts',(-5.20976929981252,2.25409308569327,135.177798235347));
#74266=CARTESIAN_POINT('Ctrl Pts',(-5.21754220007796,2.3738866972044,135.111778058601));
#74267=CARTESIAN_POINT('Ctrl Pts',(-5.22503253584005,2.48932550919602,135.048157881574));
#74268=CARTESIAN_POINT('Ctrl Pts',(-5.23252287160211,2.60205745850447,134.979975165579));
#74269=CARTESIAN_POINT('Ctrl Pts',(-5.2400132073642,2.71171483541556,134.907504011829));
#74270=CARTESIAN_POINT('Ctrl Pts',(-5.24778754148327,2.82552990510076,134.832285092259));
#74271=CARTESIAN_POINT('Ctrl Pts',(-5.25556187560229,2.93639318714155,134.752207852375));
#74272=CARTESIAN_POINT('Ctrl Pts',(-5.26333620972136,3.04386200117725,134.667531229937));
#74273=CARTESIAN_POINT('Ctrl Pts',(-5.27110096266844,3.15119836950441,134.582958963869));
#74274=CARTESIAN_POINT('Ctrl Pts',(-5.27886571561556,3.25514828935673,134.493798833173));
#74275=CARTESIAN_POINT('Ctrl Pts',(-5.28663046856263,3.35529668796039,134.400353832001));
#74276=CARTESIAN_POINT('Ctrl Pts',(-5.29438750944762,3.45534561776272,134.307001641721));
#74277=CARTESIAN_POINT('Ctrl Pts',(-5.30214455033258,3.5516002561729,134.209373315182));
#74278=CARTESIAN_POINT('Ctrl Pts',(-5.30990159121757,3.64367765251988,134.107812785682));
#74279=CARTESIAN_POINT('Ctrl Pts',(-5.31765278245768,3.73568561258603,134.006328843767));
#74280=CARTESIAN_POINT('Ctrl Pts',(-5.32540397369786,3.8235223391156,133.900918889625));
#74281=CARTESIAN_POINT('Ctrl Pts',(-5.33315516493798,3.90684115754488,133.791964211119));
#74282=CARTESIAN_POINT('Ctrl Pts',(-5.34090306171504,3.99012456325373,133.683055841259));
#74283=CARTESIAN_POINT('Ctrl Pts',(-5.34865095849204,4.06889364306066,133.570606053467));
#74284=CARTESIAN_POINT('Ctrl Pts',(-5.35639885526911,4.14284166268039,133.455029593591));
#74285=CARTESIAN_POINT('Ctrl Pts',(-5.36414513135319,4.21677421396855,133.339477309818));
#74286=CARTESIAN_POINT('Ctrl Pts',(-5.37189140743731,4.28588750037997,133.220799983984));
#74287=CARTESIAN_POINT('Ctrl Pts',(-5.37963768352139,4.34991806629484,133.099441417673));
#74288=CARTESIAN_POINT('Ctrl Pts',(-5.38738401678673,4.4139491048688,132.978081955521));
#74289=CARTESIAN_POINT('Ctrl Pts',(-5.39513035005209,4.47289716563652,132.854041559185));
#74290=CARTESIAN_POINT('Ctrl Pts',(-5.40287668331743,4.52654491126077,132.727788346606));
#74291=CARTESIAN_POINT('Ctrl Pts',(-5.41062475132039,4.58020467092568,132.601506860495));
#74292=CARTESIAN_POINT('Ctrl Pts',(-5.41837281932329,4.62856160064728,132.473011931821));
#74293=CARTESIAN_POINT('Ctrl Pts',(-5.42612088732625,4.67144678864078,132.342790974585));
#74294=CARTESIAN_POINT('Ctrl Pts',(-5.43387719006808,4.71437755552243,132.212431616966));
#74295=CARTESIAN_POINT('Ctrl Pts',(-5.4416334928099,4.75182484123462,132.080342938223));
#74296=CARTESIAN_POINT('Ctrl Pts',(-5.44938979555172,4.78366970092242,131.947027347184));
#74297=CARTESIAN_POINT('Ctrl Pts',(-5.45715023806587,4.8155315571707,131.813640601601));
#74298=CARTESIAN_POINT('Ctrl Pts',(-5.46491068058014,4.84178495439893,131.679026022447));
#74299=CARTESIAN_POINT('Ctrl Pts',(-5.4726711230943,4.86236243679116,131.543694504103));
#74300=CARTESIAN_POINT('Ctrl Pts',(-5.48044402335972,4.8829729519849,131.408145739593));
#74301=CARTESIAN_POINT('Ctrl Pts',(-5.48821692362515,4.89788930213066,131.271878124907));
#74302=CARTESIAN_POINT('Ctrl Pts',(-5.49598982389057,4.90709603078913,131.135406848648));
#74303=CARTESIAN_POINT('Ctrl Pts',(-5.50348015965275,4.9159680716707,131.003896647028));
#74304=CARTESIAN_POINT('Ctrl Pts',(-5.51097049541489,4.91953839390124,130.872197641888));
#74305=CARTESIAN_POINT('Ctrl Pts',(-5.51846083117707,4.91783885051269,130.740767356225));
#74306=CARTESIAN_POINT('Ctrl Pts',(-5.52623516529617,4.91607486842003,130.604353851336));
#74307=CARTESIAN_POINT('Ctrl Pts',(-5.53400949941523,4.90862793052933,130.46779772819));
#74308=CARTESIAN_POINT('Ctrl Pts',(-5.54178383353434,4.89547660896413,130.331611388497));
#74309=CARTESIAN_POINT('Ctrl Pts',(-5.54954858648146,4.88234149522739,130.195592886297));
#74310=CARTESIAN_POINT('Ctrl Pts',(-5.55731333942858,4.86351602292483,130.059943646211));
#74311=CARTESIAN_POINT('Ctrl Pts',(-5.5650780923757,4.8390307526441,129.925176656461));
#74312=CARTESIAN_POINT('Ctrl Pts',(-5.57283513326071,4.81456980147902,129.790543519184));
#74313=CARTESIAN_POINT('Ctrl Pts',(-5.58059217414579,4.78446030859433,129.656791270617));
#74314=CARTESIAN_POINT('Ctrl Pts',(-5.5883492150308,4.74878464062306,129.524428002354));
#74315=CARTESIAN_POINT('Ctrl Pts',(-5.59610040627095,4.71313587595048,129.392164550261));
#74316=CARTESIAN_POINT('Ctrl Pts',(-5.60385159751101,4.67192939238608,129.261288369571));
#74317=CARTESIAN_POINT('Ctrl Pts',(-5.61160278875116,4.62529859213847,129.132297222816));
#74318=CARTESIAN_POINT('Ctrl Pts',(-5.61935068552825,4.57868761122494,129.00336090074));
#74319=CARTESIAN_POINT('Ctrl Pts',(-5.6270985823054,4.5266570316894,128.876308386002));
#74320=CARTESIAN_POINT('Ctrl Pts',(-5.63484647908248,4.46938999358476,128.751621923103));
#74321=CARTESIAN_POINT('Ctrl Pts',(-5.6425927551666,4.41213493450987,128.626961541925));
#74322=CARTESIAN_POINT('Ctrl Pts',(-5.65033903125069,4.34964575865998,128.504666583208));
#74323=CARTESIAN_POINT('Ctrl Pts',(-5.6580853073348,4.28215344467957,128.385198585225));
#74324=CARTESIAN_POINT('Ctrl Pts',(-5.66583164060016,4.21466063248632,128.265729705357));
#74325=CARTESIAN_POINT('Ctrl Pts',(-5.67357797386559,4.14216480077322,128.149088168262));
#74326=CARTESIAN_POINT('Ctrl Pts',(-5.68132430713095,4.06494231428161,128.03570985518));
#74327=CARTESIAN_POINT('Ctrl Pts',(-5.68907237513394,3.98770253434956,127.92230615181));
#74328=CARTESIAN_POINT('Ctrl Pts',(-5.69682044313692,3.90573421338897,127.812167449685));
#74329=CARTESIAN_POINT('Ctrl Pts',(-5.70456851113991,3.81935612565573,127.705699318244));
#74330=CARTESIAN_POINT('Ctrl Pts',(-5.71232481388179,3.73288623426282,127.599118031206));
#74331=CARTESIAN_POINT('Ctrl Pts',(-5.72008111662366,3.64199746051794,127.496215411868));
#74332=CARTESIAN_POINT('Ctrl Pts',(-5.72783741936553,3.54704820259828,127.397363096149));
#74333=CARTESIAN_POINT('Ctrl Pts',(-5.7355978618797,3.45204826740094,127.298458019972));
#74334=CARTESIAN_POINT('Ctrl Pts',(-5.74335830439388,3.35298381195137,127.203607825172));
#74335=CARTESIAN_POINT('Ctrl Pts',(-5.75111874690805,3.25024820464688,127.113145415131));
#74336=CARTESIAN_POINT('Ctrl Pts',(-5.75889164717349,3.14734767702497,127.022537786797));
#74337=CARTESIAN_POINT('Ctrl Pts',(-5.76666454743898,3.04076452509579,126.936332264708));
#74338=CARTESIAN_POINT('Ctrl Pts',(-5.77443744770443,2.93092383703761,126.854820324825));
#74339=CARTESIAN_POINT('Ctrl Pts',(-5.78192778346631,2.82507613466472,126.776271549275));
#74340=CARTESIAN_POINT('Ctrl Pts',(-5.78941811922814,2.71620387811018,126.702081206863));
#74341=CARTESIAN_POINT('Ctrl Pts',(-5.79690845499002,2.6047092117718,126.632469801088));
#74342=CARTESIAN_POINT('Ctrl Pts',(-5.8046827891091,2.48898719126885,126.560219057704));
#74343=CARTESIAN_POINT('Ctrl Pts',(-5.81245712322821,2.37007340556484,126.492672457331));
#74344=CARTESIAN_POINT('Ctrl Pts',(-5.82023145734729,2.24838737043921,126.430124993488));
#74345=CARTESIAN_POINT('Ctrl Pts',(-5.82799621029438,2.12685130247647,126.367654613805));
#74346=CARTESIAN_POINT('Ctrl Pts',(-5.83576096324147,2.00255012738952,126.310171289135));
#74347=CARTESIAN_POINT('Ctrl Pts',(-5.84352571618857,1.87593195544035,126.257926590655));
#74348=CARTESIAN_POINT('Ctrl Pts',(-5.85128275707357,1.74943954244457,126.205733782345));
#74349=CARTESIAN_POINT('Ctrl Pts',(-5.85903979795855,1.62063507129545,126.158769394023));
#74350=CARTESIAN_POINT('Ctrl Pts',(-5.86679683884356,1.4899905350182,126.117238764226));
#74351=CARTESIAN_POINT('Ctrl Pts',(-5.87454803008368,1.3594445188022,126.075739453));
#74352=CARTESIAN_POINT('Ctrl Pts',(-5.88229922132385,1.2270615704911,126.03966586216));
#74353=CARTESIAN_POINT('Ctrl Pts',(-5.89005041256397,1.0933325789532,126.009174809456));
#74354=CARTESIAN_POINT('Ctrl Pts',(-5.89779830934105,0.959660425803852,
125.978696716263));
#74355=CARTESIAN_POINT('Ctrl Pts',(-5.90554620611812,0.824643747683947,
125.953796528763));
#74356=CARTESIAN_POINT('Ctrl Pts',(-5.91329410289521,0.688787262222854,
125.934580830974));
#74357=CARTESIAN_POINT('Ctrl Pts',(-5.92104037897931,0.552959195009791,
125.915369152695));
#74358=CARTESIAN_POINT('Ctrl Pts',(-5.92878665506345,0.416292056738909,
125.901839653716));
#74359=CARTESIAN_POINT('Ctrl Pts',(-5.93653293114755,0.27929900222865,125.894047477872));
#74360=CARTESIAN_POINT('Ctrl Pts',(-5.94427926441291,0.142304936466783,
125.886255244507));
#74361=CARTESIAN_POINT('Ctrl Pts',(-5.95202559767823,0.00498533999914305,
125.884200440988));
#74362=CARTESIAN_POINT('Ctrl Pts',(-5.95977193094359,-0.132143686050491,
125.887886158288));
#74363=CARTESIAN_POINT('Ctrl Pts',(-5.96751999894657,-0.269303421194724,
125.891572700978));
#74364=CARTESIAN_POINT('Ctrl Pts',(-5.97526806694954,-0.40627211024955,
125.901002312079));
#74365=CARTESIAN_POINT('Ctrl Pts',(-5.98301613495252,-0.542536230886556,
125.916126017971));
#74366=CARTESIAN_POINT('Ctrl Pts',(-5.99077243769438,-0.678945174652538,
125.931265797518));
#74367=CARTESIAN_POINT('Ctrl Pts',(-5.9985287404362,-0.814647664945897,
125.952111717685));
#74368=CARTESIAN_POINT('Ctrl Pts',(-6.00628504317805,-0.949137310973439,
125.978563126227));
#74369=CARTESIAN_POINT('Ctrl Pts',(-6.01404548569223,-1.08369873817465,
126.005028652682));
#74370=CARTESIAN_POINT('Ctrl Pts',(-6.02180592820645,-1.21704565131129,
126.037105537568));
#74371=CARTESIAN_POINT('Ctrl Pts',(-6.02956637072063,-1.3486853441128,126.074642771322));
#74372=CARTESIAN_POINT('Ctrl Pts',(-6.03733927098606,-1.48053635663544,
126.112240263176));
#74373=CARTESIAN_POINT('Ctrl Pts',(-6.04511217125155,-1.61067430089243,
126.155315497109));
#74374=CARTESIAN_POINT('Ctrl Pts',(-6.05288507151698,-1.73862417935703,
126.203668384276));
#74375=CARTESIAN_POINT('Ctrl Pts',(-6.06037540727895,-1.8619227574521,126.2502635222));
#74376=CARTESIAN_POINT('Ctrl Pts',(-6.06786574304089,-1.98318930772456,
126.301759142789));
#74377=CARTESIAN_POINT('Ctrl Pts',(-6.07535607880286,-2.10202094546646,
126.357936098099));
#74378=CARTESIAN_POINT('Ctrl Pts',(-6.0831310787037,-2.22536868327438,126.416248013057));
#74379=CARTESIAN_POINT('Ctrl Pts',(-6.09090607860455,-2.34648353675557,
126.479788850858));
#74380=CARTESIAN_POINT('Ctrl Pts',(-6.09868107850539,-2.46489043968613,
126.548365060373));
#74381=CARTESIAN_POINT('Ctrl Pts',(-6.1064463476794,-2.58314915158864,126.616855443989));
#74382=CARTESIAN_POINT('Ctrl Pts',(-6.11421161685342,-2.69870632152533,
126.690368465248));
#74383=CARTESIAN_POINT('Ctrl Pts',(-6.12197688602743,-2.81110799311244,
126.768663042975));
#74384=CARTESIAN_POINT('Ctrl Pts',(-6.12973429422568,-2.92339587768278,
126.846878361148));
#74385=CARTESIAN_POINT('Ctrl Pts',(-6.13749170242393,-3.03253430262064,
126.929865380053));
#74386=CARTESIAN_POINT('Ctrl Pts',(-6.14524911062219,-3.13809533106104,
127.017337940624));
#74387=CARTESIAN_POINT('Ctrl Pts',(-6.15300004877302,-3.24356831658262,
127.104737544918));
#74388=CARTESIAN_POINT('Ctrl Pts',(-6.16075098692381,-3.34546954738773,
127.196614992465));
#74389=CARTESIAN_POINT('Ctrl Pts',(-6.16850192507465,-3.44340179562564,
127.292642072981));
#74390=CARTESIAN_POINT('Ctrl Pts',(-6.17624935165313,-3.54128967553431,
127.388625648307));
#74391=CARTESIAN_POINT('Ctrl Pts',(-6.18399677823165,-3.63521187206467,
127.488754842978));
#74392=CARTESIAN_POINT('Ctrl Pts',(-6.19174420481013,-3.72480597182815,
127.592662696725));
#74393=CARTESIAN_POINT('Ctrl Pts',(-6.19948979918119,-3.81437888326883,
127.696545977056));
#74394=CARTESIAN_POINT('Ctrl Pts',(-6.20723539355222,-3.89962548024037,
127.80420584196));
#74395=CARTESIAN_POINT('Ctrl Pts',(-6.21498098792327,-3.98022208394728,
127.915240470366));
#74396=CARTESIAN_POINT('Ctrl Pts',(-6.22272642785827,-4.06081708067338,
128.026272884901));
#74397=CARTESIAN_POINT('Ctrl Pts',(-6.2304718677933,-4.13676204036941,128.140679611881));
#74398=CARTESIAN_POINT('Ctrl Pts',(-6.23821730772829,-4.20777549292051,
128.25802826226));
#74399=CARTESIAN_POINT('Ctrl Pts',(-6.2459673356742,-4.2788310102863,128.375446424106));
#74400=CARTESIAN_POINT('Ctrl Pts',(-6.25371736362005,-4.34494898254698,
128.495809655774));
#74401=CARTESIAN_POINT('Ctrl Pts',(-6.26146739156596,-4.40589286324137,
128.618659096283));
#74402=CARTESIAN_POINT('Ctrl Pts',(-6.2692199660448,-4.46685676910216,128.741548903117));
#74403=CARTESIAN_POINT('Ctrl Pts',(-6.2769725405237,-4.52264303362214,128.86692619097));
#74404=CARTESIAN_POINT('Ctrl Pts',(-6.28472511500254,-4.57306289007633,
128.994311207769));
#74405=CARTESIAN_POINT('Ctrl Pts',(-6.29248568990171,-4.62353477828403,
129.121827682018));
#74406=CARTESIAN_POINT('Ctrl Pts',(-6.30024626480089,-4.66862906700021,
129.251355655095));
#74407=CARTESIAN_POINT('Ctrl Pts',(-6.30800683970006,-4.7082064619071,129.38239895333));
#74408=CARTESIAN_POINT('Ctrl Pts',(-6.31193504554483,-4.72823953368516,
129.448729741543));
#74409=CARTESIAN_POINT('Ctrl Pts',(-6.31586325138957,-4.74685991247322,
129.515448573421));
#74410=CARTESIAN_POINT('Ctrl Pts',(-6.31979145723434,-4.76405452823404,
129.582490119308));
#74411=CARTESIAN_POINT('Origin',(213.235140564004,0.,130.804360617566));
#74412=CARTESIAN_POINT('',(-8.41516596570781,-4.76405452823401,129.582490119308));
#74413=CARTESIAN_POINT('',(-8.07013341471002,-4.76405452823399,129.582490119308));
#74414=CARTESIAN_POINT('',(213.235140564004,-4.76405452823405,129.582490119308));
#74415=CARTESIAN_POINT('',(-6.73514056397329,-4.91824973727353,130.802753039002));
#74416=CARTESIAN_POINT('Ctrl Pts',(-6.73514056400862,-4.91824973727374,
130.802753039629));
#74417=CARTESIAN_POINT('Ctrl Pts',(-6.74308048856736,-4.91829580373628,
130.943689514402));
#74418=CARTESIAN_POINT('Ctrl Pts',(-6.7510204131261,-4.91227954301344,131.084575973784));
#74419=CARTESIAN_POINT('Ctrl Pts',(-6.75896033768484,-4.90024012990961,
131.224871891759));
#74420=CARTESIAN_POINT('Ctrl Pts',(-6.76690503553524,-4.88819347900021,
131.365252152266));
#74421=CARTESIAN_POINT('Ctrl Pts',(-6.77484973338559,-4.870116489556,131.505040802365));
#74422=CARTESIAN_POINT('Ctrl Pts',(-6.782794431236,-4.84610004999722,131.643704032336));
#74423=CARTESIAN_POINT('Ctrl Pts',(-6.79074523461097,-4.82206515373128,
131.782473825422));
#74424=CARTESIAN_POINT('Ctrl Pts',(-6.79869603798591,-4.79208177130108,
131.920116117517));
#74425=CARTESIAN_POINT('Ctrl Pts',(-6.80664684136087,-4.75629154989002,
132.056108896952));
#74426=CARTESIAN_POINT('Ctrl Pts',(-6.81461084874838,-4.72044189114791,
132.192327521534));
#74427=CARTESIAN_POINT('Ctrl Pts',(-6.82257485613593,-4.6787662186234,132.326890809158));
#74428=CARTESIAN_POINT('Ctrl Pts',(-6.83053886352343,-4.63145590659714,
132.459292413063));
#74429=CARTESIAN_POINT('Ctrl Pts',(-6.83851017959729,-4.58410217720377,
132.591815523861));
#74430=CARTESIAN_POINT('Ctrl Pts',(-6.84648149567114,-4.53110363311608,
132.722172659786));
#74431=CARTESIAN_POINT('Ctrl Pts',(-6.85445281174501,-4.47269898320194,
132.849879345949));
#74432=CARTESIAN_POINT('Ctrl Pts',(-6.86243872369883,-4.41418739144137,
132.977819869466));
#74433=CARTESIAN_POINT('Ctrl Pts',(-6.8704246356527,-4.35025007827006,133.103099922917));
#74434=CARTESIAN_POINT('Ctrl Pts',(-6.87841054760653,-4.28117123850171,
133.225260427373));
#74435=CARTESIAN_POINT('Ctrl Pts',(-6.88264368309837,-4.24455424471959,
133.290014705921));
#74436=CARTESIAN_POINT('Ctrl Pts',(-6.88687681859019,-4.20649331057569,
133.353892954325));
#74437=CARTESIAN_POINT('Ctrl Pts',(-6.89110995408203,-4.16703546937306,
133.41683041825));
#74438=CARTESIAN_POINT('Ctrl Pts',(-6.89888428820112,-4.09456945884271,
133.532417758676));
#74439=CARTESIAN_POINT('Ctrl Pts',(-6.90665862232015,-4.01717569231029,
133.645170747791));
#74440=CARTESIAN_POINT('Ctrl Pts',(-6.91443295643924,-3.93510240986074,
133.754640618923));
#74441=CARTESIAN_POINT('Ctrl Pts',(-6.92219770938633,-3.85313027539681,
133.863975578223));
#74442=CARTESIAN_POINT('Ctrl Pts',(-6.92996246233349,-3.76649033207073,
133.970035160362));
#74443=CARTESIAN_POINT('Ctrl Pts',(-6.93772721528057,-3.67547552617673,
134.072397141073));
#74444=CARTESIAN_POINT('Ctrl Pts',(-6.94548425616558,-3.58455111747089,
134.174657454422));
#74445=CARTESIAN_POINT('Ctrl Pts',(-6.95324129705059,-3.48926075139595,
134.273227184521));
#74446=CARTESIAN_POINT('Ctrl Pts',(-6.96099833793559,-3.38993907244603,
134.367715237528));
#74447=CARTESIAN_POINT('Ctrl Pts',(-6.96874952917572,-3.29069229274695,
134.462132036359));
#74448=CARTESIAN_POINT('Ctrl Pts',(-6.97650072041582,-3.18742053331162,
134.552473016334));
#74449=CARTESIAN_POINT('Ctrl Pts',(-6.98425191165595,-3.08049665296856,
134.638382452865));
#74450=CARTESIAN_POINT('Ctrl Pts',(-6.99199980843303,-2.97361821812679,
134.724255375594));
#74451=CARTESIAN_POINT('Ctrl Pts',(-6.99974770521013,-2.86309105382065,
134.805700256701));
#74452=CARTESIAN_POINT('Ctrl Pts',(-7.00749560198722,-2.74932242568258,
134.882400497476));
#74453=CARTESIAN_POINT('Ctrl Pts',(-7.01524187807132,-2.63557759548895,
134.959084694214));
#74454=CARTESIAN_POINT('Ctrl Pts',(-7.02298815415538,-2.51859297409999,
135.031026006298));
#74455=CARTESIAN_POINT('Ctrl Pts',(-7.03073443023948,-2.398805913088,135.097950403961));
#74456=CARTESIAN_POINT('Ctrl Pts',(-7.03848076350481,-2.27901796783529,
135.164875295645));
#74457=CARTESIAN_POINT('Ctrl Pts',(-7.04622709677017,-2.15642788298945,
135.226783008322));
#74458=CARTESIAN_POINT('Ctrl Pts',(-7.05397343003551,-2.03149842618743,
135.283445033705));
#74459=CARTESIAN_POINT('Ctrl Pts',(-7.06172149803849,-1.90654099229959,
135.340119748155));
#74460=CARTESIAN_POINT('Ctrl Pts',(-7.06946956604152,-1.7792434999694,135.391546276265));
#74461=CARTESIAN_POINT('Ctrl Pts',(-7.0772176340445,-1.65008916941539,135.437544058299));
#74462=CARTESIAN_POINT('Ctrl Pts',(-7.08497393678636,-1.52079757210191,
135.483590727323));
#74463=CARTESIAN_POINT('Ctrl Pts',(-7.09273023952818,-1.38964556323794,
135.524196993223));
#74464=CARTESIAN_POINT('Ctrl Pts',(-7.10048654227003,-1.25713255262244,
135.559231888971));
#74465=CARTESIAN_POINT('Ctrl Pts',(-7.10824698478421,-1.12454881582311,
135.594285483899));
#74466=CARTESIAN_POINT('Ctrl Pts',(-7.11600742729848,-0.990603011485884,
135.623761699524));
#74467=CARTESIAN_POINT('Ctrl Pts',(-7.12376786981267,-0.855804268115007,
135.647580839399));
#74468=CARTESIAN_POINT('Ctrl Pts',(-7.1315407700781,-0.720789133834584,
135.671438215873));
#74469=CARTESIAN_POINT('Ctrl Pts',(-7.13931367034345,-0.58491871212966,
135.6896203175));
#74470=CARTESIAN_POINT('Ctrl Pts',(-7.14708657060888,-0.448707672328128,
135.702099329185));
#74471=CARTESIAN_POINT('Ctrl Pts',(-7.15457690637087,-0.317448246918841,
135.714124697363));
#74472=CARTESIAN_POINT('Ctrl Pts',(-7.16206724213292,-0.185872845730236,
135.720854404418));
#74473=CARTESIAN_POINT('Ctrl Pts',(-7.16955757789492,-0.0544396243900029,
135.722309314919));
#74474=CARTESIAN_POINT('Ctrl Pts',(-7.177331912014,0.0819769274861851,135.723819388794));
#74475=CARTESIAN_POINT('Ctrl Pts',(-7.18510624613308,0.218672431817819,
135.719651565866));
#74476=CARTESIAN_POINT('Ctrl Pts',(-7.19288058025217,0.355135148664519,
135.709772128202));
#74477=CARTESIAN_POINT('Ctrl Pts',(-7.20064533319926,0.491429687408728,
135.699904866062));
#74478=CARTESIAN_POINT('Ctrl Pts',(-7.20841008614631,0.627491623291929,
135.684340022767));
#74479=CARTESIAN_POINT('Ctrl Pts',(-7.21617483909341,0.762807382452408,
135.6630958398));
#74480=CARTESIAN_POINT('Ctrl Pts',(-7.22393187997841,0.897988744093086,
135.641872756855));
#74481=CARTESIAN_POINT('Ctrl Pts',(-7.23168892086349,1.03242502012493,135.61498161993));
#74482=CARTESIAN_POINT('Ctrl Pts',(-7.23944596174849,1.16560628869944,135.582492579143));
#74483=CARTESIAN_POINT('Ctrl Pts',(-7.24719715298861,1.29868712424333,135.550028038594));
#74484=CARTESIAN_POINT('Ctrl Pts',(-7.25494834422869,1.4305144578134,135.51197408895));
#74485=CARTESIAN_POINT('Ctrl Pts',(-7.26269953546881,1.56058746893522,135.468452149076));
#74486=CARTESIAN_POINT('Ctrl Pts',(-7.27044743224589,1.69060519555751,135.424948707187));
#74487=CARTESIAN_POINT('Ctrl Pts',(-7.27819532902292,1.81886971275518,135.375982021204));
#74488=CARTESIAN_POINT('Ctrl Pts',(-7.2859432258,1.94489452004455,135.321723605903));
#74489=CARTESIAN_POINT('Ctrl Pts',(-7.29368950188409,2.07089296566084,135.267476540293));
#74490=CARTESIAN_POINT('Ctrl Pts',(-7.30143577796818,2.194652274369,135.207940101588));
#74491=CARTESIAN_POINT('Ctrl Pts',(-7.30918205405226,2.31570549795869,135.143334126269));
#74492=CARTESIAN_POINT('Ctrl Pts',(-7.3169283873176,2.43675961513594,135.078727674043));
#74493=CARTESIAN_POINT('Ctrl Pts',(-7.32467472058298,2.55510726241774,135.009051794613));
#74494=CARTESIAN_POINT('Ctrl Pts',(-7.33242105384832,2.67030605209712,134.934572313186));
#74495=CARTESIAN_POINT('Ctrl Pts',(-7.34016912185128,2.78553063974656,134.860076152595));
#74496=CARTESIAN_POINT('Ctrl Pts',(-7.34791718985421,2.8976046383382,134.780774461651));
#74497=CARTESIAN_POINT('Ctrl Pts',(-7.35566525785717,3.00611494552234,134.696976190264));
#74498=CARTESIAN_POINT('Ctrl Pts',(-7.36342156059901,3.1147405787524,134.613088857075));
#74499=CARTESIAN_POINT('Ctrl Pts',(-7.37117786334091,3.2197946446404,134.524695636183));
#74500=CARTESIAN_POINT('Ctrl Pts',(-7.37893416608276,3.32089701372113,134.432145904316));
#74501=CARTESIAN_POINT('Ctrl Pts',(-7.38669460859692,3.42205334418051,134.33954677587));
#74502=CARTESIAN_POINT('Ctrl Pts',(-7.39445505111111,3.51925349824792,134.242786991681));
#74503=CARTESIAN_POINT('Ctrl Pts',(-7.40221549362528,3.61215522865279,134.142251818102));
#74504=CARTESIAN_POINT('Ctrl Pts',(-7.40998839389071,3.70520609316273,134.041555256538));
#74505=CARTESIAN_POINT('Ctrl Pts',(-7.41776129415614,3.79394449195623,133.937071492759));
#74506=CARTESIAN_POINT('Ctrl Pts',(-7.42553419442157,3.87806883206359,133.82921849791));
#74507=CARTESIAN_POINT('Ctrl Pts',(-7.43302453018363,3.95913504051197,133.725286231088));
#74508=CARTESIAN_POINT('Ctrl Pts',(-7.44051486594569,4.03591665190354,133.618225690704));
#74509=CARTESIAN_POINT('Ctrl Pts',(-7.44800520170776,4.10818357588296,133.508433613871));
#74510=CARTESIAN_POINT('Ctrl Pts',(-7.45577953582679,4.1831905222498,133.394478737075));
#74511=CARTESIAN_POINT('Ctrl Pts',(-7.46355386994592,4.25357127384649,133.277220127766));
#74512=CARTESIAN_POINT('Ctrl Pts',(-7.471328204065,4.31902085488254,133.157070101882));
#74513=CARTESIAN_POINT('Ctrl Pts',(-7.47909295701211,4.38438977515945,133.037068150167));
#74514=CARTESIAN_POINT('Ctrl Pts',(-7.48685770995917,4.44483943151815,132.91418221204));
#74515=CARTESIAN_POINT('Ctrl Pts',(-7.49462246290628,4.50010757181889,132.788854231705));
#74516=CARTESIAN_POINT('Ctrl Pts',(-7.50237950379129,4.55532081902354,132.663650728887));
#74517=CARTESIAN_POINT('Ctrl Pts',(-7.51013654467625,4.60536263491645,132.536010366068));
#74518=CARTESIAN_POINT('Ctrl Pts',(-7.51789358556127,4.6500164135625,132.406400072792));
#74519=CARTESIAN_POINT('Ctrl Pts',(-7.52564477680136,4.6946365184464,132.276887519647));
#74520=CARTESIAN_POINT('Ctrl Pts',(-7.5333959680415,4.73387654672345,132.145408361069));
#74521=CARTESIAN_POINT('Ctrl Pts',(-7.54114715928159,4.76756794582284,132.012449581369));
#74522=CARTESIAN_POINT('Ctrl Pts',(-7.54889505605869,4.80124502517909,131.879547312696));
#74523=CARTESIAN_POINT('Ctrl Pts',(-7.55664295283579,4.82937807003393,131.745167051886));
#74524=CARTESIAN_POINT('Ctrl Pts',(-7.56439084961289,4.85184841523002,131.6098108135));
#74525=CARTESIAN_POINT('Ctrl Pts',(-7.572137125697,4.87431406011427,131.474482888721));
#74526=CARTESIAN_POINT('Ctrl Pts',(-7.57988340178113,4.89111929741757,131.33817977788));
#74527=CARTESIAN_POINT('Ctrl Pts',(-7.58762967786524,4.90219668488516,131.201413164719));
#74528=CARTESIAN_POINT('Ctrl Pts',(-7.5953760111306,4.91327415412351,131.064645541979));
#74529=CARTESIAN_POINT('Ctrl Pts',(-7.60312234439584,4.91862365759332,130.927414799781));
#74530=CARTESIAN_POINT('Ctrl Pts',(-7.61086867766119,4.91822972020849,130.79023681645));
#74531=CARTESIAN_POINT('Ctrl Pts',(-7.61861674566418,4.91783569460411,130.653028113061));
#74532=CARTESIAN_POINT('Ctrl Pts',(-7.62636481366724,4.91169566987101,130.515872582938));
#74533=CARTESIAN_POINT('Ctrl Pts',(-7.63411288167023,4.89984628240653,130.37928477576));
#74534=CARTESIAN_POINT('Ctrl Pts',(-7.6418691844121,4.88798430127207,130.242551801435));
#74535=CARTESIAN_POINT('Ctrl Pts',(-7.64962548715395,4.87040086980958,130.106388145501));
#74536=CARTESIAN_POINT('Ctrl Pts',(-7.65738178989582,4.84718445929574,129.971302468298));
#74537=CARTESIAN_POINT('Ctrl Pts',(-7.66514223241,4.82395565748459,129.836144691802));
#74538=CARTESIAN_POINT('Ctrl Pts',(-7.6729026749242,4.79508796818583,129.70206642249));
#74539=CARTESIAN_POINT('Ctrl Pts',(-7.68066311743837,4.76072053388455,129.569563848559));
#74540=CARTESIAN_POINT('Ctrl Pts',(-7.68843601770381,4.72629792992673,129.436848569733));
#74541=CARTESIAN_POINT('Ctrl Pts',(-7.69620891796926,4.68635805242925,129.305714415146));
#74542=CARTESIAN_POINT('Ctrl Pts',(-7.70398181823469,4.64108953398614,129.176641047117));
#74543=CARTESIAN_POINT('Ctrl Pts',(-7.71147215399671,4.59746664021308,129.052259821131));
#74544=CARTESIAN_POINT('Ctrl Pts',(-7.71896248975872,4.54889591192813,128.929792439723));
#74545=CARTESIAN_POINT('Ctrl Pts',(-7.72645282552074,4.49558676584433,128.809646930526));
#74546=CARTESIAN_POINT('Ctrl Pts',(-7.73422715963982,4.44025638728373,128.684946067829));
#74547=CARTESIAN_POINT('Ctrl Pts',(-7.74200149375893,4.37964591371896,128.562351605692));
#74548=CARTESIAN_POINT('Ctrl Pts',(-7.74977582787801,4.313937391362,128.44234299572));
#74549=CARTESIAN_POINT('Ctrl Pts',(-7.7575405808251,4.24830984888631,128.322482285635));
#74550=CARTESIAN_POINT('Ctrl Pts',(-7.76530533377214,4.17759694465666,128.205201426504));
#74551=CARTESIAN_POINT('Ctrl Pts',(-7.77307008671923,4.10202874515994,128.090959940117));
#74552=CARTESIAN_POINT('Ctrl Pts',(-7.78082712760422,4.02653560106439,127.976831919985));
#74553=CARTESIAN_POINT('Ctrl Pts',(-7.78858416848928,3.94619697269126,127.865737589123));
#74554=CARTESIAN_POINT('Ctrl Pts',(-7.79634120937428,3.86128862029136,127.758111571065));
#74555=CARTESIAN_POINT('Ctrl Pts',(-7.80409240061442,3.77644429794027,127.650566714624));
#74556=CARTESIAN_POINT('Ctrl Pts',(-7.81184359185451,3.68703735191954,127.54648527073));
#74557=CARTESIAN_POINT('Ctrl Pts',(-7.81959478309466,3.59338638914034,127.44627227435));
#74558=CARTESIAN_POINT('Ctrl Pts',(-7.82734267987174,3.49977523051866,127.346101871168));
#74559=CARTESIAN_POINT('Ctrl Pts',(-7.83509057664887,3.40192390918442,127.249796930374));
#74560=CARTESIAN_POINT('Ctrl Pts',(-7.84283847342596,3.30019064278917,127.15772863946));
#74561=CARTESIAN_POINT('Ctrl Pts',(-7.85058474951007,3.19847865679999,127.065679607247));
#74562=CARTESIAN_POINT('Ctrl Pts',(-7.85833102559416,3.09288663059767,126.977865724356));
#74563=CARTESIAN_POINT('Ctrl Pts',(-7.86607730167827,2.98380860402038,126.894620309429));
#74564=CARTESIAN_POINT('Ctrl Pts',(-7.87382363494363,2.87472977225402,126.811374280002));
#74565=CARTESIAN_POINT('Ctrl Pts',(-7.88156996820896,2.76216519956066,126.732697023022));
#74566=CARTESIAN_POINT('Ctrl Pts',(-7.88931630147431,2.64654054432316,126.658880402952));
#74567=CARTESIAN_POINT('Ctrl Pts',(-7.89706436947725,2.53088999574628,126.585047252162));
#74568=CARTESIAN_POINT('Ctrl Pts',(-7.90481243748026,2.41217833046148,126.516077114624));
#74569=CARTESIAN_POINT('Ctrl Pts',(-7.91256050548321,2.29085825655375,126.452217293768));
#74570=CARTESIAN_POINT('Ctrl Pts',(-7.92031680822508,2.16940924222726,126.388289601934));
#74571=CARTESIAN_POINT('Ctrl Pts',(-7.92807311096692,2.04534662792984,126.329483258798));
#74572=CARTESIAN_POINT('Ctrl Pts',(-7.93582941370877,1.91914618489891,126.275998774307));
#74573=CARTESIAN_POINT('Ctrl Pts',(-7.94358985622296,1.79287838489137,126.222485743536));
#74574=CARTESIAN_POINT('Ctrl Pts',(-7.95135029873719,1.66447084842675,126.174300368511));
#74575=CARTESIAN_POINT('Ctrl Pts',(-7.95911074125138,1.53441624259946,126.13159378656));
#74576=CARTESIAN_POINT('Ctrl Pts',(-7.96688364151683,1.40415286157337,126.088818648213));
#74577=CARTESIAN_POINT('Ctrl Pts',(-7.97465654178226,1.27223750403358,126.051539984623));
#74578=CARTESIAN_POINT('Ctrl Pts',(-7.9824294420477,1.13917568399913,126.019858363048));
#74579=CARTESIAN_POINT('Ctrl Pts',(-7.98991977780966,1.01095099628687,125.989328448219));
#74580=CARTESIAN_POINT('Ctrl Pts',(-7.99741011357162,0.881662054808889,
125.963995766437));
#74581=CARTESIAN_POINT('Ctrl Pts',(-8.00490044933358,0.751765339617887,
125.943904678392));
#74582=CARTESIAN_POINT('Ctrl Pts',(-8.01267478345266,0.616943550987837,
125.923051830638));
#74583=CARTESIAN_POINT('Ctrl Pts',(-8.02044911757182,0.481039916481458,
125.907779837304));
#74584=CARTESIAN_POINT('Ctrl Pts',(-8.02822345169091,0.344556212737817,
125.898194693062));
#74585=CARTESIAN_POINT('Ctrl Pts',(-8.035988204638,0.208240712961141,125.888621361654));
#74586=CARTESIAN_POINT('Ctrl Pts',(-8.043752957585,0.0713469526128881,125.884720961571));
#74587=CARTESIAN_POINT('Ctrl Pts',(-8.0515177105321,-0.0656141030554698,
125.886548314114));
#74588=CARTESIAN_POINT('Ctrl Pts',(-8.05927475141713,-0.202439127072898,
125.888373851706));
#74589=CARTESIAN_POINT('Ctrl Pts',(-8.0670317923022,-0.339330924997757,
125.895915815604));
#74590=CARTESIAN_POINT('Ctrl Pts',(-8.07478883318723,-0.475774780592142,
125.909177125535));
#74591=CARTESIAN_POINT('Ctrl Pts',(-8.08254002442735,-0.612115742813087,
125.922428435009));
#74592=CARTESIAN_POINT('Ctrl Pts',(-8.09029121566743,-0.748009047510532,
125.941390468078));
#74593=CARTESIAN_POINT('Ctrl Pts',(-8.09804240690755,-0.882941712477918,
125.966014103015));
#74594=CARTESIAN_POINT('Ctrl Pts',(-8.10579030368463,-1.01781702746325,
125.990627272251));
#74595=CARTESIAN_POINT('Ctrl Pts',(-8.11353820046181,-1.15173213098292,
126.020897187305));
#74596=CARTESIAN_POINT('Ctrl Pts',(-8.12128609723888,-1.28418110709839,
126.056723105427));
#74597=CARTESIAN_POINT('Ctrl Pts',(-8.12903237332298,-1.4166023777435,126.092541529539));
#74598=CARTESIAN_POINT('Ctrl Pts',(-8.13677864940701,-1.54755775382855,
126.133913543029));
#74599=CARTESIAN_POINT('Ctrl Pts',(-8.14452492549111,-1.67655381678383,
126.180687795888));
#74600=CARTESIAN_POINT('Ctrl Pts',(-8.15227125875646,-1.80555083195856,
126.227462394023));
#74601=CARTESIAN_POINT('Ctrl Pts',(-8.16001759202186,-1.93258813759476,
126.279639177828));
#74602=CARTESIAN_POINT('Ctrl Pts',(-8.1677639252872,-2.05719010109988,126.337017788721));
#74603=CARTESIAN_POINT('Ctrl Pts',(-8.1755119932902,-2.18181996835114,126.394409249155));
#74604=CARTESIAN_POINT('Ctrl Pts',(-8.1832600612932,-2.30401305317887,126.45700469122));
#74605=CARTESIAN_POINT('Ctrl Pts',(-8.19100812929619,-2.42331659242449,
126.524556912327));
#74606=CARTESIAN_POINT('Ctrl Pts',(-8.19876443203806,-2.54274692889118,
126.592180928738));
#74607=CARTESIAN_POINT('Ctrl Pts',(-8.20652073477992,-2.65928124427988,
126.664772054892));
#74608=CARTESIAN_POINT('Ctrl Pts',(-8.21427703752178,-2.77249367791692,
126.742038391497));
#74609=CARTESIAN_POINT('Ctrl Pts',(-8.22203748003594,-2.8857665364384,126.819345967473));
#74610=CARTESIAN_POINT('Ctrl Pts',(-8.22979792255011,-2.99571366711432,
126.901333492397));
#74611=CARTESIAN_POINT('Ctrl Pts',(-8.23755836506427,-3.10194161523259,
126.987668164906));
#74612=CARTESIAN_POINT('Ctrl Pts',(-8.2453312653297,-3.20834008988366,127.074141429496));
#74613=CARTESIAN_POINT('Ctrl Pts',(-8.25310416559509,-3.31100715830994,
127.164975527579));
#74614=CARTESIAN_POINT('Ctrl Pts',(-8.26087706586051,-3.40958496775515,
127.259799514953));
#74615=CARTESIAN_POINT('Ctrl Pts',(-8.2683674016225,-3.5045792255241,127.351176411538));
#74616=CARTESIAN_POINT('Ctrl Pts',(-8.27585773738448,-3.59577615909364,
127.446257926368));
#74617=CARTESIAN_POINT('Ctrl Pts',(-8.28334807314647,-3.68289170793955,
127.544683987885));
#74618=CARTESIAN_POINT('Ctrl Pts',(-8.29105212000108,-3.77249280078742,
127.645918300168));
#74619=CARTESIAN_POINT('Ctrl Pts',(-8.29875616685568,-3.85807248466077,
127.751025949734));
#74620=CARTESIAN_POINT('Ctrl Pts',(-8.30646021371027,-3.93927250583388,
127.859650922659));
#74621=CARTESIAN_POINT('Ctrl Pts',(-8.31415498973554,-4.02037481322738,
127.968145179402));
#74622=CARTESIAN_POINT('Ctrl Pts',(-8.32184976576084,-4.09710770232271,
128.080148026498));
#74623=CARTESIAN_POINT('Ctrl Pts',(-8.32954454178611,-4.16915061233118,
128.195267626851));
#74624=CARTESIAN_POINT('Ctrl Pts',(-8.33723045367694,-4.24111053122496,
128.310254613128));
#74625=CARTESIAN_POINT('Ctrl Pts',(-8.34491636556771,-4.3083910161016,128.428350869654));
#74626=CARTESIAN_POINT('Ctrl Pts',(-8.35260227745854,-4.37071303132848,
128.549133209903));
#74627=CARTESIAN_POINT('Ctrl Pts',(-8.3602830297844,-4.43299320968651,128.669834468773));
#74628=CARTESIAN_POINT('Ctrl Pts',(-8.36796378211028,-4.49032135574294,
128.79321787286));
#74629=CARTESIAN_POINT('Ctrl Pts',(-8.37564453443613,-4.54246292632829,
128.918833204497));
#74630=CARTESIAN_POINT('Ctrl Pts',(-8.38332211999616,-4.59458299900082,
129.044396745071));
#74631=CARTESIAN_POINT('Ctrl Pts',(-8.3909997055562,-4.64152059544803,129.172190016107));
#74632=CARTESIAN_POINT('Ctrl Pts',(-8.39867729111623,-4.68308833391675,
129.301740665871));
#74633=CARTESIAN_POINT('Ctrl Pts',(-8.40417351598012,-4.71284581899082,
129.394483299189));
#74634=CARTESIAN_POINT('Ctrl Pts',(-8.40966974084399,-4.73985231839695,
129.488126070473));
#74635=CARTESIAN_POINT('Ctrl Pts',(-8.41516596570787,-4.76405452823401,
129.582490119308));
#74636=CARTESIAN_POINT('Ctrl Pts',(-6.66542383595777,-4.76405452823408,
129.582490119308));
#74637=CARTESIAN_POINT('Ctrl Pts',(-6.67380875453969,-4.80077876456201,
129.725677359383));
#74638=CARTESIAN_POINT('Ctrl Pts',(-6.68219367312164,-4.83108614509386,
129.870687833771));
#74639=CARTESIAN_POINT('Ctrl Pts',(-6.69057859170357,-4.8548085799642,130.016949216578));
#74640=CARTESIAN_POINT('Ctrl Pts',(-6.69893588454837,-4.87845285668149,
130.162728712951));
#74641=CARTESIAN_POINT('Ctrl Pts',(-6.70729317739312,-4.89555540448016,
130.309750619291));
#74642=CARTESIAN_POINT('Ctrl Pts',(-6.7156504702379,-4.90599870086107,130.457431504274));
#74643=CARTESIAN_POINT('Ctrl Pts',(-6.72214716814968,-4.91411699263929,
130.572234002511));
#74644=CARTESIAN_POINT('Ctrl Pts',(-6.72864386606151,-4.9182120442192,130.687434348684));
#74645=CARTESIAN_POINT('Ctrl Pts',(-6.73514056397329,-4.91824973727353,
130.802753039002));
#74646=CARTESIAN_POINT('',(-6.38985943602702,-4.91824879188756,130.80091335829));
#74647=CARTESIAN_POINT('Ctrl Pts',(-6.31979145723434,-4.76405452823404,
129.582490119308));
#74648=CARTESIAN_POINT('Ctrl Pts',(-6.32756591095457,-4.79808501180636,
129.715174458272));
#74649=CARTESIAN_POINT('Ctrl Pts',(-6.33534036467476,-4.82652757312717,
129.849123030039));
#74650=CARTESIAN_POINT('Ctrl Pts',(-6.34311481839498,-4.84932004182413,
129.983825307867));
#74651=CARTESIAN_POINT('Ctrl Pts',(-6.3466777798019,-4.85976562285889,130.045558136256));
#74652=CARTESIAN_POINT('Ctrl Pts',(-6.35024074120879,-4.86902523277928,
130.107449215245));
#74653=CARTESIAN_POINT('Ctrl Pts',(-6.35380370261569,-4.87709654325472,
130.169449308584));
#74654=CARTESIAN_POINT('Ctrl Pts',(-6.36582228040754,-4.90432267953643,
130.378587960341));
#74655=CARTESIAN_POINT('Ctrl Pts',(-6.37784085819934,-4.9181006199865,130.589514655206));
#74656=CARTESIAN_POINT('Ctrl Pts',(-6.38985943599116,-4.91824879188712,
130.80091335766));
#74657=CARTESIAN_POINT('Ctrl Pts',(-6.38985943602691,-4.91824879188756,
130.80091335829));
#74658=CARTESIAN_POINT('Ctrl Pts',(-6.39751660825043,-4.91834319386872,
130.935597869267));
#74659=CARTESIAN_POINT('Ctrl Pts',(-6.40517378047407,-4.91290100334641,
131.070498104028));
#74660=CARTESIAN_POINT('Ctrl Pts',(-6.41283095269759,-4.9018955881145,131.205113291573));
#74661=CARTESIAN_POINT('Ctrl Pts',(-6.42048006870295,-4.89090175183413,
131.339586848593));
#74662=CARTESIAN_POINT('Ctrl Pts',(-6.42812918470826,-4.8743563643088,131.47377555634));
#74663=CARTESIAN_POINT('Ctrl Pts',(-6.43577830071362,-4.85228481462837,
131.607177620517));
#74664=CARTESIAN_POINT('Ctrl Pts',(-6.44342132131879,-4.83023085324548,
131.740473379734));
#74665=CARTESIAN_POINT('Ctrl Pts',(-6.45106434192404,-4.80265955527722,
131.872983346633));
#74666=CARTESIAN_POINT('Ctrl Pts',(-6.4587073625292,-4.76964817117224,132.004210352213));
#74667=CARTESIAN_POINT('Ctrl Pts',(-6.466346844853,-4.73665206944983,132.135376607196));
#74668=CARTESIAN_POINT('Ctrl Pts',(-6.47398632717679,-4.69822098652581,
132.2652606917));
#74669=CARTESIAN_POINT('Ctrl Pts',(-6.4816258095006,-4.65448328216301,132.393375544672));
#74670=CARTESIAN_POINT('Ctrl Pts',(-6.48926362075416,-4.61075514504221,
132.521462373635));
#74671=CARTESIAN_POINT('Ctrl Pts',(-6.49690143200773,-4.56172282426308,
132.647780359251));
#74672=CARTESIAN_POINT('Ctrl Pts',(-6.50453924326129,-4.50756441087217,
132.771858049417));
#74673=CARTESIAN_POINT('Ctrl Pts',(-6.51217714705102,-4.45340534132316,
132.895937242849));
#74674=CARTESIAN_POINT('Ctrl Pts',(-6.51981505084081,-4.39412021713735,
133.017775717553));
#74675=CARTESIAN_POINT('Ctrl Pts',(-6.52745295463055,-4.3299348687763,133.136922962854));
#74676=CARTESIAN_POINT('Ctrl Pts',(-6.5350927144296,-4.26573392338656,133.256099160915));
#74677=CARTESIAN_POINT('Ctrl Pts',(-6.54273247422856,-4.19663057753906,
133.372582474692));
#74678=CARTESIAN_POINT('Ctrl Pts',(-6.55037223402761,-4.12289582368305,
133.485948410191));
#74679=CARTESIAN_POINT('Ctrl Pts',(-6.55801995493309,-4.04908423361244,
133.599432480069));
#74680=CARTESIAN_POINT('Ctrl Pts',(-6.56566767583859,-3.97063182042801,
133.709792348227));
#74681=CARTESIAN_POINT('Ctrl Pts',(-6.57331539674408,-3.88785215371226,
133.816633628662));
#74682=CARTESIAN_POINT('Ctrl Pts',(-6.5809675295815,-3.80502473182085,133.923536545297));
#74683=CARTESIAN_POINT('Ctrl Pts',(-6.58861966241889,-3.71786534616613,
134.026916526027));
#74684=CARTESIAN_POINT('Ctrl Pts',(-6.59627179525631,-3.62672590476346,
134.126414541604));
#74685=CARTESIAN_POINT('Ctrl Pts',(-6.60393521482056,-3.53545203469891,
134.226059314555));
#74686=CARTESIAN_POINT('Ctrl Pts',(-6.61159863438479,-3.44018667245611,
134.321810406574));
#74687=CARTESIAN_POINT('Ctrl Pts',(-6.61926205394903,-3.34131670019117,
134.413347424348));
#74688=CARTESIAN_POINT('Ctrl Pts',(-6.62359181144222,-3.2854561278086,134.465064948788));
#74689=CARTESIAN_POINT('Ctrl Pts',(-6.62792156893545,-3.22844549308984,
134.515438032771));
#74690=CARTESIAN_POINT('Ctrl Pts',(-6.63225132642864,-3.17035867720406,
134.564414994882));
#74691=CARTESIAN_POINT('Ctrl Pts',(-6.64002566054773,-3.06606038444297,
134.652356009637));
#74692=CARTESIAN_POINT('Ctrl Pts',(-6.6477999946668,-2.9579350890547,134.736093409582));
#74693=CARTESIAN_POINT('Ctrl Pts',(-6.65557432878589,-2.84635620073457,
134.81527565544));
#74694=CARTESIAN_POINT('Ctrl Pts',(-6.66333908173298,-2.73491482342236,
134.894360316255));
#74695=CARTESIAN_POINT('Ctrl Pts',(-6.67110383468005,-2.62002863761435,
134.968900768719));
#74696=CARTESIAN_POINT('Ctrl Pts',(-6.67886858762714,-2.50210551992899,
135.038584398809));
#74697=CARTESIAN_POINT('Ctrl Pts',(-6.68662562851214,-2.38429952514637,
135.108198818134));
#74698=CARTESIAN_POINT('Ctrl Pts',(-6.6943826693972,-2.2634629355184,135.172965817181));
#74699=CARTESIAN_POINT('Ctrl Pts',(-6.70213971028221,-2.14003382933992,
135.232615157651));
#74700=CARTESIAN_POINT('Ctrl Pts',(-6.70989090152235,-2.01669780201056,
135.292219516089));
#74701=CARTESIAN_POINT('Ctrl Pts',(-6.71764209276243,-1.89077350010286,
135.346713728155));
#74702=CARTESIAN_POINT('Ctrl Pts',(-6.72539328400256,-1.76272459183064,
135.395872903933));
#74703=CARTESIAN_POINT('Ctrl Pts',(-6.73314118077964,-1.63473010776043,
135.445011185749));
#74704=CARTESIAN_POINT('Ctrl Pts',(-6.74088907755672,-1.50461317758026,
135.488818801394));
#74705=CARTESIAN_POINT('Ctrl Pts',(-6.74863697433381,-1.37285828669157,
135.527118623982));
#74706=CARTESIAN_POINT('Ctrl Pts',(-6.7563832504179,-1.24113095608592,135.565410435072));
#74707=CARTESIAN_POINT('Ctrl Pts',(-6.76412952650198,-1.10776672146095,
135.598196635653));
#74708=CARTESIAN_POINT('Ctrl Pts',(-6.77187580258607,-0.973265719594784,
135.625349821201));
#74709=CARTESIAN_POINT('Ctrl Pts',(-6.77962213585141,-0.83876372487259,
135.652503207187));
#74710=CARTESIAN_POINT('Ctrl Pts',(-6.78736846911676,-0.703125329398517,
135.674023417797));
#74711=CARTESIAN_POINT('Ctrl Pts',(-6.7951148023821,-0.566860972950257,
135.689834156523));
#74712=CARTESIAN_POINT('Ctrl Pts',(-6.80286287038507,-0.430566101044161,
135.705648435953));
#74713=CARTESIAN_POINT('Ctrl Pts',(-6.81061093838809,-0.293645377508044,
135.715750654187));
#74714=CARTESIAN_POINT('Ctrl Pts',(-6.81835900639106,-0.156614077594845,
135.720116418376));
#74715=CARTESIAN_POINT('Ctrl Pts',(-6.82611530913291,-0.019437139185406,
135.724486822551));
#74716=CARTESIAN_POINT('Ctrl Pts',(-6.83387161187477,0.117850218973723,
135.723108581255));
#74717=CARTESIAN_POINT('Ctrl Pts',(-6.84162791461662,0.254732447592913,
135.71600946929));
#74718=CARTESIAN_POINT('Ctrl Pts',(-6.84938835713079,0.391687734379148,
135.708906568316));
#74719=CARTESIAN_POINT('Ctrl Pts',(-6.85714879964494,0.528237071708814,
135.696076749069));
#74720=CARTESIAN_POINT('Ctrl Pts',(-6.86490924215911,0.663871310428023,
135.677599575968));
#74721=CARTESIAN_POINT('Ctrl Pts',(-6.87268214242455,0.799723281268265,
135.659092741669));
#74722=CARTESIAN_POINT('Ctrl Pts',(-6.88045504269001,0.934656832912526,
135.63492050647));
#74723=CARTESIAN_POINT('Ctrl Pts',(-6.88822794295544,1.06817338119907,135.605213530351));
#74724=CARTESIAN_POINT('Ctrl Pts',(-6.89571827871748,1.19683626664769,135.576586477642));
#74725=CARTESIAN_POINT('Ctrl Pts',(-6.90320861447947,1.32418308565558,135.542820180188));
#74726=CARTESIAN_POINT('Ctrl Pts',(-6.91069895024151,1.44978393256617,135.504074397295));
#74727=CARTESIAN_POINT('Ctrl Pts',(-6.91847328436059,1.58014697376257,135.463859556267));
#74728=CARTESIAN_POINT('Ctrl Pts',(-6.92624761847968,1.70904198316749,135.41815279306));
#74729=CARTESIAN_POINT('Ctrl Pts',(-6.93402195259875,1.83597136376758,135.367078252258));
#74730=CARTESIAN_POINT('Ctrl Pts',(-6.94178670554583,1.96274431524991,135.316066656262));
#74731=CARTESIAN_POINT('Ctrl Pts',(-6.9495514584929,2.08755609868336,135.259700589705));
#74732=CARTESIAN_POINT('Ctrl Pts',(-6.95731621143997,2.20992323576158,135.19815423522));
#74733=CARTESIAN_POINT('Ctrl Pts',(-6.96507325232498,2.33216883607451,135.136669009443));
#74734=CARTESIAN_POINT('Ctrl Pts',(-6.97283029320999,2.45197427496104,135.070013909326));
#74735=CARTESIAN_POINT('Ctrl Pts',(-6.98058733409499,2.56887540126814,134.998411432144));
#74736=CARTESIAN_POINT('Ctrl Pts',(-6.9883385253351,2.68568837152621,134.926862950947));
#74737=CARTESIAN_POINT('Ctrl Pts',(-6.9960897165752,2.79960105654727,134.850374722108));
#74738=CARTESIAN_POINT('Ctrl Pts',(-7.00384090781532,2.91017362607812,134.769215284332));
#74739=CARTESIAN_POINT('Ctrl Pts',(-7.01158880459239,3.02069919931746,134.688090341483));
#74740=CARTESIAN_POINT('Ctrl Pts',(-7.01933670136957,3.12788716610135,134.602298369336));
#74741=CARTESIAN_POINT('Ctrl Pts',(-7.02708459814664,3.23132662836891,134.512151237773));
#74742=CARTESIAN_POINT('Ctrl Pts',(-7.03483087423075,3.334744453331,134.422022963046));
#74743=CARTESIAN_POINT('Ctrl Pts',(-7.04257715031474,3.4344150388515,134.327541597646));
#74744=CARTESIAN_POINT('Ctrl Pts',(-7.05032342639885,3.5299608597491,134.229059055551));
#74745=CARTESIAN_POINT('Ctrl Pts',(-7.05806975966416,3.62550738594373,134.130575786481));
#74746=CARTESIAN_POINT('Ctrl Pts',(-7.06581609292956,3.71692881451989,134.028091562386));
#74747=CARTESIAN_POINT('Ctrl Pts',(-7.07356242619488,3.80388504989494,133.921994590579));
#74748=CARTESIAN_POINT('Ctrl Pts',(-7.08131049419789,3.8908607585167,133.81587385909));
#74749=CARTESIAN_POINT('Ctrl Pts',(-7.08905856220087,3.97336903637257,133.706139072298));
#74750=CARTESIAN_POINT('Ctrl Pts',(-7.09680663020387,4.05111084220871,133.593210560937));
#74751=CARTESIAN_POINT('Ctrl Pts',(-7.10456293294572,4.12893527296091,133.48016202781));
#74752=CARTESIAN_POINT('Ctrl Pts',(-7.11231923568755,4.20198289003919,133.363913312124));
#74753=CARTESIAN_POINT('Ctrl Pts',(-7.1200755384294,4.26999839418924,133.244913173059));
#74754=CARTESIAN_POINT('Ctrl Pts',(-7.12783598094358,4.33805020026185,133.125849520036));
#74755=CARTESIAN_POINT('Ctrl Pts',(-7.13559642345776,4.40106436220009,133.004031864573));
#74756=CARTESIAN_POINT('Ctrl Pts',(-7.14335686597192,4.4588326122476,132.879931574786));
#74757=CARTESIAN_POINT('Ctrl Pts',(-7.15112976623736,4.51669359701851,132.755632068197));
#74758=CARTESIAN_POINT('Ctrl Pts',(-7.15890266650275,4.56929169155139,132.629042966118));
#74759=CARTESIAN_POINT('Ctrl Pts',(-7.16667556676819,4.61646732686937,132.500654366434));
#74760=CARTESIAN_POINT('Ctrl Pts',(-7.17416590253026,4.66192800901547,132.376933015739));
#74761=CARTESIAN_POINT('Ctrl Pts',(-7.18165623829237,4.70235353294895,132.251541021696));
#74762=CARTESIAN_POINT('Ctrl Pts',(-7.18914657405443,4.73764593419014,132.124926429918));
#74763=CARTESIAN_POINT('Ctrl Pts',(-7.19692090817352,4.77427645755113,131.993511207408));
#74764=CARTESIAN_POINT('Ctrl Pts',(-7.20469524229262,4.80549296420102,131.860362563536));
#74765=CARTESIAN_POINT('Ctrl Pts',(-7.21246957641171,4.8311309371547,131.725966243941));
#74766=CARTESIAN_POINT('Ctrl Pts',(-7.22023432935881,4.85673731359805,131.591735555799));
#74767=CARTESIAN_POINT('Ctrl Pts',(-7.22799908230588,4.87677876307636,131.456260631751));
#74768=CARTESIAN_POINT('Ctrl Pts',(-7.23576383525298,4.89114049853968,131.320042385757));
#74769=CARTESIAN_POINT('Ctrl Pts',(-7.243520876138,4.90548796972489,131.183959433646));
#74770=CARTESIAN_POINT('Ctrl Pts',(-7.25127791702304,4.91416691235429,131.047135015089));
#74771=CARTESIAN_POINT('Ctrl Pts',(-7.25903495790806,4.91711363465124,130.91007989881));
#74772=CARTESIAN_POINT('Ctrl Pts',(-7.2667861491482,4.92005813480199,130.773128136861));
#74773=CARTESIAN_POINT('Ctrl Pts',(-7.27453734038829,4.91727901034634,130.635946412761));
#74774=CARTESIAN_POINT('Ctrl Pts',(-7.28228853162844,4.90876445150753,130.499049919889));
#74775=CARTESIAN_POINT('Ctrl Pts',(-7.29003642840553,4.90025351158336,130.362211611679));
#74776=CARTESIAN_POINT('Ctrl Pts',(-7.29778432518259,4.88601200991975,130.225658682972));
#74777=CARTESIAN_POINT('Ctrl Pts',(-7.30553222195968,4.86608023104083,130.089905407232));
#74778=CARTESIAN_POINT('Ctrl Pts',(-7.31327849804379,4.84615262146037,129.954180528151));
#74779=CARTESIAN_POINT('Ctrl Pts',(-7.32102477412797,4.8205371589614,129.819255355901));
#74780=CARTESIAN_POINT('Ctrl Pts',(-7.32877105021208,4.78932585715792,129.685637731209));
#74781=CARTESIAN_POINT('Ctrl Pts',(-7.33651738347744,4.7581143249597,129.552019120183));
#74782=CARTESIAN_POINT('Ctrl Pts',(-7.34426371674279,4.72130695996176,129.419708456692));
#74783=CARTESIAN_POINT('Ctrl Pts',(-7.35201005000815,4.67904654200237,129.289201708317));
#74784=CARTESIAN_POINT('Ctrl Pts',(-7.35975811801114,4.63677666011533,129.158665733861));
#74785=CARTESIAN_POINT('Ctrl Pts',(-7.36750618601411,4.58905141569424,129.029934850263));
#74786=CARTESIAN_POINT('Ctrl Pts',(-7.37525425401711,4.53606280578764,128.903487848428));
#74787=CARTESIAN_POINT('Ctrl Pts',(-7.38301055675896,4.48301787895601,128.776906457215));
#74788=CARTESIAN_POINT('Ctrl Pts',(-7.39076685950082,4.42469856343286,128.65261415779));
#74789=CARTESIAN_POINT('Ctrl Pts',(-7.39852316224267,4.36134441754186,128.531068305945));
#74790=CARTESIAN_POINT('Ctrl Pts',(-7.40628360475684,4.29795645763556,128.409457581418));
#74791=CARTESIAN_POINT('Ctrl Pts',(-7.41404404727096,4.22952850777397,128.290596563987));
#74792=CARTESIAN_POINT('Ctrl Pts',(-7.42180448978513,4.15634456949191,128.174915261192));
#74793=CARTESIAN_POINT('Ctrl Pts',(-7.42957739005055,4.08304314985527,128.059048256501));
#74794=CARTESIAN_POINT('Ctrl Pts',(-7.43735029031603,4.00497070796082,127.94637148813));
#74795=CARTESIAN_POINT('Ctrl Pts',(-7.44512319058146,3.92245332611095,127.837284115859));
#74796=CARTESIAN_POINT('Ctrl Pts',(-7.45261352634341,3.84293565894074,127.732162344345));
#74797=CARTESIAN_POINT('Ctrl Pts',(-7.46010386210534,3.75929080620236,127.630373770501));
#74798=CARTESIAN_POINT('Ctrl Pts',(-7.4675941978673,3.67184276916407,127.532242994216));
#74799=CARTESIAN_POINT('Ctrl Pts',(-7.47536853198639,3.58107911322131,127.43039155972));
#74800=CARTESIAN_POINT('Ctrl Pts',(-7.48314286610546,3.4859306725159,127.332158134229));
#74801=CARTESIAN_POINT('Ctrl Pts',(-7.49091720022454,3.38671719316323,127.237943687925));
#74802=CARTESIAN_POINT('Ctrl Pts',(-7.49868195317163,3.28762598555703,127.143845352505));
#74803=CARTESIAN_POINT('Ctrl Pts',(-7.50644670611873,3.18447998808874,127.053756407849));
#74804=CARTESIAN_POINT('Ctrl Pts',(-7.51421145906582,3.07763858865604,126.968044183783));
#74805=CARTESIAN_POINT('Ctrl Pts',(-7.52196849995084,2.97090330560716,126.882417090306));
#74806=CARTESIAN_POINT('Ctrl Pts',(-7.52972554083585,2.86048022769284,126.801158309719));
#74807=CARTESIAN_POINT('Ctrl Pts',(-7.53748258172087,2.74676465214406,126.724597510689));
#74808=CARTESIAN_POINT('Ctrl Pts',(-7.545233772961,2.63313483039553,126.648094446754));
#74809=CARTESIAN_POINT('Ctrl Pts',(-7.55298496420114,2.51621777606994,126.576282530141));
#74810=CARTESIAN_POINT('Ctrl Pts',(-7.56073615544128,2.39644055247484,126.509450171357));
#74811=CARTESIAN_POINT('Ctrl Pts',(-7.56848405221837,2.27671423739493,126.442646218108));
#74812=CARTESIAN_POINT('Ctrl Pts',(-7.57623194899544,2.15413051157663,126.380817803341));
#74813=CARTESIAN_POINT('Ctrl Pts',(-7.58397984577252,2.02914382261941,126.324209011914));
#74814=CARTESIAN_POINT('Ctrl Pts',(-7.59172612185662,1.90418327818313,126.267612061826));
#74815=CARTESIAN_POINT('Ctrl Pts',(-7.5994723979407,1.77682112631648,126.216232724562));
#74816=CARTESIAN_POINT('Ctrl Pts',(-7.60721867402481,1.64753436341259,126.170268086781));
#74817=CARTESIAN_POINT('Ctrl Pts',(-7.61496500729014,1.51824664614354,126.1243031097));
#74818=CARTESIAN_POINT('Ctrl Pts',(-7.62271134055551,1.38703465786489,126.083753042827));
#74819=CARTESIAN_POINT('Ctrl Pts',(-7.63045767382084,1.25439284613963,126.048765844033));
#74820=CARTESIAN_POINT('Ctrl Pts',(-7.63820574182383,1.12172133019977,126.013770810098));
#74821=CARTESIAN_POINT('Ctrl Pts',(-7.64595380982687,0.987619731617193,
125.984341222867));
#74822=CARTESIAN_POINT('Ctrl Pts',(-7.65370187782986,0.85259464983481,125.960574347965));
#74823=CARTESIAN_POINT('Ctrl Pts',(-7.66145818057172,0.717426061788874,
125.936782213346));
#74824=CARTESIAN_POINT('Ctrl Pts',(-7.66921448331354,0.581332415573117,
125.918664881337));
#74825=CARTESIAN_POINT('Ctrl Pts',(-7.67697078605539,0.444827984692796,
125.906268016713));
#74826=CARTESIAN_POINT('Ctrl Pts',(-7.68473122856957,0.308250697287459,
125.893864535508));
#74827=CARTESIAN_POINT('Ctrl Pts',(-7.69249167108376,0.171262578657633,
125.887187624444));
#74828=CARTESIAN_POINT('Ctrl Pts',(-7.70025211359794,0.034378916093068,
125.886230774564));
#74829=CARTESIAN_POINT('Ctrl Pts',(-7.70802501386338,-0.102724484278419,
125.885272388664));
#74830=CARTESIAN_POINT('Ctrl Pts',(-7.71579791412883,-0.239722702549963,
125.890052399568));
#74831=CARTESIAN_POINT('Ctrl Pts',(-7.72357081439426,-0.376103658845832,
125.900512220613));
#74832=CARTESIAN_POINT('Ctrl Pts',(-7.73106115015625,-0.507526823856522,
125.910591800815));
#74833=CARTESIAN_POINT('Ctrl Pts',(-7.73855148591819,-0.638376519878124,
125.925945373882));
#74834=CARTESIAN_POINT('Ctrl Pts',(-7.74604182168017,-0.768204521231687,
125.94647580254));
#74835=CARTESIAN_POINT('Ctrl Pts',(-7.75381615579923,-0.902954990717521,
125.967784648641));
#74836=CARTESIAN_POINT('Ctrl Pts',(-7.76159048991832,-1.03703161002932,
125.994738160587));
#74837=CARTESIAN_POINT('Ctrl Pts',(-7.76936482403738,-1.16992420101081,
126.027284061095));
#74838=CARTESIAN_POINT('Ctrl Pts',(-7.77712957698444,-1.3026530137507,126.059789851688));
#74839=CARTESIAN_POINT('Ctrl Pts',(-7.78489432993153,-1.43420032545401,
126.097874225473));
#74840=CARTESIAN_POINT('Ctrl Pts',(-7.7926590828786,-1.5640628331963,126.141433369976));
#74841=CARTESIAN_POINT('Ctrl Pts',(-7.80041612376361,-1.69379635966568,
126.184949250923));
#74842=CARTESIAN_POINT('Ctrl Pts',(-7.80817316464861,-1.8218480439876,126.233928957953));
#74843=CARTESIAN_POINT('Ctrl Pts',(-7.81593020553362,-1.9477268587674,126.288218110278));
#74844=CARTESIAN_POINT('Ctrl Pts',(-7.82368139677371,-2.07351074735309,
126.34246632273));
#74845=CARTESIAN_POINT('Ctrl Pts',(-7.83143258801379,-2.19712467033849,
126.402015856764));
#74846=CARTESIAN_POINT('Ctrl Pts',(-7.83918377925389,-2.31809514164815,
126.466663304847));
#74847=CARTESIAN_POINT('Ctrl Pts',(-7.84693167603096,-2.439014197281,126.531283276041));
#74848=CARTESIAN_POINT('Ctrl Pts',(-7.85467957280802,-2.5572916917749,126.600996667899));
#74849=CARTESIAN_POINT('Ctrl Pts',(-7.8624274695851,-2.67247662959794,126.675553074612));
#74850=CARTESIAN_POINT('Ctrl Pts',(-7.87017374566919,-2.78763747321492,
126.750093885732));
#74851=CARTESIAN_POINT('Ctrl Pts',(-7.87792002175328,-2.89970671887072,
126.82947548438));
#74852=CARTESIAN_POINT('Ctrl Pts',(-7.88566629783736,-3.00826072377574,
126.913403090133));
#74853=CARTESIAN_POINT('Ctrl Pts',(-7.8934126311027,-3.11681553000191,126.997331315421));
#74854=CARTESIAN_POINT('Ctrl Pts',(-7.90115896436805,-3.22185473439564,
127.085805375641));
#74855=CARTESIAN_POINT('Ctrl Pts',(-7.9089052976334,-3.32298659482447,127.178489252898));
#74856=CARTESIAN_POINT('Ctrl Pts',(-7.91665336563638,-3.42414110303239,
127.271193886068));
#74857=CARTESIAN_POINT('Ctrl Pts',(-7.92440143363943,-3.52138623790646,
127.368109948154));
#74858=CARTESIAN_POINT('Ctrl Pts',(-7.93214950164241,-3.6143663377487,127.468863797143));
#74859=CARTESIAN_POINT('Ctrl Pts',(-7.93990580438427,-3.7074452579474,127.569724728523));
#74860=CARTESIAN_POINT('Ctrl Pts',(-7.94766210712607,-3.79624982252776,
127.674431306965));
#74861=CARTESIAN_POINT('Ctrl Pts',(-7.95541840986792,-3.88046363503061,
127.782575542531));
#74862=CARTESIAN_POINT('Ctrl Pts',(-7.96317885238207,-3.96472239498071,
127.890777497931));
#74863=CARTESIAN_POINT('Ctrl Pts',(-7.97093929489626,-4.04438529359944,
128.002420448316));
#74864=CARTESIAN_POINT('Ctrl Pts',(-7.97869973741041,-4.11917928168823,
128.117067349646));
#74865=CARTESIAN_POINT('Ctrl Pts',(-7.98647263767583,-4.1940933357267,128.231898292359));
#74866=CARTESIAN_POINT('Ctrl Pts',(-7.9942455379412,-4.2641226605189,128.349742486034));
#74867=CARTESIAN_POINT('Ctrl Pts',(-8.00201843820662,-4.32903975500504,
128.470137435845));
#74868=CARTESIAN_POINT('Ctrl Pts',(-8.00950877396876,-4.39159694959138,
128.586155725975));
#74869=CARTESIAN_POINT('Ctrl Pts',(-8.01699910973094,-4.4494070106166,128.704542262371));
#74870=CARTESIAN_POINT('Ctrl Pts',(-8.02448944549309,-4.50230938549294,
128.824867435006));
#74871=CARTESIAN_POINT('Ctrl Pts',(-8.03305066556223,-4.56277514936235,
128.962395353045));
#74872=CARTESIAN_POINT('Ctrl Pts',(-8.04161188563137,-4.61699461874163,
129.102829783133));
#74873=CARTESIAN_POINT('Ctrl Pts',(-8.05017310570051,-4.66470666636355,
129.245612793419));
#74874=CARTESIAN_POINT('Ctrl Pts',(-8.05682654203701,-4.70178655319895,
129.356578013469));
#74875=CARTESIAN_POINT('Ctrl Pts',(-8.06347997837353,-4.73493695577742,
129.468961146221));
#74876=CARTESIAN_POINT('Ctrl Pts',(-8.07013341471003,-4.76405452823399,
129.582490119308));
#74877=CARTESIAN_POINT('Origin',(213.235140564004,0.,130.804360617566));
#74878=CARTESIAN_POINT('',(-10.1650489208495,-4.76405452823411,129.582490119308));
#74879=CARTESIAN_POINT('',(-9.81992175947745,-4.76405452823407,129.582490119308));
#74880=CARTESIAN_POINT('',(213.235140564004,-4.76405452823405,129.582490119308));
#74881=CARTESIAN_POINT('',(-8.48514056406485,-4.91824798673127,130.808810731474));
#74882=CARTESIAN_POINT('Ctrl Pts',(-8.48514056406486,-4.91824798673127,
130.808810731474));
#74883=CARTESIAN_POINT('Ctrl Pts',(-8.49475443834549,-4.91809419702525,
130.978778495817));
#74884=CARTESIAN_POINT('Ctrl Pts',(-8.50436831262617,-4.90912602691106,
131.148353567338));
#74885=CARTESIAN_POINT('Ctrl Pts',(-8.51398218690682,-4.89148713916088,
131.316743901762));
#74886=CARTESIAN_POINT('Ctrl Pts',(-8.52375854373859,-4.87355013939081,
131.487980174288));
#74887=CARTESIAN_POINT('Ctrl Pts',(-8.53353490057044,-4.84664689567184,
131.657991430657));
#74888=CARTESIAN_POINT('Ctrl Pts',(-8.54331125740222,-4.81097707191774,
131.825968505154));
#74889=CARTESIAN_POINT('Ctrl Pts',(-8.54947273725463,-4.78849641739771,
131.931834870098));
#74890=CARTESIAN_POINT('Ctrl Pts',(-8.55563421710703,-4.76253458499389,
132.036893713832));
#74891=CARTESIAN_POINT('Ctrl Pts',(-8.56179569695945,-4.73315119516266,
132.140946875998));
#74892=CARTESIAN_POINT('Ctrl Pts',(-8.56957003107853,-4.69607628855403,
132.27223742116));
#74893=CARTESIAN_POINT('Ctrl Pts',(-8.57734436519764,-4.65347581258836,
132.402192148277));
#74894=CARTESIAN_POINT('Ctrl Pts',(-8.58511869931672,-4.60546193514355,
132.530310624502));
#74895=CARTESIAN_POINT('Ctrl Pts',(-8.59288345226381,-4.55750723051163,
132.658271206156));
#74896=CARTESIAN_POINT('Ctrl Pts',(-8.60064820521083,-4.50415253464717,
132.784399677059));
#74897=CARTESIAN_POINT('Ctrl Pts',(-8.60841295815791,-4.44556037787898,
132.908208518231));
#74898=CARTESIAN_POINT('Ctrl Pts',(-8.61616999904292,-4.38702641566683,
133.031894390717));
#74899=CARTESIAN_POINT('Ctrl Pts',(-8.62392703992801,-4.32326551076492,
133.153264867211));
#74900=CARTESIAN_POINT('Ctrl Pts',(-8.63168408081302,-4.25448895802691,
133.271850590905));
#74901=CARTESIAN_POINT('Ctrl Pts',(-8.63943527205314,-4.18576427022242,
133.390346888181));
#74902=CARTESIAN_POINT('Ctrl Pts',(-8.64718646329319,-4.11203165845224,
133.506062275755));
#74903=CARTESIAN_POINT('Ctrl Pts',(-8.65493765453331,-4.03354902937623,
133.618550605843));
#74904=CARTESIAN_POINT('Ctrl Pts',(-8.6626855513104,-3.95509975751107,133.73099112539));
#74905=CARTESIAN_POINT('Ctrl Pts',(-8.67043344808743,-3.87190470698588,
133.840206995465));
#74906=CARTESIAN_POINT('Ctrl Pts',(-8.67818134486453,-3.78426579744953,
133.945779952318));
#74907=CARTESIAN_POINT('Ctrl Pts',(-8.68592762094864,-3.69664522008379,
134.051330825584));
#74908=CARTESIAN_POINT('Ctrl Pts',(-8.69367389703279,-3.60458288221354,
134.153240000694));
#74909=CARTESIAN_POINT('Ctrl Pts',(-8.7014201731169,-3.50842153691041,134.25112161622));
#74910=CARTESIAN_POINT('Ctrl Pts',(-8.70916650638225,-3.41225948176621,
134.349003954286));
#74911=CARTESIAN_POINT('Ctrl Pts',(-8.71691283964761,-3.31199863280413,
134.442858394548));
#74912=CARTESIAN_POINT('Ctrl Pts',(-8.72465917291296,-3.20801892418793,
134.532335623458));
#74913=CARTESIAN_POINT('Ctrl Pts',(-8.73240724091594,-3.10401593003693,
134.621832890172));
#74914=CARTESIAN_POINT('Ctrl Pts',(-8.74015530891887,-2.99629271532096,
134.706950739993));
#74915=CARTESIAN_POINT('Ctrl Pts',(-8.74790337692184,-2.88526231356341,
134.787380131004));
#74916=CARTESIAN_POINT('Ctrl Pts',(-8.75565967966369,-2.7741139073736,134.867895003329));
#74917=CARTESIAN_POINT('Ctrl Pts',(-8.76341598240553,-2.65965160984144,
134.943711233142));
#74918=CARTESIAN_POINT('Ctrl Pts',(-8.77117228514737,-2.542317924436,135.014562825726));
#74919=CARTESIAN_POINT('Ctrl Pts',(-8.77893272766154,-2.42492161450966,
135.085452233937));
#74920=CARTESIAN_POINT('Ctrl Pts',(-8.78669317017569,-2.30465120566002,
135.151371537197));
#74921=CARTESIAN_POINT('Ctrl Pts',(-8.79445361268986,-2.18197293240709,
135.212101216188));
#74922=CARTESIAN_POINT('Ctrl Pts',(-8.8022265129553,-2.05909772509906,135.272928383852));
#74923=CARTESIAN_POINT('Ctrl Pts',(-8.80999941322072,-1.93380728679309,
135.328549120838));
#74924=CARTESIAN_POINT('Ctrl Pts',(-8.81777231348616,-1.80658774502393,
135.378792143125));
#74925=CARTESIAN_POINT('Ctrl Pts',(-8.82526264924818,-1.68399295404494,
135.427208704997));
#74926=CARTESIAN_POINT('Ctrl Pts',(-8.83275298501024,-1.55960717090831,
135.470631649492));
#74927=CARTESIAN_POINT('Ctrl Pts',(-8.84024332077226,-1.43387596132223,
135.508952288481));
#74928=CARTESIAN_POINT('Ctrl Pts',(-8.84801765489135,-1.30337761470934,
135.548725866145));
#74929=CARTESIAN_POINT('Ctrl Pts',(-8.85579198901044,-1.17101642444316,
135.583128583534));
#74930=CARTESIAN_POINT('Ctrl Pts',(-8.86356632312953,-1.03727404832743,
135.611984314484));
#74931=CARTESIAN_POINT('Ctrl Pts',(-8.87133107607662,-0.903696497737537,
135.640804483324));
#74932=CARTESIAN_POINT('Ctrl Pts',(-8.87909582902364,-0.768741526647516,
135.664091185992));
#74933=CARTESIAN_POINT('Ctrl Pts',(-8.88686058197072,-0.632907150194844,
135.681717647939));
#74934=CARTESIAN_POINT('Ctrl Pts',(-8.89461762285572,-0.497207686359793,
135.699326603036));
#74935=CARTESIAN_POINT('Ctrl Pts',(-8.90237466374083,-0.36063094054836,
135.711286455124));
#74936=CARTESIAN_POINT('Ctrl Pts',(-8.91013170462583,-0.223686005967314,
135.717521273726));
#74937=CARTESIAN_POINT('Ctrl Pts',(-8.91788289586595,-0.0868443426267111,
135.723751390602));
#74938=CARTESIAN_POINT('Ctrl Pts',(-8.92563408710603,0.0503645678496878,
135.724265049593));
#74939=CARTESIAN_POINT('Ctrl Pts',(-8.93338527834615,0.187425963848421,
135.719038081101));
#74940=CARTESIAN_POINT('Ctrl Pts',(-8.94113317512323,0.324429105097622,
135.713813334209));
#74941=CARTESIAN_POINT('Ctrl Pts',(-8.94888107190029,0.461284466706592,
135.702852827518));
#74942=CARTESIAN_POINT('Ctrl Pts',(-8.95662896867736,0.597476956591937,
135.686184492804));
#74943=CARTESIAN_POINT('Ctrl Pts',(-8.96437524476146,0.733640957944369,
135.669519644746));
#74944=CARTESIAN_POINT('Ctrl Pts',(-8.97212152084555,0.869141975548753,
135.647149390972));
#74945=CARTESIAN_POINT('Ctrl Pts',(-8.97986779692965,1.00347010684969,135.619153531821));
#74946=CARTESIAN_POINT('Ctrl Pts',(-8.987614130195,1.13779922973037,135.591157466011));
#74947=CARTESIAN_POINT('Ctrl Pts',(-8.99536046346037,1.27095506629012,135.557535791728));
#74948=CARTESIAN_POINT('Ctrl Pts',(-9.00310679672572,1.40243836545145,135.518419345839));
#74949=CARTESIAN_POINT('Ctrl Pts',(-9.01085486472869,1.53395110938598,135.479294140094));
#74950=CARTESIAN_POINT('Ctrl Pts',(-9.01860293273164,1.66379019594293,135.434671825621));
#74951=CARTESIAN_POINT('Ctrl Pts',(-9.02635100073462,1.79147236469755,135.384732854516));
#74952=CARTESIAN_POINT('Ctrl Pts',(-9.03410730347647,1.91929023558056,135.334740807679));
#74953=CARTESIAN_POINT('Ctrl Pts',(-9.04186360621828,2.04494624466254,135.279420959153));
#74954=CARTESIAN_POINT('Ctrl Pts',(-9.04961990896012,2.16797741912062,135.219001822996));
#74955=CARTESIAN_POINT('Ctrl Pts',(-9.05738035147429,2.29107425902108,135.158550439328));
#74956=CARTESIAN_POINT('Ctrl Pts',(-9.0651407939885,2.4115431295362,135.092994531708));
#74957=CARTESIAN_POINT('Ctrl Pts',(-9.07290123650267,2.52894733170234,135.02260770089));
#74958=CARTESIAN_POINT('Ctrl Pts',(-9.0806741367681,2.6465400015163,134.952107878884));
#74959=CARTESIAN_POINT('Ctrl Pts',(-9.08844703703357,2.7610578450976,134.876761851681));
#74960=CARTESIAN_POINT('Ctrl Pts',(-9.096219937299,2.87209399253994,134.796886028946));
#74961=CARTESIAN_POINT('Ctrl Pts',(-9.10371027306107,2.97909369634018,134.719913893562));
#74962=CARTESIAN_POINT('Ctrl Pts',(-9.11120060882309,3.08286020342269,134.638735773584));
#74963=CARTESIAN_POINT('Ctrl Pts',(-9.11869094458515,3.1830612322387,134.553667787473));
#74964=CARTESIAN_POINT('Ctrl Pts',(-9.12646527870423,3.28706141351713,134.465374422814));
#74965=CARTESIAN_POINT('Ctrl Pts',(-9.13423961282329,3.38754985043271,134.372610713861));
#74966=CARTESIAN_POINT('Ctrl Pts',(-9.14201394694237,3.48411801524719,134.275686692473));
#74967=CARTESIAN_POINT('Ctrl Pts',(-9.14977869988946,3.58056716842908,134.178882121279));
#74968=CARTESIAN_POINT('Ctrl Pts',(-9.15754345283659,3.67310538922981,134.077927713579));
#74969=CARTESIAN_POINT('Ctrl Pts',(-9.16530820578367,3.76135682928518,133.973173938873));
#74970=CARTESIAN_POINT('Ctrl Pts',(-9.17306524666867,3.84952061676616,133.868524207092));
#74971=CARTESIAN_POINT('Ctrl Pts',(-9.18082228755367,3.93340584623148,133.760082914975));
#74972=CARTESIAN_POINT('Ctrl Pts',(-9.18857932843866,4.01267345790768,133.648237334778));
#74973=CARTESIAN_POINT('Ctrl Pts',(-9.19633051967878,4.0918812932613,133.536476098204));
#74974=CARTESIAN_POINT('Ctrl Pts',(-9.20408171091896,4.16647821674404,133.421316001093));
#74975=CARTESIAN_POINT('Ctrl Pts',(-9.21183290215907,4.23616565256411,133.303177062713));
#74976=CARTESIAN_POINT('Ctrl Pts',(-9.21958079893614,4.30582346936498,133.185088336533));
#74977=CARTESIAN_POINT('Ctrl Pts',(-9.22732869571315,4.37057575049532,133.064023623274));
#74978=CARTESIAN_POINT('Ctrl Pts',(-9.23507659249023,4.43016757589819,132.940431382302));
#74979=CARTESIAN_POINT('Ctrl Pts',(-9.24282286857433,4.48974693597583,132.816864994163));
#74980=CARTESIAN_POINT('Ctrl Pts',(-9.2505691446584,4.54416781772878,132.690772481875));
#74981=CARTESIAN_POINT('Ctrl Pts',(-9.25831542074249,4.59322174465615,132.562625974933));
#74982=CARTESIAN_POINT('Ctrl Pts',(-9.26606175400784,4.64227603368847,132.434478522043));
#74983=CARTESIAN_POINT('Ctrl Pts',(-9.27380808727318,4.68596314907174,132.304277409371));
#74984=CARTESIAN_POINT('Ctrl Pts',(-9.28155442053853,4.72412331016522,132.172513391511));
#74985=CARTESIAN_POINT('Ctrl Pts',(-9.28930248854148,4.76229201696213,132.040719866013));
#74986=CARTESIAN_POINT('Ctrl Pts',(-9.29705055654444,4.7949311978062,131.907363114325));
#74987=CARTESIAN_POINT('Ctrl Pts',(-9.3047986245474,4.82193145809311,131.772947255896));
#74988=CARTESIAN_POINT('Ctrl Pts',(-9.31255492728925,4.84896041457799,131.638388538693));
#74989=CARTESIAN_POINT('Ctrl Pts',(-9.32031123003119,4.87033840150079,131.502768850099));
#74990=CARTESIAN_POINT('Ctrl Pts',(-9.32806753277305,4.88600742609159,131.366601219691));
#74991=CARTESIAN_POINT('Ctrl Pts',(-9.33582797528721,4.9016848137126,131.230360912519));
#74992=CARTESIAN_POINT('Ctrl Pts',(-9.34358841780132,4.91164713912134,131.093572470539));
#74993=CARTESIAN_POINT('Ctrl Pts',(-9.35134886031548,4.91588854392417,130.956751188846));
#74994=CARTESIAN_POINT('Ctrl Pts',(-9.35912176058091,4.92013675740653,130.819710269486));
#74995=CARTESIAN_POINT('Ctrl Pts',(-9.36689466084635,4.91864570251984,130.682636796235));
#74996=CARTESIAN_POINT('Ctrl Pts',(-9.37466756111178,4.91146166055344,130.546044107421));
#74997=CARTESIAN_POINT('Ctrl Pts',(-9.38215789687387,4.90453877660797,130.4144169069));
#74998=CARTESIAN_POINT('Ctrl Pts',(-9.38964823263593,4.89232965690248,130.283236448937));
#74999=CARTESIAN_POINT('Ctrl Pts',(-9.39713856839802,4.87492065455812,130.152953161159));
#75000=CARTESIAN_POINT('Ctrl Pts',(-9.40491290251711,4.85685158459867,130.017730142927));
#75001=CARTESIAN_POINT('Ctrl Pts',(-9.41268723663615,4.83312330377143,129.883045324401));
#75002=CARTESIAN_POINT('Ctrl Pts',(-9.42046157075524,4.8037758314374,129.749409991329));
#75003=CARTESIAN_POINT('Ctrl Pts',(-9.42822632370233,4.77446452724018,129.615939351861));
#75004=CARTESIAN_POINT('Ctrl Pts',(-9.4359910766495,4.7395478935791,129.483516002573));
#75005=CARTESIAN_POINT('Ctrl Pts',(-9.4437558295966,4.69911763514874,129.352645592661));
#75006=CARTESIAN_POINT('Ctrl Pts',(-9.4515128704816,4.65872753262103,129.221905165086));
#75007=CARTESIAN_POINT('Ctrl Pts',(-9.45926991136655,4.61283481788281,129.092714978569));
#75008=CARTESIAN_POINT('Ctrl Pts',(-9.46702695225156,4.56158204396177,128.965569623813));
#75009=CARTESIAN_POINT('Ctrl Pts',(-9.47477814349169,4.51036792015623,128.838520150359));
#75010=CARTESIAN_POINT('Ctrl Pts',(-9.48252933473186,4.45380192822689,128.713512800508));
#75011=CARTESIAN_POINT('Ctrl Pts',(-9.490280525972,4.39207605477006,128.591025805204));
#75012=CARTESIAN_POINT('Ctrl Pts',(-9.49802842274908,4.33037641645604,128.468590870139));
#75013=CARTESIAN_POINT('Ctrl Pts',(-9.50577631952618,4.26352143407366,128.348674507458));
#75014=CARTESIAN_POINT('Ctrl Pts',(-9.51352421630327,4.19175061867122,128.231733591865));
#75015=CARTESIAN_POINT('Ctrl Pts',(-9.52127049238738,4.11999481617606,128.11481713779));
#75016=CARTESIAN_POINT('Ctrl Pts',(-9.5290167684715,4.04332543035427,128.000875225819));
#75017=CARTESIAN_POINT('Ctrl Pts',(-9.53676304455561,3.96202699047914,127.890338450661));
#75018=CARTESIAN_POINT('Ctrl Pts',(-9.54450937782097,3.88072795047751,127.779800859545));
#75019=CARTESIAN_POINT('Ctrl Pts',(-9.55225571108635,3.79480001988117,127.672668770352));
#75020=CARTESIAN_POINT('Ctrl Pts',(-9.56000204435171,3.70456971908926,127.569341875904));
#75021=CARTESIAN_POINT('Ctrl Pts',(-9.56775011235469,3.61431921184709,127.465991842114));
#75022=CARTESIAN_POINT('Ctrl Pts',(-9.5754981803576,3.51976467429511,127.366448993173));
#75023=CARTESIAN_POINT('Ctrl Pts',(-9.58324624836058,3.42127110594655,127.271077854735));
#75024=CARTESIAN_POINT('Ctrl Pts',(-9.59100255110244,3.32267285746147,127.175605354717));
#75025=CARTESIAN_POINT('Ctrl Pts',(-9.59875885384437,3.22012749661558,127.084313694483));
#75026=CARTESIAN_POINT('Ctrl Pts',(-9.60651515658623,3.11403530321438,126.99752897001));
#75027=CARTESIAN_POINT('Ctrl Pts',(-9.61427559910041,3.00788648521504,126.910697925917));
#75028=CARTESIAN_POINT('Ctrl Pts',(-9.62203604161446,2.89818737515325,126.828378845269));
#75029=CARTESIAN_POINT('Ctrl Pts',(-9.62979648412863,2.78536833878292,126.750855186485));
#75030=CARTESIAN_POINT('Ctrl Pts',(-9.63756938439406,2.67236819527996,126.673207079842));
#75031=CARTESIAN_POINT('Ctrl Pts',(-9.64534228465955,2.55623844852386,126.600369986049));
#75032=CARTESIAN_POINT('Ctrl Pts',(-9.65311518492499,2.43743600075568,126.532582439252));
#75033=CARTESIAN_POINT('Ctrl Pts',(-9.66060552068694,2.3229523212103,126.467259140528));
#75034=CARTESIAN_POINT('Ctrl Pts',(-9.66809585644888,2.20598715927923,126.406624776928));
#75035=CARTESIAN_POINT('Ctrl Pts',(-9.67558619221083,2.08696614845374,126.35085016426));
#75036=CARTESIAN_POINT('Ctrl Pts',(-9.68336052632992,1.96343241982592,126.292960840199));
#75037=CARTESIAN_POINT('Ctrl Pts',(-9.69113486044899,1.83729255214507,126.240123680606));
#75038=CARTESIAN_POINT('Ctrl Pts',(-9.69890919456807,1.70899833603373,126.192581378494));
#75039=CARTESIAN_POINT('Ctrl Pts',(-9.70667394751516,1.58086223107793,126.145097668021));
#75040=CARTESIAN_POINT('Ctrl Pts',(-9.71443870046226,1.45057742351732,126.1028959659));
#75041=CARTESIAN_POINT('Ctrl Pts',(-9.72220345340935,1.31861889897095,126.066172434117));
#75042=CARTESIAN_POINT('Ctrl Pts',(-9.72996049429436,1.18679143749127,126.029485376664));
#75043=CARTESIAN_POINT('Ctrl Pts',(-9.73771753517933,1.05329394141015,125.998265765864));
#75044=CARTESIAN_POINT('Ctrl Pts',(-9.74547457606434,0.918619577288078,
125.972661006174));
#75045=CARTESIAN_POINT('Ctrl Pts',(-9.75322576730448,0.784046772151601,
125.947075555233));
#75046=CARTESIAN_POINT('Ctrl Pts',(-9.76097695854462,0.6482992479909,125.927096600207));
#75047=CARTESIAN_POINT('Ctrl Pts',(-9.76872814978475,0.511883127487427,
125.91282111284));
#75048=CARTESIAN_POINT('Ctrl Pts',(-9.77647604656184,0.375524987474187,
125.898551692936));
#75049=CARTESIAN_POINT('Ctrl Pts',(-9.78422394333894,0.238499204341029,
125.889980959897));
#75050=CARTESIAN_POINT('Ctrl Pts',(-9.79197184011602,0.101319621288873,
125.887154358231));
#75051=CARTESIAN_POINT('Ctrl Pts',(-9.79971811620012,-0.0358312667517578,
125.88432834783));
#75052=CARTESIAN_POINT('Ctrl Pts',(-9.80746439228426,-0.173135500085666,
125.887244086905));
#75053=CARTESIAN_POINT('Ctrl Pts',(-9.81521066836837,-0.310077012167492,
125.89589493988));
#75054=CARTESIAN_POINT('Ctrl Pts',(-9.82295700163372,-0.447019535120452,
125.904545856713));
#75055=CARTESIAN_POINT('Ctrl Pts',(-9.830703334899,-0.583598941291097,125.918931947273));
#75056=CARTESIAN_POINT('Ctrl Pts',(-9.83844966816434,-0.719302465535839,
125.938994544435));
#75057=CARTESIAN_POINT('Ctrl Pts',(-9.84619773616732,-0.855036379643933,
125.959061634477));
#75058=CARTESIAN_POINT('Ctrl Pts',(-9.85394580417038,-0.989893634827646,
125.984807703521));
#75059=CARTESIAN_POINT('Ctrl Pts',(-9.86169387217336,-1.12337025417762,
126.01612270216));
#75060=CARTESIAN_POINT('Ctrl Pts',(-9.86945017491522,-1.25698873406703,
126.047470982753));
#75061=CARTESIAN_POINT('Ctrl Pts',(-9.87720647765704,-1.38922326568352,
126.084399926788));
#75062=CARTESIAN_POINT('Ctrl Pts',(-9.88496278039889,-1.51958313423272,
126.126749030372));
#75063=CARTESIAN_POINT('Ctrl Pts',(-9.89272322291307,-1.65001257976899,
126.169120736947));
#75064=CARTESIAN_POINT('Ctrl Pts',(-9.90048366542726,-1.7785650022539,126.216918231236));
#75065=CARTESIAN_POINT('Ctrl Pts',(-9.90824410794144,-1.90476929688927,
126.269932650542));
#75066=CARTESIAN_POINT('Ctrl Pts',(-9.91601700820687,-2.03117618586211,
126.3230321733));
#75067=CARTESIAN_POINT('Ctrl Pts',(-9.92378990847223,-2.15522706047216,
126.381365189872));
#75068=CARTESIAN_POINT('Ctrl Pts',(-9.93156280873765,-2.27647426836526,
126.444676228993));
#75069=CARTESIAN_POINT('Ctrl Pts',(-9.9390531444997,-2.39331383484865,126.505685752371));
#75070=CARTESIAN_POINT('Ctrl Pts',(-9.94654348026184,-2.50754976925826,
126.571317501127));
#75071=CARTESIAN_POINT('Ctrl Pts',(-9.95403381602389,-2.61880829411776,
126.641305707868));
#75072=CARTESIAN_POINT('Ctrl Pts',(-9.96180953030539,-2.73430572015671,
126.713960434702));
#75073=CARTESIAN_POINT('Ctrl Pts',(-9.96958524458686,-2.84696028917741,
126.791540348069));
#75074=CARTESIAN_POINT('Ctrl Pts',(-9.97736095886833,-2.95632337599693,
126.873796388472));
#75075=CARTESIAN_POINT('Ctrl Pts',(-9.98518129061754,-3.06631399410443,
126.956524418469));
#75076=CARTESIAN_POINT('Ctrl Pts',(-9.99300162236678,-3.17297486361209,
127.043982262013));
#75077=CARTESIAN_POINT('Ctrl Pts',(-10.000821954116,-3.27587519215888,127.135869812358));
#75078=CARTESIAN_POINT('Ctrl Pts',(-10.0085782387396,-3.37793278532302,
127.227004820013));
#75079=CARTESIAN_POINT('Ctrl Pts',(-10.0163345233631,-3.47629089186883,
127.322497000842));
#75080=CARTESIAN_POINT('Ctrl Pts',(-10.0240908079867,-3.57055927789495,
127.422010915726));
#75081=CARTESIAN_POINT('Ctrl Pts',(-10.0318417021151,-3.66476214888378,
127.521455670013));
#75082=CARTESIAN_POINT('Ctrl Pts',(-10.0395925962436,-3.75488068681802,
127.624916314611));
#75083=CARTESIAN_POINT('Ctrl Pts',(-10.0473434903721,-3.84056004153913,
127.73201922543));
#75084=CARTESIAN_POINT('Ctrl Pts',(-10.0550906764112,-3.92619840657558,
127.839070897364));
#75085=CARTESIAN_POINT('Ctrl Pts',(-10.0628378624502,-4.00740157156914,
127.94976106293));
#75086=CARTESIAN_POINT('Ctrl Pts',(-10.0705850484893,-4.08385393653115,
128.063681853541));
#75087=CARTESIAN_POINT('Ctrl Pts',(-10.0784570378526,-4.16153791117038,
128.17943785158));
#75088=CARTESIAN_POINT('Ctrl Pts',(-10.086329027216,-4.23431642523966,128.298529150419));
#75089=CARTESIAN_POINT('Ctrl Pts',(-10.0942010165793,-4.30190329678341,
128.420495879871));
#75090=CARTESIAN_POINT('Ctrl Pts',(-10.1019474751096,-4.36841239295244,
128.540517664477));
#75091=CARTESIAN_POINT('Ctrl Pts',(-10.10969393364,-4.42989403403268,128.663323485389));
#75092=CARTESIAN_POINT('Ctrl Pts',(-10.1174403921704,-4.4861215025255,128.788449675317));
#75093=CARTESIAN_POINT('Ctrl Pts',(-10.1253751469502,-4.5437157144658,128.916617357327));
#75094=CARTESIAN_POINT('Ctrl Pts',(-10.13330990173,-4.5957968533957,129.047219274615));
#75095=CARTESIAN_POINT('Ctrl Pts',(-10.1412446565099,-4.64217365544846,
129.17973548691));
#75096=CARTESIAN_POINT('Ctrl Pts',(-10.1491794112898,-4.68855045750127,
129.312251699204));
#75097=CARTESIAN_POINT('Ctrl Pts',(-10.1571141660697,-4.72922281067665,
129.446681781197));
#75098=CARTESIAN_POINT('Ctrl Pts',(-10.1650489208495,-4.76405452823411,
129.582490119308));
#75099=CARTESIAN_POINT('Ctrl Pts',(-8.41516596570787,-4.76405452823401,
129.582490119308));
#75100=CARTESIAN_POINT('Ctrl Pts',(-8.42284261422826,-4.79785806847061,
129.71428960965));
#75101=CARTESIAN_POINT('Ctrl Pts',(-8.43051926274863,-4.82618886490382,
129.847496441167));
#75102=CARTESIAN_POINT('Ctrl Pts',(-8.43819591126902,-4.84894509276012,
129.981612448381));
#75103=CARTESIAN_POINT('Ctrl Pts',(-8.44602002005897,-4.87213844359852,
130.118304681733));
#75104=CARTESIAN_POINT('Ctrl Pts',(-8.45384412884894,-4.88954077746297,
130.255940956616));
#75105=CARTESIAN_POINT('Ctrl Pts',(-8.46166823763889,-4.90109945350708,
130.393986143052));
#75106=CARTESIAN_POINT('Ctrl Pts',(-8.46949234642882,-4.91265812955118,
130.532031329489));
#75107=CARTESIAN_POINT('Ctrl Pts',(-8.47731645521872,-4.91837314617225,
130.670484989973));
#75108=CARTESIAN_POINT('Ctrl Pts',(-8.48514056400865,-4.91824798673217,
130.80881073048));
#75109=CARTESIAN_POINT('',(-8.13985943594608,-4.91824948988454,130.802120583987));
#75110=CARTESIAN_POINT('Ctrl Pts',(-8.07013341471003,-4.76405452823399,
129.582490119308));
#75111=CARTESIAN_POINT('Ctrl Pts',(-8.07865204310352,-4.80133477966088,
129.727845253815));
#75112=CARTESIAN_POINT('Ctrl Pts',(-8.087170671497,-4.83200254344879,129.875079244239));
#75113=CARTESIAN_POINT('Ctrl Pts',(-8.09568929989047,-4.8558829875021,130.023602348838));
#75114=CARTESIAN_POINT('Ctrl Pts',(-8.10417256346428,-4.87966429263794,
130.171508864407));
#75115=CARTESIAN_POINT('Ctrl Pts',(-8.11265582703813,-4.89671441550626,
130.320693571389));
#75116=CARTESIAN_POINT('Ctrl Pts',(-8.12113909061196,-4.90690919425128,
130.470556450617));
#75117=CARTESIAN_POINT('Ctrl Pts',(-8.12737920572339,-4.91440826490383,
130.580792518279));
#75118=CARTESIAN_POINT('Ctrl Pts',(-8.13361932083473,-4.91819905960549,
130.691395148153));
#75119=CARTESIAN_POINT('Ctrl Pts',(-8.13985943594614,-4.91824948988454,
130.802120583988));
#75120=CARTESIAN_POINT('Ctrl Pts',(-8.13985943599121,-4.91824948988491,
130.802120584788));
#75121=CARTESIAN_POINT('Ctrl Pts',(-8.14774011749155,-4.91831317858587,
130.941956449707));
#75122=CARTESIAN_POINT('Ctrl Pts',(-8.15562079899188,-4.91240878708701,
131.081772089033));
#75123=CARTESIAN_POINT('Ctrl Pts',(-8.16350148049222,-4.90056794172436,
131.221034244093));
#75124=CARTESIAN_POINT('Ctrl Pts',(-8.17138511948355,-4.88872265268592,
131.360348661965));
#75125=CARTESIAN_POINT('Ctrl Pts',(-8.17926875847488,-4.87093650249959,
131.499108811236));
#75126=CARTESIAN_POINT('Ctrl Pts',(-8.18715239746621,-4.84729293307246,
131.636787361181));
#75127=CARTESIAN_POINT('Ctrl Pts',(-8.19504045733832,-4.82363610512323,
131.774543116648));
#75128=CARTESIAN_POINT('Ctrl Pts',(-8.20292851721046,-4.79411537670579,
131.911215698255));
#75129=CARTESIAN_POINT('Ctrl Pts',(-8.21081657708257,-4.75886511568041,
132.046288905858));
#75130=CARTESIAN_POINT('Ctrl Pts',(-8.2187163136846,-4.72356267353772,132.181562062928));
#75131=CARTESIAN_POINT('Ctrl Pts',(-8.22661605028666,-4.68251384709882,
132.315230755384));
#75132=CARTESIAN_POINT('Ctrl Pts',(-8.23451578688869,-4.63590292928399,
132.446793901677));
#75133=CARTESIAN_POINT('Ctrl Pts',(-8.24242159928218,-4.58925616239848,
132.578458234919));
#75134=CARTESIAN_POINT('Ctrl Pts',(-8.25032741167563,-4.53703891432322,
132.708013449104));
#75135=CARTESIAN_POINT('Ctrl Pts',(-8.2582332240691,-4.47948305945182,132.834979878428));
#75136=CARTESIAN_POINT('Ctrl Pts',(-8.2661537108043,-4.42182037251302,132.962181975977));
#75137=CARTESIAN_POINT('Ctrl Pts',(-8.27407419753948,-4.35879944090511,
133.086785352617));
#75138=CARTESIAN_POINT('Ctrl Pts',(-8.28199468427468,-4.29069798952574,
133.208335206695));
#75139=CARTESIAN_POINT('Ctrl Pts',(-8.28897547928509,-4.23067613886373,
133.315464306615));
#75140=CARTESIAN_POINT('Ctrl Pts',(-8.29595627429549,-4.16670852430057,
133.420221725413));
#75141=CARTESIAN_POINT('Ctrl Pts',(-8.3029370693059,-4.09901187452849,133.522316598625));
#75142=CARTESIAN_POINT('Ctrl Pts',(-8.31071140342498,-4.0236198348989,133.636017066123));
#75143=CARTESIAN_POINT('Ctrl Pts',(-8.31848573754406,-3.94337397269968,
133.746758355859));
#75144=CARTESIAN_POINT('Ctrl Pts',(-8.32626007166314,-3.8585338990758,133.854098182043));
#75145=CARTESIAN_POINT('Ctrl Pts',(-8.33402482461024,-3.77379838326028,
133.961305721485));
#75146=CARTESIAN_POINT('Ctrl Pts',(-8.34178957755735,-3.68448016172765,
134.065119834424));
#75147=CARTESIAN_POINT('Ctrl Pts',(-8.34955433050445,-3.59088285994828,
134.165125909673));
#75148=CARTESIAN_POINT('Ctrl Pts',(-8.35731137138946,-3.49737852032841,
134.265032657478));
#75149=CARTESIAN_POINT('Ctrl Pts',(-8.36506841227445,-3.39960382366651,
134.361138610734));
#75150=CARTESIAN_POINT('Ctrl Pts',(-8.37282545315946,-3.29790328564868,
134.45306134262));
#75151=CARTESIAN_POINT('Ctrl Pts',(-8.38057664439957,-3.19627944079823,
134.544914754858));
#75152=CARTESIAN_POINT('Ctrl Pts',(-8.38832783563969,-3.09073593617419,
134.632590963668));
#75153=CARTESIAN_POINT('Ctrl Pts',(-8.39607902687979,-2.98165458677833,
134.715743875142));
#75154=CARTESIAN_POINT('Ctrl Pts',(-8.40382692365686,-2.87261959986551,
134.79886144441));
#75155=CARTESIAN_POINT('Ctrl Pts',(-8.41157482043393,-2.76005006915821,
134.877459303569));
#75156=CARTESIAN_POINT('Ctrl Pts',(-8.419322717211,-2.64436120681958,134.951231349861));
#75157=CARTESIAN_POINT('Ctrl Pts',(-8.42706899329509,-2.528696544097,135.024987964631));
#75158=CARTESIAN_POINT('Ctrl Pts',(-8.43481526937917,-2.40991417703256,
135.093920564323));
#75159=CARTESIAN_POINT('Ctrl Pts',(-8.44256154546326,-2.2884583076316,135.157766369013));
#75160=CARTESIAN_POINT('Ctrl Pts',(-8.45030787872861,-2.16700154167099,
135.221612644998));
#75161=CARTESIAN_POINT('Ctrl Pts',(-8.45805421199396,-2.04287158005791,
135.280371869137));
#75162=CARTESIAN_POINT('Ctrl Pts',(-8.4658005452593,-1.91653687094088,135.333827416741));
#75163=CARTESIAN_POINT('Ctrl Pts',(-8.47354861326226,-1.79017387004169,
135.387294935343));
#75164=CARTESIAN_POINT('Ctrl Pts',(-8.48129668126523,-1.66160549914811,
135.435456261661));
#75165=CARTESIAN_POINT('Ctrl Pts',(-8.4890447492682,-1.53131942874953,135.478143225865));
#75166=CARTESIAN_POINT('Ctrl Pts',(-8.49680105201005,-1.4008948887649,135.520875558282));
#75167=CARTESIAN_POINT('Ctrl Pts',(-8.50455735475189,-1.26874937458389,
135.558121784147));
#75168=CARTESIAN_POINT('Ctrl Pts',(-8.51231365749373,-1.13538547546737,
135.589763723324));
#75169=CARTESIAN_POINT('Ctrl Pts',(-8.5200741000079,-1.00195039602221,135.621422550756));
#75170=CARTESIAN_POINT('Ctrl Pts',(-8.52783454252209,-0.867296019547383,
135.64747105711));
#75171=CARTESIAN_POINT('Ctrl Pts',(-8.53559498503625,-0.731933342490357,
135.66784256414));
#75172=CARTESIAN_POINT('Ctrl Pts',(-8.54336788530169,-0.596353369247186,
135.688246773322));
#75173=CARTESIAN_POINT('Ctrl Pts',(-8.55114078556709,-0.46006321221134,
135.702955730082));
#75174=CARTESIAN_POINT('Ctrl Pts',(-8.55891368583252,-0.323578082909706,
135.711954762028));
#75175=CARTESIAN_POINT('Ctrl Pts',(-8.56640402159466,-0.192054531841627,
135.720626656496));
#75176=CARTESIAN_POINT('Ctrl Pts',(-8.57389435735677,-0.0603502457845487,
135.723996551126));
#75177=CARTESIAN_POINT('Ctrl Pts',(-8.58138469311891,0.0710773012681246,
135.722096995184));
#75178=CARTESIAN_POINT('Ctrl Pts',(-8.58915902723802,0.207487963711916,
135.720125417001));
#75179=CARTESIAN_POINT('Ctrl Pts',(-8.59693336135712,0.344032595755697,
135.71247067256));
#75180=CARTESIAN_POINT('Ctrl Pts',(-8.60470769547621,0.480198763673881,
135.699112113798));
#75181=CARTESIAN_POINT('Ctrl Pts',(-8.6124724484233,0.616197118959626,135.685770018266));
#75182=CARTESIAN_POINT('Ctrl Pts',(-8.62023720137033,0.751817552800991,
135.666738132711));
#75183=CARTESIAN_POINT('Ctrl Pts',(-8.62800195431743,0.886547124080211,
135.642047798367));
#75184=CARTESIAN_POINT('Ctrl Pts',(-8.63575899520243,1.02114288004988,135.617381986811));
#75185=CARTESIAN_POINT('Ctrl Pts',(-8.64351603608747,1.15484915221111,135.587068980639));
#75186=CARTESIAN_POINT('Ctrl Pts',(-8.65127307697247,1.28715797490601,135.551191919618));
#75187=CARTESIAN_POINT('Ctrl Pts',(-8.65902426821257,1.41936702248797,135.515341913767));
#75188=CARTESIAN_POINT('Ctrl Pts',(-8.66677545945276,1.55018034237151,135.473936306651));
#75189=CARTESIAN_POINT('Ctrl Pts',(-8.67452665069285,1.67910037561594,135.427109257835));
#75190=CARTESIAN_POINT('Ctrl Pts',(-8.68227454746993,1.80796561440771,135.380302111763));
#75191=CARTESIAN_POINT('Ctrl Pts',(-8.69002244424695,1.93493880033633,135.328078240179));
#75192=CARTESIAN_POINT('Ctrl Pts',(-8.69777034102404,2.05953796816633,135.270621516817));
#75193=CARTESIAN_POINT('Ctrl Pts',(-8.70551661710814,2.18411107253629,135.213176812164));
#75194=CARTESIAN_POINT('Ctrl Pts',(-8.71326289319221,2.30631079174872,135.150501596567));
#75195=CARTESIAN_POINT('Ctrl Pts',(-8.7210091692763,2.4256759395769,135.082827550786));
#75196=CARTESIAN_POINT('Ctrl Pts',(-8.72875550254166,2.5450419685318,135.015153005451));
#75197=CARTESIAN_POINT('Ctrl Pts',(-8.73650183580706,2.6615730442427,134.942479749123));
#75198=CARTESIAN_POINT('Ctrl Pts',(-8.74424816907242,2.77483370655622,134.865084809562));
#75199=CARTESIAN_POINT('Ctrl Pts',(-8.75199623707542,2.88811973280993,134.78767253794));
#75200=CARTESIAN_POINT('Ctrl Pts',(-8.75974430507841,2.99813356556575,134.705536699542));
#75201=CARTESIAN_POINT('Ctrl Pts',(-8.76749237308141,3.10447012097299,134.618996685461));
#75202=CARTESIAN_POINT('Ctrl Pts',(-8.77524867582327,3.21091969213644,134.532364695624));
#75203=CARTESIAN_POINT('Ctrl Pts',(-8.78300497856511,3.31368387507331,134.441319426857));
#75204=CARTESIAN_POINT('Ctrl Pts',(-8.79076128130697,3.41239157971579,134.346219842491));
#75205=CARTESIAN_POINT('Ctrl Pts',(-8.79852172382113,3.51115196763213,134.251069500613));
#75206=CARTESIAN_POINT('Ctrl Pts',(-8.80628216633533,3.60585129335948,134.151860814028));
#75207=CARTESIAN_POINT('Ctrl Pts',(-8.81404260884949,3.69615725254146,134.048987657302));
#75208=CARTESIAN_POINT('Ctrl Pts',(-8.82181550911492,3.78660817886623,133.945949359451));
#75209=CARTESIAN_POINT('Ctrl Pts',(-8.82958840938038,3.87265139971772,133.839235140814));
#75210=CARTESIAN_POINT('Ctrl Pts',(-8.83736130964581,3.95399608638191,133.729270532653));
#75211=CARTESIAN_POINT('Ctrl Pts',(-8.84485164540781,4.03238368879051,133.623303414984));
#75212=CARTESIAN_POINT('Ctrl Pts',(-8.85234198116975,4.10640826025097,133.514318379429));
#75213=CARTESIAN_POINT('Ctrl Pts',(-8.85983231693174,4.17584990951577,133.402717905488));
#75214=CARTESIAN_POINT('Ctrl Pts',(-8.86760665105083,4.24792446001919,133.286886065657));
#75215=CARTESIAN_POINT('Ctrl Pts',(-8.8753809851699,4.31529001563534,133.167869623226));
#75216=CARTESIAN_POINT('Ctrl Pts',(-8.88315531928899,4.37765222161807,133.046088542418));
#75217=CARTESIAN_POINT('Ctrl Pts',(-8.89092007223609,4.43993757175541,132.924457545909));
#75218=CARTESIAN_POINT('Ctrl Pts',(-8.8986848251832,4.49723166463176,132.800069034926));
#75219=CARTESIAN_POINT('Ctrl Pts',(-8.90644957813029,4.54928361131065,132.673371502061));
#75220=CARTESIAN_POINT('Ctrl Pts',(-8.91420661901531,4.60128385926237,132.546799806972));
#75221=CARTESIAN_POINT('Ctrl Pts',(-8.92196365990035,4.64805217472143,132.417924013171));
#75222=CARTESIAN_POINT('Ctrl Pts',(-8.92972070078537,4.68938393768227,132.287216425629));
#75223=CARTESIAN_POINT('Ctrl Pts',(-8.9374718920255,4.73068453203908,132.156607405696));
#75224=CARTESIAN_POINT('Ctrl Pts',(-8.94522308326565,4.7665566167952,132.024169712818));
#75225=CARTESIAN_POINT('Ctrl Pts',(-8.95297427450578,4.79684412143037,131.890394473944));
#75226=CARTESIAN_POINT('Ctrl Pts',(-8.96072217128285,4.82711875306809,131.756676093115));
#75227=CARTESIAN_POINT('Ctrl Pts',(-8.96847006805995,4.85181343933435,131.621621677496));
#75228=CARTESIAN_POINT('Ctrl Pts',(-8.97621796483702,4.87082236442745,131.485736106334));
#75229=CARTESIAN_POINT('Ctrl Pts',(-8.98396424092111,4.88982731326321,131.349878959503));
#75230=CARTESIAN_POINT('Ctrl Pts',(-8.99171051700513,4.90314881245551,131.213191389897));
#75231=CARTESIAN_POINT('Ctrl Pts',(-8.99945679308922,4.9107324991684,131.076186635657));
#75232=CARTESIAN_POINT('Ctrl Pts',(-9.00720312635456,4.91831624186233,130.93918087008));
#75233=CARTESIAN_POINT('Ctrl Pts',(-9.01494945961993,4.92016206595188,130.801858305565));
#75234=CARTESIAN_POINT('Ctrl Pts',(-9.02269579288526,4.91626766588639,130.664735047343));
#75235=CARTESIAN_POINT('Ctrl Pts',(-9.03044386088819,4.91237239369701,130.527581081319));
#75236=CARTESIAN_POINT('Ctrl Pts',(-9.03819192889114,4.90273435048658,130.390626901135));
#75237=CARTESIAN_POINT('Ctrl Pts',(-9.04593999689408,4.88740329131241,130.254385953996));
#75238=CARTESIAN_POINT('Ctrl Pts',(-9.05369629963592,4.87205593810606,130.118000208357));
#75239=CARTESIAN_POINT('Ctrl Pts',(-9.06145260237779,4.85100352598916,129.982329599147));
#75240=CARTESIAN_POINT('Ctrl Pts',(-9.06920890511964,4.82434747773057,129.847880363397));
#75241=CARTESIAN_POINT('Ctrl Pts',(-9.07696934763382,4.79767720233635,129.713359368042));
#75242=CARTESIAN_POINT('Ctrl Pts',(-9.08472979014798,4.76539742329222,129.580061424877));
#75243=CARTESIAN_POINT('Ctrl Pts',(-9.09249023266216,4.72765989980244,129.448479009792));
#75244=CARTESIAN_POINT('Ctrl Pts',(-9.10026313292758,4.68986179668988,129.316685366933));
#75245=CARTESIAN_POINT('Ctrl Pts',(-9.10803603319306,4.64658856483965,129.186613126547));
#75246=CARTESIAN_POINT('Ctrl Pts',(-9.11580893345848,4.59804101573103,129.05873698111));
#75247=CARTESIAN_POINT('Ctrl Pts',(-9.12329926922054,4.55125829231615,128.935509455659));
#75248=CARTESIAN_POINT('Ctrl Pts',(-9.13078960498258,4.49957818431132,128.814321413378));
#75249=CARTESIAN_POINT('Ctrl Pts',(-9.13827994074464,4.44322045252909,128.695575405002));
#75250=CARTESIAN_POINT('Ctrl Pts',(-9.14605427486373,4.38472590021702,128.572327105628));
#75251=CARTESIAN_POINT('Ctrl Pts',(-9.15382860898285,4.32100672478463,128.451319261524));
#75252=CARTESIAN_POINT('Ctrl Pts',(-9.16160294310194,4.25225714809689,128.333026522596));
#75253=CARTESIAN_POINT('Ctrl Pts',(-9.16936769604905,4.183592299118,128.214879568897));
#75254=CARTESIAN_POINT('Ctrl Pts',(-9.17713244899608,4.10990957864789,128.099441397363));
#75255=CARTESIAN_POINT('Ctrl Pts',(-9.18489720194319,4.03145070460736,127.987165509161));
#75256=CARTESIAN_POINT('Ctrl Pts',(-9.19265424282818,3.95306975702682,127.875001134955));
#75257=CARTESIAN_POINT('Ctrl Pts',(-9.20041128371321,3.86992231863609,127.765993112097));
#75258=CARTESIAN_POINT('Ctrl Pts',(-9.2081683245982,3.78229515087075,127.660568885565));
#75259=CARTESIAN_POINT('Ctrl Pts',(-9.21591951583831,3.69473406343451,127.555224160263));
#75260=CARTESIAN_POINT('Ctrl Pts',(-9.22367070707846,3.60270021962093,127.453458151436));
#75261=CARTESIAN_POINT('Ctrl Pts',(-9.23142189831856,3.50652245851387,127.355667631747));
#75262=CARTESIAN_POINT('Ctrl Pts',(-9.23916979509563,3.41038557552065,127.257918675637));
#75263=CARTESIAN_POINT('Ctrl Pts',(-9.2469176918727,3.31010855184853,127.164142126162));
#75264=CARTESIAN_POINT('Ctrl Pts',(-9.25466558864977,3.20605896068198,127.074699908717));
#75265=CARTESIAN_POINT('Ctrl Pts',(-9.26241186473385,3.10203113444699,126.985276400657));
#75266=CARTESIAN_POINT('Ctrl Pts',(-9.27015814081786,2.99423260665302,126.90018567595));
#75267=CARTESIAN_POINT('Ctrl Pts',(-9.27790441690195,2.88306579464535,126.819750889343));
#75268=CARTESIAN_POINT('Ctrl Pts',(-9.28565075016727,2.77189816202967,126.739315508986));
#75269=CARTESIAN_POINT('Ctrl Pts',(-9.29339708343268,2.65736251233373,126.663536364493));
#75270=CARTESIAN_POINT('Ctrl Pts',(-9.30114341669801,2.53989181329801,126.592694363072));
#75271=CARTESIAN_POINT('Ctrl Pts',(-9.308891484701,2.42239480751324,126.521836497076));
#75272=CARTESIAN_POINT('Ctrl Pts',(-9.31663955270393,2.30196177920256,126.455918176111));
#75273=CARTESIAN_POINT('Ctrl Pts',(-9.32438762070691,2.17905159986428,126.395175070594));
#75274=CARTESIAN_POINT('Ctrl Pts',(-9.33214392344877,2.05601079012475,126.334367406581));
#75275=CARTESIAN_POINT('Ctrl Pts',(-9.33990022619064,1.93048792122188,126.278746118913));
#75276=CARTESIAN_POINT('Ctrl Pts',(-9.3476565289325,1.80296372619136,126.228499511223));
#75277=CARTESIAN_POINT('Ctrl Pts',(-9.35541697144667,1.67537146765827,126.178226085407));
#75278=CARTESIAN_POINT('Ctrl Pts',(-9.36317741396091,1.54577612382916,126.133333183463));
#75279=CARTESIAN_POINT('Ctrl Pts',(-9.37093785647508,1.41467405817407,126.093959321325));
#75280=CARTESIAN_POINT('Ctrl Pts',(-9.37871075674052,1.28336153584449,126.054522252767));
#75281=CARTESIAN_POINT('Ctrl Pts',(-9.38648365700589,1.15053783734785,126.020622025165));
#75282=CARTESIAN_POINT('Ctrl Pts',(-9.39425655727132,1.01671087841746,125.992346273011));
#75283=CARTESIAN_POINT('Ctrl Pts',(-9.40174689303338,0.887748866533404,
125.965098415669));
#75284=CARTESIAN_POINT('Ctrl Pts',(-9.40923722879547,0.757855573605318,
125.943073257155));
#75285=CARTESIAN_POINT('Ctrl Pts',(-9.41672756455753,0.627488463054982,
125.926303494978));
#75286=CARTESIAN_POINT('Ctrl Pts',(-9.42450189867662,0.492178443884476,
125.908897902171));
#75287=CARTESIAN_POINT('Ctrl Pts',(-9.43227623279572,0.355929346771139,
125.897098953564));
#75288=CARTESIAN_POINT('Ctrl Pts',(-9.44005056691481,0.219245489785435,
125.890999804669));
#75289=CARTESIAN_POINT('Ctrl Pts',(-9.44781531986191,0.0827300834374924,
125.884908172431));
#75290=CARTESIAN_POINT('Ctrl Pts',(-9.45558007280897,-0.0542186298681168,
125.884502380517));
#75291=CARTESIAN_POINT('Ctrl Pts',(-9.46334482575608,-0.191088452313938,
125.889824193254));
#75292=CARTESIAN_POINT('Ctrl Pts',(-9.47110186664108,-0.327822333722208,
125.895140720291));
#75293=CARTESIAN_POINT('Ctrl Pts',(-9.47885890752611,-0.464477092059701,
125.906173516043));
#75294=CARTESIAN_POINT('Ctrl Pts',(-9.4866159484111,-0.600538104199871,
125.922912364444));
#75295=CARTESIAN_POINT('Ctrl Pts',(-9.49436713965121,-0.736496511672199,
125.93963858995));
#75296=CARTESIAN_POINT('Ctrl Pts',(-9.50211833089134,-0.871861677694062,
125.96206225574));
#75297=CARTESIAN_POINT('Ctrl Pts',(-9.50986952213145,-1.0061220406309,125.990121165497));
#75298=CARTESIAN_POINT('Ctrl Pts',(-9.51761741890853,-1.14032533933216,
126.018168149469));
#75299=CARTESIAN_POINT('Ctrl Pts',(-9.52536531568559,-1.27342438699295,
126.051845533866));
#75300=CARTESIAN_POINT('Ctrl Pts',(-9.53311321246267,-1.40491600324223,
126.091039698476));
#75301=CARTESIAN_POINT('Ctrl Pts',(-9.54085948854675,-1.53638011427986,
126.130225664511));
#75302=CARTESIAN_POINT('Ctrl Pts',(-9.54860576463082,-1.66623708826832,
126.174926003796));
#75303=CARTESIAN_POINT('Ctrl Pts',(-9.5563520407149,-1.79399752956222,126.224976824257));
#75304=CARTESIAN_POINT('Ctrl Pts',(-9.56409837398026,-1.92175891395521,
126.275028014181));
#75305=CARTESIAN_POINT('Ctrl Pts',(-9.57184470724563,-2.04742337074434,
126.330429621481));
#75306=CARTESIAN_POINT('Ctrl Pts',(-9.57959104051099,-2.17052053509985,
126.390969215344));
#75307=CARTESIAN_POINT('Ctrl Pts',(-9.58733910851394,-2.29364526621116,
126.451522366628));
#75308=CARTESIAN_POINT('Ctrl Pts',(-9.59508717651692,-2.41420121008456,
126.51721562156));
#75309=CARTESIAN_POINT('Ctrl Pts',(-9.60283524451987,-2.53174205927058,
126.587790304169));
#75310=CARTESIAN_POINT('Ctrl Pts',(-9.61059154726173,-2.64940783227035,
126.658439994391));
#75311=CARTESIAN_POINT('Ctrl Pts',(-9.6183478500036,-2.76405177357048,126.733981274381));
#75312=CARTESIAN_POINT('Ctrl Pts',(-9.62610415274546,-2.87525561004309,
126.814111472536));
#75313=CARTESIAN_POINT('Ctrl Pts',(-9.63386459525963,-2.98651879935167,
126.894284438589));
#75314=CARTESIAN_POINT('Ctrl Pts',(-9.64162503777379,-3.09433791807148,
126.979050961613));
#75315=CARTESIAN_POINT('Ctrl Pts',(-9.64938548028798,-3.19832813224702,
127.068068308207));
#75316=CARTESIAN_POINT('Ctrl Pts',(-9.65715838055341,-3.30248528074602,
127.157228553347));
#75317=CARTESIAN_POINT('Ctrl Pts',(-9.66493128081886,-3.402800955769,127.250652991577));
#75318=CARTESIAN_POINT('Ctrl Pts',(-9.6727041810843,-3.49892688707446,127.347961667588));
#75319=CARTESIAN_POINT('Ctrl Pts',(-9.68019451684633,-3.59155839865037,
127.441732928121));
#75320=CARTESIAN_POINT('Ctrl Pts',(-9.68768485260831,-3.68029928594057,
127.539110698059));
#75321=CARTESIAN_POINT('Ctrl Pts',(-9.69517518837034,-3.76487476945033,
127.639727774272));
#75322=CARTESIAN_POINT('Ctrl Pts',(-9.70290515034446,-3.85215593977986,
127.743563730066));
#75323=CARTESIAN_POINT('Ctrl Pts',(-9.71063511231849,-3.93528669078073,
127.85119007496));
#75324=CARTESIAN_POINT('Ctrl Pts',(-9.71836507429259,-4.01391671537598,
127.962238933942));
#75325=CARTESIAN_POINT('Ctrl Pts',(-9.72608557273473,-4.09245047588179,
128.073151839548));
#75326=CARTESIAN_POINT('Ctrl Pts',(-9.73380607117693,-4.16649424273253,
128.187478605739));
#75327=CARTESIAN_POINT('Ctrl Pts',(-9.74152656961905,-4.23573638300213,
128.304816587905));
#75328=CARTESIAN_POINT('Ctrl Pts',(-9.74923780683666,-4.30489546296001,
128.422013815766));
#75329=CARTESIAN_POINT('Ctrl Pts',(-9.7569490440543,-4.36926418489053,128.542214728939));
#75330=CARTESIAN_POINT('Ctrl Pts',(-9.76466028127192,-4.42857329347761,
128.664986492548));
#75331=CARTESIAN_POINT('Ctrl Pts',(-9.77236618259188,-4.48784136230359,
128.787673302531));
#75332=CARTESIAN_POINT('Ctrl Pts',(-9.78007208391177,-4.54205660962594,
128.912927070076));
#75333=CARTESIAN_POINT('Ctrl Pts',(-9.78777798523171,-4.59099495974659,
129.040289093483));
#75334=CARTESIAN_POINT('Ctrl Pts',(-9.79548001981686,-4.63990875315239,
129.167587208056));
#75335=CARTESIAN_POINT('Ctrl Pts',(-9.80318205440206,-4.6835507774132,129.296991104518));
#75336=CARTESIAN_POINT('Ctrl Pts',(-9.81088408898722,-4.72174469572343,
129.428021236851));
#75337=CARTESIAN_POINT('Ctrl Pts',(-9.8138966458173,-4.73668378074059,129.479272073982));
#75338=CARTESIAN_POINT('Ctrl Pts',(-9.81690920264739,-4.75078989188748,
129.530771503512));
#75339=CARTESIAN_POINT('Ctrl Pts',(-9.81992175947747,-4.76405452823407,
129.582490119308));
#75340=CARTESIAN_POINT('Origin',(213.235140564004,0.,130.804360617566));
#75341=CARTESIAN_POINT('',(-11.9152857535002,-4.76405452823405,129.582490119308));
#75342=CARTESIAN_POINT('',(-11.5697518023984,-4.76405452823402,129.582490119308));
#75343=CARTESIAN_POINT('',(213.235140564004,-4.76405452823405,129.582490119308));
#75344=CARTESIAN_POINT('',(-10.2351405640601,-4.91824999126511,130.804067495121));
#75345=CARTESIAN_POINT('Ctrl Pts',(-10.2351405640602,-4.91824999126511,
130.804067495121));
#75346=CARTESIAN_POINT('Ctrl Pts',(-10.2429017491463,-4.91825810842386,
130.940263875405));
#75347=CARTESIAN_POINT('Ctrl Pts',(-10.2506629342323,-4.91260460408128,
131.076679746296));
#75348=CARTESIAN_POINT('Ctrl Pts',(-10.2584241193184,-4.90126071843733,
131.212804533426));
#75349=CARTESIAN_POINT('Ctrl Pts',(-10.2661757404953,-4.88993081157252,
131.348761577475));
#75350=CARTESIAN_POINT('Ctrl Pts',(-10.2739273616722,-4.87292450676915,
131.484427864117));
#75351=CARTESIAN_POINT('Ctrl Pts',(-10.2816789828491,-4.85026501951163,
131.61929147537));
#75352=CARTESIAN_POINT('Ctrl Pts',(-10.2894229231295,-4.8276279849996,131.754021453488));
#75353=CARTESIAN_POINT('Ctrl Pts',(-10.2971668634097,-4.79934897938044,
131.887949954395));
#75354=CARTESIAN_POINT('Ctrl Pts',(-10.3049108036901,-4.76550308931971,
132.020569221459));
#75355=CARTESIAN_POINT('Ctrl Pts',(-10.3126489392927,-4.73168256935185,
132.153089080202));
#75356=CARTESIAN_POINT('Ctrl Pts',(-10.3203870748954,-4.69230356683776,
132.284301279617));
#75357=CARTESIAN_POINT('Ctrl Pts',(-10.328125210498,-4.64749234246125,132.413707686804));
#75358=CARTESIAN_POINT('Ctrl Pts',(-10.3358601234575,-4.60269978027845,
132.543060201077));
#75359=CARTESIAN_POINT('Ctrl Pts',(-10.3435950364169,-4.55247962350084,
132.670608048639));
#75360=CARTESIAN_POINT('Ctrl Pts',(-10.3513299493764,-4.49700807573169,
132.795867943514));
#75361=CARTESIAN_POINT('Ctrl Pts',(-10.3590633079488,-4.44154767537383,
132.921102666501));
#75362=CARTESIAN_POINT('Ctrl Pts',(-10.3667966665212,-4.38083814177513,
133.044049992645));
#75363=CARTESIAN_POINT('Ctrl Pts',(-10.3745300250936,-4.31510378265571,
133.164246718082));
#75364=CARTESIAN_POINT('Ctrl Pts',(-10.3822635195478,-4.24936826852709,
133.284445555479));
#75365=CARTESIAN_POINT('Ctrl Pts',(-10.3899970140019,-4.17860794137014,
133.401893351596));
#75366=CARTESIAN_POINT('Ctrl Pts',(-10.3977305084561,-4.10309281461364,
133.516151984387));
#75367=CARTESIAN_POINT('Ctrl Pts',(-10.4054658288026,-4.02755985859584,
133.630437593854));
#75368=CARTESIAN_POINT('Ctrl Pts',(-10.4132011491492,-3.94727008565719,
133.741532214494));
#75369=CARTESIAN_POINT('Ctrl Pts',(-10.4209364694957,-3.86253628486645,
133.849027514057));
#75370=CARTESIAN_POINT('Ctrl Pts',(-10.4286800326156,-3.77771219156258,
133.956637360834));
#75371=CARTESIAN_POINT('Ctrl Pts',(-10.4364235957355,-3.6884348549411,134.060639917006));
#75372=CARTESIAN_POINT('Ctrl Pts',(-10.4441671588554,-3.59505707031016,
134.160660324641));
#75373=CARTESIAN_POINT('Ctrl Pts',(-10.4519149673367,-3.50162809187508,
134.260735567858));
#75374=CARTESIAN_POINT('Ctrl Pts',(-10.4596627758181,-3.40409446597181,
134.356824037765));
#75375=CARTESIAN_POINT('Ctrl Pts',(-10.4674105842995,-3.30284439326151,
134.448589202109));
#75376=CARTESIAN_POINT('Ctrl Pts',(-10.4751706114612,-3.20143464413844,
134.540499084693));
#75377=CARTESIAN_POINT('Ctrl Pts',(-10.4829306386228,-3.0962970395167,134.628071788221));
#75378=CARTESIAN_POINT('Ctrl Pts',(-10.4906906657845,-2.98785188863263,
134.71101188868));
#75379=CARTESIAN_POINT('Ctrl Pts',(-10.4974367984062,-2.8935757534071,134.783115362765));
#75380=CARTESIAN_POINT('Ctrl Pts',(-10.5041829310279,-2.79680051840778,
134.85171829878));
#75381=CARTESIAN_POINT('Ctrl Pts',(-10.5109290636496,-2.69781790896645,
134.916654575026));
#75382=CARTESIAN_POINT('Ctrl Pts',(-10.5187033977687,-2.58374901632448,
134.991488014612));
#75383=CARTESIAN_POINT('Ctrl Pts',(-10.5264777318878,-2.46638343527605,
135.061690237066));
#75384=CARTESIAN_POINT('Ctrl Pts',(-10.5342520660069,-2.3461339454031,135.126956894426));
#75385=CARTESIAN_POINT('Ctrl Pts',(-10.542016818954,-2.22603265227925,135.192143116465));
#75386=CARTESIAN_POINT('Ctrl Pts',(-10.549781571901,-2.10305486236609,135.252405691345));
#75387=CARTESIAN_POINT('Ctrl Pts',(-10.5575463248481,-1.97764291845774,
135.307483039794));
#75388=CARTESIAN_POINT('Ctrl Pts',(-10.5653033657331,-1.85235553546042,
135.362505684645));
#75389=CARTESIAN_POINT('Ctrl Pts',(-10.5730604066181,-1.72463916532199,
135.412353195686));
#75390=CARTESIAN_POINT('Ctrl Pts',(-10.5808174475031,-1.59496106668328,
135.456809677821));
#75391=CARTESIAN_POINT('Ctrl Pts',(-10.5885686387433,-1.4653807593068,135.501232634977));
#75392=CARTESIAN_POINT('Ctrl Pts',(-10.5963198299834,-1.3338420363354,135.540272528917));
#75393=CARTESIAN_POINT('Ctrl Pts',(-10.6040710212236,-1.20083213802427,
135.573761548374));
#75394=CARTESIAN_POINT('Ctrl Pts',(-10.6118189180007,-1.06787877246845,
135.607236334103));
#75395=CARTESIAN_POINT('Ctrl Pts',(-10.6195668147777,-0.933455853563626,
135.635164842499));
#75396=CARTESIAN_POINT('Ctrl Pts',(-10.6273147115548,-0.798065575877236,
135.657429172522));
#75397=CARTESIAN_POINT('Ctrl Pts',(-10.6350609876389,-0.662703618918261,
135.679688845326));
#75398=CARTESIAN_POINT('Ctrl Pts',(-10.6428072637231,-0.526375091203496,
135.696286633038));
#75399=CARTESIAN_POINT('Ctrl Pts',(-10.6505535398072,-0.389591778518623,
135.707155872174));
#75400=CARTESIAN_POINT('Ctrl Pts',(-10.6582998730725,-0.252807456130222,
135.718025191545));
#75401=CARTESIAN_POINT('Ctrl Pts',(-10.6660462063378,-0.115568731809494,
135.723165846992));
#75402=CARTESIAN_POINT('Ctrl Pts',(-10.6737925396032,0.0216084931659148,
135.722563148524));
#75403=CARTESIAN_POINT('Ctrl Pts',(-10.6815406076061,0.158816438028989,
135.721960315087));
#75404=CARTESIAN_POINT('Ctrl Pts',(-10.6892886756092,0.29596246525475,135.715611570095));
#75405=CARTESIAN_POINT('Ctrl Pts',(-10.6970367436121,0.432532081514863,
135.70355433296));
#75406=CARTESIAN_POINT('Ctrl Pts',(-10.704793046354,0.569246845588709,135.691484281251));
#75407=CARTESIAN_POINT('Ctrl Pts',(-10.7125493490958,0.705383584858226,
135.673693652245));
#75408=CARTESIAN_POINT('Ctrl Pts',(-10.7203056518377,0.840433774209168,
135.65027169121));
#75409=CARTESIAN_POINT('Ctrl Pts',(-10.7280660943518,0.975556043912633,
135.62683722917));
#75410=CARTESIAN_POINT('Ctrl Pts',(-10.7358265368661,1.10959022625492,135.597765528998));
#75411=CARTESIAN_POINT('Ctrl Pts',(-10.7435869793802,1.24204034536529,135.563196488132));
#75412=CARTESIAN_POINT('Ctrl Pts',(-10.7513598796457,1.37470308516524,135.528571953973));
#75413=CARTESIAN_POINT('Ctrl Pts',(-10.759132779911,1.50577630620677,135.488432558865));
#75414=CARTESIAN_POINT('Ctrl Pts',(-10.7669056801764,1.63478063379225,135.442967665148));
#75415=CARTESIAN_POINT('Ctrl Pts',(-10.7743960159385,1.75909532912736,135.399155534837));
#75416=CARTESIAN_POINT('Ctrl Pts',(-10.7818863517005,1.88148865233982,135.35039848829));
#75417=CARTESIAN_POINT('Ctrl Pts',(-10.7893766874625,2.00155289496522,135.296906562924));
#75418=CARTESIAN_POINT('Ctrl Pts',(-10.7971510215816,2.12616940984285,135.24138647495));
#75419=CARTESIAN_POINT('Ctrl Pts',(-10.8049253557006,2.24867149119457,135.180589503669));
#75420=CARTESIAN_POINT('Ctrl Pts',(-10.8126996898197,2.36857996501309,135.114698424727));
#75421=CARTESIAN_POINT('Ctrl Pts',(-10.8204644427668,2.48834066235382,135.04888855065));
#75422=CARTESIAN_POINT('Ctrl Pts',(-10.8282291957139,2.60551377267246,134.977997246802));
#75423=CARTESIAN_POINT('Ctrl Pts',(-10.835993948661,2.71964012483391,134.902255278717));
#75424=CARTESIAN_POINT('Ctrl Pts',(-10.843750989546,2.83365312509364,134.826588538623));
#75425=CARTESIAN_POINT('Ctrl Pts',(-10.851508030431,2.94462506559323,134.746080936621));
#75426=CARTESIAN_POINT('Ctrl Pts',(-10.859265071316,3.05212174296428,134.661008894065));
#75427=CARTESIAN_POINT('Ctrl Pts',(-10.8670162625561,3.15953735625457,134.576001004999));
#75428=CARTESIAN_POINT('Ctrl Pts',(-10.8747674537962,3.26348261747135,134.48643576827));
#75429=CARTESIAN_POINT('Ctrl Pts',(-10.8825186450363,3.36355297698243,134.392632406817));
#75430=CARTESIAN_POINT('Ctrl Pts',(-10.8902665418134,3.46358080392139,134.298868914294));
#75431=CARTESIAN_POINT('Ctrl Pts',(-10.8980144385905,3.55973672014155,134.200871146544));
#75432=CARTESIAN_POINT('Ctrl Pts',(-10.9057623353676,3.65165008372901,134.098997885689));
#75433=CARTESIAN_POINT('Ctrl Pts',(-10.9135086114517,3.74354422102235,133.997145934523));
#75434=CARTESIAN_POINT('Ctrl Pts',(-10.9212548875358,3.83119730913693,133.891420392813));
#75435=CARTESIAN_POINT('Ctrl Pts',(-10.9290011636199,3.91427662947989,133.782215807196));
#75436=CARTESIAN_POINT('Ctrl Pts',(-10.9367474968852,3.99735656309551,133.673010415456));
#75437=CARTESIAN_POINT('Ctrl Pts',(-10.9444938301506,4.07586242485096,133.560326239718));
#75438=CARTESIAN_POINT('Ctrl Pts',(-10.952240163416,4.14950299840011,133.444589382042));
#75439=CARTESIAN_POINT('Ctrl Pts',(-10.959988231419,4.22316006324523,133.328826605899));
#75440=CARTESIAN_POINT('Ctrl Pts',(-10.9677362994219,4.29194946197168,133.210010117272));
#75441=CARTESIAN_POINT('Ctrl Pts',(-10.9754843674249,4.35562458037932,133.088593000073));
#75442=CARTESIAN_POINT('Ctrl Pts',(-10.9832406701668,4.41936737346037,132.967046839318));
#75443=CARTESIAN_POINT('Ctrl Pts',(-10.9909969729087,4.47798484632053,132.84289487544));
#75444=CARTESIAN_POINT('Ctrl Pts',(-10.9987532756505,4.53127721328623,132.716613184267));
#75445=CARTESIAN_POINT('Ctrl Pts',(-11.0065137181647,4.58459802399285,132.590264092752));
#75446=CARTESIAN_POINT('Ctrl Pts',(-11.0142741606788,4.63258792880767,132.461783375043));
#75447=CARTESIAN_POINT('Ctrl Pts',(-11.0220346031929,4.67509654033431,132.33166392767));
#75448=CARTESIAN_POINT('Ctrl Pts',(-11.0298075034584,4.71767339045786,132.201335601008));
#75449=CARTESIAN_POINT('Ctrl Pts',(-11.0375804037239,4.75475125816114,132.069363664444));
#75450=CARTESIAN_POINT('Ctrl Pts',(-11.0453533039893,4.78623034561037,131.936253784459));
#75451=CARTESIAN_POINT('Ctrl Pts',(-11.0528436397513,4.8165650889399,131.807982783894));
#75452=CARTESIAN_POINT('Ctrl Pts',(-11.0603339755134,4.84170098562771,131.678655440099));
#75453=CARTESIAN_POINT('Ctrl Pts',(-11.0678243112754,4.86159436971924,131.548728300109));
#75454=CARTESIAN_POINT('Ctrl Pts',(-11.0755986453945,4.88224201751497,131.413874933116));
#75455=CARTESIAN_POINT('Ctrl Pts',(-11.0833729795136,4.89730717096693,131.27794821461));
#75456=CARTESIAN_POINT('Ctrl Pts',(-11.0911473136327,4.9066845991462,131.141450081954));
#75457=CARTESIAN_POINT('Ctrl Pts',(-11.0989120665797,4.91605047048332,131.005120171048));
#75458=CARTESIAN_POINT('Ctrl Pts',(-11.1066768195268,4.91974253704958,130.868220633476));
#75459=CARTESIAN_POINT('Ctrl Pts',(-11.1144415724739,4.91770675521032,130.731262517326));
#75460=CARTESIAN_POINT('Ctrl Pts',(-11.1221986133589,4.91567299533828,130.594440429907));
#75461=CARTESIAN_POINT('Ctrl Pts',(-11.129955654244,4.90792271416036,130.457560268086));
#75462=CARTESIAN_POINT('Ctrl Pts',(-11.137712695129,4.89445377526414,130.321136751948));
#75463=CARTESIAN_POINT('Ctrl Pts',(-11.1454638863691,4.88099499339952,130.184816113845));
#75464=CARTESIAN_POINT('Ctrl Pts',(-11.1532150776092,4.86182617581237,130.048951823496));
#75465=CARTESIAN_POINT('Ctrl Pts',(-11.1609662688493,4.83699722484215,129.914056787759));
#75466=CARTESIAN_POINT('Ctrl Pts',(-11.1687141656264,4.81217882683846,129.779219086011));
#75467=CARTESIAN_POINT('Ctrl Pts',(-11.1764620624034,4.78170515084539,129.64535020322));
#75468=CARTESIAN_POINT('Ctrl Pts',(-11.1842099591805,4.74567770941459,129.512955901427));
#75469=CARTESIAN_POINT('Ctrl Pts',(-11.1919562352646,4.70965780414793,129.380589293668));
#75470=CARTESIAN_POINT('Ctrl Pts',(-11.1997025113488,4.6680865467765,129.249697030389));
#75471=CARTESIAN_POINT('Ctrl Pts',(-11.2074487874329,4.62111603803288,129.12077229926));
#75472=CARTESIAN_POINT('Ctrl Pts',(-11.2151951206982,4.57414518256363,128.991846616438));
#75473=CARTESIAN_POINT('Ctrl Pts',(-11.2229414539635,4.52177513002539,128.864888862092));
#75474=CARTESIAN_POINT('Ctrl Pts',(-11.2306877872288,4.46420696259896,128.740374363352));
#75475=CARTESIAN_POINT('Ctrl Pts',(-11.2384358552318,4.40662590318075,128.615831980454));
#75476=CARTESIAN_POINT('Ctrl Pts',(-11.2461839232347,4.34384457652693,128.493734296732));
#75477=CARTESIAN_POINT('Ctrl Pts',(-11.2539319912377,4.27611087396772,128.37453369862));
#75478=CARTESIAN_POINT('Ctrl Pts',(-11.2616882939795,4.20830518322311,128.255206412693));
#75479=CARTESIAN_POINT('Ctrl Pts',(-11.2694445967213,4.13553679573822,128.138782703586));
#75480=CARTESIAN_POINT('Ctrl Pts',(-11.2772008994632,4.05809825855412,128.025687987258));
#75481=CARTESIAN_POINT('Ctrl Pts',(-11.2849613419773,3.98061839009098,127.912532908875));
#75482=CARTESIAN_POINT('Ctrl Pts',(-11.2927217844916,3.89846363929077,127.802710676572));
#75483=CARTESIAN_POINT('Ctrl Pts',(-11.3004822270057,3.81196740590188,127.696614238139));
#75484=CARTESIAN_POINT('Ctrl Pts',(-11.3082551272712,3.72533232108038,127.590347484284));
#75485=CARTESIAN_POINT('Ctrl Pts',(-11.3160280275365,3.63434208638075,127.487818768779));
#75486=CARTESIAN_POINT('Ctrl Pts',(-11.323800927802,3.53936819016689,127.389385379452));
#75487=CARTESIAN_POINT('Ctrl Pts',(-11.331291263564,3.44784683430444,127.294530291765));
#75488=CARTESIAN_POINT('Ctrl Pts',(-11.3387815993262,3.35262664336714,127.203478161678));
#75489=CARTESIAN_POINT('Ctrl Pts',(-11.3462719350883,3.25406812078933,127.11651250142));
#75490=CARTESIAN_POINT('Ctrl Pts',(-11.3540462692074,3.15177272187264,127.026249511721));
#75491=CARTESIAN_POINT('Ctrl Pts',(-11.3618206033265,3.0455568073762,126.940103059907));
#75492=CARTESIAN_POINT('Ctrl Pts',(-11.3695949374456,2.93578579153237,126.858432989145));
#75493=CARTESIAN_POINT('Ctrl Pts',(-11.3773596903927,2.8261500586549,126.776863569446));
#75494=CARTESIAN_POINT('Ctrl Pts',(-11.3851244433398,2.71296825266145,126.699759785264));
#75495=CARTESIAN_POINT('Ctrl Pts',(-11.3928891962869,2.59664112087787,126.627443339014));
#75496=CARTESIAN_POINT('Ctrl Pts',(-11.4006462371719,2.4804295268415,126.555198718478));
#75497=CARTESIAN_POINT('Ctrl Pts',(-11.4084032780569,2.36107915376604,126.487732178585));
#75498=CARTESIAN_POINT('Ctrl Pts',(-11.4161603189419,2.23902189545369,126.425323735536));
#75499=CARTESIAN_POINT('Ctrl Pts',(-11.423911510182,2.11705668147029,126.36296235518));
#75500=CARTESIAN_POINT('Ctrl Pts',(-11.4316627014221,1.99238899199366,126.305651656702));
#75501=CARTESIAN_POINT('Ctrl Pts',(-11.4394138926622,1.8654773235228,126.253626894536));
#75502=CARTESIAN_POINT('Ctrl Pts',(-11.4471617894393,1.73861959589566,126.201624244281));
#75503=CARTESIAN_POINT('Ctrl Pts',(-11.4549096862163,1.60952014720512,126.154903209876));
#75504=CARTESIAN_POINT('Ctrl Pts',(-11.4626575829934,1.47865935939255,126.113651762672));
#75505=CARTESIAN_POINT('Ctrl Pts',(-11.4704038590775,1.34782594483594,126.072408944382));
#75506=CARTESIAN_POINT('Ctrl Pts',(-11.4781501351616,1.21523229663418,126.036633555044));
#75507=CARTESIAN_POINT('Ctrl Pts',(-11.4858964112457,1.08137556170259,126.006464207987));
#75508=CARTESIAN_POINT('Ctrl Pts',(-11.493642744511,0.947517838670995,125.976294638227));
#75509=CARTESIAN_POINT('Ctrl Pts',(-11.5013890777764,0.812397391702526,
125.951731279284));
#75510=CARTESIAN_POINT('Ctrl Pts',(-11.5091354110417,0.676522816804156,
125.932861880951));
#75511=CARTESIAN_POINT('Ctrl Pts',(-11.5168834790447,0.540617813736641,
125.913988256946));
#75512=CARTESIAN_POINT('Ctrl Pts',(-11.5246315470477,0.403958733858847,
125.900811184666));
#75513=CARTESIAN_POINT('Ctrl Pts',(-11.5323796150507,0.267060174009044,
125.893366632031));
#75514=CARTESIAN_POINT('Ctrl Pts',(-11.5401359177926,0.130016116740718,
125.885914167237));
#75515=CARTESIAN_POINT('Ctrl Pts',(-11.5478922205344,-0.00726753792415963,
125.884206413957));
#75516=CARTESIAN_POINT('Ctrl Pts',(-11.5556485232763,-0.144274746668937,
125.888227191796));
#75517=CARTESIAN_POINT('Ctrl Pts',(-11.5634089657904,-0.28135508028623,
125.892250115645));
#75518=CARTESIAN_POINT('Ctrl Pts',(-11.5711694083046,-0.418158284198805,
125.90200763512));
#75519=CARTESIAN_POINT('Ctrl Pts',(-11.5789298508187,-0.554173549594789,
125.917431649448));
#75520=CARTESIAN_POINT('Ctrl Pts',(-11.5867027510842,-0.690407158769655,
125.932880423773));
#75521=CARTESIAN_POINT('Ctrl Pts',(-11.5944756513496,-0.825849915303424,
125.95401381007));
#75522=CARTESIAN_POINT('Ctrl Pts',(-11.602248551615,-0.960000424292672,
125.980712387455));
#75523=CARTESIAN_POINT('Ctrl Pts',(-11.6097388873771,-1.08927422437524,
126.006440404302));
#75524=CARTESIAN_POINT('Ctrl Pts',(-11.6172292231391,-1.21734779923011,
126.037335947329));
#75525=CARTESIAN_POINT('Ctrl Pts',(-11.6247195589011,-1.34378776107863,
126.073248960072));
#75526=CARTESIAN_POINT('Ctrl Pts',(-11.6324938930202,-1.47502173251142,
126.110523625609));
#75527=CARTESIAN_POINT('Ctrl Pts',(-11.6402682271393,-1.60491147846995,
126.153321821216));
#75528=CARTESIAN_POINT('Ctrl Pts',(-11.6480425612584,-1.73295673738869,
126.201530617573));
#75529=CARTESIAN_POINT('Ctrl Pts',(-11.6558073142055,-1.8608441919692,126.249680000896));
#75530=CARTESIAN_POINT('Ctrl Pts',(-11.6635720671526,-1.98689132005251,
126.303226581038));
#75531=CARTESIAN_POINT('Ctrl Pts',(-11.6713368200997,-2.11061085056714,
126.362007085938));
#75532=CARTESIAN_POINT('Ctrl Pts',(-11.6790938609846,-2.23420750109993,
126.420729209211));
#75533=CARTESIAN_POINT('Ctrl Pts',(-11.6868509018696,-2.35548080380598,
126.484674745483));
#75534=CARTESIAN_POINT('Ctrl Pts',(-11.6946079427546,-2.47396172397353,
126.553631685863));
#75535=CARTESIAN_POINT('Ctrl Pts',(-11.7023591339947,-2.5923532967577,126.622536625278));
#75536=CARTESIAN_POINT('Ctrl Pts',(-11.7101103252348,-2.70795634185086,
126.696445250789));
#75537=CARTESIAN_POINT('Ctrl Pts',(-11.717861516475,-2.82032510447822,126.775098977073));
#75538=CARTESIAN_POINT('Ctrl Pts',(-11.725609413252,-2.93264610738423,126.853719273425));
#75539=CARTESIAN_POINT('Ctrl Pts',(-11.7333573100291,-3.04173524228455,
126.937080435574));
#75540=CARTESIAN_POINT('Ctrl Pts',(-11.7411052068062,-3.14717470538423,
127.024879907695));
#75541=CARTESIAN_POINT('Ctrl Pts',(-11.7488514828903,-3.25259211282109,
127.112661014058));
#75542=CARTESIAN_POINT('Ctrl Pts',(-11.7565977589744,-3.35436106671577,
127.204878333738));
#75543=CARTESIAN_POINT('Ctrl Pts',(-11.7643440350585,-3.4520962276984,127.301188526844));
#75544=CARTESIAN_POINT('Ctrl Pts',(-11.7720903683238,-3.54983211013938,
127.39749943089));
#75545=CARTESIAN_POINT('Ctrl Pts',(-11.7798367015891,-3.64353386177464,
127.497902994233));
#75546=CARTESIAN_POINT('Ctrl Pts',(-11.7875830348545,-3.73285274765514,
127.602018751552));
#75547=CARTESIAN_POINT('Ctrl Pts',(-11.7953311028574,-3.82219163588085,
127.706157824874));
#75548=CARTESIAN_POINT('Ctrl Pts',(-11.8030791708604,-3.90714545074154,
127.814010449726));
#75549=CARTESIAN_POINT('Ctrl Pts',(-11.8108272388633,-3.98740577924582,
127.925163122753));
#75550=CARTESIAN_POINT('Ctrl Pts',(-11.8185835416052,-4.06775140938267,
128.036433930165));
#75551=CARTESIAN_POINT('Ctrl Pts',(-11.8263398443471,-4.1433933592699,128.151011474547));
#75552=CARTESIAN_POINT('Ctrl Pts',(-11.8340961470889,-4.21406630791313,
128.268452848145));
#75553=CARTESIAN_POINT('Ctrl Pts',(-11.8418565896031,-4.28477697683697,
128.38595690374));
#75554=CARTESIAN_POINT('Ctrl Pts',(-11.8496170321173,-4.35051317267441,
128.506327491276));
#75555=CARTESIAN_POINT('Ctrl Pts',(-11.8573774746314,-4.41105608589379,
128.629098042703));
#75556=CARTESIAN_POINT('Ctrl Pts',(-11.8651503748969,-4.47169618797222,
128.752065676318));
#75557=CARTESIAN_POINT('Ctrl Pts',(-11.8729232751623,-4.52712618983217,
128.877440614833));
#75558=CARTESIAN_POINT('Ctrl Pts',(-11.8806961754277,-4.57717554745248,
129.004736470611));
#75559=CARTESIAN_POINT('Ctrl Pts',(-11.8881865111899,-4.62540548485745,
129.127404801395));
#75560=CARTESIAN_POINT('Ctrl Pts',(-11.895676846952,-4.66863908508204,129.251856522827));
#75561=CARTESIAN_POINT('Ctrl Pts',(-11.9031671827142,-4.70676833819968,
129.37764590431));
#75562=CARTESIAN_POINT('Ctrl Pts',(-11.9072067063095,-4.72733137068994,
129.445483874553));
#75563=CARTESIAN_POINT('Ctrl Pts',(-11.9112462299048,-4.74643299116131,
129.513784013706));
#75564=CARTESIAN_POINT('Ctrl Pts',(-11.9152857535001,-4.76405452823405,
129.582490119308));
#75565=CARTESIAN_POINT('Ctrl Pts',(-10.1650489208495,-4.76405452823411,
129.582490119308));
#75566=CARTESIAN_POINT('Ctrl Pts',(-10.1728097116723,-4.79812258470992,
129.715320954453));
#75567=CARTESIAN_POINT('Ctrl Pts',(-10.1805705024952,-4.82660344262438,
129.849469839351));
#75568=CARTESIAN_POINT('Ctrl Pts',(-10.188331293318,-4.84942182258588,129.984427053716));
#75569=CARTESIAN_POINT('Ctrl Pts',(-10.1961043814061,-4.87227635912964,
130.119598112869));
#75570=CARTESIAN_POINT('Ctrl Pts',(-10.2038774694941,-4.88945044079769,
130.255579672805));
#75571=CARTESIAN_POINT('Ctrl Pts',(-10.2116505575822,-4.90092071191022,
130.39185699568));
#75572=CARTESIAN_POINT('Ctrl Pts',(-10.2185941850004,-4.91116699859684,
130.513592262907));
#75573=CARTESIAN_POINT('Ctrl Pts',(-10.2255378124186,-4.91686255298458,
130.635563317364));
#75574=CARTESIAN_POINT('Ctrl Pts',(-10.2324814398368,-4.91802585029017,
130.757405336951));
#75575=CARTESIAN_POINT('Ctrl Pts',(-10.2333678145608,-4.91817434865651,
130.7729588337));
#75576=CARTESIAN_POINT('Ctrl Pts',(-10.2342541892847,-4.91824906423311,
130.788513036023));
#75577=CARTESIAN_POINT('Ctrl Pts',(-10.2351405640087,-4.91824999126505,
130.804067494219));
#75578=CARTESIAN_POINT('',(-9.88985943603245,-4.91824816614036,130.808607823354));
#75579=CARTESIAN_POINT('Ctrl Pts',(-9.81992175947747,-4.76405452823407,
129.582490119308));
#75580=CARTESIAN_POINT('Ctrl Pts',(-9.82762241378884,-4.79796140031408,
129.71469249894));
#75581=CARTESIAN_POINT('Ctrl Pts',(-9.83532306810017,-4.8263664037375,129.848327831717));
#75582=CARTESIAN_POINT('Ctrl Pts',(-9.84302372241154,-4.84916272078742,
129.982896090136));
#75583=CARTESIAN_POINT('Ctrl Pts',(-9.85082967467481,-4.87227075232277,
130.119304421026));
#75584=CARTESIAN_POINT('Ctrl Pts',(-9.85863562693807,-4.8896154804548,130.256670973928));
#75585=CARTESIAN_POINT('Ctrl Pts',(-9.86644157920134,-4.90113965557734,
130.394466559269));
#75586=CARTESIAN_POINT('Ctrl Pts',(-9.8742475314646,-4.91266383069989,130.53226214461));
#75587=CARTESIAN_POINT('Ctrl Pts',(-9.88205348372789,-4.9183674424039,130.670486339544));
#75588=CARTESIAN_POINT('Ctrl Pts',(-9.88985943599116,-4.91824816614099,
130.808607822623));
#75589=CARTESIAN_POINT('Ctrl Pts',(-9.88985943603245,-4.91824816614036,
130.808607823354));
#75590=CARTESIAN_POINT('Ctrl Pts',(-9.89918713811298,-4.91810563725986,
130.97365572547));
#75591=CARTESIAN_POINT('Ctrl Pts',(-9.90851484019353,-4.90965128715922,
131.138340451495));
#75592=CARTESIAN_POINT('Ctrl Pts',(-9.917842542274,-4.8930171587382,131.301920811707));
#75593=CARTESIAN_POINT('Ctrl Pts',(-9.92729244968566,-4.87616510106139,
131.467644292692));
#75594=CARTESIAN_POINT('Ctrl Pts',(-9.93674235709729,-4.85091759043832,
131.632234271229));
#75595=CARTESIAN_POINT('Ctrl Pts',(-9.94619226450897,-4.81746108250809,
131.794942154351));
#75596=CARTESIAN_POINT('Ctrl Pts',(-9.95533578040038,-4.78508932492308,
131.952374608467));
#75597=CARTESIAN_POINT('Ctrl Pts',(-9.96447929629182,-4.74503259162011,
132.108045180952));
#75598=CARTESIAN_POINT('Ctrl Pts',(-9.97362281218324,-4.69750201318969,
132.261295035643));
#75599=CARTESIAN_POINT('Ctrl Pts',(-9.9813971463023,-4.65708882837325,132.39159672574));
#75600=CARTESIAN_POINT('Ctrl Pts',(-9.98917148042137,-4.61118596183109,
132.520422027973));
#75601=CARTESIAN_POINT('Ctrl Pts',(-9.99694581454045,-4.55991831526217,
132.647273534835));
#75602=CARTESIAN_POINT('Ctrl Pts',(-10.0047105674876,-4.50871385148572,
132.773968708551));
#75603=CARTESIAN_POINT('Ctrl Pts',(-10.0124753204347,-4.45215790791144,
132.898694567897));
#75604=CARTESIAN_POINT('Ctrl Pts',(-10.0202400733818,-4.39042540274467,
133.020967900202));
#75605=CARTESIAN_POINT('Ctrl Pts',(-10.0279971142668,-4.32875421117238,
133.143119788909));
#75606=CARTESIAN_POINT('Ctrl Pts',(-10.0357541551517,-4.26191686475718,
133.262823651347));
#75607=CARTESIAN_POINT('Ctrl Pts',(-10.0435111960367,-4.1901365668757,133.379615675503));
#75608=CARTESIAN_POINT('Ctrl Pts',(-10.0512623872769,-4.11841039907512,
133.496319625885));
#75609=CARTESIAN_POINT('Ctrl Pts',(-10.0590135785171,-4.04174890309284,
133.610115776934));
#75610=CARTESIAN_POINT('Ctrl Pts',(-10.0667647697572,-3.96042128667038,
133.720564707576));
#75611=CARTESIAN_POINT('Ctrl Pts',(-10.0745126665343,-3.87912823665439,
133.830966694475));
#75612=CARTESIAN_POINT('Ctrl Pts',(-10.0822605633113,-3.7931732420146,133.93802397636));
#75613=CARTESIAN_POINT('Ctrl Pts',(-10.0900084600884,-3.70286879758693,
134.041326130258));
#75614=CARTESIAN_POINT('Ctrl Pts',(-10.0977547361725,-3.6125832429023,134.144606675572));
#75615=CARTESIAN_POINT('Ctrl Pts',(-10.1055010122566,-3.51795030524627,
134.244133361121));
#75616=CARTESIAN_POINT('Ctrl Pts',(-10.1132472883407,-3.41932247271796,
134.339529197714));
#75617=CARTESIAN_POINT('Ctrl Pts',(-10.1209936216061,-3.32069391214139,
134.434925738497));
#75618=CARTESIAN_POINT('Ctrl Pts',(-10.1287399548715,-3.21807067886883,
134.526191097666));
#75619=CARTESIAN_POINT('Ctrl Pts',(-10.1364862881368,-3.11184149733245,
134.612985770817));
#75620=CARTESIAN_POINT('Ctrl Pts',(-10.1442343561398,-3.0055885265074,134.699799881034));
#75621=CARTESIAN_POINT('Ctrl Pts',(-10.1519824241428,-2.89572830323321,
134.782141065681));
#75622=CARTESIAN_POINT('Ctrl Pts',(-10.1597304921458,-2.78268161284683,
134.859710923523));
#75623=CARTESIAN_POINT('Ctrl Pts',(-10.1674867948876,-2.66951477509264,
134.937363223533));
#75624=CARTESIAN_POINT('Ctrl Pts',(-10.1752430976295,-2.55315502798265,
135.010233845267));
#75625=CARTESIAN_POINT('Ctrl Pts',(-10.1829994003714,-2.434051518698,135.078068172702));
#75626=CARTESIAN_POINT('Ctrl Pts',(-10.1907598428855,-2.31488444028432,
135.14593870536));
#75627=CARTESIAN_POINT('Ctrl Pts',(-10.1985202853997,-2.19297102905751,
135.208767408594));
#75628=CARTESIAN_POINT('Ctrl Pts',(-10.2062807279139,-2.06878296953405,
135.266346732231));
#75629=CARTESIAN_POINT('Ctrl Pts',(-10.2140536281793,-1.94439555231255,
135.324018487311));
#75630=CARTESIAN_POINT('Ctrl Pts',(-10.2218265284447,-1.81772655147486,
135.376423873872));
#75631=CARTESIAN_POINT('Ctrl Pts',(-10.2295994287101,-1.68926630717658,
135.423404068968));
#75632=CARTESIAN_POINT('Ctrl Pts',(-10.2370897644721,-1.56547591633106,
135.468676415636));
#75633=CARTESIAN_POINT('Ctrl Pts',(-10.2445801002341,-1.4400225467258,135.508911067488));
#75634=CARTESIAN_POINT('Ctrl Pts',(-10.2520704359961,-1.31335439253887,
135.544010742005));
#75635=CARTESIAN_POINT('Ctrl Pts',(-10.2598447701152,-1.18188357678526,
135.580441231351));
#75636=CARTESIAN_POINT('Ctrl Pts',(-10.2676191042343,-1.0486875808879,135.611455072283));
#75637=CARTESIAN_POINT('Ctrl Pts',(-10.2753934383534,-0.914252400291646,
135.636888487228));
#75638=CARTESIAN_POINT('Ctrl Pts',(-10.2831581913005,-0.779982899040659,
135.662290557763));
#75639=CARTESIAN_POINT('Ctrl Pts',(-10.2909229442476,-0.644477632195641,
135.682125814261));
#75640=CARTESIAN_POINT('Ctrl Pts',(-10.2986876971947,-0.508237687823909,
135.696280232112));
#75641=CARTESIAN_POINT('Ctrl Pts',(-10.3064447380797,-0.372133058885759,
135.710420591595));
#75642=CARTESIAN_POINT('Ctrl Pts',(-10.3142017789646,-0.235295590896812,
135.718891300701));
#75643=CARTESIAN_POINT('Ctrl Pts',(-10.3219588198496,-0.0982361489162156,
135.72162944503));
#75644=CARTESIAN_POINT('Ctrl Pts',(-10.3297100110897,0.0387199354732024,
135.724365524503));
#75645=CARTESIAN_POINT('Ctrl Pts',(-10.3374612023299,0.175897271364438,
135.721377636034));
#75646=CARTESIAN_POINT('Ctrl Pts',(-10.34521239357,0.312780648003097,135.712654753896));
#75647=CARTESIAN_POINT('Ctrl Pts',(-10.3529602903471,0.449605845555201,
135.703935579217));
#75648=CARTESIAN_POINT('Ctrl Pts',(-10.3607081871242,0.586136942994985,
135.689486283733));
#75649=CARTESIAN_POINT('Ctrl Pts',(-10.3684560839013,0.721859728760213,
135.669347934558));
#75650=CARTESIAN_POINT('Ctrl Pts',(-10.3762023599854,0.857554124244504,
135.649213797892));
#75651=CARTESIAN_POINT('Ctrl Pts',(-10.3839486360695,0.992440157880172,
135.623393031912));
#75652=CARTESIAN_POINT('Ctrl Pts',(-10.3916949121536,1.12601012955639,135.591978422972));
#75653=CARTESIAN_POINT('Ctrl Pts',(-10.399441245419,1.25958108721579,135.560563582136));
#75654=CARTESIAN_POINT('Ctrl Pts',(-10.4071875786843,1.39183558294953,135.523554905454));
#75655=CARTESIAN_POINT('Ctrl Pts',(-10.4149339119496,1.52227786703708,135.481095927377));
#75656=CARTESIAN_POINT('Ctrl Pts',(-10.4226819799526,1.65274936276972,135.438627440906));
#75657=CARTESIAN_POINT('Ctrl Pts',(-10.4304300479556,1.78140746760162,135.390706345259));
#75658=CARTESIAN_POINT('Ctrl Pts',(-10.4381781159586,1.90777368336913,135.337525365901));
#75659=CARTESIAN_POINT('Ctrl Pts',(-10.4459344187005,2.03427420265453,135.284287865165));
#75660=CARTESIAN_POINT('Ctrl Pts',(-10.4536907214424,2.1584776060805,135.225779465453));
#75661=CARTESIAN_POINT('Ctrl Pts',(-10.4614470241842,2.27992690295286,135.162240420829));
#75662=CARTESIAN_POINT('Ctrl Pts',(-10.4692074666984,2.40144102097172,135.098667463505));
#75663=CARTESIAN_POINT('Ctrl Pts',(-10.4769679092126,2.52019776507275,135.030058706647));
#75664=CARTESIAN_POINT('Ctrl Pts',(-10.4847283517267,2.63576756041445,134.95669880586));
#75665=CARTESIAN_POINT('Ctrl Pts',(-10.4925012519922,2.75152287865143,134.883221141248));
#75666=CARTESIAN_POINT('Ctrl Pts',(-10.5002741522576,2.86408070357802,134.8049773149));
#75667=CARTESIAN_POINT('Ctrl Pts',(-10.508047052523,2.97304237211987,134.722294016193));
#75668=CARTESIAN_POINT('Ctrl Pts',(-10.5155373882851,3.07804300955293,134.642616463661));
#75669=CARTESIAN_POINT('Ctrl Pts',(-10.5230277240471,3.17970417230188,134.558816802899));
#75670=CARTESIAN_POINT('Ctrl Pts',(-10.5305180598092,3.2777017539289,134.471219528786));
#75671=CARTESIAN_POINT('Ctrl Pts',(-10.5382923939283,3.37941494364846,134.380300977401));
#75672=CARTESIAN_POINT('Ctrl Pts',(-10.5460667280474,3.47750345565743,134.285003152324));
#75673=CARTESIAN_POINT('Ctrl Pts',(-10.5538410621665,3.57156680683667,134.18564640951));
#75674=CARTESIAN_POINT('Ctrl Pts',(-10.5616058151136,3.66551423334227,134.086412115002));
#75675=CARTESIAN_POINT('Ctrl Pts',(-10.5693705680606,3.7554461030277,133.983129136937));
#75676=CARTESIAN_POINT('Ctrl Pts',(-10.5771353210077,3.84099563341799,133.87615742181));
#75677=CARTESIAN_POINT('Ctrl Pts',(-10.5848923618927,3.92646019480855,133.769291952499));
#75678=CARTESIAN_POINT('Ctrl Pts',(-10.5926494027778,4.00755083617129,133.658745340422));
#75679=CARTESIAN_POINT('Ctrl Pts',(-10.6004064436628,4.08393849079674,133.544913384051));
#75680=CARTESIAN_POINT('Ctrl Pts',(-10.6081576349029,4.16026854089763,133.431167269244));
#75681=CARTESIAN_POINT('Ctrl Pts',(-10.615908826143,4.23190244649904,133.314141064794));
#75682=CARTESIAN_POINT('Ctrl Pts',(-10.6236600173831,4.29855244734754,133.194262272426));
#75683=CARTESIAN_POINT('Ctrl Pts',(-10.6314079141602,4.36517412016782,133.074434431742));
#75684=CARTESIAN_POINT('Ctrl Pts',(-10.6391558109372,4.42681591177529,132.951756755552));
#75685=CARTESIAN_POINT('Ctrl Pts',(-10.6469037077143,4.48323442918648,132.826684062383));
#75686=CARTESIAN_POINT('Ctrl Pts',(-10.6546499837984,4.53964114506006,132.701637531726));
#75687=CARTESIAN_POINT('Ctrl Pts',(-10.6623962598826,4.59082659931321,132.574197336737));
#75688=CARTESIAN_POINT('Ctrl Pts',(-10.6701425359667,4.63659443142271,132.444840773191));
#75689=CARTESIAN_POINT('Ctrl Pts',(-10.6778888692321,4.68236260137988,132.315483254765));
#75690=CARTESIAN_POINT('Ctrl Pts',(-10.6856352024974,4.72271293898669,132.184209708128));
#75691=CARTESIAN_POINT('Ctrl Pts',(-10.6933815357627,4.7574982390087,132.051514805439));
#75692=CARTESIAN_POINT('Ctrl Pts',(-10.7011296037657,4.79229132895751,131.918790186646));
#75693=CARTESIAN_POINT('Ctrl Pts',(-10.7088776717687,4.8215168023044,131.784643956529));
#75694=CARTESIAN_POINT('Ctrl Pts',(-10.7166257397716,4.84507816449548,131.649582861966));
#75695=CARTESIAN_POINT('Ctrl Pts',(-10.7243820425135,4.86866456798266,131.514378222865));
#75696=CARTESIAN_POINT('Ctrl Pts',(-10.7321383452553,4.88657476764966,131.378257162748));
#75697=CARTESIAN_POINT('Ctrl Pts',(-10.7398946479972,4.89876388141197,131.24173402402));
#75698=CARTESIAN_POINT('Ctrl Pts',(-10.7476550905113,4.91095950087132,131.105138018783));
#75699=CARTESIAN_POINT('Ctrl Pts',(-10.7554155330256,4.91742793160717,130.968139897661));
#75700=CARTESIAN_POINT('Ctrl Pts',(-10.7631759755397,4.91817646674643,130.831254937443));
#75701=CARTESIAN_POINT('Ctrl Pts',(-10.7709488758052,4.91892620350074,130.694150237335));
#75702=CARTESIAN_POINT('Ctrl Pts',(-10.7787217760706,4.9139377101641,130.557159452068));
#75703=CARTESIAN_POINT('Ctrl Pts',(-10.7864946763361,4.90327035263295,130.420794571766));
#75704=CARTESIAN_POINT('Ctrl Pts',(-10.7939850120981,4.89299078041754,130.289386898346));
#75705=CARTESIAN_POINT('Ctrl Pts',(-10.8014753478601,4.87743809416649,130.15856071937));
#75706=CARTESIAN_POINT('Ctrl Pts',(-10.8089656836221,4.85671011316516,130.028764112172));
#75707=CARTESIAN_POINT('Ctrl Pts',(-10.8167400177412,4.83519622446397,129.894046227161));
#75708=CARTESIAN_POINT('Ctrl Pts',(-10.8245143518603,4.80803870193853,129.760010781764));
#75709=CARTESIAN_POINT('Ctrl Pts',(-10.8322886859794,4.77529059921724,129.62716787399));
#75710=CARTESIAN_POINT('Ctrl Pts',(-10.8400534389265,4.74258285560577,129.494488683227));
#75711=CARTESIAN_POINT('Ctrl Pts',(-10.8478181918735,4.70429833330681,129.362999481787));
#75712=CARTESIAN_POINT('Ctrl Pts',(-10.8555829448206,4.66054161061392,129.233203414026));
#75713=CARTESIAN_POINT('Ctrl Pts',(-10.8633399857056,4.61682834771493,129.103536261549));
#75714=CARTESIAN_POINT('Ctrl Pts',(-10.8710970265906,4.5676538245372,128.975559264285));
#75715=CARTESIAN_POINT('Ctrl Pts',(-10.8788540674756,4.51317316895114,128.84976321412));
#75716=CARTESIAN_POINT('Ctrl Pts',(-10.8866052587158,4.45873359765126,128.724062027734));
#75717=CARTESIAN_POINT('Ctrl Pts',(-10.8943564499558,4.39899601322621,128.600538872145));
#75718=CARTESIAN_POINT('Ctrl Pts',(-10.902107641196,4.33416454353856,128.479666923327));
#75719=CARTESIAN_POINT('Ctrl Pts',(-10.909855537973,4.26936062895496,128.358846348313));
#75720=CARTESIAN_POINT('Ctrl Pts',(-10.9176034347501,4.19946731961193,128.240675082697));
#75721=CARTESIAN_POINT('Ctrl Pts',(-10.9253513315272,4.12473570736615,128.125603740416));
#75722=CARTESIAN_POINT('Ctrl Pts',(-10.9330976076113,4.05001972736262,128.010556468579));
#75723=CARTESIAN_POINT('Ctrl Pts',(-10.9408438836954,3.97046767032323,127.898608157977));
#75724=CARTESIAN_POINT('Ctrl Pts',(-10.9485901597795,3.88637496104045,127.790182002305));
#75725=CARTESIAN_POINT('Ctrl Pts',(-10.9563364930448,3.8022816310044,127.681755046255));
#75726=CARTESIAN_POINT('Ctrl Pts',(-10.9640828263102,3.71364782144745,127.576850605954));
#75727=CARTESIAN_POINT('Ctrl Pts',(-10.9718291595755,3.6208101460403,127.475859911718));
#75728=CARTESIAN_POINT('Ctrl Pts',(-10.9795772275785,3.52795168027945,127.374846601316));
#75729=CARTESIAN_POINT('Ctrl Pts',(-10.9873252955815,3.43088773987947,127.277749068799));
#75730=CARTESIAN_POINT('Ctrl Pts',(-10.9950733635845,3.32999250767726,127.184922406833));
#75731=CARTESIAN_POINT('Ctrl Pts',(-11.0028296663263,3.2289900428216,127.091997087586));
#75732=CARTESIAN_POINT('Ctrl Pts',(-11.0105859690682,3.12414844019777,127.003351971428));
#75733=CARTESIAN_POINT('Ctrl Pts',(-11.01834227181,3.01587617077401,126.919302833561));
#75734=CARTESIAN_POINT('Ctrl Pts',(-11.0261027143242,2.90754611317989,126.835208836138));
#75735=CARTESIAN_POINT('Ctrl Pts',(-11.0338631568383,2.79578205870477,126.755715931333));
#75736=CARTESIAN_POINT('Ctrl Pts',(-11.0416235993525,2.68102146641663,126.681096502922));
#75737=CARTESIAN_POINT('Ctrl Pts',(-11.0493964996179,2.56607665023778,126.60635728878));
#75738=CARTESIAN_POINT('Ctrl Pts',(-11.0571693998834,2.44812602031287,126.536507383882));
#75739=CARTESIAN_POINT('Ctrl Pts',(-11.0649423001489,2.32763241715051,126.471773585188));
#75740=CARTESIAN_POINT('Ctrl Pts',(-11.0724326359109,2.211519059968,126.409393023131));
#75741=CARTESIAN_POINT('Ctrl Pts',(-11.0799229716729,2.09304468359106,126.351763193205));
#75742=CARTESIAN_POINT('Ctrl Pts',(-11.087413307435,1.9726391418837,126.299043994019));
#75743=CARTESIAN_POINT('Ctrl Pts',(-11.095187641554,1.84766838746621,126.244325930373));
#75744=CARTESIAN_POINT('Ctrl Pts',(-11.1029619756731,1.72022126688847,126.19472489098));
#75745=CARTESIAN_POINT('Ctrl Pts',(-11.1107363097922,1.59075561683369,126.150471960753));
#75746=CARTESIAN_POINT('Ctrl Pts',(-11.1185010627393,1.4614495216221,126.106273568308));
#75747=CARTESIAN_POINT('Ctrl Pts',(-11.1262658156864,1.33013021302872,126.067410296012));
#75748=CARTESIAN_POINT('Ctrl Pts',(-11.1340305686335,1.1972775277728,126.034066120998));
#75749=CARTESIAN_POINT('Ctrl Pts',(-11.1417876095185,1.06455679367658,126.000755063888));
#75750=CARTESIAN_POINT('Ctrl Pts',(-11.1495446504035,0.930306090449464,
125.9729522899));
#75751=CARTESIAN_POINT('Ctrl Pts',(-11.1573016912885,0.795022185607245,
125.950792570563));
#75752=CARTESIAN_POINT('Ctrl Pts',(-11.1650528825286,0.65984029941039,125.928649562042));
#75753=CARTESIAN_POINT('Ctrl Pts',(-11.1728040737687,0.523627146702382,
125.912141200859));
#75754=CARTESIAN_POINT('Ctrl Pts',(-11.1805552650088,0.386891159928283,
125.901351511632));
#75755=CARTESIAN_POINT('Ctrl Pts',(-11.1883031617859,0.250213289595742,
125.890566408312));
#75756=CARTESIAN_POINT('Ctrl Pts',(-11.196051058563,0.113013416110293,125.885495173385));
#75757=CARTESIAN_POINT('Ctrl Pts',(-11.2037989553401,-0.0241936249809933,
125.886170123999));
#75758=CARTESIAN_POINT('Ctrl Pts',(-11.2115452314242,-0.161371965316938,
125.886844933429));
#75759=CARTESIAN_POINT('Ctrl Pts',(-11.2192915075083,-0.298557079563732,
125.893263535678));
#75760=CARTESIAN_POINT('Ctrl Pts',(-11.2270377835924,-0.43523323856517,
125.90540612803));
#75761=CARTESIAN_POINT('Ctrl Pts',(-11.2347841168578,-0.571910406479153,
125.917548810015));
#75762=CARTESIAN_POINT('Ctrl Pts',(-11.242530450123,-0.708078222219621,
125.935415531819));
#75763=CARTESIAN_POINT('Ctrl Pts',(-11.2502767833884,-0.843225584729596,
125.95893456037));
#75764=CARTESIAN_POINT('Ctrl Pts',(-11.2580248513914,-0.978403212554175,
125.982458855843));
#75765=CARTESIAN_POINT('Ctrl Pts',(-11.2657729193944,-1.11255954731059,
126.011637909831));
#75766=CARTESIAN_POINT('Ctrl Pts',(-11.2735209873973,-1.24519358451844,
126.046348847974));
#75767=CARTESIAN_POINT('Ctrl Pts',(-11.2812772901392,-1.37796858675939,
126.081096677316));
#75768=CARTESIAN_POINT('Ctrl Pts',(-11.2890335928811,-1.50921768065986,
126.121388036311));
#75769=CARTESIAN_POINT('Ctrl Pts',(-11.296789895623,-1.63845440706377,126.167049950976));
#75770=CARTESIAN_POINT('Ctrl Pts',(-11.3045503381372,-1.76776011099997,
126.212736236779));
#75771=CARTESIAN_POINT('Ctrl Pts',(-11.3123107806512,-1.8950509446011,126.263798644362));
#75772=CARTESIAN_POINT('Ctrl Pts',(-11.3200712231654,-2.01986128637052,
126.320016357106));
#75773=CARTESIAN_POINT('Ctrl Pts',(-11.3278441234308,-2.14487198478069,
126.376324315513));
#75774=CARTESIAN_POINT('Ctrl Pts',(-11.3356170236962,-2.26739388460155,
126.437803941228));
#75775=CARTESIAN_POINT('Ctrl Pts',(-11.3433899239617,-2.38698599852874,
126.50418842272));
#75776=CARTESIAN_POINT('Ctrl Pts',(-11.3508802597237,-2.50223063788049,
126.568159661097));
#75777=CARTESIAN_POINT('Ctrl Pts',(-11.3583705954858,-2.61475454028793,
126.63668517855));
#75778=CARTESIAN_POINT('Ctrl Pts',(-11.3658609312478,-2.72419083200988,
126.709489755952));
#75779=CARTESIAN_POINT('Ctrl Pts',(-11.3736152775995,-2.83748440607882,
126.784860463902));
#75780=CARTESIAN_POINT('Ctrl Pts',(-11.3813696239513,-2.94783205967676,
126.865059207471));
#75781=CARTESIAN_POINT('Ctrl Pts',(-11.389123970303,-3.05479306362901,126.949827909065));
#75782=CARTESIAN_POINT('Ctrl Pts',(-11.3968660482348,-3.16158484087234,
127.034462495161));
#75783=CARTESIAN_POINT('Ctrl Pts',(-11.4046081261665,-3.26500033381101,
127.123652397972));
#75784=CARTESIAN_POINT('Ctrl Pts',(-11.4123502040983,-3.36462688234458,
127.217095781357));
#75785=CARTESIAN_POINT('Ctrl Pts',(-11.4200852014054,-3.46416231603767,
127.3104537048));
#75786=CARTESIAN_POINT('Ctrl Pts',(-11.4278201987125,-3.55991541288795,
127.408057104196));
#75787=CARTESIAN_POINT('Ctrl Pts',(-11.4355551960196,-3.65150556615707,
127.509563178751));
#75788=CARTESIAN_POINT('Ctrl Pts',(-11.4432848192173,-3.74303208456201,
127.610998729073));
#75789=CARTESIAN_POINT('Ctrl Pts',(-11.4510144424151,-3.8304011512328,127.716331269275));
#75790=CARTESIAN_POINT('Ctrl Pts',(-11.4587440656128,-3.91326842645912,
127.825180649021));
#75791=CARTESIAN_POINT('Ctrl Pts',(-11.4664700171059,-3.99609633829729,
127.933978323431));
#75792=CARTESIAN_POINT('Ctrl Pts',(-11.474195968599,-4.07442647678214,128.046289200421));
#75793=CARTESIAN_POINT('Ctrl Pts',(-11.4819219200921,-4.14795456296417,
128.161699836065));
#75794=CARTESIAN_POINT('Ctrl Pts',(-11.4896475068869,-4.22147917830286,
128.277105023828));
#75795=CARTESIAN_POINT('Ctrl Pts',(-11.4973730936817,-4.29020197194233,
128.395609353431));
#75796=CARTESIAN_POINT('Ctrl Pts',(-11.5050986804765,-4.35386189480628,
128.516770255754));
#75797=CARTESIAN_POINT('Ctrl Pts',(-11.5128238147382,-4.41751808873384,
128.637924060971));
#75798=CARTESIAN_POINT('Ctrl Pts',(-11.5205489489999,-4.47611182368879,
128.761733778554));
#75799=CARTESIAN_POINT('Ctrl Pts',(-11.5282740832616,-4.52942831239543,
128.887732791051));
#75800=CARTESIAN_POINT('Ctrl Pts',(-11.536003557891,-4.58277475697797,129.013802596109));
#75801=CARTESIAN_POINT('Ctrl Pts',(-11.5437330325204,-4.63083788123895,
129.142063789657));
#75802=CARTESIAN_POINT('Ctrl Pts',(-11.5514625071497,-4.67345124333323,
129.272030190182));
#75803=CARTESIAN_POINT('Ctrl Pts',(-11.5575589388993,-4.70706147767425,
129.374537970921));
#75804=CARTESIAN_POINT('Ctrl Pts',(-11.5636553706488,-4.73728242755129,
129.47810610507));
#75805=CARTESIAN_POINT('Ctrl Pts',(-11.5697518023984,-4.76405452823402,
129.582490119308));
#75806=CARTESIAN_POINT('Origin',(213.235140564004,0.,130.804360617566));
#75807=CARTESIAN_POINT('',(-13.6653609210471,-4.76405452823398,129.582490119308));
#75808=CARTESIAN_POINT('',(-13.3199629969565,-4.76405452823408,129.582490119308));
#75809=CARTESIAN_POINT('',(213.235140564004,-4.76405452823405,129.582490119308));
#75810=CARTESIAN_POINT('',(-11.9851405639703,-4.91824811303239,130.800052351862));
#75811=CARTESIAN_POINT('Ctrl Pts',(-11.9851405640086,-4.91824811303298,
130.80005235254));
#75812=CARTESIAN_POINT('Ctrl Pts',(-11.9928382668462,-4.91836740145462,
130.936230152915));
#75813=CARTESIAN_POINT('Ctrl Pts',(-12.0005359696838,-4.91282664553037,
131.072514009752));
#75814=CARTESIAN_POINT('Ctrl Pts',(-12.0082336725213,-4.90162626731536,
131.20839402963));
#75815=CARTESIAN_POINT('Ctrl Pts',(-12.015928908627,-4.89042947826595,131.344230506702));
#75816=CARTESIAN_POINT('Ctrl Pts',(-12.0236241447325,-4.87357670326283,
131.479663009321));
#75817=CARTESIAN_POINT('Ctrl Pts',(-12.0313193808382,-4.85112042706125,
131.614183848061));
#75818=CARTESIAN_POINT('Ctrl Pts',(-12.0390136106012,-4.82866708757384,
131.74868709487));
#75819=CARTESIAN_POINT('Ctrl Pts',(-12.0467078403643,-4.80061176931338,
131.882278523772));
#75820=CARTESIAN_POINT('Ctrl Pts',(-12.0544020701273,-4.76705849692604,
132.01445827866));
#75821=CARTESIAN_POINT('Ctrl Pts',(-12.0620970149627,-4.73350210622531,
132.146650317831));
#75822=CARTESIAN_POINT('Ctrl Pts',(-12.0697919597981,-4.69444684254895,
132.277430037557));
#75823=CARTESIAN_POINT('Ctrl Pts',(-12.0774869046335,-4.65004713427463,
132.40631090129));
#75824=CARTESIAN_POINT('Ctrl Pts',(-12.0851842861471,-4.60563336640595,
132.535232576387));
#75825=CARTESIAN_POINT('Ctrl Pts',(-12.0928816676608,-4.55587191651374,
132.662253824595));
#75826=CARTESIAN_POINT('Ctrl Pts',(-12.1005790491744,-4.50096588209621,
132.786906755921));
#75827=CARTESIAN_POINT('Ctrl Pts',(-12.1082850298899,-4.44599850888841,
132.911698944436));
#75828=CARTESIAN_POINT('Ctrl Pts',(-12.1159910106053,-4.38587523653585,
133.034117170521));
#75829=CARTESIAN_POINT('Ctrl Pts',(-12.1236969913208,-4.32084596472346,
133.153716531776));
#75830=CARTESIAN_POINT('Ctrl Pts',(-12.1314078195653,-4.25577578555616,
133.273391128281));
#75831=CARTESIAN_POINT('Ctrl Pts',(-12.1391186478099,-4.18579366456531,
133.390242989437));
#75832=CARTESIAN_POINT('Ctrl Pts',(-12.1468294760544,-4.11119297665866,
133.503856009518));
#75833=CARTESIAN_POINT('Ctrl Pts',(-12.1545518572617,-4.03648051619792,
133.617639253465));
#75834=CARTESIAN_POINT('Ctrl Pts',(-12.162274238469,-3.95713590338995,133.728173646549));
#75835=CARTESIAN_POINT('Ctrl Pts',(-12.1699966196763,-3.87349322778882,
133.835075595385));
#75836=CARTESIAN_POINT('Ctrl Pts',(-12.1738693486266,-3.83154691581829,
133.888686296667));
#75837=CARTESIAN_POINT('Ctrl Pts',(-12.1777420775768,-3.78852024960521,
133.941384018686));
#75838=CARTESIAN_POINT('Ctrl Pts',(-12.1816148065271,-3.74445875092837,
133.99312397114));
#75839=CARTESIAN_POINT('Ctrl Pts',(-12.1893891406461,-3.65600721793908,
134.096989664517));
#75840=CARTESIAN_POINT('Ctrl Pts',(-12.1971634747652,-3.56309069011036,
134.197336814495));
#75841=CARTESIAN_POINT('Ctrl Pts',(-12.2049378088843,-3.46601982065049,
134.293757365624));
#75842=CARTESIAN_POINT('Ctrl Pts',(-12.2127025618314,-3.36906858236177,
134.390059087041));
#75843=CARTESIAN_POINT('Ctrl Pts',(-12.2204673147785,-3.26797346414579,
134.482443565261));
#75844=CARTESIAN_POINT('Ctrl Pts',(-12.2282320677256,-3.16308550707379,
134.57053548571));
#75845=CARTESIAN_POINT('Ctrl Pts',(-12.2359891086106,-3.05830172619941,
134.658539912022));
#75846=CARTESIAN_POINT('Ctrl Pts',(-12.2437461494956,-2.94973290061633,
134.742260015163));
#75847=CARTESIAN_POINT('Ctrl Pts',(-12.2515031903806,-2.83776681812349,
134.821357325115));
#75848=CARTESIAN_POINT('Ctrl Pts',(-12.2592543816207,-2.72588517012489,
134.90039498717));
#75849=CARTESIAN_POINT('Ctrl Pts',(-12.2670055728609,-2.61061168254893,
134.974816570206));
#75850=CARTESIAN_POINT('Ctrl Pts',(-12.274756764101,-2.49236682855777,135.044324137976));
#75851=CARTESIAN_POINT('Ctrl Pts',(-12.282504660878,-2.37417223178352,135.113802163175));
#75852=CARTESIAN_POINT('Ctrl Pts',(-12.2902525576551,-2.25300911676645,
135.178370129438));
#75853=CARTESIAN_POINT('Ctrl Pts',(-12.2980004544322,-2.1293263302984,135.237773799483));
#75854=CARTESIAN_POINT('Ctrl Pts',(-12.3057467305163,-2.00566941560299,
135.297165043561));
#75855=CARTESIAN_POINT('Ctrl Pts',(-12.3134930066003,-1.87949423001065,
135.351393970956));
#75856=CARTESIAN_POINT('Ctrl Pts',(-12.3212392826844,-1.75127321973399,
135.400252823911));
#75857=CARTESIAN_POINT('Ctrl Pts',(-12.3289856159498,-1.62305126295879,
135.449112037531));
#75858=CARTESIAN_POINT('Ctrl Pts',(-12.3367319492152,-1.49278381670479,
135.492600958396));
#75859=CARTESIAN_POINT('Ctrl Pts',(-12.3444782824805,-1.360961878156,135.530560552895));
#75860=CARTESIAN_POINT('Ctrl Pts',(-12.3522263504835,-1.22911041899807,
135.568528648183));
#75861=CARTESIAN_POINT('Ctrl Pts',(-12.3599744184865,-1.09570415045801,
135.600964844957));
#75862=CARTESIAN_POINT('Ctrl Pts',(-12.3677224864895,-0.961247357880002,
135.627760515923));
#75863=CARTESIAN_POINT('Ctrl Pts',(-12.3754787892314,-0.82664766302279,
135.654584665647));
#75864=CARTESIAN_POINT('Ctrl Pts',(-12.3832350919732,-0.690995597816443,
135.675756237735));
#75865=CARTESIAN_POINT('Ctrl Pts',(-12.3909913947151,-0.554804279500532,
135.691218020228));
#75866=CARTESIAN_POINT('Ctrl Pts',(-12.3987518372292,-0.418540271777395,
135.706688055139));
#75867=CARTESIAN_POINT('Ctrl Pts',(-12.4065122797434,-0.281736827232087,
135.716442200288));
#75868=CARTESIAN_POINT('Ctrl Pts',(-12.4142727222575,-0.144909249280095,
135.72047538148));
#75869=CARTESIAN_POINT('Ctrl Pts',(-12.422045622523,-0.00786202355299234,
135.724515037092));
#75870=CARTESIAN_POINT('Ctrl Pts',(-12.4298185227884,0.129209021837687,
135.72281538144));
#75871=CARTESIAN_POINT('Ctrl Pts',(-12.4375914230538,0.265790619590803,
135.715423476972));
#75872=CARTESIAN_POINT('Ctrl Pts',(-12.4450817588159,0.397407132237124,
135.708300286851));
#75873=CARTESIAN_POINT('Ctrl Pts',(-12.4525720945779,0.528568858092386,
135.695891546957));
#75874=CARTESIAN_POINT('Ctrl Pts',(-12.4600624303399,0.658825501465144,
135.678284295787));
#75875=CARTESIAN_POINT('Ctrl Pts',(-12.467836764459,0.794020865062038,135.660009460336));
#75876=CARTESIAN_POINT('Ctrl Pts',(-12.475611098578,0.928669417221008,135.63607623962));
#75877=CARTESIAN_POINT('Ctrl Pts',(-12.4833854326971,1.0622599336885,135.606525431041));
#75878=CARTESIAN_POINT('Ctrl Pts',(-12.4911501856442,1.19568581178377,135.577011041194));
#75879=CARTESIAN_POINT('Ctrl Pts',(-12.4989149385913,1.3280558705558,135.54189292217));
#75880=CARTESIAN_POINT('Ctrl Pts',(-12.5066796915384,1.45886460095032,135.501263548072));
#75881=CARTESIAN_POINT('Ctrl Pts',(-12.5144367324234,1.58954341026992,135.46067452764));
#75882=CARTESIAN_POINT('Ctrl Pts',(-12.5221937733084,1.71866360628769,135.414585260573));
#75883=CARTESIAN_POINT('Ctrl Pts',(-12.5299508141934,1.84573081581363,135.363139052416));
#75884=CARTESIAN_POINT('Ctrl Pts',(-12.5377020054335,1.97270220296809,135.311731640245));
#75885=CARTESIAN_POINT('Ctrl Pts',(-12.5454531966737,2.09762332425186,135.254975473912));
#75886=CARTESIAN_POINT('Ctrl Pts',(-12.5532043879138,2.22001624144654,135.193063267577));
#75887=CARTESIAN_POINT('Ctrl Pts',(-12.5609522846909,2.34235713838665,135.131177375581));
#75888=CARTESIAN_POINT('Ctrl Pts',(-12.5687001814678,2.46217162030437,135.064139978325));
#75889=CARTESIAN_POINT('Ctrl Pts',(-12.5764480782449,2.5790031775185,134.992191281866));
#75890=CARTESIAN_POINT('Ctrl Pts',(-12.584194354329,2.69581029608946,134.920257635523));
#75891=CARTESIAN_POINT('Ctrl Pts',(-12.5919406304131,2.80963539836327,134.843414938289));
#75892=CARTESIAN_POINT('Ctrl Pts',(-12.5996869064972,2.92004832313543,134.761948374401));
#75893=CARTESIAN_POINT('Ctrl Pts',(-12.6074332397625,3.03046206295041,134.680481209146));
#75894=CARTESIAN_POINT('Ctrl Pts',(-12.6151795730279,3.13746326040358,134.594390341251));
#75895=CARTESIAN_POINT('Ctrl Pts',(-12.6229259062932,3.24065272004287,134.504002899001));
#75896=CARTESIAN_POINT('Ctrl Pts',(-12.6306739742962,3.34386528824633,134.413595215109));
#75897=CARTESIAN_POINT('Ctrl Pts',(-12.6384220422991,3.44326412600791,134.318889299779));
#75898=CARTESIAN_POINT('Ctrl Pts',(-12.6461701103021,3.53848526356258,134.220250706847));
#75899=CARTESIAN_POINT('Ctrl Pts',(-12.6539264130439,3.63380760327553,134.121507279645));
#75900=CARTESIAN_POINT('Ctrl Pts',(-12.6616827157857,3.72494310121309,134.018823107179));
#75901=CARTESIAN_POINT('Ctrl Pts',(-12.6694390185276,3.81156627093222,133.912598965053));
#75902=CARTESIAN_POINT('Ctrl Pts',(-12.6771994610417,3.8982356740452,133.806318127905));
#75903=CARTESIAN_POINT('Ctrl Pts',(-12.6849599035559,3.9803877159977,133.696493869246));
#75904=CARTESIAN_POINT('Ctrl Pts',(-12.6927203460701,4.05773959364234,133.583556985707));
#75905=CARTESIAN_POINT('Ctrl Pts',(-12.7004932463355,4.13521564338795,133.470438805856));
#75906=CARTESIAN_POINT('Ctrl Pts',(-12.7082661466009,4.20787592313095,133.354198347919));
#75907=CARTESIAN_POINT('Ctrl Pts',(-12.7160390468663,4.27548259432928,133.235292876615));
#75908=CARTESIAN_POINT('Ctrl Pts',(-12.7235293826285,4.34063159273945,133.120709918697));
#75909=CARTESIAN_POINT('Ctrl Pts',(-12.7310197183906,4.40108788506207,133.003652617028));
#75910=CARTESIAN_POINT('Ctrl Pts',(-12.7385100541527,4.45668130342799,132.884546864558));
#75911=CARTESIAN_POINT('Ctrl Pts',(-12.7462843882718,4.51438256314785,132.760925181284));
#75912=CARTESIAN_POINT('Ctrl Pts',(-12.7540587223909,4.56702769815066,132.634705050508));
#75913=CARTESIAN_POINT('Ctrl Pts',(-12.7618330565099,4.61437470325191,132.506338631669));
#75914=CARTESIAN_POINT('Ctrl Pts',(-12.769597809457,4.66166335740089,132.378130412968));
#75915=CARTESIAN_POINT('Ctrl Pts',(-12.7773625624042,4.70366673935454,132.247781532468));
#75916=CARTESIAN_POINT('Ctrl Pts',(-12.7851273153513,4.74018941020094,132.115767273763));
#75917=CARTESIAN_POINT('Ctrl Pts',(-12.7928843562363,4.77667580621578,131.983884133481));
#75918=CARTESIAN_POINT('Ctrl Pts',(-12.8006413971213,4.80769222040014,131.850339281055));
#75919=CARTESIAN_POINT('Ctrl Pts',(-12.8083984380063,4.83309199898311,131.715626106798));
#75920=CARTESIAN_POINT('Ctrl Pts',(-12.8161496292464,4.85847262339537,131.581014520794));
#75921=CARTESIAN_POINT('Ctrl Pts',(-12.8239008204865,4.87824497066301,131.445236749259));
#75922=CARTESIAN_POINT('Ctrl Pts',(-12.8316520117266,4.89231283938551,131.308799061862));
#75923=CARTESIAN_POINT('Ctrl Pts',(-12.8393999085037,4.90637472888857,131.172419364121));
#75924=CARTESIAN_POINT('Ctrl Pts',(-12.8471478052808,4.91473692208736,131.035380696465));
#75925=CARTESIAN_POINT('Ctrl Pts',(-12.8548957020578,4.91735475650663,130.898196970658));
#75926=CARTESIAN_POINT('Ctrl Pts',(-12.8626419781419,4.91997204333137,130.76104194073));
#75927=CARTESIAN_POINT('Ctrl Pts',(-12.870388254226,4.91684735396236,130.62374230365));
#75928=CARTESIAN_POINT('Ctrl Pts',(-12.8781345303101,4.90798810933561,130.48681411527));
#75929=CARTESIAN_POINT('Ctrl Pts',(-12.8858808635755,4.89912879931192,130.349884916117));
#75930=CARTESIAN_POINT('Ctrl Pts',(-12.8936271968408,4.88453487480433,130.213327561284));
#75931=CARTESIAN_POINT('Ctrl Pts',(-12.9013735301061,4.8642657832114,130.07765472604));
#75932=CARTESIAN_POINT('Ctrl Pts',(-12.9091215981091,4.84399215249603,129.941951507805));
#75933=CARTESIAN_POINT('Ctrl Pts',(-12.916869666112,4.8180408834798,129.807133589919));
#75934=CARTESIAN_POINT('Ctrl Pts',(-12.9246177341149,4.78652279241,129.67370478123));
#75935=CARTESIAN_POINT('Ctrl Pts',(-12.9323740368568,4.75497120353782,129.540134162816));
#75936=CARTESIAN_POINT('Ctrl Pts',(-12.9401303395986,4.71784106381872,129.407955983891));
#75937=CARTESIAN_POINT('Ctrl Pts',(-12.9478866423404,4.67529362374644,129.277660714423));
#75938=CARTESIAN_POINT('Ctrl Pts',(-12.9556470848546,4.63272347482431,129.147295902447));
#75939=CARTESIAN_POINT('Ctrl Pts',(-12.9634075273688,4.58473040098017,129.018816368474));
#75940=CARTESIAN_POINT('Ctrl Pts',(-12.971167969883,4.53152398161148,128.892692898903));
#75941=CARTESIAN_POINT('Ctrl Pts',(-12.9789408701484,4.4782321505749,128.766366964741));
#75942=CARTESIAN_POINT('Ctrl Pts',(-12.9867137704138,4.41971041723846,128.642405006701));
#75943=CARTESIAN_POINT('Ctrl Pts',(-12.9944866706793,4.35621493382028,128.521254287834));
#75944=CARTESIAN_POINT('Ctrl Pts',(-13.0019770064414,4.29502767115931,128.404507702758));
#75945=CARTESIAN_POINT('Ctrl Pts',(-13.0094673422035,4.22922215075735,128.29037178098));
#75946=CARTESIAN_POINT('Ctrl Pts',(-13.0169576779656,4.15906470852615,128.179219895092));
#75947=CARTESIAN_POINT('Ctrl Pts',(-13.0247320120847,4.08624722554948,128.063853651668));
#75948=CARTESIAN_POINT('Ctrl Pts',(-13.0325063462037,4.00851063618618,127.95133674482));
#75949=CARTESIAN_POINT('Ctrl Pts',(-13.0402806803228,3.92610454526274,127.842117183584));
#75950=CARTESIAN_POINT('Ctrl Pts',(-13.0480454332699,3.84380001248174,127.733032225697));
#75951=CARTESIAN_POINT('Ctrl Pts',(-13.0558101862169,3.75683766158096,127.627236837004));
#75952=CARTESIAN_POINT('Ctrl Pts',(-13.063574939164,3.66551172260317,127.525152348188));
#75953=CARTESIAN_POINT('Ctrl Pts',(-13.071331980049,3.57427648983543,127.423169251125));
#75954=CARTESIAN_POINT('Ctrl Pts',(-13.0790890209341,3.47868655278733,127.324890008691));
#75955=CARTESIAN_POINT('Ctrl Pts',(-13.086846061819,3.37907774475808,127.230704694372));
#75956=CARTESIAN_POINT('Ctrl Pts',(-13.0945972530592,3.27954405250567,127.136590405931));
#75957=CARTESIAN_POINT('Ctrl Pts',(-13.1023484442993,3.17599780455103,127.046564168121));
#75958=CARTESIAN_POINT('Ctrl Pts',(-13.1100996355394,3.06881294069888,126.960980569028));
#75959=CARTESIAN_POINT('Ctrl Pts',(-13.1178475323165,2.96167363327311,126.875433345248));
#75960=CARTESIAN_POINT('Ctrl Pts',(-13.1255954290936,2.85089909071917,126.794325248056));
#75961=CARTESIAN_POINT('Ctrl Pts',(-13.1333433258707,2.73689754040064,126.717971635121));
#75962=CARTESIAN_POINT('Ctrl Pts',(-13.1410896019548,2.62291983674883,126.641633993715));
#75963=CARTESIAN_POINT('Ctrl Pts',(-13.1488358780388,2.50571679261761,126.570049075806));
#75964=CARTESIAN_POINT('Ctrl Pts',(-13.1565821541229,2.38572659160582,126.503489578741));
#75965=CARTESIAN_POINT('Ctrl Pts',(-13.1643284873882,2.26573550485362,126.436929590349));
#75966=CARTESIAN_POINT('Ctrl Pts',(-13.1720748206536,2.14295756205467,126.375395286472));
#75967=CARTESIAN_POINT('Ctrl Pts',(-13.179821153919,2.01785622420303,126.319113765837));
#75968=CARTESIAN_POINT('Ctrl Pts',(-13.187569221922,1.89272687077383,126.262819641345));
#75969=CARTESIAN_POINT('Ctrl Pts',(-13.1953172899249,1.76527344341519,126.211780801218));
#75970=CARTESIAN_POINT('Ctrl Pts',(-13.2030653579279,1.63597970966912,126.166176333598));
#75971=CARTESIAN_POINT('Ctrl Pts',(-13.2108216606698,1.50654856100455,126.120523397006));
#75972=CARTESIAN_POINT('Ctrl Pts',(-13.2185779634117,1.37527356812249,126.080316500792));
#75973=CARTESIAN_POINT('Ctrl Pts',(-13.2263342661535,1.24265453712725,126.045685091345));
#75974=CARTESIAN_POINT('Ctrl Pts',(-13.2340947086677,1.10996472336154,126.011035198071));
#75975=CARTESIAN_POINT('Ctrl Pts',(-13.2418551511819,0.975929823990999,
125.981966803931));
#75976=CARTESIAN_POINT('Ctrl Pts',(-13.2496155936961,0.841059207730189,
125.95855805539));
#75977=CARTESIAN_POINT('Ctrl Pts',(-13.2573884939615,0.705972085183458,
125.935111729048));
#75978=CARTESIAN_POINT('Ctrl Pts',(-13.2651613942269,0.570046952758284,
125.917343254465));
#75979=CARTESIAN_POINT('Ctrl Pts',(-13.2729342944924,0.433798562058226,
125.905278880132));
#75980=CARTESIAN_POINT('Ctrl Pts',(-13.2804246302544,0.302503143548553,
125.893653076195));
#75981=CARTESIAN_POINT('Ctrl Pts',(-13.2879149660165,0.170907868893959,
125.887323870572));
#75982=CARTESIAN_POINT('Ctrl Pts',(-13.2954053017785,0.0394708280954393,
125.886269004325));
#75983=CARTESIAN_POINT('Ctrl Pts',(-13.3031796358976,-0.0969496880541805,
125.885174142504));
#75984=CARTESIAN_POINT('Ctrl Pts',(-13.3109539700167,-0.23363187380239,
125.88975800022));
#75985=CARTESIAN_POINT('Ctrl Pts',(-13.3187283041358,-0.370063888953388,
125.900052737692));
#75986=CARTESIAN_POINT('Ctrl Pts',(-13.3264930570828,-0.506327763838436,
125.91033478782));
#75987=CARTESIAN_POINT('Ctrl Pts',(-13.3342578100299,-0.642341695462724,
125.92631368475));
#75988=CARTESIAN_POINT('Ctrl Pts',(-13.342022562977,-0.777592167864181,
125.94796962394));
#75989=CARTESIAN_POINT('Ctrl Pts',(-13.349779603862,-0.912708307589934,
125.969604054145));
#75990=CARTESIAN_POINT('Ctrl Pts',(-13.3575366447471,-1.04706211355146,
125.996904244292));
#75991=CARTESIAN_POINT('Ctrl Pts',(-13.3652936856321,-1.180143879775,126.029798492561));
#75992=CARTESIAN_POINT('Ctrl Pts',(-13.3730448768723,-1.31312528800377,
126.062667935022));
#75993=CARTESIAN_POINT('Ctrl Pts',(-13.3807960681123,-1.44483618782624,
126.10112294546));
#75994=CARTESIAN_POINT('Ctrl Pts',(-13.3885472593525,-1.57477613064501,
126.145040581246));
#75995=CARTESIAN_POINT('Ctrl Pts',(-13.3962951561295,-1.70466084552164,
126.188939550866));
#75996=CARTESIAN_POINT('Ctrl Pts',(-13.4040430529066,-1.83277573085865,
126.238296403107));
#75997=CARTESIAN_POINT('Ctrl Pts',(-13.4117909496837,-1.95863481045777,
126.29293814325));
#75998=CARTESIAN_POINT('Ctrl Pts',(-13.4195372257678,-2.08446756305064,
126.347568453519));
#75999=CARTESIAN_POINT('Ctrl Pts',(-13.4272835018519,-2.20804509007464,
126.40748129722));
#76000=CARTESIAN_POINT('Ctrl Pts',(-13.435029777936,-2.32890111458898,126.472455417661));
#76001=CARTESIAN_POINT('Ctrl Pts',(-13.4427761112014,-2.44975803123487,
126.537430017726));
#76002=CARTESIAN_POINT('Ctrl Pts',(-13.4505224444667,-2.56789306092889,
126.60746578395));
#76003=CARTESIAN_POINT('Ctrl Pts',(-13.4582687777321,-2.68286462709367,
126.682295545883));
#76004=CARTESIAN_POINT('Ctrl Pts',(-13.4660168457351,-2.79786194034417,
126.757142065422));
#76005=CARTESIAN_POINT('Ctrl Pts',(-13.4737649137381,-2.90969405274877,
126.836784503746));
#76006=CARTESIAN_POINT('Ctrl Pts',(-13.4815129817411,-3.01794880420848,
126.920912655036));
#76007=CARTESIAN_POINT('Ctrl Pts',(-13.489269284483,-3.1263186101057,127.005130218726));
#76008=CARTESIAN_POINT('Ctrl Pts',(-13.4970255872248,-3.23110315083192,
127.093842778627));
#76009=CARTESIAN_POINT('Ctrl Pts',(-13.5047818899667,-3.33192336206522,
127.186699802644));
#76010=CARTESIAN_POINT('Ctrl Pts',(-13.5125423324809,-3.43279738408144,
127.279606387251));
#76011=CARTESIAN_POINT('Ctrl Pts',(-13.520302774995,-3.5297025844255,127.376661567089));
#76012=CARTESIAN_POINT('Ctrl Pts',(-13.5280632175092,-3.62229789003038,
127.477479035907));
#76013=CARTESIAN_POINT('Ctrl Pts',(-13.5358361177747,-3.71504183783979,
127.578458345876));
#76014=CARTESIAN_POINT('Ctrl Pts',(-13.5436090180401,-3.80346181296698,
127.683211714854));
#76015=CARTESIAN_POINT('Ctrl Pts',(-13.5513819183056,-3.88725749599962,
127.79132025569));
#76016=CARTESIAN_POINT('Ctrl Pts',(-13.5588722540675,-3.96800699488419,
127.895498778755));
#76017=CARTESIAN_POINT('Ctrl Pts',(-13.5663625898294,-4.04446239516941,
128.002792520054));
#76018=CARTESIAN_POINT('Ctrl Pts',(-13.5738529255913,-4.11639481509704,
128.112804043993));
#76019=CARTESIAN_POINT('Ctrl Pts',(-13.5817885100048,-4.19260311984398,
128.229354992098));
#76020=CARTESIAN_POINT('Ctrl Pts',(-13.5897240944183,-4.26396836570864,
128.349313981803));
#76021=CARTESIAN_POINT('Ctrl Pts',(-13.5976596788317,-4.33017842465427,
128.472250441533));
#76022=CARTESIAN_POINT('Ctrl Pts',(-13.6055853409293,-4.39630569736891,
128.595033186762));
#76023=CARTESIAN_POINT('Ctrl Pts',(-13.6135110030269,-4.45729043700007,
128.72078567151));
#76024=CARTESIAN_POINT('Ctrl Pts',(-13.6214366651244,-4.5128632937921,128.849047866612));
#76025=CARTESIAN_POINT('Ctrl Pts',(-13.6293509155556,-4.5683561346951,128.977125384982));
#76026=CARTESIAN_POINT('Ctrl Pts',(-13.6372651659867,-4.61845247250927,
129.107705077331));
#76027=CARTESIAN_POINT('Ctrl Pts',(-13.6451794164179,-4.66292880400036,
129.240302424491));
#76028=CARTESIAN_POINT('Ctrl Pts',(-13.6519065846276,-4.70073399678446,
129.353011096812));
#76029=CARTESIAN_POINT('Ctrl Pts',(-13.6586337528374,-4.73447936189535,
129.46717699462));
#76030=CARTESIAN_POINT('Ctrl Pts',(-13.6653609210472,-4.76405452823398,
129.582490119308));
#76031=CARTESIAN_POINT('Ctrl Pts',(-11.9152857535001,-4.76405452823405,
129.582490119308));
#76032=CARTESIAN_POINT('Ctrl Pts',(-11.9248052072162,-4.80558106041339,
129.744401438022));
#76033=CARTESIAN_POINT('Ctrl Pts',(-11.9343246609324,-4.83888478217968,
129.908568752554));
#76034=CARTESIAN_POINT('Ctrl Pts',(-11.9438441146484,-4.86375462011194,
130.074241409601));
#76035=CARTESIAN_POINT('Ctrl Pts',(-11.953239736843,-4.88830094474597,130.237758953781));
#76036=CARTESIAN_POINT('Ctrl Pts',(-11.9626353590377,-4.90463134586909,
130.402742953669));
#76037=CARTESIAN_POINT('Ctrl Pts',(-11.9720309812323,-4.91258887906555,
130.568450533463));
#76038=CARTESIAN_POINT('Ctrl Pts',(-11.976400842145,-4.91628989136213,130.645520370976));
#76039=CARTESIAN_POINT('Ctrl Pts',(-11.9807707030577,-4.91818039492165,
130.72274642572));
#76040=CARTESIAN_POINT('Ctrl Pts',(-11.9851405639704,-4.91824811303239,
130.800052351862));
#76041=CARTESIAN_POINT('',(-11.6398594359493,-4.91824997562219,130.804850303521));
#76042=CARTESIAN_POINT('Ctrl Pts',(-11.5697518023984,-4.76405452823402,
129.582490119308));
#76043=CARTESIAN_POINT('Ctrl Pts',(-11.5774904387069,-4.79803826805266,
129.714992205086));
#76044=CARTESIAN_POINT('Ctrl Pts',(-11.5852290750154,-4.82646319605803,
129.84880890235));
#76045=CARTESIAN_POINT('Ctrl Pts',(-11.5929677113239,-4.84925361316315,
129.983432814575));
#76046=CARTESIAN_POINT('Ctrl Pts',(-11.6007829987615,-4.87226976916243,
130.119390175544));
#76047=CARTESIAN_POINT('Ctrl Pts',(-11.6085982861991,-4.88953914801215,
130.256170419018));
#76048=CARTESIAN_POINT('Ctrl Pts',(-11.6164135736366,-4.90103760226909,
130.393248122445));
#76049=CARTESIAN_POINT('Ctrl Pts',(-11.6242288610742,-4.91253605652603,
130.530325825872));
#76050=CARTESIAN_POINT('Ctrl Pts',(-11.6320441485117,-4.9182636309454,130.667700580587));
#76051=CARTESIAN_POINT('Ctrl Pts',(-11.6398594359493,-4.91824997562219,
130.804850303521));
#76052=CARTESIAN_POINT('Ctrl Pts',(-11.6398594359912,-4.91824997562211,
130.804850304257));
#76053=CARTESIAN_POINT('Ctrl Pts',(-11.641342475681,-4.91824738436531,130.830876024256));
#76054=CARTESIAN_POINT('Ctrl Pts',(-11.6428255153709,-4.91803821598196,
130.856900563331));
#76055=CARTESIAN_POINT('Ctrl Pts',(-11.6443085550607,-4.91762251540665,
130.882921794146));
#76056=CARTESIAN_POINT('Ctrl Pts',(-11.6520828891798,-4.91544334569996,
131.019329298222));
#76057=CARTESIAN_POINT('Ctrl Pts',(-11.6598572232989,-4.9075808124374,131.155862122931));
#76058=CARTESIAN_POINT('Ctrl Pts',(-11.667631557418,-4.89401504741631,131.292007803719));
#76059=CARTESIAN_POINT('Ctrl Pts',(-11.6753963103651,-4.88046600098822,
131.427985697122));
#76060=CARTESIAN_POINT('Ctrl Pts',(-11.6831610633122,-4.86122774625856,
131.563577010627));
#76061=CARTESIAN_POINT('Ctrl Pts',(-11.6909258162592,-4.8363324050331,131.698268851406));
#76062=CARTESIAN_POINT('Ctrl Pts',(-11.6986828571442,-4.81146179021151,
131.832826914349));
#76063=CARTESIAN_POINT('Ctrl Pts',(-11.7064398980293,-4.78094534095621,
131.966486900446));
#76064=CARTESIAN_POINT('Ctrl Pts',(-11.7141969389143,-4.74486696997474,
132.098740971149));
#76065=CARTESIAN_POINT('Ctrl Pts',(-11.7219481301544,-4.70881580597349,
132.23089530803));
#76066=CARTESIAN_POINT('Ctrl Pts',(-11.7296993213945,-4.66721117120037,
132.361645464148));
#76067=CARTESIAN_POINT('Ctrl Pts',(-11.7374505126346,-4.62018798226402,
132.490494085309));
#76068=CARTESIAN_POINT('Ctrl Pts',(-11.7451984094117,-4.57318477943728,
132.619287942369));
#76069=CARTESIAN_POINT('Ctrl Pts',(-11.7529463061887,-4.52076773675328,
132.746181505422));
#76070=CARTESIAN_POINT('Ctrl Pts',(-11.7606942029658,-4.46312146120302,
132.870693089616));
#76071=CARTESIAN_POINT('Ctrl Pts',(-11.7684404790499,-4.4054872440109,132.995178628671));
#76072=CARTESIAN_POINT('Ctrl Pts',(-11.7761867551341,-4.34262613382016,
133.11728282537));
#76073=CARTESIAN_POINT('Ctrl Pts',(-11.7839330312182,-4.27477051296915,
133.236544846597));
#76074=CARTESIAN_POINT('Ctrl Pts',(-11.7916793644835,-4.20691439122345,
133.35580774819));
#76075=CARTESIAN_POINT('Ctrl Pts',(-11.7994256977489,-4.13406387859041,
133.472228092635));
#76076=CARTESIAN_POINT('Ctrl Pts',(-11.8071720310142,-4.0564966652038,133.585370841871));
#76077=CARTESIAN_POINT('Ctrl Pts',(-11.8149200990172,-3.97891208117757,
133.698538928642));
#76078=CARTESIAN_POINT('Ctrl Pts',(-11.8226681670202,-3.89660891556575,
133.808427637239));
#76079=CARTESIAN_POINT('Ctrl Pts',(-11.8304162350232,-3.80990717556159,
133.91463237034));
#76080=CARTESIAN_POINT('Ctrl Pts',(-11.838172537765,-3.72311328791638,134.020949979095));
#76081=CARTESIAN_POINT('Ctrl Pts',(-11.8459288405069,-3.63191173498627,
134.123575487633));
#76082=CARTESIAN_POINT('Ctrl Pts',(-11.8536851432488,-3.53666204442025,
134.222138352595));
#76083=CARTESIAN_POINT('Ctrl Pts',(-11.8614455857629,-3.44136151622634,
134.320753823525));
#76084=CARTESIAN_POINT('Ctrl Pts',(-11.869206028277,-3.34200882827089,134.41530206086));
#76085=CARTESIAN_POINT('Ctrl Pts',(-11.8769664707912,-3.23899836037251,
134.505451360037));
#76086=CARTESIAN_POINT('Ctrl Pts',(-11.8847393710566,-3.13582253092622,
134.595745374872));
#76087=CARTESIAN_POINT('Ctrl Pts',(-11.8925122713221,-3.02897749272747,
134.681626095212));
#76088=CARTESIAN_POINT('Ctrl Pts',(-11.9002851715875,-2.91888921913814,
134.762803340266));
#76089=CARTESIAN_POINT('Ctrl Pts',(-11.9077755073496,-2.81280293158941,
134.84102958799));
#76090=CARTESIAN_POINT('Ctrl Pts',(-11.9152658431116,-2.70370536943968,
134.91488821706));
#76091=CARTESIAN_POINT('Ctrl Pts',(-11.9227561788736,-2.59199934636086,
134.984159948989));
#76092=CARTESIAN_POINT('Ctrl Pts',(-11.9305305129927,-2.47605795546485,
135.056058139689));
#76093=CARTESIAN_POINT('Ctrl Pts',(-11.9383048471117,-2.35693913194501,
135.123242494532));
#76094=CARTESIAN_POINT('Ctrl Pts',(-11.9460791812308,-2.23506328749638,
135.185419298226));
#76095=CARTESIAN_POINT('Ctrl Pts',(-11.9538439341779,-2.11333764413367,
135.247519474566));
#76096=CARTESIAN_POINT('Ctrl Pts',(-11.961608687125,-1.98886208533451,135.304624202958));
#76097=CARTESIAN_POINT('Ctrl Pts',(-11.9693734400721,-1.86208548498143,
135.356483277284));
#76098=CARTESIAN_POINT('Ctrl Pts',(-11.9771304809571,-1.73543480093506,
135.408290844447));
#76099=CARTESIAN_POINT('Ctrl Pts',(-11.984887521842,-1.60648798295659,135.454862978729));
#76100=CARTESIAN_POINT('Ctrl Pts',(-11.992644562727,-1.47571764686486,135.495995779131));
#76101=CARTESIAN_POINT('Ctrl Pts',(-12.0003957539672,-1.34504592570083,
135.537097560968));
#76102=CARTESIAN_POINT('Ctrl Pts',(-12.0081469452074,-1.21255379497672,
135.572768056561));
#76103=CARTESIAN_POINT('Ctrl Pts',(-12.0158981364475,-1.07873261858636,
135.602851942983));
#76104=CARTESIAN_POINT('Ctrl Pts',(-12.0236460332246,-0.94496831976576,
135.63292304295));
#76105=CARTESIAN_POINT('Ctrl Pts',(-12.0313939300016,-0.809876479428558,
135.65741217079));
#76106=CARTESIAN_POINT('Ctrl Pts',(-12.0391418267787,-0.673962137271401,
135.676214279164));
#76107=CARTESIAN_POINT('Ctrl Pts',(-12.0468881028628,-0.538076225464649,
135.695012454542));
#76108=CARTESIAN_POINT('Ctrl Pts',(-12.0546343789469,-0.401368541085799,
135.708125923096));
#76109=CARTESIAN_POINT('Ctrl Pts',(-12.0623806550309,-0.264352404415259,
135.715501103113));
#76110=CARTESIAN_POINT('Ctrl Pts',(-12.0701269882963,-0.127335256322724,
135.722876337573));
#76111=CARTESIAN_POINT('Ctrl Pts',(-12.0778733215616,0.00998995820488735,
135.724513177958));
#76112=CARTESIAN_POINT('Ctrl Pts',(-12.085619654827,0.14710713102649,135.720410104146));
#76113=CARTESIAN_POINT('Ctrl Pts',(-12.09336772283,0.284255010288242,135.716306111479));
#76114=CARTESIAN_POINT('Ctrl Pts',(-12.1011157908329,0.421194364420792,
135.70645965848));
#76115=CARTESIAN_POINT('Ctrl Pts',(-12.1088638588359,0.557411822533177,
135.69092128153));
#76116=CARTESIAN_POINT('Ctrl Pts',(-12.1166201615778,0.693774054181052,
135.675366390208));
#76117=CARTESIAN_POINT('Ctrl Pts',(-12.1243764643196,0.829412468099328,
135.654107534897));
#76118=CARTESIAN_POINT('Ctrl Pts',(-12.1321327670614,0.963820982191196,
135.627246908656));
#76119=CARTESIAN_POINT('Ctrl Pts',(-12.1398932095756,1.098301234154,135.600371946091));
#76120=CARTESIAN_POINT('Ctrl Pts',(-12.1476536520898,1.23154989863293,135.567889347648));
#76121=CARTESIAN_POINT('Ctrl Pts',(-12.1554140946039,1.3630747312608,135.529951621821));
#76122=CARTESIAN_POINT('Ctrl Pts',(-12.1631869948693,1.49481069922624,135.491952994989));
#76123=CARTESIAN_POINT('Ctrl Pts',(-12.1709598951348,1.62481693449822,135.448481865441));
#76124=CARTESIAN_POINT('Ctrl Pts',(-12.1787327954002,1.75261905075177,135.399739766825));
#76125=CARTESIAN_POINT('Ctrl Pts',(-12.1862231311623,1.87577523816644,135.352769566267));
#76126=CARTESIAN_POINT('Ctrl Pts',(-12.1937134669244,1.99688449178711,135.300905090536));
#76127=CARTESIAN_POINT('Ctrl Pts',(-12.2012038026865,2.11554459578291,135.244366712804));
#76128=CARTESIAN_POINT('Ctrl Pts',(-12.2089781368055,2.2387037336868,135.185684665297));
#76129=CARTESIAN_POINT('Ctrl Pts',(-12.2167524709246,2.35961446792742,135.121781410311));
#76130=CARTESIAN_POINT('Ctrl Pts',(-12.2245268050437,2.47780244472148,135.052851891822));
#76131=CARTESIAN_POINT('Ctrl Pts',(-12.2322915579908,2.59584476539691,134.984007322805));
#76132=CARTESIAN_POINT('Ctrl Pts',(-12.240056310938,2.71117067069839,134.910149010412));
#76133=CARTESIAN_POINT('Ctrl Pts',(-12.2478210638851,2.82332702783598,134.831519362437));
#76134=CARTESIAN_POINT('Ctrl Pts',(-12.2555781047701,2.93537198969854,134.752967810536));
#76135=CARTESIAN_POINT('Ctrl Pts',(-12.263335145655,3.04425335008034,134.669654576775));
#76136=CARTESIAN_POINT('Ctrl Pts',(-12.27109218654,3.14954410090022,134.581867072754));
#76137=CARTESIAN_POINT('Ctrl Pts',(-12.2788433777801,3.25475545114572,134.494145769972));
#76138=CARTESIAN_POINT('Ctrl Pts',(-12.2865945690203,3.35638128228575,134.401957162191));
#76139=CARTESIAN_POINT('Ctrl Pts',(-12.2943457602604,3.45402532255525,134.305630691931));
#76140=CARTESIAN_POINT('Ctrl Pts',(-12.3020936570375,3.55162786150302,134.209345162992));
#76141=CARTESIAN_POINT('Ctrl Pts',(-12.3098415538146,3.64525169782699,134.108925543494));
#76142=CARTESIAN_POINT('Ctrl Pts',(-12.3175894505916,3.73453546593352,134.004739956986));
#76143=CARTESIAN_POINT('Ctrl Pts',(-12.3253357266757,3.82380055780049,133.900576163856));
#76144=CARTESIAN_POINT('Ctrl Pts',(-12.3330820027598,3.90872713296511,133.792648267293));
#76145=CARTESIAN_POINT('Ctrl Pts',(-12.3408282788439,3.98899264946551,133.681359175962));
#76146=CARTESIAN_POINT('Ctrl Pts',(-12.3485746121093,4.06925875846772,133.570069263119));
#76147=CARTESIAN_POINT('Ctrl Pts',(-12.3563209453747,4.14486351144877,133.455418423095));
#76148=CARTESIAN_POINT('Ctrl Pts',(-12.36406727864,4.21552666042864,133.337840050622));
#76149=CARTESIAN_POINT('Ctrl Pts',(-12.371815346643,4.28620563393078,133.220235347286));
#76150=CARTESIAN_POINT('Ctrl Pts',(-12.379563414646,4.35194059999564,133.099702141972));
#76151=CARTESIAN_POINT('Ctrl Pts',(-12.387311482649,4.41249658680375,132.976699664295));
#76152=CARTESIAN_POINT('Ctrl Pts',(-12.3950677853908,4.47311693323527,132.853566458122));
#76153=CARTESIAN_POINT('Ctrl Pts',(-12.4028240881327,4.52854713205572,132.727959088441));
#76154=CARTESIAN_POINT('Ctrl Pts',(-12.4105803908746,4.57859961144396,132.600358574298));
#76155=CARTESIAN_POINT('Ctrl Pts',(-12.4183408333887,4.62867880534749,132.472689955919));
#76156=CARTESIAN_POINT('Ctrl Pts',(-12.4261012759029,4.67337443325303,132.343026442804));
#76157=CARTESIAN_POINT('Ctrl Pts',(-12.433861718417,4.71254873477078,132.211864608648));
#76158=CARTESIAN_POINT('Ctrl Pts',(-12.4416346186825,4.75178592235505,132.080492221871));
#76159=CARTESIAN_POINT('Ctrl Pts',(-12.4494075189479,4.7854839756431,131.947617086806));
#76160=CARTESIAN_POINT('Ctrl Pts',(-12.4571804192134,4.81355603320446,131.813747251964));
#76161=CARTESIAN_POINT('Ctrl Pts',(-12.4646707549753,4.84060760076405,131.684743922816));
#76162=CARTESIAN_POINT('Ctrl Pts',(-12.4721610907373,4.86243505829315,131.554817261762));
#76163=CARTESIAN_POINT('Ctrl Pts',(-12.4796514264993,4.87900640450117,131.424424781453));
#76164=CARTESIAN_POINT('Ctrl Pts',(-12.4874257606184,4.89620605833752,131.28908843062));
#76165=CARTESIAN_POINT('Ctrl Pts',(-12.4952000947375,4.90779764534939,131.152821535289));
#76166=CARTESIAN_POINT('Ctrl Pts',(-12.5029744288566,4.91368877761867,131.016128554715));
#76167=CARTESIAN_POINT('Ctrl Pts',(-12.5107391818037,4.91957264959392,130.879604036023));
#76168=CARTESIAN_POINT('Ctrl Pts',(-12.5185039347507,4.91977002840923,130.742654863755));
#76169=CARTESIAN_POINT('Ctrl Pts',(-12.5262686876978,4.91423992926441,130.605793298696));
#76170=CARTESIAN_POINT('Ctrl Pts',(-12.5340257285828,4.90871532269203,130.469067666472));
#76171=CARTESIAN_POINT('Ctrl Pts',(-12.5417827694678,4.89747457443633,130.332429856415));
#76172=CARTESIAN_POINT('Ctrl Pts',(-12.5495398103528,4.88052868371991,130.196394475509));
#76173=CARTESIAN_POINT('Ctrl Pts',(-12.5572910015929,4.86359557203149,130.060461679942));
#76174=CARTESIAN_POINT('Ctrl Pts',(-12.5650421928331,4.84096592946763,129.925130795673));
#76175=CARTESIAN_POINT('Ctrl Pts',(-12.5727933840732,4.81270273078517,129.790913289091));
#76176=CARTESIAN_POINT('Ctrl Pts',(-12.5805412808503,4.7844515447161,129.65675282853));
#76177=CARTESIAN_POINT('Ctrl Pts',(-12.5882891776274,4.75057164522366,129.523705186242));
#76178=CARTESIAN_POINT('Ctrl Pts',(-12.5960370744045,4.71117741814409,129.392273369104));
#76179=CARTESIAN_POINT('Ctrl Pts',(-12.6037833504886,4.67179143148759,129.260869044669));
#76180=CARTESIAN_POINT('Ctrl Pts',(-12.6115296265727,4.62689352375542,129.131080247359));
#76181=CARTESIAN_POINT('Ctrl Pts',(-12.6192759026568,4.57664833161018,129.003396122838));
#76182=CARTESIAN_POINT('Ctrl Pts',(-12.6270222359221,4.52640276856633,128.875711055782));
#76183=CARTESIAN_POINT('Ctrl Pts',(-12.6347685691875,4.47080998550864,128.750131056326));
#76184=CARTESIAN_POINT('Ctrl Pts',(-12.6425149024528,4.41008312882091,128.627126165471));
#76185=CARTESIAN_POINT('Ctrl Pts',(-12.6502629704558,4.34934267277468,128.504093728524));
#76186=CARTESIAN_POINT('Ctrl Pts',(-12.6580110384588,4.28346602828976,128.383637898203));
#76187=CARTESIAN_POINT('Ctrl Pts',(-12.6657591064618,4.21271255024126,128.26620458778));
#76188=CARTESIAN_POINT('Ctrl Pts',(-12.6735154092036,4.14188387455432,128.148646467837));
#76189=CARTESIAN_POINT('Ctrl Pts',(-12.6812717119455,4.06616821347661,128.034117620261));
#76190=CARTESIAN_POINT('Ctrl Pts',(-12.6890280146874,3.98586887480289,127.923035857082));
#76191=CARTESIAN_POINT('Ctrl Pts',(-12.6967884572015,3.90552667795436,127.811894806221));
#76192=CARTESIAN_POINT('Ctrl Pts',(-12.7045488997157,3.82059617074404,127.704204812573));
#76193=CARTESIAN_POINT('Ctrl Pts',(-12.7123093422299,3.73142067182779,127.600350188064));
#76194=CARTESIAN_POINT('Ctrl Pts',(-12.7200822424953,3.64210202048405,127.496328846893));
#76195=CARTESIAN_POINT('Ctrl Pts',(-12.7278551427607,3.54852502705781,127.396155464125));
#76196=CARTESIAN_POINT('Ctrl Pts',(-12.7356280430262,3.45107017642426,127.300177731372));
#76197=CARTESIAN_POINT('Ctrl Pts',(-12.7431183787882,3.3571580550848,127.207689030957));
#76198=CARTESIAN_POINT('Ctrl Pts',(-12.7506087145503,3.25964534938427,127.119096438817));
#76199=CARTESIAN_POINT('Ctrl Pts',(-12.7580990503123,3.1588996801951,127.034674175305));
#76200=CARTESIAN_POINT('Ctrl Pts',(-12.7658733844314,3.05433420833807,126.947051016014));
#76201=CARTESIAN_POINT('Ctrl Pts',(-12.7736477185505,2.94595454593777,126.86364310014));
#76202=CARTESIAN_POINT('Ctrl Pts',(-12.7814220526696,2.83413517092457,126.784800828805));
#76203=CARTESIAN_POINT('Ctrl Pts',(-12.7891868056167,2.72245360329749,126.706055723522));
#76204=CARTESIAN_POINT('Ctrl Pts',(-12.7969515585638,2.60734107413781,126.631865290355));
#76205=CARTESIAN_POINT('Ctrl Pts',(-12.8047163115108,2.48920640966427,126.562540900441));
#76206=CARTESIAN_POINT('Ctrl Pts',(-12.8124733523958,2.37118907820505,126.49328536449));
#76207=CARTESIAN_POINT('Ctrl Pts',(-12.8202303932809,2.25015591981789,126.428886450452));
#76208=CARTESIAN_POINT('Ctrl Pts',(-12.8279874341659,2.1265458332809,126.369613062016));
#76209=CARTESIAN_POINT('Ctrl Pts',(-12.835738625406,2.00302896207155,126.310384372103));
#76210=CARTESIAN_POINT('Ctrl Pts',(-12.8434898166461,1.87693938180032,126.256273682709));
#76211=CARTESIAN_POINT('Ctrl Pts',(-12.8512410078862,1.74874144302091,126.207504471463));
#76212=CARTESIAN_POINT('Ctrl Pts',(-12.8589889046633,1.62059799178526,126.158755988434));
#76213=CARTESIAN_POINT('Ctrl Pts',(-12.8667368014404,1.49034832898483,126.115344606879));
#76214=CARTESIAN_POINT('Ctrl Pts',(-12.8744846982175,1.35847747689028,126.07744597826));
#76215=CARTESIAN_POINT('Ctrl Pts',(-12.8822309743016,1.22663420933517,126.039555277217));
#76216=CARTESIAN_POINT('Ctrl Pts',(-12.8899772503857,1.09317080252731,126.007175143354));
#76217=CARTESIAN_POINT('Ctrl Pts',(-12.8977235264698,0.958587778703766,
125.980431458362));
#76218=CARTESIAN_POINT('Ctrl Pts',(-12.9054698597352,0.824003761418909,
125.953687575954));
#76219=CARTESIAN_POINT('Ctrl Pts',(-12.9132161930005,0.688300494094021,
125.932580301642));
#76220=CARTESIAN_POINT('Ctrl Pts',(-12.9209625262659,0.551988646362799,
125.917184377979));
#76221=CARTESIAN_POINT('Ctrl Pts',(-12.9287105942688,0.415646272538399,
125.901785006505));
#76222=CARTESIAN_POINT('Ctrl Pts',(-12.9364586622718,0.278695435532305,
125.892099574648));
#76223=CARTESIAN_POINT('Ctrl Pts',(-12.9442067302748,0.141651482454169,
125.888150906822));
#76224=CARTESIAN_POINT('Ctrl Pts',(-12.9519630330166,0.00446187743204438,
125.884198042303));
#76225=CARTESIAN_POINT('Ctrl Pts',(-12.9597193357585,-0.132820649928944,
125.88599413271));
#76226=CARTESIAN_POINT('Ctrl Pts',(-12.9674756385003,-0.269680637264103,
125.89350983421));
#76227=CARTESIAN_POINT('Ctrl Pts',(-12.9752360810145,-0.406613670895464,
125.901029547067));
#76228=CARTESIAN_POINT('Ctrl Pts',(-12.9829965235287,-0.543123326181341,
125.914274916099));
#76229=CARTESIAN_POINT('Ctrl Pts',(-12.9907569660429,-0.678700698492902,
125.933164827581));
#76230=CARTESIAN_POINT('Ctrl Pts',(-12.9985298663083,-0.814495711638491,
125.952085062827));
#76231=CARTESIAN_POINT('Ctrl Pts',(-13.0063027665737,-0.949355066310625,
125.976667877378));
#76232=CARTESIAN_POINT('Ctrl Pts',(-13.0140756668392,-1.08278057834101,
126.006781094341));
#76233=CARTESIAN_POINT('Ctrl Pts',(-13.0215660026012,-1.21135573692979,
126.035799620017));
#76234=CARTESIAN_POINT('Ctrl Pts',(-13.0290563383631,-1.33859919308061,
126.069953360979));
#76235=CARTESIAN_POINT('Ctrl Pts',(-13.0365466741251,-1.46408152938058,
126.109081250177));
#76236=CARTESIAN_POINT('Ctrl Pts',(-13.0443210082442,-1.59432156660144,
126.149692685187));
#76237=CARTESIAN_POINT('Ctrl Pts',(-13.0520953423633,-1.72307686330869,
126.195791548754));
#76238=CARTESIAN_POINT('Ctrl Pts',(-13.0598696764824,-1.84985020264719,
126.247252182356));
#76239=CARTESIAN_POINT('Ctrl Pts',(-13.0676344294294,-1.97646730517485,
126.298649395325));
#76240=CARTESIAN_POINT('Ctrl Pts',(-13.0753991823765,-2.10110695157109,
126.355395084934));
#76241=CARTESIAN_POINT('Ctrl Pts',(-13.0831639353236,-2.22328619592103,
126.417313597813));
#76242=CARTESIAN_POINT('Ctrl Pts',(-13.0909209762086,-2.34534409012306,
126.479170612351));
#76243=CARTESIAN_POINT('Ctrl Pts',(-13.0986780170935,-2.46494609888223,
126.546190050271));
#76244=CARTESIAN_POINT('Ctrl Pts',(-13.1064350579785,-2.58162875040061,
126.618148002611));
#76245=CARTESIAN_POINT('Ctrl Pts',(-13.1141862492186,-2.69822341062366,
126.6900516909));
#76246=CARTESIAN_POINT('Ctrl Pts',(-13.1219374404587,-2.81190276415101,
126.766886276479));
#76247=CARTESIAN_POINT('Ctrl Pts',(-13.1296886316989,-2.92222780010617,
126.848381883196));
#76248=CARTESIAN_POINT('Ctrl Pts',(-13.1374365284759,-3.03250594497834,
126.929842852106));
#76249=CARTESIAN_POINT('Ctrl Pts',(-13.145184425253,-3.13943229402284,127.01596067017));
#76250=CARTESIAN_POINT('Ctrl Pts',(-13.1529323220301,-3.24259690030668,
127.10642221832));
#76251=CARTESIAN_POINT('Ctrl Pts',(-13.1606785981142,-3.34573992677886,
127.196864843863));
#76252=CARTESIAN_POINT('Ctrl Pts',(-13.1684248741983,-3.44512248185581,
127.291649134609));
#76253=CARTESIAN_POINT('Ctrl Pts',(-13.1761711502824,-3.54036811320998,
127.390422029151));
#76254=CARTESIAN_POINT('Ctrl Pts',(-13.1839174835478,-3.63561444764578,
127.489195652813));
#76255=CARTESIAN_POINT('Ctrl Pts',(-13.1916638168131,-3.7267235260394,127.59195765759));
#76256=CARTESIAN_POINT('Ctrl Pts',(-13.1994101500785,-3.81335643595306,
127.698318802832));
#76257=CARTESIAN_POINT('Ctrl Pts',(-13.2071582180815,-3.90000874670622,
127.804703766915));
#76258=CARTESIAN_POINT('Ctrl Pts',(-13.2149062860844,-3.9821826474452,127.914689172239));
#76259=CARTESIAN_POINT('Ctrl Pts',(-13.2226543540874,-4.05958037764347,
128.027853779838));
#76260=CARTESIAN_POINT('Ctrl Pts',(-13.2304106568292,-4.13706036707044,
128.141138660128));
#76261=CARTESIAN_POINT('Ctrl Pts',(-13.2381669595711,-4.20975382469447,
128.257609169177));
#76262=CARTESIAN_POINT('Ctrl Pts',(-13.2459232623129,-4.27740681831236,
128.37681577284));
#76263=CARTESIAN_POINT('Ctrl Pts',(-13.2536837048271,-4.34509592036993,
128.496086000657));
#76264=CARTESIAN_POINT('Ctrl Pts',(-13.2614441473412,-4.40773901939108,
128.618094885301));
#76265=CARTESIAN_POINT('Ctrl Pts',(-13.2692045898554,-4.46512928326653,
128.742370426945));
#76266=CARTESIAN_POINT('Ctrl Pts',(-13.2769774901208,-4.52261167508842,
128.866845466722));
#76267=CARTESIAN_POINT('Ctrl Pts',(-13.2847503903863,-4.57482423230856,
128.993594072956));
#76268=CARTESIAN_POINT('Ctrl Pts',(-13.2925232906517,-4.62160887837857,
129.122125664359));
#76269=CARTESIAN_POINT('Ctrl Pts',(-13.3000136264139,-4.66669278472115,
129.245984808664));
#76270=CARTESIAN_POINT('Ctrl Pts',(-13.307503962176,-4.70673647130985,129.37149926329));
#76271=CARTESIAN_POINT('Ctrl Pts',(-13.3149942979381,-4.74164333781551,
129.498220686529));
#76272=CARTESIAN_POINT('Ctrl Pts',(-13.3166505309442,-4.74936180415442,
129.52624081946));
#76273=CARTESIAN_POINT('Ctrl Pts',(-13.3183067639504,-4.75683259252767,
129.554331901597));
#76274=CARTESIAN_POINT('Ctrl Pts',(-13.3199629969565,-4.76405452823408,
129.582490119308));
#76275=CARTESIAN_POINT('Origin',(213.235140564004,0.,130.804360617566));
#76276=CARTESIAN_POINT('',(-15.4150128089233,-4.76405452823406,129.582490119308));
#76277=CARTESIAN_POINT('',(-15.0701040894034,-4.76405452823398,129.582490119308));
#76278=CARTESIAN_POINT('',(213.235140564004,-4.76405452823405,129.582490119308));
#76279=CARTESIAN_POINT('',(-13.7351405640513,-4.91824955803034,130.806445667775));
#76280=CARTESIAN_POINT('Ctrl Pts',(-13.7351405640514,-4.91824955803034,
130.806445667775));
#76281=CARTESIAN_POINT('Ctrl Pts',(-13.7435813121526,-4.91818605641123,
130.956234295773));
#76282=CARTESIAN_POINT('Ctrl Pts',(-13.7520220602538,-4.91127554223146,
131.10580378366));
#76283=CARTESIAN_POINT('Ctrl Pts',(-13.7604628083551,-4.89760274164466,
131.25454996388));
#76284=CARTESIAN_POINT('Ctrl Pts',(-13.7689420453452,-4.88386759458144,
131.403974410426));
#76285=CARTESIAN_POINT('Ctrl Pts',(-13.7774212823353,-4.86330843507531,
131.552567763333));
#76286=CARTESIAN_POINT('Ctrl Pts',(-13.7859005193255,-4.83606167266655,
131.699732361964));
#76287=CARTESIAN_POINT('Ctrl Pts',(-13.7943993943312,-4.80875180642613,
131.847237795586));
#76288=CARTESIAN_POINT('Ctrl Pts',(-13.8028982693369,-4.77472344426176,
131.993307603379));
#76289=CARTESIAN_POINT('Ctrl Pts',(-13.8113971443426,-4.73416301053937,
132.137358611616));
#76290=CARTESIAN_POINT('Ctrl Pts',(-13.8199248935822,-4.69346477605517,
132.281899021391));
#76291=CARTESIAN_POINT('Ctrl Pts',(-13.8284526428218,-4.64619013709462,
132.424406650554));
#76292=CARTESIAN_POINT('Ctrl Pts',(-13.8369803920614,-4.59257492080349,
132.564314781545));
#76293=CARTESIAN_POINT('Ctrl Pts',(-13.8420871111757,-4.56046822510214,
132.648096739329));
#76294=CARTESIAN_POINT('Ctrl Pts',(-13.84719383029,-4.52608867497823,132.730946953886));
#76295=CARTESIAN_POINT('Ctrl Pts',(-13.8523005494044,-4.48949472028319,
132.812748084926));
#76296=CARTESIAN_POINT('Ctrl Pts',(-13.8600748835235,-4.43378505147807,
132.937279963378));
#76297=CARTESIAN_POINT('Ctrl Pts',(-13.8678492176427,-4.37280172328451,
133.059689380234));
#76298=CARTESIAN_POINT('Ctrl Pts',(-13.8756235517618,-4.30672824035703,
133.179497440196));
#76299=CARTESIAN_POINT('Ctrl Pts',(-13.8833883047089,-4.24073618709209,
133.299157847431));
#76300=CARTESIAN_POINT('Ctrl Pts',(-13.8911530576561,-4.16966664780707,
133.416222937569));
#76301=CARTESIAN_POINT('Ctrl Pts',(-13.8989178106032,-4.09375108654948,
133.530233891193));
#76302=CARTESIAN_POINT('Ctrl Pts',(-13.9066748514882,-4.01791092569755,
133.644131607531));
#76303=CARTESIAN_POINT('Ctrl Pts',(-13.9144318923733,-3.93723453651853,
133.754980900662));
#76304=CARTESIAN_POINT('Ctrl Pts',(-13.9221889332583,-3.85199900083047,
133.862347988387));
#76305=CARTESIAN_POINT('Ctrl Pts',(-13.9299401244985,-3.7668277419229,133.969634109756));
#76306=CARTESIAN_POINT('Ctrl Pts',(-13.9376913157386,-3.67710442191587,
134.073442947563));
#76307=CARTESIAN_POINT('Ctrl Pts',(-13.9454425069788,-3.58314887903189,
134.173370438447));
#76308=CARTESIAN_POINT('Ctrl Pts',(-13.9531904037559,-3.48923326975984,
134.273255457482));
#76309=CARTESIAN_POINT('Ctrl Pts',(-13.9609383005331,-3.3910892825532,134.369262126435));
#76310=CARTESIAN_POINT('Ctrl Pts',(-13.9686861973102,-3.28907626317128,
134.461020349828));
#76311=CARTESIAN_POINT('Ctrl Pts',(-13.9764324733943,-3.18708458271387,
134.552759379378));
#76312=CARTESIAN_POINT('Ctrl Pts',(-13.9841787494784,-3.08122577035307,
134.640251469715));
#76313=CARTESIAN_POINT('Ctrl Pts',(-13.9919250255626,-2.9718948786092,134.723164503064));
#76314=CARTESIAN_POINT('Ctrl Pts',(-13.999671358828,-2.86256317980953,134.806078148459));
#76315=CARTESIAN_POINT('Ctrl Pts',(-14.0074176920934,-2.74975966200026,
134.884412433173));
#76316=CARTESIAN_POINT('Ctrl Pts',(-14.0151640253588,-2.63391086992769,
134.957876789652));
#76317=CARTESIAN_POINT('Ctrl Pts',(-14.0229120933618,-2.51803613432153,
135.031357597964));
#76318=CARTESIAN_POINT('Ctrl Pts',(-14.0306601613648,-2.39911509752582,
135.099966098564));
#76319=CARTESIAN_POINT('Ctrl Pts',(-14.0384082293678,-2.27760121823524,
135.163456367053));
#76320=CARTESIAN_POINT('Ctrl Pts',(-14.0461645321097,-2.15595819254754,
135.227014113755));
#76321=CARTESIAN_POINT('Ctrl Pts',(-14.0539208348516,-2.0317171666187,135.285442580582));
#76322=CARTESIAN_POINT('Ctrl Pts',(-14.0616771375934,-1.90535451976567,
135.338542706599));
#76323=CARTESIAN_POINT('Ctrl Pts',(-14.0694375801077,-1.77892442936332,
135.391671173752));
#76324=CARTESIAN_POINT('Ctrl Pts',(-14.0771980226219,-1.65037082796646,
135.439465497214));
#76325=CARTESIAN_POINT('Ctrl Pts',(-14.0849584651361,-1.52018684039753,
135.481776039867));
#76326=CARTESIAN_POINT('Ctrl Pts',(-14.0927313654016,-1.38979386993457,
135.52415450316));
#76327=CARTESIAN_POINT('Ctrl Pts',(-14.1005042656671,-1.25776565998818,
135.561031489105));
#76328=CARTESIAN_POINT('Ctrl Pts',(-14.1082771659326,-1.12460802832807,
135.592307969524));
#76329=CARTESIAN_POINT('Ctrl Pts',(-14.1157675016941,-0.996291011992013,
135.622447471096));
#76330=CARTESIAN_POINT('Ctrl Pts',(-14.1232578374556,-0.866925565409542,
135.647386524473));
#76331=CARTESIAN_POINT('Ctrl Pts',(-14.1307481732171,-0.736968301537565,
135.667082158538));
#76332=CARTESIAN_POINT('Ctrl Pts',(-14.1385225073362,-0.602083668497659,
135.687524558555));
#76333=CARTESIAN_POINT('Ctrl Pts',(-14.1462968414552,-0.466134180793593,
135.702382837235));
#76334=CARTESIAN_POINT('Ctrl Pts',(-14.1540711755743,-0.329621935351554,
135.711552527634));
#76335=CARTESIAN_POINT('Ctrl Pts',(-14.1618359285214,-0.193277929051758,
135.720710917209));
#76336=CARTESIAN_POINT('Ctrl Pts',(-14.1696006814684,-0.0563729313104023,
135.724194641708));
#76337=CARTESIAN_POINT('Ctrl Pts',(-14.1773654344155,0.0805819281306172,
135.721950435288));
#76338=CARTESIAN_POINT('Ctrl Pts',(-14.1851224753005,0.2174007620747,135.719708457845));
#76339=CARTESIAN_POINT('Ctrl Pts',(-14.1928795161855,0.354268970781614,
135.711749877337));
#76340=CARTESIAN_POINT('Ctrl Pts',(-14.2006365570705,0.49067183151094,135.698073340669));
#76341=CARTESIAN_POINT('Ctrl Pts',(-14.2083877483106,0.62697182978193,135.684407117584));
#76342=CARTESIAN_POINT('Ctrl Pts',(-14.2161389395507,0.762806791124726,
135.665031559873));
#76343=CARTESIAN_POINT('Ctrl Pts',(-14.2238901307908,0.897663885218503,
135.639997350373));
#76344=CARTESIAN_POINT('Ctrl Pts',(-14.2316380275678,1.03246366144986,135.61497378108));
#76345=CARTESIAN_POINT('Ctrl Pts',(-14.2393859243449,1.16628601347475,135.584296414724));
#76346=CARTESIAN_POINT('Ctrl Pts',(-14.247133821122,1.2986253343243,135.548067533423));
#76347=CARTESIAN_POINT('Ctrl Pts',(-14.254880097206,1.43093697264083,135.511846230423));
#76348=CARTESIAN_POINT('Ctrl Pts',(-14.2626263732902,1.56176581997155,135.470075825448));
#76349=CARTESIAN_POINT('Ctrl Pts',(-14.2703726493743,1.69061892068953,135.422909169601));
#76350=CARTESIAN_POINT('Ctrl Pts',(-14.2781189826396,1.81947297257183,135.375742165581));
#76351=CARTESIAN_POINT('Ctrl Pts',(-14.2858653159049,1.94635088159795,135.323178965597));
#76352=CARTESIAN_POINT('Ctrl Pts',(-14.2936116491703,2.07077762720103,135.265421374963));
#76353=CARTESIAN_POINT('Ctrl Pts',(-14.3013597171732,2.19523223731107,135.207650849916));
#76354=CARTESIAN_POINT('Ctrl Pts',(-14.3091077851762,2.31723423715463,135.144683784072));
#76355=CARTESIAN_POINT('Ctrl Pts',(-14.3168558531792,2.43633161806993,135.076768756929));
#76356=CARTESIAN_POINT('Ctrl Pts',(-14.324612155921,2.55555557709895,135.008781548886));
#76357=CARTESIAN_POINT('Ctrl Pts',(-14.3323684586629,2.67186841029072,134.9358360686));
#76358=CARTESIAN_POINT('Ctrl Pts',(-14.3401247614047,2.78484514738517,134.858225510182));
#76359=CARTESIAN_POINT('Ctrl Pts',(-14.3478852039189,2.89788218356603,134.780573528673));
#76360=CARTESIAN_POINT('Ctrl Pts',(-14.355645646433,3.00757926315111,134.698251742264));
#76361=CARTESIAN_POINT('Ctrl Pts',(-14.3634060889472,3.11354394618366,134.611594148318));
#76362=CARTESIAN_POINT('Ctrl Pts',(-14.3711789892126,3.21967873313237,134.524797443909));
#76363=CARTESIAN_POINT('Ctrl Pts',(-14.3789518894781,3.32206885826284,134.433651283324));
#76364=CARTESIAN_POINT('Ctrl Pts',(-14.3867247897435,3.42035759950287,134.338527698226));
#76365=CARTESIAN_POINT('Ctrl Pts',(-14.3942151255057,3.51507329742683,134.246862095047));
#76366=CARTESIAN_POINT('Ctrl Pts',(-14.4017054612679,3.60598041315651,134.151503448529));
#76367=CARTESIAN_POINT('Ctrl Pts',(-14.4091957970301,3.69279598341738,134.052812693149));
#76368=CARTESIAN_POINT('Ctrl Pts',(-14.4169701311492,3.78290319240956,133.950380047784));
#76369=CARTESIAN_POINT('Ctrl Pts',(-14.4247444652682,3.86888790192637,133.844033156049));
#76370=CARTESIAN_POINT('Ctrl Pts',(-14.4325187993873,3.9503908253163,133.734137979373));
#76371=CARTESIAN_POINT('Ctrl Pts',(-14.4402835523344,4.03179330363728,133.624378238681));
#76372=CARTESIAN_POINT('Ctrl Pts',(-14.4480483052815,4.10872475509251,133.511079224916));
#76373=CARTESIAN_POINT('Ctrl Pts',(-14.4558130582286,4.18086408750844,133.394642174517));
#76374=CARTESIAN_POINT('Ctrl Pts',(-14.4635700991136,4.25293177012242,133.278320771038));
#76375=CARTESIAN_POINT('Ctrl Pts',(-14.4713271399986,4.32021660094008,133.15886786358));
#76376=CARTESIAN_POINT('Ctrl Pts',(-14.4790841808836,4.38243922135144,133.036715771582));
#76377=CARTESIAN_POINT('Ctrl Pts',(-14.4868353721237,4.44461491920074,132.914655795426));
#76378=CARTESIAN_POINT('Ctrl Pts',(-14.4945865633638,4.50173582831291,132.789901033185));
#76379=CARTESIAN_POINT('Ctrl Pts',(-14.5023377546039,4.55356739228051,132.662910338843));
#76380=CARTESIAN_POINT('Ctrl Pts',(-14.510085651381,4.60537692645076,132.535973618934));
#76381=CARTESIAN_POINT('Ctrl Pts',(-14.5178335481581,4.65190143936944,132.406803218278));
#76382=CARTESIAN_POINT('Ctrl Pts',(-14.5255814449351,4.69295369096224,132.27587980432));
#76383=CARTESIAN_POINT('Ctrl Pts',(-14.5333277210192,4.73399735530899,132.144983776717));
#76384=CARTESIAN_POINT('Ctrl Pts',(-14.5410739971033,4.76957091825835,132.012335838004));
#76385=CARTESIAN_POINT('Ctrl Pts',(-14.5488202731874,4.79953652321572,131.878433345466));
#76386=CARTESIAN_POINT('Ctrl Pts',(-14.5565666064528,4.82950234937237,131.74452986449));
#76387=CARTESIAN_POINT('Ctrl Pts',(-14.5643129397182,4.85386004955198,131.609372192738));
#76388=CARTESIAN_POINT('Ctrl Pts',(-14.5720592729835,4.87252264806201,131.473469059168));
#76389=CARTESIAN_POINT('Ctrl Pts',(-14.5798073409865,4.89118942593156,131.337535491033));
#76390=CARTESIAN_POINT('Ctrl Pts',(-14.5875554089894,4.90415851109684,131.200856516144));
#76391=CARTESIAN_POINT('Ctrl Pts',(-14.5953034769923,4.9113947188073,131.063946785479));
#76392=CARTESIAN_POINT('Ctrl Pts',(-14.6030597797342,4.91863861724543,130.926891545523));
#76393=CARTESIAN_POINT('Ctrl Pts',(-14.610816082476,4.92013744619596,130.789605450921));
#76394=CARTESIAN_POINT('Ctrl Pts',(-14.6185723852178,4.91590817136375,130.652604519767));
#76395=CARTESIAN_POINT('Ctrl Pts',(-14.626332827732,4.91167663924023,130.515530467092));
#76396=CARTESIAN_POINT('Ctrl Pts',(-14.6340932702462,4.90171093987623,130.378742270879));
#76397=CARTESIAN_POINT('Ctrl Pts',(-14.6418537127604,4.88607995132916,130.242750635711));
#76398=CARTESIAN_POINT('Ctrl Pts',(-14.6496266130258,4.87042387053163,130.106540694697));
#76399=CARTESIAN_POINT('Ctrl Pts',(-14.6573995132912,4.84908438788826,129.97113025642));
#76400=CARTESIAN_POINT('Ctrl Pts',(-14.6651724135566,4.82218168718184,129.837020533465));
#76401=CARTESIAN_POINT('Ctrl Pts',(-14.6726627493187,4.79625696740963,129.70778603674));
#76402=CARTESIAN_POINT('Ctrl Pts',(-14.6801530850808,4.76516655397933,129.579759627948));
#76403=CARTESIAN_POINT('Ctrl Pts',(-14.6876434208429,4.72906116272469,129.453374466005));
#76404=CARTESIAN_POINT('Ctrl Pts',(-14.695417754962,4.691586824587,129.322197372235));
#76405=CARTESIAN_POINT('Ctrl Pts',(-14.7031920890811,4.64859100845695,129.192372908255));
#76406=CARTESIAN_POINT('Ctrl Pts',(-14.7109664232002,4.60018740483834,129.064401163192));
#76407=CARTESIAN_POINT('Ctrl Pts',(-14.7187311761473,4.55184345433523,128.936587131867));
#76408=CARTESIAN_POINT('Ctrl Pts',(-14.7264959290943,4.49810511392687,128.810621638524));
#76409=CARTESIAN_POINT('Ctrl Pts',(-14.7342606820414,4.43913639702931,128.686991705196));
#76410=CARTESIAN_POINT('Ctrl Pts',(-14.7420177229264,4.38022624869268,128.563484562861));
#76411=CARTESIAN_POINT('Ctrl Pts',(-14.7497747638115,4.31609622914609,128.442308714808));
#76412=CARTESIAN_POINT('Ctrl Pts',(-14.7575318046965,4.24695906082515,128.323932872564));
#76413=CARTESIAN_POINT('Ctrl Pts',(-14.7652829959366,4.17787402938064,128.205646298463));
#76414=CARTESIAN_POINT('Ctrl Pts',(-14.7730341871767,4.10378956129934,128.090155863583));
#76415=CARTESIAN_POINT('Ctrl Pts',(-14.7807853784168,4.02496491996688,127.977906928659));
#76416=CARTESIAN_POINT('Ctrl Pts',(-14.7885332751939,3.94617378120971,127.865705702527));
#76417=CARTESIAN_POINT('Ctrl Pts',(-14.7962811719711,3.8626467004984,127.756743555448));
#76418=CARTESIAN_POINT('Ctrl Pts',(-14.8040290687482,3.77468686913433,127.651437830296));
#76419=CARTESIAN_POINT('Ctrl Pts',(-14.8117753448323,3.68674543707079,127.546154132832));
#76420=CARTESIAN_POINT('Ctrl Pts',(-14.8195216209163,3.59437334915317,127.444525635847));
#76421=CARTESIAN_POINT('Ctrl Pts',(-14.8272678970004,3.49791453129496,127.346937155759));
#76422=CARTESIAN_POINT('Ctrl Pts',(-14.8350142302658,3.40145500139967,127.249347955295));
#76423=CARTESIAN_POINT('Ctrl Pts',(-14.8427605635311,3.30090895620719,127.155799109296));
#76424=CARTESIAN_POINT('Ctrl Pts',(-14.8505068967965,3.19665739131176,127.066638773304));
#76425=CARTESIAN_POINT('Ctrl Pts',(-14.8582549647995,3.09238248000135,126.977458470473));
#76426=CARTESIAN_POINT('Ctrl Pts',(-14.8660030328025,2.98440069479634,126.892668887323));
#76427=CARTESIAN_POINT('Ctrl Pts',(-14.8737511008054,2.87312600792428,126.812577807206));
#76428=CARTESIAN_POINT('Ctrl Pts',(-14.8815074035473,2.76173305699068,126.732401605335));
#76429=CARTESIAN_POINT('Ctrl Pts',(-14.8892637062891,2.64704053111599,126.656934110558));
#76430=CARTESIAN_POINT('Ctrl Pts',(-14.897020009031,2.52949174131606,126.586439969532));
#76431=CARTESIAN_POINT('Ctrl Pts',(-14.9047804515452,2.41188021218753,126.51590820366));
#76432=CARTESIAN_POINT('Ctrl Pts',(-14.9125408940594,2.29140972473817,126.450355267487));
#76433=CARTESIAN_POINT('Ctrl Pts',(-14.9203013365736,2.16854717946969,126.389999260256));
#76434=CARTESIAN_POINT('Ctrl Pts',(-14.928074236839,2.04548740433648,126.329546364203));
#76435=CARTESIAN_POINT('Ctrl Pts',(-14.9358471371045,1.92002825597656,126.274307225844));
#76436=CARTESIAN_POINT('Ctrl Pts',(-14.9436200373699,1.79265638100263,126.224451648804));
#76437=CARTESIAN_POINT('Ctrl Pts',(-14.9511103731319,1.66991479451543,126.176408447567));
#76438=CARTESIAN_POINT('Ctrl Pts',(-14.9586007088939,1.54539742301994,126.133364291742));
#76439=CARTESIAN_POINT('Ctrl Pts',(-14.9660910446558,1.41955016096979,126.095426512804));
#76440=CARTESIAN_POINT('Ctrl Pts',(-14.9738653787749,1.2889313617278,126.056050311446));
#76441=CARTESIAN_POINT('Ctrl Pts',(-14.9816397128939,1.15646607451228,126.022050615341));
#76442=CARTESIAN_POINT('Ctrl Pts',(-14.989414047013,1.02263649096341,125.993602083837));
#76443=CARTESIAN_POINT('Ctrl Pts',(-14.9971787999601,0.888971840415576,
125.965188612605));
#76444=CARTESIAN_POINT('Ctrl Pts',(-15.0049435529072,0.753946617715323,
125.942312774309));
#76445=CARTESIAN_POINT('Ctrl Pts',(-15.0127083058543,0.618059221551476,
125.925099827123));
#76446=CARTESIAN_POINT('Ctrl Pts',(-15.0204653467392,0.482306790665177,
125.907903976079));
#76447=CARTESIAN_POINT('Ctrl Pts',(-15.0282223876242,0.345694275792356,
125.896359872023));
#76448=CARTESIAN_POINT('Ctrl Pts',(-15.0359794285092,0.208730998887949,
125.890541895574));
#76449=CARTESIAN_POINT('Ctrl Pts',(-15.0437306197493,0.0718710070562605,
125.884728306506));
#76450=CARTESIAN_POINT('Ctrl Pts',(-15.0514818109894,-0.0653388312787332,
125.88463226662));
#76451=CARTESIAN_POINT('Ctrl Pts',(-15.0592330022295,-0.202383683323974,
125.890276378644));
#76452=CARTESIAN_POINT('Ctrl Pts',(-15.0669808990066,-0.339370287651492,
125.895918091769));
#76453=CARTESIAN_POINT('Ctrl Pts',(-15.0747287957836,-0.476191655343469,
125.907295088337));
#76454=CARTESIAN_POINT('Ctrl Pts',(-15.0824766925607,-0.612332781717113,
125.924377868935));
#76455=CARTESIAN_POINT('Ctrl Pts',(-15.0902229686448,-0.748445430301984,
125.941457076184));
#76456=CARTESIAN_POINT('Ctrl Pts',(-15.0979692447289,-0.883877732917281,
125.964239644828));
#76457=CARTESIAN_POINT('Ctrl Pts',(-15.105715520813,-1.01812003225422,125.992644222929));
#76458=CARTESIAN_POINT('Ctrl Pts',(-15.1134618540783,-1.15236332253714,
126.021049010706));
#76459=CARTESIAN_POINT('Ctrl Pts',(-15.1212081873436,-1.28541620951664,
126.055075809818));
#76460=CARTESIAN_POINT('Ctrl Pts',(-15.1289545206089,-1.41677984265017,
126.094592264456));
#76461=CARTESIAN_POINT('Ctrl Pts',(-15.1367025886119,-1.54817289375853,
126.13411756853));
#76462=CARTESIAN_POINT('Ctrl Pts',(-15.1444506566149,-1.67787556393353,
126.179134861832));
#76463=CARTESIAN_POINT('Ctrl Pts',(-15.1521987246178,-1.80540514422299,
126.229462222223));
#76464=CARTESIAN_POINT('Ctrl Pts',(-15.1599550273597,-1.93307026446818,
126.279843071132));
#76465=CARTESIAN_POINT('Ctrl Pts',(-15.1677113301015,-2.05855731693028,
126.335545117088));
#76466=CARTESIAN_POINT('Ctrl Pts',(-15.1754676328433,-2.18140402644909,
126.396338437961));
#76467=CARTESIAN_POINT('Ctrl Pts',(-15.1832280753575,-2.30431630295578,
126.45716420606));
#76468=CARTESIAN_POINT('Ctrl Pts',(-15.1909885178716,-2.42458508583469,
126.523086475831));
#76469=CARTESIAN_POINT('Ctrl Pts',(-15.1987489603858,-2.54177451089152,
126.593830318627));
#76470=CARTESIAN_POINT('Ctrl Pts',(-15.2065218606512,-2.65915205881689,
126.66468772572));
#76471=CARTESIAN_POINT('Ctrl Pts',(-15.2142947609166,-2.7734400445704,126.740381956848));
#76472=CARTESIAN_POINT('Ctrl Pts',(-15.222067661182,-2.88423256317253,126.820595365441));
#76473=CARTESIAN_POINT('Ctrl Pts',(-15.2295579969442,-2.99099749465696,
126.897892814589));
#76474=CARTESIAN_POINT('Ctrl Pts',(-15.2370483327064,-3.09451644282916,
126.979386388111));
#76475=CARTESIAN_POINT('Ctrl Pts',(-15.2445386684686,-3.19445808983532,
127.064758957658));
#76476=CARTESIAN_POINT('Ctrl Pts',(-15.2521993888874,-3.29667313602368,
127.152073519714));
#76477=CARTESIAN_POINT('Ctrl Pts',(-15.2598601093061,-3.39548998349483,
127.243739701335));
#76478=CARTESIAN_POINT('Ctrl Pts',(-15.2675208297248,-3.49050720138212,
127.3394590981));
#76479=CARTESIAN_POINT('Ctrl Pts',(-15.2751727470799,-3.58541523337387,
127.435068502083));
#76480=CARTESIAN_POINT('Ctrl Pts',(-15.2828246644349,-3.67653203411157,
127.534721579948));
#76481=CARTESIAN_POINT('Ctrl Pts',(-15.29047658179,-3.763488323915,127.63807909214));
#76482=CARTESIAN_POINT('Ctrl Pts',(-15.298121477469,-3.85036481948236,127.741341759741));
#76483=CARTESIAN_POINT('Ctrl Pts',(-15.305766373148,-3.93308813730865,127.848301796572));
#76484=CARTESIAN_POINT('Ctrl Pts',(-15.313411268827,-4.01132545497909,127.958582840448));
#76485=CARTESIAN_POINT('Ctrl Pts',(-15.3210509175266,-4.0895090754369,128.068788194298));
#76486=CARTESIAN_POINT('Ctrl Pts',(-15.3286905662262,-4.16321258705298,
128.182309694288));
#76487=CARTESIAN_POINT('Ctrl Pts',(-15.3363302149258,-4.23214348927605,
128.298738030527));
#76488=CARTESIAN_POINT('Ctrl Pts',(-15.3439670045153,-4.30104859436498,
128.415122793895));
#76489=CARTESIAN_POINT('Ctrl Pts',(-15.3516037941048,-4.36518443513168,
128.534411884905));
#76490=CARTESIAN_POINT('Ctrl Pts',(-15.3592405836943,-4.42430214705334,
128.656167522409));
#76491=CARTESIAN_POINT('Ctrl Pts',(-15.366875705914,-4.48340695157632,128.777896576535));
#76492=CARTESIAN_POINT('Ctrl Pts',(-15.3745108281337,-4.53749563414466,
128.902090741686));
#76493=CARTESIAN_POINT('Ctrl Pts',(-15.3821459503534,-4.58636587401425,
129.028288791266));
#76494=CARTESIAN_POINT('Ctrl Pts',(-15.3897827789429,-4.6352470358704,129.154515044787));
#76495=CARTESIAN_POINT('Ctrl Pts',(-15.3974196075324,-4.67890728089378,
129.282745700816));
#76496=CARTESIAN_POINT('Ctrl Pts',(-15.4050564361219,-4.71719300835156,
129.412501003791));
#76497=CARTESIAN_POINT('Ctrl Pts',(-15.4083752270557,-4.73383110932398,
129.468889688973));
#76498=CARTESIAN_POINT('Ctrl Pts',(-15.4116940179896,-4.74945482964605,
129.525566116095));
#76499=CARTESIAN_POINT('Ctrl Pts',(-15.4150128089234,-4.76405452823406,
129.582490119308));
#76500=CARTESIAN_POINT('Ctrl Pts',(-13.6653609210472,-4.76405452823398,
129.582490119308));
#76501=CARTESIAN_POINT('Ctrl Pts',(-13.6732618994108,-4.79879020631677,
129.717924000965));
#76502=CARTESIAN_POINT('Ctrl Pts',(-13.6811628777745,-4.82777218857766,
129.854940509252));
#76503=CARTESIAN_POINT('Ctrl Pts',(-13.6890638561381,-4.85086715689499,
129.993021669495));
#76504=CARTESIAN_POINT('Ctrl Pts',(-13.6969596860506,-4.87394707602353,
130.13101285302));
#76505=CARTESIAN_POINT('Ctrl Pts',(-13.7048555159631,-4.89114756217927,
130.270066943089));
#76506=CARTESIAN_POINT('Ctrl Pts',(-13.7127513458757,-4.90238621151786,
130.409655036633));
#76507=CARTESIAN_POINT('Ctrl Pts',(-13.7202144185867,-4.91300888932577,
130.541592540764));
#76508=CARTESIAN_POINT('Ctrl Pts',(-13.7276774912976,-4.91830570436068,
130.674006763662));
#76509=CARTESIAN_POINT('Ctrl Pts',(-13.7351405640086,-4.91824955803066,
130.806445667018));
#76510=CARTESIAN_POINT('',(-13.3898594359426,-4.91824795577628,130.79987642283));
#76511=CARTESIAN_POINT('Ctrl Pts',(-13.3199629969565,-4.76405452823408,
129.582490119308));
#76512=CARTESIAN_POINT('Ctrl Pts',(-13.3298371033895,-4.80711016204549,
129.750363382079));
#76513=CARTESIAN_POINT('Ctrl Pts',(-13.3397112098226,-4.84131703731055,
129.920624555717));
#76514=CARTESIAN_POINT('Ctrl Pts',(-13.3495853162557,-4.86645366289561,
130.092453454103));
#76515=CARTESIAN_POINT('Ctrl Pts',(-13.3592886505582,-4.89115555191633,
130.261310581092));
#76516=CARTESIAN_POINT('Ctrl Pts',(-13.3689919848608,-4.90709822462204,
130.431681817717));
#76517=CARTESIAN_POINT('Ctrl Pts',(-13.3786953191633,-4.91411671521435,
130.602767036937));
#76518=CARTESIAN_POINT('Ctrl Pts',(-13.3824166914231,-4.91680841019069,
130.668380749606));
#76519=CARTESIAN_POINT('Ctrl Pts',(-13.3861380636829,-4.91818798366446,
130.73409923568));
#76520=CARTESIAN_POINT('Ctrl Pts',(-13.3898594359427,-4.91824795577628,
130.79987642283));
#76521=CARTESIAN_POINT('Ctrl Pts',(-13.3898594359912,-4.91824795577706,
130.799876423688));
#76522=CARTESIAN_POINT('Ctrl Pts',(-13.3975363273454,-4.91837167339157,
130.935569464879));
#76523=CARTESIAN_POINT('Ctrl Pts',(-13.4052132186995,-4.91287556913946,
131.071391386066));
#76524=CARTESIAN_POINT('Ctrl Pts',(-13.4128901100537,-4.90175450304585,
131.206835280582));
#76525=CARTESIAN_POINT('Ctrl Pts',(-13.4205632856729,-4.89063881972146,
131.342213618143));
#76526=CARTESIAN_POINT('Ctrl Pts',(-13.4282364612921,-4.8739036210423,131.477213895897));
#76527=CARTESIAN_POINT('Ctrl Pts',(-13.4359096369112,-4.85159584056564,
131.611330791926));
#76528=CARTESIAN_POINT('Ctrl Pts',(-13.4435809797105,-4.82929338854051,
131.745415652702));
#76529=CARTESIAN_POINT('Ctrl Pts',(-13.4512523225096,-4.80142106671531,
131.878617157695));
#76530=CARTESIAN_POINT('Ctrl Pts',(-13.4589236653089,-4.76807743543659,
132.010437162475));
#76531=CARTESIAN_POINT('Ctrl Pts',(-13.4665949157291,-4.73473420568499,
132.142255579867));
#76532=CARTESIAN_POINT('Ctrl Pts',(-13.4742661661493,-4.69591989540284,
132.272692143006));
#76533=CARTESIAN_POINT('Ctrl Pts',(-13.4819374165695,-4.65178362366143,
132.401261422605));
#76534=CARTESIAN_POINT('Ctrl Pts',(-13.489610314709,-4.6076378718244,132.529858317792));
#76535=CARTESIAN_POINT('Ctrl Pts',(-13.4972832128486,-4.55816801480284,
132.65658675421));
#76536=CARTESIAN_POINT('Ctrl Pts',(-13.5049561109881,-4.50357205354791,
132.780979402512));
#76537=CARTESIAN_POINT('Ctrl Pts',(-13.5126370681599,-4.44891874882148,
132.905502703451));
#76538=CARTESIAN_POINT('Ctrl Pts',(-13.5203180253318,-4.38912874803837,
133.027684950592));
#76539=CARTESIAN_POINT('Ctrl Pts',(-13.5279989825036,-4.32444712998896,
133.147081275782));
#76540=CARTESIAN_POINT('Ctrl Pts',(-13.5356841167854,-4.25973033634509,
133.266542531887));
#76541=CARTESIAN_POINT('Ctrl Pts',(-13.5433692510673,-4.19011683222443,
133.383214506446));
#76542=CARTESIAN_POINT('Ctrl Pts',(-13.5510543853491,-4.11589548455543,
133.496680699339));
#76543=CARTESIAN_POINT('Ctrl Pts',(-13.5587516183043,-4.04155729054306,
133.610325521564));
#76544=CARTESIAN_POINT('Ctrl Pts',(-13.5664488512594,-3.96259699478743,
133.720754156435));
#76545=CARTESIAN_POINT('Ctrl Pts',(-13.5741460842146,-3.87934467018035,
133.827582076944));
#76546=CARTESIAN_POINT('Ctrl Pts',(-13.58057803006,-3.8097775352768,133.916849402422));
#76547=CARTESIAN_POINT('Ctrl Pts',(-13.5870099759055,-3.73721425178249,
134.003603028335));
#76548=CARTESIAN_POINT('Ctrl Pts',(-13.5934419217509,-3.66186656095311,
134.087638911021));
#76549=CARTESIAN_POINT('Ctrl Pts',(-13.60121625587,-3.57079332469017,134.1892136204));
#76550=CARTESIAN_POINT('Ctrl Pts',(-13.608990589989,-3.47534633594947,134.287156991757));
#76551=CARTESIAN_POINT('Ctrl Pts',(-13.6167649241081,-3.37584655978066,
134.381069029964));
#76552=CARTESIAN_POINT('Ctrl Pts',(-13.6245296770552,-3.27646940819343,
134.474865329976));
#76553=CARTESIAN_POINT('Ctrl Pts',(-13.6322944300024,-3.17304968873191,
134.564639916411));
#76554=CARTESIAN_POINT('Ctrl Pts',(-13.6400591829495,-3.06594790565478,
134.650026554996));
#76555=CARTESIAN_POINT('Ctrl Pts',(-13.6478162238345,-2.95895249757833,
134.735328386368));
#76556=CARTESIAN_POINT('Ctrl Pts',(-13.6555732647195,-2.84828260735985,
134.816250700704));
#76557=CARTESIAN_POINT('Ctrl Pts',(-13.6633303056045,-2.73433453379736,
134.892465034014));
#76558=CARTESIAN_POINT('Ctrl Pts',(-13.6710814968446,-2.62047238936337,
134.968621893503));
#76559=CARTESIAN_POINT('Ctrl Pts',(-13.6788326880847,-2.50333730581731,
135.040077622192));
#76560=CARTESIAN_POINT('Ctrl Pts',(-13.6865838793249,-2.38335722231097,
135.106545110746));
#76561=CARTESIAN_POINT('Ctrl Pts',(-13.694331776102,-2.26342813354102,135.172984348844));
#76562=CARTESIAN_POINT('Ctrl Pts',(-13.7020796728791,-2.14065679109562,
135.234439374532));
#76563=CARTESIAN_POINT('Ctrl Pts',(-13.7098275696562,-2.01549838337967,
135.290667487263));
#76564=CARTESIAN_POINT('Ctrl Pts',(-13.7175738457403,-1.89036615610433,
135.346883838286));
#76565=CARTESIAN_POINT('Ctrl Pts',(-13.7253201218245,-1.76284821314136,
135.397875290985));
#76566=CARTESIAN_POINT('Ctrl Pts',(-13.7330663979086,-1.63342214853847,
135.443446211427));
#76567=CARTESIAN_POINT('Ctrl Pts',(-13.7408127311739,-1.50399512854177,
135.489017468262));
#76568=CARTESIAN_POINT('Ctrl Pts',(-13.7485590644393,-1.37266032757259,
135.529167983153));
#76569=CARTESIAN_POINT('Ctrl Pts',(-13.7563053977047,-1.23991264123651,
135.563751303841));
#76570=CARTESIAN_POINT('Ctrl Pts',(-13.7640534657077,-1.10713522697667,
135.598342369224));
#76571=CARTESIAN_POINT('Ctrl Pts',(-13.7718015337106,-0.972944676003497,
135.627363661002));
#76572=CARTESIAN_POINT('Ctrl Pts',(-13.7795496017136,-0.83784788145648,
135.650719455915));
#76573=CARTESIAN_POINT('Ctrl Pts',(-13.7873059044555,-0.702607504428361,
135.674100073644));
#76574=CARTESIAN_POINT('Ctrl Pts',(-13.7950622071974,-0.566459345662321,
135.69180309949));
#76575=CARTESIAN_POINT('Ctrl Pts',(-13.8028185099393,-0.429917815269413,
135.703784434161));
#76576=CARTESIAN_POINT('Ctrl Pts',(-13.8105789524535,-0.293303408550549,
135.71577216363));
#76577=CARTESIAN_POINT('Ctrl Pts',(-13.8183393949676,-0.156295602219792,
135.722032099057));
#76578=CARTESIAN_POINT('Ctrl Pts',(-13.8260998374818,-0.0194096613690958,
135.722572317721));
#76579=CARTESIAN_POINT('Ctrl Pts',(-13.8338727377473,0.117696020946017,
135.723113403593));
#76580=CARTESIAN_POINT('Ctrl Pts',(-13.8416456380127,0.254679055942418,
135.717916439378));
#76581=CARTESIAN_POINT('Ctrl Pts',(-13.8494185382781,0.391027544433969,
135.707041570065));
#76582=CARTESIAN_POINT('Ctrl Pts',(-13.85690887404,0.522419421925151,135.696562029644));
#76583=CARTESIAN_POINT('Ctrl Pts',(-13.8643992098019,0.65322178086342,135.680810266229));
#76584=CARTESIAN_POINT('Ctrl Pts',(-13.8718895455638,0.782986693298438,
135.659884780889));
#76585=CARTESIAN_POINT('Ctrl Pts',(-13.8796638796829,0.917671681832088,
135.638165899413));
#76586=CARTESIAN_POINT('Ctrl Pts',(-13.887438213802,1.05166564289178,135.610804429205));
#76587=CARTESIAN_POINT('Ctrl Pts',(-13.8952125479211,1.18445855979839,135.577854200113));
#76588=CARTESIAN_POINT('Ctrl Pts',(-13.9029773008682,1.31708782130297,135.544944579235));
#76589=CARTESIAN_POINT('Ctrl Pts',(-13.9107420538153,1.44851860795529,135.506459997087));
#76590=CARTESIAN_POINT('Ctrl Pts',(-13.9185068067624,1.57824793513165,135.462505797544));
#76591=CARTESIAN_POINT('Ctrl Pts',(-13.9262638476474,1.70784841331139,135.418595253931));
#76592=CARTESIAN_POINT('Ctrl Pts',(-13.9340208885324,1.83575042712674,135.369226028493));
#76593=CARTESIAN_POINT('Ctrl Pts',(-13.9417779294174,1.96146342133941,135.31455399582));
#76594=CARTESIAN_POINT('Ctrl Pts',(-13.9495291206575,2.0870816144049,135.259923191753));
#76595=CARTESIAN_POINT('Ctrl Pts',(-13.9572803118977,2.21051371652188,135.199997695288));
#76596=CARTESIAN_POINT('Ctrl Pts',(-13.9650315031378,2.33128686291064,135.134982354144));
#76597=CARTESIAN_POINT('Ctrl Pts',(-13.9727793999148,2.45200867749061,135.069994646254));
#76598=CARTESIAN_POINT('Ctrl Pts',(-13.9805272966919,2.57007344054672,134.999921581297));
#76599=CARTESIAN_POINT('Ctrl Pts',(-13.988275193469,2.68503092078517,134.925014936594));
#76600=CARTESIAN_POINT('Ctrl Pts',(-13.9960214695531,2.7999643543968,134.850123960748));
#76601=CARTESIAN_POINT('Ctrl Pts',(-14.0037677456372,2.91179147067523,134.770401629557));
#76602=CARTESIAN_POINT('Ctrl Pts',(-14.0115140217212,3.02008952600336,134.6861440115));
#76603=CARTESIAN_POINT('Ctrl Pts',(-14.0192603549866,3.12838838076328,134.601885771473));
#76604=CARTESIAN_POINT('Ctrl Pts',(-14.0270066882519,3.23315781401694,134.513092417853));
#76605=CARTESIAN_POINT('Ctrl Pts',(-14.0347530215173,3.33400710816931,134.420101159305));
#76606=CARTESIAN_POINT('Ctrl Pts',(-14.0425010895202,3.43487898682174,134.32708907601));
#76607=CARTESIAN_POINT('Ctrl Pts',(-14.0502491575232,3.53182869210733,134.229877482093));
#76608=CARTESIAN_POINT('Ctrl Pts',(-14.0579972255262,3.62450170121326,134.128841100349));
#76609=CARTESIAN_POINT('Ctrl Pts',(-14.065753528268,3.71727320429623,134.027697335935));
#76610=CARTESIAN_POINT('Ctrl Pts',(-14.0735098310098,3.80575866673257,133.922720951939));
#76611=CARTESIAN_POINT('Ctrl Pts',(-14.0812661337517,3.88964293530966,133.814320899413));
#76612=CARTESIAN_POINT('Ctrl Pts',(-14.0890265762659,3.97357197544682,133.705862990514));
#76613=CARTESIAN_POINT('Ctrl Pts',(-14.0967870187801,4.05289470233521,133.593978090791));
#76614=CARTESIAN_POINT('Ctrl Pts',(-14.1045474612943,4.12733939825272,133.479104073326));
#76615=CARTESIAN_POINT('Ctrl Pts',(-14.1123203615597,4.2019035994049,133.36404564989));
#76616=CARTESIAN_POINT('Ctrl Pts',(-14.1200932618251,4.27157392263712,133.245988856886));
#76617=CARTESIAN_POINT('Ctrl Pts',(-14.1278661620905,4.33612427561852,133.125396879431));
#76618=CARTESIAN_POINT('Ctrl Pts',(-14.1353564978526,4.39832806067669,133.009188724109));
#76619=CARTESIAN_POINT('Ctrl Pts',(-14.1428468336146,4.45577752603527,132.890626782133));
#76620=CARTESIAN_POINT('Ctrl Pts',(-14.1503371693767,4.50831342743531,132.770141150206));
#76621=CARTESIAN_POINT('Ctrl Pts',(-14.1581115034957,4.56284124350458,132.645087268925));
#76622=CARTESIAN_POINT('Ctrl Pts',(-14.1658858376148,4.61224827263818,132.517564811591));
#76623=CARTESIAN_POINT('Ctrl Pts',(-14.1736601717339,4.65630412693997,132.388031966029));
#76624=CARTESIAN_POINT('Ctrl Pts',(-14.181424924681,4.70030568633866,132.258658758122));
#76625=CARTESIAN_POINT('Ctrl Pts',(-14.1891896776281,4.73896906799908,132.12728045831));
#76626=CARTESIAN_POINT('Ctrl Pts',(-14.1969544305751,4.77211102522948,131.994377182738));
#76627=CARTESIAN_POINT('Ctrl Pts',(-14.2047114714601,4.80522006540083,131.861605908572));
#76628=CARTESIAN_POINT('Ctrl Pts',(-14.2124685123451,4.83281850047766,131.727313049716));
#76629=CARTESIAN_POINT('Ctrl Pts',(-14.2202255532301,4.85477231508046,131.59199557821));
#76630=CARTESIAN_POINT('Ctrl Pts',(-14.2279767444702,4.87670957414084,131.456780150662));
#76631=CARTESIAN_POINT('Ctrl Pts',(-14.2357279357103,4.89301062297737,131.320542032771));
#76632=CARTESIAN_POINT('Ctrl Pts',(-14.2434791269504,4.90359221081424,131.183789784265));
#76633=CARTESIAN_POINT('Ctrl Pts',(-14.2512270237275,4.91416930119401,131.047095659112));
#76634=CARTESIAN_POINT('Ctrl Pts',(-14.2589749205045,4.91903173539689,130.909888226946));
#76635=CARTESIAN_POINT('Ctrl Pts',(-14.2667228172815,4.91814797980413,130.772682371899));
#76636=CARTESIAN_POINT('Ctrl Pts',(-14.2744690933656,4.91726440907399,130.635505217358));
#76637=CARTESIAN_POINT('Ctrl Pts',(-14.2822153694497,4.910637041867,130.49833002999));
#76638=CARTESIAN_POINT('Ctrl Pts',(-14.2899616455338,4.89828646572864,130.361672508216));
#76639=CARTESIAN_POINT('Ctrl Pts',(-14.2977079787992,4.88593579842112,130.225013977668));
#76640=CARTESIAN_POINT('Ctrl Pts',(-14.3054543120645,4.86786187307103,130.088873509717));
#76641=CARTESIAN_POINT('Ctrl Pts',(-14.3132006453299,4.84413720047614,129.953762095663));
#76642=CARTESIAN_POINT('Ctrl Pts',(-14.3209487133328,4.82040721490538,129.818620424346));
#76643=CARTESIAN_POINT('Ctrl Pts',(-14.3286967813357,4.79102403160295,129.684508650494));
#76644=CARTESIAN_POINT('Ctrl Pts',(-14.3364448493386,4.75611128722829,129.551927591013));
#76645=CARTESIAN_POINT('Ctrl Pts',(-14.3442011520805,4.72116143717333,129.419205622805));
#76646=CARTESIAN_POINT('Ctrl Pts',(-14.3519574548224,4.68067038605675,129.288017997479));
#76647=CARTESIAN_POINT('Ctrl Pts',(-14.3597137575642,4.63481184797063,129.15885091039));
#76648=CARTESIAN_POINT('Ctrl Pts',(-14.3674742000784,4.58892883380197,129.029614882938));
#76649=CARTESIAN_POINT('Ctrl Pts',(-14.3752346425925,4.53767277036861,128.902401905029));
#76650=CARTESIAN_POINT('Ctrl Pts',(-14.3829950851067,4.48126518263077,128.777677261577));
#76651=CARTESIAN_POINT('Ctrl Pts',(-14.3907679853721,4.42476704442539,128.652752399055));
#76652=CARTESIAN_POINT('Ctrl Pts',(-14.3985408856375,4.36310103242801,128.530324202637));
#76653=CARTESIAN_POINT('Ctrl Pts',(-14.4063137859029,4.2965346289699,128.410833253076));
#76654=CARTESIAN_POINT('Ctrl Pts',(-14.4138041216651,4.23238808194635,128.295686100508));
#76655=CARTESIAN_POINT('Ctrl Pts',(-14.4212944574273,4.16369140161882,128.183266612571));
#76656=CARTESIAN_POINT('Ctrl Pts',(-14.4287847931896,4.09072036511427,128.073941243745));
#76657=CARTESIAN_POINT('Ctrl Pts',(-14.4365591273086,4.01498260958352,127.960470770334));
#76658=CARTESIAN_POINT('Ctrl Pts',(-14.4443334614278,3.93440006068489,127.849974234345));
#76659=CARTESIAN_POINT('Ctrl Pts',(-14.4521077955469,3.84923367452668,127.742893129352));
#76660=CARTESIAN_POINT('Ctrl Pts',(-14.459872548494,3.76417224832787,127.635943992251));
#76661=CARTESIAN_POINT('Ctrl Pts',(-14.4676373014411,3.67453846606171,127.532402214114));
#76662=CARTESIAN_POINT('Ctrl Pts',(-14.4754020543882,3.58063721372605,127.432681480077));
#76663=CARTESIAN_POINT('Ctrl Pts',(-14.4831590952732,3.48682922543759,127.333059790078));
#76664=CARTESIAN_POINT('Ctrl Pts',(-14.4909161361583,3.38876246819827,127.237251874522));
#76665=CARTESIAN_POINT('Ctrl Pts',(-14.4986731770434,3.28678262007412,127.14563910987));
#76666=CARTESIAN_POINT('Ctrl Pts',(-14.5064243682835,3.18487967574659,127.054095431116));
#76667=CARTESIAN_POINT('Ctrl Pts',(-14.5141755595237,3.07906980377133,126.966740866538));
#76668=CARTESIAN_POINT('Ctrl Pts',(-14.5219267507639,2.96973587077239,126.883920346328));
#76669=CARTESIAN_POINT('Ctrl Pts',(-14.529674647541,2.86044840761215,126.801135027048));
#76670=CARTESIAN_POINT('Ctrl Pts',(-14.537422544318,2.74764017347205,126.722880154878));
#76671=CARTESIAN_POINT('Ctrl Pts',(-14.5451704410951,2.63172731026352,126.649460567395));
#76672=CARTESIAN_POINT('Ctrl Pts',(-14.5529167171793,2.51583869352686,126.576056337706));
#76673=CARTESIAN_POINT('Ctrl Pts',(-14.5606629932634,2.39684706953185,126.507485589972));
#76674=CARTESIAN_POINT('Ctrl Pts',(-14.5684092693475,2.27519743803797,126.444009750899));
#76675=CARTESIAN_POINT('Ctrl Pts',(-14.5761556026129,2.15354690855448,126.380533443262));
#76676=CARTESIAN_POINT('Ctrl Pts',(-14.5839019358782,2.02923867903652,126.322152300196));
#76677=CARTESIAN_POINT('Ctrl Pts',(-14.5916482691436,1.90274185479385,126.269081519592));
#76678=CARTESIAN_POINT('Ctrl Pts',(-14.5993963371466,1.77621670246445,126.215998854155));
#76679=CARTESIAN_POINT('Ctrl Pts',(-14.6071444051495,1.64750234057987,126.168229068814));
#76680=CARTESIAN_POINT('Ctrl Pts',(-14.6148924731525,1.51708694922172,126.125938848315));
#76681=CARTESIAN_POINT('Ctrl Pts',(-14.6226487758944,1.3865329508335,126.083603681267));
#76682=CARTESIAN_POINT('Ctrl Pts',(-14.6304050786364,1.25427468404155,126.046759833413));
#76683=CARTESIAN_POINT('Ctrl Pts',(-14.6381613813782,1.12081509547845,126.015523954633));
#76684=CARTESIAN_POINT('Ctrl Pts',(-14.6459218238924,0.987284275514368,
125.984271404325));
#76685=CARTESIAN_POINT('Ctrl Pts',(-14.6536822664065,0.852551240055837,
125.95863286023));
#76686=CARTESIAN_POINT('Ctrl Pts',(-14.6614427089207,0.717127186129043,
125.938673444985));
#76687=CARTESIAN_POINT('Ctrl Pts',(-14.6692156091862,0.581485737488688,
125.918681989116));
#76688=CARTESIAN_POINT('Ctrl Pts',(-14.6769885094517,0.445151442734468,
125.904387920843));
#76689=CARTESIAN_POINT('Ctrl Pts',(-14.6847614097172,0.308639555664589,
125.895804344365));
#76690=CARTESIAN_POINT('Ctrl Pts',(-14.692251745479,0.177090219546643,125.887532802513));
#76691=CARTESIAN_POINT('Ctrl Pts',(-14.6997420812408,0.0453762867405826,
125.884563786036));
#76692=CARTESIAN_POINT('Ctrl Pts',(-14.7072324170026,-0.0860448699480239,
125.886863353423));
#76693=CARTESIAN_POINT('Ctrl Pts',(-14.7150067511217,-0.222448899741297,
125.889250109607));
#76694=CARTESIAN_POINT('Ctrl Pts',(-14.7227810852407,-0.358969600910853,
125.897320413482));
#76695=CARTESIAN_POINT('Ctrl Pts',(-14.7305554193598,-0.495094479259071,
125.911093353344));
#76696=CARTESIAN_POINT('Ctrl Pts',(-14.7383201723069,-0.631051595860555,
125.924849319289));
#76697=CARTESIAN_POINT('Ctrl Pts',(-14.746084925254,-0.766613475004552,
125.944293898638));
#76698=CARTESIAN_POINT('Ctrl Pts',(-14.7538496782011,-0.901267273341114,
125.969394189089));
#76699=CARTESIAN_POINT('Ctrl Pts',(-14.7616067190861,-1.03578733162652,
125.994469549576));
#76700=CARTESIAN_POINT('Ctrl Pts',(-14.7693637599712,-1.16940072210564,
126.02518937124));
#76701=CARTESIAN_POINT('Ctrl Pts',(-14.7771208008562,-1.30159973452234,
126.061468968625));
#76702=CARTESIAN_POINT('Ctrl Pts',(-14.7848719920963,-1.43369905463559,
126.097721207284));
#76703=CARTESIAN_POINT('Ctrl Pts',(-14.7926231833364,-1.56438574417613,
126.13952477336));
#76704=CARTESIAN_POINT('Ctrl Pts',(-14.8003743745765,-1.69316265484348,
126.186743993512));
#76705=CARTESIAN_POINT('Ctrl Pts',(-14.8081222713536,-1.82188483188873,
126.233943144235));
#76706=CARTESIAN_POINT('Ctrl Pts',(-14.8158701681307,-1.94869847818551,
126.286553236623));
#76707=CARTESIAN_POINT('Ctrl Pts',(-14.8236180649078,-2.07312219037915,
126.344388930856));
#76708=CARTESIAN_POINT('Ctrl Pts',(-14.831364340992,-2.19751987581481,126.402212527108));
#76709=CARTESIAN_POINT('Ctrl Pts',(-14.8391106170761,-2.31952826721017,
126.465259386308));
#76710=CARTESIAN_POINT('Ctrl Pts',(-14.8468568931603,-2.43868688563124,
126.533296425078));
#76711=CARTESIAN_POINT('Ctrl Pts',(-14.8546032264256,-2.55784638365399,
126.601333966082));
#76712=CARTESIAN_POINT('Ctrl Pts',(-14.862349559691,-2.67415572720725,126.674361566302));
#76713=CARTESIAN_POINT('Ctrl Pts',(-14.8700958929564,-2.78718030133189,
126.752100873871));
#76714=CARTESIAN_POINT('Ctrl Pts',(-14.8778439609594,-2.90023018652624,
126.82985759062));
#76715=CARTESIAN_POINT('Ctrl Pts',(-14.8855920289624,-3.00999351646686,
126.912327892835));
#76716=CARTESIAN_POINT('Ctrl Pts',(-14.8933400969654,-3.11606618129598,
126.999191157965));
#76717=CARTESIAN_POINT('Ctrl Pts',(-14.9010963997073,-3.22225158141542,
127.086146742406));
#76718=CARTESIAN_POINT('Ctrl Pts',(-14.9088527024491,-3.32473817787577,
127.177504368281));
#76719=CARTESIAN_POINT('Ctrl Pts',(-14.916609005191,-3.42315597488899,127.272903944452));
#76720=CARTESIAN_POINT('Ctrl Pts',(-14.9243694477052,-3.52162630044404,
127.368354438249));
#76721=CARTESIAN_POINT('Ctrl Pts',(-14.9321298902195,-3.61602323041533,
127.467850897479));
#76722=CARTESIAN_POINT('Ctrl Pts',(-14.9398903327337,-3.70601566080439,
127.570998437981));
#76723=CARTESIAN_POINT('Ctrl Pts',(-14.9476632329991,-3.79615255503162,
127.674311560071));
#76724=CARTESIAN_POINT('Ctrl Pts',(-14.9554361332646,-3.88187057596333,
127.781287170382));
#76725=CARTESIAN_POINT('Ctrl Pts',(-14.96320903353,-3.96288019140338,127.89149885444));
#76726=CARTESIAN_POINT('Ctrl Pts',(-14.9706993692919,-4.04094490326898,
127.997704066172));
#76727=CARTESIAN_POINT('Ctrl Pts',(-14.9781897050536,-4.11463741889196,
128.106913902246));
#76728=CARTESIAN_POINT('Ctrl Pts',(-14.9856800408154,-4.1837390730525,128.218725215752));
#76729=CARTESIAN_POINT('Ctrl Pts',(-14.9936823409788,-4.25756382483398,
128.338178831823));
#76730=CARTESIAN_POINT('Ctrl Pts',(-15.0016846411421,-4.32637116804915,
128.460961806611));
#76731=CARTESIAN_POINT('Ctrl Pts',(-15.0096869413055,-4.38985700074989,
128.58662786192));
#76732=CARTESIAN_POINT('Ctrl Pts',(-15.0176787073992,-4.45325926195633,
128.712128492918));
#76733=CARTESIAN_POINT('Ctrl Pts',(-15.0256704734928,-4.51135379639687,
128.840504331396));
#76734=CARTESIAN_POINT('Ctrl Pts',(-15.0336622395865,-4.5638801270555,128.971280900705));
#76735=CARTESIAN_POINT('Ctrl Pts',(-15.0416415926349,-4.61632487227774,
129.101854344013));
#76736=CARTESIAN_POINT('Ctrl Pts',(-15.0496209456833,-4.66321851569826,
129.234820755411));
#76737=CARTESIAN_POINT('Ctrl Pts',(-15.0576002987317,-4.70434710270981,
129.369682465601));
#76738=CARTESIAN_POINT('Ctrl Pts',(-15.0617682289556,-4.72583018283312,
129.440126045994));
#76739=CARTESIAN_POINT('Ctrl Pts',(-15.0659361591794,-4.74574110107282,
129.511086344752));
#76740=CARTESIAN_POINT('Ctrl Pts',(-15.0701040894033,-4.76405452823398,
129.582490119308));
#76741=CARTESIAN_POINT('Origin',(213.235140564004,0.,130.804360617566));
#76742=CARTESIAN_POINT('',(-17.1650861998779,-4.76405452823408,129.582490119308));
#76743=CARTESIAN_POINT('',(-16.8197493731202,-4.76405452823399,129.582490119308));
#76744=CARTESIAN_POINT('',(213.235140564004,-4.76405452823405,129.582490119308));
#76745=CARTESIAN_POINT('',(-15.4851405639739,-4.91824870592851,130.807928408546));
#76746=CARTESIAN_POINT('Ctrl Pts',(-15.4851405640086,-4.91824870592807,
130.807928409157));
#76747=CARTESIAN_POINT('Ctrl Pts',(-15.4977558067663,-4.91808770741904,
131.029867019779));
#76748=CARTESIAN_POINT('Ctrl Pts',(-15.510371049524,-4.90290341425378,131.251269447092));
#76749=CARTESIAN_POINT('Ctrl Pts',(-15.5229862922817,-4.87291541403578,
131.470602638271));
#76750=CARTESIAN_POINT('Ctrl Pts',(-15.530760626401,-4.85443485541762,131.60577003413));
#76751=CARTESIAN_POINT('Ctrl Pts',(-15.5385349605204,-4.83029675023916,
131.740382008084));
#76752=CARTESIAN_POINT('Ctrl Pts',(-15.5463092946397,-4.80054267385402,
131.87392739856));
#76753=CARTESIAN_POINT('Ctrl Pts',(-15.5540740475871,-4.77082526670883,
132.007308206278));
#76754=CARTESIAN_POINT('Ctrl Pts',(-15.5618388005343,-4.73550574365403,
132.139624667972));
#76755=CARTESIAN_POINT('Ctrl Pts',(-15.5696035534817,-4.69467734798167,
132.270371415905));
#76756=CARTESIAN_POINT('Ctrl Pts',(-15.5773605943669,-4.65388950364741,
132.400988304325));
#76757=CARTESIAN_POINT('Ctrl Pts',(-15.5851176352523,-4.6076037909906,132.530038210809));
#76758=CARTESIAN_POINT('Ctrl Pts',(-15.5928746761375,-4.55596426774261,
132.657026980825));
#76759=CARTESIAN_POINT('Ctrl Pts',(-15.6006258673778,-4.50436368626094,
132.783919987622));
#76760=CARTESIAN_POINT('Ctrl Pts',(-15.6083770586182,-4.44741747696651,
132.908754591029));
#76761=CARTESIAN_POINT('Ctrl Pts',(-15.6161282498585,-4.38531908113688,
133.031053146659));
#76762=CARTESIAN_POINT('Ctrl Pts',(-15.6238761466358,-4.32324707878183,
133.15329972214));
#76763=CARTESIAN_POINT('Ctrl Pts',(-15.631624043413,-4.25602742190536,133.273012045811));
#76764=CARTESIAN_POINT('Ctrl Pts',(-15.6393719401903,-4.18390101101587,
133.38973397407));
#76765=CARTESIAN_POINT('Ctrl Pts',(-15.6471182162746,-4.11178968741656,
133.506431486618));
#76766=CARTESIAN_POINT('Ctrl Pts',(-15.654864492359,-4.03477385673277,133.620139515583));
#76767=CARTESIAN_POINT('Ctrl Pts',(-15.6626107684433,-3.95313935750207,
133.730428334258));
#76768=CARTESIAN_POINT('Ctrl Pts',(-15.6703571017088,-3.87150425566404,
133.840717967061));
#76769=CARTESIAN_POINT('Ctrl Pts',(-15.6781034349744,-3.78525064984824,
133.947588024965));
#76770=CARTESIAN_POINT('Ctrl Pts',(-15.6858497682399,-3.69470627546886,
134.050639810813));
#76771=CARTESIAN_POINT('Ctrl Pts',(-15.6935978362431,-3.6041416243045,134.153714674395));
#76772=CARTESIAN_POINT('Ctrl Pts',(-15.7013459042464,-3.5092845505272,134.252969270775));
#76773=CARTESIAN_POINT('Ctrl Pts',(-15.7090939722496,-3.41050116145027,
134.348040186918));
#76774=CARTESIAN_POINT('Ctrl Pts',(-15.7168502749916,-3.31161278421204,
134.443212145563));
#76775=CARTESIAN_POINT('Ctrl Pts',(-15.7246065777337,-3.20879003793378,
134.534191270137));
#76776=CARTESIAN_POINT('Ctrl Pts',(-15.7323628804758,-3.10243419309094,
134.620652684486));
#76777=CARTESIAN_POINT('Ctrl Pts',(-15.7401233229902,-2.99602158293124,
134.707160245896));
#76778=CARTESIAN_POINT('Ctrl Pts',(-15.7478837655046,-2.88607243001839,
134.789145058891));
#76779=CARTESIAN_POINT('Ctrl Pts',(-15.755644208019,-2.77301796086281,134.866324976252));
#76780=CARTESIAN_POINT('Ctrl Pts',(-15.7634171082846,-2.659782006637,134.943628789667));
#76781=CARTESIAN_POINT('Ctrl Pts',(-15.7711900085503,-2.54343110672227,
135.01611208708));
#76782=CARTESIAN_POINT('Ctrl Pts',(-15.7789629088159,-2.42442288725927,
135.083537726104));
#76783=CARTESIAN_POINT('Ctrl Pts',(-15.7864532445754,-2.30974091637957,
135.14851227329));
#76784=CARTESIAN_POINT('Ctrl Pts',(-15.7939435803349,-2.19259174611555,
135.208790354296));
#76785=CARTESIAN_POINT('Ctrl Pts',(-15.8014339160943,-2.0734015278911,135.264202449586));
#76786=CARTESIAN_POINT('Ctrl Pts',(-15.8092082502134,-1.94969217627408,
135.321715511331));
#76787=CARTESIAN_POINT('Ctrl Pts',(-15.8169825843325,-1.82339207472626,
135.374168499819));
#76788=CARTESIAN_POINT('Ctrl Pts',(-15.8247569184515,-1.69495375045156,
135.421320098256));
#76789=CARTESIAN_POINT('Ctrl Pts',(-15.8325216713986,-1.56667371493285,
135.468413586561));
#76790=CARTESIAN_POINT('Ctrl Pts',(-15.8402864243456,-1.43626106337846,
135.510218551069));
#76791=CARTESIAN_POINT('Ctrl Pts',(-15.8480511772927,-1.30419137625695,
135.546540276393));
#76792=CARTESIAN_POINT('Ctrl Pts',(-15.8558082181777,-1.17225286261054,
135.582825926469));
#76793=CARTESIAN_POINT('Ctrl Pts',(-15.8635652590626,-1.03866096312509,
135.613639072205));
#76794=CARTESIAN_POINT('Ctrl Pts',(-15.8713222999476,-0.903909290725196,
135.638833810856));
#76795=CARTESIAN_POINT('Ctrl Pts',(-15.8790734911877,-0.769259235609679,
135.664009549959));
#76796=CARTESIAN_POINT('Ctrl Pts',(-15.8868246824278,-0.633451531156165,
135.683575243676));
#76797=CARTESIAN_POINT('Ctrl Pts',(-15.8945758736679,-0.496992592850417,
135.697435461174));
#76798=CARTESIAN_POINT('Ctrl Pts',(-15.902323770445,-0.360591653233425,
135.71128978771));
#76799=CARTESIAN_POINT('Ctrl Pts',(-15.9100716672219,-0.223540418431535,
135.719443421702));
#76800=CARTESIAN_POINT('Ctrl Pts',(-15.917819563999,-0.0863528675830361,
135.721852482812));
#76801=CARTESIAN_POINT('Ctrl Pts',(-15.9255658400831,0.0508059865870601,
135.724261039999));
#76802=CARTESIAN_POINT('Ctrl Pts',(-15.9333121161673,0.188100709429822,
135.720927407573));
#76803=CARTESIAN_POINT('Ctrl Pts',(-15.9410583922514,0.325015256986704,
135.711859791812));
#76804=CARTESIAN_POINT('Ctrl Pts',(-15.9488047255167,0.461930815215674,
135.702792109116));
#76805=CARTESIAN_POINT('Ctrl Pts',(-15.956551058782,0.598465802448268,135.68799038446));
#76806=CARTESIAN_POINT('Ctrl Pts',(-15.9642973920473,0.734107634478534,
135.66751484538));
#76807=CARTESIAN_POINT('Ctrl Pts',(-15.9720454600503,0.869779842556609,
135.647034720944));
#76808=CARTESIAN_POINT('Ctrl Pts',(-15.9797935280532,1.00455811091234,135.620878312058));
#76809=CARTESIAN_POINT('Ctrl Pts',(-15.9875415960562,1.13793879992331,135.589157201553));
#76810=CARTESIAN_POINT('Ctrl Pts',(-15.995297898798,1.27146124751781,135.557402377473));
#76811=CARTESIAN_POINT('Ctrl Pts',(-16.0030542015399,1.40358276762992,135.520071128063));
#76812=CARTESIAN_POINT('Ctrl Pts',(-16.0108105042817,1.53381313625685,135.477325450041));
#76813=CARTESIAN_POINT('Ctrl Pts',(-16.0185709467958,1.66411301275285,135.434556957363));
#76814=CARTESIAN_POINT('Ctrl Pts',(-16.02633138931,1.79251936066034,135.386368415115));
#76815=CARTESIAN_POINT('Ctrl Pts',(-16.0340918318242,1.91856171306949,135.332970118908));
#76816=CARTESIAN_POINT('Ctrl Pts',(-16.0418647320896,2.04480639985224,135.279486103016));
#76817=CARTESIAN_POINT('Ctrl Pts',(-16.049637632355,2.1686791542302,135.220775788449));
#76818=CARTESIAN_POINT('Ctrl Pts',(-16.0574105326204,2.28973310348935,135.157096007787));
#76819=CARTESIAN_POINT('Ctrl Pts',(-16.0649008683828,2.40638643678201,135.09573114755));
#76820=CARTESIAN_POINT('Ctrl Pts',(-16.0723912041451,2.52042208159645,135.029752007904));
#76821=CARTESIAN_POINT('Ctrl Pts',(-16.0798815399075,2.63146707109214,134.959425492662));
#76822=CARTESIAN_POINT('Ctrl Pts',(-16.0876558740266,2.74672236511044,134.886432526224));
#76823=CARTESIAN_POINT('Ctrl Pts',(-16.0954302081456,2.85912083980922,134.8085247953));
#76824=CARTESIAN_POINT('Ctrl Pts',(-16.1032045422647,2.96821486652741,134.725952586222));
#76825=CARTESIAN_POINT('Ctrl Pts',(-16.1109692952118,3.07717444460769,134.643482140012));
#76826=CARTESIAN_POINT('Ctrl Pts',(-16.1187340481589,3.18283736889737,134.55635888724));
#76827=CARTESIAN_POINT('Ctrl Pts',(-16.126498801106,3.28478275696856,134.464877698802));
#76828=CARTESIAN_POINT('Ctrl Pts',(-16.1342558419909,3.38662689144313,134.37348737077));
#76829=CARTESIAN_POINT('Ctrl Pts',(-16.1420128828759,3.48476054845989,134.277747980137));
#76830=CARTESIAN_POINT('Ctrl Pts',(-16.1497699237609,3.57879416606433,134.177995953438));
#76831=CARTESIAN_POINT('Ctrl Pts',(-16.157521115001,3.67275687218614,134.078319150518));
#76832=CARTESIAN_POINT('Ctrl Pts',(-16.1652723062411,3.76262542598416,133.97463601786));
#76833=CARTESIAN_POINT('Ctrl Pts',(-16.1730234974812,3.84804580885601,133.867321034458));
#76834=CARTESIAN_POINT('Ctrl Pts',(-16.1807713942583,3.93342988578649,133.760051662786));
#76835=CARTESIAN_POINT('Ctrl Pts',(-16.1885192910353,4.01436930905938,133.649153815791));
#76836=CARTESIAN_POINT('Ctrl Pts',(-16.1962671878123,4.09054934262526,133.535036200283));
#76837=CARTESIAN_POINT('Ctrl Pts',(-16.2040134638964,4.16671344097048,133.420942455721));
#76838=CARTESIAN_POINT('Ctrl Pts',(-16.2117597399805,4.23811991290414,133.30363060725));
#76839=CARTESIAN_POINT('Ctrl Pts',(-16.2195060160646,4.30449672823447,133.183539252961));
#76840=CARTESIAN_POINT('Ctrl Pts',(-16.2272523493299,4.37087403354328,133.063447012185));
#76841=CARTESIAN_POINT('Ctrl Pts',(-16.2349986825953,4.43222141903552,132.940575566826));
#76842=CARTESIAN_POINT('Ctrl Pts',(-16.2427450158606,4.48831249155759,132.815388722946));
#76843=CARTESIAN_POINT('Ctrl Pts',(-16.2504930838635,4.54441612528643,132.690173844341));
#76844=CARTESIAN_POINT('Ctrl Pts',(-16.2582411518665,4.59526094389128,132.562642892145));
#76845=CARTESIAN_POINT('Ctrl Pts',(-16.2659892198695,4.64066859564943,132.433279905884));
#76846=CARTESIAN_POINT('Ctrl Pts',(-16.2737455226113,4.68612450720022,132.303779431101));
#76847=CARTESIAN_POINT('Ctrl Pts',(-16.2815018253531,4.72613157866356,132.172443402182));
#76848=CARTESIAN_POINT('Ctrl Pts',(-16.2892581280949,4.76056112441905,132.039771821647));
#76849=CARTESIAN_POINT('Ctrl Pts',(-16.297018570609,4.79500904625977,131.907029430296));
#76850=CARTESIAN_POINT('Ctrl Pts',(-16.3047790131232,4.82387342843925,131.772950448989));
#76851=CARTESIAN_POINT('Ctrl Pts',(-16.3125394556373,4.8470768997548,131.638044364777));
#76852=CARTESIAN_POINT('Ctrl Pts',(-16.3203123559028,4.87031761934244,131.502921717341));
#76853=CARTESIAN_POINT('Ctrl Pts',(-16.3280852561681,4.88787921843632,131.366969701722));
#76854=CARTESIAN_POINT('Ctrl Pts',(-16.3358581564335,4.89973623194224,131.230703108871));
#76855=CARTESIAN_POINT('Ctrl Pts',(-16.3433484921958,4.91116221314159,131.099390149901));
#76856=CARTESIAN_POINT('Ctrl Pts',(-16.350838827958,4.9172911458286,130.967785395655));
#76857=CARTESIAN_POINT('Ctrl Pts',(-16.3583291637203,4.91814598605262,130.836346901727));
#76858=CARTESIAN_POINT('Ctrl Pts',(-16.3661034978394,4.91903323780354,130.699924877357));
#76859=CARTESIAN_POINT('Ctrl Pts',(-16.3738778319585,4.9142413783758,130.563249825736));
#76860=CARTESIAN_POINT('Ctrl Pts',(-16.3816521660775,4.90373902652287,130.426833635409));
#76861=CARTESIAN_POINT('Ctrl Pts',(-16.3894169190246,4.89324961787999,130.290585565845));
#76862=CARTESIAN_POINT('Ctrl Pts',(-16.3971816719718,4.87706374940324,130.154596108883));
#76863=CARTESIAN_POINT('Ctrl Pts',(-16.4049464249188,4.8552020070954,130.019378749752));
#76864=CARTESIAN_POINT('Ctrl Pts',(-16.4127034658039,4.83336197817822,129.884295690408));
#76865=CARTESIAN_POINT('Ctrl Pts',(-16.4204605066888,4.80585735602314,129.749983586268));
#76866=CARTESIAN_POINT('Ctrl Pts',(-16.4282175475738,4.77276061805082,129.616952033597));
#76867=CARTESIAN_POINT('Ctrl Pts',(-16.435968738814,4.73968883858605,129.484020801055));
#76868=CARTESIAN_POINT('Ctrl Pts',(-16.443719930054,4.70103343111077,129.352368575731));
#76869=CARTESIAN_POINT('Ctrl Pts',(-16.4514711212942,4.65691809970679,129.222495618546));
#76870=CARTESIAN_POINT('Ctrl Pts',(-16.4592190180713,4.61282151849548,129.092677860833));
#76871=CARTESIAN_POINT('Ctrl Pts',(-16.4669669148484,4.56326975436197,128.964638236578));
#76872=CARTESIAN_POINT('Ctrl Pts',(-16.4747148116255,4.50843654139943,128.838862458148));
#76873=CARTESIAN_POINT('Ctrl Pts',(-16.4824610877096,4.45361479836297,128.7131129893));
#76874=CARTESIAN_POINT('Ctrl Pts',(-16.4902073637937,4.39351396007996,128.589626782526));
#76875=CARTESIAN_POINT('Ctrl Pts',(-16.4979536398778,4.32835599258222,128.468869777512));
#76876=CARTESIAN_POINT('Ctrl Pts',(-16.5056999731432,4.26319754410317,128.348111881097));
#76877=CARTESIAN_POINT('Ctrl Pts',(-16.5134463064085,4.1929820775735,128.230083570715));
#76878=CARTESIAN_POINT('Ctrl Pts',(-16.5211926396739,4.1179774351402,128.115226015844));
#76879=CARTESIAN_POINT('Ctrl Pts',(-16.5289407076769,4.04295599593738,128.000342739421));
#76880=CARTESIAN_POINT('Ctrl Pts',(-16.5366887756798,3.96314346040045,127.888631958751));
#76881=CARTESIAN_POINT('Ctrl Pts',(-16.5444368436828,3.87885066122662,127.780505361374));
#76882=CARTESIAN_POINT('Ctrl Pts',(-16.5521931464246,3.79446827466261,127.672263845762));
#76883=CARTESIAN_POINT('Ctrl Pts',(-16.5599494491666,3.7055963532558,127.567614431789));
#76884=CARTESIAN_POINT('Ctrl Pts',(-16.5677057519084,3.61258600556669,127.466935649888));
#76885=CARTESIAN_POINT('Ctrl Pts',(-16.5754661944226,3.51952601545441,127.366203132688));
#76886=CARTESIAN_POINT('Ctrl Pts',(-16.5832266369368,3.42232347478573,127.269445746021));
#76887=CARTESIAN_POINT('Ctrl Pts',(-16.5909870794509,3.32136520842058,127.177003974666));
#76888=CARTESIAN_POINT('Ctrl Pts',(-16.5987599797164,3.22024487488375,127.084413807572));
#76889=CARTESIAN_POINT('Ctrl Pts',(-16.6065328799819,3.1153570670575,126.99615335163));
#76890=CARTESIAN_POINT('Ctrl Pts',(-16.6143057802473,3.00712112864498,126.912522288427));
#76891=CARTESIAN_POINT('Ctrl Pts',(-16.6217961160093,2.90281983922451,126.831931425026));
#76892=CARTESIAN_POINT('Ctrl Pts',(-16.6292864517712,2.79540987006541,126.755639396084));
#76893=CARTESIAN_POINT('Ctrl Pts',(-16.6367767875332,2.68528900461896,126.683874478265));
#76894=CARTESIAN_POINT('Ctrl Pts',(-16.6445511216523,2.57099287308778,126.609388571773));
#76895=CARTESIAN_POINT('Ctrl Pts',(-16.6523254557713,2.45341416425206,126.539543894948));
#76896=CARTESIAN_POINT('Ctrl Pts',(-16.6600997898904,2.33296658211227,126.474643537981));
#76897=CARTESIAN_POINT('Ctrl Pts',(-16.6678645428375,2.2126674408526,126.409823164905));
#76898=CARTESIAN_POINT('Ctrl Pts',(-16.6756292957847,2.08950680201563,126.349935171247));
#76899=CARTESIAN_POINT('Ctrl Pts',(-16.6833940487318,1.96392780250394,126.295239788729));
#76900=CARTESIAN_POINT('Ctrl Pts',(-16.6911510896168,1.83847352982508,126.240598730436));
#76901=CARTESIAN_POINT('Ctrl Pts',(-16.6989081305018,1.71060603258315,126.191140174984));
#76902=CARTESIAN_POINT('Ctrl Pts',(-16.7066651713868,1.5807932243651,126.147078594293));
#76903=CARTESIAN_POINT('Ctrl Pts',(-16.7144163626269,1.45107830899552,126.103050240783));
#76904=CARTESIAN_POINT('Ctrl Pts',(-16.722167553867,1.31942137129501,126.064410886299));
#76905=CARTESIAN_POINT('Ctrl Pts',(-16.7299187451071,1.18631016002169,126.031326858338));
#76906=CARTESIAN_POINT('Ctrl Pts',(-16.7376666418842,1.05325552456402,125.998256891972));
#76907=CARTESIAN_POINT('Ctrl Pts',(-16.7454145386612,0.918748223524601,
125.970737650065));
#76908=CARTESIAN_POINT('Ctrl Pts',(-16.7531624354383,0.783290807994925,
125.948885504602));
#76909=CARTESIAN_POINT('Ctrl Pts',(-16.7609087115224,0.647861727236454,
125.927037930137));
#76910=CARTESIAN_POINT('Ctrl Pts',(-16.7686549876065,0.511483313029908,
125.910855156449));
#76911=CARTESIAN_POINT('Ctrl Pts',(-16.7764012636906,0.374667551691111,
125.90040228901));
#76912=CARTESIAN_POINT('Ctrl Pts',(-16.784147596956,0.237850780409443,125.889949344411));
#76913=CARTESIAN_POINT('Ctrl Pts',(-16.7918939302213,0.100597045382613,
125.885226420245));
#76914=CARTESIAN_POINT('Ctrl Pts',(-16.7996402634867,-0.0365777097900677,
125.886246636206));
#76915=CARTESIAN_POINT('Ctrl Pts',(-16.8073883314897,-0.173783184298066,
125.887267080638));
#76916=CARTESIAN_POINT('Ctrl Pts',(-16.8151363994926,-0.310909252877284,
125.894033221554));
#76917=CARTESIAN_POINT('Ctrl Pts',(-16.8228844674956,-0.447441538474306,
125.906506073774));
#76918=CARTESIAN_POINT('Ctrl Pts',(-16.8306407702374,-0.584118932209216,
125.918992182289));
#76919=CARTESIAN_POINT('Ctrl Pts',(-16.8383970729792,-0.720200892347673,
125.937197082296));
#76920=CARTESIAN_POINT('Ctrl Pts',(-16.8461533757211,-0.855179167762777,
125.961029981163));
#76921=CARTESIAN_POINT('Ctrl Pts',(-16.8539138182352,-0.990229485147588,
125.984875600365));
#76922=CARTESIAN_POINT('Ctrl Pts',(-16.8616742607495,-1.12417456239742,
126.014355119824));
#76923=CARTESIAN_POINT('Ctrl Pts',(-16.8694347032636,-1.25651885173855,
126.04932713317));
#76924=CARTESIAN_POINT('Ctrl Pts',(-16.8772076035291,-1.38907559188209,
126.084355286697));
#76925=CARTESIAN_POINT('Ctrl Pts',(-16.8849805037944,-1.52002603529006,
126.124893437679));
#76926=CARTESIAN_POINT('Ctrl Pts',(-16.8927534040598,-1.64889138583909,
126.170750765603));
#76927=CARTESIAN_POINT('Ctrl Pts',(-16.9002437398219,-1.77307215630395,
126.21494106415));
#76928=CARTESIAN_POINT('Ctrl Pts',(-16.907734075584,-1.89531651292176,126.264070408033));
#76929=CARTESIAN_POINT('Ctrl Pts',(-16.9152244113461,-2.01521738839822,
126.317927519882));
#76930=CARTESIAN_POINT('Ctrl Pts',(-16.922999300883,-2.13967323281102,126.373830634068));
#76931=CARTESIAN_POINT('Ctrl Pts',(-16.9307741904198,-2.26199828785594,
126.435004925191));
#76932=CARTESIAN_POINT('Ctrl Pts',(-16.9385490799567,-2.38171383604301,
126.501266118755));
#76933=CARTESIAN_POINT('Ctrl Pts',(-16.9463142626309,-2.50127992070713,
126.567444585959));
#76934=CARTESIAN_POINT('Ctrl Pts',(-16.9540794453051,-2.61824264233293,
126.638697130794));
#76935=CARTESIAN_POINT('Ctrl Pts',(-16.9618446279794,-2.73214346027213,
126.714791547971));
#76936=CARTESIAN_POINT('Ctrl Pts',(-16.9696019734379,-2.84592932080268,
126.790809164846));
#76937=CARTESIAN_POINT('Ctrl Pts',(-16.9773593188965,-2.9566591048909,126.871658712568));
#76938=CARTESIAN_POINT('Ctrl Pts',(-16.985116664355,-3.06389940533845,126.957062410192));
#76939=CARTESIAN_POINT('Ctrl Pts',(-16.9928676271597,-3.17105146971085,
127.042395838643));
#76940=CARTESIAN_POINT('Ctrl Pts',(-17.0006185899644,-3.27471946287186,
127.132275713058));
#76941=CARTESIAN_POINT('Ctrl Pts',(-17.0083695527691,-3.37449984907946,
127.226381602666));
#76942=CARTESIAN_POINT('Ctrl Pts',(-17.0161170377662,-3.47423546446429,
127.320445267563));
#76943=CARTESIAN_POINT('Ctrl Pts',(-17.0238645227634,-3.5700866595763,127.418730907477));
#76944=CARTESIAN_POINT('Ctrl Pts',(-17.0316120077605,-3.66168394908057,
127.520878667022));
#76945=CARTESIAN_POINT('Ctrl Pts',(-17.0393576942952,-3.75325997564768,
127.623002714498));
#76946=CARTESIAN_POINT('Ctrl Pts',(-17.0471033808298,-3.84058380117569,
127.728986806488));
#76947=CARTESIAN_POINT('Ctrl Pts',(-17.0548490673645,-3.92332398697111,
127.838435474249));
#76948=CARTESIAN_POINT('Ctrl Pts',(-17.062594633218,-4.00606288363802,127.947882436753));
#76949=CARTESIAN_POINT('Ctrl Pts',(-17.0703401990714,-4.08421804805444,
128.060793555101));
#76950=CARTESIAN_POINT('Ctrl Pts',(-17.0780857649249,-4.15749964646109,
128.176741970925));
#76951=CARTESIAN_POINT('Ctrl Pts',(-17.0858363079725,-4.23082833461591,
128.292764893608));
#76952=CARTESIAN_POINT('Ctrl Pts',(-17.0935868510201,-4.2992769905067,128.411828682534));
#76953=CARTESIAN_POINT('Ctrl Pts',(-17.1013373940677,-4.36260014823184,
128.533479068663));
#76954=CARTESIAN_POINT('Ctrl Pts',(-17.1090904973753,-4.42594422368419,
128.655169639927));
#76955=CARTESIAN_POINT('Ctrl Pts',(-17.116843600683,-4.48415925812918,128.779448158453));
#76956=CARTESIAN_POINT('Ctrl Pts',(-17.1245967039906,-4.5370471621802,128.905838531665));
#76957=CARTESIAN_POINT('Ctrl Pts',(-17.1323587136796,-4.58999582123819,
129.032374095884));
#76958=CARTESIAN_POINT('Ctrl Pts',(-17.1401207233686,-4.63760498567923,
129.161025995706));
#76959=CARTESIAN_POINT('Ctrl Pts',(-17.1478827330576,-4.67972567458143,
129.29130058136));
#76960=CARTESIAN_POINT('Ctrl Pts',(-17.1536172219977,-4.71084398470165,
129.38754603847));
#76961=CARTESIAN_POINT('Ctrl Pts',(-17.1593517109378,-4.73896766352352,
129.484676814548));
#76962=CARTESIAN_POINT('Ctrl Pts',(-17.1650861998779,-4.76405452823408,
129.582490119308));
#76963=CARTESIAN_POINT('Ctrl Pts',(-15.4150128089234,-4.76405452823406,
129.582490119308));
#76964=CARTESIAN_POINT('Ctrl Pts',(-15.4226557882312,-4.79767677092274,
129.713582733263));
#76965=CARTESIAN_POINT('Ctrl Pts',(-15.4302987675391,-4.82586457448078,
129.845988829133));
#76966=CARTESIAN_POINT('Ctrl Pts',(-15.4379417468469,-4.84853709250063,
129.979211464294));
#76967=CARTESIAN_POINT('Ctrl Pts',(-15.4458082163681,-4.87187258312357,
130.116329694869));
#76968=CARTESIAN_POINT('Ctrl Pts',(-15.4536746858893,-4.88936523239047,
130.25431249071));
#76969=CARTESIAN_POINT('Ctrl Pts',(-15.4615411554104,-4.90098435191105,
130.3926137963));
#76970=CARTESIAN_POINT('Ctrl Pts',(-15.4694076249315,-4.91260347143165,
130.530915101889));
#76971=CARTESIAN_POINT('Ctrl Pts',(-15.4772740944527,-4.91834909952949,
130.669534455329));
#76972=CARTESIAN_POINT('Ctrl Pts',(-15.4851405639739,-4.91824870592852,
130.807928408547));
#76973=CARTESIAN_POINT('',(-15.1398594360232,-4.91824978862749,130.805802548776));
#76974=CARTESIAN_POINT('Ctrl Pts',(-15.0701040894033,-4.76405452823398,
129.582490119308));
#76975=CARTESIAN_POINT('Ctrl Pts',(-15.0780695634094,-4.79905394525373,
129.718952315078));
#76976=CARTESIAN_POINT('Ctrl Pts',(-15.0860350374154,-4.82821560351136,
129.857035172868));
#76977=CARTESIAN_POINT('Ctrl Pts',(-15.0940005114215,-4.85140006569305,
129.996214303404));
#76978=CARTESIAN_POINT('Ctrl Pts',(-15.1019581955728,-4.87456185457316,
130.135257323369));
#76979=CARTESIAN_POINT('Ctrl Pts',(-15.109915879724,-4.89175803917466,130.275394125515));
#76980=CARTESIAN_POINT('Ctrl Pts',(-15.1178735638753,-4.90289998289446,
130.416089037054));
#76981=CARTESIAN_POINT('Ctrl Pts',(-15.1252021879139,-4.91316114870974,
130.545661924242));
#76982=CARTESIAN_POINT('Ctrl Pts',(-15.1325308119525,-4.91828792975117,
130.675707821371));
#76983=CARTESIAN_POINT('Ctrl Pts',(-15.1398594359911,-4.91824978862766,
130.805802548205));
#76984=CARTESIAN_POINT('Ctrl Pts',(-15.1398594360233,-4.91824978862749,
130.805802548776));
#76985=CARTESIAN_POINT('Ctrl Pts',(-15.1481808457913,-4.91820648062839,
130.953520800515));
#76986=CARTESIAN_POINT('Ctrl Pts',(-15.1565022555593,-4.91150395054456,
131.101051023692));
#76987=CARTESIAN_POINT('Ctrl Pts',(-15.1648236653272,-4.89821807427448,
131.24780481851));
#76988=CARTESIAN_POINT('Ctrl Pts',(-15.1731762609717,-4.88488240695846,
131.395108597747));
#76989=CARTESIAN_POINT('Ctrl Pts',(-15.1815288566162,-4.86491403750072,
131.541629830756));
#76990=CARTESIAN_POINT('Ctrl Pts',(-15.1898814522606,-4.83844054493169,
131.686786906647));
#76991=CARTESIAN_POINT('Ctrl Pts',(-15.1982495793767,-4.81191782547352,
131.832213898993));
#76992=CARTESIAN_POINT('Ctrl Pts',(-15.2066177064928,-4.77886588751804,
131.976271382574));
#76993=CARTESIAN_POINT('Ctrl Pts',(-15.2149858336089,-4.73946243264698,
132.118392166665));
#76994=CARTESIAN_POINT('Ctrl Pts',(-15.2233804894101,-4.69993406071453,
132.260963502891));
#76995=CARTESIAN_POINT('Ctrl Pts',(-15.2317751452115,-4.65401396770181,
132.401585572931));
#76996=CARTESIAN_POINT('Ctrl Pts',(-15.2401698010127,-4.60192935985197,
132.539707623047));
#76997=CARTESIAN_POINT('Ctrl Pts',(-15.2481557555513,-4.55238053732816,
132.671105078656));
#76998=CARTESIAN_POINT('Ctrl Pts',(-15.2561417100897,-4.49725331014482,
132.800240000642));
#76999=CARTESIAN_POINT('Ctrl Pts',(-15.2641276646283,-4.43678145503934,
132.926659697036));
#77000=CARTESIAN_POINT('Ctrl Pts',(-15.2719019987473,-4.37791204824278,
133.049729388236));
#77001=CARTESIAN_POINT('Ctrl Pts',(-15.2796763328663,-4.31382486170124,
133.170542732587));
#77002=CARTESIAN_POINT('Ctrl Pts',(-15.2874506669854,-4.24471556105109,
133.288625673527));
#77003=CARTESIAN_POINT('Ctrl Pts',(-15.2952154199324,-4.17569143143751,
133.406563087796));
#77004=CARTESIAN_POINT('Ctrl Pts',(-15.3029801728795,-4.10165769817633,
133.521776459773));
#77005=CARTESIAN_POINT('Ctrl Pts',(-15.3107449258265,-4.02285745837033,
133.633813026096));
#77006=CARTESIAN_POINT('Ctrl Pts',(-15.3185019667114,-3.94413548407349,
133.745738316121));
#77007=CARTESIAN_POINT('Ctrl Pts',(-15.3262590075964,-3.86065664789233,
133.85449276186));
#77008=CARTESIAN_POINT('Ctrl Pts',(-15.3340160484813,-3.77270901092966,
133.959649793117));
#77009=CARTESIAN_POINT('Ctrl Pts',(-15.3417672397214,-3.68482769596416,
134.064727524639));
#77010=CARTESIAN_POINT('Ctrl Pts',(-15.3495184309614,-3.59248453772077,
134.16621294273));
#77011=CARTESIAN_POINT('Ctrl Pts',(-15.3572696222014,-3.49600958139968,
134.263710277439));
#77012=CARTESIAN_POINT('Ctrl Pts',(-15.3650175189785,-3.39957562950845,
134.36116617318));
#77013=CARTESIAN_POINT('Ctrl Pts',(-15.3727654157555,-3.29901364675454,
134.454637079522));
#77014=CARTESIAN_POINT('Ctrl Pts',(-15.3805133125325,-3.19469230619625,
134.543762191512));
#77015=CARTESIAN_POINT('Ctrl Pts',(-15.3882595886166,-3.0903927874135,134.63286866045));
#77016=CARTESIAN_POINT('Ctrl Pts',(-15.3960058647007,-2.98233577203952,
134.717630889385));
#77017=CARTESIAN_POINT('Ctrl Pts',(-15.4037521407847,-2.8709246591275,134.797726949887));
#77018=CARTESIAN_POINT('Ctrl Pts',(-15.4114984740501,-2.75951272380396,
134.87782360164));
#77019=CARTESIAN_POINT('Ctrl Pts',(-15.4192448073153,-2.64474695898088,
134.95325378801));
#77020=CARTESIAN_POINT('Ctrl Pts',(-15.4269911405806,-2.52706118537816,
135.023737920896));
#77021=CARTESIAN_POINT('Ctrl Pts',(-15.4347392085835,-2.40934905686242,
135.094237838214));
#77022=CARTESIAN_POINT('Ctrl Pts',(-15.4424872765865,-2.28871595369618,
135.159789297139));
#77023=CARTESIAN_POINT('Ctrl Pts',(-15.4502353445895,-2.16562146255197,
135.220158024992));
#77024=CARTESIAN_POINT('Ctrl Pts',(-15.4579916473313,-2.04239614511773,
135.280590913448));
#77025=CARTESIAN_POINT('Ctrl Pts',(-15.465747950073,-1.91670456556245,135.335829895047));
#77026=CARTESIAN_POINT('Ctrl Pts',(-15.4735042528148,-1.78902802782657,
135.385688130215));
#77027=CARTESIAN_POINT('Ctrl Pts',(-15.481264695329,-1.66128334527823,135.435572976223));
#77028=CARTESIAN_POINT('Ctrl Pts',(-15.4890251378431,-1.53155196317589,
135.480071226578));
#77029=CARTESIAN_POINT('Ctrl Pts',(-15.4967855803573,-1.40033066428529,
135.51904587675));
#77030=CARTESIAN_POINT('Ctrl Pts',(-15.5045584806226,-1.26889871731642,
135.558083092489));
#77031=CARTESIAN_POINT('Ctrl Pts',(-15.512331380888,-1.13597245341943,135.59157889342));
#77032=CARTESIAN_POINT('Ctrl Pts',(-15.5201042811534,-1.00206005270424,
135.619447191375));
#77033=CARTESIAN_POINT('Ctrl Pts',(-15.527594616916,-0.87301570504988,135.646302406505));
#77034=CARTESIAN_POINT('Ctrl Pts',(-15.5350849526785,-0.743055976763678,
135.6679321125));
#77035=CARTESIAN_POINT('Ctrl Pts',(-15.5425752884411,-0.612638428668537,
135.684305004362));
#77036=CARTESIAN_POINT('Ctrl Pts',(-15.5503496225602,-0.477276059607541,
135.701298679393));
#77037=CARTESIAN_POINT('Ctrl Pts',(-15.5581239566793,-0.340991681649807,
135.712682877964));
#77038=CARTESIAN_POINT('Ctrl Pts',(-15.5658982907984,-0.204289894063151,
135.718365979965));
#77039=CARTESIAN_POINT('Ctrl Pts',(-15.5736630437455,-0.0677565792123065,
135.72404207805));
#77040=CARTESIAN_POINT('Ctrl Pts',(-15.5814277966925,0.0691927348470643,
135.724031043309));
#77041=CARTESIAN_POINT('Ctrl Pts',(-15.5891925496396,0.206045725553709,
135.718292670564));
#77042=CARTESIAN_POINT('Ctrl Pts',(-15.5969495905246,0.342762791940509,
135.712559997252));
#77043=CARTESIAN_POINT('Ctrl Pts',(-15.6047066314097,0.479383337267362,
135.701111322525));
#77044=CARTESIAN_POINT('Ctrl Pts',(-15.6124636722947,0.615392771885629,
135.68395842874));
#77045=CARTESIAN_POINT('Ctrl Pts',(-15.6202148635348,0.751299640731252,
135.666818470085));
#77046=CARTESIAN_POINT('Ctrl Pts',(-15.6279660547749,0.886595929825876,
135.643982903157));
#77047=CARTESIAN_POINT('Ctrl Pts',(-15.635717246015,1.02077026920864,135.615515481006));
#77048=CARTESIAN_POINT('Ctrl Pts',(-15.6434651427921,1.15488758091813,135.587060158268));
#77049=CARTESIAN_POINT('Ctrl Pts',(-15.6512130395692,1.28788350969986,135.552977822145));
#77050=CARTESIAN_POINT('Ctrl Pts',(-15.6589609363463,1.41925522333431,135.513383623832));
#77051=CARTESIAN_POINT('Ctrl Pts',(-15.6667072124304,1.55059945683831,135.473797707771));
#77052=CARTESIAN_POINT('Ctrl Pts',(-15.6744534885145,1.68031977688197,135.428702335574));
#77053=CARTESIAN_POINT('Ctrl Pts',(-15.6821997645986,1.80792728891787,135.37826288811));
#77054=CARTESIAN_POINT('Ctrl Pts',(-15.689946097864,1.93553574292325,135.327823068313));
#77055=CARTESIAN_POINT('Ctrl Pts',(-15.6976924311293,2.06103099420758,135.27203923825));
#77056=CARTESIAN_POINT('Ctrl Pts',(-15.7054387643947,2.18394332668613,135.211125259378));
#77057=CARTESIAN_POINT('Ctrl Pts',(-15.7131868323976,2.30688318452933,135.150197639243));
#77058=CARTESIAN_POINT('Ctrl Pts',(-15.7209349004006,2.42723862232567,135.084137757774));
#77059=CARTESIAN_POINT('Ctrl Pts',(-15.7286829684036,2.54456412201361,135.013205648149));
#77060=CARTESIAN_POINT('Ctrl Pts',(-15.7364392711455,2.66201431663897,134.942198151034));
#77061=CARTESIAN_POINT('Ctrl Pts',(-15.7441955738873,2.77642780524497,134.866308284224));
#77062=CARTESIAN_POINT('Ctrl Pts',(-15.7519518766292,2.88738723786942,134.785839991001));
#77063=CARTESIAN_POINT('Ctrl Pts',(-15.7597123191433,2.998405892884,134.705328749428));
#77064=CARTESIAN_POINT('Ctrl Pts',(-15.7674727616575,3.10596651205521,134.620234454727));
#77065=CARTESIAN_POINT('Ctrl Pts',(-15.7752332041716,3.20968530637265,134.530901010015));
#77066=CARTESIAN_POINT('Ctrl Pts',(-15.7830061044371,3.31357059930645,134.441424159327));
#77067=CARTESIAN_POINT('Ctrl Pts',(-15.7907790047026,3.41360145782071,134.347694827425));
#77068=CARTESIAN_POINT('Ctrl Pts',(-15.798551904968,3.50943076974038,134.250094027872));
#77069=CARTESIAN_POINT('Ctrl Pts',(-15.80604224073,3.60177644479204,134.156041263224));
#77070=CARTESIAN_POINT('Ctrl Pts',(-15.813532576492,3.69022053660507,134.058393847598));
#77071=CARTESIAN_POINT('Ctrl Pts',(-15.821022912254,3.77448938459753,133.957519818758));
#77072=CARTESIAN_POINT('Ctrl Pts',(-15.8287972463731,3.86195331157483,133.852821120454));
#77073=CARTESIAN_POINT('Ctrl Pts',(-15.8365715804922,3.94519619546707,133.744314650906));
#77074=CARTESIAN_POINT('Ctrl Pts',(-15.8443459146113,4.0238682054511,133.632375420862));
#77075=CARTESIAN_POINT('Ctrl Pts',(-15.8521106675584,4.10244325921393,133.520574145915));
#77076=CARTESIAN_POINT('Ctrl Pts',(-15.8598754205055,4.17645842479622,133.405348844843));
#77077=CARTESIAN_POINT('Ctrl Pts',(-15.8676401734526,4.24560295358366,133.287108817248));
#77078=CARTESIAN_POINT('Ctrl Pts',(-15.8753972143376,4.31467880705024,133.168986227314));
#77079=CARTESIAN_POINT('Ctrl Pts',(-15.8831542552226,4.37889345465133,133.047855204897));
#77080=CARTESIAN_POINT('Ctrl Pts',(-15.8909112961076,4.43797866094046,132.924155057491));
#77081=CARTESIAN_POINT('Ctrl Pts',(-15.8986624873477,4.49701931061592,132.800548193329));
#77082=CARTESIAN_POINT('Ctrl Pts',(-15.9064136785878,4.55093805047412,132.674376411809));
#77083=CARTESIAN_POINT('Ctrl Pts',(-15.914164869828,4.59951210980578,132.546104403044));
#77084=CARTESIAN_POINT('Ctrl Pts',(-15.9219127666051,4.64806552386653,132.417886913303));
#77085=CARTESIAN_POINT('Ctrl Pts',(-15.9296606633821,4.69127863733705,132.287571336597));
#77086=CARTESIAN_POINT('Ctrl Pts',(-15.9374085601592,4.72897653708163,132.155642961945));
#77087=CARTESIAN_POINT('Ctrl Pts',(-15.9451548362433,4.76666655123825,132.023742183866));
#77088=CARTESIAN_POINT('Ctrl Pts',(-15.9529011123275,4.79884353902041,131.890229654555));
#77089=CARTESIAN_POINT('Ctrl Pts',(-15.9606473884116,4.82538238059169,131.75560608724));
#77090=CARTESIAN_POINT('Ctrl Pts',(-15.968393721677,4.85192141806664,131.620981526165));
#77091=CARTESIAN_POINT('Ctrl Pts',(-15.9761400549423,4.87282215066489,131.485246294304));
#77092=CARTESIAN_POINT('Ctrl Pts',(-15.9838863882077,4.88801061307185,131.348911174445));
#77093=CARTESIAN_POINT('Ctrl Pts',(-15.9916344562106,4.90320247682967,131.212545523281));
#77094=CARTESIAN_POINT('Ctrl Pts',(-15.9993825242136,4.91267948161037,131.075580105283));
#77095=CARTESIAN_POINT('Ctrl Pts',(-16.0071305922166,4.91641958729721,130.938530301699));
#77096=CARTESIAN_POINT('Ctrl Pts',(-16.0148868949584,4.92016366801287,130.801334839953));
#77097=CARTESIAN_POINT('Ctrl Pts',(-16.0226431977003,4.91815865904924,130.664055204907));
#77098=CARTESIAN_POINT('Ctrl Pts',(-16.0303995004421,4.91043468864896,130.527206813672));
#77099=CARTESIAN_POINT('Ctrl Pts',(-16.0381599429563,4.90270659573309,130.390285382329));
#77100=CARTESIAN_POINT('Ctrl Pts',(-16.0459203854705,4.88925349758212,130.253796042316));
#77101=CARTESIAN_POINT('Ctrl Pts',(-16.0536808279847,4.87015728229237,130.118247574231));
#77102=CARTESIAN_POINT('Ctrl Pts',(-16.0614537282501,4.85103041206255,129.982481511711));
#77103=CARTESIAN_POINT('Ctrl Pts',(-16.0692266285156,4.82624239299752,129.847659724063));
#77104=CARTESIAN_POINT('Ctrl Pts',(-16.076999528781,4.79592615998857,129.714280193727));
#77105=CARTESIAN_POINT('Ctrl Pts',(-16.084489864543,4.76671199841156,129.585749345282));
#77106=CARTESIAN_POINT('Ctrl Pts',(-16.091980200305,4.73236465411899,129.458558012656));
#77107=CARTESIAN_POINT('Ctrl Pts',(-16.099470536067,4.69304584747548,129.333135367649));
#77108=CARTESIAN_POINT('Ctrl Pts',(-16.1072448701861,4.65223625632728,129.202957284935));
#77109=CARTESIAN_POINT('Ctrl Pts',(-16.1150192043052,4.605941502498,129.074272291947));
#77110=CARTESIAN_POINT('Ctrl Pts',(-16.1227935384242,4.5542880010454,128.947577413734));
#77111=CARTESIAN_POINT('Ctrl Pts',(-16.1305582913713,4.50269815791701,128.821038675635));
#77112=CARTESIAN_POINT('Ctrl Pts',(-16.1383230443184,4.44576285369402,128.696485530849));
#77113=CARTESIAN_POINT('Ctrl Pts',(-16.1460877972655,4.38365847650471,128.574400657417));
#77114=CARTESIAN_POINT('Ctrl Pts',(-16.1538448381505,4.32161578225834,128.452437040402));
#77115=CARTESIAN_POINT('Ctrl Pts',(-16.1616018790355,4.25441440804822,128.332937162316));
#77116=CARTESIAN_POINT('Ctrl Pts',(-16.1693589199205,4.18227896790133,128.216364153668));
#77117=CARTESIAN_POINT('Ctrl Pts',(-16.1771101111606,4.11019792565098,128.099879053632));
#77118=CARTESIAN_POINT('Ctrl Pts',(-16.1848613024007,4.03319042841998,127.986316760903));
#77119=CARTESIAN_POINT('Ctrl Pts',(-16.1926124936408,3.9515270201495,127.876115875143));
#77120=CARTESIAN_POINT('Ctrl Pts',(-16.2003603904179,3.86989832100586,127.765961827699));
#77121=CARTESIAN_POINT('Ctrl Pts',(-16.208108287195,3.78361787896377,127.659166659132));
#77122=CARTESIAN_POINT('Ctrl Pts',(-16.2158561839721,3.69299943659804,127.556139839388));
#77123=CARTESIAN_POINT('Ctrl Pts',(-16.2236024600562,3.60239994965695,127.453134570634));
#77124=CARTESIAN_POINT('Ctrl Pts',(-16.2313487361403,3.50746452533909,127.353896376196));
#77125=CARTESIAN_POINT('Ctrl Pts',(-16.2390950122244,3.4085467975363,127.258801170666));
#77126=CARTESIAN_POINT('Ctrl Pts',(-16.2468413454897,3.30962833954531,127.163705263164));
#77127=CARTESIAN_POINT('Ctrl Pts',(-16.2545876787551,3.20672780125715,127.072752676552));
#77128=CARTESIAN_POINT('Ctrl Pts',(-16.2623340120204,3.10023493863807,126.986281730515));
#77129=CARTESIAN_POINT('Ctrl Pts',(-16.2700820800234,2.99371822768091,126.899791419909));
#77130=CARTESIAN_POINT('Ctrl Pts',(-16.2778301480265,2.88360789502998,126.81778499339));
#77131=CARTESIAN_POINT('Ctrl Pts',(-16.2855782160294,2.7703256323039,126.740559570086));
#77132=CARTESIAN_POINT('Ctrl Pts',(-16.2933345187713,2.65692297184092,126.663252070683));
#77133=CARTESIAN_POINT('Ctrl Pts',(-16.3010908215131,2.54034197059532,126.590735945525));
#77134=CARTESIAN_POINT('Ctrl Pts',(-16.308847124255,2.42103254863144,126.523264442406));
#77135=CARTESIAN_POINT('Ctrl Pts',(-16.3166075667691,2.30165944763656,126.455756927715));
#77136=CARTESIAN_POINT('Ctrl Pts',(-16.3243680092832,2.17955537214382,126.393299577986));
#77137=CARTESIAN_POINT('Ctrl Pts',(-16.3321284517974,2.05519263619625,126.336098506787));
#77138=CARTESIAN_POINT('Ctrl Pts',(-16.3399013520628,1.93063026214453,126.27880561135));
#77139=CARTESIAN_POINT('Ctrl Pts',(-16.3476742523283,1.80380234405896,126.226786004393));
#77140=CARTESIAN_POINT('Ctrl Pts',(-16.3554471525937,1.67519970322636,126.180197015701));
#77141=CARTESIAN_POINT('Ctrl Pts',(-16.3629374883558,1.55127209231853,126.135301654099));
#77142=CARTESIAN_POINT('Ctrl Pts',(-16.3704278241178,1.42569684336387,126.095449025514));
#77143=CARTESIAN_POINT('Ctrl Pts',(-16.3779181598798,1.29892244455898,126.060735047865));
#77144=CARTESIAN_POINT('Ctrl Pts',(-16.3856924939989,1.16734135589116,126.024704879202));
#77145=CARTESIAN_POINT('Ctrl Pts',(-16.3934668281179,1.03405158148503,125.994096584719));
#77146=CARTESIAN_POINT('Ctrl Pts',(-16.401241162237,0.89953961301696,125.969072462025));
#77147=CARTESIAN_POINT('Ctrl Pts',(-16.4090059151841,0.765193418528343,
125.944079179327));
#77148=CARTESIAN_POINT('Ctrl Pts',(-16.4167706681312,0.629628407636705,
125.924656446124));
#77149=CARTESIAN_POINT('Ctrl Pts',(-16.4245354210783,0.493346013140051,
125.910916761362));
#77150=CARTESIAN_POINT('Ctrl Pts',(-16.4322924619633,0.357198976239042,
125.897190723049));
#77151=CARTESIAN_POINT('Ctrl Pts',(-16.4400495028484,0.220336360147173,
125.889136539361));
#77152=CARTESIAN_POINT('Ctrl Pts',(-16.4478065437334,0.083269219047094,
125.88681556951));
#77153=CARTESIAN_POINT('Ctrl Pts',(-16.4555577349735,-0.0536945586558414,
125.884496349921));
#77154=CARTESIAN_POINT('Ctrl Pts',(-16.4633089262136,-0.190862165046312,
125.887901745174));
#77155=CARTESIAN_POINT('Ctrl Pts',(-16.4710601174537,-0.327718358197829,
125.89704121282));
#77156=CARTESIAN_POINT('Ctrl Pts',(-16.4788080142308,-0.464516383816498,
125.906176795948));
#77157=CARTESIAN_POINT('Ctrl Pts',(-16.4865559110079,-0.601002870168441,
125.9210415782));
#77158=CARTESIAN_POINT('Ctrl Pts',(-16.494303807785,-0.736663733067385,
125.941592927569));
#77159=CARTESIAN_POINT('Ctrl Pts',(-16.5020500838691,-0.872296218638321,
125.962139978038));
#77160=CARTESIAN_POINT('Ctrl Pts',(-16.5097963599532,-1.00710303796139,
125.988371171106));
#77161=CARTESIAN_POINT('Ctrl Pts',(-16.5175426360373,-1.14057677568714,
126.020192175583));
#77162=CARTESIAN_POINT('Ctrl Pts',(-16.5252889693026,-1.2740514986857,126.052013414956));
#77163=CARTESIAN_POINT('Ctrl Pts',(-16.5330353025681,-1.40619274014424,
126.089424457408));
#77164=CARTESIAN_POINT('Ctrl Pts',(-16.5407816358334,-1.53650518950799,
126.132280260261));
#77165=CARTESIAN_POINT('Ctrl Pts',(-16.5485297038364,-1.66684682144125,
126.175145660374));
#77166=CARTESIAN_POINT('Ctrl Pts',(-16.5562777718393,-1.79535847500655,
126.223458125068));
#77167=CARTESIAN_POINT('Ctrl Pts',(-16.5640258398423,-1.92156224084664,
126.277023473388));
#77168=CARTESIAN_POINT('Ctrl Pts',(-16.5717821425842,-2.04790013755073,
126.330645751598));
#77169=CARTESIAN_POINT('Ctrl Pts',(-16.5795384453261,-2.17192488623211,
126.389531912739));
#77170=CARTESIAN_POINT('Ctrl Pts',(-16.5872947480679,-2.29318022956406,
126.453440312937));
#77171=CARTESIAN_POINT('Ctrl Pts',(-16.5950551905821,-2.41450029052401,
126.517382822972));
#77172=CARTESIAN_POINT('Ctrl Pts',(-16.6028156330963,-2.53304766309654,
126.586352716718));
#77173=CARTESIAN_POINT('Ctrl Pts',(-16.6105760756105,-2.64839364082366,
126.660064032409));
#77174=CARTESIAN_POINT('Ctrl Pts',(-16.6183489758759,-2.76392478215401,
126.733893676048));
#77175=CARTESIAN_POINT('Ctrl Pts',(-16.6261218761413,-2.87624393842769,
126.812479727277));
#77176=CARTESIAN_POINT('Ctrl Pts',(-16.6338947764067,-2.98495344274703,
126.895494284838));
#77177=CARTESIAN_POINT('Ctrl Pts',(-16.6413851121687,-3.08971108276091,
126.97549105413));
#77178=CARTESIAN_POINT('Ctrl Pts',(-16.6488754479307,-3.19111671727947,
127.059599748347));
#77179=CARTESIAN_POINT('Ctrl Pts',(-16.6563657836927,-3.28884722901694,
127.147494887643));
#77180=CARTESIAN_POINT('Ctrl Pts',(-16.6640225481593,-3.38874922718535,
127.237342980002));
#77181=CARTESIAN_POINT('Ctrl Pts',(-16.6716793126258,-3.48514755370028,
127.331450921984));
#77182=CARTESIAN_POINT('Ctrl Pts',(-16.6793360770924,-3.57764871411246,
127.429510585208));
#77183=CARTESIAN_POINT('Ctrl Pts',(-16.6869840046077,-3.67004311555948,
127.527457074195));
#77184=CARTESIAN_POINT('Ctrl Pts',(-16.6946319321231,-3.7585490179369,127.629345928119));
#77185=CARTESIAN_POINT('Ctrl Pts',(-16.7022798596383,-3.84280610284961,
127.734829005349));
#77186=CARTESIAN_POINT('Ctrl Pts',(-16.7099207344897,-3.92698548868614,
127.840214809599));
#77187=CARTESIAN_POINT('Ctrl Pts',(-16.7175616093411,-4.00692359733335,
127.949187933855));
#77188=CARTESIAN_POINT('Ctrl Pts',(-16.7252024841924,-4.08229750108135,
128.061364049));
#77189=CARTESIAN_POINT('Ctrl Pts',(-16.7330813916031,-4.16001949239282,
128.177034733588));
#77190=CARTESIAN_POINT('Ctrl Pts',(-16.7409602990137,-4.23288795711076,
128.296110920379));
#77191=CARTESIAN_POINT('Ctrl Pts',(-16.7488392064244,-4.30059406355323,
128.418134776823));
#77192=CARTESIAN_POINT('Ctrl Pts',(-16.7564716269968,-4.36618202553259,
128.536341190949));
#77193=CARTESIAN_POINT('Ctrl Pts',(-16.7641040475692,-4.42692558976453,
128.657313221497));
#77194=CARTESIAN_POINT('Ctrl Pts',(-16.7717364681416,-4.4825888141779,128.780606535295));
#77195=CARTESIAN_POINT('Ctrl Pts',(-16.7797386189714,-4.54094848044659,
128.909872432524));
#77196=CARTESIAN_POINT('Ctrl Pts',(-16.7877407698011,-4.59372304626322,
129.041689728486));
#77197=CARTESIAN_POINT('Ctrl Pts',(-16.7957429206309,-4.64069621712328,
129.175520022886));
#77198=CARTESIAN_POINT('Ctrl Pts',(-16.8037450714606,-4.68766938798333,
129.309350317286));
#77199=CARTESIAN_POINT('Ctrl Pts',(-16.8117472222905,-4.72884100436561,
129.445193124185));
#77200=CARTESIAN_POINT('Ctrl Pts',(-16.8197493731203,-4.76405452823399,
129.582490119308));
#77201=CARTESIAN_POINT('Origin',(213.235140564004,0.,130.804360617566));
#77202=CARTESIAN_POINT('',(-18.9154222424341,-4.76405452823411,129.582490119308));
#77203=CARTESIAN_POINT('',(-18.5697878174478,-4.76405452823411,129.582490119308));
#77204=CARTESIAN_POINT('',(213.235140564004,-4.76405452823405,129.582490119308));
#77205=CARTESIAN_POINT('',(-17.2351405640403,-4.91824853831127,130.800568797544));
#77206=CARTESIAN_POINT('Ctrl Pts',(-17.2351405640404,-4.91824853831127,
130.800568797544));
#77207=CARTESIAN_POINT('Ctrl Pts',(-17.242791346641,-4.9183523543999,130.935225327462));
#77208=CARTESIAN_POINT('Ctrl Pts',(-17.2504421292416,-4.91292188126911,
131.070090008472));
#77209=CARTESIAN_POINT('Ctrl Pts',(-17.2580929118422,-4.90193244130674,
131.204662258038));
#77210=CARTESIAN_POINT('Ctrl Pts',(-17.2657360456441,-4.89095398793478,
131.339099970249));
#77211=CARTESIAN_POINT('Ctrl Pts',(-17.2733791794459,-4.87442765347894,
131.473245433197));
#77212=CARTESIAN_POINT('Ctrl Pts',(-17.2810223132477,-4.85238079457833,
131.606597295179));
#77213=CARTESIAN_POINT('Ctrl Pts',(-17.2889847026529,-4.82941303288812,
131.745519297663));
#77214=CARTESIAN_POINT('Ctrl Pts',(-17.2969470920581,-4.80045354815532,
131.88357952074));
#77215=CARTESIAN_POINT('Ctrl Pts',(-17.3049094814632,-4.76559332951731,
132.020215576087));
#77216=CARTESIAN_POINT('Ctrl Pts',(-17.3125438327696,-4.73216929784078,
132.151222437791));
#77217=CARTESIAN_POINT('Ctrl Pts',(-17.320178184076,-4.69332116779459,132.280919711161));
#77218=CARTESIAN_POINT('Ctrl Pts',(-17.3278125353824,-4.64918135176559,
132.408821842057));
#77219=CARTESIAN_POINT('Ctrl Pts',(-17.3354456647483,-4.60504860067531,
132.53670350117));
#77220=CARTESIAN_POINT('Ctrl Pts',(-17.3430787941143,-4.55562597908057,
132.662790207729));
#77221=CARTESIAN_POINT('Ctrl Pts',(-17.3507119234802,-4.50109547417136,
132.786612517526));
#77222=CARTESIAN_POINT('Ctrl Pts',(-17.3583455971132,-4.44656108105957,
132.910443656256));
#77223=CARTESIAN_POINT('Ctrl Pts',(-17.3659792707461,-4.3869182434371,133.032009708012));
#77224=CARTESIAN_POINT('Ctrl Pts',(-17.3736129443791,-4.32239647060258,
133.150862655371));
#77225=CARTESIAN_POINT('Ctrl Pts',(-17.3812489287406,-4.25785516689618,
133.269751579759));
#77226=CARTESIAN_POINT('Ctrl Pts',(-17.3888849131021,-4.18843218417436,
133.38592541255));
#77227=CARTESIAN_POINT('Ctrl Pts',(-17.3965208974636,-4.11440191721636,
133.498962615284));
#77228=CARTESIAN_POINT('Ctrl Pts',(-17.404165046103,-4.04029249822717,133.61212067567));
#77229=CARTESIAN_POINT('Ctrl Pts',(-17.4118091947424,-3.96156618482791,
133.72213507524));
#77230=CARTESIAN_POINT('Ctrl Pts',(-17.4194533433818,-3.87853958880925,
133.828614859613));
#77231=CARTESIAN_POINT('Ctrl Pts',(-17.4271023184276,-3.79546057098146,
133.935161873804));
#77232=CARTESIAN_POINT('Ctrl Pts',(-17.4347512934735,-3.70807612667641,
134.038169524355));
#77233=CARTESIAN_POINT('Ctrl Pts',(-17.4424002685193,-3.61674080626019,
134.137282609277));
#77234=CARTESIAN_POINT('Ctrl Pts',(-17.4500599647972,-3.52527746514158,
134.236534616652));
#77235=CARTESIAN_POINT('Ctrl Pts',(-17.4577196610751,-3.42985248215683,
134.331880882519));
#77236=CARTESIAN_POINT('Ctrl Pts',(-17.4653793573529,-3.33085478546361,
134.423005316988));
#77237=CARTESIAN_POINT('Ctrl Pts',(-17.4676261245592,-3.301816456741,134.449734234641));
#77238=CARTESIAN_POINT('Ctrl Pts',(-17.4698728917655,-3.27247093466944,
134.476100191047));
#77239=CARTESIAN_POINT('Ctrl Pts',(-17.4721196589718,-3.24282850706724,
134.50209591586));
#77240=CARTESIAN_POINT('Ctrl Pts',(-17.4798939930909,-3.14025885248444,
134.592047135461));
#77241=CARTESIAN_POINT('Ctrl Pts',(-17.48766832721,-3.03378122980677,134.677869903543));
#77242=CARTESIAN_POINT('Ctrl Pts',(-17.4954426613291,-2.92376214681279,
134.759205490802));
#77243=CARTESIAN_POINT('Ctrl Pts',(-17.5032074142761,-2.81387865250606,
134.84044083922));
#77244=CARTESIAN_POINT('Ctrl Pts',(-17.5109721672232,-2.70046269336695,
134.917199779777));
#77245=CARTESIAN_POINT('Ctrl Pts',(-17.5187369201703,-2.58391599401656,
134.989161831288));
#77246=CARTESIAN_POINT('Ctrl Pts',(-17.5264939610553,-2.46748505049051,
135.061052409074));
#77247=CARTESIAN_POINT('Ctrl Pts',(-17.5342510019404,-2.34792988529786,
135.128155374986));
#77248=CARTESIAN_POINT('Ctrl Pts',(-17.5420080428254,-2.2256832425133,135.190192028655));
#77249=CARTESIAN_POINT('Ctrl Pts',(-17.5497592340655,-2.10352878687318,
135.252181900001));
#77250=CARTESIAN_POINT('Ctrl Pts',(-17.5575104253056,-1.97868724079575,
135.309112887457));
#77251=CARTESIAN_POINT('Ctrl Pts',(-17.5652616165457,-1.85161781468985,
135.360751133185));
#77252=CARTESIAN_POINT('Ctrl Pts',(-17.5730095133228,-1.72460239647992,
135.412367431281));
#77253=CARTESIAN_POINT('Ctrl Pts',(-17.5807574100999,-1.59536134301193,
135.458695314964));
#77254=CARTESIAN_POINT('Ctrl Pts',(-17.588505306877,-1.46437560612231,135.49954827587));
#77255=CARTESIAN_POINT('Ctrl Pts',(-17.5962515829611,-1.33341726862513,
135.540392691218));
#77256=CARTESIAN_POINT('Ctrl Pts',(-17.6039978590452,-1.20071534660909,
135.575764345391));
#77257=CARTESIAN_POINT('Ctrl Pts',(-17.6117441351293,-1.06676740657806,
135.60552613885));
#77258=CARTESIAN_POINT('Ctrl Pts',(-17.6194904683946,-0.932818477773584,
135.635288152003));
#77259=CARTESIAN_POINT('Ctrl Pts',(-17.62723680166,-0.797623894258367,135.659440137008));
#77260=CARTESIAN_POINT('Ctrl Pts',(-17.6349831349254,-0.66169251676377,
135.677895892473));
#77261=CARTESIAN_POINT('Ctrl Pts',(-17.6427312029284,-0.525730698379665,
135.696355780976));
#77262=CARTESIAN_POINT('Ctrl Pts',(-17.6504792709313,-0.389032145022043,
135.70911684899));
#77263=CARTESIAN_POINT('Ctrl Pts',(-17.6582273389343,-0.25211156061956,
135.716144695017));
#77264=CARTESIAN_POINT('Ctrl Pts',(-17.6659836416762,-0.115045455390599,
135.723180010323));
#77265=CARTESIAN_POINT('Ctrl Pts',(-17.673739944418,0.0222427611993643,
135.724469911472));
#77266=CARTESIAN_POINT('Ctrl Pts',(-17.6814962471599,0.1592370974715,135.720032149441));
#77267=CARTESIAN_POINT('Ctrl Pts',(-17.689256689674,0.296304551745537,135.715592018844));
#77268=CARTESIAN_POINT('Ctrl Pts',(-17.6970171321881,0.433077423462034,
135.705418162671));
#77269=CARTESIAN_POINT('Ctrl Pts',(-17.7047775747023,0.56904511345047,135.689580236105));
#77270=CARTESIAN_POINT('Ctrl Pts',(-17.7125504749677,0.705231070845705,
135.673716885094));
#77271=CARTESIAN_POINT('Ctrl Pts',(-17.7203233752332,0.840608877259587,
135.652171355525));
#77272=CARTESIAN_POINT('Ctrl Pts',(-17.7280962754986,0.974677503587224,
135.625064593802));
#77273=CARTESIAN_POINT('Ctrl Pts',(-17.7355866112607,1.10387239764918,135.598943231146));
#77274=CARTESIAN_POINT('Ctrl Pts',(-17.7430769470227,1.23185134387066,135.567658019318));
#77275=CARTESIAN_POINT('Ctrl Pts',(-17.7505672827847,1.35818141320068,135.531360333172));
#77276=CARTESIAN_POINT('Ctrl Pts',(-17.7583416169038,1.48930132550655,135.493686409222));
#77277=CARTESIAN_POINT('Ctrl Pts',(-17.7661159510229,1.61906020683902,135.450493072147));
#77278=CARTESIAN_POINT('Ctrl Pts',(-17.773890285142,1.74695814166771,135.401894773367));
#77279=CARTESIAN_POINT('Ctrl Pts',(-17.781655038089,1.87469845372195,135.353356367648));
#77280=CARTESIAN_POINT('Ctrl Pts',(-17.7894197910361,2.0005820205927,135.299426391431));
#77281=CARTESIAN_POINT('Ctrl Pts',(-17.7971845439831,2.12412207040947,135.240269599105));
#77282=CARTESIAN_POINT('Ctrl Pts',(-17.8049415848681,2.24753941850733,135.18117156214));
#77283=CARTESIAN_POINT('Ctrl Pts',(-17.8126986257531,2.36861753126765,135.116857207842));
#77284=CARTESIAN_POINT('Ctrl Pts',(-17.8204556666381,2.48688802143333,135.0475399717));
#77285=CARTESIAN_POINT('Ctrl Pts',(-17.8282068578782,2.60506932290205,134.978275008226));
#77286=CARTESIAN_POINT('Ctrl Pts',(-17.8359580491183,2.72044688009677,134.904014869152));
#77287=CARTESIAN_POINT('Ctrl Pts',(-17.8437092403584,2.83257572735218,134.825019495327));
#77288=CARTESIAN_POINT('Ctrl Pts',(-17.8514571371355,2.94465691685683,134.746057696642));
#77289=CARTESIAN_POINT('Ctrl Pts',(-17.8592050339125,3.05349182376089,134.662364890815));
#77290=CARTESIAN_POINT('Ctrl Pts',(-17.8669529306896,3.15866356708052,134.57424490392));
#77291=CARTESIAN_POINT('Ctrl Pts',(-17.8746992067737,3.26381331073868,134.486143349826));
#77292=CARTESIAN_POINT('Ctrl Pts',(-17.8824454828578,3.36530111544672,134.393616707602));
#77293=CARTESIAN_POINT('Ctrl Pts',(-17.8901917589419,3.46274268862814,134.297009488388));
#77294=CARTESIAN_POINT('Ctrl Pts',(-17.8979380922073,3.56018498110112,134.200401556041));
#77295=CARTESIAN_POINT('Ctrl Pts',(-17.9056844254726,3.65358070480708,134.099713261861));
#77296=CARTESIAN_POINT('Ctrl Pts',(-17.913430758738,3.74258228441788,133.995326130833));
#77297=CARTESIAN_POINT('Ctrl Pts',(-17.9211788267409,3.83160379531533,133.890915623032));
#77298=CARTESIAN_POINT('Ctrl Pts',(-17.9289268947439,3.91622895038564,133.782804927556));
#77299=CARTESIAN_POINT('Ctrl Pts',(-17.9366749627469,3.99615059662795,133.671408484549));
#77300=CARTESIAN_POINT('Ctrl Pts',(-17.9444312654888,4.07615718454707,133.559893648076));
#77301=CARTESIAN_POINT('Ctrl Pts',(-17.9521875682306,4.15145004943383,133.445086406333));
#77302=CARTESIAN_POINT('Ctrl Pts',(-17.9599438709725,4.22176521958163,133.32743047257));
#77303=CARTESIAN_POINT('Ctrl Pts',(-17.9677043134867,4.29211791905289,133.209711742293));
#77304=CARTESIAN_POINT('Ctrl Pts',(-17.9754647560009,4.35748744374197,133.089141633937));
#77305=CARTESIAN_POINT('Ctrl Pts',(-17.9832251985151,4.4176564052034,132.966187379373));
#77306=CARTESIAN_POINT('Ctrl Pts',(-17.9909980987805,4.47792195522324,132.843035747724));
#77307=CARTESIAN_POINT('Ctrl Pts',(-17.9987709990459,4.5329701021494,132.717492680079));
#77308=CARTESIAN_POINT('Ctrl Pts',(-18.0065438993113,4.58263178314732,132.590045080899));
#77309=CARTESIAN_POINT('Ctrl Pts',(-18.0140342350734,4.63048813695142,132.467230522968));
#77310=CARTESIAN_POINT('Ctrl Pts',(-18.0215245708356,4.67334274869021,132.342647789781));
#77311=CARTESIAN_POINT('Ctrl Pts',(-18.0290149065977,4.71108896558805,132.216742938616));
#77312=CARTESIAN_POINT('Ctrl Pts',(-18.0367892407168,4.75026634177178,132.086064366753));
#77313=CARTESIAN_POINT('Ctrl Pts',(-18.0445635748359,4.78406440888829,131.95354749118));
#77314=CARTESIAN_POINT('Ctrl Pts',(-18.0523379089549,4.81230924160563,131.819674768781));
#77315=CARTESIAN_POINT('Ctrl Pts',(-18.060102661902,4.84051926509096,131.685967032548));
#77316=CARTESIAN_POINT('Ctrl Pts',(-18.0678674148492,4.86318959149349,131.550907153072));
#77317=CARTESIAN_POINT('Ctrl Pts',(-18.0756321677963,4.88019572126216,131.414993719088));
#77318=CARTESIAN_POINT('Ctrl Pts',(-18.0833892086813,4.89718496030306,131.279215276242));
#77319=CARTESIAN_POINT('Ctrl Pts',(-18.0911462495663,4.90852114999944,131.142585351402));
#77320=CARTESIAN_POINT('Ctrl Pts',(-18.0989032904513,4.91413068491909,131.005613379129));
#77321=CARTESIAN_POINT('Ctrl Pts',(-18.1066544816915,4.9197359896448,130.868744698485));
#77322=CARTESIAN_POINT('Ctrl Pts',(-18.1144056729316,4.91962321940245,130.73153487288));
#77323=CARTESIAN_POINT('Ctrl Pts',(-18.1221568641717,4.91377055497893,130.594498768908));
#77324=CARTESIAN_POINT('Ctrl Pts',(-18.1299047609488,4.90792037809391,130.457520908936));
#77325=CARTESIAN_POINT('Ctrl Pts',(-18.1376526577259,4.89633517586987,130.320717013532));
#77326=CARTESIAN_POINT('Ctrl Pts',(-18.145400554503,4.87904523143392,130.184602041892));
#77327=CARTESIAN_POINT('Ctrl Pts',(-18.1531468305871,4.86175890368161,130.048515542569));
#77328=CARTESIAN_POINT('Ctrl Pts',(-18.1608931066712,4.83877025650969,129.913118067973));
#77329=CARTESIAN_POINT('Ctrl Pts',(-18.1686393827553,4.81016141737309,129.778919151018));
#77330=CARTESIAN_POINT('Ctrl Pts',(-18.1763857160206,4.78155236705253,129.644719243438));
#77331=CARTESIAN_POINT('Ctrl Pts',(-18.184132049286,4.7473231234982,129.511718293527));
#77332=CARTESIAN_POINT('Ctrl Pts',(-18.1918783825514,4.70760680153173,129.380414949827));
#77333=CARTESIAN_POINT('Ctrl Pts',(-18.1996264505543,4.66788158537027,129.249082201654));
#77334=CARTESIAN_POINT('Ctrl Pts',(-18.2073745185573,4.62266695881221,129.119448190329));
#77335=CARTESIAN_POINT('Ctrl Pts',(-18.2151225865603,4.572145578387,128.991995347391));
#77336=CARTESIAN_POINT('Ctrl Pts',(-18.2228788893021,4.52157050323761,128.864407046056));
#77337=CARTESIAN_POINT('Ctrl Pts',(-18.230635192044,4.46567755185105,128.739004907937));
#77338=CARTESIAN_POINT('Ctrl Pts',(-18.2383914947858,4.40469734959564,128.616250857758));
#77339=CARTESIAN_POINT('Ctrl Pts',(-18.2461519373,4.34368460036996,128.493431290046));
#77340=CARTESIAN_POINT('Ctrl Pts',(-18.2539123798142,4.27757937832064,128.373262968909));
#77341=CARTESIAN_POINT('Ctrl Pts',(-18.2616728223284,4.20665727508862,128.256181339641));
#77342=CARTESIAN_POINT('Ctrl Pts',(-18.2694457225938,4.13562132140052,128.138911760549));
#77343=CARTESIAN_POINT('Ctrl Pts',(-18.2772186228593,4.05975325106519,128.024739100873));
#77344=CARTESIAN_POINT('Ctrl Pts',(-18.2849915231247,3.97937132800418,127.91406878172));
#77345=CARTESIAN_POINT('Ctrl Pts',(-18.2924818588866,3.90191149031716,127.807421607431));
#77346=CARTESIAN_POINT('Ctrl Pts',(-18.2999721946486,3.82026047294958,127.704026798482));
#77347=CARTESIAN_POINT('Ctrl Pts',(-18.3074625304105,3.73473590809163,127.604215189728));
#77348=CARTESIAN_POINT('Ctrl Pts',(-18.3152368645296,3.64596865336136,127.50061919349));
#77349=CARTESIAN_POINT('Ctrl Pts',(-18.3230111986487,3.55274713370896,127.400555314262));
#77350=CARTESIAN_POINT('Ctrl Pts',(-18.3307855327678,3.45538324288425,127.304430660082));
#77351=CARTESIAN_POINT('Ctrl Pts',(-18.3385502857149,3.35813934435344,127.208424470947));
#77352=CARTESIAN_POINT('Ctrl Pts',(-18.3463150386619,3.25676350783038,127.11634811941));
#77353=CARTESIAN_POINT('Ctrl Pts',(-18.354079791609,3.15160791508874,127.028575849859));
#77354=CARTESIAN_POINT('Ctrl Pts',(-18.361836832494,3.04655676436411,126.940890756962));
#77355=CARTESIAN_POINT('Ctrl Pts',(-18.3695938733791,2.93773362646882,126.857501487766));
#77356=CARTESIAN_POINT('Ctrl Pts',(-18.3773509142641,2.82552731759192,126.778745330428));
#77357=CARTESIAN_POINT('Ctrl Pts',(-18.3851021055042,2.71340562436645,126.700048563721));
#77358=CARTESIAN_POINT('Ctrl Pts',(-18.3928532967442,2.59790615703109,126.625978178244));
#77359=CARTESIAN_POINT('Ctrl Pts',(-18.4006044879843,2.47945029361585,126.55683082909));
#77360=CARTESIAN_POINT('Ctrl Pts',(-18.4083523847614,2.36104477710151,126.487712869404));
#77361=CARTESIAN_POINT('Ctrl Pts',(-18.4161002815385,2.23968570062472,126.423513981058));
#77362=CARTESIAN_POINT('Ctrl Pts',(-18.4238481783156,2.11582268270914,126.364487034024));
#77363=CARTESIAN_POINT('Ctrl Pts',(-18.4315944543997,1.99198557426674,126.305472434155));
#77364=CARTESIAN_POINT('Ctrl Pts',(-18.4393407304837,1.86564591890809,126.251627791806));
#77365=CARTESIAN_POINT('Ctrl Pts',(-18.4470870065678,1.73727679300059,126.203159425812));
#77366=CARTESIAN_POINT('Ctrl Pts',(-18.4548333398332,1.60890671950155,126.154690702035));
#77367=CARTESIAN_POINT('Ctrl Pts',(-18.4625796730985,1.47850751132211,126.111598471904));
#77368=CARTESIAN_POINT('Ctrl Pts',(-18.4703260063639,1.34657064741566,126.074040273866));
#77369=CARTESIAN_POINT('Ctrl Pts',(-18.4780740743669,1.21460423716296,126.036473664931));
#77370=CARTESIAN_POINT('Ctrl Pts',(-18.4858221423698,1.08109986192609,126.004443661191));
#77371=CARTESIAN_POINT('Ctrl Pts',(-18.4935702103728,0.946562135337526,
125.978057354566));
#77372=CARTESIAN_POINT('Ctrl Pts',(-18.5013265131146,0.811881420452674,
125.95164300426));
#77373=CARTESIAN_POINT('Ctrl Pts',(-18.5090828158565,0.676165544595105,
125.930884408462));
#77374=CARTESIAN_POINT('Ctrl Pts',(-18.5168391185983,0.539927796761214,
125.915837217112));
#77375=CARTESIAN_POINT('Ctrl Pts',(-18.5245995611125,0.403617334738895,
125.900781994623));
#77376=CARTESIAN_POINT('Ctrl Pts',(-18.5323600036267,0.266784835595289,
125.891444277281));
#77377=CARTESIAN_POINT('Ctrl Pts',(-18.5401204461409,0.129945615803143,
125.887827570852));
#77378=CARTESIAN_POINT('Ctrl Pts',(-18.5478933464063,-0.00711327045281471,
125.884205058564));
#77379=CARTESIAN_POINT('Ctrl Pts',(-18.5556662466717,-0.144178507772764,
125.886321903455));
#77380=CARTESIAN_POINT('Ctrl Pts',(-18.5634391469371,-0.2807369744749,125.894129481085));
#77381=CARTESIAN_POINT('Ctrl Pts',(-18.5709294826992,-0.412331196943699,
125.901653233603));
#77382=CARTESIAN_POINT('Ctrl Pts',(-18.5784198184614,-0.543454547332617,
125.914461127196));
#77383=CARTESIAN_POINT('Ctrl Pts',(-18.5859101542235,-0.673656996951168,
125.932464753227));
#77384=CARTESIAN_POINT('Ctrl Pts',(-18.5936844883426,-0.80879611201966,
125.951150992212));
#77385=CARTESIAN_POINT('Ctrl Pts',(-18.6014588224617,-0.943371196004674,
125.975493925947));
#77386=CARTESIAN_POINT('Ctrl Pts',(-18.6092331565808,-1.07687115119386,
126.005451201227));
#77387=CARTESIAN_POINT('Ctrl Pts',(-18.6169979095279,-1.21020657962005,
126.035371556843));
#77388=CARTESIAN_POINT('Ctrl Pts',(-18.624762662475,-1.34246913778945,126.070892402127));
#77389=CARTESIAN_POINT('Ctrl Pts',(-18.6325274154221,-1.47315360044864,
126.111919724813));
#77390=CARTESIAN_POINT('Ctrl Pts',(-18.6402844563072,-1.60370826545683,
126.152906298583));
#77391=CARTESIAN_POINT('Ctrl Pts',(-18.6480414971921,-1.73268758352382,
126.199388349629));
#77392=CARTESIAN_POINT('Ctrl Pts',(-18.6557985380771,-1.8595976199223,126.251221068367));
#77393=CARTESIAN_POINT('Ctrl Pts',(-18.6635497293172,-1.9864119524746,126.303014699649));
#77394=CARTESIAN_POINT('Ctrl Pts',(-18.6713009205574,-2.11115974888513,
126.360150820014));
#77395=CARTESIAN_POINT('Ctrl Pts',(-18.6790521117975,-2.23336365970487,
126.422435261514));
#77396=CARTESIAN_POINT('Ctrl Pts',(-18.6868000085746,-2.35551563060294,
126.484693230466));
#77397=CARTESIAN_POINT('Ctrl Pts',(-18.6945479053517,-2.47512551877083,
126.552094991278));
#77398=CARTESIAN_POINT('Ctrl Pts',(-18.7022958021288,-2.59173754774647,
126.624398949548));
#77399=CARTESIAN_POINT('Ctrl Pts',(-18.7100420782129,-2.7083251839995,126.696687783389));
#77400=CARTESIAN_POINT('Ctrl Pts',(-18.7177883542969,-2.82191587630561,
126.773876569149));
#77401=CARTESIAN_POINT('Ctrl Pts',(-18.725534630381,-2.93208033345547,126.855678814652));
#77402=CARTESIAN_POINT('Ctrl Pts',(-18.7332809636464,-3.04224560381403,
126.937481664));
#77403=CARTESIAN_POINT('Ctrl Pts',(-18.7410272969117,-3.14898427465706,
127.023897807967));
#77404=CARTESIAN_POINT('Ctrl Pts',(-18.748773630177,-3.25189814804754,127.114598904769));
#77405=CARTESIAN_POINT('Ctrl Pts',(-18.75652169818,-3.35483506828656,127.205320313452));
#77406=CARTESIAN_POINT('Ctrl Pts',(-18.764269766183,-3.45394519341066,127.300328325981));
#77407=CARTESIAN_POINT('Ctrl Pts',(-18.7720178341859,-3.54886566796082,
127.399256282414));
#77408=CARTESIAN_POINT('Ctrl Pts',(-18.7797741369278,-3.64388702512104,
127.498289380657));
#77409=CARTESIAN_POINT('Ctrl Pts',(-18.7875304396697,-3.734709565626,127.601250462603));
#77410=CARTESIAN_POINT('Ctrl Pts',(-18.7952867424115,-3.82100902436337,
127.707737763837));
#77411=CARTESIAN_POINT('Ctrl Pts',(-18.8030471849257,-3.90735454372017,
127.81428190055));
#77412=CARTESIAN_POINT('Ctrl Pts',(-18.8108076274399,-3.98917193788441,
127.924355693068));
#77413=CARTESIAN_POINT('Ctrl Pts',(-18.818568069954,-4.06617971621538,128.037527485999));
#77414=CARTESIAN_POINT('Ctrl Pts',(-18.8263409702195,-4.14331111426867,
128.150880952339));
#77415=CARTESIAN_POINT('Ctrl Pts',(-18.8341138704849,-4.21561726148516,
128.267342024756));
#77416=CARTESIAN_POINT('Ctrl Pts',(-18.8418867707503,-4.28286171218099,
128.386452716749));
#77417=CARTESIAN_POINT('Ctrl Pts',(-18.8493771065123,-4.34766165771511,
128.501233435066));
#77418=CARTESIAN_POINT('Ctrl Pts',(-18.8568674422743,-4.4077613878469,128.618474202689));
#77419=CARTESIAN_POINT('Ctrl Pts',(-18.8643577780363,-4.46299203176705,
128.737748610709));
#77420=CARTESIAN_POINT('Ctrl Pts',(-18.8728685221026,-4.52574674530165,
128.87327176916));
#77421=CARTESIAN_POINT('Ctrl Pts',(-18.8813792661689,-4.58238994528214,
129.011796482427));
#77422=CARTESIAN_POINT('Ctrl Pts',(-18.8898900102352,-4.63264986635917,
129.152774023341));
#77423=CARTESIAN_POINT('Ctrl Pts',(-18.8984007543015,-4.68290978743619,
129.293751564256));
#77424=CARTESIAN_POINT('Ctrl Pts',(-18.9069114983678,-4.72678625655128,
129.437181693642));
#77425=CARTESIAN_POINT('Ctrl Pts',(-18.9154222424341,-4.76405452823411,
129.582490119308));
#77426=CARTESIAN_POINT('Ctrl Pts',(-17.1650861998779,-4.76405452823408,
129.582490119308));
#77427=CARTESIAN_POINT('Ctrl Pts',(-17.1728615289864,-4.79806952616346,
129.715114079985));
#77428=CARTESIAN_POINT('Ctrl Pts',(-17.1806368580948,-4.82649955024039,
129.848992775321));
#77429=CARTESIAN_POINT('Ctrl Pts',(-17.1884121872032,-4.8492846135786,129.983615956292));
#77430=CARTESIAN_POINT('Ctrl Pts',(-17.1901654698551,-4.85442248693634,
130.013972547563));
#77431=CARTESIAN_POINT('Ctrl Pts',(-17.1919187525071,-4.85927353984324,
130.044366983506));
#77432=CARTESIAN_POINT('Ctrl Pts',(-17.193672035159,-4.86383745032036,130.074793403828));
#77433=CARTESIAN_POINT('Ctrl Pts',(-17.2074948781088,-4.89981922296458,
130.314674651259));
#77434=CARTESIAN_POINT('Ctrl Pts',(-17.2213177210587,-4.91806097139444,
130.557281781475));
#77435=CARTESIAN_POINT('Ctrl Pts',(-17.2351405640086,-4.91824853831084,
130.800568796985));
#77436=CARTESIAN_POINT('',(-16.8898594359349,-4.91824838856106,130.808341938514));
#77437=CARTESIAN_POINT('Ctrl Pts',(-16.8197493731203,-4.76405452823399,
129.582490119308));
#77438=CARTESIAN_POINT('Ctrl Pts',(-16.8273867555103,-4.79766288588759,
129.713528595721));
#77439=CARTESIAN_POINT('Ctrl Pts',(-16.8350241379004,-4.82584429192238,
129.845891195246));
#77440=CARTESIAN_POINT('Ctrl Pts',(-16.8426615202905,-4.84851502478482,
129.97908180593));
#77441=CARTESIAN_POINT('Ctrl Pts',(-16.8505278395646,-4.87186533170469,
130.116264915853));
#77442=CARTESIAN_POINT('Ctrl Pts',(-16.8583941588386,-4.88936933475787,
130.25432599799));
#77443=CARTESIAN_POINT('Ctrl Pts',(-16.8662604781127,-4.90099312143358,
130.392718192444));
#77444=CARTESIAN_POINT('Ctrl Pts',(-16.8741267973868,-4.91261690810929,
130.531110386897));
#77445=CARTESIAN_POINT('Ctrl Pts',(-16.8819931166608,-4.91836051132978,
130.669833229029));
#77446=CARTESIAN_POINT('Ctrl Pts',(-16.8898594359349,-4.91824838856106,
130.808341938514));
#77447=CARTESIAN_POINT('Ctrl Pts',(-16.8898594359912,-4.91824838856026,
130.808341939505));
#77448=CARTESIAN_POINT('Ctrl Pts',(-16.9024630796802,-4.91806874218068,
131.030264589901));
#77449=CARTESIAN_POINT('Ctrl Pts',(-16.9150667233692,-4.90286602102809,
131.251597493366));
#77450=CARTESIAN_POINT('Ctrl Pts',(-16.9276703670583,-4.87289314661139,
131.47076548265));
#77451=CARTESIAN_POINT('Ctrl Pts',(-16.9300513805408,-4.86723083023245,
131.512169536135));
#77452=CARTESIAN_POINT('Ctrl Pts',(-16.9324323940232,-4.86104148805206,
131.553496435964));
#77453=CARTESIAN_POINT('Ctrl Pts',(-16.9348134075057,-4.85432696824674,
131.594735685399));
#77454=CARTESIAN_POINT('Ctrl Pts',(-16.9425877416248,-4.83240314429537,
131.729387465529));
#77455=CARTESIAN_POINT('Ctrl Pts',(-16.9503620757439,-4.80483778977211,
131.863339631926));
#77456=CARTESIAN_POINT('Ctrl Pts',(-16.958136409863,-4.7716855106225,131.996082250421));
#77457=CARTESIAN_POINT('Ctrl Pts',(-16.9659011628101,-4.73857408869403,
132.128661275503));
#77458=CARTESIAN_POINT('Ctrl Pts',(-16.9736659157571,-4.69988953582749,
132.260033342977));
#77459=CARTESIAN_POINT('Ctrl Pts',(-16.9814306687042,-4.65573796123039,
132.38969562912));
#77460=CARTESIAN_POINT('Ctrl Pts',(-16.9891877095892,-4.61163023859967,
132.519229132852));
#77461=CARTESIAN_POINT('Ctrl Pts',(-16.9969447504742,-4.56206642523747,
132.647055867001));
#77462=CARTESIAN_POINT('Ctrl Pts',(-17.0047017913592,-4.50720314209734,
132.772685514113));
#77463=CARTESIAN_POINT('Ctrl Pts',(-17.0124529825993,-4.45238123178581,
132.898220422931));
#77464=CARTESIAN_POINT('Ctrl Pts',(-17.0202041738394,-4.39226796206567,
133.021561185711));
#77465=CARTESIAN_POINT('Ctrl Pts',(-17.0279553650795,-4.32706890003891,
133.142235249965));
#77466=CARTESIAN_POINT('Ctrl Pts',(-17.0357032618566,-4.26189754935266,
133.262858024523));
#77467=CARTESIAN_POINT('Ctrl Pts',(-17.0434511586337,-4.19164489106718,
133.380816011586));
#77468=CARTESIAN_POINT('Ctrl Pts',(-17.0511990554108,-4.11656338738992,
133.495659363544));
#77469=CARTESIAN_POINT('Ctrl Pts',(-17.0589453314949,-4.04149758914457,
133.610478692748));
#77470=CARTESIAN_POINT('Ctrl Pts',(-17.066691607579,-3.96160516843571,133.722184355716));
#77471=CARTESIAN_POINT('Ctrl Pts',(-17.0744378836632,-3.87718283674348,
133.830354059886));
#77472=CARTESIAN_POINT('Ctrl Pts',(-17.0821842169285,-3.79275988186488,
133.938524562539));
#77473=CARTESIAN_POINT('Ctrl Pts',(-17.0899305501939,-3.7038071898228,134.043158746103));
#77474=CARTESIAN_POINT('Ctrl Pts',(-17.0976768834592,-3.61066256349931,
134.143866406608));
#77475=CARTESIAN_POINT('Ctrl Pts',(-17.1054249514622,-3.51749707808281,
134.244596619895));
#77476=CARTESIAN_POINT('Ctrl Pts',(-17.1131730194652,-3.4201380557876,134.341398273417));
#77477=CARTESIAN_POINT('Ctrl Pts',(-17.1209210874681,-3.3189607584973,134.433917415035));
#77478=CARTESIAN_POINT('Ctrl Pts',(-17.12867739021,-3.21767592877127,134.526534887099));
#77479=CARTESIAN_POINT('Ctrl Pts',(-17.1364336929518,-3.11256500652557,
134.614860490884));
#77480=CARTESIAN_POINT('Ctrl Pts',(-17.1441899956937,-3.00403742194753,
134.698579695897));
#77481=CARTESIAN_POINT('Ctrl Pts',(-17.1519504382079,-2.89545191292975,
134.782343584371));
#77482=CARTESIAN_POINT('Ctrl Pts',(-17.159710880722,-2.78344642708021,134.861495949634));
#77483=CARTESIAN_POINT('Ctrl Pts',(-17.1674713232362,-2.66845925048317,
134.935765740646));
#77484=CARTESIAN_POINT('Ctrl Pts',(-17.1752442235016,-2.55328748626217,
135.01015475612));
#77485=CARTESIAN_POINT('Ctrl Pts',(-17.183017123767,-2.43512480359333,135.079645336333));
#77486=CARTESIAN_POINT('Ctrl Pts',(-17.1907900240325,-2.31443473113332,
135.144012094105));
#77487=CARTESIAN_POINT('Ctrl Pts',(-17.1982803597945,-2.19813204680751,
135.206038958101));
#77488=CARTESIAN_POINT('Ctrl Pts',(-17.2057706955565,-2.07948281381779,
135.263307925841));
#77489=CARTESIAN_POINT('Ctrl Pts',(-17.2132610313185,-1.95891737071349,
135.315660407784));
#77490=CARTESIAN_POINT('Ctrl Pts',(-17.2210353654376,-1.83378065218863,
135.369997849991));
#77491=CARTESIAN_POINT('Ctrl Pts',(-17.2288096995567,-1.70618315343553,
135.419210754441));
#77492=CARTESIAN_POINT('Ctrl Pts',(-17.2365840336757,-1.57658341235972,
135.463069430786));
#77493=CARTESIAN_POINT('Ctrl Pts',(-17.2443487866228,-1.44714339138213,
135.506874055232));
#77494=CARTESIAN_POINT('Ctrl Pts',(-17.2521135395699,-1.31570640461834,
135.545337456714));
#77495=CARTESIAN_POINT('Ctrl Pts',(-17.259878292517,-1.18275284652813,135.578277119405));
#77496=CARTESIAN_POINT('Ctrl Pts',(-17.267635333402,-1.04993133978614,135.611184065959));
#77497=CARTESIAN_POINT('Ctrl Pts',(-17.275392374287,-0.915596636319013,
135.638578098207));
#77498=CARTESIAN_POINT('Ctrl Pts',(-17.283149415172,-0.780245911539738,
135.660325957231));
#77499=CARTESIAN_POINT('Ctrl Pts',(-17.2909006064121,-0.64499725579471,
135.682057416025));
#77500=CARTESIAN_POINT('Ctrl Pts',(-17.2986517976523,-0.508734488243535,
135.698151114762));
#77501=CARTESIAN_POINT('Ctrl Pts',(-17.3064029888924,-0.371966294718296,
135.708524576703));
#77502=CARTESIAN_POINT('Ctrl Pts',(-17.3141508856695,-0.235256231323903,
135.718893629645));
#77503=CARTESIAN_POINT('Ctrl Pts',(-17.3218987824465,-0.0980415582443893,
135.723547251862));
#77504=CARTESIAN_POINT('Ctrl Pts',(-17.3296466792236,0.039162792995575,
135.722454693338));
#77505=CARTESIAN_POINT('Ctrl Pts',(-17.3373929553077,0.176338444043044,
135.721362363354));
#77506=CARTESIAN_POINT('Ctrl Pts',(-17.3451392313919,0.313503386840421,
135.714526246537));
#77507=CARTESIAN_POINT('Ctrl Pts',(-17.352885507476,0.450141954892986,135.701967715215));
#77508=CARTESIAN_POINT('Ctrl Pts',(-17.3606318407413,0.58678153158042,135.689409091189));
#77509=CARTESIAN_POINT('Ctrl Pts',(-17.3683781740066,0.722894336445406,
135.671128004152));
#77510=CARTESIAN_POINT('Ctrl Pts',(-17.376124507272,0.857969489129146,135.647197742457));
#77511=CARTESIAN_POINT('Ctrl Pts',(-17.3838725752749,0.993074890956783,
135.623262121747));
#77512=CARTESIAN_POINT('Ctrl Pts',(-17.3916206432778,1.12714179330706,135.593674877179));
#77513=CARTESIAN_POINT('Ctrl Pts',(-17.3993687112808,1.25966956800745,135.558560407429));
#77514=CARTESIAN_POINT('Ctrl Pts',(-17.4071250140226,1.3923381948039,135.523408617603));
#77515=CARTESIAN_POINT('Ctrl Pts',(-17.4148813167645,1.52346404773039,135.482717968141));
#77516=CARTESIAN_POINT('Ctrl Pts',(-17.4226376195064,1.6525611963574,135.436662912839));
#77517=CARTESIAN_POINT('Ctrl Pts',(-17.4303980620205,1.78172724801967,135.390583276568));
#77518=CARTESIAN_POINT('Ctrl Pts',(-17.4381585045348,1.90886207561422,135.339133675991));
#77519=CARTESIAN_POINT('Ctrl Pts',(-17.4459189470489,2.03350073189098,135.282536343897));
#77520=CARTESIAN_POINT('Ctrl Pts',(-17.4536918473144,2.15833946920369,135.22584815674));
#77521=CARTESIAN_POINT('Ctrl Pts',(-17.4614647475798,2.28067367867874,135.163995901277));
#77522=CARTESIAN_POINT('Ctrl Pts',(-17.4692376478452,2.40006318713692,135.097247730017));
#77523=CARTESIAN_POINT('Ctrl Pts',(-17.4767279836073,2.51511258623958,135.032926022911));
#77524=CARTESIAN_POINT('Ctrl Pts',(-17.4842183193693,2.62742739934127,134.964058338811));
#77525=CARTESIAN_POINT('Ctrl Pts',(-17.4917086551314,2.73664159207249,134.890921012206));
#77526=CARTESIAN_POINT('Ctrl Pts',(-17.4994829892505,2.84999667411525,134.815010661634));
#77527=CARTESIAN_POINT('Ctrl Pts',(-17.5072573233696,2.96037044922866,134.734260049131));
#77528=CARTESIAN_POINT('Ctrl Pts',(-17.5150316574887,3.06732182148153,134.64893080238));
#77529=CARTESIAN_POINT('Ctrl Pts',(-17.5227964104358,3.17414138572662,134.563706716301));
#77530=CARTESIAN_POINT('Ctrl Pts',(-17.5305611633829,3.2775466366057,134.473915464869));
#77531=CARTESIAN_POINT('Ctrl Pts',(-17.53832591633,3.37712435344672,134.379862563287));
#77532=CARTESIAN_POINT('Ctrl Pts',(-17.546082957215,3.47660316829543,134.285903076374));
#77533=CARTESIAN_POINT('Ctrl Pts',(-17.5538399981,3.57226173199629,134.187690629357));
#77534=CARTESIAN_POINT('Ctrl Pts',(-17.561597038985,3.66371919459305,134.085571480292));
#77535=CARTESIAN_POINT('Ctrl Pts',(-17.5693482302251,3.75510768840584,133.983529340072));
#77536=CARTESIAN_POINT('Ctrl Pts',(-17.5770994214652,3.84230112721457,133.877586651846));
#77537=CARTESIAN_POINT('Ctrl Pts',(-17.5848506127053,3.92495516388607,133.768126806722));
#77538=CARTESIAN_POINT('Ctrl Pts',(-17.5925985094824,4.0075740703871,133.658713484952));
#77539=CARTESIAN_POINT('Ctrl Pts',(-17.6003464062594,4.08565717701009,133.545786290848));
#77540=CARTESIAN_POINT('Ctrl Pts',(-17.6080943030365,4.15890027982851,133.429761829751));
#77541=CARTESIAN_POINT('Ctrl Pts',(-17.6158405791206,4.23212806176876,133.31376163847));
#77542=CARTESIAN_POINT('Ctrl Pts',(-17.6235868552048,4.30051764510405,133.194665799261));
#77543=CARTESIAN_POINT('Ctrl Pts',(-17.6313331312889,4.36380828064201,133.072919709214));
#77544=CARTESIAN_POINT('Ctrl Pts',(-17.6390794645542,4.42709938337706,132.951172720466));
#77545=CARTESIAN_POINT('Ctrl Pts',(-17.6468257978196,4.48529128287434,132.826775788734));
#77546=CARTESIAN_POINT('Ctrl Pts',(-17.6545721310849,4.53816949539015,132.700198346279));
#77547=CARTESIAN_POINT('Ctrl Pts',(-17.6623201990879,4.59105954961502,132.573592557683));
#77548=CARTESIAN_POINT('Ctrl Pts',(-17.6700682670909,4.6386333982926,132.444805647367));
#77549=CARTESIAN_POINT('Ctrl Pts',(-17.6778163350939,4.68072509979499,132.314326048511));
#77550=CARTESIAN_POINT('Ctrl Pts',(-17.6855726378357,4.72286153685864,132.183707774385));
#77551=CARTESIAN_POINT('Ctrl Pts',(-17.6933289405775,4.7595040674805,132.051393590682));
#77552=CARTESIAN_POINT('Ctrl Pts',(-17.7010852433194,4.79053680731456,131.917886620973));
#77553=CARTESIAN_POINT('Ctrl Pts',(-17.7088456858336,4.82158611025628,131.784308394575));
#77554=CARTESIAN_POINT('Ctrl Pts',(-17.7166061283477,4.84701958391824,131.649536497636));
#77555=CARTESIAN_POINT('Ctrl Pts',(-17.7243665708619,4.86677288369339,131.514082225696));
#77556=CARTESIAN_POINT('Ctrl Pts',(-17.7321394711274,4.88655789321896,131.378410510534));
#77557=CARTESIAN_POINT('Ctrl Pts',(-17.7399123713927,4.90064446735117,131.242054620514));
#77558=CARTESIAN_POINT('Ctrl Pts',(-17.7476852716582,4.90902028603632,131.105529828781));
#77559=CARTESIAN_POINT('Ctrl Pts',(-17.7551756074202,4.91709162261487,130.973968057112));
#77560=CARTESIAN_POINT('Ctrl Pts',(-17.7626659431823,4.91986018947052,130.842249758487));
#77561=CARTESIAN_POINT('Ctrl Pts',(-17.7701562789443,4.91736062411741,130.710832253528));
#77562=CARTESIAN_POINT('Ctrl Pts',(-17.7779306130634,4.91476628698421,130.574432013925));
#77563=CARTESIAN_POINT('Ctrl Pts',(-17.7857049471825,4.9064882311872,130.437923752473));
#77564=CARTESIAN_POINT('Ctrl Pts',(-17.7934792813016,4.89250814838155,130.301819991825));
#77565=CARTESIAN_POINT('Ctrl Pts',(-17.8012440342487,4.87854529477853,130.165883966898));
#77566=CARTESIAN_POINT('Ctrl Pts',(-17.8090087871958,4.85889443584218,130.030351836073));
#77567=CARTESIAN_POINT('Ctrl Pts',(-17.8167735401429,4.83358925429883,129.895736392032));
#77568=CARTESIAN_POINT('Ctrl Pts',(-17.8245305810279,4.80830920621857,129.761254649949));
#77569=CARTESIAN_POINT('Ctrl Pts',(-17.8322876219129,4.7773860832927,129.627688164531));
#77570=CARTESIAN_POINT('Ctrl Pts',(-17.8400446627979,4.74090534352596,129.49554451657));
#77571=CARTESIAN_POINT('Ctrl Pts',(-17.847795854038,4.70445211416886,129.363500519161));
#77572=CARTESIAN_POINT('Ctrl Pts',(-17.8555470452781,4.66244971360641,129.232877598865));
#77573=CARTESIAN_POINT('Ctrl Pts',(-17.8632982365182,4.61503457159742,129.104172696935));
#77574=CARTESIAN_POINT('Ctrl Pts',(-17.8710461332953,4.56763958228862,128.975522498021));
#77575=CARTESIAN_POINT('Ctrl Pts',(-17.8787940300724,4.51483656204039,128.848789062177));
#77576=CARTESIAN_POINT('Ctrl Pts',(-17.8865419268494,4.45681158307164,128.724453510145));
#77577=CARTESIAN_POINT('Ctrl Pts',(-17.8942882029335,4.39879874167762,128.600143966431));
#77578=CARTESIAN_POINT('Ctrl Pts',(-17.9020344790176,4.33556627948259,128.478231662907));
#77579=CARTESIAN_POINT('Ctrl Pts',(-17.9097807551017,4.26734798036601,128.359176723261));
#77580=CARTESIAN_POINT('Ctrl Pts',(-17.9175270883671,4.19912917767735,128.240120904779));
#77581=CARTESIAN_POINT('Ctrl Pts',(-17.9252734216325,4.12592465900117,128.123922831486));
#77582=CARTESIAN_POINT('Ctrl Pts',(-17.9330197548979,4.04801343729121,128.011016694235));
#77583=CARTESIAN_POINT('Ctrl Pts',(-17.9407678229009,3.97008476790346,127.898085272437));
#77584=CARTESIAN_POINT('Ctrl Pts',(-17.9485158909038,3.88744752008537,127.788447575362));
#77585=CARTESIAN_POINT('Ctrl Pts',(-17.9562639589068,3.80042293100301,127.682507224467));
#77586=CARTESIAN_POINT('Ctrl Pts',(-17.9640202616486,3.71330585115176,127.576454278905));
#77587=CARTESIAN_POINT('Ctrl Pts',(-17.9717765643904,3.62179236391466,127.474106831878));
#77588=CARTESIAN_POINT('Ctrl Pts',(-17.9795328671323,3.5262431230819,127.375834330746));
#77589=CARTESIAN_POINT('Ctrl Pts',(-17.9872933096464,3.43064288474225,127.277509378621));
#77590=CARTESIAN_POINT('Ctrl Pts',(-17.9950537521606,3.33100288467038,127.183263974634));
#77591=CARTESIAN_POINT('Ctrl Pts',(-18.0028141946748,3.22771851045276,127.093428621452));
#77592=CARTESIAN_POINT('Ctrl Pts',(-18.0105870949402,3.12426833498848,127.003449056587));
#77593=CARTESIAN_POINT('Ctrl Pts',(-18.0183599952057,3.01716240031762,126.917893933583));
#77594=CARTESIAN_POINT('Ctrl Pts',(-18.0261328954711,2.90682756103946,126.837052135373));
#77595=CARTESIAN_POINT('Ctrl Pts',(-18.0336232312332,2.80050367108575,126.759149140155));
#77596=CARTESIAN_POINT('Ctrl Pts',(-18.0411135669951,2.69118181400784,126.685622908645));
#77597=CARTESIAN_POINT('Ctrl Pts',(-18.0486039027572,2.57926546902013,126.616691492286));
#77598=CARTESIAN_POINT('Ctrl Pts',(-18.0563782368763,2.46310578179614,126.545146520326));
#77599=CARTESIAN_POINT('Ctrl Pts',(-18.0641525709953,2.34378302396081,126.4783250334));
#77600=CARTESIAN_POINT('Ctrl Pts',(-18.0719269051144,2.22171849923021,126.416519465852));
#77601=CARTESIAN_POINT('Ctrl Pts',(-18.0796916580615,2.09980440811712,126.354790068142));
#77602=CARTESIAN_POINT('Ctrl Pts',(-18.0874564110086,1.97515561873021,126.298064465038));
#77603=CARTESIAN_POINT('Ctrl Pts',(-18.0952211639557,1.84822176441418,126.246591495282));
#77604=CARTESIAN_POINT('Ctrl Pts',(-18.1029782048407,1.72141398259172,126.195169649205));
#77605=CARTESIAN_POINT('Ctrl Pts',(-18.1107352457257,1.59232601232948,126.148990200399));
#77606=CARTESIAN_POINT('Ctrl Pts',(-18.1184922866107,1.46143108786168,126.108255610442));
#77607=CARTESIAN_POINT('Ctrl Pts',(-18.1262434778508,1.33063487227445,126.067551738756));
#77608=CARTESIAN_POINT('Ctrl Pts',(-18.133994669091,1.1980347865262,126.032284668857));
#77609=CARTESIAN_POINT('Ctrl Pts',(-18.1417458603311,1.06412266498436,126.00260822741));
#77610=CARTESIAN_POINT('Ctrl Pts',(-18.1494937571082,0.93026745966658,125.972944399243));
#77611=CARTESIAN_POINT('Ctrl Pts',(-18.1572416538852,0.795101708584325,
125.948866557927));
#77612=CARTESIAN_POINT('Ctrl Pts',(-18.1649895506623,0.659130768822893,
125.930478213148));
#77613=CARTESIAN_POINT('Ctrl Pts',(-18.1727358267464,0.523188271250865,
125.912093714815));
#77614=CARTESIAN_POINT('Ctrl Pts',(-18.1804821028305,0.386441307205254,
125.899396398168));
#77615=CARTESIAN_POINT('Ctrl Pts',(-18.1882283789145,0.249403357673105,
125.8924382823));
#77616=CARTESIAN_POINT('Ctrl Pts',(-18.1959747121799,0.112364396557943,
125.885480115069));
#77617=CARTESIAN_POINT('Ctrl Pts',(-18.2037210454453,-0.024965163867713,
125.884261252981));
#77618=CARTESIAN_POINT('Ctrl Pts',(-18.2114673787106,-0.162069213226618,
125.888781645296));
#77619=CARTESIAN_POINT('Ctrl Pts',(-18.2192154467136,-0.299203966086765,
125.893303049921));
#77620=CARTESIAN_POINT('Ctrl Pts',(-18.2269635147165,-0.436112716709654,
125.9035662536));
#77621=CARTESIAN_POINT('Ctrl Pts',(-18.2347115827195,-0.572282250397577,
125.919519157664));
#77622=CARTESIAN_POINT('Ctrl Pts',(-18.2424678854613,-0.708596506686528,
125.935489016663));
#77623=CARTESIAN_POINT('Ctrl Pts',(-18.2502241882032,-0.84416958769425,
125.957160610179));
#77624=CARTESIAN_POINT('Ctrl Pts',(-18.2579804909451,-0.978495724708584,
125.984430205285));
#77625=CARTESIAN_POINT('Ctrl Pts',(-18.2657409334593,-1.11289355562672,
126.011714354996));
#77626=CARTESIAN_POINT('Ctrl Pts',(-18.2735013759734,-1.24604273705096,
126.044602366081));
#77627=CARTESIAN_POINT('Ctrl Pts',(-18.2812618184876,-1.37745149107752,
126.082940232531));
#77628=CARTESIAN_POINT('Ctrl Pts',(-18.289034718753,-1.50907119410196,126.121339642327));
#77629=CARTESIAN_POINT('Ctrl Pts',(-18.2968076190184,-1.63894451602914,
126.16520626478));
#77630=CARTESIAN_POINT('Ctrl Pts',(-18.3045805192839,-1.76659768613051,
126.214337123306));
#77631=CARTESIAN_POINT('Ctrl Pts',(-18.3120708550459,-1.88961034195994,
126.261681951372));
#77632=CARTESIAN_POINT('Ctrl Pts',(-18.3195611908079,-2.01056117698658,
126.313914801778));
#77633=CARTESIAN_POINT('Ctrl Pts',(-18.32705152657,-2.12904864798273,126.370814078166));
#77634=CARTESIAN_POINT('Ctrl Pts',(-18.3348265613507,-2.25203969102043,
126.42987603039));
#77635=CARTESIAN_POINT('Ctrl Pts',(-18.3426015961315,-2.3727660408316,126.494153263206));
#77636=CARTESIAN_POINT('Ctrl Pts',(-18.3503766309122,-2.49075381185636,
126.563449334454));
#77637=CARTESIAN_POINT('Ctrl Pts',(-18.3581419274936,-2.60859380367939,
126.632658612656));
#77638=CARTESIAN_POINT('Ctrl Pts',(-18.3659072240749,-2.72370170798766,
126.706874024767));
#77639=CARTESIAN_POINT('Ctrl Pts',(-18.3736725206563,-2.83562503968742,
126.785851727841));
#77640=CARTESIAN_POINT('Ctrl Pts',(-18.3814299488222,-2.94743496177422,
126.864749404431));
#77641=CARTESIAN_POINT('Ctrl Pts',(-18.3891873769882,-3.05606641597749,
126.948399544035));
#77642=CARTESIAN_POINT('Ctrl Pts',(-18.396944805154,-3.16109321225825,127.036513385271));
#77643=CARTESIAN_POINT('Ctrl Pts',(-18.4046957368811,-3.2660320541111,127.124553435791));
#77644=CARTESIAN_POINT('Ctrl Pts',(-18.4124466686081,-3.36737195112619,
127.217049493631));
#77645=CARTESIAN_POINT('Ctrl Pts',(-18.4201976003352,-3.46471768203348,
127.313670936958));
#77646=CARTESIAN_POINT('Ctrl Pts',(-18.4279450099172,-3.56201917751277,
127.410248473984));
#77647=CARTESIAN_POINT('Ctrl Pts',(-18.4356924194992,-3.65532984134678,
127.510947391778));
#77648=CARTESIAN_POINT('Ctrl Pts',(-18.4434398290812,-3.74428950334184,
127.615398532864));
#77649=CARTESIAN_POINT('Ctrl Pts',(-18.4511853958899,-3.83322800568385,
127.719824829546));
#77650=CARTESIAN_POINT('Ctrl Pts',(-18.4589309626985,-3.91781731295466,
127.828001275673));
#77651=CARTESIAN_POINT('Ctrl Pts',(-18.4666765295072,-3.99773620201954,
127.939524091416));
#77652=CARTESIAN_POINT('Ctrl Pts',(-18.4744219313113,-4.07765338856494,
128.051044531378));
#77653=CARTESIAN_POINT('Ctrl Pts',(-18.4821673331153,-4.15290012864465,
128.16591088051));
#77654=CARTESIAN_POINT('Ctrl Pts',(-18.4899127349194,-4.22319759362039,
128.283689050753));
#77655=CARTESIAN_POINT('Ctrl Pts',(-18.4976626067608,-4.29353562876832,
128.4015351933));
#77656=CARTESIAN_POINT('Ctrl Pts',(-18.5054124786022,-4.35891848282762,
128.52229617776));
#77657=CARTESIAN_POINT('Ctrl Pts',(-18.5131623504435,-4.41911242054446,
128.645511739787));
#77658=CARTESIAN_POINT('Ctrl Pts',(-18.5209147645197,-4.47932610402394,
128.768767720921));
#77659=CARTESIAN_POINT('Ctrl Pts',(-18.5286671785959,-4.53434731955563,
128.894479527453));
#77660=CARTESIAN_POINT('Ctrl Pts',(-18.5364195926722,-4.58399023429016,
129.022166297512));
#77661=CARTESIAN_POINT('Ctrl Pts',(-18.5441797389906,-4.63368266276793,
129.149980422098));
#77662=CARTESIAN_POINT('Ctrl Pts',(-18.551939885309,-4.67798594931462,129.279773075077));
#77663=CARTESIAN_POINT('Ctrl Pts',(-18.5597000316274,-4.71676384159292,
129.411047327189));
#77664=CARTESIAN_POINT('Ctrl Pts',(-18.5630626269009,-4.73356692132093,
129.467930556134));
#77665=CARTESIAN_POINT('Ctrl Pts',(-18.5664252221743,-4.74933318412891,
129.52509182207));
#77666=CARTESIAN_POINT('Ctrl Pts',(-18.5697878174477,-4.76405452823411,
129.582490119308));
#77667=CARTESIAN_POINT('Origin',(213.235140564004,0.,130.804360617566));
#77668=CARTESIAN_POINT('',(-20.6651747065899,-4.7640545282341,129.582490119308));
#77669=CARTESIAN_POINT('',(-20.320130187517,-4.76405452823408,129.582490119308));
#77670=CARTESIAN_POINT('',(213.235140564004,-4.76405452823405,129.582490119308));
#77671=CARTESIAN_POINT('',(-18.9851405639704,-4.91824968425682,130.802598287368));
#77672=CARTESIAN_POINT('Ctrl Pts',(-18.9851405640086,-4.91824968425706,
130.802598288046));
#77673=CARTESIAN_POINT('Ctrl Pts',(-18.9930656157456,-4.91830008698088,
130.943260506847));
#77674=CARTESIAN_POINT('Ctrl Pts',(-19.0009906674826,-4.91231171566778,
131.083879878867));
#77675=CARTESIAN_POINT('Ctrl Pts',(-19.0089157192196,-4.9003219196573,131.22391770096));
#77676=CARTESIAN_POINT('Ctrl Pts',(-19.0168450820189,-4.88832560144877,
131.364031700697));
#77677=CARTESIAN_POINT('Ctrl Pts',(-19.0247744448181,-4.87032138336905,
131.503563156307));
#77678=CARTESIAN_POINT('Ctrl Pts',(-19.0327038076174,-4.8463983542322,131.641979895398));
#77679=CARTESIAN_POINT('Ctrl Pts',(-19.0406388492404,-4.82245819198274,
131.780495765312));
#77680=CARTESIAN_POINT('Ctrl Pts',(-19.0485738908634,-4.79259083272611,
131.917894968326));
#77681=CARTESIAN_POINT('Ctrl Pts',(-19.0565089324864,-4.75693616462916,
132.053656974778));
#77682=CARTESIAN_POINT('Ctrl Pts',(-19.0644567932359,-4.72122389611616,
132.189638305893));
#77683=CARTESIAN_POINT('Ctrl Pts',(-19.0724046539854,-4.67970573199247,
132.323976802585));
#77684=CARTESIAN_POINT('Ctrl Pts',(-19.0803525147348,-4.63257133438727,
132.456167475014));
#77685=CARTESIAN_POINT('Ctrl Pts',(-19.0883073765969,-4.58539541702783,
132.58847459158));
#77686=CARTESIAN_POINT('Ctrl Pts',(-19.0962622384589,-4.53259353845703,
132.718629773762));
#77687=CARTESIAN_POINT('Ctrl Pts',(-19.104217100321,-4.47440275290421,132.84614980044));
#77688=CARTESIAN_POINT('Ctrl Pts',(-19.1121865675191,-4.41610512753542,
132.973903957249));
#77689=CARTESIAN_POINT('Ctrl Pts',(-19.1201560347171,-4.35239898874052,
133.099012965156));
#77690=CARTESIAN_POINT('Ctrl Pts',(-19.1281255019152,-4.28356696116366,
133.221018878828));
#77691=CARTESIAN_POINT('Ctrl Pts',(-19.1330188018932,-4.24130368927173,
133.295931231166));
#77692=CARTESIAN_POINT('Ctrl Pts',(-19.1379121018712,-4.19710879656985,
133.369674274505));
#77693=CARTESIAN_POINT('Ctrl Pts',(-19.1428054018492,-4.15105541867314,
133.442147942883));
#77694=CARTESIAN_POINT('Ctrl Pts',(-19.1505797359683,-4.07788713782147,
133.557292020569));
#77695=CARTESIAN_POINT('Ctrl Pts',(-19.1583540700874,-3.99980844576856,
133.669571802808));
#77696=CARTESIAN_POINT('Ctrl Pts',(-19.1661284042065,-3.91707030977014,
133.778540042351));
#77697=CARTESIAN_POINT('Ctrl Pts',(-19.1738931571535,-3.83443414112981,
133.887373988278));
#77698=CARTESIAN_POINT('Ctrl Pts',(-19.1816579101006,-3.74715018826146,
133.992904203453));
#77699=CARTESIAN_POINT('Ctrl Pts',(-19.1894226630477,-3.65551396223064,
134.094710254677));
#77700=CARTESIAN_POINT('Ctrl Pts',(-19.1971797039327,-3.56396875059148,
134.196415190696));
#77701=CARTESIAN_POINT('Ctrl Pts',(-19.2049367448177,-3.46808012810207,
134.294403035021));
#77702=CARTESIAN_POINT('Ctrl Pts',(-19.2126937857027,-3.36818511375556,
134.388284738132));
#77703=CARTESIAN_POINT('Ctrl Pts',(-19.2204449769428,-3.26836543101645,
134.482095644321));
#77704=CARTESIAN_POINT('Ctrl Pts',(-19.2281961681829,-3.16454565378088,
134.571806305975));
#77705=CARTESIAN_POINT('Ctrl Pts',(-19.235947359423,-3.05710079936569,134.657063274795));
#77706=CARTESIAN_POINT('Ctrl Pts',(-19.2436952562001,-2.94970161187965,
134.742284007129));
#77707=CARTESIAN_POINT('Ctrl Pts',(-19.2514431529772,-2.83868071727795,
134.823054569031));
#77708=CARTESIAN_POINT('Ctrl Pts',(-19.2591910497543,-2.72444730087353,
134.899060846797));
#77709=CARTESIAN_POINT('Ctrl Pts',(-19.2669373258384,-2.61023777963723,
134.975051225688));
#77710=CARTESIAN_POINT('Ctrl Pts',(-19.2746836019224,-2.49281739851653,
135.046279086271));
#77711=CARTESIAN_POINT('Ctrl Pts',(-19.2824298780065,-2.37262516907755,
135.11247306614));
#77712=CARTESIAN_POINT('Ctrl Pts',(-19.2901762112718,-2.25243205240716,
135.178667534638));
#77713=CARTESIAN_POINT('Ctrl Pts',(-19.2979225445372,-2.12946738905345,
135.239827859667));
#77714=CARTESIAN_POINT('Ctrl Pts',(-19.3056688778025,-2.00419532907419,
135.295728354171));
#77715=CARTESIAN_POINT('Ctrl Pts',(-19.3134169458055,-1.87889521528567,
135.351641367203));
#77716=CARTESIAN_POINT('Ctrl Pts',(-19.3211650138084,-1.75128703361055,
135.402292046531));
#77717=CARTESIAN_POINT('Ctrl Pts',(-19.3289130818113,-1.62185509443274,
135.447502777264));
#77718=CARTESIAN_POINT('Ctrl Pts',(-19.3366693845532,-1.49228559344954,
135.4927615585));
#77719=CARTESIAN_POINT('Ctrl Pts',(-19.3444256872951,-1.36088883266296,
135.532568712557));
#77720=CARTESIAN_POINT('Ctrl Pts',(-19.3521819900369,-1.22816500985251,
135.566796314882));
#77721=CARTESIAN_POINT('Ctrl Pts',(-19.3599424325511,-1.09537034834123,
135.60104218551));
#77722=CARTESIAN_POINT('Ctrl Pts',(-19.3677028750652,-0.961247595618872,
135.62970248888));
#77723=CARTESIAN_POINT('Ctrl Pts',(-19.3754633175794,-0.826306355891596,
135.652700629231));
#77724=CARTESIAN_POINT('Ctrl Pts',(-19.3832362178448,-0.69114849650679,
135.675735688239));
#77725=CARTESIAN_POINT('Ctrl Pts',(-19.3910091181103,-0.555169912552802,
135.693090371172));
#77726=CARTESIAN_POINT('Ctrl Pts',(-19.3987820183757,-0.418885433140261,
135.70473999639));
#77727=CARTESIAN_POINT('Ctrl Pts',(-19.4062723541379,-0.287555237832218,
135.715966128388));
#77728=CARTESIAN_POINT('Ctrl Pts',(-19.4137626899,-0.155941308791479,135.721894773945));
#77729=CARTESIAN_POINT('Ctrl Pts',(-19.4212530256621,-0.0245016661486505,
135.722549586166));
#77730=CARTESIAN_POINT('Ctrl Pts',(-19.4290273597812,0.111921550492895,
135.723229225791));
#77731=CARTESIAN_POINT('Ctrl Pts',(-19.4368016939003,0.248589151452131,
135.71822937575));
#77732=CARTESIAN_POINT('Ctrl Pts',(-19.4445760280194,0.384989201019398,
135.707519433839));
#77733=CARTESIAN_POINT('Ctrl Pts',(-19.4523407809665,0.521221149716367,
135.696822690975));
#77734=CARTESIAN_POINT('Ctrl Pts',(-19.4601055339136,0.657185817068261,
135.680429888437));
#77735=CARTESIAN_POINT('Ctrl Pts',(-19.4678702868607,0.792369749769786,
135.658362393642));
#77736=CARTESIAN_POINT('Ctrl Pts',(-19.4756273277457,0.927419415883409,
135.636316816594));
#77737=CARTESIAN_POINT('Ctrl Pts',(-19.4833843686307,1.06168950713955,135.608607826131));
#77738=CARTESIAN_POINT('Ctrl Pts',(-19.4911414095157,1.19467053816105,135.575308675107));
#77739=CARTESIAN_POINT('Ctrl Pts',(-19.4988926007558,1.32755128715226,135.542034635231));
#77740=CARTESIAN_POINT('Ctrl Pts',(-19.5066437919959,1.45914453307452,135.503178920243));
#77741=CARTESIAN_POINT('Ctrl Pts',(-19.514394983236,1.58895020384354,135.458865995391));
#77742=CARTESIAN_POINT('Ctrl Pts',(-19.5221428800131,1.71870070373998,135.414571904715));
#77743=CARTESIAN_POINT('Ctrl Pts',(-19.5298907767902,1.84666477037726,135.36482534345));
#77744=CARTESIAN_POINT('Ctrl Pts',(-19.5376386735672,1.97235695634455,135.309800784659));
#77745=CARTESIAN_POINT('Ctrl Pts',(-19.5453849496513,2.09802285021613,135.254787735821));
#77746=CARTESIAN_POINT('Ctrl Pts',(-19.5531312257355,2.22141745075026,135.194499042148));
#77747=CARTESIAN_POINT('Ctrl Pts',(-19.5608775018196,2.34207515659514,135.129157378497));
#77748=CARTESIAN_POINT('Ctrl Pts',(-19.5686238350849,2.4627337531078,135.063815232509));
#77749=CARTESIAN_POINT('Ctrl Pts',(-19.5763701683503,2.58065507082735,134.993420228291));
#77750=CARTESIAN_POINT('Ctrl Pts',(-19.5841165016156,2.69539834839675,134.918240879066));
#77751=CARTESIAN_POINT('Ctrl Pts',(-19.5918645696186,2.81016732192758,134.843044693947));
#77752=CARTESIAN_POINT('Ctrl Pts',(-19.5996126376216,2.92175651214648,134.76306224604));
#77753=CARTESIAN_POINT('Ctrl Pts',(-19.6073607056246,3.02975470502338,134.678604994201));
#77754=CARTESIAN_POINT('Ctrl Pts',(-19.6151170083664,3.13786767966501,134.59405798019));
#77755=CARTESIAN_POINT('Ctrl Pts',(-19.6228733111082,3.24238172452007,134.505026903102));
#77756=CARTESIAN_POINT('Ctrl Pts',(-19.6306296138501,3.34291884392157,134.41186344715));
#77757=CARTESIAN_POINT('Ctrl Pts',(-19.6383900563643,3.44350962301081,134.318650267056));
#77758=CARTESIAN_POINT('Ctrl Pts',(-19.6461504988784,3.54011897191441,134.221300590675));
#77759=CARTESIAN_POINT('Ctrl Pts',(-19.6539109413926,3.63240699492851,134.120201760579));
#77760=CARTESIAN_POINT('Ctrl Pts',(-19.661683841658,3.7248431668701,134.018940637665));
#77761=CARTESIAN_POINT('Ctrl Pts',(-19.6694567419235,3.81294389922043,133.913918633908));
#77762=CARTESIAN_POINT('Ctrl Pts',(-19.677229642189,3.89641014890662,133.805555548589));
#77763=CARTESIAN_POINT('Ctrl Pts',(-19.684719977951,3.97684219017792,133.701131734372));
#77764=CARTESIAN_POINT('Ctrl Pts',(-19.692210313713,4.05297067108701,133.59360578611));
#77765=CARTESIAN_POINT('Ctrl Pts',(-19.699700649475,4.12456792059302,133.483375834192));
#77766=CARTESIAN_POINT('Ctrl Pts',(-19.7074749835941,4.19887980157557,133.368966480144));
#77767=CARTESIAN_POINT('Ctrl Pts',(-19.7152493177132,4.26854546274312,133.251281615754));
#77768=CARTESIAN_POINT('Ctrl Pts',(-19.7230236518323,4.33326244383982,133.130735405795));
#77769=CARTESIAN_POINT('Ctrl Pts',(-19.7307884047794,4.39789966704124,133.010337758266));
#77770=CARTESIAN_POINT('Ctrl Pts',(-19.7385531577264,4.45760016182317,132.887086122716));
#77771=CARTESIAN_POINT('Ctrl Pts',(-19.7463179106735,4.51210437114458,132.761424031561));
#77772=CARTESIAN_POINT('Ctrl Pts',(-19.7540749515585,4.56655444611685,132.635886749767));
#77773=CARTESIAN_POINT('Ctrl Pts',(-19.7618319924436,4.61581835173356,132.507944133091));
#77774=CARTESIAN_POINT('Ctrl Pts',(-19.7695890333286,4.65968232840544,132.378064420969));
#77775=CARTESIAN_POINT('Ctrl Pts',(-19.7773402245688,4.70351322691155,132.248282652148));
#77776=CARTESIAN_POINT('Ctrl Pts',(-19.7850914158088,4.74195217720557,132.116567064383));
#77777=CARTESIAN_POINT('Ctrl Pts',(-19.792842607049,4.77483359425135,131.983405658991));
#77778=CARTESIAN_POINT('Ctrl Pts',(-19.8005905038261,4.80770103581756,131.850300850749));
#77779=CARTESIAN_POINT('Ctrl Pts',(-19.8083384006033,4.83501554864285,131.715751825865));
#77780=CARTESIAN_POINT('Ctrl Pts',(-19.8160862973803,4.8566615256736,131.580261311948));
#77781=CARTESIAN_POINT('Ctrl Pts',(-19.8238325734644,4.87830297483263,131.444799139724));
#77782=CARTESIAN_POINT('Ctrl Pts',(-19.8315788495485,4.89427818505058,131.308396256015));
#77783=CARTESIAN_POINT('Ctrl Pts',(-19.8393251256326,4.90452283008644,131.171564745621));
#77784=CARTESIAN_POINT('Ctrl Pts',(-19.8470714588979,4.91476755074593,131.034732225169));
#77785=CARTESIAN_POINT('Ctrl Pts',(-19.8548177921633,4.91928159262324,130.897471461593));
#77786=CARTESIAN_POINT('Ctrl Pts',(-19.8625641254286,4.91805262121678,130.760298417862));
#77787=CARTESIAN_POINT('Ctrl Pts',(-19.8703121934316,4.91682337459069,130.623094655178));
#77788=CARTESIAN_POINT('Ctrl Pts',(-19.8780602614345,4.90984855897678,130.485979042304));
#77789=CARTESIAN_POINT('Ctrl Pts',(-19.8858083294375,4.89716794230353,130.349465896367));
#77790=CARTESIAN_POINT('Ctrl Pts',(-19.8935646321793,4.88447384851994,130.212807662634));
#77791=CARTESIAN_POINT('Ctrl Pts',(-19.9013209349212,4.86606187601619,130.076753564835));
#77792=CARTESIAN_POINT('Ctrl Pts',(-19.909077237663,4.84202359078967,129.941811715337));
#77793=CARTESIAN_POINT('Ctrl Pts',(-19.9168376801772,4.81797247560658,129.806797843312));
#77794=CARTESIAN_POINT('Ctrl Pts',(-19.9245981226914,4.78828914867807,129.672897783978));
#77795=CARTESIAN_POINT('Ctrl Pts',(-19.9323585652055,4.75311577034962,129.540606869341));
#77796=CARTESIAN_POINT('Ctrl Pts',(-19.940131465471,4.71788592859169,129.408103589582));
#77797=CARTESIAN_POINT('Ctrl Pts',(-19.9479043657364,4.67714854026842,129.277214989978));
#77798=CARTESIAN_POINT('Ctrl Pts',(-19.9556772660019,4.63109515431962,129.1484195757));
#77799=CARTESIAN_POINT('Ctrl Pts',(-19.9631676017639,4.58671592495166,129.024306199147));
#77800=CARTESIAN_POINT('Ctrl Pts',(-19.9706579375259,4.53740060285889,128.902136750585));
#77801=CARTESIAN_POINT('Ctrl Pts',(-19.9781482732879,4.48336108465437,128.782317975309));
#77802=CARTESIAN_POINT('Ctrl Pts',(-19.985922607407,4.42727264169201,128.657956234749));
#77803=CARTESIAN_POINT('Ctrl Pts',(-19.9936969415261,4.36591702381149,128.53573299716));
#77804=CARTESIAN_POINT('Ctrl Pts',(-20.0014712756452,4.29947919240989,128.416126597095));
#77805=CARTESIAN_POINT('Ctrl Pts',(-20.0092360285923,4.23312323969769,128.296667601229));
#77806=CARTESIAN_POINT('Ctrl Pts',(-20.0170007815394,4.16169772373649,128.179819364559));
#77807=CARTESIAN_POINT('Ctrl Pts',(-20.0247655344865,4.08543550399017,128.066039999881));
#77808=CARTESIAN_POINT('Ctrl Pts',(-20.0325225753715,4.00924902895561,127.952373642472));
#77809=CARTESIAN_POINT('Ctrl Pts',(-20.0402796162564,3.92823562634669,127.841770413965));
#77810=CARTESIAN_POINT('Ctrl Pts',(-20.0480366571414,3.84267369698184,127.734663251208));
#77811=CARTESIAN_POINT('Ctrl Pts',(-20.0557878483816,3.75717629053361,127.627636858796));
#77812=CARTESIAN_POINT('Ctrl Pts',(-20.0635390396218,3.66713742772582,127.524101588748));
#77813=CARTESIAN_POINT('Ctrl Pts',(-20.0712902308619,3.57287817512937,127.424460529075));
#77814=CARTESIAN_POINT('Ctrl Pts',(-20.079038127639,3.47865898522973,127.32486181951));
#77815=CARTESIAN_POINT('Ctrl Pts',(-20.0867860244161,3.38022324134464,127.229154311791));
#77816=CARTESIAN_POINT('Ctrl Pts',(-20.0945339211932,3.2779314140123,127.137707005956));
#77817=CARTESIAN_POINT('Ctrl Pts',(-20.1022801972773,3.17566098392507,127.046278828927));
#77818=CARTESIAN_POINT('Ctrl Pts',(-20.1100264733614,3.06953636606886,126.959109341658));
#77819=CARTESIAN_POINT('Ctrl Pts',(-20.1177727494455,2.9599536219864,126.876529457983));
#77820=CARTESIAN_POINT('Ctrl Pts',(-20.1255190827108,2.85037006898916,126.793948964722));
#77821=CARTESIAN_POINT('Ctrl Pts',(-20.1332654159762,2.73732865106229,126.715958377953));
#77822=CARTESIAN_POINT('Ctrl Pts',(-20.1410117492415,2.621256795364,126.642846965629));
#77823=CARTESIAN_POINT('Ctrl Pts',(-20.1487598172445,2.50515894617906,126.569719180511));
#77824=CARTESIAN_POINT('Ctrl Pts',(-20.1565078852474,2.38602963954354,126.501472952431));
#77825=CARTESIAN_POINT('Ctrl Pts',(-20.1642559532503,2.26432308056103,126.438352824474));
#77826=CARTESIAN_POINT('Ctrl Pts',(-20.1720122559922,2.14248717039847,126.375165611694));
#77827=CARTESIAN_POINT('Ctrl Pts',(-20.179768558734,2.01806888379208,126.317115562449));
#77828=CARTESIAN_POINT('Ctrl Pts',(-20.1875248614759,1.89154520372528,126.264400286818));
#77829=CARTESIAN_POINT('Ctrl Pts',(-20.19528530399,1.76495399416105,126.211656875458));
#77830=CARTESIAN_POINT('Ctrl Pts',(-20.2030457465042,1.63625551873682,126.164254046318));
#77831=CARTESIAN_POINT('Ctrl Pts',(-20.2108061890183,1.50594335543481,126.12233993492));
#77832=CARTESIAN_POINT('Ctrl Pts',(-20.2185790892837,1.37542200347953,126.08035853927));
#77833=CARTESIAN_POINT('Ctrl Pts',(-20.2263519895492,1.24328216421977,126.043883572591));
#77834=CARTESIAN_POINT('Ctrl Pts',(-20.2341248898146,1.11002995449002,126.01301252307));
#77835=CARTESIAN_POINT('Ctrl Pts',(-20.2416152255767,0.981621798226189,
125.983263713957));
#77836=CARTESIAN_POINT('Ctrl Pts',(-20.2491055613387,0.852181044947484,
125.958718520014));
#77837=CARTESIAN_POINT('Ctrl Pts',(-20.2565958971007,0.72216443628521,125.939418522385));
#77838=CARTESIAN_POINT('Ctrl Pts',(-20.2643702312198,0.587218208387621,
125.91938675948));
#77839=CARTESIAN_POINT('Ctrl Pts',(-20.2721445653389,0.451224126902702,
125.904942333098));
#77840=CARTESIAN_POINT('Ctrl Pts',(-20.279918899458,0.314684604392407,125.89618818149));
#77841=CARTESIAN_POINT('Ctrl Pts',(-20.2876836524051,0.178313354640533,
125.887444818591));
#77842=CARTESIAN_POINT('Ctrl Pts',(-20.2954484053522,0.0413983877740623,
125.884377801948));
#77843=CARTESIAN_POINT('Ctrl Pts',(-20.3032131582993,-0.0955490067097157,
125.887038841455));
#77844=CARTESIAN_POINT('Ctrl Pts',(-20.3109701991843,-0.232360383110673,
125.88969723798));
#77845=CARTESIAN_POINT('Ctrl Pts',(-20.3187272400693,-0.369203734672447,
125.898072361371));
#77846=CARTESIAN_POINT('Ctrl Pts',(-20.3264842809544,-0.50556433692043,
125.912163998078));
#77847=CARTESIAN_POINT('Ctrl Pts',(-20.3342354721944,-0.641822108576228,
125.926245008171));
#77848=CARTESIAN_POINT('Ctrl Pts',(-20.3419866634345,-0.777597468207187,
125.946033911033));
#77849=CARTESIAN_POINT('Ctrl Pts',(-20.3497378546746,-0.912377742128987,
125.971478463182));
#77850=CARTESIAN_POINT('Ctrl Pts',(-20.3574857514517,-1.04710073084009,
125.996912200717));
#77851=CARTESIAN_POINT('Ctrl Pts',(-20.3652336482288,-1.18082909165864,
126.027996734184));
#77852=CARTESIAN_POINT('Ctrl Pts',(-20.3729815450058,-1.31305753126929,
126.064628243046));
#77853=CARTESIAN_POINT('Ctrl Pts',(-20.3807278210899,-1.44525831154071,
126.101252089385));
#77854=CARTESIAN_POINT('Ctrl Pts',(-20.388474097174,-1.57595941813688,126.143420498891));
#77855=CARTESIAN_POINT('Ctrl Pts',(-20.396220373258,-1.70466836294043,126.19097912078));
#77856=CARTESIAN_POINT('Ctrl Pts',(-20.4039667065234,-1.83337825784399,
126.238538093735));
#77857=CARTESIAN_POINT('Ctrl Pts',(-20.4117130397887,-1.96009559488043,
126.291487222962));
#77858=CARTESIAN_POINT('Ctrl Pts',(-20.4194593730541,-2.08434596990911,
126.349623258279));
#77859=CARTESIAN_POINT('Ctrl Pts',(-20.427207441057,-2.20862416994745,126.407772312759));
#77860=CARTESIAN_POINT('Ctrl Pts',(-20.43495550906,-2.33043395459699,126.471110419064));
#77861=CARTESIAN_POINT('Ctrl Pts',(-20.4427035770629,-2.44932407388013,
126.53938762309));
#77862=CARTESIAN_POINT('Ctrl Pts',(-20.4504598798048,-2.56834055099749,
126.607737392941));
#77863=CARTESIAN_POINT('Ctrl Pts',(-20.4582161825467,-2.6844308244866,126.681036551603));
#77864=CARTESIAN_POINT('Ctrl Pts',(-20.4659724852885,-2.79717081843783,
126.758990612859));
#77865=CARTESIAN_POINT('Ctrl Pts',(-20.4737329278027,-2.90997098511852,
126.836986280545));
#77866=CARTESIAN_POINT('Ctrl Pts',(-20.4814933703169,-3.01941699739412,
126.919641565822));
#77867=CARTESIAN_POINT('Ctrl Pts',(-20.4892538128311,-3.12511743369867,
127.006621278421));
#77868=CARTESIAN_POINT('Ctrl Pts',(-20.4970267130965,-3.23098754972722,
127.093740618576));
#77869=CARTESIAN_POINT('Ctrl Pts',(-20.5047996133619,-3.33309978303407,
127.185197997299));
#77870=CARTESIAN_POINT('Ctrl Pts',(-20.5125725136274,-3.43109854553576,
127.28062029891));
#77871=CARTESIAN_POINT('Ctrl Pts',(-20.5200628493895,-3.52553480617799,
127.372573759504));
#77872=CARTESIAN_POINT('Ctrl Pts',(-20.5275531851516,-3.61615126191351,
127.468208654316));
#77873=CARTESIAN_POINT('Ctrl Pts',(-20.5350435209138,-3.70266604933885,
127.5671631893));
#77874=CARTESIAN_POINT('Ctrl Pts',(-20.5427532107793,-3.79171441793137,
127.669015602828));
#77875=CARTESIAN_POINT('Ctrl Pts',(-20.5504629006448,-3.87671110562716,
127.774721472327));
#77876=CARTESIAN_POINT('Ctrl Pts',(-20.5581725905103,-3.95729975157023,
127.883921996618));
#77877=CARTESIAN_POINT('Ctrl Pts',(-20.5658729677856,-4.03779105390427,
127.992990616806));
#77878=CARTESIAN_POINT('Ctrl Pts',(-20.573573345061,-4.11388466924951,128.105545180213));
#77879=CARTESIAN_POINT('Ctrl Pts',(-20.5812737223363,-4.18526216519003,
128.221191310082));
#77880=CARTESIAN_POINT('Ctrl Pts',(-20.5889651432378,-4.25655664136295,
128.336702930961));
#77881=CARTESIAN_POINT('Ctrl Pts',(-20.5966565641393,-4.32314571066714,
128.45529862336));
#77882=CARTESIAN_POINT('Ctrl Pts',(-20.6043479850409,-4.38475267177753,
128.576552935148));
#77883=CARTESIAN_POINT('Ctrl Pts',(-20.6120342090159,-4.44631800639856,
128.697725318024));
#77884=CARTESIAN_POINT('Ctrl Pts',(-20.6197204329908,-4.50290774779655,
128.821552394619));
#77885=CARTESIAN_POINT('Ctrl Pts',(-20.6274066569658,-4.55428985373553,
128.947581957989));
#77886=CARTESIAN_POINT('Ctrl Pts',(-20.6350895374991,-4.60564960889726,
129.073556699575));
#77887=CARTESIAN_POINT('Ctrl Pts',(-20.6427724180323,-4.651806083931,129.201731654703));
#77888=CARTESIAN_POINT('Ctrl Pts',(-20.6504552985656,-4.69257454021657,
129.331632792402));
#77889=CARTESIAN_POINT('Ctrl Pts',(-20.655361767907,-4.71861024127915,129.414590733344));
#77890=CARTESIAN_POINT('Ctrl Pts',(-20.6602682372484,-4.74244944925163,
129.498252244259));
#77891=CARTESIAN_POINT('Ctrl Pts',(-20.6651747065899,-4.7640545282341,129.582490119308));
#77892=CARTESIAN_POINT('Ctrl Pts',(-18.9154222424341,-4.76405452823411,
129.582490119308));
#77893=CARTESIAN_POINT('Ctrl Pts',(-18.9238373913451,-4.80090419183842,
129.72616639843));
#77894=CARTESIAN_POINT('Ctrl Pts',(-18.9322525402561,-4.83129321364356,
129.871678730157));
#77895=CARTESIAN_POINT('Ctrl Pts',(-18.9406676891671,-4.85505190900469,
130.018450938678));
#77896=CARTESIAN_POINT('Ctrl Pts',(-18.9490535319284,-4.87872786359806,
130.164712006119));
#77897=CARTESIAN_POINT('Ctrl Pts',(-18.9574393746897,-4.89581948998125,
130.31222392731));
#77898=CARTESIAN_POINT('Ctrl Pts',(-18.965825217451,-4.90620768672381,130.460399577284));
#77899=CARTESIAN_POINT('Ctrl Pts',(-18.9722636662908,-4.91418349490053,
130.57416528561));
#77900=CARTESIAN_POINT('Ctrl Pts',(-18.9787021151306,-4.91820873619813,
130.68832187259));
#77901=CARTESIAN_POINT('Ctrl Pts',(-18.9851405639703,-4.91824968425682,
130.802598287368));
#77902=CARTESIAN_POINT('',(-18.6398594360279,-4.91824887451795,130.801033335958));
#77903=CARTESIAN_POINT('Ctrl Pts',(-18.5697878174477,-4.76405452823411,
129.582490119308));
#77904=CARTESIAN_POINT('Ctrl Pts',(-18.5775620177684,-4.798089750661,129.715192934994));
#77905=CARTESIAN_POINT('Ctrl Pts',(-18.5853362180891,-4.82653616263435,
129.849162946845));
#77906=CARTESIAN_POINT('Ctrl Pts',(-18.5931104184099,-4.84933091075927,
129.983889545282));
#77907=CARTESIAN_POINT('Ctrl Pts',(-18.5972399957342,-4.86143925259346,
130.05545496461));
#77908=CARTESIAN_POINT('Ctrl Pts',(-18.6013695730585,-4.87195378562811,
130.12723379226));
#77909=CARTESIAN_POINT('Ctrl Pts',(-18.6054991503828,-4.88087106729867,
130.199149342963));
#77910=CARTESIAN_POINT('Ctrl Pts',(-18.6169525789189,-4.90560324696964,
130.398607920906));
#77911=CARTESIAN_POINT('Ctrl Pts',(-18.6284060074551,-4.9181126100524,130.599612926342));
#77912=CARTESIAN_POINT('Ctrl Pts',(-18.6398594359912,-4.91824887451751,
130.801033335313));
#77913=CARTESIAN_POINT('Ctrl Pts',(-18.6398594360279,-4.91824887451795,
130.801033335958));
#77914=CARTESIAN_POINT('Ctrl Pts',(-18.6475192066,-4.91834000481437,130.935738338606));
#77915=CARTESIAN_POINT('Ctrl Pts',(-18.6551789771722,-4.91289285644884,
131.070661083684));
#77916=CARTESIAN_POINT('Ctrl Pts',(-18.6628387477443,-4.90188026565471,
131.205300667555));
#77917=CARTESIAN_POINT('Ctrl Pts',(-18.6704903422589,-4.89087942972647,
131.33979653681));
#77918=CARTESIAN_POINT('Ctrl Pts',(-18.6781419367735,-4.87432499867613,
131.474009447759));
#77919=CARTESIAN_POINT('Ctrl Pts',(-18.685793531288,-4.85224182597472,131.607437403908));
#77920=CARTESIAN_POINT('Ctrl Pts',(-18.6934389095863,-4.83017659381875,
131.740756962122));
#77921=CARTESIAN_POINT('Ctrl Pts',(-18.7010842878844,-4.80259162042394,
131.873292438638));
#77922=CARTESIAN_POINT('Ctrl Pts',(-18.7087296661827,-4.76956362517859,
132.0045463898));
#77923=CARTESIAN_POINT('Ctrl Pts',(-18.7163713466381,-4.73655160459547,
132.135736857317));
#77924=CARTESIAN_POINT('Ctrl Pts',(-18.7240130270935,-4.69810189448041,
132.265646642174));
#77925=CARTESIAN_POINT('Ctrl Pts',(-18.7316547075489,-4.65434233516547,
132.393788341493));
#77926=CARTESIAN_POINT('Ctrl Pts',(-18.7392946056689,-4.6105929822718,132.521900153212));
#77927=CARTESIAN_POINT('Ctrl Pts',(-18.7469345037889,-4.56153637234276,
132.648244318281));
#77928=CARTESIAN_POINT('Ctrl Pts',(-18.7545744019089,-4.50735010023958,
132.772348965187));
#77929=CARTESIAN_POINT('Ctrl Pts',(-18.762214280099,-4.45316396949025,132.896453288345));
#77930=CARTESIAN_POINT('Ctrl Pts',(-18.7698541582891,-4.39384836455577,
133.018317735854));
#77931=CARTESIAN_POINT('Ctrl Pts',(-18.7774940364792,-4.32962865359607,
133.137491300674));
#77932=CARTESIAN_POINT('Ctrl Pts',(-18.7851356569152,-4.2653942975696,133.256692042583));
#77933=CARTESIAN_POINT('Ctrl Pts',(-18.7927772773512,-4.19625380309849,
133.373200327278));
#77934=CARTESIAN_POINT('Ctrl Pts',(-18.8004188977871,-4.12247774498443,
133.486591089507));
#77935=CARTESIAN_POINT('Ctrl Pts',(-18.8080684299223,-4.04862530333567,
133.600099250082));
#77936=CARTESIAN_POINT('Ctrl Pts',(-18.8157179620574,-3.97012793564836,
133.710483105901));
#77937=CARTESIAN_POINT('Ctrl Pts',(-18.8233674941926,-3.88729885673946,
133.817347617354));
#77938=CARTESIAN_POINT('Ctrl Pts',(-18.8310213335106,-3.80442313968473,
133.924272300461));
#77939=CARTESIAN_POINT('Ctrl Pts',(-18.8386751728287,-3.71721111504135,
134.02767338695));
#77940=CARTESIAN_POINT('Ctrl Pts',(-18.8463290121468,-3.62601440507188,
134.127191127344));
#77941=CARTESIAN_POINT('Ctrl Pts',(-18.8539942937547,-3.53468135840313,
134.22685764416));
#77942=CARTESIAN_POINT('Ctrl Pts',(-18.8616595753627,-3.43935201575192,
134.322628938515));
#77943=CARTESIAN_POINT('Ctrl Pts',(-18.8693248569706,-3.34041309220821,
134.414183803804));
#77944=CARTESIAN_POINT('Ctrl Pts',(-18.8741988293789,-3.27750273768657,
134.472399001901));
#77945=CARTESIAN_POINT('Ctrl Pts',(-18.8790728017874,-3.21313366910852,
134.528910295268));
#77946=CARTESIAN_POINT('Ctrl Pts',(-18.8839467741957,-3.14741141957671,
134.583644202906));
#77947=CARTESIAN_POINT('Ctrl Pts',(-18.8917211083148,-3.04257973730417,
134.670948695005));
#77948=CARTESIAN_POINT('Ctrl Pts',(-18.8994954424339,-2.93394671190642,
134.754026354128));
#77949=CARTESIAN_POINT('Ctrl Pts',(-18.9072697765529,-2.82188788607974,
134.832527920558));
#77950=CARTESIAN_POINT('Ctrl Pts',(-18.9150345295,-2.70996716274091,134.910932740824));
#77951=CARTESIAN_POINT('Ctrl Pts',(-18.9227992824472,-2.59462935661664,
134.984772467404));
#77952=CARTESIAN_POINT('Ctrl Pts',(-18.9305640353943,-2.47628423973866,
135.05373697493));
#77953=CARTESIAN_POINT('Ctrl Pts',(-18.9383210762792,-2.3580566648993,135.122632985934));
#77954=CARTESIAN_POINT('Ctrl Pts',(-18.9460781171642,-2.23682805898759,
135.186663218379));
#77955=CARTESIAN_POINT('Ctrl Pts',(-18.9538351580491,-2.11303813719905,
135.245560105682));
#77956=CARTESIAN_POINT('Ctrl Pts',(-18.9615863492893,-1.98934156635347,
135.304412578384));
#77957=CARTESIAN_POINT('Ctrl Pts',(-18.9693375405294,-1.86308787579569,
135.358139243832));
#77958=CARTESIAN_POINT('Ctrl Pts',(-18.9770887317695,-1.7347420941176,135.406518038754));
#77959=CARTESIAN_POINT('Ctrl Pts',(-18.9848366285466,-1.60645086282029,
135.454876271398));
#77960=CARTESIAN_POINT('Ctrl Pts',(-18.9925845253236,-1.47606967401502,
135.497891016704));
#77961=CARTESIAN_POINT('Ctrl Pts',(-19.0003324221007,-1.34408408234849,
135.535388100268));
#77962=CARTESIAN_POINT('Ctrl Pts',(-19.0080786981848,-1.21212609922246,
135.572877340249));
#77963=CARTESIAN_POINT('Ctrl Pts',(-19.015824974269,-1.07856475661898,135.604851107429));
#77964=CARTESIAN_POINT('Ctrl Pts',(-19.0235712503531,-0.943900957597308,
135.631185044117));
#77965=CARTESIAN_POINT('Ctrl Pts',(-19.0313175836184,-0.80923616451788,
135.657519175195));
#77966=CARTESIAN_POINT('Ctrl Pts',(-19.0390639168837,-0.673469282478845,
135.678213317675));
#77967=CARTESIAN_POINT('Ctrl Pts',(-19.0468102501491,-0.537111206239121,
135.69319428365));
#77968=CARTESIAN_POINT('Ctrl Pts',(-19.054558318152,-0.400722593554221,
135.708178604508));
#77969=CARTESIAN_POINT('Ctrl Pts',(-19.062306386155,-0.263742911772665,
135.717447160264));
#77970=CARTESIAN_POINT('Ctrl Pts',(-19.0700544541579,-0.126687575086714,
135.720978695149));
#77971=CARTESIAN_POINT('Ctrl Pts',(-19.0778107568998,0.0105134256424208,
135.724513983392));
#77972=CARTESIAN_POINT('Ctrl Pts',(-19.0855670596416,0.147789850438779,
135.722300060515));
#77973=CARTESIAN_POINT('Ctrl Pts',(-19.0933233623835,0.284626328637788,
135.714367839103));
#77974=CARTESIAN_POINT('Ctrl Pts',(-19.1010838048977,0.421535840585279,
135.706431384026));
#77975=CARTESIAN_POINT('Ctrl Pts',(-19.1088442474118,0.558004549220509,
135.692770587913));
#77976=CARTESIAN_POINT('Ctrl Pts',(-19.116604689926,0.693523799154114,135.673468113043));
#77977=CARTESIAN_POINT('Ctrl Pts',(-19.1243775901914,0.829260596618731,
135.654134652126));
#77978=CARTESIAN_POINT('Ctrl Pts',(-19.1321504904569,0.964044505000242,
135.629141485955));
#77979=CARTESIAN_POINT('Ctrl Pts',(-19.1399233907223,1.09737774473891,135.598622307112));
#77980=CARTESIAN_POINT('Ctrl Pts',(-19.1474137264845,1.22586398536982,135.569212577293));
#77981=CARTESIAN_POINT('Ctrl Pts',(-19.1549040622467,1.35300289990215,135.534671709217));
#77982=CARTESIAN_POINT('Ctrl Pts',(-19.1623943980089,1.47836556314473,135.495162076188));
#77983=CARTESIAN_POINT('Ctrl Pts',(-19.170168732128,1.60848138986436,135.454154423415));
#77984=CARTESIAN_POINT('Ctrl Pts',(-19.1779430662471,1.73709578110266,135.407663886541));
#77985=CARTESIAN_POINT('Ctrl Pts',(-19.1857174003661,1.86371190476886,135.355817636865));
#77986=CARTESIAN_POINT('Ctrl Pts',(-19.1934821533133,1.99017198537883,135.304035283058));
#77987=CARTESIAN_POINT('Ctrl Pts',(-19.2012469062603,2.11463834009371,135.246910496081));
#77988=CARTESIAN_POINT('Ctrl Pts',(-19.2090116592074,2.23662855986402,135.184620398412));
#77989=CARTESIAN_POINT('Ctrl Pts',(-19.2167687000924,2.35849761722796,135.122392168147));
#77990=CARTESIAN_POINT('Ctrl Pts',(-19.2245257409774,2.47789508788356,135.055009013283));
#77991=CARTESIAN_POINT('Ctrl Pts',(-19.2322827818624,2.59435818368148,134.982696252393));
#77992=CARTESIAN_POINT('Ctrl Pts',(-19.2400339731025,2.7107334537526,134.910438023118));
#77993=CARTESIAN_POINT('Ctrl Pts',(-19.2477851643427,2.82417842267631,134.833257792583));
#77994=CARTESIAN_POINT('Ctrl Pts',(-19.2555363555828,2.93425490301979,134.751426771889));
#77995=CARTESIAN_POINT('Ctrl Pts',(-19.2632842523598,3.04428459792318,134.669630531562));
#77996=CARTESIAN_POINT('Ctrl Pts',(-19.2710321491369,3.15094833867724,134.583187665364));
#77997=CARTESIAN_POINT('Ctrl Pts',(-19.2787800459139,3.25383713327456,134.492412538652));
#77998=CARTESIAN_POINT('Ctrl Pts',(-19.286526321998,3.35670440575394,134.401656400139));
#77999=CARTESIAN_POINT('Ctrl Pts',(-19.2942725980821,3.45579800972093,134.306570062116));
#78000=CARTESIAN_POINT('Ctrl Pts',(-19.3020188741662,3.55074256918915,134.207507730144));
#78001=CARTESIAN_POINT('Ctrl Pts',(-19.3097652074316,3.64568782951667,134.108444666916));
#78002=CARTESIAN_POINT('Ctrl Pts',(-19.317511540697,3.73648371370533,134.005405833431));
#78003=CARTESIAN_POINT('Ctrl Pts',(-19.3252578739624,3.82279249560179,133.898781500069));
#78004=CARTESIAN_POINT('Ctrl Pts',(-19.3330059419654,3.90912060575165,133.792133288927));
#78005=CARTESIAN_POINT('Ctrl Pts',(-19.3407540099683,3.99095936812634,133.68189828396));
#78006=CARTESIAN_POINT('Ctrl Pts',(-19.3485020779713,4.06801230568507,133.568498628465));
#78007=CARTESIAN_POINT('Ctrl Pts',(-19.3562583807132,4.14514713602268,133.454978450466));
#78008=CARTESIAN_POINT('Ctrl Pts',(-19.364014683455,4.21748576077008,133.338287227021));
#78009=CARTESIAN_POINT('Ctrl Pts',(-19.3717709861968,4.28477561712758,133.218875263073));
#78010=CARTESIAN_POINT('Ctrl Pts',(-19.379531428711,4.35210138810748,133.099399565365));
#78011=CARTESIAN_POINT('Ctrl Pts',(-19.3872918712252,4.41437284389436,132.977200581812));
#78012=CARTESIAN_POINT('Ctrl Pts',(-19.3950523137394,4.47138458994209,132.852750939582));
#78013=CARTESIAN_POINT('Ctrl Pts',(-19.4028252140048,4.52848785630583,132.728101519737));
#78014=CARTESIAN_POINT('Ctrl Pts',(-19.4105981142703,4.58031439252309,132.60119458353));
#78015=CARTESIAN_POINT('Ctrl Pts',(-19.4183710145357,4.62670761593839,132.472521191107));
#78016=CARTESIAN_POINT('Ctrl Pts',(-19.4258613502977,4.67141432882488,132.348525400608));
#78017=CARTESIAN_POINT('Ctrl Pts',(-19.4333516860596,4.7110758071084,132.222889648152));
#78018=CARTESIAN_POINT('Ctrl Pts',(-19.4408420218216,4.74559681550516,132.096062567385));
#78019=CARTESIAN_POINT('Ctrl Pts',(-19.4486163559407,4.78142669842783,131.964426799303));
#78020=CARTESIAN_POINT('Ctrl Pts',(-19.4563906900598,4.81183211312075,131.831090598631));
#78021=CARTESIAN_POINT('Ctrl Pts',(-19.4641650241789,4.83665150251854,131.696540703471));
#78022=CARTESIAN_POINT('Ctrl Pts',(-19.471929777126,4.86144030423708,131.562156629031));
#78023=CARTESIAN_POINT('Ctrl Pts',(-19.4796945300731,4.88065670807868,131.426562217028));
#78024=CARTESIAN_POINT('Ctrl Pts',(-19.4874592830201,4.89418897832559,131.290259070883));
#78025=CARTESIAN_POINT('Ctrl Pts',(-19.4952163239051,4.90770780813094,131.154091302945));
#78026=CARTESIAN_POINT('Ctrl Pts',(-19.5029733647901,4.9155537008885,131.017216588241));
#78027=CARTESIAN_POINT('Ctrl Pts',(-19.5107304056751,4.91766607519587,130.880146073741));
#78028=CARTESIAN_POINT('Ctrl Pts',(-19.5184815969153,4.91977685654536,130.743178925182));
#78029=CARTESIAN_POINT('Ctrl Pts',(-19.5262327881554,4.91616271948905,130.60601666006));
#78030=CARTESIAN_POINT('Ctrl Pts',(-19.5339839793956,4.9068149905973,130.469174534099));
#78031=CARTESIAN_POINT('Ctrl Pts',(-19.5417318761727,4.89747123473974,130.332390569693));
#78032=CARTESIAN_POINT('Ctrl Pts',(-19.5494797729498,4.88239876050282,130.195926863059));
#78033=CARTESIAN_POINT('Ctrl Pts',(-19.5572276697269,4.86164098219284,130.060297432908));
#78034=CARTESIAN_POINT('Ctrl Pts',(-19.564973945811,4.84088754596257,129.924696373511));
#78035=CARTESIAN_POINT('Ctrl Pts',(-19.5727202218951,4.814451230239,129.789929629702));
#78036=CARTESIAN_POINT('Ctrl Pts',(-19.5804664979792,4.78242713830198,129.656504472689));
#78037=CARTESIAN_POINT('Ctrl Pts',(-19.5882128312445,4.75040280997042,129.523078330761));
#78038=CARTESIAN_POINT('Ctrl Pts',(-19.5959591645098,4.71279071436487,129.390994175558));
#78039=CARTESIAN_POINT('Ctrl Pts',(-19.6037054977752,4.66973664777365,129.260747096331));
#78040=CARTESIAN_POINT('Ctrl Pts',(-19.6114535657782,4.62667293952267,129.130470849173));
#78041=CARTESIAN_POINT('Ctrl Pts',(-19.6192016337811,4.57816495791328,129.002032867769));
#78042=CARTESIAN_POINT('Ctrl Pts',(-19.6269497017841,4.52440761097292,128.875910765413));
#78043=CARTESIAN_POINT('Ctrl Pts',(-19.634706004526,4.47059313008457,128.749654618985));
#78044=CARTESIAN_POINT('Ctrl Pts',(-19.6424623072679,4.41151829257835,128.625719628635));
#78045=CARTESIAN_POINT('Ctrl Pts',(-19.6502186100097,4.34742543639397,128.504561683421));
#78046=CARTESIAN_POINT('Ctrl Pts',(-19.6579790525239,4.28329837192219,128.383339072563));
#78047=CARTESIAN_POINT('Ctrl Pts',(-19.6657394950381,4.21414814912197,128.264896797703));
#78048=CARTESIAN_POINT('Ctrl Pts',(-19.6734999375523,4.14026138184423,128.14966312962));
#78049=CARTESIAN_POINT('Ctrl Pts',(-19.6812728378177,4.0662560049685,128.034244478222));
#78050=CARTESIAN_POINT('Ctrl Pts',(-19.6890457380832,3.98749911410493,127.922045046604));
#78051=CARTESIAN_POINT('Ctrl Pts',(-19.6968186383486,3.90431921531321,127.813462002194));
#78052=CARTESIAN_POINT('Ctrl Pts',(-19.7043089741106,3.82416311536076,127.708826224953));
#78053=CARTESIAN_POINT('Ctrl Pts',(-19.7117993098725,3.73990019642763,127.607548706975));
#78054=CARTESIAN_POINT('Ctrl Pts',(-19.7192896456345,3.65185642971071,127.509952069848));
#78055=CARTESIAN_POINT('Ctrl Pts',(-19.7270639797536,3.56047445681761,127.408655026559));
#78056=CARTESIAN_POINT('Ctrl Pts',(-19.7348383138727,3.46472980424949,127.31100261667));
#78057=CARTESIAN_POINT('Ctrl Pts',(-19.7426126479918,3.36494465301688,127.21739385655));
#78058=CARTESIAN_POINT('Ctrl Pts',(-19.7503774009388,3.26528247806525,127.123900460861));
#78059=CARTESIAN_POINT('Ctrl Pts',(-19.7581421538859,3.16158999467696,127.034441064307));
#78060=CARTESIAN_POINT('Ctrl Pts',(-19.765906906833,3.054228820132,126.949380802214));
#78061=CARTESIAN_POINT('Ctrl Pts',(-19.773663947718,2.94697427821883,126.864405023171));
#78062=CARTESIAN_POINT('Ctrl Pts',(-19.7814209886031,2.83605860092695,126.783819924739));
#78063=CARTESIAN_POINT('Ctrl Pts',(-19.7891780294881,2.72187908495015,126.707952763188));
#78064=CARTESIAN_POINT('Ctrl Pts',(-19.7969292207283,2.60778567263452,126.632142813654));
#78065=CARTESIAN_POINT('Ctrl Pts',(-19.8046804119684,2.4904336449919,126.561043934844));
#78066=CARTESIAN_POINT('Ctrl Pts',(-19.8124316032085,2.37025181305394,126.494941932266));
#78067=CARTESIAN_POINT('Ctrl Pts',(-19.8201794999856,2.25012106160083,126.428868024802));
#78068=CARTESIAN_POINT('Ctrl Pts',(-19.8279273967627,2.1271632398655,126.367786957505));
#78069=CARTESIAN_POINT('Ctrl Pts',(-19.8356752935397,2.00183427284138,126.311940044359));
#78070=CARTESIAN_POINT('Ctrl Pts',(-19.8434215696238,1.87653152193539,126.256104813183));
#78071=CARTESIAN_POINT('Ctrl Pts',(-19.8511678457079,1.74885896918546,126.205501717427));
#78072=CARTESIAN_POINT('Ctrl Pts',(-19.858914121792,1.61929480186951,126.160324936487));
#78073=CARTESIAN_POINT('Ctrl Pts',(-19.8666604550574,1.48972967814066,126.115147822062));
#78074=CARTESIAN_POINT('Ctrl Pts',(-19.8744067883227,1.35827328114988,126.075397231103));
#78075=CARTESIAN_POINT('Ctrl Pts',(-19.882153121588,1.22542094996073,126.041218108896));
#78076=CARTESIAN_POINT('Ctrl Pts',(-19.889901189591,1.09253886741261,126.007031332512));
#78077=CARTESIAN_POINT('Ctrl Pts',(-19.897649257594,0.958260607171626,125.978418605037));
#78078=CARTESIAN_POINT('Ctrl Pts',(-19.905397325597,0.823093351378072,125.955474106477));
#78079=CARTESIAN_POINT('Ctrl Pts',(-19.9131536283389,0.68778243821655,125.932505222232));
#78080=CARTESIAN_POINT('Ctrl Pts',(-19.9209099310806,0.551581028158589,
125.915216666548));
#78081=CARTESIAN_POINT('Ctrl Pts',(-19.9286662338225,0.415003663155578,
125.903650972824));
#78082=CARTESIAN_POINT('Ctrl Pts',(-19.9364266763367,0.278353402700785,
125.892079106141));
#78083=CARTESIAN_POINT('Ctrl Pts',(-19.9441871188509,0.141327177891082,
125.886236204344));
#78084=CARTESIAN_POINT('Ctrl Pts',(-19.951947561365,0.00444022684729692,
125.886112621899));
#78085=CARTESIAN_POINT('Ctrl Pts',(-19.9597204616305,-0.132666467282743,
125.885988841068));
#78086=CARTESIAN_POINT('Ctrl Pts',(-19.9674933618959,-0.269633050011513,
125.891602710449));
#78087=CARTESIAN_POINT('Ctrl Pts',(-19.9752662621614,-0.405947807584604,
125.902892527288));
#78088=CARTESIAN_POINT('Ctrl Pts',(-19.9827565979234,-0.53730718036376,
125.913771930847));
#78089=CARTESIAN_POINT('Ctrl Pts',(-19.9902469336854,-0.66806099048736,
125.929921738687));
#78090=CARTESIAN_POINT('Ctrl Pts',(-19.9977372694475,-0.797761611883198,
125.951242086858));
#78091=CARTESIAN_POINT('Ctrl Pts',(-20.0055116035666,-0.932379871761093,
125.973370802509));
#78092=CARTESIAN_POINT('Ctrl Pts',(-20.0132859376856,-1.06628993326668,
126.001139977507));
#78093=CARTESIAN_POINT('Ctrl Pts',(-20.0210602718047,-1.19898194592276,
126.034494229935));
#78094=CARTESIAN_POINT('Ctrl Pts',(-20.0288250247518,-1.3315104275319,126.067807376228));
#78095=CARTESIAN_POINT('Ctrl Pts',(-20.0365897776989,-1.46282347157565,
126.106691810222));
#78096=CARTESIAN_POINT('Ctrl Pts',(-20.044354530646,-1.5924184163906,126.151040657619));
#78097=CARTESIAN_POINT('Ctrl Pts',(-20.052111571531,-1.72188464567939,126.195345457116));
#78098=CARTESIAN_POINT('Ctrl Pts',(-20.0598686124161,-1.84963580412119,
126.245103743613));
#78099=CARTESIAN_POINT('Ctrl Pts',(-20.067625653301,-1.97518181317857,126.30015815016));
#78100=CARTESIAN_POINT('Ctrl Pts',(-20.0753768445412,-2.10063314701426,
126.35517103975));
#78101=CARTESIAN_POINT('Ctrl Pts',(-20.0831280357812,-2.22388228480489,
126.415471943505));
#78102=CARTESIAN_POINT('Ctrl Pts',(-20.0908792270214,-2.344456987447,126.480854575416));
#78103=CARTESIAN_POINT('Ctrl Pts',(-20.0986271237984,-2.46498044262372,
126.546209417964));
#78104=CARTESIAN_POINT('Ctrl Pts',(-20.1063750205756,-2.58283138050623,
126.616641506874));
#78105=CARTESIAN_POINT('Ctrl Pts',(-20.1141229173526,-2.69756033820974,
126.69189769564));
#78106=CARTESIAN_POINT('Ctrl Pts',(-20.1218691934367,-2.81226529708873,
126.767138142433));
#78107=CARTESIAN_POINT('Ctrl Pts',(-20.1296154695208,-2.92384924803899,
126.847200467631));
#78108=CARTESIAN_POINT('Ctrl Pts',(-20.1373617456049,-3.03189035053216,
126.93178731744));
#78109=CARTESIAN_POINT('Ctrl Pts',(-20.1451080788703,-3.13993225056021,
127.016374791649));
#78110=CARTESIAN_POINT('Ctrl Pts',(-20.1528544121356,-3.24443094210425,
127.105486616101));
#78111=CARTESIAN_POINT('Ctrl Pts',(-20.160600745401,-3.34499673572624,127.19878439448));
#78112=CARTESIAN_POINT('Ctrl Pts',(-20.168348813404,-3.44558505036043,127.29210306625));
#78113=CARTESIAN_POINT('Ctrl Pts',(-20.1760968814069,-3.54223842792924,
127.389609291444));
#78114=CARTESIAN_POINT('Ctrl Pts',(-20.1838449494099,-3.63460348778926,
127.490927269957));
#78115=CARTESIAN_POINT('Ctrl Pts',(-20.1916012521518,-3.72706671433406,
127.592352930423));
#78116=CARTESIAN_POINT('Ctrl Pts',(-20.1993575548936,-3.81523225490922,
127.697598147485));
#78117=CARTESIAN_POINT('Ctrl Pts',(-20.2071138576355,-3.89878620246822,
127.806253012769));
#78118=CARTESIAN_POINT('Ctrl Pts',(-20.2148743001496,-3.98238474528457,
127.914965870425));
#78119=CARTESIAN_POINT('Ctrl Pts',(-20.2226347426638,-4.06136656560708,
128.027091683));
#78120=CARTESIAN_POINT('Ctrl Pts',(-20.230395185178,-4.13546127970726,128.142191752422));
#78121=CARTESIAN_POINT('Ctrl Pts',(-20.2381680854434,-4.20967493722053,
128.257476590694));
#78122=CARTESIAN_POINT('Ctrl Pts',(-20.2459409857088,-4.27898561347636,
128.375744889366));
#78123=CARTESIAN_POINT('Ctrl Pts',(-20.2537138859742,-4.34316862696734,
128.496532777317));
#78124=CARTESIAN_POINT('Ctrl Pts',(-20.2612042217362,-4.40501842625039,
128.612929721295));
#78125=CARTESIAN_POINT('Ctrl Pts',(-20.2686945574983,-4.4621067637387,128.73166597051));
#78126=CARTESIAN_POINT('Ctrl Pts',(-20.2761848932603,-4.51427570497735,
128.852310945567));
#78127=CARTESIAN_POINT('Ctrl Pts',(-20.2847817142089,-4.57415113128143,
128.990777802311));
#78128=CARTESIAN_POINT('Ctrl Pts',(-20.2933785351576,-4.6277091580921,129.132133849189));
#78129=CARTESIAN_POINT('Ctrl Pts',(-20.3019753561063,-4.67469033843641,
129.275814477527));
#78130=CARTESIAN_POINT('Ctrl Pts',(-20.3080269665765,-4.70776207560217,
129.376956422905));
#78131=CARTESIAN_POINT('Ctrl Pts',(-20.3140785770467,-4.73757573071408,
129.47924968965));
#78132=CARTESIAN_POINT('Ctrl Pts',(-20.320130187517,-4.76405452823408,129.582490119308));
#78133=CARTESIAN_POINT('Origin',(213.235140564004,0.,130.804360617566));
#78134=CARTESIAN_POINT('',(-22.4150500904691,-4.76405452823408,129.582490119308));
#78135=CARTESIAN_POINT('',(-22.0699306202468,-4.76405452823405,129.582490119308));
#78136=CARTESIAN_POINT('',(213.235140564004,-4.76405452823405,129.582490119308));
#78137=CARTESIAN_POINT('',(-20.7351405640401,-4.91824802158401,130.808772044207));
#78138=CARTESIAN_POINT('Ctrl Pts',(-20.7351405640403,-4.91824802158401,
130.808772044207));
#78139=CARTESIAN_POINT('Ctrl Pts',(-20.7446813187049,-4.91809669710575,
130.977481937026));
#78140=CARTESIAN_POINT('Ctrl Pts',(-20.7542220733695,-4.90926088785877,
131.145806171752));
#78141=CARTESIAN_POINT('Ctrl Pts',(-20.7637628280341,-4.89188139518882,
131.312966042139));
#78142=CARTESIAN_POINT('Ctrl Pts',(-20.7734548646572,-4.87422632644771,
131.482776465176));
#78143=CARTESIAN_POINT('Ctrl Pts',(-20.7831469012802,-4.84775452509061,
131.651385380119));
#78144=CARTESIAN_POINT('Ctrl Pts',(-20.7928389379032,-4.81266233021236,
131.817999783076));
#78145=CARTESIAN_POINT('Ctrl Pts',(-20.7997230068444,-4.78773701283744,
131.936342818823));
#78146=CARTESIAN_POINT('Ctrl Pts',(-20.8066070757855,-4.7584637302795,132.053680119585));
#78147=CARTESIAN_POINT('Ctrl Pts',(-20.8134911447266,-4.7249273209099,132.169734146905));
#78148=CARTESIAN_POINT('Ctrl Pts',(-20.8212654788457,-4.6870538984003,132.300796574077));
#78149=CARTESIAN_POINT('Ctrl Pts',(-20.8290398129648,-4.64366314041326,
132.430489572245));
#78150=CARTESIAN_POINT('Ctrl Pts',(-20.8368141470839,-4.59487025902523,
132.558313400632));
#78151=CARTESIAN_POINT('Ctrl Pts',(-20.844578900031,-4.54613751050276,132.685979697575));
#78152=CARTESIAN_POINT('Ctrl Pts',(-20.8523436529781,-4.49201602337523,
132.811781046432));
#78153=CARTESIAN_POINT('Ctrl Pts',(-20.8601084059252,-4.43267129262655,
132.935230926624));
#78154=CARTESIAN_POINT('Ctrl Pts',(-20.8678654468102,-4.37338550390114,
133.058558194655));
#78155=CARTESIAN_POINT('Ctrl Pts',(-20.8756224876953,-4.30888696380172,
133.17953829171));
#78156=CARTESIAN_POINT('Ctrl Pts',(-20.8833795285803,-4.23938982037526,
133.297703155887));
#78157=CARTESIAN_POINT('Ctrl Pts',(-20.8911307198204,-4.16994508528527,
133.41577891102));
#78158=CARTESIAN_POINT('Ctrl Pts',(-20.8988819110604,-4.09550944720151,
133.53104332332));
#78159=CARTESIAN_POINT('Ctrl Pts',(-20.9066331023006,-4.01634352383359,
133.64305182322));
#78160=CARTESIAN_POINT('Ctrl Pts',(-20.9143809990776,-3.93721124809482,
133.755012716521));
#78161=CARTESIAN_POINT('Ctrl Pts',(-20.9221288958547,-3.85335291098092,
133.863720131193));
#78162=CARTESIAN_POINT('Ctrl Pts',(-20.9298767926318,-3.76507297263704,
133.968757649106));
#78163=CARTESIAN_POINT('Ctrl Pts',(-20.9376230687159,-3.67681150055305,
134.073773195435));
#78164=CARTESIAN_POINT('Ctrl Pts',(-20.9453693448,-3.58413051831039,134.175120072823));
#78165=CARTESIAN_POINT('Ctrl Pts',(-20.9531156208841,-3.48737512147832,
134.272414513427));
#78166=CARTESIAN_POINT('Ctrl Pts',(-20.9608619541495,-3.39061901041988,
134.369709672236));
#78167=CARTESIAN_POINT('Ctrl Pts',(-20.9686082874148,-3.28978870044187,
134.462952057347));
#78168=CARTESIAN_POINT('Ctrl Pts',(-20.9763546206802,-3.1852662450395,134.551794674452));
#78169=CARTESIAN_POINT('Ctrl Pts',(-20.9841026886832,-3.08072038255823,
134.640657187245));
#78170=CARTESIAN_POINT('Ctrl Pts',(-20.9918507566862,-2.97248102719271,
134.725117718246));
#78171=CARTESIAN_POINT('Ctrl Pts',(-20.9995988246891,-2.86096308603967,
134.804869745517));
#78172=CARTESIAN_POINT('Ctrl Pts',(-21.007355127431,-2.74932662229153,134.884706534192));
#78173=CARTESIAN_POINT('Ctrl Pts',(-21.0151114301728,-2.63440493057037,
134.959824594812));
#78174=CARTESIAN_POINT('Ctrl Pts',(-21.0228677329147,-2.51664212533206,
135.029960631233));
#78175=CARTESIAN_POINT('Ctrl Pts',(-21.0306281754289,-2.39881646653865,
135.100134101369));
#78176=CARTESIAN_POINT('Ctrl Pts',(-21.0383886179431,-2.27814701651188,
135.165320063181));
#78177=CARTESIAN_POINT('Ctrl Pts',(-21.0461490604573,-2.15510133740986,
135.225301839523));
#78178=CARTESIAN_POINT('Ctrl Pts',(-21.0539219607227,-2.03185813446044,
135.285379903936));
#78179=CARTESIAN_POINT('Ctrl Pts',(-21.0616948609882,-1.906231438283,135.34023693194));
#78180=CARTESIAN_POINT('Ctrl Pts',(-21.0694677612536,-1.77870841005995,
135.38970460188));
#78181=CARTESIAN_POINT('Ctrl Pts',(-21.0769580970156,-1.65582116512497,
135.437373997415));
#78182=CARTESIAN_POINT('Ctrl Pts',(-21.0844484327775,-1.53117335878165,
135.480038965816));
#78183=CARTESIAN_POINT('Ctrl Pts',(-21.0919387685395,-1.40521121009835,
135.517593533253));
#78184=CARTESIAN_POINT('Ctrl Pts',(-21.0997131026586,-1.27447316826143,
135.556571993529));
#78185=CARTESIAN_POINT('Ctrl Pts',(-21.1074874367776,-1.14190501123633,
135.590168353381));
#78186=CARTESIAN_POINT('Ctrl Pts',(-21.1152617708967,-1.00798946003274,
135.618209421897));
#78187=CARTESIAN_POINT('Ctrl Pts',(-21.1230265238438,-0.874238947777619,
135.646215932303));
#78188=CARTESIAN_POINT('Ctrl Pts',(-21.1307912767909,-0.739144724321958,
135.668680694308));
#78189=CARTESIAN_POINT('Ctrl Pts',(-21.138556029738,-0.60320556728882,135.685479967274));
#78190=CARTESIAN_POINT('Ctrl Pts',(-21.146313070623,-0.467401426943038,
135.702262554965));
#78191=CARTESIAN_POINT('Ctrl Pts',(-21.1540701115079,-0.3307544085683,135.713390804047));
#78192=CARTESIAN_POINT('Ctrl Pts',(-21.1618271523929,-0.193774058149417,
135.718791884446));
#78193=CARTESIAN_POINT('Ctrl Pts',(-21.169578343633,-0.0568970056783372,
135.724188891848));
#78194=CARTESIAN_POINT('Ctrl Pts',(-21.1773295348731,0.0803124894226256,
135.723867311739));
#78195=CARTESIAN_POINT('Ctrl Pts',(-21.1850807261132,0.217339527950154,
135.717806108471));
#78196=CARTESIAN_POINT('Ctrl Pts',(-21.1928286228903,0.354308326331179,
135.711747481375));
#78197=CARTESIAN_POINT('Ctrl Pts',(-21.2005765196674,0.491094432612081,
135.699954100326));
#78198=CARTESIAN_POINT('Ctrl Pts',(-21.2083244164445,0.627182934281594,
135.682457032096));
#78199=CARTESIAN_POINT('Ctrl Pts',(-21.2160706925286,0.763242969170286,
135.664963623875));
#78200=CARTESIAN_POINT('Ctrl Pts',(-21.2238169686127,0.898605302170506,
135.641768951416));
#78201=CARTESIAN_POINT('Ctrl Pts',(-21.2315632446968,1.03276052594148,135.612955917501));
#78202=CARTESIAN_POINT('Ctrl Pts',(-21.2393095779621,1.16691674001583,135.584142670895));
#78203=CARTESIAN_POINT('Ctrl Pts',(-21.2470559112275,1.29986544483202,135.549711062173));
#78204=CARTESIAN_POINT('Ctrl Pts',(-21.2548022444928,1.43110819500367,135.50979496486));
#78205=CARTESIAN_POINT('Ctrl Pts',(-21.2625503124958,1.56238033607907,135.469869928614));
#78206=CARTESIAN_POINT('Ctrl Pts',(-21.2702983804987,1.69194538832479,135.424458073516));
#78207=CARTESIAN_POINT('Ctrl Pts',(-21.2780464485017,1.81932119873293,135.373742790064));
#78208=CARTESIAN_POINT('Ctrl Pts',(-21.2858027512435,1.94683238566833,135.322973605804));
#78209=CARTESIAN_POINT('Ctrl Pts',(-21.2935590539854,2.0721493190159,135.266889878434));
#78210=CARTESIAN_POINT('Ctrl Pts',(-21.3013153567272,2.19481042556054,135.205722936025));
#78211=CARTESIAN_POINT('Ctrl Pts',(-21.3090757992414,2.31753700003099,135.144523346977));
#78212=CARTESIAN_POINT('Ctrl Pts',(-21.3168362417556,2.43760458112017,135.078235325748));
#78213=CARTESIAN_POINT('Ctrl Pts',(-21.3245966842697,2.55457814344091,135.007135126334));
#78214=CARTESIAN_POINT('Ctrl Pts',(-21.3323695845352,2.67173948210831,134.935920790569));
#78215=CARTESIAN_POINT('Ctrl Pts',(-21.3401424848006,2.78579655128592,134.859879056735));
#78216=CARTESIAN_POINT('Ctrl Pts',(-21.347915385066,2.89634441468123,134.779328805369));
#78217=CARTESIAN_POINT('Ctrl Pts',(-21.3554057208282,3.00287358479019,134.701706758533));
#78218=CARTESIAN_POINT('Ctrl Pts',(-21.3628960565902,3.10614401506301,134.619898486416));
#78219=CARTESIAN_POINT('Ctrl Pts',(-21.3703863923523,3.20582535441011,134.534222124314));
#78220=CARTESIAN_POINT('Ctrl Pts',(-21.3781607264714,3.30928614203488,134.445297316904));
#78221=CARTESIAN_POINT('Ctrl Pts',(-21.3859350605905,3.40920803810672,134.35192362501));
#78222=CARTESIAN_POINT('Ctrl Pts',(-21.3937093947096,3.50518440970838,134.254413561571));
#78223=CARTESIAN_POINT('Ctrl Pts',(-21.4014741476567,3.6010424990097,134.15702367057));
#78224=CARTESIAN_POINT('Ctrl Pts',(-21.4092389006037,3.69296446715769,134.055507826906));
#78225=CARTESIAN_POINT('Ctrl Pts',(-21.4170036535508,3.78057660615906,133.95021878148));
#78226=CARTESIAN_POINT('Ctrl Pts',(-21.4247606944358,3.86810172754874,133.845034310618));
#78227=CARTESIAN_POINT('Ctrl Pts',(-21.4325177353209,3.95132528989059,133.736084394466));
#78228=CARTESIAN_POINT('Ctrl Pts',(-21.4402747762059,4.02991059712929,133.623758362058));
#78229=CARTESIAN_POINT('Ctrl Pts',(-21.4480259674461,4.10843664257649,133.511517035584));
#78230=CARTESIAN_POINT('Ctrl Pts',(-21.4557771586861,4.18233117175354,133.395904979477));
#78231=CARTESIAN_POINT('Ctrl Pts',(-21.4635283499262,4.25129817117705,133.277344022736));
#78232=CARTESIAN_POINT('Ctrl Pts',(-21.4712762467033,4.32023585778604,133.158833457565));
#78233=CARTESIAN_POINT('Ctrl Pts',(-21.4790241434803,4.38424998393468,133.03737682184));
#78234=CARTESIAN_POINT('Ctrl Pts',(-21.4867720402574,4.44308836418855,132.913424118391));
#78235=CARTESIAN_POINT('Ctrl Pts',(-21.4945183163415,4.50191443672168,132.789497343175));
#78236=CARTESIAN_POINT('Ctrl Pts',(-21.5022645924256,4.55556674927008,132.663075891736));
#78237=CARTESIAN_POINT('Ctrl Pts',(-21.5100108685097,4.6038397031817,132.534633153876));
#78238=CARTESIAN_POINT('Ctrl Pts',(-21.517757201775,4.65211301343329,132.40618946788));
#78239=CARTESIAN_POINT('Ctrl Pts',(-21.5255035350405,4.69500674826715,132.275724831662));
#78240=CARTESIAN_POINT('Ctrl Pts',(-21.5332498683058,4.73236411736538,132.143730963353));
#78241=CARTESIAN_POINT('Ctrl Pts',(-21.5409979363088,4.76972985238741,132.011707535931));
#78242=CARTESIAN_POINT('Ctrl Pts',(-21.5487460043117,4.80155664810437,131.878154571077));
#78243=CARTESIAN_POINT('Ctrl Pts',(-21.5564940723147,4.82773818065694,131.743576844815));
#78244=CARTESIAN_POINT('Ctrl Pts',(-21.5642503750566,4.85394753925388,131.608856087743));
#78245=CARTESIAN_POINT('Ctrl Pts',(-21.5720066777984,4.87449957455411,131.473108777993));
#78246=CARTESIAN_POINT('Ctrl Pts',(-21.5797629805403,4.88933941781885,131.336848288656));
#78247=CARTESIAN_POINT('Ctrl Pts',(-21.5875234230545,4.90418718155478,131.200515072993));
#78248=CARTESIAN_POINT('Ctrl Pts',(-21.5952838655686,4.91331665231312,131.063668521883));
#78249=CARTESIAN_POINT('Ctrl Pts',(-21.6030443080828,4.91672510855631,130.926823956537));
#78250=CARTESIAN_POINT('Ctrl Pts',(-21.6108172083482,4.92013903635605,130.789759716146));
#78251=CARTESIAN_POINT('Ctrl Pts',(-21.6185901086136,4.91781360395731,130.652697859023));
#78252=CARTESIAN_POINT('Ctrl Pts',(-21.626363008879,4.90979821662803,130.516151432258));
#78253=CARTESIAN_POINT('Ctrl Pts',(-21.6338533446411,4.90207420881771,130.384568812044));
#78254=CARTESIAN_POINT('Ctrl Pts',(-21.6413436804031,4.8890667826379,130.253465104929));
#78255=CARTESIAN_POINT('Ctrl Pts',(-21.6488340161652,4.87086503149063,130.123290204538));
#78256=CARTESIAN_POINT('Ctrl Pts',(-21.6566083502843,4.85197315541634,129.988179683233));
#78257=CARTESIAN_POINT('Ctrl Pts',(-21.6643826844033,4.82742544950069,129.853641800885));
#78258=CARTESIAN_POINT('Ctrl Pts',(-21.6721570185224,4.7972650447047,129.72018759016));
#78259=CARTESIAN_POINT('Ctrl Pts',(-21.6799217714695,4.76714180991215,129.586897849823));
#78260=CARTESIAN_POINT('Ctrl Pts',(-21.6876865244166,4.73141972466212,129.454689501492));
#78261=CARTESIAN_POINT('Ctrl Pts',(-21.6954512773637,4.69019356998027,129.324067626765));
#78262=CARTESIAN_POINT('Ctrl Pts',(-21.7032083182487,4.64900836169645,129.193575487525));
#78263=CARTESIAN_POINT('Ctrl Pts',(-21.7109653591336,4.60233007991013,129.064667056583));
#78264=CARTESIAN_POINT('Ctrl Pts',(-21.7187224000186,4.5503042857218,128.937836047719));
#78265=CARTESIAN_POINT('Ctrl Pts',(-21.7264735912588,4.4983177245895,128.811100683105));
#78266=CARTESIAN_POINT('Ctrl Pts',(-21.734224782499,4.44099182547712,128.686439982599));
#78267=CARTESIAN_POINT('Ctrl Pts',(-21.7419759737391,4.37852148255138,128.564330999606));
#78268=CARTESIAN_POINT('Ctrl Pts',(-21.7497238705162,4.31607769118784,128.442273916189));
#78269=CARTESIAN_POINT('Ctrl Pts',(-21.7574717672932,4.24849398253747,128.322766740533));
#78270=CARTESIAN_POINT('Ctrl Pts',(-21.7652196640703,4.17601264433699,128.206264880909));
#78271=CARTESIAN_POINT('Ctrl Pts',(-21.7729659401544,4.10354646766994,128.089787390961));
#78272=CARTESIAN_POINT('Ctrl Pts',(-21.7807122162386,4.02618490559565,127.976314298383));
#78273=CARTESIAN_POINT('Ctrl Pts',(-21.7884584923227,3.94421510326795,127.866274457895));
#78274=CARTESIAN_POINT('Ctrl Pts',(-21.796204825588,3.8622446958578,127.756233805117));
#78275=CARTESIAN_POINT('Ctrl Pts',(-21.8039511588534,3.77566621387236,127.649626768535));
#78276=CARTESIAN_POINT('Ctrl Pts',(-21.8116974921188,3.68480860470474,127.546851045946));
#78277=CARTESIAN_POINT('Ctrl Pts',(-21.8194455601218,3.59393064860564,127.444052307447));
#78278=CARTESIAN_POINT('Ctrl Pts',(-21.8271936281248,3.49877191735522,127.345086883113));
#78279=CARTESIAN_POINT('Ctrl Pts',(-21.8349416961277,3.39969962267526,127.250317069988));
#78280=CARTESIAN_POINT('Ctrl Pts',(-21.8426979988696,3.3005220327814,127.155446534378));
#78281=CARTESIAN_POINT('Ctrl Pts',(-21.8504543016114,3.19742285361602,127.064780788284));
#78282=CARTESIAN_POINT('Ctrl Pts',(-21.8582106043532,3.09080434260711,126.978643485025));
#78283=CARTESIAN_POINT('Ctrl Pts',(-21.8659710468674,2.98412892608866,126.892460207693));
#78284=CARTESIAN_POINT('Ctrl Pts',(-21.8737314893816,2.87393074888859,126.810810421846));
#78285=CARTESIAN_POINT('Ctrl Pts',(-21.8814919318958,2.76064189427898,126.733974960893));
#78286=CARTESIAN_POINT('Ctrl Pts',(-21.8892648321612,2.64717117834265,126.657016156836));
#78287=CARTESIAN_POINT('Ctrl Pts',(-21.8970377324267,2.53060020313822,126.584887327276));
#78288=CARTESIAN_POINT('Ctrl Pts',(-21.9048106326921,2.41138731446645,126.517824220645));
#78289=CARTESIAN_POINT('Ctrl Pts',(-21.9123009684541,2.29650811457737,126.453199026862));
#78290=CARTESIAN_POINT('Ctrl Pts',(-21.9197913042162,2.17917602115765,126.393277786815));
#78291=CARTESIAN_POINT('Ctrl Pts',(-21.9272816399782,2.05981769961689,126.338228722196));
#78292=CARTESIAN_POINT('Ctrl Pts',(-21.9350559740973,1.93593387103638,126.281092455559));
#78293=CARTESIAN_POINT('Ctrl Pts',(-21.9428303082163,1.80947470564764,126.229024124094));
#78294=CARTESIAN_POINT('Ctrl Pts',(-21.9506046423354,1.68089346304385,126.182263666138));
#78295=CARTESIAN_POINT('Ctrl Pts',(-21.9583693952825,1.55247068532992,126.135560836268));
#78296=CARTESIAN_POINT('Ctrl Pts',(-21.9661341482296,1.42193139790572,126.09415299665));
#78297=CARTESIAN_POINT('Ctrl Pts',(-21.9738989011767,1.28975177168359,126.058233414262));
#78298=CARTESIAN_POINT('Ctrl Pts',(-21.9816559420617,1.15770342812981,126.022349507711));
#78299=CARTESIAN_POINT('Ctrl Pts',(-21.9894129829468,1.02401836281609,125.991943112488));
#78300=CARTESIAN_POINT('Ctrl Pts',(-21.9971700238318,0.889190630458458,
125.967158628275));
#78301=CARTESIAN_POINT('Ctrl Pts',(-22.0049212150719,0.754464572742602,
125.942392834234));
#78302=CARTESIAN_POINT('Ctrl Pts',(-22.012672406312,0.618597946099293,125.923240583081));
#78303=CARTESIAN_POINT('Ctrl Pts',(-22.0204235975521,0.482097454127241,
125.909795763851));
#78304=CARTESIAN_POINT('Ctrl Pts',(-22.0281714943292,0.345654978505546,
125.896356659028));
#78305=CARTESIAN_POINT('Ctrl Pts',(-22.0359193911062,0.208579561658239,
125.888620199619));
#78306=CARTESIAN_POINT('Ctrl Pts',(-22.0436672878833,0.0713853138995451,
125.886628701382));
#78307=CARTESIAN_POINT('Ctrl Pts',(-22.0514135639674,-0.0657802357800839,
125.884637619723));
#78308=CARTESIAN_POINT('Ctrl Pts',(-22.0591598400515,-0.203064176253083,
125.888389114617));
#78309=CARTESIAN_POINT('Ctrl Pts',(-22.0669061161356,-0.339950490928263,
125.897873409163));
#78310=CARTESIAN_POINT('Ctrl Pts',(-22.074652449401,-0.476837816067122,
125.907357773721));
#78311=CARTESIAN_POINT('Ctrl Pts',(-22.0823987826663,-0.613327119521069,
125.922574995352));
#78312=CARTESIAN_POINT('Ctrl Pts',(-22.0901451159317,-0.748906002770302,
125.94346328667));
#78313=CARTESIAN_POINT('Ctrl Pts',(-22.0978931839347,-0.884515247970401,
125.964356255776));
#78314=CARTESIAN_POINT('Ctrl Pts',(-22.1056412519377,-1.0192132809315,125.990922762194));
#78315=CARTESIAN_POINT('Ctrl Pts',(-22.1133893199406,-1.15249680398375,
126.023049690706));
#78316=CARTESIAN_POINT('Ctrl Pts',(-22.1211456226825,-1.2859219823504,126.0552107641));
#78317=CARTESIAN_POINT('Ctrl Pts',(-22.1289019254244,-1.41792926700313,
126.092943973055));
#78318=CARTESIAN_POINT('Ctrl Pts',(-22.1366582281662,-1.54802892927213,
126.136085829527));
#78319=CARTESIAN_POINT('Ctrl Pts',(-22.1444186706804,-1.67819802964829,
126.179250712108));
#78320=CARTESIAN_POINT('Ctrl Pts',(-22.1521791131944,-1.80645711344013,
126.227829855904));
#78321=CARTESIAN_POINT('Ctrl Pts',(-22.1599395557086,-1.9323363559845,126.281611534338));
#78322=CARTESIAN_POINT('Ctrl Pts',(-22.167712455974,-2.05841767106386,126.335479547897));
#78323=CARTESIAN_POINT('Ctrl Pts',(-22.1754853562395,-2.18211115766965,
126.394566616576));
#78324=CARTESIAN_POINT('Ctrl Pts',(-22.1832582565049,-2.30297072686775,
126.458614548858));
#78325=CARTESIAN_POINT('Ctrl Pts',(-22.1907485922669,-2.4194367462991,126.520334177475));
#78326=CARTESIAN_POINT('Ctrl Pts',(-22.198238928029,-2.53327104509812,126.586660096784));
#78327=CARTESIAN_POINT('Ctrl Pts',(-22.2057292637911,-2.64410147051529,
126.657324269025));
#78328=CARTESIAN_POINT('Ctrl Pts',(-22.2135050158773,-2.75915504608735,
126.730681072002));
#78329=CARTESIAN_POINT('Ctrl Pts',(-22.2212807679636,-2.87133580835104,
126.808945712742));
#78330=CARTESIAN_POINT('Ctrl Pts',(-22.2290565200499,-2.98019665006642,
126.891866401668));
#78331=CARTESIAN_POINT('Ctrl Pts',(-22.2368199666371,-3.0888852143012,126.974655864645));
#78332=CARTESIAN_POINT('Ctrl Pts',(-22.2445834132244,-3.19426401401315,
127.062086465408));
#78333=CARTESIAN_POINT('Ctrl Pts',(-22.2523468598116,-3.29591328084603,
127.153862198495));
#78334=CARTESIAN_POINT('Ctrl Pts',(-22.2601032064868,-3.39746958628009,
127.245553999835));
#78335=CARTESIAN_POINT('Ctrl Pts',(-22.267859553162,-3.49530285553143,127.341582768679));
#78336=CARTESIAN_POINT('Ctrl Pts',(-22.2756158998372,-3.58902465571209,
127.441610986209));
#78337=CARTESIAN_POINT('Ctrl Pts',(-22.2833668330945,-3.68268104426293,
127.541569390647));
#78338=CARTESIAN_POINT('Ctrl Pts',(-22.2911177663518,-3.77223140701409,
127.645521405863));
#78339=CARTESIAN_POINT('Ctrl Pts',(-22.298868699609,-3.85732289862148,127.75309151795));
#78340=CARTESIAN_POINT('Ctrl Pts',(-22.3066159019005,-3.94237343084635,
127.860609850415));
#78341=CARTESIAN_POINT('Ctrl Pts',(-22.3143631041919,-4.02296912173825,
127.971742507572));
#78342=CARTESIAN_POINT('Ctrl Pts',(-22.3221103064834,-4.09879655867963,
128.08607994165));
#78343=CARTESIAN_POINT('Ctrl Pts',(-22.3298572073455,-4.17462104531473,
128.200412927069));
#78344=CARTESIAN_POINT('Ctrl Pts',(-22.3376041082076,-4.24567742114018,
128.317950122415));
#78345=CARTESIAN_POINT('Ctrl Pts',(-22.3453510090697,-4.31169491968724,
128.438252001707));
#78346=CARTESIAN_POINT('Ctrl Pts',(-22.3530973593788,-4.37770772653487,
128.558545331443));
#78347=CARTESIAN_POINT('Ctrl Pts',(-22.3608437096879,-4.43868218493249,
128.681602608968));
#78348=CARTESIAN_POINT('Ctrl Pts',(-22.368590059997,-4.49439330747625,128.806959340854));
#78349=CARTESIAN_POINT('Ctrl Pts',(-22.3763411935889,-4.55013883100134,
128.932393479088));
#78350=CARTESIAN_POINT('Ctrl Pts',(-22.3840923271808,-4.60061436663891,
129.060129550598));
#78351=CARTESIAN_POINT('Ctrl Pts',(-22.3918434607727,-4.64564283081932,
129.189682398552));
#78352=CARTESIAN_POINT('Ctrl Pts',(-22.3995790040048,-4.69058072631766,
129.318974668427));
#78353=CARTESIAN_POINT('Ctrl Pts',(-22.407314547237,-4.73009335830748,129.450076033197));
#78354=CARTESIAN_POINT('Ctrl Pts',(-22.4150500904691,-4.76405452823408,
129.582490119308));
#78355=CARTESIAN_POINT('Ctrl Pts',(-20.6651747065899,-4.7640545282341,129.582490119308));
#78356=CARTESIAN_POINT('Ctrl Pts',(-20.6728565465615,-4.79788063571959,
129.714377599012));
#78357=CARTESIAN_POINT('Ctrl Pts',(-20.6805383865331,-4.82622772596712,
129.847678318042));
#78358=CARTESIAN_POINT('Ctrl Pts',(-20.6882202265047,-4.8489928090036,129.981893718091));
#78359=CARTESIAN_POINT('Ctrl Pts',(-20.6960402827554,-4.87216749508839,
130.118524002238));
#78360=CARTESIAN_POINT('Ctrl Pts',(-20.703860339006,-4.88955727877376,130.256101781898));
#78361=CARTESIAN_POINT('Ctrl Pts',(-20.7116803952567,-4.90110841950362,
130.394093237958));
#78362=CARTESIAN_POINT('Ctrl Pts',(-20.7195004515073,-4.91265956023348,
130.532084694017));
#78363=CARTESIAN_POINT('Ctrl Pts',(-20.727320507758,-4.91837205430769,130.670489392195));
#78364=CARTESIAN_POINT('Ctrl Pts',(-20.7351405640086,-4.91824802158451,
130.808772043649));
#78365=CARTESIAN_POINT('',(-20.3898594359439,-4.91824942229388,130.80197679587));
#78366=CARTESIAN_POINT('Ctrl Pts',(-20.320130187517,-4.76405452823408,129.582490119308));
#78367=CARTESIAN_POINT('Ctrl Pts',(-20.3286835810525,-4.80147986759645,
129.728410949473));
#78368=CARTESIAN_POINT('Ctrl Pts',(-20.3372369745881,-4.83224103412311,
129.87622469168));
#78369=CARTESIAN_POINT('Ctrl Pts',(-20.3457903681237,-4.85616156344646,
130.025336913045));
#78370=CARTESIAN_POINT('Ctrl Pts',(-20.3543062507495,-4.87997718928168,
130.173795202721));
#78371=CARTESIAN_POINT('Ctrl Pts',(-20.3628221333753,-4.89701194625247,
130.323540373495));
#78372=CARTESIAN_POINT('Ctrl Pts',(-20.3713380160011,-4.90714008083112,
130.473967988107));
#78373=CARTESIAN_POINT('Ctrl Pts',(-20.3775118226487,-4.9144827307169,130.583024329991));
#78374=CARTESIAN_POINT('Ctrl Pts',(-20.3836856292964,-4.91819633051015,
130.692438974677));
#78375=CARTESIAN_POINT('Ctrl Pts',(-20.389859435944,-4.91824942229388,130.80197679587));
#78376=CARTESIAN_POINT('Ctrl Pts',(-20.3898594359911,-4.91824942229429,
130.801976796707));
#78377=CARTESIAN_POINT('Ctrl Pts',(-20.3977271603077,-4.91831708093587,
130.941568693342));
#78378=CARTESIAN_POINT('Ctrl Pts',(-20.4055948846243,-4.91243745220422,
131.081147358311));
#78379=CARTESIAN_POINT('Ctrl Pts',(-20.413462608941,-4.90064040371127,131.220181126936));
#78380=CARTESIAN_POINT('Ctrl Pts',(-20.4213329011031,-4.88883950493117,
131.359260273007));
#78381=CARTESIAN_POINT('Ctrl Pts',(-20.4292031932653,-4.87111737031541,
131.497793796023));
#78382=CARTESIAN_POINT('Ctrl Pts',(-20.4370734854275,-4.84755570480307,
131.63525576819));
#78383=CARTESIAN_POINT('Ctrl Pts',(-20.4449478339736,-4.82398189550227,
131.772788588877));
#78384=CARTESIAN_POINT('Ctrl Pts',(-20.4528221825198,-4.79456262260292,
131.909248390416));
#78385=CARTESIAN_POINT('Ctrl Pts',(-20.4606965310659,-4.7594305555103,132.044120211106));
#78386=CARTESIAN_POINT('Ctrl Pts',(-20.4685822234648,-4.72424787686653,
132.179186329275));
#78387=CARTESIAN_POINT('Ctrl Pts',(-20.4764679158635,-4.68333605498181,
132.312659533615));
#78388=CARTESIAN_POINT('Ctrl Pts',(-20.4843536082624,-4.63687773177912,
132.444039843217));
#78389=CARTESIAN_POINT('Ctrl Pts',(-20.4922451030626,-4.59038522390083,
132.575516824265));
#78390=CARTESIAN_POINT('Ctrl Pts',(-20.5001365978628,-4.53833821785165,
132.704897494192));
#78391=CARTESIAN_POINT('Ctrl Pts',(-20.508028092663,-4.48096699767772,132.831703170817));
#78392=CARTESIAN_POINT('Ctrl Pts',(-20.5159342962008,-4.4234888448823,132.958745197016));
#78393=CARTESIAN_POINT('Ctrl Pts',(-20.5238404997386,-4.36066681064876,
133.083202302654));
#78394=CARTESIAN_POINT('Ctrl Pts',(-20.5317467032764,-4.29277712002305,
133.204620532722));
#78395=CARTESIAN_POINT('Ctrl Pts',(-20.5393753078754,-4.22727114061728,
133.321775582408));
#78396=CARTESIAN_POINT('Ctrl Pts',(-20.5470039124743,-4.15704756176367,
133.436101329416));
#78397=CARTESIAN_POINT('Ctrl Pts',(-20.5546325170732,-4.08239095982688,
133.547218089916));
#78398=CARTESIAN_POINT('Ctrl Pts',(-20.5624068511923,-4.00630819001947,
133.660457518064));
#78399=CARTESIAN_POINT('Ctrl Pts',(-20.5701811853113,-3.92538970092749,
133.77070827668));
#78400=CARTESIAN_POINT('Ctrl Pts',(-20.5779555194304,-3.83989779120505,
133.877529668497));
#78401=CARTESIAN_POINT('Ctrl Pts',(-20.5857202723775,-3.75451124262072,
133.984219412495));
#78402=CARTESIAN_POINT('Ctrl Pts',(-20.5934850253246,-3.66456272997648,
134.087487896633));
#78403=CARTESIAN_POINT('Ctrl Pts',(-20.6012497782717,-3.57035839697324,
134.186922365659));
#78404=CARTESIAN_POINT('Ctrl Pts',(-20.6090068191567,-3.47624762904158,
134.286258074969));
#78405=CARTESIAN_POINT('Ctrl Pts',(-20.6167638600417,-3.37788971970297,
134.381767065273));
#78406=CARTESIAN_POINT('Ctrl Pts',(-20.6245209009267,-3.275631506201,134.473069014002));
#78407=CARTESIAN_POINT('Ctrl Pts',(-20.6322720921668,-3.17345040641329,
134.564302111222));
#78408=CARTESIAN_POINT('Ctrl Pts',(-20.640023283407,-3.06737514729707,134.651334222326));
#78409=CARTESIAN_POINT('Ctrl Pts',(-20.6477744746471,-2.95778964355184,
134.733821584034));
#78410=CARTESIAN_POINT('Ctrl Pts',(-20.6555223714242,-2.848250716569,134.816273886414));
#78411=CARTESIAN_POINT('Ctrl Pts',(-20.6632702682012,-2.73520482403686,
134.894185046652));
#78412=CARTESIAN_POINT('Ctrl Pts',(-20.6710181649782,-2.61906903376005,
134.967251495177));
#78413=CARTESIAN_POINT('Ctrl Pts',(-20.6787644410624,-2.50295753658696,
135.040302659777));
#78414=CARTESIAN_POINT('Ctrl Pts',(-20.6865107171464,-2.38375775798487,
135.108510920324));
#78415=CARTESIAN_POINT('Ctrl Pts',(-20.6942569932305,-2.26191549134503,
135.171616205749));
#78416=CARTESIAN_POINT('Ctrl Pts',(-20.7020033264959,-2.1400723252936,135.234721957002));
#78417=CARTESIAN_POINT('Ctrl Pts',(-20.7097496597612,-2.01558697944628,
135.29272447816));
#78418=CARTESIAN_POINT('Ctrl Pts',(-20.7174959930266,-1.88892921192834,
135.345410000123));
#78419=CARTESIAN_POINT('Ctrl Pts',(-20.7252440610295,-1.76224308028137,
135.398107320644));
#78420=CARTESIAN_POINT('Ctrl Pts',(-20.7329921290325,-1.63338391979895,
135.445485122478));
#78421=CARTESIAN_POINT('Ctrl Pts',(-20.7407401970354,-1.50284041563251,
135.487378207501));
#78422=CARTESIAN_POINT('Ctrl Pts',(-20.7484964997773,-1.37215816827617,
135.529315816994));
#78423=CARTESIAN_POINT('Ctrl Pts',(-20.7562528025191,-1.23978837409685,
135.56575694552));
#78424=CARTESIAN_POINT('Ctrl Pts',(-20.764009105261,-1.10623433243964,135.596586474538));
#78425=CARTESIAN_POINT('Ctrl Pts',(-20.7717695477751,-0.972609008969159,
135.627432458204));
#78426=CARTESIAN_POINT('Ctrl Pts',(-20.7795299902893,-0.837798562676585,
135.652660802529));
#78427=CARTESIAN_POINT('Ctrl Pts',(-20.7872904328035,-0.702314386431186,
135.672207941087));
#78428=CARTESIAN_POINT('Ctrl Pts',(-20.7950633330689,-0.566612718958359,
135.691786458447));
#78429=CARTESIAN_POINT('Ctrl Pts',(-20.8028362333343,-0.430235549468906,
135.705665505815));
#78430=CARTESIAN_POINT('Ctrl Pts',(-20.8106091335997,-0.293698169259079,
135.713833547308));
#78431=CARTESIAN_POINT('Ctrl Pts',(-20.8180994693619,-0.162124266735123,
135.72170465992));
#78432=CARTESIAN_POINT('Ctrl Pts',(-20.825589805124,-0.0304019073486875,
135.724272770742));
#78433=CARTESIAN_POINT('Ctrl Pts',(-20.8330801408861,0.10101164151941,135.721573213212));
#78434=CARTESIAN_POINT('Ctrl Pts',(-20.8408544750052,0.237407775033773,
135.718771301138));
#78435=CARTESIAN_POINT('Ctrl Pts',(-20.8486288091243,0.373903280619894,
135.71028551259));
#78436=CARTESIAN_POINT('Ctrl Pts',(-20.8564031432434,0.509985608355766,
135.696098319219));
#78437=CARTESIAN_POINT('Ctrl Pts',(-20.8641678961905,0.645900226784547,
135.681928610295));
#78438=CARTESIAN_POINT('Ctrl Pts',(-20.8719326491376,0.781402295404141,
135.662071517282));
#78439=CARTESIAN_POINT('Ctrl Pts',(-20.8796974020847,0.915979073383363,
135.636561503252));
#78440=CARTESIAN_POINT('Ctrl Pts',(-20.8874544429697,1.0504221878095,135.611076826127));
#78441=CARTESIAN_POINT('Ctrl Pts',(-20.8952114838547,1.18394145883076,135.579950473556));
#78442=CARTESIAN_POINT('Ctrl Pts',(-20.9029685247397,1.31602943629607,135.543268675896));
#78443=CARTESIAN_POINT('Ctrl Pts',(-20.9107197159798,1.44801780519044,135.506614540265));
#78444=CARTESIAN_POINT('Ctrl Pts',(-20.9184709072199,1.57857665372421,135.464413402491));
#78445=CARTESIAN_POINT('Ctrl Pts',(-20.9262220984601,1.70720924884263,135.416802448437));
#78446=CARTESIAN_POINT('Ctrl Pts',(-20.9339699952372,1.83578717167639,135.369211730308));
#78447=CARTESIAN_POINT('Ctrl Pts',(-20.9417178920143,1.96244010355671,135.316215904489));
#78448=CARTESIAN_POINT('Ctrl Pts',(-20.9494657887914,2.08668720746943,135.258001775168));
#78449=CARTESIAN_POINT('Ctrl Pts',(-20.9572120648755,2.21090832156646,135.199799822987));
#78450=CARTESIAN_POINT('Ctrl Pts',(-20.9649583409596,2.33272425487457,135.136381904241));
#78451=CARTESIAN_POINT('Ctrl Pts',(-20.9727046170437,2.45167524001829,135.067982502769));
#78452=CARTESIAN_POINT('Ctrl Pts',(-20.9804509503091,2.57062710323117,134.999582596388));
#78453=CARTESIAN_POINT('Ctrl Pts',(-20.9881972835744,2.68671363715254,134.926201328794));
#78454=CARTESIAN_POINT('Ctrl Pts',(-20.9959436168398,2.79950107604371,134.848118373383));
#78455=CARTESIAN_POINT('Ctrl Pts',(-21.0036916848427,2.91231377289981,134.770017931836));
#78456=CARTESIAN_POINT('Ctrl Pts',(-21.0114397528457,3.02182558319254,134.687213929799));
#78457=CARTESIAN_POINT('Ctrl Pts',(-21.0191878208487,3.12763337480069,134.600028218309));
#78458=CARTESIAN_POINT('Ctrl Pts',(-21.0269441235906,3.23355362018904,134.512749844808));
#78459=CARTESIAN_POINT('Ctrl Pts',(-21.0347004263324,3.33576168075101,134.42108070815));
#78460=CARTESIAN_POINT('Ctrl Pts',(-21.0424567290743,3.43388865840592,134.325382023944));
#78461=CARTESIAN_POINT('Ctrl Pts',(-21.0502171715884,3.53206800938322,134.229632262468));
#78462=CARTESIAN_POINT('Ctrl Pts',(-21.0579776141026,3.62616166911746,134.129848952317));
#78463=CARTESIAN_POINT('Ctrl Pts',(-21.0657380566168,3.71583973703538,134.026427983586));
#78464=CARTESIAN_POINT('Ctrl Pts',(-21.0735109568822,3.80566176414928,133.922840994334));
#78465=CARTESIAN_POINT('Ctrl Pts',(-21.0812838571477,3.89105379108128,133.815604983357));
#78466=CARTESIAN_POINT('Ctrl Pts',(-21.0890567574131,3.97172758483533,133.70514724439));
#78467=CARTESIAN_POINT('Ctrl Pts',(-21.096547093175,4.04946868298019,133.598704922461));
#78468=CARTESIAN_POINT('Ctrl Pts',(-21.104037428937,4.12282846009108,133.48927129757));
#78469=CARTESIAN_POINT('Ctrl Pts',(-21.1115277646989,4.19158947900152,133.3772501803));
#78470=CARTESIAN_POINT('Ctrl Pts',(-21.119302098818,4.26295759284442,133.260981748318));
#78471=CARTESIAN_POINT('Ctrl Pts',(-21.1270764329371,4.3295974134669,133.141557437729));
#78472=CARTESIAN_POINT('Ctrl Pts',(-21.1348507670562,4.39121714801795,133.019398996794));
#78473=CARTESIAN_POINT('Ctrl Pts',(-21.1426155200032,4.45276094175319,132.89739110522));
#78474=CARTESIAN_POINT('Ctrl Pts',(-21.1503802729504,4.50929678493063,132.772656133463));
#78475=CARTESIAN_POINT('Ctrl Pts',(-21.1581450258975,4.56057652336387,132.645644093037));
#78476=CARTESIAN_POINT('Ctrl Pts',(-21.1659020667825,4.61180533003799,132.51875820276));
#78477=CARTESIAN_POINT('Ctrl Pts',(-21.1736591076675,4.65778827545224,132.389600104719));
#78478=CARTESIAN_POINT('Ctrl Pts',(-21.1814161485524,4.69832361844659,132.258643340714));
#78479=CARTESIAN_POINT('Ctrl Pts',(-21.1891673397926,4.73882839342353,132.127785332223));
#78480=CARTESIAN_POINT('Ctrl Pts',(-21.1969185310327,4.77389362772621,131.995131729547));
#78481=CARTESIAN_POINT('Ctrl Pts',(-21.2046697222728,4.80336624335519,131.861174600581));
#78482=CARTESIAN_POINT('Ctrl Pts',(-21.2124176190499,4.83282633233631,131.727274406968));
#78483=CARTESIAN_POINT('Ctrl Pts',(-21.220165515827,4.85669844650645,131.59207217003));
#78484=CARTESIAN_POINT('Ctrl Pts',(-21.2279134126041,4.87487984536769,131.45607340379));
#78485=CARTESIAN_POINT('Ctrl Pts',(-21.2356596886882,4.89305744107224,131.32010308556));
#78486=CARTESIAN_POINT('Ctrl Pts',(-21.2434059647723,4.90554663741534,131.183336956711));
#78487=CARTESIAN_POINT('Ctrl Pts',(-21.2511522408564,4.9122961967945,131.046288576798));
#78488=CARTESIAN_POINT('Ctrl Pts',(-21.2588985741217,4.91904580599737,130.909239185226));
#78489=CARTESIAN_POINT('Ctrl Pts',(-21.2666449073871,4.92005567446114,130.771907928925));
#78490=CARTESIAN_POINT('Ctrl Pts',(-21.2743912406524,4.91532663835688,130.634810917598));
#78491=CARTESIAN_POINT('Ctrl Pts',(-21.2821393086554,4.91059654321776,130.497683204345));
#78492=CARTESIAN_POINT('Ctrl Pts',(-21.2898873766584,4.90012499961088,130.360790231109));
#78493=CARTESIAN_POINT('Ctrl Pts',(-21.2976354446614,4.88396488717058,130.224645132707));
#78494=CARTESIAN_POINT('Ctrl Pts',(-21.3053917474032,4.86778759957049,130.088355337675));
#78495=CARTESIAN_POINT('Ctrl Pts',(-21.3131480501451,4.8459097119998,129.952815394135));
#78496=CARTESIAN_POINT('Ctrl Pts',(-21.320904352887,4.81843572695672,129.81853091235));
#78497=CARTESIAN_POINT('Ctrl Pts',(-21.3286647954012,4.7909470782206,129.684174758893));
#78498=CARTESIAN_POINT('Ctrl Pts',(-21.3364252379153,4.75785647483153,129.551075781608));
#78499=CARTESIAN_POINT('Ctrl Pts',(-21.3441856804295,4.71931867102253,129.419725523457));
#78500=CARTESIAN_POINT('Ctrl Pts',(-21.3519585806949,4.68071900290958,129.288164410211));
#78501=CARTESIAN_POINT('Ctrl Pts',(-21.3597314809604,4.63665478616584,129.158357996207));
#78502=CARTESIAN_POINT('Ctrl Pts',(-21.3675043812258,4.58732971813785,129.030779742728));
#78503=CARTESIAN_POINT('Ctrl Pts',(-21.3749947169879,4.53979774057481,128.907839280114));
#78504=CARTESIAN_POINT('Ctrl Pts',(-21.3824850527499,4.48738088407196,128.786968074653));
#78505=CARTESIAN_POINT('Ctrl Pts',(-21.389975388512,4.43030135581073,128.668567331875));
#78506=CARTESIAN_POINT('Ctrl Pts',(-21.3977497226311,4.37105763988686,128.545677388949));
#78507=CARTESIAN_POINT('Ctrl Pts',(-21.4055240567502,4.30660303593,128.425059663547));
#78508=CARTESIAN_POINT('Ctrl Pts',(-21.4132983908692,4.23713465153532,128.307187614497));
#78509=CARTESIAN_POINT('Ctrl Pts',(-21.4210631438163,4.16775188071584,128.189460832212));
#78510=CARTESIAN_POINT('Ctrl Pts',(-21.4288278967634,4.09336782050057,128.074473327113));
#78511=CARTESIAN_POINT('Ctrl Pts',(-21.4365926497105,4.01422694492218,127.962677120559));
#78512=CARTESIAN_POINT('Ctrl Pts',(-21.4443496905955,3.93516467317721,127.850991951574));
#78513=CARTESIAN_POINT('Ctrl Pts',(-21.4521067314806,3.85135521254061,127.74249209044));
#78514=CARTESIAN_POINT('Ctrl Pts',(-21.4598637723656,3.76308792111388,127.637603228616));
#78515=CARTESIAN_POINT('Ctrl Pts',(-21.4676149636057,3.67488719273787,127.532793464299));
#78516=CARTESIAN_POINT('Ctrl Pts',(-21.4753661548458,3.58223557551724,127.43158957709));
#78517=CARTESIAN_POINT('Ctrl Pts',(-21.4831173460859,3.48546431771102,127.334386330563));
#78518=CARTESIAN_POINT('Ctrl Pts',(-21.490865242863,3.38873419027122,127.237224398008));
#78519=CARTESIAN_POINT('Ctrl Pts',(-21.4986131396401,3.28788818002643,127.144060000701));
#78520=CARTESIAN_POINT('Ctrl Pts',(-21.5063610364172,3.18329605649346,127.055252819808));
#78521=CARTESIAN_POINT('Ctrl Pts',(-21.5141073125013,3.07872581137784,126.966464215462));
#78522=CARTESIAN_POINT('Ctrl Pts',(-21.5218535885854,2.97041130944767,126.882031267525));
#78523=CARTESIAN_POINT('Ctrl Pts',(-21.5295998646695,2.858756927727,126.802274675126));
#78524=CARTESIAN_POINT('Ctrl Pts',(-21.5373461979348,2.7471017217992,126.722517493983));
#78525=CARTESIAN_POINT('Ctrl Pts',(-21.5450925312002,2.632106905022,126.64743696451));
#78526=CARTESIAN_POINT('Ctrl Pts',(-21.5528388644655,2.51420714707588,126.577311353115));
#78527=CARTESIAN_POINT('Ctrl Pts',(-21.5605869324685,2.39628098629643,126.507170037576));
#78528=CARTESIAN_POINT('Ctrl Pts',(-21.5683350004714,2.27544892580137,126.441986047951));
#78529=CARTESIAN_POINT('Ctrl Pts',(-21.5760830684744,2.15217126317994,126.38199225701));
#78530=CARTESIAN_POINT('Ctrl Pts',(-21.5838393712163,2.02876257959166,126.321934703955));
#78531=CARTESIAN_POINT('Ctrl Pts',(-21.5915956739581,1.90290345377174,126.267078540152));
#78532=CARTESIAN_POINT('Ctrl Pts',(-21.5993519767,1.77507575610665,126.217609139386));
#78533=CARTESIAN_POINT('Ctrl Pts',(-21.6071124192141,1.64717983295033,126.168113335313));
#78534=CARTESIAN_POINT('Ctrl Pts',(-21.6148728617283,1.51731361438653,126.124010148772));
#78535=CARTESIAN_POINT('Ctrl Pts',(-21.6226333042425,1.38597429787458,126.085435071625));
#78536=CARTESIAN_POINT('Ctrl Pts',(-21.6304062045079,1.25442414383201,126.04679807034));
#78537=CARTESIAN_POINT('Ctrl Pts',(-21.6381791047734,1.12139654594342,126.013707006383));
#78538=CARTESIAN_POINT('Ctrl Pts',(-21.6459520050388,0.987399943987629,
125.986246420796));
#78539=CARTESIAN_POINT('Ctrl Pts',(-21.6534423408008,0.858274456030554,
125.959784096665));
#78540=CARTESIAN_POINT('Ctrl Pts',(-21.6609326765628,0.728249496334088,
125.938550043569));
#78541=CARTESIAN_POINT('Ctrl Pts',(-21.6684230123248,0.597782718883282,
125.922574173701));
#78542=CARTESIAN_POINT('Ctrl Pts',(-21.6761973464439,0.462369253910339,
125.905992573872));
#78543=CARTESIAN_POINT('Ctrl Pts',(-21.683971680563,0.326050857628112,125.895023230798));
#78544=CARTESIAN_POINT('Ctrl Pts',(-21.6917460146821,0.189332405827244,
125.88975622834));
#78545=CARTESIAN_POINT('Ctrl Pts',(-21.6995107676292,0.052782447299527,
125.884495716991));
#78546=CARTESIAN_POINT('Ctrl Pts',(-21.7072755205762,-0.0841661988337974,
125.884923578284));
#78547=CARTESIAN_POINT('Ctrl Pts',(-21.7150402735233,-0.221001090013797,
125.891078457878));
#78548=CARTESIAN_POINT('Ctrl Pts',(-21.7227973144083,-0.357700074850843,
125.897227224358));
#78549=CARTESIAN_POINT('Ctrl Pts',(-21.7305543552934,-0.494285141532955,
125.909091671999));
#78550=CARTESIAN_POINT('Ctrl Pts',(-21.7383113961784,-0.630241738656434,
125.926658452268));
#78551=CARTESIAN_POINT('Ctrl Pts',(-21.7460625874186,-0.766095809853174,
125.944211985291));
#78552=CARTESIAN_POINT('Ctrl Pts',(-21.7538137786586,-0.901321968654677,
125.96745924181));
#78553=CARTESIAN_POINT('Ctrl Pts',(-21.7615649698988,-1.03540904151109,
125.996334912637));
#78554=CARTESIAN_POINT('Ctrl Pts',(-21.7693128666759,-1.16943912378393,
126.025198310534));
#78555=CARTESIAN_POINT('Ctrl Pts',(-21.777060763453,-1.30233070163004,126.059685282648));
#78556=CARTESIAN_POINT('Ctrl Pts',(-21.7848086602301,-1.43358129563961,
126.099679147871));
#78557=CARTESIAN_POINT('Ctrl Pts',(-21.7925549363142,-1.5648044348547,126.139664647239));
#78558=CARTESIAN_POINT('Ctrl Pts',(-21.8003012123983,-1.69438689924198,
126.18515463459));
#78559=CARTESIAN_POINT('Ctrl Pts',(-21.8080474884824,-1.82184029988104,
126.235982241793));
#78560=CARTESIAN_POINT('Ctrl Pts',(-21.8157938217477,-1.94929464135147,
126.286810224194));
#78561=CARTESIAN_POINT('Ctrl Pts',(-21.8235401550131,-2.07461952456006,
126.342975760247));
#78562=CARTESIAN_POINT('Ctrl Pts',(-21.8312864882784,-2.19734588651852,
126.40426355983));
#78563=CARTESIAN_POINT('Ctrl Pts',(-21.8390345562814,-2.32009973219481,
126.46556508439));
#78564=CARTESIAN_POINT('Ctrl Pts',(-21.8467826242843,-2.44025354895704,
126.531990980426));
#78565=CARTESIAN_POINT('Ctrl Pts',(-21.8545306922873,-2.55736261225882,
126.603279859961));
#78566=CARTESIAN_POINT('Ctrl Pts',(-21.8622869950291,-2.67459614046701,
126.674644506165));
#78567=CARTESIAN_POINT('Ctrl Pts',(-21.870043297771,-2.78877811646778,126.750882256761));
#78568=CARTESIAN_POINT('Ctrl Pts',(-21.8777996005128,-2.89949211733087,
126.831687899604));
#78569=CARTESIAN_POINT('Ctrl Pts',(-21.885560043027,-3.01026520958991,126.912536670852));
#78570=CARTESIAN_POINT('Ctrl Pts',(-21.8933204855411,-3.11756633278576,
126.997957948927));
#78571=CARTESIAN_POINT('Ctrl Pts',(-21.9010809280553,-3.22101274640848,
127.087606664185));
#78572=CARTESIAN_POINT('Ctrl Pts',(-21.9088538283207,-3.32462522139788,
127.177399291519));
#78573=CARTESIAN_POINT('Ctrl Pts',(-21.9166267285861,-3.42437033673121,
127.271432648797));
#78574=CARTESIAN_POINT('Ctrl Pts',(-21.9243996288516,-3.51990214151541,
127.369324667732));
#78575=CARTESIAN_POINT('Ctrl Pts',(-21.9318899646136,-3.61196112456562,
127.463658065203));
#78576=CARTESIAN_POINT('Ctrl Pts',(-21.9393803003756,-3.70010760156797,
127.561574221925));
#78577=CARTESIAN_POINT('Ctrl Pts',(-21.9468706361377,-3.78406903338846,
127.66270426891));
#78578=CARTESIAN_POINT('Ctrl Pts',(-21.9546076688493,-3.87079576569405,
127.767165071004));
#78579=CARTESIAN_POINT('Ctrl Pts',(-21.962344701561,-3.95334046479952,127.875396627304));
#78580=CARTESIAN_POINT('Ctrl Pts',(-21.9700817342727,-4.03135472329717,
127.987028163373));
#78581=CARTESIAN_POINT('Ctrl Pts',(-21.9778092501755,-4.10927302164879,
128.098522388921));
#78582=CARTESIAN_POINT('Ctrl Pts',(-21.9855367660781,-4.18267173935463,
128.213407955476));
#78583=CARTESIAN_POINT('Ctrl Pts',(-21.9932642819809,-4.25124137468817,
128.331279576306));
#78584=CARTESIAN_POINT('Ctrl Pts',(-22.0009824375401,-4.31972795159038,
128.449008419187));
#78585=CARTESIAN_POINT('Ctrl Pts',(-22.0087005930991,-4.38339689614496,
128.569715775096));
#78586=CARTESIAN_POINT('Ctrl Pts',(-22.0164187486583,-4.44198128320627,
128.692966447321));
#78587=CARTESIAN_POINT('Ctrl Pts',(-22.0241315180154,-4.50052478649122,
128.816131107672));
#78588=CARTESIAN_POINT('Ctrl Pts',(-22.0318442873726,-4.55399062093118,
128.941835199043));
#78589=CARTESIAN_POINT('Ctrl Pts',(-22.0395570567297,-4.60215720039006,
129.069617937686));
#78590=CARTESIAN_POINT('Ctrl Pts',(-22.0472658083821,-4.65029868910855,
129.197334112259));
#78591=CARTESIAN_POINT('Ctrl Pts',(-22.0549745600344,-4.69314627838737,
129.327126410124));
#78592=CARTESIAN_POINT('Ctrl Pts',(-22.0626833116868,-4.73052625149337,
129.458513506475));
#78593=CARTESIAN_POINT('Ctrl Pts',(-22.0650990812068,-4.74224039196137,
129.499687610532));
#78594=CARTESIAN_POINT('Ctrl Pts',(-22.0675148507268,-4.75341793402174,
129.541018199907));
#78595=CARTESIAN_POINT('Ctrl Pts',(-22.0699306202468,-4.76405452823405,
129.582490119308));
#78596=CARTESIAN_POINT('Origin',(213.235140564004,0.,130.804360617566));
#78597=CARTESIAN_POINT('',(-24.1652761364937,-4.76405452823408,129.582490119308));
#78598=CARTESIAN_POINT('',(-23.8197459990105,-4.76405452823405,129.582490119308));
#78599=CARTESIAN_POINT('',(213.235140564004,-4.76405452823405,129.582490119308));
#78600=CARTESIAN_POINT('',(-22.4851405640465,-4.91824999885107,130.804254309485));
#78601=CARTESIAN_POINT('Ctrl Pts',(-22.4851405640464,-4.91824999885107,
130.804254309485));
#78602=CARTESIAN_POINT('Ctrl Pts',(-22.4929100480016,-4.91825294584514,
130.940594401862));
#78603=CARTESIAN_POINT('Ctrl Pts',(-22.5006795319569,-4.91258231712604,
131.077151886514));
#78604=CARTESIAN_POINT('Ctrl Pts',(-22.5084490159121,-4.90120978706623,
131.213415241872));
#78605=CARTESIAN_POINT('Ctrl Pts',(-22.516208922518,-4.88985127578729,131.349510627033));
#78606=CARTESIAN_POINT('Ctrl Pts',(-22.523968829124,-4.87280488002072,131.485312217893));
#78607=CARTESIAN_POINT('Ctrl Pts',(-22.5317287357299,-4.85009425012328,
131.620307201247));
#78608=CARTESIAN_POINT('Ctrl Pts',(-22.5394809393304,-4.82740616432516,
131.755168179498));
#78609=CARTESIAN_POINT('Ctrl Pts',(-22.547233142931,-4.79906509809244,131.889223760036));
#78610=CARTESIAN_POINT('Ctrl Pts',(-22.5549853465315,-4.76514656917072,
132.021965330443));
#78611=CARTESIAN_POINT('Ctrl Pts',(-22.5627317147411,-4.73125357206994,
132.15460698101));
#78612=CARTESIAN_POINT('Ctrl Pts',(-22.5704780829507,-4.69179156525008,
132.285936212367));
#78613=CARTESIAN_POINT('Ctrl Pts',(-22.5782244511603,-4.64688723496165,
132.41545406242));
#78614=CARTESIAN_POINT('Ctrl Pts',(-22.5859675484736,-4.60200186548225,
132.544917223689));
#78615=CARTESIAN_POINT('Ctrl Pts',(-22.5937106457868,-4.55167887093173,
132.672570155688));
#78616=CARTESIAN_POINT('Ctrl Pts',(-22.6014537431001,-4.49609487543769,
132.797928758755));
#78617=CARTESIAN_POINT('Ctrl Pts',(-22.6091952422889,-4.44052235211583,
132.923261488628));
#78618=CARTESIAN_POINT('Ctrl Pts',(-22.6169367414778,-4.37969114618855,
133.046300473741));
#78619=CARTESIAN_POINT('Ctrl Pts',(-22.6246782406666,-4.31382598535281,
133.166581697523));
#78620=CARTESIAN_POINT('Ctrl Pts',(-22.6324198242689,-4.2479601063212,133.286864232856));
#78621=CARTESIAN_POINT('Ctrl Pts',(-22.6401614078713,-4.17706035102051,
133.404388603519));
#78622=CARTESIAN_POINT('Ctrl Pts',(-22.6479029914736,-4.10139715885603,
133.518715864734));
#78623=CARTESIAN_POINT('Ctrl Pts',(-22.6556463417301,-4.02571670010955,
133.633069215795));
#78624=CARTESIAN_POINT('Ctrl Pts',(-22.6633896919866,-3.94527085754286,
133.744223679236));
#78625=CARTESIAN_POINT('Ctrl Pts',(-22.671133042243,-3.86037286112385,133.851770080634));
#78626=CARTESIAN_POINT('Ctrl Pts',(-22.6788846293804,-3.77538455564472,
133.959430883018));
#78627=CARTESIAN_POINT('Ctrl Pts',(-22.6866362165177,-3.68593487914394,
134.063475649012));
#78628=CARTESIAN_POINT('Ctrl Pts',(-22.694387803655,-3.59237710244734,134.16352864199));
#78629=CARTESIAN_POINT('Ctrl Pts',(-22.7021435681625,-3.49876890698442,
134.26363555404));
#78630=CARTESIAN_POINT('Ctrl Pts',(-22.7098993326699,-3.40104847917913,
134.359746132506));
#78631=CARTESIAN_POINT('Ctrl Pts',(-22.7176550971774,-3.29960453595577,
134.451522934875));
#78632=CARTESIAN_POINT('Ctrl Pts',(-22.7254232328219,-3.19799878058225,
134.543446129442));
#78633=CARTESIAN_POINT('Ctrl Pts',(-22.7331913684666,-3.09265794297792,
134.631021484481));
#78634=CARTESIAN_POINT('Ctrl Pts',(-22.7409595041112,-2.98400294132002,
134.713952605062));
#78635=CARTESIAN_POINT('Ctrl Pts',(-22.7481811732131,-2.88299151410723,
134.791049754042));
#78636=CARTESIAN_POINT('Ctrl Pts',(-22.7554028423149,-2.77911632718114,
134.864133413423));
#78637=CARTESIAN_POINT('Ctrl Pts',(-22.7626245114168,-2.67273522412218,
134.933000767087));
#78638=CARTESIAN_POINT('Ctrl Pts',(-22.7703988455359,-2.55821291252541,
135.007138450457));
#78639=CARTESIAN_POINT('Ctrl Pts',(-22.778173179655,-2.44042216513535,135.076624934622));
#78640=CARTESIAN_POINT('Ctrl Pts',(-22.7859475137741,-2.31977760653852,
135.141158389967));
#78641=CARTESIAN_POINT('Ctrl Pts',(-22.7937122667212,-2.19928173157784,
135.205612313595));
#78642=CARTESIAN_POINT('Ctrl Pts',(-22.8014770196682,-2.07593938476042,
135.265125171237));
#78643=CARTESIAN_POINT('Ctrl Pts',(-22.8092417726153,-1.95019449299208,
135.319438081132));
#78644=CARTESIAN_POINT('Ctrl Pts',(-22.8169988135003,-1.8245744928231,135.37369704668));
#78645=CARTESIAN_POINT('Ctrl Pts',(-22.8247558543854,-1.69655705302487,
135.422766188367));
#78646=CARTESIAN_POINT('Ctrl Pts',(-22.8325128952704,-1.56661073779577,
135.466432459432));
#78647=CARTESIAN_POINT('Ctrl Pts',(-22.8402640865106,-1.43676241609329,
135.510065801424));
#78648=CARTESIAN_POINT('Ctrl Pts',(-22.8480152777506,-1.30498848331449,
135.548304258503));
#78649=CARTESIAN_POINT('Ctrl Pts',(-22.8557664689908,-1.17177719220194,
135.580982988482));
#78650=CARTESIAN_POINT('Ctrl Pts',(-22.8635143657679,-1.03862251944218,
135.613647829129));
#78651=CARTESIAN_POINT('Ctrl Pts',(-22.871262262545,-0.904032082325198,
135.640757549613));
#78652=CARTESIAN_POINT('Ctrl Pts',(-22.8790101593221,-0.768508783811016,
135.66219730808));
#78653=CARTESIAN_POINT('Ctrl Pts',(-22.8867564354062,-0.63301383384934,
135.683632581812));
#78654=CARTESIAN_POINT('Ctrl Pts',(-22.8945027114902,-0.496586796541796,
135.699400191562));
#78655=CARTESIAN_POINT('Ctrl Pts',(-22.9022489875743,-0.359739853991382,
135.709436590469));
#78656=CARTESIAN_POINT('Ctrl Pts',(-22.9099953208397,-0.22289190126774,
135.719473063462));
#78657=CARTESIAN_POINT('Ctrl Pts',(-22.9177416541051,-0.0856244270340815,
135.723778212596));
#78658=CARTESIAN_POINT('Ctrl Pts',(-22.9254879873704,0.0515465875682617,
135.722340488591));
#78659=CARTESIAN_POINT('Ctrl Pts',(-22.9332360553734,0.188748320668248,
135.720902442618));
#78660=CARTESIAN_POINT('Ctrl Pts',(-22.9409841233763,0.325853160283593,
135.713718968459));
#78661=CARTESIAN_POINT('Ctrl Pts',(-22.9487321913793,0.462346850400912,
135.700830616701));
#78662=CARTESIAN_POINT('Ctrl Pts',(-22.9564884941211,0.598985607636197,
135.687928567048));
#78663=CARTESIAN_POINT('Ctrl Pts',(-22.9642447968631,0.735011527998921,
135.669309564689));
#78664=CARTESIAN_POINT('Ctrl Pts',(-22.9720010996049,0.869916639057891,
135.645065948774));
#78665=CARTESIAN_POINT('Ctrl Pts',(-22.9797615421191,1.00489375303692,135.620809393312));
#78666=CARTESIAN_POINT('Ctrl Pts',(-22.9875219846333,1.13874848434594,135.59092232766));
#78667=CARTESIAN_POINT('Ctrl Pts',(-22.9952824271475,1.27098571789894,135.55554766581));
#78668=CARTESIAN_POINT('Ctrl Pts',(-23.0030553274129,1.40343523039835,135.520116217411));
#78669=CARTESIAN_POINT('Ctrl Pts',(-23.0108282276783,1.53426168306555,135.479179686094));
#78670=CARTESIAN_POINT('Ctrl Pts',(-23.0186011279437,1.66298686278692,135.432930348779));
#78671=CARTESIAN_POINT('Ctrl Pts',(-23.0260914637057,1.78703255798572,135.38836229137));
#78672=CARTESIAN_POINT('Ctrl Pts',(-23.0335817994677,1.9091268155518,135.33886110528));
#78673=CARTESIAN_POINT('Ctrl Pts',(-23.0410721352297,2.02886321313201,135.284639305873));
#78674=CARTESIAN_POINT('Ctrl Pts',(-23.0488464693488,2.15313945262027,135.228361670461));
#78675=CARTESIAN_POINT('Ctrl Pts',(-23.0566208034678,2.27526917587172,135.166820120668));
#78676=CARTESIAN_POINT('Ctrl Pts',(-23.0643951375869,2.39477433036429,135.10020034562));
#78677=CARTESIAN_POINT('Ctrl Pts',(-23.072159890534,2.51413220543427,135.033662673491));
#78678=CARTESIAN_POINT('Ctrl Pts',(-23.0799246434811,2.63087160931883,134.962059417115));
#78679=CARTESIAN_POINT('Ctrl Pts',(-23.0876893964281,2.74453478412558,134.885624132854));
#78680=CARTESIAN_POINT('Ctrl Pts',(-23.0954464373132,2.85808506706504,134.809264765196));
#78681=CARTESIAN_POINT('Ctrl Pts',(-23.1032034781982,2.9685648788877,134.728083137114));
#78682=CARTESIAN_POINT('Ctrl Pts',(-23.1109605190832,3.07554170692518,134.642358307959));
#78683=CARTESIAN_POINT('Ctrl Pts',(-23.1187117103234,3.18243786290462,134.556698124565));
#78684=CARTESIAN_POINT('Ctrl Pts',(-23.1264629015635,3.28583598923935,134.466501802965));
#78685=CARTESIAN_POINT('Ctrl Pts',(-23.1342140928037,3.38533348699316,134.372091022788));
#78686=CARTESIAN_POINT('Ctrl Pts',(-23.1419619895808,3.48478869565584,134.277720369711));
#78687=CARTESIAN_POINT('Ctrl Pts',(-23.1497098863579,3.58034629010211,134.179139089279));
#78688=CARTESIAN_POINT('Ctrl Pts',(-23.157457783135,3.67163781929383,134.076708213166));
#78689=CARTESIAN_POINT('Ctrl Pts',(-23.1652040592191,3.76291025226577,133.974298763385));
#78690=CARTESIAN_POINT('Ctrl Pts',(-23.1729503353032,3.84991813499068,133.868041611299));
#78691=CARTESIAN_POINT('Ctrl Pts',(-23.1806966113873,3.93233115675755,133.758333321586));
#78692=CARTESIAN_POINT('Ctrl Pts',(-23.1884429446526,4.0147447868785,133.648624222031));
#78693=CARTESIAN_POINT('Ctrl Pts',(-23.196189277918,4.09256325354067,133.535464246608));
#78694=CARTESIAN_POINT('Ctrl Pts',(-23.2039356111833,4.16549793959766,133.419281262195));
#78695=CARTESIAN_POINT('Ctrl Pts',(-23.2116836791863,4.2384489588721,133.303072259408));
#78696=CARTESIAN_POINT('Ctrl Pts',(-23.2194317471893,4.3065138133998,133.18383923158));
#78697=CARTESIAN_POINT('Ctrl Pts',(-23.2271798151923,4.36944865160021,133.062036755441));
#78698=CARTESIAN_POINT('Ctrl Pts',(-23.2349361179341,4.43245037769543,132.940104826181));
#78699=CARTESIAN_POINT('Ctrl Pts',(-23.242692420676,4.49031101626684,132.815598341356));
#78700=CARTESIAN_POINT('Ctrl Pts',(-23.2504487234178,4.54283368335113,132.688994584126));
#78701=CARTESIAN_POINT('Ctrl Pts',(-23.258209165932,4.59538438336426,132.562323254658));
#78702=CARTESIAN_POINT('Ctrl Pts',(-23.2659696084462,4.64259130044129,132.433552789228));
#78703=CARTESIAN_POINT('Ctrl Pts',(-23.2737300509604,4.68430705037323,132.303176990683));
#78704=CARTESIAN_POINT('Ctrl Pts',(-23.2815029512258,4.72608976613036,132.172591901332));
#78705=CARTESIAN_POINT('Ctrl Pts',(-23.2892758514912,4.76236359623064,132.040396706397));
#78706=CARTESIAN_POINT('Ctrl Pts',(-23.2970487517566,4.79303182282468,131.907097670489));
#78707=CARTESIAN_POINT('Ctrl Pts',(-23.3045390875186,4.82258518213326,131.778644390297));
#78708=CARTESIAN_POINT('Ctrl Pts',(-23.3120294232806,4.84693336086172,131.649166433302));
#78709=CARTESIAN_POINT('Ctrl Pts',(-23.3195197590426,4.86603547299593,131.519120603887));
#78710=CARTESIAN_POINT('Ctrl Pts',(-23.3272940931617,4.88586184751777,131.384144047322));
#78711=CARTESIAN_POINT('Ctrl Pts',(-23.3350684272807,4.9000992973312,131.248128141357));
#78712=CARTESIAN_POINT('Ctrl Pts',(-23.3428427613998,4.9086456488922,131.111575454629));
#78713=CARTESIAN_POINT('Ctrl Pts',(-23.3506075143469,4.91718146783871,130.975191056883));
#78714=CARTESIAN_POINT('Ctrl Pts',(-23.3583722672941,4.9200401196576,130.838271581084));
#78715=CARTESIAN_POINT('Ctrl Pts',(-23.3661370202412,4.91717067261028,130.701328394833));
#78716=CARTESIAN_POINT('Ctrl Pts',(-23.3738940611262,4.91430407553822,130.564521222484));
#78717=CARTESIAN_POINT('Ctrl Pts',(-23.3816511020111,4.90572070955883,130.427690774897));
#78718=CARTESIAN_POINT('Ctrl Pts',(-23.3894081428961,4.89142157154652,130.291351775625));
#78719=CARTESIAN_POINT('Ctrl Pts',(-23.3971593341362,4.87713321662544,130.155115590653));
#78720=CARTESIAN_POINT('Ctrl Pts',(-23.4049105253764,4.85713770969391,130.019370503589));
#78721=CARTESIAN_POINT('Ctrl Pts',(-23.4126617166165,4.83148807437643,129.884629108016));
#78722=CARTESIAN_POINT('Ctrl Pts',(-23.4204096133935,4.80584934083815,129.749944981131));
#78723=CARTESIAN_POINT('Ctrl Pts',(-23.4281575101706,4.77456133156568,129.616264080537));
#78724=CARTESIAN_POINT('Ctrl Pts',(-23.4359054069477,4.73772863594695,129.484091540965));
#78725=CARTESIAN_POINT('Ctrl Pts',(-23.4436516830318,4.70090364493413,129.35194664904));
#78726=CARTESIAN_POINT('Ctrl Pts',(-23.4513979591159,4.65853637942354,129.221309866934));
#78727=CARTESIAN_POINT('Ctrl Pts',(-23.4591442352,4.61078193950301,129.0926734473));
#78728=CARTESIAN_POINT('Ctrl Pts',(-23.4668905684654,4.56302714706993,128.964036078101));
#78729=CARTESIAN_POINT('Ctrl Pts',(-23.4746369017308,4.50988523694162,128.837399467362));
#78730=CARTESIAN_POINT('Ctrl Pts',(-23.4823832349961,4.45156018102447,128.713237709362));
#78731=CARTESIAN_POINT('Ctrl Pts',(-23.4901313029991,4.39322206361529,128.589048146196));
#78732=CARTESIAN_POINT('Ctrl Pts',(-23.4978793710021,4.32969865689708,128.467334892415));
#78733=CARTESIAN_POINT('Ctrl Pts',(-23.5056274390051,4.26124060141183,128.348548817085));
#78734=CARTESIAN_POINT('Ctrl Pts',(-23.513383741747,4.19270978789084,128.229636494502));
#78735=CARTESIAN_POINT('Ctrl Pts',(-23.5211400444888,4.11923404447307,128.113657904285));
#78736=CARTESIAN_POINT('Ctrl Pts',(-23.5288963472307,4.04110850240705,128.001036673696));
#78737=CARTESIAN_POINT('Ctrl Pts',(-23.5366567897449,3.96294126238692,127.888355333766));
#78738=CARTESIAN_POINT('Ctrl Pts',(-23.5444172322591,3.88011951462452,127.779035235501));
#78739=CARTESIAN_POINT('Ctrl Pts',(-23.5521776747732,3.79297904467585,127.673467289912));
#78740=CARTESIAN_POINT('Ctrl Pts',(-23.5599505750387,3.70569868910885,127.567729877285));
#78741=CARTESIAN_POINT('Ctrl Pts',(-23.5677234753041,3.61408601885497,127.465756944784));
#78742=CARTESIAN_POINT('Ctrl Pts',(-23.5754963755695,3.51851469030773,127.367903512263));
#78743=CARTESIAN_POINT('Ctrl Pts',(-23.5829867113315,3.42641762028361,127.273607298493));
#78744=CARTESIAN_POINT('Ctrl Pts',(-23.5904770470935,3.33064493339792,127.183136487722));
#78745=CARTESIAN_POINT('Ctrl Pts',(-23.5979673828554,3.23155885222512,127.096772392438));
#78746=CARTESIAN_POINT('Ctrl Pts',(-23.6057417169745,3.12871589216721,127.007133776232));
#78747=CARTESIAN_POINT('Ctrl Pts',(-23.6135160510936,3.02197754770216,126.921635486931));
#78748=CARTESIAN_POINT('Ctrl Pts',(-23.6212903852127,2.91171141675949,126.840635136656));
#78749=CARTESIAN_POINT('Ctrl Pts',(-23.6290551381598,2.8015811789686,126.759734612074));
#78750=CARTESIAN_POINT('Ctrl Pts',(-23.6368198911069,2.68793211735317,126.683321226224));
#78751=CARTESIAN_POINT('Ctrl Pts',(-23.644584644054,2.57116693010801,126.6117142361));
#78752=CARTESIAN_POINT('Ctrl Pts',(-23.652341684939,2.45451771569293,126.540178367048));
#78753=CARTESIAN_POINT('Ctrl Pts',(-23.660098725824,2.3347588659261,126.47343959675));
#78754=CARTESIAN_POINT('Ctrl Pts',(-23.667855766709,2.21232397114588,126.41177530716));
#78755=CARTESIAN_POINT('Ctrl Pts',(-23.6756069579492,2.08998140547188,126.350157519091));
#78756=CARTESIAN_POINT('Ctrl Pts',(-23.6833581491893,1.96496715930937,126.293606770058));
#78757=CARTESIAN_POINT('Ctrl Pts',(-23.6911093404294,1.83774115272297,126.242355519137));
#78758=CARTESIAN_POINT('Ctrl Pts',(-23.6988572372065,1.71056922058358,126.191126051366));
#78759=CARTESIAN_POINT('Ctrl Pts',(-23.7066051339836,1.58118775960948,126.14519174758));
#78760=CARTESIAN_POINT('Ctrl Pts',(-23.7143530307606,1.45007828707664,126.104737651428));
#78761=CARTESIAN_POINT('Ctrl Pts',(-23.7220993068447,1.31899623981923,126.064292017401));
#78762=CARTESIAN_POINT('Ctrl Pts',(-23.7298455829289,1.18618727332162,126.02932442607));
#78763=CARTESIAN_POINT('Ctrl Pts',(-23.737591859013,1.05214936906679,125.99997046192));
#78764=CARTESIAN_POINT('Ctrl Pts',(-23.7453381922783,0.918110475374609,
125.970616281085));
#78765=CARTESIAN_POINT('Ctrl Pts',(-23.7530845255436,0.782843007737389,
125.946875893757));
#78766=CARTESIAN_POINT('Ctrl Pts',(-23.7608308588089,0.646856086896882,
125.928833952133));
#78767=CARTESIAN_POINT('Ctrl Pts',(-23.7685789268119,0.510838712728319,
125.910787970142));
#78768=CARTESIAN_POINT('Ctrl Pts',(-23.7763269948149,0.374101952248003,
125.89844302461));
#78769=CARTESIAN_POINT('Ctrl Pts',(-23.7840750628178,0.237160611706851,
125.891831950295));
#78770=CARTESIAN_POINT('Ctrl Pts',(-23.7918313655597,0.100073728279162,
125.885213849653));
#78771=CARTESIAN_POINT('Ctrl Pts',(-23.7995876683015,-0.0372177784163698,
125.884341812584));
#78772=CARTESIAN_POINT('Ctrl Pts',(-23.8073439710434,-0.17419797311882,
125.889196517695));
#78773=CARTESIAN_POINT('Ctrl Pts',(-23.8151044135576,-0.311251278275576,
125.894053813908));
#78774=CARTESIAN_POINT('Ctrl Pts',(-23.8228648560717,-0.447992550750946,
125.90464391253));
#78775=CARTESIAN_POINT('Ctrl Pts',(-23.8306252985859,-0.583911405745882,
125.920895604613));
#78776=CARTESIAN_POINT('Ctrl Pts',(-23.8383981988513,-0.720048449753165,
125.937173385354));
#78777=CARTESIAN_POINT('Ctrl Pts',(-23.8461710991167,-0.855360051925455,
125.9591308586));
#78778=CARTESIAN_POINT('Ctrl Pts',(-23.8539439993822,-0.989345553597839,
125.986645553547));
#78779=CARTESIAN_POINT('Ctrl Pts',(-23.8614343351442,-1.11846034479641,
126.013160020027));
#78780=CARTESIAN_POINT('Ctrl Pts',(-23.8689246709063,-1.24634347680606,
126.044834610834));
#78781=CARTESIAN_POINT('Ctrl Pts',(-23.8764150066684,-1.37256248331411,
126.081516634128));
#78782=CARTESIAN_POINT('Ctrl Pts',(-23.8841893407875,-1.50356712181625,
126.119589467484));
#78783=CARTESIAN_POINT('Ctrl Pts',(-23.8919636749066,-1.63319393645424,
126.163177545891));
#78784=CARTESIAN_POINT('Ctrl Pts',(-23.8997380090257,-1.76094336236402,
126.212164896884));
#78785=CARTESIAN_POINT('Ctrl Pts',(-23.9075027619728,-1.88853534852383,
126.261091875346));
#78786=CARTESIAN_POINT('Ctrl Pts',(-23.9152675149198,-2.01425418801448,
126.31540474804));
#78787=CARTESIAN_POINT('Ctrl Pts',(-23.9230322678669,-2.13761361267586,
126.374937279771));
#78788=CARTESIAN_POINT('Ctrl Pts',(-23.9307893087519,-2.26085051501727,
126.434410682952));
#78789=CARTESIAN_POINT('Ctrl Pts',(-23.9385463496369,-2.38173231618071,
126.499093259477));
#78790=CARTESIAN_POINT('Ctrl Pts',(-23.9463033905219,-2.49979128070281,
126.568770149234));
#78791=CARTESIAN_POINT('Ctrl Pts',(-23.9540545817621,-2.61776121604219,
126.638394495108));
#78792=CARTESIAN_POINT('Ctrl Pts',(-23.9618057730022,-2.73291221649801,
126.713005459811));
#78793=CARTESIAN_POINT('Ctrl Pts',(-23.9695569642424,-2.84480010963653,
126.792341749376));
#78794=CARTESIAN_POINT('Ctrl Pts',(-23.9773048610195,-2.9566404474353,126.871644318901));
#78795=CARTESIAN_POINT('Ctrl Pts',(-23.9850527577966,-3.0652201181117,126.955667993089));
#78796=CARTESIAN_POINT('Ctrl Pts',(-23.9928006545737,-3.17012316735488,
127.044107678427));
#78797=CARTESIAN_POINT('Ctrl Pts',(-24.0005469306578,-3.2750042731416,127.132528864091));
#78798=CARTESIAN_POINT('Ctrl Pts',(-24.0082932067419,-3.37620998849391,
127.225363971705));
#78799=CARTESIAN_POINT('Ctrl Pts',(-24.016039482826,-3.47335707118877,127.322267322072));
#78800=CARTESIAN_POINT('Ctrl Pts',(-24.0237858160913,-3.5705048710016,127.419171387758));
#78801=CARTESIAN_POINT('Ctrl Pts',(-24.0315321493568,-3.66359370157296,
127.520143480014));
#78802=CARTESIAN_POINT('Ctrl Pts',(-24.0392784826221,-3.75227715041547,
127.62480101772));
#78803=CARTESIAN_POINT('Ctrl Pts',(-24.0470265506251,-3.84098045930134,
127.729481992757));
#78804=CARTESIAN_POINT('Ctrl Pts',(-24.0547746186282,-3.92527617062519,
127.837849757334));
#78805=CARTESIAN_POINT('Ctrl Pts',(-24.0625226866312,-4.0048583942221,127.949488938361));
#78806=CARTESIAN_POINT('Ctrl Pts',(-24.070278989373,-4.08452519875317,128.061246770837));
#78807=CARTESIAN_POINT('Ctrl Pts',(-24.0780352921148,-4.15946828113642,
128.176282646382));
#78808=CARTESIAN_POINT('Ctrl Pts',(-24.0857915948567,-4.22942502139845,
128.294152050361));
#78809=CARTESIAN_POINT('Ctrl Pts',(-24.0935520373709,-4.29941909967912,
128.41208436479));
#78810=CARTESIAN_POINT('Ctrl Pts',(-24.1013124798851,-4.36442134764529,
128.532852877021));
#78811=CARTESIAN_POINT('Ctrl Pts',(-24.1090729223993,-4.42421579995151,
128.655989695691));
#78812=CARTESIAN_POINT('Ctrl Pts',(-24.1168458226647,-4.48410623962088,
128.779324184513));
#78813=CARTESIAN_POINT('Ctrl Pts',(-24.12461872293,-4.53877202165465,128.905034218276));
#78814=CARTESIAN_POINT('Ctrl Pts',(-24.1323916231955,-4.58804556597105,
129.032632380202));
#78815=CARTESIAN_POINT('Ctrl Pts',(-24.1398819589574,-4.63552789283838,
129.15559202754));
#78816=CARTESIAN_POINT('Ctrl Pts',(-24.1473722947194,-4.67800311909113,
129.280304618362));
#78817=CARTESIAN_POINT('Ctrl Pts',(-24.1548626304813,-4.71536595009257,
129.406323772841));
#78818=CARTESIAN_POINT('Ctrl Pts',(-24.1583337991521,-4.73268061962758,
129.464723523514));
#78819=CARTESIAN_POINT('Ctrl Pts',(-24.1618049678229,-4.74891401369239,
129.5234574829));
#78820=CARTESIAN_POINT('Ctrl Pts',(-24.1652761364937,-4.76405452823407,
129.582490119308));
#78821=CARTESIAN_POINT('Ctrl Pts',(-22.4150500904691,-4.76405452823408,
129.582490119308));
#78822=CARTESIAN_POINT('Ctrl Pts',(-22.4228105212612,-4.79812496141817,
129.715330221202));
#78823=CARTESIAN_POINT('Ctrl Pts',(-22.4305709520533,-4.8266080734547,129.849491122361));
#78824=CARTESIAN_POINT('Ctrl Pts',(-22.4383313828454,-4.84942792020898,
129.984463118364));
#78825=CARTESIAN_POINT('Ctrl Pts',(-22.4461042768808,-4.87228441561213,
130.119651879245));
#78826=CARTESIAN_POINT('Ctrl Pts',(-22.4538771709163,-4.88945942155506,
130.255653949909));
#78827=CARTESIAN_POINT('Ctrl Pts',(-22.4616500649517,-4.90092891478267,
130.391954464912));
#78828=CARTESIAN_POINT('Ctrl Pts',(-22.4691590058357,-4.9120089251653,130.523626465707));
#78829=CARTESIAN_POINT('Ctrl Pts',(-22.4766679467197,-4.91776464845334,
130.655576656357));
#78830=CARTESIAN_POINT('Ctrl Pts',(-22.4841768876037,-4.91822056078252,
130.787343626173));
#78831=CARTESIAN_POINT('Ctrl Pts',(-22.484498113072,-4.91824006428557,130.792980493906));
#78832=CARTESIAN_POINT('Ctrl Pts',(-22.4848193385403,-4.91824987700829,
130.798617395189));
#78833=CARTESIAN_POINT('Ctrl Pts',(-22.4851405640086,-4.91824999885106,
130.80425430882));
#78834=CARTESIAN_POINT('',(-22.139859436035,-4.91824822085812,130.808543980559));
#78835=CARTESIAN_POINT('Ctrl Pts',(-22.0699306202468,-4.76405452823405,
129.582490119308));
#78836=CARTESIAN_POINT('Ctrl Pts',(-22.0776378832166,-4.79798948271468,
129.714801991793));
#78837=CARTESIAN_POINT('Ctrl Pts',(-22.0853451461864,-4.82641450282772,
129.848553263949));
#78838=CARTESIAN_POINT('Ctrl Pts',(-22.0930524091562,-4.84922153977913,
129.983243378286));
#78839=CARTESIAN_POINT('Ctrl Pts',(-22.1008535802954,-4.87230646618314,
130.11957460726));
#78840=CARTESIAN_POINT('Ctrl Pts',(-22.1086547514346,-4.88963550117929,
130.256867306196));
#78841=CARTESIAN_POINT('Ctrl Pts',(-22.1164559225737,-4.90115030148244,
130.394593873212));
#78842=CARTESIAN_POINT('Ctrl Pts',(-22.1242570937129,-4.91266510178558,
130.532320440228));
#78843=CARTESIAN_POINT('Ctrl Pts',(-22.132058264852,-4.91836565489243,130.670480456408));
#78844=CARTESIAN_POINT('Ctrl Pts',(-22.1398594359911,-4.91824822085878,
130.808543979782));
#78845=CARTESIAN_POINT('Ctrl Pts',(-22.139859436035,-4.91824822085812,130.808543980559));
#78846=CARTESIAN_POINT('Ctrl Pts',(-22.1491261022749,-4.91810872613641,
130.972543535006));
#78847=CARTESIAN_POINT('Ctrl Pts',(-22.1583927685146,-4.90976258893785,
131.136186978294));
#78848=CARTESIAN_POINT('Ctrl Pts',(-22.1676594347545,-4.89333921015692,
131.298743502424));
#78849=CARTESIAN_POINT('Ctrl Pts',(-22.1772692389539,-4.87630768551886,
131.467319377263));
#78850=CARTESIAN_POINT('Ctrl Pts',(-22.1868790431532,-4.85058951655298,
131.634726219696));
#78851=CARTESIAN_POINT('Ctrl Pts',(-22.1964888473526,-4.81638261423217,
131.800172635882));
#78852=CARTESIAN_POINT('Ctrl Pts',(-22.2060986515519,-4.78217571191136,
131.965619052067));
#78853=CARTESIAN_POINT('Ctrl Pts',(-22.2157084557512,-4.73948020609989,
132.129105063668));
#78854=CARTESIAN_POINT('Ctrl Pts',(-22.2253182599506,-4.68854620602673,
132.289863070089));
#78855=CARTESIAN_POINT('Ctrl Pts',(-22.2330925940696,-4.64734058660124,
132.41991633947));
#78856=CARTESIAN_POINT('Ctrl Pts',(-22.2408669281887,-4.60065437435307,
132.548459831092));
#78857=CARTESIAN_POINT('Ctrl Pts',(-22.2486412623078,-4.54861549652774,
132.674996906973));
#78858=CARTESIAN_POINT('Ctrl Pts',(-22.256406015255,-4.49664075196847,132.801378037217));
#78859=CARTESIAN_POINT('Ctrl Pts',(-22.264170768202,-4.43932661453742,132.925757313601));
#78860=CARTESIAN_POINT('Ctrl Pts',(-22.2719355211491,-4.37685094065176,
133.047652597183));
#78861=CARTESIAN_POINT('Ctrl Pts',(-22.2796925620342,-4.31443731848607,
133.169426812652));
#78862=CARTESIAN_POINT('Ctrl Pts',(-22.2874496029192,-4.24687253902505,
133.288721599357));
#78863=CARTESIAN_POINT('Ctrl Pts',(-22.2952066438042,-4.17438262486525,
133.405074512581));
#78864=CARTESIAN_POINT('Ctrl Pts',(-22.3029578350444,-4.1019473759137,133.521339683168));
#78865=CARTESIAN_POINT('Ctrl Pts',(-22.3107090262846,-4.02459459082052,
133.634667065552));
#78866=CARTESIAN_POINT('Ctrl Pts',(-22.3184602175247,-3.94259614722024,
133.744618885546));
#78867=CARTESIAN_POINT('Ctrl Pts',(-22.3262081143018,-3.86063255514586,
133.854523973083));
#78868=CARTESIAN_POINT('Ctrl Pts',(-22.3339560110789,-3.77402746499148,
133.961056038995));
#78869=CARTESIAN_POINT('Ctrl Pts',(-22.341703907856,-3.68309586416433,134.063806570159));
#78870=CARTESIAN_POINT('Ctrl Pts',(-22.3494501839402,-3.59218328426782,
134.166535608127));
#78871=CARTESIAN_POINT('Ctrl Pts',(-22.3571964600242,-3.49694625275671,
134.265484392125));
#78872=CARTESIAN_POINT('Ctrl Pts',(-22.3649427361083,-3.39773954603953,
134.360278085644));
#78873=CARTESIAN_POINT('Ctrl Pts',(-22.3726890693737,-3.29853210700111,
134.455072478907));
#78874=CARTESIAN_POINT('Ctrl Pts',(-22.3804354026391,-3.19535521695379,
134.545711450391));
#78875=CARTESIAN_POINT('Ctrl Pts',(-22.3881817359045,-3.08859965978725,
134.631857868259));
#78876=CARTESIAN_POINT('Ctrl Pts',(-22.3959298039074,-2.98182019545387,
134.718023578019));
#78877=CARTESIAN_POINT('Ctrl Pts',(-22.4036778719104,-2.8714607734729,134.799694486714));
#78878=CARTESIAN_POINT('Ctrl Pts',(-22.4114259399134,-2.75794398783813,
134.876574760075));
#78879=CARTESIAN_POINT('Ctrl Pts',(-22.4191822426552,-2.64430655521256,
134.953536742705));
#78880=CARTESIAN_POINT('Ctrl Pts',(-22.4269385453972,-2.52750537982127,
135.025697699508));
#78881=CARTESIAN_POINT('Ctrl Pts',(-22.4346948481391,-2.40799115044376,
135.092805753263));
#78882=CARTESIAN_POINT('Ctrl Pts',(-22.4424552906532,-2.28841313272353,
135.159949624607));
#78883=CARTESIAN_POINT('Ctrl Pts',(-22.4502157331673,-2.16611952412009,
135.222035042234));
#78884=CARTESIAN_POINT('Ctrl Pts',(-22.4579761756815,-2.04158326382754,
135.278857331092));
#78885=CARTESIAN_POINT('Ctrl Pts',(-22.4657490759469,-1.91684708687399,
135.335770836134));
#78886=CARTESIAN_POINT('Ctrl Pts',(-22.4735219762125,-1.78986142645664,
135.387404181583));
#78887=CARTESIAN_POINT('Ctrl Pts',(-22.481294876478,-1.66111758044659,135.433601532277));
#78888=CARTESIAN_POINT('Ctrl Pts',(-22.4887852122399,-1.53705389752832,
135.478119492907));
#78889=CARTESIAN_POINT('Ctrl Pts',(-22.4962755480017,-1.41135793253972,
135.517589729034));
#78890=CARTESIAN_POINT('Ctrl Pts',(-22.5037658837635,-1.28447846354116,
135.551917688229));
#78891=CARTESIAN_POINT('Ctrl Pts',(-22.5115402178826,-1.15278832090854,
135.58754720243));
#78892=CARTESIAN_POINT('Ctrl Pts',(-22.5193145520017,-1.0194060027721,135.617749666915));
#78893=CARTESIAN_POINT('Ctrl Pts',(-22.5270888861207,-0.884818492532877,
135.642364265536));
#78894=CARTESIAN_POINT('Ctrl Pts',(-22.5348536390678,-0.750396849371779,
135.666948528865));
#78895=CARTESIAN_POINT('Ctrl Pts',(-22.5426183920149,-0.614773350289618,
135.685958558841));
#78896=CARTESIAN_POINT('Ctrl Pts',(-22.550383144962,-0.478449768169881,
135.699283383232));
#78897=CARTESIAN_POINT('Ctrl Pts',(-22.5581401858469,-0.342261584553731,
135.71259497322));
#78898=CARTESIAN_POINT('Ctrl Pts',(-22.5658972267319,-0.205375088235683,
135.720232556877));
#78899=CARTESIAN_POINT('Ctrl Pts',(-22.5736542676169,-0.0683015177875444,
135.722136330749));
#78900=CARTESIAN_POINT('Ctrl Pts',(-22.581405458857,0.0686686844150285,
135.72403866897));
#78901=CARTESIAN_POINT('Ctrl Pts',(-22.5891566500972,0.205825290602621,
135.72021579848));
#78902=CARTESIAN_POINT('Ctrl Pts',(-22.5969078413373,0.34265303244978,135.710659829992));
#78903=CARTESIAN_POINT('Ctrl Pts',(-22.6046557381143,0.479422618856468,
135.701107923046));
#78904=CARTESIAN_POINT('Ctrl Pts',(-22.6124036348914,0.61586322972809,135.685827791731));
#78905=CARTESIAN_POINT('Ctrl Pts',(-22.6201515316685,0.751460913016745,
135.664863632554));
#78906=CARTESIAN_POINT('Ctrl Pts',(-22.6278978077526,0.887030232193389,
135.643903858627));
#78907=CARTESIAN_POINT('Ctrl Pts',(-22.6356440838367,1.02175658837179,135.617262481474));
#78908=CARTESIAN_POINT('Ctrl Pts',(-22.6433903599207,1.1551328556645,135.585035376244));
#78909=CARTESIAN_POINT('Ctrl Pts',(-22.6511366931861,1.28851010751034,135.552808033122));
#78910=CARTESIAN_POINT('Ctrl Pts',(-22.6588830264514,1.42053687055499,135.514994971471));
#78911=CARTESIAN_POINT('Ctrl Pts',(-22.6666293597168,1.55071827799797,135.471742740853));
#78912=CARTESIAN_POINT('Ctrl Pts',(-22.6743774277197,1.68092883866453,135.428480824199));
#78913=CARTESIAN_POINT('Ctrl Pts',(-22.6821254957227,1.8092928504486,135.379777438017));
#78914=CARTESIAN_POINT('Ctrl Pts',(-22.6898735637256,1.93533299722661,135.325828216957));
#78915=CARTESIAN_POINT('Ctrl Pts',(-22.6976298664675,2.0615071009725,135.271821658023));
#78916=CARTESIAN_POINT('Ctrl Pts',(-22.7053861692093,2.18535204596109,135.212558280967));
#78917=CARTESIAN_POINT('Ctrl Pts',(-22.7131424719511,2.30641231245985,135.148281117234));
#78918=CARTESIAN_POINT('Ctrl Pts',(-22.7209029144653,2.42753719246822,135.083969646842));
#78919=CARTESIAN_POINT('Ctrl Pts',(-22.7286633569794,2.54587409530542,135.014639255138));
#78920=CARTESIAN_POINT('Ctrl Pts',(-22.7364237994936,2.66099518686844,134.940577207393));
#78921=CARTESIAN_POINT('Ctrl Pts',(-22.744196699759,2.77630108102745,134.866396268675));
#78922=CARTESIAN_POINT('Ctrl Pts',(-22.7519696000244,2.88838052813893,134.787468720576));
#78923=CARTESIAN_POINT('Ctrl Pts',(-22.7597425002898,2.99683686116581,134.704123673196));
#78924=CARTESIAN_POINT('Ctrl Pts',(-22.767232836052,3.10135053330376,134.623808428221));
#78925=CARTESIAN_POINT('Ctrl Pts',(-22.7747231718141,3.20249970018748,134.539391479719));
#78926=CARTESIAN_POINT('Ctrl Pts',(-22.7822135075762,3.29996223667653,134.451199289486));
#78927=CARTESIAN_POINT('Ctrl Pts',(-22.7899878416953,3.40112009485836,134.359663265555));
#78928=CARTESIAN_POINT('Ctrl Pts',(-22.7977621758145,3.49862668460454,134.263770113513));
#78929=CARTESIAN_POINT('Ctrl Pts',(-22.8055365099335,3.59208348031357,134.163842621232));
#78930=CARTESIAN_POINT('Ctrl Pts',(-22.8133012628806,3.68542509887436,134.064038280655));
#78931=CARTESIAN_POINT('Ctrl Pts',(-22.8210660158277,3.77472658952797,133.960209775368));
#78932=CARTESIAN_POINT('Ctrl Pts',(-22.8288307687748,3.85962336769156,133.852719277906));
#78933=CARTESIAN_POINT('Ctrl Pts',(-22.8365878096598,3.94443582517813,133.745335541522));
#78934=CARTESIAN_POINT('Ctrl Pts',(-22.8443448505448,4.02485203551462,133.634297355867));
#78935=CARTESIAN_POINT('Ctrl Pts',(-22.8521018914298,4.10054534742606,133.520002515203));
#78936=CARTESIAN_POINT('Ctrl Pts',(-22.8598530826699,4.17618157842229,133.405793865168));
#78937=CARTESIAN_POINT('Ctrl Pts',(-22.8676042739101,4.24710178509104,133.288333773027));
#78938=CARTESIAN_POINT('Ctrl Pts',(-22.8753554651503,4.31302081483474,133.168051484262));
#78939=CARTESIAN_POINT('Ctrl Pts',(-22.8831033619274,4.37891182723236,133.047820318679));
#78940=CARTESIAN_POINT('Ctrl Pts',(-22.8908512587045,4.43980570292522,132.92476968434));
#78941=CARTESIAN_POINT('Ctrl Pts',(-22.8985991554815,4.49546182204881,132.799355872949));
#78942=CARTESIAN_POINT('Ctrl Pts',(-22.9063454315657,4.55110629911209,132.673968295424));
#78943=CARTESIAN_POINT('Ctrl Pts',(-22.9140917076498,4.60151504037863,132.546218881219));
#78944=CARTESIAN_POINT('Ctrl Pts',(-22.9218379837339,4.64649459439816,132.416586112566));
#78945=CARTESIAN_POINT('Ctrl Pts',(-22.9295843169993,4.69147448044653,132.286952386993));
#78946=CARTESIAN_POINT('Ctrl Pts',(-22.9373306502646,4.73102497111685,132.155435648594));
#78947=CARTESIAN_POINT('Ctrl Pts',(-22.94507698353,4.76500187511187,132.022531456439));
#78948=CARTESIAN_POINT('Ctrl Pts',(-22.9528250515329,4.79898638799897,131.889597501312));
#78949=CARTESIAN_POINT('Ctrl Pts',(-22.960573119536,4.82739473368754,131.755275852862));
#78950=CARTESIAN_POINT('Ctrl Pts',(-22.968321187539,4.85013350412361,131.620073835969));
#78951=CARTESIAN_POINT('Ctrl Pts',(-22.9760774902808,4.87289644159549,131.484728124763));
#78952=CARTESIAN_POINT('Ctrl Pts',(-22.9838337930227,4.88997770189924,131.348500562186));
#78953=CARTESIAN_POINT('Ctrl Pts',(-22.9915900957646,4.90133553473013,131.21190575432));
#78954=CARTESIAN_POINT('Ctrl Pts',(-22.9993505382788,4.91269942957839,131.075238041692));
#78955=CARTESIAN_POINT('Ctrl Pts',(-23.0071109807929,4.91833379402113,130.938203083654));
#78956=CARTESIAN_POINT('Ctrl Pts',(-23.0148714233071,4.91824905768622,130.801316103051));
#78957=CARTESIAN_POINT('Ctrl Pts',(-23.0226443235725,4.91816418532502,130.664209379315));
#78958=CARTESIAN_POINT('Ctrl Pts',(-23.030417223838,4.91234188262093,130.527251498545));
#78959=CARTESIAN_POINT('Ctrl Pts',(-23.0381901241034,4.9008446309997,130.390954080001));
#78960=CARTESIAN_POINT('Ctrl Pts',(-23.0456804598654,4.88976533343487,130.259611415936));
#78961=CARTESIAN_POINT('Ctrl Pts',(-23.0531707956273,4.87341655925481,130.128882334483));
#78962=CARTESIAN_POINT('Ctrl Pts',(-23.0606611313893,4.85189885350642,129.99921430922));
#78963=CARTESIAN_POINT('Ctrl Pts',(-23.0684354655083,4.82956529740414,129.864629881366));
#78964=CARTESIAN_POINT('Ctrl Pts',(-23.0762097996274,4.80159236624469,129.730762234883));
#78965=CARTESIAN_POINT('Ctrl Pts',(-23.0839841337465,4.76803621778487,129.598121135377));
#78966=CARTESIAN_POINT('Ctrl Pts',(-23.0917488866936,4.73452142427907,129.465643504171));
#78967=CARTESIAN_POINT('Ctrl Pts',(-23.0995136396408,4.69543719921333,129.334389787675));
#78968=CARTESIAN_POINT('Ctrl Pts',(-23.1072783925879,4.65089118172614,129.204862484325));
#78969=CARTESIAN_POINT('Ctrl Pts',(-23.1150354334729,4.60638940797152,129.075463829319));
#78970=CARTESIAN_POINT('Ctrl Pts',(-23.1227924743578,4.55643676357715,128.947788542452));
#78971=CARTESIAN_POINT('Ctrl Pts',(-23.1305495152428,4.5011913611288,128.82232646221));
#78972=CARTESIAN_POINT('Ctrl Pts',(-23.138300706483,4.44598761966818,128.696958993898));
#78973=CARTESIAN_POINT('Ctrl Pts',(-23.1460518977231,4.38549922153395,128.573801766538));
#78974=CARTESIAN_POINT('Ctrl Pts',(-23.1538030889632,4.31993317116313,128.453326704756));
#78975=CARTESIAN_POINT('Ctrl Pts',(-23.1615509857403,4.25439498811275,128.332902848088));
#78976=CARTESIAN_POINT('Ctrl Pts',(-23.1692988825174,4.18378363169591,128.215159232324));
#78977=CARTESIAN_POINT('Ctrl Pts',(-23.1770467792945,4.10835293213205,128.100544934584));
#78978=CARTESIAN_POINT('Ctrl Pts',(-23.1847930553786,4.03293801104444,127.985954611683));
#78979=CARTESIAN_POINT('Ctrl Pts',(-23.1925393314627,3.9527059667789,127.874492631175));
#78980=CARTESIAN_POINT('Ctrl Pts',(-23.2002856075468,3.8679547947545,127.766580380578));
#78981=CARTESIAN_POINT('Ctrl Pts',(-23.2080319408121,3.7832029971162,127.658667333397));
#78982=CARTESIAN_POINT('Ctrl Pts',(-23.2157782740776,3.69393224663472,127.554304375888));
#78983=CARTESIAN_POINT('Ctrl Pts',(-23.2235246073429,3.60048153227411,127.453880682056));
#78984=CARTESIAN_POINT('Ctrl Pts',(-23.2312726753459,3.50700989027408,127.353434499035));
#78985=CARTESIAN_POINT('Ctrl Pts',(-23.2390207433488,3.40935668800406,127.256929621265));
#78986=CARTESIAN_POINT('Ctrl Pts',(-23.2467688113518,3.30789826291805,127.164718857079));
#78987=CARTESIAN_POINT('Ctrl Pts',(-23.2545251140936,3.20633200661035,127.072410090194));
#78988=CARTESIAN_POINT('Ctrl Pts',(-23.2622814168355,3.10095273847587,126.984404817018));
#78989=CARTESIAN_POINT('Ctrl Pts',(-23.2700377195774,2.99217084412811,126.901016320422));
#78990=CARTESIAN_POINT('Ctrl Pts',(-23.2777981620916,2.88333088960783,126.817583316874));
#78991=CARTESIAN_POINT('Ctrl Pts',(-23.2855586046057,2.77108500998726,126.73877222441));
#78992=CARTESIAN_POINT('Ctrl Pts',(-23.2933190471199,2.65587231430665,126.664852758822));
#78993=CARTESIAN_POINT('Ctrl Pts',(-23.3010919473853,2.54047466897883,126.590814631146));
#78994=CARTESIAN_POINT('Ctrl Pts',(-23.3088648476508,2.42210102820884,126.521684019369));
#78995=CARTESIAN_POINT('Ctrl Pts',(-23.3166377479162,2.30121560450737,126.457684898804));
#78996=CARTESIAN_POINT('Ctrl Pts',(-23.3241280836782,2.18472467045093,126.396012307477));
#78997=CARTESIAN_POINT('Ctrl Pts',(-23.3316184194401,2.06590167999925,126.339104732456));
#78998=CARTESIAN_POINT('Ctrl Pts',(-23.3391087552021,1.94517745240033,126.287119452743));
#78999=CARTESIAN_POINT('Ctrl Pts',(-23.3468830893211,1.81987592901743,126.233163135348));
#79000=CARTESIAN_POINT('Ctrl Pts',(-23.3546574234402,1.6921292341346,126.184338821745));
#79001=CARTESIAN_POINT('Ctrl Pts',(-23.3624317575593,1.5623966026319,126.140874805581));
#79002=CARTESIAN_POINT('Ctrl Pts',(-23.3701965105064,1.43282385500317,126.097464354933));
#79003=CARTESIAN_POINT('Ctrl Pts',(-23.3779612634534,1.30127040768345,126.059401180587));
#79004=CARTESIAN_POINT('Ctrl Pts',(-23.3857260164005,1.16821720842277,126.026866335367));
#79005=CARTESIAN_POINT('Ctrl Pts',(-23.3934830572855,1.03529615947513,125.994363804214));
#79006=CARTESIAN_POINT('Ctrl Pts',(-23.4012400981705,0.900878700226168,
125.967378767481));
#79007=CARTESIAN_POINT('Ctrl Pts',(-23.4089971390555,0.765462409380287,
125.946042970239));
#79008=CARTESIAN_POINT('Ctrl Pts',(-23.4167483302956,0.630148237012718,
125.924723262488));
#79009=CARTESIAN_POINT('Ctrl Pts',(-23.4244995215357,0.493837116938609,
125.909044375288));
#79010=CARTESIAN_POINT('Ctrl Pts',(-23.4322507127758,0.357037983664662,
125.899087236732));
#79011=CARTESIAN_POINT('Ctrl Pts',(-23.4399986095529,0.220296993671779,
125.889134330225));
#79012=CARTESIAN_POINT('Ctrl Pts',(-23.4477465063301,0.0830687921361914,
125.884898363828));
#79013=CARTESIAN_POINT('Ctrl Pts',(-23.4554944031071,-0.0541315982100819,
125.88640852014));
#79014=CARTESIAN_POINT('Ctrl Pts',(-23.4632406791912,-0.19130328919258,
125.887918360561));
#79015=CARTESIAN_POINT('Ctrl Pts',(-23.4709869552753,-0.328446789863249,
125.895171928616));
#79016=CARTESIAN_POINT('Ctrl Pts',(-23.4787332313594,-0.465046501165917,
125.908146282567));
#79017=CARTESIAN_POINT('Ctrl Pts',(-23.4864795646247,-0.601647220816437,
125.921120732291));
#79018=CARTESIAN_POINT('Ctrl Pts',(-23.49422589789,-0.737703753875519,125.93981601521));
#79019=CARTESIAN_POINT('Ctrl Pts',(-23.5019722311554,-0.872705445415273,
125.964157288361));
#79020=CARTESIAN_POINT('Ctrl Pts',(-23.5097202991583,-1.00773736964763,
125.988504012573));
#79021=CARTESIAN_POINT('Ctrl Pts',(-23.5174683671613,-1.14171359761394,
126.018499173628));
#79022=CARTESIAN_POINT('Ctrl Pts',(-23.5252164351643,-1.27413388208736,
126.054016849688));
#79023=CARTESIAN_POINT('Ctrl Pts',(-23.5329727379061,-1.40669490441529,
126.089572274357));
#79024=CARTESIAN_POINT('Ctrl Pts',(-23.540729040648,-1.53769630163585,126.130661837334));
#79025=CARTESIAN_POINT('Ctrl Pts',(-23.5484853433898,-1.66665267654765,
126.177109606625));
#79026=CARTESIAN_POINT('Ctrl Pts',(-23.556245785904,-1.79567787935972,126.223582166488));
#79027=CARTESIAN_POINT('Ctrl Pts',(-23.5640062284182,-1.9226555231884,126.275418483437));
#79028=CARTESIAN_POINT('Ctrl Pts',(-23.5717666709324,-2.04712133933738,
126.332394910572));
#79029=CARTESIAN_POINT('Ctrl Pts',(-23.5795395711978,-2.17178695906383,
126.389462801326));
#79030=CARTESIAN_POINT('Ctrl Pts',(-23.5873124714632,-2.29393234490585,
126.451687113547));
#79031=CARTESIAN_POINT('Ctrl Pts',(-23.5950853717286,-2.4131181418871,126.518798356229));
#79032=CARTESIAN_POINT('Ctrl Pts',(-23.6025757074908,-2.52797123493895,
126.583469936198));
#79033=CARTESIAN_POINT('Ctrl Pts',(-23.6100660432529,-2.64007591826598,
126.652679148965));
#79034=CARTESIAN_POINT('Ctrl Pts',(-23.617556379015,-2.74906700026126,126.726148547237));
#79035=CARTESIAN_POINT('Ctrl Pts',(-23.6253031721824,-2.86178976678577,
126.802133423033));
#79036=CARTESIAN_POINT('Ctrl Pts',(-23.6330499653498,-2.97154496364008,
126.882920231638));
#79037=CARTESIAN_POINT('Ctrl Pts',(-23.6407967585171,-3.07789393071905,
126.968249042841));
#79038=CARTESIAN_POINT('Ctrl Pts',(-23.6485312997414,-3.18407470155647,
127.053442902235));
#79039=CARTESIAN_POINT('Ctrl Pts',(-23.6562658409657,-3.28685966616888,
127.143164214412));
#79040=CARTESIAN_POINT('Ctrl Pts',(-23.6640003821899,-3.38583845623077,
127.237109433418));
#79041=CARTESIAN_POINT('Ctrl Pts',(-23.6717278517343,-3.48472675012762,
127.330968758445));
#79042=CARTESIAN_POINT('Ctrl Pts',(-23.6794553212787,-3.57981550709763,
127.429044039738));
#79043=CARTESIAN_POINT('Ctrl Pts',(-23.6871827908231,-3.67072663227632,
127.530990938841));
#79044=CARTESIAN_POINT('Ctrl Pts',(-23.6949049018569,-3.76157471634971,
127.632867144228));
#79045=CARTESIAN_POINT('Ctrl Pts',(-23.7026270128907,-3.84825067058314,
127.738609333425));
#79046=CARTESIAN_POINT('Ctrl Pts',(-23.7103491239246,-3.930412875896,127.847836021441));
#79047=CARTESIAN_POINT('Ctrl Pts',(-23.7180675854749,-4.01253625120348,
127.957011088729));
#79048=CARTESIAN_POINT('Ctrl Pts',(-23.7257860470253,-4.09014988648217,
128.069667063224));
#79049=CARTESIAN_POINT('Ctrl Pts',(-23.7335045085756,-4.16295241656001,
128.18538939971));
#79050=CARTESIAN_POINT('Ctrl Pts',(-23.7412225938894,-4.23575139787648,
128.301106095307));
#79051=CARTESIAN_POINT('Ctrl Pts',(-23.748940679203,-4.30373952188243,128.419888527669));
#79052=CARTESIAN_POINT('Ctrl Pts',(-23.7566587645167,-4.3666588322444,128.541293295262));
#79053=CARTESIAN_POINT('Ctrl Pts',(-23.7643764315985,-4.42957473309934,
128.662691484104));
#79054=CARTESIAN_POINT('Ctrl Pts',(-23.7720940986803,-4.48742219024157,
128.786711372921));
#79055=CARTESIAN_POINT('Ctrl Pts',(-23.779811765762,-4.53998965728447,128.91288580297));
#79056=CARTESIAN_POINT('Ctrl Pts',(-23.7875336500506,-4.59258584905459,
129.0391291792));
#79057=CARTESIAN_POINT('Ctrl Pts',(-23.7952555343392,-4.63989613882725,
129.167529082938));
#79058=CARTESIAN_POINT('Ctrl Pts',(-23.8029774186278,-4.6817574591316,129.29759913798));
#79059=CARTESIAN_POINT('Ctrl Pts',(-23.8085669454221,-4.71205899729742,
129.391751035445));
#79060=CARTESIAN_POINT('Ctrl Pts',(-23.8141564722163,-4.73950647488403,
129.486777631865));
#79061=CARTESIAN_POINT('Ctrl Pts',(-23.8197459990105,-4.76405452823405,
129.582490119308));
#79062=CARTESIAN_POINT('Origin',(213.235140564004,0.,130.804360617566));
#79063=CARTESIAN_POINT('',(-25.9153671414536,-4.76405452823411,129.582490119308));
#79064=CARTESIAN_POINT('',(-25.5699526237868,-4.76405452823406,129.582490119308));
#79065=CARTESIAN_POINT('',(213.235140564004,-4.76405452823405,129.582490119308));
#79066=CARTESIAN_POINT('',(-24.2351405639732,-4.91824806745606,130.800000633076));
#79067=CARTESIAN_POINT('Ctrl Pts',(-24.2351405640086,-4.91824806745661,
130.800000633701));
#79068=CARTESIAN_POINT('Ctrl Pts',(-24.2428327878828,-4.91836867782199,
130.936054278564));
#79069=CARTESIAN_POINT('Ctrl Pts',(-24.250525011757,-4.9128395587903,131.072219580756));
#79070=CARTESIAN_POINT('Ctrl Pts',(-24.2582172356313,-4.90165976709171,
131.207987413226));
#79071=CARTESIAN_POINT('Ctrl Pts',(-24.2659066851318,-4.8904840076367,131.34370627797));
#79072=CARTESIAN_POINT('Ctrl Pts',(-24.2735961346324,-4.87366165881892,
131.479027562654));
#79073=CARTESIAN_POINT('Ctrl Pts',(-24.2812855841329,-4.85124384364944,
131.613444192948));
#79074=CARTESIAN_POINT('Ctrl Pts',(-24.288973822721,-4.82882955877303,131.747839655698));
#79075=CARTESIAN_POINT('Ctrl Pts',(-24.2966620613091,-4.80082162501622,
131.88133035557));
#79076=CARTESIAN_POINT('Ctrl Pts',(-24.3043502998972,-4.76732272740965,
132.013416892197));
#79077=CARTESIAN_POINT('Ctrl Pts',(-24.3120390541298,-4.73382158305711,
132.145512287768));
#79078=CARTESIAN_POINT('Ctrl Pts',(-24.3197278083623,-4.69482883996834,
132.276202947606));
#79079=CARTESIAN_POINT('Ctrl Pts',(-24.3274165625948,-4.65049762531464,
132.40500264483));
#79080=CARTESIAN_POINT('Ctrl Pts',(-24.3351075590924,-4.60615348238504,
132.533839903803));
#79081=CARTESIAN_POINT('Ctrl Pts',(-24.3427985555901,-4.5564679003707,132.66078472772));
#79082=CARTESIAN_POINT('Ctrl Pts',(-24.3504895520877,-4.5016427275876,132.785369404941));
#79083=CARTESIAN_POINT('Ctrl Pts',(-24.358189014574,-4.44675720510963,132.910091220759));
#79084=CARTESIAN_POINT('Ctrl Pts',(-24.3658884770604,-4.38672095606205,
133.032447338702));
#79085=CARTESIAN_POINT('Ctrl Pts',(-24.3735879395467,-4.32178269779036,
133.151992908957));
#79086=CARTESIAN_POINT('Ctrl Pts',(-24.3812920853721,-4.25680493963322,
133.271611194995));
#79087=CARTESIAN_POINT('Ctrl Pts',(-24.3889962311975,-4.1869194381364,133.388415188816));
#79088=CARTESIAN_POINT('Ctrl Pts',(-24.396700377023,-4.11241846104265,133.501988735705));
#79089=CARTESIAN_POINT('Ctrl Pts',(-24.4044162002136,-4.03780456096723,
133.615734428841));
#79090=CARTESIAN_POINT('Ctrl Pts',(-24.4121320234043,-3.9585614471088,133.726239575841));
#79091=CARTESIAN_POINT('Ctrl Pts',(-24.4198478465949,-3.87502221888228,
133.83312040759));
#79092=CARTESIAN_POINT('Ctrl Pts',(-24.4243353158279,-3.8264363833653,133.895281557765));
#79093=CARTESIAN_POINT('Ctrl Pts',(-24.4288227850611,-3.7763981025758,133.956217445617));
#79094=CARTESIAN_POINT('Ctrl Pts',(-24.4333102542941,-3.72497846716922,
134.01585847396));
#79095=CARTESIAN_POINT('Ctrl Pts',(-24.4410845884132,-3.63589631302594,
134.11918381336));
#79096=CARTESIAN_POINT('Ctrl Pts',(-24.4488589225323,-3.5423706651416,134.21896349486));
#79097=CARTESIAN_POINT('Ctrl Pts',(-24.4566332566513,-3.44471465491814,
134.314791361605));
#79098=CARTESIAN_POINT('Ctrl Pts',(-24.4643980095984,-3.34717899699938,
134.410501129069));
#79099=CARTESIAN_POINT('Ctrl Pts',(-24.4721627625455,-3.24552338130106,
134.502268500939));
#79100=CARTESIAN_POINT('Ctrl Pts',(-24.4799275154926,-3.14010112703675,
134.589720306484));
#79101=CARTESIAN_POINT('Ctrl Pts',(-24.4876845563776,-3.034783579642,134.677085253661));
#79102=CARTESIAN_POINT('Ctrl Pts',(-24.4954415972625,-2.92570713755785,
134.760142916406));
#79103=CARTESIAN_POINT('Ctrl Pts',(-24.5031986381475,-2.81326164176152,
134.838557191544));
#79104=CARTESIAN_POINT('Ctrl Pts',(-24.5109498293877,-2.70090094198781,
134.916912333867));
#79105=CARTESIAN_POINT('Ctrl Pts',(-24.5187010206279,-2.58517656486285,
134.990630835607));
#79106=CARTESIAN_POINT('Ctrl Pts',(-24.526452211868,-2.46651078938088,135.059417325574));
#79107=CARTESIAN_POINT('Ctrl Pts',(-24.5342001086451,-2.34789545001916,
135.128174579449));
#79108=CARTESIAN_POINT('Ctrl Pts',(-24.5419480054221,-2.22634153633676,
135.192003795146));
#79109=CARTESIAN_POINT('Ctrl Pts',(-24.5496959021992,-2.10229943442395,
135.250653472352));
#79110=CARTESIAN_POINT('Ctrl Pts',(-24.5574421782833,-1.97828327944482,
135.30929088131));
#79111=CARTESIAN_POINT('Ctrl Pts',(-24.5651884543674,-1.85178032471338,
135.362750739801));
#79112=CARTESIAN_POINT('Ctrl Pts',(-24.5729347304515,-1.72326427236933,
135.410828169832));
#79113=CARTESIAN_POINT('Ctrl Pts',(-24.5806810637168,-1.59474727134916,
135.458905954758));
#79114=CARTESIAN_POINT('Ctrl Pts',(-24.5884273969821,-1.46421750924465,
135.501601094955));
#79115=CARTESIAN_POINT('Ctrl Pts',(-24.5961737302475,-1.33216694222551,
135.538757548595));
#79116=CARTESIAN_POINT('Ctrl Pts',(-24.6039217982504,-1.20008680339781,
135.575922323166));
#79117=CARTESIAN_POINT('Ctrl Pts',(-24.6116698662534,-1.06648555823141,
135.607545837151));
#79118=CARTESIAN_POINT('Ctrl Pts',(-24.6194179342563,-0.931868143972421,
135.633522534995));
#79119=CARTESIAN_POINT('Ctrl Pts',(-24.6271742369982,-0.79710765672322,
135.659526841184));
#79120=CARTESIAN_POINT('Ctrl Pts',(-24.63493053974,-0.661329227467334,135.679872268388));
#79121=CARTESIAN_POINT('Ctrl Pts',(-24.6426868424819,-0.525046312202897,
135.694504729199));
#79122=CARTESIAN_POINT('Ctrl Pts',(-24.650447284996,-0.388690658642998,
135.709144999796));
#79123=CARTESIAN_POINT('Ctrl Pts',(-24.6582077275102,-0.251830372498786,
135.718066202827));
#79124=CARTESIAN_POINT('Ctrl Pts',(-24.6659681700243,-0.114980778526438,
135.72126640099));
#79125=CARTESIAN_POINT('Ctrl Pts',(-24.6737410702898,0.0220884985630899,
135.724471736395));
#79126=CARTESIAN_POINT('Ctrl Pts',(-24.6815139705552,0.159146658058194,
135.721937721875));
#79127=CARTESIAN_POINT('Ctrl Pts',(-24.6892868708206,0.29568072864988,135.713714543411));
#79128=CARTESIAN_POINT('Ctrl Pts',(-24.6967772065827,0.427251441869022,
135.705790298196));
#79129=CARTESIAN_POINT('Ctrl Pts',(-24.7042675423449,0.558335202081555,
135.692583369554));
#79130=CARTESIAN_POINT('Ctrl Pts',(-24.711757878107,0.688482251766975,135.674183535445));
#79131=CARTESIAN_POINT('Ctrl Pts',(-24.719532212226,0.82356386639702,135.655086066034));
#79132=CARTESIAN_POINT('Ctrl Pts',(-24.7273065463451,0.958064235523123,
135.63033364479));
#79133=CARTESIAN_POINT('Ctrl Pts',(-24.7350808804642,1.09147239270891,135.599970180328));
#79134=CARTESIAN_POINT('Ctrl Pts',(-24.7428456334113,1.2247161362638,135.569644136123));
#79135=CARTESIAN_POINT('Ctrl Pts',(-24.7506103863585,1.35686996856732,135.533720893638));
#79136=CARTESIAN_POINT('Ctrl Pts',(-24.7583751393056,1.48742895284718,135.492296002438));
#79137=CARTESIAN_POINT('Ctrl Pts',(-24.7661321801906,1.61785826410365,135.450912255023));
#79138=CARTESIAN_POINT('Ctrl Pts',(-24.7738892210757,1.74669550937336,135.404037850602));
#79139=CARTESIAN_POINT('Ctrl Pts',(-24.7816462619608,1.8734471969674,135.351819101453));
#79140=CARTESIAN_POINT('Ctrl Pts',(-24.7893974532009,2.00010330012767,135.299639730869));
#79141=CARTESIAN_POINT('Ctrl Pts',(-24.797148644441,2.12467661601915,135.242124185774));
#79142=CARTESIAN_POINT('Ctrl Pts',(-24.8048998356812,2.24669038838435,135.179468086102));
#79143=CARTESIAN_POINT('Ctrl Pts',(-24.8126477324583,2.36865230164146,135.116838616944));
#79144=CARTESIAN_POINT('Ctrl Pts',(-24.8203956292353,2.48805648801008,135.049073116977));
#79145=CARTESIAN_POINT('Ctrl Pts',(-24.8281435260124,2.60444790846954,134.97641456671));
#79146=CARTESIAN_POINT('Ctrl Pts',(-24.8358898020966,2.72081498235294,134.903771215046));
#79147=CARTESIAN_POINT('Ctrl Pts',(-24.8436360781807,2.8341702124029,134.826237055824));
#79148=CARTESIAN_POINT('Ctrl Pts',(-24.8513823542648,2.94408518138219,134.744099886511));
#79149=CARTESIAN_POINT('Ctrl Pts',(-24.8591286875302,3.05400096172865,134.66196211088));
#79150=CARTESIAN_POINT('Ctrl Pts',(-24.8668750207955,3.16047611714944,134.575221491389));
#79151=CARTESIAN_POINT('Ctrl Pts',(-24.8746213540609,3.26311345091137,134.484207580278));
#79152=CARTESIAN_POINT('Ctrl Pts',(-24.8823694220639,3.36577376959242,134.393173287233));
#79153=CARTESIAN_POINT('Ctrl Pts',(-24.8901174900669,3.4645942639364,134.297864057646));
#79154=CARTESIAN_POINT('Ctrl Pts',(-24.8978655580699,3.55921319615178,134.198647654167));
#79155=CARTESIAN_POINT('Ctrl Pts',(-24.9056218608118,3.65393269049443,134.099325802314));
#79156=CARTESIAN_POINT('Ctrl Pts',(-24.9133781635536,3.74444143219922,133.996088764704));
#79157=CARTESIAN_POINT('Ctrl Pts',(-24.9211344662955,3.83041638048846,133.889339290845));
#79158=CARTESIAN_POINT('Ctrl Pts',(-24.9288949088097,3.91643721619638,133.782532841577));
#79159=CARTESIAN_POINT('Ctrl Pts',(-24.9366553513239,3.99791920462755,133.67221053491));
#79160=CARTESIAN_POINT('Ctrl Pts',(-24.9444157938381,4.07458217025562,133.558804880995));
#79161=CARTESIAN_POINT('Ctrl Pts',(-24.9521886941035,4.15136820208194,133.445217178256));
#79162=CARTESIAN_POINT('Ctrl Pts',(-24.9599615943689,4.22331954693774,133.328536570238));
#79163=CARTESIAN_POINT('Ctrl Pts',(-24.9677344946344,4.29020115418773,133.209221760981));
#79164=CARTESIAN_POINT('Ctrl Pts',(-24.9752248303963,4.35465144654804,133.094244345578));
#79165=CARTESIAN_POINT('Ctrl Pts',(-24.9827151661581,4.41439405773337,132.976821198102));
#79166=CARTESIAN_POINT('Ctrl Pts',(-24.99020550192,4.46926141555867,132.857379239473));
#79167=CARTESIAN_POINT('Ctrl Pts',(-24.997979836039,4.52620908593361,132.733408602677));
#79168=CARTESIAN_POINT('Ctrl Pts',(-25.0057541701581,4.57808490778234,132.606870344589));
#79169=CARTESIAN_POINT('Ctrl Pts',(-25.0135285042772,4.62464963282695,132.478218089424));
#79170=CARTESIAN_POINT('Ctrl Pts',(-25.0212932572243,4.67115697100956,132.349724386665));
#79171=CARTESIAN_POINT('Ctrl Pts',(-25.0290580101713,4.71236610410475,132.21912223472));
#79172=CARTESIAN_POINT('Ctrl Pts',(-25.0368227631184,4.74808449000776,132.08688809807));
#79173=CARTESIAN_POINT('Ctrl Pts',(-25.0445798040034,4.7837673999064,131.954785298229));
#79174=CARTESIAN_POINT('Ctrl Pts',(-25.0523368448885,4.81397031400719,131.821054114362));
#79175=CARTESIAN_POINT('Ctrl Pts',(-25.0600938857735,4.83854958466325,131.686188820367));
#79176=CARTESIAN_POINT('Ctrl Pts',(-25.0678450770137,4.86311031990014,131.551425229339));
#79177=CARTESIAN_POINT('Ctrl Pts',(-25.0755962682538,4.8820557829984,131.41552961356));
#79178=CARTESIAN_POINT('Ctrl Pts',(-25.0833474594939,4.89529285614709,131.279008818927));
#79179=CARTESIAN_POINT('Ctrl Pts',(-25.091095356271,4.90852430318652,131.142546049274));
#79180=CARTESIAN_POINT('Ctrl Pts',(-25.098843253048,4.91605214818696,131.005459017584));
#79181=CARTESIAN_POINT('Ctrl Pts',(-25.1065911498251,4.91783485782742,130.868261897973));
#79182=CARTESIAN_POINT('Ctrl Pts',(-25.1143374259092,4.91961719456345,130.731093477041));
#79183=CARTESIAN_POINT('Ctrl Pts',(-25.1220837019932,4.9156567812265,130.593815404678));
#79184=CARTESIAN_POINT('Ctrl Pts',(-25.1298299780773,4.90596417999352,130.456943681996));
#79185=CARTESIAN_POINT('Ctrl Pts',(-25.1375763113426,4.89627150721195,130.320070948959));
#79186=CARTESIAN_POINT('Ctrl Pts',(-25.145322644608,4.88084658971753,130.183604961579));
#79187=CARTESIAN_POINT('Ctrl Pts',(-25.1530689778733,4.85975199460728,130.048058023752));
#79188=CARTESIAN_POINT('Ctrl Pts',(-25.1608170458763,4.83865267550872,129.912480731127));
#79189=CARTESIAN_POINT('Ctrl Pts',(-25.1685651138793,4.81188121237726,129.777823283845));
#79190=CARTESIAN_POINT('Ctrl Pts',(-25.1763131818822,4.77955148623449,129.644588806849));
#79191=CARTESIAN_POINT('Ctrl Pts',(-25.1840694846241,4.74718739967403,129.511212726666));
#79192=CARTESIAN_POINT('Ctrl Pts',(-25.1918257873658,4.70925334179871,129.379263018396));
#79193=CARTESIAN_POINT('Ctrl Pts',(-25.1995820901077,4.66591354574455,129.249229161342));
#79194=CARTESIAN_POINT('Ctrl Pts',(-25.2073425326218,4.62255061793624,129.119125901303));
#79195=CARTESIAN_POINT('Ctrl Pts',(-25.2151029751361,4.57377634190246,128.99094089522));
#79196=CARTESIAN_POINT('Ctrl Pts',(-25.2228634176502,4.5198031589681,128.865143645002));
#79197=CARTESIAN_POINT('Ctrl Pts',(-25.2306363179157,4.46574333348898,128.739144453869));
#79198=CARTESIAN_POINT('Ctrl Pts',(-25.2384092181811,4.40646809280162,128.615541030958));
#79199=CARTESIAN_POINT('Ctrl Pts',(-25.2461821184465,4.34223630699538,128.494779071764));
#79200=CARTESIAN_POINT('Ctrl Pts',(-25.2536724542086,4.2803395083926,128.378407113965));
#79201=CARTESIAN_POINT('Ctrl Pts',(-25.2611627899707,4.21384042946294,128.264673883742));
#79202=CARTESIAN_POINT('Ctrl Pts',(-25.2686531257328,4.1430076740085,128.153951125505));
#79203=CARTESIAN_POINT('Ctrl Pts',(-25.2764274598519,4.06948927310268,128.039030280237));
#79204=CARTESIAN_POINT('Ctrl Pts',(-25.2842017939709,3.99106920167037,127.926988662751));
#79205=CARTESIAN_POINT('Ctrl Pts',(-25.29197612809,3.90799978707162,127.818272754366));
#79206=CARTESIAN_POINT('Ctrl Pts',(-25.2997408810371,3.82503274810234,127.709690828623));
#79207=CARTESIAN_POINT('Ctrl Pts',(-25.3075056339842,3.73742800185325,127.604426764586));
#79208=CARTESIAN_POINT('Ctrl Pts',(-25.3152703869312,3.64548233767515,127.502900094071));
#79209=CARTESIAN_POINT('Ctrl Pts',(-25.3230274278162,3.55362799522716,127.401474261276));
#79210=CARTESIAN_POINT('Ctrl Pts',(-25.3307844687012,3.45744157559582,127.303778722807));
#79211=CARTESIAN_POINT('Ctrl Pts',(-25.3385415095861,3.35726128034615,127.210201500611));
#79212=CARTESIAN_POINT('Ctrl Pts',(-25.3462927008263,3.25715653183559,127.116694845726));
#79213=CARTESIAN_POINT('Ctrl Pts',(-25.3540438920664,3.15306418709066,127.027300591294));
#79214=CARTESIAN_POINT('Ctrl Pts',(-25.3617950833066,3.04536033746614,126.942371042556));
#79215=CARTESIAN_POINT('Ctrl Pts',(-25.3695429800837,2.93770226485124,126.857477591141));
#79216=CARTESIAN_POINT('Ctrl Pts',(-25.3772908768608,2.82643604668417,126.777045312777));
#79217=CARTESIAN_POINT('Ctrl Pts',(-25.3850387736379,2.71197182243664,126.701387074292));
#79218=CARTESIAN_POINT('Ctrl Pts',(-25.392785049722,2.59753154163711,126.625744661879));
#79219=CARTESIAN_POINT('Ctrl Pts',(-25.4005313258061,2.47989491129314,126.554874518468));
#79220=CARTESIAN_POINT('Ctrl Pts',(-25.4082776018902,2.35950176687121,126.489046669007));
#79221=CARTESIAN_POINT('Ctrl Pts',(-25.4160239351555,2.23910773373444,126.423218333619));
#79222=CARTESIAN_POINT('Ctrl Pts',(-25.4237702684209,2.11595748895299,126.362432554017));
#79223=CARTESIAN_POINT('Ctrl Pts',(-25.4315166016863,1.99051586734849,126.3069136035));
#79224=CARTESIAN_POINT('Ctrl Pts',(-25.4392646696893,1.86504615396242,126.251382219898));
#79225=CARTESIAN_POINT('Ctrl Pts',(-25.4470127376922,1.73728440011416,126.20112017059));
#79226=CARTESIAN_POINT('Ctrl Pts',(-25.4547608056952,1.607715454543,126.15630359557));
#79227=CARTESIAN_POINT('Ctrl Pts',(-25.4625171084371,1.47800880155494,126.111439388961));
#79228=CARTESIAN_POINT('Ctrl Pts',(-25.4702734111789,1.34649149010508,126.072032345829));
#79229=CARTESIAN_POINT('Ctrl Pts',(-25.4780297139208,1.21366410501443,126.038208867705));
#79230=CARTESIAN_POINT('Ctrl Pts',(-25.485790156435,1.08076582594882,126.004367336973));
#79231=CARTESIAN_POINT('Ctrl Pts',(-25.4935505989491,0.946556462369149,
125.976115389879));
#79232=CARTESIAN_POINT('Ctrl Pts',(-25.5013110414633,0.811545849252267,
125.953528070769));
#79233=CARTESIAN_POINT('Ctrl Pts',(-25.5090839417287,0.676318505113714,
125.93090449249));
#79234=CARTESIAN_POINT('Ctrl Pts',(-25.5168568419941,0.540287729318321,
125.913963761978));
#79235=CARTESIAN_POINT('Ctrl Pts',(-25.5246297422595,0.403968423714513,
125.902728993796));
#79236=CARTESIAN_POINT('Ctrl Pts',(-25.5321200780216,0.272604668236464,
125.891902637736));
#79237=CARTESIAN_POINT('Ctrl Pts',(-25.5396104137837,0.14097330406644,125.886374607167));
#79238=CARTESIAN_POINT('Ctrl Pts',(-25.5471007495457,0.00953227722159142,
125.886119855038));
#79239=CARTESIAN_POINT('Ctrl Pts',(-25.5548750836648,-0.126892376106331,
125.885855443904));
#79240=CARTESIAN_POINT('Ctrl Pts',(-25.5626494177839,-0.263544126207083,
125.891271239952));
#79241=CARTESIAN_POINT('Ctrl Pts',(-25.570423751903,-0.399910946599676,
125.902396287087));
#79242=CARTESIAN_POINT('Ctrl Pts',(-25.5781885048501,-0.536109707073772,
125.913507623595));
#79243=CARTESIAN_POINT('Ctrl Pts',(-25.5859532577971,-0.672023850594534,
125.93031417988));
#79244=CARTESIAN_POINT('Ctrl Pts',(-25.5937180107443,-0.807139991270013,
125.95279302585));
#79245=CARTESIAN_POINT('Ctrl Pts',(-25.6014750516293,-0.94212193268977,
125.975249545513));
#79246=CARTESIAN_POINT('Ctrl Pts',(-25.6092320925143,-1.07630706538066,
126.003367079601));
#79247=CARTESIAN_POINT('Ctrl Pts',(-25.6169891333993,-1.20918612928194,
126.037070824901));
#79248=CARTESIAN_POINT('Ctrl Pts',(-25.6247403246395,-1.34196498804748,
126.070749153944));
#79249=CARTESIAN_POINT('Ctrl Pts',(-25.6324915158796,-1.47343936100866,
126.11000521353));
#79250=CARTESIAN_POINT('Ctrl Pts',(-25.6402427071197,-1.60310955722688,
126.154713016938));
#79251=CARTESIAN_POINT('Ctrl Pts',(-25.6479906038968,-1.73272464015265,
126.199401818337));
#79252=CARTESIAN_POINT('Ctrl Pts',(-25.655738500674,-1.86053670264897,126.24953762778));
#79253=CARTESIAN_POINT('Ctrl Pts',(-25.6634863974511,-1.98606083058957,
126.304944495479));
#79254=CARTESIAN_POINT('Ctrl Pts',(-25.6712326735352,-2.11155870158841,
126.360339773255));
#79255=CARTESIAN_POINT('Ctrl Pts',(-25.6789789496193,-2.23476923252213,
126.421003758393));
#79256=CARTESIAN_POINT('Ctrl Pts',(-25.6867252257034,-2.35522750194124,
126.486712359938));
#79257=CARTESIAN_POINT('Ctrl Pts',(-25.6944715589688,-2.47568666055592,
126.552421446529));
#79258=CARTESIAN_POINT('Ctrl Pts',(-25.7022178922341,-2.59339317389404,
126.62317503661));
#79259=CARTESIAN_POINT('Ctrl Pts',(-25.7099642254995,-2.70790709990199,
126.698703276676));
#79260=CARTESIAN_POINT('Ctrl Pts',(-25.7177122935025,-2.82244667050953,
126.774248430769));
#79261=CARTESIAN_POINT('Ctrl Pts',(-25.7254603615054,-2.93379190479616,
126.854570147313));
#79262=CARTESIAN_POINT('Ctrl Pts',(-25.7332084295084,-3.04153253861013,
126.939355717301));
#79263=CARTESIAN_POINT('Ctrl Pts',(-25.7409647322503,-3.14938768045215,
127.024231398402));
#79264=CARTESIAN_POINT('Ctrl Pts',(-25.7487210349921,-3.25363026123202,
127.113580167905));
#79265=CARTESIAN_POINT('Ctrl Pts',(-25.756477337734,-3.35388335743939,127.207049192739));
#79266=CARTESIAN_POINT('Ctrl Pts',(-25.7642377802481,-3.45418996174249,
127.300568104805));
#79267=CARTESIAN_POINT('Ctrl Pts',(-25.7719982227624,-3.55050256422987,
127.398211375895));
#79268=CARTESIAN_POINT('Ctrl Pts',(-25.7797586652765,-3.6424824497096,127.499590630705));
#79269=CARTESIAN_POINT('Ctrl Pts',(-25.787531565542,-3.73460998946734,127.601132628495));
#79270=CARTESIAN_POINT('Ctrl Pts',(-25.7953044658074,-3.82239066288767,
127.706422294122));
#79271=CARTESIAN_POINT('Ctrl Pts',(-25.8030773660728,-3.90552670600746,
127.815038920063));
#79272=CARTESIAN_POINT('Ctrl Pts',(-25.8105677018348,-3.98564054455155,
127.919707058061));
#79273=CARTESIAN_POINT('Ctrl Pts',(-25.8180580375966,-4.0614414008384,128.027464217177));
#79274=CARTESIAN_POINT('Ctrl Pts',(-25.8255483733586,-4.13270281665368,
128.137911575915));
#79275=CARTESIAN_POINT('Ctrl Pts',(-25.833499057336,-4.20834388468305,128.255146914006));
#79276=CARTESIAN_POINT('Ctrl Pts',(-25.8414497413134,-4.27910134301528,
128.375771468827));
#79277=CARTESIAN_POINT('Ctrl Pts',(-25.8494004252908,-4.34466498045625,
128.499351014528));
#79278=CARTESIAN_POINT('Ctrl Pts',(-25.8573410544048,-4.41014570258818,
128.622774274877));
#79279=CARTESIAN_POINT('Ctrl Pts',(-25.8652816835188,-4.4704455054632,128.749144767636));
#79280=CARTESIAN_POINT('Ctrl Pts',(-25.8732223126328,-4.52529716041595,
128.877999106211));
#79281=CARTESIAN_POINT('Ctrl Pts',(-25.8811512875611,-4.58006831149897,
129.006664329746));
#79282=CARTESIAN_POINT('Ctrl Pts',(-25.8890802624895,-4.62940710430368,
129.137805799789));
#79283=CARTESIAN_POINT('Ctrl Pts',(-25.8970092374178,-4.67309232257847,
129.270935951285));
#79284=CARTESIAN_POINT('Ctrl Pts',(-25.9031285387631,-4.70680702307544,
129.373681075656));
#79285=CARTESIAN_POINT('Ctrl Pts',(-25.9092478401083,-4.7371552205288,129.477610126819));
#79286=CARTESIAN_POINT('Ctrl Pts',(-25.9153671414536,-4.76405452823411,
129.582490119308));
#79287=CARTESIAN_POINT('Ctrl Pts',(-24.1652761364937,-4.76405452823407,
129.582490119308));
#79288=CARTESIAN_POINT('Ctrl Pts',(-24.1748731237573,-4.80591458719474,
129.745701853881));
#79289=CARTESIAN_POINT('Ctrl Pts',(-24.1844701110211,-4.8394173052575,129.911198225682));
#79290=CARTESIAN_POINT('Ctrl Pts',(-24.1940670982847,-4.86434929394215,
130.078213931955));
#79291=CARTESIAN_POINT('Ctrl Pts',(-24.2035307701994,-4.8889349430225,130.24290956042));
#79292=CARTESIAN_POINT('Ctrl Pts',(-24.212994442114,-4.90518630260743,130.409082652632));
#79293=CARTESIAN_POINT('Ctrl Pts',(-24.2224581140287,-4.9129445827565,130.575978067305));
#79294=CARTESIAN_POINT('Ctrl Pts',(-24.2266855973436,-4.91641025656448,
130.650531326042));
#79295=CARTESIAN_POINT('Ctrl Pts',(-24.2309130806584,-4.91818178254436,
130.725228431567));
#79296=CARTESIAN_POINT('Ctrl Pts',(-24.2351405639733,-4.91824806745606,
130.800000633076));
#79297=CARTESIAN_POINT('',(-23.8898594359345,-4.91824995370166,130.805035460958));
#79298=CARTESIAN_POINT('Ctrl Pts',(-23.8197459990105,-4.76405452823405,
129.582490119308));
#79299=CARTESIAN_POINT('Ctrl Pts',(-23.8274769694886,-4.79800736229832,
129.714871704019));
#79300=CARTESIAN_POINT('Ctrl Pts',(-23.8352079399666,-4.82641147466578,
129.848565479955));
#79301=CARTESIAN_POINT('Ctrl Pts',(-23.8429389104446,-4.84919130876466,
129.983064864806));
#79302=CARTESIAN_POINT('Ctrl Pts',(-23.8507589980263,-4.87223373251392,
130.119114662461));
#79303=CARTESIAN_POINT('Ctrl Pts',(-23.8585790856079,-4.88952135646728,
130.255988344086));
#79304=CARTESIAN_POINT('Ctrl Pts',(-23.8663991731895,-4.90103010817356,
130.393158792088));
#79305=CARTESIAN_POINT('Ctrl Pts',(-23.8742192607711,-4.91253885987984,
130.53032924009));
#79306=CARTESIAN_POINT('Ctrl Pts',(-23.8820393483529,-4.91826878461024,
130.667796041645));
#79307=CARTESIAN_POINT('Ctrl Pts',(-23.8898594359345,-4.91824995370166,
130.805035460958));
#79308=CARTESIAN_POINT('Ctrl Pts',(-23.8898594359911,-4.91824995370153,
130.805035461952));
#79309=CARTESIAN_POINT('Ctrl Pts',(-23.8919076249367,-4.91824502161922,
130.840980361367));
#79310=CARTESIAN_POINT('Ctrl Pts',(-23.8939558138823,-4.91784604244065,
130.876922193558));
#79311=CARTESIAN_POINT('Ctrl Pts',(-23.896004002828,-4.91705317907111,130.912855302628));
#79312=CARTESIAN_POINT('Ctrl Pts',(-23.903778336947,-4.91404369854502,131.049247014164));
#79313=CARTESIAN_POINT('Ctrl Pts',(-23.911552671066,-4.90535019690039,131.185729447764));
#79314=CARTESIAN_POINT('Ctrl Pts',(-23.9193270051851,-4.89095592581988,
131.321790027425));
#79315=CARTESIAN_POINT('Ctrl Pts',(-23.9270917581322,-4.87657939439202,
131.457682924582));
#79316=CARTESIAN_POINT('Ctrl Pts',(-23.9348565110792,-4.85651611329203,
131.593154617177));
#79317=CARTESIAN_POINT('Ctrl Pts',(-23.9426212640263,-4.83080132585475,
131.727692417419));
#79318=CARTESIAN_POINT('Ctrl Pts',(-23.9503783049113,-4.8051120787068,131.862096592822));
#79319=CARTESIAN_POINT('Ctrl Pts',(-23.9581353457964,-4.77378256857804,
131.99556834022));
#79320=CARTESIAN_POINT('Ctrl Pts',(-23.9658923866814,-4.73689979797866,
132.127600341278));
#79321=CARTESIAN_POINT('Ctrl Pts',(-23.9736435779215,-4.70004484096355,
132.259532775977));
#79322=CARTESIAN_POINT('Ctrl Pts',(-23.9813947691616,-4.65764506371638,
132.390027250377));
#79323=CARTESIAN_POINT('Ctrl Pts',(-23.9891459604017,-4.60983840788225,
132.518587240774));
#79324=CARTESIAN_POINT('Ctrl Pts',(-23.9968938571788,-4.56205207115219,
132.647092589744));
#79325=CARTESIAN_POINT('Ctrl Pts',(-24.0046417539559,-4.50886356249979,
132.773664724337));
#79326=CARTESIAN_POINT('Ctrl Pts',(-24.012389650733,-4.45046041764813,132.897823092378));
#79327=CARTESIAN_POINT('Ctrl Pts',(-24.020135926817,-4.39206948947535,133.021955489166));
#79328=CARTESIAN_POINT('Ctrl Pts',(-24.0278822029011,-4.32846626105303,
133.143674770136));
#79329=CARTESIAN_POINT('Ctrl Pts',(-24.0356284789852,-4.25988591563597,
133.262521525291));
#79330=CARTESIAN_POINT('Ctrl Pts',(-24.0433748122505,-4.19130506397438,
133.381369157745));
#79331=CARTESIAN_POINT('Ctrl Pts',(-24.0511211455159,-4.11774721741212,
133.497343883443));
#79332=CARTESIAN_POINT('Ctrl Pts',(-24.0588674787812,-4.03949270913817,
133.610012362762));
#79333=CARTESIAN_POINT('Ctrl Pts',(-24.0666155467842,-3.96122067630978,
133.722706073405));
#79334=CARTESIAN_POINT('Ctrl Pts',(-24.0743636147871,-3.87825011182596,
133.832091743289));
#79335=CARTESIAN_POINT('Ctrl Pts',(-24.0821116827901,-3.79090347984968,
133.937766730562));
#79336=CARTESIAN_POINT('Ctrl Pts',(-24.0898679855319,-3.70346401483337,
134.04355403047));
#79337=CARTESIAN_POINT('Ctrl Pts',(-24.0976242882737,-3.61163944105797,
134.145622467855));
#79338=CARTESIAN_POINT('Ctrl Pts',(-24.1053805910155,-3.51579153511385,
134.243603694774));
#79339=CARTESIAN_POINT('Ctrl Pts',(-24.1131410335297,-3.41989247225626,
134.341637217224));
#79340=CARTESIAN_POINT('Ctrl Pts',(-24.1209014760439,-3.31996608311959,
134.435578914787));
#79341=CARTESIAN_POINT('Ctrl Pts',(-24.128661918558,-3.21640875939532,134.525099489751));
#79342=CARTESIAN_POINT('Ctrl Pts',(-24.1364348188235,-3.11268519626163,
134.614763771088));
#79343=CARTESIAN_POINT('Ctrl Pts',(-24.1442077190889,-3.00531935733366,
134.699992504184));
#79344=CARTESIAN_POINT('Ctrl Pts',(-24.1519806193543,-2.89473897449381,
134.780498106643));
#79345=CARTESIAN_POINT('Ctrl Pts',(-24.1594709551165,-2.78817846710343,
134.858077127674));
#79346=CARTESIAN_POINT('Ctrl Pts',(-24.1669612908786,-2.67863332783829,
134.931270280489));
#79347=CARTESIAN_POINT('Ctrl Pts',(-24.1744516266408,-2.56650769771754,
134.999860742707));
#79348=CARTESIAN_POINT('Ctrl Pts',(-24.1822259607599,-2.45013079025304,
135.071051833145));
#79349=CARTESIAN_POINT('Ctrl Pts',(-24.1900002948789,-2.33060520349197,
135.137509833129));
#79350=CARTESIAN_POINT('Ctrl Pts',(-24.197774628998,-2.20835312926849,135.198943591973));
#79351=CARTESIAN_POINT('Ctrl Pts',(-24.2055393819451,-2.0862517198005,135.2603016392));
#79352=CARTESIAN_POINT('Ctrl Pts',(-24.2133041348922,-1.96143085455517,
135.316647591517));
#79353=CARTESIAN_POINT('Ctrl Pts',(-24.2210688878393,-1.83434092217407,
135.367733979865));
#79354=CARTESIAN_POINT('Ctrl Pts',(-24.2288259287243,-1.70737721730547,
135.418769628492));
#79355=CARTESIAN_POINT('Ctrl Pts',(-24.2365829696093,-1.57814929061276,
135.46455596402));
#79356=CARTESIAN_POINT('Ctrl Pts',(-24.2443400104943,-1.44713099036155,
135.504891966173));
#79357=CARTESIAN_POINT('Ctrl Pts',(-24.2520912017344,-1.31621149202973,
135.545197550633));
#79358=CARTESIAN_POINT('Ctrl Pts',(-24.2598423929745,-1.18350467964676,
135.580060868129));
#79359=CARTESIAN_POINT('Ctrl Pts',(-24.2675935842147,-1.04950285349737,
135.609329589682));
#79360=CARTESIAN_POINT('Ctrl Pts',(-24.2753414809917,-0.915557981698705,
135.638585871248));
#79361=CARTESIAN_POINT('Ctrl Pts',(-24.2830893777689,-0.780319572028402,
135.662252202986));
#79362=CARTESIAN_POINT('Ctrl Pts',(-24.2908372745459,-0.644293294278856,
135.680226613822));
#79363=CARTESIAN_POINT('Ctrl Pts',(-24.29858355063,-0.508295470294227,135.698197264799));
#79364=CARTESIAN_POINT('Ctrl Pts',(-24.306329826714,-0.371510493386991,
135.710478311914));
#79365=CARTESIAN_POINT('Ctrl Pts',(-24.3140761027981,-0.234452000494012,
135.717019299173));
#79366=CARTESIAN_POINT('Ctrl Pts',(-24.3218224360635,-0.0973924958663737,
135.723560334716));
#79367=CARTESIAN_POINT('Ctrl Pts',(-24.3295687693289,0.0399401382551061,
135.724361207216));
#79368=CARTESIAN_POINT('Ctrl Pts',(-24.3373151025942,0.177029794038206,
135.719423538274));
#79369=CARTESIAN_POINT('Ctrl Pts',(-24.3450631705972,0.314150150099393,
135.714484763576));
#79370=CARTESIAN_POINT('Ctrl Pts',(-24.3528112386002,0.451027028908924,
135.703804904293));
#79371=CARTESIAN_POINT('Ctrl Pts',(-24.3605593066032,0.587147376716695,
135.687437620903));
#79372=CARTESIAN_POINT('Ctrl Pts',(-24.368315609345,0.723412394849784,135.671052942168));
#79373=CARTESIAN_POINT('Ctrl Pts',(-24.3760719120869,0.858918887016169,
135.648968811211));
#79374=CARTESIAN_POINT('Ctrl Pts',(-24.3838282148287,0.993161402573715,
135.62129049986));
#79375=CARTESIAN_POINT('Ctrl Pts',(-24.3915886573429,1.12747556740396,135.593597415761));
#79376=CARTESIAN_POINT('Ctrl Pts',(-24.3993490998571,1.26052403229758,135.560304296705));
#79377=CARTESIAN_POINT('Ctrl Pts',(-24.4071095423712,1.39181549037001,135.521566644789));
#79378=CARTESIAN_POINT('Ctrl Pts',(-24.4148824426367,1.52331770914627,135.482766807755));
#79379=CARTESIAN_POINT('Ctrl Pts',(-24.422655342902,1.6530569145997,135.438505098772));
#79380=CARTESIAN_POINT('Ctrl Pts',(-24.4304282431675,1.78055995598714,135.388985935478));
#79381=CARTESIAN_POINT('Ctrl Pts',(-24.4379185789295,1.90342794066004,135.3412669185));
#79382=CARTESIAN_POINT('Ctrl Pts',(-24.4454089146916,2.02421923662176,135.288666177296));
#79383=CARTESIAN_POINT('Ctrl Pts',(-24.4528992504537,2.1425329769676,135.231406529357));
#79384=CARTESIAN_POINT('Ctrl Pts',(-24.4606735845728,2.26533261873883,135.171975864463));
#79385=CARTESIAN_POINT('Ctrl Pts',(-24.4684479186918,2.3858521155326,135.107337775498));
#79386=CARTESIAN_POINT('Ctrl Pts',(-24.4762222528109,2.50361830903366,135.037690090354));
#79387=CARTESIAN_POINT('Ctrl Pts',(-24.483987005758,2.62123936622628,134.968128239756));
#79388=CARTESIAN_POINT('Ctrl Pts',(-24.4917517587051,2.73611353829486,134.893569274268));
#79389=CARTESIAN_POINT('Ctrl Pts',(-24.4995165116522,2.84778917644996,134.814258355538));
#79390=CARTESIAN_POINT('Ctrl Pts',(-24.5072735525372,2.95935389678676,134.735026209531));
#79391=CARTESIAN_POINT('Ctrl Pts',(-24.5150305934222,3.06772608854799,134.651051727626));
#79392=CARTESIAN_POINT('Ctrl Pts',(-24.5227876343072,3.17248050111997,134.562624915419));
#79393=CARTESIAN_POINT('Ctrl Pts',(-24.5305388255473,3.2771559175747,134.474264786558));
#79394=CARTESIAN_POINT('Ctrl Pts',(-24.5382900167875,3.37821868760179,134.381459261539));
#79395=CARTESIAN_POINT('Ctrl Pts',(-24.5460412080277,3.47527455218835,134.284540188998));
#79396=CARTESIAN_POINT('Ctrl Pts',(-24.5537891048047,3.57228916544327,134.187662309649));
#79397=CARTESIAN_POINT('Ctrl Pts',(-24.5615370015818,3.66529998440791,134.086674635829));
#79398=CARTESIAN_POINT('Ctrl Pts',(-24.5692848983589,3.75394789105644,133.981947484));
#79399=CARTESIAN_POINT('Ctrl Pts',(-24.577031174443,3.84257725447391,133.877242238834));
#79400=CARTESIAN_POINT('Ctrl Pts',(-24.5847774505271,3.92684526840573,133.768799369756));
#79401=CARTESIAN_POINT('Ctrl Pts',(-24.5925237266112,4.00643184948538,133.657023741373));
#79402=CARTESIAN_POINT('Ctrl Pts',(-24.6002700598766,4.0860190180551,133.545247287888));
#79403=CARTESIAN_POINT('Ctrl Pts',(-24.6080163931418,4.16092445805009,133.430138344488));
#79404=CARTESIAN_POINT('Ctrl Pts',(-24.6157627264072,4.23087056487944,133.312132003824));
#79405=CARTESIAN_POINT('Ctrl Pts',(-24.6235107944102,4.30083233565444,133.194099236459));
#79406=CARTESIAN_POINT('Ctrl Pts',(-24.6312588624131,4.36583236397042,133.07316811695));
#79407=CARTESIAN_POINT('Ctrl Pts',(-24.6390069304161,4.42563847782243,132.949799296745));
#79408=CARTESIAN_POINT('Ctrl Pts',(-24.646763233158,4.48550815432402,132.82629935869));
#79409=CARTESIAN_POINT('Ctrl Pts',(-24.6545195358999,4.54017271844043,132.700356896869));
#79410=CARTESIAN_POINT('Ctrl Pts',(-24.6622758386418,4.58944752992524,132.57245406322));
#79411=CARTESIAN_POINT('Ctrl Pts',(-24.6700362811559,4.63874864086059,132.444482963976));
#79412=CARTESIAN_POINT('Ctrl Pts',(-24.6777967236701,4.68265414205246,132.314549778253));
#79413=CARTESIAN_POINT('Ctrl Pts',(-24.6855571661843,4.72102929844848,132.183151909129));
#79414=CARTESIAN_POINT('Ctrl Pts',(-24.6933300664497,4.75946605805232,132.051543108481));
#79415=CARTESIAN_POINT('Ctrl Pts',(-24.7011029667151,4.79235463833192,131.91846530567));
#79416=CARTESIAN_POINT('Ctrl Pts',(-24.7088758669805,4.8196112721016,131.784427068543));
#79417=CARTESIAN_POINT('Ctrl Pts',(-24.7163662027426,4.84587705857844,131.655261458958));
#79418=CARTESIAN_POINT('Ctrl Pts',(-24.7238565385046,4.86691321123197,131.525204335214));
#79419=CARTESIAN_POINT('Ctrl Pts',(-24.7313468742666,4.88269051437392,131.394713396286));
#79420=CARTESIAN_POINT('Ctrl Pts',(-24.7391212083857,4.89906601875989,131.259274853748));
#79421=CARTESIAN_POINT('Ctrl Pts',(-24.7468955425048,4.90982789573741,131.122939921847));
#79422=CARTESIAN_POINT('Ctrl Pts',(-24.7546698766239,4.91488682988674,130.986213612883));
#79423=CARTESIAN_POINT('Ctrl Pts',(-24.762434629571,4.91993952935187,130.849655806875));
#79424=CARTESIAN_POINT('Ctrl Pts',(-24.770199382518,4.91930325602775,130.712707970458));
#79425=CARTESIAN_POINT('Ctrl Pts',(-24.7779641354651,4.91294014415034,130.575882604409));
#79426=CARTESIAN_POINT('Ctrl Pts',(-24.7857211763501,4.90658335220537,130.439193135243));
#79427=CARTESIAN_POINT('Ctrl Pts',(-24.7934782172352,4.89451105908241,130.302626282394));
#79428=CARTESIAN_POINT('Ctrl Pts',(-24.8012352581202,4.87673739635905,130.166696576355));
#79429=CARTESIAN_POINT('Ctrl Pts',(-24.8089864493603,4.858977136893,130.030869375965));
#79430=CARTESIAN_POINT('Ctrl Pts',(-24.8167376406004,4.83552411609995,129.895678752121));
#79431=CARTESIAN_POINT('Ctrl Pts',(-24.8244888318405,4.80644442101107,129.761635778391));
#79432=CARTESIAN_POINT('Ctrl Pts',(-24.8322367286176,4.77737708556832,129.627649776501));
#79433=CARTESIAN_POINT('Ctrl Pts',(-24.8399846253946,4.74268791502992,129.494810835842));
#79434=CARTESIAN_POINT('Ctrl Pts',(-24.8477325221717,4.70249435505845,129.363621257674));
#79435=CARTESIAN_POINT('Ctrl Pts',(-24.8554787982558,4.66230920271324,129.232459121536));
#79436=CARTESIAN_POINT('Ctrl Pts',(-24.8632250743399,4.61662206558767,129.102946035221));
#79437=CARTESIAN_POINT('Ctrl Pts',(-24.870971350424,4.56560055486246,128.975570133137));
#79438=CARTESIAN_POINT('Ctrl Pts',(-24.8787176836893,4.51457866750805,128.848193290793));
#79439=CARTESIAN_POINT('Ctrl Pts',(-24.8864640169547,4.45822247335537,128.722954027093));
#79440=CARTESIAN_POINT('Ctrl Pts',(-24.8942103502201,4.39674797611212,128.600321076847));
#79441=CARTESIAN_POINT('Ctrl Pts',(-24.901958418223,4.33525971208145,128.477660663802));
#79442=CARTESIAN_POINT('Ctrl Pts',(-24.909706486226,4.26865103930964,128.357608075082));
#79443=CARTESIAN_POINT('Ctrl Pts',(-24.917454554229,4.19718402226721,128.240607636929));
#79444=CARTESIAN_POINT('Ctrl Pts',(-24.9252108569708,4.12564104922859,128.123482849318));
#79445=CARTESIAN_POINT('Ctrl Pts',(-24.9329671597127,4.04922962138445,128.009417026417));
#79446=CARTESIAN_POINT('Ctrl Pts',(-24.9407234624545,3.96825558425035,127.898826126192));
#79447=CARTESIAN_POINT('Ctrl Pts',(-24.9484839049687,3.88723832883445,127.788176200273));
#79448=CARTESIAN_POINT('Ctrl Pts',(-24.9562443474829,3.80165385563229,127.681005197974));
#79449=CARTESIAN_POINT('Ctrl Pts',(-24.964004789997,3.71184781635464,127.577695334224));
#79450=CARTESIAN_POINT('Ctrl Pts',(-24.9717776902625,3.62189761245014,127.47421962831));
#79451=CARTESIAN_POINT('Ctrl Pts',(-24.9795505905278,3.52771256897532,127.374617731242));
#79452=CARTESIAN_POINT('Ctrl Pts',(-24.9873234907933,3.42967528025342,127.279235012071));
#79453=CARTESIAN_POINT('Ctrl Pts',(-24.9948138265553,3.33520189391731,127.187319694996));
#79454=CARTESIAN_POINT('Ctrl Pts',(-25.0023041623174,3.23715170664756,127.099322331787));
#79455=CARTESIAN_POINT('Ctrl Pts',(-25.0097944980795,3.13589400176253,127.015514899909));
#79456=CARTESIAN_POINT('Ctrl Pts',(-25.0175688321986,3.03079708022061,126.928529883778));
#79457=CARTESIAN_POINT('Ctrl Pts',(-25.0253431663177,2.92191169818666,126.845783251027));
#79458=CARTESIAN_POINT('Ctrl Pts',(-25.0331175004367,2.80961445964391,126.767623116729));
#79459=CARTESIAN_POINT('Ctrl Pts',(-25.0408822533838,2.69745561741137,126.689559307812));
#79460=CARTESIAN_POINT('Ctrl Pts',(-25.0486470063309,2.58189360279594,126.61607097186));
#79461=CARTESIAN_POINT('Ctrl Pts',(-25.056411759278,2.46333912984626,126.547466985601));
#79462=CARTESIAN_POINT('Ctrl Pts',(-25.064168800163,2.3449024068706,126.478931137787));
#79463=CARTESIAN_POINT('Ctrl Pts',(-25.071925841048,2.22347947647936,126.415270180101));
#79464=CARTESIAN_POINT('Ctrl Pts',(-25.0796828819329,2.09951086621194,126.356750339545));
#79465=CARTESIAN_POINT('Ctrl Pts',(-25.0874340731731,1.97563574163769,126.298274629256));
#79466=CARTESIAN_POINT('Ctrl Pts',(-25.0951852644132,1.84921911038972,126.244932485471));
#79467=CARTESIAN_POINT('Ctrl Pts',(-25.1029364556533,1.72072667479015,126.196944555046));
#79468=CARTESIAN_POINT('Ctrl Pts',(-25.1106843524304,1.59228885190337,126.148977020772));
#79469=CARTESIAN_POINT('Ctrl Pts',(-25.1184322492075,1.46177734492655,126.106359310197));
#79470=CARTESIAN_POINT('Ctrl Pts',(-25.1261801459845,1.32967823638432,126.069264119058));
#79471=CARTESIAN_POINT('Ctrl Pts',(-25.1339264220686,1.19760676012787,126.032176687433));
#79472=CARTESIAN_POINT('Ctrl Pts',(-25.1416726981526,1.0639487190226,126.000609583137));
#79473=CARTESIAN_POINT('Ctrl Pts',(-25.1494189742367,0.929205392309645,
125.974685638708));
#79474=CARTESIAN_POINT('Ctrl Pts',(-25.1571653075021,0.794461070952247,
125.948761502915));
#79475=CARTESIAN_POINT('Ctrl Pts',(-25.1649116407674,0.658631831925272,
125.928480683977));
#79476=CARTESIAN_POINT('Ctrl Pts',(-25.1726579740328,0.522228790380028,
125.913914814472));
#79477=CARTESIAN_POINT('Ctrl Pts',(-25.1804060420357,0.385795202319383,
125.899345683041));
#79478=CARTESIAN_POINT('Ctrl Pts',(-25.1881541100387,0.248787944722713,
125.890494089249));
#79479=CARTESIAN_POINT('Ctrl Pts',(-25.1959021780417,0.111722494090165,
125.887379720022));
#79480=CARTESIAN_POINT('Ctrl Pts',(-25.2036584807836,-0.0254886313346032,
125.884262040806));
#79481=CARTESIAN_POINT('Ctrl Pts',(-25.2114147835254,-0.162757681856225,
125.886893775644));
#79482=CARTESIAN_POINT('Ctrl Pts',(-25.2191710862672,-0.299569383284561,
125.895242443484));
#79483=CARTESIAN_POINT('Ctrl Pts',(-25.2269315287814,-0.436454105237271,
125.90359556726));
#79484=CARTESIAN_POINT('Ctrl Pts',(-25.2346919712955,-0.572880602994445,
125.917671663903));
#79485=CARTESIAN_POINT('Ctrl Pts',(-25.2424524138096,-0.708340475118342,
125.937386523346));
#79486=CARTESIAN_POINT('Ctrl Pts',(-25.2502253140751,-0.844017799454534,
125.957133030831));
#79487=CARTESIAN_POINT('Ctrl Pts',(-25.2579982143405,-0.9787250129254,125.982536317089));
#79488=CARTESIAN_POINT('Ctrl Pts',(-25.265771114606,-1.11196474519111,126.013461175086));
#79489=CARTESIAN_POINT('Ctrl Pts',(-25.2732614503681,-1.24036087757994,
126.043261836601));
#79490=CARTESIAN_POINT('Ctrl Pts',(-25.2807517861302,-1.36739407269115,
126.078189511808));
#79491=CARTESIAN_POINT('Ctrl Pts',(-25.2882421218923,-1.49263590152876,
126.118080522654));
#79492=CARTESIAN_POINT('Ctrl Pts',(-25.2960164560114,-1.62262631237189,
126.159484013301));
#79493=CARTESIAN_POINT('Ctrl Pts',(-25.3037907901305,-1.75109860667504,
126.2063657928));
#79494=CARTESIAN_POINT('Ctrl Pts',(-25.3115651242496,-1.87755634171447,
126.258597178254));
#79495=CARTESIAN_POINT('Ctrl Pts',(-25.3193298771967,-2.00385822889731,
126.310764193193));
#79496=CARTESIAN_POINT('Ctrl Pts',(-25.3270946301438,-2.12815013889102,
126.368267548341));
#79497=CARTESIAN_POINT('Ctrl Pts',(-25.3348593830909,-2.24995020398048,
126.430928653752));
#79498=CARTESIAN_POINT('Ctrl Pts',(-25.3426164239759,-2.37162929552822,
126.49352752327));
#79499=CARTESIAN_POINT('Ctrl Pts',(-25.3503734648609,-2.49082112199857,
126.56127377085));
#79500=CARTESIAN_POINT('Ctrl Pts',(-25.3581305057459,-2.60706358317803,
126.633940670394));
#79501=CARTESIAN_POINT('Ctrl Pts',(-25.365881696986,-2.72321838501295,126.706552771265));
#79502=CARTESIAN_POINT('Ctrl Pts',(-25.3736328882262,-2.83642791839467,
126.784077931768));
#79503=CARTESIAN_POINT('Ctrl Pts',(-25.3813840794663,-2.94625482339331,
126.866243608368));
#79504=CARTESIAN_POINT('Ctrl Pts',(-25.3891319762434,-3.05603504902789,
126.948374362364));
#79505=CARTESIAN_POINT('Ctrl Pts',(-25.3968798730204,-3.16243519337324,
127.0351414759));
#79506=CARTESIAN_POINT('Ctrl Pts',(-25.4046277697975,-3.26504722313634,
127.126229340247));
#79507=CARTESIAN_POINT('Ctrl Pts',(-25.4123740458817,-3.36763778867489,
127.217298150977));
#79508=CARTESIAN_POINT('Ctrl Pts',(-25.4201203219658,-3.46644152354261,
127.31268565541));
#79509=CARTESIAN_POINT('Ctrl Pts',(-25.4278665980499,-3.56108413157174,
127.412036507112));
#79510=CARTESIAN_POINT('Ctrl Pts',(-25.4356129313153,-3.65572743823111,
127.511388092199));
#79511=CARTESIAN_POINT('Ctrl Pts',(-25.4433592645806,-3.74620928709418,
127.614702799855));
#79512=CARTESIAN_POINT('Ctrl Pts',(-25.451105597846,-3.83219314142072,127.721589333583));
#79513=CARTESIAN_POINT('Ctrl Pts',(-25.458853665849,-3.91819625123514,127.82849980381));
#79514=CARTESIAN_POINT('Ctrl Pts',(-25.4666017338519,-3.99969911710219,
127.938983387217));
#79515=CARTESIAN_POINT('Ctrl Pts',(-25.4743498018549,-4.07640654821327,
128.052617040089));
#79516=CARTESIAN_POINT('Ctrl Pts',(-25.4821061045968,-4.15319550489508,
128.166371464161));
#79517=CARTESIAN_POINT('Ctrl Pts',(-25.4898624073387,-4.22517862663083,
128.28328232099));
#79518=CARTESIAN_POINT('Ctrl Pts',(-25.4976187100806,-4.29210472236403,
128.402898539006));
#79519=CARTESIAN_POINT('Ctrl Pts',(-25.5053791525948,-4.35906653856971,
128.522578599799));
#79520=CARTESIAN_POINT('Ctrl Pts',(-25.5131395951089,-4.42096577424825,
128.644966550226));
#79521=CARTESIAN_POINT('Ctrl Pts',(-25.5209000376231,-4.47759847431941,
128.769589140158));
#79522=CARTESIAN_POINT('Ctrl Pts',(-25.5286729378886,-4.53432208622826,
128.894411785335));
#79523=CARTESIAN_POINT('Ctrl Pts',(-25.536445838154,-4.58576212132881,129.021475875867));
#79524=CARTESIAN_POINT('Ctrl Pts',(-25.5442187384194,-4.63176349230904,
129.150289877297));
#79525=CARTESIAN_POINT('Ctrl Pts',(-25.5517090741814,-4.67609259758325,
129.274421165311));
#79526=CARTESIAN_POINT('Ctrl Pts',(-25.5591994099434,-4.71537150014363,
129.400177051728));
#79527=CARTESIAN_POINT('Ctrl Pts',(-25.5666897457053,-4.74950633063405,
129.527108615114));
#79528=CARTESIAN_POINT('Ctrl Pts',(-25.5677773717325,-4.75446284143058,
129.545539574205));
#79529=CARTESIAN_POINT('Ctrl Pts',(-25.5688649977596,-4.7593123489355,129.564000434196));
#79530=CARTESIAN_POINT('Ctrl Pts',(-25.5699526237868,-4.76405452823406,
129.582490119308));
#79531=CARTESIAN_POINT('Origin',(213.235140564004,0.,130.804360617566));
#79532=CARTESIAN_POINT('',(-27.6650164504902,-4.76405452823402,129.582490119308));
#79533=CARTESIAN_POINT('',(-27.320109157184,-4.76405452823409,129.582490119308));
#79534=CARTESIAN_POINT('',(213.235140564004,-4.76405452823405,129.582490119308));
#79535=CARTESIAN_POINT('',(-25.9851405640488,-4.91824961917714,130.806296066854));
#79536=CARTESIAN_POINT('Ctrl Pts',(-25.9851405640487,-4.91824961917714,
130.806296066854));
#79537=CARTESIAN_POINT('Ctrl Pts',(-25.9935514421844,-4.91819087722613,
130.955567649422));
#79538=CARTESIAN_POINT('Ctrl Pts',(-26.0019623203201,-4.91133226515802,
131.104627492812));
#79539=CARTESIAN_POINT('Ctrl Pts',(-26.0103731984557,-4.89775637761353,
131.252875420049));
#79540=CARTESIAN_POINT('Ctrl Pts',(-26.0188206508137,-4.88412145609892,
131.401767994913));
#79541=CARTESIAN_POINT('Ctrl Pts',(-26.0272681031716,-4.86371079700626,
131.549841309758));
#79542=CARTESIAN_POINT('Ctrl Pts',(-26.0357155555295,-4.83665867837743,
131.696501801111));
#79543=CARTESIAN_POINT('Ctrl Pts',(-26.0441815759815,-4.80954709729033,
131.843484662532));
#79544=CARTESIAN_POINT('Ctrl Pts',(-26.0526475964335,-4.77576494785516,
131.989048229664));
#79545=CARTESIAN_POINT('Ctrl Pts',(-26.0611136168855,-4.73549654337785,
132.13261343618));
#79546=CARTESIAN_POINT('Ctrl Pts',(-26.0696079068611,-4.69509367565232,
132.27665803204));
#79547=CARTESIAN_POINT('Ctrl Pts',(-26.0781021968367,-4.64816129120635,
132.41869065189));
#79548=CARTESIAN_POINT('Ctrl Pts',(-26.0865964868123,-4.59493312340749,
132.558148704512));
#79549=CARTESIAN_POINT('Ctrl Pts',(-26.0923963235987,-4.5585893340428,132.653369605386));
#79550=CARTESIAN_POINT('Ctrl Pts',(-26.0981961603851,-4.51931140517969,
132.747390694804));
#79551=CARTESIAN_POINT('Ctrl Pts',(-26.1039959971716,-4.47718591578177,
132.840039702792));
#79552=CARTESIAN_POINT('Ctrl Pts',(-26.1117703312906,-4.42071921825757,
132.964230153389));
#79553=CARTESIAN_POINT('Ctrl Pts',(-26.1195446654097,-4.35899187907983,
133.086266079454));
#79554=CARTESIAN_POINT('Ctrl Pts',(-26.1273189995288,-4.29219031467474,
133.205669711605));
#79555=CARTESIAN_POINT('Ctrl Pts',(-26.1350837524759,-4.22547107722756,
133.32492618945));
#79556=CARTESIAN_POINT('Ctrl Pts',(-26.142848505423,-4.1536902462662,133.441556490185));
#79557=CARTESIAN_POINT('Ctrl Pts',(-26.1506132583701,-4.07708207451369,
133.555103211881));
#79558=CARTESIAN_POINT('Ctrl Pts',(-26.1583702992551,-4.00054999107736,
133.668537157372));
#79559=CARTESIAN_POINT('Ctrl Pts',(-26.16612734014,-3.91920032553539,133.778893296642));
#79560=CARTESIAN_POINT('Ctrl Pts',(-26.1738843810251,-3.8333127951275,133.885739542205));
#79561=CARTESIAN_POINT('Ctrl Pts',(-26.1816355722652,-3.7474900331744,133.992505214183));
#79562=CARTESIAN_POINT('Ctrl Pts',(-26.1893867635054,-3.65713646167303,
134.095765957337));
#79563=CARTESIAN_POINT('Ctrl Pts',(-26.1971379547455,-3.5625743725684,134.195119662738));
#79564=CARTESIAN_POINT('Ctrl Pts',(-26.2048858515226,-3.46805247487416,
134.294431140165));
#79565=CARTESIAN_POINT('Ctrl Pts',(-26.2126337482997,-3.36932588620517,
134.38983860003));
#79566=CARTESIAN_POINT('Ctrl Pts',(-26.2203816450768,-3.26675619853912,
134.480974141151));
#79567=CARTESIAN_POINT('Ctrl Pts',(-26.2281279211609,-3.16420796624058,
134.572090618681));
#79568=CARTESIAN_POINT('Ctrl Pts',(-26.235874197245,-3.05781852601209,134.658936695355));
#79569=CARTESIAN_POINT('Ctrl Pts',(-26.2436204733291,-2.94798494474973,
134.741182664348));
#79570=CARTESIAN_POINT('Ctrl Pts',(-26.2513668065944,-2.83815055272083,
134.823429240462));
#79571=CARTESIAN_POINT('Ctrl Pts',(-26.2591131398598,-2.72487228187536,
134.901075406792));
#79572=CARTESIAN_POINT('Ctrl Pts',(-26.2668594731251,-2.60857843782391,
134.973833197668));
#79573=CARTESIAN_POINT('Ctrl Pts',(-26.2746075411281,-2.49225855057241,
135.046607282146));
#79574=CARTESIAN_POINT('Ctrl Pts',(-26.2823556091311,-2.37292207769225,
135.114490605484));
#79575=CARTESIAN_POINT('Ctrl Pts',(-26.2901036771341,-2.25102396648818,
135.177240008173));
#79576=CARTESIAN_POINT('Ctrl Pts',(-26.297859979876,-2.12899630052091,135.240056101674));
#79577=CARTESIAN_POINT('Ctrl Pts',(-26.3056162826178,-2.0044019058299,135.297727195568));
#79578=CARTESIAN_POINT('Ctrl Pts',(-26.3133725853597,-1.87771836464632,
135.350057132466));
#79579=CARTESIAN_POINT('Ctrl Pts',(-26.3211330278739,-1.75096720864244,
135.402414999426));
#79580=CARTESIAN_POINT('Ctrl Pts',(-26.328893470388,-1.62212505143446,135.44942589511));
#79581=CARTESIAN_POINT('Ctrl Pts',(-26.3366539129022,-1.49168591959197,
135.490943186965));
#79582=CARTESIAN_POINT('Ctrl Pts',(-26.3444268131676,-1.3610373952752,135.532527126062));
#79583=CARTESIAN_POINT('Ctrl Pts',(-26.3521997134331,-1.22878715082634,
135.568599735574));
#79584=CARTESIAN_POINT('Ctrl Pts',(-26.3599726136985,-1.09544159745608,
135.599065068214));
#79585=CARTESIAN_POINT('Ctrl Pts',(-26.3674629494605,-0.9669434908291,135.628422909274));
#79586=CARTESIAN_POINT('Ctrl Pts',(-26.3749532852224,-0.837428629984786,
135.652574016398));
#79587=CARTESIAN_POINT('Ctrl Pts',(-26.3824436209844,-0.707353880997542,
135.671478198798));
#79588=CARTESIAN_POINT('Ctrl Pts',(-26.3902179551035,-0.572347308366123,
135.691099139019));
#79589=CARTESIAN_POINT('Ctrl Pts',(-26.3979922892225,-0.43630989293138,
135.705129579291));
#79590=CARTESIAN_POINT('Ctrl Pts',(-26.4057666233416,-0.299744358236747,
135.713468111012));
#79591=CARTESIAN_POINT('Ctrl Pts',(-26.4135313762887,-0.163347128358413,
135.721796366237));
#79592=CARTESIAN_POINT('Ctrl Pts',(-26.4212961292358,-0.0264234607293649,
135.724446646612));
#79593=CARTESIAN_POINT('Ctrl Pts',(-26.4290608821829,0.11051520013423,135.72136879867));
#79594=CARTESIAN_POINT('Ctrl Pts',(-26.4368179230678,0.247317851589359,
135.718294007689));
#79595=CARTESIAN_POINT('Ctrl Pts',(-26.4445749639529,0.384135078307084,
135.709502419001));
#79596=CARTESIAN_POINT('Ctrl Pts',(-26.4523320048379,0.52045215884695,135.694995812799));
#79597=CARTESIAN_POINT('Ctrl Pts',(-26.460083196078,0.656666441615988,135.680500146142));
#79598=CARTESIAN_POINT('Ctrl Pts',(-26.467834387318,0.792380941732509,135.66029808145));
#79599=CARTESIAN_POINT('Ctrl Pts',(-26.4755855785582,0.927083146898066,
135.634443422367));
#79600=CARTESIAN_POINT('Ctrl Pts',(-26.4833334753352,1.06172810003313,135.608599752205));
#79601=CARTESIAN_POINT('Ctrl Pts',(-26.4910813721124,1.19536123080366,135.577108339589));
#79602=CARTESIAN_POINT('Ctrl Pts',(-26.4988292688894,1.3274775642288,135.540074542516));
#79603=CARTESIAN_POINT('Ctrl Pts',(-26.5065755449735,1.45956626176509,135.503048492116));
#79604=CARTESIAN_POINT('Ctrl Pts',(-26.5143218210576,1.59013841682948,135.460482468722));
#79605=CARTESIAN_POINT('Ctrl Pts',(-26.5220680971417,1.71870201337645,135.412532321367));
#79606=CARTESIAN_POINT('Ctrl Pts',(-26.5298144304071,1.84726655895069,135.364581820056));
#79607=CARTESIAN_POINT('Ctrl Pts',(-26.5375607636724,1.97382215010562,135.311247252101));
#79608=CARTESIAN_POINT('Ctrl Pts',(-26.5453070969378,2.09789500352166,135.252733310664));
#79609=CARTESIAN_POINT('Ctrl Pts',(-26.5530551649407,2.22199564219279,135.194206265435));
#79610=CARTESIAN_POINT('Ctrl Pts',(-26.5608032329437,2.34361208321983,135.130497705424));
#79611=CARTESIAN_POINT('Ctrl Pts',(-26.5685513009467,2.46229383948965,135.061858957027));
#79612=CARTESIAN_POINT('Ctrl Pts',(-26.5763076036885,2.58110173214252,134.993147258551));
#79613=CARTESIAN_POINT('Ctrl Pts',(-26.5840639064303,2.69696837048407,134.919495100546));
#79614=CARTESIAN_POINT('Ctrl Pts',(-26.5918202091721,2.80947057688375,134.841198258607));
#79615=CARTESIAN_POINT('Ctrl Pts',(-26.5995806516863,2.92203282909851,134.762859627286));
#79616=CARTESIAN_POINT('Ctrl Pts',(-26.6073410942005,3.03122676017127,134.67987160885));
#79617=CARTESIAN_POINT('Ctrl Pts',(-26.6151015367147,3.13666197055301,134.592570583366));
#79618=CARTESIAN_POINT('Ctrl Pts',(-26.6228744369801,3.24226643489442,134.505129414526));
#79619=CARTESIAN_POINT('Ctrl Pts',(-26.6306473372456,3.34409983042321,134.413361664914));
#79620=CARTESIAN_POINT('Ctrl Pts',(-26.638420237511,3.44180770633878,134.31764153077));
#79621=CARTESIAN_POINT('Ctrl Pts',(-26.6459105732731,3.53596365485444,134.225401064607));
#79622=CARTESIAN_POINT('Ctrl Pts',(-26.6534009090351,3.62628861113713,134.129490807449));
#79623=CARTESIAN_POINT('Ctrl Pts',(-26.6608912447972,3.71250181426558,134.030273409564));
#79624=CARTESIAN_POINT('Ctrl Pts',(-26.6686655789163,3.80198381719383,133.927294153882));
#79625=CARTESIAN_POINT('Ctrl Pts',(-26.6764399130354,3.8873195698984,133.820425819176));
#79626=CARTESIAN_POINT('Ctrl Pts',(-26.6842142471545,3.96815202009563,133.710036547175));
#79627=CARTESIAN_POINT('Ctrl Pts',(-26.6919790001016,4.0488848515222,133.599783320087));
#79628=CARTESIAN_POINT('Ctrl Pts',(-26.6997437530487,4.12512519436103,133.486018101909));
#79629=CARTESIAN_POINT('Ctrl Pts',(-26.7075085059958,4.19655440482771,133.369144076227));
#79630=CARTESIAN_POINT('Ctrl Pts',(-26.7152655468808,4.26791267079559,133.252386131475));
#79631=CARTESIAN_POINT('Ctrl Pts',(-26.7230225877658,4.33446911122874,133.132525855339));
#79632=CARTESIAN_POINT('Ctrl Pts',(-26.7307796286508,4.39594700434421,133.009997259785));
#79633=CARTESIAN_POINT('Ctrl Pts',(-26.7385308198909,4.45737853650225,132.887561063997));
#79634=CARTESIAN_POINT('Ctrl Pts',(-26.7462820111311,4.5137389696489,132.762460901986));
#79635=CARTESIAN_POINT('Ctrl Pts',(-26.7540332023712,4.56479654489694,132.635157047046));
#79636=CARTESIAN_POINT('Ctrl Pts',(-26.7617810991483,4.6158324193135,132.50790729964));
#79637=CARTESIAN_POINT('Ctrl Pts',(-26.7695289959254,4.66156977334897,132.378456084297));
#79638=CARTESIAN_POINT('Ctrl Pts',(-26.7772768927025,4.70182429635734,132.247285199339));
#79639=CARTESIAN_POINT('Ctrl Pts',(-26.7850231687866,4.74207039898729,132.116141752502));
#79640=CARTESIAN_POINT('Ctrl Pts',(-26.7927694448707,4.77683583718795,131.983279725073));
#79641=CARTESIAN_POINT('Ctrl Pts',(-26.8005157209548,4.80598578447387,131.849197304295));
#79642=CARTESIAN_POINT('Ctrl Pts',(-26.8082620542201,4.83513594693807,131.715113893751));
#79643=CARTESIAN_POINT('Ctrl Pts',(-26.8160083874854,4.85867045271556,131.579810453923));
#79644=CARTESIAN_POINT('Ctrl Pts',(-26.8237547207508,4.87650542450284,131.443796233789));
#79645=CARTESIAN_POINT('Ctrl Pts',(-26.8315027887538,4.89434439030839,131.307751554213));
#79646=CARTESIAN_POINT('Ctrl Pts',(-26.8392508567568,4.9064812314722,131.170996165166));
#79647=CARTESIAN_POINT('Ctrl Pts',(-26.8469989247598,4.9128838967222,131.034044922271));
#79648=CARTESIAN_POINT('Ctrl Pts',(-26.8547552275016,4.91929336680103,130.896948125965));
#79649=CARTESIAN_POINT('Ctrl Pts',(-26.8625115302436,4.91995646855731,130.759655451158));
#79650=CARTESIAN_POINT('Ctrl Pts',(-26.8702678329854,4.9148933085302,130.622682803111));
#79651=CARTESIAN_POINT('Ctrl Pts',(-26.8780282754996,4.90982744614213,130.485637048638));
#79652=CARTESIAN_POINT('Ctrl Pts',(-26.8857887180137,4.89902926284382,130.348912050833));
#79653=CARTESIAN_POINT('Ctrl Pts',(-26.8935491605279,4.88257074422027,130.213018085539));
#79654=CARTESIAN_POINT('Ctrl Pts',(-26.9013220607934,4.86608580492153,130.076905971187));
#79655=CARTESIAN_POINT('Ctrl Pts',(-26.9090949610588,4.84392243587731,129.94162794124));
#79656=CARTESIAN_POINT('Ctrl Pts',(-26.9168678613242,4.81620386966694,129.807684467402));
#79657=CARTESIAN_POINT('Ctrl Pts',(-26.9243581970861,4.78949294315743,129.678610176223));
#79658=CARTESIAN_POINT('Ctrl Pts',(-26.9318485328481,4.75762377267252,129.550775395638));
#79659=CARTESIAN_POINT('Ctrl Pts',(-26.9393388686101,4.72074970801481,129.424612359086));
#79660=CARTESIAN_POINT('Ctrl Pts',(-26.9471132027291,4.6824775519876,129.293665812656));
#79661=CARTESIAN_POINT('Ctrl Pts',(-26.9548875368482,4.63869225410969,129.164105481759));
#79662=CARTESIAN_POINT('Ctrl Pts',(-26.9626618709673,4.5895105469629,129.03643075419));
#79663=CARTESIAN_POINT('Ctrl Pts',(-26.9704266239144,4.54038945187474,128.908913374312));
#79664=CARTESIAN_POINT('Ctrl Pts',(-26.9781913768615,4.48588531940227,128.783277335349));
#79665=CARTESIAN_POINT('Ctrl Pts',(-26.9859561298086,4.4261651245641,128.660008651915));
#79666=CARTESIAN_POINT('Ctrl Pts',(-26.9937131706936,4.36650424466528,128.536862400675));
#79667=CARTESIAN_POINT('Ctrl Pts',(-27.0014702115786,4.30163778151859,128.416079175361));
#79668=CARTESIAN_POINT('Ctrl Pts',(-27.0092272524636,4.23178130679853,128.298126383914));
#79669=CARTESIAN_POINT('Ctrl Pts',(-27.0169784437037,4.16197751138945,128.180262541584));
#79670=CARTESIAN_POINT('Ctrl Pts',(-27.0247296349438,4.08719139286464,128.065225219659));
#79671=CARTESIAN_POINT('Ctrl Pts',(-27.0324808261839,4.00768492084337,127.953458192413));
#79672=CARTESIAN_POINT('Ctrl Pts',(-27.040228722961,3.92821224119373,127.841738669135));
#79673=CARTESIAN_POINT('Ctrl Pts',(-27.0479766197382,3.84402342452957,127.73328699392));
#79674=CARTESIAN_POINT('Ctrl Pts',(-27.0557245165153,3.75542419701934,127.628518656299));
#79675=CARTESIAN_POINT('Ctrl Pts',(-27.0634707925994,3.6668435025574,127.523772233956));
#79676=CARTESIAN_POINT('Ctrl Pts',(-27.0712170686834,3.57385448457397,127.422707915029));
#79677=CARTESIAN_POINT('Ctrl Pts',(-27.0789633447675,3.47680340509713,127.325708415232));
#79678=CARTESIAN_POINT('Ctrl Pts',(-27.0867096780328,3.3797516092114,127.228708199407));
#79679=CARTESIAN_POINT('Ctrl Pts',(-27.0944560112982,3.27863796852657,127.135773138967));
#79680=CARTESIAN_POINT('Ctrl Pts',(-27.1022023445635,3.17384559089952,127.047249063775));
#79681=CARTESIAN_POINT('Ctrl Pts',(-27.1099504125665,3.06902974574608,126.958705164231));
#79682=CARTESIAN_POINT('Ctrl Pts',(-27.1176984805694,2.96053382293475,126.87457446781));
#79683=CARTESIAN_POINT('Ctrl Pts',(-27.1254465485724,2.84877366058778,126.795162232198));
#79684=CARTESIAN_POINT('Ctrl Pts',(-27.1332028513143,2.73689471821015,126.715665596316));
#79685=CARTESIAN_POINT('Ctrl Pts',(-27.1409591540561,2.62174492526147,126.640897665735));
#79686=CARTESIAN_POINT('Ctrl Pts',(-27.148715456798,2.5037691955234,126.57112038365));
#79687=CARTESIAN_POINT('Ctrl Pts',(-27.1564758993121,2.38573049858618,126.501305859328));
#79688=CARTESIAN_POINT('Ctrl Pts',(-27.1642363418263,2.26486320384756,126.43648747575));
#79689=CARTESIAN_POINT('Ctrl Pts',(-27.1719967843405,2.14163553079064,126.376880485961));
#79690=CARTESIAN_POINT('Ctrl Pts',(-27.1797696846059,2.01821004173328,126.317177809741));
#79691=CARTESIAN_POINT('Ctrl Pts',(-27.1875425848713,1.89241696152696,126.262703400281));
#79692=CARTESIAN_POINT('Ctrl Pts',(-27.1953154851368,1.7647439614108,126.213624095703));
#79693=CARTESIAN_POINT('Ctrl Pts',(-27.2028058208989,1.64171219643653,126.16632894747));
#79694=CARTESIAN_POINT('Ctrl Pts',(-27.2102961566609,1.5169351099634,126.124043561736));
#79695=CARTESIAN_POINT('Ctrl Pts',(-27.217786492423,1.39085924154083,126.0868725537));
#79696=CARTESIAN_POINT('Ctrl Pts',(-27.2255608265422,1.2600031682482,126.048292195597));
#79697=CARTESIAN_POINT('Ctrl Pts',(-27.2333351606612,1.12733336950668,126.015099483229));
#79698=CARTESIAN_POINT('Ctrl Pts',(-27.2411094947803,0.993333091223592,
125.98746613747));
#79699=CARTESIAN_POINT('Ctrl Pts',(-27.2488742477274,0.859497956307722,
125.95986684734));
#79700=CARTESIAN_POINT('Ctrl Pts',(-27.2566390006746,0.724335983591141,
125.937813369736));
#79701=CARTESIAN_POINT('Ctrl Pts',(-27.2644037536217,0.588346325010557,
125.921427926616));
#79702=CARTESIAN_POINT('Ctrl Pts',(-27.2721607945067,0.452491733275992,
125.905058757749));
#79703=CARTESIAN_POINT('Ctrl Pts',(-27.2799178353917,0.315811477278347,
125.894346466732));
#79704=CARTESIAN_POINT('Ctrl Pts',(-27.2876748762767,0.178815322311946,
125.889362332418));
#79705=CARTESIAN_POINT('Ctrl Pts',(-27.2954260675168,0.0419224772116804,
125.884381956679));
#79706=CARTESIAN_POINT('Ctrl Pts',(-27.3031772587569,-0.0952854035653323,
125.885121153803));
#79707=CARTESIAN_POINT('Ctrl Pts',(-27.3109284499971,-0.232293359175477,
125.891599392167));
#79708=CARTESIAN_POINT('Ctrl Pts',(-27.3186763467742,-0.369243082749681,
125.898074877107));
#79709=CARTESIAN_POINT('Ctrl Pts',(-27.3264242435513,-0.505992660451609,
125.910284533385));
#79710=CARTESIAN_POINT('Ctrl Pts',(-27.3341721403284,-0.642027276711597,
125.928195727157));
#79711=CARTESIAN_POINT('Ctrl Pts',(-27.3419184164125,-0.77803343746243,
125.946103174293));
#79712=CARTESIAN_POINT('Ctrl Pts',(-27.3496646924965,-0.913324546869294,
125.969709735695));
#79713=CARTESIAN_POINT('Ctrl Pts',(-27.3574109685806,-1.04739145227851,
125.998930958504));
#79714=CARTESIAN_POINT('Ctrl Pts',(-27.365157301846,-1.18145934733917,126.028152397017));
#79715=CARTESIAN_POINT('Ctrl Pts',(-27.3729036351113,-1.3143026383731,126.06298849638));
#79716=CARTESIAN_POINT('Ctrl Pts',(-27.3806499683767,-1.44542328976766,
126.10330386659));
#79717=CARTESIAN_POINT('Ctrl Pts',(-27.3883980363797,-1.5765733047228,126.143628265148));
#79718=CARTESIAN_POINT('Ctrl Pts',(-27.3961461043827,-1.70599953876617,
126.189434261352));
#79719=CARTESIAN_POINT('Ctrl Pts',(-27.4038941723857,-1.83322039930074,
126.240536998046));
#79720=CARTESIAN_POINT('Ctrl Pts',(-27.4116504751275,-1.96057647168002,
126.291694047337));
#79721=CARTESIAN_POINT('Ctrl Pts',(-27.4194067778694,-2.08572212499398,
126.34815893657));
#79722=CARTESIAN_POINT('Ctrl Pts',(-27.4271630806113,-2.20819649224858,
126.409698933873));
#79723=CARTESIAN_POINT('Ctrl Pts',(-27.4349235231255,-2.33073622776078,
126.471271776925));
#79724=CARTESIAN_POINT('Ctrl Pts',(-27.4426839656396,-2.45060149477074,
126.537924935528));
#79725=CARTESIAN_POINT('Ctrl Pts',(-27.4504444081538,-2.56735811072846,
126.609380832898));
#79726=CARTESIAN_POINT('Ctrl Pts',(-27.4582173084192,-2.68430215477111,
126.680951437617));
#79727=CARTESIAN_POINT('Ctrl Pts',(-27.4659902086847,-2.79812725076357,
126.757339969715));
#79728=CARTESIAN_POINT('Ctrl Pts',(-27.4737631089501,-2.90842943485161,
126.838226317648));
#79729=CARTESIAN_POINT('Ctrl Pts',(-27.4812534447121,-3.01472185671256,
126.916172243092));
#79730=CARTESIAN_POINT('Ctrl Pts',(-27.488743780474,-3.11774281240201,126.998294455943));
#79731=CARTESIAN_POINT('Ctrl Pts',(-27.4962341162359,-3.21716292065497,
127.084273816904));
#79732=CARTESIAN_POINT('Ctrl Pts',(-27.5038934172043,-3.31882572398132,
127.172192679768));
#79733=CARTESIAN_POINT('Ctrl Pts',(-27.5115527181727,-3.41706547671011,
127.264441057515));
#79734=CARTESIAN_POINT('Ctrl Pts',(-27.519212019141,-3.51148264535747,127.360718258979));
#79735=CARTESIAN_POINT('Ctrl Pts',(-27.5268625104388,-3.6057912160842,127.456884723127));
#79736=CARTESIAN_POINT('Ctrl Pts',(-27.5345130017364,-3.69628566326201,
127.557070515036));
#79737=CARTESIAN_POINT('Ctrl Pts',(-27.5421634930342,-3.78259884884492,
127.660934300437));
#79738=CARTESIAN_POINT('Ctrl Pts',(-27.5498069570394,-3.86883275219898,
127.764702682658));
#79739=CARTESIAN_POINT('Ctrl Pts',(-27.5574504210446,-3.95089277429838,
127.872142033216));
#79740=CARTESIAN_POINT('Ctrl Pts',(-27.5650938850498,-4.02844845775133,
127.98287411472));
#79741=CARTESIAN_POINT('Ctrl Pts',(-27.5727320974051,-4.10595085446164,
128.093530114735));
#79742=CARTESIAN_POINT('Ctrl Pts',(-27.5803703097604,-4.1789548374162,128.207474016999));
#79743=CARTESIAN_POINT('Ctrl Pts',(-27.5880085221157,-4.2471704704547,128.324294881059));
#79744=CARTESIAN_POINT('Ctrl Pts',(-27.5956438189238,-4.31536006521479,
128.441071153959));
#79745=CARTESIAN_POINT('Ctrl Pts',(-27.6032791157318,-4.37876474033592,
128.560721857964));
#79746=CARTESIAN_POINT('Ctrl Pts',(-27.6109144125398,-4.43713837373944,
128.682807857254));
#79747=CARTESIAN_POINT('Ctrl Pts',(-27.6185480443435,-4.49549927779408,
128.804867233646));
#79748=CARTESIAN_POINT('Ctrl Pts',(-27.6261816761471,-4.54883115212521,
128.929360483547));
#79749=CARTESIAN_POINT('Ctrl Pts',(-27.6338153079508,-4.59693455979449,
129.055825311812));
#79750=CARTESIAN_POINT('Ctrl Pts',(-27.6414504912618,-4.64504774430282,
129.182315843585));
#79751=CARTESIAN_POINT('Ctrl Pts',(-27.6490856745728,-4.68793019774338,
129.310778376485));
#79752=CARTESIAN_POINT('Ctrl Pts',(-27.6567208578838,-4.72543132371363,
129.440732417738));
#79753=CARTESIAN_POINT('Ctrl Pts',(-27.6594860554192,-4.73901292573772,
129.487797246435));
#79754=CARTESIAN_POINT('Ctrl Pts',(-27.6622512529547,-4.75188916809314,
129.535057564754));
#79755=CARTESIAN_POINT('Ctrl Pts',(-27.6650164504902,-4.76405452823402,
129.582490119308));
#79756=CARTESIAN_POINT('Ctrl Pts',(-25.9153671414536,-4.76405452823411,
129.582490119308));
#79757=CARTESIAN_POINT('Ctrl Pts',(-25.923282705383,-4.79884987132734,129.718156633936));
#79758=CARTESIAN_POINT('Ctrl Pts',(-25.9311982693124,-4.82787263050501,
129.855414641848));
#79759=CARTESIAN_POINT('Ctrl Pts',(-25.9391138332419,-4.85098804002467,
129.993744741804));
#79760=CARTESIAN_POINT('Ctrl Pts',(-25.9470236550876,-4.87408668123604,
130.13197449477));
#79761=CARTESIAN_POINT('Ctrl Pts',(-25.9549334769334,-4.89128645037956,
130.271274429011));
#79762=CARTESIAN_POINT('Ctrl Pts',(-25.9628432987791,-4.90250346835763,
130.411114123314));
#79763=CARTESIAN_POINT('Ctrl Pts',(-25.9702757205222,-4.9130434792377,130.542513743276));
#79764=CARTESIAN_POINT('Ctrl Pts',(-25.9777081422654,-4.91830152752587,
130.67438958289));
#79765=CARTESIAN_POINT('Ctrl Pts',(-25.9851405640086,-4.91824961917742,
130.806296066141));
#79766=CARTESIAN_POINT('',(-25.6398594359502,-4.91824793218808,130.799850625585));
#79767=CARTESIAN_POINT('Ctrl Pts',(-25.5699526237868,-4.76405452823406,
129.582490119308));
#79768=CARTESIAN_POINT('Ctrl Pts',(-25.5799243591641,-4.80753248471586,
129.752010011761));
#79769=CARTESIAN_POINT('Ctrl Pts',(-25.5898960945415,-4.84198469666304,
129.923954638454));
#79770=CARTESIAN_POINT('Ctrl Pts',(-25.5998678299188,-4.86718685273507,
130.097483539806));
#79771=CARTESIAN_POINT('Ctrl Pts',(-25.6096542149229,-4.891920561856,130.267786959792));
#79772=CARTESIAN_POINT('Ctrl Pts',(-25.6194405999269,-4.9077449112389,130.439616485704));
#79773=CARTESIAN_POINT('Ctrl Pts',(-25.6292269849311,-4.91449288853822,
130.612155750283));
#79774=CARTESIAN_POINT('Ctrl Pts',(-25.6327711352708,-4.9169366761092,130.674641039071));
#79775=CARTESIAN_POINT('Ctrl Pts',(-25.6363152856105,-4.91819049968701,
130.737219188364));
#79776=CARTESIAN_POINT('Ctrl Pts',(-25.6398594359502,-4.91824793218808,
130.799850625585));
#79777=CARTESIAN_POINT('Ctrl Pts',(-25.6398594359912,-4.91824793218874,
130.799850626309));
#79778=CARTESIAN_POINT('Ctrl Pts',(-25.6475321901618,-4.91837226816469,
130.935441832968));
#79779=CARTESIAN_POINT('Ctrl Pts',(-25.6552049443324,-4.91288521422851,
131.071167098629));
#79780=CARTESIAN_POINT('Ctrl Pts',(-25.6628776985029,-4.90178036831504,
131.206520142259));
#79781=CARTESIAN_POINT('Ctrl Pts',(-25.6705464539726,-4.89068130975733,
131.341802645854));
#79782=CARTESIAN_POINT('Ctrl Pts',(-25.6782152094422,-4.87397031425118,
131.476712915772));
#79783=CARTESIAN_POINT('Ctrl Pts',(-25.6858839649119,-4.85169305430979,
131.61074611425));
#79784=CARTESIAN_POINT('Ctrl Pts',(-25.6935507019143,-4.82942165789072,
131.744744034302));
#79785=CARTESIAN_POINT('Ctrl Pts',(-25.7012174389168,-4.80158697541088,
131.877864947818));
#79786=CARTESIAN_POINT('Ctrl Pts',(-25.7088841759192,-4.7682863246519,132.009611043261));
#79787=CARTESIAN_POINT('Ctrl Pts',(-25.7165506385416,-4.73498686566862,
132.141352423727));
#79788=CARTESIAN_POINT('Ctrl Pts',(-25.7242171011641,-4.69622192537889,
132.271718696317));
#79789=CARTESIAN_POINT('Ctrl Pts',(-25.7318835637865,-4.65213941487484,
132.400224624011));
#79790=CARTESIAN_POINT('Ctrl Pts',(-25.7395514956454,-4.60804845619458,
132.528755179176));
#79791=CARTESIAN_POINT('Ctrl Pts',(-25.7472194275042,-4.55863803045239,
132.655424302297));
#79792=CARTESIAN_POINT('Ctrl Pts',(-25.754887359363,-4.5041049791734,132.77976472789));
#79793=CARTESIAN_POINT('Ctrl Pts',(-25.7625632282976,-4.44951548073676,
132.904233858249));
#79794=CARTESIAN_POINT('Ctrl Pts',(-25.7702390972321,-4.3897929272935,133.026369110101));
#79795=CARTESIAN_POINT('Ctrl Pts',(-25.7779149661667,-4.32518130200142,
133.145725554375));
#79796=CARTESIAN_POINT('Ctrl Pts',(-25.7855948590658,-4.26053580498894,
133.265144569557));
#79797=CARTESIAN_POINT('Ctrl Pts',(-25.7932747519649,-4.19099633650859,
133.381781532978));
#79798=CARTESIAN_POINT('Ctrl Pts',(-25.8009546448639,-4.11685074135035,
133.495219780722));
#79799=CARTESIAN_POINT('Ctrl Pts',(-25.8086467760269,-4.04258699176298,
133.608838797552));
#79800=CARTESIAN_POINT('Ctrl Pts',(-25.8163389071898,-3.96370268422352,
133.71924859037));
#79801=CARTESIAN_POINT('Ctrl Pts',(-25.8240310383528,-3.88052698662211,
133.826064337092));
#79802=CARTESIAN_POINT('Ctrl Pts',(-25.8310664820746,-3.80445210865978,
133.923761081822));
#79803=CARTESIAN_POINT('Ctrl Pts',(-25.8381019257964,-3.72478791801777,
134.018451483989));
#79804=CARTESIAN_POINT('Ctrl Pts',(-25.8451373695182,-3.64181246816916,
134.109868900597));
#79805=CARTESIAN_POINT('Ctrl Pts',(-25.8529117036373,-3.55012260519602,
134.210887339394));
#79806=CARTESIAN_POINT('Ctrl Pts',(-25.8606860377563,-3.45408117576585,
134.308247883175));
#79807=CARTESIAN_POINT('Ctrl Pts',(-25.8684603718754,-3.35401157386546,
134.40155249803));
#79808=CARTESIAN_POINT('Ctrl Pts',(-25.8762251248225,-3.2540652988062,134.494742123286));
#79809=CARTESIAN_POINT('Ctrl Pts',(-25.8839898777696,-3.15010101208414,
134.583885501219));
#79810=CARTESIAN_POINT('Ctrl Pts',(-25.8917546307167,-3.0424814406506,134.668618598834));
#79811=CARTESIAN_POINT('Ctrl Pts',(-25.8995116716017,-2.93496875849244,
134.753267538343));
#79812=CARTESIAN_POINT('Ctrl Pts',(-25.9072687124867,-2.82380832163516,
134.833514674342));
#79813=CARTESIAN_POINT('Ctrl Pts',(-25.9150257533717,-2.70939842098782,
134.909033961311));
#79814=CARTESIAN_POINT('Ctrl Pts',(-25.9227769446118,-2.59507479773668,
134.984496298598));
#79815=CARTESIAN_POINT('Ctrl Pts',(-25.9305281358518,-2.477506913131,135.055237668877));
#79816=CARTESIAN_POINT('Ctrl Pts',(-25.9382793270919,-2.35712444610986,
135.120973573119));
#79817=CARTESIAN_POINT('Ctrl Pts',(-25.946027223869,-2.23679314484834,135.186681537849));
#79818=CARTESIAN_POINT('Ctrl Pts',(-25.9537751206461,-2.11364998288739,
135.247388080909));
#79819=CARTESIAN_POINT('Ctrl Pts',(-25.9615230174232,-1.98815161758541,
135.302853277112));
#79820=CARTESIAN_POINT('Ctrl Pts',(-25.9692692935073,-1.86267950383601,
135.358306871192));
#79821=CARTESIAN_POINT('Ctrl Pts',(-25.9770155695914,-1.73485352403987,
135.408521141224));
#79822=CARTESIAN_POINT('Ctrl Pts',(-25.9847618456755,-1.60515245427527,
135.453303364152));
#79823=CARTESIAN_POINT('Ctrl Pts',(-25.9925081789408,-1.47545042708684,
135.498085917652));
#79824=CARTESIAN_POINT('Ctrl Pts',(-26.0002545122062,-1.34387365186748,
135.537436216435));
#79825=CARTESIAN_POINT('Ctrl Pts',(-26.0080008454715,-1.21091790655001,
135.57121082353));
#79826=CARTESIAN_POINT('Ctrl Pts',(-26.0157489134745,-1.07793238671522,
135.604992994213));
#79827=CARTESIAN_POINT('Ctrl Pts',(-26.0234969814775,-0.943567661142076,
135.633196892322));
#79828=CARTESIAN_POINT('Ctrl Pts',(-26.0312450494805,-0.808331196273148,
135.655729881973));
#79829=CARTESIAN_POINT('Ctrl Pts',(-26.0390013522223,-0.672951000480024,
135.678286819953));
#79830=CARTESIAN_POINT('Ctrl Pts',(-26.046757654964,-0.536697600881362,
135.695160745317));
#79831=CARTESIAN_POINT('Ctrl Pts',(-26.0545139577059,-0.400085666502281,
135.706310690951));
#79832=CARTESIAN_POINT('Ctrl Pts',(-26.0622744002201,-0.263400818220329,
135.717466587647));
#79833=CARTESIAN_POINT('Ctrl Pts',(-26.0700348427343,-0.126357444323342,
135.722892401686));
#79834=CARTESIAN_POINT('Ctrl Pts',(-26.0777952852485,0.0105292488120982,
135.722599346768));
#79835=CARTESIAN_POINT('Ctrl Pts',(-26.0855681855139,0.147635684619589,
135.722305821411));
#79836=CARTESIAN_POINT('Ctrl Pts',(-26.0933410857793,0.284584546241221,
135.716275098869));
#79837=CARTESIAN_POINT('Ctrl Pts',(-26.1011139860448,0.42086431009477,135.704570439093));
#79838=CARTESIAN_POINT('Ctrl Pts',(-26.1086043218068,0.552189961265159,
135.693291273182));
#79839=CARTESIAN_POINT('Ctrl Pts',(-26.116094657569,0.682894011287214,135.676743570525));
#79840=CARTESIAN_POINT('Ctrl Pts',(-26.123584993331,0.812529140113618,135.655028557032));
#79841=CARTESIAN_POINT('Ctrl Pts',(-26.1313593274501,0.947079424250089,
135.632490212203));
#79842=CARTESIAN_POINT('Ctrl Pts',(-26.1391336615691,1.08090434567657,135.604313589666));
#79843=CARTESIAN_POINT('Ctrl Pts',(-26.1469079956882,1.21349422484095,135.57055562289));
#79844=CARTESIAN_POINT('Ctrl Pts',(-26.1546727486353,1.34592069882933,135.536839259791));
#79845=CARTESIAN_POINT('Ctrl Pts',(-26.1624375015824,1.47711478379883,135.497555334171));
#79846=CARTESIAN_POINT('Ctrl Pts',(-26.1702022545295,1.60657414570291,135.452812249761));
#79847=CARTESIAN_POINT('Ctrl Pts',(-26.1779592954145,1.73590492674369,135.408113604814));
#79848=CARTESIAN_POINT('Ctrl Pts',(-26.1857163362995,1.86350404634305,135.357966718211));
#79849=CARTESIAN_POINT('Ctrl Pts',(-26.1934733771845,1.98888190720445,135.302530447807));
#79850=CARTESIAN_POINT('Ctrl Pts',(-26.2012245684247,2.11416521964568,135.247135982326));
#79851=CARTESIAN_POINT('Ctrl Pts',(-26.2089757596649,2.23723025134615,135.186460229902));
#79852=CARTESIAN_POINT('Ctrl Pts',(-26.216726950905,2.35760539325344,135.12071091292));
#79853=CARTESIAN_POINT('Ctrl Pts',(-26.2244748476821,2.47792937251415,135.054989541152));
#79854=CARTESIAN_POINT('Ctrl Pts',(-26.2322227444591,2.59556539346812,134.984199080762));
#79855=CARTESIAN_POINT('Ctrl Pts',(-26.2399706412362,2.71006476580336,134.908594045096));
#79856=CARTESIAN_POINT('Ctrl Pts',(-26.2477169173203,2.82454018733822,134.833004824373));
#79857=CARTESIAN_POINT('Ctrl Pts',(-26.2554631934044,2.93587993926146,134.752603246854));
#79858=CARTESIAN_POINT('Ctrl Pts',(-26.2632094694885,3.0436630880413,134.667687948895));
#79859=CARTESIAN_POINT('Ctrl Pts',(-26.2709558027539,3.15144703245185,134.58277202411));
#79860=CARTESIAN_POINT('Ctrl Pts',(-26.2787021360192,3.25567401422449,134.493342554348));
#79861=CARTESIAN_POINT('Ctrl Pts',(-26.2864484692846,3.35595537568815,134.399739120435));
#79862=CARTESIAN_POINT('Ctrl Pts',(-26.2941965372875,3.45625919446753,134.306114724682));
#79863=CARTESIAN_POINT('Ctrl Pts',(-26.3019446052905,3.55261534893573,134.208314771496));
#79864=CARTESIAN_POINT('Ctrl Pts',(-26.3096926732935,3.64467160389241,134.106716134811));
#79865=CARTESIAN_POINT('Ctrl Pts',(-26.3174489760354,3.73682569733222,134.005009517886));
#79866=CARTESIAN_POINT('Ctrl Pts',(-26.3252052787772,3.82467049929258,133.899496442735));
#79867=CARTESIAN_POINT('Ctrl Pts',(-26.332961581519,3.90789335180106,133.790587771258));
#79868=CARTESIAN_POINT('Ctrl Pts',(-26.3407220240332,3.99116062285183,133.681620971944));
#79869=CARTESIAN_POINT('Ctrl Pts',(-26.3484824665474,4.0698008049323,133.569255285236));
#79870=CARTESIAN_POINT('Ctrl Pts',(-26.3562429090615,4.14354485081241,133.453930230127));
#79871=CARTESIAN_POINT('Ctrl Pts',(-26.364015809327,4.21740727718156,133.338420045001));
#79872=CARTESIAN_POINT('Ctrl Pts',(-26.3717887095925,4.28635766437638,133.219941336283));
#79873=CARTESIAN_POINT('Ctrl Pts',(-26.3795616098579,4.35017274379426,133.098958656798));
#79874=CARTESIAN_POINT('Ctrl Pts',(-26.3870519456199,4.4116679843349,132.98237400245));
#79875=CARTESIAN_POINT('Ctrl Pts',(-26.3945422813819,4.46839466509504,132.86346454595));
#79876=CARTESIAN_POINT('Ctrl Pts',(-26.4020326171439,4.52019616288691,132.7426613454));
#79877=CARTESIAN_POINT('Ctrl Pts',(-26.409806951263,4.5739617302122,132.617277854784));
#79878=CARTESIAN_POINT('Ctrl Pts',(-26.4175812853821,4.62259157855505,132.489457005536));
#79879=CARTESIAN_POINT('Ctrl Pts',(-26.4253556195011,4.66585811340718,132.359658379428));
#79880=CARTESIAN_POINT('Ctrl Pts',(-26.4331203724482,4.70907132612194,132.230019718526));
#79881=CARTESIAN_POINT('Ctrl Pts',(-26.4408851253953,4.74693425443892,132.098408497871));
#79882=CARTESIAN_POINT('Ctrl Pts',(-26.4486498783424,4.77926657766478,131.965305940187));
#79883=CARTESIAN_POINT('Ctrl Pts',(-26.4564069192274,4.81156678797144,131.83233558184));
#79884=CARTESIAN_POINT('Ctrl Pts',(-26.4641639601125,4.83834723296443,131.697877211612));
#79885=CARTESIAN_POINT('Ctrl Pts',(-26.4719210009975,4.8594769249571,131.562428608125));
#79886=CARTESIAN_POINT('Ctrl Pts',(-26.4796721922376,4.88059068288468,131.427082147482));
#79887=CARTESIAN_POINT('Ctrl Pts',(-26.4874233834778,4.89606210960789,131.290747324657));
#79888=CARTESIAN_POINT('Ctrl Pts',(-26.4951745747179,4.90581105164078,131.153933196724));
#79889=CARTESIAN_POINT('Ctrl Pts',(-26.502922471495,4.91555585011323,131.017177218445));
#79890=CARTESIAN_POINT('Ctrl Pts',(-26.510670368272,4.91958297364262,130.879942729398));
#79891=CARTESIAN_POINT('Ctrl Pts',(-26.5184182650491,4.91786402344031,130.742744796128));
#79892=CARTESIAN_POINT('Ctrl Pts',(-26.5261645411332,4.91614543280533,130.605575561708));
#79893=CARTESIAN_POINT('Ctrl Pts',(-26.5339108172173,4.90868316408747,130.468443258544));
#79894=CARTESIAN_POINT('Ctrl Pts',(-26.5416570933014,4.89550094365343,130.331863450179));
#79895=CARTESIAN_POINT('Ctrl Pts',(-26.5494034265667,4.88231862591124,130.195282633614));
#79896=CARTESIAN_POINT('Ctrl Pts',(-26.557149759832,4.86341630975927,130.059254709144));
#79897=CARTESIAN_POINT('Ctrl Pts',(-26.5648960930973,4.83886961520092,129.924290217209));
#79898=CARTESIAN_POINT('Ctrl Pts',(-26.5726441611003,4.81431742358058,129.789295500911));
#79899=CARTESIAN_POINT('Ctrl Pts',(-26.5803922291033,4.78411840824743,129.655365075616));
#79900=CARTESIAN_POINT('Ctrl Pts',(-26.5881402971062,4.74839925218484,129.52299899634));
#79901=CARTESIAN_POINT('Ctrl Pts',(-26.5958965998481,4.71264213337798,129.39049223682));
#79902=CARTESIAN_POINT('Ctrl Pts',(-26.6036529025899,4.67135325615571,129.259553522617));
#79903=CARTESIAN_POINT('Ctrl Pts',(-26.6114092053318,4.62470929100075,129.130667982632));
#79904=CARTESIAN_POINT('Ctrl Pts',(-26.6191696478459,4.5780404305571,129.001713652554));
#79905=CARTESIAN_POINT('Ctrl Pts',(-26.6269300903601,4.52601093527567,128.874815041814));
#79906=CARTESIAN_POINT('Ctrl Pts',(-26.6346905328743,4.46884515833365,128.750436078218));
#79907=CARTESIAN_POINT('Ctrl Pts',(-26.6424634331397,4.41158761381155,128.625857450467));
#79908=CARTESIAN_POINT('Ctrl Pts',(-26.6502363334052,4.34917748916139,128.503806900878));
#79909=CARTESIAN_POINT('Ctrl Pts',(-26.6580092336706,4.28188494369869,128.384723373799));
#79910=CARTESIAN_POINT('Ctrl Pts',(-26.6654995694327,4.2170386517627,128.269968832881));
#79911=CARTESIAN_POINT('Ctrl Pts',(-26.6729899051948,4.14765891489515,128.15796960401));
#79912=CARTESIAN_POINT('Ctrl Pts',(-26.6804802409569,4.0740237358259,128.049090456143));
#79913=CARTESIAN_POINT('Ctrl Pts',(-26.688254575076,3.99759665656185,127.936083122292));
#79914=CARTESIAN_POINT('Ctrl Pts',(-26.696028909195,3.91634297689393,127.826079162396));
#79915=CARTESIAN_POINT('Ctrl Pts',(-26.7038032433141,3.83052633559218,127.719518473333));
#79916=CARTESIAN_POINT('Ctrl Pts',(-26.7115679962612,3.74481545563165,127.613089110797));
#79917=CARTESIAN_POINT('Ctrl Pts',(-26.7193327492083,3.6545530458801,127.510094877324));
#79918=CARTESIAN_POINT('Ctrl Pts',(-26.7270975021554,3.56004650490541,127.410947594456));
#79919=CARTESIAN_POINT('Ctrl Pts',(-26.7348545430404,3.46563382915901,127.311898786068));
#79920=CARTESIAN_POINT('Ctrl Pts',(-26.7426115839254,3.36698567889441,127.216689605797));
#79921=CARTESIAN_POINT('Ctrl Pts',(-26.7503686248104,3.26445004731979,127.125699318798));
#79922=CARTESIAN_POINT('Ctrl Pts',(-26.7581198160506,3.16199173866268,127.034777648283));
#79923=CARTESIAN_POINT('Ctrl Pts',(-26.7658710072906,3.05565207507122,126.948068796906));
#79924=CARTESIAN_POINT('Ctrl Pts',(-26.7736221985307,2.94581601576378,126.865915357851));
#79925=CARTESIAN_POINT('Ctrl Pts',(-26.7813700953078,2.83602663971152,126.783796836199));
#79926=CARTESIAN_POINT('Ctrl Pts',(-26.789117992085,2.72274413602858,126.706230109651));
#79927=CARTESIAN_POINT('Ctrl Pts',(-26.7968658888621,2.6063864945491,126.633517476961));
#79928=CARTESIAN_POINT('Ctrl Pts',(-26.8046121649462,2.49005319257984,126.560820054186));
#79929=CARTESIAN_POINT('Ctrl Pts',(-26.8123584410303,2.37064636362032,126.492974912698));
#79930=CARTESIAN_POINT('Ctrl Pts',(-26.8201047171144,2.24861259056381,126.430240765521));
#79931=CARTESIAN_POINT('Ctrl Pts',(-26.8278510503798,2.12657791668171,126.367506155254));
#79932=CARTESIAN_POINT('Ctrl Pts',(-26.8355973836451,2.00191660771909,126.309882793331));
#79933=CARTESIAN_POINT('Ctrl Pts',(-26.8433437169105,1.87509907026491,126.25758301808));
#79934=CARTESIAN_POINT('Ctrl Pts',(-26.8510917849134,1.74825313290234,126.205271530656));
#79935=CARTESIAN_POINT('Ctrl Pts',(-26.8588398529165,1.61925036755467,126.158286151231));
#79936=CARTESIAN_POINT('Ctrl Pts',(-26.8665879209194,1.48857995991605,126.116790589776));
#79937=CARTESIAN_POINT('Ctrl Pts',(-26.8743442236613,1.35777067421338,126.075250926344));
#79938=CARTESIAN_POINT('Ctrl Pts',(-26.8821005264031,1.22529057890167,126.03921285473));
#79939=CARTESIAN_POINT('Ctrl Pts',(-26.889856829145,1.09164332137603,126.008789961075));
#79940=CARTESIAN_POINT('Ctrl Pts',(-26.8976172716592,0.957924732285,125.978350829806));
#79941=CARTESIAN_POINT('Ctrl Pts',(-26.9053777141734,0.823038124023069,
125.953532918962));
#79942=CARTESIAN_POINT('Ctrl Pts',(-26.9131381566875,0.687495080565086,
125.934398238173));
#79943=CARTESIAN_POINT('Ctrl Pts',(-26.920911056953,0.551734451380798,125.915232840697));
#79944=CARTESIAN_POINT('Ctrl Pts',(-26.9286839572184,0.41531567053489,125.901768942808));
#79945=CARTESIAN_POINT('Ctrl Pts',(-26.9364568574838,0.278754062048078,
125.894016511967));
#79946=CARTESIAN_POINT('Ctrl Pts',(-26.9439471932458,0.147156812008808,
125.886545901514));
#79947=CARTESIAN_POINT('Ctrl Pts',(-26.9514375290078,0.0154272463080015,
125.884378720139));
#79948=CARTESIAN_POINT('Ctrl Pts',(-26.9589278647697,-0.115977477334406,
125.887478242803));
#79949=CARTESIAN_POINT('Ctrl Pts',(-26.9667021988888,-0.25236445101447,
125.890695284812));
#79950=CARTESIAN_POINT('Ctrl Pts',(-26.9744765330078,-0.388833496541188,
125.89959647942));
#79951=CARTESIAN_POINT('Ctrl Pts',(-26.9822508671269,-0.524872013016396,
125.914197794873));
#79952=CARTESIAN_POINT('Ctrl Pts',(-26.990015620074,-0.660742874177605,
125.928781115509));
#79953=CARTESIAN_POINT('Ctrl Pts',(-26.9977803730211,-0.796183876999741,
125.949050538231));
#79954=CARTESIAN_POINT('Ctrl Pts',(-27.0055451259682,-0.930682387920349,
125.97497003952));
#79955=CARTESIAN_POINT('Ctrl Pts',(-27.0133021668531,-1.06504731302363,
126.000863797196));
#79956=CARTESIAN_POINT('Ctrl Pts',(-27.0210592077381,-1.19847122768184,
126.032396392324));
#79957=CARTESIAN_POINT('Ctrl Pts',(-27.028816248623,-1.33044694654991,126.069480050443));
#79958=CARTESIAN_POINT('Ctrl Pts',(-27.0365674398632,-1.46232314150229,
126.106535743488));
#79959=CARTESIAN_POINT('Ctrl Pts',(-27.0443186311033,-1.59275293954911,
126.149134062013));
#79960=CARTESIAN_POINT('Ctrl Pts',(-27.0520698223434,-1.721240027483,126.197136308908));
#79961=CARTESIAN_POINT('Ctrl Pts',(-27.0598177191205,-1.84967250497719,
126.245118153568));
#79962=CARTESIAN_POINT('Ctrl Pts',(-27.0675656158976,-1.97616354914584,
126.298499221871));
#79963=CARTESIAN_POINT('Ctrl Pts',(-27.0753135126747,-2.10023289376968,
126.357091246994));
#79964=CARTESIAN_POINT('Ctrl Pts',(-27.0830597887588,-2.22427628576092,
126.415671015928));
#79965=CARTESIAN_POINT('Ctrl Pts',(-27.0908060648428,-2.34589863249586,
126.479459406724));
#79966=CARTESIAN_POINT('Ctrl Pts',(-27.0985523409269,-2.46464088241683,
126.548220537256));
#79967=CARTESIAN_POINT('Ctrl Pts',(-27.1062986741922,-2.58338400886595,
126.616982175367));
#79968=CARTESIAN_POINT('Ctrl Pts',(-27.1140450074575,-2.69924665774559,
126.690716430541));
#79969=CARTESIAN_POINT('Ctrl Pts',(-27.1217913407229,-2.81179591655585,
126.769142310443));
#79970=CARTESIAN_POINT('Ctrl Pts',(-27.1295394087258,-2.92437037999225,
126.847585753277));
#79971=CARTESIAN_POINT('Ctrl Pts',(-27.1372874767288,-3.03362965613461,
126.930722688052));
#79972=CARTESIAN_POINT('Ctrl Pts',(-27.1450355447318,-3.13917159433288,
127.018230038223));
#79973=CARTESIAN_POINT('Ctrl Pts',(-27.1527918474736,-3.24482570375917,
127.105830392248));
#79974=CARTESIAN_POINT('Ctrl Pts',(-27.1605481502154,-3.34675428158102,
127.197810190479));
#79975=CARTESIAN_POINT('Ctrl Pts',(-27.1683044529572,-3.44458953084251,
127.293807096181));
#79976=CARTESIAN_POINT('Ctrl Pts',(-27.1760648954714,-3.54247699772243,
127.389855238322));
#79977=CARTESIAN_POINT('Ctrl Pts',(-27.1838253379856,-3.63626651554925,
127.489924475017));
#79978=CARTESIAN_POINT('Ctrl Pts',(-27.1915857804997,-3.72562939023108,
127.5936179139));
#79979=CARTESIAN_POINT('Ctrl Pts',(-27.1993586807651,-3.81513571813261,
127.697477810696));
#79980=CARTESIAN_POINT('Ctrl Pts',(-27.2071315810306,-3.90020096000481,
127.804973228919));
#79981=CARTESIAN_POINT('Ctrl Pts',(-27.214904481296,-3.98053818472183,127.915675999531));
#79982=CARTESIAN_POINT('Ctrl Pts',(-27.2223948170582,-4.05795494896487,
128.02235444559));
#79983=CARTESIAN_POINT('Ctrl Pts',(-27.2298851528203,-4.13098130797035,
128.132010845523));
#79984=CARTESIAN_POINT('Ctrl Pts',(-27.2373754885825,-4.19940105463946,
128.244240728812));
#79985=CARTESIAN_POINT('Ctrl Pts',(-27.2453950705407,-4.27265514943476,
128.36440046207));
#79986=CARTESIAN_POINT('Ctrl Pts',(-27.2534146524989,-4.34084847910697,
128.487870880693));
#79987=CARTESIAN_POINT('Ctrl Pts',(-27.2614342344571,-4.40367885088525,
128.614201801232));
#79988=CARTESIAN_POINT('Ctrl Pts',(-27.2694431127645,-4.46642536363424,
128.740364109234));
#79989=CARTESIAN_POINT('Ctrl Pts',(-27.2774519910719,-4.52382301045794,
128.869379001647));
#79990=CARTESIAN_POINT('Ctrl Pts',(-27.2854608693793,-4.57561342169677,
129.000768402655));
#79991=CARTESIAN_POINT('Ctrl Pts',(-27.2934571006645,-4.62732204938768,
129.131950323337));
#79992=CARTESIAN_POINT('Ctrl Pts',(-27.3014533319497,-4.67344095730387,
129.265498949696));
#79993=CARTESIAN_POINT('Ctrl Pts',(-27.3094495632349,-4.71375845183941,
129.400913318872));
#79994=CARTESIAN_POINT('Ctrl Pts',(-27.3130027612179,-4.73167389664767,
129.461085923473));
#79995=CARTESIAN_POINT('Ctrl Pts',(-27.3165559592009,-4.74844444045746,
129.521626623983));
#79996=CARTESIAN_POINT('Ctrl Pts',(-27.3201091571839,-4.76405452823409,
129.582490119308));
#79997=CARTESIAN_POINT('Origin',(213.235140564004,0.,130.804360617566));
#79998=CARTESIAN_POINT('',(-29.4150816029337,-4.76405452823407,129.582490119308));
#79999=CARTESIAN_POINT('',(-29.0697544875928,-4.76405452823408,129.582490119308));
#80000=CARTESIAN_POINT('',(213.235140564004,-4.76405452823405,129.582490119308));
#80001=CARTESIAN_POINT('',(-27.7351405639751,-4.9182486262395,130.808036619917));
#80002=CARTESIAN_POINT('Ctrl Pts',(-27.7351405640086,-4.91824862623906,
130.808036620505));
#80003=CARTESIAN_POINT('Ctrl Pts',(-27.748320956022,-4.91807527927719,131.039963382041));
#80004=CARTESIAN_POINT('Ctrl Pts',(-27.7615013480354,-4.90149533204166,
131.271289001323));
#80005=CARTESIAN_POINT('Ctrl Pts',(-27.7746817400487,-4.86876952591759,
131.500253113571));
#80006=CARTESIAN_POINT('Ctrl Pts',(-27.7824560741679,-4.84946650739838,
131.635305508681));
#80007=CARTESIAN_POINT('Ctrl Pts',(-27.7902304082869,-4.82450942815123,
131.769768053086));
#80008=CARTESIAN_POINT('Ctrl Pts',(-27.798004742406,-4.79394297434503,131.903129847763));
#80009=CARTESIAN_POINT('Ctrl Pts',(-27.8057694953531,-4.76341419096134,
132.036327285947));
#80010=CARTESIAN_POINT('Ctrl Pts',(-27.8135342483003,-4.72728987443892,
132.168426296159));
#80011=CARTESIAN_POINT('Ctrl Pts',(-27.8212990012474,-4.68566634265908,
132.298922087621));
#80012=CARTESIAN_POINT('Ctrl Pts',(-27.8290560421324,-4.64408415195784,
132.429288268823));
#80013=CARTESIAN_POINT('Ctrl Pts',(-27.8368130830173,-4.59701373346094,
132.558054030036));
#80014=CARTESIAN_POINT('Ctrl Pts',(-27.8445701239023,-4.54460215028954,
132.684726102807));
#80015=CARTESIAN_POINT('Ctrl Pts',(-27.8523213151424,-4.49223009110064,
132.811302651181));
#80016=CARTESIAN_POINT('Ctrl Pts',(-27.8600725063826,-4.434525033227,132.93578829395));
#80017=CARTESIAN_POINT('Ctrl Pts',(-27.8678236976228,-4.37168332191907,
133.057706573107));
#80018=CARTESIAN_POINT('Ctrl Pts',(-27.8755715943998,-4.30886832001488,
133.179573033744));
#80019=CARTESIAN_POINT('Ctrl Pts',(-27.8833194911769,-4.24092118567372,
133.298873954289));
#80020=CARTESIAN_POINT('Ctrl Pts',(-27.8910673879539,-4.16808559161616,
133.415154666024));
#80021=CARTESIAN_POINT('Ctrl Pts',(-27.898813664038,-4.09526523319463,133.531411054341));
#80022=CARTESIAN_POINT('Ctrl Pts',(-27.9065599401222,-4.01755865639306,
133.644648159335));
#80023=CARTESIAN_POINT('Ctrl Pts',(-27.9143062162063,-3.93525431032151,
133.754438002245));
#80024=CARTESIAN_POINT('Ctrl Pts',(-27.9220525494716,-3.85294935669797,
133.864228655599));
#80025=CARTESIAN_POINT('Ctrl Pts',(-27.929798882737,-3.76604680059003,133.970571683266));
#80026=CARTESIAN_POINT('Ctrl Pts',(-27.9375452160024,-3.6748767983224,134.073070390497));
#80027=CARTESIAN_POINT('Ctrl Pts',(-27.9452932840054,-3.5836863791649,134.175592051602));
#80028=CARTESIAN_POINT('Ctrl Pts',(-27.9530413520084,-3.48822687197404,
134.27426738709));
#80029=CARTESIAN_POINT('Ctrl Pts',(-27.9607894200113,-3.38886658947828,
134.368735219262));
#80030=CARTESIAN_POINT('Ctrl Pts',(-27.9685457227532,-3.28940070569189,
134.463303452971));
#80031=CARTESIAN_POINT('Ctrl Pts',(-27.976302025495,-3.18602604873139,134.553654980671));
#80032=CARTESIAN_POINT('Ctrl Pts',(-27.9840583282369,-3.07914585925095,
134.639467374875));
#80033=CARTESIAN_POINT('Ctrl Pts',(-27.9918187707511,-2.97220862459528,
134.725325569738));
#80034=CARTESIAN_POINT('Ctrl Pts',(-27.9995792132653,-2.86176244396381,
134.806639572044));
#80035=CARTESIAN_POINT('Ctrl Pts',(-28.0073396557794,-2.74824025338752,
134.883129864797));
#80036=CARTESIAN_POINT('Ctrl Pts',(-28.0151125560449,-2.6345358269129,134.959742946559));
#80037=CARTESIAN_POINT('Ctrl Pts',(-28.0228854563103,-2.51774585631129,
135.031516640074));
#80038=CARTESIAN_POINT('Ctrl Pts',(-28.0306583565757,-2.39832940279758,
135.098216593047));
#80039=CARTESIAN_POINT('Ctrl Pts',(-28.0381486923377,-2.28325403816147,
135.162491834723));
#80040=CARTESIAN_POINT('Ctrl Pts',(-28.0456390280997,-2.16574010857344,
135.222055678687));
#80041=CARTESIAN_POINT('Ctrl Pts',(-28.0531293638617,-2.04621478947577,
135.276741202649));
#80042=CARTESIAN_POINT('Ctrl Pts',(-28.0609036979808,-1.92215763157506,
135.333500144874));
#80043=CARTESIAN_POINT('Ctrl Pts',(-28.0686780320999,-1.79554057384626,
135.385183336964));
#80044=CARTESIAN_POINT('Ctrl Pts',(-28.0764523662189,-1.66681760407285,
135.431552221255));
#80045=CARTESIAN_POINT('Ctrl Pts',(-28.084217119166,-1.53825327385538,135.477863960041));
#80046=CARTESIAN_POINT('Ctrl Pts',(-28.0919818721132,-1.40758855986009,
135.518874291174));
#80047=CARTESIAN_POINT('Ctrl Pts',(-28.0997466250603,-1.27530021903194,
135.55439139787));
#80048=CARTESIAN_POINT('Ctrl Pts',(-28.1075036659453,-1.14314326884901,
135.589873228475));
#80049=CARTESIAN_POINT('Ctrl Pts',(-28.1152607068303,-1.00936627614765,
135.619872591505));
#80050=CARTESIAN_POINT('Ctrl Pts',(-28.1230177477153,-0.874463732858376,
135.644246591679));
#80051=CARTESIAN_POINT('Ctrl Pts',(-28.1307689389554,-0.739662920626569,
135.66860221123));
#80052=CARTESIAN_POINT('Ctrl Pts',(-28.1385201301955,-0.60373863044392,
135.687340842396));
#80053=CARTESIAN_POINT('Ctrl Pts',(-28.1462713214356,-0.467197849328054,
135.700370138807));
#80054=CARTESIAN_POINT('Ctrl Pts',(-28.1540192182127,-0.330715101686322,
135.713393897419));
#80055=CARTESIAN_POINT('Ctrl Pts',(-28.1617671149898,-0.19361677264173,
135.720713110577));
#80056=CARTESIAN_POINT('Ctrl Pts',(-28.1695150117668,-0.0564170989217934,
135.722287027492));
#80057=CARTESIAN_POINT('Ctrl Pts',(-28.1772612878509,0.0807538755842706,
135.723860615178));
#80058=CARTESIAN_POINT('Ctrl Pts',(-28.1850075639351,0.218025761907662,
135.71969129257));
#80059=CARTESIAN_POINT('Ctrl Pts',(-28.1927538400192,0.354882575604865,
135.709790407098));
#80060=CARTESIAN_POINT('Ctrl Pts',(-28.2005001732845,0.491740399547791,
135.699889448541));
#80061=CARTESIAN_POINT('Ctrl Pts',(-28.2082465065499,0.628182754804501,
135.684256870906));
#80062=CARTESIAN_POINT('Ctrl Pts',(-28.2159928398152,0.763697433288137,
135.662956020858));
#80063=CARTESIAN_POINT('Ctrl Pts',(-28.2237409078182,0.899242459344428,
135.641650400632));
#80064=CARTESIAN_POINT('Ctrl Pts',(-28.2314889758212,1.03385900908642,135.614674042789));
#80065=CARTESIAN_POINT('Ctrl Pts',(-28.2392370438242,1.16704413145933,135.58214159389));
#80066=CARTESIAN_POINT('Ctrl Pts',(-28.246993346566,1.30037080456523,135.549574569117));
#80067=CARTESIAN_POINT('Ctrl Pts',(-28.2547496493079,1.43226263086088,135.511439750175));
#80068=CARTESIAN_POINT('Ctrl Pts',(-28.2625059520497,1.56223038154622,135.467902114913));
#80069=CARTESIAN_POINT('Ctrl Pts',(-28.2702663945639,1.69226749993354,135.424341242303));
#80070=CARTESIAN_POINT('Ctrl Pts',(-28.278026837078,1.82037813143489,135.375371946991));
#80071=CARTESIAN_POINT('Ctrl Pts',(-28.2857872795922,1.94609309798619,135.321207384556));
#80072=CARTESIAN_POINT('Ctrl Pts',(-28.2935601798576,2.07200987336224,135.266955872357));
#80073=CARTESIAN_POINT('Ctrl Pts',(-28.3013330801231,2.19552294631646,135.207492596941));
#80074=CARTESIAN_POINT('Ctrl Pts',(-28.3091059803886,2.31618701582715,135.143077106369));
#80075=CARTESIAN_POINT('Ctrl Pts',(-28.3165963161506,2.43246464247684,135.081003281133));
#80076=CARTESIAN_POINT('Ctrl Pts',(-28.3240866519126,2.54609654071978,135.014331196593));
#80077=CARTESIAN_POINT('Ctrl Pts',(-28.3315769876746,2.65671137534498,134.943330021972));
#80078=CARTESIAN_POINT('Ctrl Pts',(-28.3393513217937,2.77152020504548,134.869636816236));
#80079=CARTESIAN_POINT('Ctrl Pts',(-28.3471256559128,2.88344235079026,134.791046327344));
#80080=CARTESIAN_POINT('Ctrl Pts',(-28.3548999900319,2.99203171577573,134.707811561832));
#80081=CARTESIAN_POINT('Ctrl Pts',(-28.362664742979,3.10048725407376,134.62467937573));
#80082=CARTESIAN_POINT('Ctrl Pts',(-28.3704294959261,3.20561787670635,134.536914536939));
#80083=CARTESIAN_POINT('Ctrl Pts',(-28.3781942488732,3.30700450400641,134.444814472923));
#80084=CARTESIAN_POINT('Ctrl Pts',(-28.3859512897582,3.4082904326788,134.352805883988));
#80085=CARTESIAN_POINT('Ctrl Pts',(-28.3937083306432,3.50583947866144,134.25647089976));
#80086=CARTESIAN_POINT('Ctrl Pts',(-28.4014653715282,3.59926413514131,134.156148311914));
#80087=CARTESIAN_POINT('Ctrl Pts',(-28.4092165627683,3.69261833936099,134.055901378113));
#80088=CARTESIAN_POINT('Ctrl Pts',(-28.4169677540084,3.78185407944575,133.951673111068));
#80089=CARTESIAN_POINT('Ctrl Pts',(-28.4247189452485,3.8666196229123,133.843840137847));
#80090=CARTESIAN_POINT('Ctrl Pts',(-28.4324668420256,3.95134913876168,133.736052996517));
#80091=CARTESIAN_POINT('Ctrl Pts',(-28.4402147388027,4.0316119957434,133.624664502959));
#80092=CARTESIAN_POINT('Ctrl Pts',(-28.4479626355798,4.10709595155373,133.510085272299));
#80093=CARTESIAN_POINT('Ctrl Pts',(-28.4557089116639,4.18256411774785,133.395530009145));
#80094=CARTESIAN_POINT('Ctrl Pts',(-28.463455187748,4.25325515616629,133.277785662728));
#80095=CARTESIAN_POINT('Ctrl Pts',(-28.4712014638321,4.31889971152841,133.157292478938));
#80096=CARTESIAN_POINT('Ctrl Pts',(-28.4789477970974,4.38454475146363,133.036798405695));
#80097=CARTESIAN_POINT('Ctrl Pts',(-28.4866941303628,4.44514304696789,132.913555797911));
#80098=CARTESIAN_POINT('Ctrl Pts',(-28.4944404636281,4.50047103240126,132.788029831174));
#80099=CARTESIAN_POINT('Ctrl Pts',(-28.5021885316311,4.55581140815335,132.662475753768));
#80100=CARTESIAN_POINT('Ctrl Pts',(-28.5099365996341,4.60587896761775,132.534637657583));
#80101=CARTESIAN_POINT('Ctrl Pts',(-28.517684667637,4.65049830886217,132.405000658853));
#80102=CARTESIAN_POINT('Ctrl Pts',(-28.5254409703789,4.69516507207344,132.275225880378));
#80103=CARTESIAN_POINT('Ctrl Pts',(-28.5331972731208,4.73437192261259,132.143648750411));
#80104=CARTESIAN_POINT('Ctrl Pts',(-28.5409535758627,4.76799322090075,132.010770045557));
#80105=CARTESIAN_POINT('Ctrl Pts',(-28.5487140183768,4.80163246388817,131.877820419336));
#80106=CARTESIAN_POINT('Ctrl Pts',(-28.5564744608909,4.82968013446193,131.743568216514));
#80107=CARTESIAN_POINT('Ctrl Pts',(-28.5642349034051,4.85206196424514,131.608523385683));
#80108=CARTESIAN_POINT('Ctrl Pts',(-28.5720078036705,4.87447972332848,131.4732617689));
#80109=CARTESIAN_POINT('Ctrl Pts',(-28.579780703936,4.89121341853944,131.337205369718));
#80110=CARTESIAN_POINT('Ctrl Pts',(-28.5875536042014,4.90224071893429,131.200869124565));
#80111=CARTESIAN_POINT('Ctrl Pts',(-28.5950439399634,4.91286714918369,131.069489045334));
#80112=CARTESIAN_POINT('Ctrl Pts',(-28.6025342757255,4.91819485282245,130.937849420869));
#80113=CARTESIAN_POINT('Ctrl Pts',(-28.6100246114875,4.91824957378903,130.806408158542));
#80114=CARTESIAN_POINT('Ctrl Pts',(-28.6177989456066,4.91830636951769,130.669983260803));
#80115=CARTESIAN_POINT('Ctrl Pts',(-28.6255732797256,4.9126826190398,130.533339910863));
#80116=CARTESIAN_POINT('Ctrl Pts',(-28.6333476138447,4.90135005770111,130.396990178809));
#80117=CARTESIAN_POINT('Ctrl Pts',(-28.6411123667918,4.89003146273146,130.260808485614));
#80118=CARTESIAN_POINT('Ctrl Pts',(-28.6488771197389,4.87301808771849,130.124920076197));
#80119=CARTESIAN_POINT('Ctrl Pts',(-28.656641872686,4.85033364401388,129.989838300961));
#80120=CARTESIAN_POINT('Ctrl Pts',(-28.664398913571,4.82767173081856,129.854890690849));
#80121=CARTESIAN_POINT('Ctrl Pts',(-28.672155954456,4.7993500223603,129.720748503643));
#80122=CARTESIAN_POINT('Ctrl Pts',(-28.679912995341,4.76544409677402,129.587920884977));
#80123=CARTESIAN_POINT('Ctrl Pts',(-28.6876641865811,4.73156373990992,129.455193432651));
#80124=CARTESIAN_POINT('Ctrl Pts',(-28.6954153778213,4.69210764416697,129.323778952975));
#80125=CARTESIAN_POINT('Ctrl Pts',(-28.7031665690614,4.64720255656525,129.194176944579));
#80126=CARTESIAN_POINT('Ctrl Pts',(-28.7109144658385,4.60231655482371,129.064630020494));
#80127=CARTESIAN_POINT('Ctrl Pts',(-28.7186623626156,4.55198629523495,128.93689440417));
#80128=CARTESIAN_POINT('Ctrl Pts',(-28.7264102593927,4.49638846534228,128.811454741405));
#80129=CARTESIAN_POINT('Ctrl Pts',(-28.7341565354767,4.44080226531707,128.686041317914));
#80130=CARTESIAN_POINT('Ctrl Pts',(-28.7419028115608,4.37995084497337,128.562923249914));
#80131=CARTESIAN_POINT('Ctrl Pts',(-28.7496490876449,4.31405900253759,128.44256511729));
#80132=CARTESIAN_POINT('Ctrl Pts',(-28.7573954209103,4.2481666737032,128.322206096209));
#80133=CARTESIAN_POINT('Ctrl Pts',(-28.7651417541756,4.17723403627797,128.204607394093));
#80134=CARTESIAN_POINT('Ctrl Pts',(-28.772888087441,4.10153161297023,128.090208541815));
#80135=CARTESIAN_POINT('Ctrl Pts',(-28.7806361554439,4.02581223662968,127.975784070706));
#80136=CARTESIAN_POINT('Ctrl Pts',(-28.7883842234469,3.94532116460504,127.864561201335));
#80137=CARTESIAN_POINT('Ctrl Pts',(-28.7961322914499,3.86037172989342,127.756949721487));
#80138=CARTESIAN_POINT('Ctrl Pts',(-28.8038885941917,3.77533200991168,127.649223870878));
#80139=CARTESIAN_POINT('Ctrl Pts',(-28.8116448969336,3.68582470441006,127.545117384427));
#80140=CARTESIAN_POINT('Ctrl Pts',(-28.8194011996754,3.59220321966602,127.445006648256));
#80141=CARTESIAN_POINT('Ctrl Pts',(-28.8271616421896,3.49853176631657,127.34484247997));
#80142=CARTESIAN_POINT('Ctrl Pts',(-28.8349220847038,3.40074203691041,127.248678585448));
#80143=CARTESIAN_POINT('Ctrl Pts',(-28.842682527218,3.29922292176801,127.156853088447));
#80144=CARTESIAN_POINT('Ctrl Pts',(-28.8504554274834,3.19754083912955,127.064880185006));
#80145=CARTESIAN_POINT('Ctrl Pts',(-28.8582283277487,3.09211770818492,126.977259846182));
#80146=CARTESIAN_POINT('Ctrl Pts',(-28.8660012280141,2.98337468911472,126.894289195348));
#80147=CARTESIAN_POINT('Ctrl Pts',(-28.8734915637762,2.87858475269455,126.814334736661));
#80148=CARTESIAN_POINT('Ctrl Pts',(-28.8809818995384,2.77071236235782,126.738697956201));
#80149=CARTESIAN_POINT('Ctrl Pts',(-28.8884722353004,2.66015668377066,126.667604704983));
#80150=CARTESIAN_POINT('Ctrl Pts',(-28.8962465694195,2.54540925302752,126.593815931537));
#80151=CARTESIAN_POINT('Ctrl Pts',(-28.9040209035385,2.4274075582807,126.524688283744));
#80152=CARTESIAN_POINT('Ctrl Pts',(-28.9117952376576,2.30656714086174,126.460522327851));
#80153=CARTESIAN_POINT('Ctrl Pts',(-28.9195599906047,2.18587564845742,126.396435450763));
#80154=CARTESIAN_POINT('Ctrl Pts',(-28.9273247435519,2.06235273628625,126.337298280457));
#80155=CARTESIAN_POINT('Ctrl Pts',(-28.935089496499,1.93644311714481,126.283368346331));
#80156=CARTESIAN_POINT('Ctrl Pts',(-28.942846537384,1.81065855321212,126.229491976177));
#80157=CARTESIAN_POINT('Ctrl Pts',(-28.950603578269,1.68249235679357,126.180812702825));
#80158=CARTESIAN_POINT('Ctrl Pts',(-28.958360619154,1.55241373835822,126.137542145903));
#80159=CARTESIAN_POINT('Ctrl Pts',(-28.9661118103941,1.4224332132209,126.094304219644));
#80160=CARTESIAN_POINT('Ctrl Pts',(-28.9738630016343,1.29054350610047,126.056467014205));
#80161=CARTESIAN_POINT('Ctrl Pts',(-28.9816141928744,1.15723336920089,126.02419388494));
#80162=CARTESIAN_POINT('Ctrl Pts',(-28.9893620896515,1.02397989266566,125.991934472615));
#80163=CARTESIAN_POINT('Ctrl Pts',(-28.9971099864285,0.88930756629846,125.965234524695));
#80164=CARTESIAN_POINT('Ctrl Pts',(-29.0048578832056,0.753719640269004,
125.944207351837));
#80165=CARTESIAN_POINT('Ctrl Pts',(-29.0126041592897,0.618160076310736,
125.923184577411));
#80166=CARTESIAN_POINT('Ctrl Pts',(-29.0203504353738,0.481685679743536,
125.907832277669));
#80167=CARTESIAN_POINT('Ctrl Pts',(-29.0280967114579,0.344808823712795,
125.89821244027));
#80168=CARTESIAN_POINT('Ctrl Pts',(-29.0358430447232,0.207930957288196,
125.888592531859));
#80169=CARTESIAN_POINT('Ctrl Pts',(-29.0435893779887,0.0706510154751086,
125.88470519764));
#80170=CARTESIAN_POINT('Ctrl Pts',(-29.051335711254,-0.0665149878230809,
125.886560416369));
#80171=CARTESIAN_POINT('Ctrl Pts',(-29.059083779257,-0.203711708496667,
125.888416050561));
#80172=CARTESIAN_POINT('Ctrl Pts',(-29.0668318472599,-0.340794049027356,
125.896016791416));
#80173=CARTESIAN_POINT('Ctrl Pts',(-29.0745799152629,-0.477247879205806,
125.909320523318));
#80174=CARTESIAN_POINT('Ctrl Pts',(-29.0823362180048,-0.613846734138791,
125.922638394585));
#80175=CARTESIAN_POINT('Ctrl Pts',(-29.0900925207466,-0.749815354600336,
125.941671326813));
#80176=CARTESIAN_POINT('Ctrl Pts',(-29.0978488234885,-0.884646051560765,
125.966325435185));
#80177=CARTESIAN_POINT('Ctrl Pts',(-29.1056092660027,-1.01954871172402,
125.990992702197));
#80178=CARTESIAN_POINT('Ctrl Pts',(-29.1133697085168,-1.15331185707987,
126.021287037173));
#80179=CARTESIAN_POINT('Ctrl Pts',(-29.121130151031,-1.28544080981666,126.057064019821));
#80180=CARTESIAN_POINT('Ctrl Pts',(-29.1289030512965,-1.41778186767807,
126.092898434859));
#80181=CARTESIAN_POINT('Ctrl Pts',(-29.1366759515619,-1.54848311764643,
126.134232967281));
#80182=CARTESIAN_POINT('Ctrl Pts',(-29.1444488518273,-1.67706693404797,
126.18087388554));
#80183=CARTESIAN_POINT('Ctrl Pts',(-29.1519391875893,-1.80097640483918,
126.225819288938));
#80184=CARTESIAN_POINT('Ctrl Pts',(-29.1594295233512,-1.92291943228982,
126.275691858664));
#80185=CARTESIAN_POINT('Ctrl Pts',(-29.1669198591132,-2.04249024275295,
126.330277843325));
#80186=CARTESIAN_POINT('Ctrl Pts',(-29.1746947830569,-2.16660403241195,
126.386937770546));
#80187=CARTESIAN_POINT('Ctrl Pts',(-29.1824697070006,-2.28855496587655,
126.448855852897));
#80188=CARTESIAN_POINT('Ctrl Pts',(-29.1902446309443,-2.40786544995348,
126.51584490261));
#80189=CARTESIAN_POINT('Ctrl Pts',(-29.1980098405491,-2.52702686215729,
126.582750253199));
#80190=CARTESIAN_POINT('Ctrl Pts',(-29.2057750501539,-2.64355405184961,
126.654713774174));
#80191=CARTESIAN_POINT('Ctrl Pts',(-29.2135402597586,-2.75698989575442,
126.731500470543));
#80192=CARTESIAN_POINT('Ctrl Pts',(-29.221297624704,-2.870311143195,126.808209594571));
#80193=CARTESIAN_POINT('Ctrl Pts',(-29.2290549896493,-2.98054693844968,
126.889731978877));
#80194=CARTESIAN_POINT('Ctrl Pts',(-29.2368123545947,-3.08726557027292,
126.975787206868));
#80195=CARTESIAN_POINT('Ctrl Pts',(-29.2445633089976,-3.19389601179866,
127.061771320414));
#80196=CARTESIAN_POINT('Ctrl Pts',(-29.2523142634005,-3.29701477442576,
127.152280574189));
#80197=CARTESIAN_POINT('Ctrl Pts',(-29.2600652178033,-3.39622028205886,
127.246992087566));
#80198=CARTESIAN_POINT('Ctrl Pts',(-29.2678126838207,-3.49538114137613,
127.341660975189));
#80199=CARTESIAN_POINT('Ctrl Pts',(-29.2755601498379,-3.59063196760138,
127.440528090245));
#80200=CARTESIAN_POINT('Ctrl Pts',(-29.2833076158553,-3.68160547577825,
127.543231337206));
#80201=CARTESIAN_POINT('Ctrl Pts',(-29.2910532728381,-3.77255774162731,
127.645910602944));
#80202=CARTESIAN_POINT('Ctrl Pts',(-29.298798929821,-3.85923441827731,127.752423925421));
#80203=CARTESIAN_POINT('Ctrl Pts',(-29.3065445868038,-3.94130648447086,
127.862373830042));
#80204=CARTESIAN_POINT('Ctrl Pts',(-29.31429011253,-4.02337715988486,127.972321871469));
#80205=CARTESIAN_POINT('Ctrl Pts',(-29.3220356382563,-4.10084314747055,
128.085706065174));
#80206=CARTESIAN_POINT('Ctrl Pts',(-29.3297811639825,-4.17341722173141,
128.202097803042));
#80207=CARTESIAN_POINT('Ctrl Pts',(-29.3375315429424,-4.24603676985053,
128.318562470278));
#80208=CARTESIAN_POINT('Ctrl Pts',(-29.3452819219022,-4.3137580736368,128.438038114628));
#80209=CARTESIAN_POINT('Ctrl Pts',(-29.353032300862,-4.37633845182278,128.560069010489));
#80210=CARTESIAN_POINT('Ctrl Pts',(-29.3607852357813,-4.43893946808426,
128.682140150319));
#80211=CARTESIAN_POINT('Ctrl Pts',(-29.3685381707006,-4.49639601355354,
128.806767867301));
#80212=CARTESIAN_POINT('Ctrl Pts',(-29.3762911056198,-4.5485129116741,128.93347490357));
#80213=CARTESIAN_POINT('Ctrl Pts',(-29.384052654986,-4.60068771796163,129.060322726656));
#80214=CARTESIAN_POINT('Ctrl Pts',(-29.3918142043521,-4.64751088883166,
129.18925411777));
#80215=CARTESIAN_POINT('Ctrl Pts',(-29.3995757537182,-4.6888364732971,129.319774618313));
#80216=CARTESIAN_POINT('Ctrl Pts',(-29.4047443701234,-4.71635624850492,
129.406691594356));
#80217=CARTESIAN_POINT('Ctrl Pts',(-29.4099129865286,-4.7414391129661,129.494312958415));
#80218=CARTESIAN_POINT('Ctrl Pts',(-29.4150816029337,-4.76405452823407,
129.582490119308));
#80219=CARTESIAN_POINT('Ctrl Pts',(-27.6650164504902,-4.76405452823402,
129.582490119308));
#80220=CARTESIAN_POINT('Ctrl Pts',(-27.6726576270515,-4.79767153518427,
129.713562319198));
#80221=CARTESIAN_POINT('Ctrl Pts',(-27.6802988036129,-4.82585647153979,
129.845950237151));
#80222=CARTESIAN_POINT('Ctrl Pts',(-27.6879399801743,-4.84852785224846,
129.979157170851));
#80223=CARTESIAN_POINT('Ctrl Pts',(-27.6958067441411,-4.87186855107991,
130.11629671968));
#80224=CARTESIAN_POINT('Ctrl Pts',(-27.7036735081079,-4.88936504333653,
130.254303931843));
#80225=CARTESIAN_POINT('Ctrl Pts',(-27.7115402720748,-4.90098591852434,
130.392632443978));
#80226=CARTESIAN_POINT('Ctrl Pts',(-27.7194070360416,-4.91260679371213,
130.530960956112));
#80227=CARTESIAN_POINT('Ctrl Pts',(-27.7272738000084,-4.91835208897519,
130.669610305378));
#80228=CARTESIAN_POINT('Ctrl Pts',(-27.7351405639752,-4.9182486262395,130.808036619917));
#80229=CARTESIAN_POINT('',(-27.38985943602,-4.9182498326282,130.80564372033));
#80230=CARTESIAN_POINT('Ctrl Pts',(-27.3201091571839,-4.76405452823409,
129.582490119308));
#80231=CARTESIAN_POINT('Ctrl Pts',(-27.3280913567537,-4.79912232815121,
129.719218938957));
#80232=CARTESIAN_POINT('Ctrl Pts',(-27.3360735563233,-4.82833034249597,
129.857577834223));
#80233=CARTESIAN_POINT('Ctrl Pts',(-27.344055755893,-4.85153765587541,129.99704070816));
#80234=CARTESIAN_POINT('Ctrl Pts',(-27.3520294712711,-4.87472030245806,
130.13635534855));
#80235=CARTESIAN_POINT('Ctrl Pts',(-27.3600031866493,-4.89191490313895,
130.276771277517));
#80236=CARTESIAN_POINT('Ctrl Pts',(-27.3679769020273,-4.90303131735161,
130.417751042453));
#80237=CARTESIAN_POINT('Ctrl Pts',(-27.3752710800153,-4.91320036653513,
130.546716204787));
#80238=CARTESIAN_POINT('Ctrl Pts',(-27.3825652580032,-4.91828361497706,
130.676152846472));
#80239=CARTESIAN_POINT('Ctrl Pts',(-27.3898594359911,-4.91824983262833,
130.805643719816));
#80240=CARTESIAN_POINT('Ctrl Pts',(-27.3898594360201,-4.9182498326282,130.80564372033));
#80241=CARTESIAN_POINT('Ctrl Pts',(-27.3981545579858,-4.91821141447941,
130.95290398593));
#80242=CARTESIAN_POINT('Ctrl Pts',(-27.4064496799514,-4.91155496272104,
131.09998366834));
#80243=CARTESIAN_POINT('Ctrl Pts',(-27.4147448019172,-4.89835427534359,
131.246297780207));
#80244=CARTESIAN_POINT('Ctrl Pts',(-27.423167994457,-4.88494977907478,131.394870874207));
#80245=CARTESIAN_POINT('Ctrl Pts',(-27.4315911869969,-4.86479739107107,
131.542654243628));
#80246=CARTESIAN_POINT('Ctrl Pts',(-27.4400143795368,-4.83802743156649,
131.689049056459));
#80247=CARTESIAN_POINT('Ctrl Pts',(-27.448354056866,-4.81152289384773,131.83399237764));
#80248=CARTESIAN_POINT('Ctrl Pts',(-27.4566937341952,-4.77853157841535,
131.977574290635));
#80249=CARTESIAN_POINT('Ctrl Pts',(-27.4650334115245,-4.73922973640288,
132.119231169406));
#80250=CARTESIAN_POINT('Ctrl Pts',(-27.4734983616696,-4.69933752953261,
132.263015919004));
#80251=CARTESIAN_POINT('Ctrl Pts',(-27.4819633118148,-4.65294382769438,
132.404817037884));
#80252=CARTESIAN_POINT('Ctrl Pts',(-27.49042826196,-4.60028281832949,132.544067792318));
#80253=CARTESIAN_POINT('Ctrl Pts',(-27.4988932121051,-4.54762180896466,
132.683318546751));
#80254=CARTESIAN_POINT('Ctrl Pts',(-27.5073581622503,-4.48869367965767,
132.820018676014));
#80255=CARTESIAN_POINT('Ctrl Pts',(-27.5158231123954,-4.42378021487808,
132.953628323775));
#80256=CARTESIAN_POINT('Ctrl Pts',(-27.5235974465145,-4.36416273865318,
133.076337379991));
#80257=CARTESIAN_POINT('Ctrl Pts',(-27.5313717806336,-4.2993413143803,133.196758369057));
#80258=CARTESIAN_POINT('Ctrl Pts',(-27.5391461147527,-4.22951448978743,
133.314418434266));
#80259=CARTESIAN_POINT('Ctrl Pts',(-27.5469108676998,-4.15977372051527,
133.431933493961));
#80260=CARTESIAN_POINT('Ctrl Pts',(-27.5546756206469,-4.08504002243042,
133.546694066953));
#80261=CARTESIAN_POINT('Ctrl Pts',(-27.562440373594,-4.00555924423072,133.658248878073));
#80262=CARTESIAN_POINT('Ctrl Pts',(-27.570197414479,-3.92615740746052,133.769692891381));
#80263=CARTESIAN_POINT('Ctrl Pts',(-27.577954455364,-3.84201809876874,133.877937162782));
#80264=CARTESIAN_POINT('Ctrl Pts',(-27.585711496249,-3.75343197057496,133.982556883495));
#80265=CARTESIAN_POINT('Ctrl Pts',(-27.5934626874891,-3.66491264586956,
134.087097709663));
#80266=CARTESIAN_POINT('Ctrl Pts',(-27.6012138787292,-3.57195342798532,
134.18801912845));
#80267=CARTESIAN_POINT('Ctrl Pts',(-27.6089650699693,-3.47488676517149,
134.284927386317));
#80268=CARTESIAN_POINT('Ctrl Pts',(-27.6167129667464,-3.37786135827857,
134.38179445559));
#80269=CARTESIAN_POINT('Ctrl Pts',(-27.6244608635235,-3.27673225476734,
134.474651480802));
#80270=CARTESIAN_POINT('Ctrl Pts',(-27.6322087603006,-3.17187031718759,
134.5631399079));
#80271=CARTESIAN_POINT('Ctrl Pts',(-27.6399550363847,-3.06703031446462,
134.651609825127));
#80272=CARTESIAN_POINT('Ctrl Pts',(-27.6477013124688,-2.95845932939005,
134.735712709892));
#80273=CARTESIAN_POINT('Ctrl Pts',(-27.6554475885529,-2.84656271321275,
134.815129095333));
#80274=CARTESIAN_POINT('Ctrl Pts',(-27.6631939218182,-2.7346652710402,134.894546067007));
#80275=CARTESIAN_POINT('Ctrl Pts',(-27.6709402550836,-2.61944246760607,
134.969276244046));
#80276=CARTESIAN_POINT('Ctrl Pts',(-27.6786865883489,-2.50132981752473,
135.039042684317));
#80277=CARTESIAN_POINT('Ctrl Pts',(-27.6864346563519,-2.38319071693433,
135.108824748298));
#80278=CARTESIAN_POINT('Ctrl Pts',(-27.6941827243548,-2.26216081848309,
135.173640664767));
#80279=CARTESIAN_POINT('Ctrl Pts',(-27.7019307923578,-2.13870112641277,
135.233258963022));
#80280=CARTESIAN_POINT('Ctrl Pts',(-27.7096870950996,-2.01511021991237,
135.292940624313));
#80281=CARTESIAN_POINT('Ctrl Pts',(-27.7174433978415,-1.88908471377028,
135.347413462141));
#80282=CARTESIAN_POINT('Ctrl Pts',(-27.7251997005833,-1.76110704035503,
135.396493570227));
#80283=CARTESIAN_POINT('Ctrl Pts',(-27.7329601430975,-1.63306106140197,
135.445599873844));
#80284=CARTESIAN_POINT('Ctrl Pts',(-27.7407205856117,-1.50306120944049,
135.489307588004));
#80285=CARTESIAN_POINT('Ctrl Pts',(-27.7484810281259,-1.37160509201754,
135.527482734773));
#80286=CARTESIAN_POINT('Ctrl Pts',(-27.7562539283913,-1.23993794956496,
135.565719163677));
#80287=CARTESIAN_POINT('Ctrl Pts',(-27.7640268286567,-1.10681025003527,
135.59840518411));
#80288=CARTESIAN_POINT('Ctrl Pts',(-27.7717997289222,-0.97273068816611,
135.625457802938));
#80289=CARTESIAN_POINT('Ctrl Pts',(-27.7792900646843,-0.843525256095834,
135.65152699093));
#80290=CARTESIAN_POINT('Ctrl Pts',(-27.7867804004464,-0.713436269511016,
135.672365194421));
#80291=CARTESIAN_POINT('Ctrl Pts',(-27.7942707362085,-0.582921471319326,
135.687943894298));
#80292=CARTESIAN_POINT('Ctrl Pts',(-27.8020450703275,-0.447458164886229,
135.704113265315));
#80293=CARTESIAN_POINT('Ctrl Pts',(-27.8098194044467,-0.311107013114465,
135.714667651273));
#80294=CARTESIAN_POINT('Ctrl Pts',(-27.8175937385658,-0.174373163640406,
135.719518505396));
#80295=CARTESIAN_POINT('Ctrl Pts',(-27.8253584915129,-0.0378078264155682,
135.724363381276));
#80296=CARTESIAN_POINT('Ctrl Pts',(-27.8331232444599,0.0991388831185796,
135.723518697394));
#80297=CARTESIAN_POINT('Ctrl Pts',(-27.840887997407,0.235954407152601,135.71694736797));
#80298=CARTESIAN_POINT('Ctrl Pts',(-27.848645038292,0.372634044079205,135.710382565283));
#80299=CARTESIAN_POINT('Ctrl Pts',(-27.8564020791771,0.509182366811173,
135.698102454637));
#80300=CARTESIAN_POINT('Ctrl Pts',(-27.8641591200621,0.645084866956548,
135.680121950622));
#80301=CARTESIAN_POINT('Ctrl Pts',(-27.8719103113022,0.780884881969396,
135.662155005845));
#80302=CARTESIAN_POINT('Ctrl Pts',(-27.8796615025422,0.916039657759709,
135.638496275094));
#80303=CARTESIAN_POINT('Ctrl Pts',(-27.8874126937823,1.05003822192403,135.609212623091));
#80304=CARTESIAN_POINT('Ctrl Pts',(-27.8951605905594,1.18397983312424,135.579941417421));
#80305=CARTESIAN_POINT('Ctrl Pts',(-27.9029084873365,1.3167658289457,135.545050128798));
#80306=CARTESIAN_POINT('Ctrl Pts',(-27.9106563841136,1.4478940874432,135.504656967164));
#80307=CARTESIAN_POINT('Ctrl Pts',(-27.9184026601977,1.57899491673583,135.464272254909));
#80308=CARTESIAN_POINT('Ctrl Pts',(-27.9261489362819,1.70843832503221,135.418388073818));
#80309=CARTESIAN_POINT('Ctrl Pts',(-27.933895212366,1.83573643356326,135.367172777735));
#80310=CARTESIAN_POINT('Ctrl Pts',(-27.9416415456313,1.96303548177987,135.315957103593));
#80311=CARTESIAN_POINT('Ctrl Pts',(-27.9493878788966,2.08818883592086,135.25941038186));
#80312=CARTESIAN_POINT('Ctrl Pts',(-27.9571342121619,2.21072809043967,135.197749329328));
#80313=CARTESIAN_POINT('Ctrl Pts',(-27.9648822801649,2.3332947867749,135.136074468232));
#80314=CARTESIAN_POINT('Ctrl Pts',(-27.9726303481679,2.45324586941514,135.069283172988));
#80315=CARTESIAN_POINT('Ctrl Pts',(-27.9803784161709,2.57013741144903,134.997638183954));
#80316=CARTESIAN_POINT('Ctrl Pts',(-27.9881347189127,2.68715318720497,134.925917049772));
#80317=CARTESIAN_POINT('Ctrl Pts',(-27.9958910216545,2.80110259283458,134.849332121646));
#80318=CARTESIAN_POINT('Ctrl Pts',(-28.0036473243964,2.9115701362972,134.768189877754));
#80319=CARTESIAN_POINT('Ctrl Pts',(-28.0114077669105,3.02209663961389,134.687004325803));
#80320=CARTESIAN_POINT('Ctrl Pts',(-28.0191682094248,3.12913727281141,134.601256855685));
#80321=CARTESIAN_POINT('Ctrl Pts',(-28.026928651939,3.23231034742593,134.511293700375));
#80322=CARTESIAN_POINT('Ctrl Pts',(-28.0347015522044,3.3356490446191,134.421186128222));
#80323=CARTESIAN_POINT('Ctrl Pts',(-28.0424744524698,3.43510749274633,134.326849616679));
#80324=CARTESIAN_POINT('Ctrl Pts',(-28.0502473527352,3.53034090540144,134.228667285221));
#80325=CARTESIAN_POINT('Ctrl Pts',(-28.0577376884972,3.62211234362779,134.134054128819));
#80326=CARTESIAN_POINT('Ctrl Pts',(-28.0652280242593,3.70996038924204,134.035870138083));
#80327=CARTESIAN_POINT('Ctrl Pts',(-28.0727183600213,3.79361362708284,133.934485009808));
#80328=CARTESIAN_POINT('Ctrl Pts',(-28.0804926941403,3.88043860286236,133.82925583358));
#80329=CARTESIAN_POINT('Ctrl Pts',(-28.0882670282594,3.96301943477866,133.720244651344));
#80330=CARTESIAN_POINT('Ctrl Pts',(-28.0960413623785,4.04100858128699,133.607828596421));
#80331=CARTESIAN_POINT('Ctrl Pts',(-28.1038061153256,4.11890161314245,133.495551084238));
#80332=CARTESIAN_POINT('Ctrl Pts',(-28.1115708682726,4.19221399828266,133.379877366704));
#80333=CARTESIAN_POINT('Ctrl Pts',(-28.1193356212197,4.2606374853736,133.26121862745));
#80334=CARTESIAN_POINT('Ctrl Pts',(-28.1270926621047,4.32899301329248,133.142677741728));
#80335=CARTESIAN_POINT('Ctrl Pts',(-28.1348497029898,4.39246911223033,133.021158070802));
#80336=CARTESIAN_POINT('Ctrl Pts',(-28.1426067438748,4.45080022589988,132.897100546852));
#80337=CARTESIAN_POINT('Ctrl Pts',(-28.1503579351149,4.50908735162287,132.773136575647));
#80338=CARTESIAN_POINT('Ctrl Pts',(-28.1581091263551,4.56223704904577,132.646638913125));
#80339=CARTESIAN_POINT('Ctrl Pts',(-28.1658603175952,4.61002938028732,132.518073596856));
#80340=CARTESIAN_POINT('Ctrl Pts',(-28.1736082143723,4.65780139851319,132.389562924277));
#80341=CARTESIAN_POINT('Ctrl Pts',(-28.1813561111493,4.70022044344138,132.258986711529));
#80342=CARTESIAN_POINT('Ctrl Pts',(-28.1891040079264,4.73711455926891,132.12683130339));
#80343=CARTESIAN_POINT('Ctrl Pts',(-28.1968502840105,4.77400095764276,131.994703539312));
#80344=CARTESIAN_POINT('Ctrl Pts',(-28.2045965600946,4.80536462059856,131.860997613222));
#80345=CARTESIAN_POINT('Ctrl Pts',(-28.2123428361787,4.83108347860162,131.726214990709));
#80346=CARTESIAN_POINT('Ctrl Pts',(-28.220089169444,4.85680252645544,131.591431373261));
#80347=CARTESIAN_POINT('Ctrl Pts',(-28.2278355027094,4.87687661292898,131.455571427568));
#80348=CARTESIAN_POINT('Ctrl Pts',(-28.2355818359747,4.89123488335785,131.319146377201));
#80349=CARTESIAN_POINT('Ctrl Pts',(-28.2433299039777,4.90559636922183,131.18269077539));
#80350=CARTESIAN_POINT('Ctrl Pts',(-28.2510779719806,4.91423945104085,131.045670205827));
#80351=CARTESIAN_POINT('Ctrl Pts',(-28.2588260399836,4.91714522637847,130.908600174374));
#80352=CARTESIAN_POINT('Ctrl Pts',(-28.2665823427254,4.92005409000869,130.77138446326));
#80353=CARTESIAN_POINT('Ctrl Pts',(-28.2743386454673,4.91721345809016,130.634119576746));
#80354=CARTESIAN_POINT('Ctrl Pts',(-28.2820949482092,4.90865659579756,130.497320738995));
#80355=CARTESIAN_POINT('Ctrl Pts',(-28.2898553907234,4.90009516644991,130.360448887584));
#80356=CARTESIAN_POINT('Ctrl Pts',(-28.2976158332376,4.88581146820079,130.22404396923));
#80357=CARTESIAN_POINT('Ctrl Pts',(-28.3053762757518,4.86589048472126,130.088614256626));
#80358=CARTESIAN_POINT('Ctrl Pts',(-28.3131491760172,4.84593752231055,129.952967140225));
#80359=CARTESIAN_POINT('Ctrl Pts',(-28.3209220762826,4.82032926402175,129.818298742219));
#80360=CARTESIAN_POINT('Ctrl Pts',(-28.328694976548,4.78920167364366,129.685106226612));
#80361=CARTESIAN_POINT('Ctrl Pts',(-28.3361853123101,4.75920564958139,129.556755594439));
#80362=CARTESIAN_POINT('Ctrl Pts',(-28.3436756480721,4.72408469192248,129.429775700407));
#80363=CARTESIAN_POINT('Ctrl Pts',(-28.3511659838342,4.6840031305258,129.304594723926));
#80364=CARTESIAN_POINT('Ctrl Pts',(-28.3589403179533,4.64240186454643,129.174667472675));
#80365=CARTESIAN_POINT('Ctrl Pts',(-28.3667146520724,4.59532462637429,129.046266673229));
#80366=CARTESIAN_POINT('Ctrl Pts',(-28.3744889861914,4.54290085425753,128.919888571903));
#80367=CARTESIAN_POINT('Ctrl Pts',(-28.3822537391385,4.49054168975466,128.793666220292));
#80368=CARTESIAN_POINT('Ctrl Pts',(-28.3900184920856,4.43284925006628,128.669461964544));
#80369=CARTESIAN_POINT('Ctrl Pts',(-28.3977832450327,4.37000285825083,128.547757400033));
#80370=CARTESIAN_POINT('Ctrl Pts',(-28.4055402859177,4.30721888635772,128.426173714211));
#80371=CARTESIAN_POINT('Ctrl Pts',(-28.4132973268027,4.23929132755739,128.30708512402));
#80372=CARTESIAN_POINT('Ctrl Pts',(-28.4210543676877,4.16644761092212,128.190953384098));
#80373=CARTESIAN_POINT('Ctrl Pts',(-28.4288055589278,4.0936588263002,128.074909220025));
#80374=CARTESIAN_POINT('Ctrl Pts',(-28.4365567501679,4.0159614699311,127.961817797835));
#80375=CARTESIAN_POINT('Ctrl Pts',(-28.444307941408,3.93362875062406,127.852116062187));
#80376=CARTESIAN_POINT('Ctrl Pts',(-28.4520558381851,3.85133102491902,127.742460952703));
#80377=CARTESIAN_POINT('Ctrl Pts',(-28.4598037349622,3.76440208895066,127.636192976344));
#80378=CARTESIAN_POINT('Ctrl Pts',(-28.4675516317393,3.67315817204063,127.533719685628));
#80379=CARTESIAN_POINT('Ctrl Pts',(-28.4752979078234,3.58193334139091,127.431267830115));
#80380=CARTESIAN_POINT('Ctrl Pts',(-28.4830441839076,3.48639558494988,127.332609373204));
#80381=CARTESIAN_POINT('Ctrl Pts',(-28.4907904599917,3.38690081835619,127.238118069853));
#80382=CARTESIAN_POINT('Ctrl Pts',(-28.498536793257,3.28740531731487,127.143626068989));
#80383=CARTESIAN_POINT('Ctrl Pts',(-28.5062831265224,3.18395303132537,127.0533015523));
#80384=CARTESIAN_POINT('Ctrl Pts',(-28.5140294597877,3.07693576858063,126.967480460651));
#80385=CARTESIAN_POINT('Ctrl Pts',(-28.5217775277907,2.9698945400619,126.881640149963));
#80386=CARTESIAN_POINT('Ctrl Pts',(-28.5295255957936,2.859287051106,126.800305515681));
#80387=CARTESIAN_POINT('Ctrl Pts',(-28.5372736637966,2.74553679416704,126.723771104472));
#80388=CARTESIAN_POINT('Ctrl Pts',(-28.5450299665384,2.63166564210137,126.647155351579));
#80389=CARTESIAN_POINT('Ctrl Pts',(-28.5527862692802,2.51464537459536,126.575350231621));
#80390=CARTESIAN_POINT('Ctrl Pts',(-28.5605425720221,2.39492744496857,126.508606248909));
#80391=CARTESIAN_POINT('Ctrl Pts',(-28.5683030145362,2.2751456182781,126.441826642923));
#80392=CARTESIAN_POINT('Ctrl Pts',(-28.5760634570504,2.15266360947595,126.38011373255));
#80393=CARTESIAN_POINT('Ctrl Pts',(-28.5838238995646,2.02795497852603,126.323670752426));
#80394=CARTESIAN_POINT('Ctrl Pts',(-28.59159679983,1.90304615421043,126.267137165019));
#80395=CARTESIAN_POINT('Ctrl Pts',(-28.5993697000955,1.77590392783999,126.215890559401));
#80396=CARTESIAN_POINT('Ctrl Pts',(-28.607142600361,1.64702006931879,126.170085274671));
#80397=CARTESIAN_POINT('Ctrl Pts',(-28.614632936123,1.52282146369298,126.125945127418));
#80398=CARTESIAN_POINT('Ctrl Pts',(-28.622123271885,1.39700594709441,126.086857649393));
#80399=CARTESIAN_POINT('Ctrl Pts',(-28.6296136076471,1.27002258328984,126.052916026662));
#80400=CARTESIAN_POINT('Ctrl Pts',(-28.6373879417662,1.13822460665161,126.017687496988));
#80401=CARTESIAN_POINT('Ctrl Pts',(-28.6451622758853,1.0047509804201,125.987891142294));
#80402=CARTESIAN_POINT('Ctrl Pts',(-28.6529366100044,0.870089175209734,
125.963686295771));
#80403=CARTESIAN_POINT('Ctrl Pts',(-28.6607013629515,0.735593328639214,
125.939511279558));
#80404=CARTESIAN_POINT('Ctrl Pts',(-28.6684661158986,0.599912597763412,
125.920914128914));
#80405=CARTESIAN_POINT('Ctrl Pts',(-28.6762308688457,0.463549090902945,
125.908004288333));
#80406=CARTESIAN_POINT('Ctrl Pts',(-28.6839879097307,0.327321022200065,
125.895107269988));
#80407=CARTESIAN_POINT('Ctrl Pts',(-28.6917449506157,0.190411913753323,
125.887886357116));
#80408=CARTESIAN_POINT('Ctrl Pts',(-28.6995019915007,0.0533331837876476,
125.886399796859));
#80409=CARTESIAN_POINT('Ctrl Pts',(-28.7072531827408,-0.0836421740414438,
125.884914357629));
#80410=CARTESIAN_POINT('Ctrl Pts',(-28.7150043739809,-0.220786509426215,
125.889154667941));
#80411=CARTESIAN_POINT('Ctrl Pts',(-28.722755565221,-0.357584532415619,
125.899127048746));
#80412=CARTESIAN_POINT('Ctrl Pts',(-28.7305034619981,-0.494324412596046,
125.909095191023));
#80413=CARTESIAN_POINT('Ctrl Pts',(-28.7382513587751,-0.630717884020645,
125.924790529847));
#80414=CARTESIAN_POINT('Ctrl Pts',(-28.7459992555522,-0.766251131541064,
125.946167304624));
#80415=CARTESIAN_POINT('Ctrl Pts',(-28.7537455316363,-0.901756028427861,
125.967539607841));
#80416=CARTESIAN_POINT('Ctrl Pts',(-28.7614918077204,-1.03640067337513,
125.994590922277));
#80417=CARTESIAN_POINT('Ctrl Pts',(-28.7692380838045,-1.16967823465537,
126.027223829711));
#80418=CARTESIAN_POINT('Ctrl Pts',(-28.7769844170699,-1.30295677976047,
126.059856978034));
#80419=CARTESIAN_POINT('Ctrl Pts',(-28.7847307503352,-1.43486784131396,
126.098071708589));
#80420=CARTESIAN_POINT('Ctrl Pts',(-28.7924770836006,-1.56491700085398,
126.141719966289));
#80421=CARTESIAN_POINT('Ctrl Pts',(-28.8002251516036,-1.69499528400158,
126.185377998714));
#80422=CARTESIAN_POINT('Ctrl Pts',(-28.8079732196066,-1.82321046485832,
126.234471855202));
#80423=CARTESIAN_POINT('Ctrl Pts',(-28.8157212876095,-1.94908582495608,
126.288804449224));
#80424=CARTESIAN_POINT('Ctrl Pts',(-28.8234775903514,-2.07509496688448,
126.343194788573));
#80425=CARTESIAN_POINT('Ctrl Pts',(-28.8312338930932,-2.19875896089797,
126.402834832537));
#80426=CARTESIAN_POINT('Ctrl Pts',(-28.8389901958351,-2.31962302907808,
126.467480164352));
#80427=CARTESIAN_POINT('Ctrl Pts',(-28.8467506383492,-2.44055160605051,
126.532159999327));
#80428=CARTESIAN_POINT('Ctrl Pts',(-28.8545110808634,-2.55867694289546,
126.601850246724));
#80429=CARTESIAN_POINT('Ctrl Pts',(-28.8622715233776,-2.67357208182827,
126.676262340421));
#80430=CARTESIAN_POINT('Ctrl Pts',(-28.870044423643,-2.78865166063801,126.750793887016));
#80431=CARTESIAN_POINT('Ctrl Pts',(-28.8778173239085,-2.9004903602987,126.830062200812));
#80432=CARTESIAN_POINT('Ctrl Pts',(-28.8855902241739,-3.00869251730853,
126.913736965914));
#80433=CARTESIAN_POINT('Ctrl Pts',(-28.8930805599359,-3.11296125336598,
126.994369942541));
#80434=CARTESIAN_POINT('Ctrl Pts',(-28.9005708956979,-3.21385301557886,
127.079094363298));
#80435=CARTESIAN_POINT('Ctrl Pts',(-28.9080612314599,-3.31104667393621,
127.167582787465));
#80436=CARTESIAN_POINT('Ctrl Pts',(-28.9157178265862,-3.41039769297248,
127.258035346433));
#80437=CARTESIAN_POINT('Ctrl Pts',(-28.9233744217124,-3.50621937401956,
127.352726200813));
#80438=CARTESIAN_POINT('Ctrl Pts',(-28.9310310168386,-3.59812010972619,
127.45134484986));
#80439=CARTESIAN_POINT('Ctrl Pts',(-28.9386787643668,-3.68991464930377,
127.549849539876));
#80440=CARTESIAN_POINT('Ctrl Pts',(-28.9463265118951,-3.77779697796692,
127.652272710351));
#80441=CARTESIAN_POINT('Ctrl Pts',(-28.9539742594233,-3.86140890898757,
127.758264049811));
#80442=CARTESIAN_POINT('Ctrl Pts',(-28.9616149438516,-3.94494361996105,
127.864157500654));
#80443=CARTESIAN_POINT('Ctrl Pts',(-28.9692556282801,-4.02421552685795,
127.973612253527));
#80444=CARTESIAN_POINT('Ctrl Pts',(-28.9768963127084,-4.09890405487364,
128.08624203821));
#80445=CARTESIAN_POINT('Ctrl Pts',(-28.9846344939487,-4.17454562491685,
128.200309003692));
#80446=CARTESIAN_POINT('Ctrl Pts',(-28.992372675189,-4.24548573850194,128.317632293919));
#80447=CARTESIAN_POINT('Ctrl Pts',(-29.0001108564294,-4.31143403894221,
128.437776667999));
#80448=CARTESIAN_POINT('Ctrl Pts',(-29.0077430609832,-4.3764791578535,128.556275629251));
#80449=CARTESIAN_POINT('Ctrl Pts',(-29.0153752655371,-4.43666813624174,
128.677518522198));
#80450=CARTESIAN_POINT('Ctrl Pts',(-29.0230074700909,-4.49176690799423,
128.801060064292));
#80451=CARTESIAN_POINT('Ctrl Pts',(-29.0307986396745,-4.54801328760144,
128.927174753474));
#80452=CARTESIAN_POINT('Ctrl Pts',(-29.0385898092582,-4.5989548535771,129.055684531569));
#80453=CARTESIAN_POINT('Ctrl Pts',(-29.0463809788419,-4.64439333110353,
129.186091898069));
#80454=CARTESIAN_POINT('Ctrl Pts',(-29.0541721484255,-4.68983180862997,
129.31649926457));
#80455=CARTESIAN_POINT('Ctrl Pts',(-29.0619633180091,-4.72976705823019,
129.448803794148));
#80456=CARTESIAN_POINT('Ctrl Pts',(-29.0697544875927,-4.76405452823408,
129.582490119308));
#80457=CARTESIAN_POINT('Origin',(213.235140564004,0.,130.804360617566));
#80458=CARTESIAN_POINT('',(-31.1654202583464,-4.76405452823401,129.582490119308));
#80459=CARTESIAN_POINT('',(-30.8197844671783,-4.7640545282341,129.582490119308));
#80460=CARTESIAN_POINT('',(213.235140564004,-4.76405452823405,129.582490119308));
#80461=CARTESIAN_POINT('',(-29.4851405640419,-4.91824861549777,130.800670271478));
#80462=CARTESIAN_POINT('Ctrl Pts',(-29.4851405640418,-4.91824861549777,
130.800670271479));
#80463=CARTESIAN_POINT('Ctrl Pts',(-29.4927930356503,-4.91834965534574,
130.935329482471));
#80464=CARTESIAN_POINT('Ctrl Pts',(-29.5004455072588,-4.9129161848214,131.070199397566));
#80465=CARTESIAN_POINT('Ctrl Pts',(-29.5080979788673,-4.90192287276748,
131.204779413252));
#80466=CARTESIAN_POINT('Ctrl Pts',(-29.5157426700542,-4.89094073783477,
131.339222598733));
#80467=CARTESIAN_POINT('Ctrl Pts',(-29.523387361241,-4.87441003651631,131.473376071944));
#80468=CARTESIAN_POINT('Ctrl Pts',(-29.5310320524279,-4.85235746788152,
131.60673837548));
#80469=CARTESIAN_POINT('Ctrl Pts',(-29.5390646796908,-4.82918582370335,
131.746868257648));
#80470=CARTESIAN_POINT('Ctrl Pts',(-29.5470973069538,-4.79991719261537,
131.886124119136));
#80471=CARTESIAN_POINT('Ctrl Pts',(-29.5551299342168,-4.76464445377761,
132.023928693397));
#80472=CARTESIAN_POINT('Ctrl Pts',(-29.5627655150732,-4.7311152184967,132.154921696647));
#80473=CARTESIAN_POINT('Ctrl Pts',(-29.5704010959297,-4.69216129203358,
132.284602997777));
#80474=CARTESIAN_POINT('Ctrl Pts',(-29.5780366767862,-4.64791490469885,
132.41248688785));
#80475=CARTESIAN_POINT('Ctrl Pts',(-29.5856709314088,-4.60367620257575,
132.540348565607));
#80476=CARTESIAN_POINT('Ctrl Pts',(-29.5933051860314,-4.55414699898319,
132.666413071893));
#80477=CARTESIAN_POINT('Ctrl Pts',(-29.600939440654,-4.49950911101767,132.790210768602));
#80478=CARTESIAN_POINT('Ctrl Pts',(-29.6085741346125,-4.44486807875266,
132.914015589617));
#80479=CARTESIAN_POINT('Ctrl Pts',(-29.616208828571,-4.38511794075102,133.035552972723));
#80480=CARTESIAN_POINT('Ctrl Pts',(-29.6238435225295,-4.3204880540809,133.154374667959));
#80481=CARTESIAN_POINT('Ctrl Pts',(-29.6314804215562,-4.25583950087188,
133.273230681525));
#80482=CARTESIAN_POINT('Ctrl Pts',(-29.639117320583,-4.18630858960663,133.38936909364));
#80483=CARTESIAN_POINT('Ctrl Pts',(-29.6467542196097,-4.11216958661395,
133.502368095952));
#80484=CARTESIAN_POINT('Ctrl Pts',(-29.6543992370009,-4.03795177055231,
133.615487221247));
#80485=CARTESIAN_POINT('Ctrl Pts',(-29.6620442543922,-3.95911630688897,
133.725459938272));
#80486=CARTESIAN_POINT('Ctrl Pts',(-29.6696892717835,-3.8759797160554,133.831894977937));
#80487=CARTESIAN_POINT('Ctrl Pts',(-29.6773390192001,-3.79279168803573,
133.9383958697));
#80488=CARTESIAN_POINT('Ctrl Pts',(-29.6849887666167,-3.70529749652613,
134.041354421144));
#80489=CARTESIAN_POINT('Ctrl Pts',(-29.6926385140333,-3.61385163861373,
134.140415083037));
#80490=CARTESIAN_POINT('Ctrl Pts',(-29.7002991120519,-3.52227607150229,
134.239616255167));
#80491=CARTESIAN_POINT('Ctrl Pts',(-29.7079597100705,-3.42673793667808,
134.334908220911));
#80492=CARTESIAN_POINT('Ctrl Pts',(-29.7156203080891,-3.32762618744494,
134.42597448698));
#80493=CARTESIAN_POINT('Ctrl Pts',(-29.7183519076392,-3.29228513326763,
134.458446700091));
#80494=CARTESIAN_POINT('Ctrl Pts',(-29.7210835071891,-3.25648998315958,
134.490382017532));
#80495=CARTESIAN_POINT('Ctrl Pts',(-29.7238151067391,-3.22025926066219,
134.521767422937));
#80496=CARTESIAN_POINT('Ctrl Pts',(-29.7315894408582,-3.11714394785248,
134.61109260535));
#80497=CARTESIAN_POINT('Ctrl Pts',(-29.7393637749773,-3.01014587040966,
134.696265623824));
#80498=CARTESIAN_POINT('Ctrl Pts',(-29.7471381090964,-2.89963371300888,
134.776929986738));
#80499=CARTESIAN_POINT('Ctrl Pts',(-29.7549028620435,-2.78925775196533,
134.857494938034));
#80500=CARTESIAN_POINT('Ctrl Pts',(-29.7626676149905,-2.67537664070298,
134.933562061292));
#80501=CARTESIAN_POINT('Ctrl Pts',(-29.7704323679376,-2.55839404725985,
135.004813326673));
#80502=CARTESIAN_POINT('Ctrl Pts',(-29.7781894088226,-2.44152764257769,
135.075993824293));
#80503=CARTESIAN_POINT('Ctrl Pts',(-29.7859464497077,-2.32156621766588,
135.142367780719));
#80504=CARTESIAN_POINT('Ctrl Pts',(-29.7937034905927,-2.19894420510965,
135.203659134979));
#80505=CARTESIAN_POINT('Ctrl Pts',(-29.8014546818328,-2.07641466276745,
135.264904268953));
#80506=CARTESIAN_POINT('Ctrl Pts',(-29.809205873073,-1.95122887463564,135.321074255684));
#80507=CARTESIAN_POINT('Ctrl Pts',(-29.8169570643131,-1.82384746617401,
135.371938037012));
#80508=CARTESIAN_POINT('Ctrl Pts',(-29.8247049610902,-1.69652019820863,
135.422780199876));
#80509=CARTESIAN_POINT('Ctrl Pts',(-29.8324528578671,-1.56699952830063,
135.468320498235));
#80510=CARTESIAN_POINT('Ctrl Pts',(-29.8402007546442,-1.43576753470486,
135.508375354872));
#80511=CARTESIAN_POINT('Ctrl Pts',(-29.8479470307283,-1.30456299201311,
135.548421832896));
#80512=CARTESIAN_POINT('Ctrl Pts',(-29.8556933068124,-1.17164821135772,
135.58298503745));
#80513=CARTESIAN_POINT('Ctrl Pts',(-29.8634395828965,-1.0375215845876,135.611930900361));
#80514=CARTESIAN_POINT('Ctrl Pts',(-29.8711859161619,-0.903393967725188,
135.640876976944));
#80515=CARTESIAN_POINT('Ctrl Pts',(-29.8789322494272,-0.768054869064787,
135.664205546666));
#80516=CARTESIAN_POINT('Ctrl Pts',(-29.8866785826926,-0.632013664642088,
135.681833507312));
#80517=CARTESIAN_POINT('Ctrl Pts',(-29.8944266506956,-0.495941994734903,
135.699465415617));
#80518=CARTESIAN_POINT('Ctrl Pts',(-29.9021747186985,-0.359168293842022,
135.711394124304));
#80519=CARTESIAN_POINT('Ctrl Pts',(-29.9099227867015,-0.222207465767521,
135.717588365662));
#80520=CARTESIAN_POINT('Ctrl Pts',(-29.9176790894434,-0.0851010740949017,
135.723789190333));
#80521=CARTESIAN_POINT('Ctrl Pts',(-29.9254353921852,0.052192450856806,
135.724243355241));
#80522=CARTESIAN_POINT('Ctrl Pts',(-29.9331916949271,0.189157235024127,
135.718971752024));
#80523=CARTESIAN_POINT('Ctrl Pts',(-29.9409521374413,0.326195121420689,
135.713697335193));
#80524=CARTESIAN_POINT('Ctrl Pts',(-29.9487125799554,0.462903527902638,
135.702691092227));
#80525=CARTESIAN_POINT('Ctrl Pts',(-29.9564730224696,0.598772288770548,
135.68602578518));
#80526=CARTESIAN_POINT('Ctrl Pts',(-29.964245922735,0.734859158235081,135.669333725503));
#80527=CARTESIAN_POINT('Ctrl Pts',(-29.9720188230004,0.870103302657755,
135.646964511991));
#80528=CARTESIAN_POINT('Ctrl Pts',(-29.9797917232658,1.00400443845168,135.619042138712));
#80529=CARTESIAN_POINT('Ctrl Pts',(-29.9872820590279,1.13303793068343,135.592134814035));
#80530=CARTESIAN_POINT('Ctrl Pts',(-29.9947723947899,1.26082406378781,135.560071137679));
#80531=CARTESIAN_POINT('Ctrl Pts',(-30.002262730552,1.3869308381967,135.523005117055));
#80532=CARTESIAN_POINT('Ctrl Pts',(-30.0100370646711,1.51781898928626,135.484533726994));
#80533=CARTESIAN_POINT('Ctrl Pts',(-30.0178113987902,1.64731253638487,135.44055131105));
#80534=CARTESIAN_POINT('Ctrl Pts',(-30.0255857329093,1.77491226992272,135.391175361653));
#80535=CARTESIAN_POINT('Ctrl Pts',(-30.0333504858564,1.9023547481929,135.341860263702));
#80536=CARTESIAN_POINT('Ctrl Pts',(-30.0411152388034,2.02790769566083,135.28716499768));
#80537=CARTESIAN_POINT('Ctrl Pts',(-30.0488799917505,2.15108535238151,135.227257278044));
#80538=CARTESIAN_POINT('Ctrl Pts',(-30.0566370326355,2.27414066731688,135.167409059601));
#80539=CARTESIAN_POINT('Ctrl Pts',(-30.0643940735206,2.39482503705114,135.10235886006));
#80540=CARTESIAN_POINT('Ctrl Pts',(-30.0721511144056,2.51267138224773,135.032322962163));
#80541=CARTESIAN_POINT('Ctrl Pts',(-30.0799023056457,2.63042885859885,134.962339878882));
#80542=CARTESIAN_POINT('Ctrl Pts',(-30.0876534968858,2.74535223557114,134.887378779737));
#80543=CARTESIAN_POINT('Ctrl Pts',(-30.0954046881259,2.85699813807721,134.807702309393));
#80544=CARTESIAN_POINT('Ctrl Pts',(-30.103152584903,2.96859658809631,134.728059703675));
#80545=CARTESIAN_POINT('Ctrl Pts',(-30.11090048168,3.07692001667762,134.643705939512));
#80546=CARTESIAN_POINT('Ctrl Pts',(-30.1186483784571,3.18155340003668,134.554947375023));
#80547=CARTESIAN_POINT('Ctrl Pts',(-30.1263946545412,3.28616489634743,134.466207376913));
#80548=CARTESIAN_POINT('Ctrl Pts',(-30.1341409306253,3.38708758478787,134.37306466392));
#80549=CARTESIAN_POINT('Ctrl Pts',(-30.1418872067094,3.48393927703865,134.275866080101));
#80550=CARTESIAN_POINT('Ctrl Pts',(-30.1496335399748,3.58079168422675,134.178666778783));
#80551=CARTESIAN_POINT('Ctrl Pts',(-30.1573798732401,3.67357275930074,134.077411823844));
#80552=CARTESIAN_POINT('Ctrl Pts',(-30.1651262065054,3.76193725582314,133.972484848992));
#80553=CARTESIAN_POINT('Ctrl Pts',(-30.1728742745084,3.85032154096186,133.867534376471));
#80554=CARTESIAN_POINT('Ctrl Pts',(-30.1806223425114,3.93428702763511,133.758910546698));
#80555=CARTESIAN_POINT('Ctrl Pts',(-30.1883704105143,4.01352909134764,133.647029661863));
#80556=CARTESIAN_POINT('Ctrl Pts',(-30.1961267132562,4.09285537446848,133.535029868693));
#80557=CARTESIAN_POINT('Ctrl Pts',(-30.2038830159981,4.16744798008595,133.419766425023));
#80558=CARTESIAN_POINT('Ctrl Pts',(-30.2116393187399,4.23704564239276,133.301684642754));
#80559=CARTESIAN_POINT('Ctrl Pts',(-30.2193997612541,4.30668045106768,133.183539836682));
#80560=CARTESIAN_POINT('Ctrl Pts',(-30.2271602037682,4.3713148201394,133.06257403936));
#80561=CARTESIAN_POINT('Ctrl Pts',(-30.2349206462824,4.43073420936317,132.939255797306));
#80562=CARTESIAN_POINT('Ctrl Pts',(-30.2426935465478,4.49024898386537,132.815739593864));
#80563=CARTESIAN_POINT('Ctrl Pts',(-30.2504664468134,4.54453189459061,132.689863758546));
#80564=CARTESIAN_POINT('Ctrl Pts',(-30.2582393470788,4.59341684576232,132.562116215926));
#80565=CARTESIAN_POINT('Ctrl Pts',(-30.2657296828408,4.6405247058253,132.439012618257));
#80566=CARTESIAN_POINT('Ctrl Pts',(-30.2732200186028,4.68262015310914,132.314171325116));
#80567=CARTESIAN_POINT('Ctrl Pts',(-30.2807103543649,4.71959925209145,132.188039034742));
#80568=CARTESIAN_POINT('Ctrl Pts',(-30.2884846884839,4.75798042485118,132.057124400241));
#80569=CARTESIAN_POINT('Ctrl Pts',(-30.296259022603,4.79097119793339,131.924404241471));
#80570=CARTESIAN_POINT('Ctrl Pts',(-30.3040333567221,4.81840058608051,131.79036206511));
#80571=CARTESIAN_POINT('Ctrl Pts',(-30.3117981096692,4.84579616995811,131.656485083752));
#80572=CARTESIAN_POINT('Ctrl Pts',(-30.3195628626163,4.86764392851099,131.521289705912));
#80573=CARTESIAN_POINT('Ctrl Pts',(-30.3273276155633,4.88382239954593,131.385275268951));
#80574=CARTESIAN_POINT('Ctrl Pts',(-30.3350846564484,4.89998480189542,131.249395923445));
#80575=CARTESIAN_POINT('Ctrl Pts',(-30.3428416973333,4.91048907642576,131.112699523437));
#80576=CARTESIAN_POINT('Ctrl Pts',(-30.3505987382184,4.91526472014121,130.975695942106));
#80577=CARTESIAN_POINT('Ctrl Pts',(-30.3583499294585,4.92003676250659,130.838795676241));
#80578=CARTESIAN_POINT('Ctrl Pts',(-30.3661011206987,4.91908875920035,130.70158907928));
#80579=CARTESIAN_POINT('Ctrl Pts',(-30.3738523119389,4.91240202555274,130.564591141099));
#80580=CARTESIAN_POINT('Ctrl Pts',(-30.381600208716,4.90571813394531,130.427651430696));
#80581=CARTESIAN_POINT('Ctrl Pts',(-30.389348105493,4.89330038222731,130.290920592366));
#80582=CARTESIAN_POINT('Ctrl Pts',(-30.3970960022701,4.87518218766754,130.15491339142));
#80583=CARTESIAN_POINT('Ctrl Pts',(-30.4048422783542,4.85706778304351,130.018934640248));
#80584=CARTESIAN_POINT('Ctrl Pts',(-30.4125885544383,4.83325535893973,129.883679612674));
#80585=CARTESIAN_POINT('Ctrl Pts',(-30.4203348305223,4.80383014296098,129.749657332239));
#80586=CARTESIAN_POINT('Ctrl Pts',(-30.4280811637876,4.77440470977205,129.615634062482));
#80587=CARTESIAN_POINT('Ctrl Pts',(-30.435827497053,4.73936648587419,129.482843939892));
#80588=CARTESIAN_POINT('Ctrl Pts',(-30.4435738303184,4.69885161903793,129.351784793464));
#80589=CARTESIAN_POINT('Ctrl Pts',(-30.4513218983214,4.65832767917798,129.220696297249));
#80590=CARTESIAN_POINT('Ctrl Pts',(-30.4590699663244,4.61232477132086,129.091339922007));
#80591=CARTESIAN_POINT('Ctrl Pts',(-30.4668180343274,4.56102848530953,128.964196978458));
#80592=CARTESIAN_POINT('Ctrl Pts',(-30.4745743370693,4.50967768099499,128.836918905875));
#80593=CARTESIAN_POINT('Ctrl Pts',(-30.482330639811,4.45302240676723,128.711859327427));
#80594=CARTESIAN_POINT('Ctrl Pts',(-30.4900869425529,4.39129609558846,128.589478755396));
#80595=CARTESIAN_POINT('Ctrl Pts',(-30.4978473850671,4.32953683921888,128.467032865169));
#80596=CARTESIAN_POINT('Ctrl Pts',(-30.5056078275813,4.26270134326782,128.347269171722));
#80597=CARTESIAN_POINT('Ctrl Pts',(-30.5133682700954,4.19106784494925,128.230621434678));
#80598=CARTESIAN_POINT('Ctrl Pts',(-30.5211411703609,4.11931935417987,128.113786444332));
#80599=CARTESIAN_POINT('Ctrl Pts',(-30.5289140706263,4.04275768811868,128.000077730489));
#80600=CARTESIAN_POINT('Ctrl Pts',(-30.5366869708918,3.96170357270389,127.889898769381));
#80601=CARTESIAN_POINT('Ctrl Pts',(-30.5441773066538,3.88359597854754,127.783725091034));
#80602=CARTESIAN_POINT('Ctrl Pts',(-30.5516676424158,3.80131708043434,127.680829230668));
#80603=CARTESIAN_POINT('Ctrl Pts',(-30.5591579781778,3.7151865185552,127.581540083493));
#80604=CARTESIAN_POINT('Ctrl Pts',(-30.5669323122969,3.62579029024359,127.478486358123));
#80605=CARTESIAN_POINT('Ctrl Pts',(-30.574706646416,3.53196138053587,127.378991798697));
#80606=CARTESIAN_POINT('Ctrl Pts',(-30.5824809805351,3.43401415558535,127.283461607123));
#80607=CARTESIAN_POINT('Ctrl Pts',(-30.5902457334821,3.33618764183565,127.188049147972));
#80608=CARTESIAN_POINT('Ctrl Pts',(-30.5980104864293,3.23425318868581,127.096591605888));
#80609=CARTESIAN_POINT('Ctrl Pts',(-30.6057752393764,3.12856524951621,127.009461074492));
#80610=CARTESIAN_POINT('Ctrl Pts',(-30.6135322802613,3.02298228109817,126.92241708237));
#80611=CARTESIAN_POINT('Ctrl Pts',(-30.6212893211463,2.91365354529384,126.839691795512));
#80612=CARTESIAN_POINT('Ctrl Pts',(-30.6290463620313,2.80096990425718,126.761620128993));
#80613=CARTESIAN_POINT('Ctrl Pts',(-30.6367975532714,2.68837123882986,126.683607336925));
#80614=CARTESIAN_POINT('Ctrl Pts',(-30.6445487445116,2.57242302397057,126.61024140184));
#80615=CARTESIAN_POINT('Ctrl Pts',(-30.6522999357518,2.45354843572592,126.541816408288));
#80616=CARTESIAN_POINT('Ctrl Pts',(-30.6600478325288,2.334724372353,126.473420497184));
#80617=CARTESIAN_POINT('Ctrl Pts',(-30.6677957293059,2.21297674752372,126.40996154544));
#80618=CARTESIAN_POINT('Ctrl Pts',(-30.675543626083,2.08875671072263,126.351689681385));
#80619=CARTESIAN_POINT('Ctrl Pts',(-30.6832899021671,1.96456265807554,126.293430006548));
#80620=CARTESIAN_POINT('Ctrl Pts',(-30.6910361782511,1.83789757587744,126.240355427158));
#80621=CARTESIAN_POINT('Ctrl Pts',(-30.6987824543352,1.70923578765204,126.192669378475));
#80622=CARTESIAN_POINT('Ctrl Pts',(-30.7065287876006,1.58057304967456,126.144982977784));
#80623=CARTESIAN_POINT('Ctrl Pts',(-30.7142751208659,1.44991394285471,126.102685323045));
#80624=CARTESIAN_POINT('Ctrl Pts',(-30.7220214541313,1.31775089602114,126.065930958013));
#80625=CARTESIAN_POINT('Ctrl Pts',(-30.7297695221342,1.18555825218942,126.029168362095));
#80626=CARTESIAN_POINT('Ctrl Pts',(-30.7375175901372,1.05186137475576,125.997951630822));
#80627=CARTESIAN_POINT('Ctrl Pts',(-30.7452656581402,0.917165519902225,
125.972384782403));
#80628=CARTESIAN_POINT('Ctrl Pts',(-30.753021960882,0.782326508691256,125.946790761232));
#80629=CARTESIAN_POINT('Ctrl Pts',(-30.7607782636239,0.646486783869696,
125.9268586911));
#80630=CARTESIAN_POINT('Ctrl Pts',(-30.7685345663657,0.510159963680854,
125.91264109638));
#80631=CARTESIAN_POINT('Ctrl Pts',(-30.7762950088799,0.373760381763356,
125.898415913301));
#80632=CARTESIAN_POINT('Ctrl Pts',(-30.7840554513941,0.236873576473364,
125.889911307225));
#80633=CARTESIAN_POINT('Ctrl Pts',(-30.7918158939082,0.100014876076593,
125.887127646975));
#80634=CARTESIAN_POINT('Ctrl Pts',(-30.7995887941737,-0.0370635220559864,
125.884339518147));
#80635=CARTESIAN_POINT('Ctrl Pts',(-30.8073616944391,-0.17411333403871,
125.887290678821));
#80636=CARTESIAN_POINT('Ctrl Pts',(-30.8151345947045,-0.310621743687501,
125.895929381942));
#80637=CARTESIAN_POINT('Ctrl Pts',(-30.8226249304666,-0.44216772880218,
125.904254046445));
#80638=CARTESIAN_POINT('Ctrl Pts',(-30.8301152662286,-0.573210684494612,
125.917859887788));
#80639=CARTESIAN_POINT('Ctrl Pts',(-30.8376056019907,-0.703301128580765,
125.936655759521));
#80640=CARTESIAN_POINT('Ctrl Pts',(-30.8453799361097,-0.838323991393825,
125.956164282443));
#80641=CARTESIAN_POINT('Ctrl Pts',(-30.8531542702288,-0.972748399667074,
125.981325961893));
#80642=CARTESIAN_POINT('Ctrl Pts',(-30.8609286043479,-1.10606352297363,
126.012095334253));
#80643=CARTESIAN_POINT('Ctrl Pts',(-30.868693357295,-1.23921434730562,126.042826786112));
#80644=CARTESIAN_POINT('Ctrl Pts',(-30.876458110242,-1.3712582294884,126.079152093009));
#80645=CARTESIAN_POINT('Ctrl Pts',(-30.8842228631891,-1.50169052590856,
126.12097416897));
#80646=CARTESIAN_POINT('Ctrl Pts',(-30.8919799040741,-1.63199327513315,
126.162754706655));
#80647=CARTESIAN_POINT('Ctrl Pts',(-30.8997369449592,-1.76068725407411,
126.210021030214));
#80648=CARTESIAN_POINT('Ctrl Pts',(-30.9074939858442,-1.88727941865261,
126.262625326025));
#80649=CARTESIAN_POINT('Ctrl Pts',(-30.9152451770844,-2.01377611909574,
126.315189952528));
#80650=CARTESIAN_POINT('Ctrl Pts',(-30.9229963683245,-2.13817380043774,
126.373084389537));
#80651=CARTESIAN_POINT('Ctrl Pts',(-30.9307475595647,-2.25999630402923,
126.436111566942));
#80652=CARTESIAN_POINT('Ctrl Pts',(-30.9384954563418,-2.38176702980647,
126.499111956116));
#80653=CARTESIAN_POINT('Ctrl Pts',(-30.9462433531189,-2.50096440823137,
126.567240567468));
#80654=CARTESIAN_POINT('Ctrl Pts',(-30.9539912498959,-2.61713414194007,
126.640253036632));
#80655=CARTESIAN_POINT('Ctrl Pts',(-30.96173752598,-2.73327957544448,126.713250233161));
#80656=CARTESIAN_POINT('Ctrl Pts',(-30.9694838020642,-2.8463982931303,126.791129047577));
#80657=CARTESIAN_POINT('Ctrl Pts',(-30.9772300781483,-2.95606275570117,
126.873600379793));
#80658=CARTESIAN_POINT('Ctrl Pts',(-30.9849764114136,-3.06572802779019,
126.956072320793));
#80659=CARTESIAN_POINT('Ctrl Pts',(-30.992722744679,-3.17193868141687,127.043136612255));
#80660=CARTESIAN_POINT('Ctrl Pts',(-31.0004690779443,-3.27429852473151,
127.134462494533));
#80661=CARTESIAN_POINT('Ctrl Pts',(-31.0082171459473,-3.37668129082363,
127.22580882861));
#80662=CARTESIAN_POINT('Ctrl Pts',(-31.0159652139503,-3.47521123892816,
127.321418392323));
#80663=CARTESIAN_POINT('Ctrl Pts',(-31.0237132819533,-3.5695277522721,127.420922323721));
#80664=CARTESIAN_POINT('Ctrl Pts',(-31.0314695846951,-3.66394450632867,
127.52053200908));
#80665=CARTESIAN_POINT('Ctrl Pts',(-31.039225887437,-3.75413861077265,127.624044045979));
#80666=CARTESIAN_POINT('Ctrl Pts',(-31.0469821901788,-3.83978825215359,
127.73105470355));
#80667=CARTESIAN_POINT('Ctrl Pts',(-31.054742632693,-3.92548360732699,127.838122475931));
#80668=CARTESIAN_POINT('Ctrl Pts',(-31.0625030752072,-4.00662943518677,
127.948692274737));
#80669=CARTESIAN_POINT('Ctrl Pts',(-31.0702635177213,-4.08294687791647,
128.062330739061));
#80670=CARTESIAN_POINT('Ctrl Pts',(-31.0780364179868,-4.15938683218039,
128.176151625937));
#80671=CARTESIAN_POINT('Ctrl Pts',(-31.0858093182522,-4.230982708128,128.293050688641));
#80672=CARTESIAN_POINT('Ctrl Pts',(-31.0935822185176,-4.29750085235006,
128.412568509846));
#80673=CARTESIAN_POINT('Ctrl Pts',(-31.1010725542795,-4.36160089447973,
128.527741557202));
#80674=CARTESIAN_POINT('Ctrl Pts',(-31.1085628900415,-4.42098583327287,
128.645345996741));
#80675=CARTESIAN_POINT('Ctrl Pts',(-31.1160532258035,-4.47548939672102,
128.764954399487));
#80676=CARTESIAN_POINT('Ctrl Pts',(-31.1245404803809,-4.53724705793451,
128.900481964068));
#80677=CARTESIAN_POINT('Ctrl Pts',(-31.1330277349583,-4.59290752930504,
129.038954402169));
#80678=CARTESIAN_POINT('Ctrl Pts',(-31.1415149895357,-4.64220592367311,
129.179827692472));
#80679=CARTESIAN_POINT('Ctrl Pts',(-31.1494834124726,-4.68849067368878,
129.312089302797));
#80680=CARTESIAN_POINT('Ctrl Pts',(-31.1574518354095,-4.72916767521412,
129.446466808865));
#80681=CARTESIAN_POINT('Ctrl Pts',(-31.1654202583464,-4.76405452823401,
129.582490119308));
#80682=CARTESIAN_POINT('Ctrl Pts',(-29.4150816029337,-4.76405452823407,
129.582490119308));
#80683=CARTESIAN_POINT('Ctrl Pts',(-29.4228566469627,-4.7980744352381,129.715133220393));
#80684=CARTESIAN_POINT('Ctrl Pts',(-29.4306316909917,-4.82650842637683,
129.849034037413));
#80685=CARTESIAN_POINT('Ctrl Pts',(-29.4384067350207,-4.84929583035118,
129.983682232181));
#80686=CARTESIAN_POINT('Ctrl Pts',(-29.4407269843226,-4.85609610800431,
130.0238643043));
#80687=CARTESIAN_POINT('Ctrl Pts',(-29.4430472336244,-4.86239387499183,
130.064112915958));
#80688=CARTESIAN_POINT('Ctrl Pts',(-29.4453674829263,-4.86818841738373,
130.104414480102));
#80689=CARTESIAN_POINT('Ctrl Pts',(-29.4586251766203,-4.90129790612179,
130.33469395584));
#80690=CARTESIAN_POINT('Ctrl Pts',(-29.4718828703144,-4.91807356675018,
130.567376942442));
#80691=CARTESIAN_POINT('Ctrl Pts',(-29.4851405640086,-4.91824861549733,
130.800670270894));
#80692=CARTESIAN_POINT('',(-29.1398594359388,-4.9182483209296,130.808424627057));
#80693=CARTESIAN_POINT('Ctrl Pts',(-29.0697544875927,-4.76405452823408,
129.582490119308));
#80694=CARTESIAN_POINT('Ctrl Pts',(-29.0773912973827,-4.79766268985716,
129.713527831402));
#80695=CARTESIAN_POINT('Ctrl Pts',(-29.0850281071728,-4.82584473991743,
129.845892683461));
#80696=CARTESIAN_POINT('Ctrl Pts',(-29.0926649169627,-4.84851619709028,
129.979088693257));
#80697=CARTESIAN_POINT('Ctrl Pts',(-29.1005306701254,-4.87186732025087,
130.116277776672));
#80698=CARTESIAN_POINT('Ctrl Pts',(-29.108396423288,-4.88937218816657,130.254348176387));
#80699=CARTESIAN_POINT('Ctrl Pts',(-29.1162621764507,-4.9009960473005,130.392753029146));
#80700=CARTESIAN_POINT('Ctrl Pts',(-29.1241279296134,-4.91261990643446,
130.531157881905));
#80701=CARTESIAN_POINT('Ctrl Pts',(-29.1319936827761,-4.91836278825225,
130.669896722895));
#80702=CARTESIAN_POINT('Ctrl Pts',(-29.1398594359388,-4.9182483209296,130.808424627058));
#80703=CARTESIAN_POINT('Ctrl Pts',(-29.1398594359911,-4.91824832092884,
130.80842462798));
#80704=CARTESIAN_POINT('Ctrl Pts',(-29.1521788354858,-4.91806904133954,
131.025388033418));
#80705=CARTESIAN_POINT('Ctrl Pts',(-29.1644982349803,-4.90353032655609,
131.241777625956));
#80706=CARTESIAN_POINT('Ctrl Pts',(-29.1768176344749,-4.87487472503856,
131.456111703242));
#80707=CARTESIAN_POINT('Ctrl Pts',(-29.1800480414075,-4.86736062065044,
131.512314628512));
#80708=CARTESIAN_POINT('Ctrl Pts',(-29.1832784483402,-4.85887604229768,
131.568376420214));
#80709=CARTESIAN_POINT('Ctrl Pts',(-29.1865088552728,-4.84942579143849,
131.624270707656));
#80710=CARTESIAN_POINT('Ctrl Pts',(-29.1942831893919,-4.82668271008041,
131.758786536462));
#80711=CARTESIAN_POINT('Ctrl Pts',(-29.202057523511,-4.79830246142229,131.892568422899));
#80712=CARTESIAN_POINT('Ctrl Pts',(-29.2098318576301,-4.76434275451195,
132.025106774648));
#80713=CARTESIAN_POINT('Ctrl Pts',(-29.2175966105772,-4.73042489990527,
132.157481784724));
#80714=CARTESIAN_POINT('Ctrl Pts',(-29.2253613635244,-4.6909413647112,132.288615934325));
#80715=CARTESIAN_POINT('Ctrl Pts',(-29.2331261164715,-4.64600131700206,
132.41800705496));
#80716=CARTESIAN_POINT('Ctrl Pts',(-29.2408831573565,-4.60110590438204,
132.547269662509));
#80717=CARTESIAN_POINT('Ctrl Pts',(-29.2486401982414,-4.55076489171014,
132.674792319326));
#80718=CARTESIAN_POINT('Ctrl Pts',(-29.2563972391264,-4.49513788173963,
132.800085670435));
#80719=CARTESIAN_POINT('Ctrl Pts',(-29.2641484303666,-4.43955282052989,
132.925284536854));
#80720=CARTESIAN_POINT('Ctrl Pts',(-29.2718996216067,-4.37868985433787,
133.048257087881));
#80721=CARTESIAN_POINT('Ctrl Pts',(-29.2796508128469,-4.31275742301797,
133.168532031128));
#80722=CARTESIAN_POINT('Ctrl Pts',(-29.287398709624,-4.24685301474019,133.288755854316));
#80723=CARTESIAN_POINT('Ctrl Pts',(-29.295146606401,-4.17588361432586,133.406284008019));
#80724=CARTESIAN_POINT('Ctrl Pts',(-29.3028945031781,-4.100104417655,133.520668189772));
#80725=CARTESIAN_POINT('Ctrl Pts',(-29.3106407792622,-4.02434107235847,
133.635028444821));
#80726=CARTESIAN_POINT('Ctrl Pts',(-29.3183870553464,-3.94377014779473,
133.7462457103));
#80727=CARTESIAN_POINT('Ctrl Pts',(-29.3261333314306,-3.8586909205612,133.853899507641));
#80728=CARTESIAN_POINT('Ctrl Pts',(-29.3338796646959,-3.77361106529214,
133.961554099657));
#80729=CARTESIAN_POINT('Ctrl Pts',(-29.3416259979612,-3.68402308336316,
134.065644864308));
#80730=CARTESIAN_POINT('Ctrl Pts',(-29.3493723312266,-3.59026714667992,
134.165783661155));
#80731=CARTESIAN_POINT('Ctrl Pts',(-29.3571203992296,-3.49649021400472,
134.265944883392));
#80732=CARTESIAN_POINT('Ctrl Pts',(-29.3648684672326,-3.39854373640565,
134.362152091401));
#80733=CARTESIAN_POINT('Ctrl Pts',(-29.3726165352356,-3.29680512342074,
134.454053623928));
#80734=CARTESIAN_POINT('Ctrl Pts',(-29.3803728379774,-3.19495838142724,
134.546052830497));
#80735=CARTESIAN_POINT('Ctrl Pts',(-29.3881291407194,-3.08931174362308,
134.633736957796));
#80736=CARTESIAN_POINT('Ctrl Pts',(-29.3958854434613,-2.98027654724618,
134.716793973476));
#80737=CARTESIAN_POINT('Ctrl Pts',(-29.4036458859754,-2.87118315550183,
134.799895319185));
#80738=CARTESIAN_POINT('Ctrl Pts',(-29.4114063284895,-2.75869792194067,
134.878364408755));
#80739=CARTESIAN_POINT('Ctrl Pts',(-29.4191667710037,-2.64326077449113,
134.951932864138));
#80740=CARTESIAN_POINT('Ctrl Pts',(-29.4269396712691,-2.52763831708462,
135.025619418138));
#80741=CARTESIAN_POINT('Ctrl Pts',(-29.4347125715347,-2.40905481481085,
135.094389421063));
#80742=CARTESIAN_POINT('Ctrl Pts',(-29.4424854718001,-2.28797515973411,
135.158020311541));
#80743=CARTESIAN_POINT('Ctrl Pts',(-29.4499758075619,-2.1712970551036,135.219338058871));
#80744=CARTESIAN_POINT('Ctrl Pts',(-29.4574661433238,-2.05230140795038,
135.275883713991));
#80745=CARTESIAN_POINT('Ctrl Pts',(-29.4649564790856,-1.93141951423011,
135.327501309889));
#80746=CARTESIAN_POINT('Ctrl Pts',(-29.4727308132047,-1.80595434676516,
135.381076002626));
#80747=CARTESIAN_POINT('Ctrl Pts',(-29.4805051473238,-1.67805963918038,
135.429511273083));
#80748=CARTESIAN_POINT('Ctrl Pts',(-29.4882794814429,-1.54819531907598,
135.47258022642));
#80749=CARTESIAN_POINT('Ctrl Pts',(-29.49604423439,-1.41849104513997,135.515596101121));
#80750=CARTESIAN_POINT('Ctrl Pts',(-29.5038089873371,-1.28682235595714,
135.55325869572));
#80751=CARTESIAN_POINT('Ctrl Pts',(-29.5115737402841,-1.15367074811228,
135.585388422071));
#80752=CARTESIAN_POINT('Ctrl Pts',(-29.5193307811692,-1.02065138832126,
135.617486236725));
#80753=CARTESIAN_POINT('Ctrl Pts',(-29.5270878220542,-0.886152418515271,
135.644062027956));
#80754=CARTESIAN_POINT('Ctrl Pts',(-29.5348448629392,-0.750671816080639,
135.664985565764));
#80755=CARTESIAN_POINT('Ctrl Pts',(-29.5425960541793,-0.615293380622188,
135.685893324969));
#80756=CARTESIAN_POINT('Ctrl Pts',(-29.5503472454194,-0.478935170792394,
135.701157255385));
#80757=CARTESIAN_POINT('Ctrl Pts',(-29.5580984366596,-0.342106365057883,
135.710697978316));
#80758=CARTESIAN_POINT('Ctrl Pts',(-29.5658463334367,-0.205335715215836,
135.720234646185));
#80759=CARTESIAN_POINT('Ctrl Pts',(-29.5735942302137,-0.0680952564869745,
135.72405291752));
#80760=CARTESIAN_POINT('Ctrl Pts',(-29.5813421269908,0.0690999019604429,
135.722125177409));
#80761=CARTESIAN_POINT('Ctrl Pts',(-29.5890884030749,0.206266362138298,
135.72019784054));
#80762=CARTESIAN_POINT('Ctrl Pts',(-29.5968346791591,0.343387150203734,
135.712526888442));
#80763=CARTESIAN_POINT('Ctrl Pts',(-29.6045809552432,0.479946739315554,
135.699136832054));
#80764=CARTESIAN_POINT('Ctrl Pts',(-29.6123272885085,0.616507336479052,
135.685746676824));
#80765=CARTESIAN_POINT('Ctrl Pts',(-29.6200736217739,0.752506337323381,
135.666637371216));
#80766=CARTESIAN_POINT('Ctrl Pts',(-29.6278199550392,0.887433317082195,
135.641885312101));
#80767=CARTESIAN_POINT('Ctrl Pts',(-29.6355680230422,1.02239051280261,135.617127709933));
#80768=CARTESIAN_POINT('Ctrl Pts',(-29.6433160910451,1.15627482524811,135.586724910262));
#80769=CARTESIAN_POINT('Ctrl Pts',(-29.6510641590481,1.2885863927717,135.550804356921));
#80770=CARTESIAN_POINT('Ctrl Pts',(-29.6588204617899,1.42103858260379,135.514845626789));
#80771=CARTESIAN_POINT('Ctrl Pts',(-29.6665767645318,1.55191431053923,135.473357530945));
#80772=CARTESIAN_POINT('Ctrl Pts',(-29.6743330672737,1.68072871710143,135.426517477952));
#80773=CARTESIAN_POINT('Ctrl Pts',(-29.6820935097878,1.80961187579113,135.379652425011));
#80774=CARTESIAN_POINT('Ctrl Pts',(-29.6898539523019,1.93643115955007,135.327429871896));
#80775=CARTESIAN_POINT('Ctrl Pts',(-29.6976143948161,2.06072298253663,135.270074877541));
#80776=CARTESIAN_POINT('Ctrl Pts',(-29.7053872950815,2.18521432979157,135.212627811858));
#80777=CARTESIAN_POINT('Ctrl Pts',(-29.713160195347,2.30716976046241,135.150032019318));
#80778=CARTESIAN_POINT('Ctrl Pts',(-29.7209330956125,2.42615074184579,135.082558326922));
#80779=CARTESIAN_POINT('Ctrl Pts',(-29.7284234313746,2.54080646486216,135.0175374732));
#80780=CARTESIAN_POINT('Ctrl Pts',(-29.7359137671366,2.65269997989081,134.947987372913));
#80781=CARTESIAN_POINT('Ctrl Pts',(-29.7434041028988,2.7614669414705,134.874186583583));
#80782=CARTESIAN_POINT('Ctrl Pts',(-29.7511784370179,2.87435783545621,134.797587614895));
#80783=CARTESIAN_POINT('Ctrl Pts',(-29.7589527711369,2.98423801370107,134.716166622017));
#80784=CARTESIAN_POINT('Ctrl Pts',(-29.766727105256,3.09066798104836,134.630187912861));
#80785=CARTESIAN_POINT('Ctrl Pts',(-29.7744918582031,3.19696678297281,134.544315164779));
#80786=CARTESIAN_POINT('Ctrl Pts',(-29.7822566111502,3.29982353315876,134.453896119859));
#80787=CARTESIAN_POINT('Ctrl Pts',(-29.7900213640973,3.39882687834791,134.359238803034));
#80788=CARTESIAN_POINT('Ctrl Pts',(-29.7977784049823,3.49773189201893,134.264675501191));
#80789=CARTESIAN_POINT('Ctrl Pts',(-29.8055354458673,3.5927908363472,134.165882572995));
#80790=CARTESIAN_POINT('Ctrl Pts',(-29.8132924867523,3.68362497620382,134.063208588427));
#80791=CARTESIAN_POINT('Ctrl Pts',(-29.8210436779925,3.77439061732898,133.96061203111));
#80792=CARTESIAN_POINT('Ctrl Pts',(-29.8287948692326,3.86093753743193,133.854140534547));
#80793=CARTESIAN_POINT('Ctrl Pts',(-29.8365460604727,3.94292372956989,133.744179578879));
#80794=CARTESIAN_POINT('Ctrl Pts',(-29.8442939572498,4.02487507538914,133.63426535955));
#80795=CARTESIAN_POINT('Ctrl Pts',(-29.8520418540269,4.10226931542995,133.520864943693));
#80796=CARTESIAN_POINT('Ctrl Pts',(-29.859789750804,4.17480478739694,133.404396780704));
#80797=CARTESIAN_POINT('Ctrl Pts',(-29.8675360268881,4.24732508650688,133.287952980345));
#80798=CARTESIAN_POINT('Ctrl Pts',(-29.8752823029722,4.31498843256487,133.168443040901));
#80799=CARTESIAN_POINT('Ctrl Pts',(-29.8830285790563,4.37753679246813,133.046313938464));
#80800=CARTESIAN_POINT('Ctrl Pts',(-29.8907749123216,4.44008561408918,132.924183934499));
#80801=CARTESIAN_POINT('Ctrl Pts',(-29.898521245587,4.49751919599378,132.799435076945));
#80802=CARTESIAN_POINT('Ctrl Pts',(-29.9062675788523,4.54962591597954,132.672538094988));
#80803=CARTESIAN_POINT('Ctrl Pts',(-29.9140156468553,4.60174430490396,132.545612695332));
#80804=CARTESIAN_POINT('Ctrl Pts',(-29.9217637148583,4.64853330967106,132.416538575619));
#80805=CARTESIAN_POINT('Ctrl Pts',(-29.9295117828613,4.68982996495887,132.285805170114));
#80806=CARTESIAN_POINT('Ctrl Pts',(-29.9372680856031,4.73117051082336,132.15493281959));
#80807=CARTESIAN_POINT('Ctrl Pts',(-29.9450243883451,4.76700692855247,132.022398033878));
#80808=CARTESIAN_POINT('Ctrl Pts',(-29.9527806910869,4.79722639860321,131.888704632648));
#80809=CARTESIAN_POINT('Ctrl Pts',(-29.9605411336011,4.82746199769505,131.754939875225));
#80810=CARTESIAN_POINT('Ctrl Pts',(-29.9683015761152,4.85207460534403,131.620015654524));
#80811=CARTESIAN_POINT('Ctrl Pts',(-29.9760620186294,4.87100299053636,131.484443648295));
#80812=CARTESIAN_POINT('Ctrl Pts',(-29.9838349188948,4.88996176125298,131.348654009847));
#80813=CARTESIAN_POINT('Ctrl Pts',(-29.9916078191603,4.90321803738849,131.212214897211));
#80814=CARTESIAN_POINT('Ctrl Pts',(-29.9993807194257,4.91076263573133,131.07564164898));
#80815=CARTESIAN_POINT('Ctrl Pts',(-30.0068710551877,4.91803296892063,130.944033182331));
#80816=CARTESIAN_POINT('Ctrl Pts',(-30.0143613909496,4.91999967781119,130.81230047109));
#80817=CARTESIAN_POINT('Ctrl Pts',(-30.0218517267116,4.91670018311583,130.680900616559));
#80818=CARTESIAN_POINT('Ctrl Pts',(-30.0296260608306,4.91327558707621,130.544518696603));
#80819=CARTESIAN_POINT('Ctrl Pts',(-30.0374003949497,4.90416672011928,130.408063355208));
#80820=CARTESIAN_POINT('Ctrl Pts',(-30.0451747290688,4.8893583941103,130.27204721698));
#80821=CARTESIAN_POINT('Ctrl Pts',(-30.0529394820159,4.87456831803966,130.136198706486));
#80822=CARTESIAN_POINT('Ctrl Pts',(-30.060704234963,4.85409280063932,130.000788707113));
#80823=CARTESIAN_POINT('Ctrl Pts',(-30.0684689879101,4.82796864552613,129.866329797008));
#80824=CARTESIAN_POINT('Ctrl Pts',(-30.076226028795,4.80187043729209,129.732004433388));
#80825=CARTESIAN_POINT('Ctrl Pts',(-30.08398306968,4.77013483019267,129.598628660474));
#80826=CARTESIAN_POINT('Ctrl Pts',(-30.091740110565,4.73285037043758,129.466709529446));
#80827=CARTESIAN_POINT('Ctrl Pts',(-30.0994913018051,4.69559402718363,129.334889879661));
#80828=CARTESIAN_POINT('Ctrl Pts',(-30.1072424930453,4.65279726603736,129.204525060039));
#80829=CARTESIAN_POINT('Ctrl Pts',(-30.1149936842854,4.60459953925229,129.076111172139));
#80830=CARTESIAN_POINT('Ctrl Pts',(-30.1227415810625,4.55642229778682,128.947751863568));
#80831=CARTESIAN_POINT('Ctrl Pts',(-30.1304894778395,4.50284879346106,128.821342202773));
#80832=CARTESIAN_POINT('Ctrl Pts',(-30.1382373746166,4.44406802376494,128.697362168907));
#80833=CARTESIAN_POINT('Ctrl Pts',(-30.1459836507007,4.38529954973868,128.573408068992));
#80834=CARTESIAN_POINT('Ctrl Pts',(-30.1537299267847,4.32132614430036,128.451882938166));
#80835=CARTESIAN_POINT('Ctrl Pts',(-30.1614762028688,4.25238438790143,128.333245468482));
#80836=CARTESIAN_POINT('Ctrl Pts',(-30.1692225361342,4.18344212259021,128.214607123043));
#80837=CARTESIAN_POINT('Ctrl Pts',(-30.1769688693995,4.10953162957136,128.098856819315));
#80838=CARTESIAN_POINT('Ctrl Pts',(-30.1847152026649,4.03093455967212,127.986427041674));
#80839=CARTESIAN_POINT('Ctrl Pts',(-30.1924632706678,3.95231988850402,127.873972086163));
#80840=CARTESIAN_POINT('Ctrl Pts',(-30.2002113386707,3.86901677598191,127.764839456803));
#80841=CARTESIAN_POINT('Ctrl Pts',(-30.2079594066737,3.78134891027844,127.659430812112));
#80842=CARTESIAN_POINT('Ctrl Pts',(-30.2157157094155,3.69358787012391,127.553910137857));
#80843=CARTESIAN_POINT('Ctrl Pts',(-30.2234720121574,3.60145306046009,127.452121655662));
#80844=CARTESIAN_POINT('Ctrl Pts',(-30.2312283148993,3.50530737732605,127.354432610641));
#80845=CARTESIAN_POINT('Ctrl Pts',(-30.2389887574134,3.40911037834604,127.256691426036));
#80846=CARTESIAN_POINT('Ctrl Pts',(-30.2467491999277,3.30889852584867,127.163054305159));
#80847=CARTESIAN_POINT('Ctrl Pts',(-30.2545096424419,3.20506921195834,127.07384933772));
#80848=CARTESIAN_POINT('Ctrl Pts',(-30.2622825427073,3.10107322203582,126.984501170548));
#80849=CARTESIAN_POINT('Ctrl Pts',(-30.2700554429727,2.99344847347289,126.899599616908));
#80850=CARTESIAN_POINT('Ctrl Pts',(-30.2778283432381,2.88262357147262,126.819430955992));
#80851=CARTESIAN_POINT('Ctrl Pts',(-30.2853186790002,2.77582743380993,126.742176627832));
#80852=CARTESIAN_POINT('Ctrl Pts',(-30.2928090147623,2.66606002717133,126.669317231765));
#80853=CARTESIAN_POINT('Ctrl Pts',(-30.3002993505244,2.55372615063673,126.601068359103));
#80854=CARTESIAN_POINT('Ctrl Pts',(-30.3080736846435,2.43713310103148,126.530231809691));
#80855=CARTESIAN_POINT('Ctrl Pts',(-30.3158480187625,2.31740579261338,126.464137912308));
#80856=CARTESIAN_POINT('Ctrl Pts',(-30.3236223528816,2.19496730142352,126.403076531281));
#80857=CARTESIAN_POINT('Ctrl Pts',(-30.3313871058287,2.07267970473141,126.34209040295));
#80858=CARTESIAN_POINT('Ctrl Pts',(-30.3391518587758,1.94768791995112,126.286124623402));
#80859=CARTESIAN_POINT('Ctrl Pts',(-30.3469166117229,1.82044308684874,126.235425289719));
#80860=CARTESIAN_POINT('Ctrl Pts',(-30.3546736526079,1.69332463510843,126.18477631133));
#80861=CARTESIAN_POINT('Ctrl Pts',(-30.3624306934929,1.56395794913512,126.139383513238));
#80862=CARTESIAN_POINT('Ctrl Pts',(-30.3701877343779,1.43281748683617,126.099446472556));
#80863=CARTESIAN_POINT('Ctrl Pts',(-30.377938925618,1.30177591857979,126.059539548707));
#80864=CARTESIAN_POINT('Ctrl Pts',(-30.3856901168582,1.16896360893954,126.025080306583));
#80865=CARTESIAN_POINT('Ctrl Pts',(-30.3934413080983,1.03487331955688,125.996219576065));
#80866=CARTESIAN_POINT('Ctrl Pts',(-30.4011892048754,0.900840022124366,
125.967371112127));
#80867=CARTESIAN_POINT('Ctrl Pts',(-30.4089371016525,0.765530206696216,
125.944116509209));
#80868=CARTESIAN_POINT('Ctrl Pts',(-30.4166849984296,0.629449851087463,
125.926556198827));
#80869=CARTESIAN_POINT('Ctrl Pts',(-30.4244312745137,0.493397960555551,
125.908999561684));
#80870=CARTESIAN_POINT('Ctrl Pts',(-30.4321775505977,0.356576237944092,
125.897134897872));
#80871=CARTESIAN_POINT('Ctrl Pts',(-30.4399238266818,0.219498471381506,
125.891011099817));
#80872=CARTESIAN_POINT('Ctrl Pts',(-30.4476701599472,0.0824196929418009,
125.884887256558));
#80873=CARTESIAN_POINT('Ctrl Pts',(-30.4554164932126,-0.0549147426448532,
125.884504381065));
#80874=CARTESIAN_POINT('Ctrl Pts',(-30.4631628264779,-0.191988734872408,
125.889859280891));
#80875=CARTESIAN_POINT('Ctrl Pts',(-30.4709108944809,-0.329093423869931,
125.895215379909));
#80876=CARTESIAN_POINT('Ctrl Pts',(-30.4786589624839,-0.465937162856939,
125.906311795859));
#80877=CARTESIAN_POINT('Ctrl Pts',(-30.4864070304868,-0.602007063783788,
125.923093306953));
#80878=CARTESIAN_POINT('Ctrl Pts',(-30.4941633332287,-0.738221581420594,
125.939892653637));
#80879=CARTESIAN_POINT('Ctrl Pts',(-30.5019196359706,-0.873660229432092,
125.962389117453));
#80880=CARTESIAN_POINT('Ctrl Pts',(-30.5096759387124,-1.0078178799286,125.990475888639));
#80881=CARTESIAN_POINT('Ctrl Pts',(-30.5174363812266,-1.14204713440277,
126.018577650581));
#80882=CARTESIAN_POINT('Ctrl Pts',(-30.5251968237407,-1.27499365022287,
126.052275569187));
#80883=CARTESIAN_POINT('Ctrl Pts',(-30.5329572662549,-1.40616659607493,
126.091412647709));
#80884=CARTESIAN_POINT('Ctrl Pts',(-30.5407301665203,-1.53755011238465,
126.130612552543));
#80885=CARTESIAN_POINT('Ctrl Pts',(-30.5485030667857,-1.66715399947828,
126.175268938022));
#80886=CARTESIAN_POINT('Ctrl Pts',(-30.5562759670512,-1.79450573098123,
126.225175947346));
#80887=CARTESIAN_POINT('Ctrl Pts',(-30.5637663028132,-1.91722790626457,
126.273268711173));
#80888=CARTESIAN_POINT('Ctrl Pts',(-30.5712566385752,-2.0378585441665,126.326236855888));
#80889=CARTESIAN_POINT('Ctrl Pts',(-30.5787469743373,-2.15599745781895,
126.383856344932));
#80890=CARTESIAN_POINT('Ctrl Pts',(-30.5865220441461,-2.27862724772009,
126.443666153717));
#80891=CARTESIAN_POINT('Ctrl Pts',(-30.594297113955,-2.39896061875612,126.508677407539));
#80892=CARTESIAN_POINT('Ctrl Pts',(-30.6020721837638,-2.51652488359778,
126.5786907804));
#80893=CARTESIAN_POINT('Ctrl Pts',(-30.609837507902,-2.63394178736863,126.648616394914));
#80894=CARTESIAN_POINT('Ctrl Pts',(-30.6176028320401,-2.74859615878053,
126.723531454025));
#80895=CARTESIAN_POINT('Ctrl Pts',(-30.6253681561782,-2.86003700080638,
126.803189361981));
#80896=CARTESIAN_POINT('Ctrl Pts',(-30.6334688358033,-2.97629055858908,
126.886287398905));
#80897=CARTESIAN_POINT('Ctrl Pts',(-30.6415695154282,-3.08904642401237,
126.974546941627));
#80898=CARTESIAN_POINT('Ctrl Pts',(-30.6496701950532,-3.197822017491,127.067635124979));
#80899=CARTESIAN_POINT('Ctrl Pts',(-30.6574209290212,-3.30189855505178,
127.15670194136));
#80900=CARTESIAN_POINT('Ctrl Pts',(-30.6651716629892,-3.40233117176396,
127.250188660896));
#80901=CARTESIAN_POINT('Ctrl Pts',(-30.6729223969572,-3.49872814195416,
127.347760488653));
#80902=CARTESIAN_POINT('Ctrl Pts',(-30.6806696726043,-3.59508210052151,
127.445288780575));
#80903=CARTESIAN_POINT('Ctrl Pts',(-30.6884169482515,-3.6874037212943,127.546898276432));
#80904=CARTESIAN_POINT('Ctrl Pts',(-30.6961642238987,-3.77533674529737,
127.652216026639));
#80905=CARTESIAN_POINT('Ctrl Pts',(-30.7039097205091,-3.86324957690148,
127.757509592326));
#80906=CARTESIAN_POINT('Ctrl Pts',(-30.7116552171195,-3.94677556751609,
127.866509417449));
#80907=CARTESIAN_POINT('Ctrl Pts',(-30.7194007137299,-4.02559777753427,
127.978808353669));
#80908=CARTESIAN_POINT('Ctrl Pts',(-30.727146109024,-4.10441895650438,128.091105820943));
#80909=CARTESIAN_POINT('Ctrl Pts',(-30.7348915043181,-4.17853625430074,
128.20670199259));
#80910=CARTESIAN_POINT('Ctrl Pts',(-30.7426368996122,-4.24767545038139,
128.325159873228));
#80911=CARTESIAN_POINT('Ctrl Pts',(-30.7503866983179,-4.31685395347359,
128.443685099533));
#80912=CARTESIAN_POINT('Ctrl Pts',(-30.7581364970237,-4.38104850528407,
128.565074946332));
#80913=CARTESIAN_POINT('Ctrl Pts',(-30.7658862957294,-4.44003026842972,
128.688866756093));
#80914=CARTESIAN_POINT('Ctrl Pts',(-30.7736386990034,-4.49903185428767,
128.812700170062));
#80915=CARTESIAN_POINT('Ctrl Pts',(-30.7813911022774,-4.55281700442514,
128.938936797377));
#80916=CARTESIAN_POINT('Ctrl Pts',(-30.7891435055514,-4.60120499790612,
129.067093905244));
#80917=CARTESIAN_POINT('Ctrl Pts',(-30.7969033255299,-4.64963928405729,
129.195373620689));
#80918=CARTESIAN_POINT('Ctrl Pts',(-30.8046631455085,-4.69266597925393,
129.325577115149));
#80919=CARTESIAN_POINT('Ctrl Pts',(-30.812422965487,-4.73015412448565,129.457206201357));
#80920=CARTESIAN_POINT('Ctrl Pts',(-30.8148767993841,-4.74200873989752,
129.498830351722));
#80921=CARTESIAN_POINT('Ctrl Pts',(-30.8173306332813,-4.75330989944343,
129.540596974726));
#80922=CARTESIAN_POINT('Ctrl Pts',(-30.8197844671784,-4.7640545282341,129.582490119308));
#80923=CARTESIAN_POINT('Origin',(213.235140564004,0.,130.804360617566));
#80924=CARTESIAN_POINT('',(-32.9151834992122,-4.76405452823401,129.582490119308));
#80925=CARTESIAN_POINT('',(-32.5701265742934,-4.76405452823409,129.582490119308));
#80926=CARTESIAN_POINT('',(213.235140564004,-4.76405452823405,129.582490119308));
#80927=CARTESIAN_POINT('',(-31.2351405639676,-4.91824962726525,130.802445831626));
#80928=CARTESIAN_POINT('Ctrl Pts',(-31.2351405640085,-4.91824962726554,
130.802445832352));
#80929=CARTESIAN_POINT('Ctrl Pts',(-31.243051214989,-4.91830428636559,130.942841264952));
#80930=CARTESIAN_POINT('Ctrl Pts',(-31.2509618659695,-4.91234303963147,
131.083200981546));
#80931=CARTESIAN_POINT('Ctrl Pts',(-31.25887251695,-4.90040142640427,131.222988044516));
#80932=CARTESIAN_POINT('Ctrl Pts',(-31.2667870358457,-4.8884539743217,131.362843456413));
#80933=CARTESIAN_POINT('Ctrl Pts',(-31.2747015547414,-4.87052035993673,
131.502125290756));
#80934=CARTESIAN_POINT('Ctrl Pts',(-31.2826160736371,-4.8466878869723,131.640302953362));
#80935=CARTESIAN_POINT('Ctrl Pts',(-31.2905358609123,-4.82283954968131,
131.778572595325));
#80936=CARTESIAN_POINT('Ctrl Pts',(-31.2984556481875,-4.79308459129735,
131.915736239297));
#80937=CARTESIAN_POINT('Ctrl Pts',(-31.3063754354627,-4.75756115508497,
132.051274775849));
#80938=CARTESIAN_POINT('Ctrl Pts',(-31.3143076703234,-4.72198188643707,
132.187026339276));
#80939=CARTESIAN_POINT('Ctrl Pts',(-31.3222399051842,-4.68061611918711,
132.321147336433));
#80940=CARTESIAN_POINT('Ctrl Pts',(-31.3301721400449,-4.6336518177189,132.453134069151));
#80941=CARTESIAN_POINT('Ctrl Pts',(-31.3381110771738,-4.58664783420092,
132.585232322831));
#80942=CARTESIAN_POINT('Ctrl Pts',(-31.3460500143026,-4.53403602217863,
132.715192376689));
#80943=CARTESIAN_POINT('Ctrl Pts',(-31.3539889514314,-4.47605179660929,
132.842532194389));
#80944=CARTESIAN_POINT('Ctrl Pts',(-31.3619425090092,-4.41796078654283,
132.970106522739));
#80945=CARTESIAN_POINT('Ctrl Pts',(-31.369896066587,-4.35447775671424,133.095050644233));
#80946=CARTESIAN_POINT('Ctrl Pts',(-31.3778496241648,-4.28588377862541,
133.216907673815));
#80947=CARTESIAN_POINT('Ctrl Pts',(-31.3834000326486,-4.23801531294763,
133.301945882717));
#80948=CARTESIAN_POINT('Ctrl Pts',(-31.3889504411325,-4.18765875834085,
133.385481264039));
#80949=CARTESIAN_POINT('Ctrl Pts',(-31.3945008496164,-4.13492154908751,
133.467367723338));
#80950=CARTESIAN_POINT('Ctrl Pts',(-31.4022751837355,-4.06105370919175,
133.582064271578));
#80951=CARTESIAN_POINT('Ctrl Pts',(-31.4100495178546,-3.98229298485263,
133.693866686373));
#80952=CARTESIAN_POINT('Ctrl Pts',(-31.4178238519737,-3.898893061197,133.80232925647));
#80953=CARTESIAN_POINT('Ctrl Pts',(-31.4255886049208,-3.81559592049373,
133.910658156142));
#80954=CARTESIAN_POINT('Ctrl Pts',(-31.4333533578679,-3.72767119242189,
134.015655093891));
#80955=CARTESIAN_POINT('Ctrl Pts',(-31.441118110815,-3.63541694186813,134.116901443168));
#80956=CARTESIAN_POINT('Ctrl Pts',(-31.4488751517,-3.54325431953646,134.218047233143));
#80957=CARTESIAN_POINT('Ctrl Pts',(-31.456632192585,-3.44677099382002,134.315449560719));
#80958=CARTESIAN_POINT('Ctrl Pts',(-31.4643892334701,-3.34630634572266,
134.408721435114));
#80959=CARTESIAN_POINT('Ctrl Pts',(-31.4721404247102,-3.24591745879792,
134.501922972463));
#80960=CARTESIAN_POINT('Ctrl Pts',(-31.4798916159503,-3.14155351084147,
134.590999991535));
#80961=CARTESIAN_POINT('Ctrl Pts',(-31.4876428071904,-3.03359166376204,
134.675601333416));
#80962=CARTESIAN_POINT('Ctrl Pts',(-31.4953907039675,-2.92567570334774,
134.760166717469));
#80963=CARTESIAN_POINT('Ctrl Pts',(-31.5031386007447,-2.81416519237015,
134.840259967183));
#80964=CARTESIAN_POINT('Ctrl Pts',(-31.5108864975218,-2.69947122066022,
134.9155694655));
#80965=CARTESIAN_POINT('Ctrl Pts',(-31.5186327736059,-2.58480124045666,
134.990863210693));
#80966=CARTESIAN_POINT('Ctrl Pts',(-31.5263790496899,-2.46694945065919,
135.061374980401));
#80967=CARTESIAN_POINT('Ctrl Pts',(-31.534125325774,-2.34635650656006,135.126836089633));
#80968=CARTESIAN_POINT('Ctrl Pts',(-31.5418716590394,-2.22576267227138,
135.192297682085));
#80969=CARTESIAN_POINT('Ctrl Pts',(-31.5496179923047,-2.10242798690988,
135.252708353148));
#80970=CARTESIAN_POINT('Ctrl Pts',(-31.5573643255701,-1.97681796575485,
135.307845245359));
#80971=CARTESIAN_POINT('Ctrl Pts',(-31.565112393573,-1.85117981510634,135.362994485095));
#80972=CARTESIAN_POINT('Ctrl Pts',(-31.572860461576,-1.72326567265324,135.412867438762));
#80973=CARTESIAN_POINT('Ctrl Pts',(-31.580608529579,-1.5935609209986,135.457289442894));
#80974=CARTESIAN_POINT('Ctrl Pts',(-31.5883648323209,-1.46371831759039,
135.50175865926));
#80975=CARTESIAN_POINT('Ctrl Pts',(-31.5961211350627,-1.33208167383569,
135.540765226405));
#80976=CARTESIAN_POINT('Ctrl Pts',(-31.6038774378046,-1.19915195695956,
135.574184266992));
#80977=CARTESIAN_POINT('Ctrl Pts',(-31.6116378803188,-1.06615129149093,
135.607621144326));
#80978=CARTESIAN_POINT('Ctrl Pts',(-31.619398322833,-0.93185656035094,135.635464473422));
#80979=CARTESIAN_POINT('Ctrl Pts',(-31.6271587653472,-0.796777824564119,
135.657640762044));
#80980=CARTESIAN_POINT('Ctrl Pts',(-31.6349316656126,-0.661482248398888,
135.679852650013));
#80981=CARTESIAN_POINT('Ctrl Pts',(-31.642704565878,-0.525400540932047,
135.696379271167));
#80982=CARTESIAN_POINT('Ctrl Pts',(-31.6504774661435,-0.389047671979803,
135.707199078236));
#80983=CARTESIAN_POINT('Ctrl Pts',(-31.6579678019054,-0.257651573267969,
135.717625558064));
#80984=CARTESIAN_POINT('Ctrl Pts',(-31.6654581376674,-0.126003993383963,
135.722752922434));
#80985=CARTESIAN_POINT('Ctrl Pts',(-31.6729484734293,0.0054372000108684,
135.722607612112));
#80986=CARTESIAN_POINT('Ctrl Pts',(-31.6807228075484,0.141862026205495,
135.722456792304));
#80987=CARTESIAN_POINT('Ctrl Pts',(-31.6884971416674,0.278496659524296,
135.71662510042));
#80988=CARTESIAN_POINT('Ctrl Pts',(-31.6962714757865,0.414828987458322,
135.705085051123));
#80989=CARTESIAN_POINT('Ctrl Pts',(-31.7040362287336,0.550993297982538,
135.693559223905));
#80990=CARTESIAN_POINT('Ctrl Pts',(-31.7118009816807,0.686855658581828,
135.676339069567));
#80991=CARTESIAN_POINT('Ctrl Pts',(-31.7195657346278,0.821902755533517,
135.653449080664));
#80992=CARTESIAN_POINT('Ctrl Pts',(-31.7273227755128,0.956815721804867,
135.63058182642));
#80993=CARTESIAN_POINT('Ctrl Pts',(-31.7350798163978,1.09091465285752,135.602056009184));
#80994=CARTESIAN_POINT('Ctrl Pts',(-31.7428368572828,1.22369051866483,135.567947981836));
#80995=CARTESIAN_POINT('Ctrl Pts',(-31.750588048523,1.35636625715889,135.533865675616));
#80996=CARTESIAN_POINT('Ctrl Pts',(-31.7583392397631,1.48772053919776,135.494209635095));
#80997=CARTESIAN_POINT('Ctrl Pts',(-31.7660904310032,1.61725405961764,135.449107367298));
#80998=CARTESIAN_POINT('Ctrl Pts',(-31.7738383277803,1.74673252483575,135.404024269169));
#80999=CARTESIAN_POINT('Ctrl Pts',(-31.7815862245574,1.8743913991571,135.353499675998));
#81000=CARTESIAN_POINT('Ctrl Pts',(-31.7893341213344,1.99974630623212,135.297711012673));
#81001=CARTESIAN_POINT('Ctrl Pts',(-31.7970803974185,2.12507499176275,135.241934019135));
#81002=CARTESIAN_POINT('Ctrl Pts',(-31.8048266735026,2.24810031169022,135.180895304515));
#81003=CARTESIAN_POINT('Ctrl Pts',(-31.8125729495867,2.36835802877431,135.114820373792));
#81004=CARTESIAN_POINT('Ctrl Pts',(-31.820319282852,2.48861663357372,135.048744955318));
#81005=CARTESIAN_POINT('Ctrl Pts',(-31.8280656161174,2.60610725211323,134.977633434826));
#81006=CARTESIAN_POINT('Ctrl Pts',(-31.8358119493828,2.72039076571828,134.901757003601));
#81007=CARTESIAN_POINT('Ctrl Pts',(-31.8435600173857,2.83469987232367,134.825863580376));
#81008=CARTESIAN_POINT('Ctrl Pts',(-31.8513080853887,2.94580011919107,134.745203339285));
#81009=CARTESIAN_POINT('Ctrl Pts',(-31.8590561533917,3.0532821958477,134.66009023659));
#81010=CARTESIAN_POINT('Ctrl Pts',(-31.8668124561335,3.1608785057346,134.574886674676));
#81011=CARTESIAN_POINT('Ctrl Pts',(-31.8745687588753,3.2648486567501,134.485221040473));
#81012=CARTESIAN_POINT('Ctrl Pts',(-31.8823250616172,3.36481680103221,134.391447312642));
#81013=CARTESIAN_POINT('Ctrl Pts',(-31.8900855041314,3.46483830132291,134.29762353495));
#81014=CARTESIAN_POINT('Ctrl Pts',(-31.8978459466455,3.56085326516767,134.199687573705));
#81015=CARTESIAN_POINT('Ctrl Pts',(-31.9056063891596,3.65252416102431,134.098028833345));
#81016=CARTESIAN_POINT('Ctrl Pts',(-31.913379289425,3.74434221514114,133.99620690135));
#81017=CARTESIAN_POINT('Ctrl Pts',(-31.9211521896905,3.83180201644321,133.890650549244));
#81018=CARTESIAN_POINT('Ctrl Pts',(-31.9289250899559,3.91460708283561,133.78178138889));
#81019=CARTESIAN_POINT('Ctrl Pts',(-31.936415425718,3.99440197649193,133.676869896739));
#81020=CARTESIAN_POINT('Ctrl Pts',(-31.9439057614801,4.06987450595057,133.568882525012));
#81021=CARTESIAN_POINT('Ctrl Pts',(-31.9513960972422,4.14079942792155,133.45821878262));
#81022=CARTESIAN_POINT('Ctrl Pts',(-31.9591704313612,4.21441348986561,133.343359190801));
#81023=CARTESIAN_POINT('Ctrl Pts',(-31.9669447654803,4.28336147911722,133.225252432186));
#81024=CARTESIAN_POINT('Ctrl Pts',(-31.9747190995994,4.34734346216295,133.104314505036));
#81025=CARTESIAN_POINT('Ctrl Pts',(-31.9824838525465,4.4112465931329,132.983525623073));
#81026=CARTESIAN_POINT('Ctrl Pts',(-31.9902486054936,4.47019571411436,132.859912857233));
#81027=CARTESIAN_POINT('Ctrl Pts',(-31.9980133584407,4.523933972783,132.733921311714));
#81028=CARTESIAN_POINT('Ctrl Pts',(-32.0057703993257,4.57761885785548,132.608054902774));
#81029=CARTESIAN_POINT('Ctrl Pts',(-32.0135274402108,4.62610302770397,132.479814773202));
#81030=CARTESIAN_POINT('Ctrl Pts',(-32.0212844810958,4.66917557700601,132.349670454974));
#81031=CARTESIAN_POINT('Ctrl Pts',(-32.0290356723359,4.71221564496364,132.219624279589));
#81032=CARTESIAN_POINT('Ctrl Pts',(-32.0367868635759,4.74985209290475,132.087677143409));
#81033=CARTESIAN_POINT('Ctrl Pts',(-32.0445380548161,4.78192230946361,131.954318046671));
#81034=CARTESIAN_POINT('Ctrl Pts',(-32.0522859515932,4.81397889532488,131.821015631107));
#81035=CARTESIAN_POINT('Ctrl Pts',(-32.0600338483702,4.84047386397152,131.686302827913));
#81036=CARTESIAN_POINT('Ctrl Pts',(-32.0677817451473,4.86129467073749,131.550683059115));
#81037=CARTESIAN_POINT('Ctrl Pts',(-32.0755280212314,4.88211112223951,131.415091659049));
#81038=CARTESIAN_POINT('Ctrl Pts',(-32.0832742973155,4.89725571340494,131.27859405693));
#81039=CARTESIAN_POINT('Ctrl Pts',(-32.0910205733996,4.90666723639013,131.141702719646));
#81040=CARTESIAN_POINT('Ctrl Pts',(-32.0987669066649,4.91607882884905,131.004810371861));
#81041=CARTESIAN_POINT('Ctrl Pts',(-32.1065132399303,4.91975724186456,130.867524673155));
#81042=CARTESIAN_POINT('Ctrl Pts',(-32.1142595731956,4.91769328197664,130.73036165202));
#81043=CARTESIAN_POINT('Ctrl Pts',(-32.1220076411986,4.91562885987921,130.593167914178));
#81044=CARTESIAN_POINT('Ctrl Pts',(-32.1297557092016,4.90781951183897,130.456097299421));
#81045=CARTESIAN_POINT('Ctrl Pts',(-32.1375037772045,4.89430813584194,130.31966387327));
#81046=CARTESIAN_POINT('Ctrl Pts',(-32.1452600799464,4.88078239979366,130.183085444049));
#81047=CARTESIAN_POINT('Ctrl Pts',(-32.1530163826882,4.86154256851119,130.04714594592));
#81048=CARTESIAN_POINT('Ctrl Pts',(-32.16077268543,4.83668329931962,129.912352924447));
#81049=CARTESIAN_POINT('Ctrl Pts',(-32.1685331279442,4.81181076198754,129.777487959881));
#81050=CARTESIAN_POINT('Ctrl Pts',(-32.1762935704584,4.78131289735586,129.643771072241));
#81051=CARTESIAN_POINT('Ctrl Pts',(-32.1840540129726,4.74533487836266,129.511696718985));
#81052=CARTESIAN_POINT('Ctrl Pts',(-32.191826913238,4.70929910425938,129.379410348252));
#81053=CARTESIAN_POINT('Ctrl Pts',(-32.1995998135034,4.66776571464926,129.248772153755));
#81054=CARTESIAN_POINT('Ctrl Pts',(-32.2073727137688,4.62092916771991,129.120259465789));
#81055=CARTESIAN_POINT('Ctrl Pts',(-32.2148630495309,4.5757952472452,128.996418537734));
#81056=CARTESIAN_POINT('Ctrl Pts',(-32.222353385293,4.52573715874137,128.874551549051));
#81057=CARTESIAN_POINT('Ctrl Pts',(-32.2298437210551,4.47096927086958,128.755063947623));
#81058=CARTESIAN_POINT('Ctrl Pts',(-32.2376180551742,4.41412484188327,128.631045937471));
#81059=CARTESIAN_POINT('Ctrl Pts',(-32.2453923892933,4.35202635324192,128.509198453455));
#81060=CARTESIAN_POINT('Ctrl Pts',(-32.2531667234124,4.28486167467389,128.389998695357));
#81061=CARTESIAN_POINT('Ctrl Pts',(-32.2609314763595,4.21777977056952,128.270945840308));
#81062=CARTESIAN_POINT('Ctrl Pts',(-32.2686962293065,4.14564428957568,128.154534555954));
#81063=CARTESIAN_POINT('Ctrl Pts',(-32.2764609822536,4.06869087550451,128.041221529122));
#81064=CARTESIAN_POINT('Ctrl Pts',(-32.2842180231386,3.99181389264904,127.928021046385));
#81065=CARTESIAN_POINT('Ctrl Pts',(-32.2919750640237,3.91012871778607,127.817913018676));
#81066=CARTESIAN_POINT('Ctrl Pts',(-32.2997321049087,3.82391638198536,127.711328680116));
#81067=CARTESIAN_POINT('Ctrl Pts',(-32.3074832961488,3.73776905957771,127.604824717635));
#81068=CARTESIAN_POINT('Ctrl Pts',(-32.315234487389,3.6471016164059,127.50183945797));
#81069=CARTESIAN_POINT('Ctrl Pts',(-32.3229856786291,3.55223756680335,127.402774027239));
#81070=CARTESIAN_POINT('Ctrl Pts',(-32.3307335754062,3.45741383695245,127.30375070196));
#81071=CARTESIAN_POINT('Ctrl Pts',(-32.3384814721833,3.35839731808918,127.208644173791));
#81072=CARTESIAN_POINT('Ctrl Pts',(-32.3462293689604,3.255550720281,127.11782124165));
#81073=CARTESIAN_POINT('Ctrl Pts',(-32.3539756450445,3.15272563576397,127.027017307709));
#81074=CARTESIAN_POINT('Ctrl Pts',(-32.3617219211285,3.04607235874047,126.94049544616));
#81075=CARTESIAN_POINT('Ctrl Pts',(-32.3694681972126,2.93598895778154,126.858584153765));
#81076=CARTESIAN_POINT('Ctrl Pts',(-32.377214530478,2.82590474421194,126.77667225672));
#81077=CARTESIAN_POINT('Ctrl Pts',(-32.3849608637434,2.71239066984251,126.699371230132));
#81078=CARTESIAN_POINT('Ctrl Pts',(-32.3927071970087,2.59587591476838,126.626967734723));
#81079=CARTESIAN_POINT('Ctrl Pts',(-32.4004552650117,2.47933506702335,126.554548025054));
#81080=CARTESIAN_POINT('Ctrl Pts',(-32.4082033330147,2.35979253341687,126.487028235321));
#81081=CARTESIAN_POINT('Ctrl Pts',(-32.4159514010176,2.2377039992403,126.424650139203));
#81082=CARTESIAN_POINT('Ctrl Pts',(-32.4237077037595,2.11548570791608,126.362205746902));
#81083=CARTESIAN_POINT('Ctrl Pts',(-32.4314640065013,1.99071635936602,126.304914142614));
#81084=CARTESIAN_POINT('Ctrl Pts',(-32.4392203092432,1.8638741306448,126.252970029228));
#81085=CARTESIAN_POINT('Ctrl Pts',(-32.4469807517573,1.73696420240696,126.200998191704));
#81086=CARTESIAN_POINT('Ctrl Pts',(-32.4547411942715,1.60797955699168,126.154379664978));
#81087=CARTESIAN_POINT('Ctrl Pts',(-32.4625016367857,1.47741466497931,126.113259577277));
#81088=CARTESIAN_POINT('Ctrl Pts',(-32.4702745370511,1.34664017861128,126.07207347996));
#81089=CARTESIAN_POINT('Ctrl Pts',(-32.4780474373166,1.21428075412166,126.036403561786));
#81090=CARTESIAN_POINT('Ctrl Pts',(-32.485820337582,1.08084309240601,126.006344228255));
#81091=CARTESIAN_POINT('Ctrl Pts',(-32.493310673344,0.952256225803273,125.977377627213));
#81092=CARTESIAN_POINT('Ctrl Pts',(-32.500801009106,0.8226684571998,125.95362083064));
#81093=CARTESIAN_POINT('Ctrl Pts',(-32.508291344868,0.69253677288075,125.935112638596));
#81094=CARTESIAN_POINT('Ctrl Pts',(-32.5160656789871,0.557471106197878,
125.915902702824));
#81095=CARTESIAN_POINT('Ctrl Pts',(-32.5238400131062,0.421391617045269,
125.902286378638));
#81096=CARTESIAN_POINT('Ctrl Pts',(-32.5316143472252,0.284801335290685,
125.894363544052));
#81097=CARTESIAN_POINT('Ctrl Pts',(-32.5393791001723,0.148379388850939,
125.886450473651));
#81098=CARTESIAN_POINT('Ctrl Pts',(-32.5471438531194,0.0114482889012248,
125.884216954098));
#81099=CARTESIAN_POINT('Ctrl Pts',(-32.5549086060664,-0.125480369761398,
125.887711581962));
#81100=CARTESIAN_POINT('Ctrl Pts',(-32.5626656469514,-0.262273028949322,
125.891202738913));
#81101=CARTESIAN_POINT('Ctrl Pts',(-32.5704226878364,-0.399062863366618,
125.900410711454));
#81102=CARTESIAN_POINT('Ctrl Pts',(-32.5781797287214,-0.535335159375257,
125.915332152765));
#81103=CARTESIAN_POINT('Ctrl Pts',(-32.5859309199615,-0.671504691386174,
125.9302423417));
#81104=CARTESIAN_POINT('Ctrl Pts',(-32.5936821112017,-0.807157074746824,
125.950857381072));
#81105=CARTESIAN_POINT('Ctrl Pts',(-32.6014333024418,-0.941779963292485,
125.977121907574));
#81106=CARTESIAN_POINT('Ctrl Pts',(-32.6091811992189,-1.07634563351915,
126.003375270953));
#81107=CARTESIAN_POINT('Ctrl Pts',(-32.616929095996,-1.2098822962827,126.035273270984));
#81108=CARTESIAN_POINT('Ctrl Pts',(-32.6246769927731,-1.34188529961477,
126.072709013192));
#81109=CARTESIAN_POINT('Ctrl Pts',(-32.6324232688572,-1.47386069076437,
126.110136924649));
#81110=CARTESIAN_POINT('Ctrl Pts',(-32.6401695449412,-1.60430268469447,
126.153100167605));
#81111=CARTESIAN_POINT('Ctrl Pts',(-32.6479158210253,-1.73271974198939,
126.201441396222));
#81112=CARTESIAN_POINT('Ctrl Pts',(-32.6556621542907,-1.8611377472302,126.249782981683));
#81113=CARTESIAN_POINT('Ctrl Pts',(-32.6634084875561,-1.9875304201102,126.303502494282));
#81114=CARTESIAN_POINT('Ctrl Pts',(-32.6711548208215,-2.11142460251992,
126.362393799773));
#81115=CARTESIAN_POINT('Ctrl Pts',(-32.6789028888245,-2.2353465301726,126.421298293564));
#81116=CARTESIAN_POINT('Ctrl Pts',(-32.6866509568275,-2.35676850093917,
126.485376717094));
#81117=CARTESIAN_POINT('Ctrl Pts',(-32.6943990248305,-2.47524079474421,
126.554376374003));
#81118=CARTESIAN_POINT('Ctrl Pts',(-32.7021553275723,-2.59383900231279,
126.623449364568));
#81119=CARTESIAN_POINT('Ctrl Pts',(-32.7099116303142,-2.70948093213436,
126.697453839612));
#81120=CARTESIAN_POINT('Ctrl Pts',(-32.717667933056,-2.82174430877767,126.776092736903));
#81121=CARTESIAN_POINT('Ctrl Pts',(-32.7254283755702,-2.93406760376544,
126.854773606141));
#81122=CARTESIAN_POINT('Ctrl Pts',(-32.7331888180844,-3.04300844207798,
126.938093588948));
#81123=CARTESIAN_POINT('Ctrl Pts',(-32.7409492605986,-3.14817744979978,
127.025715118571));
#81124=CARTESIAN_POINT('Ctrl Pts',(-32.748722160864,-3.25351528414911,127.113477306053));
#81125=CARTESIAN_POINT('Ctrl Pts',(-32.7564950611295,-3.35506889852955,
127.20555457643));
#81126=CARTESIAN_POINT('Ctrl Pts',(-32.7642679613949,-3.45248498270692,
127.301571656369));
#81127=CARTESIAN_POINT('Ctrl Pts',(-32.7717582971569,-3.54635974684788,
127.3940982736));
#81128=CARTESIAN_POINT('Ctrl Pts',(-32.7792486329189,-3.63639236691941,
127.490283004602));
#81129=CARTESIAN_POINT('Ctrl Pts',(-32.7867389686809,-3.72230318708338,
127.589762346253));
#81130=CARTESIAN_POINT('Ctrl Pts',(-32.7944546360175,-3.81079846020092,
127.692234322334));
#81131=CARTESIAN_POINT('Ctrl Pts',(-32.8021703033541,-3.89521147350888,
127.798539935146));
#81132=CARTESIAN_POINT('Ctrl Pts',(-32.8098859706907,-3.97518776059449,
127.90831757049));
#81133=CARTESIAN_POINT('Ctrl Pts',(-32.817592281136,-4.05506705938423,128.01796207705));
#81134=CARTESIAN_POINT('Ctrl Pts',(-32.8252985915813,-4.13052010076039,
128.131069914492));
#81135=CARTESIAN_POINT('Ctrl Pts',(-32.8330049020266,-4.20123058136087,
128.247244142953));
#81136=CARTESIAN_POINT('Ctrl Pts',(-32.8407021623806,-4.27185802140532,
128.36328193941));
#81137=CARTESIAN_POINT('Ctrl Pts',(-32.8483994227347,-4.33775378375465,
128.482378620389));
#81138=CARTESIAN_POINT('Ctrl Pts',(-32.8560966830887,-4.39864350046135,
128.60410644626));
#81139=CARTESIAN_POINT('Ctrl Pts',(-32.8637887063279,-4.45949178860543,
128.725751450119));
#81140=CARTESIAN_POINT('Ctrl Pts',(-32.8714807295672,-4.51534062785411,
128.850023684835));
#81141=CARTESIAN_POINT('Ctrl Pts',(-32.8791727528065,-4.56596047428187,
128.976468933194));
#81142=CARTESIAN_POINT('Ctrl Pts',(-32.8868612619777,-4.61655719524825,
129.102856415579));
#81143=CARTESIAN_POINT('Ctrl Pts',(-32.8945497711488,-4.66192952821856,
129.231414568632));
#81144=CARTESIAN_POINT('Ctrl Pts',(-32.90223828032,-4.70189537228377,129.361667659728));
#81145=CARTESIAN_POINT('Ctrl Pts',(-32.906553353284,-4.72432566785483,129.434770465402));
#81146=CARTESIAN_POINT('Ctrl Pts',(-32.9108684262481,-4.74505385564512,
129.508406785259));
#81147=CARTESIAN_POINT('Ctrl Pts',(-32.9151834992122,-4.76405452823401,
129.582490119308));
#81148=CARTESIAN_POINT('Ctrl Pts',(-31.1654202583464,-4.76405452823401,
129.582490119308));
#81149=CARTESIAN_POINT('Ctrl Pts',(-31.1738666463901,-4.80103397831636,
129.726672433938));
#81150=CARTESIAN_POINT('Ctrl Pts',(-31.1823130344338,-4.83150726471108,
129.872703889186));
#81151=CARTESIAN_POINT('Ctrl Pts',(-31.1907594224775,-4.8553031000455,130.020004276871));
#81152=CARTESIAN_POINT('Ctrl Pts',(-31.1991747260673,-4.87901136178704,
130.16676256868));
#81153=CARTESIAN_POINT('Ctrl Pts',(-31.207590029657,-4.89609112909457,130.314780213512));
#81154=CARTESIAN_POINT('Ctrl Pts',(-31.2160053332468,-4.90642171873993,
130.463466234542));
#81155=CARTESIAN_POINT('Ctrl Pts',(-31.222383743487,-4.91425182707523,130.576163349865));
#81156=CARTESIAN_POINT('Ctrl Pts',(-31.2287621537274,-4.91820555525443,
130.689244065148));
#81157=CARTESIAN_POINT('Ctrl Pts',(-31.2351405639676,-4.91824962726525,
130.802445831626));
#81158=CARTESIAN_POINT('',(-30.8898594360284,-4.91824895780906,130.801158819624));
#81159=CARTESIAN_POINT('Ctrl Pts',(-30.8197844671784,-4.7640545282341,129.582490119308));
#81160=CARTESIAN_POINT('Ctrl Pts',(-30.8275584240133,-4.79809443636444,
129.715211204481));
#81161=CARTESIAN_POINT('Ctrl Pts',(-30.8353323808482,-4.82654466266992,
129.849202443635));
#81162=CARTESIAN_POINT('Ctrl Pts',(-30.8431063376831,-4.84934167116051,
129.983953146338));
#81163=CARTESIAN_POINT('Ctrl Pts',(-30.8478024245054,-4.86311287332117,
130.06535326377));
#81164=CARTESIAN_POINT('Ctrl Pts',(-30.8524985113278,-4.8748221571778,130.147030419108));
#81165=CARTESIAN_POINT('Ctrl Pts',(-30.8571945981501,-4.88446472887062,
130.22887180367));
#81166=CARTESIAN_POINT('Ctrl Pts',(-30.8680828774305,-4.90682185673984,
130.41862805936));
#81167=CARTESIAN_POINT('Ctrl Pts',(-30.8789711567108,-4.91812432521411,
130.609712008915));
#81168=CARTESIAN_POINT('Ctrl Pts',(-30.8898594359911,-4.91824895780864,
130.801158818967));
#81169=CARTESIAN_POINT('Ctrl Pts',(-30.8898594360285,-4.91824895780906,
130.801158819624));
#81170=CARTESIAN_POINT('Ctrl Pts',(-30.8975220895259,-4.91833666828801,
130.935889986125));
#81171=CARTESIAN_POINT('Ctrl Pts',(-30.9051847430233,-4.91288394704376,
131.070840739474));
#81172=CARTESIAN_POINT('Ctrl Pts',(-30.9128473965207,-4.90186313858186,
131.205510007585));
#81173=CARTESIAN_POINT('Ctrl Pts',(-30.9205017579385,-4.89085425620024,
131.340033544417));
#81174=CARTESIAN_POINT('Ctrl Pts',(-30.9281561193564,-4.87428930275188,
131.474275803935));
#81175=CARTESIAN_POINT('Ctrl Pts',(-30.9358104807742,-4.85219263597003,
131.607734556612));
#81176=CARTESIAN_POINT('Ctrl Pts',(-30.9434585087382,-4.8301142526492,131.741082881417));
#81177=CARTESIAN_POINT('Ctrl Pts',(-30.9511065367022,-4.80251332647413,
131.873648593866));
#81178=CARTESIAN_POINT('Ctrl Pts',(-30.9587545646662,-4.76946608516426,
132.00493394934));
#81179=CARTESIAN_POINT('Ctrl Pts',(-30.966398738977,-4.73643549554682,132.136153153352));
#81180=CARTESIAN_POINT('Ctrl Pts',(-30.9740429132878,-4.69796414544094,
132.266092893788));
#81181=CARTESIAN_POINT('Ctrl Pts',(-30.9816870875985,-4.65417939426002,
132.394265403566));
#81182=CARTESIAN_POINT('Ctrl Pts',(-30.989329371168,-4.61040547297844,132.522406210631));
#81183=CARTESIAN_POINT('Ctrl Pts',(-30.9969716547374,-4.56132089337728,
132.648780275366));
#81184=CARTESIAN_POINT('Ctrl Pts',(-31.0046139383068,-4.50710279138551,
132.772915287974));
#81185=CARTESIAN_POINT('Ctrl Pts',(-31.0122560921489,-4.4528856097433,132.897048193396));
#81186=CARTESIAN_POINT('Ctrl Pts',(-31.0198982459908,-4.3935352402735,133.018941753405));
#81187=CARTESIAN_POINT('Ctrl Pts',(-31.0275403998329,-4.32927662460057,
133.138144448641));
#81188=CARTESIAN_POINT('Ctrl Pts',(-31.0351841846384,-4.26500429506366,
133.257372583727));
#81189=CARTESIAN_POINT('Ctrl Pts',(-31.0428279694441,-4.1958218277138,133.373908358008));
#81190=CARTESIAN_POINT('Ctrl Pts',(-31.0504717542497,-4.12199941387091,
133.48732612136));
#81191=CARTESIAN_POINT('Ctrl Pts',(-31.0581234028725,-4.04810105257745,
133.600860567295));
#81192=CARTESIAN_POINT('Ctrl Pts',(-31.0657750514952,-3.96955343324428,
133.711270259487));
#81193=CARTESIAN_POINT('Ctrl Pts',(-31.073426700118,-3.88666944840212,133.818159492965));
#81194=CARTESIAN_POINT('Ctrl Pts',(-31.0810825530534,-3.8037399217166,133.925107458329));
#81195=CARTESIAN_POINT('Ctrl Pts',(-31.0887384059889,-3.71646954504271,
134.02853080672));
#81196=CARTESIAN_POINT('Ctrl Pts',(-31.0963942589243,-3.62520968580912,
134.12806905791));
#81197=CARTESIAN_POINT('Ctrl Pts',(-31.1040617118269,-3.53381155179644,
134.227758127103));
#81198=CARTESIAN_POINT('Ctrl Pts',(-31.1117291647294,-3.43841214779178,
134.323550059335));
#81199=CARTESIAN_POINT('Ctrl Pts',(-31.119396617632,-3.33939805141746,134.415122824731));
#81200=CARTESIAN_POINT('Ctrl Pts',(-31.1248118190757,-3.26946853447863,
134.479796840687));
#81201=CARTESIAN_POINT('Ctrl Pts',(-31.1302270205194,-3.19773671950685,
134.542367169959));
#81202=CARTESIAN_POINT('Ctrl Pts',(-31.1356422219631,-3.1243475334576,134.602733368189));
#81203=CARTESIAN_POINT('Ctrl Pts',(-31.1434165560821,-3.01898634624972,
134.689398102534));
#81204=CARTESIAN_POINT('Ctrl Pts',(-31.1511908902012,-2.90984961627873,
134.771812942361));
#81205=CARTESIAN_POINT('Ctrl Pts',(-31.1589652243203,-2.79731500532604,
134.84963092046));
#81206=CARTESIAN_POINT('Ctrl Pts',(-31.1667299772674,-2.68491908322369,
134.927352994856));
#81207=CARTESIAN_POINT('Ctrl Pts',(-31.1744947302146,-2.5691339306675,135.000489259395));
#81208=CARTESIAN_POINT('Ctrl Pts',(-31.1822594831617,-2.45037119991824,
135.068732088851));
#81209=CARTESIAN_POINT('Ctrl Pts',(-31.1900165240467,-2.33172642598775,
135.136907138567));
#81210=CARTESIAN_POINT('Ctrl Pts',(-31.1977735649317,-2.21011029596223,
135.200198231747));
#81211=CARTESIAN_POINT('Ctrl Pts',(-31.2055306058166,-2.08596414564402,
135.258340483437));
#81212=CARTESIAN_POINT('Ctrl Pts',(-31.2132817970567,-1.96191161490399,
135.316438889603));
#81213=CARTESIAN_POINT('Ctrl Pts',(-31.2210329882969,-1.83533321407292,
135.36939601757));
#81214=CARTESIAN_POINT('Ctrl Pts',(-31.228784179537,-1.70669531488896,135.416992638943));
#81215=CARTESIAN_POINT('Ctrl Pts',(-31.2365320763141,-1.57811209024298,
135.464569030483));
#81216=CARTESIAN_POINT('Ctrl Pts',(-31.2442799730911,-1.44747147413522,
135.506789311523));
#81217=CARTESIAN_POINT('Ctrl Pts',(-31.2520278698682,-1.3152600724652,135.543482266593));
#81218=CARTESIAN_POINT('Ctrl Pts',(-31.2597741459523,-1.18307632657025,
135.580167546289));
#81219=CARTESIAN_POINT('Ctrl Pts',(-31.2675204220364,-1.04932282515283,
135.611327695267));
#81220=CARTESIAN_POINT('Ctrl Pts',(-31.2752666981205,-0.914501218992165,
135.636841407281));
#81221=CARTESIAN_POINT('Ctrl Pts',(-31.2830130313859,-0.77967861760885,
135.662355307631));
#81222=CARTESIAN_POINT('Ctrl Pts',(-31.2907593646513,-0.643788279896508,
135.682222615149));
#81223=CARTESIAN_POINT('Ctrl Pts',(-31.2985056979167,-0.507341536663927,
135.696373253248));
#81224=CARTESIAN_POINT('Ctrl Pts',(-31.3062537659197,-0.37086423712907,
135.710527060285));
#81225=CARTESIAN_POINT('Ctrl Pts',(-31.3140018339226,-0.23383067293322,
135.718961610113));
#81226=CARTESIAN_POINT('Ctrl Pts',(-31.3217499019256,-0.0967563781090899,
135.721658784832));
#81227=CARTESIAN_POINT('Ctrl Pts',(-31.3295062046675,0.0404636009064103,
135.724358826139));
#81228=CARTESIAN_POINT('Ctrl Pts',(-31.3372625074094,0.177724005511788,
135.72130930372));
#81229=CARTESIAN_POINT('Ctrl Pts',(-31.3450188101512,0.314509662764759,
135.712544266792));
#81230=CARTESIAN_POINT('Ctrl Pts',(-31.3527792526654,0.451368326641543,
135.7037745517));
#81231=CARTESIAN_POINT('Ctrl Pts',(-31.3605396951796,0.587751349684457,
135.689283284926));
#81232=CARTESIAN_POINT('Ctrl Pts',(-31.3683001376938,0.723150589117112,
135.669156223546));
#81233=CARTESIAN_POINT('Ctrl Pts',(-31.3760730379592,0.858767183429083,
135.64899685242));
#81234=CARTESIAN_POINT('Ctrl Pts',(-31.3838459382246,0.993396454080462,
135.623183681408));
#81235=CARTESIAN_POINT('Ctrl Pts',(-31.39161883849,1.12654144455891,135.59185343074));
#81236=CARTESIAN_POINT('Ctrl Pts',(-31.399109174252,1.25484627926058,135.5616621136));
#81237=CARTESIAN_POINT('Ctrl Pts',(-31.406599510014,1.38177257813163,135.526347954828));
#81238=CARTESIAN_POINT('Ctrl Pts',(-31.414089845776,1.50689241234026,135.486075935709));
#81239=CARTESIAN_POINT('Ctrl Pts',(-31.421864179895,1.63675620309353,135.444276990744));
#81240=CARTESIAN_POINT('Ctrl Pts',(-31.4296385140142,1.76508521031181,135.397004402927));
#81241=CARTESIAN_POINT('Ctrl Pts',(-31.4374128481333,1.89138338523731,135.344388365559));
#81242=CARTESIAN_POINT('Ctrl Pts',(-31.4451776010804,2.01752590894998,135.291837172755));
#81243=CARTESIAN_POINT('Ctrl Pts',(-31.4529423540275,2.14164222279959,135.233955782139));
#81244=CARTESIAN_POINT('Ctrl Pts',(-31.4607071069747,2.2632510048694,135.170924249469));
#81245=CARTESIAN_POINT('Ctrl Pts',(-31.4684641478597,2.38473900338198,135.107955320606));
#81246=CARTESIAN_POINT('Ctrl Pts',(-31.4762211887447,2.50372408148981,135.039846607903));
#81247=CARTESIAN_POINT('Ctrl Pts',(-31.4839782296297,2.61974483119606,134.96682624288));
#81248=CARTESIAN_POINT('Ctrl Pts',(-31.4917294208699,2.73567808875276,134.893860943083));
#81249=CARTESIAN_POINT('Ctrl Pts',(-31.4994806121099,2.84865113783499,134.815991570792));
#81250=CARTESIAN_POINT('Ctrl Pts',(-31.50723180335,2.95822745006749,134.733491999458));
#81251=CARTESIAN_POINT('Ctrl Pts',(-31.5149797001271,3.0677571894441,134.651027492642));
#81252=CARTESIAN_POINT('Ctrl Pts',(-31.5227275969042,3.17389275170417,134.563936935566));
#81253=CARTESIAN_POINT('Ctrl Pts',(-31.5304754936813,3.2762270660491,134.47253717741));
#81254=CARTESIAN_POINT('Ctrl Pts',(-31.5382217697654,3.37853997426153,134.381156538113));
#81255=CARTESIAN_POINT('Ctrl Pts',(-31.5459680458496,3.47705292472543,134.285468750926));
#81256=CARTESIAN_POINT('Ctrl Pts',(-31.5537143219337,3.57139270455902,134.185830299867));
#81257=CARTESIAN_POINT('Ctrl Pts',(-31.5614606551991,3.66573318078744,134.0861911133));
#81258=CARTESIAN_POINT('Ctrl Pts',(-31.5692069884645,3.75590015611331,133.982601488568));
#81259=CARTESIAN_POINT('Ctrl Pts',(-31.5769533217299,3.84155828632714,133.875453744655));
#81260=CARTESIAN_POINT('Ctrl Pts',(-31.5847013897329,3.92723559908567,133.768282005747));
#81261=CARTESIAN_POINT('Ctrl Pts',(-31.5924494577359,4.00840181341415,133.657550867404));
#81262=CARTESIAN_POINT('Ctrl Pts',(-31.6001975257389,4.08476302747088,133.54368426984));
#81263=CARTESIAN_POINT('Ctrl Pts',(-31.6079538284808,4.16120539913441,133.429696653501));
#81264=CARTESIAN_POINT('Ctrl Pts',(-31.6157101312226,4.23283235101661,133.312567246333));
#81265=CARTESIAN_POINT('Ctrl Pts',(-31.6234664339645,4.2993940661312,133.192747882357));
#81266=CARTESIAN_POINT('Ctrl Pts',(-31.6312268764787,4.36599130723727,133.072864567179));
#81267=CARTESIAN_POINT('Ctrl Pts',(-31.6389873189928,4.42751774938116,132.950288783664));
#81268=CARTESIAN_POINT('Ctrl Pts',(-31.646747761507,4.48377087883792,132.825494400517));
#81269=CARTESIAN_POINT('Ctrl Pts',(-31.6545206617725,4.540114310812,132.700499686347));
#81270=CARTESIAN_POINT('Ctrl Pts',(-31.6622935620379,4.5911673682623,132.573279618595));
#81271=CARTESIAN_POINT('Ctrl Pts',(-31.6700664623034,4.63677646065695,132.444326201472));
#81272=CARTESIAN_POINT('Ctrl Pts',(-31.6775567980652,4.68072754765951,132.32006056588));
#81273=CARTESIAN_POINT('Ctrl Pts',(-31.6850471338271,4.7196235106219,132.19418571049));
#81274=CARTESIAN_POINT('Ctrl Pts',(-31.6925374695889,4.75337184698519,132.067150840362));
#81275=CARTESIAN_POINT('Ctrl Pts',(-31.700311803708,4.78839976178011,131.935299404518));
#81276=CARTESIAN_POINT('Ctrl Pts',(-31.7080861378271,4.8179929578323,131.801780587867));
#81277=CARTESIAN_POINT('Ctrl Pts',(-31.7158604719462,4.84199284398262,131.667082102937));
#81278=CARTESIAN_POINT('Ctrl Pts',(-31.7236252248933,4.86596315241815,131.532549621852));
#81279=CARTESIAN_POINT('Ctrl Pts',(-31.7313899778404,4.88435379855211,131.396840746395));
#81280=CARTESIAN_POINT('Ctrl Pts',(-31.7391547307874,4.89705610213931,131.260457750861));
#81281=CARTESIAN_POINT('Ctrl Pts',(-31.7469117716724,4.90974578961949,131.124210212842));
#81282=CARTESIAN_POINT('Ctrl Pts',(-31.7546688125574,4.91675834177269,130.987290273934));
#81283=CARTESIAN_POINT('Ctrl Pts',(-31.7624258534424,4.91803628981564,130.850209440412));
#81284=CARTESIAN_POINT('Ctrl Pts',(-31.7701770446825,4.91931327414804,130.713231980613));
#81285=CARTESIAN_POINT('Ctrl Pts',(-31.7779282359226,4.91486425841429,130.576094257069));
#81286=CARTESIAN_POINT('Ctrl Pts',(-31.7856794271627,4.90468370585328,130.439311568756));
#81287=CARTESIAN_POINT('Ctrl Pts',(-31.7934273239398,4.89450748029868,130.302587016733));
#81288=CARTESIAN_POINT('Ctrl Pts',(-31.801175220717,4.87860459200456,130.166217588884));
#81289=CARTESIAN_POINT('Ctrl Pts',(-31.808923117494,4.85702158345065,130.030717030121));
#81290=CARTESIAN_POINT('Ctrl Pts',(-31.8166693935781,4.83544308959683,129.895244815154));
#81291=CARTESIAN_POINT('Ctrl Pts',(-31.8244156696621,4.80818690025611,129.760641493618));
#81292=CARTESIAN_POINT('Ctrl Pts',(-31.8321619457462,4.77535120485009,129.627413748401));
#81293=CARTESIAN_POINT('Ctrl Pts',(-31.8399082790116,4.74251526705855,129.494185019728));
#81294=CARTESIAN_POINT('Ctrl Pts',(-31.8476546122769,4.70409983457553,129.36233226724));
#81295=CARTESIAN_POINT('Ctrl Pts',(-31.8554009455423,4.66025371473688,129.232349683513));
#81296=CARTESIAN_POINT('Ctrl Pts',(-31.8631490135452,4.61639777586364,129.102337991088));
#81297=CARTESIAN_POINT('Ctrl Pts',(-31.8708970815482,4.5671088545472,128.974197671195));
#81298=CARTESIAN_POINT('Ctrl Pts',(-31.8786451495512,4.51258476257148,128.848405141818));
#81299=CARTESIAN_POINT('Ctrl Pts',(-31.886401452293,4.45800272174188,128.722478918644));
#81300=CARTESIAN_POINT('Ctrl Pts',(-31.8941577550348,4.39817455129249,128.598905829826));
#81301=CARTESIAN_POINT('Ctrl Pts',(-31.9019140577767,4.33334535979917,128.478140280795));
#81302=CARTESIAN_POINT('Ctrl Pts',(-31.9096745002908,4.26848156701429,128.357310275554));
#81303=CARTESIAN_POINT('Ctrl Pts',(-31.9174349428051,4.19861163366287,128.23929113219));
#81304=CARTESIAN_POINT('Ctrl Pts',(-31.9251953853192,4.12402477529131,128.124509368843));
#81305=CARTESIAN_POINT('Ctrl Pts',(-31.9329682855847,4.04931818347317,128.00954334762));
#81306=CARTESIAN_POINT('Ctrl Pts',(-31.9407411858501,3.96987976200627,127.897825410346));
#81307=CARTESIAN_POINT('Ctrl Pts',(-31.9485140861155,3.88604042853469,127.789750717381));
#81308=CARTESIAN_POINT('Ctrl Pts',(-31.9560044218776,3.80524886601265,127.685604811728));
#81309=CARTESIAN_POINT('Ctrl Pts',(-31.9634947576397,3.72037100327695,127.584842102491));
#81310=CARTESIAN_POINT('Ctrl Pts',(-31.9709850934018,3.63173476937418,127.487783220999));
#81311=CARTESIAN_POINT('Ctrl Pts',(-31.9787594275209,3.53973786572348,127.387044322516));
#81312=CARTESIAN_POINT('Ctrl Pts',(-31.98653376164,3.44340054914609,127.289976546777));
#81313=CARTESIAN_POINT('Ctrl Pts',(-31.994308095759,3.34304742360918,127.196976941548));
#81314=CARTESIAN_POINT('Ctrl Pts',(-32.0020728487061,3.24281797433095,127.104091950022));
#81315=CARTESIAN_POINT('Ctrl Pts',(-32.0098376016531,3.13858284738608,127.015265416521));
#81316=CARTESIAN_POINT('Ctrl Pts',(-32.0176023546002,3.03070587603699,126.93086026834));
#81317=CARTESIAN_POINT('Ctrl Pts',(-32.0253593954852,2.92293604961649,126.846538952542));
#81318=CARTESIAN_POINT('Ctrl Pts',(-32.0331164363702,2.81153188296877,126.766630522374));
#81319=CARTESIAN_POINT('Ctrl Pts',(-32.0408734772552,2.69689265752841,126.691459809588));
#81320=CARTESIAN_POINT('Ctrl Pts',(-32.0486246684953,2.58233988241957,126.616345783621));
#81321=CARTESIAN_POINT('Ctrl Pts',(-32.0563758597354,2.464557229983,126.54596257721));
#81322=CARTESIAN_POINT('Ctrl Pts',(-32.0641270509756,2.34397524308472,126.480593380271));
#81323=CARTESIAN_POINT('Ctrl Pts',(-32.0718749477526,2.22344450674766,126.415251966985));
#81324=CARTESIAN_POINT('Ctrl Pts',(-32.0796228445297,2.10011714534268,126.354920510539));
#81325=CARTESIAN_POINT('Ctrl Pts',(-32.0873707413067,1.97445054436269,126.299837545101));
#81326=CARTESIAN_POINT('Ctrl Pts',(-32.0951170173908,1.84881023012673,126.244766101833));
#81327=CARTESIAN_POINT('Ctrl Pts',(-32.102863293475,1.72083200744713,126.194941122702));
#81328=CARTESIAN_POINT('Ctrl Pts',(-32.110609569559,1.59099523676721,126.150553872644));
#81329=CARTESIAN_POINT('Ctrl Pts',(-32.1183559028244,1.46115750766157,126.106166294929));
#81330=CARTESIAN_POINT('Ctrl Pts',(-32.1261022360897,1.32946157312347,126.067216652856));
#81331=CARTESIAN_POINT('Ctrl Pts',(-32.1338485693551,1.19640364536209,126.033846873758));
#81332=CARTESIAN_POINT('Ctrl Pts',(-32.141596637358,1.06331592020052,126.000469621728));
#81333=CARTESIAN_POINT('Ctrl Pts',(-32.1493447053609,0.928865974031862,
125.972674814263));
#81334=CARTESIAN_POINT('Ctrl Pts',(-32.1570927733639,0.793561552899899,
125.950553542263));
#81335=CARTESIAN_POINT('Ctrl Pts',(-32.1648490761057,0.658113328618644,
125.928408759512));
#81336=CARTESIAN_POINT('Ctrl Pts',(-32.1726053788476,0.521809201712001,
125.911949620786));
#81337=CARTESIAN_POINT('Ctrl Pts',(-32.1803616815894,0.38516396351098,125.901215526534));
#81338=CARTESIAN_POINT('Ctrl Pts',(-32.1881221241036,0.248445793631837,
125.890475703172));
#81339=CARTESIAN_POINT('Ctrl Pts',(-32.1958825666177,0.111386540198871,
125.885467027153));
#81340=CARTESIAN_POINT('Ctrl Pts',(-32.2036430091319,-0.0254986269283883,
125.886176716722));
#81341=CARTESIAN_POINT('Ctrl Pts',(-32.2114159093973,-0.162603534277642,
125.886887545546));
#81342=CARTESIAN_POINT('Ctrl Pts',(-32.2191888096628,-0.299533406116201,
125.893335065381));
#81343=CARTESIAN_POINT('Ctrl Pts',(-32.2269617099282,-0.435776913772694,
125.905454459665));
#81344=CARTESIAN_POINT('Ctrl Pts',(-32.2344520456904,-0.56706762675232,
125.91713328344));
#81345=CARTESIAN_POINT('Ctrl Pts',(-32.2419423814526,-0.697720705849254,
125.934078727617));
#81346=CARTESIAN_POINT('Ctrl Pts',(-32.2494327172147,-0.827289141184968,
125.956188205267));
#81347=CARTESIAN_POINT('Ctrl Pts',(-32.2572070513338,-0.961770203125248,
125.979135970482));
#81348=CARTESIAN_POINT('Ctrl Pts',(-32.2649813854529,-1.0955087447375,126.007719779533));
#81349=CARTESIAN_POINT('Ctrl Pts',(-32.272755719572,-1.22799526211631,126.041881147928));
#81350=CARTESIAN_POINT('Ctrl Pts',(-32.2805204725191,-1.36031850170311,
126.07600041549));
#81351=CARTESIAN_POINT('Ctrl Pts',(-32.2882852254662,-1.49139241223421,
126.115683468815));
#81352=CARTESIAN_POINT('Ctrl Pts',(-32.2960499784134,-1.62071499193351,
126.160820375744));
#81353=CARTESIAN_POINT('Ctrl Pts',(-32.3038070192984,-1.74990912662388,
126.20591245206));
#81354=CARTESIAN_POINT('Ctrl Pts',(-32.3115640601834,-1.87735502532025,
126.256447474214));
#81355=CARTESIAN_POINT('Ctrl Pts',(-32.3193211010685,-2.00256357650255,
126.312265094921));
#81356=CARTESIAN_POINT('Ctrl Pts',(-32.3270722923086,-2.12767770694225,
126.368040623127));
#81357=CARTESIAN_POINT('Ctrl Pts',(-32.3348234835488,-2.25055749249534,
126.429090662129));
#81358=CARTESIAN_POINT('Ctrl Pts',(-32.3425746747889,-2.37073195852932,
126.49520605509));
#81359=CARTESIAN_POINT('Ctrl Pts',(-32.350322571566,-2.49085534720916,126.561293347245));
#81360=CARTESIAN_POINT('Ctrl Pts',(-32.3580704683431,-2.60827536147061,
126.632441523321));
#81361=CARTESIAN_POINT('Ctrl Pts',(-32.3658183651202,-2.72254408773107,
126.708394705493));
#81362=CARTESIAN_POINT('Ctrl Pts',(-32.3735646412043,-2.83678891143734,
126.784331999898));
#81363=CARTESIAN_POINT('Ctrl Pts',(-32.3813109172884,-2.94788343289747,
126.865072084907));
#81364=CARTESIAN_POINT('Ctrl Pts',(-32.3890571933725,-3.05540762947576,
126.950315044374));
#81365=CARTESIAN_POINT('Ctrl Pts',(-32.3968035266379,-3.16293261977325,
127.035558633085));
#81366=CARTESIAN_POINT('Ctrl Pts',(-32.4045498599032,-3.26688692623008,
127.125304919697));
#81367=CARTESIAN_POINT('Ctrl Pts',(-32.4122961931685,-3.36688292654267,
127.219213142014));
#81368=CARTESIAN_POINT('Ctrl Pts',(-32.4200442611715,-3.46690132026594,
127.313142394427));
#81369=CARTESIAN_POINT('Ctrl Pts',(-32.4277923291744,-3.56295935900285,
127.411235169598));
#81370=CARTESIAN_POINT('Ctrl Pts',(-32.4355403971774,-3.65470595625923,
127.513113523259));
#81371=CARTESIAN_POINT('Ctrl Pts',(-32.4432966999192,-3.74655006289123,
127.615100154447));
#81372=CARTESIAN_POINT('Ctrl Pts',(-32.4510530026612,-3.83407331245463,
127.720880110229));
#81373=CARTESIAN_POINT('Ctrl Pts',(-32.458809305403,-3.91696429894751,127.830041578984));
#81374=CARTESIAN_POINT('Ctrl Pts',(-32.4665697479172,-3.9998995268559,127.939261310502));
#81375=CARTESIAN_POINT('Ctrl Pts',(-32.4743301904314,-4.07819734218227,
128.051865830404));
#81376=CARTESIAN_POINT('Ctrl Pts',(-32.4820906329456,-4.15159003668739,
128.167414802844));
#81377=CARTESIAN_POINT('Ctrl Pts',(-32.4898635332111,-4.22510054766113,
128.283149264754));
#81378=CARTESIAN_POINT('Ctrl Pts',(-32.4976364334765,-4.29369000704804,
128.401837285947));
#81379=CARTESIAN_POINT('Ctrl Pts',(-32.505409333742,-4.3571365612187,128.523013636199));
#81380=CARTESIAN_POINT('Ctrl Pts',(-32.5128996695039,-4.41827667333174,
128.639784920892));
#81381=CARTESIAN_POINT('Ctrl Pts',(-32.5203900052657,-4.47464117185407,
128.758866483112));
#81382=CARTESIAN_POINT('Ctrl Pts',(-32.5278803410276,-4.52607474631596,
128.879826790048));
#81383=CARTESIAN_POINT('Ctrl Pts',(-32.5365140061901,-4.5853591728265,129.01925055171));
#81384=CARTESIAN_POINT('Ctrl Pts',(-32.5451476713527,-4.63825300021984,
129.161546301435));
#81385=CARTESIAN_POINT('Ctrl Pts',(-32.5537813365152,-4.6844984378688,129.306142526598));
#81386=CARTESIAN_POINT('Ctrl Pts',(-32.5592297491079,-4.71368236150979,
129.39739228892));
#81387=CARTESIAN_POINT('Ctrl Pts',(-32.5646781617006,-4.74021949285508,
129.489557678113));
#81388=CARTESIAN_POINT('Ctrl Pts',(-32.5701265742934,-4.76405452823409,
129.582490119308));
#81389=CARTESIAN_POINT('Origin',(213.235140564004,0.,130.804360617566));
#81390=CARTESIAN_POINT('',(-34.6650476268334,-4.76405452823403,129.582490119308));
#81391=CARTESIAN_POINT('',(-34.31993947219,-4.764054528234,129.582490119308));
#81392=CARTESIAN_POINT('',(213.235140564004,-4.76405452823405,129.582490119308));
#81393=CARTESIAN_POINT('',(-32.9851405640433,-4.91824806159545,130.808727208065));
#81394=CARTESIAN_POINT('Ctrl Pts',(-32.9851405640433,-4.91824806159545,
130.808727208065));
#81395=CARTESIAN_POINT('Ctrl Pts',(-32.9946113937143,-4.91809934263803,
130.976234723177));
#81396=CARTESIAN_POINT('Ctrl Pts',(-33.0040822233852,-4.90938940149991,
131.143363614817));
#81397=CARTESIAN_POINT('Ctrl Pts',(-33.0135530530561,-4.89225623805502,
131.309347710185));
#81398=CARTESIAN_POINT('Ctrl Pts',(-33.0231650569598,-4.87486768397501,
131.477806000332));
#81399=CARTESIAN_POINT('Ctrl Pts',(-33.0327770608635,-4.84880296886926,
131.645085156236));
#81400=CARTESIAN_POINT('Ctrl Pts',(-33.0423890647672,-4.81425522540968,
131.810407180661));
#81401=CARTESIAN_POINT('Ctrl Pts',(-33.0499882406761,-4.7869420467601,131.941109493914));
#81402=CARTESIAN_POINT('Ctrl Pts',(-33.057587416585,-4.75432763833278,132.070588999782));
#81403=CARTESIAN_POINT('Ctrl Pts',(-33.0651865924938,-4.71652836273839,
132.198470823391));
#81404=CARTESIAN_POINT('Ctrl Pts',(-33.0729609266129,-4.67785782774121,
132.329300276008));
#81405=CARTESIAN_POINT('Ctrl Pts',(-33.0807352607321,-4.633678395593,132.458726739406));
#81406=CARTESIAN_POINT('Ctrl Pts',(-33.0885095948512,-4.58410831829956,
132.586251183397));
#81407=CARTESIAN_POINT('Ctrl Pts',(-33.0962743477984,-4.53459933169618,
132.713618464907));
#81408=CARTESIAN_POINT('Ctrl Pts',(-33.1040391007455,-4.47971305879685,
132.839088030104));
#81409=CARTESIAN_POINT('Ctrl Pts',(-33.1118038536927,-4.4196179531081,132.962174374836));
#81410=CARTESIAN_POINT('Ctrl Pts',(-33.1195608945777,-4.3595825347256,133.085138468476));
#81411=CARTESIAN_POINT('Ctrl Pts',(-33.1273179354628,-4.29434874944517,
133.20572370313));
#81412=CARTESIAN_POINT('Ctrl Pts',(-33.1350749763478,-4.22413359057179,
133.323463329149));
#81413=CARTESIAN_POINT('Ctrl Pts',(-33.142826167588,-4.15397138149572,133.4411141668));
#81414=CARTESIAN_POINT('Ctrl Pts',(-33.1505773588282,-4.07883547533745,
133.555923332661));
#81415=CARTESIAN_POINT('Ctrl Pts',(-33.1583285500684,-3.9989891911991,133.667447851859));
#81416=CARTESIAN_POINT('Ctrl Pts',(-33.1660764468455,-3.91917684386148,
133.778924970162));
#81417=CARTESIAN_POINT('Ctrl Pts',(-33.1738243436226,-3.83465832755951,
133.887119901237));
#81418=CARTESIAN_POINT('Ctrl Pts',(-33.1815722403998,-3.74574063165275,
133.991618088008));
#81419=CARTESIAN_POINT('Ctrl Pts',(-33.189318516484,-3.65684153541113,134.09609441601));
#81420=CARTESIAN_POINT('Ctrl Pts',(-33.1970647925681,-3.56354534312323,
134.196875240231));
#81421=CARTESIAN_POINT('Ctrl Pts',(-33.2048110686523,-3.46619948006827,
134.293578900631));
#81422=CARTESIAN_POINT('Ctrl Pts',(-33.2125574019177,-3.36885289842826,
134.390283274876));
#81423=CARTESIAN_POINT('Ctrl Pts',(-33.2203037351831,-3.26745686373794,
134.482910149706));
#81424=CARTESIAN_POINT('Ctrl Pts',(-33.2280500684485,-3.16239553466678,
134.57111486291));
#81425=CARTESIAN_POINT('Ctrl Pts',(-33.2357981364515,-3.05731067783942,
134.659339328948));
#81426=CARTESIAN_POINT('Ctrl Pts',(-33.2435462044546,-2.94855919267224,
134.743139411413));
#81427=CARTESIAN_POINT('Ctrl Pts',(-33.2512942724577,-2.83655784446072,
134.822211119704));
#81428=CARTESIAN_POINT('Ctrl Pts',(-33.2590505751996,-2.72443745988365,
134.901366866347));
#81429=CARTESIAN_POINT('Ctrl Pts',(-33.2668068779414,-2.6090606324382,134.975783974247));
#81430=CARTESIAN_POINT('Ctrl Pts',(-33.2745631806833,-2.4908730711102,135.045201855589));
#81431=CARTESIAN_POINT('Ctrl Pts',(-33.2823236231975,-2.372622429522,135.114656787345));
#81432=CARTESIAN_POINT('Ctrl Pts',(-33.2900840657117,-2.25155840976807,
135.179106992219));
#81433=CARTESIAN_POINT('Ctrl Pts',(-33.2978445082259,-2.12814988431899,
135.238338643264));
#81434=CARTESIAN_POINT('Ctrl Pts',(-33.3056174084914,-2.00454325254916,
135.297665378213));
#81435=CARTESIAN_POINT('Ctrl Pts',(-33.313390308757,-1.87858495364245,135.351756664486));
#81436=CARTESIAN_POINT('Ctrl Pts',(-33.3211632090225,-1.75076316437698,
135.400447149036));
#81437=CARTESIAN_POINT('Ctrl Pts',(-33.3286535447839,-1.62758801912603,
135.447367611824));
#81438=CARTESIAN_POINT('Ctrl Pts',(-33.3361438805453,-1.50268280845453,
135.489273023162));
#81439=CARTESIAN_POINT('Ctrl Pts',(-33.3436342163067,-1.37649438825613,
135.526060127446));
#81440=CARTESIAN_POINT('Ctrl Pts',(-33.3514085504258,-1.24552149574123,
135.564242025973));
#81441=CARTESIAN_POINT('Ctrl Pts',(-33.3591828845448,-1.11275128431885,
135.597030783363));
#81442=CARTESIAN_POINT('Ctrl Pts',(-33.3669572186639,-0.978667520317207,
135.624256150373));
#81443=CARTESIAN_POINT('Ctrl Pts',(-33.374721971611,-0.844749002571108,
135.651447964552));
#81444=CARTESIAN_POINT('Ctrl Pts',(-33.3824867245581,-0.709520532715764,
135.673089953455));
#81445=CARTESIAN_POINT('Ctrl Pts',(-33.3902514775052,-0.573481632377448,
135.689061414936));
#81446=CARTESIAN_POINT('Ctrl Pts',(-33.3980085183901,-0.437577847792946,
135.705017013336));
#81447=CARTESIAN_POINT('Ctrl Pts',(-33.4057655592752,-0.300865620360074,
135.715313247052));
#81448=CARTESIAN_POINT('Ctrl Pts',(-33.4135226001601,-0.163854929960267,
135.719880389109));
#81449=CARTESIAN_POINT('Ctrl Pts',(-33.4212737914003,-0.0269475603878786,
135.724444087048));
#81450=CARTESIAN_POINT('Ctrl Pts',(-33.4290249826404,0.110257434989688,
135.723287279756));
#81451=CARTESIAN_POINT('Ctrl Pts',(-33.4367761738805,0.247245038459042,
135.716392066311));
#81452=CARTESIAN_POINT('Ctrl Pts',(-33.4445240706576,0.384174418542658,
135.709499783515));
#81453=CARTESIAN_POINT('Ctrl Pts',(-33.4522719674346,0.52088620083598,135.696873965117));
#81454=CARTESIAN_POINT('Ctrl Pts',(-33.4600198642117,0.656865671480133,
135.67854881173));
#81455=CARTESIAN_POINT('Ctrl Pts',(-33.4677661402958,0.792816698150591,
135.660227491571));
#81456=CARTESIAN_POINT('Ctrl Pts',(-33.47551241638,0.92803533064574,135.636209259914));
#81457=CARTESIAN_POINT('Ctrl Pts',(-33.4832586924641,1.06201267571571,135.606580118913));
#81458=CARTESIAN_POINT('Ctrl Pts',(-33.4910050257294,1.19599100977583,135.576950759197));
#81459=CARTESIAN_POINT('Ctrl Pts',(-33.4987513589948,1.32872765638524,135.541710491911));
#81460=CARTESIAN_POINT('Ctrl Pts',(-33.5064976922601,1.45972499431876,135.500996222279));
#81461=CARTESIAN_POINT('Ctrl Pts',(-33.5142457602631,1.59075166819785,135.46027283497));
#81462=CARTESIAN_POINT('Ctrl Pts',(-33.5219938282661,1.72003788505195,135.414073122));
#81463=CARTESIAN_POINT('Ctrl Pts',(-33.5297418962691,1.84710261715635,135.362583405473));
#81464=CARTESIAN_POINT('Ctrl Pts',(-33.5374981990109,1.97430239517012,135.311038965062));
#81465=CARTESIAN_POINT('Ctrl Pts',(-33.5452545017528,2.09927560911814,135.254193437051));
#81466=CARTESIAN_POINT('Ctrl Pts',(-33.5530108044946,2.22156210249681,135.192280954953));
#81467=CARTESIAN_POINT('Ctrl Pts',(-33.5607712470088,2.34391386385896,135.130335428298));
#81468=CARTESIAN_POINT('Ctrl Pts',(-33.5685316895229,2.46357570637388,135.063317749788));
#81469=CARTESIAN_POINT('Ctrl Pts',(-33.5762921320371,2.58011429435089,134.991506816421));
#81470=CARTESIAN_POINT('Ctrl Pts',(-33.5840650323025,2.69683996041528,134.919580605769));
#81471=CARTESIAN_POINT('Ctrl Pts',(-33.5918379325679,2.81043202876259,134.842845983059));
#81472=CARTESIAN_POINT('Ctrl Pts',(-33.5996108328333,2.92048751171914,134.761624287881));
#81473=CARTESIAN_POINT('Ctrl Pts',(-33.6071011685954,3.02654220065749,134.683355205907));
#81474=CARTESIAN_POINT('Ctrl Pts',(-33.6145915043575,3.12931272739518,134.600919813088));
#81475=CARTESIAN_POINT('Ctrl Pts',(-33.6220818401195,3.22847068354311,134.514638249766));
#81476=CARTESIAN_POINT('Ctrl Pts',(-33.6298561742386,3.3313882437361,134.425085294747));
#81477=CARTESIAN_POINT('Ctrl Pts',(-33.6376305083577,3.43073989632107,134.331105079909));
#81478=CARTESIAN_POINT('Ctrl Pts',(-33.6454048424768,3.5261209182697,134.233012587691));
#81479=CARTESIAN_POINT('Ctrl Pts',(-33.6531695954238,3.62138439163323,134.135040985702));
#81480=CARTESIAN_POINT('Ctrl Pts',(-33.6609343483709,3.71268670092573,134.032967467781));
#81481=CARTESIAN_POINT('Ctrl Pts',(-33.6686991013179,3.79965629237272,133.92714705316));
#81482=CARTESIAN_POINT('Ctrl Pts',(-33.6764561422029,3.88653950439544,133.821431740867));
#81483=CARTESIAN_POINT('Ctrl Pts',(-33.6842131830879,3.96909831573404,133.71197723786));
#81484=CARTESIAN_POINT('Ctrl Pts',(-33.6919702239729,4.04699840652773,133.599174915522));
#81485=CARTESIAN_POINT('Ctrl Pts',(-33.699721415213,4.12483975225699,133.486457658294));
#81486=CARTESIAN_POINT('Ctrl Pts',(-33.7074726064531,4.19802914893938,133.370397927238));
#81487=CARTESIAN_POINT('Ctrl Pts',(-33.7152237976932,4.26627315636882,133.251419345457));
#81488=CARTESIAN_POINT('Ctrl Pts',(-33.7229716944703,4.33448815827464,133.132491332747));
#81489=CARTESIAN_POINT('Ctrl Pts',(-33.7307195912473,4.39776175737465,133.010647275178));
#81490=CARTESIAN_POINT('Ctrl Pts',(-33.7384674880243,4.45584451220179,132.886338702364));
#81491=CARTESIAN_POINT('Ctrl Pts',(-33.7462137641084,4.51391511736875,132.762056132225));
#81492=CARTESIAN_POINT('Ctrl Pts',(-33.7539600401925,4.56679687260656,132.635310426228));
#81493=CARTESIAN_POINT('Ctrl Pts',(-33.7617063162766,4.61428706473051,132.506576216943));
#81494=CARTESIAN_POINT('Ctrl Pts',(-33.7694526495419,4.66177760741627,132.37784105737));
#81495=CARTESIAN_POINT('Ctrl Pts',(-33.7771989828073,4.70387637225777,132.247117732022));
#81496=CARTESIAN_POINT('Ctrl Pts',(-33.7849453160726,4.74042956506992,132.114898904344));
#81497=CARTESIAN_POINT('Ctrl Pts',(-33.7926933840755,4.77699094371617,131.982650467177));
#81498=CARTESIAN_POINT('Ctrl Pts',(-33.8004414520785,4.8080041749526,131.848906238011));
#81499=CARTESIAN_POINT('Ctrl Pts',(-33.8081895200814,4.83336600960478,131.714171630742));
#81500=CARTESIAN_POINT('Ctrl Pts',(-33.8159458228232,4.85875479911663,131.57929382593));
#81501=CARTESIAN_POINT('Ctrl Pts',(-33.8237021255651,4.87848012123137,131.443423925191));
#81502=CARTESIAN_POINT('Ctrl Pts',(-33.8314584283069,4.89249023327454,131.307075626108));
#81503=CARTESIAN_POINT('Ctrl Pts',(-33.8392188708211,4.90650782293634,131.170654553832));
#81504=CARTESIAN_POINT('Ctrl Pts',(-33.8469793133352,4.91480410074876,131.033754964492));
#81505=CARTESIAN_POINT('Ctrl Pts',(-33.8547397558494,4.91737948213112,130.896892186319));
#81506=CARTESIAN_POINT('Ctrl Pts',(-33.8625126561148,4.9199589977443,130.759809703864));
#81507=CARTESIAN_POINT('Ctrl Pts',(-33.8702855563802,4.91679927400373,130.622764541747));
#81508=CARTESIAN_POINT('Ctrl Pts',(-33.8780584566456,4.90795283832523,130.486269436809));
#81509=CARTESIAN_POINT('Ctrl Pts',(-33.8855487924079,4.89942799286611,130.35473627274));
#81510=CARTESIAN_POINT('Ctrl Pts',(-33.8930391281702,4.88562274220658,130.223714174563));
#81511=CARTESIAN_POINT('Ctrl Pts',(-33.9005294639325,4.86662891672818,130.093652485232));
#81512=CARTESIAN_POINT('Ctrl Pts',(-33.9083037980516,4.84691493458444,129.958659467424));
#81513=CARTESIAN_POINT('Ctrl Pts',(-33.9160781321707,4.82154871320462,129.824273506605));
#81514=CARTESIAN_POINT('Ctrl Pts',(-33.9238524662898,4.7905764935515,129.691005363421));
#81515=CARTESIAN_POINT('Ctrl Pts',(-33.9316172192369,4.75964244439104,129.557901461314));
#81516=CARTESIAN_POINT('Ctrl Pts',(-33.939381972184,4.72311623124687,129.425913012969));
#81517=CARTESIAN_POINT('Ctrl Pts',(-33.9471467251311,4.68109570796365,129.295544513667));
#81518=CARTESIAN_POINT('Ctrl Pts',(-33.9549037660161,4.6391169200566,129.165305498197));
#81519=CARTESIAN_POINT('Ctrl Pts',(-33.9626608069012,4.59165480090288,129.03668359958));
#81520=CARTESIAN_POINT('Ctrl Pts',(-33.9704178477862,4.538857914282,128.910171636377));
#81521=CARTESIAN_POINT('Ctrl Pts',(-33.9781690390263,4.48610084220394,128.783755076828));
#81522=CARTESIAN_POINT('Ctrl Pts',(-33.9859202302664,4.42801716014065,128.659445645015));
#81523=CARTESIAN_POINT('Ctrl Pts',(-33.9936714215066,4.36480466260737,128.537719199128));
#81524=CARTESIAN_POINT('Ctrl Pts',(-34.0014193182837,4.3016190320718,128.416044490227));
#81525=CARTESIAN_POINT('Ctrl Pts',(-34.0091672150607,4.23330910149245,128.296950929979));
#81526=CARTESIAN_POINT('Ctrl Pts',(-34.0169151118378,4.1601199263164,128.180892443342));
#81527=CARTESIAN_POINT('Ctrl Pts',(-34.0246613879219,4.08694606073803,128.064858233639));
#81528=CARTESIAN_POINT('Ctrl Pts',(-34.0324076640061,4.00889518907209,127.95185816524));
#81529=CARTESIAN_POINT('Ctrl Pts',(-34.0401539400902,3.92625706171269,127.842319336987));
#81530=CARTESIAN_POINT('Ctrl Pts',(-34.0479002733555,3.84361832433741,127.732779700144));
#81531=CARTESIAN_POINT('Ctrl Pts',(-34.0556466066209,3.75639249916016,127.626701666538));
#81532=CARTESIAN_POINT('Ctrl Pts',(-34.0633929398863,3.66491094837876,127.5244809242));
#81533=CARTESIAN_POINT('Ctrl Pts',(-34.0711410078892,3.57340891093847,127.422237290236));
#81534=CARTESIAN_POINT('Ctrl Pts',(-34.0788890758922,3.47764951213106,127.323852957708));
#81535=CARTESIAN_POINT('Ctrl Pts',(-34.0866371438952,3.37800216227966,127.229687981627));
#81536=CARTESIAN_POINT('Ctrl Pts',(-34.094393446637,3.27824890603889,127.135422925888));
#81537=CARTESIAN_POINT('Ctrl Pts',(-34.1021497493789,3.17459972893179,127.045386453586));
#81538=CARTESIAN_POINT('Ctrl Pts',(-34.1099060521208,3.06745885110309,126.95989976339));
#81539=CARTESIAN_POINT('Ctrl Pts',(-34.117666494635,2.96026078896195,126.874367446374));
#81540=CARTESIAN_POINT('Ctrl Pts',(-34.1254269371491,2.8495676280572,126.793389980891));
#81541=CARTESIAN_POINT('Ctrl Pts',(-34.1331873796633,2.73581315316811,126.717245564934));
#81542=CARTESIAN_POINT('Ctrl Pts',(-34.1409602799287,2.62187606949727,126.6409789152));
#81543=CARTESIAN_POINT('Ctrl Pts',(-34.1487331801942,2.50486818542463,126.569561022633));
#81544=CARTESIAN_POINT('Ctrl Pts',(-34.1565060804596,2.38524927332648,126.503224841216));
#81545=CARTESIAN_POINT('Ctrl Pts',(-34.1639964162215,2.26997880998739,126.439300147086));
#81546=CARTESIAN_POINT('Ctrl Pts',(-34.1714867519834,2.15228413286571,126.380094250997));
#81547=CARTESIAN_POINT('Ctrl Pts',(-34.1789770877453,2.03259292347908,126.325772774292));
#81548=CARTESIAN_POINT('Ctrl Pts',(-34.1867514218644,1.90836358550693,126.269391682285));
#81549=CARTESIAN_POINT('Ctrl Pts',(-34.1945257559835,1.78158980840141,126.218094108359));
#81550=CARTESIAN_POINT('Ctrl Pts',(-34.2023000901025,1.65272630393062,126.172117227286));
#81551=CARTESIAN_POINT('Ctrl Pts',(-34.2100648430496,1.52402161221223,126.12619700861));
#81552=CARTESIAN_POINT('Ctrl Pts',(-34.2178295959967,1.39323268210615,126.085584565877));
#81553=CARTESIAN_POINT('Ctrl Pts',(-34.2255943489438,1.26083685217334,126.050470263898));
#81554=CARTESIAN_POINT('Ctrl Pts',(-34.2333513898288,1.12857251964528,126.015390837938));
#81555=CARTESIAN_POINT('Ctrl Pts',(-34.2411084307137,0.994704838848106,
125.985798785012));
#81556=CARTESIAN_POINT('Ctrl Pts',(-34.2488654715987,0.859728734345996,
125.961835494674));
#81557=CARTESIAN_POINT('Ctrl Pts',(-34.2566166628389,0.724854416374068,
125.937890275239));
#81558=CARTESIAN_POINT('Ctrl Pts',(-34.2643678540791,0.58887372183565,125.919565437653));
#81559=CARTESIAN_POINT('Ctrl Pts',(-34.2721190453193,0.452293916470628,
125.906951784762));
#81560=CARTESIAN_POINT('Ctrl Pts',(-34.2798669420963,0.315772161166458,
125.894343493011));
#81561=CARTESIAN_POINT('Ctrl Pts',(-34.2876148388734,0.178652189984851,
125.887441593909));
#81562=CARTESIAN_POINT('Ctrl Pts',(-34.2953627356504,0.0414483613027857,
125.886285272897));
#81563=CARTESIAN_POINT('Ctrl Pts',(-34.3031090117345,-0.0957267672960914,
125.885129193761));
#81564=CARTESIAN_POINT('Ctrl Pts',(-34.3108552878186,-0.232985327801419,
125.88971630546));
#81565=CARTESIAN_POINT('Ctrl Pts',(-34.3186015639027,-0.36981137269736,
125.900033690135));
#81566=CARTESIAN_POINT('Ctrl Pts',(-34.3263478971681,-0.506638427612083,
125.910351150971));
#81567=CARTESIAN_POINT('Ctrl Pts',(-34.3340942304334,-0.643032570688132,
125.926398939792));
#81568=CARTESIAN_POINT('Ctrl Pts',(-34.3418405636988,-0.778481789016616,
125.948112151242));
#81569=CARTESIAN_POINT('Ctrl Pts',(-34.3495886317017,-0.913961340258221,
125.969830225216));
#81570=CARTESIAN_POINT('Ctrl Pts',(-34.3573366997047,-1.04849515971152,
125.997216184577));
#81571=CARTESIAN_POINT('Ctrl Pts',(-34.3650847677077,-1.18158064759604,
126.030153852487));
#81572=CARTESIAN_POINT('Ctrl Pts',(-34.3728410704495,-1.31480758032101,
126.063126526942));
#81573=CARTESIAN_POINT('Ctrl Pts',(-34.3805973731914,-1.44658272643163,
126.101662602597));
#81574=CARTESIAN_POINT('Ctrl Pts',(-34.3883536759332,-1.57641736152975,
126.145595613322));
#81575=CARTESIAN_POINT('Ctrl Pts',(-34.3961141184474,-1.70632129328187,
126.189552072418));
#81576=CARTESIAN_POINT('Ctrl Pts',(-34.4038745609615,-1.83428228569309,
126.238911065602));
#81577=CARTESIAN_POINT('Ctrl Pts',(-34.4116350034757,-1.95983181164479,
126.293458010264));
#81578=CARTESIAN_POINT('Ctrl Pts',(-34.4194079037411,-2.08558288084148,
126.348092518524));
#81579=CARTESIAN_POINT('Ctrl Pts',(-34.4271808040066,-2.20891439593567,
126.407931449818));
#81580=CARTESIAN_POINT('Ctrl Pts',(-34.4349537042721,-2.32938184794327,
126.472713901942));
#81581=CARTESIAN_POINT('Ctrl Pts',(-34.4424440400341,-2.44547000463184,
126.535141348755));
#81582=CARTESIAN_POINT('Ctrl Pts',(-34.4499343757961,-2.5588984496489,126.602158980885));
#81583=CARTESIAN_POINT('Ctrl Pts',(-34.4574247115582,-2.66929666876196,
126.67349650014));
#81584=CARTESIAN_POINT('Ctrl Pts',(-34.4651967991377,-2.78384755871116,
126.747517407208));
#81585=CARTESIAN_POINT('Ctrl Pts',(-34.4729688867172,-2.89549949137508,
126.82642457917));
#81586=CARTESIAN_POINT('Ctrl Pts',(-34.4807409742967,-3.00380714388975,
126.909963911423));
#81587=CARTESIAN_POINT('Ctrl Pts',(-34.4885007573929,-3.1119433277124,126.993370987278));
#81588=CARTESIAN_POINT('Ctrl Pts',(-34.4962605404892,-3.21674546924396,
127.081395380739));
#81589=CARTESIAN_POINT('Ctrl Pts',(-34.5040203235855,-3.31779583247672,
127.173738924729));
#81590=CARTESIAN_POINT('Ctrl Pts',(-34.5117730050702,-3.41875371626542,
127.265997957597));
#81591=CARTESIAN_POINT('Ctrl Pts',(-34.5195256865548,-3.51596636494148,
127.362568015953));
#81592=CARTESIAN_POINT('Ctrl Pts',(-34.5272783680395,-3.60904761639883,
127.463109599599));
#81593=CARTESIAN_POINT('Ctrl Pts',(-34.5350256379881,-3.70206389516783,
127.563581003086));
#81594=CARTESIAN_POINT('Ctrl Pts',(-34.5427729079366,-3.79095424973157,
127.668018130206));
#81595=CARTESIAN_POINT('Ctrl Pts',(-34.5505201778852,-3.87536832769674,
127.776043694392));
#81596=CARTESIAN_POINT('Ctrl Pts',(-34.5582637223173,-3.95974181251877,
127.884017311114));
#81597=CARTESIAN_POINT('Ctrl Pts',(-34.5660072667493,-4.03964306452908,
127.995575622787));
#81598=CARTESIAN_POINT('Ctrl Pts',(-34.5737508111814,-4.11476136648118,
128.110307544701));
#81599=CARTESIAN_POINT('Ctrl Pts',(-34.581494001961,-4.18987623773411,128.225034226737));
#81600=CARTESIAN_POINT('Ctrl Pts',(-34.5892371927407,-4.26020836969045,
128.342933909747));
#81601=CARTESIAN_POINT('Ctrl Pts',(-34.5969803835203,-4.32548987863497,
128.4635658012));
#81602=CARTESIAN_POINT('Ctrl Pts',(-34.6047230389637,-4.39076687425237,
128.584189352601));
#81603=CARTESIAN_POINT('Ctrl Pts',(-34.6124656944072,-4.45099375982855,
128.707544389925));
#81604=CARTESIAN_POINT('Ctrl Pts',(-34.6202083498507,-4.50594858202552,
128.833165437316));
#81605=CARTESIAN_POINT('Ctrl Pts',(-34.6279556026154,-4.560936034497,128.958861074143));
#81606=CARTESIAN_POINT('Ctrl Pts',(-34.6357028553801,-4.61064501347426,
129.086825049675));
#81607=CARTESIAN_POINT('Ctrl Pts',(-34.6434501081448,-4.65490160907204,
129.216571565973));
#81608=CARTESIAN_POINT('Ctrl Pts',(-34.650649281041,-4.69602726911979,129.337139157076));
#81609=CARTESIAN_POINT('Ctrl Pts',(-34.6578484539372,-4.73244513292729,
129.459245566747));
#81610=CARTESIAN_POINT('Ctrl Pts',(-34.6650476268334,-4.76405452823403,
129.582490119308));
#81611=CARTESIAN_POINT('Ctrl Pts',(-32.9151834992122,-4.76405452823401,
129.582490119308));
#81612=CARTESIAN_POINT('Ctrl Pts',(-32.9228708627559,-4.79790449531073,
129.714470627195));
#81613=CARTESIAN_POINT('Ctrl Pts',(-32.9305582262996,-4.82626875440093,
129.847870405711));
#81614=CARTESIAN_POINT('Ctrl Pts',(-32.9382455898434,-4.84904313388873,
129.982190472045));
#81615=CARTESIAN_POINT('Ctrl Pts',(-32.9460614188709,-4.8721981018139,130.118755195107));
#81616=CARTESIAN_POINT('Ctrl Pts',(-32.9538772478985,-4.88957459330449,
130.256270826341));
#81617=CARTESIAN_POINT('Ctrl Pts',(-32.961693076926,-4.90111776738139,130.394204924251));
#81618=CARTESIAN_POINT('Ctrl Pts',(-32.9695089059535,-4.91266094145829,
130.532139022162));
#81619=CARTESIAN_POINT('Ctrl Pts',(-32.977324734981,-4.91837079231979,130.670491155864));
#81620=CARTESIAN_POINT('Ctrl Pts',(-32.9851405640085,-4.918248061596,130.808727207449));
#81621=CARTESIAN_POINT('',(-32.6398594359421,-4.91824935210416,130.801836132062));
#81622=CARTESIAN_POINT('Ctrl Pts',(-32.5701265742934,-4.76405452823409,
129.582490119308));
#81623=CARTESIAN_POINT('Ctrl Pts',(-32.5787159453649,-4.80163023673377,
129.728997236458));
#81624=CARTESIAN_POINT('Ctrl Pts',(-32.5873053164363,-4.83248793567468,
129.877411663971));
#81625=CARTESIAN_POINT('Ctrl Pts',(-32.5958946875078,-4.8564495174955,130.02713404409));
#81626=CARTESIAN_POINT('Ctrl Pts',(-32.6044442660324,-4.8803000909132,130.176162795446));
#81627=CARTESIAN_POINT('Ctrl Pts',(-32.6129938445571,-4.89731819714702,
130.326487182374));
#81628=CARTESIAN_POINT('Ctrl Pts',(-32.6215434230817,-4.90737648749908,
130.477498150401));
#81629=CARTESIAN_POINT('Ctrl Pts',(-32.6276487607019,-4.91455921098699,
130.585336559217));
#81630=CARTESIAN_POINT('Ctrl Pts',(-32.633754098322,-4.91819375699317,130.693524708538));
#81631=CARTESIAN_POINT('Ctrl Pts',(-32.6398594359422,-4.91824935210415,
130.801836132062));
#81632=CARTESIAN_POINT('Ctrl Pts',(-32.6398594359911,-4.9182493521046,130.801836132932));
#81633=CARTESIAN_POINT('Ctrl Pts',(-32.6477146369204,-4.91832088141948,
130.941190915199));
#81634=CARTESIAN_POINT('Ctrl Pts',(-32.6555698378496,-4.91246529782376,
131.080539411816));
#81635=CARTESIAN_POINT('Ctrl Pts',(-32.6634250387788,-4.9007107268889,131.21935150163));
#81636=CARTESIAN_POINT('Ctrl Pts',(-32.6712824326159,-4.88895287447336,
131.358202343108));
#81637=CARTESIAN_POINT('Ctrl Pts',(-32.679139826453,-4.87129278575712,131.496516105238));
#81638=CARTESIAN_POINT('Ctrl Pts',(-32.68699722029,-4.84781044438552,131.633768212061));
#81639=CARTESIAN_POINT('Ctrl Pts',(-32.6948583187497,-4.82431703150399,
131.771085030833));
#81640=CARTESIAN_POINT('Ctrl Pts',(-32.7027194172094,-4.79499596115353,
131.907338827296));
#81641=CARTESIAN_POINT('Ctrl Pts',(-32.7105805156691,-4.75997821932935,
132.042015825615));
#81642=CARTESIAN_POINT('Ctrl Pts',(-32.7185594697667,-4.72443548238876,
132.178711936609));
#81643=CARTESIAN_POINT('Ctrl Pts',(-32.7265384238643,-4.68302399350987,
132.313783201881));
#81644=CARTESIAN_POINT('Ctrl Pts',(-32.7345173779619,-4.63593256907531,
132.446710238532));
#81645=CARTESIAN_POINT('Ctrl Pts',(-32.7423951192043,-4.58943849831233,
132.57795109868));
#81646=CARTESIAN_POINT('Ctrl Pts',(-32.7502728604466,-4.53740795696268,
132.707101490471));
#81647=CARTESIAN_POINT('Ctrl Pts',(-32.758150601689,-4.48007028516977,132.833683978304));
#81648=CARTESIAN_POINT('Ctrl Pts',(-32.7661801622142,-4.42162760574246,
132.962705955065));
#81649=CARTESIAN_POINT('Ctrl Pts',(-32.7742097227395,-4.35767134368835,
133.089059673188));
#81650=CARTESIAN_POINT('Ctrl Pts',(-32.7822392832647,-4.2884918207682,133.212268623638));
#81651=CARTESIAN_POINT('Ctrl Pts',(-32.79026884379,-4.21931229784813,133.335477574087));
#81652=CARTESIAN_POINT('Ctrl Pts',(-32.7982984043152,-4.14490978357858,
133.455541446482));
#81653=CARTESIAN_POINT('Ctrl Pts',(-32.8063279648404,-4.0656187706269,133.572017943614));
#81654=CARTESIAN_POINT('Ctrl Pts',(-32.8141022989595,-3.98884808991657,
133.684792136283));
#81655=CARTESIAN_POINT('Ctrl Pts',(-32.8218766330786,-3.90725997239606,
133.794548278398));
#81656=CARTESIAN_POINT('Ctrl Pts',(-32.8296509671977,-3.82111939450904,
133.900847277542));
#81657=CARTESIAN_POINT('Ctrl Pts',(-32.8374157201448,-3.73508497718567,
134.007015272669));
#81658=CARTESIAN_POINT('Ctrl Pts',(-32.8451804730919,-3.64450950650486,
134.109734301355));
#81659=CARTESIAN_POINT('Ctrl Pts',(-32.852945226039,-3.54970163305374,134.208593479577));
#81660=CARTESIAN_POINT('Ctrl Pts',(-32.860702266924,-3.45498792411934,134.30735446947));
#81661=CARTESIAN_POINT('Ctrl Pts',(-32.868459307809,-3.35605044679242,134.402262957702));
#81662=CARTESIAN_POINT('Ctrl Pts',(-32.876216348694,-3.25323834702194,134.492940740048));
#81663=CARTESIAN_POINT('Ctrl Pts',(-32.8839675399341,-3.15050377865551,
134.583550141572));
#81664=CARTESIAN_POINT('Ctrl Pts',(-32.8917187311742,-3.04390069570522,
134.669934929962));
#81665=CARTESIAN_POINT('Ctrl Pts',(-32.8994699224144,-2.93381509834212,
134.751753685306));
#81666=CARTESIAN_POINT('Ctrl Pts',(-32.9072178191914,-2.82377629029454,
134.833537665496));
#81667=CARTESIAN_POINT('Ctrl Pts',(-32.9149657159685,-2.71025822489476,
134.910759239786));
#81668=CARTESIAN_POINT('Ctrl Pts',(-32.9227136127456,-2.59367981013424,
134.983117383041));
#81669=CARTESIAN_POINT('Ctrl Pts',(-32.9304598888296,-2.47712578106495,
135.055460390532));
#81670=CARTESIAN_POINT('Ctrl Pts',(-32.9382061649138,-2.3575130079169,135.122941784453));
#81671=CARTESIAN_POINT('Ctrl Pts',(-32.9459524409979,-2.23528885894826,
135.185304212222));
#81672=CARTESIAN_POINT('Ctrl Pts',(-32.9536987742632,-2.11306380774889,
135.247667100337));
#81673=CARTESIAN_POINT('Ctrl Pts',(-32.9614451075285,-1.98822769051716,
135.304910769209));
#81674=CARTESIAN_POINT('Ctrl Pts',(-32.9691914407938,-1.86125155794798,
135.356824313252));
#81675=CARTESIAN_POINT('Ctrl Pts',(-32.9769395087968,-1.73424698995447,
135.408749482972));
#81676=CARTESIAN_POINT('Ctrl Pts',(-32.9846875767997,-1.60510181480681,
135.45534200472));
#81677=CARTESIAN_POINT('Ctrl Pts',(-32.9924356448027,-1.4743057142101,135.496439658199));
#81678=CARTESIAN_POINT('Ctrl Pts',(-33.0001919475445,-1.34337060196082,
135.537580990753));
#81679=CARTESIAN_POINT('Ctrl Pts',(-33.0079482502864,-1.21078143279462,
135.573215671602));
#81680=CARTESIAN_POINT('Ctrl Pts',(-33.0157045530282,-1.07704219749085,
135.603231648061));
#81681=CARTESIAN_POINT('Ctrl Pts',(-33.0234649955424,-0.943231581530391,
135.633263644951));
#81682=CARTESIAN_POINT('Ctrl Pts',(-33.0312254380566,-0.808270060870548,
135.657670892403));
#81683=CARTESIAN_POINT('Ctrl Pts',(-33.0389858805707,-0.672669405852567,
135.676392938162));
#81684=CARTESIAN_POINT('Ctrl Pts',(-33.0467587808362,-0.536851072624907,
135.69514503821));
#81685=CARTESIAN_POINT('Ctrl Pts',(-33.0545316811016,-0.400391944187662,
135.708193661892));
#81686=CARTESIAN_POINT('Ctrl Pts',(-33.062304581367,-0.263807372512092,
135.715530410264));
#81687=CARTESIAN_POINT('Ctrl Pts',(-33.0697949171291,-0.132187994051589,
135.722600449352));
#81688=CARTESIAN_POINT('Ctrl Pts',(-33.0772852528912,-0.000452442356223659,
135.724366681204));
#81689=CARTESIAN_POINT('Ctrl Pts',(-33.0847755886533,0.130942238749945,
135.720867222119));
#81690=CARTESIAN_POINT('Ctrl Pts',(-33.0925499227724,0.267318789125649,
135.717235079979));
#81691=CARTESIAN_POINT('Ctrl Pts',(-33.1003242568915,0.403760110362607,
135.707918561769));
#81692=CARTESIAN_POINT('Ctrl Pts',(-33.1080985910106,0.539753555335134,
135.6929032595));
#81693=CARTESIAN_POINT('Ctrl Pts',(-33.1158633439577,0.675579400540446,
135.677906462248));
#81694=CARTESIAN_POINT('Ctrl Pts',(-33.1236280969047,0.810958082858944,
135.65722489759));
#81695=CARTESIAN_POINT('Ctrl Pts',(-33.1313928498518,0.945377080745844,
135.630896149156));
#81696=CARTESIAN_POINT('Ctrl Pts',(-33.1391498907368,1.07966257178925,135.604593550806));
#81697=CARTESIAN_POINT('Ctrl Pts',(-33.1469069316218,1.21298989406473,135.572655005234));
#81698=CARTESIAN_POINT('Ctrl Pts',(-33.1546639725068,1.34485213173174,135.535169830193));
#81699=CARTESIAN_POINT('Ctrl Pts',(-33.1624151637469,1.47661493105923,135.497712923014));
#81700=CARTESIAN_POINT('Ctrl Pts',(-33.170166354987,1.60691447033537,135.454717818362));
#81701=CARTESIAN_POINT('Ctrl Pts',(-33.1779175462271,1.73525486079802,135.406324723312));
#81702=CARTESIAN_POINT('Ctrl Pts',(-33.1856654430042,1.86354070317147,135.357952196618));
#81703=CARTESIAN_POINT('Ctrl Pts',(-33.1934133397814,1.98986868783246,135.304186380345));
#81704=CARTESIAN_POINT('Ctrl Pts',(-33.2011612365584,2.11375912380571,135.245217002209));
#81705=CARTESIAN_POINT('Ctrl Pts',(-33.2089075126425,2.23762364457053,135.186259959197));
#81706=CARTESIAN_POINT('Ctrl Pts',(-33.2166537887266,2.35905127803991,135.122101687277));
#81707=CARTESIAN_POINT('Ctrl Pts',(-33.2244000648107,2.4775836927265,135.052979464678));
#81708=CARTESIAN_POINT('Ctrl Pts',(-33.232146398076,2.59611698239213,134.983856731835));
#81709=CARTESIAN_POINT('Ctrl Pts',(-33.2398927313413,2.71175467289462,134.909770172145));
#81710=CARTESIAN_POINT('Ctrl Pts',(-33.2476390646066,2.82406470898329,134.831002094278));
#81711=CARTESIAN_POINT('Ctrl Pts',(-33.2553871326096,2.93639989612568,134.752216376845));
#81712=CARTESIAN_POINT('Ctrl Pts',(-33.2631352006125,3.04540562595478,134.668747279503));
#81713=CARTESIAN_POINT('Ctrl Pts',(-33.2708832686155,3.15068073301714,134.580919101304));
#81714=CARTESIAN_POINT('Ctrl Pts',(-33.2786395713573,3.2560677277165,134.492997578272));
#81715=CARTESIAN_POINT('Ctrl Pts',(-33.2863958740992,3.35771587854612,134.400707970556));
#81716=CARTESIAN_POINT('Ctrl Pts',(-33.2941521768411,3.45525849308206,134.304413732661));
#81717=CARTESIAN_POINT('Ctrl Pts',(-33.3019126193552,3.55285316904847,134.208068099631));
#81718=CARTESIAN_POINT('Ctrl Pts',(-33.3096730618694,3.64633767611456,134.107713863419));
#81719=CARTESIAN_POINT('Ctrl Pts',(-33.3174335043836,3.73538452971476,134.003748914986));
#81720=CARTESIAN_POINT('Ctrl Pts',(-33.325206404649,3.82457432922944,133.899617072788));
#81721=CARTESIAN_POINT('Ctrl Pts',(-33.3329793049144,3.90931199800893,133.791863243141));
#81722=CARTESIAN_POINT('Ctrl Pts',(-33.3407522051798,3.98931190945571,133.68091646642));
#81723=CARTESIAN_POINT('Ctrl Pts',(-33.348242540942,4.06640362261519,133.574002884488));
#81724=CARTESIAN_POINT('Ctrl Pts',(-33.3557328767041,4.13909588700599,133.46412472536));
#81725=CARTESIAN_POINT('Ctrl Pts',(-33.3632232124663,4.20717372759986,133.351687115739));
#81726=CARTESIAN_POINT('Ctrl Pts',(-33.3709975465854,4.27783276021036,133.234986399977));
#81727=CARTESIAN_POINT('Ctrl Pts',(-33.3787718807045,4.34374437647595,133.11515864654));
#81728=CARTESIAN_POINT('Ctrl Pts',(-33.3865462148236,4.40461935625323,132.992627372105));
#81729=CARTESIAN_POINT('Ctrl Pts',(-33.3943109677707,4.46541931305849,132.870247106514));
#81730=CARTESIAN_POINT('Ctrl Pts',(-33.4020757207177,4.52119481158055,132.745170296083));
#81731=CARTESIAN_POINT('Ctrl Pts',(-33.4098404736648,4.57170044157857,132.617848454572));
#81732=CARTESIAN_POINT('Ctrl Pts',(-33.4175975145498,4.62215590867286,132.49065307091));
#81733=CARTESIAN_POINT('Ctrl Pts',(-33.4253545554347,4.66735178012736,132.36121745463));
#81734=CARTESIAN_POINT('Ctrl Pts',(-33.4331115963197,4.70708920110316,132.230016366812));
#81735=CARTESIAN_POINT('Ctrl Pts',(-33.4408627875599,4.74679665578085,132.098914218754));
#81736=CARTESIAN_POINT('Ctrl Pts',(-33.4486139788001,4.78105374027489,131.966049621808));
#81737=CARTESIAN_POINT('Ctrl Pts',(-33.4563651700402,4.80971037477895,131.83191556658));
#81738=CARTESIAN_POINT('Ctrl Pts',(-33.4641130668173,4.83835482944879,131.697838521905));
#81739=CARTESIAN_POINT('Ctrl Pts',(-33.4718609635944,4.86140348693259,131.562493473616));
#81740=CARTESIAN_POINT('Ctrl Pts',(-33.4796088603714,4.87875668584335,131.426386551783));
#81741=CARTESIAN_POINT('Ctrl Pts',(-33.4873551364555,4.89610625483896,131.290308100584));
#81742=CARTESIAN_POINT('Ctrl Pts',(-33.4951014125396,4.9077626855409,131.153468480412));
#81743=CARTESIAN_POINT('Ctrl Pts',(-33.5028476886236,4.91367786747877,131.016381553205));
#81744=CARTESIAN_POINT('Ctrl Pts',(-33.510594021889,4.91959309308118,130.879293614054));
#81745=CARTESIAN_POINT('Ctrl Pts',(-33.5183403551543,4.91976696849799,130.741958754827));
#81746=CARTESIAN_POINT('Ctrl Pts',(-33.5260866884197,4.91420347159105,130.604893070575));
#81747=CARTESIAN_POINT('Ctrl Pts',(-33.5338347564226,4.90863872877755,130.467796691414));
#81748=CARTESIAN_POINT('Ctrl Pts',(-33.5415828244256,4.89733407280118,130.330969997746));
#81749=CARTESIAN_POINT('Ctrl Pts',(-33.5493308924285,4.88034550591383,130.194925792989));
#81750=CARTESIAN_POINT('Ctrl Pts',(-33.5570871951704,4.8633388833754,130.058736998833));
#81751=CARTESIAN_POINT('Ctrl Pts',(-33.5648434979122,4.84063633104417,129.923332743445));
#81752=CARTESIAN_POINT('Ctrl Pts',(-33.572599800654,4.81234542727534,129.789217991586));
#81753=CARTESIAN_POINT('Ctrl Pts',(-33.5803602431682,4.78403942379938,129.655031658645));
#81754=CARTESIAN_POINT('Ctrl Pts',(-33.5881206856823,4.75013922224993,129.522136579271));
#81755=CARTESIAN_POINT('Ctrl Pts',(-33.5958811281965,4.71080256615432,129.391023345287));
#81756=CARTESIAN_POINT('Ctrl Pts',(-33.6036540284619,4.67140276336609,129.259699636699));
#81757=CARTESIAN_POINT('Ctrl Pts',(-33.6114269287274,4.62654919454484,129.130163859102));
#81758=CARTESIAN_POINT('Ctrl Pts',(-33.6191998289928,4.57644843535629,129.002888225042));
#81759=CARTESIAN_POINT('Ctrl Pts',(-33.6266901647549,4.52816896496011,128.880239380868));
#81760=CARTESIAN_POINT('Ctrl Pts',(-33.6341805005169,4.4750173022852,128.759689491154));
#81761=CARTESIAN_POINT('Ctrl Pts',(-33.641670836279,4.41721809264798,128.641638401357));
#81762=CARTESIAN_POINT('Ctrl Pts',(-33.6494451703981,4.35722740841002,128.519111368611));
#81763=CARTESIAN_POINT('Ctrl Pts',(-33.6572195045172,4.29203976431774,128.398888231444));
#81764=CARTESIAN_POINT('Ctrl Pts',(-33.6649938386363,4.22185514639264,128.281441240063));
#81765=CARTESIAN_POINT('Ctrl Pts',(-33.6727585915834,4.15175702473647,128.164138991603));
#81766=CARTESIAN_POINT('Ctrl Pts',(-33.6805233445305,4.07667438110451,128.049606413842));
#81767=CARTESIAN_POINT('Ctrl Pts',(-33.6882880974777,3.99685443658223,127.938294031586));
#81768=CARTESIAN_POINT('Ctrl Pts',(-33.6960451383627,3.91711377035411,127.827092206356));
#81769=CARTESIAN_POINT('Ctrl Pts',(-33.7038021792477,3.83264539306175,127.719104527448));
#81770=CARTESIAN_POINT('Ctrl Pts',(-33.7115592201327,3.74374124875022,127.614754917028));
#81771=CARTESIAN_POINT('Ctrl Pts',(-33.7193104113729,3.65490414774548,127.510483997461));
#81772=CARTESIAN_POINT('Ctrl Pts',(-33.727061602613,3.56163819035822,127.409845982017));
#81773=CARTESIAN_POINT('Ctrl Pts',(-33.7348127938532,3.46427702174812,127.313233610554));
#81774=CARTESIAN_POINT('Ctrl Pts',(-33.7425606906303,3.36695723423201,127.216662301926));
#81775=CARTESIAN_POINT('Ctrl Pts',(-33.7503085874073,3.26554597430036,127.124113509026));
#81776=CARTESIAN_POINT('Ctrl Pts',(-33.7580564841844,3.16041519410034,127.035944655467));
#81777=CARTESIAN_POINT('Ctrl Pts',(-33.7658027602685,3.05530640499318,126.947794244932));
#81778=CARTESIAN_POINT('Ctrl Pts',(-33.7735490363527,2.94647994256069,126.864022202458));
#81779=CARTESIAN_POINT('Ctrl Pts',(-33.7812953124368,2.83434212852143,126.784946759677));
#81780=CARTESIAN_POINT('Ctrl Pts',(-33.7890416457021,2.7222034867063,126.705870733179));
#81781=CARTESIAN_POINT('Ctrl Pts',(-33.7967879789676,2.60675376402312,126.631491600864));
#81782=CARTESIAN_POINT('Ctrl Pts',(-33.8045343122329,2.48842931598555,126.562084978025));
#81783=CARTESIAN_POINT('Ctrl Pts',(-33.8122823802359,2.37007837000825,126.492662812054));
#81784=CARTESIAN_POINT('Ctrl Pts',(-33.8200304482388,2.24885175480483,126.428215569186));
#81785=CARTESIAN_POINT('Ctrl Pts',(-33.8277785162418,2.12521117699891,126.368973315914));
#81786=CARTESIAN_POINT('Ctrl Pts',(-33.8355348189837,2.00143919251555,126.30966809927));
#81787=CARTESIAN_POINT('Ctrl Pts',(-33.8432911217256,1.87524847353427,126.255579092046));
#81788=CARTESIAN_POINT('Ctrl Pts',(-33.8510474244675,1.74712200993646,126.206888731312));
#81789=CARTESIAN_POINT('Ctrl Pts',(-33.8588078669816,1.61892716138704,126.158172383066));
#81790=CARTESIAN_POINT('Ctrl Pts',(-33.8665683094958,1.48879488032868,126.114860546189));
#81791=CARTESIAN_POINT('Ctrl Pts',(-33.87432875201,1.35722317978619,126.077085683447));
#81792=CARTESIAN_POINT('Ctrl Pts',(-33.8821016522755,1.22544026866979,126.039250181142));
#81793=CARTESIAN_POINT('Ctrl Pts',(-33.8898745525409,1.09221370077561,126.006969507032));
#81794=CARTESIAN_POINT('Ctrl Pts',(-33.8976474528064,0.958052421087607,
125.980325105575));
#81795=CARTESIAN_POINT('Ctrl Pts',(-33.9051377885683,0.828768241850493,
125.954649295225));
#81796=CARTESIAN_POINT('Ctrl Pts',(-33.9126281243302,0.69861643350888,125.934207134382));
#81797=CARTESIAN_POINT('Ctrl Pts',(-33.9201184600921,0.568054823652561,
125.919025748816));
#81798=CARTESIAN_POINT('Ctrl Pts',(-33.9278927942112,0.432542930672723,
125.903268756401));
#81799=CARTESIAN_POINT('Ctrl Pts',(-33.9356671283302,0.29616028654971,125.893129425334));
#81800=CARTESIAN_POINT('Ctrl Pts',(-33.9434414624493,0.159412306085997,
125.888694764483));
#81801=CARTESIAN_POINT('Ctrl Pts',(-33.9512062153964,0.0228328552870593,
125.884265568954));
#81802=CARTESIAN_POINT('Ctrl Pts',(-33.9589709683435,-0.114110648991904,
125.8855270676));
#81803=CARTESIAN_POINT('Ctrl Pts',(-33.9667357212906,-0.250905538439235,
125.892514785979));
#81804=CARTESIAN_POINT('Ctrl Pts',(-33.9744927621756,-0.387564561274083,
125.899495564057));
#81805=CARTESIAN_POINT('Ctrl Pts',(-33.9822498030606,-0.524074875091091,
125.912191223946));
#81806=CARTESIAN_POINT('Ctrl Pts',(-33.9900068439456,-0.659922019276341,
125.930585285139));
#81807=CARTESIAN_POINT('Ctrl Pts',(-33.9977580351857,-0.795666720072131,
125.948965475227));
#81808=CARTESIAN_POINT('Ctrl Pts',(-34.0055092264257,-0.930748860795491,
125.973035461038));
#81809=CARTESIAN_POINT('Ctrl Pts',(-34.0132604176658,-1.06465767492297,
126.002726822937));
#81810=CARTESIAN_POINT('Ctrl Pts',(-34.0210083144429,-1.19850957423359,
126.032405565215));
#81811=CARTESIAN_POINT('Ctrl Pts',(-34.02875621122,-1.33118875791891,126.067700847119));
#81812=CARTESIAN_POINT('Ctrl Pts',(-34.0365041079971,-1.46219346614992,
126.108492930967));
#81813=CARTESIAN_POINT('Ctrl Pts',(-34.0442503840812,-1.59317077102029,
126.14927648199));
#81814=CARTESIAN_POINT('Ctrl Pts',(-34.0519966601652,-1.72247392408005,
126.195554431757));
#81815=CARTESIAN_POINT('Ctrl Pts',(-34.0597429362493,-1.84961556123117,
126.247156942268));
#81816=CARTESIAN_POINT('Ctrl Pts',(-34.0674892695146,-1.9767581369121,126.298759833696));
#81817=CARTESIAN_POINT('Ctrl Pts',(-34.07523560278,-2.1017388025811,126.355687217268));
#81818=CARTESIAN_POINT('Ctrl Pts',(-34.0829819360453,-2.22408981447257,
126.417720951528));
#81819=CARTESIAN_POINT('Ctrl Pts',(-34.0907300040483,-2.34646822602566,
126.479768577813));
#81820=CARTESIAN_POINT('Ctrl Pts',(-34.0984780720513,-2.46621546333353,
126.546924653518));
#81821=CARTESIAN_POINT('Ctrl Pts',(-34.1062261400543,-2.58288840123231,
126.618925088343));
#81822=CARTESIAN_POINT('Ctrl Pts',(-34.1139824427961,-2.6996853405176,126.691002046087));
#81823=CARTESIAN_POINT('Ctrl Pts',(-34.121738745538,-2.8134011201641,126.767933442271));
#81824=CARTESIAN_POINT('Ctrl Pts',(-34.1294950482799,-2.92362118286983,
126.84941153552));
#81825=CARTESIAN_POINT('Ctrl Pts',(-34.1372554907941,-3.03390007334213,
126.930933116082));
#81826=CARTESIAN_POINT('Ctrl Pts',(-34.1450159333082,-3.14067922493189,
127.017005983891));
#81827=CARTESIAN_POINT('Ctrl Pts',(-34.1527763758224,-3.24357800475732,
127.107282745847));
#81828=CARTESIAN_POINT('Ctrl Pts',(-34.1605492760878,-3.34664196683876,
127.197704428075));
#81829=CARTESIAN_POINT('Ctrl Pts',(-34.1683221763533,-3.44581282639051,
127.292343219961));
#81830=CARTESIAN_POINT('Ctrl Pts',(-34.1760950766187,-3.5407469646873,127.390814954394));
#81831=CARTESIAN_POINT('Ctrl Pts',(-34.1835854123808,-3.6322300079326,127.485706993246));
#81832=CARTESIAN_POINT('Ctrl Pts',(-34.1910757481428,-3.71977880834725,
127.584157908433));
#81833=CARTESIAN_POINT('Ctrl Pts',(-34.1985660839049,-3.80312307725695,
127.68579717878));
#81834=CARTESIAN_POINT('Ctrl Pts',(-34.206310538568,-3.88929490352841,127.79088468703));
#81835=CARTESIAN_POINT('Ctrl Pts',(-34.2140549932311,-3.97125274011145,
127.899723368308));
#81836=CARTESIAN_POINT('Ctrl Pts',(-34.2217994478943,-4.04865008092329,
128.011939520249));
#81837=CARTESIAN_POINT('Ctrl Pts',(-34.2295343293618,-4.12595174813202,
128.124016957818));
#81838=CARTESIAN_POINT('Ctrl Pts',(-34.2372692108293,-4.19870391135565,
128.239463240276));
#81839=CARTESIAN_POINT('Ctrl Pts',(-34.2450040922969,-4.26659920068892,
128.357870412562));
#81840=CARTESIAN_POINT('Ctrl Pts',(-34.252729512362,-4.33441143966738,128.476132747735));
#81841=CARTESIAN_POINT('Ctrl Pts',(-34.2604549324272,-4.39737844007198,
128.597348421123));
#81842=CARTESIAN_POINT('Ctrl Pts',(-34.2681803524924,-4.45523560581082,
128.721079849351));
#81843=CARTESIAN_POINT('Ctrl Pts',(-34.2759003324996,-4.51305202990301,
128.844724148836));
#81844=CARTESIAN_POINT('Ctrl Pts',(-34.2836203125069,-4.56576561011797,
128.970880324095));
#81845=CARTESIAN_POINT('Ctrl Pts',(-34.2913402925141,-4.61315724699001,
129.099085485207));
#81846=CARTESIAN_POINT('Ctrl Pts',(-34.299056110084,-4.66052333137096,129.227221521015));
#81847=CARTESIAN_POINT('Ctrl Pts',(-34.3067719276538,-4.70257304827278,
129.357403974628));
#81848=CARTESIAN_POINT('Ctrl Pts',(-34.3144877452236,-4.73913529537912,
129.489149716383));
#81849=CARTESIAN_POINT('Ctrl Pts',(-34.3163049875457,-4.74774649726812,
129.520178694907));
#81850=CARTESIAN_POINT('Ctrl Pts',(-34.3181222298679,-4.7560535205127,129.551294311635));
#81851=CARTESIAN_POINT('Ctrl Pts',(-34.31993947219,-4.764054528234,129.582490119308));
#81852=CARTESIAN_POINT('Origin',(213.235140564004,0.,130.804360617566));
#81853=CARTESIAN_POINT('',(-36.4152663115527,-4.76405452823401,129.582490119308));
#81854=CARTESIAN_POINT('',(-36.0696835869212,-4.76181538791775,129.583090555045));
#81855=CARTESIAN_POINT('',(213.235140564004,-4.76405452823405,129.582490119308));
#81856=CARTESIAN_POINT('',(-34.7351405639796,-4.91824999933744,130.804441346932));
#81857=CARTESIAN_POINT('Ctrl Pts',(-34.7351405640085,-4.91824999933744,
130.804441347438));
#81858=CARTESIAN_POINT('Ctrl Pts',(-34.7353844877961,-4.91824992907732,
130.808721755457));
#81859=CARTESIAN_POINT('Ctrl Pts',(-34.7356284115836,-4.91824427088825,
130.813002158059));
#81860=CARTESIAN_POINT('Ctrl Pts',(-34.7358723353711,-4.91823302480335,
130.817282545971));
#81861=CARTESIAN_POINT('Ctrl Pts',(-34.7436466694902,-4.91787458980837,
130.953706984666));
#81862=CARTESIAN_POINT('Ctrl Pts',(-34.7514210036093,-4.91183497002536,
131.090332584922));
#81863=CARTESIAN_POINT('Ctrl Pts',(-34.7591953377284,-4.90008745949622,
131.226647192995));
#81864=CARTESIAN_POINT('Ctrl Pts',(-34.7669600906755,-4.8883544267239,131.362793805497));
#81865=CARTESIAN_POINT('Ctrl Pts',(-34.7747248436226,-4.87092753294101,
131.498629802626));
#81866=CARTESIAN_POINT('Ctrl Pts',(-34.7824895965697,-4.84783205185145,
131.633641908529));
#81867=CARTESIAN_POINT('Ctrl Pts',(-34.7902466374547,-4.82475950951933,
131.768519918505));
#81868=CARTESIAN_POINT('Ctrl Pts',(-34.7980036783397,-4.79602964957033,
131.902575282835));
#81869=CARTESIAN_POINT('Ctrl Pts',(-34.8057607192247,-4.76171959945346,
132.035299088279));
#81870=CARTESIAN_POINT('Ctrl Pts',(-34.8135119104649,-4.72743542281228,
132.167922805668));
#81871=CARTESIAN_POINT('Ctrl Pts',(-34.8212631017049,-4.6875795293558,132.299216585858));
#81872=CARTESIAN_POINT('Ctrl Pts',(-34.8290142929451,-4.64228018581905,
132.428681318306));
#81873=CARTESIAN_POINT('Ctrl Pts',(-34.8367621897222,-4.59700009571163,
132.558091024789));
#81874=CARTESIAN_POINT('Ctrl Pts',(-34.8445100864992,-4.54628128597217,
132.685672861454));
#81875=CARTESIAN_POINT('Ctrl Pts',(-34.8522579832763,-4.49030191842068,
132.810942722522));
#81876=CARTESIAN_POINT('Ctrl Pts',(-34.8600042593604,-4.43433426054609,
132.936186379835));
#81877=CARTESIAN_POINT('Ctrl Pts',(-34.8677505354446,-4.3731083930137,133.059118666768));
#81878=CARTESIAN_POINT('Ctrl Pts',(-34.8754968115287,-4.30685052703,133.179275689799));
#81879=CARTESIAN_POINT('Ctrl Pts',(-34.883243144794,-4.24059217194589,133.299433599802));
#81880=CARTESIAN_POINT('Ctrl Pts',(-34.8909894780594,-4.16930193307872,
133.416815862661));
#81881=CARTESIAN_POINT('Ctrl Pts',(-34.8987358113247,-4.09325166966457,
133.530983772916));
#81882=CARTESIAN_POINT('Ctrl Pts',(-34.9064838793277,-4.01718437532132,
133.645177250282));
#81883=CARTESIAN_POINT('Ctrl Pts',(-34.9142319473306,-3.93635515197055,
133.756154617341));
#81884=CARTESIAN_POINT('Ctrl Pts',(-34.9219800153336,-3.85107857841109,
133.863507041882));
#81885=CARTESIAN_POINT('Ctrl Pts',(-34.9297363180754,-3.76571137189434,
133.970973561857));
#81886=CARTESIAN_POINT('Ctrl Pts',(-34.9374926208173,-3.67588761665074,
134.074807136645));
#81887=CARTESIAN_POINT('Ctrl Pts',(-34.9452489235591,-3.5819618629107,134.174632457515));
#81888=CARTESIAN_POINT('Ctrl Pts',(-34.9530093660733,-3.48798597816771,
134.274511058165));
#81889=CARTESIAN_POINT('Ctrl Pts',(-34.9607698085874,-3.38990401190089,
134.370376868964));
#81890=CARTESIAN_POINT('Ctrl Pts',(-34.9685302511016,-3.2881058817618,134.46189295137));
#81891=CARTESIAN_POINT('Ctrl Pts',(-34.976303151367,-3.186144336227,134.553555943516));
#81892=CARTESIAN_POINT('Ctrl Pts',(-34.9840760516325,-3.08045500742379,
134.640855004742));
#81893=CARTESIAN_POINT('Ctrl Pts',(-34.9918489518979,-2.9714599579233,134.723494294918));
#81894=CARTESIAN_POINT('Ctrl Pts',(-34.99933928766,-2.86642715301413,134.803129438741));
#81895=CARTESIAN_POINT('Ctrl Pts',(-35.006829623422,-2.75832504999342,134.878437542406));
#81896=CARTESIAN_POINT('Ctrl Pts',(-35.014319959184,-2.6475535000912,134.949193970869));
#81897=CARTESIAN_POINT('Ctrl Pts',(-35.0220942933031,-2.53258201320617,
135.022633150823));
#81898=CARTESIAN_POINT('Ctrl Pts',(-35.0298686274221,-2.4143704642541,135.091401321853));
#81899=CARTESIAN_POINT('Ctrl Pts',(-35.0376429615412,-2.29333530746205,
135.155199183871));
#81900=CARTESIAN_POINT('Ctrl Pts',(-35.0454077144883,-2.17244931568352,
135.218918420726));
#81901=CARTESIAN_POINT('Ctrl Pts',(-35.0531724674355,-2.04874698245789,
135.277679355858));
#81902=CARTESIAN_POINT('Ctrl Pts',(-35.0609372203826,-1.92267380235278,
135.331225814614));
#81903=CARTESIAN_POINT('Ctrl Pts',(-35.0686942612676,-1.79672583990764,
135.384719090272));
#81904=CARTESIAN_POINT('Ctrl Pts',(-35.0764513021525,-1.66841207418315,
135.43300804433));
#81905=CARTESIAN_POINT('Ctrl Pts',(-35.0842083430375,-1.53820235757236,
135.475882486257));
#81906=CARTESIAN_POINT('Ctrl Pts',(-35.0919595342776,-1.40809083312157,
135.518724596234));
#81907=CARTESIAN_POINT('Ctrl Pts',(-35.0997107255179,-1.27608657346729,
135.556160199513));
#81908=CARTESIAN_POINT('Ctrl Pts',(-35.107461916758,-1.1426788257471,135.588027429091));
#81909=CARTESIAN_POINT('Ctrl Pts',(-35.1152098135351,-1.00932777987864,
135.619881114247));
#81910=CARTESIAN_POINT('Ctrl Pts',(-35.122957710312,-0.874574811847501,
135.646171042259));
#81911=CARTESIAN_POINT('Ctrl Pts',(-35.1307056070891,-0.738923514371043,
135.666785434713));
#81912=CARTESIAN_POINT('Ctrl Pts',(-35.1384518831732,-0.603300592221713,
135.687395515081));
#81913=CARTESIAN_POINT('Ctrl Pts',(-35.1461981592574,-0.466780100675269,
135.702332362595));
#81914=CARTESIAN_POINT('Ctrl Pts',(-35.1539444353415,-0.329874599172941,
135.711535549369));
#81915=CARTESIAN_POINT('Ctrl Pts',(-35.1616907686068,-0.192968087065114,
135.72073880408));
#81916=CARTESIAN_POINT('Ctrl Pts',(-35.1694371018721,-0.0556769494151028,
135.724208287373));
#81917=CARTESIAN_POINT('Ctrl Pts',(-35.1771834351375,0.0814827718919483,
135.721935591106));
#81918=CARTESIAN_POINT('Ctrl Pts',(-35.1849315031405,0.218673209167401,
135.719662385884));
#81919=CARTESIAN_POINT('Ctrl Pts',(-35.1926795711435,0.355731780701311,
135.711644448745));
#81920=CARTESIAN_POINT('Ctrl Pts',(-35.2004276391465,0.492144486851199,
135.697925459944));
#81921=CARTESIAN_POINT('Ctrl Pts',(-35.2081839418883,0.628702174048701,
135.684191890439));
#81922=CARTESIAN_POINT('Ctrl Pts',(-35.2159402446302,0.764612235014296,
135.664745204661));
#81923=CARTESIAN_POINT('Ctrl Pts',(-35.223696547372,0.899367268822977,135.639680832223));
#81924=CARTESIAN_POINT('Ctrl Pts',(-35.2314569898862,1.0341942254506,135.614603082175));
#81925=CARTESIAN_POINT('Ctrl Pts',(-35.2392174324004,1.16786454568972,135.583901758519));
#81926=CARTESIAN_POINT('Ctrl Pts',(-35.2469778749146,1.29988399358569,135.547722786505));
#81927=CARTESIAN_POINT('Ctrl Pts',(-35.25475077518,1.43211537081956,135.511485736793));
#81928=CARTESIAN_POINT('Ctrl Pts',(-35.2625236754455,1.5626902072905,135.469753586184));
#81929=CARTESIAN_POINT('Ctrl Pts',(-35.2702965757109,1.69113146918927,135.422721519057));
#81930=CARTESIAN_POINT('Ctrl Pts',(-35.2777869114729,1.81490356769382,135.377399186036));
#81931=CARTESIAN_POINT('Ctrl Pts',(-35.2852772472349,1.93669423536678,135.327155694687));
#81932=CARTESIAN_POINT('Ctrl Pts',(-35.2927675829969,2.05609835102641,135.272206030448));
#81933=CARTESIAN_POINT('Ctrl Pts',(-35.300541917116,2.18002971002338,135.215172932986));
#81934=CARTESIAN_POINT('Ctrl Pts',(-35.308316251235,2.30178254961261,135.152889085126));
#81935=CARTESIAN_POINT('Ctrl Pts',(-35.3160905853541,2.42087995647165,135.085543082593));
#81936=CARTESIAN_POINT('Ctrl Pts',(-35.3238553383012,2.53983058642062,135.018280077989));
#81937=CARTESIAN_POINT('Ctrl Pts',(-35.3316200912483,2.65613195804929,134.94596752237));
#81938=CARTESIAN_POINT('Ctrl Pts',(-35.3393848441954,2.76932774367032,134.868841754272));
#81939=CARTESIAN_POINT('Ctrl Pts',(-35.3471418850803,2.8824111016413,134.791792588574));
#81940=CARTESIAN_POINT('Ctrl Pts',(-35.3548989259652,2.99239469091629,134.709939942627));
#81941=CARTESIAN_POINT('Ctrl Pts',(-35.3626559668502,3.09884770555388,134.62356550344));
#81942=CARTESIAN_POINT('Ctrl Pts',(-35.3704071580904,3.20522044314504,134.537256199889));
#81943=CARTESIAN_POINT('Ctrl Pts',(-35.3781583493305,3.30806760314114,134.446432135675));
#81944=CARTESIAN_POINT('Ctrl Pts',(-35.3859095405706,3.40698855222042,134.351417435202));
#81945=CARTESIAN_POINT('Ctrl Pts',(-35.3936574373477,3.50586745725754,134.256443118512));
#81946=CARTESIAN_POINT('Ctrl Pts',(-35.4014053341248,3.60082318900819,134.157281978362));
#81947=CARTESIAN_POINT('Ctrl Pts',(-35.4091532309019,3.69148950096306,134.054297282607));
#81948=CARTESIAN_POINT('Ctrl Pts',(-35.4168995069859,3.78213684748001,133.95133412903));
#81949=CARTESIAN_POINT('Ctrl Pts',(-35.4246457830701,3.86849630070615,133.844549303965));
#81950=CARTESIAN_POINT('Ctrl Pts',(-35.4323920591542,3.95023997005212,133.734341375438));
#81951=CARTESIAN_POINT('Ctrl Pts',(-35.4401383924195,4.03198424281128,133.624132633381));
#81952=CARTESIAN_POINT('Ctrl Pts',(-35.4478847256848,4.10911243078851,133.510501051456));
#81953=CARTESIAN_POINT('Ctrl Pts',(-35.4556310589501,4.18133852673198,133.39387624551));
#81954=CARTESIAN_POINT('Ctrl Pts',(-35.4633791269531,4.25358079720886,133.277225322247));
#81955=CARTESIAN_POINT('Ctrl Pts',(-35.471127194956,4.3209185853696,133.157580173443));
#81956=CARTESIAN_POINT('Ctrl Pts',(-35.478875262959,4.38311081128926,133.035396851799));
#81957=CARTESIAN_POINT('Ctrl Pts',(-35.4866315657008,4.44536913584672,132.913083672267));
#81958=CARTESIAN_POINT('Ctrl Pts',(-35.4943878684427,4.50247079608237,132.788227280129));
#81959=CARTESIAN_POINT('Ctrl Pts',(-35.5021441711845,4.55422181703875,132.661306148191));
#81960=CARTESIAN_POINT('Ctrl Pts',(-35.5099046136987,4.60600045907328,132.534317274624));
#81961=CARTESIAN_POINT('Ctrl Pts',(-35.5176650562128,4.65242263914321,132.405261833109));
#81962=CARTESIAN_POINT('Ctrl Pts',(-35.525425498727,4.69334398168834,132.274634514515));
#81963=CARTESIAN_POINT('Ctrl Pts',(-35.5331983989924,4.73433101480536,132.143797501353));
#81964=CARTESIAN_POINT('Ctrl Pts',(-35.5409712992579,4.76979946316274,132.01138394659));
#81965=CARTESIAN_POINT('Ctrl Pts',(-35.5487441995233,4.79965569247943,131.877900694205));
#81966=CARTESIAN_POINT('Ctrl Pts',(-35.5562345352855,4.82842657265772,131.749269894265));
#81967=CARTESIAN_POINT('Ctrl Pts',(-35.5637248710476,4.85198613119707,131.619646121919));
#81968=CARTESIAN_POINT('Ctrl Pts',(-35.5712152068098,4.87029626353875,131.48948642197));
#81969=CARTESIAN_POINT('Ctrl Pts',(-35.5789895409288,4.88930063011309,131.354391677439));
#81970=CARTESIAN_POINT('Ctrl Pts',(-35.586763875048,4.90270984871404,131.218291624136));
#81971=CARTESIAN_POINT('Ctrl Pts',(-35.5945382091671,4.91042480696855,131.081689443345));
#81972=CARTESIAN_POINT('Ctrl Pts',(-35.6023029621142,4.91813025722651,130.945255612533));
#81973=CARTESIAN_POINT('Ctrl Pts',(-35.6100677150612,4.92015538836963,130.80832127211));
#81974=CARTESIAN_POINT('Ctrl Pts',(-35.6178324680083,4.91645238244269,130.671398090237));
#81975=CARTESIAN_POINT('Ctrl Pts',(-35.6255895088933,4.91275305439344,130.534610902399));
#81976=CARTESIAN_POINT('Ctrl Pts',(-35.6333465497784,4.90333692167235,130.397835239348));
#81977=CARTESIAN_POINT('Ctrl Pts',(-35.6411035906634,4.88820811440373,130.261585809034));
#81978=CARTESIAN_POINT('Ctrl Pts',(-35.6488547819035,4.87309071588636,130.125439125474));
#81979=CARTESIAN_POINT('Ctrl Pts',(-35.6566059731437,4.85226926055118,129.989818271777));
#81980=CARTESIAN_POINT('Ctrl Pts',(-35.6643571643838,4.82579989134293,129.855235509261));
#81981=CARTESIAN_POINT('Ctrl Pts',(-35.6721050611609,4.79934177232264,129.720709948009));
#81982=CARTESIAN_POINT('Ctrl Pts',(-35.6798529579379,4.76724058915932,129.587221983205));
#81983=CARTESIAN_POINT('Ctrl Pts',(-35.687600854715,4.72960400420158,129.455276103556));
#81984=CARTESIAN_POINT('Ctrl Pts',(-35.6953471307991,4.69197529200606,129.323357824142));
#81985=CARTESIAN_POINT('Ctrl Pts',(-35.7030934068832,4.6488135882908,129.192981364004));
#81986=CARTESIAN_POINT('Ctrl Pts',(-35.7108396829673,4.60027698675157,129.064638022534));
#81987=CARTESIAN_POINT('Ctrl Pts',(-35.7185860162327,4.55174002692618,128.936293733664));
#81988=CARTESIAN_POINT('Ctrl Pts',(-35.7263323494981,4.49782822840101,128.809982959098));
#81989=CARTESIAN_POINT('Ctrl Pts',(-35.7340786827635,4.43874844524977,128.686178542698));
#81990=CARTESIAN_POINT('Ctrl Pts',(-35.7418267507664,4.37965543159079,128.562346401157));
#81991=CARTESIAN_POINT('Ctrl Pts',(-35.7495748187694,4.31539229869233,128.441022087448));
#81992=CARTESIAN_POINT('Ctrl Pts',(-35.7573228867724,4.24621242702055,128.322654936564));
#81993=CARTESIAN_POINT('Ctrl Pts',(-35.7650791895143,4.17695903015782,128.204161983664));
#81994=CARTESIAN_POINT('Ctrl Pts',(-35.7728354922561,4.10277865347802,128.088632809967));
#81995=CARTESIAN_POINT('Ctrl Pts',(-35.780591794998,4.02396900150094,127.976489238338));
#81996=CARTESIAN_POINT('Ctrl Pts',(-35.7883522375122,3.94511728643959,127.864285812307));
#81997=CARTESIAN_POINT('Ctrl Pts',(-35.7961126800264,3.86163161070525,127.755471898977));
#81998=CARTESIAN_POINT('Ctrl Pts',(-35.8038731225406,3.77385013321886,127.650436358091));
#81999=CARTESIAN_POINT('Ctrl Pts',(-35.811646022806,3.68592774111206,127.545232204831));
#82000=CARTESIAN_POINT('Ctrl Pts',(-35.8194189230713,3.59369603004515,127.443818833979));
#82001=CARTESIAN_POINT('Ctrl Pts',(-35.8271918233368,3.49753081059526,127.346548984258));
#82002=CARTESIAN_POINT('Ctrl Pts',(-35.8346821590988,3.40486143909886,127.252815138584));
#82003=CARTESIAN_POINT('Ctrl Pts',(-35.8421724948608,3.30853980515541,127.162928999557));
#82004=CARTESIAN_POINT('Ctrl Pts',(-35.8496628306227,3.20892983705715,127.0771696695));
#82005=CARTESIAN_POINT('Ctrl Pts',(-35.8574371647418,3.10554312674165,126.988158748378));
#82006=CARTESIAN_POINT('Ctrl Pts',(-35.8652114988609,2.99828630753648,126.903311789761));
#82007=CARTESIAN_POINT('Ctrl Pts',(-35.87298583298,2.88752914744693,126.822984161471));
#82008=CARTESIAN_POINT('Ctrl Pts',(-35.8807505859271,2.77690848565869,126.742755529804));
#82009=CARTESIAN_POINT('Ctrl Pts',(-35.8885153388742,2.66279637972862,126.667035373814));
#82010=CARTESIAN_POINT('Ctrl Pts',(-35.8962800918213,2.54559746379843,126.596140493238));
#82011=CARTESIAN_POINT('Ctrl Pts',(-35.9040371327063,2.42851495148375,126.525316026456));
#82012=CARTESIAN_POINT('Ctrl Pts',(-35.9117941735913,2.30835206273338,126.459307498783));
#82013=CARTESIAN_POINT('Ctrl Pts',(-35.9195512144763,2.1855440683549,126.398389647646));
#82014=CARTESIAN_POINT('Ctrl Pts',(-35.9273024057165,2.06282868444028,126.337517735134));
#82015=CARTESIAN_POINT('Ctrl Pts',(-35.9350535969566,1.93747251404203,126.281729031055));
#82016=CARTESIAN_POINT('Ctrl Pts',(-35.9428047881967,1.80993688374789,126.231253190515));
#82017=CARTESIAN_POINT('Ctrl Pts',(-35.9505526849738,1.68245545949875,126.180798803553));
#82018=CARTESIAN_POINT('Ctrl Pts',(-35.958300581751,1.55279678051847,126.1356529325));
#82019=CARTESIAN_POINT('Ctrl Pts',(-35.9660484785281,1.42144348157484,126.095997686441));
#82020=CARTESIAN_POINT('Ctrl Pts',(-35.9737947546122,1.29011765890953,126.056350735405));
#82021=CARTESIAN_POINT('Ctrl Pts',(-35.9815410306963,1.15709829540054,126.022192237817));
#82022=CARTESIAN_POINT('Ctrl Pts',(-35.9892873067804,1.02288418864571,125.993654744296));
#82023=CARTESIAN_POINT('Ctrl Pts',(-35.9970336400458,0.888669091153008,
125.965117040117));
#82024=CARTESIAN_POINT('Ctrl Pts',(-36.0047799733111,0.753259615232364,
125.942200504113));
#82025=CARTESIAN_POINT('Ctrl Pts',(-36.0125263065764,0.617165387494643,
125.924986687749));
#82026=CARTESIAN_POINT('Ctrl Pts',(-36.0202743745794,0.48104068239823,125.90776901647));
#82027=CARTESIAN_POINT('Ctrl Pts',(-36.0280224425825,0.344231308145707,
125.896256655134));
#82028=CARTESIAN_POINT('Ctrl Pts',(-36.0357705105855,0.207252261324314,
125.890479304116));
#82029=CARTESIAN_POINT('Ctrl Pts',(-36.0435268133273,0.0701276315418873,
125.88469581286));
#82030=CARTESIAN_POINT('Ctrl Pts',(-36.0512831160691,-0.0671666397972779,
125.884659524318));
#82031=CARTESIAN_POINT('Ctrl Pts',(-36.059039418811,-0.204114744606161,
125.890347976808));
#82032=CARTESIAN_POINT('Ctrl Pts',(-36.0667998613252,-0.341135942742196,
125.896039465395));
#82033=CARTESIAN_POINT('Ctrl Pts',(-36.0745603038393,-0.477810216782652,
125.907461750745));
#82034=CARTESIAN_POINT('Ctrl Pts',(-36.0823207463535,-0.61362762485381,
125.92454051837));
#82035=CARTESIAN_POINT('Ctrl Pts',(-36.0900936466189,-0.749663059085706,
125.94164670235));
#82036=CARTESIAN_POINT('Ctrl Pts',(-36.0978665468844,-0.884838492875758,
125.964427448903));
#82037=CARTESIAN_POINT('Ctrl Pts',(-36.1056394471499,-1.01865402234965,
125.992757241845));
#82038=CARTESIAN_POINT('Ctrl Pts',(-36.1131297829118,-1.1476050202642,126.020057175454));
#82039=CARTESIAN_POINT('Ctrl Pts',(-36.1206201186737,-1.27529297066829,
126.052509640326));
#82040=CARTESIAN_POINT('Ctrl Pts',(-36.1281104544356,-1.40128634474042,
126.089959314904));
#82041=CARTESIAN_POINT('Ctrl Pts',(-36.1358847885547,-1.53205679588701,
126.128828905276));
#82042=CARTESIAN_POINT('Ctrl Pts',(-36.1436591226738,-1.66141587583529,
126.17320525131));
#82043=CARTESIAN_POINT('Ctrl Pts',(-36.1514334567928,-1.78886473493432,
126.222969341697));
#82044=CARTESIAN_POINT('Ctrl Pts',(-36.1591982097399,-1.91615652470476,
126.27267210229));
#82045=CARTESIAN_POINT('Ctrl Pts',(-36.166962962687,-2.04154241704425,126.327749254951));
#82046=CARTESIAN_POINT('Ctrl Pts',(-36.1747277156341,-2.1645371647229,126.388031607513));
#82047=CARTESIAN_POINT('Ctrl Pts',(-36.1824847565191,-2.28740975228439,
126.448254086793));
#82048=CARTESIAN_POINT('Ctrl Pts',(-36.1902417974041,-2.40789557258581,
126.513671306734));
#82049=CARTESIAN_POINT('Ctrl Pts',(-36.1979988382891,-2.52552820674429,
126.584065563966));
#82050=CARTESIAN_POINT('Ctrl Pts',(-36.2057500295292,-2.64307213321831,
126.654406736342));
#82051=CARTESIAN_POINT('Ctrl Pts',(-36.2135012207693,-2.75776682207294,
126.7297172755));
#82052=CARTESIAN_POINT('Ctrl Pts',(-36.2212524120094,-2.86916969967449,
126.80973318851));
#82053=CARTESIAN_POINT('Ctrl Pts',(-36.2290003087865,-2.98052522808114,
126.889715092622));
#82054=CARTESIAN_POINT('Ctrl Pts',(-36.2367482055636,-3.08859141107396,
126.974398165319));
#82055=CARTESIAN_POINT('Ctrl Pts',(-36.2444961023407,-3.19295415923958,
127.063474786711));
#82056=CARTESIAN_POINT('Ctrl Pts',(-36.2522423784248,-3.29729507696807,
127.152532775193));
#82057=CARTESIAN_POINT('Ctrl Pts',(-36.2599886545088,-3.39793380356293,
127.245982230703));
#82058=CARTESIAN_POINT('Ctrl Pts',(-36.2677349305929,-3.49448920814908,
127.343475147541));
#82059=CARTESIAN_POINT('Ctrl Pts',(-36.2754812638583,-3.59104532548529,
127.44096878405));
#82060=CARTESIAN_POINT('Ctrl Pts',(-36.2832275971236,-3.68351778555101,
127.542505663659));
#82061=CARTESIAN_POINT('Ctrl Pts',(-36.290973930389,-3.77156251115694,127.647701103628));
#82062=CARTESIAN_POINT('Ctrl Pts',(-36.298721998392,-3.8596269537687,127.752920101386));
#82063=CARTESIAN_POINT('Ctrl Pts',(-36.3064700663949,-3.9432614379467,127.86179899008));
#82064=CARTESIAN_POINT('Ctrl Pts',(-36.3142181343979,-4.02216260768733,
127.973920542274));
#82065=CARTESIAN_POINT('Ctrl Pts',(-36.3219744371397,-4.1011476345301,128.086161258587));
#82066=CARTESIAN_POINT('Ctrl Pts',(-36.3297307398815,-4.17538907236613,
128.201651202597));
#82067=CARTESIAN_POINT('Ctrl Pts',(-36.3374870426233,-4.24462701197451,
128.319944269263));
#82068=CARTESIAN_POINT('Ctrl Pts',(-36.3452474851375,-4.31390190595607,
128.4383004725));
#82069=CARTESIAN_POINT('Ctrl Pts',(-36.3530079276517,-4.37816779736918,
128.559462434303));
#82070=CARTESIAN_POINT('Ctrl Pts',(-36.3607683701658,-4.43721157305724,
128.682960957335));
#82071=CARTESIAN_POINT('Ctrl Pts',(-36.3685412704313,-4.49635013105569,
128.806657731161));
#82072=CARTESIAN_POINT('Ctrl Pts',(-36.3763141706967,-4.55024966760307,
128.932698201938));
#82073=CARTESIAN_POINT('Ctrl Pts',(-36.3840870709621,-4.59874557276672,
129.060593941815));
#82074=CARTESIAN_POINT('Ctrl Pts',(-36.3915774067242,-4.64547852962464,
129.1838403494));
#82075=CARTESIAN_POINT('Ctrl Pts',(-36.3990677424864,-4.68719380797315,
129.308809188348));
#82076=CARTESIAN_POINT('Ctrl Pts',(-36.4065580782486,-4.72378883236707,
129.435053446145));
#82077=CARTESIAN_POINT('Ctrl Pts',(-36.4094608226833,-4.73797057358291,
129.483977129726));
#82078=CARTESIAN_POINT('Ctrl Pts',(-36.412363567118,-4.75139468639191,129.533129588106));
#82079=CARTESIAN_POINT('Ctrl Pts',(-36.4152663115528,-4.76405452823402,
129.582490119308));
#82080=CARTESIAN_POINT('Ctrl Pts',(-34.6650476268334,-4.76405452823403,
129.582490119308));
#82081=CARTESIAN_POINT('Ctrl Pts',(-34.6728041571113,-4.79811111157992,
129.715276220893));
#82082=CARTESIAN_POINT('Ctrl Pts',(-34.6805606873892,-4.82658522312024,
129.84938326537));
#82083=CARTESIAN_POINT('Ctrl Pts',(-34.688317217667,-4.84940066901136,129.984301952657));
#82084=CARTESIAN_POINT('Ctrl Pts',(-34.6961211087191,-4.87235542425136,
130.120044443019));
#82085=CARTESIAN_POINT('Ctrl Pts',(-34.7039249997712,-4.88958214057927,
130.256608121163));
#82086=CARTESIAN_POINT('Ctrl Pts',(-34.7117288908233,-4.90105633548391,
130.393471509761));
#82087=CARTESIAN_POINT('Ctrl Pts',(-34.7195327818754,-4.91253053038855,
130.530334898358));
#82088=CARTESIAN_POINT('Ctrl Pts',(-34.7273366729275,-4.91825224716583,
130.667497598343));
#82089=CARTESIAN_POINT('Ctrl Pts',(-34.7351405639796,-4.91824999933744,
130.804441346932));
#82090=CARTESIAN_POINT('',(-34.3898612108785,-4.91451134145429,130.808502671262));
#82091=CARTESIAN_POINT('Ctrl Pts',(-34.31993947219,-4.764054528234,129.582490119308));
#82092=CARTESIAN_POINT('Ctrl Pts',(-34.3276536921924,-4.79801892200384,
129.714916775135));
#82093=CARTESIAN_POINT('Ctrl Pts',(-34.3353679121948,-4.82646487016461,
129.848789404461));
#82094=CARTESIAN_POINT('Ctrl Pts',(-34.3430821321972,-4.84928307828942,
129.983606885247));
#82095=CARTESIAN_POINT('Ctrl Pts',(-34.3508783494962,-4.87234382958494,
130.119857390881));
#82096=CARTESIAN_POINT('Ctrl Pts',(-34.3586745667951,-4.88965640799597,
130.25707255254));
#82097=CARTESIAN_POINT('Ctrl Pts',(-34.3664707840941,-4.90116138148723,
130.394726420851));
#82098=CARTESIAN_POINT('Ctrl Pts',(-34.3742670013931,-4.91266635497847,
130.532380289162));
#82099=CARTESIAN_POINT('Ctrl Pts',(-34.3820632186921,-4.91836370896115,
130.670472449304));
#82100=CARTESIAN_POINT('Ctrl Pts',(-34.3898594359911,-4.9182482795467,130.808474403648));
#82101=CARTESIAN_POINT('Ctrl Pts',(-34.3898612383632,-4.91445347382228,
130.808503108995));
#82102=CARTESIAN_POINT('Ctrl Pts',(-34.4189120614814,-4.91848817089666,
131.322342766133));
#82103=CARTESIAN_POINT('Ctrl Pts',(-34.5407787592039,-4.6074576551442,133.47310541816));
#82104=CARTESIAN_POINT('Ctrl Pts',(-34.7554613315307,-1.48508419419027,
136.428967694209));
#82105=CARTESIAN_POINT('Ctrl Pts',(-35.0339089553435,3.92941694857211,135.094041523499));
#82106=CARTESIAN_POINT('Ctrl Pts',(-35.3123565791566,5.73297587828731,129.817108162799));
#82107=CARTESIAN_POINT('Ctrl Pts',(-35.5908042029694,2.26821004729653,125.447411578065));
#82108=CARTESIAN_POINT('Ctrl Pts',(-35.8432465388909,-2.7626746087458,125.948835401795));
#82109=CARTESIAN_POINT('Ctrl Pts',(-36.0028730002082,-4.45755648309024,
128.442094762146));
#82110=CARTESIAN_POINT('Ctrl Pts',(-36.0696835869212,-4.76181538791761,
129.583090555045));
#82111=CARTESIAN_POINT('Origin',(213.235140564004,0.,130.804360617566));
#82112=CARTESIAN_POINT('',(-38.1653731028237,-4.76405452823409,129.582490119308));
#82113=CARTESIAN_POINT('',(-37.8199424078995,-4.77192532739619,129.580475997939));
#82114=CARTESIAN_POINT('',(213.235140564004,-4.76405452823405,129.582490119308));
#82115=CARTESIAN_POINT('',(-36.4851405639765,-4.91824802675748,130.799954962542));
#82116=CARTESIAN_POINT('Ctrl Pts',(-36.4851405640085,-4.91824802675798,
130.799954963109));
#82117=CARTESIAN_POINT('Ctrl Pts',(-36.4928276338665,-4.91836979410064,
130.935889816499));
#82118=CARTESIAN_POINT('Ctrl Pts',(-36.5005147037245,-4.91285169280305,
131.071941831601));
#82119=CARTESIAN_POINT('Ctrl Pts',(-36.5082017735825,-4.90169143817275,
131.207602613697));
#82120=CARTESIAN_POINT('Ctrl Pts',(-36.5158857677113,-4.89053564895279,
131.343209115575));
#82121=CARTESIAN_POINT('Ctrl Pts',(-36.5235697618401,-4.87374222681335,
131.478424299786));
#82122=CARTESIAN_POINT('Ctrl Pts',(-36.5312537559689,-4.85136095628237,
131.612741675211));
#82123=CARTESIAN_POINT('Ctrl Pts',(-36.538936339408,-4.82898379468568,131.747034391568));
#82124=CARTESIAN_POINT('Ctrl Pts',(-36.5466189228472,-4.80102088990743,
131.880429234494));
#82125=CARTESIAN_POINT('Ctrl Pts',(-36.5543015062863,-4.76757360973981,
132.012427229228));
#82126=CARTESIAN_POINT('Ctrl Pts',(-36.5619844103365,-4.7341249337437,132.144430732529));
#82127=CARTESIAN_POINT('Ctrl Pts',(-36.5696673143867,-4.69519152486053,
132.275036885866));
#82128=CARTESIAN_POINT('Ctrl Pts',(-36.5773502184369,-4.65092523053898,
132.403759742999));
#82129=CARTESIAN_POINT('Ctrl Pts',(-36.5850351743359,-4.60664711415884,
132.532516977737));
#82130=CARTESIAN_POINT('Ctrl Pts',(-36.592720130235,-4.55703340891382,132.659389539654));
#82131=CARTESIAN_POINT('Ctrl Pts',(-36.600405086134,-4.50228473464615,132.783909866934));
#82132=CARTESIAN_POINT('Ctrl Pts',(-36.6080983775956,-4.44747667669282,
132.908565256406));
#82133=CARTESIAN_POINT('Ctrl Pts',(-36.6157916690573,-4.38752268863135,
133.030862952023));
#82134=CARTESIAN_POINT('Ctrl Pts',(-36.623484960519,-4.32267032552709,133.150358128074));
#82135=CARTESIAN_POINT('Ctrl Pts',(-36.6311827738555,-4.25777984424232,
133.269923539632));
#82136=CARTESIAN_POINT('Ctrl Pts',(-36.638880587192,-4.18798545839921,133.386682810443));
#82137=CARTESIAN_POINT('Ctrl Pts',(-36.6465784005286,-4.11357834835301,
133.500219707812));
#82138=CARTESIAN_POINT('Ctrl Pts',(-36.6542880192234,-4.03905712764318,
133.613930725244));
#82139=CARTESIAN_POINT('Ctrl Pts',(-36.6619976379181,-3.95990928697845,
133.724409177488));
#82140=CARTESIAN_POINT('Ctrl Pts',(-36.6697072566129,-3.87646695557892,
133.831271089451));
#82141=CARTESIAN_POINT('Ctrl Pts',(-36.6748067384291,-3.82127451759782,
133.901954270872));
#82142=CARTESIAN_POINT('Ctrl Pts',(-36.6799062202452,-3.7642040135486,133.971055898711));
#82143=CARTESIAN_POINT('Ctrl Pts',(-36.6850057020614,-3.70536015296158,
134.038473973549));
#82144=CARTESIAN_POINT('Ctrl Pts',(-36.6927800361805,-3.61565067863599,
134.141255130212));
#82145=CARTESIAN_POINT('Ctrl Pts',(-36.7005543702996,-3.521519376323,134.240463645861));
#82146=CARTESIAN_POINT('Ctrl Pts',(-36.7083287044187,-3.423281844015,134.335695277286));
#82147=CARTESIAN_POINT('Ctrl Pts',(-36.7160934573658,-3.32516538068582,
134.430809544235));
#82148=CARTESIAN_POINT('Ctrl Pts',(-36.7238582103129,-3.22295303439132,
134.521956409283));
#82149=CARTESIAN_POINT('Ctrl Pts',(-36.73162296326,-3.11700038939506,134.608764859364));
#82150=CARTESIAN_POINT('Ctrl Pts',(-36.739380004145,-3.01115297805947,134.695487090068));
#82151=CARTESIAN_POINT('Ctrl Pts',(-36.74713704503,-2.90157296134098,134.777879234684));
#82152=CARTESIAN_POINT('Ctrl Pts',(-36.754894085915,-2.78865221894935,134.855607569339));
#82153=CARTESIAN_POINT('Ctrl Pts',(-36.7626452771551,-2.67581663096857,
134.933277288451));
#82154=CARTESIAN_POINT('Ctrl Pts',(-36.7703964683952,-2.55964565250498,
135.006289977227));
#82155=CARTESIAN_POINT('Ctrl Pts',(-36.7781476596353,-2.44056335273725,
135.074352840483));
#82156=CARTESIAN_POINT('Ctrl Pts',(-36.7858955564124,-2.32153166612289,
135.142386775207));
#82157=CARTESIAN_POINT('Ctrl Pts',(-36.7936434531895,-2.19959145799996,
135.205474875124));
#82158=CARTESIAN_POINT('Ctrl Pts',(-36.8013913499666,-2.0751946370679,135.263368386205));
#82159=CARTESIAN_POINT('Ctrl Pts',(-36.8091376260507,-1.95082383726926,
135.321249787212));
#82160=CARTESIAN_POINT('Ctrl Pts',(-36.8168839021347,-1.82399780101219,
135.373938595825));
#82161=CARTESIAN_POINT('Ctrl Pts',(-36.8246301782188,-1.69519146881032,
135.421232821404));
#82162=CARTESIAN_POINT('Ctrl Pts',(-36.8323765114841,-1.56638418578972,
135.468527396098));
#82163=CARTESIAN_POINT('Ctrl Pts',(-36.8401228447495,-1.43559694466283,
135.510427173542));
#82164=CARTESIAN_POINT('Ctrl Pts',(-36.8478691780148,-1.30332264235544,
135.546779109477));
#82165=CARTESIAN_POINT('Ctrl Pts',(-36.8556172460178,-1.17101871813535,
135.583139186177));
#82166=CARTESIAN_POINT('Ctrl Pts',(-36.8633653140207,-1.03722744698512,
135.613948845551));
#82167=CARTESIAN_POINT('Ctrl Pts',(-36.8711133820236,-0.902454399342149,
135.639105607698));
#82168=CARTESIAN_POINT('Ctrl Pts',(-36.8788696847655,-0.767538113299777,
135.664289106751));
#82169=CARTESIAN_POINT('Ctrl Pts',(-36.8866259875073,-0.631638351313373,
135.683807635165));
#82170=CARTESIAN_POINT('Ctrl Pts',(-36.8943822902492,-0.495268889113341,
135.697610232084));
#82171=CARTESIAN_POINT('Ctrl Pts',(-36.9021427327633,-0.358826642425143,
135.711420195864));
#82172=CARTESIAN_POINT('Ctrl Pts',(-36.9099031752775,-0.221914586089837,
135.719508126199));
#82173=CARTESIAN_POINT('Ctrl Pts',(-36.9176636177917,-0.0850480471087371,
135.721875222748));
#82174=CARTESIAN_POINT('Ctrl Pts',(-36.9254365180571,0.0520382021909894,
135.724246119172));
#82175=CARTESIAN_POINT('Ctrl Pts',(-36.9332094183226,0.189078397050262,
135.720877839682));
#82176=CARTESIAN_POINT('Ctrl Pts',(-36.940982318588,0.325559881160564,135.711823691933));
#82177=CARTESIAN_POINT('Ctrl Pts',(-36.9484726543501,0.457079919549005,
135.703098685261));
#82178=CARTESIAN_POINT('Ctrl Pts',(-36.9559629901122,0.588080856759524,
135.689094057259));
#82179=CARTESIAN_POINT('Ctrl Pts',(-36.9634533258743,0.718113490108519,
135.669902322024));
#82180=CARTESIAN_POINT('Ctrl Pts',(-36.9712276599934,0.853076350271984,
135.649982926316));
#82181=CARTESIAN_POINT('Ctrl Pts',(-36.9790019941125,0.987423552403778,
135.624412221754));
#82182=CARTESIAN_POINT('Ctrl Pts',(-36.9867763282316,1.12064440681875,135.593237226539));
#82183=CARTESIAN_POINT('Ctrl Pts',(-36.9945410811787,1.25370107843695,135.562100651719));
#82184=CARTESIAN_POINT('Ctrl Pts',(-37.0023058341258,1.38563378726269,135.525373616921));
#82185=CARTESIAN_POINT('Ctrl Pts',(-37.0100705870729,1.51593818751635,135.483154743634));
#82186=CARTESIAN_POINT('Ctrl Pts',(-37.0178276279579,1.64611316760271,135.440977802727));
#82187=CARTESIAN_POINT('Ctrl Pts',(-37.0255846688429,1.77466268801198,135.393319997899));
#82188=CARTESIAN_POINT('Ctrl Pts',(-37.0333417097279,1.90109415684289,135.340330642745));
#82189=CARTESIAN_POINT('Ctrl Pts',(-37.041092900968,2.02743028271915,135.287381247275));
#82190=CARTESIAN_POINT('Ctrl Pts',(-37.0488440922081,2.15165117710705,135.229108454678));
#82191=CARTESIAN_POINT('Ctrl Pts',(-37.0565952834482,2.27328128337633,135.165710783415));
#82192=CARTESIAN_POINT('Ctrl Pts',(-37.0643431802253,2.39485969360619,135.102340057853));
#82193=CARTESIAN_POINT('Ctrl Pts',(-37.0720910770023,2.51384915985902,135.033848966251));
#82194=CARTESIAN_POINT('Ctrl Pts',(-37.0798389737794,2.6297961306363,134.960483254567));
#82195=CARTESIAN_POINT('Ctrl Pts',(-37.0875852498635,2.74571884780682,134.887132889408));
#82196=CARTESIAN_POINT('Ctrl Pts',(-37.0953315259476,2.85860000521263,134.808910141256));
#82197=CARTESIAN_POINT('Ctrl Pts',(-37.1030778020317,2.96801294545895,134.726105410141));
#82198=CARTESIAN_POINT('Ctrl Pts',(-37.110824135297,3.07742669336659,134.64330006778));
#82199=CARTESIAN_POINT('Ctrl Pts',(-37.1185704685623,3.18337186127836,134.5559129109));
#82200=CARTESIAN_POINT('Ctrl Pts',(-37.1263168018276,3.28545326589827,134.464275903484));
#82201=CARTESIAN_POINT('Ctrl Pts',(-37.1340648698306,3.38755753094068,134.372618374597));
#82202=CARTESIAN_POINT('Ctrl Pts',(-37.1418129378335,3.48579602003702,134.276709362472));
#82203=CARTESIAN_POINT('Ctrl Pts',(-37.1495610058365,3.57980924077354,134.176918824947));
#82204=CARTESIAN_POINT('Ctrl Pts',(-37.1573173085783,3.67392237988009,134.077022228851));
#82205=CARTESIAN_POINT('Ctrl Pts',(-37.1650736113202,3.76380101151736,133.973236151585));
#82206=CARTESIAN_POINT('Ctrl Pts',(-37.172829914062,3.8491245525434,133.865965301634));
#82207=CARTESIAN_POINT('Ctrl Pts',(-37.1805903565762,3.93449363331256,133.758637198001));
#82208=CARTESIAN_POINT('Ctrl Pts',(-37.1883507990903,4.0153025488774,133.647820931359));
#82209=CARTESIAN_POINT('Ctrl Pts',(-37.1961112416045,4.09127376171465,133.533950709357));
#82210=CARTESIAN_POINT('Ctrl Pts',(-37.2038841418699,4.16736693028706,133.419897692766));
#82211=CARTESIAN_POINT('Ctrl Pts',(-37.2116570421354,4.23860667407224,133.302781258312));
#82212=CARTESIAN_POINT('Ctrl Pts',(-37.2194299424008,4.3047607390515,133.183061532356));
#82213=CARTESIAN_POINT('Ctrl Pts',(-37.2269202781629,4.36850993713755,133.067693919992));
#82214=CARTESIAN_POINT('Ctrl Pts',(-37.234410613925,4.42753665340542,132.94990927786));
#82215=CARTESIAN_POINT('Ctrl Pts',(-37.2419009496871,4.48167591756359,132.83013553903));
#82216=CARTESIAN_POINT('Ctrl Pts',(-37.2496752838062,4.53786788837688,132.705820542489));
#82217=CARTESIAN_POINT('Ctrl Pts',(-37.2574496179253,4.58897247479398,132.57896884601));
#82218=CARTESIAN_POINT('Ctrl Pts',(-37.2652239520444,4.63475319430905,132.450035521775));
#82219=CARTESIAN_POINT('Ctrl Pts',(-37.2729887049914,4.68047749317892,132.321261096338));
#82220=CARTESIAN_POINT('Ctrl Pts',(-37.2807534579385,4.72089085039618,132.190410512459));
#82221=CARTESIAN_POINT('Ctrl Pts',(-37.2885182108856,4.75580362779796,132.057961397848));
#82222=CARTESIAN_POINT('Ctrl Pts',(-37.2962752517706,4.79068172933704,131.925643833565));
#82223=CARTESIAN_POINT('Ctrl Pts',(-37.3040322926557,4.82007002417415,131.791731273717));
#82224=CARTESIAN_POINT('Ctrl Pts',(-37.3117893335407,4.84382787610935,131.656718857466));
#82225=CARTESIAN_POINT('Ctrl Pts',(-37.3195405247808,4.86756781206351,131.521808255129));
#82226=CARTESIAN_POINT('Ctrl Pts',(-37.3272917160209,4.88568568896112,131.385799830772));
#82227=CARTESIAN_POINT('Ctrl Pts',(-37.335042907261,4.89809147603133,131.249200987732));
#82228=CARTESIAN_POINT('Ctrl Pts',(-37.3427908040381,4.91049199031114,131.112660202844));
#82229=CARTESIAN_POINT('Ctrl Pts',(-37.3505387008151,4.91718520816626,130.975529886929));
#82230=CARTESIAN_POINT('Ctrl Pts',(-37.3582865975922,4.918132726969,130.838324457403));
#82231=CARTESIAN_POINT('Ctrl Pts',(-37.3660328736763,4.91908004757123,130.701147728295));
#82232=CARTESIAN_POINT('Ctrl Pts',(-37.3737791497605,4.91428405702093,130.563896307536));
#82233=CARTESIAN_POINT('Ctrl Pts',(-37.3815254258446,4.90375845834459,130.427086122385));
#82234=CARTESIAN_POINT('Ctrl Pts',(-37.3892717591099,4.89323278197069,130.290274927333));
#82235=CARTESIAN_POINT('Ctrl Pts',(-37.3970180923752,4.87697744306541,130.153905364202));
#82236=CARTESIAN_POINT('Ctrl Pts',(-37.4047644256406,4.85505812610579,130.018489346534));
#82237=CARTESIAN_POINT('Ctrl Pts',(-37.4125124936435,4.83313390046718,129.883043003387));
#82238=CARTESIAN_POINT('Ctrl Pts',(-37.4202605616464,4.80554323524706,129.74855101649));
#82239=CARTESIAN_POINT('Ctrl Pts',(-37.4280086296494,4.77240307202143,129.61551580824));
#82240=CARTESIAN_POINT('Ctrl Pts',(-37.4357649323912,4.7392276870358,129.482339208588));
#82241=CARTESIAN_POINT('Ctrl Pts',(-37.4435212351331,4.70049111666466,129.350622860418));
#82242=CARTESIAN_POINT('Ctrl Pts',(-37.4512775378749,4.65636057060059,129.220855234229));
#82243=CARTESIAN_POINT('Ctrl Pts',(-37.4590379803891,4.61220647073529,129.091018347152));
#82244=CARTESIAN_POINT('Ctrl Pts',(-37.4667984229033,4.56265279986055,128.963132618902));
#82245=CARTESIAN_POINT('Ctrl Pts',(-37.4745588654175,4.50791485335659,128.837666249499));
#82246=CARTESIAN_POINT('Ctrl Pts',(-37.4823317656829,4.45308903664149,128.711998470341));
#82247=CARTESIAN_POINT('Ctrl Pts',(-37.4901046659483,4.39306248506888,128.58875816273));
#82248=CARTESIAN_POINT('Ctrl Pts',(-37.4978775662137,4.32809677700681,128.468389438086));
#82249=CARTESIAN_POINT('Ctrl Pts',(-37.5053679019758,4.26549273607101,128.352396419772));
#82250=CARTESIAN_POINT('Ctrl Pts',(-37.512858237738,4.19830256276164,128.23907009553));
#82251=CARTESIAN_POINT('Ctrl Pts',(-37.5203485735001,4.12679711881795,128.128780567817));
#82252=CARTESIAN_POINT('Ctrl Pts',(-37.5281229076191,4.05258052423415,128.014309379139));
#82253=CARTESIAN_POINT('Ctrl Pts',(-37.5358972417382,3.97347987661718,127.902747202758));
#82254=CARTESIAN_POINT('Ctrl Pts',(-37.5436715758573,3.88975021651057,127.794538975731));
#82255=CARTESIAN_POINT('Ctrl Pts',(-37.5514363288044,3.80612374572714,127.686464105674));
#82256=CARTESIAN_POINT('Ctrl Pts',(-37.5592010817515,3.7178798503558,127.581735266892));
#82257=CARTESIAN_POINT('Ctrl Pts',(-37.5669658346985,3.62531786805777,127.480770176786));
#82258=CARTESIAN_POINT('Ctrl Pts',(-37.5747228755835,3.53284781962546,127.379905366632));
#82259=CARTESIAN_POINT('Ctrl Pts',(-37.5824799164686,3.43606848163346,127.282797152272));
#82260=CARTESIAN_POINT('Ctrl Pts',(-37.5902369573535,3.33532041138046,127.189831489736));
#82261=CARTESIAN_POINT('Ctrl Pts',(-37.5979881485937,3.23464831603053,127.09693593333));
#82262=CARTESIAN_POINT('Ctrl Pts',(-37.6057393398338,3.13001373167596,127.008176974815));
#82263=CARTESIAN_POINT('Ctrl Pts',(-37.6134905310739,3.02179488728543,126.923904623527));
#82264=CARTESIAN_POINT('Ctrl Pts',(-37.621238427851,2.91362203879075,126.839668090236));
#82265=CARTESIAN_POINT('Ctrl Pts',(-37.628986324628,2.80186826802107,126.759914611147));
#82266=CARTESIAN_POINT('Ctrl Pts',(-37.6367342214051,2.68694561135834,126.684954550655));
#82267=CARTESIAN_POINT('Ctrl Pts',(-37.6444804974892,2.57204699403793,126.610010170192));
#82268=CARTESIAN_POINT('Ctrl Pts',(-37.6522267735734,2.45398113654999,126.539857427399));
#82269=CARTESIAN_POINT('Ctrl Pts',(-37.6599730496575,2.33318950993037,126.474763664817));
#82270=CARTESIAN_POINT('Ctrl Pts',(-37.6677193829229,2.21239699165456,126.409669421728));
#82271=CARTESIAN_POINT('Ctrl Pts',(-37.6754657161882,2.08887900826863,126.34963441884));
#82272=CARTESIAN_POINT('Ctrl Pts',(-37.6832120494535,1.96310175119711,126.294880095716));
#82273=CARTESIAN_POINT('Ctrl Pts',(-37.6909601174565,1.83729632718076,126.24011351074));
#82274=CARTESIAN_POINT('Ctrl Pts',(-37.6987081854595,1.70923098110191,126.190630114731));
#82275=CARTESIAN_POINT('Ctrl Pts',(-37.7064562534625,1.57939162493083,126.146603093006));
#82276=CARTESIAN_POINT('Ctrl Pts',(-37.7142125562043,1.4494142739469,126.102529278838));
#82277=CARTESIAN_POINT('Ctrl Pts',(-37.7219688589462,1.31765951735152,126.063923549032));
#82278=CARTESIAN_POINT('Ctrl Pts',(-37.7297251616881,1.18462870013296,126.030909255572));
#82279=CARTESIAN_POINT('Ctrl Pts',(-37.7374856042022,1.05152688036194,125.99787734139));
#82280=CARTESIAN_POINT('Ctrl Pts',(-37.7452460467163,0.91714802575034,125.970442888229));
#82281=CARTESIAN_POINT('Ctrl Pts',(-37.7530064892305,0.782002418645201,
125.948677835533));
#82282=CARTESIAN_POINT('Ctrl Pts',(-37.7607793894959,0.646639863813688,
125.926877843642));
#82283=CARTESIAN_POINT('Ctrl Pts',(-37.7685522897614,0.510508485318408,
125.910765484945));
#82284=CARTESIAN_POINT('Ctrl Pts',(-37.7763251900268,0.374123316172745,
125.900360739222));
#82285=CARTESIAN_POINT('Ctrl Pts',(-37.7838155257889,0.242696091459036,
125.890334232215));
#82286=CARTESIAN_POINT('Ctrl Pts',(-37.7913058615508,0.111033515422634,
125.885607581543));
#82287=CARTESIAN_POINT('Ctrl Pts',(-37.7987961973129,-0.0204066268725122,
125.886152952971));
#82288=CARTESIAN_POINT('Ctrl Pts',(-37.806570531432,-0.156830362113137,
125.886719002323));
#82289=CARTESIAN_POINT('Ctrl Pts',(-37.8143448655511,-0.293446612885683,
125.892966536018));
#82290=CARTESIAN_POINT('Ctrl Pts',(-37.8221191996702,-0.429743185397317,
125.904921480572));
#82291=CARTESIAN_POINT('Ctrl Pts',(-37.8298839526173,-0.565871784564505,
125.916861691726));
#82292=CARTESIAN_POINT('Ctrl Pts',(-37.8376487055644,-0.701681103632381,
125.934495284593));
#82293=CARTESIAN_POINT('Ctrl Pts',(-37.8454134585115,-0.836657905802827,
125.95779620438));
#82294=CARTESIAN_POINT('Ctrl Pts',(-37.8531704993965,-0.971500647110885,
125.981073981366));
#82295=CARTESIAN_POINT('Ctrl Pts',(-37.8609275402815,-1.1055121342515,126.01000781749));
#82296=CARTESIAN_POINT('Ctrl Pts',(-37.8686845811665,-1.23818357194774,
126.044519810915));
#82297=CARTESIAN_POINT('Ctrl Pts',(-37.8764357724066,-1.37075496107898,
126.079005778577));
#82298=CARTESIAN_POINT('Ctrl Pts',(-37.8841869636466,-1.50198793534603,
126.119061432664));
#82299=CARTESIAN_POINT('Ctrl Pts',(-37.8919381548866,-1.63138357998536,
126.164557747028));
#82300=CARTESIAN_POINT('Ctrl Pts',(-37.8996860516637,-1.76072422802539,
126.210034724245));
#82301=CARTESIAN_POINT('Ctrl Pts',(-37.9074339484408,-1.88822873155778,
126.26094763309));
#82302=CARTESIAN_POINT('Ctrl Pts',(-37.9151818452179,-2.01341325649687,
126.317117575222));
#82303=CARTESIAN_POINT('Ctrl Pts',(-37.922928121302,-2.13857159553202,126.373275767813));
#82304=CARTESIAN_POINT('Ctrl Pts',(-37.9306743973861,-2.26141056476401,
126.434688646461));
#82305=CARTESIAN_POINT('Ctrl Pts',(-37.9384206734702,-2.38146661546252,
126.501129294254));
#82306=CARTESIAN_POINT('Ctrl Pts',(-37.9461670067355,-2.50152355238737,
126.567570432496));
#82307=CARTESIAN_POINT('Ctrl Pts',(-37.9539133400008,-2.61879718771126,
126.639039224632));
#82308=CARTESIAN_POINT('Ctrl Pts',(-37.9616596732662,-2.73284923020659,
126.715263144106));
#82309=CARTESIAN_POINT('Ctrl Pts',(-37.9694077412691,-2.84692681386574,
126.791504133397));
#82310=CARTESIAN_POINT('Ctrl Pts',(-37.9771558092721,-2.95778104409628,
126.87250215181));
#82311=CARTESIAN_POINT('Ctrl Pts',(-37.9849038772751,-3.06500356789617,
126.957941998736));
#82312=CARTESIAN_POINT('Ctrl Pts',(-37.9926601800169,-3.17234004907076,
127.043472652148));
#82313=CARTESIAN_POINT('Ctrl Pts',(-38.0004164827588,-3.2760368071569,127.133454320402));
#82314=CARTESIAN_POINT('Ctrl Pts',(-38.0081727855006,-3.37571907342281,
127.227531882523));
#82315=CARTESIAN_POINT('Ctrl Pts',(-38.0159332280148,-3.47545454311545,
127.321659656671));
#82316=CARTESIAN_POINT('Ctrl Pts',(-38.0236936705289,-3.57117097884798,
127.419887400805));
#82317=CARTESIAN_POINT('Ctrl Pts',(-38.0314541130431,-3.66253203585477,
127.521824684962));
#82318=CARTESIAN_POINT('Ctrl Pts',(-38.0392270133085,-3.75403975374105,
127.623925607897));
#82319=CARTESIAN_POINT('Ctrl Pts',(-38.0469999135739,-3.84117787270947,
127.729747668624));
#82320=CARTESIAN_POINT('Ctrl Pts',(-38.0547728138393,-3.92365119527987,
127.838868354842));
#82321=CARTESIAN_POINT('Ctrl Pts',(-38.0622631496015,-4.00312640483864,
127.944022229259));
#82322=CARTESIAN_POINT('Ctrl Pts',(-38.0697534853637,-4.07826990830115,
128.052238813215));
#82323=CARTESIAN_POINT('Ctrl Pts',(-38.0772438211259,-4.14885767938843,
128.163117914087));
#82324=CARTESIAN_POINT('Ctrl Pts',(-38.0852101053287,-4.22393071530854,
128.28104245816));
#82325=CARTESIAN_POINT('Ctrl Pts',(-38.0931763895316,-4.29407895943621,
128.402337430133));
#82326=CARTESIAN_POINT('Ctrl Pts',(-38.1011426737345,-4.35899411609593,
128.52656489399));
#82327=CARTESIAN_POINT('Ctrl Pts',(-38.109098762519,-4.42382619297043,128.650633368922));
#82328=CARTESIAN_POINT('Ctrl Pts',(-38.1170548513034,-4.48343834476155,
128.777626545651));
#82329=CARTESIAN_POINT('Ctrl Pts',(-38.1250109400879,-4.53756546112957,
128.907077626427));
#82330=CARTESIAN_POINT('Ctrl Pts',(-38.1329551346756,-4.59161165851954,
129.036335180376));
#82331=CARTESIAN_POINT('Ctrl Pts',(-38.1408993292633,-4.64018902028521,
129.168042981875));
#82332=CARTESIAN_POINT('Ctrl Pts',(-38.148843523851,-4.68307861145244,129.301710365027));
#82333=CARTESIAN_POINT('Ctrl Pts',(-38.1543533835086,-4.71282557012691,
129.39441812965));
#82334=CARTESIAN_POINT('Ctrl Pts',(-38.1598632431662,-4.73983742116825,
129.488067986405));
#82335=CARTESIAN_POINT('Ctrl Pts',(-38.1653731028237,-4.76405452823409,
129.582490119308));
#82336=CARTESIAN_POINT('Ctrl Pts',(-36.4152663115528,-4.76405452823402,
129.582490119308));
#82337=CARTESIAN_POINT('Ctrl Pts',(-36.4249449713455,-4.806266409085,129.747073602091));
#82338=CARTESIAN_POINT('Ctrl Pts',(-36.4346236311382,-4.83997782400976,
129.913971994365));
#82339=CARTESIAN_POINT('Ctrl Pts',(-36.444302290931,-4.86497297357822,130.08240422771));
#82340=CARTESIAN_POINT('Ctrl Pts',(-36.4538371830679,-4.88959684301709,
130.248334553985));
#82341=CARTESIAN_POINT('Ctrl Pts',(-36.4633720752047,-4.90576145259318,
130.415753566812));
#82342=CARTESIAN_POINT('Ctrl Pts',(-36.4729069673416,-4.91330612857632,
130.583893047628));
#82343=CARTESIAN_POINT('Ctrl Pts',(-36.4769848328865,-4.91653282205094,
130.655802638813));
#82344=CARTESIAN_POINT('Ctrl Pts',(-36.4810626984315,-4.91818343115418,
130.727843733526));
#82345=CARTESIAN_POINT('Ctrl Pts',(-36.4851405639764,-4.91824802675748,
130.799954962542));
#82346=CARTESIAN_POINT('',(-36.1398594359911,-4.92619932659902,130.805220646693));
#82347=CARTESIAN_POINT('Ctrl Pts',(-36.0696835869212,-4.76181538791761,
129.583090555045));
#82348=CARTESIAN_POINT('Ctrl Pts',(-36.0930755366112,-4.86834354976456,
129.982579879972));
#82349=CARTESIAN_POINT('Ctrl Pts',(-36.1164674863011,-4.92520919812032,
130.394016325281));
#82350=CARTESIAN_POINT('Ctrl Pts',(-36.1398594359911,-4.92619932659902,
130.805220646693));
#82351=CARTESIAN_POINT('Ctrl Pts',(-36.1398594359911,-4.92619932659902,
130.805220646693));
#82352=CARTESIAN_POINT('Ctrl Pts',(-36.1424727741925,-4.92630994331169,
130.851160210344));
#82353=CARTESIAN_POINT('Ctrl Pts',(-36.2379019869981,-4.90488295595626,
132.528593278985));
#82354=CARTESIAN_POINT('Ctrl Pts',(-36.426147074408,-3.00542925083882,135.785231510157));
#82355=CARTESIAN_POINT('Ctrl Pts',(-36.7045946982209,2.56603982576222,136.025195746457));
#82356=CARTESIAN_POINT('Ctrl Pts',(-36.9830423220338,5.77944366050238,131.467467551281));
#82357=CARTESIAN_POINT('Ctrl Pts',(-37.2614899458467,3.68182111275986,126.300376478595));
#82358=CARTESIAN_POINT('Ctrl Pts',(-37.5399375696596,-1.79921517064808,
125.272226797766));
#82359=CARTESIAN_POINT('Ctrl Pts',(-37.7260883903438,-4.35811414719312,
127.983527806903));
#82360=CARTESIAN_POINT('Ctrl Pts',(-37.8194233364238,-4.76966346126612,
129.571636985164));
#82361=CARTESIAN_POINT('Ctrl Pts',(-37.8199424078995,-4.77192532739619,
129.580475997939));
#82362=CARTESIAN_POINT('Origin',(213.235140564004,0.,130.804360617566));
#82363=CARTESIAN_POINT('',(-39.9150204635389,-4.76405452823403,129.582490119308));
#82364=CARTESIAN_POINT('',(-39.5701139254339,-4.76405452823409,129.582490119308));
#82365=CARTESIAN_POINT('',(213.235140564004,-4.76405452823405,129.582490119308));
#82366=CARTESIAN_POINT('',(-38.235140564046,-4.91824967668966,130.806143940884));
#82367=CARTESIAN_POINT('Ctrl Pts',(-38.2351405640459,-4.91824967668966,
130.806143940884));
#82368=CARTESIAN_POINT('Ctrl Pts',(-38.2435224758346,-4.91819573390039,
130.954913433905));
#82369=CARTESIAN_POINT('Ctrl Pts',(-38.2519043876232,-4.91138754394824,
131.103478602525));
#82370=CARTESIAN_POINT('Ctrl Pts',(-38.2602862994119,-4.89790558294522,
131.25124311113));
#82371=CARTESIAN_POINT('Ctrl Pts',(-38.2687029849859,-4.88436768973608,
131.399620645908));
#82372=CARTESIAN_POINT('Ctrl Pts',(-38.2771196705599,-4.86410061939569,
131.547190589583));
#82373=CARTESIAN_POINT('Ctrl Pts',(-38.2855363561339,-4.8372365346784,131.693363300392));
#82374=CARTESIAN_POINT('Ctrl Pts',(-38.2939705996134,-4.81031640924787,
131.839840939624));
#82375=CARTESIAN_POINT('Ctrl Pts',(-38.3024048430931,-4.7767718368876,131.984915250611));
#82376=CARTESIAN_POINT('Ctrl Pts',(-38.3108390865726,-4.73678503963418,
132.128011081547));
#82377=CARTESIAN_POINT('Ctrl Pts',(-38.3193010235034,-4.69666694756791,
132.271576761075));
#82378=CARTESIAN_POINT('Ctrl Pts',(-38.3277629604342,-4.65006438485824,
132.41315069266));
#82379=CARTESIAN_POINT('Ctrl Pts',(-38.3362248973649,-4.5972090155243,132.552174203187));
#82380=CARTESIAN_POINT('Ctrl Pts',(-38.3427137465562,-4.5566780444993,132.658781307593));
#82381=CARTESIAN_POINT('Ctrl Pts',(-38.3492025957475,-4.51247125317275,
132.763889122567));
#82382=CARTESIAN_POINT('Ctrl Pts',(-38.3556914449387,-4.46471120750986,
132.86725588782));
#82383=CARTESIAN_POINT('Ctrl Pts',(-38.3634657790578,-4.40748957366053,
132.991100308641));
#82384=CARTESIAN_POINT('Ctrl Pts',(-38.3712401131769,-4.34502051082752,
133.112758221829));
#82385=CARTESIAN_POINT('Ctrl Pts',(-38.379014447296,-4.277493340301,133.231753001624));
#82386=CARTESIAN_POINT('Ctrl Pts',(-38.3867792002431,-4.21004939097709,
133.350601130987));
#82387=CARTESIAN_POINT('Ctrl Pts',(-38.3945439531902,-4.13755992820406,
133.466792320541));
#82388=CARTESIAN_POINT('Ctrl Pts',(-38.4023087061373,-4.06026198470017,
133.579870602794));
#82389=CARTESIAN_POINT('Ctrl Pts',(-38.4100657470223,-3.98304081460369,
133.692836574102));
#82390=CARTESIAN_POINT('Ctrl Pts',(-38.4178227879073,-3.90102088714029,
133.802695470224));
#82391=CARTESIAN_POINT('Ctrl Pts',(-38.4255798287923,-3.81448454460635,
133.909016914398));
#82392=CARTESIAN_POINT('Ctrl Pts',(-38.4333310200324,-3.72801345980123,
134.015258180744));
#82393=CARTESIAN_POINT('Ctrl Pts',(-38.4410822112725,-3.63703298488982,
134.11796700288));
#82394=CARTESIAN_POINT('Ctrl Pts',(-38.4488334025126,-3.54186785359698,
134.216743241211));
#82395=CARTESIAN_POINT('Ctrl Pts',(-38.4565812992897,-3.44674317002368,
134.315477497006));
#82396=CARTESIAN_POINT('Ctrl Pts',(-38.4643291960668,-3.3474376382418,134.410282212424));
#82397=CARTESIAN_POINT('Ctrl Pts',(-38.4720770928439,-3.24431508304851,
134.500791694213));
#82398=CARTESIAN_POINT('Ctrl Pts',(-38.479823368928,-3.14121409887057,134.59128224337));
#82399=CARTESIAN_POINT('Ctrl Pts',(-38.4875696450121,-3.03429797307346,
134.677479088268));
#82400=CARTESIAN_POINT('Ctrl Pts',(-38.4953159210962,-2.92396577221555,
134.759054945249));
#82401=CARTESIAN_POINT('Ctrl Pts',(-38.5030622543616,-2.81363275691055,
134.840631404406));
#82402=CARTESIAN_POINT('Ctrl Pts',(-38.5108085876269,-2.6998839305962,134.917586575146));
#82403=CARTESIAN_POINT('Ctrl Pts',(-38.5185549208923,-2.58314934387634,
134.989635104351));
#82404=CARTESIAN_POINT('Ctrl Pts',(-38.5263029888952,-2.46638861525516,
135.061699768325));
#82405=CARTESIAN_POINT('Ctrl Pts',(-38.5340510568982,-2.3466411283469,135.12885539896));
#82406=CARTESIAN_POINT('Ctrl Pts',(-38.5417991249012,-2.22436330220813,
135.190861610646));
#82407=CARTESIAN_POINT('Ctrl Pts',(-38.549555427643,-2.10195551774045,135.252933723271));
#82408=CARTESIAN_POINT('Ctrl Pts',(-38.5573117303849,-1.97701237117749,
135.30984530721));
#82409=CARTESIAN_POINT('Ctrl Pts',(-38.5650680331267,-1.85001262996764,
135.361403115882));
#82410=CARTESIAN_POINT('Ctrl Pts',(-38.5728284756409,-1.72294510517185,
135.41298844251));
#82411=CARTESIAN_POINT('Ctrl Pts',(-38.5805889181551,-1.59381916644517,
135.459214168411));
#82412=CARTESIAN_POINT('Ctrl Pts',(-38.5883493606693,-1.463129723798,135.499936671027));
#82413=CARTESIAN_POINT('Ctrl Pts',(-38.5961222609347,-1.3322304868556,135.54072454502));
#82414=CARTESIAN_POINT('Ctrl Pts',(-38.6038951612002,-1.19976310848476,
135.575991441416));
#82415=CARTESIAN_POINT('Ctrl Pts',(-38.6116680614656,-1.06623457457192,
135.605644497372));
#82416=CARTESIAN_POINT('Ctrl Pts',(-38.6191583972276,-0.937560139205245,
135.634219590053));
#82417=CARTESIAN_POINT('Ctrl Pts',(-38.6266487329896,-0.807900663326651,
135.657581855994));
#82418=CARTESIAN_POINT('Ctrl Pts',(-38.6341390687516,-0.677713249198604,
135.675693886227));
#82419=CARTESIAN_POINT('Ctrl Pts',(-38.6419134028707,-0.542589739693904,
135.69449263959));
#82420=CARTESIAN_POINT('Ctrl Pts',(-38.6496877369898,-0.406469437444971,
135.707694721551));
#82421=CARTESIAN_POINT('Ctrl Pts',(-38.6574620711089,-0.269855673983883,
135.715201785606));
#82422=CARTESIAN_POINT('Ctrl Pts',(-38.6652268240559,-0.133410274776922,
135.722699597876));
#82423=CARTESIAN_POINT('Ctrl Pts',(-38.672991577003,0.00352698898255541,
135.724516335918));
#82424=CARTESIAN_POINT('Ctrl Pts',(-38.68075632995,0.140444376955893,135.720604960505));
#82425=CARTESIAN_POINT('Ctrl Pts',(-38.688513370835,0.277225776649299,135.716697469925));
#82426=CARTESIAN_POINT('Ctrl Pts',(-38.69627041172,0.413986951564987,135.707073198832));
#82427=CARTESIAN_POINT('Ctrl Pts',(-38.704027452605,0.550213200635643,135.691737060643));
#82428=CARTESIAN_POINT('Ctrl Pts',(-38.7117786438452,0.686336720432375,
135.676412487556));
#82429=CARTESIAN_POINT('Ctrl Pts',(-38.7195298350853,0.821925730371897,
135.655384664479));
#82430=CARTESIAN_POINT('Ctrl Pts',(-38.7272810263255,0.956468055169481,
135.628710513867));
#82431=CARTESIAN_POINT('Ctrl Pts',(-38.7350289231026,1.09095319588981,135.602047700481));
#82432=CARTESIAN_POINT('Ctrl Pts',(-38.7427768198796,1.224392153581,135.569743408532));
#82433=CARTESIAN_POINT('Ctrl Pts',(-38.7505247166567,1.35628060396224,135.531906067989));
#82434=CARTESIAN_POINT('Ctrl Pts',(-38.7582709927408,1.48814146612284,135.494076642202));
#82435=CARTESIAN_POINT('Ctrl Pts',(-38.7660172688249,1.61845209052152,135.450716577689));
#82436=CARTESIAN_POINT('Ctrl Pts',(-38.773763544909,1.74672141892598,135.401984715637));
#82437=CARTESIAN_POINT('Ctrl Pts',(-38.7815098781744,1.87499169418549,135.353252493857));
#82438=CARTESIAN_POINT('Ctrl Pts',(-38.7892562114397,2.00122027790512,135.299148534265));
#82439=CARTESIAN_POINT('Ctrl Pts',(-38.797002544705,2.12493464156878,135.23988041028));
#82440=CARTESIAN_POINT('Ctrl Pts',(-38.804750612708,2.2486767102064,135.180599013611));
#82441=CARTESIAN_POINT('Ctrl Pts',(-38.8124986807109,2.36990308587518,135.116151320176));
#82442=CARTESIAN_POINT('Ctrl Pts',(-38.8202467487139,2.48816481970358,135.046791393959));
#82443=CARTESIAN_POINT('Ctrl Pts',(-38.8280030514558,2.60655224351019,134.977357751188));
#82444=CARTESIAN_POINT('Ctrl Pts',(-38.8357593541977,2.72196839352068,134.903001644672));
#82445=CARTESIAN_POINT('Ctrl Pts',(-38.8435156569396,2.83399190041499,134.82402142053));
#82446=CARTESIAN_POINT('Ctrl Pts',(-38.8512760994538,2.94607519762788,134.744999042264));
#82447=CARTESIAN_POINT('Ctrl Pts',(-38.8590365419678,3.05476193396696,134.661347866952));
#82448=CARTESIAN_POINT('Ctrl Pts',(-38.866796984482,3.15966376475733,134.573406644902));
#82449=CARTESIAN_POINT('Ctrl Pts',(-38.8745698847474,3.26473399327922,134.485324251796));
#82450=CARTESIAN_POINT('Ctrl Pts',(-38.8823427850129,3.36600688573248,134.392938313645));
#82451=CARTESIAN_POINT('Ctrl Pts',(-38.8901156852783,3.46313027572235,134.2966251774));
#82452=CARTESIAN_POINT('Ctrl Pts',(-38.8976060210403,3.55672298584717,134.203813266256));
#82453=CARTESIAN_POINT('Ctrl Pts',(-38.9050963568024,3.64646243565909,134.107354952448));
#82454=CARTESIAN_POINT('Ctrl Pts',(-38.9125866925644,3.7320700769938,134.007614588594));
#82455=CARTESIAN_POINT('Ctrl Pts',(-38.9203610266835,3.82092355806935,133.904092538529));
#82456=CARTESIAN_POINT('Ctrl Pts',(-38.9281353608026,3.90560719181378,133.796706720899));
#82457=CARTESIAN_POINT('Ctrl Pts',(-38.9359096949217,3.98576617354197,133.685827444088));
#82458=CARTESIAN_POINT('Ctrl Pts',(-38.9436744478688,4.06582636648919,133.575084816077));
#82459=CARTESIAN_POINT('Ctrl Pts',(-38.9514392008159,4.14137277559752,133.4608576091));
#82460=CARTESIAN_POINT('Ctrl Pts',(-38.959203953763,4.21208921727919,133.343550938944));
#82461=CARTESIAN_POINT('Ctrl Pts',(-38.966960994648,4.28273542239405,133.226360779427));
#82462=CARTESIAN_POINT('Ctrl Pts',(-38.974718035533,4.34856100616923,133.106097576081));
#82463=CARTESIAN_POINT('Ctrl Pts',(-38.982475076418,4.40929189390279,132.983197017313));
#82464=CARTESIAN_POINT('Ctrl Pts',(-38.9902262676581,4.4699769840015,132.860389138812));
#82465=CARTESIAN_POINT('Ctrl Pts',(-38.9979774588982,4.52557485272603,132.734948212664));
#82466=CARTESIAN_POINT('Ctrl Pts',(-39.0057286501384,4.57585654729728,132.607335914417));
#82467=CARTESIAN_POINT('Ctrl Pts',(-39.0134765469154,4.62611687080704,132.479777854802));
#82468=CARTESIAN_POINT('Ctrl Pts',(-39.0212244436925,4.67106537114485,132.350050621634));
#82469=CARTESIAN_POINT('Ctrl Pts',(-39.0289723404696,4.71052067392268,132.218637126261));
#82470=CARTESIAN_POINT('Ctrl Pts',(-39.0367186165536,4.74996772350172,132.087251119759));
#82471=CARTESIAN_POINT('Ctrl Pts',(-39.0444648926377,4.78392374870767,131.954179926866));
#82472=CARTESIAN_POINT('Ctrl Pts',(-39.0522111687218,4.8122569581602,131.819922546322));
#82473=CARTESIAN_POINT('Ctrl Pts',(-39.0599575019871,4.84059037676205,131.685664174721));
#82474=CARTESIAN_POINT('Ctrl Pts',(-39.0677038352525,4.86330081605778,131.550219980535));
#82475=CARTESIAN_POINT('Ctrl Pts',(-39.0754501685179,4.88030750024101,131.414099713894));
#82476=CARTESIAN_POINT('Ctrl Pts',(-39.0831982365209,4.89731799295323,131.277948964064));
#82477=CARTESIAN_POINT('Ctrl Pts',(-39.0909463045238,4.90862214038062,131.14112222838));
#82478=CARTESIAN_POINT('Ctrl Pts',(-39.0986943725268,4.91419102591724,131.004134548033));
#82479=CARTESIAN_POINT('Ctrl Pts',(-39.1064506752687,4.91976583013169,130.86700127555));
#82480=CARTESIAN_POINT('Ctrl Pts',(-39.1142069780105,4.91959318012247,130.729707107971));
#82481=CARTESIAN_POINT('Ctrl Pts',(-39.1219632807524,4.91369632251795,130.592767818602));
#82482=CARTESIAN_POINT('Ctrl Pts',(-39.1297237232665,4.90779631758299,130.455755440611));
#82483=CARTESIAN_POINT('Ctrl Pts',(-39.1374841657807,4.89616605048132,130.319098707611));
#82484=CARTESIAN_POINT('Ctrl Pts',(-39.1452446082948,4.87888061165811,130.183307447792));
#82485=CARTESIAN_POINT('Ctrl Pts',(-39.1530175085603,4.86156742471398,130.047298203787));
#82486=CARTESIAN_POINT('Ctrl Pts',(-39.1607904088257,4.83858099054103,129.912157594946));
#82487=CARTESIAN_POINT('Ctrl Pts',(-39.1685633090911,4.8100475859487,129.778385333551));
#82488=CARTESIAN_POINT('Ctrl Pts',(-39.1760536448532,4.78255144248439,129.649476030809));
#82489=CARTESIAN_POINT('Ctrl Pts',(-39.1835439806153,4.74990469586761,129.52183761539));
#82490=CARTESIAN_POINT('Ctrl Pts',(-39.1910343163774,4.71226332418739,129.395901379243));
#82491=CARTESIAN_POINT('Ctrl Pts',(-39.1988086504965,4.67319476845935,129.265190232426));
#82492=CARTESIAN_POINT('Ctrl Pts',(-39.2065829846156,4.62862161131375,129.135898835517));
#82493=CARTESIAN_POINT('Ctrl Pts',(-39.2143573187347,4.5786636230849,129.008525856476));
#82494=CARTESIAN_POINT('Ctrl Pts',(-39.2221220716818,4.52876720361166,128.881309853248));
#82495=CARTESIAN_POINT('Ctrl Pts',(-39.2298868246288,4.47349929874544,128.756007924153));
#82496=CARTESIAN_POINT('Ctrl Pts',(-39.2376515775759,4.41302983892011,128.633105058379));
#82497=CARTESIAN_POINT('Ctrl Pts',(-39.2454086184609,4.35262043821475,128.510324261463));
#82498=CARTESIAN_POINT('Ctrl Pts',(-39.2531656593459,4.28701993511846,128.389938134555));
#82499=CARTESIAN_POINT('Ctrl Pts',(-39.2609227002309,4.21644674255645,128.27241276469));
#82500=CARTESIAN_POINT('Ctrl Pts',(-39.2686738914711,4.14592676978804,128.15497602162));
#82501=CARTESIAN_POINT('Ctrl Pts',(-39.2764250827112,4.07044177204677,128.0403960754));
#82502=CARTESIAN_POINT('Ctrl Pts',(-39.2841762739513,3.9902564154782,127.9291150974));
#82503=CARTESIAN_POINT('Ctrl Pts',(-39.2919241707284,3.91010513982509,127.817881416784));
#82504=CARTESIAN_POINT('Ctrl Pts',(-39.2996720675055,3.82525770685523,127.70994423215));
#82505=CARTESIAN_POINT('Ctrl Pts',(-39.3074199642826,3.73602236627537,127.605717164289));
#82506=CARTESIAN_POINT('Ctrl Pts',(-39.3151662403667,3.64680569180507,127.501511898484));
#82507=CARTESIAN_POINT('Ctrl Pts',(-39.3229125164508,3.55320318949789,127.40101550259));
#82508=CARTESIAN_POINT('Ctrl Pts',(-39.3306587925349,3.45556344466568,127.304608577437));
#82509=CARTESIAN_POINT('Ctrl Pts',(-39.3384051258003,3.35792297907919,127.208200940629));
#82510=CARTESIAN_POINT('Ctrl Pts',(-39.3461514590656,3.25624548970483,127.115883109491));
#82511=CARTESIAN_POINT('Ctrl Pts',(-39.3538977923309,3.15091618246592,127.027998575392));
#82512=CARTESIAN_POINT('Ctrl Pts',(-39.3616458603339,3.04556328745881,126.94009436016));
#82513=CARTESIAN_POINT('Ctrl Pts',(-39.3693939283369,2.93655724739715,126.856625667964));
#82514=CARTESIAN_POINT('Ctrl Pts',(-39.3771419963399,2.82431575088884,126.777895219505));
#82515=CARTESIAN_POINT('Ctrl Pts',(-39.3848982990817,2.71195496278234,126.699081095389));
#82516=CARTESIAN_POINT('Ctrl Pts',(-39.3926546018236,2.59635216967742,126.625015499558));
#82517=CARTESIAN_POINT('Ctrl Pts',(-39.4004109045655,2.47795387163507,126.555957662037));
#82518=CARTESIAN_POINT('Ctrl Pts',(-39.4081713470797,2.35949238085615,126.486862966268));
#82519=CARTESIAN_POINT('Ctrl Pts',(-39.4159317895937,2.23823275760998,126.422781537154));
#82520=CARTESIAN_POINT('Ctrl Pts',(-39.4236922321079,2.11464452301101,126.363925773567));
#82521=CARTESIAN_POINT('Ctrl Pts',(-39.4314651323733,1.99085789360621,126.304975529483));
#82522=CARTESIAN_POINT('Ctrl Pts',(-39.4392380326388,1.86473554286216,126.251267867491));
#82523=CARTESIAN_POINT('Ctrl Pts',(-39.4470109329042,1.73676614857357,126.20296665403));
#82524=CARTESIAN_POINT('Ctrl Pts',(-39.4545012686662,1.61344876410352,126.156421311341));
#82525=CARTESIAN_POINT('Ctrl Pts',(-39.4619916044282,1.48841658631768,126.114896262598));
#82526=CARTESIAN_POINT('Ctrl Pts',(-39.4694819401902,1.36211678331456,126.078493402852));
#82527=CARTESIAN_POINT('Ctrl Pts',(-39.4772562743093,1.23102828489201,126.040710317613));
#82528=CARTESIAN_POINT('Ctrl Pts',(-39.4850306084284,1.0981588907535,126.00832581895));
#82529=CARTESIAN_POINT('Ctrl Pts',(-39.4928049425475,0.96399288316662,125.981508682901));
#82530=CARTESIAN_POINT('Ctrl Pts',(-39.5005696954946,0.829992223193326,
125.954724596575));
#82531=CARTESIAN_POINT('Ctrl Pts',(-39.5083344484416,0.694698508937481,
125.933494296862));
#82532=CARTESIAN_POINT('Ctrl Pts',(-39.5160992013887,0.55861162708742,125.917936964977));
#82533=CARTESIAN_POINT('Ctrl Pts',(-39.5238562422737,0.422659908646901,
125.902395084853));
#82534=CARTESIAN_POINT('Ctrl Pts',(-39.5316132831587,0.285916976262028,
125.892515003822));
#82535=CARTESIAN_POINT('Ctrl Pts',(-39.5393703240437,0.14889301967697,125.888364896332));
#82536=CARTESIAN_POINT('Ctrl Pts',(-39.5471215152838,0.0119723939232769,
125.88421791847));
#82537=CARTESIAN_POINT('Ctrl Pts',(-39.554872706524,-0.125228445006856,
125.885792325214));
#82538=CARTESIAN_POINT('Ctrl Pts',(-39.5626238977641,-0.262194427301316,
125.893104449864));
#82539=CARTESIAN_POINT('Ctrl Pts',(-39.5703717945412,-0.399102195399427,
125.900413466666));
#82540=CARTESIAN_POINT('Ctrl Pts',(-39.5781196913183,-0.535774915805013,
125.913455330221));
#82541=CARTESIAN_POINT('Ctrl Pts',(-39.5858675880954,-0.671697981138233,
125.93219427346));
#82542=CARTESIAN_POINT('Ctrl Pts',(-39.5936138641795,-0.807592614296347,
125.950929296917));
#82543=CARTESIAN_POINT('Ctrl Pts',(-39.6013601402636,-0.942737517232608,
125.975358976327));
#82544=CARTESIAN_POINT('Ctrl Pts',(-39.6091064163477,-1.07662406081528,
126.00539576104));
#82545=CARTESIAN_POINT('Ctrl Pts',(-39.616852749613,-1.210511592718,126.035432767477));
#82546=CARTESIAN_POINT('Ctrl Pts',(-39.6245990828783,-1.34314036524885,
126.071076876226));
#82547=CARTESIAN_POINT('Ctrl Pts',(-39.6323454161437,-1.47401317618001,
126.112189668107));
#82548=CARTESIAN_POINT('Ctrl Pts',(-39.6400934841467,-1.60491529516978,
126.153311666913));
#82549=CARTESIAN_POINT('Ctrl Pts',(-39.6478415521496,-1.7340602971447,126.19990466866));
#82550=CARTESIAN_POINT('Ctrl Pts',(-39.6555896201526,-1.86096772370854,
126.251780888026));
#82551=CARTESIAN_POINT('Ctrl Pts',(-39.6633459228944,-1.98801002899555,
126.303712242056));
#82552=CARTESIAN_POINT('Ctrl Pts',(-39.6711022256363,-2.11280964584294,
126.360937882237));
#82553=CARTESIAN_POINT('Ctrl Pts',(-39.6788585283782,-2.2349071325004,126.423222275582));
#82554=CARTESIAN_POINT('Ctrl Pts',(-39.6866189708923,-2.35706978626293,
126.485539911984));
#82555=CARTESIAN_POINT('Ctrl Pts',(-39.6943794134065,-2.47652709575224,
126.55292148956));
#82556=CARTESIAN_POINT('Ctrl Pts',(-39.7021398559207,-2.59284657615135,
126.625086793677));
#82557=CARTESIAN_POINT('Ctrl Pts',(-39.7099127561861,-2.70935278290675,
126.697367943948));
#82558=CARTESIAN_POINT('Ctrl Pts',(-39.7176856564515,-2.82271077130739,
126.77444794641));
#82559=CARTESIAN_POINT('Ctrl Pts',(-39.7254585567169,-2.93251853359339,
126.856004236408));
#82560=CARTESIAN_POINT('Ctrl Pts',(-39.732948892479,-3.03833450713154,126.934595749837));
#82561=CARTESIAN_POINT('Ctrl Pts',(-39.7404392282411,-3.14085365286397,
127.017343558953));
#82562=CARTESIAN_POINT('Ctrl Pts',(-39.7479295640031,-3.23974853831984,
127.103926525334));
#82563=CARTESIAN_POINT('Ctrl Pts',(-39.7555877436823,-3.34085946661956,
127.192449648298));
#82564=CARTESIAN_POINT('Ctrl Pts',(-39.7632459233616,-3.438522303563,127.285280320083));
#82565=CARTESIAN_POINT('Ctrl Pts',(-39.7709041030409,-3.53233941002593,
127.382115542345));
#82566=CARTESIAN_POINT('Ctrl Pts',(-39.77855346555,-3.62604850108378,127.478839274323));
#82567=CARTESIAN_POINT('Ctrl Pts',(-39.7862028280591,-3.71592038553408,
127.579558105399));
#82568=CARTESIAN_POINT('Ctrl Pts',(-39.7938521905683,-3.80159006410806,
127.683928588668));
#82569=CARTESIAN_POINT('Ctrl Pts',(-39.8014945190874,-3.88718096491826,
127.788203097801));
#82570=CARTESIAN_POINT('Ctrl Pts',(-39.8091368476064,-3.96857708869918,
127.896122273078));
#82571=CARTESIAN_POINT('Ctrl Pts',(-39.8167791761255,-4.0454503397911,128.007305986211));
#82572=CARTESIAN_POINT('Ctrl Pts',(-39.824416247059,-4.12227070547103,128.118413209845));
#82573=CARTESIAN_POINT('Ctrl Pts',(-39.8320533179927,-4.1945741585436,128.232780173941));
#82574=CARTESIAN_POINT('Ctrl Pts',(-39.8396903889262,-4.2620733229811,128.349994293638));
#82575=CARTESIAN_POINT('Ctrl Pts',(-39.8473244869759,-4.32954621200796,
128.467162785375));
#82576=CARTESIAN_POINT('Ctrl Pts',(-39.8549585850255,-4.39221832954647,
128.587175880213));
#82577=CARTESIAN_POINT('Ctrl Pts',(-39.8625926830752,-4.44984629012379,
128.709593075147));
#82578=CARTESIAN_POINT('Ctrl Pts',(-39.8702251171496,-4.50746168975395,
128.831983587272));
#82579=CARTESIAN_POINT('Ctrl Pts',(-39.8778575512241,-4.56003495129283,
128.956776790592));
#82580=CARTESIAN_POINT('Ctrl Pts',(-39.8854899852985,-4.60736951399532,
129.083509309635));
#82581=CARTESIAN_POINT('Ctrl Pts',(-39.893123820201,-4.65471276430396,129.210265088685));
#82582=CARTESIAN_POINT('Ctrl Pts',(-39.9007576551033,-4.69681525624594,
129.338960515656));
#82583=CARTESIAN_POINT('Ctrl Pts',(-39.9083914900058,-4.73352938745337,
129.469114347916));
#82584=CARTESIAN_POINT('Ctrl Pts',(-39.9106011478501,-4.74415650594061,
129.506788130503));
#82585=CARTESIAN_POINT('Ctrl Pts',(-39.9128108056945,-4.75433248306291,
129.544584012739));
#82586=CARTESIAN_POINT('Ctrl Pts',(-39.9150204635388,-4.76405452823403,
129.582490119308));
#82587=CARTESIAN_POINT('Ctrl Pts',(-38.1653731028237,-4.76405452823409,
129.582490119308));
#82588=CARTESIAN_POINT('Ctrl Pts',(-38.1733037435307,-4.79891152769259,
129.718397031168));
#82589=CARTESIAN_POINT('Ctrl Pts',(-38.1812343842377,-4.82797634339808,
129.855904430386));
#82590=CARTESIAN_POINT('Ctrl Pts',(-38.1891650249446,-4.85111275434098,
129.994491426171));
#82591=CARTESIAN_POINT('Ctrl Pts',(-38.1970893081135,-4.87423061815535,
130.132967324742));
#82592=CARTESIAN_POINT('Ctrl Pts',(-38.2050135912824,-4.89142948732574,
130.272520736319));
#82593=CARTESIAN_POINT('Ctrl Pts',(-38.2129378744513,-4.90262400013599,
130.412619662609));
#82594=CARTESIAN_POINT('Ctrl Pts',(-38.2203387709704,-4.91307913268544,
130.543465271456));
#82595=CARTESIAN_POINT('Ctrl Pts',(-38.2277396674894,-4.91829730602107,
130.674786363234));
#82596=CARTESIAN_POINT('Ctrl Pts',(-38.2351405640085,-4.9182496766899,130.806143940219));
#82597=CARTESIAN_POINT('',(-37.8898589934247,-4.91743469503477,130.799824135819));
#82598=CARTESIAN_POINT('Ctrl Pts',(-37.8199424078995,-4.77192532739619,
129.580475997939));
#82599=CARTESIAN_POINT('Ctrl Pts',(-37.8432478679745,-4.87347941629538,
129.977333211189));
#82600=CARTESIAN_POINT('Ctrl Pts',(-37.8665533280494,-4.9207712278546,130.388155924214));
#82601=CARTESIAN_POINT('Ctrl Pts',(-37.8898587881243,-4.91705745387562,
130.799820856863));
#82602=CARTESIAN_POINT('Ctrl Pts',(-37.8898594359911,-4.91824791434055,
130.799831204269));
#82603=CARTESIAN_POINT('Ctrl Pts',(-37.8975283655907,-4.91837269683403,
130.935325847404));
#82604=CARTESIAN_POINT('Ctrl Pts',(-37.9051972951903,-4.9128940792562,131.070959621141));
#82605=CARTESIAN_POINT('Ctrl Pts',(-37.9128662247899,-4.90180442327651,
131.206226837155));
#82606=CARTESIAN_POINT('Ctrl Pts',(-37.9205314994772,-4.89072005248292,
131.34142958657));
#82607=CARTESIAN_POINT('Ctrl Pts',(-37.9281967741646,-4.87402998909565,
131.476265727456));
#82608=CARTESIAN_POINT('Ctrl Pts',(-37.935862048852,-4.85177868278434,131.610230753369));
#82609=CARTESIAN_POINT('Ctrl Pts',(-37.9435245019742,-4.82953556711341,
131.74414646715));
#82610=CARTESIAN_POINT('Ctrl Pts',(-37.9511869550964,-4.80173534968034,
131.877191309779));
#82611=CARTESIAN_POINT('Ctrl Pts',(-37.9588494082187,-4.7684741342957,132.008867775308));
#82612=CARTESIAN_POINT('Ctrl Pts',(-37.9665114089083,-4.73521488283284,
132.140536465949));
#82613=CARTESIAN_POINT('Ctrl Pts',(-37.974173409598,-4.69649537264059,132.270836552027));
#82614=CARTESIAN_POINT('Ctrl Pts',(-37.9818354102876,-4.65246233438006,
132.399282963536));
#82615=CARTESIAN_POINT('Ctrl Pts',(-37.9894987053801,-4.60842185726729,
132.527751074522));
#82616=CARTESIAN_POINT('Ctrl Pts',(-37.9971620004726,-4.55906619690956,
132.654364509553));
#82617=CARTESIAN_POINT('Ctrl Pts',(-38.0048252955652,-4.50459106188987,
132.778656043191));
#82618=CARTESIAN_POINT('Ctrl Pts',(-38.0124964083817,-4.45006035396499,
132.903074373056));
#82619=CARTESIAN_POINT('Ctrl Pts',(-38.0201675211983,-4.39039990053984,
133.025165702982));
#82620=CARTESIAN_POINT('Ctrl Pts',(-38.0278386340148,-4.32585261457259,
133.144485020134));
#82621=CARTESIAN_POINT('Ctrl Pts',(-38.0355136202747,-4.26127273616834,
133.263864586254));
#82622=CARTESIAN_POINT('Ctrl Pts',(-38.0431886065347,-4.19180131578868,
133.380469008353));
#82623=CARTESIAN_POINT('Ctrl Pts',(-38.0508635927947,-4.11772520068029,
133.493881436259));
#82624=CARTESIAN_POINT('Ctrl Pts',(-38.0585509603689,-4.04352958572797,
133.607476821484));
#82625=CARTESIAN_POINT('Ctrl Pts',(-38.0662383279431,-3.96471466712519,
133.717869598399));
#82626=CARTESIAN_POINT('Ctrl Pts',(-38.0739256955174,-3.88160873183472,
133.824674626977));
#82627=CARTESIAN_POINT('Ctrl Pts',(-38.0815614027734,-3.79906128148991,
133.930761908978));
#82628=CARTESIAN_POINT('Ctrl Pts',(-38.0891971100294,-3.71228063013956,
134.033309287622));
#82629=CARTESIAN_POINT('Ctrl Pts',(-38.0968328172854,-3.62162342668443,
134.131976403349));
#82630=CARTESIAN_POINT('Ctrl Pts',(-38.1046071514045,-3.52932033460267,
134.232434828287));
#82631=CARTESIAN_POINT('Ctrl Pts',(-38.1123814855235,-3.43268802333354,
134.329208936762));
#82632=CARTESIAN_POINT('Ctrl Pts',(-38.1201558196426,-3.33205230381746,
134.421902670829));
#82633=CARTESIAN_POINT('Ctrl Pts',(-38.1279205725897,-3.23154060883189,
134.514482168152));
#82634=CARTESIAN_POINT('Ctrl Pts',(-38.1356853255368,-3.12703560728388,
134.602991034343));
#82635=CARTESIAN_POINT('Ctrl Pts',(-38.1434500784839,-3.01890223537644,
134.687067451173));
#82636=CARTESIAN_POINT('Ctrl Pts',(-38.1512071193689,-2.91087626305824,
134.77106036212));
#82637=CARTESIAN_POINT('Ctrl Pts',(-38.1589641602539,-2.79922939865271,
134.850629346196));
#82638=CARTESIAN_POINT('Ctrl Pts',(-38.1667212011389,-2.68436191042112,
134.925450788429));
#82639=CARTESIAN_POINT('Ctrl Pts',(-38.174472392379,-2.56958104465596,135.00021580723));
#82640=CARTESIAN_POINT('Ctrl Pts',(-38.1822235836191,-2.45158471551103,
135.070240197752));
#82641=CARTESIAN_POINT('Ctrl Pts',(-38.1899747748592,-2.33080432579081,
135.135242081815));
#82642=CARTESIAN_POINT('Ctrl Pts',(-38.1977226716363,-2.21007527095797,
135.200216338343));
#82643=CARTESIAN_POINT('Ctrl Pts',(-38.2054705684135,-2.08656485259624,
135.260172149273));
#82644=CARTESIAN_POINT('Ctrl Pts',(-38.2132184651906,-1.96073118009593,
135.314872373664));
#82645=CARTESIAN_POINT('Ctrl Pts',(-38.2209647412747,-1.83492382928724,
135.369561155948));
#82646=CARTESIAN_POINT('Ctrl Pts',(-38.2287110173588,-1.70679454929606,
135.418996382606));
#82647=CARTESIAN_POINT('Ctrl Pts',(-38.2364572934429,-1.57682328049001,
135.462988248597));
#82648=CARTESIAN_POINT('Ctrl Pts',(-38.2442036267083,-1.44685105226558,
135.506980439326));
#82649=CARTESIAN_POINT('Ctrl Pts',(-38.2519499599735,-1.3150371784213,135.545529063864));
#82650=CARTESIAN_POINT('Ctrl Pts',(-38.2596962932389,-1.18187830084589,
135.578493705833));
#82651=CARTESIAN_POINT('Ctrl Pts',(-38.2674443612419,-1.04868960326346,
135.611465730006));
#82652=CARTESIAN_POINT('Ctrl Pts',(-38.2751924292448,-0.914155682024639,
135.63885118934));
#82653=CARTESIAN_POINT('Ctrl Pts',(-38.2829404972478,-0.778784558070727,
135.660560538761));
#82654=CARTESIAN_POINT('Ctrl Pts',(-38.2906967999897,-0.643269560075155,
135.682292961136));
#82655=CARTESIAN_POINT('Ctrl Pts',(-38.2984531027315,-0.506915968563318,
135.698337160748));
#82656=CARTESIAN_POINT('Ctrl Pts',(-38.3062094054733,-0.370238692403159,
135.70865530418));
#82657=CARTESIAN_POINT('Ctrl Pts',(-38.3139698479875,-0.233488467465254,
135.718978954715));
#82658=CARTESIAN_POINT('Ctrl Pts',(-38.3217302905017,-0.0964146041944834,
135.723570446313));
#82659=CARTESIAN_POINT('Ctrl Pts',(-38.3294907330158,0.0404677688391133,
135.722444128669));
#82660=CARTESIAN_POINT('Ctrl Pts',(-38.3372636332813,0.17756987760975,135.721316002961));
#82661=CARTESIAN_POINT('Ctrl Pts',(-38.3450365335467,0.314479491166332,
135.714451745563));
#82662=CARTESIAN_POINT('Ctrl Pts',(-38.3528094338121,0.45068548048526,135.701917729043));
#82663=CARTESIAN_POINT('Ctrl Pts',(-38.3602997695741,0.581940039010632,
135.689839355595));
#82664=CARTESIAN_POINT('Ctrl Pts',(-38.3677901053363,0.712540936825952,
135.672496326879));
#82665=CARTESIAN_POINT('Ctrl Pts',(-38.3752804410983,0.842041478362543,
135.649992589891));
#82666=CARTESIAN_POINT('Ctrl Pts',(-38.3830547752174,0.976452072291771,
135.626635616876));
#82667=CARTESIAN_POINT('Ctrl Pts',(-38.3908291093365,1.11010299515356,135.597644886106));
#82668=CARTESIAN_POINT('Ctrl Pts',(-38.3986034434556,1.24248492340916,135.563080432558));
#82669=CARTESIAN_POINT('Ctrl Pts',(-38.4063681964026,1.3747037027695,135.528558576611));
#82670=CARTESIAN_POINT('Ctrl Pts',(-38.4141329493498,1.50565622461094,135.488476763199));
#82671=CARTESIAN_POINT('Ctrl Pts',(-38.4218977022969,1.63484082407832,135.442946451894));
#82672=CARTESIAN_POINT('Ctrl Pts',(-38.4296547431819,1.76389711558032,135.397461361936));
#82673=CARTESIAN_POINT('Ctrl Pts',(-38.4374117840668,1.89118861273123,135.346538672381));
#82674=CARTESIAN_POINT('Ctrl Pts',(-38.4451688249518,2.01622669431847,135.290340218458));
#82675=CARTESIAN_POINT('Ctrl Pts',(-38.4529200161919,2.14117048371573,135.234184144226));
#82676=CARTESIAN_POINT('Ctrl Pts',(-38.4606712074321,2.26386388477921,135.172760384204));
#82677=CARTESIAN_POINT('Ctrl Pts',(-38.4684223986722,2.38383656165944,135.10627952775));
#82678=CARTESIAN_POINT('Ctrl Pts',(-38.4761702954493,2.50375824695161,135.039826927432));
#82679=CARTESIAN_POINT('Ctrl Pts',(-38.4839181922263,2.62096116675749,134.968321694778));
#82680=CARTESIAN_POINT('Ctrl Pts',(-38.4916660890034,2.7349981883732,134.892021069719));
#82681=CARTESIAN_POINT('Ctrl Pts',(-38.4994123650875,2.84901135590235,134.815736405106));
#82682=CARTESIAN_POINT('Ctrl Pts',(-38.5071586411715,2.95985961773483,134.734658560571));
#82683=CARTESIAN_POINT('Ctrl Pts',(-38.5149049172556,3.06712386602207,134.649088729277));
#82684=CARTESIAN_POINT('Ctrl Pts',(-38.522651250521,3.17438890610948,134.563518266325));
#82685=CARTESIAN_POINT('Ctrl Pts',(-38.5303975837863,3.27806957423187,134.473455994262));
#82686=CARTESIAN_POINT('Ctrl Pts',(-38.5381439170516,3.37777928704401,134.379243853494));
#82687=CARTESIAN_POINT('Ctrl Pts',(-38.5458919850545,3.47751132915458,134.28501061457));
#82688=CARTESIAN_POINT('Ctrl Pts',(-38.5536400530575,3.57327036229184,134.186625926131));
#82689=CARTESIAN_POINT('Ctrl Pts',(-38.5613881210605,3.66470645192017,134.084468799281));
#82690=CARTESIAN_POINT('Ctrl Pts',(-38.5691444238023,3.75623972091328,133.982203098621));
#82691=CARTESIAN_POINT('Ctrl Pts',(-38.5769007265442,3.8434406072765,133.876157242139));
#82692=CARTESIAN_POINT('Ctrl Pts',(-38.584657029286,3.92599895986322,133.766743987364));
#82693=CARTESIAN_POINT('Ctrl Pts',(-38.5924174718002,4.00860137632839,133.657272335439));
#82694=CARTESIAN_POINT('Ctrl Pts',(-38.6001779143143,4.08655609956023,133.544430025498));
#82695=CARTESIAN_POINT('Ctrl Pts',(-38.6079383568285,4.15959676279037,133.428658206157));
#82696=CARTESIAN_POINT('Ctrl Pts',(-38.6157112570939,4.23275467737736,133.312700539613));
#82697=CARTESIAN_POINT('Ctrl Pts',(-38.6234841573593,4.30098257355306,133.193804305454));
#82698=CARTESIAN_POINT('Ctrl Pts',(-38.6312570576248,4.36406001471642,133.072435406997));
#82699=CARTESIAN_POINT('Ctrl Pts',(-38.6387473933869,4.42484443201185,132.955478573707));
#82700=CARTESIAN_POINT('Ctrl Pts',(-38.646237729149,4.48084622614649,132.836226008916));
#82701=CARTESIAN_POINT('Ctrl Pts',(-38.6537280649111,4.53191140080741,132.715109716148));
#82702=CARTESIAN_POINT('Ctrl Pts',(-38.6615023990302,4.58491272708586,132.589401262329));
#82703=CARTESIAN_POINT('Ctrl Pts',(-38.6692767331493,4.63276359264101,132.461286757615));
#82704=CARTESIAN_POINT('Ctrl Pts',(-38.6770510672684,4.67523920478611,132.331227160696));
#82705=CARTESIAN_POINT('Ctrl Pts',(-38.6848158202155,4.71766246953545,132.201327850607));
#82706=CARTESIAN_POINT('Ctrl Pts',(-38.6925805731626,4.75472354148426,132.069488586011));
#82707=CARTESIAN_POINT('Ctrl Pts',(-38.7003453261097,4.78624503261944,131.936191678381));
#82708=CARTESIAN_POINT('Ctrl Pts',(-38.7081023669947,4.81773521616519,131.803027163119));
#82709=CARTESIAN_POINT('Ctrl Pts',(-38.7158594078797,4.84369667871507,131.668408263923));
#82710=CARTESIAN_POINT('Ctrl Pts',(-38.7236164487647,4.86400146512909,131.532833547552));
#82711=CARTESIAN_POINT('Ctrl Pts',(-38.7313676400049,4.88429093954567,131.397361069129));
#82712=CARTESIAN_POINT('Ctrl Pts',(-38.7391188312449,4.89893217085611,131.260934593307));
#82713=CARTESIAN_POINT('Ctrl Pts',(-38.746870022485,4.90784810583442,131.124063655646));
#82714=CARTESIAN_POINT('Ctrl Pts',(-38.7546179192621,4.91676025130254,130.987250891784));
#82715=CARTESIAN_POINT('Ctrl Pts',(-38.7623658160393,4.91995191493199,130.84999443113));
#82716=CARTESIAN_POINT('Ctrl Pts',(-38.7701137128164,4.91739783381656,130.712809503558));
#82717=CARTESIAN_POINT('Ctrl Pts',(-38.7778599889005,4.91484428695985,130.575653272115));
#82718=CARTESIAN_POINT('Ctrl Pts',(-38.7856062649846,4.90654739324831,130.438568934642));
#82719=CARTESIAN_POINT('Ctrl Pts',(-38.7933525410687,4.89253401699069,130.302071900702));
#82720=CARTESIAN_POINT('Ctrl Pts',(-38.801098874334,4.87852053728949,130.165573859172));
#82721=CARTESIAN_POINT('Ctrl Pts',(-38.8088452075994,4.85879053076791,130.029663518748));
#82722=CARTESIAN_POINT('Ctrl Pts',(-38.8165915408647,4.83342272383283,129.894850950088));
#82723=CARTESIAN_POINT('Ctrl Pts',(-38.8243396088677,4.80804923595334,129.760008191088));
#82724=CARTESIAN_POINT('Ctrl Pts',(-38.8320876768707,4.77703550762498,129.626264077191));
#82725=CARTESIAN_POINT('Ctrl Pts',(-38.8398357448737,4.7405112634608,129.494117882993));
#82726=CARTESIAN_POINT('Ctrl Pts',(-38.8475920476156,4.70394820089523,129.361831242247));
#82727=CARTESIAN_POINT('Ctrl Pts',(-38.8553483503574,4.66186302754181,129.23114629115));
#82728=CARTESIAN_POINT('Ctrl Pts',(-38.8631046530992,4.61443536372731,129.102547074171));
#82729=CARTESIAN_POINT('Ctrl Pts',(-38.8708650956134,4.56698238634054,128.973879219918));
#82730=CARTESIAN_POINT('Ctrl Pts',(-38.8786255381276,4.51418138718322,128.84729967862));
#82731=CARTESIAN_POINT('Ctrl Pts',(-38.8863859806418,4.45625953933603,128.723271003788));
#82732=CARTESIAN_POINT('Ctrl Pts',(-38.8941588809072,4.3982447101967,128.599043227115));
#82733=CARTESIAN_POINT('Ctrl Pts',(-38.9019317811727,4.335092785524,128.477374846983));
#82734=CARTESIAN_POINT('Ctrl Pts',(-38.9097046814381,4.26707659160689,128.35870315507));
#82735=CARTESIAN_POINT('Ctrl Pts',(-38.9171950172001,4.20153295766167,128.244345478075));
#82736=CARTESIAN_POINT('Ctrl Pts',(-38.924685352962,4.13147273514576,128.132770658444));
#82737=CARTESIAN_POINT('Ctrl Pts',(-38.932175688724,4.05717614209043,128.024341766092));
#82738=CARTESIAN_POINT('Ctrl Pts',(-38.9399500228431,3.98006257112689,127.911801759329));
#82739=CARTESIAN_POINT('Ctrl Pts',(-38.9477243569622,3.89814077157495,127.802294451762));
#82740=CARTESIAN_POINT('Ctrl Pts',(-38.9554986910813,3.8116770550972,127.696258127276));
#82741=CARTESIAN_POINT('Ctrl Pts',(-38.9632634440284,3.7253198974223,127.590352483083));
#82742=CARTESIAN_POINT('Ctrl Pts',(-38.9710281969755,3.63443220489126,127.487909610761));
#82743=CARTESIAN_POINT('Ctrl Pts',(-38.9787929499226,3.53932387725116,127.389339453002));
#82744=CARTESIAN_POINT('Ctrl Pts',(-38.9865499908076,3.44431001254313,127.290867196513));
#82745=CARTESIAN_POINT('Ctrl Pts',(-38.9943070316927,3.34508412469663,127.196260279539));
#82746=CARTESIAN_POINT('Ctrl Pts',(-39.0020640725777,3.24199650916696,127.105895841872));
#82747=CARTESIAN_POINT('Ctrl Pts',(-39.0098152638178,3.13898663280965,127.01559954873));
#82748=CARTESIAN_POINT('Ctrl Pts',(-39.0175664550579,3.03212111805632,126.929539623583));
#82749=CARTESIAN_POINT('Ctrl Pts',(-39.025317646298,2.92178700245488,126.848056309909));
#82750=CARTESIAN_POINT('Ctrl Pts',(-39.0330655430751,2.81149978179627,126.766607628817));
#82751=CARTESIAN_POINT('Ctrl Pts',(-39.0408134398523,2.69774720629531,126.689731922154));
#82752=CARTESIAN_POINT('Ctrl Pts',(-39.0485613366293,2.58094909822007,126.617728938651));
#82753=CARTESIAN_POINT('Ctrl Pts',(-39.0563076127135,2.46417542179101,126.545741016619));
#82754=CARTESIAN_POINT('Ctrl Pts',(-39.0640538887975,2.34435781253047,126.478623995404));
#82755=CARTESIAN_POINT('Ctrl Pts',(-39.0718001648816,2.22194441991716,126.416633864759));
#82756=CARTESIAN_POINT('Ctrl Pts',(-39.079546498147,2.09953012367601,126.354643276517));
#82757=CARTESIAN_POINT('Ctrl Pts',(-39.0872928314123,1.97452035463921,126.297779830993));
#82758=CARTESIAN_POINT('Ctrl Pts',(-39.0950391646777,1.84738680324385,126.24625299908));
#82759=CARTESIAN_POINT('Ctrl Pts',(-39.1027872326807,1.72022478117166,126.194714628091));
#82760=CARTESIAN_POINT('Ctrl Pts',(-39.1105353006836,1.59093839260654,126.148515395645));
#82761=CARTESIAN_POINT('Ctrl Pts',(-39.1182833686866,1.46001781072822,126.107816030867));
#82762=CARTESIAN_POINT('Ctrl Pts',(-39.1260396714284,1.32895808489714,126.067073410319));
#82763=CARTESIAN_POINT('Ctrl Pts',(-39.1337959741703,1.1962610701642,126.031842450349));
#82764=CARTESIAN_POINT('Ctrl Pts',(-39.1415522769121,1.06243109602415,126.00223366915));
#82765=CARTESIAN_POINT('Ctrl Pts',(-39.1493127194263,0.928529692797354,
125.972609084853));
#82766=CARTESIAN_POINT('Ctrl Pts',(-39.1570731619404,0.793494510004567,
125.948612726898));
#82767=CARTESIAN_POINT('Ctrl Pts',(-39.1648336044546,0.657837499612393,
125.930303489607));
#82768=CARTESIAN_POINT('Ctrl Pts',(-39.17260650472,0.521962720544074,125.911964860704));
#82769=CARTESIAN_POINT('Ctrl Pts',(-39.1803794049855,0.385464508654437,
125.89933163211));
#82770=CARTESIAN_POINT('Ctrl Pts',(-39.188152305251,0.24885823909118,125.892410634175));
#82771=CARTESIAN_POINT('Ctrl Pts',(-39.195642641013,0.117217951516797,125.885741231948));
#82772=CARTESIAN_POINT('Ctrl Pts',(-39.203132976775,-0.0145223657895349,
125.884375965981));
#82773=CARTESIAN_POINT('Ctrl Pts',(-39.210623312537,-0.145905787133676,
125.888275329069));
#82774=CARTESIAN_POINT('Ctrl Pts',(-39.2183976466561,-0.282270650831207,
125.892322537692));
#82775=CARTESIAN_POINT('Ctrl Pts',(-39.2261719807751,-0.41868298380456,
125.902054293197));
#82776=CARTESIAN_POINT('Ctrl Pts',(-39.2339463148942,-0.554630097449639,
125.917483443183));
#82777=CARTESIAN_POINT('Ctrl Pts',(-39.2417110678413,-0.690409668426355,
125.932893578121));
#82778=CARTESIAN_POINT('Ctrl Pts',(-39.2494758207884,-0.825724776110992,
125.953987093124));
#82779=CARTESIAN_POINT('Ctrl Pts',(-39.2572405737355,-0.960063015724354,
125.980724844797));
#82780=CARTESIAN_POINT('Ctrl Pts',(-39.2649976146204,-1.09426782870466,
126.007436040157));
#82781=CARTESIAN_POINT('Ctrl Pts',(-39.2727546555054,-1.22749732347055,
126.039780240298));
#82782=CARTESIAN_POINT('Ctrl Pts',(-39.2805116963904,-1.35924485838201,
126.077666585003));
#82783=CARTESIAN_POINT('Ctrl Pts',(-39.2882628876306,-1.4908930414529,126.115524359321));
#82784=CARTESIAN_POINT('Ctrl Pts',(-39.2960140788707,-1.62106111488213,
126.158915851799));
#82785=CARTESIAN_POINT('Ctrl Pts',(-39.3037652701108,-1.74925361894652,
126.207699346697));
#82786=CARTESIAN_POINT('Ctrl Pts',(-39.3115131668879,-1.87739163777705,
126.256462107309));
#82787=CARTESIAN_POINT('Ctrl Pts',(-39.319261063665,-2.0035553926455,126.310612173473));
#82788=CARTESIAN_POINT('Ctrl Pts',(-39.327008960442,-2.12726577226441,126.369958358337));
#82789=CARTESIAN_POINT('Ctrl Pts',(-39.3347552365261,-2.25095027433863,
126.429292129259));
#82790=CARTESIAN_POINT('Ctrl Pts',(-39.3425015126102,-2.37218206965326,
126.493819687949));
#82791=CARTESIAN_POINT('Ctrl Pts',(-39.3502477886943,-2.49050355103721,
126.563302362275));
#82792=CARTESIAN_POINT('Ctrl Pts',(-39.3579941219597,-2.60882590584362,
126.632785549507));
#82793=CARTESIAN_POINT('Ctrl Pts',(-39.3657404552251,-2.72423756671765,
126.707223727385));
#82794=CARTESIAN_POINT('Ctrl Pts',(-39.3734867884904,-2.83630733966034,
126.786333273522));
#82795=CARTESIAN_POINT('Ctrl Pts',(-39.3812348564934,-2.94840220985179,
126.865460535693));
#82796=CARTESIAN_POINT('Ctrl Pts',(-39.3889829244964,-3.05715338355428,
126.949261022358));
#82797=CARTESIAN_POINT('Ctrl Pts',(-39.3967309924994,-3.16216068422731,
127.037409214956));
#82798=CARTESIAN_POINT('Ctrl Pts',(-39.4044872952412,-3.2672795879088,127.125651092502));
#82799=CARTESIAN_POINT('Ctrl Pts',(-39.4122435979831,-3.3686463700914,127.218249654744));
#82800=CARTESIAN_POINT('Ctrl Pts',(-39.4199999007249,-3.46589544628015,
127.314840332777));
#82801=CARTESIAN_POINT('Ctrl Pts',(-39.4277603432391,-3.56319642722884,
127.411482564163));
#82802=CARTESIAN_POINT('Ctrl Pts',(-39.4355207857532,-3.65637505750607,
127.512120870223));
#82803=CARTESIAN_POINT('Ctrl Pts',(-39.4432812282674,-3.74510506510637,
127.616356365089));
#82804=CARTESIAN_POINT('Ctrl Pts',(-39.4510541285328,-3.83397750999219,
127.720759188024));
#82805=CARTESIAN_POINT('Ctrl Pts',(-39.4588270287982,-3.91838682068088,
127.828770430879));
#82806=CARTESIAN_POINT('Ctrl Pts',(-39.4665999290637,-3.99804867774925,
127.939960185914));
#82807=CARTESIAN_POINT('Ctrl Pts',(-39.4740902648257,-4.0748146256575,128.047107913285));
#82808=CARTESIAN_POINT('Ctrl Pts',(-39.4815806005878,-4.1471721220219,128.157206813712));
#82809=CARTESIAN_POINT('Ctrl Pts',(-39.4890709363498,-4.21490742587628,
128.269851108057));
#82810=CARTESIAN_POINT('Ctrl Pts',(-39.4971083552182,-4.28759001668972,
128.390722775968));
#82811=CARTESIAN_POINT('Ctrl Pts',(-39.5051457740864,-4.35516775034002,
128.514886492627));
#82812=CARTESIAN_POINT('Ctrl Pts',(-39.5131831929548,-4.41734034050855,
128.641888102454));
#82813=CARTESIAN_POINT('Ctrl Pts',(-39.5212097282743,-4.47942874215494,
128.768717738139));
#82814=CARTESIAN_POINT('Ctrl Pts',(-39.5292362635939,-4.53612641755964,
128.898377300592));
#82815=CARTESIAN_POINT('Ctrl Pts',(-39.5372627989135,-4.58717710024377,
129.030385050232));
#82816=CARTESIAN_POINT('Ctrl Pts',(-39.545276454415,-4.63814586420752,129.16218097301));
#82817=CARTESIAN_POINT('Ctrl Pts',(-39.5532901099165,-4.68348556729917,
129.296317244772));
#82818=CARTESIAN_POINT('Ctrl Pts',(-39.5613037654181,-4.72298676985517,
129.432289542777));
#82819=CARTESIAN_POINT('Ctrl Pts',(-39.5642404854233,-4.73746255706055,
129.482118558715));
#82820=CARTESIAN_POINT('Ctrl Pts',(-39.5671772054286,-4.75115471100942,
129.532193927731));
#82821=CARTESIAN_POINT('Ctrl Pts',(-39.5701139254339,-4.76405452823409,
129.582490119308));
#82822=CARTESIAN_POINT('Origin',(213.235140564004,0.,130.804360617566));
#82823=CARTESIAN_POINT('',(-41.6650773111923,-4.76405452823405,129.582490119308));
#82824=CARTESIAN_POINT('',(-41.3197599198393,-4.76405452823404,129.582490119308));
#82825=CARTESIAN_POINT('',(213.235140564004,-4.76405452823405,129.582490119308));
#82826=CARTESIAN_POINT('',(-39.9851405639765,-4.91824854872011,130.808138912485));
#82827=CARTESIAN_POINT('Ctrl Pts',(-39.9851405640085,-4.91824854871968,
130.808138913047));
#82828=CARTESIAN_POINT('Ctrl Pts',(-39.9988861052777,-4.91806270117596,
131.050058693222));
#82829=CARTESIAN_POINT('Ctrl Pts',(-40.012631646547,-4.90002514730396,131.291308336928));
#82830=CARTESIAN_POINT('Ctrl Pts',(-40.0263771878162,-4.86444322375335,
131.529877802325));
#82831=CARTESIAN_POINT('Ctrl Pts',(-40.0341515219352,-4.84431846061283,
131.664810192274));
#82832=CARTESIAN_POINT('Ctrl Pts',(-40.0419258560543,-4.81854333208972,
131.799118324574));
#82833=CARTESIAN_POINT('Ctrl Pts',(-40.0497001901734,-4.78716563351233,
131.932291581685));
#82834=CARTESIAN_POINT('Ctrl Pts',(-40.0574649431205,-4.75582660514417,
132.065300714659));
#82835=CARTESIAN_POINT('Ctrl Pts',(-40.0652296960675,-4.71889883375243,
132.197177378413));
#82836=CARTESIAN_POINT('Ctrl Pts',(-40.0729944490145,-4.67648170823861,
132.327417377838));
#82837=CARTESIAN_POINT('Ctrl Pts',(-40.0807514898996,-4.63410671201165,
132.457528021059));
#82838=CARTESIAN_POINT('Ctrl Pts',(-40.0885085307846,-4.58625333188387,
132.586004865544));
#82839=CARTESIAN_POINT('Ctrl Pts',(-40.0962655716696,-4.5330716309168,132.712355547192));
#82840=CARTESIAN_POINT('Ctrl Pts',(-40.1040167629097,-4.4799300346842,132.838610946807));
#82841=CARTESIAN_POINT('Ctrl Pts',(-40.1117679541499,-4.42146826651086,
132.962743016079));
#82842=CARTESIAN_POINT('Ctrl Pts',(-40.11951914539,-4.35788556834454,133.084276501039));
#82843=CARTESIAN_POINT('Ctrl Pts',(-40.1272670421671,-4.29432989452124,
133.205758331027));
#82844=CARTESIAN_POINT('Ctrl Pts',(-40.1350149389442,-4.22565780051822,
133.324643427709));
#82845=CARTESIAN_POINT('Ctrl Pts',(-40.1427628357212,-4.15211572223893,
133.440478614097));
#82846=CARTESIAN_POINT('Ctrl Pts',(-40.1505091118053,-4.07858902737693,
133.556289570262));
#82847=CARTESIAN_POINT('Ctrl Pts',(-40.1582553878894,-4.00019458389978,
133.669051555246));
#82848=CARTESIAN_POINT('Ctrl Pts',(-40.1660016639735,-3.91722344080143,
133.778338354089));
#82849=CARTESIAN_POINT('Ctrl Pts',(-40.1737479972388,-3.83425168522907,
133.887625959662));
#82850=CARTESIAN_POINT('Ctrl Pts',(-40.1814943305042,-3.74670339903135,
133.993438016515));
#82851=CARTESIAN_POINT('Ctrl Pts',(-40.1892406637695,-3.65491114720952,
134.095379847));
#82852=CARTESIAN_POINT('Ctrl Pts',(-40.1969887317725,-3.56309833914934,
134.197344506651));
#82853=CARTESIAN_POINT('Ctrl Pts',(-40.2047367997754,-3.46703993582788,
134.2954369248));
#82854=CARTESIAN_POINT('Ctrl Pts',(-40.2124848677783,-3.36710644174079,
134.38929817246));
#82855=CARTESIAN_POINT('Ctrl Pts',(-40.2202411705202,-3.26706673714696,
134.483259176971));
#82856=CARTESIAN_POINT('Ctrl Pts',(-40.227997473262,-3.16314400008589,134.572979759788));
#82857=CARTESIAN_POINT('Ctrl Pts',(-40.2357537760038,-3.05574342644822,
134.658139954038));
#82858=CARTESIAN_POINT('Ctrl Pts',(-40.243514218518,-2.9482855298905,134.743345600848));
#82859=CARTESIAN_POINT('Ctrl Pts',(-40.2512746610322,-2.8373464141595,134.823985779344));
#82860=CARTESIAN_POINT('Ctrl Pts',(-40.2590351035464,-2.72336070876421,
134.899783613113));
#82861=CARTESIAN_POINT('Ctrl Pts',(-40.2668080038118,-2.60919202339545,
134.975703124295));
#82862=CARTESIAN_POINT('Ctrl Pts',(-40.2745809040772,-2.49196730979754,
135.04676455431));
#82863=CARTESIAN_POINT('Ctrl Pts',(-40.2823538043426,-2.37214704724894,
135.11273634964));
#82864=CARTESIAN_POINT('Ctrl Pts',(-40.2898441401047,-2.25668255305155,
135.176309904039));
#82865=CARTESIAN_POINT('Ctrl Pts',(-40.2973344758668,-2.13880821869824,
135.23515730378));
#82866=CARTESIAN_POINT('Ctrl Pts',(-40.3048248116289,-2.01895222782011,
135.289114230005));
#82867=CARTESIAN_POINT('Ctrl Pts',(-40.312599145748,-1.89455186061979,135.345116949486));
#82868=CARTESIAN_POINT('Ctrl Pts',(-40.3203734798671,-1.76762253855215,
135.396028430037));
#82869=CARTESIAN_POINT('Ctrl Pts',(-40.3281478139862,-1.63861969315752,
135.441612881967));
#82870=CARTESIAN_POINT('Ctrl Pts',(-40.3359125669333,-1.50977583224052,
135.487141155135));
#82871=CARTESIAN_POINT('Ctrl Pts',(-40.3436773198804,-1.37886389763405,
135.52735533324));
#82872=CARTESIAN_POINT('Ctrl Pts',(-40.3514420728275,-1.24636180509307,
135.562066505208));
#82873=CARTESIAN_POINT('Ctrl Pts',(-40.3591991137125,-1.11399131549854,
135.596743201551));
#82874=CARTESIAN_POINT('Ctrl Pts',(-40.3669561545976,-0.980034186737435,
135.625927670236));
#82875=CARTESIAN_POINT('Ctrl Pts',(-40.3747131954826,-0.844985771422639,
135.649480028746));
#82876=CARTESIAN_POINT('Ctrl Pts',(-40.3824643867227,-0.710039197168354,
135.673014626239));
#82877=CARTESIAN_POINT('Ctrl Pts',(-40.3902155779628,-0.574003357981259,
135.690925500487));
#82878=CARTESIAN_POINT('Ctrl Pts',(-40.3979667692029,-0.437385793624253,
135.703123393006));
#82879=CARTESIAN_POINT('Ctrl Pts',(-40.40571466598,-0.300826295376491,135.715316101095));
#82880=CARTESIAN_POINT('Ctrl Pts',(-40.413462562757,-0.163685952318491,
135.721800622202));
#82881=CARTESIAN_POINT('Ctrl Pts',(-40.4212104595341,-0.0264792397117674,
135.722539336601));
#82882=CARTESIAN_POINT('Ctrl Pts',(-40.4289567356182,0.110698772208513,
135.723277896476));
#82883=CARTESIAN_POINT('Ctrl Pts',(-40.4367030117023,0.247942735351468,
135.718273038181));
#82884=CARTESIAN_POINT('Ctrl Pts',(-40.4444492877864,0.384736743908612,
135.707539249881));
#82885=CARTESIAN_POINT('Ctrl Pts',(-40.4521956210518,0.521531762248052,
135.696805382346));
#82886=CARTESIAN_POINT('Ctrl Pts',(-40.4599419543171,0.6578764296068,135.680342531003));
#82887=CARTESIAN_POINT('Ctrl Pts',(-40.4676882875824,0.793258932997148,
135.658217159299));
#82888=CARTESIAN_POINT('Ctrl Pts',(-40.4754363555854,0.92867175436027,135.636086832771));
#82889=CARTESIAN_POINT('Ctrl Pts',(-40.4831844235883,1.0631215972222,135.60829152559));
#82890=CARTESIAN_POINT('Ctrl Pts',(-40.4909324915913,1.19610621773281,135.5749489438));
#82891=CARTESIAN_POINT('Ctrl Pts',(-40.4986887943332,1.32923217588082,135.541570925117));
#82892=CARTESIAN_POINT('Ctrl Pts',(-40.506445097075,1.46088942105955,135.502633949742));
#82893=CARTESIAN_POINT('Ctrl Pts',(-40.5142013998169,1.59058973780019,135.458305970544));
#82894=CARTESIAN_POINT('Ctrl Pts',(-40.5219618423311,1.72035927950526,135.413954332168));
#82895=CARTESIAN_POINT('Ctrl Pts',(-40.5297222848452,1.84816944741361,135.364206098367));
#82896=CARTESIAN_POINT('Ctrl Pts',(-40.5374827273594,1.97355236969247,135.309277276793));
#82897=CARTESIAN_POINT('Ctrl Pts',(-40.5452556276249,2.09913656776914,135.254260278598));
#82898=CARTESIAN_POINT('Ctrl Pts',(-40.5530285278902,2.22228538247704,135.194046245766));
#82899=CARTESIAN_POINT('Ctrl Pts',(-40.5608014281557,2.34255510098758,135.128897432225));
#82900=CARTESIAN_POINT('Ctrl Pts',(-40.5682917639177,2.45845271228946,135.066116942155));
#82901=CARTESIAN_POINT('Ctrl Pts',(-40.5757820996798,2.57167665329429,134.998754383277));
#82902=CARTESIAN_POINT('Ctrl Pts',(-40.5832724354419,2.68185723418049,134.92708118025));
#82903=CARTESIAN_POINT('Ctrl Pts',(-40.5910467695609,2.79621534527919,134.852690465945));
#82904=CARTESIAN_POINT('Ctrl Pts',(-40.59882110368,2.90765701475315,134.773420131284));
#82905=CARTESIAN_POINT('Ctrl Pts',(-40.6065954377991,3.01573769418655,134.689525893634));
#82906=CARTESIAN_POINT('Ctrl Pts',(-40.6143601907462,3.12368517384198,134.605735048134));
#82907=CARTESIAN_POINT('Ctrl Pts',(-40.6221249436933,3.22827959916315,134.517331875483));
#82908=CARTESIAN_POINT('Ctrl Pts',(-40.6298896966404,3.32910370877294,134.42461634869));
#82909=CARTESIAN_POINT('Ctrl Pts',(-40.6376467375254,3.4298276784557,134.331992908265));
#82910=CARTESIAN_POINT('Ctrl Pts',(-40.6454037784103,3.52678849868834,134.23506590017));
#82911=CARTESIAN_POINT('Ctrl Pts',(-40.6531608192953,3.61960073215858,134.134176468669));
#82912=CARTESIAN_POINT('Ctrl Pts',(-40.6609120105354,3.71234297520158,134.033363118673));
#82913=CARTESIAN_POINT('Ctrl Pts',(-40.6686632017757,3.80094259490978,133.928593579458));
#82914=CARTESIAN_POINT('Ctrl Pts',(-40.6764143930158,3.88505015795253,133.820246612211));
#82915=CARTESIAN_POINT('Ctrl Pts',(-40.6841622897929,3.96912197303734,133.711945695314));
#82916=CARTESIAN_POINT('Ctrl Pts',(-40.6919101865699,4.04870528955814,133.600070682735));
#82917=CARTESIAN_POINT('Ctrl Pts',(-40.6996580833469,4.12349037052715,133.485034082699));
#82918=CARTESIAN_POINT('Ctrl Pts',(-40.707404359431,4.1982598080694,133.37002154584));
#82919=CARTESIAN_POINT('Ctrl Pts',(-40.7151506355151,4.2682327934901,133.251849064539));
#82920=CARTESIAN_POINT('Ctrl Pts',(-40.7228969115992,4.33314265640084,133.130958516168));
#82921=CARTESIAN_POINT('Ctrl Pts',(-40.7306432448646,4.39805299846145,133.010067075411));
#82922=CARTESIAN_POINT('Ctrl Pts',(-40.7383895781299,4.45789995848569,132.886457872002));
#82923=CARTESIAN_POINT('Ctrl Pts',(-40.7461359113953,4.51246280663164,132.76059743382));
#82924=CARTESIAN_POINT('Ctrl Pts',(-40.7538839793982,4.56703787374912,132.634708810065));
#82925=CARTESIAN_POINT('Ctrl Pts',(-40.7616320474012,4.61632631880141,132.506568306978));
#82926=CARTESIAN_POINT('Ctrl Pts',(-40.7693801154042,4.66015569614619,132.376662099527));
#82927=CARTESIAN_POINT('Ctrl Pts',(-40.777136418146,4.70403165587479,132.246617826212));
#82928=CARTESIAN_POINT('Ctrl Pts',(-40.7848927208879,4.74243683266572,132.114804470838));
#82929=CARTESIAN_POINT('Ctrl Pts',(-40.7926490236297,4.77524863763722,131.981723565532));
#82930=CARTESIAN_POINT('Ctrl Pts',(-40.8004094661439,4.80807795525697,131.848571630941));
#82931=CARTESIAN_POINT('Ctrl Pts',(-40.808169908658,4.83530787490849,131.71415118137));
#82932=CARTESIAN_POINT('Ctrl Pts',(-40.8159303511722,4.8568672337927,131.578972608056));
#82933=CARTESIAN_POINT('Ctrl Pts',(-40.8237032514376,4.87846120167374,131.443577034096));
#82934=CARTESIAN_POINT('Ctrl Pts',(-40.8314761517031,4.89436637292891,131.307421292971));
#82935=CARTESIAN_POINT('Ctrl Pts',(-40.8392490519686,4.9045635515924,131.171020447506));
#82936=CARTESIAN_POINT('Ctrl Pts',(-40.8467393877306,4.91439003712641,131.039578116345));
#82937=CARTESIAN_POINT('Ctrl Pts',(-40.8542297234927,4.91891631429733,130.907908499613));
#82938=CARTESIAN_POINT('Ctrl Pts',(-40.8617200592547,4.91817091397879,130.776469339485));
#82939=CARTESIAN_POINT('Ctrl Pts',(-40.8694943933738,4.91739725158062,130.640046623651));
#82940=CARTESIAN_POINT('Ctrl Pts',(-40.877268727493,4.91094181844268,130.503440038761));
#82941=CARTESIAN_POINT('Ctrl Pts',(-40.8850430616121,4.8987794675504,130.367161817469));
#82942=CARTESIAN_POINT('Ctrl Pts',(-40.8928078145592,4.88663210566861,130.231051546905));
#82943=CARTESIAN_POINT('Ctrl Pts',(-40.9005725675062,4.86879185455618,130.095269220428));
#82944=CARTESIAN_POINT('Ctrl Pts',(-40.9083373204533,4.84528555003507,129.960328034592));
#82945=CARTESIAN_POINT('Ctrl Pts',(-40.9160943613383,4.82180259230702,129.825520874244));
#82946=CARTESIAN_POINT('Ctrl Pts',(-40.9238514022233,4.79266484701677,129.691553574661));
#82947=CARTESIAN_POINT('Ctrl Pts',(-40.9316084431083,4.75795099021294,129.558934811975));
#82948=CARTESIAN_POINT('Ctrl Pts',(-40.9393596343484,4.72326331139855,129.42641605813));
#82949=CARTESIAN_POINT('Ctrl Pts',(-40.9471108255886,4.68300798944803,129.295244193714));
#82950=CARTESIAN_POINT('Ctrl Pts',(-40.9548620168287,4.63731480962308,129.165917936557));
#82951=CARTESIAN_POINT('Ctrl Pts',(-40.9626099136058,4.5916410506184,129.03664664651));
#82952=CARTESIAN_POINT('Ctrl Pts',(-40.9703578103828,4.54053416058043,128.909219771406));
#82953=CARTESIAN_POINT('Ctrl Pts',(-40.9781057071599,4.4841737739554,128.784120872518));
#82954=CARTESIAN_POINT('Ctrl Pts',(-40.985851983244,4.42782517670834,128.659048141624));
#82955=CARTESIAN_POINT('Ctrl Pts',(-40.9935982593281,4.3662254291755,128.536302774585));
#82956=CARTESIAN_POINT('Ctrl Pts',(-41.0013445354122,4.29960215344792,128.416347974265));
#82957=CARTESIAN_POINT('Ctrl Pts',(-41.0090908686776,4.23297838592236,128.296392288466));
#82958=CARTESIAN_POINT('Ctrl Pts',(-41.0168372019429,4.16133120603621,128.179227552278));
#82959=CARTESIAN_POINT('Ctrl Pts',(-41.0245835352083,4.08493380703481,128.065291641683));
#82960=CARTESIAN_POINT('Ctrl Pts',(-41.0323316032113,4.00851929936571,127.951330215931));
#82961=CARTESIAN_POINT('Ctrl Pts',(-41.0400796712143,3.92735267347948,127.840599379263));
#82962=CARTESIAN_POINT('Ctrl Pts',(-41.0478277392172,3.84174975106248,127.733507004528));
#82963=CARTESIAN_POINT('Ctrl Pts',(-41.0555840419591,3.75605584884073,127.626300810741));
#82964=CARTESIAN_POINT('Ctrl Pts',(-41.0633403447009,3.66591647597003,127.522741109516));
#82965=CARTESIAN_POINT('Ctrl Pts',(-41.0710966474428,3.57168732334919,127.423202128715));
#82966=CARTESIAN_POINT('Ctrl Pts',(-41.0788570899569,3.47740787779242,127.323610020964));
#82967=CARTESIAN_POINT('Ctrl Pts',(-41.0866175324712,3.37903458328288,127.228043181974));
#82968=CARTESIAN_POINT('Ctrl Pts',(-41.0943779749853,3.27695838119108,127.136837361956));
#82969=CARTESIAN_POINT('Ctrl Pts',(-41.1021508752508,3.17471831731777,127.045485130258));
#82970=CARTESIAN_POINT('Ctrl Pts',(-41.1099237755162,3.06876376974749,126.958508155357));
#82971=CARTESIAN_POINT('Ctrl Pts',(-41.1176966757817,2.959517699532,126.876200991398));
#82972=CARTESIAN_POINT('Ctrl Pts',(-41.1251870115437,2.85424299914339,126.796885900169));
#82973=CARTESIAN_POINT('Ctrl Pts',(-41.1326773473057,2.74591218488185,126.721907170942));
#82974=CARTESIAN_POINT('Ctrl Pts',(-41.1401676830677,2.63492578983711,126.651488220712));
#82975=CARTESIAN_POINT('Ctrl Pts',(-41.1479420171867,2.51973131189035,126.578399314581));
#82976=CARTESIAN_POINT('Ctrl Pts',(-41.1557163513058,2.40131100382872,126.509991257373));
#82977=CARTESIAN_POINT('Ctrl Pts',(-41.1634906854249,2.28008222891679,126.446562080245));
#82978=CARTESIAN_POINT('Ctrl Pts',(-41.171255438372,2.15900285763557,126.383211073909));
#82979=CARTESIAN_POINT('Ctrl Pts',(-41.1790201913191,2.03512224931721,126.324826918304));
#82980=CARTESIAN_POINT('Ctrl Pts',(-41.1867849442662,1.90888667617337,126.271664430965));
#82981=CARTESIAN_POINT('Ctrl Pts',(-41.1945419851512,1.78277648198039,126.218554745357));
#82982=CARTESIAN_POINT('Ctrl Pts',(-41.2022990260361,1.65431633563104,126.170656557936));
#82983=CARTESIAN_POINT('Ctrl Pts',(-41.2100560669211,1.52397672708972,126.128178628187));
#82984=CARTESIAN_POINT('Ctrl Pts',(-41.2178072581612,1.39373540866109,126.085732731376));
#82985=CARTESIAN_POINT('Ctrl Pts',(-41.2255584494014,1.26161781934262,126.048699077056));
#82986=CARTESIAN_POINT('Ctrl Pts',(-41.2333096406415,1.12811369667322,126.017238042378));
#82987=CARTESIAN_POINT('Ctrl Pts',(-41.2410575374186,0.99466631681729,125.985790379479));
#82988=CARTESIAN_POINT('Ctrl Pts',(-41.2488054341957,0.859833955455193,
125.959910714922));
#82989=CARTESIAN_POINT('Ctrl Pts',(-41.2565533309727,0.72412054318671,125.939709293839));
#82990=CARTESIAN_POINT('Ctrl Pts',(-41.2642996070568,0.588435519238431,
125.919512098459));
#82991=CARTESIAN_POINT('Ctrl Pts',(-41.2720458831409,0.451870197419816,
125.904990841547));
#82992=CARTESIAN_POINT('Ctrl Pts',(-41.279792159225,0.314937318719655,125.896204390654));
#82993=CARTESIAN_POINT('Ctrl Pts',(-41.2875384924904,0.17800342921209,125.887417874901));
#82994=CARTESIAN_POINT('Ctrl Pts',(-41.2952848257557,0.0407023675717651,
125.884366274676));
#82995=CARTESIAN_POINT('Ctrl Pts',(-41.3030311590211,-0.0964498011149574,
125.887056427426));
#82996=CARTESIAN_POINT('Ctrl Pts',(-41.310779227024,-0.233632684078911,
125.889747182618));
#82997=CARTESIAN_POINT('Ctrl Pts',(-41.3185272950269,-0.370666216924256,
125.898182241764));
#82998=CARTESIAN_POINT('Ctrl Pts',(-41.3262753630299,-0.507036535337007,
125.912316360373));
#82999=CARTESIAN_POINT('Ctrl Pts',(-41.3340316657718,-0.643551789746993,
125.926465500891));
#83000=CARTESIAN_POINT('Ctrl Pts',(-41.3417879685136,-0.779402032164128,
125.946325760069));
#83001=CARTESIAN_POINT('Ctrl Pts',(-41.3495442712555,-0.914080154468566,
125.971800164379));
#83002=CARTESIAN_POINT('Ctrl Pts',(-41.3573047137696,-1.04883015854214,
125.997288165146));
#83003=CARTESIAN_POINT('Ctrl Pts',(-41.3650651562838,-1.18240641536105,
126.02839619307));
#83004=CARTESIAN_POINT('Ctrl Pts',(-41.372825598798,-1.31431513540615,126.064976819292));
#83005=CARTESIAN_POINT('Ctrl Pts',(-41.3805984990634,-1.44643560703898,
126.101616167983));
#83006=CARTESIAN_POINT('Ctrl Pts',(-41.3883713993288,-1.57688282038497,
126.143745550177));
#83007=CARTESIAN_POINT('Ctrl Pts',(-41.3961442995943,-1.70518033791856,
126.191168330475));
#83008=CARTESIAN_POINT('Ctrl Pts',(-41.4036346353563,-1.82881391752839,
126.236867173258));
#83009=CARTESIAN_POINT('Ctrl Pts',(-41.4111249711184,-1.9504510971713,126.287481120781));
#83010=CARTESIAN_POINT('Ctrl Pts',(-41.4186153068805,-2.06968741188378,
126.342793955553));
#83011=CARTESIAN_POINT('Ctrl Pts',(-41.4263902653792,-2.19345454701301,
126.400208604035));
#83012=CARTESIAN_POINT('Ctrl Pts',(-41.4341652238779,-2.31502683861591,
126.462868190964));
#83013=CARTESIAN_POINT('Ctrl Pts',(-41.4419401823766,-2.43392783549776,
126.530582622151));
#83014=CARTESIAN_POINT('Ctrl Pts',(-41.4497054190613,-2.55268015848356,
126.598212383163));
#83015=CARTESIAN_POINT('Ctrl Pts',(-41.457470655746,-2.66876749656911,126.670884219826));
#83016=CARTESIAN_POINT('Ctrl Pts',(-41.4652358924307,-2.78173416079713,
126.748360356083));
#83017=CARTESIAN_POINT('Ctrl Pts',(-41.4729932770136,-2.89458659466821,
126.825758149522));
#83018=CARTESIAN_POINT('Ctrl Pts',(-41.4807506615965,-3.00432431453443,
126.907950354258));
#83019=CARTESIAN_POINT('Ctrl Pts',(-41.4885080461793,-3.11051732110719,
126.994653928385));
#83020=CARTESIAN_POINT('Ctrl Pts',(-41.4962589928004,-3.21662219662083,
127.081285546004));
#83021=CARTESIAN_POINT('Ctrl Pts',(-41.5040099394213,-3.3191879152424,127.172420831183));
#83022=CARTESIAN_POINT('Ctrl Pts',(-41.5117608860424,-3.41781487530316,
127.267734465333));
#83023=CARTESIAN_POINT('Ctrl Pts',(-41.5195083337016,-3.51639731280616,
127.36300507264));
#83024=CARTESIAN_POINT('Ctrl Pts',(-41.5272557813608,-3.61104424889036,
127.462450005041));
#83025=CARTESIAN_POINT('Ctrl Pts',(-41.53500322902,-3.70139061247776,127.565704940227));
#83026=CARTESIAN_POINT('Ctrl Pts',(-41.5427488570747,-3.7917157568632,127.668935624439));
#83027=CARTESIAN_POINT('Ctrl Pts',(-41.5504944851293,-3.87774208194308,
127.77597423644));
#83028=CARTESIAN_POINT('Ctrl Pts',(-41.5582401131839,-3.95914299596626,
127.886421310454));
#83029=CARTESIAN_POINT('Ctrl Pts',(-41.5659855994087,-4.04054241946133,
127.996866362076));
#83030=CARTESIAN_POINT('Ctrl Pts',(-41.5737310856335,-4.11731636978816,
128.110719436078));
#83031=CARTESIAN_POINT('Ctrl Pts',(-41.5814765718583,-4.18918024022112,
128.227550190421));
#83032=CARTESIAN_POINT('Ctrl Pts',(-41.5892267892329,-4.26108800702499,
128.344452308109));
#83033=CARTESIAN_POINT('Ctrl Pts',(-41.5969770066076,-4.3280794971936,128.464335406502));
#83034=CARTESIAN_POINT('Ctrl Pts',(-41.6047272239822,-4.38991482252266,
128.586742320046));
#83035=CARTESIAN_POINT('Ctrl Pts',(-41.6124799930164,-4.45177050633902,
128.709189534495));
#83036=CARTESIAN_POINT('Ctrl Pts',(-41.6202327620507,-4.50846647793683,
128.834161865338));
#83037=CARTESIAN_POINT('Ctrl Pts',(-41.6279855310849,-4.55981048029157,
128.961180906761));
#83038=CARTESIAN_POINT('Ctrl Pts',(-41.6357466300772,-4.61120964917867,
129.088336423717));
#83039=CARTESIAN_POINT('Ctrl Pts',(-41.6435077290694,-4.65724522892415,
129.217542676514));
#83040=CARTESIAN_POINT('Ctrl Pts',(-41.6512688280616,-4.69777430233468,
129.348304414384));
#83041=CARTESIAN_POINT('Ctrl Pts',(-41.6558716557719,-4.72181063305927,
129.425854481857));
#83042=CARTESIAN_POINT('Ctrl Pts',(-41.6604744834821,-4.74391114867854,
129.50395138814));
#83043=CARTESIAN_POINT('Ctrl Pts',(-41.6650773111923,-4.76405452823405,
129.582490119308));
#83044=CARTESIAN_POINT('Ctrl Pts',(-39.9150204635388,-4.76405452823403,
129.582490119308));
#83045=CARTESIAN_POINT('Ctrl Pts',(-39.9226601301531,-4.79766750777594,
129.713546616394));
#83046=CARTESIAN_POINT('Ctrl Pts',(-39.9302997967672,-4.82585041976442,
129.845921259423));
#83047=CARTESIAN_POINT('Ctrl Pts',(-39.9379394633814,-4.84852111043041,
129.979117559909));
#83048=CARTESIAN_POINT('Ctrl Pts',(-39.9458063134806,-4.87186596749284,
130.116274766186));
#83049=CARTESIAN_POINT('Ctrl Pts',(-39.9536731635798,-4.88936559114322,
130.254302799531));
#83050=CARTESIAN_POINT('Ctrl Pts',(-39.961540013679,-4.90098781854546,130.392655061411));
#83051=CARTESIAN_POINT('Ctrl Pts',(-39.9694068637782,-4.91261004594769,
130.531007323291));
#83052=CARTESIAN_POINT('Ctrl Pts',(-39.9772737138774,-4.91835491299647,
130.669683350103));
#83053=CARTESIAN_POINT('Ctrl Pts',(-39.9851405639765,-4.91824854872011,
130.808138912485));
#83054=CARTESIAN_POINT('',(-39.6398594360423,-4.91824987188027,130.80548322601));
#83055=CARTESIAN_POINT('Ctrl Pts',(-39.5701139254339,-4.76405452823409,
129.582490119308));
#83056=CARTESIAN_POINT('Ctrl Pts',(-39.5781133945864,-4.79919294448669,
129.719494270977));
#83057=CARTESIAN_POINT('Ctrl Pts',(-39.5861128637389,-4.82844873500477,
129.858138048181));
#83058=CARTESIAN_POINT('Ctrl Pts',(-39.5941123328914,-4.85167949962034,
129.997893572075));
#83059=CARTESIAN_POINT('Ctrl Pts',(-39.6021025955522,-4.87488352823167,
130.137488253037));
#83060=CARTESIAN_POINT('Ctrl Pts',(-39.6100928582131,-4.89207629594091,
130.278191781637));
#83061=CARTESIAN_POINT('Ctrl Pts',(-39.6180831208739,-4.90316615218488,
130.419464856913));
#83062=CARTESIAN_POINT('Ctrl Pts',(-39.6253418925796,-4.91324075650532,
130.547804693176));
#83063=CARTESIAN_POINT('Ctrl Pts',(-39.6326006642854,-4.91827928667657,
130.67661421901));
#83064=CARTESIAN_POINT('Ctrl Pts',(-39.6398594359911,-4.91824987188048,
130.8054832251));
#83065=CARTESIAN_POINT('Ctrl Pts',(-39.6398594360424,-4.91824987188027,
130.80548322601));
#83066=CARTESIAN_POINT('Ctrl Pts',(-39.6481290507699,-4.91821636080731,
130.952298289754));
#83067=CARTESIAN_POINT('Ctrl Pts',(-39.6563986654975,-4.9116047325426,131.098940220869));
#83068=CARTESIAN_POINT('Ctrl Pts',(-39.6646682802251,-4.89848671975691,
131.244827323306));
#83069=CARTESIAN_POINT('Ctrl Pts',(-39.6732391368865,-4.88489084969848,
131.396028737753));
#83070=CARTESIAN_POINT('Ctrl Pts',(-39.681809993548,-4.86430572391944,131.546418918438));
#83071=CARTESIAN_POINT('Ctrl Pts',(-39.6903808502094,-4.83686829731992,
131.695364622541));
#83072=CARTESIAN_POINT('Ctrl Pts',(-39.6986930973762,-4.81025874351182,
131.839816169898));
#83073=CARTESIAN_POINT('Ctrl Pts',(-39.707005344543,-4.77720456139641,131.982908891268));
#83074=CARTESIAN_POINT('Ctrl Pts',(-39.7153175917098,-4.73788102594566,
132.124082727135));
#83075=CARTESIAN_POINT('Ctrl Pts',(-39.7240177531187,-4.69672234782602,
132.271844834553));
#83076=CARTESIAN_POINT('Ctrl Pts',(-39.7327179145274,-4.64869527844162,
132.417504279031));
#83077=CARTESIAN_POINT('Ctrl Pts',(-39.7414180759363,-4.59405636483465,
132.560444094859));
#83078=CARTESIAN_POINT('Ctrl Pts',(-39.7501182373451,-4.53941745122775,
132.703383910688));
#83079=CARTESIAN_POINT('Ctrl Pts',(-39.7588183987539,-4.47816691515689,
132.84360378822));
#83080=CARTESIAN_POINT('Ctrl Pts',(-39.7675185601628,-4.41061504991322,
132.980517308611));
#83081=CARTESIAN_POINT('Ctrl Pts',(-39.7752928942818,-4.35025171340783,
133.102861182813));
#83082=CARTESIAN_POINT('Ctrl Pts',(-39.783067228401,-4.28469845338574,133.222885354349));
#83083=CARTESIAN_POINT('Ctrl Pts',(-39.7908415625201,-4.2141566923093,133.340118183889));
#83084=CARTESIAN_POINT('Ctrl Pts',(-39.7986063154672,-4.14370186764889,
133.457206534444));
#83085=CARTESIAN_POINT('Ctrl Pts',(-39.8063710684142,-4.06827097402557,
133.571510055957));
#83086=CARTESIAN_POINT('Ctrl Pts',(-39.8141358213613,-3.98811260262222,
133.682578978168));
#83087=CARTESIAN_POINT('Ctrl Pts',(-39.8218928622463,-3.90803384564349,
133.793537585159));
#83088=CARTESIAN_POINT('Ctrl Pts',(-39.8296499031313,-3.82323718225476,
133.901267671191));
#83089=CARTESIAN_POINT('Ctrl Pts',(-39.8374069440163,-3.7340158454221,134.005346204637));
#83090=CARTESIAN_POINT('Ctrl Pts',(-39.8451581352565,-3.64486179109347,
134.109346251651));
#83091=CARTESIAN_POINT('Ctrl Pts',(-39.8529093264966,-3.55128995820697,
134.209699931454));
#83092=CARTESIAN_POINT('Ctrl Pts',(-39.8606605177367,-3.45363518574191,
134.306015521509));
#83093=CARTESIAN_POINT('Ctrl Pts',(-39.8684084145138,-3.35602191916003,
134.402290174868));
#83094=CARTESIAN_POINT('Ctrl Pts',(-39.8761563112909,-3.25432944226823,
134.494529878097));
#83095=CARTESIAN_POINT('Ctrl Pts',(-39.883904208068,-3.14893079336533,134.582378341333));
#83096=CARTESIAN_POINT('Ctrl Pts',(-39.8916504841521,-3.04355419158781,
134.670208428563));
#83097=CARTESIAN_POINT('Ctrl Pts',(-39.8993967602362,-2.93447325995125,
134.753648852694));
#83098=CARTESIAN_POINT('Ctrl Pts',(-39.9071430363203,-2.82209528687978,
134.83238262027));
#83099=CARTESIAN_POINT('Ctrl Pts',(-39.9148893695857,-2.70971648425965,
134.911116969042));
#83100=CARTESIAN_POINT('Ctrl Pts',(-39.922635702851,-2.59404091183839,134.985144367595));
#83101=CARTESIAN_POINT('Ctrl Pts',(-39.9303820361164,-2.47550576198666,
135.05419053003));
#83102=CARTESIAN_POINT('Ctrl Pts',(-39.9381301041194,-2.35694406700999,
135.123252154874));
#83103=CARTESIAN_POINT('Ctrl Pts',(-39.9458781721224,-2.23552185808173,
135.18733012711));
#83104=CARTESIAN_POINT('Ctrl Pts',(-39.9536262401253,-2.11170153993017,
135.246195786588));
#83105=CARTESIAN_POINT('Ctrl Pts',(-39.9613825428672,-1.98774962407101,
135.305124009189));
#83106=CARTESIAN_POINT('Ctrl Pts',(-39.9691388456091,-1.86139486126452,
135.358828684735));
#83107=CARTESIAN_POINT('Ctrl Pts',(-39.976895148351,-1.73312079443059,135.407128847057));
#83108=CARTESIAN_POINT('Ctrl Pts',(-39.9846555908651,-1.60477826386476,
135.45545478863));
#83109=CARTESIAN_POINT('Ctrl Pts',(-39.9924160333793,-1.47451475923758,
135.49837034699));
#83110=CARTESIAN_POINT('Ctrl Pts',(-40.0001764758935,-1.34282869443821,
135.535744575764));
#83111=CARTESIAN_POINT('Ctrl Pts',(-40.0079493761589,-1.21093123547708,
135.573178800968));
#83112=CARTESIAN_POINT('Ctrl Pts',(-40.0157222764243,-1.07760703341135,
135.605053829711));
#83113=CARTESIAN_POINT('Ctrl Pts',(-40.0234951766897,-0.94336527875647,
135.631289766967));
#83114=CARTESIAN_POINT('Ctrl Pts',(-40.0309855124517,-0.814003550019504,
135.656571961819));
#83115=CARTESIAN_POINT('Ctrl Pts',(-40.0384758482137,-0.683790125625639,
135.676617890641));
#83116=CARTESIAN_POINT('Ctrl Pts',(-40.0459661839756,-0.553182913605547,
135.691401821259));
#83117=CARTESIAN_POINT('Ctrl Pts',(-40.0537405180947,-0.417623689442982,
135.7067462891));
#83118=CARTESIAN_POINT('Ctrl Pts',(-40.0615148522138,-0.281210816399245,
135.716470471348));
#83119=CARTESIAN_POINT('Ctrl Pts',(-40.0692891863329,-0.144449971760837,
135.720488897845));
#83120=CARTESIAN_POINT('Ctrl Pts',(-40.0770539392799,-0.00785767264096399,
135.724502371991));
#83121=CARTESIAN_POINT('Ctrl Pts',(-40.0848186922271,0.12908135775712,135.722824070268));
#83122=CARTESIAN_POINT('Ctrl Pts',(-40.0925834451741,0.265854345368811,
135.715420027668));
#83123=CARTESIAN_POINT('Ctrl Pts',(-40.1003404860591,0.402491488121046,
135.708023338867));
#83124=CARTESIAN_POINT('Ctrl Pts',(-40.1080975269441,0.538962528409856,
135.694912247346));
#83125=CARTESIAN_POINT('Ctrl Pts',(-40.1158545678291,0.674753058165272,
135.676104799376));
#83126=CARTESIAN_POINT('Ctrl Pts',(-40.1236057590692,0.810441187225903,
135.657311534249));
#83127=CARTESIAN_POINT('Ctrl Pts',(-40.1313569503093,0.945449441502048,
135.632830516358));
#83128=CARTESIAN_POINT('Ctrl Pts',(-40.1391081415495,1.07926726508193,135.60273171962));
#83129=CARTESIAN_POINT('Ctrl Pts',(-40.1468560383265,1.21302821251708,135.572645715673));
#83130=CARTESIAN_POINT('Ctrl Pts',(-40.1546039351036,1.34559935494425,135.536946767459));
#83131=CARTESIAN_POINT('Ctrl Pts',(-40.1623518318806,1.47647929929888,135.495756139289));
#83132=CARTESIAN_POINT('Ctrl Pts',(-40.1700981079647,1.60733186639079,135.45457412731));
#83133=CARTESIAN_POINT('Ctrl Pts',(-40.1778443840488,1.73649356636687,135.40790283758));
#83134=CARTESIAN_POINT('Ctrl Pts',(-40.1855906601329,1.86347755431497,135.35591359068));
#83135=CARTESIAN_POINT('Ctrl Pts',(-40.1933369933983,1.99046247962985,135.303923960007));
#83136=CARTESIAN_POINT('Ctrl Pts',(-40.2010833266636,2.11526929902405,135.246616441965));
#83137=CARTESIAN_POINT('Ctrl Pts',(-40.2088296599289,2.23743093484609,135.184210600647));
#83138=CARTESIAN_POINT('Ctrl Pts',(-40.2165777279319,2.35961992791946,135.121790783974));
#83139=CARTESIAN_POINT('Ctrl Pts',(-40.2243257959349,2.47916221057224,135.054270549932));
#83140=CARTESIAN_POINT('Ctrl Pts',(-40.2320738639379,2.59561546349312,134.981915336319));
#83141=CARTESIAN_POINT('Ctrl Pts',(-40.2398301666797,2.71219248431702,134.909483222724));
#83142=CARTESIAN_POINT('Ctrl Pts',(-40.2475864694216,2.82567358453307,134.832206071165));
#83143=CARTESIAN_POINT('Ctrl Pts',(-40.2553427721634,2.93564514541842,134.750392883359));
#83144=CARTESIAN_POINT('Ctrl Pts',(-40.2631032146776,3.04567540143714,134.668536029392));
#83145=CARTESIAN_POINT('Ctrl Pts',(-40.2708636571918,3.15219208223108,134.58213856126));
#83146=CARTESIAN_POINT('Ctrl Pts',(-40.278624099706,3.25481561402661,134.49154902897));
#83147=CARTESIAN_POINT('Ctrl Pts',(-40.2863969999714,3.35760388622587,134.40081407432));
#83148=CARTESIAN_POINT('Ctrl Pts',(-40.2941699002368,3.45648623849685,134.305873878812));
#83149=CARTESIAN_POINT('Ctrl Pts',(-40.3019428005022,3.55112022297843,134.207113653632));
#83150=CARTESIAN_POINT('Ctrl Pts',(-40.3094331362643,3.64231402375677,134.111943611398));
#83151=CARTESIAN_POINT('Ctrl Pts',(-40.3169234720264,3.72956276793215,134.013226683794));
#83152=CARTESIAN_POINT('Ctrl Pts',(-40.3244138077886,3.81259729582122,133.911334212947));
#83153=CARTESIAN_POINT('Ctrl Pts',(-40.3321881419077,3.89878010307179,133.8055784581));
#83154=CARTESIAN_POINT('Ctrl Pts',(-40.3399624760268,3.98069582294925,133.696066602626));
#83155=CARTESIAN_POINT('Ctrl Pts',(-40.3477368101459,4.05799921606556,133.583177888441));
#83156=CARTESIAN_POINT('Ctrl Pts',(-40.355501563093,4.13520733965865,133.470428299506));
#83157=CARTESIAN_POINT('Ctrl Pts',(-40.36326631604,4.20781422773934,133.354310451841));
#83158=CARTESIAN_POINT('Ctrl Pts',(-40.3710310689871,4.27551413767626,133.235237397872));
#83159=CARTESIAN_POINT('Ctrl Pts',(-40.3787881098721,4.34314680710823,133.116282608938));
#83160=CARTESIAN_POINT('Ctrl Pts',(-40.3865451507571,4.40588200525265,132.994378792459));
#83161=CARTESIAN_POINT('Ctrl Pts',(-40.3943021916421,4.46345686482174,132.869968488963));
#83162=CARTESIAN_POINT('Ctrl Pts',(-40.4020533828823,4.52098830674137,132.745652004244));
#83163=CARTESIAN_POINT('Ctrl Pts',(-40.4098045741223,4.57336699224735,132.618833148137));
#83164=CARTESIAN_POINT('Ctrl Pts',(-40.4175557653624,4.62037582443633,132.4899792884));
#83165=CARTESIAN_POINT('Ctrl Pts',(-40.4253036621395,4.66736467661769,132.361180194991));
#83166=CARTESIAN_POINT('Ctrl Pts',(-40.4330515589168,4.70898808115027,132.230348184752));
#83167=CARTESIAN_POINT('Ctrl Pts',(-40.4407994556938,4.74507704593572,132.09797064019));
#83168=CARTESIAN_POINT('Ctrl Pts',(-40.448545731778,4.78115846168768,131.965620786158));
#83169=CARTESIAN_POINT('Ctrl Pts',(-40.456292007862,4.81170763762495,131.83172641781));
#83170=CARTESIAN_POINT('Ctrl Pts',(-40.4640382839461,4.83660555903792,131.696789734518));
#83171=CARTESIAN_POINT('Ctrl Pts',(-40.4717846172115,4.86150366424168,131.561852055154));
#83172=CARTESIAN_POINT('Ctrl Pts',(-40.4795309504768,4.88075036073767,131.425872429969));
#83173=CARTESIAN_POINT('Ctrl Pts',(-40.4872772837422,4.89427790713727,131.289362504375));
#83174=CARTESIAN_POINT('Ctrl Pts',(-40.4950253517452,4.90780848293709,131.152822008329));
#83175=CARTESIAN_POINT('Ctrl Pts',(-40.5027734197482,4.91561732152165,131.015751364547));
#83176=CARTESIAN_POINT('Ctrl Pts',(-40.5105214877512,4.91768865883524,130.878666184405));
#83177=CARTESIAN_POINT('Ctrl Pts',(-40.5182777904931,4.91976219759078,130.741435308502));
#83178=CARTESIAN_POINT('Ctrl Pts',(-40.5260340932349,4.91608604797777,130.604190256921));
#83179=CARTESIAN_POINT('Ctrl Pts',(-40.5337903959767,4.90669661087029,130.467446041784));
#83180=CARTESIAN_POINT('Ctrl Pts',(-40.5415508384909,4.89730216233751,130.330628842143));
#83181=CARTESIAN_POINT('Ctrl Pts',(-40.5493112810051,4.88218839327771,130.194313399981));
#83182=CARTESIAN_POINT('Ctrl Pts',(-40.5570717235192,4.86144337978754,130.059007461257));
#83183=CARTESIAN_POINT('Ctrl Pts',(-40.5648446237847,4.84066506456003,129.923484317428));
#83184=CARTESIAN_POINT('Ctrl Pts',(-40.5726175240501,4.81423751597063,129.788974299253));
#83185=CARTESIAN_POINT('Ctrl Pts',(-40.5803904243155,4.78229972166743,129.655973733872));
#83186=CARTESIAN_POINT('Ctrl Pts',(-40.5878807600775,4.75152294663399,129.527808074053));
#83187=CARTESIAN_POINT('Ctrl Pts',(-40.5953710958395,4.71562967702933,129.401044323904));
#83188=CARTESIAN_POINT('Ctrl Pts',(-40.6028614316014,4.67478684611728,129.27610965458));
#83189=CARTESIAN_POINT('Ctrl Pts',(-40.6106357657205,4.63239544685687,129.146438049293));
#83190=CARTESIAN_POINT('Ctrl Pts',(-40.6184100998396,4.58453746880618,129.018326201327));
#83191=CARTESIAN_POINT('Ctrl Pts',(-40.6261844339586,4.53134536860734,128.892269559875));
#83192=CARTESIAN_POINT('Ctrl Pts',(-40.6339491869057,4.47821882291807,128.766368271968));
#83193=CARTESIAN_POINT('Ctrl Pts',(-40.6417139398528,4.41977138557886,128.642517507693));
#83194=CARTESIAN_POINT('Ctrl Pts',(-40.6494786927999,4.35618530793343,128.521197761911));
#83195=CARTESIAN_POINT('Ctrl Pts',(-40.6572357336849,4.29266238487672,128.39999851261));
#83196=CARTESIAN_POINT('Ctrl Pts',(-40.6649927745699,4.22401115856685,128.281325623185));
#83197=CARTESIAN_POINT('Ctrl Pts',(-40.6727498154549,4.1504618646939,128.165639455294));
#83198=CARTESIAN_POINT('Ctrl Pts',(-40.680501006695,4.0769680349156,128.050040527243));
#83199=CARTESIAN_POINT('Ctrl Pts',(-40.6882521979351,3.9985836985125,127.937424166236));
#83200=CARTESIAN_POINT('Ctrl Pts',(-40.6960033891752,3.91558471903809,127.828225645738));
#83201=CARTESIAN_POINT('Ctrl Pts',(-40.7037512859523,3.83262101634403,127.719073537525));
#83202=CARTESIAN_POINT('Ctrl Pts',(-40.7114991827294,3.74504680763295,127.613336691172));
#83203=CARTESIAN_POINT('Ctrl Pts',(-40.7192470795065,3.65318079725539,127.511420726668));
#83204=CARTESIAN_POINT('Ctrl Pts',(-40.7269933555906,3.5613340032668,127.409526080788));
#83205=CARTESIAN_POINT('Ctrl Pts',(-40.7347396316747,3.46519745488942,127.31145101723));
#83206=CARTESIAN_POINT('Ctrl Pts',(-40.7424859077588,3.36512933632013,127.217567117469));
#83207=CARTESIAN_POINT('Ctrl Pts',(-40.7502322410242,3.26506047907071,127.123682524678));
#83208=CARTESIAN_POINT('Ctrl Pts',(-40.7579785742895,3.16106027884223,127.033989424922));
#83209=CARTESIAN_POINT('Ctrl Pts',(-40.7657249075548,3.0535225815357,126.948821367792));
#83210=CARTESIAN_POINT('Ctrl Pts',(-40.7734729755578,2.94596080190748,126.863634237866));
#83211=CARTESIAN_POINT('Ctrl Pts',(-40.7812210435608,2.83486025524777,126.782974409706));
#83212=CARTESIAN_POINT('Ctrl Pts',(-40.7889691115638,2.72064621915353,126.707133846602));
#83213=CARTESIAN_POINT('Ctrl Pts',(-40.7967254143056,2.60631079502256,126.631212679245));
#83214=CARTESIAN_POINT('Ctrl Pts',(-40.8044817170475,2.48885559748517,126.560121225252));
#83215=CARTESIAN_POINT('Ctrl Pts',(-40.8122380197893,2.36873359638736,126.494107236169));
#83216=CARTESIAN_POINT('Ctrl Pts',(-40.8199984623035,2.24854748256076,126.428058013432));
#83217=CARTESIAN_POINT('Ctrl Pts',(-40.8277589048176,2.12569207906489,126.367091829208));
#83218=CARTESIAN_POINT('Ctrl Pts',(-40.8355193473317,2.00064217423662,126.311409031674));
#83219=CARTESIAN_POINT('Ctrl Pts',(-40.8432922475972,1.87539152819971,126.255636847171));
#83220=CARTESIAN_POINT('Ctrl Pts',(-40.8510651478626,1.7479397048465,126.205165141853));
#83221=CARTESIAN_POINT('Ctrl Pts',(-40.858838048128,1.61877940447563,126.160145258418));
#83222=CARTESIAN_POINT('Ctrl Pts',(-40.8663283838901,1.49431440635718,126.116761961144));
#83223=CARTESIAN_POINT('Ctrl Pts',(-40.8738187196522,1.36826328425528,126.078441082079));
#83224=CARTESIAN_POINT('Ctrl Pts',(-40.8813090554143,1.24107566086662,126.045273071985));
#83225=CARTESIAN_POINT('Ctrl Pts',(-40.8890833895334,1.10906568008046,126.010847486707));
#83226=CARTESIAN_POINT('Ctrl Pts',(-40.8968577236525,0.975413147937866,
125.981864175918));
#83227=CARTESIAN_POINT('Ctrl Pts',(-40.9046320577716,0.84060649592791,125.958479502484));
#83228=CARTESIAN_POINT('Ctrl Pts',(-40.9123968107187,0.705965981068539,
125.935123648571));
#83229=CARTESIAN_POINT('Ctrl Pts',(-40.9201615636658,0.570174557907952,
125.917352769608));
#83230=CARTESIAN_POINT('Ctrl Pts',(-40.9279263166129,0.433734991683567,
125.905273251588));
#83231=CARTESIAN_POINT('Ctrl Pts',(-40.9356833574979,0.297430939159817,
125.893205731115));
#83232=CARTESIAN_POINT('Ctrl Pts',(-40.9434403983829,0.160480411575381,
125.886818356632));
#83233=CARTESIAN_POINT('Ctrl Pts',(-40.9511974392679,0.0233951722466785,
125.886166261055));
#83234=CARTESIAN_POINT('Ctrl Pts',(-40.958948630508,-0.113586690036492,
125.885514657228));
#83235=CARTESIAN_POINT('Ctrl Pts',(-40.9666998217481,-0.250702672481956,
125.890589725473));
#83236=CARTESIAN_POINT('Ctrl Pts',(-40.9744510129883,-0.387437456208372,
125.901394649907));
#83237=CARTESIAN_POINT('Ctrl Pts',(-40.9821989097653,-0.52411412400437,
125.912194981959));
#83238=CARTESIAN_POINT('Ctrl Pts',(-40.9899468065424,-0.66040952639174,
125.928720295759));
#83239=CARTESIAN_POINT('Ctrl Pts',(-40.9976947033195,-0.795810136299649,
125.95092170382));
#83240=CARTESIAN_POINT('Ctrl Pts',(-41.0054409794036,-0.931182423318865,
125.973118467826));
#83241=CARTESIAN_POINT('Ctrl Pts',(-41.0131872554878,-1.06565990458383,
126.000988901235));
#83242=CARTESIAN_POINT('Ctrl Pts',(-41.0209335315719,-1.19873635076984,
126.034432502401));
#83243=CARTESIAN_POINT('Ctrl Pts',(-41.0286798648372,-1.33181377929576,
126.06787635044));
#83244=CARTESIAN_POINT('Ctrl Pts',(-41.0364261981025,-1.46348977293108,
126.106893353037));
#83245=CARTESIAN_POINT('Ctrl Pts',(-41.0441725313679,-1.59327082362771,
126.151332448182));
#83246=CARTESIAN_POINT('Ctrl Pts',(-41.0519205993709,-1.72308093789099,
126.195781495155));
#83247=CARTESIAN_POINT('Ctrl Pts',(-41.0596686673738,-1.85099489497844,
126.245654924245));
#83248=CARTESIAN_POINT('Ctrl Pts',(-41.0674167353768,-1.97653718497606,
126.300752750655));
#83249=CARTESIAN_POINT('Ctrl Pts',(-41.0751730381187,-2.10221290281345,
126.35590913569));
#83250=CARTESIAN_POINT('Ctrl Pts',(-41.0829293408606,-2.22551155974407,
126.416300852494));
#83251=CARTESIAN_POINT('Ctrl Pts',(-41.0906856436024,-2.34597987410962,
126.481680720468));
#83252=CARTESIAN_POINT('Ctrl Pts',(-41.0984460861166,-2.46651248604193,
126.547095483647));
#83253=CARTESIAN_POINT('Ctrl Pts',(-41.1062065286308,-2.58421140998175,
126.617503502299));
#83254=CARTESIAN_POINT('Ctrl Pts',(-41.113966971145,-2.69865145263887,126.692613616634));
#83255=CARTESIAN_POINT('Ctrl Pts',(-41.1217398714104,-2.81327520461181,
126.767844304393));
#83256=CARTESIAN_POINT('Ctrl Pts',(-41.1295127716758,-2.92462930343529,
126.847791943439));
#83257=CARTESIAN_POINT('Ctrl Pts',(-41.1372856719413,-3.03232010366483,
126.932123815482));
#83258=CARTESIAN_POINT('Ctrl Pts',(-41.1447760077032,-3.13609607204853,
127.013390011558));
#83259=CARTESIAN_POINT('Ctrl Pts',(-41.1522663434652,-3.23647022337348,
127.09872701936));
#83260=CARTESIAN_POINT('Ctrl Pts',(-41.1597566792272,-3.33312342680312,
127.187805449427));
#83261=CARTESIAN_POINT('Ctrl Pts',(-41.1674134037402,-3.43192366426608,
127.278862649096));
#83262=CARTESIAN_POINT('Ctrl Pts',(-41.1750701282532,-3.52716869389441,
127.37413670988));
#83263=CARTESIAN_POINT('Ctrl Pts',(-41.1827268527662,-3.61846879384522,
127.473314738196));
#83264=CARTESIAN_POINT('Ctrl Pts',(-41.1903747179501,-3.70966325363188,
127.572378011072));
#83265=CARTESIAN_POINT('Ctrl Pts',(-41.198022583134,-3.79692158697122,127.67533597854));
#83266=CARTESIAN_POINT('Ctrl Pts',(-41.2056704483179,-3.87988773714554,
127.781836141297));
#83267=CARTESIAN_POINT('Ctrl Pts',(-41.2133112386969,-3.96277713788632,
127.888237784029));
#83268=CARTESIAN_POINT('Ctrl Pts',(-41.220952029076,-4.04138200396901,127.998174790541));
#83269=CARTESIAN_POINT('Ctrl Pts',(-41.2285928194551,-4.11538411119943,
128.111258933673));
#83270=CARTESIAN_POINT('Ctrl Pts',(-41.2362283501721,-4.18933527787853,
128.2242652335));
#83271=CARTESIAN_POINT('Ctrl Pts',(-41.243863880889,-4.2586897672421,128.340414024735));
#83272=CARTESIAN_POINT('Ctrl Pts',(-41.251499411606,-4.32317089112018,128.45928567022));
#83273=CARTESIAN_POINT('Ctrl Pts',(-41.2591316827896,-4.38762448863661,
128.578106570561));
#83274=CARTESIAN_POINT('Ctrl Pts',(-41.2667639539732,-4.44720866698158,
128.699647658746));
#83275=CARTESIAN_POINT('Ctrl Pts',(-41.2743962251567,-4.50169145460962,
128.823462561129));
#83276=CARTESIAN_POINT('Ctrl Pts',(-41.2820290199258,-4.55617797984057,
128.947285957405));
#83277=CARTESIAN_POINT('Ctrl Pts',(-41.2896618146949,-4.60556224143734,
129.073383114953));
#83278=CARTESIAN_POINT('Ctrl Pts',(-41.2972946094639,-4.64965950561795,
129.201285589903));
#83279=CARTESIAN_POINT('Ctrl Pts',(-41.3047830462557,-4.69292276442373,
129.326769063277));
#83280=CARTESIAN_POINT('Ctrl Pts',(-41.3122714830475,-4.73109715056116,
129.45398980396));
#83281=CARTESIAN_POINT('Ctrl Pts',(-41.3197599198393,-4.76405452823403,
129.582490119308));
#83282=CARTESIAN_POINT('Origin',(213.235140564004,0.,130.804360617566));
#83283=CARTESIAN_POINT('',(-43.4154178838317,-4.76405452823406,129.582490119308));
#83284=CARTESIAN_POINT('',(-43.0697814015304,-4.7640545282341,129.582490119308));
#83285=CARTESIAN_POINT('',(213.235140564004,-4.76405452823405,129.582490119308));
#83286=CARTESIAN_POINT('',(-41.7351405640431,-4.91824869491783,130.800777680352));
#83287=CARTESIAN_POINT('Ctrl Pts',(-41.7351405640431,-4.91824869491783,
130.800777680352));
#83288=CARTESIAN_POINT('Ctrl Pts',(-41.7427950097377,-4.91834679994633,
130.935445105295));
#83289=CARTESIAN_POINT('Ctrl Pts',(-41.7504494554324,-4.91290971845572,
131.070325623503));
#83290=CARTESIAN_POINT('Ctrl Pts',(-41.758103901127,-4.90191150312827,131.204918575918));
#83291=CARTESIAN_POINT('Ctrl Pts',(-41.7657504384142,-4.89092465091859,
131.339372469809));
#83292=CARTESIAN_POINT('Ctrl Pts',(-41.7733969757012,-4.87438812458713,
131.473538989973));
#83293=CARTESIAN_POINT('Ctrl Pts',(-41.7810435129884,-4.85232800297637,
131.606916543363));
#83294=CARTESIAN_POINT('Ctrl Pts',(-41.7886841035495,-4.83028503756258,
131.740190368785));
#83295=CARTESIAN_POINT('Ctrl Pts',(-41.7963246941106,-4.8027270877807,131.872676051988));
#83296=CARTESIAN_POINT('Ctrl Pts',(-41.8039652846717,-4.7697320877363,132.003876717382));
#83297=CARTESIAN_POINT('Ctrl Pts',(-41.8116025319927,-4.73675152508488,
132.135019974213));
#83298=CARTESIAN_POINT('Ctrl Pts',(-41.8192397793138,-4.6983387395161,132.264878940731));
#83299=CARTESIAN_POINT('Ctrl Pts',(-41.8268770266347,-4.65462275942882,
132.392966934407));
#83300=CARTESIAN_POINT('Ctrl Pts',(-41.8345127392591,-4.61091556402089,
132.521029188938));
#83301=CARTESIAN_POINT('Ctrl Pts',(-41.8421484518834,-4.56190742286855,
132.647320796677));
#83302=CARTESIAN_POINT('Ctrl Pts',(-41.8497841645077,-4.50777706630277,
132.77137078099));
#83303=CARTESIAN_POINT('Ctrl Pts',(-41.8574201072333,-4.45364507852555,
132.895424503535));
#83304=CARTESIAN_POINT('Ctrl Pts',(-41.8650560499588,-4.39439072996786,
133.017236098825));
#83305=CARTESIAN_POINT('Ctrl Pts',(-41.8726919926844,-4.33024044805813,
133.136355627102));
#83306=CARTESIAN_POINT('Ctrl Pts',(-41.8803299302943,-4.26607340693537,
133.255506275266));
#83307=CARTESIAN_POINT('Ctrl Pts',(-41.887967867904,-4.197008080667,133.371963103274));
#83308=CARTESIAN_POINT('Ctrl Pts',(-41.8956058055139,-4.12331600337679,
133.485302280265));
#83309=CARTESIAN_POINT('Ctrl Pts',(-41.9032517650887,-4.04954652885077,
133.598760495006));
#83310=CARTESIAN_POINT('Ctrl Pts',(-41.9108977246635,-3.97114082297043,
133.709094184074));
#83311=CARTESIAN_POINT('Ctrl Pts',(-41.9185436842382,-3.88841291985857,
133.815909725115));
#83312=CARTESIAN_POINT('Ctrl Pts',(-41.926194183097,-3.80563590251286,133.922788680835));
#83313=CARTESIAN_POINT('Ctrl Pts',(-41.9338446819558,-3.71853183935376,
134.026145023419));
#83314=CARTESIAN_POINT('Ctrl Pts',(-41.9414951808145,-3.62745301867817,
134.125620568215));
#83315=CARTESIAN_POINT('Ctrl Pts',(-41.9491567837371,-3.53624200465687,
134.225240493503));
#83316=CARTESIAN_POINT('Ctrl Pts',(-41.9568183866597,-3.44104500103126,
134.320968093023));
#83317=CARTESIAN_POINT('Ctrl Pts',(-41.9644799895823,-3.3422491270763,134.41248392963));
#83318=CARTESIAN_POINT('Ctrl Pts',(-41.9681568445569,-3.29483632008411,
134.456402997543));
#83319=CARTESIAN_POINT('Ctrl Pts',(-41.9718336995316,-3.2465951175301,134.499352671356));
#83320=CARTESIAN_POINT('Ctrl Pts',(-41.9755105545062,-3.19757068636793,
134.541301180136));
#83321=CARTESIAN_POINT('Ctrl Pts',(-41.9832848886253,-3.09391353630704,
134.629997015383));
#83322=CARTESIAN_POINT('Ctrl Pts',(-41.9910592227443,-2.98639896895209,
134.714517128132));
#83323=CARTESIAN_POINT('Ctrl Pts',(-41.9988335568634,-2.87539783221303,
134.794507277653));
#83324=CARTESIAN_POINT('Ctrl Pts',(-42.0065983098106,-2.76453349445439,
134.874398846464));
#83325=CARTESIAN_POINT('Ctrl Pts',(-42.0143630627577,-2.65019145097514,
134.949771333727));
#83326=CARTESIAN_POINT('Ctrl Pts',(-42.0221278157049,-2.53277729827217,
135.020309172738));
#83327=CARTESIAN_POINT('Ctrl Pts',(-42.0298848565899,-2.41547976296108,
135.090776952572));
#83328=CARTESIAN_POINT('Ctrl Pts',(-42.0376418974749,-2.2951165235444,135.15641944));
#83329=CARTESIAN_POINT('Ctrl Pts',(-42.04539893836,-2.17212368501981,135.216963223679));
#83330=CARTESIAN_POINT('Ctrl Pts',(-42.0531501296002,-2.04922359635099,
135.27746135082));
#83331=CARTESIAN_POINT('Ctrl Pts',(-42.0609013208404,-1.92369820496837,
135.332868255428));
#83332=CARTESIAN_POINT('Ctrl Pts',(-42.0686525120805,-1.79600953431401,
135.38295568758));
#83333=CARTESIAN_POINT('Ctrl Pts',(-42.0764004088577,-1.66837513475141,
135.433021831236));
#83334=CARTESIAN_POINT('Ctrl Pts',(-42.0841483056347,-1.53857964783893,
135.477772856759));
#83335=CARTESIAN_POINT('Ctrl Pts',(-42.0918962024118,-1.40710626038626,
135.517028124879));
#83336=CARTESIAN_POINT('Ctrl Pts',(-42.099642478496,-1.275660374332,135.556275181643));
#83337=CARTESIAN_POINT('Ctrl Pts',(-42.1073887545801,-1.14253766024279,
135.590028655825));
#83338=CARTESIAN_POINT('Ctrl Pts',(-42.1151350306642,-1.00823731684453,
135.61815751559));
#83339=CARTESIAN_POINT('Ctrl Pts',(-42.1228813639296,-0.873935982071649,
135.646286582995));
#83340=CARTESIAN_POINT('Ctrl Pts',(-42.130627697195,-0.738457383305424,
135.668790872985));
#83341=CARTESIAN_POINT('Ctrl Pts',(-42.1383740304604,-0.602311393010782,
135.685590385601));
#83342=CARTESIAN_POINT('Ctrl Pts',(-42.1461220984634,-0.466134913765027,
135.702393660351));
#83343=CARTESIAN_POINT('Ctrl Pts',(-42.1538701664664,-0.329291133535421,
135.713489567688));
#83344=CARTESIAN_POINT('Ctrl Pts',(-42.1616182344695,-0.192295136921508,
135.718849974846));
#83345=CARTESIAN_POINT('Ctrl Pts',(-42.1693745372114,-0.0551535393326823,
135.724216079108));
#83346=CARTESIAN_POINT('Ctrl Pts',(-42.1771308399532,0.0821402065189988,
135.723834490947));
#83347=CARTESIAN_POINT('Ctrl Pts',(-42.184887142695,0.219070363301342,135.717729241883));
#83348=CARTESIAN_POINT('Ctrl Pts',(-42.1926475852092,0.356073603831433,
135.711620734264));
#83349=CARTESIAN_POINT('Ctrl Pts',(-42.2004080277235,0.49271247929883,135.699782512345));
#83350=CARTESIAN_POINT('Ctrl Pts',(-42.2081684702377,0.628477276379563,
135.682290442356));
#83351=CARTESIAN_POINT('Ctrl Pts',(-42.2159413705032,0.764460015165017,
135.664770292543));
#83352=CARTESIAN_POINT('Ctrl Pts',(-42.2237142707686,0.899565486075578,
135.641578223986));
#83353=CARTESIAN_POINT('Ctrl Pts',(-42.231487171034,1.03329416958053,135.612841273824));
#83354=CARTESIAN_POINT('Ctrl Pts',(-42.2389775067958,1.16216147859261,135.585148984186));
#83355=CARTESIAN_POINT('Ctrl Pts',(-42.2464678425575,1.28975006341186,135.552308031435));
#83356=CARTESIAN_POINT('Ctrl Pts',(-42.2539581783193,1.41562886996102,135.514475049831));
#83357=CARTESIAN_POINT('Ctrl Pts',(-42.2617325124384,1.5462804097255,135.475207619229));
#83358=CARTESIAN_POINT('Ctrl Pts',(-42.2695068465575,1.67550382415904,135.430437754202));
#83359=CARTESIAN_POINT('Ctrl Pts',(-42.2772811806765,1.80280062815081,135.380285983832));
#83360=CARTESIAN_POINT('Ctrl Pts',(-42.2850459336236,1.92994055020849,135.330196021037));
#83361=CARTESIAN_POINT('Ctrl Pts',(-42.2928106865707,2.05515822586244,135.274737491965));
#83362=CARTESIAN_POINT('Ctrl Pts',(-42.3005754395178,2.17796892509315,135.214081064922));
#83363=CARTESIAN_POINT('Ctrl Pts',(-42.3083324804028,2.30065764700606,135.153484882698));
#83364=CARTESIAN_POINT('Ctrl Pts',(-42.3160895212879,2.42094380171056,135.087701248374));
#83365=CARTESIAN_POINT('Ctrl Pts',(-42.3238465621729,2.53836163509838,135.016949283928));
#83366=CARTESIAN_POINT('Ctrl Pts',(-42.331597753413,2.65569092278451,134.946250674089));
#83367=CARTESIAN_POINT('Ctrl Pts',(-42.3393489446531,2.77015586100561,134.870591392585));
#83368=CARTESIAN_POINT('Ctrl Pts',(-42.3471001358932,2.88131468168165,134.790236778164));
#83369=CARTESIAN_POINT('Ctrl Pts',(-42.3548480326703,2.99242625689379,134.709916316598));
#83370=CARTESIAN_POINT('Ctrl Pts',(-42.3625959294474,3.10023419318805,134.62490471986));
#83371=CARTESIAN_POINT('Ctrl Pts',(-42.3703438262245,3.20432533935822,134.535510866758));
#83372=CARTESIAN_POINT('Ctrl Pts',(-42.3780901023086,3.30839471190456,134.446135712924));
#83373=CARTESIAN_POINT('Ctrl Pts',(-42.3858363783927,3.40874854435049,134.3523803806));
#83374=CARTESIAN_POINT('Ctrl Pts',(-42.3935826544768,3.50500676679596,134.254594033904));
#83375=CARTESIAN_POINT('Ctrl Pts',(-42.4013289877421,3.60126569979764,134.156806965372));
#83376=CARTESIAN_POINT('Ctrl Pts',(-42.4090753210075,3.69342868820284,134.054989101715));
#83377=CARTESIAN_POINT('Ctrl Pts',(-42.4168216542728,3.78115282725794,133.949526171145));
#83378=CARTESIAN_POINT('Ctrl Pts',(-42.4245697222758,3.86889661152588,133.844039622883));
#83379=CARTESIAN_POINT('Ctrl Pts',(-42.4323177902788,3.95219931843022,133.734906683908));
#83380=CARTESIAN_POINT('Ctrl Pts',(-42.4400658582817,4.03075886326929,133.622545503033));
#83381=CARTESIAN_POINT('Ctrl Pts',(-42.4478221610236,4.10940190212737,133.510064903359));
#83382=CARTESIAN_POINT('Ctrl Pts',(-42.4555784637654,4.18329148441925,133.394349528891));
#83383=CARTESIAN_POINT('Ctrl Pts',(-42.4633347665072,4.25216905991821,133.275846273679));
#83384=CARTESIAN_POINT('Ctrl Pts',(-42.4710952090214,4.32108339745308,133.157279769712));
#83385=CARTESIAN_POINT('Ctrl Pts',(-42.4788556515356,4.38498021585691,133.035922765856));
#83386=CARTESIAN_POINT('Ctrl Pts',(-42.4866160940498,4.44364783103554,132.912245105918));
#83387=CARTESIAN_POINT('Ctrl Pts',(-42.4943889943152,4.5024096246784,132.788368907619));
#83388=CARTESIAN_POINT('Ctrl Pts',(-42.5021618945807,4.55592528772964,132.662164969004));
#83389=CARTESIAN_POINT('Ctrl Pts',(-42.5099347948461,4.60403169762542,132.534122216677));
#83390=CARTESIAN_POINT('Ctrl Pts',(-42.5174251306081,4.65038931834863,132.410734140918));
#83391=CARTESIAN_POINT('Ctrl Pts',(-42.5249154663701,4.69172404131558,132.285638913862));
#83392=CARTESIAN_POINT('Ctrl Pts',(-42.5324058021321,4.72793465210855,132.159283858156));
#83393=CARTESIAN_POINT('Ctrl Pts',(-42.5401801362512,4.76551819921577,132.028138012108));
#83394=CARTESIAN_POINT('Ctrl Pts',(-42.5479544703703,4.79770045577841,131.895219488136));
#83395=CARTESIAN_POINT('Ctrl Pts',(-42.5557288044893,4.82431338294927,131.761012824795));
#83396=CARTESIAN_POINT('Ctrl Pts',(-42.5634935574364,4.85089351206586,131.626971559173));
#83397=CARTESIAN_POINT('Ctrl Pts',(-42.5712583103834,4.87191789319248,131.491645692683));
#83398=CARTESIAN_POINT('Ctrl Pts',(-42.5790230633305,4.88726810599457,131.355535292808));
#83399=CARTESIAN_POINT('Ctrl Pts',(-42.5867801042155,4.90260307274888,131.219560079702));
#83400=CARTESIAN_POINT('Ctrl Pts',(-42.5945371451005,4.91227504287343,131.082802269862));
#83401=CARTESIAN_POINT('Ctrl Pts',(-42.6022941859855,4.91621661842149,130.945772156191));
#83402=CARTESIAN_POINT('Ctrl Pts',(-42.6100453772256,4.92015522159677,130.808845377995));
#83403=CARTESIAN_POINT('Ctrl Pts',(-42.6177965684657,4.91837202035535,130.671647093921));
#83404=CARTESIAN_POINT('Ctrl Pts',(-42.6255477597058,4.91085146526319,130.53469239804));
#83405=CARTESIAN_POINT('Ctrl Pts',(-42.6332956564829,4.90333410660755,130.397795911558));
#83406=CARTESIAN_POINT('Ctrl Pts',(-42.64104355326,4.8900842655401,130.261143196913));
#83407=CARTESIAN_POINT('Ctrl Pts',(-42.6487914500371,4.87113849223304,130.125248806459));
#83408=CARTESIAN_POINT('Ctrl Pts',(-42.6565377261212,4.85219668197333,129.989382842181));
#83409=CARTESIAN_POINT('Ctrl Pts',(-42.6642840022053,4.82756136331593,129.854275273553));
#83410=CARTESIAN_POINT('Ctrl Pts',(-42.6720302782894,4.79732086085732,129.720434595882));
#83411=CARTESIAN_POINT('Ctrl Pts',(-42.6797766115547,4.76708013517024,129.58659293023));
#83412=CARTESIAN_POINT('Ctrl Pts',(-42.68752294482,4.73123422928303,129.454018555547));
#83413=CARTESIAN_POINT('Ctrl Pts',(-42.6952692780854,4.68992231887011,129.323208462835));
#83414=CARTESIAN_POINT('Ctrl Pts',(-42.7030173460883,4.64860115694135,129.19236907611));
#83415=CARTESIAN_POINT('Ctrl Pts',(-42.7107654140913,4.60181167244005,129.0632951303));
#83416=CARTESIAN_POINT('Ctrl Pts',(-42.7185134820942,4.54974238164558,128.936466797469));
#83417=CARTESIAN_POINT('Ctrl Pts',(-42.726269784836,4.49761775098907,128.809503669975));
#83418=CARTESIAN_POINT('Ctrl Pts',(-42.734026087578,4.44020225330236,128.684791285326));
#83419=CARTESIAN_POINT('Ctrl Pts',(-42.7417823903198,4.37773212049169,128.5627887263));
#83420=CARTESIAN_POINT('Ctrl Pts',(-42.749542832834,4.3152286454901,128.440721050834));
#83421=CARTESIAN_POINT('Ctrl Pts',(-42.7573032753481,4.24766535225111,128.321366422965));
#83422=CARTESIAN_POINT('Ctrl Pts',(-42.7650637178623,4.17532311325151,128.20515690057));
#83423=CARTESIAN_POINT('Ctrl Pts',(-42.7728366181277,4.10286474406773,128.088760828333));
#83424=CARTESIAN_POINT('Ctrl Pts',(-42.7806095183931,4.02561231930156,127.975520273841));
#83425=CARTESIAN_POINT('Ctrl Pts',(-42.7883824186585,3.94388901502325,127.865836753501));
#83426=CARTESIAN_POINT('Ctrl Pts',(-42.7958727544207,3.86513655870292,127.7601405054));
#83427=CARTESIAN_POINT('Ctrl Pts',(-42.8033630901828,3.78223282871864,127.657747406461));
#83428=CARTESIAN_POINT('Ctrl Pts',(-42.8108534259449,3.6954994614176,127.558984400059));
#83429=CARTESIAN_POINT('Ctrl Pts',(-42.818627760064,3.60547757213457,127.456476764252));
#83430=CARTESIAN_POINT('Ctrl Pts',(-42.8264020941831,3.51104474923607,127.357555211434));
#83431=CARTESIAN_POINT('Ctrl Pts',(-42.8341764283022,3.41251781962994,127.262623022372));
#83432=CARTESIAN_POINT('Ctrl Pts',(-42.8419411812493,3.31411231565869,127.167807828749));
#83433=CARTESIAN_POINT('Ctrl Pts',(-42.8497059341964,3.2116230231006,127.07697248511));
#83434=CARTESIAN_POINT('Ctrl Pts',(-42.8574706871435,3.10540665380837,126.990486920525));
#83435=CARTESIAN_POINT('Ctrl Pts',(-42.8652277280285,2.9992957801115,126.904087254622));
#83436=CARTESIAN_POINT('Ctrl Pts',(-42.8729847689135,2.88946549761346,126.822029015518));
#83437=CARTESIAN_POINT('Ctrl Pts',(-42.8807418097985,2.77630869994954,126.744644732792));
#83438=CARTESIAN_POINT('Ctrl Pts',(-42.8884930010386,2.66323723470773,126.667318806157));
#83439=CARTESIAN_POINT('Ctrl Pts',(-42.8962441922787,2.54684456883082,126.594660040068));
#83440=CARTESIAN_POINT('Ctrl Pts',(-42.9039953835188,2.42755566070103,126.526959937632));
#83441=CARTESIAN_POINT('Ctrl Pts',(-42.9117432802959,2.30831745353868,126.459288609546));
#83442=CARTESIAN_POINT('Ctrl Pts',(-42.919491177073,2.18618579175968,126.396571945897));
#83443=CARTESIAN_POINT('Ctrl Pts',(-42.9272390738501,2.06161333909198,126.339057324107));
#83444=CARTESIAN_POINT('Ctrl Pts',(-42.9349853499342,1.93706694429607,126.281554733135));
#83445=CARTESIAN_POINT('Ctrl Pts',(-42.9427316260183,1.8100811288793,126.229252183401));
#83446=CARTESIAN_POINT('Ctrl Pts',(-42.9504779021024,1.68113144594543,126.182350219054));
#83447=CARTESIAN_POINT('Ctrl Pts',(-42.9582242353677,1.55218081113428,126.135447908487));
#83448=CARTESIAN_POINT('Ctrl Pts',(-42.9659705686331,1.42126664729498,126.093946396493));
#83449=CARTESIAN_POINT('Ctrl Pts',(-42.9737169018984,1.28888231488431,126.057997226413));
#83450=CARTESIAN_POINT('Ctrl Pts',(-42.9814649699014,1.1564683359201,126.022040005765));
#83451=CARTESIAN_POINT('Ctrl Pts',(-42.9892130379044,1.02258391047611,125.991637703707));
#83452=CARTESIAN_POINT('Ctrl Pts',(-42.9969611059074,0.887734918561544,
125.966891260881));
#83453=CARTESIAN_POINT('Ctrl Pts',(-43.0047174086493,0.752742607533467,
125.942118517242));
#83454=CARTESIAN_POINT('Ctrl Pts',(-43.0124737113911,0.616784067338725,
125.923013711365));
#83455=CARTESIAN_POINT('Ctrl Pts',(-43.0202300141329,0.480373226435244,
125.909626240113));
#83456=CARTESIAN_POINT('Ctrl Pts',(-43.0279904566471,0.343889578958907,
125.896231623564));
#83457=CARTESIAN_POINT('Ctrl Pts',(-43.0357508991613,0.2069535399131,125.888560443896));
#83458=CARTESIAN_POINT('Ctrl Pts',(-43.0435113416754,0.0700804302608409,
125.886609932975));
#83459=CARTESIAN_POINT('Ctrl Pts',(-43.0512842419409,-0.0670124002582414,
125.884656290921));
#83460=CARTESIAN_POINT('Ctrl Pts',(-43.0590571422064,-0.204041708472887,
125.888441658022));
#83461=CARTESIAN_POINT('Ctrl Pts',(-43.0668300424718,-0.340495002699345,
125.897911166523));
#83462=CARTESIAN_POINT('Ctrl Pts',(-43.0743203782338,-0.47198787597483,
125.907036434538));
#83463=CARTESIAN_POINT('Ctrl Pts',(-43.0818107139958,-0.602945581125637,
125.921439719462));
#83464=CARTESIAN_POINT('Ctrl Pts',(-43.0893010497578,-0.732919199129937,
125.941027140408));
#83465=CARTESIAN_POINT('Ctrl Pts',(-43.0970753838769,-0.867820806365882,
125.961357224372));
#83466=CARTESIAN_POINT('Ctrl Pts',(-43.1048497179959,-1.00208955778166,
125.987336717162));
#83467=CARTESIAN_POINT('Ctrl Pts',(-43.112624052115,-1.13521490916483,126.018917046432));
#83468=CARTESIAN_POINT('Ctrl Pts',(-43.1203888050621,-1.26817619545018,
126.050458455768));
#83469=CARTESIAN_POINT('Ctrl Pts',(-43.1281535580092,-1.39999650871206,
126.087586878231));
#83470=CARTESIAN_POINT('Ctrl Pts',(-43.1359183109563,-1.53017180567683,
126.130202157735));
#83471=CARTESIAN_POINT('Ctrl Pts',(-43.1436753518413,-1.66021781070133,
126.172775111142));
#83472=CARTESIAN_POINT('Ctrl Pts',(-43.1514323927263,-1.78862168171332,
126.220823955743));
#83473=CARTESIAN_POINT('Ctrl Pts',(-43.1591894336113,-1.91489128355243,
126.274197879355));
#83474=CARTESIAN_POINT('Ctrl Pts',(-43.1669406248513,-2.04106566450204,
126.327531553276));
#83475=CARTESIAN_POINT('Ctrl Pts',(-43.1746918160914,-2.16510862117123,
126.386182161629));
#83476=CARTESIAN_POINT('Ctrl Pts',(-43.1824430073315,-2.28654520335439,
126.449949739443));
#83477=CARTESIAN_POINT('Ctrl Pts',(-43.1901909041086,-2.40793017175136,
126.513690214335));
#83478=CARTESIAN_POINT('Ctrl Pts',(-43.1979388008856,-2.52671062353022,
126.582543151696));
#83479=CARTESIAN_POINT('Ctrl Pts',(-43.2056866976626,-2.64243375725943,
126.65626142625));
#83480=CARTESIAN_POINT('Ctrl Pts',(-43.2134329737467,-2.75813268420361,
126.72996428053));
#83481=CARTESIAN_POINT('Ctrl Pts',(-43.2211792498309,-2.8707752356136,126.808530237773));
#83482=CARTESIAN_POINT('Ctrl Pts',(-43.228925525915,-2.97993563994864,126.891667600696));
#83483=CARTESIAN_POINT('Ctrl Pts',(-43.2366718591804,-3.08909685008129,
126.97480557732));
#83484=CARTESIAN_POINT('Ctrl Pts',(-43.2444181924457,-3.19477555081695,
127.062514790077));
#83485=CARTESIAN_POINT('Ctrl Pts',(-43.2521645257111,-3.29657757107428,
127.154462073717));
#83486=CARTESIAN_POINT('Ctrl Pts',(-43.2599125937141,-3.39840238918834,
127.246429948314));
#83487=CARTESIAN_POINT('Ctrl Pts',(-43.2676606617171,-3.49634850920976,
127.342637520364));
#83488=CARTESIAN_POINT('Ctrl Pts',(-43.2754087297201,-3.59005756641433,
127.442713739571));
#83489=CARTESIAN_POINT('Ctrl Pts',(-43.2831650324619,-3.68386621871967,
127.542896320975));
#83490=CARTESIAN_POINT('Ctrl Pts',(-43.2909213352037,-3.77342854492692,
127.646955477149));
#83491=CARTESIAN_POINT('Ctrl Pts',(-43.2986776379456,-3.85842519517247,
127.754485525737));
#83492=CARTESIAN_POINT('Ctrl Pts',(-43.3064380804597,-3.94346721068957,
127.86207296635));
#83493=CARTESIAN_POINT('Ctrl Pts',(-43.3141985229738,-4.02393846535643,
127.97313467424));
#83494=CARTESIAN_POINT('Ctrl Pts',(-43.321958965488,-4.09956274451401,128.087235599041));
#83495=CARTESIAN_POINT('Ctrl Pts',(-43.3297318657534,-4.17530842247811,
128.201519688777));
#83496=CARTESIAN_POINT('Ctrl Pts',(-43.3375047660189,-4.24619137414552,
128.31885241003));
#83497=CARTESIAN_POINT('Ctrl Pts',(-43.3452776662843,-4.3119807470397,128.438772931671));
#83498=CARTESIAN_POINT('Ctrl Pts',(-43.3527680020464,-4.37537851051663,
128.55433404029));
#83499=CARTESIAN_POINT('Ctrl Pts',(-43.3602583378085,-4.43404645744239,
128.672297793872));
#83500=CARTESIAN_POINT('Ctrl Pts',(-43.3677486735707,-4.48782092077067,
128.792235759215));
#83501=CARTESIAN_POINT('Ctrl Pts',(-43.376268988075,-4.54898978614722,128.928666116704));
#83502=CARTESIAN_POINT('Ctrl Pts',(-43.3847893025794,-4.60399456945207,
129.068023789314));
#83503=CARTESIAN_POINT('Ctrl Pts',(-43.3933096170837,-4.6525721106131,129.209758529882));
#83504=CARTESIAN_POINT('Ctrl Pts',(-43.4006790393331,-4.69458797897907,
129.332348271155));
#83505=CARTESIAN_POINT('Ctrl Pts',(-43.4080484615824,-4.73179629584008,
129.456715760791));
#83506=CARTESIAN_POINT('Ctrl Pts',(-43.4154178838317,-4.76405452823406,
129.582490119308));
#83507=CARTESIAN_POINT('Ctrl Pts',(-41.6650773111923,-4.76405452823405,
129.582490119308));
#83508=CARTESIAN_POINT('Ctrl Pts',(-41.67285208007,-4.79807929090603,129.715152152568));
#83509=CARTESIAN_POINT('Ctrl Pts',(-41.6806268489478,-4.82651721256817,
129.849074877393));
#83510=CARTESIAN_POINT('Ctrl Pts',(-41.6884016178255,-4.84930693794822,
129.983747868416));
#83511=CARTESIAN_POINT('Ctrl Pts',(-41.6912887221148,-4.85776973792735,
130.0337577113));
#83512=CARTESIAN_POINT('Ctrl Pts',(-41.6941758264041,-4.86545419363686,
130.083870981395));
#83513=CARTESIAN_POINT('Ctrl Pts',(-41.6970629306933,-4.87235899193441,
130.134061493133));
#83514=CARTESIAN_POINT('Ctrl Pts',(-41.7097554751317,-4.90271447980346,
130.354713481002));
#83515=CARTESIAN_POINT('Ctrl Pts',(-41.7224480195701,-4.91808601786737,
130.577473165781));
#83516=CARTESIAN_POINT('Ctrl Pts',(-41.7351405640085,-4.91824869491739,
130.800777679744));
#83517=CARTESIAN_POINT('',(-41.3898594359429,-4.91824825723657,130.808500990674));
#83518=CARTESIAN_POINT('Ctrl Pts',(-41.3197599198393,-4.76405452823403,
129.582490119308));
#83519=CARTESIAN_POINT('Ctrl Pts',(-41.3273964518608,-4.79766368818847,
129.71353172388));
#83520=CARTESIAN_POINT('Ctrl Pts',(-41.3350329838823,-4.82584721264061,
129.845903662855));
#83521=CARTESIAN_POINT('Ctrl Pts',(-41.3426695159038,-4.84851983346089,
129.979110057411));
#83522=CARTESIAN_POINT('Ctrl Pts',(-41.350534502577,-4.87187072887995,130.116301457253));
#83523=CARTESIAN_POINT('Ctrl Pts',(-41.3583994892502,-4.88937575275814,
130.254377564647));
#83524=CARTESIAN_POINT('Ctrl Pts',(-41.3662644759234,-4.9009992852771,130.39279158543));
#83525=CARTESIAN_POINT('Ctrl Pts',(-41.3741294625966,-4.91262281779606,
130.531205606213));
#83526=CARTESIAN_POINT('Ctrl Pts',(-41.3819944492698,-4.91836488890507,
130.669957075579));
#83527=CARTESIAN_POINT('Ctrl Pts',(-41.389859435943,-4.91824825723657,130.808500990674));
#83528=CARTESIAN_POINT('Ctrl Pts',(-41.3898594359911,-4.91824825723585,
130.808500991522));
#83529=CARTESIAN_POINT('Ctrl Pts',(-41.4019188502082,-4.91806942541481,
131.020930907655));
#83530=CARTESIAN_POINT('Ctrl Pts',(-41.4139782644253,-4.90412471843964,
131.232801737864));
#83531=CARTESIAN_POINT('Ctrl Pts',(-41.4260376786424,-4.87664726816819,
131.442713564115));
#83532=CARTESIAN_POINT('Ctrl Pts',(-41.4300932201083,-4.86740669172328,
131.513306223113));
#83533=CARTESIAN_POINT('Ctrl Pts',(-41.4341487615742,-4.85663595382896,
131.583677646618));
#83534=CARTESIAN_POINT('Ctrl Pts',(-41.4382043030401,-4.84434491737359,
131.653775347846));
#83535=CARTESIAN_POINT('Ctrl Pts',(-41.4459786371593,-4.82078342136201,
131.788150240794));
#83536=CARTESIAN_POINT('Ctrl Pts',(-41.4537529712782,-4.79158933020956,
131.921756889933));
#83537=CARTESIAN_POINT('Ctrl Pts',(-41.4615273053973,-4.75682345392793,
132.054086063679));
#83538=CARTESIAN_POINT('Ctrl Pts',(-41.4692920583445,-4.72210042348165,
132.186252153544));
#83539=CARTESIAN_POINT('Ctrl Pts',(-41.4770568112917,-4.68181936903707,
132.317143526048));
#83540=CARTESIAN_POINT('Ctrl Pts',(-41.4848215642388,-4.63609251348601,
132.44625868654));
#83541=CARTESIAN_POINT('Ctrl Pts',(-41.4925786051239,-4.59041107449259,
132.575245608033));
#83542=CARTESIAN_POINT('Ctrl Pts',(-41.5003356460088,-4.53929472791557,
132.702459462118));
#83543=CARTESIAN_POINT('Ctrl Pts',(-41.5080926868939,-4.4829060523938,132.827411874433));
#83544=CARTESIAN_POINT('Ctrl Pts',(-41.515843878134,-4.42655990001088,132.952270059162));
#83545=CARTESIAN_POINT('Ctrl Pts',(-41.5235950693742,-4.36494949264671,
133.074869841642));
#83546=CARTESIAN_POINT('Ctrl Pts',(-41.5313462606143,-4.29828613518435,
133.19474120705));
#83547=CARTESIAN_POINT('Ctrl Pts',(-41.5390941573914,-4.23165111142721,
133.31456162393));
#83548=CARTESIAN_POINT('Ctrl Pts',(-41.5468420541685,-4.15996759868137,
133.431655589225));
#83549=CARTESIAN_POINT('Ctrl Pts',(-41.5545899509456,-4.08349351704301,
133.545576362225));
#83550=CARTESIAN_POINT('Ctrl Pts',(-41.5623362270297,-4.00703543213384,
133.659473305456));
#83551=CARTESIAN_POINT('Ctrl Pts',(-41.5700825031138,-3.92578898930033,
133.770198052251));
#83552=CARTESIAN_POINT('Ctrl Pts',(-41.5778287791979,-3.84005601916743,
133.877331953611));
#83553=CARTESIAN_POINT('Ctrl Pts',(-41.5855751124633,-3.75432241617333,
133.98446664581));
#83554=CARTESIAN_POINT('Ctrl Pts',(-41.5933214457287,-3.66410246407318,
134.088010134425));
#83555=CARTESIAN_POINT('Ctrl Pts',(-41.6010677789941,-3.56973869119103,
134.187576356935));
#83556=CARTESIAN_POINT('Ctrl Pts',(-41.6088158469971,-3.47535378619622,
134.28716487661));
#83557=CARTESIAN_POINT('Ctrl Pts',(-41.6165639150001,-3.37682348273643,
134.382774074112));
#83558=CARTESIAN_POINT('Ctrl Pts',(-41.6243119830031,-3.27452732401904,
134.474054592103));
#83559=CARTESIAN_POINT('Ctrl Pts',(-41.6320682857449,-3.17212244372682,
134.565432124114));
#83560=CARTESIAN_POINT('Ctrl Pts',(-41.6398245884867,-3.0659440051395,134.652471525759));
#83561=CARTESIAN_POINT('Ctrl Pts',(-41.6475808912286,-2.95640523730333,
134.734863274396));
#83562=CARTESIAN_POINT('Ctrl Pts',(-41.6553413337428,-2.84680800532847,
134.81729899799));
#83563=CARTESIAN_POINT('Ctrl Pts',(-41.663101776257,-2.73384719223768,134.895081904165));
#83564=CARTESIAN_POINT('Ctrl Pts',(-41.6708622187712,-2.61796435150189,
134.967946297814));
#83565=CARTESIAN_POINT('Ctrl Pts',(-41.6786351190367,-2.50189548534255,
135.040927659856));
#83566=CARTESIAN_POINT('Ctrl Pts',(-41.6864080193021,-2.3828955576191,135.108974537196));
#83567=CARTESIAN_POINT('Ctrl Pts',(-41.6941809195676,-2.26143080657674,
135.171867202514));
#83568=CARTESIAN_POINT('Ctrl Pts',(-41.7016712553294,-2.14438160518978,
135.232473561029));
#83569=CARTESIAN_POINT('Ctrl Pts',(-41.7091615910912,-2.0250439532986,135.288293808208));
#83570=CARTESIAN_POINT('Ctrl Pts',(-41.716651926853,-1.90385008828339,135.339174605355));
#83571=CARTESIAN_POINT('Ctrl Pts',(-41.7244262609721,-1.7780611210365,135.391984563391));
#83572=CARTESIAN_POINT('Ctrl Pts',(-41.7322005950912,-1.64987394380568,
135.439640405068));
#83573=CARTESIAN_POINT('Ctrl Pts',(-41.7399749292103,-1.51974985684307,
135.481918039461));
#83574=CARTESIAN_POINT('Ctrl Pts',(-41.7477396821574,-1.38978613618811,
135.524143570448));
#83575=CARTESIAN_POINT('Ctrl Pts',(-41.7555044351044,-1.25789062361781,
135.561003962563));
#83576=CARTESIAN_POINT('Ctrl Pts',(-41.7632691880515,-1.12454589999998,
135.592322561994));
#83577=CARTESIAN_POINT('Ctrl Pts',(-41.7710262289364,-0.991333616241483,
135.623610055351));
#83578=CARTESIAN_POINT('Ctrl Pts',(-41.7787832698215,-0.856675364005673,
135.64936662079));
#83579=CARTESIAN_POINT('Ctrl Pts',(-41.7865403107065,-0.721069904199495,
135.669465062052));
#83580=CARTESIAN_POINT('Ctrl Pts',(-41.7942915019466,-0.585566705525228,
135.689548346923));
#83581=CARTESIAN_POINT('Ctrl Pts',(-41.8020426931867,-0.449118106220323,
135.703981943407));
#83582=CARTESIAN_POINT('Ctrl Pts',(-41.8097938844269,-0.312233758518155,
135.712689573794));
#83583=CARTESIAN_POINT('Ctrl Pts',(-41.8175417812039,-0.175407590315456,
135.721393503205));
#83584=CARTESIAN_POINT('Ctrl Pts',(-41.825289677981,-0.038146431433194,
135.72437628217));
#83585=CARTESIAN_POINT('Ctrl Pts',(-41.8330375747581,0.0990344504043435,
135.721613431906));
#83586=CARTESIAN_POINT('Ctrl Pts',(-41.8407838508422,0.236186636958678,
135.71885115957));
#83587=CARTESIAN_POINT('Ctrl Pts',(-41.8485301269263,0.373258189230657,
135.710345656441));
#83588=CARTESIAN_POINT('Ctrl Pts',(-41.8562764030104,0.50973373913565,135.696124571161));
#83589=CARTESIAN_POINT('Ctrl Pts',(-41.8640227362758,0.646210296471964,
135.681903380904));
#83590=CARTESIAN_POINT('Ctrl Pts',(-41.8717690695411,0.782090453802543,
135.661966564827));
#83591=CARTESIAN_POINT('Ctrl Pts',(-41.8795154028064,0.916864260867472,
135.636393625488));
#83592=CARTESIAN_POINT('Ctrl Pts',(-41.8872634708094,1.05166824959204,135.610814959265));
#83593=CARTESIAN_POINT('Ctrl Pts',(-41.8950115388123,1.18536501100023,135.579597731077));
#83594=CARTESIAN_POINT('Ctrl Pts',(-41.9027596068153,1.31745546849312,135.542872425195));
#83595=CARTESIAN_POINT('Ctrl Pts',(-41.9105159095571,1.44968631329632,135.506108087221));
#83596=CARTESIAN_POINT('Ctrl Pts',(-41.918272212299,1.58030706659254,135.463824082352));
#83597=CARTESIAN_POINT('Ctrl Pts',(-41.9260285150408,1.7088339578248,135.416200767342));
#83598=CARTESIAN_POINT('Ctrl Pts',(-41.933788957555,1.83742944772879,135.368552034334));
#83599=CARTESIAN_POINT('Ctrl Pts',(-41.9415494000692,1.96392848831663,135.315558463806));
#83600=CARTESIAN_POINT('Ctrl Pts',(-41.9493098425833,2.08786887233352,135.257447932502));
#83601=CARTESIAN_POINT('Ctrl Pts',(-41.9570827428487,2.21200821645775,135.199244117014));
#83602=CARTESIAN_POINT('Ctrl Pts',(-41.9648556431142,2.33358034922079,135.135907106908));
#83603=CARTESIAN_POINT('Ctrl Pts',(-41.9726285433796,2.45214839464508,135.067710393639));
#83604=CARTESIAN_POINT('Ctrl Pts',(-41.9801188791417,2.5664061929646,135.001992802674));
#83605=CARTESIAN_POINT('Ctrl Pts',(-41.9876092149038,2.67787426366432,134.931762863403));
#83606=CARTESIAN_POINT('Ctrl Pts',(-41.9950995506659,2.78618996369219,134.857301346064));
#83607=CARTESIAN_POINT('Ctrl Pts',(-42.002873884785,2.89861248640719,134.780016597665));
#83608=CARTESIAN_POINT('Ctrl Pts',(-42.0106482189041,3.00799499613306,134.697928241496));
#83609=CARTESIAN_POINT('Ctrl Pts',(-42.0184225530231,3.11389961477315,134.611303255907));
#83610=CARTESIAN_POINT('Ctrl Pts',(-42.0261873059702,3.21967371543574,134.52478502787));
#83611=CARTESIAN_POINT('Ctrl Pts',(-42.0339520589173,3.32197815353384,134.433741539973));
#83612=CARTESIAN_POINT('Ctrl Pts',(-42.0417168118644,3.42040345846579,134.338483315466));
#83613=CARTESIAN_POINT('Ctrl Pts',(-42.0494738527494,3.51873100599732,134.243319702772));
#83614=CARTESIAN_POINT('Ctrl Pts',(-42.0572308936343,3.61318680850876,134.143949954204));
#83615=CARTESIAN_POINT('Ctrl Pts',(-42.0649879345193,3.70339425973269,134.040724938757));
#83616=CARTESIAN_POINT('Ctrl Pts',(-42.0727391257594,3.79353368481595,133.937577766097));
#83617=CARTESIAN_POINT('Ctrl Pts',(-42.0804903169997,3.87943087918509,133.830581406537));
#83618=CARTESIAN_POINT('Ctrl Pts',(-42.0882415082398,3.960746188761,133.720123414968));
#83619=CARTESIAN_POINT('Ctrl Pts',(-42.0959894050168,4.04202693716118,133.609712370993));
#83620=CARTESIAN_POINT('Ctrl Pts',(-42.1037373017938,4.11872944274777,133.495842935477));
#83621=CARTESIAN_POINT('Ctrl Pts',(-42.1114851985709,4.19055459603477,133.378935386368));
#83622=CARTESIAN_POINT('Ctrl Pts',(-42.119231474655,4.26236472504806,133.262052291798));
#83623=CARTESIAN_POINT('Ctrl Pts',(-42.1269777507391,4.32929932653864,133.142132680604));
#83624=CARTESIAN_POINT('Ctrl Pts',(-42.1347240268231,4.3911030930548,133.019625091317));
#83625=CARTESIAN_POINT('Ctrl Pts',(-42.1424703600885,4.45290731579233,132.897116597707));
#83626=CARTESIAN_POINT('Ctrl Pts',(-42.1502166933538,4.50958045188186,132.772020436946));
#83627=CARTESIAN_POINT('Ctrl Pts',(-42.1579630266192,4.56091374850402,132.644808617703));
#83628=CARTESIAN_POINT('Ctrl Pts',(-42.1657110946221,4.61225854086198,132.517568310255));
#83629=CARTESIAN_POINT('Ctrl Pts',(-42.1734591626251,4.65826096793492,132.388211764034));
#83630=CARTESIAN_POINT('Ctrl Pts',(-42.1812072306281,4.69876104674554,132.257229396254));
#83631=CARTESIAN_POINT('Ctrl Pts',(-42.1889635333699,4.73930416952194,132.126107818855));
#83632=CARTESIAN_POINT('Ctrl Pts',(-42.1967198361118,4.77433314642686,131.99335734226));
#83633=CARTESIAN_POINT('Ctrl Pts',(-42.2044761388536,4.80373822690096,131.859482463568));
#83634=CARTESIAN_POINT('Ctrl Pts',(-42.2122365813678,4.83315900175188,131.725536131822));
#83635=CARTESIAN_POINT('Ctrl Pts',(-42.2199970238819,4.85694983135891,131.590464587026));
#83636=CARTESIAN_POINT('Ctrl Pts',(-42.2277574663961,4.87505260057043,131.45477987018));
#83637=CARTESIAN_POINT('Ctrl Pts',(-42.2355303666615,4.89318442995417,131.318877340182));
#83638=CARTESIAN_POINT('Ctrl Pts',(-42.2433032669269,4.90560991687712,131.182360060731));
#83639=CARTESIAN_POINT('Ctrl Pts',(-42.2510761671923,4.91232301531016,131.045743416775));
#83640=CARTESIAN_POINT('Ctrl Pts',(-42.2585665029544,4.91879207570596,130.914093131942));
#83641=CARTESIAN_POINT('Ctrl Pts',(-42.2660568387165,4.91995685375458,130.782350889485));
#83642=CARTESIAN_POINT('Ctrl Pts',(-42.2735471744786,4.91585755198091,130.650973554447));
#83643=CARTESIAN_POINT('Ctrl Pts',(-42.2813215085977,4.91160282393456,130.51461500782));
#83644=CARTESIAN_POINT('Ctrl Pts',(-42.2890958427168,4.9016634833501,130.378217642885));
#83645=CARTESIAN_POINT('Ctrl Pts',(-42.2968701768359,4.88602746286568,130.242294167204));
#83646=CARTESIAN_POINT('Ctrl Pts',(-42.304634929783,4.87041071237908,130.106538205059));
#83647=CARTESIAN_POINT('Ctrl Pts',(-42.3123996827301,4.84911129524245,129.971255354806));
#83648=CARTESIAN_POINT('Ctrl Pts',(-42.3201644356772,4.82216913459946,129.836957961059));
#83649=CARTESIAN_POINT('Ctrl Pts',(-42.3279214765622,4.79525373329024,129.702793953378));
#83650=CARTESIAN_POINT('Ctrl Pts',(-42.3356785174472,4.76270681799171,129.569613835256));
#83651=CARTESIAN_POINT('Ctrl Pts',(-42.3434355583323,4.72462001983748,129.437924109472));
#83652=CARTESIAN_POINT('Ctrl Pts',(-42.3511867495724,4.68656194323402,129.306333691936));
#83653=CARTESIAN_POINT('Ctrl Pts',(-42.3589379408125,4.64297240735345,129.176231803704));
#83654=CARTESIAN_POINT('Ctrl Pts',(-42.3666891320527,4.59399388177659,129.048113688259));
#83655=CARTESIAN_POINT('Ctrl Pts',(-42.3744370288298,4.54503617337964,128.920050026431));
#83656=CARTESIAN_POINT('Ctrl Pts',(-42.3821849256069,4.49069417016202,128.793968824841));
#83657=CARTESIAN_POINT('Ctrl Pts',(-42.389932822384,4.43115978788133,128.670348903267));
#83658=CARTESIAN_POINT('Ctrl Pts',(-42.3976790984681,4.37163785891,128.546754840317));
#83659=CARTESIAN_POINT('Ctrl Pts',(-42.4054253745522,4.30692588078618,128.425621385346));
#83660=CARTESIAN_POINT('Ctrl Pts',(-42.4131716506363,4.23726322176676,128.307405781778));
#83661=CARTESIAN_POINT('Ctrl Pts',(-42.4209179839017,4.16760004851341,128.18918930557));
#83662=CARTESIAN_POINT('Ctrl Pts',(-42.428664317167,4.09298631993178,128.073891060576));
#83663=CARTESIAN_POINT('Ctrl Pts',(-42.4364106504324,4.0137063142859,127.961941808671));
#83664=CARTESIAN_POINT('Ctrl Pts',(-42.4441587184353,3.93440855443244,127.849967486507));
#83665=CARTESIAN_POINT('Ctrl Pts',(-42.4519067864384,3.85044266403317,127.741343968812));
#83666=CARTESIAN_POINT('Ctrl Pts',(-42.4596548544414,3.76213477027295,127.636470936279));
#83667=CARTESIAN_POINT('Ctrl Pts',(-42.4674111571833,3.67373302183235,127.53148644344));
#83668=CARTESIAN_POINT('Ctrl Pts',(-42.4751674599251,3.58098030383065,127.430260697887));
#83669=CARTESIAN_POINT('Ctrl Pts',(-42.482923762667,3.48424174110856,127.33315872888));
#83670=CARTESIAN_POINT('Ctrl Pts',(-42.4906842051811,3.38745154610281,127.236004933629));
#83671=CARTESIAN_POINT('Ctrl Pts',(-42.4984446476954,3.28667155456641,127.142979565621));
#83672=CARTESIAN_POINT('Ctrl Pts',(-42.5062050902095,3.1823011484362,127.054408289447));
#83673=CARTESIAN_POINT('Ctrl Pts',(-42.513977990475,3.07776319766451,126.965694830799));
#83674=CARTESIAN_POINT('Ctrl Pts',(-42.5217508907404,2.96962362328354,126.881449992579));
#83675=CARTESIAN_POINT('Ctrl Pts',(-42.5295237910058,2.85831276521803,126.801957439638));
#83676=CARTESIAN_POINT('Ctrl Pts',(-42.5370141267678,2.75104833721968,126.725354641226));
#83677=CARTESIAN_POINT('Ctrl Pts',(-42.5445044625297,2.64083944849535,126.653164780436));
#83678=CARTESIAN_POINT('Ctrl Pts',(-42.5519947982916,2.52809220299046,126.58560098046));
#83679=CARTESIAN_POINT('Ctrl Pts',(-42.5597691324108,2.41107011140215,126.515475478471));
#83680=CARTESIAN_POINT('Ctrl Pts',(-42.5675434665299,2.29094268894056,126.450111619763));
#83681=CARTESIAN_POINT('Ctrl Pts',(-42.5753178006489,2.16813476829461,126.389796687911));
#83682=CARTESIAN_POINT('Ctrl Pts',(-42.583082553596,2.0454781974352,126.329556088822));
#83683=CARTESIAN_POINT('Ctrl Pts',(-42.5908473065431,1.92014804887794,126.27435220666));
#83684=CARTESIAN_POINT('Ctrl Pts',(-42.5986120594902,1.79259695209313,126.224428387735));
#83685=CARTESIAN_POINT('Ctrl Pts',(-42.6063691003752,1.6651725408558,126.17455415385));
#83686=CARTESIAN_POINT('Ctrl Pts',(-42.6141261412602,1.53553193290139,126.129949688517));
#83687=CARTESIAN_POINT('Ctrl Pts',(-42.6218831821452,1.40415079222919,126.090811676992));
#83688=CARTESIAN_POINT('Ctrl Pts',(-42.6296343733854,1.27286872709735,126.051703179747));
#83689=CARTESIAN_POINT('Ctrl Pts',(-42.6373855646255,1.13984911497429,126.018053042298));
#83690=CARTESIAN_POINT('Ctrl Pts',(-42.6451367558656,1.00558562651601,125.990009092153));
#83691=CARTESIAN_POINT('Ctrl Pts',(-42.6528846526427,0.871379203621746,
125.961977061435));
#83692=CARTESIAN_POINT('Ctrl Pts',(-42.6606325494197,0.735930337802519,
125.939546558623));
#83693=CARTESIAN_POINT('Ctrl Pts',(-42.6683804461968,0.599745608853917,
125.922814933343));
#83694=CARTESIAN_POINT('Ctrl Pts',(-42.6761267222809,0.463589366814808,
125.906086807957));
#83695=CARTESIAN_POINT('Ctrl Pts',(-42.683872998365,0.326697955616605,125.89505523663));
#83696=CARTESIAN_POINT('Ctrl Pts',(-42.6916192744492,0.189585451490489,
125.889765983307));
#83697=CARTESIAN_POINT('Ctrl Pts',(-42.6993656077145,0.0524719352312011,
125.884476690941));
#83698=CARTESIAN_POINT('Ctrl Pts',(-42.7071119409799,-0.0848622865380212,
125.884929816231));
#83699=CARTESIAN_POINT('Ctrl Pts',(-42.7148582742452,-0.221901142306615,
125.89111902514));
#83700=CARTESIAN_POINT('Ctrl Pts',(-42.7226063422482,-0.358970686976984,
125.89730962008));
#83701=CARTESIAN_POINT('Ctrl Pts',(-42.7303544102512,-0.495744343533176,
125.909238837119));
#83702=CARTESIAN_POINT('Ctrl Pts',(-42.7381024782542,-0.63170956957887,
125.926848333399));
#83703=CARTESIAN_POINT('Ctrl Pts',(-42.745858780996,-0.767819301084812,
125.944476545261));
#83704=CARTESIAN_POINT('Ctrl Pts',(-42.7536150837379,-0.903118497371499,
125.967797045761));
#83705=CARTESIAN_POINT('Ctrl Pts',(-42.7613713864798,-1.03710269008942,
125.996699952262));
#83706=CARTESIAN_POINT('Ctrl Pts',(-42.7691318289939,-1.17115839420536,
126.025618285115));
#83707=CARTESIAN_POINT('Ctrl Pts',(-42.7768922715081,-1.30389731803941,
126.060124862553));
#83708=CARTESIAN_POINT('Ctrl Pts',(-42.7846527140223,-1.43482959505532,
126.100059702908));
#83709=CARTESIAN_POINT('Ctrl Pts',(-42.7924256142878,-1.56597205618575,
126.140058650214));
#83710=CARTESIAN_POINT('Ctrl Pts',(-42.8001985145531,-1.69530170592608,
126.185503143961));
#83711=CARTESIAN_POINT('Ctrl Pts',(-42.8079714148186,-1.8223472797653,126.23618445476));
#83712=CARTESIAN_POINT('Ctrl Pts',(-42.8154617505806,-1.94477442698611,
126.285023372252));
#83713=CARTESIAN_POINT('Ctrl Pts',(-42.8229520863426,-2.06508039774963,
126.338724848522));
#83714=CARTESIAN_POINT('Ctrl Pts',(-42.8304424221045,-2.18286637637645,
126.397062415109));
#83715=CARTESIAN_POINT('Ctrl Pts',(-42.8382175270897,-2.30513036809968,
126.457617872061));
#83716=CARTESIAN_POINT('Ctrl Pts',(-42.845992632075,-2.42506629975389,126.523360745701));
#83717=CARTESIAN_POINT('Ctrl Pts',(-42.8537677370602,-2.54220269976336,
126.594088833487));
#83718=CARTESIAN_POINT('Ctrl Pts',(-42.8615330889043,-2.65919216312966,
126.66472819951));
#83719=CARTESIAN_POINT('Ctrl Pts',(-42.8692984407485,-2.77338875112387,
126.740340135858));
#83720=CARTESIAN_POINT('Ctrl Pts',(-42.8770637925927,-2.88434297150766,
126.820675303034));
#83721=CARTESIAN_POINT('Ctrl Pts',(-42.8850936929651,-2.99907715914755,
126.903747313392));
#83722=CARTESIAN_POINT('Ctrl Pts',(-42.8931235933375,-3.11034374475109,
126.991869935696));
#83723=CARTESIAN_POINT('Ctrl Pts',(-42.9011534937099,-3.21767452558208,
127.084716318722));
#83724=CARTESIAN_POINT('Ctrl Pts',(-42.9089042614454,-3.3212743106991,127.174335207693));
#83725=CARTESIAN_POINT('Ctrl Pts',(-42.9166550291809,-3.42120701176852,
127.268354664679));
#83726=CARTESIAN_POINT('Ctrl Pts',(-42.9244057969164,-3.51708264249682,
127.366437880164));
#83727=CARTESIAN_POINT('Ctrl Pts',(-42.9321530804166,-3.6129151738474,127.464477003886));
#83728=CARTESIAN_POINT('Ctrl Pts',(-42.9399003639166,-3.70469399111762,
127.566575972256));
#83729=CARTESIAN_POINT('Ctrl Pts',(-42.9476476474167,-3.79206477075871,
127.672360005039));
#83730=CARTESIAN_POINT('Ctrl Pts',(-42.9553931259917,-3.8794151951721,127.778119392762));
#83731=CARTESIAN_POINT('Ctrl Pts',(-42.9631386045667,-3.96235937759712,
127.887561834711));
#83732=CARTESIAN_POINT('Ctrl Pts',(-42.9708840831417,-4.04058248929738,
128.000278555699));
#83733=CARTESIAN_POINT('Ctrl Pts',(-42.9786294345188,-4.11880431640182,
128.11299342563));
#83734=CARTESIAN_POINT('Ctrl Pts',(-42.9863747858959,-4.19230500583251,
128.228982145526));
#83735=CARTESIAN_POINT('Ctrl Pts',(-42.994120137273,-4.26081260070424,128.347806314445));
#83736=CARTESIAN_POINT('Ctrl Pts',(-43.0018697678768,-4.32935804531452,
128.466696132491));
#83737=CARTESIAN_POINT('Ctrl Pts',(-43.0096193984806,-4.39290469076406,
128.588424189267));
#83738=CARTESIAN_POINT('Ctrl Pts',(-43.0173690290843,-4.45122610263049,
128.712526674405));
#83739=CARTESIAN_POINT('Ctrl Pts',(-43.0251212462136,-4.50956697991787,
128.83667058013));
#83740=CARTESIAN_POINT('Ctrl Pts',(-43.0328734633429,-4.56267899430795,
128.963190134387));
#83741=CARTESIAN_POINT('Ctrl Pts',(-43.0406256804722,-4.61038392677963,
129.091601699857));
#83742=CARTESIAN_POINT('Ctrl Pts',(-43.0483850744578,-4.65813302357772,
129.220132146331));
#83743=CARTESIAN_POINT('Ctrl Pts',(-43.0561444684436,-4.70046492196504,
129.350557730384));
#83744=CARTESIAN_POINT('Ctrl Pts',(-43.0639038624292,-4.73725125030763,
129.482379659322));
#83745=CARTESIAN_POINT('Ctrl Pts',(-43.0658630421296,-4.74653947924328,
129.515663553363));
#83746=CARTESIAN_POINT('Ctrl Pts',(-43.06782222183,-4.75547442177194,129.549036414434));
#83747=CARTESIAN_POINT('Ctrl Pts',(-43.0697814015304,-4.7640545282341,129.582490119308));
#83748=CARTESIAN_POINT('Origin',(213.235140564004,0.,130.804360617566));
#83749=CARTESIAN_POINT('',(-45.1651923290374,-4.76405452823407,129.582490119308));
#83750=CARTESIAN_POINT('',(-44.8201225776941,-4.76405452823406,129.582490119308));
#83751=CARTESIAN_POINT('',(213.235140564004,-4.76405452823405,129.582490119308));
#83752=CARTESIAN_POINT('',(-43.4851405639651,-4.91824956659705,130.802295873524));
#83753=CARTESIAN_POINT('Ctrl Pts',(-43.4851405640086,-4.91824956659737,
130.802295874294));
#83754=CARTESIAN_POINT('Ctrl Pts',(-43.4930372764877,-4.91830839744131,
130.942431830506));
#83755=CARTESIAN_POINT('Ctrl Pts',(-43.500933988967,-4.91237352301066,131.082539161257));
#83756=CARTESIAN_POINT('Ctrl Pts',(-43.5088307014462,-4.90047868839197,
131.22208263891));
#83757=CARTESIAN_POINT('Ctrl Pts',(-43.5167308566085,-4.88857866805239,
131.361686952511));
#83758=CARTESIAN_POINT('Ctrl Pts',(-43.5246310117707,-4.87071354147857,
131.500726555114));
#83759=CARTESIAN_POINT('Ctrl Pts',(-43.5325311669331,-4.84696884207495,
131.638672373719));
#83760=CARTESIAN_POINT('Ctrl Pts',(-43.5404361953534,-4.82320949561139,
131.776703285027));
#83761=CARTESIAN_POINT('Ctrl Pts',(-43.5483412237738,-4.79356341218359,
131.913638704233));
#83762=CARTESIAN_POINT('Ctrl Pts',(-43.5562462521941,-4.75816700446225,
132.04896088277));
#83763=CARTESIAN_POINT('Ctrl Pts',(-43.564163369394,-4.72271646671761,132.184490003005));
#83764=CARTESIAN_POINT('Ctrl Pts',(-43.572080486594,-4.68149812895479,132.31840059567));
#83765=CARTESIAN_POINT('Ctrl Pts',(-43.5799976037939,-4.63469827231357,
132.450190191706));
#83766=CARTESIAN_POINT('Ctrl Pts',(-43.5879211327744,-4.5878605141987,132.582086519263));
#83767=CARTESIAN_POINT('Ctrl Pts',(-43.5958446617549,-4.5354323630066,132.711858083544));
#83768=CARTESIAN_POINT('Ctrl Pts',(-43.6037681907354,-4.47764760974547,
132.839023966978));
#83769=CARTESIAN_POINT('Ctrl Pts',(-43.6117063611401,-4.41975607943011,
132.966424832785));
#83770=CARTESIAN_POINT('Ctrl Pts',(-43.6196445315447,-4.35648833193795,
133.091210065452));
#83771=CARTESIAN_POINT('Ctrl Pts',(-43.6275827019493,-4.28812390246818,
133.212923770066));
#83772=CARTESIAN_POINT('Ctrl Pts',(-43.6337872337607,-4.234689766415,133.308056088178));
#83773=CARTESIAN_POINT('Ctrl Pts',(-43.6399917655722,-4.17814293966459,
133.401312488867));
#83774=CARTESIAN_POINT('Ctrl Pts',(-43.6461962973837,-4.11863445846413,
133.492488825084));
#83775=CARTESIAN_POINT('Ctrl Pts',(-43.6539706315028,-4.04406979672443,
133.606733593754));
#83776=CARTESIAN_POINT('Ctrl Pts',(-43.6617449656219,-3.96462995860692,
133.718054498226));
#83777=CARTESIAN_POINT('Ctrl Pts',(-43.669519299741,-3.88057133770916,133.826007379755));
#83778=CARTESIAN_POINT('Ctrl Pts',(-43.6772840526881,-3.79661631154923,
133.933827219007));
#83779=CARTESIAN_POINT('Ctrl Pts',(-43.6850488056352,-3.70805406635717,
134.038286988629));
#83780=CARTESIAN_POINT('Ctrl Pts',(-43.6928135585823,-3.61518520979579,
134.138969884238));
#83781=CARTESIAN_POINT('Ctrl Pts',(-43.7005705994673,-3.52240859189197,
134.239552780175));
#83782=CARTESIAN_POINT('Ctrl Pts',(-43.7083276403523,-3.42533413817417,
134.336365981722));
#83783=CARTESIAN_POINT('Ctrl Pts',(-43.7160846812373,-3.32430357908102,
134.429024571177));
#83784=CARTESIAN_POINT('Ctrl Pts',(-43.7238358724774,-3.22334920791825,
134.521613286069));
#83785=CARTESIAN_POINT('Ctrl Pts',(-43.7315870637176,-3.11844495648586,
134.610053361777));
#83786=CARTESIAN_POINT('Ctrl Pts',(-43.7393382549577,-3.00997011730864,
134.693995941785));
#83787=CARTESIAN_POINT('Ctrl Pts',(-43.7470861517348,-2.90154138283189,
134.777902843956));
#83788=CARTESIAN_POINT('Ctrl Pts',(-43.754834048512,-2.78954538754161,134.857315813596));
#83789=CARTESIAN_POINT('Ctrl Pts',(-43.762581945289,-2.6743951105537,134.931925741843));
#83790=CARTESIAN_POINT('Ctrl Pts',(-43.7703282213731,-2.55926892052122,
135.006520063301));
#83791=CARTESIAN_POINT('Ctrl Pts',(-43.7780744974572,-2.44099008908846,
135.076313129294));
#83792=CARTESIAN_POINT('Ctrl Pts',(-43.7858207735414,-2.32000089894515,
135.141038942205));
#83793=CARTESIAN_POINT('Ctrl Pts',(-43.7935671068067,-2.19901081568729,
135.205765232907));
#83794=CARTESIAN_POINT('Ctrl Pts',(-43.8013134400721,-2.07531067853034,
135.265424011464));
#83795=CARTESIAN_POINT('Ctrl Pts',(-43.8090597733374,-1.94936735072531,
135.319795258265));
#83796=CARTESIAN_POINT('Ctrl Pts',(-43.8168078413404,-1.82339581878525,
135.37417868113));
#83797=CARTESIAN_POINT('Ctrl Pts',(-43.8245559093433,-1.69518045546037,
135.423272061075));
#83798=CARTESIAN_POINT('Ctrl Pts',(-43.8323039773463,-1.56520769758678,
135.466903692532));
#83799=CARTESIAN_POINT('Ctrl Pts',(-43.8400602800882,-1.43509680311924,
135.510581696207));
#83800=CARTESIAN_POINT('Ctrl Pts',(-43.84781658283,-1.30322515424092,135.548786231037));
#83801=CARTESIAN_POINT('Ctrl Pts',(-43.8555728855719,-1.17009446905893,
135.581395471529));
#83802=CARTESIAN_POINT('Ctrl Pts',(-43.8633333280861,-1.03689272802176,
135.614022116555));
#83803=CARTESIAN_POINT('Ctrl Pts',(-43.8710937706003,-0.902430994805061,
135.641047439633));
#83804=CARTESIAN_POINT('Ctrl Pts',(-43.8788542131145,-0.767219768351191,
135.662401054774));
#83805=CARTESIAN_POINT('Ctrl Pts',(-43.8866271133799,-0.631791488833129,
135.683788948635));
#83806=CARTESIAN_POINT('Ctrl Pts',(-43.8944000136453,-0.495611700411419,
135.699486895612));
#83807=CARTESIAN_POINT('Ctrl Pts',(-43.9021729139107,-0.359195494525443,
135.709476483599));
#83808=CARTESIAN_POINT('Ctrl Pts',(-43.9096632496726,-0.227738361337324,
135.719102924902));
#83809=CARTESIAN_POINT('Ctrl Pts',(-43.9171535854345,-0.0960620088562741,
135.723428818088));
#83810=CARTESIAN_POINT('Ctrl Pts',(-43.9246439211965,0.0353758646920503,
135.722483390606));
#83811=CARTESIAN_POINT('Ctrl Pts',(-43.9324182553156,0.171797245167937,
135.721502116954));
#83812=CARTESIAN_POINT('Ctrl Pts',(-43.9401925894346,0.308393847800017,
135.714838799324));
#83813=CARTESIAN_POINT('Ctrl Pts',(-43.9479669235537,0.444653402256518,
135.702469070261));
#83814=CARTESIAN_POINT('Ctrl Pts',(-43.9557316765008,0.580745028990202,
135.690114585784));
#83815=CARTESIAN_POINT('Ctrl Pts',(-43.963496429448,0.716500048407952,135.672067717744));
#83816=CARTESIAN_POINT('Ctrl Pts',(-43.9712611823951,0.851405305390756,
135.648356082929));
#83817=CARTESIAN_POINT('Ctrl Pts',(-43.9790182232801,0.986176572570312,
135.624667998844));
#83818=CARTESIAN_POINT('Ctrl Pts',(-43.986775264165,1.12009937433432,135.59532641187));
#83819=CARTESIAN_POINT('Ctrl Pts',(-43.9945323050501,1.25266515486895,135.560410772083));
#83820=CARTESIAN_POINT('Ctrl Pts',(-44.0022834962902,1.38513096651745,135.525521462451));
#83821=CARTESIAN_POINT('Ctrl Pts',(-44.0100346875303,1.51624141729157,135.485066565867));
#83822=CARTESIAN_POINT('Ctrl Pts',(-44.0177858787705,1.64549798744993,135.439176626406));
#83823=CARTESIAN_POINT('Ctrl Pts',(-44.0255337755476,1.77469962011776,135.393306191393));
#83824=CARTESIAN_POINT('Ctrl Pts',(-44.0332816723247,1.90204857167684,135.342005438524));
#83825=CARTESIAN_POINT('Ctrl Pts',(-44.0410295691018,2.02706155478761,135.285454737935));
#83826=CARTESIAN_POINT('Ctrl Pts',(-44.0487758451859,2.15204838787728,135.228915866533));
#83827=CARTESIAN_POINT('Ctrl Pts',(-44.05652212127,2.27469986845013,135.167129392778));
#83828=CARTESIAN_POINT('Ctrl Pts',(-44.0642683973541,2.39455314057997,135.100323643412));
#83829=CARTESIAN_POINT('Ctrl Pts',(-44.0720147306195,2.51440729743944,135.033517400902));
#83830=CARTESIAN_POINT('Ctrl Pts',(-44.0797610638849,2.63146286314099,134.961691999199));
#83831=CARTESIAN_POINT('Ctrl Pts',(-44.0875073971502,2.74528237796421,134.885121297603));
#83832=CARTESIAN_POINT('Ctrl Pts',(-44.0952554651532,2.85912738187861,134.80853344853));
#83833=CARTESIAN_POINT('Ctrl Pts',(-44.1030035331562,2.96973456853441,134.72719840315));
#83834=CARTESIAN_POINT('Ctrl Pts',(-44.1107516011591,3.07669654618326,134.641432603495));
#83835=CARTESIAN_POINT('Ctrl Pts',(-44.118507903901,3.18377220429482,134.555575650928));
#83836=CARTESIAN_POINT('Ctrl Pts',(-44.126264206643,3.28719460881878,134.465278782201));
#83837=CARTESIAN_POINT('Ctrl Pts',(-44.1340205093848,3.38659007362532,134.370898257312));
#83838=CARTESIAN_POINT('Ctrl Pts',(-44.141780951899,3.4860385887843,134.276467358694));
#83839=CARTESIAN_POINT('Ctrl Pts',(-44.1495413944132,3.5814556097007,134.177948741638));
#83840=CARTESIAN_POINT('Ctrl Pts',(-44.1573018369274,3.67250598150133,134.075733858017));
#83841=CARTESIAN_POINT('Ctrl Pts',(-44.1650747371929,3.76370251544173,133.97335488999));
#83842=CARTESIAN_POINT('Ctrl Pts',(-44.1728476374583,3.85051814484051,133.867268100963));
#83843=CARTESIAN_POINT('Ctrl Pts',(-44.1806205377237,3.93265895956695,133.75789689976));
#83844=CARTESIAN_POINT('Ctrl Pts',(-44.1881108734857,4.01181374877653,133.652501617212));
#83845=CARTESIAN_POINT('Ctrl Pts',(-44.1956012092476,4.08662753011999,133.544056823535));
#83846=CARTESIAN_POINT('Ctrl Pts',(-44.2030915450095,4.15687749640477,133.432963391357));
#83847=CARTESIAN_POINT('Ctrl Pts',(-44.2108658791286,4.22979101151448,133.317657817931));
#83848=CARTESIAN_POINT('Ctrl Pts',(-44.2186402132476,4.29801877395729,133.19913354158));
#83849=CARTESIAN_POINT('Ctrl Pts',(-44.2264145473667,4.36126338807634,133.077808378638));
#83850=CARTESIAN_POINT('Ctrl Pts',(-44.2341793003138,4.42443005886066,132.956632738118));
#83851=CARTESIAN_POINT('Ctrl Pts',(-44.2419440532609,4.48262562166015,132.832663422505));
#83852=CARTESIAN_POINT('Ctrl Pts',(-44.249708806208,4.53559593838496,132.706347091284));
#83853=CARTESIAN_POINT('Ctrl Pts',(-44.257465847093,4.58851364424459,132.580156219223));
#83854=CARTESIAN_POINT('Ctrl Pts',(-44.265222887978,4.63621628172619,132.451623328741));
#83855=CARTESIAN_POINT('Ctrl Pts',(-44.272979928863,4.67849580758928,132.321219226952));
#83856=CARTESIAN_POINT('Ctrl Pts',(-44.2807311201031,4.72074345013275,132.190913463912));
#83857=CARTESIAN_POINT('Ctrl Pts',(-44.2884823113432,4.75757600108842,132.058739668667));
#83858=CARTESIAN_POINT('Ctrl Pts',(-44.2962335025833,4.78883382878659,131.925187822254));
#83859=CARTESIAN_POINT('Ctrl Pts',(-44.3039813993604,4.82007837107434,131.791692738938));
#83860=CARTESIAN_POINT('Ctrl Pts',(-44.3117292961374,4.8457528137615,131.656821149266));
#83861=CARTESIAN_POINT('Ctrl Pts',(-44.3194771929145,4.86574767873999,131.521077151027));
#83862=CARTESIAN_POINT('Ctrl Pts',(-44.3272234689986,4.88573836122371,131.385361547507));
#83863=CARTESIAN_POINT('Ctrl Pts',(-44.3349697450827,4.9000517721482,131.248774284948));
#83864=CARTESIAN_POINT('Ctrl Pts',(-44.3427160211668,4.9086298243352,131.111828193331));
#83865=CARTESIAN_POINT('Ctrl Pts',(-44.3504623544322,4.91720793984345,130.97488109081));
#83866=CARTESIAN_POINT('Ctrl Pts',(-44.3582086876976,4.92005058769212,130.837575544146));
#83867=CARTESIAN_POINT('Ctrl Pts',(-44.3659550209629,4.91715171580341,130.700427628233));
#83868=CARTESIAN_POINT('Ctrl Pts',(-44.3737030889658,4.91425219473244,130.563248998997));
#83869=CARTESIAN_POINT('Ctrl Pts',(-44.3814511569688,4.905608603644,130.426228461559));
#83870=CARTESIAN_POINT('Ctrl Pts',(-44.3891992249717,4.89126696899205,130.289879810784));
#83871=CARTESIAN_POINT('Ctrl Pts',(-44.3969555277135,4.87691009188006,130.153386247039));
#83872=CARTESIAN_POINT('Ctrl Pts',(-44.4047118304553,4.85684311475774,130.017566385868));
#83873=CARTESIAN_POINT('Ctrl Pts',(-44.4124681331972,4.8311637827703,129.882927187226));
#83874=CARTESIAN_POINT('Ctrl Pts',(-44.4202285757113,4.80547074495019,129.748216127589));
#83875=CARTESIAN_POINT('Ctrl Pts',(-44.4279890182255,4.7741594727249,129.614687366572));
#83876=CARTESIAN_POINT('Ctrl Pts',(-44.4357494607397,4.73737814624568,129.482834468762));
#83877=CARTESIAN_POINT('Ctrl Pts',(-44.4435223610051,4.70053777511584,129.350769908974));
#83878=CARTESIAN_POINT('Ctrl Pts',(-44.4512952612706,4.65820992325379,129.220386960431));
#83879=CARTESIAN_POINT('Ctrl Pts',(-44.459068161536,4.61059195088929,129.092161760863));
#83880=CARTESIAN_POINT('Ctrl Pts',(-44.4665584972981,4.56470501176229,128.968597870278));
#83881=CARTESIAN_POINT('Ctrl Pts',(-44.4740488330602,4.51390601176882,128.8470378573));
#83882=CARTESIAN_POINT('Ctrl Pts',(-44.4815391688223,4.45841178367465,128.72788585738));
#83883=CARTESIAN_POINT('Ctrl Pts',(-44.4893135029414,4.40081347505575,128.604216173168));
#83884=CARTESIAN_POINT('Ctrl Pts',(-44.4970878370605,4.33797441673603,128.48274895783));
#83885=CARTESIAN_POINT('Ctrl Pts',(-44.5048621711796,4.27008537981359,128.36396025869));
#83886=CARTESIAN_POINT('Ctrl Pts',(-44.5126269241266,4.20228001006175,128.245317956005));
#83887=CARTESIAN_POINT('Ctrl Pts',(-44.5203916770737,4.12943723704211,128.12934793763));
#83888=CARTESIAN_POINT('Ctrl Pts',(-44.5281564300208,4.05179548018321,128.016505447499));
#83889=CARTESIAN_POINT('Ctrl Pts',(-44.5359134709058,3.97423083821178,127.903775034121));
#83890=CARTESIAN_POINT('Ctrl Pts',(-44.5436705117908,3.89187691796901,127.794166287303));
#83891=CARTESIAN_POINT('Ctrl Pts',(-44.5514275526758,3.80501737036232,127.688108722462));
#83892=CARTESIAN_POINT('Ctrl Pts',(-44.5591787439159,3.71822332421578,127.582131136455));
#83893=CARTESIAN_POINT('Ctrl Pts',(-44.5669299351561,3.62693066039519,127.479699703329));
#83894=CARTESIAN_POINT('Ctrl Pts',(-44.5746811263963,3.53146532900853,127.381213572446));
#83895=CARTESIAN_POINT('Ctrl Pts',(-44.5824290231733,3.43604057293472,127.282769300798));
#83896=CARTESIAN_POINT('Ctrl Pts',(-44.5901769199504,3.33644694818695,127.188267276387));
#83897=CARTESIAN_POINT('Ctrl Pts',(-44.5979248167275,3.23304939092162,127.098072083417));
#83898=CARTESIAN_POINT('Ctrl Pts',(-44.6056710928116,3.12967346219642,127.007895757338));
#83899=CARTESIAN_POINT('Ctrl Pts',(-44.6134173688957,3.02249547808234,126.922024727607));
#83900=CARTESIAN_POINT('Ctrl Pts',(-44.6211636449798,2.91191549942818,126.840785061747));
#83901=CARTESIAN_POINT('Ctrl Pts',(-44.6289099782451,2.80133470449758,126.759544796193));
#83902=CARTESIAN_POINT('Ctrl Pts',(-44.6366563115104,2.68735217999173,126.682936194203));
#83903=CARTESIAN_POINT('Ctrl Pts',(-44.6444026447758,2.57039884303922,126.611243298649));
#83904=CARTESIAN_POINT('Ctrl Pts',(-44.6521507127788,2.45341931519795,126.539534347968));
#83905=CARTESIAN_POINT('Ctrl Pts',(-44.6598987807817,2.33346798431292,126.472743498552));
#83906=CARTESIAN_POINT('Ctrl Pts',(-44.6676468487847,2.2110019989777,126.411109745715));
#83907=CARTESIAN_POINT('Ctrl Pts',(-44.6754031515265,2.0884058553359,126.349410487793));
#83908=CARTESIAN_POINT('Ctrl Pts',(-44.6831594542683,1.96329006821664,126.292879451425));
#83909=CARTESIAN_POINT('Ctrl Pts',(-44.6909157570102,1.8361339910268,126.241708425091));
#83910=CARTESIAN_POINT('Ctrl Pts',(-44.6986761995243,1.7089100468098,126.19051008724));
#83911=CARTESIAN_POINT('Ctrl Pts',(-44.7064366420385,1.57964401097734,126.144677590393));
#83912=CARTESIAN_POINT('Ctrl Pts',(-44.7141970845527,1.44883122838508,126.104353050109));
#83913=CARTESIAN_POINT('Ctrl Pts',(-44.7219699848181,1.3178084535012,126.063963777292));
#83914=CARTESIAN_POINT('Ctrl Pts',(-44.7297428850836,1.18523434840905,126.029100229383));
#83915=CARTESIAN_POINT('Ctrl Pts',(-44.737515785349,1.05161617928934,125.999853725703));
#83916=CARTESIAN_POINT('Ctrl Pts',(-44.7450061211111,0.9228553671799,125.971670406099));
#83917=CARTESIAN_POINT('Ctrl Pts',(-44.7524964568731,0.793125385172624,
125.948702887214));
#83918=CARTESIAN_POINT('Ctrl Pts',(-44.7599867926352,0.662883447272754,
125.930987186581));
#83919=CARTESIAN_POINT('Ctrl Pts',(-44.7677611267543,0.527703346711997,
125.912599789774));
#83920=CARTESIAN_POINT('Ctrl Pts',(-44.7755354608734,0.391543492366668,
125.899812072342));
#83921=CARTESIAN_POINT('Ctrl Pts',(-44.7833097949925,0.254907512770367,
125.892720848361));
#83922=CARTESIAN_POINT('Ctrl Pts',(-44.7910745479396,0.118439924807596,
125.885638363681));
#83923=CARTESIAN_POINT('Ctrl Pts',(-44.7988393008868,-0.0185022341936729,
125.88423842398));
#83924=CARTESIAN_POINT('Ctrl Pts',(-44.8066040538339,-0.155407083093876,
125.888566510708));
#83925=CARTESIAN_POINT('Ctrl Pts',(-44.8143610947189,-0.292175956168876,
125.892890298718));
#83926=CARTESIAN_POINT('Ctrl Pts',(-44.8221181356039,-0.428907204646427,
125.902930779205));
#83927=CARTESIAN_POINT('Ctrl Pts',(-44.829875176489,-0.565086144798041,
125.918681472201));
#83928=CARTESIAN_POINT('Ctrl Pts',(-44.8376263677291,-0.701162391350457,
125.934420287476));
#83929=CARTESIAN_POINT('Ctrl Pts',(-44.8453775589691,-0.836686771790337,
125.955860699459));
#83930=CARTESIAN_POINT('Ctrl Pts',(-44.8531287502092,-0.971147286457694,
125.982944227074));
#83931=CARTESIAN_POINT('Ctrl Pts',(-44.8608766469863,-1.10555065181983,
126.010016243467));
#83932=CARTESIAN_POINT('Ctrl Pts',(-44.8686245437635,-1.23889066827852,
126.042726528072));
#83933=CARTESIAN_POINT('Ctrl Pts',(-44.8763724405406,-1.37066334391245,
126.08096511643));
#83934=CARTESIAN_POINT('Ctrl Pts',(-44.8841187166247,-1.50240845554332,
126.119195706099));
#83935=CARTESIAN_POINT('Ctrl Pts',(-44.8918649927088,-1.63258650323105,
126.162952190487));
#83936=CARTESIAN_POINT('Ctrl Pts',(-44.8996112687929,-1.76070691447579,
126.21207423453));
#83937=CARTESIAN_POINT('Ctrl Pts',(-44.9073576020582,-1.88882827147647,
126.261196641181));
#83938=CARTESIAN_POINT('Ctrl Pts',(-44.9151039353236,-2.01489159667214,
126.315684546556));
#83939=CARTESIAN_POINT('Ctrl Pts',(-44.9228502685889,-2.1384249955175,126.375328939982));
#83940=CARTESIAN_POINT('Ctrl Pts',(-44.9305983365919,-2.26198605881085,
126.434986690355));
#83941=CARTESIAN_POINT('Ctrl Pts',(-44.938346404595,-2.38301571635764,126.499803056661));
#83942=CARTESIAN_POINT('Ctrl Pts',(-44.9460944725979,-2.50106579464921,
126.569522609645));
#83943=CARTESIAN_POINT('Ctrl Pts',(-44.9538507753398,-2.61924133796896,
126.639316261399));
#83944=CARTESIAN_POINT('Ctrl Pts',(-44.9616070780816,-2.73443063896892,
126.714023310562));
#83945=CARTESIAN_POINT('Ctrl Pts',(-44.9693633808235,-2.84621323834376,
126.793344129894));
#83946=CARTESIAN_POINT('Ctrl Pts',(-44.9771238233376,-2.95805549945745,
126.872707285136));
#83947=CARTESIAN_POINT('Ctrl Pts',(-44.9848842658519,-3.06648712696398,
126.95668887802));
#83948=CARTESIAN_POINT('Ctrl Pts',(-44.9926447083661,-3.17112080902666,
127.04494897782));
#83949=CARTESIAN_POINT('Ctrl Pts',(-45.0004176086316,-3.27592245836488,
127.133350760568));
#83950=CARTESIAN_POINT('Ctrl Pts',(-45.0081905088969,-3.37691369071269,
127.226044510642));
#83951=CARTESIAN_POINT('Ctrl Pts',(-45.0159634091624,-3.47374348677721,
127.322652810961));
#83952=CARTESIAN_POINT('Ctrl Pts',(-45.0234537449243,-3.56705327585367,
127.415749156221));
#83953=CARTESIAN_POINT('Ctrl Pts',(-45.0309440806862,-3.65649872407,127.512480159255));
#83954=CARTESIAN_POINT('Ctrl Pts',(-45.0384344164481,-3.74180239351616,
127.612480621329));
#83955=CARTESIAN_POINT('Ctrl Pts',(-45.04615639937,-3.82974417604411,127.715573711527));
#83956=CARTESIAN_POINT('Ctrl Pts',(-45.0538783822918,-3.91357280490112,
127.822480679164));
#83957=CARTESIAN_POINT('Ctrl Pts',(-45.0616003652137,-3.99293570973049,
127.932837070656));
#83958=CARTESIAN_POINT('Ctrl Pts',(-45.0693129442786,-4.07220196614547,
128.04305906976));
#83959=CARTESIAN_POINT('Ctrl Pts',(-45.0770255233434,-4.14701308527094,
128.156721819437));
#83960=CARTESIAN_POINT('Ctrl Pts',(-45.0847381024084,-4.21705489348378,
128.273425792675));
#83961=CARTESIAN_POINT('Ctrl Pts',(-45.0924415360908,-4.28701364788033,
128.389991381275));
#83962=CARTESIAN_POINT('Ctrl Pts',(-45.1001449697733,-4.35221414822146,
128.509590675735));
#83963=CARTESIAN_POINT('Ctrl Pts',(-45.1078484034558,-4.4123843589793,128.631793626393));
#83964=CARTESIAN_POINT('Ctrl Pts',(-45.1155465568533,-4.47251332632922,
128.753912813573));
#83965=CARTESIAN_POINT('Ctrl Pts',(-45.1232447102508,-4.52761868702478,
128.878631753324));
#83966=CARTESIAN_POINT('Ctrl Pts',(-45.1309428636483,-4.57747339277889,
129.005494196483));
#83967=CARTESIAN_POINT('Ctrl Pts',(-45.1386373384577,-4.62730427529659,
129.132296018002));
#83968=CARTESIAN_POINT('Ctrl Pts',(-45.146331813267,-4.67188935044903,129.261238936517));
#83969=CARTESIAN_POINT('Ctrl Pts',(-45.1540262880764,-4.71104914957288,
129.391845494529));
#83970=CARTESIAN_POINT('Ctrl Pts',(-45.1577483017301,-4.72999174287846,
129.455023216755));
#83971=CARTESIAN_POINT('Ctrl Pts',(-45.1614703153837,-4.74766559605856,
129.518589921493));
#83972=CARTESIAN_POINT('Ctrl Pts',(-45.1651923290374,-4.76405452823407,
129.582490119308));
#83973=CARTESIAN_POINT('Ctrl Pts',(-43.4154178838317,-4.76405452823406,
129.582490119308));
#83974=CARTESIAN_POINT('Ctrl Pts',(-43.423896563135,-4.80116832061884,129.727196232536));
#83975=CARTESIAN_POINT('Ctrl Pts',(-43.4323752424382,-4.83172860360835,
129.873764859095));
#83976=CARTESIAN_POINT('Ctrl Pts',(-43.4408539217414,-4.85556247859763,
130.021611565229));
#83977=CARTESIAN_POINT('Ctrl Pts',(-43.4492996326952,-4.87930367836105,
130.168883386797));
#83978=CARTESIAN_POINT('Ctrl Pts',(-43.4577453436491,-4.89637057697915,
130.317423117939));
#83979=CARTESIAN_POINT('Ctrl Pts',(-43.4661910546028,-4.90664090648471,
130.46663576312));
#83980=CARTESIAN_POINT('Ctrl Pts',(-43.4725075577236,-4.91432203229262,
130.578231121296));
#83981=CARTESIAN_POINT('Ctrl Pts',(-43.4788240608444,-4.91820250836251,
130.690202491997));
#83982=CARTESIAN_POINT('Ctrl Pts',(-43.4851405639651,-4.91824956659705,
130.802295873524));
#83983=CARTESIAN_POINT('',(-43.1398594360288,-4.91824904124129,130.801289652058));
#83984=CARTESIAN_POINT('Ctrl Pts',(-43.0697814015304,-4.7640545282341,129.582490119308));
#83985=CARTESIAN_POINT('Ctrl Pts',(-43.0775551247889,-4.79809906899389,
129.715229267033));
#83986=CARTESIAN_POINT('Ctrl Pts',(-43.0853288480475,-4.82655307337718,
129.849241521043));
#83987=CARTESIAN_POINT('Ctrl Pts',(-43.0931025713061,-4.84935232322232,
129.984016112033));
#83988=CARTESIAN_POINT('Ctrl Pts',(-43.0983650628433,-4.86478647946545,
130.075252977679));
#83989=CARTESIAN_POINT('Ctrl Pts',(-43.1036275543804,-4.87763029253095,
130.166839069195));
#83990=CARTESIAN_POINT('Ctrl Pts',(-43.1088900459175,-4.88787739480595,
130.258615589329));
#83991=CARTESIAN_POINT('Ctrl Pts',(-43.119213175942,-4.90797855191232,130.438648363512));
#83992=CARTESIAN_POINT('Ctrl Pts',(-43.1295363059665,-4.91813572606594,
130.619811829999));
#83993=CARTESIAN_POINT('Ctrl Pts',(-43.1398594359911,-4.91824904124087,
130.801289651394));
#83994=CARTESIAN_POINT('Ctrl Pts',(-43.1398594360288,-4.91824904124129,
130.801289652058));
#83995=CARTESIAN_POINT('Ctrl Pts',(-43.1475252570698,-4.91833318758668,
130.936052703421));
#83996=CARTESIAN_POINT('Ctrl Pts',(-43.1551910781108,-4.91287427796632,
131.071037008464));
#83997=CARTESIAN_POINT('Ctrl Pts',(-43.1628568991518,-4.90184420580349,
131.205741290408));
#83998=CARTESIAN_POINT('Ctrl Pts',(-43.1705143159875,-4.89082622614698,
131.340297893137));
#83999=CARTESIAN_POINT('Ctrl Pts',(-43.1781717328232,-4.87424926385755,
131.474574685797));
#84000=CARTESIAN_POINT('Ctrl Pts',(-43.185829149659,-4.85213722165147,131.608069174671));
#84001=CARTESIAN_POINT('Ctrl Pts',(-43.1934801194527,-4.83004379633255,
131.741451269954));
#84002=CARTESIAN_POINT('Ctrl Pts',(-43.2011310892465,-4.80242462678519,
131.874051976868));
#84003=CARTESIAN_POINT('Ctrl Pts',(-43.2087820590402,-4.76935548930471,
132.005373223303));
#84004=CARTESIAN_POINT('Ctrl Pts',(-43.2164290232409,-4.7363036648593,132.136625717737));
#84005=CARTESIAN_POINT('Ctrl Pts',(-43.2240759874416,-4.69780764424593,
132.266599694645));
#84006=CARTESIAN_POINT('Ctrl Pts',(-43.2317229516423,-4.65399434532609,
132.394807000244));
#84007=CARTESIAN_POINT('Ctrl Pts',(-43.2393679196004,-4.61019248388249,
132.522980837283));
#84008=CARTESIAN_POINT('Ctrl Pts',(-43.2470128875585,-4.56107623362987,
132.649388539521));
#84009=CARTESIAN_POINT('Ctrl Pts',(-43.2546578555166,-4.50682230966105,
132.773557339999));
#84010=CARTESIAN_POINT('Ctrl Pts',(-43.2623025866572,-4.45257006631166,
132.89772229411));
#84011=CARTESIAN_POINT('Ctrl Pts',(-43.2699473177977,-4.39318062689535,
133.019648115778));
#84012=CARTESIAN_POINT('Ctrl Pts',(-43.2775920489383,-4.32887854308547,
133.138882757473));
#84013=CARTESIAN_POINT('Ctrl Pts',(-43.285238302273,-4.26456365565251,133.258141140784));
#84014=CARTESIAN_POINT('Ctrl Pts',(-43.2928845556078,-4.19533436993311,
133.374706924719));
#84015=CARTESIAN_POINT('Ctrl Pts',(-43.3005308089425,-4.12146052871224,
133.488153860863));
#84016=CARTESIAN_POINT('Ctrl Pts',(-43.3081848797822,-4.04751115911255,
133.601716784792));
#84017=CARTESIAN_POINT('Ctrl Pts',(-43.3158389506219,-3.96890797140104,
133.712154155884));
#84018=CARTESIAN_POINT('Ctrl Pts',(-43.3234930214615,-3.88596356903981,
133.819069592342));
#84019=CARTESIAN_POINT('Ctrl Pts',(-43.3311511956406,-3.80297470027136,
133.926042346053));
#84020=CARTESIAN_POINT('Ctrl Pts',(-43.3388093698195,-3.71564024226348,
134.029489098929));
#84021=CARTESIAN_POINT('Ctrl Pts',(-43.3464675439986,-3.62431133920984,
134.129048629842));
#84022=CARTESIAN_POINT('Ctrl Pts',(-43.354137477867,-3.53284219391221,134.228761041734));
#84023=CARTESIAN_POINT('Ctrl Pts',(-43.3618074117354,-3.43736663688643,
134.324574025734));
#84024=CARTESIAN_POINT('Ctrl Pts',(-43.3694773456038,-3.33827113849234,
134.416164719176));
#84025=CARTESIAN_POINT('Ctrl Pts',(-43.3754307869793,-3.26135271254595,
134.487257877645));
#84026=CARTESIAN_POINT('Ctrl Pts',(-43.3813842283549,-3.18225401859903,
134.555807905523));
#84027=CARTESIAN_POINT('Ctrl Pts',(-43.3873376697304,-3.10116787349353,
134.621681783372));
#84028=CARTESIAN_POINT('Ctrl Pts',(-43.3951120038495,-2.9952810855481,134.707703548568));
#84029=CARTESIAN_POINT('Ctrl Pts',(-43.4028863379686,-2.88564469510584,
134.789452515187));
#84030=CARTESIAN_POINT('Ctrl Pts',(-43.4106606720877,-2.77263846903882,
134.866584021381));
#84031=CARTESIAN_POINT('Ctrl Pts',(-43.4184254250348,-2.65977151304591,
134.943620469888));
#84032=CARTESIAN_POINT('Ctrl Pts',(-43.4261901779818,-2.54354330452,135.016050562293));
#84033=CARTESIAN_POINT('Ctrl Pts',(-43.4339549309289,-2.42436736069691,
135.083569184917));
#84034=CARTESIAN_POINT('Ctrl Pts',(-43.4417119718139,-2.30530978410148,
135.151020747092));
#84035=CARTESIAN_POINT('Ctrl Pts',(-43.4494690126989,-2.18331063649303,
135.213570355733));
#84036=CARTESIAN_POINT('Ctrl Pts',(-43.4572260535839,-2.05881285792689,
135.270955817328));
#84037=CARTESIAN_POINT('Ctrl Pts',(-43.464977244824,-1.93440896410333,135.3282980041));
#84038=CARTESIAN_POINT('Ctrl Pts',(-43.4727284360641,-1.80751054340688,
135.380483632242));
#84039=CARTESIAN_POINT('Ctrl Pts',(-43.4804796273042,-1.67858529344036,
135.427296316356));
#84040=CARTESIAN_POINT('Ctrl Pts',(-43.4882275240813,-1.5497148401448,135.47408910383));
#84041=CARTESIAN_POINT('Ctrl Pts',(-43.4959754208584,-1.41881963767101,
135.515513356115));
#84042=CARTESIAN_POINT('Ctrl Pts',(-43.5037233176355,-1.28638732514,135.551400823022));
#84043=CARTESIAN_POINT('Ctrl Pts',(-43.5114695937196,-1.15398271459386,
135.587280783045));
#84044=CARTESIAN_POINT('Ctrl Pts',(-43.5192158698037,-1.02004201064806,
135.617626159171));
#84045=CARTESIAN_POINT('Ctrl Pts',(-43.5269621458878,-0.885067593212989,
135.642318701091));
#84046=CARTESIAN_POINT('Ctrl Pts',(-43.5347084791532,-0.750092179427247,
135.667011425286));
#84047=CARTESIAN_POINT('Ctrl Pts',(-43.5424548124186,-0.614083421508419,
135.686051161653));
#84048=CARTESIAN_POINT('Ctrl Pts',(-43.5502011456839,-0.477553067367593,
135.699370947519));
#84049=CARTESIAN_POINT('Ctrl Pts',(-43.5579492136869,-0.340992138200592,
135.712693716259));
#84050=CARTESIAN_POINT('Ctrl Pts',(-43.5656972816898,-0.203909769420831,
135.720293947615));
#84051=CARTESIAN_POINT('Ctrl Pts',(-43.5734453496928,-0.0668215957981928,
135.722156662222));
#84052=CARTESIAN_POINT('Ctrl Pts',(-43.5812016524346,0.0704122767665552,
135.724021356544));
#84053=CARTESIAN_POINT('Ctrl Pts',(-43.5889579551765,0.207651574945859,
135.720136347583));
#84054=CARTESIAN_POINT('Ctrl Pts',(-43.5967142579183,0.344381342609671,
135.710538819931));
#84055=CARTESIAN_POINT('Ctrl Pts',(-43.6044747004325,0.481184087067524,
135.70093616979));
#84056=CARTESIAN_POINT('Ctrl Pts',(-43.6122351429467,0.617476370794974,
135.685614969333));
#84057=CARTESIAN_POINT('Ctrl Pts',(-43.6199955854609,0.752750582458009,
135.66466406726));
#84058=CARTESIAN_POINT('Ctrl Pts',(-43.6277684857263,0.888241948294685,
135.643679532939));
#84059=CARTESIAN_POINT('Ctrl Pts',(-43.6355413859918,1.02271159247896,135.617047313602));
#84060=CARTESIAN_POINT('Ctrl Pts',(-43.6433142862572,1.15566339996077,135.584907152063));
#84061=CARTESIAN_POINT('Ctrl Pts',(-43.6508046220192,1.28378207435486,135.553935366352));
#84062=CARTESIAN_POINT('Ctrl Pts',(-43.6582949577812,1.41049105426834,135.517849225462));
#84063=CARTESIAN_POINT('Ctrl Pts',(-43.6657852935432,1.53536342308586,135.476816312546));
#84064=CARTESIAN_POINT('Ctrl Pts',(-43.6735596276623,1.66497036572161,135.434227624265));
#84065=CARTESIAN_POINT('Ctrl Pts',(-43.6813339617814,1.79300923364071,135.386174737209));
#84066=CARTESIAN_POINT('Ctrl Pts',(-43.6891082959005,1.9189847797996,135.332790861856));
#84067=CARTESIAN_POINT('Ctrl Pts',(-43.6968730488476,2.04480507235661,135.279472777358));
#84068=CARTESIAN_POINT('Ctrl Pts',(-43.7046378017946,2.16856674616459,135.22083692792));
#84069=CARTESIAN_POINT('Ctrl Pts',(-43.7124025547417,2.28978958427508,135.157066295905));
#84070=CARTESIAN_POINT('Ctrl Pts',(-43.7201595956267,2.41089202215381,135.093359001781));
#84071=CARTESIAN_POINT('Ctrl Pts',(-43.7279166365118,2.52946029867803,135.024527255032));
#84072=CARTESIAN_POINT('Ctrl Pts',(-43.7356736773968,2.64503440310105,134.950801991674));
#84073=CARTESIAN_POINT('Ctrl Pts',(-43.7434248686368,2.7605213521921,134.87713232511));
#84074=CARTESIAN_POINT('Ctrl Pts',(-43.7511760598769,2.87301829517336,134.798576696545));
#84075=CARTESIAN_POINT('Ctrl Pts',(-43.758927251117,2.98209037890282,134.715411631623));
#84076=CARTESIAN_POINT('Ctrl Pts',(-43.7666751478941,3.09111610408784,134.632281914072));
#84077=CARTESIAN_POINT('Ctrl Pts',(-43.7744230446712,3.19671955496161,134.544546893289));
#84078=CARTESIAN_POINT('Ctrl Pts',(-43.7821709414483,3.29849559701849,134.452525890542));
#84079=CARTESIAN_POINT('Ctrl Pts',(-43.7899172175324,3.40025034972128,134.360524136605));
#84080=CARTESIAN_POINT('Ctrl Pts',(-43.7976634936165,3.49817899624824,134.264238446001));
#84081=CARTESIAN_POINT('Ctrl Pts',(-43.8054097697006,3.59191050065179,134.164027567995));
#84082=CARTESIAN_POINT('Ctrl Pts',(-43.8131561029659,3.68564269695988,134.063815950256));
#84083=CARTESIAN_POINT('Ctrl Pts',(-43.8209024362313,3.77517742225239,133.959679372829));
#84084=CARTESIAN_POINT('Ctrl Pts',(-43.8286487694966,3.86018172668997,133.852012188765));
#84085=CARTESIAN_POINT('Ctrl Pts',(-43.8363968374996,3.94520506725216,133.744320893381));
#84086=CARTESIAN_POINT('Ctrl Pts',(-43.8441449055025,4.02569572588994,133.633097724846));
#84087=CARTESIAN_POINT('Ctrl Pts',(-43.8518929735054,4.10136238685134,133.518768404583));
#84088=CARTESIAN_POINT('Ctrl Pts',(-43.8596492762473,4.17710946724056,133.404317573758));
#84089=CARTESIAN_POINT('Ctrl Pts',(-43.8674055789892,4.24802209209454,133.286754323141));
#84090=CARTESIAN_POINT('Ctrl Pts',(-43.875161881731,4.31385319949746,133.166531999089));
#84091=CARTESIAN_POINT('Ctrl Pts',(-43.8829223242452,4.37971944294453,133.046245508762));
#84092=CARTESIAN_POINT('Ctrl Pts',(-43.8906827667594,4.44049859156064,132.923297467377));
#84093=CARTESIAN_POINT('Ctrl Pts',(-43.8984432092736,4.49599101994625,132.798162967615));
#84094=CARTESIAN_POINT('Ctrl Pts',(-43.906216109539,4.55157252970437,132.672827590846));
#84095=CARTESIAN_POINT('Ctrl Pts',(-43.9139890098044,4.60185021659823,132.545299105736));
#84096=CARTESIAN_POINT('Ctrl Pts',(-43.9217619100698,4.64667348791094,132.416070442331));
#84097=CARTESIAN_POINT('Ctrl Pts',(-43.9292522458319,4.68986732040879,132.291539566348));
#84098=CARTESIAN_POINT('Ctrl Pts',(-43.936742581594,4.72799632674821,132.165430272357));
#84099=CARTESIAN_POINT('Ctrl Pts',(-43.9442329173561,4.76097074052283,132.038192320184));
#84100=CARTESIAN_POINT('Ctrl Pts',(-43.9520072514752,4.79519538921773,131.906130102383));
#84101=CARTESIAN_POINT('Ctrl Pts',(-43.9597815855943,4.82397527004242,131.772433617343));
#84102=CARTESIAN_POINT('Ctrl Pts',(-43.9675559197134,4.84715476362069,131.637591533945));
#84103=CARTESIAN_POINT('Ctrl Pts',(-43.9753206726604,4.8703056905447,131.502915631363));
#84104=CARTESIAN_POINT('Ctrl Pts',(-43.9830854256075,4.88786989749892,131.367097321195));
#84105=CARTESIAN_POINT('Ctrl Pts',(-43.9908501785546,4.89974176373797,131.230639529995));
#84106=CARTESIAN_POINT('Ctrl Pts',(-43.9986072194395,4.91160183867211,131.094317270598));
#84107=CARTESIAN_POINT('Ctrl Pts',(-44.0063642603246,4.91778079036836,130.957357181104));
#84108=CARTESIAN_POINT('Ctrl Pts',(-44.0141213012096,4.91822426479209,130.820271108139));
#84109=CARTESIAN_POINT('Ctrl Pts',(-44.0218724924497,4.91866740478831,130.683288412848));
#84110=CARTESIAN_POINT('Ctrl Pts',(-44.0296236836898,4.91338367523699,130.546180312571));
#84111=CARTESIAN_POINT('Ctrl Pts',(-44.03737487493,4.9023706762507,130.409462130436));
#84112=CARTESIAN_POINT('Ctrl Pts',(-44.045122771707,4.89136235808281,130.272802057177));
#84113=CARTESIAN_POINT('Ctrl Pts',(-44.0528706684841,4.87462964501886,130.136531961333));
#84114=CARTESIAN_POINT('Ctrl Pts',(-44.0606185652611,4.85222220598737,130.001165294981));
#84115=CARTESIAN_POINT('Ctrl Pts',(-44.0683648413452,4.82981945410904,129.865826944417));
#84116=CARTESIAN_POINT('Ctrl Pts',(-44.0761111174292,4.80174440113933,129.73139203293));
#84117=CARTESIAN_POINT('Ctrl Pts',(-44.0838573935133,4.76809831900315,129.598366636313));
#84118=CARTESIAN_POINT('Ctrl Pts',(-44.0916037267786,4.73445198849929,129.465340257732));
#84119=CARTESIAN_POINT('Ctrl Pts',(-44.099350060044,4.69523464263664,129.333723793812));
#84120=CARTESIAN_POINT('Ctrl Pts',(-44.1070963933093,4.65059809428449,129.204010522138));
#84121=CARTESIAN_POINT('Ctrl Pts',(-44.1148444613123,4.60595154988658,129.074268202075));
#84122=CARTESIAN_POINT('Ctrl Pts',(-44.1225925293153,4.55588351528176,128.946430291979));
#84123=CARTESIAN_POINT('Ctrl Pts',(-44.1303405973183,4.50059469868046,128.820971996869));
#84124=CARTESIAN_POINT('Ctrl Pts',(-44.1380969000601,4.44524712046716,128.695380363191));
#84125=CARTESIAN_POINT('Ctrl Pts',(-44.145853202802,4.38466783402944,128.572173754951));
#84126=CARTESIAN_POINT('Ctrl Pts',(-44.1536095055439,4.3191047094967,128.451805077116));
#84127=CARTESIAN_POINT('Ctrl Pts',(-44.161369948058,4.25350659195023,128.331372154892));
#84128=CARTESIAN_POINT('Ctrl Pts',(-44.1691303905721,4.1829195371035,128.213780516265));
#84129=CARTESIAN_POINT('Ctrl Pts',(-44.1768908330862,4.10763535148138,128.099454910936));
#84130=CARTESIAN_POINT('Ctrl Pts',(-44.1846637333516,4.03223031300107,127.984945779996));
#84131=CARTESIAN_POINT('Ctrl Pts',(-44.1924366336171,3.95211330455078,127.873713476816));
#84132=CARTESIAN_POINT('Ctrl Pts',(-44.2002095338825,3.86761764309672,127.766151140044));
#84133=CARTESIAN_POINT('Ctrl Pts',(-44.2076998696447,3.78619361176687,127.662498965145));
#84134=CARTESIAN_POINT('Ctrl Pts',(-44.2151902054068,3.70070395040982,127.562254798448));
#84135=CARTESIAN_POINT('Ctrl Pts',(-44.222680541169,3.61147853377034,127.465737269146));
#84136=CARTESIAN_POINT('Ctrl Pts',(-44.2304548752881,3.5188701083408,127.365560248386));
#84137=CARTESIAN_POINT('Ctrl Pts',(-44.2382292094072,3.42194369756848,127.269080703677));
#84138=CARTESIAN_POINT('Ctrl Pts',(-44.2460035435263,3.32102631634885,127.176693699474));
#84139=CARTESIAN_POINT('Ctrl Pts',(-44.2537682964734,3.22023330678206,127.084420553997));
#84140=CARTESIAN_POINT('Ctrl Pts',(-44.2615330494204,3.11545939875045,126.996230175049));
#84141=CARTESIAN_POINT('Ctrl Pts',(-44.2692978023676,3.00707062801688,126.912483268443));
#84142=CARTESIAN_POINT('Ctrl Pts',(-44.2770548432526,2.89878951053901,126.828819540445));
#84143=CARTESIAN_POINT('Ctrl Pts',(-44.2848118841376,2.78690098265716,126.749590739578));
#84144=CARTESIAN_POINT('Ctrl Pts',(-44.2925689250226,2.67180629575129,126.675119261035));
#84145=CARTESIAN_POINT('Ctrl Pts',(-44.3003201162627,2.55679840264411,126.600703942013));
#84146=CARTESIAN_POINT('Ctrl Pts',(-44.3080713075028,2.43858948989276,126.531039016076));
#84147=CARTESIAN_POINT('Ctrl Pts',(-44.315822498743,2.3176118162437,126.466405047057));
#84148=CARTESIAN_POINT('Ctrl Pts',(-44.3235703955201,2.19668556133264,126.401798549199));
#84149=CARTESIAN_POINT('Ctrl Pts',(-44.3313182922971,2.0729932301979,126.342218939208));
#84150=CARTESIAN_POINT('Ctrl Pts',(-44.3390661890742,1.9469936518833,126.287901962599));
#84151=CARTESIAN_POINT('Ctrl Pts',(-44.3468124651583,1.82102042996425,126.23359634793));
#84152=CARTESIAN_POINT('Ctrl Pts',(-44.3545587412426,1.69274127963389,126.184551331707));
#84153=CARTESIAN_POINT('Ctrl Pts',(-44.3623050173267,1.56263671673807,126.140955257317));
#84154=CARTESIAN_POINT('Ctrl Pts',(-44.3700513505921,1.43253119343992,126.09735886111));
#84155=CARTESIAN_POINT('Ctrl Pts',(-44.3777976838574,1.30060060139527,126.059211611218));
#84156=CARTESIAN_POINT('Ctrl Pts',(-44.3855440171227,1.16734200757159,126.026652411757));
#84157=CARTESIAN_POINT('Ctrl Pts',(-44.3932920851257,1.03405357140977,125.994085920888));
#84158=CARTESIAN_POINT('Ctrl Pts',(-44.4010401531287,0.899436921404208,
125.967110063381));
#84159=CARTESIAN_POINT('Ctrl Pts',(-44.4087882211317,0.764000348687499,
125.945812837652));
#84160=CARTESIAN_POINT('Ctrl Pts',(-44.4165445238736,0.628419832369775,
125.924492976979));
#84161=CARTESIAN_POINT('Ctrl Pts',(-44.4243008266155,0.492018039413514,
125.908863865111));
#84162=CARTESIAN_POINT('Ctrl Pts',(-44.4320571293573,0.355309991453566,
125.898961768087));
#84163=CARTESIAN_POINT('Ctrl Pts',(-44.4398175718715,0.218528978291663,
125.889054386015));
#84164=CARTESIAN_POINT('Ctrl Pts',(-44.4475780143858,0.0814417750159961,
125.884880121373));
#84165=CARTESIAN_POINT('Ctrl Pts',(-44.4553384569,-0.0554365358649684,125.886423056658));
#84166=CARTESIAN_POINT('Ctrl Pts',(-44.4631113571654,-0.192534575961671,
125.887968468799));
#84167=CARTESIAN_POINT('Ctrl Pts',(-44.4708842574308,-0.329422662924207,
125.895249400172));
#84168=CARTESIAN_POINT('Ctrl Pts',(-44.4786571576963,-0.465589872111775,
125.908197922813));
#84169=CARTESIAN_POINT('Ctrl Pts',(-44.4861474934582,-0.596807060257929,
125.920675734042));
#84170=CARTESIAN_POINT('Ctrl Pts',(-44.49363782922,-0.727354566922098,125.938416186634));
#84171=CARTESIAN_POINT('Ctrl Pts',(-44.5011281649819,-0.856786014983597,
125.961313974488));
#84172=CARTESIAN_POINT('Ctrl Pts',(-44.5089024991011,-0.991124895741017,
125.985079938928));
#84173=CARTESIAN_POINT('Ctrl Pts',(-44.5166768332201,-1.12468696172905,
126.014477322851));
#84174=CARTESIAN_POINT('Ctrl Pts',(-44.5244511673392,-1.25696307449394,
126.04944454135));
#84175=CARTESIAN_POINT('Ctrl Pts',(-44.5322159202863,-1.38907616877134,
126.084368665877));
#84176=CARTESIAN_POINT('Ctrl Pts',(-44.5399806732334,-1.51990608879708,
126.124848868064));
#84177=CARTESIAN_POINT('Ctrl Pts',(-44.5477454261805,-1.64895151128427,
126.170772161959));
#84178=CARTESIAN_POINT('Ctrl Pts',(-44.5555024670654,-1.77786876403828,
126.216649844191));
#84179=CARTESIAN_POINT('Ctrl Pts',(-44.5632595079504,-1.90500468043288,
126.267959729406));
#84180=CARTESIAN_POINT('Ctrl Pts',(-44.5710165488354,-2.02987113408955,
126.324538495931));
#84181=CARTESIAN_POINT('Ctrl Pts',(-44.5787677400755,-2.1546434249827,126.381074595968));
#84182=CARTESIAN_POINT('Ctrl Pts',(-44.5865189313157,-2.27714930494219,
126.442871507987));
#84183=CARTESIAN_POINT('Ctrl Pts',(-44.5942701225558,-2.39691908125864,
126.509717212067));
#84184=CARTESIAN_POINT('Ctrl Pts',(-44.6020180193329,-2.51663795222535,
126.576534504939));
#84185=CARTESIAN_POINT('Ctrl Pts',(-44.6097659161099,-2.63362269182408,
126.648396131759));
#84186=CARTESIAN_POINT('Ctrl Pts',(-44.617513812887,-2.74742695237193,126.725043492865));
#84187=CARTESIAN_POINT('Ctrl Pts',(-44.6252600889711,-2.86120740752135,
126.801674820995));
#84188=CARTESIAN_POINT('Ctrl Pts',(-44.6330063650553,-2.97180838284285,
126.883089673962));
#84189=CARTESIAN_POINT('Ctrl Pts',(-44.6407526411394,-3.07881168915751,
126.968985584377));
#84190=CARTESIAN_POINT('Ctrl Pts',(-44.6484989744048,-3.1858157853464,127.054882128857));
#84191=CARTESIAN_POINT('Ctrl Pts',(-44.65624530767,-3.28922185465103,127.145259552047));
#84192=CARTESIAN_POINT('Ctrl Pts',(-44.6639916409354,-3.38864435626574,
127.239774738498));
#84193=CARTESIAN_POINT('Ctrl Pts',(-44.6717397089384,-3.4880891228606,127.334311090971));
#84194=CARTESIAN_POINT('Ctrl Pts',(-44.6794877769414,-3.58354826330052,
127.432986781257));
#84195=CARTESIAN_POINT('Ctrl Pts',(-44.6872358449444,-3.67467299825015,
127.535421734927));
#84196=CARTESIAN_POINT('Ctrl Pts',(-44.6949921476863,-3.76589458165249,
127.637965557684));
#84197=CARTESIAN_POINT('Ctrl Pts',(-44.7027484504281,-3.85277229699821,
127.744276332471));
#84198=CARTESIAN_POINT('Ctrl Pts',(-44.7105047531699,-3.93499725086926,
127.853940359679));
#84199=CARTESIAN_POINT('Ctrl Pts',(-44.7182651956841,-4.01726609067383,
127.96366291788));
#84200=CARTESIAN_POINT('Ctrl Pts',(-44.7260256381983,-4.09487699964931,
128.076741972505));
#84201=CARTESIAN_POINT('Ctrl Pts',(-44.7337860807125,-4.16756495496575,
128.192735566254));
#84202=CARTESIAN_POINT('Ctrl Pts',(-44.7415589809779,-4.2403695954411,128.308915363216));
#84203=CARTESIAN_POINT('Ctrl Pts',(-44.7493318812434,-4.30823529635164,
128.428018708903));
#84204=CARTESIAN_POINT('Ctrl Pts',(-44.7571047815088,-4.37094304016679,
128.549579031222));
#84205=CARTESIAN_POINT('Ctrl Pts',(-44.7645951172708,-4.43137119954257,
128.666720329631));
#84206=CARTESIAN_POINT('Ctrl Pts',(-44.7720854530329,-4.48700977049351,
128.786142792248));
#84207=CARTESIAN_POINT('Ctrl Pts',(-44.7795757887949,-4.53770607229015,
128.907413948837));
#84208=CARTESIAN_POINT('Ctrl Pts',(-44.788247599836,-4.5963988683989,129.047813603552));
#84209=CARTESIAN_POINT('Ctrl Pts',(-44.7969194108771,-4.64862565067612,
129.191068172679));
#84210=CARTESIAN_POINT('Ctrl Pts',(-44.8055912219183,-4.69413025906848,
129.33659899748));
#84211=CARTESIAN_POINT('Ctrl Pts',(-44.8104350071769,-4.71954762001937,
129.417887676454));
#84212=CARTESIAN_POINT('Ctrl Pts',(-44.8152787924355,-4.74286849138426,
129.499886083174));
#84213=CARTESIAN_POINT('Ctrl Pts',(-44.8201225776941,-4.76405452823406,
129.582490119308));
#84214=CARTESIAN_POINT('Origin',(213.235140564004,0.,130.804360617566));
#84215=CARTESIAN_POINT('',(-46.915040585789,-4.76405452823398,129.582490119308));
#84216=CARTESIAN_POINT('',(-46.5699483010518,-4.76405452823402,129.582490119308));
#84217=CARTESIAN_POINT('',(213.235140564004,-4.76405452823405,129.582490119308));
#84218=CARTESIAN_POINT('',(-45.2351405640464,-4.91824810652024,130.808676311034));
#84219=CARTESIAN_POINT('Ctrl Pts',(-45.2351405640464,-4.91824810652024,
130.808676311034));
#84220=CARTESIAN_POINT('Ctrl Pts',(-45.2445444544636,-4.91810213064542,
130.9750332535));
#84221=CARTESIAN_POINT('Ctrl Pts',(-45.2539483448808,-4.90951205841258,
131.141018612161));
#84222=CARTESIAN_POINT('Ctrl Pts',(-45.263352235298,-4.8926131430149,131.305878010383));
#84223=CARTESIAN_POINT('Ctrl Pts',(-45.272888149729,-4.87547697871907,131.473051918717));
#84224=CARTESIAN_POINT('Ctrl Pts',(-45.28242406416,-4.84979708838166,131.639068048438));
#84225=CARTESIAN_POINT('Ctrl Pts',(-45.291959978591,-4.8157635036038,131.803162369596));
#84226=CARTESIAN_POINT('Ctrl Pts',(-45.300267332481,-4.78611463930858,131.946115581588));
#84227=CARTESIAN_POINT('Ctrl Pts',(-45.3085746863711,-4.75012670806714,
132.087610656431));
#84228=CARTESIAN_POINT('Ctrl Pts',(-45.3168820402611,-4.70795463187301,
132.227155840613));
#84229=CARTESIAN_POINT('Ctrl Pts',(-45.3246563743801,-4.66848841733956,
132.35774747074));
#84230=CARTESIAN_POINT('Ctrl Pts',(-45.3324307084993,-4.62352194811584,
132.486902603422));
#84231=CARTESIAN_POINT('Ctrl Pts',(-45.3402050426184,-4.57317651175509,
132.614122937549));
#84232=CARTESIAN_POINT('Ctrl Pts',(-45.3479697955655,-4.52289312164516,
132.741186483985));
#84233=CARTESIAN_POINT('Ctrl Pts',(-45.3557345485126,-4.46724409680583,
132.866319616198));
#84234=CARTESIAN_POINT('Ctrl Pts',(-45.3634993014597,-4.40640084302413,
132.98903786446));
#84235=CARTESIAN_POINT('Ctrl Pts',(-45.3712563423447,-4.34561801962,133.111634227227));
#84236=CARTESIAN_POINT('Ctrl Pts',(-45.3790133832296,-4.27965140642154,
133.231820131149));
#84237=CARTESIAN_POINT('Ctrl Pts',(-45.3867704241146,-4.20872083395094,
133.349130156123));
#84238=CARTESIAN_POINT('Ctrl Pts',(-45.3945216153548,-4.1378437507766,133.466351716695));
#84239=CARTESIAN_POINT('Ctrl Pts',(-45.402272806595,-4.06201036073395,133.580701381821));
#84240=CARTESIAN_POINT('Ctrl Pts',(-45.4100239978351,-3.98148667456019,
133.691737787733));
#84241=CARTESIAN_POINT('Ctrl Pts',(-45.4177718946122,-3.90099721310121,
133.80272700021));
#84242=CARTESIAN_POINT('Ctrl Pts',(-45.4255197913893,-3.81582164947759,
133.910405438486));
#84243=CARTESIAN_POINT('Ctrl Pts',(-45.4332676881664,-3.72626949088769,
134.014360421893));
#84244=CARTESIAN_POINT('Ctrl Pts',(-45.4410139642505,-3.63673606467872,
134.118293660159));
#84245=CARTESIAN_POINT('Ctrl Pts',(-45.4487602403346,-3.54282811947194,
134.218504696741));
#84246=CARTESIAN_POINT('Ctrl Pts',(-45.4565065164187,-3.44489539738257,
134.314613993548));
#84247=CARTESIAN_POINT('Ctrl Pts',(-45.4642528496841,-3.34696195237609,
134.410723999812));
#84248=CARTESIAN_POINT('Ctrl Pts',(-45.4719991829495,-3.24500395024257,
134.502731932038));
#84249=CARTESIAN_POINT('Ctrl Pts',(-45.4797455162149,-3.13940764059065,
134.590295472883));
#84250=CARTESIAN_POINT('Ctrl Pts',(-45.4874935842179,-3.03378768337762,
134.677878622975));
#84251=CARTESIAN_POINT('Ctrl Pts',(-45.4952416522208,-2.92452809823754,
134.761015151661));
#84252=CARTESIAN_POINT('Ctrl Pts',(-45.5029897202237,-2.81204749322128,
134.839403610939));
#84253=CARTESIAN_POINT('Ctrl Pts',(-45.5107460229656,-2.69944734247932,
134.917875382405));
#84254=CARTESIAN_POINT('Ctrl Pts',(-45.5185023257074,-2.58361965464235,
134.991588780032));
#84255=CARTESIAN_POINT('Ctrl Pts',(-45.5262586284493,-2.46501171671025,
135.06028593399));
#84256=CARTESIAN_POINT('Ctrl Pts',(-45.5340190709635,-2.3463404741503,135.129019753688));
#84257=CARTESIAN_POINT('Ctrl Pts',(-45.5417795134777,-2.22488637074305,
135.192731813399));
#84258=CARTESIAN_POINT('Ctrl Pts',(-45.5495399559919,-2.10111957189729,
135.251211144297));
#84259=CARTESIAN_POINT('Ctrl Pts',(-45.5573128562573,-1.97715409159852,
135.309784351409));
#84260=CARTESIAN_POINT('Ctrl Pts',(-45.5650857565228,-1.8508688573959,135.363107891579));
#84261=CARTESIAN_POINT('Ctrl Pts',(-45.5728586567882,-1.72275304357371,
135.411019386496));
#84262=CARTESIAN_POINT('Ctrl Pts',(-45.5803489925501,-1.5992945622903,135.45718917789));
#84263=CARTESIAN_POINT('Ctrl Pts',(-45.587839328312,-1.47413657568182,135.498333479351));
#84264=CARTESIAN_POINT('Ctrl Pts',(-45.5953296640739,-1.34772655990897,
135.534351757327));
#84265=CARTESIAN_POINT('Ctrl Pts',(-45.603103998193,-1.21652366996474,135.57173567926));
#84266=CARTESIAN_POINT('Ctrl Pts',(-45.6108783323121,-1.08355632399403,
135.60371561919));
#84267=CARTESIAN_POINT('Ctrl Pts',(-45.6186526664312,-0.949309315717473,
135.630124275848));
#84268=CARTESIAN_POINT('Ctrl Pts',(-45.6264174193783,-0.815227754880802,
135.656500386196));
#84269=CARTESIAN_POINT('Ctrl Pts',(-45.6341821723253,-0.679870049566951,
135.677318800045));
#84270=CARTESIAN_POINT('Ctrl Pts',(-45.6419469252724,-0.54373644689543,
135.692461858213));
#84271=CARTESIAN_POINT('Ctrl Pts',(-45.6497039661574,-0.407738054037044,
135.707589876083));
#84272=CARTESIAN_POINT('Ctrl Pts',(-45.6574610070424,-0.270965683468014,
135.717053712901));
#84273=CARTESIAN_POINT('Ctrl Pts',(-45.6652180479274,-0.133929730068915,
135.720786747379));
#84274=CARTESIAN_POINT('Ctrl Pts',(-45.6729692391675,0.00300288345174166,
135.724516966746));
#84275=CARTESIAN_POINT('Ctrl Pts',(-45.6807204304076,0.140198294924244,
135.722524975136));
#84276=CARTESIAN_POINT('Ctrl Pts',(-45.6884716216477,0.277141387209298,
135.714796007019));
#84277=CARTESIAN_POINT('Ctrl Pts',(-45.6962195184248,0.414026275027054,
135.70707032392));
#84278=CARTESIAN_POINT('Ctrl Pts',(-45.703967415202,0.550658667427509,135.693612536027));
#84279=CARTESIAN_POINT('Ctrl Pts',(-45.711715311979,0.686524068277104,135.674459976529));
#84280=CARTESIAN_POINT('Ctrl Pts',(-45.7194615880631,0.822361049013761,
135.655311423335));
#84281=CARTESIAN_POINT('Ctrl Pts',(-45.7272078641471,0.957430970427422,
135.630470522485));
#84282=CARTESIAN_POINT('Ctrl Pts',(-45.7349541402312,1.09122547221634,135.600026372316));
#84283=CARTESIAN_POINT('Ctrl Pts',(-45.7427004734966,1.22502096164588,135.569581997416));
#84284=CARTESIAN_POINT('Ctrl Pts',(-45.7504468067619,1.35754063144337,135.533534377408));
#84285=CARTESIAN_POINT('Ctrl Pts',(-45.7581931400272,1.48828770298435,135.49202344414));
#84286=CARTESIAN_POINT('Ctrl Pts',(-45.7659412080302,1.61906405442546,135.450503214787));
#84287=CARTESIAN_POINT('Ctrl Pts',(-45.7736892760332,1.74806664513958,135.403517355894));
#84288=CARTESIAN_POINT('Ctrl Pts',(-45.7814373440362,1.87481559050982,135.351255114262));
#84289=CARTESIAN_POINT('Ctrl Pts',(-45.789193646778,2.00169924616753,135.298937327698));
#84290=CARTESIAN_POINT('Ctrl Pts',(-45.7969499495199,2.12632410978771,135.241332105477));
#84291=CARTESIAN_POINT('Ctrl Pts',(-45.8047062522618,2.24823145862955,135.17867637788));
#84292=CARTESIAN_POINT('Ctrl Pts',(-45.8124666947759,2.37020387309402,135.115987209034));
#84293=CARTESIAN_POINT('Ctrl Pts',(-45.8202271372901,2.48945554292122,135.048242356606));
#84294=CARTESIAN_POINT('Ctrl Pts',(-45.8279875798042,2.60555483817438,134.975723350267));
#84295=CARTESIAN_POINT('Ctrl Pts',(-45.8357604800696,2.72184050632309,134.903087929981));
#84296=CARTESIAN_POINT('Ctrl Pts',(-45.843533380335,2.83496336464404,134.825663261825));
#84297=CARTESIAN_POINT('Ctrl Pts',(-45.8513062806004,2.94452238901528,134.743773132534));
#84298=CARTESIAN_POINT('Ctrl Pts',(-45.8587966163625,3.05009866688914,134.664859915711));
#84299=CARTESIAN_POINT('Ctrl Pts',(-45.8662869521247,3.15236548189355,134.581800456862));
#84300=CARTESIAN_POINT('Ctrl Pts',(-45.8737772878868,3.25099638050922,134.494916889514));
#84301=CARTESIAN_POINT('Ctrl Pts',(-45.8815516220059,3.35336689962325,134.404739105303));
#84302=CARTESIAN_POINT('Ctrl Pts',(-45.8893259561249,3.45214462721011,134.310155849992));
#84303=CARTESIAN_POINT('Ctrl Pts',(-45.897100290244,3.54692676512755,134.211484563847));
#84304=CARTESIAN_POINT('Ctrl Pts',(-45.9048650431911,3.64159209253094,134.112934881244));
#84305=CARTESIAN_POINT('Ctrl Pts',(-45.9126297961382,3.7322713597279,134.010307471436));
#84306=CARTESIAN_POINT('Ctrl Pts',(-45.9203945490853,3.81859518093083,133.903959608834));
#84307=CARTESIAN_POINT('Ctrl Pts',(-45.9281515899703,3.90483326409748,133.797717372429));
#84308=CARTESIAN_POINT('Ctrl Pts',(-45.9359086308553,3.98672426518592,133.687762338442));
#84309=CARTESIAN_POINT('Ctrl Pts',(-45.9436656717403,4.06393625291824,133.574487906107));
#84310=CARTESIAN_POINT('Ctrl Pts',(-45.9514168629804,4.1410900144901,133.461298894902));
#84311=CARTESIAN_POINT('Ctrl Pts',(-45.9591680542206,4.21357156661799,133.344795789532));
#84312=CARTESIAN_POINT('Ctrl Pts',(-45.9669192454607,4.28109005324667,133.225403991505));
#84313=CARTESIAN_POINT('Ctrl Pts',(-45.9746671422378,4.34857984271733,133.106062938177));
#84314=CARTESIAN_POINT('Ctrl Pts',(-45.9824150390148,4.41111057014216,132.983835973739));
#84315=CARTESIAN_POINT('Ctrl Pts',(-45.9901629357919,4.46843554726462,132.85917613786));
#84316=CARTESIAN_POINT('Ctrl Pts',(-45.997909211876,4.52574853323773,132.734542378132));
#84317=CARTESIAN_POINT('Ctrl Pts',(-46.0056554879601,4.57785777161193,132.607477114185));
#84318=CARTESIAN_POINT('Ctrl Pts',(-46.0134017640442,4.62456344218149,132.478456203767));
#84319=CARTESIAN_POINT('Ctrl Pts',(-46.0211480973096,4.67126945752163,132.349434340946));
#84320=CARTESIAN_POINT('Ctrl Pts',(-46.0288944305749,4.71257169238525,132.218457170467));
#84321=CARTESIAN_POINT('Ctrl Pts',(-46.0366407638403,4.74831935441895,132.086018282838));
#84322=CARTESIAN_POINT('Ctrl Pts',(-46.0443888318432,4.78407502189371,131.953549736438));
#84323=CARTESIAN_POINT('Ctrl Pts',(-46.0521368998463,4.8142735394425,131.819619198902));
#84324=CARTESIAN_POINT('Ctrl Pts',(-46.0598849678492,4.83881473640168,131.684732703267));
#84325=CARTESIAN_POINT('Ctrl Pts',(-46.0676412705911,4.86338201603706,131.549702848659));
#84326=CARTESIAN_POINT('Ctrl Pts',(-46.075397573333,4.88227989403673,131.41371539164));
#84327=CARTESIAN_POINT('Ctrl Pts',(-46.0831538760748,4.89545975570788,131.277284335246));
#84328=CARTESIAN_POINT('Ctrl Pts',(-46.090914318589,4.90864665186805,131.14078046149));
#84329=CARTESIAN_POINT('Ctrl Pts',(-46.0986747611032,4.91610942931226,131.003832906784));
#84330=CARTESIAN_POINT('Ctrl Pts',(-46.1064352036173,4.91785164040135,130.866956987283));
#84331=CARTESIAN_POINT('Ctrl Pts',(-46.1142081038828,4.91959664824235,130.729861342404));
#84332=CARTESIAN_POINT('Ctrl Pts',(-46.1219810041482,4.91560275024385,130.592837953552));
#84333=CARTESIAN_POINT('Ctrl Pts',(-46.1297539044137,4.90592559402316,130.456399228316));
#84334=CARTESIAN_POINT('Ctrl Pts',(-46.1372442401757,4.89660022680639,130.324920394412));
#84335=CARTESIAN_POINT('Ctrl Pts',(-46.1447345759377,4.88199766322645,130.193984760255));
#84336=CARTESIAN_POINT('Ctrl Pts',(-46.1522249116997,4.86221246724157,130.064041101478));
#84337=CARTESIAN_POINT('Ctrl Pts',(-46.1599992458188,4.84167710953731,129.929170589383));
#84338=CARTESIAN_POINT('Ctrl Pts',(-46.1677735799379,4.81549331264808,129.794941529813));
#84339=CARTESIAN_POINT('Ctrl Pts',(-46.175547914057,4.78371042582497,129.661864392472));
#84340=CARTESIAN_POINT('Ctrl Pts',(-46.1833126670041,4.75196670856935,129.528951260809));
#84341=CARTESIAN_POINT('Ctrl Pts',(-46.1910774199511,4.71463772102353,129.397187603332));
#84342=CARTESIAN_POINT('Ctrl Pts',(-46.1988421728982,4.67182438622515,129.267077310309));
#84343=CARTESIAN_POINT('Ctrl Pts',(-46.2065992137832,4.62905357423451,129.137096244663));
#84344=CARTESIAN_POINT('Ctrl Pts',(-46.2143562546683,4.58080937643992,129.008765644503));
#84345=CARTESIAN_POINT('Ctrl Pts',(-46.2221132955533,4.5272433537948,128.882577414907));
#84346=CARTESIAN_POINT('Ctrl Pts',(-46.2298644867934,4.47371772570404,128.756484344838));
#84347=CARTESIAN_POINT('Ctrl Pts',(-46.2376156780334,4.41487841300241,128.632530788049));
#84348=CARTESIAN_POINT('Ctrl Pts',(-46.2453668692735,4.35092610322437,128.511191389885));
#84349=CARTESIAN_POINT('Ctrl Pts',(-46.2531147660506,4.28700097488397,128.389903564203));
#84350=CARTESIAN_POINT('Ctrl Pts',(-46.2608626628277,4.2179673536257,128.271228032419));
#84351=CARTESIAN_POINT('Ctrl Pts',(-46.2686105596048,4.14407305352638,128.155617219361));
#84352=CARTESIAN_POINT('Ctrl Pts',(-46.2763568356888,4.07019421052167,128.040030589592));
#84353=CARTESIAN_POINT('Ctrl Pts',(-46.2841031117729,3.99145692146836,127.927507732632));
#84354=CARTESIAN_POINT('Ctrl Pts',(-46.291849387857,3.90815353126402,127.818473975617));
#84355=CARTESIAN_POINT('Ctrl Pts',(-46.2995957211224,3.82484952613298,127.709439413739));
#84356=CARTESIAN_POINT('Ctrl Pts',(-46.3073420543878,3.73697958994952,127.603894313869));
#84357=CARTESIAN_POINT('Ctrl Pts',(-46.3150883876531,3.64487748743746,127.502232339611));
#84358=CARTESIAN_POINT('Ctrl Pts',(-46.3228364556561,3.55275475929814,127.400547598858));
#84359=CARTESIAN_POINT('Ctrl Pts',(-46.3305845236591,3.45639824133398,127.302748003804));
#84360=CARTESIAN_POINT('Ctrl Pts',(-46.3383325916621,3.35617952878086,127.209191354083));
#84361=CARTESIAN_POINT('Ctrl Pts',(-46.3460888944039,3.25585430258727,127.115535271241));
#84362=CARTESIAN_POINT('Ctrl Pts',(-46.3538451971457,3.15165896829736,127.026131409067));
#84363=CARTESIAN_POINT('Ctrl Pts',(-46.3616014998876,3.04399969379405,126.941298499675));
#84364=CARTESIAN_POINT('Ctrl Pts',(-46.3693619424018,2.93628295829437,126.856420312405));
#84365=CARTESIAN_POINT('Ctrl Pts',(-46.3771223849159,2.82509891546129,126.776118167936));
#84366=CARTESIAN_POINT('Ctrl Pts',(-46.3848828274301,2.71088303550717,126.700667618535));
#84367=CARTESIAN_POINT('Ctrl Pts',(-46.3926557276955,2.59648380608293,126.625095949213));
#84368=CARTESIAN_POINT('Ctrl Pts',(-46.4004286279609,2.47904334891283,126.554391640055));
#84369=CARTESIAN_POINT('Ctrl Pts',(-46.4082015282264,2.35902284591166,126.488784841964));
#84370=CARTESIAN_POINT('Ctrl Pts',(-46.4156918639884,2.24336539050798,126.425563016236));
#84371=CARTESIAN_POINT('Ctrl Pts',(-46.4231821997504,2.12531249089972,126.367074658));
#84372=CARTESIAN_POINT('Ctrl Pts',(-46.4306725355125,2.00529282886471,126.313482782108));
#84373=CARTESIAN_POINT('Ctrl Pts',(-46.4384468696315,1.88072258486446,126.257858953954));
#84374=CARTESIAN_POINT('Ctrl Pts',(-46.4462212037507,1.75363889369082,126.207334038416));
#84375=CARTESIAN_POINT('Ctrl Pts',(-46.4539955378698,1.62449790243732,126.162142437916));
#84376=CARTESIAN_POINT('Ctrl Pts',(-46.4617602908169,1.49551606591388,126.117006532024));
#84377=CARTESIAN_POINT('Ctrl Pts',(-46.469525043764,1.36448233955753,126.077190991085));
#84378=CARTESIAN_POINT('Ctrl Pts',(-46.4772897967111,1.23187521188992,126.042883270688));
#84379=CARTESIAN_POINT('Ctrl Pts',(-46.4850468375961,1.09939979149095,126.008609625203));
#84380=CARTESIAN_POINT('Ctrl Pts',(-46.492803878481,0.965354455726345,125.979833011118));
#84381=CARTESIAN_POINT('Ctrl Pts',(-46.5005609193661,0.830234980668827,
125.956691802623));
#84382=CARTESIAN_POINT('Ctrl Pts',(-46.5083121106062,0.695217400258342,
125.933568045093));
#84383=CARTESIAN_POINT('Ctrl Pts',(-46.5160633018463,0.559127676639525,
125.916071300107));
#84384=CARTESIAN_POINT('Ctrl Pts',(-46.5238144930865,0.422473618896509,
125.904289280959));
#84385=CARTESIAN_POINT('Ctrl Pts',(-46.5315623898636,0.285877642773586,
125.892512269484));
#84386=CARTESIAN_POINT('Ctrl Pts',(-46.5393102866406,0.148718198288503,
125.886445186443));
#84387=CARTESIAN_POINT('Ctrl Pts',(-46.5470581834177,0.0115098728212643,
125.886124085502));
#84388=CARTESIAN_POINT('Ctrl Pts',(-46.5548044595018,-0.125669751622156,
125.885803051729));
#84389=CARTESIAN_POINT('Ctrl Pts',(-46.5625507355859,-0.262897845993511,
125.891225610255));
#84390=CARTESIAN_POINT('Ctrl Pts',(-46.57029701167,-0.399658550970937,125.902375702745));
#84391=CARTESIAN_POINT('Ctrl Pts',(-46.5780433449354,-0.536420265484821,
125.913525877541));
#84392=CARTESIAN_POINT('Ctrl Pts',(-46.5857896782008,-0.672714194047978,
125.930403638896));
#84393=CARTESIAN_POINT('Ctrl Pts',(-46.5935360114661,-0.808028728335253,
125.952940965888));
#84394=CARTESIAN_POINT('Ctrl Pts',(-46.6012840794691,-0.943373565374276,
125.975483339958));
#84395=CARTESIAN_POINT('Ctrl Pts',(-46.6090321474721,-1.07773818612011,
126.003687737466));
#84396=CARTESIAN_POINT('Ctrl Pts',(-46.6167802154751,-1.2106207073057,126.037434924256));
#84397=CARTESIAN_POINT('Ctrl Pts',(-46.6245365182169,-1.34364445761613,
126.071217977957));
#84398=CARTESIAN_POINT('Ctrl Pts',(-46.6322928209588,-1.47518258220828,
126.110555492345));
#84399=CARTESIAN_POINT('Ctrl Pts',(-46.6400491237006,-1.60474737906548,
126.155278029368));
#84400=CARTESIAN_POINT('Ctrl Pts',(-46.6478095662148,-1.73438132855607,
126.200024436156));
#84401=CARTESIAN_POINT('Ctrl Pts',(-46.655570008729,-1.86203948794549,126.250161449713));
#84402=CARTESIAN_POINT('Ctrl Pts',(-46.6633304512431,-1.98725464502111,
126.305471639347));
#84403=CARTESIAN_POINT('Ctrl Pts',(-46.6711033515086,-2.11267080858278,
126.360870617807));
#84404=CARTESIAN_POINT('Ctrl Pts',(-46.6788762517741,-2.23563578207047,
126.421459194362));
#84405=CARTESIAN_POINT('Ctrl Pts',(-46.6866491520395,-2.35570665292161,
126.486973765791));
#84406=CARTESIAN_POINT('Ctrl Pts',(-46.6941394878016,-2.47141264517719,
126.550106717527));
#84407=CARTESIAN_POINT('Ctrl Pts',(-46.7016298235635,-2.5844310332787,126.617813579115));
#84408=CARTESIAN_POINT('Ctrl Pts',(-46.7091201593256,-2.69439295524025,
126.689821801945));
#84409=CARTESIAN_POINT('Ctrl Pts',(-46.7168839525298,-2.80836937092695,
126.764458903514));
#84410=CARTESIAN_POINT('Ctrl Pts',(-46.724647745734,-2.91942549512991,126.843955537909));
#84411=CARTESIAN_POINT('Ctrl Pts',(-46.7324115389382,-3.02711811027867,
126.928055803839));
#84412=CARTESIAN_POINT('Ctrl Pts',(-46.7401630440496,-3.13464027564649,
127.012022960624));
#84413=CARTESIAN_POINT('Ctrl Pts',(-46.7479145491609,-3.23880922797593,
127.100578998185));
#84414=CARTESIAN_POINT('Ctrl Pts',(-46.7556660542723,-3.33920955541522,
127.193424089804));
#84415=CARTESIAN_POINT('Ctrl Pts',(-46.7634104675609,-3.43951802697391,
127.2861842378));
#84416=CARTESIAN_POINT('Ctrl Pts',(-46.7711548808495,-3.53606444594628,
127.383225370047));
#84417=CARTESIAN_POINT('Ctrl Pts',(-46.7788992941381,-3.6284651924949,127.484206493229));
#84418=CARTESIAN_POINT('Ctrl Pts',(-46.7866383135098,-3.72080158272198,
127.585117283931));
#84419=CARTESIAN_POINT('Ctrl Pts',(-46.7943773328816,-3.80899778156704,
127.689962317673));
#84420=CARTESIAN_POINT('Ctrl Pts',(-46.8021163522533,-3.89270618738852,
127.798363012582));
#84421=CARTESIAN_POINT('Ctrl Pts',(-46.8098516715358,-3.97637457152954,
127.906711880224));
#84422=CARTESIAN_POINT('Ctrl Pts',(-46.8175869908184,-4.05555919375947,
128.018612715882));
#84423=CARTESIAN_POINT('Ctrl Pts',(-46.825322310101,-4.12995228204412,128.133653368439));
#84424=CARTESIAN_POINT('Ctrl Pts',(-46.8330572732535,-4.20434194530896,
128.248688724584));
#84425=CARTESIAN_POINT('Ctrl Pts',(-46.8407922364058,-4.27394029121761,
128.366863286923));
#84426=CARTESIAN_POINT('Ctrl Pts',(-46.8485271995583,-4.33848256268185,
128.487735461049));
#84427=CARTESIAN_POINT('Ctrl Pts',(-46.8562616664843,-4.40302069352118,
128.60859988078));
#84428=CARTESIAN_POINT('Ctrl Pts',(-46.8639961334103,-4.46250321509175,
128.732161219404));
#84429=CARTESIAN_POINT('Ctrl Pts',(-46.8717306003363,-4.51671145296347,
128.85795348822));
#84430=CARTESIAN_POINT('Ctrl Pts',(-46.8794695499381,-4.57095110837883,
128.983818662636));
#84431=CARTESIAN_POINT('Ctrl Pts',(-46.8872084995397,-4.61991021949255,
129.111916988931));
#84432=CARTESIAN_POINT('Ctrl Pts',(-46.8949474491414,-4.66341829462873,
129.241762501664));
#84433=CARTESIAN_POINT('Ctrl Pts',(-46.9016451613573,-4.70107257348113,
129.354137942978));
#84434=CARTESIAN_POINT('Ctrl Pts',(-46.9083428735732,-4.73464468864475,
129.467821601106));
#84435=CARTESIAN_POINT('Ctrl Pts',(-46.9150405857891,-4.76405452823398,
129.582490119308));
#84436=CARTESIAN_POINT('Ctrl Pts',(-45.1651923290374,-4.76405452823407,
129.582490119308));
#84437=CARTESIAN_POINT('Ctrl Pts',(-45.1728855518329,-4.79792966098168,
129.714568747764));
#84438=CARTESIAN_POINT('Ctrl Pts',(-45.1805787746285,-4.82631197159566,
129.84807280976));
#84439=CARTESIAN_POINT('Ctrl Pts',(-45.188271997424,-4.84909609083771,129.982502865688));
#84440=CARTESIAN_POINT('Ctrl Pts',(-45.1960834251881,-4.87223028392675,
130.118998414968));
#84441=CARTESIAN_POINT('Ctrl Pts',(-45.2038948529522,-4.88959273668898,
130.256448238861));
#84442=CARTESIAN_POINT('Ctrl Pts',(-45.2117062807163,-4.90112750835848,
130.394321339799));
#84443=CARTESIAN_POINT('Ctrl Pts',(-45.2195177084804,-4.91266228002797,
130.532194440737));
#84444=CARTESIAN_POINT('Ctrl Pts',(-45.2273291362445,-4.91836936270034,
130.6704903914));
#84445=CARTESIAN_POINT('Ctrl Pts',(-45.2351405640086,-4.91824810652082,
130.808676310364));
#84446=CARTESIAN_POINT('',(-44.8898594359405,-4.91824927968631,130.801698782662));
#84447=CARTESIAN_POINT('Ctrl Pts',(-44.8201225776941,-4.76405452823406,
129.582490119308));
#84448=CARTESIAN_POINT('Ctrl Pts',(-44.8287491969274,-4.80178614993221,
129.729605139652));
#84449=CARTESIAN_POINT('Ctrl Pts',(-44.8373758161607,-4.83274365385713,
129.878642232481));
#84450=CARTESIAN_POINT('Ctrl Pts',(-44.846002435394,-4.85674727733277,130.028996866401));
#84451=CARTESIAN_POINT('Ctrl Pts',(-44.8545868334649,-4.88063342015264,
130.178615621382));
#84452=CARTESIAN_POINT('Ctrl Pts',(-44.8631712315358,-4.89763348754675,
130.329538834179));
#84453=CARTESIAN_POINT('Ctrl Pts',(-44.8717556296067,-4.90761853185545,
130.481152622168));
#84454=CARTESIAN_POINT('Ctrl Pts',(-44.8777902317179,-4.91463775078828,
130.587733057691));
#84455=CARTESIAN_POINT('Ctrl Pts',(-44.8838248338292,-4.91819134554488,
130.694654371707));
#84456=CARTESIAN_POINT('Ctrl Pts',(-44.8898594359405,-4.91824927968631,
130.801698782662));
#84457=CARTESIAN_POINT('Ctrl Pts',(-44.8898594359911,-4.9182492796868,130.80169878356));
#84458=CARTESIAN_POINT('Ctrl Pts',(-44.8977025392354,-4.91832457600144,
130.940823178404));
#84459=CARTESIAN_POINT('Ctrl Pts',(-44.9055456424797,-4.91249232923136,
131.079948183281));
#84460=CARTESIAN_POINT('Ctrl Pts',(-44.913388745724,-4.90077893990125,131.218545171503));
#84461=CARTESIAN_POINT('Ctrl Pts',(-44.9212336807835,-4.88906281482177,
131.357174530085));
#84462=CARTESIAN_POINT('Ctrl Pts',(-44.929078615843,-4.87146284270923,131.495275250381));
#84463=CARTESIAN_POINT('Ctrl Pts',(-44.9369235509025,-4.84805730189472,
131.632324058815));
#84464=CARTESIAN_POINT('Ctrl Pts',(-44.944771850857,-4.82464172184031,131.769431651017));
#84465=CARTESIAN_POINT('Ctrl Pts',(-44.9526201508114,-4.79541567671351,
131.905486060992));
#84466=CARTESIAN_POINT('Ctrl Pts',(-44.9604684507658,-4.76050848440808,
132.03997464807));
#84467=CARTESIAN_POINT('Ctrl Pts',(-44.9685980309193,-4.72435023110115,
132.179283256907));
#84468=CARTESIAN_POINT('Ctrl Pts',(-44.9767276110727,-4.68209613988705,
132.316911285416));
#84469=CARTESIAN_POINT('Ctrl Pts',(-44.9848571912262,-4.63394568844649,
132.452307952595));
#84470=CARTESIAN_POINT('Ctrl Pts',(-44.992721685211,-4.58736530808628,132.583289658228));
#84471=CARTESIAN_POINT('Ctrl Pts',(-45.0005861791959,-4.53526728341086,
132.71218292079));
#84472=CARTESIAN_POINT('Ctrl Pts',(-45.0084506731807,-4.47788036622893,
132.838511666097));
#84473=CARTESIAN_POINT('Ctrl Pts',(-45.0167127964186,-4.41759196332404,
132.971227599791));
#84474=CARTESIAN_POINT('Ctrl Pts',(-45.0249749196563,-4.35146616301392,
133.101112505185));
#84475=CARTESIAN_POINT('Ctrl Pts',(-45.0332370428942,-4.27982097372728,
133.227646711973));
#84476=CARTESIAN_POINT('Ctrl Pts',(-45.041499166132,-4.20817578444064,133.35418091876));
#84477=CARTESIAN_POINT('Ctrl Pts',(-45.0497612893698,-4.1310115217808,133.477364064907));
#84478=CARTESIAN_POINT('Ctrl Pts',(-45.0580234126077,-4.04869592842835,
133.596715240752));
#84479=CARTESIAN_POINT('Ctrl Pts',(-45.0657977467268,-3.971240181581,133.709020019053));
#84480=CARTESIAN_POINT('Ctrl Pts',(-45.0735720808459,-3.88898545890976,
133.818277477611));
#84481=CARTESIAN_POINT('Ctrl Pts',(-45.0813464149649,-3.80219940482909,
133.924050145134));
#84482=CARTESIAN_POINT('Ctrl Pts',(-45.089111167912,-3.71552030680378,134.029692457297));
#84483=CARTESIAN_POINT('Ctrl Pts',(-45.0968759208591,-3.62432123439391,
134.131858224238));
#84484=CARTESIAN_POINT('Ctrl Pts',(-45.1046406738062,-3.52891333363567,
134.230138448393));
#84485=CARTESIAN_POINT('Ctrl Pts',(-45.1123977146912,-3.43360019334961,
134.328321059244));
#84486=CARTESIAN_POINT('Ctrl Pts',(-45.1201547555763,-3.33408681419874,
134.422625528536));
#84487=CARTESIAN_POINT('Ctrl Pts',(-45.1279117964613,-3.23072463789963,
134.5126757844));
#84488=CARTESIAN_POINT('Ctrl Pts',(-45.1356629877014,-3.12744040782129,
134.602658132665));
#84489=CARTESIAN_POINT('Ctrl Pts',(-45.1434141789415,-3.02031345125291,
134.688392397322));
#84490=CARTESIAN_POINT('Ctrl Pts',(-45.1511653701816,-2.90973183953378,
134.769539514476));
#84491=CARTESIAN_POINT('Ctrl Pts',(-45.1589132669587,-2.79919722794979,
134.850652141941));
#84492=CARTESIAN_POINT('Ctrl Pts',(-45.1666611637359,-2.68521119613585,
134.927181268811));
#84493=CARTESIAN_POINT('Ctrl Pts',(-45.174409060513,-2.56819447674748,134.998828425537));
#84494=CARTESIAN_POINT('Ctrl Pts',(-45.1821553365971,-2.45120223473422,
135.070460595222));
#84495=CARTESIAN_POINT('Ctrl Pts',(-45.1899016126811,-2.33118089933533,
135.137212621969));
#84496=CARTESIAN_POINT('Ctrl Pts',(-45.1976478887652,-2.20857939709849,
135.198829881221));
#84497=CARTESIAN_POINT('Ctrl Pts',(-45.2053942220306,-2.08597698984522,
135.260447595318));
#84498=CARTESIAN_POINT('Ctrl Pts',(-45.213140555296,-1.96079472707713,135.316930290719));
#84499=CARTESIAN_POINT('Ctrl Pts',(-45.2208868885614,-1.83350493460382,
135.368069933165));
#84500=CARTESIAN_POINT('Ctrl Pts',(-45.2286349565643,-1.7061866364644,135.419221027978));
#84501=CARTESIAN_POINT('Ctrl Pts',(-45.2363830245672,-1.5767602321731,135.465026543138));
#84502=CARTESIAN_POINT('Ctrl Pts',(-45.2441310925702,-1.44571638184337,
135.505327242184));
#84503=CARTESIAN_POINT('Ctrl Pts',(-45.2518873953121,-1.31453325654971,
135.545670773292));
#84504=CARTESIAN_POINT('Ctrl Pts',(-45.2596436980539,-1.18172962553687,
135.580497686006));
#84505=CARTESIAN_POINT('Ctrl Pts',(-45.2674000007957,-1.04781015234293,
135.609698997654));
#84506=CARTESIAN_POINT('Ctrl Pts',(-45.2751604433099,-0.913819202293729,
135.638915894921));
#84507=CARTESIAN_POINT('Ctrl Pts',(-45.2829208858241,-0.778711608315073,
135.662501141081));
#84508=CARTESIAN_POINT('Ctrl Pts',(-45.2906813283383,-0.642999499256316,
135.680397400288));
#84509=CARTESIAN_POINT('Ctrl Pts',(-45.2984542286037,-0.507069533072328,
135.698322388159));
#84510=CARTESIAN_POINT('Ctrl Pts',(-45.3062271288692,-0.370533502230687,
135.710540104633));
#84511=CARTESIAN_POINT('Ctrl Pts',(-45.3140000291346,-0.233906800281148,
135.717045288017));
#84512=CARTESIAN_POINT('Ctrl Pts',(-45.3214903648966,-0.102246823090481,
135.723313991599));
#84513=CARTESIAN_POINT('Ctrl Pts',(-45.3289807006585,0.0294970394025631,
135.724278279032));
#84514=CARTESIAN_POINT('Ctrl Pts',(-45.3364710364205,0.16086798386666,135.719979048066));
#84515=CARTESIAN_POINT('Ctrl Pts',(-45.3442453705396,0.297219897620416,
135.71551681045));
#84516=CARTESIAN_POINT('Ctrl Pts',(-45.3520197046586,0.433601978624816,
135.705369907805));
#84517=CARTESIAN_POINT('Ctrl Pts',(-45.3597940387777,0.56950150154682,135.689527053035));
#84518=CARTESIAN_POINT('Ctrl Pts',(-45.3675587917248,0.705233540452327,
135.673703723168));
#84519=CARTESIAN_POINT('Ctrl Pts',(-45.3753235446718,0.840483819963181,
135.652198453227));
#84520=CARTESIAN_POINT('Ctrl Pts',(-45.3830882976189,0.974740056812664,
135.625051946011));
#84521=CARTESIAN_POINT('Ctrl Pts',(-45.3908453385039,1.10886294847503,135.597932401089));
#84522=CARTESIAN_POINT('Ctrl Pts',(-45.3986023793889,1.24199338151171,135.565182846011));
#84523=CARTESIAN_POINT('Ctrl Pts',(-45.4063594202739,1.37362499317664,135.526895682615));
#84524=CARTESIAN_POINT('Ctrl Pts',(-45.414110611514,1.50515734041982,135.488637391868));
#84525=CARTESIAN_POINT('Ctrl Pts',(-45.4218618027542,1.63519274214251,135.444849913537));
#84526=CARTESIAN_POINT('Ctrl Pts',(-45.4296129939943,1.76323617225048,135.395676470714));
#84527=CARTESIAN_POINT('Ctrl Pts',(-45.4373608907714,1.89122518048464,135.346523927916));
#84528=CARTESIAN_POINT('Ctrl Pts',(-45.4451087875485,2.01722353679644,135.2919901135));
#84529=CARTESIAN_POINT('Ctrl Pts',(-45.4528566843256,2.14075271402463,135.232267671683));
#84530=CARTESIAN_POINT('Ctrl Pts',(-45.4606029604097,2.2642560516121,135.172557722513));
#84531=CARTESIAN_POINT('Ctrl Pts',(-45.4683492364939,2.38529088569735,135.107661474826));
#84532=CARTESIAN_POINT('Ctrl Pts',(-45.476095512578,2.50340033766479,135.037818992451));
#84533=CARTESIAN_POINT('Ctrl Pts',(-45.4838418458434,2.62151066148953,134.967975994513));
#84534=CARTESIAN_POINT('Ctrl Pts',(-45.4915881791086,2.73669522357693,134.893186888031));
#84535=CARTESIAN_POINT('Ctrl Pts',(-45.499334512374,2.84852369517427,134.813736606486));
#84536=CARTESIAN_POINT('Ctrl Pts',(-45.5070825803769,2.96037720998231,134.734268532602));
#84537=CARTESIAN_POINT('Ctrl Pts',(-45.51483064838,3.06887282010134,134.650137432931));
#84538=CARTESIAN_POINT('Ctrl Pts',(-45.522578716383,3.17361134161095,134.561670042527));
#84539=CARTESIAN_POINT('Ctrl Pts',(-45.5303350191248,3.27846118046748,134.473108627928));
#84540=CARTESIAN_POINT('Ctrl Pts',(-45.5380913218667,3.37954565495509,134.380201968979));
#84541=CARTESIAN_POINT('Ctrl Pts',(-45.5458476246086,3.47650029189455,134.283315745612));
#84542=CARTESIAN_POINT('Ctrl Pts',(-45.5536080671227,3.573506676443,134.18637781115));
#84543=CARTESIAN_POINT('Ctrl Pts',(-45.5613685096368,3.6663785667377,134.085456367541));
#84544=CARTESIAN_POINT('Ctrl Pts',(-45.569128952151,3.75479090635583,133.980951291866));
#84545=CARTESIAN_POINT('Ctrl Pts',(-45.5769018524164,3.84334517331038,133.876278455365));
#84546=CARTESIAN_POINT('Ctrl Pts',(-45.5846747526819,3.92742534395177,133.768010799906));
#84547=CARTESIAN_POINT('Ctrl Pts',(-45.5924476529473,4.006748408665,133.656579096603));
#84548=CARTESIAN_POINT('Ctrl Pts',(-45.5999379887094,4.08318788017349,133.549198216395));
#84549=CARTESIAN_POINT('Ctrl Pts',(-45.6074283244714,4.15520993820216,133.43887959461));
#84550=CARTESIAN_POINT('Ctrl Pts',(-45.6149186602334,4.22260207782701,133.32602965906));
#84551=CARTESIAN_POINT('Ctrl Pts',(-45.6226929943525,4.29254941090894,133.208900983905));
#84552=CARTESIAN_POINT('Ctrl Pts',(-45.6304673284716,4.35773038043868,133.088674227883));
#84553=CARTESIAN_POINT('Ctrl Pts',(-45.6382416625907,4.41785834969763,132.965774660388));
#84554=CARTESIAN_POINT('Ctrl Pts',(-45.6460064155378,4.47791221660827,132.843026555626));
#84555=CARTESIAN_POINT('Ctrl Pts',(-45.6537711684849,4.53292530369345,132.717612541287));
#84556=CARTESIAN_POINT('Ctrl Pts',(-45.661535921432,4.58265495375163,132.589985616651));
#84557=CARTESIAN_POINT('Ctrl Pts',(-45.669292962317,4.63233521162038,132.462485452874));
#84558=CARTESIAN_POINT('Ctrl Pts',(-45.6770500032021,4.67674233436563,132.332777114638));
#84559=CARTESIAN_POINT('Ctrl Pts',(-45.6848070440871,4.71568036083824,132.201336564712));
#84560=CARTESIAN_POINT('Ctrl Pts',(-45.6925582353273,4.75458902384208,132.069995135127));
#84561=CARTESIAN_POINT('Ctrl Pts',(-45.7003094265673,4.78803668911843,131.936924467258));
#84562=CARTESIAN_POINT('Ctrl Pts',(-45.7080606178074,4.81587628061533,131.802618456156));
#84563=CARTESIAN_POINT('Ctrl Pts',(-45.7158085145845,4.8437040395432,131.668369528692));
#84564=CARTESIAN_POINT('Ctrl Pts',(-45.7235564113615,4.8659283862643,131.532886684314));
#84565=CARTESIAN_POINT('Ctrl Pts',(-45.7313043081386,4.8824527421955,131.396676650379));
#84566=CARTESIAN_POINT('Ctrl Pts',(-45.7390505842227,4.89897364158768,131.260495108648));
#84567=CARTESIAN_POINT('Ctrl Pts',(-45.7467968603069,4.90979687471523,131.123587067794));
#84568=CARTESIAN_POINT('Ctrl Pts',(-45.754543136391,4.91487746002262,130.986466673098));
#84569=CARTESIAN_POINT('Ctrl Pts',(-45.7622894696563,4.91995808283373,130.849345266212));
#84570=CARTESIAN_POINT('Ctrl Pts',(-45.7700358029217,4.91929595876057,130.712011893053));
#84571=CARTESIAN_POINT('Ctrl Pts',(-45.7777821361871,4.91289820720832,130.574982614895));
#84572=CARTESIAN_POINT('Ctrl Pts',(-45.7855302041901,4.90649902292397,130.437922649981));
#84573=CARTESIAN_POINT('Ctrl Pts',(-45.793278272193,4.89436167347615,130.301167306044));
#84574=CARTESIAN_POINT('Ctrl Pts',(-45.801026340196,4.87654528165912,130.165229036099));
#84575=CARTESIAN_POINT('Ctrl Pts',(-45.8087826429378,4.85870995436887,130.029146289344));
#84576=CARTESIAN_POINT('Ctrl Pts',(-45.8165389456797,4.83518357852838,129.893882739564));
#84577=CARTESIAN_POINT('Ctrl Pts',(-45.8242952484215,4.80607680436346,129.759942687301));
#84578=CARTESIAN_POINT('Ctrl Pts',(-45.8320556909357,4.77695449503674,129.625931147199));
#84579=CARTESIAN_POINT('Ctrl Pts',(-45.8398161334499,4.742245951511,129.493244890212));
#84580=CARTESIAN_POINT('Ctrl Pts',(-45.847576575964,4.70211190076259,129.362373538842));
#84581=CARTESIAN_POINT('Ctrl Pts',(-45.8553494762295,4.661913423273,129.231292101161));
#84582=CARTESIAN_POINT('Ctrl Pts',(-45.863122376495,4.61627216443944,129.102031759966));
#84583=CARTESIAN_POINT('Ctrl Pts',(-45.8708952767604,4.5653975705921,128.975063461571));
#84584=CARTESIAN_POINT('Ctrl Pts',(-45.8783856125224,4.51637239637668,128.852710780637));
#84585=CARTESIAN_POINT('Ctrl Pts',(-45.8858759482844,4.46248789708463,128.732486673691));
#84586=CARTESIAN_POINT('Ctrl Pts',(-45.8933662840464,4.40397114784299,128.614789611303));
#84587=CARTESIAN_POINT('Ctrl Pts',(-45.9011406181655,4.34323571826789,128.492630029022));
#84588=CARTESIAN_POINT('Ctrl Pts',(-45.9089149522845,4.27731744959246,128.372805935004));
#84589=CARTESIAN_POINT('Ctrl Pts',(-45.9166892864036,4.20641919885393,128.255788353334));
#84590=CARTESIAN_POINT('Ctrl Pts',(-45.9244540393507,4.13560832387318,128.138914985375));
#84591=CARTESIAN_POINT('Ctrl Pts',(-45.9322187922978,4.05982987904001,128.024841579002));
#84592=CARTESIAN_POINT('Ctrl Pts',(-45.9399835452449,3.97933382333182,127.914017145764));
#84593=CARTESIAN_POINT('Ctrl Pts',(-45.9477405861299,3.89891771744073,127.803302784916));
#84594=CARTESIAN_POINT('Ctrl Pts',(-45.9554976270149,3.81379355349988,127.695831289756));
#84595=CARTESIAN_POINT('Ctrl Pts',(-45.9632546678999,3.72425585067987,127.592024797454));
#84596=CARTESIAN_POINT('Ctrl Pts',(-45.97100585914,3.63478566893794,127.488296586434));
#84597=CARTESIAN_POINT('Ctrl Pts',(-45.9787570503801,3.54090882738847,127.388228171935));
#84598=CARTESIAN_POINT('Ctrl Pts',(-45.9865082416203,3.44296135572847,127.292210255543));
#84599=CARTESIAN_POINT('Ctrl Pts',(-45.9942561383973,3.34505551435703,127.196233149327));
#84600=CARTESIAN_POINT('Ctrl Pts',(-46.0020040351744,3.24308276257053,127.104303390265));
#84601=CARTESIAN_POINT('Ctrl Pts',(-46.0097519319515,3.13741722136372,127.01677613117));
#84602=CARTESIAN_POINT('Ctrl Pts',(-46.0174982080355,3.03177378311039,126.92926718089));
#84603=CARTESIAN_POINT('Ctrl Pts',(-46.0252444841197,2.92243939278076,126.846159148084));
#84604=CARTESIAN_POINT('Ctrl Pts',(-46.0329907602038,2.80982230173143,126.76776778509));
#84605=CARTESIAN_POINT('Ctrl Pts',(-46.0407370934691,2.69720437936831,126.68937584343));
#84606=CARTESIAN_POINT('Ctrl Pts',(-46.0484834267344,2.58130402881186,126.615700864419));
#84607=CARTESIAN_POINT('Ctrl Pts',(-46.0562297599997,2.46255927523958,126.547015802023));
#84608=CARTESIAN_POINT('Ctrl Pts',(-46.0639778280026,2.34378792960338,126.478315358084));
#84609=CARTESIAN_POINT('Ctrl Pts',(-46.0717258960056,2.22217125178955,126.414607250089));
#84610=CARTESIAN_POINT('Ctrl Pts',(-46.0794739640085,2.09817234034742,126.35611872973));
#84611=CARTESIAN_POINT('Ctrl Pts',(-46.0872302667504,1.97404164138593,126.297568047074));
#84612=CARTESIAN_POINT('Ctrl Pts',(-46.0949865694922,1.84752400528735,126.244248200718));
#84613=CARTESIAN_POINT('Ctrl Pts',(-46.1027428722341,1.71910352353059,126.196338684254));
#84614=CARTESIAN_POINT('Ctrl Pts',(-46.1105033147482,1.59061449989605,126.148403597038));
#84615=CARTESIAN_POINT('Ctrl Pts',(-46.1182637572625,1.4602209784434,126.10588471476));
#84616=CARTESIAN_POINT('Ctrl Pts',(-46.1260241997767,1.32842176930888,126.068911466184));
#84617=CARTESIAN_POINT('Ctrl Pts',(-46.1337971000421,1.19641098438327,126.031878864867));
#84618=CARTESIAN_POINT('Ctrl Pts',(-46.1415700003075,1.06299038324338,126.000409776776));
#84619=CARTESIAN_POINT('Ctrl Pts',(-46.149342900573,0.928669397219115,125.974582546767));
#84620=CARTESIAN_POINT('Ctrl Pts',(-46.1568332363351,0.799231317370065,
125.949694201624));
#84621=CARTESIAN_POINT('Ctrl Pts',(-46.1643235720971,0.668957483201672,
125.930044690525));
#84622=CARTESIAN_POINT('Ctrl Pts',(-46.1718139078592,0.538305878943531,
125.915658351811));
#84623=CARTESIAN_POINT('Ctrl Pts',(-46.1795882419783,0.402700579400201,
125.900726550693));
#84624=CARTESIAN_POINT('Ctrl Pts',(-46.1873625760974,0.266258741145796,
125.891417607349));
#84625=CARTESIAN_POINT('Ctrl Pts',(-46.1951369102165,0.129486299266316,
125.887815452432));
#84626=CARTESIAN_POINT('Ctrl Pts',(-46.2029016631636,-0.00711758280243635,
125.884217736849));
#84627=CARTESIAN_POINT('Ctrl Pts',(-46.2106664161107,-0.144050870735498,
125.886312826102));
#84628=CARTESIAN_POINT('Ctrl Pts',(-46.2184311690578,-0.280800689465603,
125.894133124334));
#84629=CARTESIAN_POINT('Ctrl Pts',(-46.2261882099428,-0.41741468634754,
125.901945655335));
#84630=CARTESIAN_POINT('Ctrl Pts',(-46.2339452508278,-0.553845188859211,
125.915472057029));
#84631=CARTESIAN_POINT('Ctrl Pts',(-46.2417022917128,-0.689577846239994,
125.934692717547));
#84632=CARTESIAN_POINT('Ctrl Pts',(-46.2494534829529,-0.825208146567447,
125.953898883615));
#84633=CARTESIAN_POINT('Ctrl Pts',(-46.257204674193,-0.960141263696641,
125.978790706797));
#84634=CARTESIAN_POINT('Ctrl Pts',(-46.2649558654331,-1.09386685705719,
126.009296659543));
#84635=CARTESIAN_POINT('Ctrl Pts',(-46.2727037622101,-1.22753561347404,
126.039789646445));
#84636=CARTESIAN_POINT('Ctrl Pts',(-46.2804516589872,-1.35999748652241,
126.07589193026));
#84637=CARTESIAN_POINT('Ctrl Pts',(-46.2881995557643,-1.49075145454704,
126.117480721167));
#84638=CARTESIAN_POINT('Ctrl Pts',(-46.2959458318484,-1.62147807165992,
126.159060812596));
#84639=CARTESIAN_POINT('Ctrl Pts',(-46.3036921079325,-1.75049712201573,
126.206125009933));
#84640=CARTESIAN_POINT('Ctrl Pts',(-46.3114383840166,-1.87732228439825,
126.258500511601));
#84641=CARTESIAN_POINT('Ctrl Pts',(-46.3191847172819,-2.00414838297548,
126.310876399894));
#84642=CARTESIAN_POINT('Ctrl Pts',(-46.3269310505472,-2.12878019990099,
126.368563521518));
#84643=CARTESIAN_POINT('Ctrl Pts',(-46.3346773838125,-2.25075132796435,
126.431340891774));
#84644=CARTESIAN_POINT('Ctrl Pts',(-46.3424254518155,-2.37274977061549,
126.494132320586));
#84645=CARTESIAN_POINT('Ctrl Pts',(-46.3501735198185,-2.49208599118945,
126.562016087466));
#84646=CARTESIAN_POINT('Ctrl Pts',(-46.3579215878214,-2.60831848032506,
126.634725409578));
#84647=CARTESIAN_POINT('Ctrl Pts',(-46.3656778905632,-2.72467450273394,
126.707512008023));
#84648=CARTESIAN_POINT('Ctrl Pts',(-46.3734341933051,-2.83791987224614,
126.785134199073));
#84649=CARTESIAN_POINT('Ctrl Pts',(-46.381190496047,-2.94764191254957,126.867281723528));
#84650=CARTESIAN_POINT('Ctrl Pts',(-46.3889509385611,-3.05742251480973,
126.94947309259));
#84651=CARTESIAN_POINT('Ctrl Pts',(-46.3967113810753,-3.16367573805213,
127.036194360671));
#84652=CARTESIAN_POINT('Ctrl Pts',(-46.4044718235894,-3.26602307112765,
127.127095824087));
#84653=CARTESIAN_POINT('Ctrl Pts',(-46.4122447238549,-3.36853470122818,
127.218143210601));
#84654=CARTESIAN_POINT('Ctrl Pts',(-46.4200176241203,-3.46712763018577,
127.313383930219));
#84655=CARTESIAN_POINT('Ctrl Pts',(-46.4277905243858,-3.56146058417582,
127.412431731245));
#84656=CARTESIAN_POINT('Ctrl Pts',(-46.4352808601479,-3.65236429767885,
127.507878895217));
#84657=CARTESIAN_POINT('Ctrl Pts',(-46.44277119591,-3.7393121773532,127.606860920735));
#84658=CARTESIAN_POINT('Ctrl Pts',(-46.4502615316721,-3.82203619499996,
127.709005648163));
#84659=CARTESIAN_POINT('Ctrl Pts',(-46.4580137640801,-3.90765262541002,
127.814721825838));
#84660=CARTESIAN_POINT('Ctrl Pts',(-46.4657659964882,-3.98902275759095,
127.924169647303));
#84661=CARTESIAN_POINT('Ctrl Pts',(-46.4735182288962,-4.06580198842802,
128.036972452997));
#84662=CARTESIAN_POINT('Ctrl Pts',(-46.4815540682425,-4.14539010339482,
128.153902025881));
#84663=CARTESIAN_POINT('Ctrl Pts',(-46.4895899075888,-4.22004469059768,
128.27443647339));
#84664=CARTESIAN_POINT('Ctrl Pts',(-46.4976257469351,-4.28942536002038,
128.398116003377));
#84665=CARTESIAN_POINT('Ctrl Pts',(-46.5053585457352,-4.35618960631028,
128.517131439085));
#84666=CARTESIAN_POINT('Ctrl Pts',(-46.5130913445354,-4.41807022567004,
128.639058690767));
#84667=CARTESIAN_POINT('Ctrl Pts',(-46.5208241433355,-4.47480662911583,
128.763456726022));
#84668=CARTESIAN_POINT('Ctrl Pts',(-46.5285515023032,-4.53150311990737,
128.88776725034));
#84669=CARTESIAN_POINT('Ctrl Pts',(-46.536278861271,-4.58306243067394,129.014544744627));
#84670=CARTESIAN_POINT('Ctrl Pts',(-46.5440062202387,-4.6292697277998,129.143323336294));
#84671=CARTESIAN_POINT('Ctrl Pts',(-46.5517293393805,-4.67545167203406,
129.27203127008));
#84672=CARTESIAN_POINT('Ctrl Pts',(-46.5594524585223,-4.7162873165601,129.402737746014));
#84673=CARTESIAN_POINT('Ctrl Pts',(-46.5671755776641,-4.75161003122865,
129.534957145999));
#84674=CARTESIAN_POINT('Ctrl Pts',(-46.5680998187933,-4.75583717120834,
129.550780106295));
#84675=CARTESIAN_POINT('Ctrl Pts',(-46.5690240599226,-4.75998541624853,
129.566624713434));
#84676=CARTESIAN_POINT('Ctrl Pts',(-46.5699483010518,-4.76405452823401,
129.582490119308));
#84677=CARTESIAN_POINT('Origin',(213.235140564004,0.,130.804360617566));
#84678=CARTESIAN_POINT('',(-48.6652562953714,-4.76405452823406,129.582490119308));
#84679=CARTESIAN_POINT('',(-48.3197360547346,-4.76405452823404,129.582490119308));
#84680=CARTESIAN_POINT('',(213.235140564004,-4.76405452823405,129.582490119308));
#84681=CARTESIAN_POINT('',(-46.9851405639615,-4.91824999272014,130.804628214911));
#84682=CARTESIAN_POINT('Ctrl Pts',(-46.9851405640085,-4.91824999272009,
130.804628215736));
#84683=CARTESIAN_POINT('Ctrl Pts',(-46.9859496370517,-4.9182492202234,130.818826114959));
#84684=CARTESIAN_POINT('Ctrl Pts',(-46.986758710095,-4.91818696861465,130.833023819215));
#84685=CARTESIAN_POINT('Ctrl Pts',(-46.9875677831383,-4.91806324189077,
130.84722098694));
#84686=CARTESIAN_POINT('Ctrl Pts',(-46.9953421172574,-4.91687435925656,
130.983640716111));
#84687=CARTESIAN_POINT('Ctrl Pts',(-47.0031164513764,-4.91000317256601,
131.120227020131));
#84688=CARTESIAN_POINT('Ctrl Pts',(-47.0108907854955,-4.897426093981,131.256467592179));
#84689=CARTESIAN_POINT('Ctrl Pts',(-47.0186555384426,-4.8848645155213,131.392540259899));
#84690=CARTESIAN_POINT('Ctrl Pts',(-47.0264202913897,-4.86661107234901,
131.528267657853));
#84691=CARTESIAN_POINT('Ctrl Pts',(-47.0341850443368,-4.84269416215559,
131.663136673546));
#84692=CARTESIAN_POINT('Ctrl Pts',(-47.0419420852218,-4.81880100657457,
131.797871735431));
#84693=CARTESIAN_POINT('Ctrl Pts',(-47.0496991261068,-4.78925564587121,
131.931749729213));
#84694=CARTESIAN_POINT('Ctrl Pts',(-47.0574561669918,-4.75413830396486,
132.064262220579));
#84695=CARTESIAN_POINT('Ctrl Pts',(-47.065207358232,-4.71904744431921,132.196674783244));
#84696=CARTESIAN_POINT('Ctrl Pts',(-47.0729585494721,-4.67839306679449,
132.327723516728));
#84697=CARTESIAN_POINT('Ctrl Pts',(-47.0807097407122,-4.63230647397676,
132.456910100533));
#84698=CARTESIAN_POINT('Ctrl Pts',(-47.0884576374893,-4.58623946919031,
132.586041776593));
#84699=CARTESIAN_POINT('Ctrl Pts',(-47.0962055342664,-4.53474497230109,
132.713312509672));
#84700=CARTESIAN_POINT('Ctrl Pts',(-47.1039534310435,-4.47800408871746,
132.83823928748));
#84701=CARTESIAN_POINT('Ctrl Pts',(-47.1116997071276,-4.42127507410349,
132.963139933299));
#84702=CARTESIAN_POINT('Ctrl Pts',(-47.1194459832117,-4.35930201722169,
133.085697243348));
#84703=CARTESIAN_POINT('Ctrl Pts',(-47.1271922592958,-4.29231394893896,
133.205448709712));
#84704=CARTESIAN_POINT('Ctrl Pts',(-47.1349385925612,-4.22532538616561,
133.325201060053));
#84705=CARTESIAN_POINT('Ctrl Pts',(-47.1426849258266,-4.15332192899037,
133.442147184172));
#84706=CARTESIAN_POINT('Ctrl Pts',(-47.1504312590919,-4.076578102137,133.55585003962));
#84707=CARTESIAN_POINT('Ctrl Pts',(-47.1581793270949,-3.99981708903582,
133.669578358035));
#84708=CARTESIAN_POINT('Ctrl Pts',(-47.1659273950978,-3.91831381253091,
133.780061638516));
#84709=CARTESIAN_POINT('Ctrl Pts',(-47.1736754631008,-3.83238533427041,
133.886892971357));
#84710=CARTESIAN_POINT('Ctrl Pts',(-47.1814317658427,-3.74636553020042,
133.993837845811));
#84711=CARTESIAN_POINT('Ctrl Pts',(-47.1891880685845,-3.6559113747416,134.09712271411));
#84712=CARTESIAN_POINT('Ctrl Pts',(-47.1969443713264,-3.56137969616614,
134.196374432726));
#84713=CARTESIAN_POINT('Ctrl Pts',(-47.2047048138406,-3.46679756318753,
134.295679124972));
#84714=CARTESIAN_POINT('Ctrl Pts',(-47.2124652563547,-3.36813385175206,
134.390946106833));
#84715=CARTESIAN_POINT('Ctrl Pts',(-47.2202256988689,-3.26578052332756,
134.481840819546));
#84716=CARTESIAN_POINT('Ctrl Pts',(-47.2279985991343,-3.16326288825377,
134.572881444521));
#84717=CARTESIAN_POINT('Ctrl Pts',(-47.2357714993997,-3.0570441034649,134.659535527355));
#84718=CARTESIAN_POINT('Ctrl Pts',(-47.2435443996651,-2.94754802457509,
134.741509802614));
#84719=CARTESIAN_POINT('Ctrl Pts',(-47.2510347354271,-2.84203240395706,
134.820504106486));
#84720=CARTESIAN_POINT('Ctrl Pts',(-47.2585250711892,-2.73347388201609,
134.895152766682));
#84721=CARTESIAN_POINT('Ctrl Pts',(-47.2660154069513,-2.62227366999117,
134.965233586328));
#84722=CARTESIAN_POINT('Ctrl Pts',(-47.2737897410703,-2.50685726812874,
135.03797154155));
#84723=CARTESIAN_POINT('Ctrl Pts',(-47.2815640751894,-2.38822929798725,
135.106018851214));
#84724=CARTESIAN_POINT('Ctrl Pts',(-47.2893384093084,-2.2668080280024,135.169078755852));
#84725=CARTESIAN_POINT('Ctrl Pts',(-47.2971031622555,-2.14553639888107,
135.232060944793));
#84726=CARTESIAN_POINT('Ctrl Pts',(-47.3048679152026,-2.02147866308284,
135.290067780008));
#84727=CARTESIAN_POINT('Ctrl Pts',(-47.3126326681497,-1.8950818663292,135.342845803441));
#84728=CARTESIAN_POINT('Ctrl Pts',(-47.3203897090347,-1.7688106086558,135.395571406997));
#84729=CARTESIAN_POINT('Ctrl Pts',(-47.3281467499197,-1.64020527171864,
135.443078384061));
#84730=CARTESIAN_POINT('Ctrl Pts',(-47.3359037908047,-1.50973697869491,
135.485159408121));
#84731=CARTESIAN_POINT('Ctrl Pts',(-47.3436549820449,-1.37936707282603,
135.527208698553));
#84732=CARTESIAN_POINT('Ctrl Pts',(-47.351406173285,-1.24713737776247,135.563840060841));
#84733=CARTESIAN_POINT('Ctrl Pts',(-47.3591573645251,-1.1135381169076,135.594894609168));
#84734=CARTESIAN_POINT('Ctrl Pts',(-47.3669052613022,-0.979995639302471,
135.625935958483));
#84735=CARTESIAN_POINT('Ctrl Pts',(-47.3746531580793,-0.845085133677955,
135.651405119839));
#84736=CARTESIAN_POINT('Ctrl Pts',(-47.3824010548563,-0.709310863847926,
135.671193382407));
#84737=CARTESIAN_POINT('Ctrl Pts',(-47.3901473309404,-0.573564995068006,
135.690977505696));
#84738=CARTESIAN_POINT('Ctrl Pts',(-47.3978936070245,-0.436956108099488,
135.705083037484));
#84739=CARTESIAN_POINT('Ctrl Pts',(-47.4056398831086,-0.299997120728754,
135.713452671098));
#84740=CARTESIAN_POINT('Ctrl Pts',(-47.413386216374,-0.163037122358075,
135.721822366496));
#84741=CARTESIAN_POINT('Ctrl Pts',(-47.4211325496393,-0.025727408665489,
135.724456055384));
#84742=CARTESIAN_POINT('Ctrl Pts',(-47.4288788829047,0.111415936842174,
135.721348471071));
#84743=CARTESIAN_POINT('Ctrl Pts',(-47.4366269509077,0.248589994651179,
135.718240190836));
#84744=CARTESIAN_POINT('Ctrl Pts',(-47.4443750189106,0.385597219348077,
135.709388087824));
#84745=CARTESIAN_POINT('Ctrl Pts',(-47.4521230869136,0.521923886707727,
135.694838970343));
#84746=CARTESIAN_POINT('Ctrl Pts',(-47.4598793896554,0.658395443671755,
135.680274389888));
#84747=CARTESIAN_POINT('Ctrl Pts',(-47.4676356923973,0.794184609042562,
135.660000741295));
#84748=CARTESIAN_POINT('Ctrl Pts',(-47.4753919951391,0.928784572203252,
135.634116541103));
#84749=CARTESIAN_POINT('Ctrl Pts',(-47.4831524376533,1.06345637541719,135.608218525734));
#84750=CARTESIAN_POINT('Ctrl Pts',(-47.4909128801675,1.19693733138371,135.576704081723));
#84751=CARTESIAN_POINT('Ctrl Pts',(-47.4986733226816,1.32873410159363,135.53972214017));
#84752=CARTESIAN_POINT('Ctrl Pts',(-47.5064462229471,1.46074244367946,135.502680831922));
#84753=CARTESIAN_POINT('Ctrl Pts',(-47.5142191232125,1.59106082545536,135.460154608423));
#84754=CARTESIAN_POINT('Ctrl Pts',(-47.521992023478,1.71921341009314,135.412341554273));
#84755=CARTESIAN_POINT('Ctrl Pts',(-47.52948235924,1.8427073254828,135.366266625075));
#84756=CARTESIAN_POINT('Ctrl Pts',(-47.536972695002,1.96418989026465,135.31528269026));
#84757=CARTESIAN_POINT('Ctrl Pts',(-47.5444630307641,2.08325729944026,135.259607197367));
#84758=CARTESIAN_POINT('Ctrl Pts',(-47.5522373648832,2.20683918562417,135.201820751239));
#84759=CARTESIAN_POINT('Ctrl Pts',(-47.5600116990023,2.32821062995524,135.138796913261));
#84760=CARTESIAN_POINT('Ctrl Pts',(-47.5677860331213,2.44689587598283,135.070727178775));
#84761=CARTESIAN_POINT('Ctrl Pts',(-47.5755507860684,2.56543485305188,135.002741334152));
#84762=CARTESIAN_POINT('Ctrl Pts',(-47.5833155390155,2.68129388283498,134.929722158857));
#84763=CARTESIAN_POINT('Ctrl Pts',(-47.5910802919626,2.79401808475923,134.851908764845));
#84764=CARTESIAN_POINT('Ctrl Pts',(-47.5988373328476,2.90663032741685,134.774172656193));
#84765=CARTESIAN_POINT('Ctrl Pts',(-47.6065943737326,3.01611361866234,134.69165202546));
#84766=CARTESIAN_POINT('Ctrl Pts',(-47.6143514146176,3.12203887524488,134.604631176876));
#84767=CARTESIAN_POINT('Ctrl Pts',(-47.6221026058578,3.22788425276761,134.517675951391));
#84768=CARTESIAN_POINT('Ctrl Pts',(-47.6298537970979,3.33017663538644,134.426227510081));
#84769=CARTESIAN_POINT('Ctrl Pts',(-47.637604988338,3.42851737023967,134.330612410116));
#84770=CARTESIAN_POINT('Ctrl Pts',(-47.6453528851151,3.52681630765726,134.23503794912));
#84771=CARTESIAN_POINT('Ctrl Pts',(-47.6531007818922,3.62116665809292,134.135300623705));
#84772=CARTESIAN_POINT('Ctrl Pts',(-47.6608486786693,3.71120439313757,134.031765924443));
#84773=CARTESIAN_POINT('Ctrl Pts',(-47.6685949547534,3.80122329422903,133.928252882407));
#84774=CARTESIAN_POINT('Ctrl Pts',(-47.6763412308376,3.88693111787532,133.820944341314));
#84775=CARTESIAN_POINT('Ctrl Pts',(-47.6840875069217,3.96800240575882,133.710240857767));
#84776=CARTESIAN_POINT('Ctrl Pts',(-47.691833840187,4.04907429209216,133.599536557033));
#84777=CARTESIAN_POINT('Ctrl Pts',(-47.6995801734523,4.1255093433711,133.485437579265));
#84778=CARTESIAN_POINT('Ctrl Pts',(-47.7073265067177,4.19702417283647,133.36837527336));
#84779=CARTESIAN_POINT('Ctrl Pts',(-47.7150745747207,4.26855501755195,133.251286752163));
#84780=CARTESIAN_POINT('Ctrl Pts',(-47.7228226427236,4.33516324411925,133.131233915876));
#84781=CARTESIAN_POINT('Ctrl Pts',(-47.7305707107266,4.39661055320231,133.008674276275));
#84782=CARTESIAN_POINT('Ctrl Pts',(-47.7383270134684,4.45812316921677,132.885984378829));
#84783=CARTESIAN_POINT('Ctrl Pts',(-47.7460833162103,4.51446373519345,132.760782705978));
#84784=CARTESIAN_POINT('Ctrl Pts',(-47.7538396189522,4.56544119236859,132.633548902441));
#84785=CARTESIAN_POINT('Ctrl Pts',(-47.7616000614664,4.61644585774753,132.506247190392));
#84786=CARTESIAN_POINT('Ctrl Pts',(-47.7693605039805,4.66208158061902,132.37691155499));
#84787=CARTESIAN_POINT('Ctrl Pts',(-47.7771209464946,4.70220699942155,132.24603755679));
#84788=CARTESIAN_POINT('Ctrl Pts',(-47.7848938467601,4.7423968311085,132.114953468031));
#84789=CARTESIAN_POINT('Ctrl Pts',(-47.7926667470255,4.7770585834262,131.982326460072));
#84790=CARTESIAN_POINT('Ctrl Pts',(-47.800439647291,4.80610170913157,131.84866393748));
#84791=CARTESIAN_POINT('Ctrl Pts',(-47.807929983053,4.83408904406217,131.71986038426));
#84792=CARTESIAN_POINT('Ctrl Pts',(-47.815420318815,4.85685910940292,131.590095599825));
#84793=CARTESIAN_POINT('Ctrl Pts',(-47.822910654577,4.87437658346252,131.459826852465));
#84794=CARTESIAN_POINT('Ctrl Pts',(-47.8306849886961,4.8925582378755,131.324618925953));
#84795=CARTESIAN_POINT('Ctrl Pts',(-47.8384593228152,4.90513872838041,131.18843976855));
#84796=CARTESIAN_POINT('Ctrl Pts',(-47.8462336569342,4.91202200744782,131.05179315554));
#84797=CARTESIAN_POINT('Ctrl Pts',(-47.8539984098813,4.91889680348895,130.915314947269));
#84798=CARTESIAN_POINT('Ctrl Pts',(-47.8617631628284,4.92008833891436,130.778370816374));
#84799=CARTESIAN_POINT('Ctrl Pts',(-47.8695279157755,4.9155519113241,130.641472712619));
#84800=CARTESIAN_POINT('Ctrl Pts',(-47.8772849566605,4.91101998937768,130.504710577991));
#84801=CARTESIAN_POINT('Ctrl Pts',(-47.8850419975454,4.90077143883322,130.367994767749));
#84802=CARTESIAN_POINT('Ctrl Pts',(-47.8927990384304,4.88481352291191,130.231839955164));
#84803=CARTESIAN_POINT('Ctrl Pts',(-47.9005502296705,4.86886764097912,130.095787817983));
#84804=CARTESIAN_POINT('Ctrl Pts',(-47.9083014209108,4.84722100878712,129.960296223135));
#84805=CARTESIAN_POINT('Ctrl Pts',(-47.9160526121509,4.81993288652047,129.825877080689));
#84806=CARTESIAN_POINT('Ctrl Pts',(-47.923800508928,4.79265636243372,129.691515069965));
#84807=CARTESIAN_POINT('Ctrl Pts',(-47.931548405705,4.75974319490094,129.558224987397));
#84808=CARTESIAN_POINT('Ctrl Pts',(-47.9392963024821,4.72130411524199,129.426510656976));
#84809=CARTESIAN_POINT('Ctrl Pts',(-47.9470425785662,4.68287307620985,129.294823878353));
#84810=CARTESIAN_POINT('Ctrl Pts',(-47.9547888546502,4.63891853366306,129.16471257133));
#84811=CARTESIAN_POINT('Ctrl Pts',(-47.9625351307343,4.58960156904713,129.036667063836));
#84812=CARTESIAN_POINT('Ctrl Pts',(-47.9702814639997,4.54028424038465,128.908620611139));
#84813=CARTESIAN_POINT('Ctrl Pts',(-47.978027797265,4.48560455118449,128.782640353239));
#84814=CARTESIAN_POINT('Ctrl Pts',(-47.9857741305303,4.42577223002262,128.659197866057));
#84815=CARTESIAN_POINT('Ctrl Pts',(-47.9935221985333,4.36592650982727,128.535727734786));
#84816=CARTESIAN_POINT('Ctrl Pts',(-48.0012702665362,4.3009260320426,128.414796856866));
#84817=CARTESIAN_POINT('Ctrl Pts',(-48.0090183345392,4.23102690766987,128.296853016566));
#84818=CARTESIAN_POINT('Ctrl Pts',(-48.0167746372811,4.16105349367586,128.178783824149));
#84819=CARTESIAN_POINT('Ctrl Pts',(-48.0245309400229,4.08617123251555,128.063708347948));
#84820=CARTESIAN_POINT('Ctrl Pts',(-48.0322872427647,4.00668039094847,127.952046590799));
#84821=CARTESIAN_POINT('Ctrl Pts',(-48.0400476852789,3.92714712272583,127.84032523641));
#84822=CARTESIAN_POINT('Ctrl Pts',(-48.0478081277931,3.84300061261264,127.732021540153));
#84823=CARTESIAN_POINT('Ctrl Pts',(-48.0555685703073,3.7545813803642,127.627522296102));
#84824=CARTESIAN_POINT('Ctrl Pts',(-48.0633414705727,3.66602020971466,127.522855300587));
#84825=CARTESIAN_POINT('Ctrl Pts',(-48.071114370838,3.57317287551519,127.422005249294));
#84826=CARTESIAN_POINT('Ctrl Pts',(-48.0788872711035,3.47641732860077,127.325322586744));
#84827=CARTESIAN_POINT('Ctrl Pts',(-48.0863776068656,3.38317908952815,127.232154582506));
#84828=CARTESIAN_POINT('Ctrl Pts',(-48.0938679426277,3.28631207775877,127.142856445984));
#84829=CARTESIAN_POINT('Ctrl Pts',(-48.1013582783898,3.18618191381722,127.057705058996));
#84830=CARTESIAN_POINT('Ctrl Pts',(-48.1091326125089,3.08225528427696,126.96932513129));
#84831=CARTESIAN_POINT('Ctrl Pts',(-48.116906946628,2.97448396477283,126.885132647393));
#84832=CARTESIAN_POINT('Ctrl Pts',(-48.1246812807471,2.86323987968398,126.805480717658));
#84833=CARTESIAN_POINT('Ctrl Pts',(-48.1324460336942,2.75213289298782,126.725926951808));
#84834=CARTESIAN_POINT('Ctrl Pts',(-48.1402107866413,2.63756197120931,126.650902831514));
#84835=CARTESIAN_POINT('Ctrl Pts',(-48.1479755395884,2.51993366944313,126.580722687522));
#84836=CARTESIAN_POINT('Ctrl Pts',(-48.1557325804734,2.4024221977647,126.510612247439));
#84837=CARTESIAN_POINT('Ctrl Pts',(-48.1634896213584,2.28185972271108,126.445336408361));
#84838=CARTESIAN_POINT('Ctrl Pts',(-48.1712466622434,2.15868317943003,126.385167253009));
#84839=CARTESIAN_POINT('Ctrl Pts',(-48.1789978534836,2.03559952453826,126.325043471685));
#84840=CARTESIAN_POINT('Ctrl Pts',(-48.1867490447236,1.90990607502303,126.270018879831));
#84841=CARTESIAN_POINT('Ctrl Pts',(-48.1945002359638,1.78206554690058,126.220320320072));
#84842=CARTESIAN_POINT('Ctrl Pts',(-48.2022481327408,1.65427935441301,126.170642883526));
#84843=CARTESIAN_POINT('Ctrl Pts',(-48.2099960295179,1.52434826197686,126.126287118102));
#84844=CARTESIAN_POINT('Ctrl Pts',(-48.217743926295,1.39275600396752,126.087432191576));
#84845=CARTESIAN_POINT('Ctrl Pts',(-48.2254902023791,1.26119127222158,126.048585392663));
#84846=CARTESIAN_POINT('Ctrl Pts',(-48.2332364784633,1.1279664407833,126.015237254574));
#84847=CARTESIAN_POINT('Ctrl Pts',(-48.2409827545474,0.993581104882178,
125.987517289148));
#84848=CARTESIAN_POINT('Ctrl Pts',(-48.2487290878127,0.859194776979217,
125.9597971191));
#84849=CARTESIAN_POINT('Ctrl Pts',(-48.2564754210781,0.723648310423534,
125.9377052836));
#84850=CARTESIAN_POINT('Ctrl Pts',(-48.2642217543434,0.587451818810714,
125.921320230361));
#84851=CARTESIAN_POINT('Ctrl Pts',(-48.2719698223464,0.451224826937732,
125.904931507803));
#84852=CARTESIAN_POINT('Ctrl Pts',(-48.2797178903493,0.314347908434946,
125.894252157255));
#84853=CARTESIAN_POINT('Ctrl Pts',(-48.2874659583523,0.177336231142527,
125.889308743616));
#84854=CARTESIAN_POINT('Ctrl Pts',(-48.2952222610942,0.0401789362092088,
125.884360076057));
#84855=CARTESIAN_POINT('Ctrl Pts',(-48.302978563836,-0.0971130122836188,
125.885159537386));
#84856=CARTESIAN_POINT('Ctrl Pts',(-48.3107348665779,-0.234023952536301,
125.891681526465));
#84857=CARTESIAN_POINT('Ctrl Pts',(-48.318495309092,-0.371007966280291,
125.898206996527));
#84858=CARTESIAN_POINT('Ctrl Pts',(-48.3262557516063,-0.507610177369921,
125.910461045347));
#84859=CARTESIAN_POINT('Ctrl Pts',(-48.3340161941204,-0.643321105752883,
125.928366255654));
#84860=CARTESIAN_POINT('Ctrl Pts',(-48.3417890943859,-0.779249889365936,
125.946300208996));
#84861=CARTESIAN_POINT('Ctrl Pts',(-48.3495619946513,-0.914284145797944,
125.969903384707));
#84862=CARTESIAN_POINT('Ctrl Pts',(-48.3573348949168,-1.04792474448931,
125.999047225873));
#84863=CARTESIAN_POINT('Ctrl Pts',(-48.3648252306788,-1.17670717079752,
126.027131615003));
#84864=CARTESIAN_POINT('Ctrl Pts',(-48.3723155664407,-1.30419520807634,
126.060360751402));
#84865=CARTESIAN_POINT('Ctrl Pts',(-48.3798059022027,-1.42995828098586,
126.098576689554));
#84866=CARTESIAN_POINT('Ctrl Pts',(-48.3875802363218,-1.56048969902998,
126.138241596616));
#84867=CARTESIAN_POINT('Ctrl Pts',(-48.3953545704409,-1.6895762508405,126.183404565895));
#84868=CARTESIAN_POINT('Ctrl Pts',(-48.40312890456,-1.81671982046462,126.233943551648));
#84869=CARTESIAN_POINT('Ctrl Pts',(-48.4108936575071,-1.94370669700215,
126.284420252618));
#84870=CARTESIAN_POINT('Ctrl Pts',(-48.4186584104542,-2.06875499597062,
126.340259644343));
#84871=CARTESIAN_POINT('Ctrl Pts',(-48.4264231634013,-2.1913805090514,126.401289583952));
#84872=CARTESIAN_POINT('Ctrl Pts',(-48.4341802042863,-2.31388422874404,
126.462258907765));
#84873=CARTESIAN_POINT('Ctrl Pts',(-48.4419372451712,-2.43396960353701,
126.528408347062));
#84874=CARTESIAN_POINT('Ctrl Pts',(-48.4496942860562,-2.55117154841131,
126.599517363285));
#84875=CARTESIAN_POINT('Ctrl Pts',(-48.4574454772963,-2.66828511038713,
126.670572755645));
#84876=CARTESIAN_POINT('Ctrl Pts',(-48.4651966685365,-2.78251923758726,
126.746580078598));
#84877=CARTESIAN_POINT('Ctrl Pts',(-48.4729478597766,-2.89343297157776,
126.827272650034));
#84878=CARTESIAN_POINT('Ctrl Pts',(-48.4806957565537,-3.00429956427274,
126.907930924975));
#84879=CARTESIAN_POINT('Ctrl Pts',(-48.4884436533308,-3.11184825515029,
126.99327025822));
#84880=CARTESIAN_POINT('Ctrl Pts',(-48.4961915501079,-3.21566683503874,
127.082980514898));
#84881=CARTESIAN_POINT('Ctrl Pts',(-48.503937826192,-3.3194636983182,127.172672006125));
#84882=CARTESIAN_POINT('Ctrl Pts',(-48.5116841022761,-3.4195317069508,127.266732346726));
#84883=CARTESIAN_POINT('Ctrl Pts',(-48.5194303783602,-3.51549185553239,
127.3648112174));
#84884=CARTESIAN_POINT('Ctrl Pts',(-48.5271767116256,-3.61145271247001,
127.462890812069));
#84885=CARTESIAN_POINT('Ctrl Pts',(-48.5349230448908,-3.70330537542946,
127.564988716547));
#84886=CARTESIAN_POINT('Ctrl Pts',(-48.5426693781561,-3.79070811526944,
127.670718160723));
#84887=CARTESIAN_POINT('Ctrl Pts',(-48.5504174461591,-3.878130428347,127.776471282275));
#84888=CARTESIAN_POINT('Ctrl Pts',(-48.5581655141622,-3.96110058627273,
127.885857260538));
#84889=CARTESIAN_POINT('Ctrl Pts',(-48.5659135821652,-4.03931777844532,
127.998457029195));
#84890=CARTESIAN_POINT('Ctrl Pts',(-48.573669884907,-4.11761810078055,128.111176470225));
#84891=CARTESIAN_POINT('Ctrl Pts',(-48.5814261876489,-4.19115514302552,
128.227116203178));
#84892=CARTESIAN_POINT('Ctrl Pts',(-48.5891824903907,-4.25967171634283,
128.345828549138));
#84893=CARTESIAN_POINT('Ctrl Pts',(-48.5969429329049,-4.32822485901841,
128.464604255451));
#84894=CARTESIAN_POINT('Ctrl Pts',(-48.604703375419,-4.39175201248198,128.586155177126));
#84895=CARTESIAN_POINT('Ctrl Pts',(-48.6124638179332,-4.4500429236628,128.710010828238));
#84896=CARTESIAN_POINT('Ctrl Pts',(-48.6202367181986,-4.50842740858908,
128.834065303437));
#84897=CARTESIAN_POINT('Ctrl Pts',(-48.6280096184641,-4.56155870238263,
128.960431540754));
#84898=CARTESIAN_POINT('Ctrl Pts',(-48.6357825187295,-4.60927517135961,
129.088620119359));
#84899=CARTESIAN_POINT('Ctrl Pts',(-48.6432728544915,-4.65525702649881,
129.212148720244));
#84900=CARTESIAN_POINT('Ctrl Pts',(-48.6507631902536,-4.69621081116611,
129.337369176547));
#84901=CARTESIAN_POINT('Ctrl Pts',(-48.6582535260156,-4.73203667290888,
129.463833859629));
#84902=CARTESIAN_POINT('Ctrl Pts',(-48.6605877824675,-4.74320129243672,
129.503244776816));
#84903=CARTESIAN_POINT('Ctrl Pts',(-48.6629220389195,-4.75387503723625,
129.542800438403));
#84904=CARTESIAN_POINT('Ctrl Pts',(-48.6652562953714,-4.76405452823406,
129.582490119308));
#84905=CARTESIAN_POINT('Ctrl Pts',(-46.9150405857891,-4.76405452823398,
129.582490119308));
#84906=CARTESIAN_POINT('Ctrl Pts',(-46.922788768966,-4.7980770148678,129.71514327833));
#84907=CARTESIAN_POINT('Ctrl Pts',(-46.9305369521428,-4.82652808527651,
129.849114315221));
#84908=CARTESIAN_POINT('Ctrl Pts',(-46.9382851353198,-4.84933180294816,
129.983894818513));
#84909=CARTESIAN_POINT('Ctrl Pts',(-46.9460943734267,-4.87231521169769,
130.119737379066));
#84910=CARTESIAN_POINT('Ctrl Pts',(-46.9539036115337,-4.88956184041191,
130.256401813749));
#84911=CARTESIAN_POINT('Ctrl Pts',(-46.9617128496407,-4.90104738870751,
130.393364807194));
#84912=CARTESIAN_POINT('Ctrl Pts',(-46.9695220877476,-4.91253293700309,
130.530327800639));
#84913=CARTESIAN_POINT('Ctrl Pts',(-46.9773313258545,-4.91825744889735,
130.667588949323));
#84914=CARTESIAN_POINT('Ctrl Pts',(-46.9851405639614,-4.91824999272014,
130.80462821491));
#84915=CARTESIAN_POINT('',(-46.6398594360395,-4.91824834186539,130.808399211173));
#84916=CARTESIAN_POINT('Ctrl Pts',(-46.5699483010518,-4.76405452823401,
129.582490119308));
#84917=CARTESIAN_POINT('Ctrl Pts',(-46.5776698308829,-4.7980497363981,129.715036919991));
#84918=CARTESIAN_POINT('Ctrl Pts',(-46.5853913607139,-4.82651753434675,
129.849036394156));
#84919=CARTESIAN_POINT('Ctrl Pts',(-46.593112890545,-4.84934736789346,129.983986819834));
#84920=CARTESIAN_POINT('Ctrl Pts',(-46.6009039814527,-4.87238286894861,
130.1201529757));
#84921=CARTESIAN_POINT('Ctrl Pts',(-46.6086950723604,-4.88967822118436,
130.257286906837));
#84922=CARTESIAN_POINT('Ctrl Pts',(-46.6164861632681,-4.90117291008143,
130.394864380729));
#84923=CARTESIAN_POINT('Ctrl Pts',(-46.6242772541758,-4.9126675989785,130.53244185462));
#84924=CARTESIAN_POINT('Ctrl Pts',(-46.6320683450834,-4.91836160787432,
130.670462460698));
#84925=CARTESIAN_POINT('Ctrl Pts',(-46.6398594359911,-4.91824834186609,
130.808399210317));
#84926=CARTESIAN_POINT('Ctrl Pts',(-46.6398594360394,-4.91824834186539,
130.808399211173));
#84927=CARTESIAN_POINT('Ctrl Pts',(-46.6490111898273,-4.91811529466422,
130.970425708587));
#84928=CARTESIAN_POINT('Ctrl Pts',(-46.6581629436152,-4.90997173897153,
131.132110276553));
#84929=CARTESIAN_POINT('Ctrl Pts',(-46.6673146974032,-4.89394191360149,
131.292741215865));
#84930=CARTESIAN_POINT('Ctrl Pts',(-46.6765304058137,-4.87780006801593,
131.454494682217));
#84931=CARTESIAN_POINT('Ctrl Pts',(-46.6857461142242,-4.85366144978944,
131.615179685457));
#84932=CARTESIAN_POINT('Ctrl Pts',(-46.6949618226347,-4.82170173736842,
131.774090176958));
#84933=CARTESIAN_POINT('Ctrl Pts',(-46.7042476070203,-4.78949900423655,
131.934209019151));
#84934=CARTESIAN_POINT('Ctrl Pts',(-46.7135333914058,-4.7493558473027,132.092526207359));
#84935=CARTESIAN_POINT('Ctrl Pts',(-46.7228191757913,-4.70150009146582,
132.248341210388));
#84936=CARTESIAN_POINT('Ctrl Pts',(-46.7247825023559,-4.69138177805227,
132.281285733102));
#84937=CARTESIAN_POINT('Ctrl Pts',(-46.7267458289205,-4.68091884761776,
132.3141184762));
#84938=CARTESIAN_POINT('Ctrl Pts',(-46.7287091554851,-4.67011372258824,
132.346832944901));
#84939=CARTESIAN_POINT('Ctrl Pts',(-46.7364834896042,-4.62732784392044,
132.47637492472));
#84940=CARTESIAN_POINT('Ctrl Pts',(-46.7442578237232,-4.57908015914792,
132.604340516058));
#84941=CARTESIAN_POINT('Ctrl Pts',(-46.7520321578423,-4.52550463227619,
132.730234675169));
#84942=CARTESIAN_POINT('Ctrl Pts',(-46.7597969107894,-4.47199513245315,
132.85597368098));
#84943=CARTESIAN_POINT('Ctrl Pts',(-46.7675616637365,-4.41317100671473,
132.979645977692));
#84944=CARTESIAN_POINT('Ctrl Pts',(-46.7753264166836,-4.34921596802157,
133.100771627382));
#84945=CARTESIAN_POINT('Ctrl Pts',(-46.7830834575686,-4.28532445037463,
133.221776973369));
#84946=CARTESIAN_POINT('Ctrl Pts',(-46.7908404984536,-4.21631234259891,
133.340240362392));
#84947=CARTESIAN_POINT('Ctrl Pts',(-46.7985975393385,-4.14241128050061,
133.455702135681));
#84948=CARTESIAN_POINT('Ctrl Pts',(-46.8063487305787,-4.06856594776781,
133.571076838349));
#84949=CARTESIAN_POINT('Ctrl Pts',(-46.8140999218189,-3.98983920897081,
133.683454102768));
#84950=CARTESIAN_POINT('Ctrl Pts',(-46.821851113059,-3.906508251208,133.792399497123));
#84951=CARTESIAN_POINT('Ctrl Pts',(-46.8295990098361,-3.8232127113254,133.901298586779));
#84952=CARTESIAN_POINT('Ctrl Pts',(-46.8373469066131,-3.73531708166364,
134.006768397599));
#84953=CARTESIAN_POINT('Ctrl Pts',(-46.8450948033902,-3.64314129966474,
134.108404281499));
#84954=CARTESIAN_POINT('Ctrl Pts',(-46.8528410794743,-3.55098479885237,
134.210018905364));
#84955=CARTESIAN_POINT('Ctrl Pts',(-46.8605873555584,-3.45455018901577,
134.30780090806));
#84956=CARTESIAN_POINT('Ctrl Pts',(-46.8683336316425,-3.35419678365892,
134.401379800027));
#84957=CARTESIAN_POINT('Ctrl Pts',(-46.8760799649079,-3.25384263751602,
134.494959382772));
#84958=CARTESIAN_POINT('Ctrl Pts',(-46.8838262981731,-3.14956992406675,
134.584335526241));
#84959=CARTESIAN_POINT('Ctrl Pts',(-46.8915726314385,-3.0417735025981,134.669175881119));
#84960=CARTESIAN_POINT('Ctrl Pts',(-46.8993206994415,-2.93395294086827,
134.754035235406));
#84961=CARTESIAN_POINT('Ctrl Pts',(-46.9070687674445,-2.82260740804753,
134.834356538108));
#84962=CARTESIAN_POINT('Ctrl Pts',(-46.9148168354475,-2.70816306839881,
134.909849121686));
#84963=CARTESIAN_POINT('Ctrl Pts',(-46.9225731381893,-2.593597095944,134.98542193968));
#84964=CARTESIAN_POINT('Ctrl Pts',(-46.9303294409311,-2.47592606451947,
135.056155571163));
#84965=CARTESIAN_POINT('Ctrl Pts',(-46.938085743673,-2.35560369594359,135.121803644423));
#84966=CARTESIAN_POINT('Ctrl Pts',(-46.9458461861872,-2.2352171076966,135.187486756036));
#84967=CARTESIAN_POINT('Ctrl Pts',(-46.9536066287013,-2.11217671316505,
135.248078728282));
#84968=CARTESIAN_POINT('Ctrl Pts',(-46.9613670712155,-1.98695790827754,
135.303380659001));
#84969=CARTESIAN_POINT('Ctrl Pts',(-46.9691399714809,-1.86153809104803,
135.358771365289));
#84970=CARTESIAN_POINT('Ctrl Pts',(-46.9769128717463,-1.73393323953328,
135.408854917317));
#84971=CARTESIAN_POINT('Ctrl Pts',(-46.9846857720118,-1.60463651238487,
135.453481472698));
#84972=CARTESIAN_POINT('Ctrl Pts',(-46.9921761077738,-1.48004004694693,
135.496485740383));
#84973=CARTESIAN_POINT('Ctrl Pts',(-46.9996664435359,-1.35387287313202,
135.534422785692));
#84974=CARTESIAN_POINT('Ctrl Pts',(-47.0071567792979,-1.2265848868552,135.567203526779));
#84975=CARTESIAN_POINT('Ctrl Pts',(-47.014931113417,-1.09447073789053,135.601227159628));
#84976=CARTESIAN_POINT('Ctrl Pts',(-47.0227054475361,-0.960730609589093,
135.629803543835));
#84977=CARTESIAN_POINT('Ctrl Pts',(-47.0304797816552,-0.825853407092362,
135.652777803875));
#84978=CARTESIAN_POINT('Ctrl Pts',(-47.0382445346023,-0.691142428693386,
135.675723750193));
#84979=CARTESIAN_POINT('Ctrl Pts',(-47.0460092875494,-0.55529754606672,
135.69308124446));
#84980=CARTESIAN_POINT('Ctrl Pts',(-47.0537740404964,-0.418821845923377,
135.704745431423));
#84981=CARTESIAN_POINT('Ctrl Pts',(-47.0615310813814,-0.282481695369571,
135.71639803335));
#84982=CARTESIAN_POINT('Ctrl Pts',(-47.0692881222665,-0.145512361160019,
135.72236854795));
#84983=CARTESIAN_POINT('Ctrl Pts',(-47.0770451631515,-0.00842577204631309,
135.722603400193));
#84984=CARTESIAN_POINT('Ctrl Pts',(-47.0847963543916,0.128557439004164,
135.722838075333));
#84985=CARTESIAN_POINT('Ctrl Pts',(-47.0925475456317,0.265657339575808,
135.717345696711));
#84986=CARTESIAN_POINT('Ctrl Pts',(-47.1002987368718,0.402358603482833,
135.706124648678));
#84987=CARTESIAN_POINT('Ctrl Pts',(-47.1080466336489,0.539001765706071,
135.69490836989));
#84988=CARTESIAN_POINT('Ctrl Pts',(-47.115794530426,0.675246239411549,135.677968296313));
#84989=CARTESIAN_POINT('Ctrl Pts',(-47.123542427203,0.810578648703746,135.655354878206));
#84990=CARTESIAN_POINT('Ctrl Pts',(-47.1312887032871,0.945882749373532,
135.632746190339));
#84991=CARTESIAN_POINT('Ctrl Pts',(-47.1390349793713,1.08027477973574,135.604466582829));
#84992=CARTESIAN_POINT('Ctrl Pts',(-47.1467812554554,1.21324881870292,135.570618097646));
#84993=CARTESIAN_POINT('Ctrl Pts',(-47.1545275887208,1.34622383925407,135.5367693626));
#84994=CARTESIAN_POINT('Ctrl Pts',(-47.1622739219861,1.47778046864058,135.497351764298));
#84995=CARTESIAN_POINT('Ctrl Pts',(-47.1700202552514,1.60742566088105,135.452517866115));
#84996=CARTESIAN_POINT('Ctrl Pts',(-47.1777683232544,1.73709988626343,135.407673927692));
#84997=CARTESIAN_POINT('Ctrl Pts',(-47.1855163912574,1.8648614532996,135.357411403528));
#84998=CARTESIAN_POINT('Ctrl Pts',(-47.1932644592604,1.99023546296301,135.301931724782));
#84999=CARTESIAN_POINT('Ctrl Pts',(-47.2010207620023,2.11574272161586,135.246393081573));
#85000=CARTESIAN_POINT('Ctrl Pts',(-47.2087770647441,2.23885699582329,135.185626365801));
#85001=CARTESIAN_POINT('Ctrl Pts',(-47.2165333674859,2.3591257583593,135.119880136552));
#85002=CARTESIAN_POINT('Ctrl Pts',(-47.2242938100001,2.47945871195526,135.05409881656));
#85003=CARTESIAN_POINT('Ctrl Pts',(-47.2320542525142,2.59694279293212,134.983332888996));
#85004=CARTESIAN_POINT('Ctrl Pts',(-47.2398146950284,2.7111536961594,134.907874806441));
#85005=CARTESIAN_POINT('Ctrl Pts',(-47.2475875952938,2.82554794086771,134.832295591874));
#85006=CARTESIAN_POINT('Ctrl Pts',(-47.2553604955592,2.9366581907942,134.752009399567));
#85007=CARTESIAN_POINT('Ctrl Pts',(-47.2631333958247,3.04409181499776,134.667350144392));
#85008=CARTESIAN_POINT('Ctrl Pts',(-47.2706237315867,3.14761995635256,134.585768466385));
#85009=CARTESIAN_POINT('Ctrl Pts',(-47.2781140673488,3.24773390625493,134.500126349468));
#85010=CARTESIAN_POINT('Ctrl Pts',(-47.2856044031108,3.34411553789474,134.410754152902));
#85011=CARTESIAN_POINT('Ctrl Pts',(-47.2933787372299,3.4441515083926,134.317993382339));
#85012=CARTESIAN_POINT('Ctrl Pts',(-47.3011530713489,3.5404834358823,134.220920258363));
#85013=CARTESIAN_POINT('Ctrl Pts',(-47.308927405468,3.63271675402707,134.119862396711));
#85014=CARTESIAN_POINT('Ctrl Pts',(-47.3166921584151,3.72483640285035,134.018929079841));
#85015=CARTESIAN_POINT('Ctrl Pts',(-47.3244569113623,3.81286723162271,133.914021082392));
#85016=CARTESIAN_POINT('Ctrl Pts',(-47.3322216643093,3.89644909199301,133.805504988636));
#85017=CARTESIAN_POINT('Ctrl Pts',(-47.3399787051943,3.9799479376813,133.697096674594));
#85018=CARTESIAN_POINT('Ctrl Pts',(-47.3477357460793,4.05900637151,133.58508770353));
#85019=CARTESIAN_POINT('Ctrl Pts',(-47.3554927869643,4.13330260929571,133.469879816988));
#85020=CARTESIAN_POINT('Ctrl Pts',(-47.3632439782044,4.20754281971057,133.354758809611));
#85021=CARTESIAN_POINT('Ctrl Pts',(-47.3709951694446,4.27702777113424,133.236444015585));
#85022=CARTESIAN_POINT('Ctrl Pts',(-47.3787463606847,4.34147755788319,133.115368120128));
#85023=CARTESIAN_POINT('Ctrl Pts',(-47.3864942574618,4.40589995175351,132.994343685156));
#85024=CARTESIAN_POINT('Ctrl Pts',(-47.3942421542388,4.46529125407996,132.870560827231));
#85025=CARTESIAN_POINT('Ctrl Pts',(-47.4019900510159,4.5194164178817,132.74447873363));
#85026=CARTESIAN_POINT('Ctrl Pts',(-47.4097363271,4.57353025986597,132.618423013686));
#85027=CARTESIAN_POINT('Ctrl Pts',(-47.417482603184,4.62238000026643,132.490069373735));
#85028=CARTESIAN_POINT('Ctrl Pts',(-47.4252288792681,4.66577802717588,132.359898615695));
#85029=CARTESIAN_POINT('Ctrl Pts',(-47.4329752125335,4.7091763744397,132.229726896764));
#85030=CARTESIAN_POINT('Ctrl Pts',(-47.4407215457988,4.74712280425592,132.097738403872));
#85031=CARTESIAN_POINT('Ctrl Pts',(-47.4484678790641,4.77947916911898,131.964430414801));
#85032=CARTESIAN_POINT('Ctrl Pts',(-47.4562159470671,4.81184277996561,131.831092572331));
#85033=CARTESIAN_POINT('Ctrl Pts',(-47.4639640150702,4.83861374261053,131.696435025546));
#85034=CARTESIAN_POINT('Ctrl Pts',(-47.4717120830731,4.85970483226885,131.560966198911));
#85035=CARTESIAN_POINT('Ctrl Pts',(-47.479468385815,4.88081833778825,131.425353394395));
#85036=CARTESIAN_POINT('Ctrl Pts',(-47.4872246885568,4.89623985124863,131.288927974543));
#85037=CARTESIAN_POINT('Ctrl Pts',(-47.4949809912987,4.90593389042989,131.152205015582));
#85038=CARTESIAN_POINT('Ctrl Pts',(-47.5027414338128,4.91563310361174,131.015409083463));
#85039=CARTESIAN_POINT('Ctrl Pts',(-47.510501876327,4.91959874003263,130.878315686412));
#85040=CARTESIAN_POINT('Ctrl Pts',(-47.5182623188411,4.91784750104666,130.74143988212));
#85041=CARTESIAN_POINT('Ctrl Pts',(-47.5260352191065,4.91609345081641,130.604344352635));
#85042=CARTESIAN_POINT('Ctrl Pts',(-47.533808119372,4.90860420750972,130.467467504525));
#85043=CARTESIAN_POINT('Ctrl Pts',(-47.5415810196374,4.89544847654975,130.331320158465));
#85044=CARTESIAN_POINT('Ctrl Pts',(-47.5490713553995,4.88277098954736,130.200122111367));
#85045=CARTESIAN_POINT('Ctrl Pts',(-47.5565616911615,4.86483188641534,130.06960175382));
#85046=CARTESIAN_POINT('Ctrl Pts',(-47.5640520269236,4.84173715244562,129.94020530217));
#85047=CARTESIAN_POINT('Ctrl Pts',(-47.5718263610427,4.81776677461811,129.805902744727));
#85048=CARTESIAN_POINT('Ctrl Pts',(-47.5796006951618,4.78816616600944,129.672385571216));
#85049=CARTESIAN_POINT('Ctrl Pts',(-47.5873750292809,4.7529976862754,129.540162825778));
#85050=CARTESIAN_POINT('Ctrl Pts',(-47.595139782228,4.71787254854954,129.408103033058));
#85051=CARTESIAN_POINT('Ctrl Pts',(-47.6029045351751,4.67719329237095,129.277334868508));
#85052=CARTESIAN_POINT('Ctrl Pts',(-47.6106692881222,4.63107366648888,129.148359482888));
#85053=CARTESIAN_POINT('Ctrl Pts',(-47.6184263290072,4.58499984726946,129.019512197441));
#85054=CARTESIAN_POINT('Ctrl Pts',(-47.6261833698922,4.5334965422479,128.892454513178));
#85055=CARTESIAN_POINT('Ctrl Pts',(-47.6339404107772,4.47672781575351,128.767674307365));
#85056=CARTESIAN_POINT('Ctrl Pts',(-47.6416916020174,4.42000189899729,128.642988199277));
#85057=CARTESIAN_POINT('Ctrl Pts',(-47.6494427932575,4.3580186254431,128.520576505557));
#85058=CARTESIAN_POINT('Ctrl Pts',(-47.6571939844976,4.29099072955867,128.400908595715));
#85059=CARTESIAN_POINT('Ctrl Pts',(-47.6649418812747,4.22399132231802,128.281291547926));
#85060=CARTESIAN_POINT('Ctrl Pts',(-47.6726897780518,4.15195174785371,128.164416304957));
#85061=CARTESIAN_POINT('Ctrl Pts',(-47.6804376748289,4.07513128479229,128.050728820428));
#85062=CARTESIAN_POINT('Ctrl Pts',(-47.688183950913,3.99832689091568,127.937065116871));
#85063=CARTESIAN_POINT('Ctrl Pts',(-47.695930226997,3.91674381636887,127.82658816917));
#85064=CARTESIAN_POINT('Ctrl Pts',(-47.7036765030811,3.83068516460228,127.719715705717));
#85065=CARTESIAN_POINT('Ctrl Pts',(-47.7114228363465,3.74462587757039,127.612842453356));
#85066=CARTESIAN_POINT('Ctrl Pts',(-47.7191691696119,3.6540911926013,127.509574042847));
#85067=CARTESIAN_POINT('Ctrl Pts',(-47.7269155028772,3.55942481147405,127.410295492386));
#85068=CARTESIAN_POINT('Ctrl Pts',(-47.7346635708802,3.46473723046698,127.310994709182));
#85069=CARTESIAN_POINT('Ctrl Pts',(-47.7424116388831,3.36591638188401,127.215685846886));
#85070=CARTESIAN_POINT('Ctrl Pts',(-47.7501597068861,3.26334287049806,127.124717106019));
#85071=CARTESIAN_POINT('Ctrl Pts',(-47.7579160096279,3.16066034276356,127.033651682492));
#85072=CARTESIAN_POINT('Ctrl Pts',(-47.7656723123699,3.05421747798942,126.946935854651));
#85073=CARTESIAN_POINT('Ctrl Pts',(-47.7734286151118,2.94442844538828,126.864877885977));
#85074=CARTESIAN_POINT('Ctrl Pts',(-47.781189057626,2.83458081507476,126.782776120494));
#85075=CARTESIAN_POINT('Ctrl Pts',(-47.7889495001401,2.72138378080093,126.705337388462));
#85076=CARTESIAN_POINT('Ctrl Pts',(-47.7967099426542,2.60527970267697,126.632826039821));
#85077=CARTESIAN_POINT('Ctrl Pts',(-47.8044828429197,2.48898924397957,126.560198289526));
#85078=CARTESIAN_POINT('Ctrl Pts',(-47.8122557431851,2.36978275616859,126.49251392222));
#85079=CARTESIAN_POINT('Ctrl Pts',(-47.8200286434506,2.24812714410402,126.429991245137));
#85080=CARTESIAN_POINT('Ctrl Pts',(-47.8275189792126,2.13089401997065,126.369741424851));
#85081=CARTESIAN_POINT('Ctrl Pts',(-47.8350093149745,2.01138702320944,126.314284658988));
#85082=CARTESIAN_POINT('Ctrl Pts',(-47.8424996507365,1.89003885590877,126.263772969953));
#85083=CARTESIAN_POINT('Ctrl Pts',(-47.8502739848556,1.76408973596122,126.211346114876));
#85084=CARTESIAN_POINT('Ctrl Pts',(-47.8580483189747,1.63575810449533,126.16408065161));
#85085=CARTESIAN_POINT('Ctrl Pts',(-47.8658226530938,1.50550594168224,126.122199266004));
#85086=CARTESIAN_POINT('Ctrl Pts',(-47.8735874060409,1.37541430301884,126.080369495463));
#85087=CARTESIAN_POINT('Ctrl Pts',(-47.881352158988,1.24340721102521,126.043910718653));
#85088=CARTESIAN_POINT('Ctrl Pts',(-47.8891169119351,1.10996778200734,126.012998119757));
#85089=CARTESIAN_POINT('Ctrl Pts',(-47.8968739528201,0.976660886911533,
125.982116223691));
#85090=CARTESIAN_POINT('Ctrl Pts',(-47.9046309937051,0.841924864278071,
125.956769630954));
#85091=CARTESIAN_POINT('Ctrl Pts',(-47.9123880345901,0.706258859845322,
125.93708401916));
#85092=CARTESIAN_POINT('Ctrl Pts',(-47.9201392258302,0.570695162202028,
125.917413252439));
#85093=CARTESIAN_POINT('Ctrl Pts',(-47.9278904170704,0.434203264015171,
125.903395025411));
#85094=CARTESIAN_POINT('Ctrl Pts',(-47.9356416083105,0.297293047320565,
125.895104064226));
#85095=CARTESIAN_POINT('Ctrl Pts',(-47.9433895050876,0.160441021120067,
125.88681662692));
#85096=CARTESIAN_POINT('Ctrl Pts',(-47.9511374018646,0.0231714194688175,
125.884251637523));
#85097=CARTESIAN_POINT('Ctrl Pts',(-47.9588852986417,-0.114000417790578,
125.887432006406));
#85098=CARTESIAN_POINT('Ctrl Pts',(-47.9666315747258,-0.251143561658701,
125.890611710025));
#85099=CARTESIAN_POINT('Ctrl Pts',(-47.9743778508099,-0.388188591199009,
125.899534372412));
#85100=CARTESIAN_POINT('Ctrl Pts',(-47.982124126894,-0.524620224866981,
125.914170776449));
#85101=CARTESIAN_POINT('Ctrl Pts',(-47.9898704601594,-0.661052865642094,
125.928807288529));
#85102=CARTESIAN_POINT('Ctrl Pts',(-47.9976167934247,-0.796871712775053,
125.949157584718));
#85103=CARTESIAN_POINT('Ctrl Pts',(-48.0053631266901,-0.931567060346423,
125.975140610714));
#85104=CARTESIAN_POINT('Ctrl Pts',(-48.0131111946931,-1.06629257200715,
126.001129455429));
#85105=CARTESIAN_POINT('Ctrl Pts',(-48.0208592626961,-1.19989369963706,
126.032753465974));
#85106=CARTESIAN_POINT('Ctrl Pts',(-48.0286073306991,-1.33187176609815,
126.069880639662));
#85107=CARTESIAN_POINT('Ctrl Pts',(-48.0363636334409,-1.46399010041865,
126.107047272553));
#85108=CARTESIAN_POINT('Ctrl Pts',(-48.0441199361827,-1.59448155072266,
126.149728646206));
#85109=CARTESIAN_POINT('Ctrl Pts',(-48.0518762389246,-1.72286289763792,
126.197742932274));
#85110=CARTESIAN_POINT('Ctrl Pts',(-48.0596366814387,-1.85131276554368,
126.245782845013));
#85111=CARTESIAN_POINT('Ctrl Pts',(-48.067397123953,-1.97764992599705,126.299161189645));
#85112=CARTESIAN_POINT('Ctrl Pts',(-48.0751575664671,-2.10141286746253,
126.35764868368));
#85113=CARTESIAN_POINT('Ctrl Pts',(-48.0829304667326,-2.2253744841888,126.416230067033));
#85114=CARTESIAN_POINT('Ctrl Pts',(-48.090703366998,-2.34675327776635,126.47993680752));
#85115=CARTESIAN_POINT('Ctrl Pts',(-48.0984762672634,-2.46511320665511,
126.548494085252));
#85116=CARTESIAN_POINT('Ctrl Pts',(-48.1059666030254,-2.57917045399778,
126.614559133252));
#85117=CARTESIAN_POINT('Ctrl Pts',(-48.1134569387875,-2.69042425260649,
126.685128017685));
#85118=CARTESIAN_POINT('Ctrl Pts',(-48.1209472745495,-2.79851281567694,
126.759918865854));
#85119=CARTESIAN_POINT('Ctrl Pts',(-48.1286799548003,-2.91009850736653,
126.837129518747));
#85120=CARTESIAN_POINT('Ctrl Pts',(-48.136412635051,-3.01867289244847,126.919090705006));
#85121=CARTESIAN_POINT('Ctrl Pts',(-48.1441453153018,-3.12380140471801,
127.005538715136));
#85122=CARTESIAN_POINT('Ctrl Pts',(-48.1518657761139,-3.22876378941267,
127.091850117243));
#85123=CARTESIAN_POINT('Ctrl Pts',(-48.1595862369259,-3.33029084180872,
127.182633975219));
#85124=CARTESIAN_POINT('Ctrl Pts',(-48.1673066977379,-3.42797673765221,
127.277583257338));
#85125=CARTESIAN_POINT('Ctrl Pts',(-48.175020103386,-3.52557336550705,127.37244577226));
#85126=CARTESIAN_POINT('Ctrl Pts',(-48.1827335090342,-3.61933553607707,
127.471465867113));
#85127=CARTESIAN_POINT('Ctrl Pts',(-48.1904469146823,-3.7088901410447,127.574296069579));
#85128=CARTESIAN_POINT('Ctrl Pts',(-48.1981549902434,-3.79838286234331,
127.677055214726));
#85129=CARTESIAN_POINT('Ctrl Pts',(-48.2058630658044,-3.88367354310419,
127.783618932773));
#85130=CARTESIAN_POINT('Ctrl Pts',(-48.2135711413654,-3.96442596832126,
127.893603017868));
#85131=CARTESIAN_POINT('Ctrl Pts',(-48.2212756076997,-4.04514058204955,
128.003535604051));
#85132=CARTESIAN_POINT('Ctrl Pts',(-48.228980074034,-4.12132093532961,128.116885051816));
#85133=CARTESIAN_POINT('Ctrl Pts',(-48.2366845403683,-4.19267145129361,
128.233234567757));
#85134=CARTESIAN_POINT('Ctrl Pts',(-48.244388596637,-4.264018169669,128.349577891064));
#85135=CARTESIAN_POINT('Ctrl Pts',(-48.2520926529056,-4.330535347054,128.468920632802));
#85136=CARTESIAN_POINT('Ctrl Pts',(-48.2597967091743,-4.39197116966303,
128.590817686573));
#85137=CARTESIAN_POINT('Ctrl Pts',(-48.2675004098361,-4.45340415649271,
128.712709113771));
#85138=CARTESIAN_POINT('Ctrl Pts',(-48.2752041104979,-4.50975608213834,
128.837154262443));
#85139=CARTESIAN_POINT('Ctrl Pts',(-48.2829078111596,-4.56082183334964,
128.963684853902));
#85140=CARTESIAN_POINT('Ctrl Pts',(-48.2906154750572,-4.61191385578068,
129.090280540124));
#85141=CARTESIAN_POINT('Ctrl Pts',(-48.2983231389547,-4.65771412821306,
129.218963443053));
#85142=CARTESIAN_POINT('Ctrl Pts',(-48.3060308028522,-4.69806627517386,
129.349246760655));
#85143=CARTESIAN_POINT('Ctrl Pts',(-48.3105992201464,-4.72198343716756,
129.426467118105));
#85144=CARTESIAN_POINT('Ctrl Pts',(-48.3151676374405,-4.74398758183023,
129.504249399838));
#85145=CARTESIAN_POINT('Ctrl Pts',(-48.3197360547346,-4.76405452823404,
129.582490119308));
#85146=CARTESIAN_POINT('Origin',(213.235140564004,0.,130.804360617566));
#85147=CARTESIAN_POINT('',(-50.4153787949643,-4.76405452823401,129.582490119308));
#85148=CARTESIAN_POINT('',(-50.0699315015413,-4.76405452823402,129.582490119308));
#85149=CARTESIAN_POINT('',(213.235140564004,-4.76405452823405,129.582490119308));
#85150=CARTESIAN_POINT('',(-48.7351405639799,-4.91824799118596,130.799915429687));
#85151=CARTESIAN_POINT('Ctrl Pts',(-48.7351405640085,-4.91824799118642,
130.799915430193));
#85152=CARTESIAN_POINT('Ctrl Pts',(-48.7428228016083,-4.91837074863296,
130.93573682854));
#85153=CARTESIAN_POINT('Ctrl Pts',(-48.7505050392081,-4.91286304742632,
131.071680793918));
#85154=CARTESIAN_POINT('Ctrl Pts',(-48.7581872768079,-4.90172128579977,
131.207239630221));
#85155=CARTESIAN_POINT('Ctrl Pts',(-48.7658661433431,-4.89058441332145,
131.342738981563));
#85156=CARTESIAN_POINT('Ctrl Pts',(-48.7735450098783,-4.87381842854621,
131.477853143451));
#85157=CARTESIAN_POINT('Ctrl Pts',(-48.7812238764135,-4.85147180124849,
131.612076176529));
#85158=CARTESIAN_POINT('Ctrl Pts',(-48.7889011370898,-4.82912984723533,
131.746271139938));
#85159=CARTESIAN_POINT('Ctrl Pts',(-48.7965783977663,-4.80120963665041,
131.879574952118));
#85160=CARTESIAN_POINT('Ctrl Pts',(-48.8042556584427,-4.76781124290074,
132.011489034334));
#85161=CARTESIAN_POINT('Ctrl Pts',(-48.8119330489346,-4.73441228441417,
132.143405347099));
#85162=CARTESIAN_POINT('Ctrl Pts',(-48.8196104394266,-4.69553505633905,
132.273931496716));
#85163=CARTESIAN_POINT('Ctrl Pts',(-48.8272878299186,-4.65133014834854,
132.402581789233));
#85164=CARTESIAN_POINT('Ctrl Pts',(-48.8349670857104,-4.60711450032767,
132.531263338642));
#85165=CARTESIAN_POINT('Ctrl Pts',(-48.8426463415022,-4.55756872745563,
132.65806774763));
#85166=CARTESIAN_POINT('Ctrl Pts',(-48.850325597294,-4.50289224223815,132.782527576468));
#85167=CARTESIAN_POINT('Ctrl Pts',(-48.8580130609432,-4.4481573168793,132.907120432328));
#85168=CARTESIAN_POINT('Ctrl Pts',(-48.8657005245923,-4.38828088881619,
133.029363338446));
#85169=CARTESIAN_POINT('Ctrl Pts',(-48.8733879882415,-4.32350937127147,
133.148811465638));
#85170=CARTESIAN_POINT('Ctrl Pts',(-48.8810798149675,-4.25870109217349,
133.268327386498));
#85171=CARTESIAN_POINT('Ctrl Pts',(-48.8887716416935,-4.18899239512965,
133.38504502804));
#85172=CARTESIAN_POINT('Ctrl Pts',(-48.8964634684195,-4.11467339318653,
133.498548051636));
#85173=CARTESIAN_POINT('Ctrl Pts',(-48.9041672321142,-4.04023905536352,
133.612227220913));
#85174=CARTESIAN_POINT('Ctrl Pts',(-48.911870995809,-3.96118035448186,133.722681484809));
#85175=CARTESIAN_POINT('Ctrl Pts',(-48.9195747595037,-3.87782846972253,
133.829526633161));
#85176=CARTESIAN_POINT('Ctrl Pts',(-48.9252835562787,-3.81606139199834,
133.908703158104));
#85177=CARTESIAN_POINT('Ctrl Pts',(-48.9309923530537,-3.75193760199575,
133.985898461072));
#85178=CARTESIAN_POINT('Ctrl Pts',(-48.9367011498286,-3.68560453527068,
134.060969631877));
#85179=CARTESIAN_POINT('Ctrl Pts',(-48.9444754839477,-3.59527106498049,
134.163202797211));
#85180=CARTESIAN_POINT('Ctrl Pts',(-48.9522498180668,-3.50053759630902,
134.261836470801));
#85181=CARTESIAN_POINT('Ctrl Pts',(-48.9600241521859,-3.40172218214453,
134.356468338062));
#85182=CARTESIAN_POINT('Ctrl Pts',(-48.967788905133,-3.30302854914647,134.450983580004));
#85183=CARTESIAN_POINT('Ctrl Pts',(-48.9755536580801,-3.20026325977176,
134.541506560748));
#85184=CARTESIAN_POINT('Ctrl Pts',(-48.9833184110272,-3.09378415015764,
134.627668438646));
#85185=CARTESIAN_POINT('Ctrl Pts',(-48.9910754519122,-2.98741079709658,
134.713744739352));
#85186=CARTESIAN_POINT('Ctrl Pts',(-48.9988324927972,-2.8773312662722,134.795468312768));
#85187=CARTESIAN_POINT('Ctrl Pts',(-49.0065895336822,-2.76393946160558,
134.872507826687));
#85188=CARTESIAN_POINT('Ctrl Pts',(-49.0143407249223,-2.65063316658077,
134.949489244509));
#85189=CARTESIAN_POINT('Ctrl Pts',(-49.0220919161624,-2.53401989153566,
135.021793414811));
#85190=CARTESIAN_POINT('Ctrl Pts',(-49.0298431074025,-2.41452548011929,
135.089130129261));
#85191=CARTESIAN_POINT('Ctrl Pts',(-49.0375910041796,-2.29508185701555,
135.156438223812));
#85192=CARTESIAN_POINT('Ctrl Pts',(-49.0453389009567,-2.17275987299166,
135.218782870194));
#85193=CARTESIAN_POINT('Ctrl Pts',(-49.0530867977338,-2.04801294261065,
135.275918069886));
#85194=CARTESIAN_POINT('Ctrl Pts',(-49.0608330738179,-1.92329210659824,
135.333041318126));
#85195=CARTESIAN_POINT('Ctrl Pts',(-49.068579349902,-1.79614768840098,135.384957124457));
#85196=CARTESIAN_POINT('Ctrl Pts',(-49.0763256259861,-1.66705584930732,
135.431466393079));
#85197=CARTESIAN_POINT('Ctrl Pts',(-49.0840719592515,-1.53796305728667,
135.477976005023));
#85198=CARTESIAN_POINT('Ctrl Pts',(-49.0918182925168,-1.40692318350586,
135.519078867102));
#85199=CARTESIAN_POINT('Ctrl Pts',(-49.0995646257822,-1.27443004738224,
135.554624938299));
#85200=CARTESIAN_POINT('Ctrl Pts',(-49.1073126937851,-1.14190724033979,
135.590178969792));
#85201=CARTESIAN_POINT('Ctrl Pts',(-49.115060761788,-1.00793090088994,135.620173632892));
#85202=CARTESIAN_POINT('Ctrl Pts',(-49.122808829791,-0.873007213927309,
135.644509527148));
#85203=CARTESIAN_POINT('Ctrl Pts',(-49.1305651325329,-0.737940128464558,
135.668871285883));
#85204=CARTESIAN_POINT('Ctrl Pts',(-49.1383214352748,-0.601924069563516,
135.687562192238));
#85205=CARTESIAN_POINT('Ctrl Pts',(-49.1460777380166,-0.465473113648684,
135.700534413804));
#85206=CARTESIAN_POINT('Ctrl Pts',(-49.1538381805308,-0.328949329750221,
135.713513559035));
#85207=CARTESIAN_POINT('Ctrl Pts',(-49.161598623045,-0.19199057655083,135.720767916972));
#85208=CARTESIAN_POINT('Ctrl Pts',(-49.1693590655591,-0.0551121642013376,
135.722301824195));
#85209=CARTESIAN_POINT('Ctrl Pts',(-49.1771319658246,0.0819859775273392,
135.723838193781));
#85210=CARTESIAN_POINT('Ctrl Pts',(-49.18490486609,0.219003129676087,135.719635774135));
#85211=CARTESIAN_POINT('Ctrl Pts',(-49.1926777663554,0.355426969933536,
135.709750992607));
#85212=CARTESIAN_POINT('Ctrl Pts',(-49.2001681021175,0.48689145996634,135.700225547785));
#85213=CARTESIAN_POINT('Ctrl Pts',(-49.2076584378794,0.617804719885413,
135.685423739369));
#85214=CARTESIAN_POINT('Ctrl Pts',(-49.2151487736414,0.747718118489417,
135.665440814167));
#85215=CARTESIAN_POINT('Ctrl Pts',(-49.2229231077605,0.882557223088012,
135.644700230282));
#85216=CARTESIAN_POINT('Ctrl Pts',(-49.2306974418796,1.01674627994064,135.618312189934));
#85217=CARTESIAN_POINT('Ctrl Pts',(-49.2384717759986,1.14977489503716,135.586326819166));
#85218=CARTESIAN_POINT('Ctrl Pts',(-49.2462365289457,1.28263956425468,135.554380867508));
#85219=CARTESIAN_POINT('Ctrl Pts',(-49.2540012818929,1.41434626078754,135.516851401332));
#85220=CARTESIAN_POINT('Ctrl Pts',(-49.26176603484,1.54439124853745,135.473840110394));
#85221=CARTESIAN_POINT('Ctrl Pts',(-49.2695230757249,1.67430707377222,135.430871538876));
#85222=CARTESIAN_POINT('Ctrl Pts',(-49.2772801166099,1.80256410587156,135.38243209962));
#85223=CARTESIAN_POINT('Ctrl Pts',(-49.2850371574949,1.92867067097503,135.328674101999));
#85224=CARTESIAN_POINT('Ctrl Pts',(-49.2927883487351,2.05468213813697,135.274956643702));
#85225=CARTESIAN_POINT('Ctrl Pts',(-49.3005395399752,2.1785460079716,135.215928762922));
#85226=CARTESIAN_POINT('Ctrl Pts',(-49.3082907312154,2.29978794109783,135.151791869292));
#85227=CARTESIAN_POINT('Ctrl Pts',(-49.3160386279924,2.42097834316809,135.087682235552));
#85228=CARTESIAN_POINT('Ctrl Pts',(-49.3237865247695,2.53954868010703,135.018468090276));
#85229=CARTESIAN_POINT('Ctrl Pts',(-49.3315344215465,2.65504690474479,134.944397935768));
#85230=CARTESIAN_POINT('Ctrl Pts',(-49.3392806976306,2.77052096964366,134.87034327514));
#85231=CARTESIAN_POINT('Ctrl Pts',(-49.3470269737147,2.88292387155265,134.791434836629));
#85232=CARTESIAN_POINT('Ctrl Pts',(-49.3547732497987,2.99183072872938,134.707965612072));
#85233=CARTESIAN_POINT('Ctrl Pts',(-49.3625195830641,3.10073838983164,134.624495771363));
#85234=CARTESIAN_POINT('Ctrl Pts',(-49.3702659163295,3.20614964439734,134.536465315257));
#85235=CARTESIAN_POINT('Ctrl Pts',(-49.3780122495948,3.30767133721131,134.444208607179));
#85236=CARTESIAN_POINT('Ctrl Pts',(-49.3857603175978,3.40921576510476,134.351931238851));
#85237=CARTESIAN_POINT('Ctrl Pts',(-49.3935083856007,3.5068686086908,134.255425998131));
#85238=CARTESIAN_POINT('Ctrl Pts',(-49.4012564536037,3.60027263425461,134.155065024334));
#85239=CARTESIAN_POINT('Ctrl Pts',(-49.4090127563455,3.69377593072818,134.054597385701));
#85240=CARTESIAN_POINT('Ctrl Pts',(-49.4167690590874,3.78302112181224,133.950266114609));
#85241=CARTESIAN_POINT('Ctrl Pts',(-49.4245253618292,3.86769009387992,133.842477863527));
#85242=CARTESIAN_POINT('Ctrl Pts',(-49.4322858043434,3.95240425632756,133.734632082609));
#85243=CARTESIAN_POINT('Ctrl Pts',(-49.4400462468576,4.03253710462189,133.623325962331));
#85244=CARTESIAN_POINT('Ctrl Pts',(-49.4478066893718,4.10781374952696,133.508995391745));
#85245=CARTESIAN_POINT('Ctrl Pts',(-49.4555795896372,4.18321123518507,133.394481287577));
#85246=CARTESIAN_POINT('Ctrl Pts',(-49.4633524899026,4.25373673808465,133.276933366479));
#85247=CARTESIAN_POINT('Ctrl Pts',(-49.4711253901681,4.31916080942989,133.156813160081));
#85248=CARTESIAN_POINT('Ctrl Pts',(-49.4786157259302,4.38220655098914,133.041059625749));
#85249=CARTESIAN_POINT('Ctrl Pts',(-49.4861060616922,4.44051518508065,132.922917853518));
#85250=CARTESIAN_POINT('Ctrl Pts',(-49.4935963974544,4.49392434941947,132.802816772751));
#85251=CARTESIAN_POINT('Ctrl Pts',(-49.5013707315734,4.54935853845701,132.678162023003));
#85252=CARTESIAN_POINT('Ctrl Pts',(-49.5091450656925,4.59968999574327,132.551001588669));
#85253=CARTESIAN_POINT('Ctrl Pts',(-49.5169193998116,4.64468501330742,132.421791973036));
#85254=CARTESIAN_POINT('Ctrl Pts',(-49.5246841527587,4.68962457853374,132.292741596706));
#85255=CARTESIAN_POINT('Ctrl Pts',(-49.5324489057057,4.72924066234118,132.161647429609));
#85256=CARTESIAN_POINT('Ctrl Pts',(-49.5402136586528,4.76334653753586,132.028988244988));
#85257=CARTESIAN_POINT('Ctrl Pts',(-49.5479706995379,4.79741853829448,131.896460819339));
#85258=CARTESIAN_POINT('Ctrl Pts',(-49.5557277404229,4.82599112487382,131.762371845689));
#85259=CARTESIAN_POINT('Ctrl Pts',(-49.5634847813079,4.84892667773223,131.627217310117));
#85260=CARTESIAN_POINT('Ctrl Pts',(-49.571235972548,4.87184493471168,131.492164695633));
#85261=CARTESIAN_POINT('Ctrl Pts',(-49.5789871637882,4.88913455404411,131.356048502538));
#85262=CARTESIAN_POINT('Ctrl Pts',(-49.5867383550283,4.90070859533483,131.219376672811));
#85263=CARTESIAN_POINT('Ctrl Pts',(-49.5944862518054,4.91227771734933,131.082762932257));
#85264=CARTESIAN_POINT('Ctrl Pts',(-49.6022341485824,4.91813606003942,130.945594413533));
#85265=CARTESIAN_POINT('Ctrl Pts',(-49.6099820453595,4.91824835289376,130.80838575829));
#85266=CARTESIAN_POINT('Ctrl Pts',(-49.6177283214436,4.91836062225885,130.671205804139));
#85267=CARTESIAN_POINT('Ctrl Pts',(-49.6254745975277,4.91272923221237,130.533986120887));
#85268=CARTESIAN_POINT('Ctrl Pts',(-49.6332208736118,4.90137102612259,130.397242542819));
#85269=CARTESIAN_POINT('Ctrl Pts',(-49.6409672068772,4.89001273618913,130.260497955341));
#85270=CARTESIAN_POINT('Ctrl Pts',(-49.6487135401425,4.87292757822051,130.124229869683));
#85271=CARTESIAN_POINT('Ctrl Pts',(-49.6564598734078,4.8501843516398,129.988949790063));
#85272=CARTESIAN_POINT('Ctrl Pts',(-49.6642079414108,4.82743603187119,129.853639415408));
#85273=CARTESIAN_POINT('Ctrl Pts',(-49.6719560094138,4.79902718694441,129.719317872546));
#85274=CARTESIAN_POINT('Ctrl Pts',(-49.6797040774168,4.76507781465651,129.586486862709));
#85275=CARTESIAN_POINT('Ctrl Pts',(-49.6874603801587,4.73109236057169,129.453514678495));
#85276=CARTESIAN_POINT('Ctrl Pts',(-49.6952166829005,4.69155471310247,129.322036571222));
#85277=CARTESIAN_POINT('Ctrl Pts',(-49.7029729856423,4.646635052302,129.192539984487));
#85278=CARTESIAN_POINT('Ctrl Pts',(-49.7107334281565,4.601691416526,129.062974281525));
#85279=CARTESIAN_POINT('Ctrl Pts',(-49.7184938706707,4.55136018703969,128.935392569961));
#85280=CARTESIAN_POINT('Ctrl Pts',(-49.7262543131849,4.49585950530076,128.810261730575));
#85281=CARTESIAN_POINT('Ctrl Pts',(-49.7340272134503,4.44026972894046,128.684930020058));
#85282=CARTESIAN_POINT('Ctrl Pts',(-49.7418001137157,4.3794940907885,128.562057394461));
#85283=CARTESIAN_POINT('Ctrl Pts',(-49.7495730139812,4.3137968677988,128.442086364676));
#85284=CARTESIAN_POINT('Ctrl Pts',(-49.7570633497432,4.25048790434618,128.326476584011));
#85285=CARTESIAN_POINT('Ctrl Pts',(-49.7645536855052,4.18260912641421,128.213561365101));
#85286=CARTESIAN_POINT('Ctrl Pts',(-49.7720440212672,4.11043364364238,128.103709154731));
#85287=CARTESIAN_POINT('Ctrl Pts',(-49.7798183553863,4.03552160550398,127.989691864416));
#85288=CARTESIAN_POINT('Ctrl Pts',(-49.7875926895054,3.95574331280614,127.878613263117));
#85289=CARTESIAN_POINT('Ctrl Pts',(-49.7953670236245,3.87135650982524,127.770916727145));
#85290=CARTESIAN_POINT('Ctrl Pts',(-49.8031317765716,3.78707370603716,127.663352917528));
#85291=CARTESIAN_POINT('Ctrl Pts',(-49.8108965295187,3.69819393145342,127.559163184767));
#85292=CARTESIAN_POINT('Ctrl Pts',(-49.8186612824657,3.6050190609536,127.458763416368));
#85293=CARTESIAN_POINT('Ctrl Pts',(-49.8264183233507,3.51193673304882,127.358463366436));
#85294=CARTESIAN_POINT('Ctrl Pts',(-49.8341753642357,3.41456806289036,127.261946074566));
#85295=CARTESIAN_POINT('Ctrl Pts',(-49.8419324051207,3.31325595089106,127.169595416568));
#85296=CARTESIAN_POINT('Ctrl Pts',(-49.8496835963609,3.21202023914311,127.07731440092));
#85297=CARTESIAN_POINT('Ctrl Pts',(-49.857434787601,3.10684729245172,126.989194027316));
#85298=CARTESIAN_POINT('Ctrl Pts',(-49.8651859788411,2.99811746338405,126.905581996222));
#85299=CARTESIAN_POINT('Ctrl Pts',(-49.8729338756182,2.88943384739435,126.822005502471));
#85300=CARTESIAN_POINT('Ctrl Pts',(-49.8806817723953,2.77719666509922,126.742933777951));
#85301=CARTESIAN_POINT('Ctrl Pts',(-49.8884296691724,2.66181983452268,126.668674673126));
#85302=CARTESIAN_POINT('Ctrl Pts',(-49.8961759452565,2.54646713829201,126.594431101704));
#85303=CARTESIAN_POINT('Ctrl Pts',(-49.9039222213406,2.42797642863396,126.524998359065));
#85304=CARTESIAN_POINT('Ctrl Pts',(-49.9116684974247,2.30679079579489,126.460641095436));
#85305=CARTESIAN_POINT('Ctrl Pts',(-49.9194148306901,2.18560426839068,126.396283356736));
#85306=CARTESIAN_POINT('Ctrl Pts',(-49.9271611639554,2.06172312340398,126.337001355181));
#85307=CARTESIAN_POINT('Ctrl Pts',(-49.9349074972207,1.93561489158732,126.28301368839));
#85308=CARTESIAN_POINT('Ctrl Pts',(-49.9426555652237,1.80947841870703,126.229013931437));
#85309=CARTESIAN_POINT('Ctrl Pts',(-49.9504036332267,1.68111422590616,126.180311022351));
#85310=CARTESIAN_POINT('Ctrl Pts',(-49.9581517012296,1.55100927038034,126.137075185359));
#85311=CARTESIAN_POINT('Ctrl Pts',(-49.9659080039715,1.42076603775934,126.093793396804));
#85312=CARTESIAN_POINT('Ctrl Pts',(-49.9736643067134,1.28877871823962,126.055990410872));
#85313=CARTESIAN_POINT('Ctrl Pts',(-49.9814206094553,1.15554939839926,126.023786525434));
#85314=CARTESIAN_POINT('Ctrl Pts',(-49.9891810519695,1.02224897005926,125.991565451813));
#85315=CARTESIAN_POINT('Ctrl Pts',(-49.9969414944835,0.887705603873172,
125.964949509178));
#85316=CARTESIAN_POINT('Ctrl Pts',(-50.0047019369977,0.752430010649473,
125.944007529407));
#85317=CARTESIAN_POINT('Ctrl Pts',(-50.0124748372631,0.616937261034513,
125.923031931712));
#85318=CARTESIAN_POINT('Ctrl Pts',(-50.0202477375286,0.48071032423789,125.907748541879));
#85319=CARTESIAN_POINT('Ctrl Pts',(-50.028020637794,0.344264345353241,125.898174204167));
#85320=CARTESIAN_POINT('Ctrl Pts',(-50.0355109735561,0.212778521487179,
125.888947917748));
#85321=CARTESIAN_POINT('Ctrl Pts',(-50.0430013093181,0.0810896123887326,
125.88502282212));
#85322=CARTESIAN_POINT('Ctrl Pts',(-50.0504916450801,-0.0503447747947326,
125.886368296898));
#85323=CARTESIAN_POINT('Ctrl Pts',(-50.0582659791992,-0.186762536716492,
125.88776478576));
#85324=CARTESIAN_POINT('Ctrl Pts',(-50.0660403133184,-0.323338225795499,
125.894843825598));
#85325=CARTESIAN_POINT('Ctrl Pts',(-50.0738146474374,-0.459559499906637,
125.907628224577));
#85326=CARTESIAN_POINT('Ctrl Pts',(-50.0815794003846,-0.595612893472248,
125.920396867927));
#85327=CARTESIAN_POINT('Ctrl Pts',(-50.0893441533316,-0.731312355623601,
125.938856843957));
#85328=CARTESIAN_POINT('Ctrl Pts',(-50.0971089062787,-0.866144817674582,
125.962978974139));
#85329=CARTESIAN_POINT('Ctrl Pts',(-50.1048659471638,-1.00084336222308,
125.98707714588));
#85330=CARTESIAN_POINT('Ctrl Pts',(-50.1126229880488,-1.134676237968,126.016826211887));
#85331=CARTESIAN_POINT('Ctrl Pts',(-50.1203800289338,-1.2671351332698,126.052145174582));
#85332=CARTESIAN_POINT('Ctrl Pts',(-50.1281312201739,-1.39949414028773,
126.087437502973));
#85333=CARTESIAN_POINT('Ctrl Pts',(-50.135882411414,-1.53048085297704,126.128291267284));
#85334=CARTESIAN_POINT('Ctrl Pts',(-50.1436336026541,-1.65959715123671,
126.174574406724));
#85335=CARTESIAN_POINT('Ctrl Pts',(-50.1513814994312,-1.78865857162569,
126.220837874594));
#85336=CARTESIAN_POINT('Ctrl Pts',(-50.1591293962082,-1.91585079146782,
126.272525996244));
#85337=CARTESIAN_POINT('Ctrl Pts',(-50.1668772929853,-2.04069107464674,
126.329456931412));
#85338=CARTESIAN_POINT('Ctrl Pts',(-50.1746235690694,-2.16550524392966,
126.386375957855));
#85339=CARTESIAN_POINT('Ctrl Pts',(-50.1823698451535,-2.28796809961651,
126.448535454336));
#85340=CARTESIAN_POINT('Ctrl Pts',(-50.1901161212376,-2.40761748287308,
126.515705686394));
#85341=CARTESIAN_POINT('Ctrl Pts',(-50.197862454503,-2.5272677493547,126.582876414288));
#85342=CARTESIAN_POINT('Ctrl Pts',(-50.2056087877684,-2.64410416104717,
126.655057760178));
#85343=CARTESIAN_POINT('Ctrl Pts',(-50.2133551210337,-2.75769009378995,
126.731974534554));
#85344=CARTESIAN_POINT('Ctrl Pts',(-50.2211031890367,-2.87130146331436,
126.808908533908));
#85345=CARTESIAN_POINT('Ctrl Pts',(-50.2288512570397,-2.98166058174492,
126.890579852778));
#85346=CARTESIAN_POINT('Ctrl Pts',(-50.2365993250426,-3.08836102236103,
126.976670810638));
#85347=CARTESIAN_POINT('Ctrl Pts',(-50.2443556277845,-3.19517486547518,
127.062853266992));
#85348=CARTESIAN_POINT('Ctrl Pts',(-50.2521119305263,-3.29832195834583,
127.153464499694));
#85349=CARTESIAN_POINT('Ctrl Pts',(-50.2598682332681,-3.39742970090696,
127.248147113023));
#85350=CARTESIAN_POINT('Ctrl Pts',(-50.2676286757823,-3.4965903402545,127.342880261314));
#85351=CARTESIAN_POINT('Ctrl Pts',(-50.2753891182965,-3.59170706242428,
127.441688838627));
#85352=CARTESIAN_POINT('Ctrl Pts',(-50.2831495608107,-3.68244590554037,
127.544180374808));
#85353=CARTESIAN_POINT('Ctrl Pts',(-50.2909224610761,-3.77333041070297,
127.646836439502));
#85354=CARTESIAN_POINT('Ctrl Pts',(-50.2986953613416,-3.85982274628432,
127.753186974054));
#85355=CARTESIAN_POINT('Ctrl Pts',(-50.306468261607,-3.94163029222587,127.862807677042));
#85356=CARTESIAN_POINT('Ctrl Pts',(-50.313958597369,-4.02046392781113,127.968443391357));
#85357=CARTESIAN_POINT('Ctrl Pts',(-50.321448933131,-4.09494729397454,128.077115390142));
#85358=CARTESIAN_POINT('Ctrl Pts',(-50.328939268893,-4.16485880467396,128.188422124476));
#85359=CARTESIAN_POINT('Ctrl Pts',(-50.336921665962,-4.23936299992356,128.30704091249));
#85360=CARTESIAN_POINT('Ctrl Pts',(-50.344904063031,-4.30890056710795,128.429011375594));
#85361=CARTESIAN_POINT('Ctrl Pts',(-50.3528864600999,-4.37316512444513,
128.553891809331));
#85362=CARTESIAN_POINT('Ctrl Pts',(-50.3608585126971,-4.43734640067066,
128.678610409209));
#85363=CARTESIAN_POINT('Ctrl Pts',(-50.3688305652943,-4.49626810400048,
128.806231154193));
#85364=CARTESIAN_POINT('Ctrl Pts',(-50.3768026178915,-4.54966723934897,
128.936283779292));
#85365=CARTESIAN_POINT('Ctrl Pts',(-50.3847625385116,-4.60298511117318,
129.066138488553));
#85366=CARTESIAN_POINT('Ctrl Pts',(-50.3927224591317,-4.65079702562367,
129.198417369794));
#85367=CARTESIAN_POINT('Ctrl Pts',(-50.4006823797517,-4.69288632300249,
129.33262659884));
#85368=CARTESIAN_POINT('Ctrl Pts',(-50.4055811848226,-4.71878950385977,
129.415223509437));
#85369=CARTESIAN_POINT('Ctrl Pts',(-50.4104799898935,-4.74252609117121,
129.49855106994));
#85370=CARTESIAN_POINT('Ctrl Pts',(-50.4153787949644,-4.76405452823401,
129.582490119308));
#85371=CARTESIAN_POINT('Ctrl Pts',(-48.6652562953714,-4.76405452823406,
129.582490119308));
#85372=CARTESIAN_POINT('Ctrl Pts',(-48.6750211380865,-4.80663816484833,
129.74852307217));
#85373=CARTESIAN_POINT('Ctrl Pts',(-48.6847859808016,-4.8405687531086,129.916903017672));
#85374=CARTESIAN_POINT('Ctrl Pts',(-48.6945508235167,-4.86562797313288,
130.086831879767));
#85375=CARTESIAN_POINT('Ctrl Pts',(-48.7041603425565,-4.8902885907148,130.254057782258));
#85376=CARTESIAN_POINT('Ctrl Pts',(-48.7137698615963,-4.90635781315228,
130.422783822178));
#85377=CARTESIAN_POINT('Ctrl Pts',(-48.723379380636,-4.91367303920693,130.592227814184));
#85378=CARTESIAN_POINT('Ctrl Pts',(-48.727299775084,-4.91665743119279,130.661355861357));
#85379=CARTESIAN_POINT('Ctrl Pts',(-48.731220169532,-4.91818534567931,130.73060314286));
#85380=CARTESIAN_POINT('Ctrl Pts',(-48.7351405639799,-4.91824799118596,
130.799915429687));
#85381=CARTESIAN_POINT('',(-48.3898594359496,-4.91824988988752,130.805401348769));
#85382=CARTESIAN_POINT('Ctrl Pts',(-48.3197360547346,-4.76405452823404,
129.582490119308));
#85383=CARTESIAN_POINT('Ctrl Pts',(-48.327452615951,-4.79794981633546,129.714647333183));
#85384=CARTESIAN_POINT('Ctrl Pts',(-48.3351691771674,-4.82631527570629,
129.848112744647));
#85385=CARTESIAN_POINT('Ctrl Pts',(-48.3428857383838,-4.84907548571991,
129.982381301348));
#85386=CARTESIAN_POINT('Ctrl Pts',(-48.3507146879782,-4.87216718835205,
130.118605421527));
#85387=CARTESIAN_POINT('Ctrl Pts',(-48.3585436375725,-4.88948903909917,
130.255655842828));
#85388=CARTESIAN_POINT('Ctrl Pts',(-48.3663725871668,-4.9010169722093,130.393002257232));
#85389=CARTESIAN_POINT('Ctrl Pts',(-48.374201536761,-4.91254490531941,130.530348671637));
#85390=CARTESIAN_POINT('Ctrl Pts',(-48.3820304863554,-4.91827896681453,
130.667990658427));
#85391=CARTESIAN_POINT('Ctrl Pts',(-48.3898594359497,-4.91824988988752,
130.805401348769));
#85392=CARTESIAN_POINT('Ctrl Pts',(-48.3898594359911,-4.91824988988736,
130.805401349497));
#85393=CARTESIAN_POINT('Ctrl Pts',(-48.3930379234482,-4.91823808489216,
130.861188929996));
#85394=CARTESIAN_POINT('Ctrl Pts',(-48.3962164109053,-4.91727711705718,
130.916965370821));
#85395=CARTESIAN_POINT('Ctrl Pts',(-48.3993948983624,-4.91536792460722,
130.972709149613));
#85396=CARTESIAN_POINT('Ctrl Pts',(-48.4071692324815,-4.91069818775784,
131.109054114708));
#85397=CARTESIAN_POINT('Ctrl Pts',(-48.4149435666005,-4.90034374655151,
131.245420595926));
#85398=CARTESIAN_POINT('Ctrl Pts',(-48.4227179007196,-4.88429409418772,
131.381295851351));
#85399=CARTESIAN_POINT('Ctrl Pts',(-48.4304826536667,-4.86826422158607,
131.517003652667));
#85400=CARTESIAN_POINT('Ctrl Pts',(-48.4382474066139,-4.84655314864596,
131.652221048201));
#85401=CARTESIAN_POINT('Ctrl Pts',(-48.446012159561,-4.81920235772692,131.786435817222));
#85402=CARTESIAN_POINT('Ctrl Pts',(-48.453769200446,-4.791878731999,131.920517282242));
#85403=CARTESIAN_POINT('Ctrl Pts',(-48.461526241331,-4.75892661298791,132.053597721868));
#85404=CARTESIAN_POINT('Ctrl Pts',(-48.469283282216,-4.72043917302311,132.185170914562));
#85405=CARTESIAN_POINT('Ctrl Pts',(-48.4770344734562,-4.68198075673611,
132.316644886887));
#85406=CARTESIAN_POINT('Ctrl Pts',(-48.4847856646964,-4.63799543736451,
132.446613500943));
#85407=CARTESIAN_POINT('Ctrl Pts',(-48.4925368559365,-4.58862719118,132.574581949169));
#85408=CARTESIAN_POINT('Ctrl Pts',(-48.5002847527136,-4.53927992781713,
132.702496007392));
#85409=CARTESIAN_POINT('Ctrl Pts',(-48.5080326494907,-4.48455442850029,
132.828411226618));
#85410=CARTESIAN_POINT('Ctrl Pts',(-48.5157805462678,-4.42464406546086,
132.951849373411));
#85411=CARTESIAN_POINT('Ctrl Pts',(-48.5235268223519,-4.36474623437785,
133.075261699606));
#85412=CARTESIAN_POINT('Ctrl Pts',(-48.5312730984361,-4.29966586742658,
133.196197632493));
#85413=CARTESIAN_POINT('Ctrl Pts',(-48.5390193745202,-4.22964372344691,
133.314200659323));
#85414=CARTESIAN_POINT('Ctrl Pts',(-48.5467657077855,-4.15962106257968,
133.432204557224));
#85415=CARTESIAN_POINT('Ctrl Pts',(-48.5545120410509,-4.08465675140677,
133.547275169641));
#85416=CARTESIAN_POINT('Ctrl Pts',(-48.5622583743163,-4.00503637796646,
133.658982601939));
#85417=CARTESIAN_POINT('Ctrl Pts',(-48.5700064423192,-3.92539817409556,
133.770715050342));
#85418=CARTESIAN_POINT('Ctrl Pts',(-48.5777545103223,-3.8411020599975,133.879082501613));
#85419=CARTESIAN_POINT('Ctrl Pts',(-48.5855025783253,-3.75247537783706,
133.983686269528));
#85420=CARTESIAN_POINT('Ctrl Pts',(-48.5932588810671,-3.66375450218415,
134.088401211574));
#85421=CARTESIAN_POINT('Ctrl Pts',(-48.601015183809,-3.57069411745731,134.189344180888));
#85422=CARTESIAN_POINT('Ctrl Pts',(-48.6087714865509,-3.47366045782954,
134.286151261216));
#85423=CARTESIAN_POINT('Ctrl Pts',(-48.616531929065,-3.376575008416,134.383010010399));
#85424=CARTESIAN_POINT('Ctrl Pts',(-48.6242923715792,-3.2755123464647,134.475728207892));
#85425=CARTESIAN_POINT('Ctrl Pts',(-48.6320528140934,-3.17087284327355,
134.563981406195));
#85426=CARTESIAN_POINT('Ctrl Pts',(-48.6398257143588,-3.06606536346241,
134.652376276366));
#85427=CARTESIAN_POINT('Ctrl Pts',(-48.6475986146243,-2.95766987766794,
134.736291584703));
#85428=CARTESIAN_POINT('Ctrl Pts',(-48.6553715148898,-2.84611758719976,
134.815444977478));
#85429=CARTESIAN_POINT('Ctrl Pts',(-48.6628618506516,-2.73862050347623,
134.891720945048));
#85430=CARTESIAN_POINT('Ctrl Pts',(-48.6703521864134,-2.62819240412949,
134.963575033512));
#85431=CARTESIAN_POINT('Ctrl Pts',(-48.6778425221753,-2.51524003989757,
135.030795356704));
#85432=CARTESIAN_POINT('Ctrl Pts',(-48.6856168562944,-2.39800505244169,
135.100564358884));
#85433=CARTESIAN_POINT('Ctrl Pts',(-48.6933911904134,-2.27767924130043,
135.165562288279));
#85434=CARTESIAN_POINT('Ctrl Pts',(-48.7011655245325,-2.15468831158728,
135.22550315569));
#85435=CARTESIAN_POINT('Ctrl Pts',(-48.7089302774796,-2.03184895720299,
135.285370151339));
#85436=CARTESIAN_POINT('Ctrl Pts',(-48.7166950304267,-1.90635136753844,
135.34019231594));
#85437=CARTESIAN_POINT('Ctrl Pts',(-48.7244597833738,-1.77864891062985,
135.389727681958));
#85438=CARTESIAN_POINT('Ctrl Pts',(-48.7322168242588,-1.65107328960193,
135.439213848753));
#85439=CARTESIAN_POINT('Ctrl Pts',(-48.7399738651438,-1.52129752148494,
135.483423526065));
#85440=CARTESIAN_POINT('Ctrl Pts',(-48.7477309060287,-1.38979786671721,
135.522161477307));
#85441=CARTESIAN_POINT('Ctrl Pts',(-48.7554820972689,-1.25839737686206,
135.560870215957));
#85442=CARTESIAN_POINT('Ctrl Pts',(-48.763233288509,-1.12527596143351,135.594115331598));
#85443=CARTESIAN_POINT('Ctrl Pts',(-48.7709844797491,-0.990927738736999,
135.621750499971));
#85444=CARTESIAN_POINT('Ctrl Pts',(-48.7787323765262,-0.85663661761881,
135.649373922661));
#85445=CARTESIAN_POINT('Ctrl Pts',(-48.7864802733034,-0.721120108454675,
135.671392061821));
#85446=CARTESIAN_POINT('Ctrl Pts',(-48.7942281700805,-0.584885084992501,
135.687709110133));
#85447=CARTESIAN_POINT('Ctrl Pts',(-48.8019744461645,-0.448678558960533,
135.70402274527));
#85448=CARTESIAN_POINT('Ctrl Pts',(-48.8097207222486,-0.311754205525746,
135.714637615132));
#85449=CARTESIAN_POINT('Ctrl Pts',(-48.8174669983327,-0.174626237827864,
135.719509520658));
#85450=CARTESIAN_POINT('Ctrl Pts',(-48.825213331598,-0.0374972578822876,
135.724381462146));
#85451=CARTESIAN_POINT('Ctrl Pts',(-48.8329596648634,0.0998349486068893,
135.723510340824));
#85452=CARTESIAN_POINT('Ctrl Pts',(-48.8407059981288,0.23685433179815,135.716904061446));
#85453=CARTESIAN_POINT('Ctrl Pts',(-48.8484540661317,0.373904399530065,
135.710296302637));
#85454=CARTESIAN_POINT('Ctrl Pts',(-48.8562021341346,0.51064111412667,135.697950848891));
#85455=CARTESIAN_POINT('Ctrl Pts',(-48.8639502021375,0.646552113141298,
135.679927602799));
#85456=CARTESIAN_POINT('Ctrl Pts',(-48.8717065048794,0.782607559983041,
135.661885201387));
#85457=CARTESIAN_POINT('Ctrl Pts',(-48.8794628076213,0.917835149991321,
135.638153004693));
#85458=CARTESIAN_POINT('Ctrl Pts',(-48.8872191103631,1.05173075159825,135.608842430274));
#85459=CARTESIAN_POINT('Ctrl Pts',(-48.8949795528773,1.18569781731946,135.579516211919));
#85460=CARTESIAN_POINT('Ctrl Pts',(-48.9027399953915,1.31833110016377,135.54460578269));
#85461=CARTESIAN_POINT('Ctrl Pts',(-48.9105004379057,1.44914122279315,135.504272614498));
#85462=CARTESIAN_POINT('Ctrl Pts',(-48.9182733381712,1.58016133344414,135.463874699923));
#85463=CARTESIAN_POINT('Ctrl Pts',(-48.9260462384365,1.70935206673169,135.418036781706));
#85464=CARTESIAN_POINT('Ctrl Pts',(-48.933819138702,1.83624279562809,135.366969022635));
#85465=CARTESIAN_POINT('Ctrl Pts',(-48.9413094744641,1.95852072691203,135.317757705237));
#85466=CARTESIAN_POINT('Ctrl Pts',(-48.9487998102262,2.07866269160748,135.263690307716));
#85467=CARTESIAN_POINT('Ctrl Pts',(-48.9562901459883,2.19627056517438,135.204994511342));
#85468=CARTESIAN_POINT('Ctrl Pts',(-48.9640644801074,2.31833757701233,135.144073246008));
#85469=CARTESIAN_POINT('Ctrl Pts',(-48.9718388142264,2.43806121589239,135.077972701792));
#85470=CARTESIAN_POINT('Ctrl Pts',(-48.9796131483455,2.55497076698948,135.006896452313));
#85471=CARTESIAN_POINT('Ctrl Pts',(-48.9873779012926,2.67173623751335,134.935907797959));
#85472=CARTESIAN_POINT('Ctrl Pts',(-48.9951426542397,2.78569418989876,134.85995584057));
#85473=CARTESIAN_POINT('Ctrl Pts',(-49.0029074071868,2.89639599350979,134.779291222153));
#85474=CARTESIAN_POINT('Ctrl Pts',(-49.0106644480718,3.00698784652871,134.698706720972));
#85475=CARTESIAN_POINT('Ctrl Pts',(-49.0184214889568,3.11432967275093,134.613419102283));
#85476=CARTESIAN_POINT('Ctrl Pts',(-49.0261785298418,3.21799978370546,134.523723527336));
#85477=CARTESIAN_POINT('Ctrl Pts',(-49.0339297210819,3.32159171622301,134.43409559252));
#85478=CARTESIAN_POINT('Ctrl Pts',(-49.041680912322,3.42151715027272,134.340066572586));
#85479=CARTESIAN_POINT('Ctrl Pts',(-49.0494321035622,3.51738589609908,134.241973091424));
#85480=CARTESIAN_POINT('Ctrl Pts',(-49.0571800003393,3.61321389515108,134.143921302608));
#85481=CARTESIAN_POINT('Ctrl Pts',(-49.0649278971164,3.70498836259032,134.04180876746));
#85482=CARTESIAN_POINT('Ctrl Pts',(-49.0726757938935,3.79235471536453,133.936010147024));
#85483=CARTESIAN_POINT('Ctrl Pts',(-49.0804220699776,3.87970279298113,133.830233657378));
#85484=CARTESIAN_POINT('Ctrl Pts',(-49.0881683460616,3.96264434121974,133.720772917377));
#85485=CARTESIAN_POINT('Ctrl Pts',(-49.0959146221457,4.04086422939547,133.608036658426));
#85486=CARTESIAN_POINT('Ctrl Pts',(-49.1036609554111,4.11908469497254,133.495299567282));
#85487=CARTESIAN_POINT('Ctrl Pts',(-49.1114072886765,4.19258320806575,133.37928723016));
#85488=CARTESIAN_POINT('Ctrl Pts',(-49.1191536219418,4.26108748162426,133.260438087119));
#85489=CARTESIAN_POINT('Ctrl Pts',(-49.1269016899448,4.32960709623995,133.141562328636));
#85490=CARTESIAN_POINT('Ctrl Pts',(-49.1346497579477,4.39313005058105,133.019848838757));
#85491=CARTESIAN_POINT('Ctrl Pts',(-49.1423978259507,4.4514297979772,132.895761061331));
#85492=CARTESIAN_POINT('Ctrl Pts',(-49.1501541286925,4.50979150703867,132.771541401939));
#85493=CARTESIAN_POINT('Ctrl Pts',(-49.1579104314345,4.56291875334618,132.644942768616));
#85494=CARTESIAN_POINT('Ctrl Pts',(-49.1656667341763,4.61063278021964,132.51644952544));
#85495=CARTESIAN_POINT('Ctrl Pts',(-49.1734271766905,4.65837227350588,132.387887701551));
#85496=CARTESIAN_POINT('Ctrl Pts',(-49.1811876192046,4.70069266980552,132.257429624591));
#85497=CARTESIAN_POINT('Ctrl Pts',(-49.1889480617188,4.73746529960663,132.125574301087));
#85498=CARTESIAN_POINT('Ctrl Pts',(-49.1967209619842,4.77429696009762,131.993507311713));
#85499=CARTESIAN_POINT('Ctrl Pts',(-49.2044938622497,4.80556296830533,131.860038974476));
#85500=CARTESIAN_POINT('Ctrl Pts',(-49.2122667625151,4.83118575473103,131.725678839346));
#85501=CARTESIAN_POINT('Ctrl Pts',(-49.2197570982771,4.85587708833012,131.596203033561));
#85502=CARTESIAN_POINT('Ctrl Pts',(-49.2272474340391,4.87532832207602,131.465899447038));
#85503=CARTESIAN_POINT('Ctrl Pts',(-49.2347377698011,4.88951581462955,131.335226100516));
#85504=CARTESIAN_POINT('Ctrl Pts',(-49.2425121039201,4.90424123027552,131.199598234342));
#85505=CARTESIAN_POINT('Ctrl Pts',(-49.2502864380392,4.91334252158849,131.063142387458));
#85506=CARTESIAN_POINT('Ctrl Pts',(-49.2580607721582,4.91673652796036,130.926364622092));
#85507=CARTESIAN_POINT('Ctrl Pts',(-49.2658255251053,4.92012635152271,130.789755423098));
#85508=CARTESIAN_POINT('Ctrl Pts',(-49.2735902780525,4.91782287554224,130.6528254821));
#85509=CARTESIAN_POINT('Ctrl Pts',(-49.2813550309996,4.90979447642093,130.516087722887));
#85510=CARTESIAN_POINT('Ctrl Pts',(-49.2891120718846,4.90177405121882,130.379485773544));
#85511=CARTESIAN_POINT('Ctrl Pts',(-49.2968691127695,4.88804004118779,130.243076013898));
#85512=CARTESIAN_POINT('Ctrl Pts',(-49.3046261536545,4.86861284092837,130.107372764266));
#85513=CARTESIAN_POINT('Ctrl Pts',(-49.3123773448947,4.84920029087179,129.971771849511));
#85514=CARTESIAN_POINT('Ctrl Pts',(-49.3201285361348,4.82410315127968,129.836876769749));
#85515=CARTESIAN_POINT('Ctrl Pts',(-49.3278797273749,4.79339372626994,129.703197756107));
#85516=CARTESIAN_POINT('Ctrl Pts',(-49.335627624152,4.76269735358503,129.569575559612));
#85517=CARTESIAN_POINT('Ctrl Pts',(-49.3433755209291,4.72639352715479,129.437168781483));
#85518=CARTESIAN_POINT('Ctrl Pts',(-49.3511234177061,4.68460579912524,129.306478255929));
#85519=CARTESIAN_POINT('Ctrl Pts',(-49.3588696937902,4.64282681218755,129.175815068017));
#85520=CARTESIAN_POINT('Ctrl Pts',(-49.3666159698744,4.59556632431853,129.046867790759));
#85521=CARTESIAN_POINT('Ctrl Pts',(-49.3743622459585,4.54299787699253,128.920122481835));
#85522=CARTESIAN_POINT('Ctrl Pts',(-49.3821085792239,4.4904290416182,128.793376237307));
#85523=CARTESIAN_POINT('Ctrl Pts',(-49.3898549124891,4.43255231838501,128.668832354682));
#85524=CARTESIAN_POINT('Ctrl Pts',(-49.3976012457545,4.36958940153057,128.54695690433));
#85525=CARTESIAN_POINT('Ctrl Pts',(-49.4053493137575,4.30661238456745,128.425054160816));
#85526=CARTESIAN_POINT('Ctrl Pts',(-49.4130973817605,4.2385470868824,128.305821385968));
#85527=CARTESIAN_POINT('Ctrl Pts',(-49.4208454497634,4.16566096290401,128.189699682638));
#85528=CARTESIAN_POINT('Ctrl Pts',(-49.4286017525053,4.09269737468571,128.07345456378));
#85529=CARTESIAN_POINT('Ctrl Pts',(-49.4363580552471,4.01490293334614,127.960327453165));
#85530=CARTESIAN_POINT('Ctrl Pts',(-49.444114357989,3.93258852574926,127.850730554466));
#85531=CARTESIAN_POINT('Ctrl Pts',(-49.4518748005031,3.8502301844746,127.741075160603));
#85532=CARTESIAN_POINT('Ctrl Pts',(-49.4596352430173,3.76334731749674,127.634954035408));
#85533=CARTESIAN_POINT('Ctrl Pts',(-49.4673956855314,3.67229020412545,127.532745157402));
#85534=CARTESIAN_POINT('Ctrl Pts',(-49.4751685857969,3.58108691779199,127.430372204632));
#85535=CARTESIAN_POINT('Ctrl Pts',(-49.4829414860623,3.48569626680652,127.331924330005));
#85536=CARTESIAN_POINT('Ctrl Pts',(-49.4907143863278,3.38650502177914,127.237742219144));
#85537=CARTESIAN_POINT('Ctrl Pts',(-49.4982047220898,3.29091962835577,127.146983865242));
#85538=CARTESIAN_POINT('Ctrl Pts',(-49.5056950578519,3.19180539758634,127.060186720045));
#85539=CARTESIAN_POINT('Ctrl Pts',(-49.513185393614,3.08953489656831,126.977618245079));
#85540=CARTESIAN_POINT('Ctrl Pts',(-49.520959727733,2.98338677842018,126.891919161289));
#85541=CARTESIAN_POINT('Ctrl Pts',(-49.5287340618521,2.87350208007221,126.810504268785));
#85542=CARTESIAN_POINT('Ctrl Pts',(-49.5365083959712,2.76026161566952,126.733717071938));
#85543=CARTESIAN_POINT('Ctrl Pts',(-49.5442731489183,2.64716071001861,126.657024508449));
#85544=CARTESIAN_POINT('Ctrl Pts',(-49.5520379018654,2.53071258756723,126.58494851022));
#85545=CARTESIAN_POINT('Ctrl Pts',(-49.5598026548125,2.41133169229693,126.517792930917));
#85546=CARTESIAN_POINT('Ctrl Pts',(-49.5675596956975,2.29206936781495,126.450704051482));
#85547=CARTESIAN_POINT('Ctrl Pts',(-49.5753167365826,2.16988040580546,126.388526056006));
#85548=CARTESIAN_POINT('Ctrl Pts',(-49.5830737774675,2.04520854229898,126.331519788629));
#85549=CARTESIAN_POINT('Ctrl Pts',(-49.5908249687077,1.9206306948144,126.274556510122));
#85550=CARTESIAN_POINT('Ctrl Pts',(-49.5985761599478,1.79357402680211,126.222757358842));
#85551=CARTESIAN_POINT('Ctrl Pts',(-49.6063273511879,1.66450689230132,126.176337295673));
#85552=CARTESIAN_POINT('Ctrl Pts',(-49.614075247965,1.53549461477584,126.12993696227));
#85553=CARTESIAN_POINT('Ctrl Pts',(-49.621823144742,1.40447393742505,126.08891130183));
#85554=CARTESIAN_POINT('Ctrl Pts',(-49.6295710415191,1.27193300920695,126.053427079556));
#85555=CARTESIAN_POINT('Ctrl Pts',(-49.6373173176032,1.13941980569379,126.017950279816));
#85556=CARTESIAN_POINT('Ctrl Pts',(-49.6450635936874,1.00538736126562,125.988012713677));
#85557=CARTESIAN_POINT('Ctrl Pts',(-49.6528098697715,0.870338413419094,
125.963731101829));
#85558=CARTESIAN_POINT('Ctrl Pts',(-49.6605562030368,0.735288468671917,
125.939449310739));
#85559=CARTESIAN_POINT('Ctrl Pts',(-49.6683025363021,0.599222390328442,
125.920823626437));
#85560=CARTESIAN_POINT('Ctrl Pts',(-49.6760488695675,0.462652127740718,
125.9079194537));
#85561=CARTESIAN_POINT('Ctrl Pts',(-49.6837969375705,0.3260512811896,125.895012391164));
#85562=CARTESIAN_POINT('Ctrl Pts',(-49.6915450055734,0.188946414876321,
125.887829426588));
#85563=CARTESIAN_POINT('Ctrl Pts',(-49.6992930735764,0.0518532067744206,
125.886383969853));
#85564=CARTESIAN_POINT('Ctrl Pts',(-49.7070493763183,-0.0853857056206671,
125.88493697687));
#85565=CARTESIAN_POINT('Ctrl Pts',(-49.7148056790601,-0.222612543486195,
125.889239677051));
#85566=CARTESIAN_POINT('Ctrl Pts',(-49.722561981802,-0.359312466254466,
125.899253318628));
#85567=CARTESIAN_POINT('Ctrl Pts',(-49.7303224243162,-0.496085349887473,
125.909272304787));
#85568=CARTESIAN_POINT('Ctrl Pts',(-49.7380828668303,-0.63233036985443,
125.925008261105));
#85569=CARTESIAN_POINT('Ctrl Pts',(-49.7458433093445,-0.767540187597426,
125.946370794303));
#85570=CARTESIAN_POINT('Ctrl Pts',(-49.7536162096099,-0.902967056143042,
125.967767620536));
#85571=CARTESIAN_POINT('Ctrl Pts',(-49.7613891098753,-1.03735501815833,
125.994808995856));
#85572=CARTESIAN_POINT('Ctrl Pts',(-49.7691620101407,-1.17020838622026,
126.027353668092));
#85573=CARTESIAN_POINT('Ctrl Pts',(-49.7766523459027,-1.29823219971588,
126.058715259518));
#85574=CARTESIAN_POINT('Ctrl Pts',(-49.7841426816648,-1.42483075892259,
126.095186891809));
#85575=CARTESIAN_POINT('Ctrl Pts',(-49.7916330174268,-1.54957765926795,
126.1365996832));
#85576=CARTESIAN_POINT('Ctrl Pts',(-49.7994073543303,-1.67905442262962,
126.179582668558));
#85577=CARTESIAN_POINT('Ctrl Pts',(-49.8071816912339,-1.80694648626056,
126.228025058616));
#85578=CARTESIAN_POINT('Ctrl Pts',(-49.8149560281375,-1.93275901032833,
126.281792135996));
#85579=CARTESIAN_POINT('Ctrl Pts',(-49.8227207832134,-2.05841647114915,
126.335492945747));
#85580=CARTESIAN_POINT('Ctrl Pts',(-49.8304855382893,-2.18199913599579,
126.394505232937));
#85581=CARTESIAN_POINT('Ctrl Pts',(-49.8382502933652,-2.30302734669305,
126.458644554259));
#85582=CARTESIAN_POINT('Ctrl Pts',(-49.8460073357261,-2.42393534032146,
126.522720166127));
#85583=CARTESIAN_POINT('Ctrl Pts',(-49.853764378087,-2.54229358599368,126.591912495585));
#85584=CARTESIAN_POINT('Ctrl Pts',(-49.8615214204479,-2.6576427777372,126.665989207405));
#85585=CARTESIAN_POINT('Ctrl Pts',(-49.8692726125132,-2.77290497409687,
126.740010051196));
#85586=CARTESIAN_POINT('Ctrl Pts',(-49.8770238045784,-2.88516230599961,
126.818907734636));
#85587=CARTESIAN_POINT('Ctrl Pts',(-49.8847749966436,-2.99398076385158,
126.902404409689));
#85588=CARTESIAN_POINT('Ctrl Pts',(-49.8925228908177,-3.10275292283416,
126.985865559504));
#85589=CARTESIAN_POINT('Ctrl Pts',(-49.9002707849918,-3.20808880831806,
127.073921571624));
#85590=CARTESIAN_POINT('Ctrl Pts',(-49.9080186791658,-3.30958426000976,
127.166251893463));
#85591=CARTESIAN_POINT('Ctrl Pts',(-49.91576495172,-3.41105846889104,127.258562890736));
#85592=CARTESIAN_POINT('Ctrl Pts',(-49.9235112242741,-3.50869355375994,
127.355146155383));
#85593=CARTESIAN_POINT('Ctrl Pts',(-49.9312574968283,-3.60211957281576,
127.455641810972));
#85594=CARTESIAN_POINT('Ctrl Pts',(-49.9390038256361,-3.69554627033357,
127.556138196362));
#85595=CARTESIAN_POINT('Ctrl Pts',(-49.9467501544438,-3.78476357485034,
127.660546743044));
#85596=CARTESIAN_POINT('Ctrl Pts',(-49.9544964832516,-3.86943973891063,
127.768472087096));
#85597=CARTESIAN_POINT('Ctrl Pts',(-49.9622445458679,-3.95413485546566,
127.87642158735));
#85598=CARTESIAN_POINT('Ctrl Pts',(-49.9699926084842,-4.03428656774275,
127.987889143755));
#85599=CARTESIAN_POINT('Ctrl Pts',(-49.9777406711005,-4.10960485765943,
128.102448151108));
#85600=CARTESIAN_POINT('Ctrl Pts',(-49.9854969553295,-4.18500306920807,
128.217128719145));
#85601=CARTESIAN_POINT('Ctrl Pts',(-49.9932532395585,-4.25555739792462,
128.334906963841));
#85602=CARTESIAN_POINT('Ctrl Pts',(-50.0010095237875,-4.32102216451849,
128.455328792273));
#85603=CARTESIAN_POINT('Ctrl Pts',(-50.0087699474057,-4.38652186847922,
128.575814887666));
#85604=CARTESIAN_POINT('Ctrl Pts',(-50.0165303710239,-4.44692642594108,
128.69894702717));
#85605=CARTESIAN_POINT('Ctrl Pts',(-50.0242907946421,-4.50203765966367,
128.824249516271));
#85606=CARTESIAN_POINT('Ctrl Pts',(-50.0320636447594,-4.5572371411067,128.949752647933));
#85607=CARTESIAN_POINT('Ctrl Pts',(-50.0398364948765,-4.60712621879869,
129.077432709554));
#85608=CARTESIAN_POINT('Ctrl Pts',(-50.0476093449938,-4.65155580344958,
129.206796324683));
#85609=CARTESIAN_POINT('Ctrl Pts',(-50.055050063843,-4.69408692690964,129.330632276099));
#85610=CARTESIAN_POINT('Ctrl Pts',(-50.0624907826922,-4.73161543421519,
129.456010584061));
#85611=CARTESIAN_POINT('Ctrl Pts',(-50.0699315015413,-4.76405452823403,
129.582490119308));
#85612=CARTESIAN_POINT('Origin',(213.235140564004,0.,130.804360617566));
#85613=CARTESIAN_POINT('',(-52.1650248355919,-4.76405452823407,129.582490119308));
#85614=CARTESIAN_POINT('',(-51.8201183854057,-4.76405452823404,129.582490119308));
#85615=CARTESIAN_POINT('',(213.235140564004,-4.76405452823405,129.582490119308));
#85616=CARTESIAN_POINT('',(-50.4851405640431,-4.9182497302669,130.805989491289));
#85617=CARTESIAN_POINT('Ctrl Pts',(-50.4851405640431,-4.9182497302669,130.805989491289));
#85618=CARTESIAN_POINT('Ctrl Pts',(-50.4934943809599,-4.91820062086283,
130.954271282496));
#85619=CARTESIAN_POINT('Ctrl Pts',(-50.5018481978766,-4.91144143289579,
131.10235617592));
#85620=CARTESIAN_POINT('Ctrl Pts',(-50.5102020147934,-4.89805053678207,
131.249651535539));
#85621=CARTESIAN_POINT('Ctrl Pts',(-50.5185889108578,-4.88460661587328,
131.397530150094));
#85622=CARTESIAN_POINT('Ctrl Pts',(-50.5269758069222,-4.8644784451024,131.544612685482));
#85623=CARTESIAN_POINT('Ctrl Pts',(-50.5353627029866,-4.83779608759408,
131.690313255893));
#85624=CARTESIAN_POINT('Ctrl Pts',(-50.5437662021802,-4.81106090832361,
131.83630226262));
#85625=CARTESIAN_POINT('Ctrl Pts',(-50.5521697013737,-4.77774568641162,
131.980903561024));
#85626=CARTESIAN_POINT('Ctrl Pts',(-50.5605732005673,-4.73803057145959,
132.123545732102));
#85627=CARTESIAN_POINT('Ctrl Pts',(-50.569003845401,-4.69818716563829,132.266648677074));
#85628=CARTESIAN_POINT('Ctrl Pts',(-50.5774344902347,-4.65190258321221,
132.407779556749));
#85629=CARTESIAN_POINT('Ctrl Pts',(-50.5858651350684,-4.59940644198817,
132.546383419913));
#85630=CARTESIAN_POINT('Ctrl Pts',(-50.5930390542809,-4.55473570996948,
132.664326108343));
#85631=CARTESIAN_POINT('Ctrl Pts',(-50.6002129734934,-4.505568117783,132.78043930485));
#85632=CARTESIAN_POINT('Ctrl Pts',(-50.6073868927059,-4.45207105772289,
132.894395631504));
#85633=CARTESIAN_POINT('Ctrl Pts',(-50.615161226825,-4.39409660791693,133.017889433448));
#85634=CARTESIAN_POINT('Ctrl Pts',(-50.6229355609442,-4.33088813624253,
133.139164825681));
#85635=CARTESIAN_POINT('Ctrl Pts',(-50.6307098950633,-4.26263786183846,
133.257746343725));
#85636=CARTESIAN_POINT('Ctrl Pts',(-50.6384746480104,-4.19447169979789,
133.376181720646));
#85637=CARTESIAN_POINT('Ctrl Pts',(-50.6462394009575,-4.12127629133662,
133.491929493512));
#85638=CARTESIAN_POINT('Ctrl Pts',(-50.6540041539047,-4.04329144038476,
133.604535146164));
#85639=CARTESIAN_POINT('Ctrl Pts',(-50.6617611947897,-3.96538404508604,
133.717028957295));
#85640=CARTESIAN_POINT('Ctrl Pts',(-50.6695182356748,-3.88269689497874,
133.826386539409));
#85641=CARTESIAN_POINT('Ctrl Pts',(-50.6772752765598,-3.79551494695359,
133.932179242415));
#85642=CARTESIAN_POINT('Ctrl Pts',(-50.6850264678,-3.70839874351374,134.03789216632));
#85643=CARTESIAN_POINT('Ctrl Pts',(-50.6927776590402,-3.61679473650666,
134.140045261526));
#85644=CARTESIAN_POINT('Ctrl Pts',(-50.7005288502804,-3.52103008940392,
134.238240372597));
#85645=CARTESIAN_POINT('Ctrl Pts',(-50.7082767470575,-3.42530614483094,
134.336393748126));
#85646=CARTESIAN_POINT('Ctrl Pts',(-50.7160246438346,-3.3254253497384,134.430592206075));
#85647=CARTESIAN_POINT('Ctrl Pts',(-50.7237725406117,-3.22175374826125,
134.52047227467));
#85648=CARTESIAN_POINT('Ctrl Pts',(-50.7315188166958,-3.11810383264824,
134.610333542292));
#85649=CARTESIAN_POINT('Ctrl Pts',(-50.73926509278,-3.0106649830983,134.695877961358));
#85650=CARTESIAN_POINT('Ctrl Pts',(-50.7470113688641,-2.89983825104456,
134.776780683506));
#85651=CARTESIAN_POINT('Ctrl Pts',(-50.7547577021295,-2.78901070089305,
134.857684002858));
#85652=CARTESIAN_POINT('Ctrl Pts',(-50.7625040353948,-2.67479553411351,
134.933945326406));
#85653=CARTESIAN_POINT('Ctrl Pts',(-50.7702503686602,-2.55762453036736,
135.005281924156));
#85654=CARTESIAN_POINT('Ctrl Pts',(-50.7779984366632,-2.44042728698732,
135.076634497243));
#85655=CARTESIAN_POINT('Ctrl Pts',(-50.7857465046662,-2.32027322333718,
135.143059946699));
#85656=CARTESIAN_POINT('Ctrl Pts',(-50.7934945726692,-2.19762021331256,
135.204320669719));
#85657=CARTESIAN_POINT('Ctrl Pts',(-50.8012508754111,-2.07483684620931,
135.265646501364));
#85658=CARTESIAN_POINT('Ctrl Pts',(-50.809007178153,-1.949549577588,135.321796466466));
#85659=CARTESIAN_POINT('Ctrl Pts',(-50.8167634808949,-1.82223834237338,
135.37258023642));
#85660=CARTESIAN_POINT('Ctrl Pts',(-50.8245239234091,-1.69485915731925,
135.423391111201));
#85661=CARTESIAN_POINT('Ctrl Pts',(-50.8322843659232,-1.56545422188273,
135.468829954407));
#85662=CARTESIAN_POINT('Ctrl Pts',(-50.8400448084374,-1.43451931117596,
135.508756158798));
#85663=CARTESIAN_POINT('Ctrl Pts',(-50.8478177087029,-1.3033742121265,135.548746456277));
#85664=CARTESIAN_POINT('Ctrl Pts',(-50.8555906089684,-1.17069460846028,
135.583206332728));
#85665=CARTESIAN_POINT('Ctrl Pts',(-50.8633635092338,-1.03698804195296,
135.612046013195));
#85666=CARTESIAN_POINT('Ctrl Pts',(-50.8708538449955,-0.90814204593158,
135.639837298634));
#85667=CARTESIAN_POINT('Ctrl Pts',(-50.8783441807572,-0.778342759604827,
135.662409857694));
#85668=CARTESIAN_POINT('Ctrl Pts',(-50.8858345165188,-0.64804750448508,
135.67972906461));
#85669=CARTESIAN_POINT('Ctrl Pts',(-50.8936088506379,-0.51281206515897,
135.697704934521));
#85670=CARTESIAN_POINT('Ctrl Pts',(-50.901383184757,-0.376613920084245,
135.710078168962));
#85671=CARTESIAN_POINT('Ctrl Pts',(-50.909157518876,-0.239956990130485,
135.716753487175));
#85672=CARTESIAN_POINT('Ctrl Pts',(-50.9169222718231,-0.103468477629513,
135.723420578655));
#85673=CARTESIAN_POINT('Ctrl Pts',(-50.9246870247701,0.0334773079995623,
135.724403707046));
#85674=CARTESIAN_POINT('Ctrl Pts',(-50.9324517777172,0.170368349558318,
135.719658949099));
#85675=CARTESIAN_POINT('Ctrl Pts',(-50.9402088186022,0.307123429004959,
135.714918903712));
#85676=CARTESIAN_POINT('Ctrl Pts',(-50.9479658594872,0.443823484383001,
135.704462306846));
#85677=CARTESIAN_POINT('Ctrl Pts',(-50.9557229003722,0.57995385407072,135.688297204956));
#85678=CARTESIAN_POINT('Ctrl Pts',(-50.9634740916123,0.715981566787347,
135.672144293296));
#85679=CARTESIAN_POINT('Ctrl Pts',(-50.9712252828524,0.851440062248544,
135.650291491028));
#85680=CARTESIAN_POINT('Ctrl Pts',(-50.9789764740925,0.98581752116214,135.622798837308));
#85681=CARTESIAN_POINT('Ctrl Pts',(-50.9867243708696,1.12013786607125,135.595317868699));
#85682=CARTESIAN_POINT('Ctrl Pts',(-50.9944722676467,1.25337770605331,135.562201894464));
#85683=CARTESIAN_POINT('Ctrl Pts',(-51.0022201644237,1.38503338621548,135.523562412528));
#85684=CARTESIAN_POINT('Ctrl Pts',(-51.0099664405078,1.51666152684771,135.484931013138));
#85685=CARTESIAN_POINT('Ctrl Pts',(-51.0177127165919,1.64670579187263,135.440778514229));
#85686=CARTESIAN_POINT('Ctrl Pts',(-51.0254589926761,1.7746760990675,135.391266743257));
#85687=CARTESIAN_POINT('Ctrl Pts',(-51.0332053259414,1.90264735090993,135.341754606799));
#85688=CARTESIAN_POINT('Ctrl Pts',(-51.0409516592067,2.02854424974756,135.28688326041));
#85689=CARTESIAN_POINT('Ctrl Pts',(-51.048697992472,2.15189553937748,135.226863150082));
#85690=CARTESIAN_POINT('Ctrl Pts',(-51.056446060475,2.27527445267345,135.166829598665));
#85691=CARTESIAN_POINT('Ctrl Pts',(-51.064194128478,2.39610627089577,135.10164515994));
#85692=CARTESIAN_POINT('Ctrl Pts',(-51.0719421964809,2.51394360005048,135.031566626062));
#85693=CARTESIAN_POINT('Ctrl Pts',(-51.0796984992228,2.63190616812089,134.961413611884));
#85694=CARTESIAN_POINT('Ctrl Pts',(-51.0874548019646,2.74686755301205,134.886356312151));
#85695=CARTESIAN_POINT('Ctrl Pts',(-51.0952111047065,2.85840820932839,134.806695632447));
#85696=CARTESIAN_POINT('Ctrl Pts',(-51.1029715472206,2.97000839825158,134.72699243544));
#85697=CARTESIAN_POINT('Ctrl Pts',(-51.1107319897348,3.07818391242994,134.642681202978));
#85698=CARTESIAN_POINT('Ctrl Pts',(-51.1184924322489,3.18254847645298,134.554103043057));
#85699=CARTESIAN_POINT('Ctrl Pts',(-51.1262653325144,3.28708057573924,134.46538268961));
#85700=CARTESIAN_POINT('Ctrl Pts',(-51.1340382327799,3.38778921241254,134.372381986316));
#85701=CARTESIAN_POINT('Ctrl Pts',(-51.1418111330453,3.48432451753367,134.275479416889));
#85702=CARTESIAN_POINT('Ctrl Pts',(-51.1493014688075,3.57735052115772,134.182099499942));
#85703=CARTESIAN_POINT('Ctrl Pts',(-51.1567918045696,3.66650113917274,134.085096703779));
#85704=CARTESIAN_POINT('Ctrl Pts',(-51.1642821403318,3.75150004649306,133.98483706987));
#85705=CARTESIAN_POINT('Ctrl Pts',(-51.1720564744509,3.83972171321756,133.880776061471));
#85706=CARTESIAN_POINT('Ctrl Pts',(-51.1798308085699,3.92375009001871,133.772876740136));
#85707=CARTESIAN_POINT('Ctrl Pts',(-51.187605142689,4.00323263295736,133.661511567188));
#85708=CARTESIAN_POINT('Ctrl Pts',(-51.1953698956361,4.0826172207654,133.550283641863));
#85709=CARTESIAN_POINT('Ctrl Pts',(-51.2031346485832,4.15746689674329,133.435598678816));
#85710=CARTESIAN_POINT('Ctrl Pts',(-51.2108994015303,4.22746794921622,133.317863711029));
#85711=CARTESIAN_POINT('Ctrl Pts',(-51.2186564424153,4.297399475657,133.200245679272));
#85712=CARTESIAN_POINT('Ctrl Pts',(-51.2264134833002,4.36249176358301,133.079584005113));
#85713=CARTESIAN_POINT('Ctrl Pts',(-51.2341705241852,4.42247339552931,132.956316037257));
#85714=CARTESIAN_POINT('Ctrl Pts',(-51.2419217154253,4.48240979486037,132.833141026734));
#85715=CARTESIAN_POINT('Ctrl Pts',(-51.2496729066655,4.5372430389633,132.707363984707));
#85716=CARTESIAN_POINT('Ctrl Pts',(-51.2574240979056,4.58674698965109,132.579447971875));
#85717=CARTESIAN_POINT('Ctrl Pts',(-51.2651719946827,4.63622989983927,132.45158632676));
#85718=CARTESIAN_POINT('Ctrl Pts',(-51.2729198914598,4.68038788089619,132.321587882857));
#85719=CARTESIAN_POINT('Ctrl Pts',(-51.2806677882369,4.71904250141271,132.189936646646));
#85720=CARTESIAN_POINT('Ctrl Pts',(-51.2884140643209,4.75768903621591,132.058312949035));
#85721=CARTESIAN_POINT('Ctrl Pts',(-51.296160340405,4.7908343901741,131.92503752168));
#85722=CARTESIAN_POINT('Ctrl Pts',(-51.3039066164891,4.81834981189573,131.790610156326));
#85723=CARTESIAN_POINT('Ctrl Pts',(-51.3116529497545,4.84586543672995,131.65618179866));
#85724=CARTESIAN_POINT('Ctrl Pts',(-51.3193992830199,4.86775096800018,131.520601869052));
#85725=CARTESIAN_POINT('Ctrl Pts',(-51.3271456162852,4.88392873439036,131.384380599891));
#85726=CARTESIAN_POINT('Ctrl Pts',(-51.3348936842882,4.90011012367915,131.248128824921));
#85727=CARTESIAN_POINT('Ctrl Pts',(-51.3426417522911,4.9105811584907,131.111235812766));
#85728=CARTESIAN_POINT('Ctrl Pts',(-51.3503898202941,4.91531605795677,130.974216771097));
#85729=CARTESIAN_POINT('Ctrl Pts',(-51.3581461230359,4.92005598973034,130.83705210396));
#85730=CARTESIAN_POINT('Ctrl Pts',(-51.3659024257777,4.91904759435314,130.699761531093));
#85731=CARTESIAN_POINT('Ctrl Pts',(-51.3736587285196,4.91231725768135,130.562860674738));
#85732=CARTESIAN_POINT('Ctrl Pts',(-51.3814191710338,4.90558332882623,130.425886750274));
#85733=CARTESIAN_POINT('Ctrl Pts',(-51.3891796135479,4.89312140888488,130.289303345944));
#85734=CARTESIAN_POINT('Ctrl Pts',(-51.3969400560621,4.87500969038011,130.153619823394));
#85735=CARTESIAN_POINT('Ctrl Pts',(-51.4047129563275,4.85686889733693,130.017718489608));
#85736=CARTESIAN_POINT('Ctrl Pts',(-51.4124858565929,4.83306024980587,129.882720309559));
#85737=CARTESIAN_POINT('Ctrl Pts',(-51.4202587568583,4.80371306414723,129.749124217587));
#85738=CARTESIAN_POINT('Ctrl Pts',(-51.4277490926204,4.77543272260815,129.620384680065));
#85739=CARTESIAN_POINT('Ctrl Pts',(-51.4352394283825,4.74200960959721,129.492947359503));
#85740=CARTESIAN_POINT('Ctrl Pts',(-51.4427297641446,4.70360232571002,129.367242590376));
#85741=CARTESIAN_POINT('Ctrl Pts',(-51.4505040982636,4.6637388179809,129.236771686721));
#85742=CARTESIAN_POINT('Ctrl Pts',(-51.4582784323828,4.61837945324241,129.107754014742));
#85743=CARTESIAN_POINT('Ctrl Pts',(-51.4660527665019,4.56764703514317,128.980687504081));
#85744=CARTESIAN_POINT('Ctrl Pts',(-51.473817519449,4.51697714021509,128.853777591538));
#85745=CARTESIAN_POINT('Ctrl Pts',(-51.481582272396,4.46094751092773,128.728814415422));
#85746=CARTESIAN_POINT('Ctrl Pts',(-51.4893470253431,4.39973102683338,128.606281921518));
#85747=CARTESIAN_POINT('Ctrl Pts',(-51.4971040662281,4.33857534381411,128.483871128615));
#85748=CARTESIAN_POINT('Ctrl Pts',(-51.5048611071132,4.27224323161904,128.363886561065));
#85749=CARTESIAN_POINT('Ctrl Pts',(-51.5126181479982,4.20095593633078,128.246792967726));
#85750=CARTESIAN_POINT('Ctrl Pts',(-51.5203693392383,4.12972239934643,128.129787675577));
#85751=CARTESIAN_POINT('Ctrl Pts',(-51.5281205304784,4.05354131951291,128.015669350865));
#85752=CARTESIAN_POINT('Ctrl Pts',(-51.5358717217185,3.97268004969477,127.904878545668));
#85753=CARTESIAN_POINT('Ctrl Pts',(-51.5436196184956,3.89185314807334,127.794134829519));
#85754=CARTESIAN_POINT('Ctrl Pts',(-51.5513675152727,3.80635024285079,127.686716135119));
#85755=CARTESIAN_POINT('Ctrl Pts',(-51.5591154120498,3.71648209584986,127.58303419919));
#85756=CARTESIAN_POINT('Ctrl Pts',(-51.5668616881339,3.62663274732795,127.479373951287));
#85757=CARTESIAN_POINT('Ctrl Pts',(-51.574607964218,3.53242022917225,127.379449202358));
#85758=CARTESIAN_POINT('Ctrl Pts',(-51.5823542403021,3.4341954370614,127.283638424242));
#85759=CARTESIAN_POINT('Ctrl Pts',(-51.5901005735675,3.33596991987745,127.187826938872));
#85760=CARTESIAN_POINT('Ctrl Pts',(-51.5978469068328,3.23373234951027,127.096129757907));
#85761=CARTESIAN_POINT('Ctrl Pts',(-51.6055932400982,3.12787001567564,127.008888021494));
#85762=CARTESIAN_POINT('Ctrl Pts',(-51.6133413081011,3.02198397470535,126.921626747898));
#85763=CARTESIAN_POINT('Ctrl Pts',(-51.6210893761042,2.9124718566525,126.838823152889));
#85764=CARTESIAN_POINT('Ctrl Pts',(-51.6288374441072,2.79975318513301,126.76077740897));
#85765=CARTESIAN_POINT('Ctrl Pts',(-51.6365937468491,2.68691471486791,126.682648717106));
#85766=CARTESIAN_POINT('Ctrl Pts',(-51.6443500495908,2.57086320531068,126.609288200553));
#85767=CARTESIAN_POINT('Ctrl Pts',(-51.6521063523327,2.45204672625646,126.540952366559));
#85768=CARTESIAN_POINT('Ctrl Pts',(-51.6598667948469,2.33316683126987,126.472580059673));
#85769=CARTESIAN_POINT('Ctrl Pts',(-51.667627237361,2.21151937283599,126.409237959584));
#85770=CARTESIAN_POINT('Ctrl Pts',(-51.6753876798752,2.08757515630237,126.35113560312));
#85771=CARTESIAN_POINT('Ctrl Pts',(-51.6831605801407,1.96343197350912,126.292939975595));
#85772=CARTESIAN_POINT('Ctrl Pts',(-51.6909334804062,1.83698502573734,126.240001051229));
#85773=CARTESIAN_POINT('Ctrl Pts',(-51.6987063806716,1.70872397922919,126.192479718702));
#85774=CARTESIAN_POINT('Ctrl Pts',(-51.7061967164335,1.58512554483359,126.146685906312));
#85775=CARTESIAN_POINT('Ctrl Pts',(-51.7136870521954,1.45984290884758,126.105922733287));
#85776=CARTESIAN_POINT('Ctrl Pts',(-51.7211773879573,1.33332385134872,126.070289370751));
#85777=CARTESIAN_POINT('Ctrl Pts',(-51.7289517220764,1.20200778532849,126.033304958442));
#85778=CARTESIAN_POINT('Ctrl Pts',(-51.7367260561955,1.06894371931695,126.001729873504));
#85779=CARTESIAN_POINT('Ctrl Pts',(-51.7445003903146,0.934616953996705,
125.975729940883));
#85780=CARTESIAN_POINT('Ctrl Pts',(-51.7522651432617,0.800455734409594,
125.949762050856));
#85781=CARTESIAN_POINT('Ctrl Pts',(-51.7600298962088,0.665035291972695,
125.929355715731));
#85782=CARTESIAN_POINT('Ctrl Pts',(-51.7677946491559,0.528856229602482,
125.914627071563));
#85783=CARTESIAN_POINT('Ctrl Pts',(-51.7755516900409,0.392812422196804,
125.899913056092));
#85784=CARTESIAN_POINT('Ctrl Pts',(-51.7833087309258,0.25601188048422,125.890865551157));
#85785=CARTESIAN_POINT('Ctrl Pts',(-51.7910657718108,0.118965199753478,
125.887549624275));
#85786=CARTESIAN_POINT('Ctrl Pts',(-51.798816963051,-0.0179781330094434,
125.884236197959));
#85787=CARTESIAN_POINT('Ctrl Pts',(-51.8065681542912,-0.155166846065093,
125.886645755981));
#85788=CARTESIAN_POINT('Ctrl Pts',(-51.8143193455313,-0.292085779718963,
125.894791495964));
#85789=CARTESIAN_POINT('Ctrl Pts',(-51.8220672423084,-0.428946519173413,
125.902933773791));
#85790=CARTESIAN_POINT('Ctrl Pts',(-51.8298151390855,-0.565537317824866,
125.916807361352));
#85791=CARTESIAN_POINT('Ctrl Pts',(-51.8375630358625,-0.701343795552268,
125.93637335968));
#85792=CARTESIAN_POINT('Ctrl Pts',(-51.8453093119466,-0.837121865492178,
125.955935265223));
#85793=CARTESIAN_POINT('Ctrl Pts',(-51.8530555880307,-0.972115554113877,
125.981187157391));
#85794=CARTESIAN_POINT('Ctrl Pts',(-51.8608018641148,-1.105816774655,126.012038390984));
#85795=CARTESIAN_POINT('Ctrl Pts',(-51.8685481973802,-1.23951898214817,
126.042889852314));
#85796=CARTESIAN_POINT('Ctrl Pts',(-51.8762945306455,-1.37192832156811,
126.079340649642));
#85797=CARTESIAN_POINT('Ctrl Pts',(-51.8840408639108,-1.50254844249584,
126.121249339745));
#85798=CARTESIAN_POINT('Ctrl Pts',(-51.8917889319138,-1.633197814894,126.163167415008));
#85799=CARTESIAN_POINT('Ctrl Pts',(-51.8995369999168,-1.76205679928488,
126.210545695777));
#85800=CARTESIAN_POINT('Ctrl Pts',(-51.9072850679198,-1.88864608927655,
126.263193475524));
#85801=CARTESIAN_POINT('Ctrl Pts',(-51.9150413706616,-2.01536991987205,
126.315897209958));
#85802=CARTESIAN_POINT('Ctrl Pts',(-51.9227976734035,-2.13981887575725,
126.37388148057));
#85803=CARTESIAN_POINT('Ctrl Pts',(-51.9305539761453,-2.26153495745039,
126.436907961986));
#85804=CARTESIAN_POINT('Ctrl Pts',(-51.9383144186595,-2.38331600268113,
126.499968082533));
#85805=CARTESIAN_POINT('Ctrl Pts',(-51.9460748611737,-2.50236092811516,
126.568075582234));
#85806=CARTESIAN_POINT('Ctrl Pts',(-51.9538353036879,-2.61823896269446,
126.640947618988));
#85807=CARTESIAN_POINT('Ctrl Pts',(-51.9616082039533,-2.7343030149822,126.713936636405));
#85808=CARTESIAN_POINT('Ctrl Pts',(-51.9693811042187,-2.847189695269,126.791705253004));
#85809=CARTESIAN_POINT('Ctrl Pts',(-51.9771540044841,-2.95649896678588,
126.873928462968));
#85810=CARTESIAN_POINT('Ctrl Pts',(-51.9846443402462,-3.06183457095012,
126.953162652144));
#85811=CARTESIAN_POINT('Ctrl Pts',(-51.9921346760082,-3.16384810783968,
127.036532991273));
#85812=CARTESIAN_POINT('Ctrl Pts',(-51.9996250117703,-3.26221410591101,
127.12371635471));
#85813=CARTESIAN_POINT('Ctrl Pts',(-52.0072823682229,-3.36277348455108,
127.212843746561));
#85814=CARTESIAN_POINT('Ctrl Pts',(-52.0149397246753,-3.45985953892064,
127.306256855097));
#85815=CARTESIAN_POINT('Ctrl Pts',(-52.0225970811278,-3.55307652160224,
127.40365035438));
#85816=CARTESIAN_POINT('Ctrl Pts',(-52.0302456119749,-3.64618606559832,
127.500931601269));
#85817=CARTESIAN_POINT('Ctrl Pts',(-52.037894142822,-3.73543512631841,127.602183831351));
#85818=CARTESIAN_POINT('Ctrl Pts',(-52.045542673669,-3.82046084072659,127.707061467181));
#85819=CARTESIAN_POINT('Ctrl Pts',(-52.0531841627059,-3.90540827409576,
127.811842544807));
#85820=CARTESIAN_POINT('Ctrl Pts',(-52.0608256517427,-3.98613983993017,
127.920242080387));
#85821=CARTESIAN_POINT('Ctrl Pts',(-52.0684671407796,-4.0623298012738,128.031878039049));
#85822=CARTESIAN_POINT('Ctrl Pts',(-52.0761033649914,-4.13846726933831,
128.143437082885));
#85823=CARTESIAN_POINT('Ctrl Pts',(-52.0837395892031,-4.21006912986374,
128.258227782799));
#85824=CARTESIAN_POINT('Ctrl Pts',(-52.0913758134149,-4.27685056291799,
128.375835895648));
#85825=CARTESIAN_POINT('Ctrl Pts',(-52.099009006558,-4.34360548822308,128.493397325965));
#85826=CARTESIAN_POINT('Ctrl Pts',(-52.1066421997011,-4.40554359168371,
128.613773595245));
#85827=CARTESIAN_POINT('Ctrl Pts',(-52.1142753928442,-4.46242421877927,
128.736522820699));
#85828=CARTESIAN_POINT('Ctrl Pts',(-52.1219069216737,-4.51929244383109,
128.859245282361));
#85829=CARTESIAN_POINT('Ctrl Pts',(-52.1295384505033,-4.57110522009044,
128.984339303371));
#85830=CARTESIAN_POINT('Ctrl Pts',(-52.1371699793328,-4.61766885556299,
129.111340416014));
#85831=CARTESIAN_POINT('Ctrl Pts',(-52.1448027627309,-4.66424014576289,
129.238362406727));
#85832=CARTESIAN_POINT('Ctrl Pts',(-52.152435546129,-4.70556043530697,129.367291735476));
#85833=CARTESIAN_POINT('Ctrl Pts',(-52.1600683295271,-4.74148510574168,
129.497646396885));
#85834=CARTESIAN_POINT('Ctrl Pts',(-52.1617204982154,-4.74926124879883,
129.525862563742));
#85835=CARTESIAN_POINT('Ctrl Pts',(-52.1633726669036,-4.75678477467003,
129.554145460496));
#85836=CARTESIAN_POINT('Ctrl Pts',(-52.1650248355919,-4.76405452823407,
129.582490119308));
#85837=CARTESIAN_POINT('Ctrl Pts',(-50.4153787949644,-4.76405452823401,
129.582490119308));
#85838=CARTESIAN_POINT('Ctrl Pts',(-50.4233250152514,-4.79897522845777,
129.718645399485));
#85839=CARTESIAN_POINT('Ctrl Pts',(-50.4312712355385,-4.82808341113277,
129.856410290236));
#85840=CARTESIAN_POINT('Ctrl Pts',(-50.4392174558255,-4.85124139258481,
129.995262345802));
#85841=CARTESIAN_POINT('Ctrl Pts',(-50.4471566799911,-4.87437898496585,
130.133992151316));
#85842=CARTESIAN_POINT('Ctrl Pts',(-50.4550959041567,-4.89157675695739,
130.273806857429));
#85843=CARTESIAN_POINT('Ctrl Pts',(-50.4630351283223,-4.90274785718882,
130.414172827738));
#85844=CARTESIAN_POINT('Ctrl Pts',(-50.4704036068844,-4.91311587437202,
130.544447980763));
#85845=CARTESIAN_POINT('Ctrl Pts',(-50.4777720854464,-4.9182930471674,130.675197637016));
#85846=CARTESIAN_POINT('Ctrl Pts',(-50.4851405640085,-4.9182497302671,130.805989490675));
#85847=CARTESIAN_POINT('',(-50.139859435941,-4.91824790236153,130.799818215517));
#85848=CARTESIAN_POINT('Ctrl Pts',(-50.0699315015413,-4.76405452823403,
129.582490119308));
#85849=CARTESIAN_POINT('Ctrl Pts',(-50.0699812147741,-4.76427126162551,
129.583335159512));
#85850=CARTESIAN_POINT('Ctrl Pts',(-50.0700309280068,-4.76448776799205,
129.584180248854));
#85851=CARTESIAN_POINT('Ctrl Pts',(-50.0700806412396,-4.76470404731428,
129.585025387202));
#85852=CARTESIAN_POINT('Ctrl Pts',(-50.0802659710137,-4.80901571441495,
129.758178736929));
#85853=CARTESIAN_POINT('Ctrl Pts',(-50.0904513007877,-4.84390632131328,
129.933834040213));
#85854=CARTESIAN_POINT('Ctrl Pts',(-50.1006366305617,-4.8691456428026,130.111104696801));
#85855=CARTESIAN_POINT('Ctrl Pts',(-50.1106019485555,-4.89383977349548,
130.284546156533));
#85856=CARTESIAN_POINT('Ctrl Pts',(-50.1205672665494,-4.90929511545234,
130.459534200369));
#85857=CARTESIAN_POINT('Ctrl Pts',(-50.1305325845432,-4.91534060276653,
130.635216237539));
#85858=CARTESIAN_POINT('Ctrl Pts',(-50.1336415350092,-4.91722665603788,
130.690025000456));
#85859=CARTESIAN_POINT('Ctrl Pts',(-50.1367504854751,-4.918197181964,130.744901128459));
#85860=CARTESIAN_POINT('Ctrl Pts',(-50.139859435941,-4.91824790236153,130.799818215517));
#85861=CARTESIAN_POINT('Ctrl Pts',(-50.139859435991,-4.91824790236235,130.7998182164));
#85862=CARTESIAN_POINT('Ctrl Pts',(-50.1475248510763,-4.91837295833512,
130.935221553372));
#85863=CARTESIAN_POINT('Ctrl Pts',(-50.1551902661616,-4.9129021639932,131.070768982495));
#85864=CARTESIAN_POINT('Ctrl Pts',(-50.1628556812468,-4.90182667104543,
131.20595537541));
#85865=CARTESIAN_POINT('Ctrl Pts',(-50.1705920389054,-4.89064867562888,
131.342392903519));
#85866=CARTESIAN_POINT('Ctrl Pts',(-50.178328396564,-4.87376167017608,131.478462266883));
#85867=CARTESIAN_POINT('Ctrl Pts',(-50.1860647542226,-4.85121043588478,
131.613644479547));
#85868=CARTESIAN_POINT('Ctrl Pts',(-50.1937232281112,-4.82888623028358,
131.747465780419));
#85869=CARTESIAN_POINT('Ctrl Pts',(-50.2013817019996,-4.80101139998182,
131.880417309493));
#85870=CARTESIAN_POINT('Ctrl Pts',(-50.2090401758882,-4.76768135676842,
132.012001931377));
#85871=CARTESIAN_POINT('Ctrl Pts',(-50.2166980399471,-4.73435396756279,
132.143576075428));
#85872=CARTESIAN_POINT('Ctrl Pts',(-50.224355904006,-4.69557232760295,132.273783140227));
#85873=CARTESIAN_POINT('Ctrl Pts',(-50.2320137680649,-4.65148249520225,
132.402138342823));
#85874=CARTESIAN_POINT('Ctrl Pts',(-50.2396727720677,-4.60738609962224,
132.530512652278));
#85875=CARTESIAN_POINT('Ctrl Pts',(-50.2473317760705,-4.55798007063612,
132.657034172352));
#85876=CARTESIAN_POINT('Ctrl Pts',(-50.2549907800733,-4.50345947224149,
132.781235890409));
#85877=CARTESIAN_POINT('Ctrl Pts',(-50.2627855704882,-4.44797227865465,
132.907639579594));
#85878=CARTESIAN_POINT('Ctrl Pts',(-50.2705803609032,-4.38718761060133,
133.031640032764));
#85879=CARTESIAN_POINT('Ctrl Pts',(-50.2783751513181,-4.32136051551518,
133.152769942502));
#85880=CARTESIAN_POINT('Ctrl Pts',(-50.2860456817218,-4.25658279765894,
133.271968869732));
#85881=CARTESIAN_POINT('Ctrl Pts',(-50.2937162121256,-4.18692249311526,
133.38838778584));
#85882=CARTESIAN_POINT('Ctrl Pts',(-50.3013867425293,-4.11266659077473,
133.501610434625));
#85883=CARTESIAN_POINT('Ctrl Pts',(-50.3092436629499,-4.03660630749094,
133.617584336622));
#85884=CARTESIAN_POINT('Ctrl Pts',(-50.3171005833704,-3.95572449336865,
133.73020428153));
#85885=CARTESIAN_POINT('Ctrl Pts',(-50.324957503791,-3.87037285449671,133.8390594543));
#85886=CARTESIAN_POINT('Ctrl Pts',(-50.3328144242115,-3.78502121562477,
133.94791462707));
#85887=CARTESIAN_POINT('Ctrl Pts',(-50.3406713446321,-3.69520009384722,
134.053004736021));
#85888=CARTESIAN_POINT('Ctrl Pts',(-50.3485282650526,-3.60130018461268,
134.153960600073));
#85889=CARTESIAN_POINT('Ctrl Pts',(-50.3563025991717,-3.50838728374742,
134.253855288628));
#85890=CARTESIAN_POINT('Ctrl Pts',(-50.3640769332908,-3.41116767138523,
134.350039375797));
#85891=CARTESIAN_POINT('Ctrl Pts',(-50.3718512674099,-3.30996956334717,
134.442118794275));
#85892=CARTESIAN_POINT('Ctrl Pts',(-50.379616020357,-3.20889617293307,134.534084733099));
#85893=CARTESIAN_POINT('Ctrl Pts',(-50.387380773304,-3.10385432903034,134.621955807819));
#85894=CARTESIAN_POINT('Ctrl Pts',(-50.3951455262511,-2.99521116357081,
134.705372428381));
#85895=CARTESIAN_POINT('Ctrl Pts',(-50.402902567136,-2.88667590403512,134.788706198379));
#85896=CARTESIAN_POINT('Ctrl Pts',(-50.410659608021,-2.77454674919739,134.867594082073));
#85897=CARTESIAN_POINT('Ctrl Pts',(-50.418416648906,-2.65922592983904,134.941714907033));
#85898=CARTESIAN_POINT('Ctrl Pts',(-50.4261678401461,-2.54399207480686,
135.015779836903));
#85899=CARTESIAN_POINT('Ctrl Pts',(-50.4339190313863,-2.42557167351986,
135.085084652889));
#85900=CARTESIAN_POINT('Ctrl Pts',(-50.4416702226264,-2.30439783666213,
135.149350108104));
#85901=CARTESIAN_POINT('Ctrl Pts',(-50.4494181194035,-2.18327550191782,
135.213588248786));
#85902=CARTESIAN_POINT('Ctrl Pts',(-50.4571660161806,-2.05940240387961,
135.272791105901));
#85903=CARTESIAN_POINT('Ctrl Pts',(-50.4649139129577,-1.9332380869943,135.326724331543));
#85904=CARTESIAN_POINT('Ctrl Pts',(-50.4726601890417,-1.80710016096448,
135.380646275517));
#85905=CARTESIAN_POINT('Ctrl Pts',(-50.4804064651258,-1.67867232865637,
135.42930062696));
#85906=CARTESIAN_POINT('Ctrl Pts',(-50.4881527412099,-1.54843567694259,
135.47250050588));
#85907=CARTESIAN_POINT('Ctrl Pts',(-50.4958990744753,-1.41819806385125,
135.515700703693));
#85908=CARTESIAN_POINT('Ctrl Pts',(-50.5036454077406,-1.28615197579398,
135.55344622555));
#85909=CARTESIAN_POINT('Ctrl Pts',(-50.511391741006,-1.15279490021219,135.585599680878));
#85910=CARTESIAN_POINT('Ctrl Pts',(-50.5191398090089,-1.01940796023851,
135.61776033675));
#85911=CARTESIAN_POINT('Ctrl Pts',(-50.5268878770118,-0.884709828538143,
135.644326342531));
#85912=CARTESIAN_POINT('Ctrl Pts',(-50.5346359450147,-0.749209061726243,
135.665211247273));
#85913=CARTESIAN_POINT('Ctrl Pts',(-50.5423922477565,-0.613564283086526,
135.686118348741));
#85914=CARTESIAN_POINT('Ctrl Pts',(-50.5501485504984,-0.477115552294207,
135.701332228078));
#85915=CARTESIAN_POINT('Ctrl Pts',(-50.5579048532402,-0.340377998979923,
135.710818186965));
#85916=CARTESIAN_POINT('Ctrl Pts',(-50.5656652957544,-0.203567464716348,
135.720309208793));
#85917=CARTESIAN_POINT('Ctrl Pts',(-50.5734257382685,-0.0664681913946131,
135.724066207809));
#85918=CARTESIAN_POINT('Ctrl Pts',(-50.5811861807827,0.0704047893100568,
135.722106669178));
#85919=CARTESIAN_POINT('Ctrl Pts',(-50.5889590810481,0.207497490674553,
135.720143984921));
#85920=CARTESIAN_POINT('Ctrl Pts',(-50.5967319813135,0.344362782929777,
135.712446447024));
#85921=CARTESIAN_POINT('Ctrl Pts',(-50.6045048815789,0.480489950550833,
135.699083538214));
#85922=CARTESIAN_POINT('Ctrl Pts',(-50.6119952173411,0.611668552747988,
135.686206404798));
#85923=CARTESIAN_POINT('Ctrl Pts',(-50.6194855531033,0.742161458894984,
135.668068692674));
#85924=CARTESIAN_POINT('Ctrl Pts',(-50.6269758888655,0.87152261445422,135.644777066075));
#85925=CARTESIAN_POINT('Ctrl Pts',(-50.6347502229845,1.00578853754267,135.620602330375));
#85926=CARTESIAN_POINT('Ctrl Pts',(-50.6425245571037,1.1392605093561,135.590798565633));
#85927=CARTESIAN_POINT('Ctrl Pts',(-50.6502988912228,1.27142958124231,135.555428906114));
#85928=CARTESIAN_POINT('Ctrl Pts',(-50.6580636441699,1.40343576655988,135.520102836538));
#85929=CARTESIAN_POINT('Ctrl Pts',(-50.665828397117,1.53414187278016,135.479224620579));
#85930=CARTESIAN_POINT('Ctrl Pts',(-50.6735931500641,1.66304692282871,135.432908769521));
#85931=CARTESIAN_POINT('Ctrl Pts',(-50.6813501909492,1.79182394256414,135.38663892002));
#85932=CARTESIAN_POINT('Ctrl Pts',(-50.6891072318342,1.91880310043388,135.334942314472));
#85933=CARTESIAN_POINT('Ctrl Pts',(-50.6968642727192,2.04349676941535,135.277983759482));
#85934=CARTESIAN_POINT('Ctrl Pts',(-50.7046154639594,2.1680964059314,135.221068157382));
#85935=CARTESIAN_POINT('Ctrl Pts',(-50.7123666551995,2.29041362990957,135.158898665844));
#85936=CARTESIAN_POINT('Ctrl Pts',(-50.7201178464397,2.4099793961318,135.091688733388));
#85937=CARTESIAN_POINT('Ctrl Pts',(-50.7278657432168,2.5294943437137,135.024507366947));
#85938=CARTESIAN_POINT('Ctrl Pts',(-50.735613639994,2.64625981937454,134.952290011679));
#85939=CARTESIAN_POINT('Ctrl Pts',(-50.7433615367711,2.7598302645873,134.875296624576));
#85940=CARTESIAN_POINT('Ctrl Pts',(-50.7511078128552,2.87337695331105,134.798319342829));
#85941=CARTESIAN_POINT('Ctrl Pts',(-50.7588540889393,2.98372961752984,134.716568235646));
#85942=CARTESIAN_POINT('Ctrl Pts',(-50.7666003650234,3.09047099060843,134.630347041837));
#85943=CARTESIAN_POINT('Ctrl Pts',(-50.7743466982888,3.1972131516276,134.544125211563));
#85944=CARTESIAN_POINT('Ctrl Pts',(-50.7820930315542,3.30034366417484,134.45343347449));
#85945=CARTESIAN_POINT('Ctrl Pts',(-50.7898393648196,3.39947803355569,134.358616117931));
#85946=CARTESIAN_POINT('Ctrl Pts',(-50.7975874328226,3.49863460339162,134.263777527681));
#85947=CARTESIAN_POINT('Ctrl Pts',(-50.8053355008256,3.59379296681325,134.164811749667));
#85948=CARTESIAN_POINT('Ctrl Pts',(-50.8130835688286,3.68460550291662,134.06209991812));
#85949=CARTESIAN_POINT('Ctrl Pts',(-50.8208398715705,3.77551455566367,133.959278923218));
#85950=CARTESIAN_POINT('Ctrl Pts',(-50.8285961743123,3.86206829516841,133.852704214974));
#85951=CARTESIAN_POINT('Ctrl Pts',(-50.8363524770542,3.94395908860282,133.742790431247));
#85952=CARTESIAN_POINT('Ctrl Pts',(-50.8441129195684,4.02589358961959,133.632817983223));
#85953=CARTESIAN_POINT('Ctrl Pts',(-50.8518733620827,4.10315996536191,133.519503231461));
#85954=CARTESIAN_POINT('Ctrl Pts',(-50.8596338045969,4.1754945393934,133.403288937854));
#85955=CARTESIAN_POINT('Ctrl Pts',(-50.8674067048623,4.24794523130448,133.286888086746));
#85956=CARTESIAN_POINT('Ctrl Pts',(-50.8751796051278,4.31544810825091,133.167578732889));
#85957=CARTESIAN_POINT('Ctrl Pts',(-50.8829525053933,4.37778557380154,133.045828112828));
#85958=CARTESIAN_POINT('Ctrl Pts',(-50.890442841155,4.43785691545828,132.928503434482));
#85959=CARTESIAN_POINT('Ctrl Pts',(-50.8979331769167,4.4931317477964,132.808912180355));
#85960=CARTESIAN_POINT('Ctrl Pts',(-50.9054235126785,4.54345870708427,132.687487283385));
#85961=CARTESIAN_POINT('Ctrl Pts',(-50.9131978467976,4.59569382833208,132.561458524536));
#85962=CARTESIAN_POINT('Ctrl Pts',(-50.9209721809166,4.64276393796802,132.433055111687));
#85963=CARTESIAN_POINT('Ctrl Pts',(-50.9287465150357,4.68444705345657,132.302739363365));
#85964=CARTESIAN_POINT('Ctrl Pts',(-50.9365112679828,4.72607879823062,132.172584217556));
#85965=CARTESIAN_POINT('Ctrl Pts',(-50.9442760209298,4.76233664049947,132.040521794372));
#85966=CARTESIAN_POINT('Ctrl Pts',(-50.9520407738769,4.79304613150344,131.907035476162));
#85967=CARTESIAN_POINT('Ctrl Pts',(-50.9597978147619,4.82372512140802,131.773681738445));
#85968=CARTESIAN_POINT('Ctrl Pts',(-50.9675548556469,4.84886663950332,131.638907298634));
#85969=CARTESIAN_POINT('Ctrl Pts',(-50.9753118965319,4.86834576793745,131.503211493151));
#85970=CARTESIAN_POINT('Ctrl Pts',(-50.9830630877721,4.88781020700935,131.367618016929));
#85971=CARTESIAN_POINT('Ctrl Pts',(-50.9908142790122,4.90162070037098,131.231104943442));
#85972=CARTESIAN_POINT('Ctrl Pts',(-50.9985654702523,4.90970329791155,131.094182267855));
#85973=CARTESIAN_POINT('Ctrl Pts',(-51.0063133670294,4.91778246013251,130.957317788059));
#85974=CARTESIAN_POINT('Ctrl Pts',(-51.0140612638065,4.92013854559381,130.820044441887));
#85975=CARTESIAN_POINT('Ctrl Pts',(-51.0218091605836,4.91674942820777,130.68287760345));
#85976=CARTESIAN_POINT('Ctrl Pts',(-51.0295554366676,4.91336101975203,130.54573945736));
#85977=CARTESIAN_POINT('Ctrl Pts',(-51.0373017127517,4.9042298084914,130.408708165289));
#85978=CARTESIAN_POINT('Ctrl Pts',(-51.0450479888358,4.88938579568122,130.272298963722));
#85979=CARTESIAN_POINT('Ctrl Pts',(-51.0527943221011,4.87454167329593,130.135888755214));
#85980=CARTESIAN_POINT('Ctrl Pts',(-51.0605406553664,4.85398470750775,130.000101035044));
#85981=CARTESIAN_POINT('Ctrl Pts',(-51.0682869886317,4.82779672820983,129.865445385191));
#85982=CARTESIAN_POINT('Ctrl Pts',(-51.0760350566347,4.80160288429546,129.730759580138));
#85983=CARTESIAN_POINT('Ctrl Pts',(-51.0837831246377,4.76977559219737,129.597206733576));
#85984=CARTESIAN_POINT('Ctrl Pts',(-51.0915311926407,4.73244761335131,129.465285321182));
#85985=CARTESIAN_POINT('Ctrl Pts',(-51.0992874953825,4.69507996188511,129.333223701141));
#85986=CARTESIAN_POINT('Ctrl Pts',(-51.1070437981243,4.65220005188253,129.202797355729));
#85987=CARTESIAN_POINT('Ctrl Pts',(-51.1148001008662,4.60399044685841,129.074489227047));
#85988=CARTESIAN_POINT('Ctrl Pts',(-51.1225605433803,4.55575511091647,128.946112616453));
#85989=CARTESIAN_POINT('Ctrl Pts',(-51.1303209858946,4.50218456444414,128.81985683505));
#85990=CARTESIAN_POINT('Ctrl Pts',(-51.1380814284088,4.44350879200761,128.69618304491));
#85991=CARTESIAN_POINT('Ctrl Pts',(-51.1458543286742,4.38473882801225,128.572310722622));
#85992=CARTESIAN_POINT('Ctrl Pts',(-51.1536272289396,4.32084744343521,128.451029020414));
#85993=CARTESIAN_POINT('Ctrl Pts',(-51.161400129205,4.25211012142916,128.33277356109));
#85994=CARTESIAN_POINT('Ctrl Pts',(-51.1688904649671,4.18587157421624,128.218816985579));
#85995=CARTESIAN_POINT('Ctrl Pts',(-51.1763808007292,4.11513346215704,128.107670709628));
#85996=CARTESIAN_POINT('Ctrl Pts',(-51.1838711364913,4.04017820820069,127.999696090661));
#85997=CARTESIAN_POINT('Ctrl Pts',(-51.1916454706104,3.96238100300919,127.887627581198));
#85998=CARTESIAN_POINT('Ctrl Pts',(-51.1994198047294,3.8797941192154,127.778620983794));
#85999=CARTESIAN_POINT('Ctrl Pts',(-51.2071941388485,3.7926865315062,127.673112953099));
#86000=CARTESIAN_POINT('Ctrl Pts',(-51.2149588917955,3.70568629611372,127.567734951622));
#86001=CARTESIAN_POINT('Ctrl Pts',(-51.2227236447427,3.61417668868066,127.465847236511));
#86002=CARTESIAN_POINT('Ctrl Pts',(-51.2304883976898,3.5184700986499,127.367857856414));
#86003=CARTESIAN_POINT('Ctrl Pts',(-51.2382454385747,3.42285856575384,127.269965800751));
#86004=CARTESIAN_POINT('Ctrl Pts',(-51.2460024794598,3.32305861717709,127.175964652766));
#86005=CARTESIAN_POINT('Ctrl Pts',(-51.2537595203447,3.21942283764176,127.086229412919));
#86006=CARTESIAN_POINT('Ctrl Pts',(-51.2615107115849,3.11586521065353,126.996561843114));
#86007=CARTESIAN_POINT('Ctrl Pts',(-51.269261902825,3.00847780467973,126.911154033178));
#86008=CARTESIAN_POINT('Ctrl Pts',(-51.2770130940651,2.89764972125601,126.830343864279));
#86009=CARTESIAN_POINT('Ctrl Pts',(-51.2847609908422,2.78686874272463,126.749568041858));
#86010=CARTESIAN_POINT('Ctrl Pts',(-51.2925088876193,2.67265031054922,126.673386203738));
#86011=CARTESIAN_POINT('Ctrl Pts',(-51.3002567843964,2.55541606387512,126.602095537518));
#86012=CARTESIAN_POINT('Ctrl Pts',(-51.3080030604805,2.43820634007814,126.530819783769));
#86013=CARTESIAN_POINT('Ctrl Pts',(-51.3157493365645,2.31798239040251,126.464433369873));
#86014=CARTESIAN_POINT('Ctrl Pts',(-51.3234956126486,2.19519391430608,126.403189552827));
#86015=CARTESIAN_POINT('Ctrl Pts',(-51.3312419459139,2.07240453181317,126.341945283694));
#86016=CARTESIAN_POINT('Ctrl Pts',(-51.3389882791793,1.94705093498571,126.285843861664));
#86017=CARTESIAN_POINT('Ctrl Pts',(-51.3467346124446,1.81960608063025,126.235091882436));
#86018=CARTESIAN_POINT('Ctrl Pts',(-51.3544826804476,1.69213268588278,126.184328537655));
#86019=CARTESIAN_POINT('Ctrl Pts',(-51.3622307484505,1.56256746485369,126.138917164117));
#86020=CARTESIAN_POINT('Ctrl Pts',(-51.3699788164535,1.43140156004473,126.099015504144));
#86021=CARTESIAN_POINT('Ctrl Pts',(-51.3777351191953,1.30009625055143,126.059071436213));
#86022=CARTESIAN_POINT('Ctrl Pts',(-51.3854914219372,1.16718723353377,126.024648893384));
#86023=CARTESIAN_POINT('Ctrl Pts',(-51.3932477246791,1.03317950189805,125.995855321805));
#86024=CARTESIAN_POINT('Ctrl Pts',(-51.4010081671932,0.899100246300877,
125.96704638223));
#86025=CARTESIAN_POINT('Ctrl Pts',(-51.4087686097074,0.76392149275524,125.943872466357));
#86026=CARTESIAN_POINT('Ctrl Pts',(-51.4165290522215,0.628155542248925,
125.926389351021));
#86027=CARTESIAN_POINT('Ctrl Pts',(-51.424301952487,0.492171648186308,125.908878170236));
#86028=CARTESIAN_POINT('Ctrl Pts',(-51.4320748527524,0.355599063244194,
125.897076079064));
#86029=CARTESIAN_POINT('Ctrl Pts',(-51.4398477530179,0.218953194599875,
125.890986770496));
#86030=CARTESIAN_POINT('Ctrl Pts',(-51.4473380887799,0.0872747474698428,
125.885118823631));
#86031=CARTESIAN_POINT('Ctrl Pts',(-51.454828424542,-0.044471439755898,
125.884555523664));
#86032=CARTESIAN_POINT('Ctrl Pts',(-51.4623187603041,-0.175828690340573,
125.889254582682));
#86033=CARTESIAN_POINT('Ctrl Pts',(-51.4700930944232,-0.312166391005563,
125.894131807951));
#86034=CARTESIAN_POINT('Ctrl Pts',(-51.4778674285423,-0.448516956616542,
125.904693763738));
#86035=CARTESIAN_POINT('Ctrl Pts',(-51.4856417626614,-0.584367629861358,
125.920950176525));
#86036=CARTESIAN_POINT('Ctrl Pts',(-51.4934065156085,-0.720050879292724,
125.937186554736));
#86037=CARTESIAN_POINT('Ctrl Pts',(-51.5011712685556,-0.855235077689818,
125.959103380393));
#86038=CARTESIAN_POINT('Ctrl Pts',(-51.5089360215027,-0.989408068044108,
125.986658391671));
#86039=CARTESIAN_POINT('Ctrl Pts',(-51.5166930623877,-1.12344779589251,
126.014186034924));
#86040=CARTESIAN_POINT('Ctrl Pts',(-51.5244501032727,-1.25647793389795,
126.047340641552));
#86041=CARTESIAN_POINT('Ctrl Pts',(-51.5322071441577,-1.38799240289921,
126.08602826895));
#86042=CARTESIAN_POINT('Ctrl Pts',(-51.5399583353979,-1.51940769581708,
126.124686721708));
#86043=CARTESIAN_POINT('Ctrl Pts',(-51.5477095266381,-1.64930922120316,
126.168869780251));
#86044=CARTESIAN_POINT('Ctrl Pts',(-51.5554607178782,-1.77720239117796,
126.218432715463));
#86045=CARTESIAN_POINT('Ctrl Pts',(-51.5632086146553,-1.90504120314334,
126.267974585104));
#86046=CARTESIAN_POINT('Ctrl Pts',(-51.5709565114324,-2.03087299366717,
126.322891642578));
#86047=CARTESIAN_POINT('Ctrl Pts',(-51.5787044082095,-2.15421982414746,
126.382989788089));
#86048=CARTESIAN_POINT('Ctrl Pts',(-51.5864506842936,-2.27754085313004,
126.443075362363));
#86049=CARTESIAN_POINT('Ctrl Pts',(-51.5941969603778,-2.39837760473566,
126.508339697855));
#86050=CARTESIAN_POINT('Ctrl Pts',(-51.6019432364619,-2.51627393313666,
126.57854134127));
#86051=CARTESIAN_POINT('Ctrl Pts',(-51.6096895697273,-2.63417113182158,
126.648743502897));
#86052=CARTESIAN_POINT('Ctrl Pts',(-51.6174359029926,-2.74912752806806,
126.723882845146));
#86053=CARTESIAN_POINT('Ctrl Pts',(-51.625182236258,-2.86071366235615,126.803673126083));
#86054=CARTESIAN_POINT('Ctrl Pts',(-51.632930304261,-2.97232478558532,126.8834812755));
#86055=CARTESIAN_POINT('Ctrl Pts',(-51.6406783722639,-3.08056382703257,
126.967942208798));
#86056=CARTESIAN_POINT('Ctrl Pts',(-51.6484264402669,-3.18503259909559,
127.056727977459));
#86057=CARTESIAN_POINT('Ctrl Pts',(-51.6561827430087,-3.28961240181262,
127.14560810869));
#86058=CARTESIAN_POINT('Ctrl Pts',(-51.6639390457507,-3.39041363217254,
127.23882200367));
#86059=CARTESIAN_POINT('Ctrl Pts',(-51.6716953484925,-3.48707293168823,
127.336002874831));
#86060=CARTESIAN_POINT('Ctrl Pts',(-51.6794557910067,-3.5837838211823,127.433235614349));
#86061=CARTESIAN_POINT('Ctrl Pts',(-51.6872162335209,-3.67634811114175,
127.534439260585));
#86062=CARTESIAN_POINT('Ctrl Pts',(-51.6949766760351,-3.76444196373765,
127.639212948949));
#86063=CARTESIAN_POINT('Ctrl Pts',(-51.7027495763005,-3.85267723240659,
127.74415482934));
#86064=CARTESIAN_POINT('Ctrl Pts',(-51.7105224765659,-3.93642748409369,
127.852677894429));
#86065=CARTESIAN_POINT('Ctrl Pts',(-51.7182953768314,-4.01541102161395,
127.964350513711));
#86066=CARTESIAN_POINT('Ctrl Pts',(-51.7257857125933,-4.09152330859643,
128.071963551993));
#86067=CARTESIAN_POINT('Ctrl Pts',(-51.7332760483551,-4.1632092610856,128.182500873158));
#86068=CARTESIAN_POINT('Ctrl Pts',(-51.7407663841171,-4.23025761216825,
128.295555404483));
#86069=CARTESIAN_POINT('Ctrl Pts',(-51.7488222097794,-4.30236784119367,
128.417145093335));
#86070=CARTESIAN_POINT('Ctrl Pts',(-51.7568780354418,-4.369328357198,128.542008231541));
#86071=CARTESIAN_POINT('Ctrl Pts',(-51.7649338611041,-4.43084077719799,
128.669686621467));
#86072=CARTESIAN_POINT('Ctrl Pts',(-51.7729786123424,-4.4922686354595,128.797189490635));
#86073=CARTESIAN_POINT('Ctrl Pts',(-51.7810233635806,-4.54826315846495,
128.927499591582));
#86074=CARTESIAN_POINT('Ctrl Pts',(-51.7890681148189,-4.59857017835228,
129.060131453359));
#86075=CARTESIAN_POINT('Ctrl Pts',(-51.7970997542386,-4.64879520483839,
129.192547143766));
#86076=CARTESIAN_POINT('Ctrl Pts',(-51.8051313936585,-4.693351078895,129.327276726197));
#86077=CARTESIAN_POINT('Ctrl Pts',(-51.8131630330782,-4.73203060737242,
129.463812448573));
#86078=CARTESIAN_POINT('Ctrl Pts',(-51.8154814838541,-4.74319602181914,
129.50322549178));
#86079=CARTESIAN_POINT('Ctrl Pts',(-51.8177999346299,-4.75387207661904,
129.542788895002));
#86080=CARTESIAN_POINT('Ctrl Pts',(-51.8201183854058,-4.76405452823404,
129.582490119308));
#86081=CARTESIAN_POINT('Origin',(213.235140564004,0.,130.804360617566));
#86082=CARTESIAN_POINT('',(-53.9150733197311,-4.76405452823399,129.582490119308));
#86083=CARTESIAN_POINT('',(-53.5697656565505,-4.76405452823409,129.582490119308));
#86084=CARTESIAN_POINT('',(213.235140564004,-4.76405452823405,129.582490119308));
#86085=CARTESIAN_POINT('',(-52.2351405639781,-4.91824847382902,130.808235172839));
#86086=CARTESIAN_POINT('Ctrl Pts',(-52.2351405640084,-4.9182484738286,130.808235173372));
#86087=CARTESIAN_POINT('Ctrl Pts',(-52.2481165697295,-4.91806852435966,
131.036657796555));
#86088=CARTESIAN_POINT('Ctrl Pts',(-52.2610925754504,-4.90197300803857,
131.264470097888));
#86089=CARTESIAN_POINT('Ctrl Pts',(-52.2740685811715,-4.87022848596664,
131.489968054062));
#86090=CARTESIAN_POINT('Ctrl Pts',(-52.2754032659754,-4.86696331083278,
131.513162302115));
#86091=CARTESIAN_POINT('Ctrl Pts',(-52.2767379507793,-4.86353260158788,
131.536332098239));
#86092=CARTESIAN_POINT('Ctrl Pts',(-52.2780726355832,-4.85993666785756,
131.559475606765));
#86093=CARTESIAN_POINT('Ctrl Pts',(-52.2858469697023,-4.83899090582646,
131.694282991584));
#86094=CARTESIAN_POINT('Ctrl Pts',(-52.2936213038213,-4.81239868313447,
131.828431734942));
#86095=CARTESIAN_POINT('Ctrl Pts',(-52.3013956379403,-4.78021090249829,
131.961411519703));
#86096=CARTESIAN_POINT('Ctrl Pts',(-52.3091603908874,-4.74806279042503,
132.094227418765));
#86097=CARTESIAN_POINT('Ctrl Pts',(-52.3169251438343,-4.71033293253625,
132.225876849324));
#86098=CARTESIAN_POINT('Ctrl Pts',(-52.3246898967814,-4.66712378507074,
132.35585623062));
#86099=CARTESIAN_POINT('Ctrl Pts',(-52.3324469376664,-4.62395755353964,
132.485706514563));
#86100=CARTESIAN_POINT('Ctrl Pts',(-52.3402039785514,-4.57532298500618,
132.613889681561));
#86101=CARTESIAN_POINT('Ctrl Pts',(-52.3479610194363,-4.52137313691162,
132.739914290114));
#86102=CARTESIAN_POINT('Ctrl Pts',(-52.3557122106764,-4.46746397281724,
132.865843862529));
#86103=CARTESIAN_POINT('Ctrl Pts',(-52.3634634019165,-4.40824766066713,
132.989617758544));
#86104=CARTESIAN_POINT('Ctrl Pts',(-52.3712145931566,-4.34392633172333,
133.110761945839));
#86105=CARTESIAN_POINT('Ctrl Pts',(-52.3789624899336,-4.27963234106016,
133.231854643623));
#86106=CARTESIAN_POINT('Ctrl Pts',(-52.3867103867107,-4.21023783206539,
133.350319511113));
#86107=CARTESIAN_POINT('Ctrl Pts',(-52.3944582834877,-4.13599199469353,
133.465704879839));
#86108=CARTESIAN_POINT('Ctrl Pts',(-52.4022045595718,-4.06176168795028,
133.581066112433));
#86109=CARTESIAN_POINT('Ctrl Pts',(-52.4099508356558,-3.98268228273301,
133.69334879897));
#86110=CARTESIAN_POINT('Ctrl Pts',(-52.4176971117398,-3.89904741713465,
133.802128504083));
#86111=CARTESIAN_POINT('Ctrl Pts',(-52.4254434450052,-3.8154119341627,133.910909012184));
#86112=CARTESIAN_POINT('Ctrl Pts',(-52.4331897782705,-3.72722116200948,
134.016186177316));
#86113=CARTESIAN_POINT('Ctrl Pts',(-52.4409361115358,-3.63481006202942,
134.117567353565));
#86114=CARTESIAN_POINT('Ctrl Pts',(-52.4486841795387,-3.54237826722425,
134.218971233425));
#86115=CARTESIAN_POINT('Ctrl Pts',(-52.4564322475416,-3.44572452725197,
134.316477099382));
#86116=CARTESIAN_POINT('Ctrl Pts',(-52.4641803155446,-3.34522152464625,
134.409728284468));
#86117=CARTESIAN_POINT('Ctrl Pts',(-52.4719366182864,-3.24461170625323,
134.503078578023));
#86118=CARTESIAN_POINT('Ctrl Pts',(-52.4796929210283,-3.14014473998698,
134.592164891329));
#86119=CARTESIAN_POINT('Ctrl Pts',(-52.4874492237701,-3.03222776196002,
134.676669729982));
#86120=CARTESIAN_POINT('Ctrl Pts',(-52.4952096662842,-2.92425318539241,
134.761219671412));
#86121=CARTESIAN_POINT('Ctrl Pts',(-52.5029701087983,-2.81282524545193,
134.841183037947));
#86122=CARTESIAN_POINT('Ctrl Pts',(-52.5107305513125,-2.69838024902019,
134.916285604017));
#86123=CARTESIAN_POINT('Ctrl Pts',(-52.5185034515779,-2.58375153532038,
134.991508731393));
#86124=CARTESIAN_POINT('Ctrl Pts',(-52.5262763518433,-2.46609642253151,
135.0618552647));
#86125=CARTESIAN_POINT('Ctrl Pts',(-52.5340492521087,-2.34587679093241,
135.127096457779));
#86126=CARTESIAN_POINT('Ctrl Pts',(-52.5415395878712,-2.23002744574942,
135.189965969162));
#86127=CARTESIAN_POINT('Ctrl Pts',(-52.5490299236337,-2.11179707450387,
135.24809474407));
#86128=CARTESIAN_POINT('Ctrl Pts',(-52.5565202593961,-1.99161485314921,
135.301321073164));
#86129=CARTESIAN_POINT('Ctrl Pts',(-52.5642945935152,-1.86687588635034,
135.356565494701));
#86130=CARTESIAN_POINT('Ctrl Pts',(-52.5720689276343,-1.73963900335625,
135.40670337717));
#86131=CARTESIAN_POINT('Ctrl Pts',(-52.5798432617534,-1.61036106258794,
135.451501707591));
#86132=CARTESIAN_POINT('Ctrl Pts',(-52.5876080147005,-1.48124244532791,
135.496244828074));
#86133=CARTESIAN_POINT('Ctrl Pts',(-52.5953727676477,-1.35008814109999,
135.535661363));
#86134=CARTESIAN_POINT('Ctrl Pts',(-52.6031375205948,-1.2173772067598,135.569565314005));
#86135=CARTESIAN_POINT('Ctrl Pts',(-52.6108945614798,-1.0847980827905,135.603435591127));
#86136=CARTESIAN_POINT('Ctrl Pts',(-52.6186516023648,-0.950665781799995,
135.631804084028));
#86137=CARTESIAN_POINT('Ctrl Pts',(-52.6264086432498,-0.815476498728038,
135.654533928132));
#86138=CARTESIAN_POINT('Ctrl Pts',(-52.63415983449,-0.680389162945881,135.677246631483));
#86139=CARTESIAN_POINT('Ctrl Pts',(-52.64191102573,-0.544246815612059,135.69432908512));
#86140=CARTESIAN_POINT('Ctrl Pts',(-52.6496622169702,-0.407557530427672,
135.705695121749));
#86141=CARTESIAN_POINT('Ctrl Pts',(-52.6574101137473,-0.27092634183598,
135.717056327509));
#86142=CARTESIAN_POINT('Ctrl Pts',(-52.6651580105245,-0.133749066550099,
135.72270591628));
#86143=CARTESIAN_POINT('Ctrl Pts',(-52.6729059073016,0.00345960069853902,
135.722609400788));
#86144=CARTESIAN_POINT('Ctrl Pts',(-52.6806521833857,0.140639566851865,
135.722512905485));
#86145=CARTESIAN_POINT('Ctrl Pts',(-52.6883984594698,0.277850521189361,
135.71667269696));
#86146=CARTESIAN_POINT('Ctrl Pts',(-52.6961447355539,0.414576655654646,
135.705106403575));
#86147=CARTESIAN_POINT('Ctrl Pts',(-52.7038910688192,0.551303799401197,
135.69354002481));
#86148=CARTESIAN_POINT('Ctrl Pts',(-52.7116374020846,0.687545726560492,
135.676247509796));
#86149=CARTESIAN_POINT('Ctrl Pts',(-52.71938373535,0.822791038209392,135.653298436299));
#86150=CARTESIAN_POINT('Ctrl Pts',(-52.7271318033529,0.95806663710811,135.630344223516));
#86151=CARTESIAN_POINT('Ctrl Pts',(-52.7348798713559,1.09234479100224,135.601730996964));
#86152=CARTESIAN_POINT('Ctrl Pts',(-52.7426279393589,1.22512398185717,135.567579517803));
#86153=CARTESIAN_POINT('Ctrl Pts',(-52.7503842421007,1.35804429201622,135.533391742045));
#86154=CARTESIAN_POINT('Ctrl Pts',(-52.7581405448427,1.48946207747062,135.493654053061));
#86155=CARTESIAN_POINT('Ctrl Pts',(-52.7658968475845,1.61889015417386,135.448537372516));
#86156=CARTESIAN_POINT('Ctrl Pts',(-52.7736572900987,1.74838731053865,135.40339661184));
#86157=CARTESIAN_POINT('Ctrl Pts',(-52.7814177326129,1.87589227880128,135.35287128299));
#86158=CARTESIAN_POINT('Ctrl Pts',(-52.7891781751271,2.00093851069744,135.297180237683));
#86159=CARTESIAN_POINT('Ctrl Pts',(-52.7969510753925,2.12618547790612,135.241399792166));
#86160=CARTESIAN_POINT('Ctrl Pts',(-52.8047239756579,2.24896547104311,135.180437233172));
#86161=CARTESIAN_POINT('Ctrl Pts',(-52.8124968759234,2.36883638191488,135.114557510774));
#86162=CARTESIAN_POINT('Ctrl Pts',(-52.8199872116853,2.48434968323808,135.051072682227));
#86163=CARTESIAN_POINT('Ctrl Pts',(-52.8274775474471,2.59716147144785,134.983022145156));
#86164=CARTESIAN_POINT('Ctrl Pts',(-52.834967883209,2.70690371581109,134.910679569599));
#86165=CARTESIAN_POINT('Ctrl Pts',(-52.8427422173282,2.8208068707264,134.835594103301));
#86166=CARTESIAN_POINT('Ctrl Pts',(-52.8505165514472,2.93176393441776,134.755646860263));
#86167=CARTESIAN_POINT('Ctrl Pts',(-52.8582908855663,3.03933192332999,134.671096259206));
#86168=CARTESIAN_POINT('Ctrl Pts',(-52.8660556385134,3.14676734430951,134.586649859208));
#86169=CARTESIAN_POINT('Ctrl Pts',(-52.8738203914605,3.25082169653457,134.497611628508));
#86170=CARTESIAN_POINT('Ctrl Pts',(-52.8815851444076,3.35107955237981,134.404284074547));
#86171=CARTESIAN_POINT('Ctrl Pts',(-52.8893421852926,3.45123783070923,134.311049214828));
#86172=CARTESIAN_POINT('Ctrl Pts',(-52.8970992261777,3.54760683227307,134.213533774532));
#86173=CARTESIAN_POINT('Ctrl Pts',(-52.9048562670627,3.63980320354225,134.11208123787));
#86174=CARTESIAN_POINT('Ctrl Pts',(-52.9126074583028,3.73193004881067,134.010705207355));
#86175=CARTESIAN_POINT('Ctrl Pts',(-52.9203586495429,3.81989026505082,133.905398278244));
#86176=CARTESIAN_POINT('Ctrl Pts',(-52.928109840783,3.90333673103308,133.796541331806));
#86177=CARTESIAN_POINT('Ctrl Pts',(-52.9358577375601,3.98674773004128,133.687730652474));
#86178=CARTESIAN_POINT('Ctrl Pts',(-52.9436056343373,4.06564855711208,133.575373266443));
#86179=CARTESIAN_POINT('Ctrl Pts',(-52.9513535311144,4.13973199205104,133.459883559754));
#86180=CARTESIAN_POINT('Ctrl Pts',(-52.9590998071985,4.21379993033247,133.344418011023));
#86181=CARTESIAN_POINT('Ctrl Pts',(-52.9668460832825,4.28305226988077,133.22582177376));
#86182=CARTESIAN_POINT('Ctrl Pts',(-52.9745923593666,4.34722503508131,133.104538340452));
#86183=CARTESIAN_POINT('Ctrl Pts',(-52.982338692632,4.41139827399062,132.983254011858));
#86184=CARTESIAN_POINT('Ctrl Pts',(-52.9900850258973,4.47049168088363,132.859282793209));
#86185=CARTESIAN_POINT('Ctrl Pts',(-52.9978313591627,4.52428736989566,132.733092547385));
#86186=CARTESIAN_POINT('Ctrl Pts',(-53.0055794271657,4.57809510607925,132.60687404213));
#86187=CARTESIAN_POINT('Ctrl Pts',(-53.0133274951687,4.62660261031784,132.478435880436));
#86188=CARTESIAN_POINT('Ctrl Pts',(-53.0210755631716,4.66964039964916,132.348265277985));
#86189=CARTESIAN_POINT('Ctrl Pts',(-53.0288318659135,4.71272393005514,132.217956328669));
#86190=CARTESIAN_POINT('Ctrl Pts',(-53.0365881686554,4.75032600997975,132.085911632279));
#86191=CARTESIAN_POINT('Ctrl Pts',(-53.0443444713972,4.78232710578093,131.952633457884));
#86192=CARTESIAN_POINT('Ctrl Pts',(-53.0521049139114,4.81434528153053,131.819284148915));
#86193=CARTESIAN_POINT('Ctrl Pts',(-53.0598653564256,4.840756441245,131.684700433594));
#86194=CARTESIAN_POINT('Ctrl Pts',(-53.0676257989398,4.8614925303401,131.549393126889));
#86195=CARTESIAN_POINT('Ctrl Pts',(-53.0753986992053,4.88226190684624,131.413868612883));
#86196=CARTESIAN_POINT('Ctrl Pts',(-53.0831715994707,4.89733796477343,131.277618575117));
#86197=CARTESIAN_POINT('Ctrl Pts',(-53.0909444997361,4.90670464384513,131.141158183722));
#86198=CARTESIAN_POINT('Ctrl Pts',(-53.0984348354981,4.91573082053923,131.009658471279));
#86199=CARTESIAN_POINT('Ctrl Pts',(-53.10592517126,4.91945550351924,130.877963741348));
#86200=CARTESIAN_POINT('Ctrl Pts',(-53.113415507022,4.91791000953669,130.746531553949));
#86201=CARTESIAN_POINT('Ctrl Pts',(-53.121189841141,4.91630591768004,130.610116075215));
#86202=CARTESIAN_POINT('Ctrl Pts',(-53.1289641752601,4.90901904109058,130.473551317383));
#86203=CARTESIAN_POINT('Ctrl Pts',(-53.1367385093792,4.89602735132519,130.337349656693));
#86204=CARTESIAN_POINT('Ctrl Pts',(-53.1445032623262,4.88305167265633,130.201315852377));
#86205=CARTESIAN_POINT('Ctrl Pts',(-53.1522680152733,4.86438520652166,130.065644640305));
#86206=CARTESIAN_POINT('Ctrl Pts',(-53.1600327682204,4.840057912219,129.930849044165));
#86207=CARTESIAN_POINT('Ctrl Pts',(-53.1677898091054,4.81575478012801,129.79618732891));
#86208=CARTESIAN_POINT('Ctrl Pts',(-53.1755468499903,4.78580207771579,129.662399881156));
#86209=CARTESIAN_POINT('Ctrl Pts',(-53.1833038908753,4.75028157602928,129.529994888689));
#86210=CARTESIAN_POINT('Ctrl Pts',(-53.1910550821154,4.71478786062946,129.397689743856));
#86211=CARTESIAN_POINT('Ctrl Pts',(-53.1988062733556,4.67373480414731,129.266765355322));
#86212=CARTESIAN_POINT('Ctrl Pts',(-53.2065574645957,4.62725522527689,129.137719641636));
#86213=CARTESIAN_POINT('Ctrl Pts',(-53.2143053613728,4.58079540146732,129.008728775821));
#86214=CARTESIAN_POINT('Ctrl Pts',(-53.2220532581497,4.52891377476509,128.881615363788));
#86215=CARTESIAN_POINT('Ctrl Pts',(-53.2298011549268,4.47179291986293,128.756861864364));
#86216=CARTESIAN_POINT('Ctrl Pts',(-53.2375474310109,4.41468401341223,128.632134460683));
#86217=CARTESIAN_POINT('Ctrl Pts',(-53.245293707095,4.35233822129179,128.509766342978));
#86218=CARTESIAN_POINT('Ctrl Pts',(-53.2530399831791,4.28498598102263,128.390219319933));
#86219=CARTESIAN_POINT('Ctrl Pts',(-53.2607863164444,4.21763324357454,128.270671414418));
#86220=CARTESIAN_POINT('Ctrl Pts',(-53.2685326497097,4.14527417614053,128.153944985742));
#86221=CARTESIAN_POINT('Ctrl Pts',(-53.2762789829751,4.06818463237967,128.040476238767));
#86222=CARTESIAN_POINT('Ctrl Pts',(-53.284027050978,3.99107782494998,127.926982081253));
#86223=CARTESIAN_POINT('Ctrl Pts',(-53.291775118981,3.90923865286163,127.816747380461));
#86224=CARTESIAN_POINT('Ctrl Pts',(-53.299523186984,3.82298541478731,127.710178079185));
#86225=CARTESIAN_POINT('Ctrl Pts',(-53.3072794897258,3.73664050574514,127.603495514787));
#86226=CARTESIAN_POINT('Ctrl Pts',(-53.3150357924677,3.64587240565352,127.50048643623));
#86227=CARTESIAN_POINT('Ctrl Pts',(-53.3227920952095,3.55103907685237,127.401522899254));
#86228=CARTESIAN_POINT('Ctrl Pts',(-53.3305525377237,3.45615513264814,127.302506542458));
#86229=CARTESIAN_POINT('Ctrl Pts',(-53.3383129802378,3.35720191829415,127.207540300266));
#86230=CARTESIAN_POINT('Ctrl Pts',(-53.346073422752,3.25457241172448,127.116957536895));
#86231=CARTESIAN_POINT('Ctrl Pts',(-53.3538463230174,3.15177815515998,127.026229362031));
#86232=CARTESIAN_POINT('Ctrl Pts',(-53.3616192232828,3.04529611714926,126.939898974016));
#86233=CARTESIAN_POINT('Ctrl Pts',(-53.3693921235482,2.9355510439423,126.858258346855));
#86234=CARTESIAN_POINT('Ctrl Pts',(-53.3768824593104,2.82979548057489,126.77958556213));
#86235=CARTESIAN_POINT('Ctrl Pts',(-53.3843727950726,2.72101025662343,126.705267662498));
#86236=CARTESIAN_POINT('Ctrl Pts',(-53.3918631308348,2.60959725775939,126.635525622655));
#86237=CARTESIAN_POINT('Ctrl Pts',(-53.3996374649539,2.49396000118262,126.563139292175));
#86238=CARTESIAN_POINT('Ctrl Pts',(-53.407411799073,2.37512546791411,126.495453360436));
#86239=CARTESIAN_POINT('Ctrl Pts',(-53.4151861331921,2.25351282768591,126.432763312466));
#86240=CARTESIAN_POINT('Ctrl Pts',(-53.4229508861392,2.13205006416796,126.370150524377));
#86241=CARTESIAN_POINT('Ctrl Pts',(-53.4307156390863,2.00781635014345,126.31252154692));
#86242=CARTESIAN_POINT('Ctrl Pts',(-53.4384803920334,1.88125950070231,126.260128476322));
#86243=CARTESIAN_POINT('Ctrl Pts',(-53.4462374329184,1.75482834930836,126.20778744326));
#86244=CARTESIAN_POINT('Ctrl Pts',(-53.4539944738035,1.62607901316586,126.160672116653));
#86245=CARTESIAN_POINT('Ctrl Pts',(-53.4617515146885,1.49548324430038,126.118988388114));
#86246=CARTESIAN_POINT('Ctrl Pts',(-53.4695027059286,1.36498595871992,126.0773360936));
#86247=CARTESIAN_POINT('Ctrl Pts',(-53.4772538971687,1.23264538286877,126.041107362692));
#86248=CARTESIAN_POINT('Ctrl Pts',(-53.4850050884088,1.09895222147341,126.010459588402));
#86249=CARTESIAN_POINT('Ctrl Pts',(-53.4927529851859,0.965315883238017,
125.979824840234));
#86250=CARTESIAN_POINT('Ctrl Pts',(-53.5005008819631,0.830328483143253,
125.954766418021));
#86251=CARTESIAN_POINT('Ctrl Pts',(-53.5082487787402,0.694494613545642,
125.935391497284));
#86252=CARTESIAN_POINT('Ctrl Pts',(-53.5159950548243,0.558689157465312,
125.916020629364));
#86253=CARTESIAN_POINT('Ctrl Pts',(-53.5237413309084,0.42203797087301,125.902330953373));
#86254=CARTESIAN_POINT('Ctrl Pts',(-53.5314876069926,0.285054143601113,
125.894378214571));
#86255=CARTESIAN_POINT('Ctrl Pts',(-53.5392339402579,0.148069305145721,
125.886425417065));
#86256=CARTESIAN_POINT('Ctrl Pts',(-53.5469802735232,0.0107522114190008,
125.884209663912));
#86257=CARTESIAN_POINT('Ctrl Pts',(-53.5547266067886,-0.126381040432686,
125.887734650999));
#86258=CARTESIAN_POINT('Ctrl Pts',(-53.5624746747916,-0.263545002325309,
125.891260427483));
#86259=CARTESIAN_POINT('Ctrl Pts',(-53.5702227427946,-0.400524649657835,
125.900529492357));
#86260=CARTESIAN_POINT('Ctrl Pts',(-53.5779708107976,-0.536806403053045,
125.915493473928));
#86261=CARTESIAN_POINT('Ctrl Pts',(-53.5857271135395,-0.673232998317537,
125.930473359397));
#86262=CARTESIAN_POINT('Ctrl Pts',(-53.5934834162814,-0.808959828710015,
125.951160209594));
#86263=CARTESIAN_POINT('Ctrl Pts',(-53.6012397190233,-0.943480385811545,
125.97745396588));
#86264=CARTESIAN_POINT('Ctrl Pts',(-53.6090001615375,-1.07807274058492,
126.003761755935));
#86265=CARTESIAN_POINT('Ctrl Pts',(-53.6167606040516,-1.21145715914997,
126.035682324089));
#86266=CARTESIAN_POINT('Ctrl Pts',(-53.6245210465658,-1.34314075857766,
126.073065238376));
#86267=CARTESIAN_POINT('Ctrl Pts',(-53.6322939468312,-1.47503574820929,
126.110508163036));
#86268=CARTESIAN_POINT('Ctrl Pts',(-53.6400668470967,-1.60522409116347,
126.153430833884));
#86269=CARTESIAN_POINT('Ctrl Pts',(-53.6478397473621,-1.73323055571743,
126.201633718952));
#86270=CARTESIAN_POINT('Ctrl Pts',(-53.655330083124,-1.85658366285307,126.248084307731));
#86271=CARTESIAN_POINT('Ctrl Pts',(-53.6628204188859,-1.97791048737297,
126.29943775753));
#86272=CARTESIAN_POINT('Ctrl Pts',(-53.6703107546477,-2.09680788798463,
126.355475392773));
#86273=CARTESIAN_POINT('Ctrl Pts',(-53.6780857478496,-2.22022378159239,
126.413642642801));
#86274=CARTESIAN_POINT('Ctrl Pts',(-53.6858607410514,-2.34141292501956,
126.477041420202));
#86275=CARTESIAN_POINT('Ctrl Pts',(-53.6936357342533,-2.45990002673024,
126.54547873132));
#86276=CARTESIAN_POINT('Ctrl Pts',(-53.7014009981672,-2.57823885884242,
126.613830402968));
#86277=CARTESIAN_POINT('Ctrl Pts',(-53.7091662620812,-2.69388204188799,
126.687207868635));
#86278=CARTESIAN_POINT('Ctrl Pts',(-53.7169315259951,-2.80637533812242,
126.765370579936));
#86279=CARTESIAN_POINT('Ctrl Pts',(-53.724688930366,-2.91875477526293,126.84345417954));
#86280=CARTESIAN_POINT('Ctrl Pts',(-53.7324463347369,-3.02799035158682,
126.926313163742));
#86281=CARTESIAN_POINT('Ctrl Pts',(-53.7402037391077,-3.13365379570381,
127.013661875755));
#86282=CARTESIAN_POINT('Ctrl Pts',(-53.7479546785665,-3.2392291813876,127.100937792575));
#86283=CARTESIAN_POINT('Ctrl Pts',(-53.7557056180253,-3.34123806288523,
127.192695738132));
#86284=CARTESIAN_POINT('Ctrl Pts',(-53.7634565574841,-3.43928282766282,
127.28860796787));
#86285=CARTESIAN_POINT('Ctrl Pts',(-53.7712039874065,-3.53728319889611,
127.384476769652));
#86286=CARTESIAN_POINT('Ctrl Pts',(-53.7789514173288,-3.63132274580799,
127.484495840307));
#86287=CARTESIAN_POINT('Ctrl Pts',(-53.7866988472512,-3.72103862461811,
127.588298644189));
#86288=CARTESIAN_POINT('Ctrl Pts',(-53.7944444470007,-3.81073330987601,
127.692076926769));
#86289=CARTESIAN_POINT('Ctrl Pts',(-53.8021900467503,-3.89610610462482,
127.799636867971));
#86290=CARTESIAN_POINT('Ctrl Pts',(-53.8099356464998,-3.97683285860141,
127.91057702558));
#86291=CARTESIAN_POINT('Ctrl Pts',(-53.8176810938486,-4.05755802421499,
128.021515000354));
#86292=CARTESIAN_POINT('Ctrl Pts',(-53.8254265411972,-4.13363710231795,
128.135832742306));
#86293=CARTESIAN_POINT('Ctrl Pts',(-53.833171988546,-4.20478811536839,128.253098191363));
#86294=CARTESIAN_POINT('Ctrl Pts',(-53.840922046836,-4.27598148532006,128.3704334497));
#86295=CARTESIAN_POINT('Ctrl Pts',(-53.8486721051261,-4.34224072672372,
128.490719586115));
#86296=CARTESIAN_POINT('Ctrl Pts',(-53.8564221634162,-4.40332875277113,
128.61349801176));
#86297=CARTESIAN_POINT('Ctrl Pts',(-53.8641747690669,-4.46443685779391,
128.736316793349));
#86298=CARTESIAN_POINT('Ctrl Pts',(-53.8719273747176,-4.5203701980571,128.861629141036));
#86299=CARTESIAN_POINT('Ctrl Pts',(-53.8796799803683,-4.57093944266997,
128.988955518437));
#86300=CARTESIAN_POINT('Ctrl Pts',(-53.8874406389297,-4.62156121537877,
129.116414154332));
#86301=CARTESIAN_POINT('Ctrl Pts',(-53.895201297491,-4.66680763261751,129.245890630247));
#86302=CARTESIAN_POINT('Ctrl Pts',(-53.9029619560525,-4.70653881476726,
129.376888919917));
#86303=CARTESIAN_POINT('Ctrl Pts',(-53.9069990772786,-4.72720711211976,
129.445034679924));
#86304=CARTESIAN_POINT('Ctrl Pts',(-53.9110361985049,-4.74638375651336,
129.513592048561));
#86305=CARTESIAN_POINT('Ctrl Pts',(-53.9150733197311,-4.76405452823399,
129.582490119308));
#86306=CARTESIAN_POINT('Ctrl Pts',(-52.1650248355919,-4.76405452823407,
129.582490119308));
#86307=CARTESIAN_POINT('Ctrl Pts',(-52.1726632853586,-4.79766468427344,
129.713535607601));
#86308=CARTESIAN_POINT('Ctrl Pts',(-52.1803017351253,-4.82584641107061,
129.845901857919));
#86309=CARTESIAN_POINT('Ctrl Pts',(-52.187940184892,-4.8485168568208,129.979092569218));
#86310=CARTESIAN_POINT('Ctrl Pts',(-52.1958069147397,-4.87186482371074,
130.116263772277));
#86311=CARTESIAN_POINT('Ctrl Pts',(-52.2036736445873,-4.88936686806602,
130.254309027462));
#86312=CARTESIAN_POINT('Ctrl Pts',(-52.211540374435,-4.90099004563023,130.39268157373));
#86313=CARTESIAN_POINT('Ctrl Pts',(-52.2194071042827,-4.91261322319444,
130.531054119999));
#86314=CARTESIAN_POINT('Ctrl Pts',(-52.2272738341305,-4.91835756854535,
130.669753493166));
#86315=CARTESIAN_POINT('Ctrl Pts',(-52.2351405639781,-4.91824847382902,
130.808235172838));
#86316=CARTESIAN_POINT('',(-51.8898594360354,-4.91824990617988,130.805321274443));
#86317=CARTESIAN_POINT('Ctrl Pts',(-51.8201183854058,-4.76405452823404,
129.582490119308));
#86318=CARTESIAN_POINT('Ctrl Pts',(-51.828135682534,-4.79926586027597,129.719778568533));
#86319=CARTESIAN_POINT('Ctrl Pts',(-51.8361529796623,-4.82857088525035,
129.858716332355));
#86320=CARTESIAN_POINT('Ctrl Pts',(-51.8441702767905,-4.85182571170561,
129.998773672704));
#86321=CARTESIAN_POINT('Ctrl Pts',(-51.8521776154136,-4.8750516527016,130.138657043979));
#86322=CARTESIAN_POINT('Ctrl Pts',(-51.8601849540367,-4.89224231988163,
130.279656873771));
#86323=CARTESIAN_POINT('Ctrl Pts',(-51.8681922926598,-4.90330454694982,
130.421231941582));
#86324=CARTESIAN_POINT('Ctrl Pts',(-51.8754146737702,-4.91328234651313,
130.548928438958));
#86325=CARTESIAN_POINT('Ctrl Pts',(-51.8826370548806,-4.91827495242315,
130.677092572184));
#86326=CARTESIAN_POINT('Ctrl Pts',(-51.889859435991,-4.91824990618003,130.805321273655));
#86327=CARTESIAN_POINT('Ctrl Pts',(-51.8898594360354,-4.91824990617988,
130.805321274443));
#86328=CARTESIAN_POINT('Ctrl Pts',(-51.8981042988535,-4.91822131408472,
130.951703476768));
#86329=CARTESIAN_POINT('Ctrl Pts',(-51.9063491616717,-4.91165329920825,
131.097920000058));
#86330=CARTESIAN_POINT('Ctrl Pts',(-51.9145940244898,-4.89861554147768,
131.243392324044));
#86331=CARTESIAN_POINT('Ctrl Pts',(-51.9228547446132,-4.8855527082899,131.389144434257));
#86332=CARTESIAN_POINT('Ctrl Pts',(-51.9311154647366,-4.86599530976217,
131.534149180284));
#86333=CARTESIAN_POINT('Ctrl Pts',(-51.93937618486,-4.84006424513526,131.677837100056));
#86334=CARTESIAN_POINT('Ctrl Pts',(-51.9476611144281,-4.81405718511522,
131.821946121704));
#86335=CARTESIAN_POINT('Ctrl Pts',(-51.9559460439962,-4.7816391523339,131.9647302936));
#86336=CARTESIAN_POINT('Ctrl Pts',(-51.9642309735642,-4.74298172897772,
132.105632065452));
#86337=CARTESIAN_POINT('Ctrl Pts',(-51.9725292725657,-4.70426192393872,
132.246761211218));
#86338=CARTESIAN_POINT('Ctrl Pts',(-51.9808275715673,-4.65928271751152,
132.386001598625));
#86339=CARTESIAN_POINT('Ctrl Pts',(-51.9891258705688,-4.60826434017012,
132.522814234518));
#86340=CARTESIAN_POINT('Ctrl Pts',(-51.9974438725248,-4.55712482803094,
132.659951709653));
#86341=CARTESIAN_POINT('Ctrl Pts',(-52.0057618744809,-4.49991759387119,
132.794649623649));
#86342=CARTESIAN_POINT('Ctrl Pts',(-52.014079876437,-4.43691017137636,132.92639058758));
#86343=CARTESIAN_POINT('Ctrl Pts',(-52.0157912536013,-4.42394678610545,
132.953495471477));
#86344=CARTESIAN_POINT('Ctrl Pts',(-52.0175026307656,-4.41073802523113,
132.980475279727));
#86345=CARTESIAN_POINT('Ctrl Pts',(-52.0192140079299,-4.39728644798685,
133.007325655158));
#86346=CARTESIAN_POINT('Ctrl Pts',(-52.026988342049,-4.33617948798705,133.129299813848));
#86347=CARTESIAN_POINT('Ctrl Pts',(-52.0347626761681,-4.2698968213164,133.248922720314));
#86348=CARTESIAN_POINT('Ctrl Pts',(-52.0425370102871,-4.19864273770781,
133.365723970078));
#86349=CARTESIAN_POINT('Ctrl Pts',(-52.0503017632342,-4.12747646838921,
133.482381272742));
#86350=CARTESIAN_POINT('Ctrl Pts',(-52.0580665161812,-4.0513511743476,133.596223507215));
#86351=CARTESIAN_POINT('Ctrl Pts',(-52.0658312691282,-3.97051818003925,
133.706802424817));
#86352=CARTESIAN_POINT('Ctrl Pts',(-52.0735883100132,-3.88976547020052,
133.817271513879));
#86353=CARTESIAN_POINT('Ctrl Pts',(-52.0813453508981,-3.80431459428713,
133.924483422563));
#86354=CARTESIAN_POINT('Ctrl Pts',(-52.089102391783,-3.71446135494585,134.028016912073));
#86355=CARTESIAN_POINT('Ctrl Pts',(-52.0968535830231,-3.62467587463107,
134.131472326173));
#86356=CARTESIAN_POINT('Ctrl Pts',(-52.1046047742632,-3.53049489408182,
134.231254548349));
#86357=CARTESIAN_POINT('Ctrl Pts',(-52.1123559655033,-3.4322556305999,134.32697390158));
#86358=CARTESIAN_POINT('Ctrl Pts',(-52.1201038622804,-3.3340581214257,134.422652571534));
#86359=CARTESIAN_POINT('Ctrl Pts',(-52.1278517590574,-3.23180603940663,
134.514271534803));
#86360=CARTESIAN_POINT('Ctrl Pts',(-52.1355996558344,-3.12587458476752,
134.601476778919));
#86361=CARTESIAN_POINT('Ctrl Pts',(-52.1433459319185,-3.01996528870496,
134.688663781577));
#86362=CARTESIAN_POINT('Ctrl Pts',(-52.1510922080025,-2.91037845254127,
134.771438653157));
#86363=CARTESIAN_POINT('Ctrl Pts',(-52.1588384840866,-2.79752328678356,
134.849486885361));
#86364=CARTESIAN_POINT('Ctrl Pts',(-52.1665848173519,-2.68466728795466,
134.927535693699));
#86365=CARTESIAN_POINT('Ctrl Pts',(-52.1743311506172,-2.56854323294814,
135.000857570654));
#86366=CARTESIAN_POINT('Ctrl Pts',(-52.1820774838825,-2.44958997569059,
135.069180896722));
#86367=CARTESIAN_POINT('Ctrl Pts',(-52.1898255518854,-2.33061007967616,
135.137519523324));
#86368=CARTESIAN_POINT('Ctrl Pts',(-52.1975736198884,-2.20880005961682,
135.200857176895));
#86369=CARTESIAN_POINT('Ctrl Pts',(-52.2053216878913,-2.0846237035928,135.258968016307));
#86370=CARTESIAN_POINT('Ctrl Pts',(-52.2130779906331,-1.96031537145971,
135.317140616611));
#86371=CARTESIAN_POINT('Ctrl Pts',(-52.220834293375,-1.83363603411204,135.37007513983));
#86372=CARTESIAN_POINT('Ctrl Pts',(-52.2285905961168,-1.70507032710317,
135.417593566609));
#86373=CARTESIAN_POINT('Ctrl Pts',(-52.2363510386309,-1.57643600070525,
135.465137355403));
#86374=CARTESIAN_POINT('Ctrl Pts',(-52.244111481145,-1.44591367037546,135.507259167711));
#86375=CARTESIAN_POINT('Ctrl Pts',(-52.2518719236591,-1.31400253787622,
135.543831093574));
#86376=CARTESIAN_POINT('Ctrl Pts',(-52.2596448239245,-1.18187964991658,
135.580461727939));
#86377=CARTESIAN_POINT('Ctrl Pts',(-52.26741772419,-1.04836388569331,135.611524583853));
#86378=CARTESIAN_POINT('Ctrl Pts',(-52.2751906244553,-0.913964912631464,
135.636942867355));
#86379=CARTESIAN_POINT('Ctrl Pts',(-52.2826809602179,-0.784451680762086,
135.661437132229));
#86380=CARTESIAN_POINT('Ctrl Pts',(-52.2901712959803,-0.654118643653161,
135.680690043575));
#86381=CARTESIAN_POINT('Ctrl Pts',(-52.2976616317428,-0.523423857490555,
135.694678657112));
#86382=CARTESIAN_POINT('Ctrl Pts',(-52.3054359658619,-0.387773738795743,
135.709197653182));
#86383=CARTESIAN_POINT('Ctrl Pts',(-52.313210299981,-0.251304199309538,
135.718091271386));
#86384=CARTESIAN_POINT('Ctrl Pts',(-52.3209846341001,-0.114521427230507,
135.721277121352));
#86385=CARTESIAN_POINT('Ctrl Pts',(-52.3287493870472,0.0220927723065638,
135.724459045043));
#86386=CARTESIAN_POINT('Ctrl Pts',(-52.3365141399942,0.159019049242489,
135.72194718767));
#86387=CARTESIAN_POINT('Ctrl Pts',(-52.3442788929413,0.295744432258527,
135.713710706253));
#86388=CARTESIAN_POINT('Ctrl Pts',(-52.3520359338263,0.432334017696848,
135.705482405425));
#86389=CARTESIAN_POINT('Ctrl Pts',(-52.3597929747113,0.568722718557942,
135.691540818865));
#86390=CARTESIAN_POINT('Ctrl Pts',(-52.3675500155963,0.7043962461554,135.671907123857));
#86391=CARTESIAN_POINT('Ctrl Pts',(-52.3753012068364,0.839967461290311,
135.652288234771));
#86392=CARTESIAN_POINT('Ctrl Pts',(-52.3830523980765,0.974824191271789,
135.626985836893));
#86393=CARTESIAN_POINT('Ctrl Pts',(-52.3908035893166,1.10845631559856,135.596073010741));
#86394=CARTESIAN_POINT('Ctrl Pts',(-52.3985514860937,1.24203164270757,135.565173323366));
#86395=CARTESIAN_POINT('Ctrl Pts',(-52.4062993828708,1.37438301926801,135.528668038398));
#86396=CARTESIAN_POINT('Ctrl Pts',(-52.4140472796479,1.5050097996753,135.486681470026));
#86397=CARTESIAN_POINT('Ctrl Pts',(-52.421793555732,1.63560925577612,135.444703684339));
#86398=CARTESIAN_POINT('Ctrl Pts',(-52.4295398318161,1.76448446129726,135.397247015391));
#86399=CARTESIAN_POINT('Ctrl Pts',(-52.4372861079002,1.89114962322367,135.344485744155));
#86400=CARTESIAN_POINT('Ctrl Pts',(-52.4450324411655,2.01781572016353,135.291724083446));
#86401=CARTESIAN_POINT('Ctrl Pts',(-52.4527787744308,2.14227138004817,135.233657892645));
#86402=CARTESIAN_POINT('Ctrl Pts',(-52.4605251076962,2.26405087042892,135.170509575012));
#86403=CARTESIAN_POINT('Ctrl Pts',(-52.4682731756991,2.38585763248201,135.107347115752));
#86404=CARTESIAN_POINT('Ctrl Pts',(-52.476021243702,2.50498668546375,135.039100444899));
#86405=CARTESIAN_POINT('Ctrl Pts',(-52.4837693117049,2.62099733405319,134.966037687857));
#86406=CARTESIAN_POINT('Ctrl Pts',(-52.4915256144468,2.73713128014065,134.892897278847));
#86407=CARTESIAN_POINT('Ctrl Pts',(-52.4992819171886,2.85013986985923,134.814930767388));
#86408=CARTESIAN_POINT('Ctrl Pts',(-52.5070382199305,2.95961137313065,134.732449667287));
#86409=CARTESIAN_POINT('Ctrl Pts',(-52.5147986624446,3.06914130463963,134.649924544539));
#86410=CARTESIAN_POINT('Ctrl Pts',(-52.5225591049588,3.17513008601504,134.562880279883));
#86411=CARTESIAN_POINT('Ctrl Pts',(-52.5303195474729,3.27720027223872,134.471667727441));
#86412=CARTESIAN_POINT('Ctrl Pts',(-52.5380924477384,3.37943431058668,134.380308752512));
#86413=CARTESIAN_POINT('Ctrl Pts',(-52.5458653480038,3.47773690287933,134.284768391082));
#86414=CARTESIAN_POINT('Ctrl Pts',(-52.5536382482693,3.57176795249014,134.185433931776));
#86415=CARTESIAN_POINT('Ctrl Pts',(-52.5611285840314,3.66238073659946,134.089710530273));
#86416=CARTESIAN_POINT('Ctrl Pts',(-52.5686189197935,3.74902694630057,133.990464323796));
#86417=CARTESIAN_POINT('Ctrl Pts',(-52.5761092555557,3.83143968736196,133.88806828604));
#86418=CARTESIAN_POINT('Ctrl Pts',(-52.5838835896748,3.91697713254828,133.781789871393));
#86419=CARTESIAN_POINT('Ctrl Pts',(-52.5916579237939,3.99822470497009,133.671781400682));
#86420=CARTESIAN_POINT('Ctrl Pts',(-52.599432257913,4.07483948018898,133.558424210367));
#86421=CARTESIAN_POINT('Ctrl Pts',(-52.6071970108602,4.15135983454468,133.445206722659));
#86422=CARTESIAN_POINT('Ctrl Pts',(-52.6149617638072,4.22325853509124,133.328649047652));
#86423=CARTESIAN_POINT('Ctrl Pts',(-52.6227265167543,4.29023235922937,133.209166091263));
#86424=CARTESIAN_POINT('Ctrl Pts',(-52.6304835576394,4.35713966402121,133.08980180703));
#86425=CARTESIAN_POINT('Ctrl Pts',(-52.6382405985244,4.41913163669655,132.967518362188));
#86426=CARTESIAN_POINT('Ctrl Pts',(-52.6459976394094,4.47594810870774,132.842759889214));
#86427=CARTESIAN_POINT('Ctrl Pts',(-52.6537488306496,4.53272173497543,132.718095497575));
#86428=CARTESIAN_POINT('Ctrl Pts',(-52.6615000218899,4.58432746765317,132.590960147201));
#86429=CARTESIAN_POINT('Ctrl Pts',(-52.66925121313,4.63055105886011,132.461822518724));
#86430=CARTESIAN_POINT('Ctrl Pts',(-52.6769991099071,4.67675500380774,132.332739777183));
#86431=CARTESIAN_POINT('Ctrl Pts',(-52.6847470066842,4.71758122557412,132.20165681748));
#86432=CARTESIAN_POINT('Ctrl Pts',(-52.6924949034613,4.75286370202761,132.069062041796));
#86433=CARTESIAN_POINT('Ctrl Pts',(-52.7002411795455,4.78813879814762,131.93649500208));
#86434=CARTESIAN_POINT('Ctrl Pts',(-52.7079874556296,4.81787235505548,131.802417152979));
#86435=CARTESIAN_POINT('Ctrl Pts',(-52.7157337317137,4.84194841727673,131.667331409037));
#86436=CARTESIAN_POINT('Ctrl Pts',(-52.7234800649791,4.86602465722201,131.532244667922));
#86437=CARTESIAN_POINT('Ctrl Pts',(-52.7312263982445,4.88444325054703,131.396150402019));
#86438=CARTESIAN_POINT('Ctrl Pts',(-52.7389727315098,4.89713957164911,131.259560659623));
#86439=CARTESIAN_POINT('Ctrl Pts',(-52.7467207995128,4.90983873600426,131.122940328901));
#86440=CARTESIAN_POINT('Ctrl Pts',(-52.7544688675158,4.91681304199492,130.985824690103));
#86441=CARTESIAN_POINT('Ctrl Pts',(-52.7622169355188,4.91804986453024,130.848729441013));
#86442=CARTESIAN_POINT('Ctrl Pts',(-52.7699732382607,4.91928800157527,130.711488485461));
#86443=CARTESIAN_POINT('Ctrl Pts',(-52.7777295410026,4.91477647048875,130.574268354479));
#86444=CARTESIAN_POINT('Ctrl Pts',(-52.7854858437445,4.90455480649529,130.437583829064));
#86445=CARTESIAN_POINT('Ctrl Pts',(-52.7932462862587,4.894327686892,130.300826351003));
#86446=CARTESIAN_POINT('Ctrl Pts',(-52.8010067287729,4.87838440706759,130.164605436252));
#86447=CARTESIAN_POINT('Ctrl Pts',(-52.8087671712871,4.85681613228064,130.029428285218));
#86448=CARTESIAN_POINT('Ctrl Pts',(-52.8165400715525,4.83521323418427,129.894034135821));
#86449=CARTESIAN_POINT('Ctrl Pts',(-52.8243129718181,4.80796737457661,129.759687481794));
#86450=CARTESIAN_POINT('Ctrl Pts',(-52.8320858720835,4.77522055981481,129.626883795025));
#86451=CARTESIAN_POINT('Ctrl Pts',(-52.8395762078452,4.74366417425527,129.498907856787));
#86452=CARTESIAN_POINT('Ctrl Pts',(-52.8470665436069,4.70699992274369,129.372364947801));
#86453=CARTESIAN_POINT('Ctrl Pts',(-52.8545568793686,4.66539733576304,129.247681215134));
#86454=CARTESIAN_POINT('Ctrl Pts',(-52.8623312134877,4.62221737405043,129.118270060842));
#86455=CARTESIAN_POINT('Ctrl Pts',(-52.8701055476068,4.57358042951609,128.990451911587));
#86456=CARTESIAN_POINT('Ctrl Pts',(-52.8778798817259,4.5196219722879,128.864721401085));
#86457=CARTESIAN_POINT('Ctrl Pts',(-52.885644634673,4.46573001403592,128.739145842199));
#86458=CARTESIAN_POINT('Ctrl Pts',(-52.89340938762,4.40652974483713,128.615653158733));
#86459=CARTESIAN_POINT('Ctrl Pts',(-52.9011741405671,4.3422063375672,128.494722727227));
#86460=CARTESIAN_POINT('Ctrl Pts',(-52.9089311814521,4.27794681721208,128.37391240553));
#86461=CARTESIAN_POINT('Ctrl Pts',(-52.9166882223371,4.20857446728899,128.255659614338));
#86462=CARTESIAN_POINT('Ctrl Pts',(-52.9244452632221,4.13432232157438,128.140423305272));
#86463=CARTESIAN_POINT('Ctrl Pts',(-52.9321964544622,4.06012616998055,128.025273896803));
#86464=CARTESIAN_POINT('Ctrl Pts',(-52.9399476457024,3.98105775810385,127.913136770021));
#86465=CARTESIAN_POINT('Ctrl Pts',(-52.9476988369425,3.89739559401976,127.804445511065));
#86466=CARTESIAN_POINT('Ctrl Pts',(-52.9554467337196,3.81376898858717,127.695800448793));
#86467=CARTESIAN_POINT('Ctrl Pts',(-52.9631946304966,3.72555275222789,127.590598650564));
#86468=CARTESIAN_POINT('Ctrl Pts',(-52.9709425272737,3.63306805251157,127.489243788807));
#86469=CARTESIAN_POINT('Ctrl Pts',(-52.9786888033578,3.5406026986007,127.387910128303));
#86470=CARTESIAN_POINT('Ctrl Pts',(-52.986435079442,3.44387092066199,127.290422092306));
#86471=CARTESIAN_POINT('Ctrl Pts',(-52.9941813555261,3.34323315817787,127.197149075036));
#86472=CARTESIAN_POINT('Ctrl Pts',(-53.0019276887914,3.24259465280851,127.103875369246));
#86473=CARTESIAN_POINT('Ctrl Pts',(-53.0096740220567,3.13805039210655,127.014817010033));
#86474=CARTESIAN_POINT('Ctrl Pts',(-53.0174203553221,3.02999624508699,126.930305143356));
#86475=CARTESIAN_POINT('Ctrl Pts',(-53.025168423325,2.92191790009055,126.845774350832));
#86476=CARTESIAN_POINT('Ctrl Pts',(-53.032916491328,2.81032841259863,126.765792317674));
#86477=CARTESIAN_POINT('Ctrl Pts',(-53.040664559331,2.6956548295922,126.690648412976));
#86478=CARTESIAN_POINT('Ctrl Pts',(-53.0484208620729,2.58085937013712,126.615424644441));
#86479=CARTESIAN_POINT('Ctrl Pts',(-53.0561771648148,2.46297359491387,126.545049490733));
#86480=CARTESIAN_POINT('Ctrl Pts',(-53.0639334675567,2.34245197350996,126.479767941452));
#86481=CARTESIAN_POINT('Ctrl Pts',(-53.0716939100708,2.2218660260877,126.414451549442));
#86482=CARTESIAN_POINT('Ctrl Pts',(-53.0794543525849,2.0986417803501,126.354234350491));
#86483=CARTESIAN_POINT('Ctrl Pts',(-53.0872147950991,1.9732552354135,126.299313798895));
#86484=CARTESIAN_POINT('Ctrl Pts',(-53.0949876953645,1.84766740886368,126.244305083955));
#86485=CARTESIAN_POINT('Ctrl Pts',(-53.10276059563,1.71991071130153,126.194610149184));
#86486=CARTESIAN_POINT('Ctrl Pts',(-53.1105334958954,1.59047875516304,126.150377335272));
#86487=CARTESIAN_POINT('Ctrl Pts',(-53.1180238316574,1.46575197664943,126.107752495561));
#86488=CARTESIAN_POINT('Ctrl Pts',(-53.1255141674195,1.33946991991614,126.070199635451));
#86489=CARTESIAN_POINT('Ctrl Pts',(-53.1330045031815,1.21208274992882,126.037806467048));
#86490=CARTESIAN_POINT('Ctrl Pts',(-53.1407788373006,1.07986565667348,126.004185101818));
#86491=CARTESIAN_POINT('Ctrl Pts',(-53.1485531714196,0.946039171163907,
125.976015908921));
#86492=CARTESIAN_POINT('Ctrl Pts',(-53.1563275055387,0.811092667664798,
125.953452275105));
#86493=CARTESIAN_POINT('Ctrl Pts',(-53.1640922584857,0.676312473670737,
125.930916448951));
#86494=CARTESIAN_POINT('Ctrl Pts',(-53.1718570114329,0.54041539002685,125.913972500176));
#86495=CARTESIAN_POINT('Ctrl Pts',(-53.17962176438,0.40390482025721,125.902723752327));
#86496=CARTESIAN_POINT('Ctrl Pts',(-53.1873788052649,0.267529834709927,
125.891486176892));
#86497=CARTESIAN_POINT('Ctrl Pts',(-53.1951358461499,0.130542962740503,
125.885932577486));
#86498=CARTESIAN_POINT('Ctrl Pts',(-53.2028928870349,-0.00654370620673618,
125.886114970752));
#86499=CARTESIAN_POINT('Ctrl Pts',(-53.210644078275,-0.143526997030357,
125.886297226473));
#86500=CARTESIAN_POINT('Ctrl Pts',(-53.2183952695151,-0.280609545653028,
125.892206864592));
#86501=CARTESIAN_POINT('Ctrl Pts',(-53.2261464607552,-0.417276023358432,
125.903843932274));
#86502=CARTESIAN_POINT('Ctrl Pts',(-53.2338943575323,-0.553884414165485,
125.915476053891));
#86503=CARTESIAN_POINT('Ctrl Pts',(-53.2416422543094,-0.690076697039048,
125.932830730314));
#86504=CARTESIAN_POINT('Ctrl Pts',(-53.2493901510864,-0.825339652014751,
125.955855948979));
#86505=CARTESIAN_POINT('Ctrl Pts',(-53.2571364271705,-0.960574312896021,
125.978876351264));
#86506=CARTESIAN_POINT('Ctrl Pts',(-53.2648827032546,-1.09487964736569,
126.007564870896));
#86507=CARTESIAN_POINT('Ctrl Pts',(-53.2726289793387,-1.22775004726036,
126.041817926529));
#86508=CARTESIAN_POINT('Ctrl Pts',(-53.280375312604,-1.36062142797415,126.07607123501));
#86509=CARTESIAN_POINT('Ctrl Pts',(-53.2881216458693,-1.49205747438903,
126.115889063859));
#86510=CARTESIAN_POINT('Ctrl Pts',(-53.2958679791347,-1.62156560715783,
126.161117349743));
#86511=CARTESIAN_POINT('Ctrl Pts',(-53.3036160471376,-1.75110274237485,
126.206355764188));
#86512=CARTESIAN_POINT('Ctrl Pts',(-53.3113641151406,-1.87871073579389,
126.257006917801));
#86513=CARTESIAN_POINT('Ctrl Pts',(-53.3191121831436,-2.00391530367527,
126.312867934927));
#86514=CARTESIAN_POINT('Ctrl Pts',(-53.3268684858854,-2.12925294046152,
126.368788321808));
#86515=CARTESIAN_POINT('Ctrl Pts',(-53.3346247886273,-2.252181691432,126.429929473614));
#86516=CARTESIAN_POINT('Ctrl Pts',(-53.3423810913692,-2.37224978798514,
126.496041455073));
#86517=CARTESIAN_POINT('Ctrl Pts',(-53.3501415338833,-2.49238196849675,
126.562188722488));
#86518=CARTESIAN_POINT('Ctrl Pts',(-53.3579019763974,-2.60965011815424,
126.633311903399));
#86519=CARTESIAN_POINT('Ctrl Pts',(-53.3656624189116,-2.72363082391754,
126.709117255139));
#86520=CARTESIAN_POINT('Ctrl Pts',(-53.373435319177,-2.83779450162847,126.785044296359));
#86521=CARTESIAN_POINT('Ctrl Pts',(-53.3812082194424,-2.94865987334772,
126.865668298165));
#86522=CARTESIAN_POINT('Ctrl Pts',(-53.3889811197078,-3.05583532627483,
126.950654152202));
#86523=CARTESIAN_POINT('Ctrl Pts',(-53.39647145547,-3.15911468153169,127.032550556379));
#86524=CARTESIAN_POINT('Ctrl Pts',(-53.4039617912322,-3.25896750257098,
127.118496989036));
#86525=CARTESIAN_POINT('Ctrl Pts',(-53.4114521269944,-3.35507666955602,
127.20816212417));
#86526=CARTESIAN_POINT('Ctrl Pts',(-53.4191092801371,-3.45332628524492,
127.299824192879));
#86527=CARTESIAN_POINT('Ctrl Pts',(-53.4267664332797,-3.54799461589064,
127.395681804218));
#86528=CARTESIAN_POINT('Ctrl Pts',(-53.4344235864223,-3.63869382386666,
127.495419651236));
#86529=CARTESIAN_POINT('Ctrl Pts',(-53.4420718673701,-3.72928794042992,
127.595041933946));
#86530=CARTESIAN_POINT('Ctrl Pts',(-53.449720148318,-3.81592180784249,127.69853521981));
#86531=CARTESIAN_POINT('Ctrl Pts',(-53.4573684292659,-3.89824149798524,
127.805544803634));
#86532=CARTESIAN_POINT('Ctrl Pts',(-53.465009622384,-3.98048490066586,127.912455219331));
#86533=CARTESIAN_POINT('Ctrl Pts',(-53.4726508155022,-4.05842183125482,
128.022875136013));
#86534=CARTESIAN_POINT('Ctrl Pts',(-53.4802920086204,-4.1317364140721,128.136414353652));
#86535=CARTESIAN_POINT('Ctrl Pts',(-53.4879278738848,-4.20499987799149,
128.2498744056));
#86536=CARTESIAN_POINT('Ctrl Pts',(-53.4955637391492,-4.27364718674857,
128.366449094643));
#86537=CARTESIAN_POINT('Ctrl Pts',(-53.5031996044137,-4.33740419922716,
128.48571707553));
#86538=CARTESIAN_POINT('Ctrl Pts',(-53.5108322038416,-4.4011339430232,128.60493404586));
#86539=CARTESIAN_POINT('Ctrl Pts',(-53.5184648032694,-4.45997736130885,
128.726841661266));
#86540=CARTESIAN_POINT('Ctrl Pts',(-53.5260974026973,-4.5137051911607,128.850992114239));
#86541=CARTESIAN_POINT('Ctrl Pts',(-53.5337303321047,-4.56743534382382,
128.9751479346));
#86542=CARTESIAN_POINT('Ctrl Pts',(-53.5413632615123,-4.61604929520416,
129.101546420496));
#86543=CARTESIAN_POINT('Ctrl Pts',(-53.5489961909197,-4.6593651655302,129.229718017881));
#86544=CARTESIAN_POINT('Ctrl Pts',(-53.55591934613,-4.6986531606534,129.34597113839));
#86545=CARTESIAN_POINT('Ctrl Pts',(-53.5628425013403,-4.73358309749759,
129.463682473335));
#86546=CARTESIAN_POINT('Ctrl Pts',(-53.5697656565506,-4.76405452823409,
129.582490119308));
#86547=CARTESIAN_POINT('Origin',(213.235140564004,0.,130.804360617566));
#86548=CARTESIAN_POINT('',(-55.665415119611,-4.764054528234,129.582490119308));
#86549=CARTESIAN_POINT('',(-55.3197786156161,-4.76405452823412,129.582490119309));
#86550=CARTESIAN_POINT('',(213.235140564004,-4.76405452823405,129.582490119308));
#86551=CARTESIAN_POINT('',(-53.9851405640441,-4.91824877609614,130.800890901613));
#86552=CARTESIAN_POINT('Ctrl Pts',(-53.9851405640439,-4.91824877609614,
130.800890901613));
#86553=CARTESIAN_POINT('Ctrl Pts',(-53.9927972686402,-4.91834379071892,
130.935572114287));
#86554=CARTESIAN_POINT('Ctrl Pts',(-54.0004539732365,-4.91290248423804,
131.070468642337));
#86555=CARTESIAN_POINT('Ctrl Pts',(-54.0081106778327,-4.90189833130391,
131.205079736226));
#86556=CARTESIAN_POINT('Ctrl Pts',(-54.0157593497178,-4.89090572291623,
131.339549608521));
#86557=CARTESIAN_POINT('Ctrl Pts',(-54.0234080216029,-4.87436190749982,
131.473734243646));
#86558=CARTESIAN_POINT('Ctrl Pts',(-54.031056693488,-4.85229238178572,131.607131882725));
#86559=CARTESIAN_POINT('Ctrl Pts',(-54.0386992936412,-4.8302403754848,131.740423626987));
#86560=CARTESIAN_POINT('Ctrl Pts',(-54.0463418937945,-4.80267145024832,
131.872929222193));
#86561=CARTESIAN_POINT('Ctrl Pts',(-54.0539844939477,-4.76966296323101,
132.004151549221));
#86562=CARTESIAN_POINT('Ctrl Pts',(-54.061623586964,-4.73666962358229,132.135313659222));
#86563=CARTESIAN_POINT('Ctrl Pts',(-54.0692626799804,-4.6982417827371,132.265193281768));
#86564=CARTESIAN_POINT('Ctrl Pts',(-54.0769017729967,-4.65450790482404,
132.393303419063));
#86565=CARTESIAN_POINT('Ctrl Pts',(-54.0845392166914,-4.61078346929268,
132.521385896685));
#86566=CARTESIAN_POINT('Ctrl Pts',(-54.0921766603861,-4.56175540431634,
132.647699267331));
#86567=CARTESIAN_POINT('Ctrl Pts',(-54.0998141040808,-4.50760190068792,
132.771772157487));
#86568=CARTESIAN_POINT('Ctrl Pts',(-54.1074516622702,-4.45344758523193,
132.895846907648));
#86569=CARTESIAN_POINT('Ctrl Pts',(-54.1150892204595,-4.39416783982267,
133.01768074119));
#86570=CARTESIAN_POINT('Ctrl Pts',(-54.1227267786489,-4.32998858797518,
133.136823241169));
#86571=CARTESIAN_POINT('Ctrl Pts',(-54.1303662150348,-4.26579355343277,
133.255995040177));
#86572=CARTESIAN_POINT('Ctrl Pts',(-54.1380056514206,-4.19669680812159,
133.372473835057));
#86573=CARTESIAN_POINT('Ctrl Pts',(-54.1456450878066,-4.12296942876577,
133.485835240225));
#86574=CARTESIAN_POINT('Ctrl Pts',(-54.1532924949838,-4.04916512416028,
133.599314923765));
#86575=CARTESIAN_POINT('Ctrl Pts',(-54.160939902161,-3.97072076004615,133.709670386039));
#86576=CARTESIAN_POINT('Ctrl Pts',(-54.1685873093382,-3.88794997798313,
133.816507365519));
#86577=CARTESIAN_POINT('Ctrl Pts',(-54.1762391488307,-3.80513122329416,
133.923406266008));
#86578=CARTESIAN_POINT('Ctrl Pts',(-54.1838909883232,-3.7179813182745,134.026782316829));
#86579=CARTESIAN_POINT('Ctrl Pts',(-54.1915428278157,-3.62685222945442,
134.126276626167));
#86580=CARTESIAN_POINT('Ctrl Pts',(-54.1992059243301,-3.53558907585785,
134.225917306796));
#86581=CARTESIAN_POINT('Ctrl Pts',(-54.2068690208445,-3.44033533527844,
134.321664560761));
#86582=CARTESIAN_POINT('Ctrl Pts',(-54.2145321173589,-3.34147792538912,
134.413198150157));
#86583=CARTESIAN_POINT('Ctrl Pts',(-54.2187567456638,-3.2869783100992,134.463660178383));
#86584=CARTESIAN_POINT('Ctrl Pts',(-54.2229813739687,-3.23138400646271,
134.51284229533));
#86585=CARTESIAN_POINT('Ctrl Pts',(-54.2272060022736,-3.17476362491381,
134.56069646363));
#86586=CARTESIAN_POINT('Ctrl Pts',(-54.2349803363927,-3.07056847865618,
134.648759665055));
#86587=CARTESIAN_POINT('Ctrl Pts',(-54.2427546705117,-2.96254140538158,
134.732623740153));
#86588=CARTESIAN_POINT('Ctrl Pts',(-54.2505290046308,-2.85105540249286,
134.811936712217));
#86589=CARTESIAN_POINT('Ctrl Pts',(-54.2582937575779,-2.73970679613877,
134.891151938131));
#86590=CARTESIAN_POINT('Ctrl Pts',(-54.266058510525,-2.62490805742996,134.965826996443));
#86591=CARTESIAN_POINT('Ctrl Pts',(-54.2738232634721,-2.50706669629267,
135.035648795277));
#86592=CARTESIAN_POINT('Ctrl Pts',(-54.281580304357,-2.38934237685669,135.105401246116));
#86593=CARTESIAN_POINT('Ctrl Pts',(-54.2893373452421,-2.26858178304,135.170309832139));
#86594=CARTESIAN_POINT('Ctrl Pts',(-54.2970943861271,-2.14522267609269,
135.230103801764));
#86595=CARTESIAN_POINT('Ctrl Pts',(-54.3048455773673,-2.02195659520702,
135.289852680292));
#86596=CARTESIAN_POINT('Ctrl Pts',(-54.3125967686073,-1.89609625196496,
135.344494449653));
#86597=CARTESIAN_POINT('Ctrl Pts',(-54.3203479598475,-1.7681050506704,135.393803676619));
#86598=CARTESIAN_POINT('Ctrl Pts',(-54.3280958566245,-1.6401682490512,135.443091945849));
#86599=CARTESIAN_POINT('Ctrl Pts',(-54.3358437534017,-1.51010275475476,
135.48705204027));
#86600=CARTESIAN_POINT('Ctrl Pts',(-54.3435916501788,-1.37839284524093,
135.525506265255));
#86601=CARTESIAN_POINT('Ctrl Pts',(-54.3513379262628,-1.24671048660084,
135.563952446444));
#86602=CARTESIAN_POINT('Ctrl Pts',(-54.3590842023469,-1.11338477198998,
135.596894939508));
#86603=CARTESIAN_POINT('Ctrl Pts',(-54.366830478431,-0.978915688513234,
135.6242057538));
#86604=CARTESIAN_POINT('Ctrl Pts',(-54.3745768116964,-0.844445612415897,
135.651516769695));
#86605=CARTESIAN_POINT('Ctrl Pts',(-54.3823231449617,-0.708832533753829,
135.67319594605));
#86606=CARTESIAN_POINT('Ctrl Pts',(-54.3900694782271,-0.572586802527636,
135.689166388123));
#86607=CARTESIAN_POINT('Ctrl Pts',(-54.3978175462301,-0.436310560014969,
135.705140406667));
#86608=CARTESIAN_POINT('Ctrl Pts',(-54.4055656142329,-0.299401771247377,
135.715403101492));
#86609=CARTESIAN_POINT('Ctrl Pts',(-54.4133136822359,-0.16237568253322,
135.719929475819));
#86610=CARTESIAN_POINT('Ctrl Pts',(-54.4210699849777,-0.0252039608615334,
135.724460660829));
#86611=CARTESIAN_POINT('Ctrl Pts',(-54.4288262877196,0.112084918418896,
135.723243333739));
#86612=CARTESIAN_POINT('Ctrl Pts',(-54.4365825904614,0.24897537381797,135.716304665062));
#86613=CARTESIAN_POINT('Ctrl Pts',(-54.4443430329756,0.385938891775156,
135.709362293009));
#86614=CARTESIAN_POINT('Ctrl Pts',(-54.4521034754898,0.522503173023274,
135.696692530807));
#86615=CARTESIAN_POINT('Ctrl Pts',(-54.4598639180039,0.658158975501423,
135.678374346052));
#86616=CARTESIAN_POINT('Ctrl Pts',(-54.4676368182694,0.794032544716666,
135.66002675532));
#86617=CARTESIAN_POINT('Ctrl Pts',(-54.4754097185348,0.92899433573148,135.636012691109));
#86618=CARTESIAN_POINT('Ctrl Pts',(-54.4831826188003,1.06254561158124,135.606462228924));
#86619=CARTESIAN_POINT('Ctrl Pts',(-54.4906729545623,1.19124196215814,135.577986000473));
#86620=CARTESIAN_POINT('Ctrl Pts',(-54.4981632903242,1.31862827086018,135.544368988257));
#86621=CARTESIAN_POINT('Ctrl Pts',(-54.5056536260862,1.4442744450737,135.505770447586));
#86622=CARTESIAN_POINT('Ctrl Pts',(-54.5134279602053,1.57468453217258,135.465708431513));
#86623=CARTESIAN_POINT('Ctrl Pts',(-54.5212022943244,1.70363302552022,135.420152776365));
#86624=CARTESIAN_POINT('Ctrl Pts',(-54.5289766284435,1.83062218293633,135.369227043415));
#86625=CARTESIAN_POINT('Ctrl Pts',(-54.5367413813906,1.95745483756511,135.318364071879));
#86626=CARTESIAN_POINT('Ctrl Pts',(-54.5445061343378,2.0823326014182,135.262144334791));
#86627=CARTESIAN_POINT('Ctrl Pts',(-54.5522708872849,2.20477179236346,135.200741447988));
#86628=CARTESIAN_POINT('Ctrl Pts',(-54.5600279281699,2.32708937497868,135.139399547397));
#86629=CARTESIAN_POINT('Ctrl Pts',(-54.5677849690549,2.44697285740616,135.072884915926));
#86630=CARTESIAN_POINT('Ctrl Pts',(-54.57554200994,2.56395782802465,135.001419506671));
#86631=CARTESIAN_POINT('Ctrl Pts',(-54.5832932011801,2.68085457936631,134.930007990037));
#86632=CARTESIAN_POINT('Ctrl Pts',(-54.5910443924203,2.79485683729627,134.853653329756));
#86633=CARTESIAN_POINT('Ctrl Pts',(-54.5987955836605,2.90552445711169,134.772623548828));
#86634=CARTESIAN_POINT('Ctrl Pts',(-54.6065434804376,3.01614504023667,134.691628207718));
#86635=CARTESIAN_POINT('Ctrl Pts',(-54.6142913772147,3.12343348938125,134.605961928539));
#86636=CARTESIAN_POINT('Ctrl Pts',(-54.6220392739918,3.22697854122691,134.515936099347));
#86637=CARTESIAN_POINT('Ctrl Pts',(-54.6297855500759,3.3305019336799,134.425929101618));
#86638=CARTESIAN_POINT('Ctrl Pts',(-54.63753182616,3.43028319148311,134.331564624101));
#86639=CARTESIAN_POINT('Ctrl Pts',(-54.6452781022441,3.52594437723939,134.233194138038));
#86640=CARTESIAN_POINT('Ctrl Pts',(-54.6530244355095,3.62160626914468,134.134822925827));
#86641=CARTESIAN_POINT('Ctrl Pts',(-54.6607707687749,3.71314775574784,134.032445926349));
#86642=CARTESIAN_POINT('Ctrl Pts',(-54.6685171020402,3.8002282866856,133.92645094803));
#86643=CARTESIAN_POINT('Ctrl Pts',(-54.6762651700432,3.88732831870449,133.82043223287));
#86644=CARTESIAN_POINT('Ctrl Pts',(-54.6840132380463,3.96996515902742,133.710794228654));
#86645=CARTESIAN_POINT('Ctrl Pts',(-54.6917613060492,4.04783927394014,133.597956915324));
#86646=CARTESIAN_POINT('Ctrl Pts',(-54.6995176087911,4.12579615438902,133.484999677155));
#86647=CARTESIAN_POINT('Ctrl Pts',(-54.707273911533,4.19897997534989,133.368836659765));
#86648=CARTESIAN_POINT('Ctrl Pts',(-54.7150302142748,4.26713491175729,133.249916322792));
#86649=CARTESIAN_POINT('Ctrl Pts',(-54.722790656789,4.33532622450636,133.130932514454));
#86650=CARTESIAN_POINT('Ctrl Pts',(-54.7305510993032,4.3984831245225,133.009188800992));
#86651=CARTESIAN_POINT('Ctrl Pts',(-54.7383115418174,4.45639679170617,132.885156306088));
#86652=CARTESIAN_POINT('Ctrl Pts',(-54.7460844420828,4.51440342704965,132.760924703212));
#86653=CARTESIAN_POINT('Ctrl Pts',(-54.7538573423483,4.56714985938415,132.634397337832));
#86654=CARTESIAN_POINT('Ctrl Pts',(-54.7616302426137,4.61447594540314,132.50606412047));
#86655=CARTESIAN_POINT('Ctrl Pts',(-54.7691205783756,4.66008160898704,132.382396138813));
#86656=CARTESIAN_POINT('Ctrl Pts',(-54.7766109141375,4.70065407596304,132.257051613294));
#86657=CARTESIAN_POINT('Ctrl Pts',(-54.7841012498994,4.73609485676863,132.130478474391));
#86658=CARTESIAN_POINT('Ctrl Pts',(-54.7918755840184,4.77287938555128,131.999106276453));
#86659=CARTESIAN_POINT('Ctrl Pts',(-54.7996499181375,4.80425193306907,131.865994312623));
#86660=CARTESIAN_POINT('Ctrl Pts',(-54.8074242522565,4.83004741311189,131.731628135379));
#86661=CARTESIAN_POINT('Ctrl Pts',(-54.8151890052036,4.85581110253089,131.597427552441));
#86662=CARTESIAN_POINT('Ctrl Pts',(-54.8229537581507,4.87601132716498,131.46197621185));
#86663=CARTESIAN_POINT('Ctrl Pts',(-54.8307185110978,4.89053271292637,131.325774892684));
#86664=CARTESIAN_POINT('Ctrl Pts',(-54.8384755519828,4.90503967584271,131.189708850588));
#86665=CARTESIAN_POINT('Ctrl Pts',(-54.8462325928678,4.91387898316304,131.052894698526));
#86666=CARTESIAN_POINT('Ctrl Pts',(-54.8539896337528,4.91698634448713,130.915843130218));
#86667=CARTESIAN_POINT('Ctrl Pts',(-54.8617408249929,4.92009136252587,130.778894913562));
#86668=CARTESIAN_POINT('Ctrl Pts',(-54.8694920162329,4.91747302942635,130.641710026306));
#86669=CARTESIAN_POINT('Ctrl Pts',(-54.877243207473,4.90911893156643,130.504803647632));
#86670=CARTESIAN_POINT('Ctrl Pts',(-54.8849911042501,4.90076838442096,130.367955457821));
#86671=CARTESIAN_POINT('Ctrl Pts',(-54.8927390010272,4.88668694498166,130.231385930578));
#86672=CARTESIAN_POINT('Ctrl Pts',(-54.9004868978043,4.86691429496976,130.095609386231));
#86673=CARTESIAN_POINT('Ctrl Pts',(-54.9082331738884,4.84714578097,129.95986124341));
#86674=CARTESIAN_POINT('Ctrl Pts',(-54.9159794499725,4.82168848062965,129.82490614019));
#86675=CARTESIAN_POINT('Ctrl Pts',(-54.9237257260566,4.79063381226401,129.691252024799));
#86676=CARTESIAN_POINT('Ctrl Pts',(-54.931472059322,4.75957891465986,129.557596922803));
#86677=CARTESIAN_POINT('Ctrl Pts',(-54.9392183925873,4.72292665506641,129.425243208619));
#86678=CARTESIAN_POINT('Ctrl Pts',(-54.9469647258526,4.68081923190478,129.29468701684));
#86679=CARTESIAN_POINT('Ctrl Pts',(-54.9547127938556,4.63870237907779,129.164101587906));
#86680=CARTESIAN_POINT('Ctrl Pts',(-54.9624608618585,4.59112805173356,129.035314854411));
#86681=CARTESIAN_POINT('Ctrl Pts',(-54.9702089298615,4.53828768560231,128.908805831966));
#86682=CARTESIAN_POINT('Ctrl Pts',(-54.9779652326033,4.48539116010098,128.782162354227));
#86683=CARTESIAN_POINT('Ctrl Pts',(-54.9857215353451,4.42721756650751,128.657801784641));
#86684=CARTESIAN_POINT('Ctrl Pts',(-54.993477838087,4.36400592691846,128.536181759468));
#86685=CARTESIAN_POINT('Ctrl Pts',(-55.0012382806012,4.30076054937409,128.414496822027));
#86686=CARTESIAN_POINT('Ctrl Pts',(-55.0089987231153,4.23247196242981,128.295555682466));
#86687=CARTESIAN_POINT('Ctrl Pts',(-55.0167591656295,4.15942366341745,128.179788680906));
#86688=CARTESIAN_POINT('Ctrl Pts',(-55.0245320658949,4.08625810079059,128.063835839878));
#86689=CARTESIAN_POINT('Ctrl Pts',(-55.0323049661603,4.00831777993626,127.951067640908));
#86690=CARTESIAN_POINT('Ctrl Pts',(-55.0400778664257,3.9259283150813,127.841883625699));
#86691=CARTESIAN_POINT('Ctrl Pts',(-55.0475682021878,3.84653391479925,127.736668724458));
#86692=CARTESIAN_POINT('Ctrl Pts',(-55.05505853795,3.76300842497322,127.634782181162));
#86693=CARTESIAN_POINT('Ctrl Pts',(-55.0625488737121,3.67567546618837,127.536548975234));
#86694=CARTESIAN_POINT('Ctrl Pts',(-55.0703232078312,3.58503125172818,127.434591227447));
#86695=CARTESIAN_POINT('Ctrl Pts',(-55.0780975419503,3.48999801488191,127.336246346813));
#86696=CARTESIAN_POINT('Ctrl Pts',(-55.0858718760694,3.39089503157182,127.241915678011));
#86697=CARTESIAN_POINT('Ctrl Pts',(-55.0936366290165,3.29191418383131,127.147701263327));
#86698=CARTESIAN_POINT('Ctrl Pts',(-55.1014013819636,3.18887384964357,127.05749148407));
#86699=CARTESIAN_POINT('Ctrl Pts',(-55.1091661349107,3.0821329861155,126.97165409105));
#86700=CARTESIAN_POINT('Ctrl Pts',(-55.1169231757957,2.97549813911787,126.885901952939));
#86701=CARTESIAN_POINT('Ctrl Pts',(-55.1246802166807,2.86517037972825,126.804513802287));
#86702=CARTESIAN_POINT('Ctrl Pts',(-55.1324372575657,2.75154461850447,126.727819770858));
#86703=CARTESIAN_POINT('Ctrl Pts',(-55.1401884488058,2.63800454335172,126.651183574995));
#86704=CARTESIAN_POINT('Ctrl Pts',(-55.1479396400459,2.52117173942896,126.579234670298));
#86705=CARTESIAN_POINT('Ctrl Pts',(-55.155690831286,2.40147293170706,126.51226196763));
#86706=CARTESIAN_POINT('Ctrl Pts',(-55.1634387280631,2.28182499917135,126.445317730148));
#86707=CARTESIAN_POINT('Ctrl Pts',(-55.1711866248403,2.15931382607675,126.383345678585));
#86708=CARTESIAN_POINT('Ctrl Pts',(-55.1789345216173,2.03439357362095,126.326590430284));
#86709=CARTESIAN_POINT('Ctrl Pts',(-55.1866807977014,1.90949945178884,126.269847053958));
#86710=CARTESIAN_POINT('Ctrl Pts',(-55.1944270737855,1.78219760865962,126.218318471971));
#86711=CARTESIAN_POINT('Ctrl Pts',(-55.2021733498696,1.65296480929534,126.172202329928));
#86712=CARTESIAN_POINT('Ctrl Pts',(-55.2099196831349,1.52373105596406,126.126085847467));
#86713=CARTESIAN_POINT('Ctrl Pts',(-55.2176660164002,1.39256668617812,126.085382016074));
#86714=CARTESIAN_POINT('Ctrl Pts',(-55.2254123496656,1.25996597374079,126.050239373055));
#86715=CARTESIAN_POINT('Ctrl Pts',(-55.2331604176685,1.12733556629384,126.015088860084));
#86716=CARTESIAN_POINT('Ctrl Pts',(-55.2409084856714,0.993268553977209,
125.985502113809));
#86717=CARTESIAN_POINT('Ctrl Pts',(-55.2486565536744,0.858271421881679,
125.961576993566));
#86718=CARTESIAN_POINT('Ctrl Pts',(-55.2564128564162,0.723130813226935,
125.937626445421));
#86719=CARTESIAN_POINT('Ctrl Pts',(-55.2641691591581,0.587058495653427,
125.919349611736));
#86720=CARTESIAN_POINT('Ctrl Pts',(-55.2719254618999,0.450568688789894,
125.906792760029));
#86721=CARTESIAN_POINT('Ctrl Pts',(-55.2796859044141,0.314006033206624,
125.894229206352));
#86722=CARTESIAN_POINT('Ctrl Pts',(-55.2874463469283,0.177025834620456,
125.88739173735));
#86723=CARTESIAN_POINT('Ctrl Pts',(-55.2952067894425,0.0401433875962681,
125.886274448035));
#86724=CARTESIAN_POINT('Ctrl Pts',(-55.3029796897079,-0.0969587952835497,
125.885155365148));
#86725=CARTESIAN_POINT('Ctrl Pts',(-55.3107525899733,-0.233962522058218,
125.889774798408));
#86726=CARTESIAN_POINT('Ctrl Pts',(-55.3185254902387,-0.370355644534846,
125.900074761393));
#86727=CARTESIAN_POINT('Ctrl Pts',(-55.3260158260008,-0.501790533457566,
125.910000294779));
#86728=CARTESIAN_POINT('Ctrl Pts',(-55.333506161763,-0.632658135384008,
125.925200489566));
#86729=CARTESIAN_POINT('Ctrl Pts',(-55.3409964975251,-0.762510111089371,
125.945578733906));
#86730=CARTESIAN_POINT('Ctrl Pts',(-55.3487708316442,-0.897285463919555,
125.966729625573));
#86731=CARTESIAN_POINT('Ctrl Pts',(-55.3565451657633,-1.03139358309989,
125.993525969023));
#86732=CARTESIAN_POINT('Ctrl Pts',(-55.3643194998823,-1.16432422955083,
126.025916084982));
#86733=CARTESIAN_POINT('Ctrl Pts',(-55.3720842528294,-1.29709105086072,
126.058266283018));
#86734=CARTESIAN_POINT('Ctrl Pts',(-55.3798490057765,-1.42868291055205,
126.096196445239));
#86735=CARTESIAN_POINT('Ctrl Pts',(-55.3876137587236,-1.55859638436842,
126.139603349161));
#86736=CARTESIAN_POINT('Ctrl Pts',(-55.3953707996087,-1.68838082629131,
126.182967140735));
#86737=CARTESIAN_POINT('Ctrl Pts',(-55.4031278404937,-1.81648983132267,
126.23179672591));
#86738=CARTESIAN_POINT('Ctrl Pts',(-55.4108848813787,-1.94243219145681,
126.285938299534));
#86739=CARTESIAN_POINT('Ctrl Pts',(-55.4186360726188,-2.06827957747696,
126.340039044575));
#86740=CARTESIAN_POINT('Ctrl Pts',(-55.4263872638589,-2.191963213018,126.399443650954));
#86741=CARTESIAN_POINT('Ctrl Pts',(-55.434138455099,-2.31300937391758,126.463949266246));
#86742=CARTESIAN_POINT('Ctrl Pts',(-55.4418863518761,-2.43400408696978,
126.528427464931));
#86743=CARTESIAN_POINT('Ctrl Pts',(-55.4496342486532,-2.5523632106494,126.59800217693));
#86744=CARTESIAN_POINT('Ctrl Pts',(-55.4573821454303,-2.66763545623592,
126.672423525217));
#86745=CARTESIAN_POINT('Ctrl Pts',(-55.4651284215144,-2.7828835893538,126.746829306161));
#86746=CARTESIAN_POINT('Ctrl Pts',(-55.4728746975985,-2.89504580047696,
126.826079494942));
#86747=CARTESIAN_POINT('Ctrl Pts',(-55.4806209736826,-3.00369810159739,
126.909879807887));
#86748=CARTESIAN_POINT('Ctrl Pts',(-55.4883673069479,-3.11235120476458,
126.993680739427));
#86749=CARTESIAN_POINT('Ctrl Pts',(-55.4961136402133,-3.21749403664578,
127.082031623382));
#86750=CARTESIAN_POINT('Ctrl Pts',(-55.5038599734786,-3.31873446153417,
127.174596901244));
#86751=CARTESIAN_POINT('Ctrl Pts',(-55.5116080414816,-3.41999755851294,
127.267182908458));
#86752=CARTESIAN_POINT('Ctrl Pts',(-55.5193561094845,-3.51735622102066,
127.363984923837));
#86753=CARTESIAN_POINT('Ctrl Pts',(-55.5271041774875,-3.61045434966125,
127.464629722492));
#86754=CARTESIAN_POINT('Ctrl Pts',(-55.5348604802293,-3.70365142410148,
127.565381487637));
#86755=CARTESIAN_POINT('Ctrl Pts',(-55.5426167829712,-3.79257865330724,
127.669983907137));
#86756=CARTESIAN_POINT('Ctrl Pts',(-55.5503730857131,-3.8769191628354,127.778029362178));
#86757=CARTESIAN_POINT('Ctrl Pts',(-55.5581335282272,-3.96130468743271,
127.886132484331));
#86758=CARTESIAN_POINT('Ctrl Pts',(-55.5658939707413,-4.04109838701436,
127.997681985872));
#86759=CARTESIAN_POINT('Ctrl Pts',(-55.5736544132554,-4.11602670031402,
128.112241143099));
#86760=CARTESIAN_POINT('Ctrl Pts',(-55.5814273135208,-4.19107529519421,
128.226984200857));
#86761=CARTESIAN_POINT('Ctrl Pts',(-55.5892002137863,-4.2612426959874,128.344746232852));
#86762=CARTESIAN_POINT('Ctrl Pts',(-55.5969731140517,-4.32630085970409,
128.46506501123));
#86763=CARTESIAN_POINT('Ctrl Pts',(-55.6044634498137,-4.38899399529805,
128.581009898949));
#86764=CARTESIAN_POINT('Ctrl Pts',(-55.6119537855758,-4.44694277639168,
128.699328595379));
#86765=CARTESIAN_POINT('Ctrl Pts',(-55.6194441213379,-4.49998614696551,
128.819591678969));
#86766=CARTESIAN_POINT('Ctrl Pts',(-55.6279986247142,-4.56056549975874,
128.956940789518));
#86767=CARTESIAN_POINT('Ctrl Pts',(-55.6365531280906,-4.61491201809283,
129.09719976048));
#86768=CARTESIAN_POINT('Ctrl Pts',(-55.645107631467,-4.66276424856004,129.239811920705));
#86769=CARTESIAN_POINT('Ctrl Pts',(-55.6518767941817,-4.70062963010714,
129.352660659571));
#86770=CARTESIAN_POINT('Ctrl Pts',(-55.6586459568963,-4.73442942243786,
129.466982281433));
#86771=CARTESIAN_POINT('Ctrl Pts',(-55.665415119611,-4.764054528234,129.582490119308));
#86772=CARTESIAN_POINT('Ctrl Pts',(-53.9150733197311,-4.76405452823399,
129.582490119308));
#86773=CARTESIAN_POINT('Ctrl Pts',(-53.922847823381,-4.79808409324873,129.71517087683));
#86774=CARTESIAN_POINT('Ctrl Pts',(-53.930622327031,-4.82652590896521,129.849115295931));
#86775=CARTESIAN_POINT('Ctrl Pts',(-53.9383968306809,-4.84931793657393,
129.983812866047));
#86776=CARTESIAN_POINT('Ctrl Pts',(-53.9418506799408,-4.85944337110096,
130.043652712268));
#86777=CARTESIAN_POINT('Ctrl Pts',(-53.9453045292007,-4.86845444587565,
130.103641154042));
#86778=CARTESIAN_POINT('Ctrl Pts',(-53.9487583784606,-4.87634901943149,
130.163733344349));
#86779=CARTESIAN_POINT('Ctrl Pts',(-53.9608857736432,-4.90406899390232,
130.374733212729));
#86780=CARTESIAN_POINT('Ctrl Pts',(-53.9730131688258,-4.91809828314246,
130.587570370039));
#86781=CARTESIAN_POINT('Ctrl Pts',(-53.9851405640084,-4.9182487760957,130.800890900986));
#86782=CARTESIAN_POINT('',(-53.6398594359473,-4.9182481978369,130.808570958887));
#86783=CARTESIAN_POINT('Ctrl Pts',(-53.5697656565506,-4.76405452823409,
129.582490119308));
#86784=CARTESIAN_POINT('Ctrl Pts',(-53.5774022064258,-4.7976658793482,129.713540267179));
#86785=CARTESIAN_POINT('Ctrl Pts',(-53.5850387563011,-4.82585170671341,
129.845924118334));
#86786=CARTESIAN_POINT('Ctrl Pts',(-53.5926753061764,-4.84852592904176,
129.979145871024));
#86787=CARTESIAN_POINT('Ctrl Pts',(-53.6005393278049,-4.87187555390005,
130.116335932197));
#86788=CARTESIAN_POINT('Ctrl Pts',(-53.6084033494333,-4.889380025036,130.254414134824));
#86789=CARTESIAN_POINT('Ctrl Pts',(-53.6162673710618,-4.90100283232545,
130.392833826168));
#86790=CARTESIAN_POINT('Ctrl Pts',(-53.6241313926903,-4.9126256396149,130.531253517513));
#86791=CARTESIAN_POINT('Ctrl Pts',(-53.6319954143188,-4.91836681143365,
130.670014232959));
#86792=CARTESIAN_POINT('Ctrl Pts',(-53.6398594359473,-4.9182481978369,130.808570958887));
#86793=CARTESIAN_POINT('Ctrl Pts',(-53.639859435991,-4.91824819783625,130.808570959657));
#86794=CARTESIAN_POINT('Ctrl Pts',(-53.6516810374523,-4.91806989174917,
131.016856550807));
#86795=CARTESIAN_POINT('Ctrl Pts',(-53.6635026389136,-4.90465736337878,
131.224596674198));
#86796=CARTESIAN_POINT('Ctrl Pts',(-53.6753242403749,-4.87823520261405,
131.4304631415));
#86797=CARTESIAN_POINT('Ctrl Pts',(-53.6801827438523,-4.86737608505906,
131.515071216857));
#86798=CARTESIAN_POINT('Ctrl Pts',(-53.6850412473298,-4.85432000492346,
131.599363263414));
#86799=CARTESIAN_POINT('Ctrl Pts',(-53.6898997508072,-4.83908453432629,
131.683248512661));
#86800=CARTESIAN_POINT('Ctrl Pts',(-53.6976740849262,-4.81470549674104,
131.817477490439));
#86801=CARTESIAN_POINT('Ctrl Pts',(-53.7054484190455,-4.78469864489195,
131.950903951438));
#86802=CARTESIAN_POINT('Ctrl Pts',(-53.7132227531646,-4.74912788750124,
132.083019043674));
#86803=CARTESIAN_POINT('Ctrl Pts',(-53.7209875061117,-4.71360096789001,
132.214971315867));
#86804=CARTESIAN_POINT('Ctrl Pts',(-53.7287522590588,-4.67252388682418,
132.345615061045));
#86805=CARTESIAN_POINT('Ctrl Pts',(-53.7365170120059,-4.62601191785663,
132.474449476983));
#86806=CARTESIAN_POINT('Ctrl Pts',(-53.744274052891,-4.57954614523229,132.603155932763));
#86807=CARTESIAN_POINT('Ctrl Pts',(-53.7520310937759,-4.52765635888517,
132.730056270159));
#86808=CARTESIAN_POINT('Ctrl Pts',(-53.759788134661,-4.47050810731524,132.854663113523));
#86809=CARTESIAN_POINT('Ctrl Pts',(-53.7675393259011,-4.41340295168643,
132.979175989897));
#86810=CARTESIAN_POINT('Ctrl Pts',(-53.7752905171413,-4.35104738614633,
133.101398460851));
#86811=CARTESIAN_POINT('Ctrl Pts',(-53.7830417083814,-4.28365557277662,
133.220861806541));
#86812=CARTESIAN_POINT('Ctrl Pts',(-53.7907896051585,-4.21629240272533,
133.340274377123));
#86813=CARTESIAN_POINT('Ctrl Pts',(-53.7985375019356,-4.1438974339068,133.456929815051));
#86814=CARTESIAN_POINT('Ctrl Pts',(-53.8062853987127,-4.06673130107604,
133.570382957922));
#86815=CARTESIAN_POINT('Ctrl Pts',(-53.8140316747969,-3.98958130973666,
133.683812368842));
#86816=CARTESIAN_POINT('Ctrl Pts',(-53.821777950881,-3.9076623592502,133.794040494006));
#86817=CARTESIAN_POINT('Ctrl Pts',(-53.8295242269652,-3.82127882308466,
133.9006505295));
#86818=CARTESIAN_POINT('Ctrl Pts',(-53.8372705602306,-3.73489464925548,
134.007261351966));
#86819=CARTESIAN_POINT('Ctrl Pts',(-53.8450168934961,-3.6440460701174,134.110253727704));
#86820=CARTESIAN_POINT('Ctrl Pts',(-53.8527632267615,-3.54907795772038,
134.209243686413));
#86821=CARTESIAN_POINT('Ctrl Pts',(-53.8605112947645,-3.45408857787319,
134.308255813237));
#86822=CARTESIAN_POINT('Ctrl Pts',(-53.8682593627674,-3.35497809962917,
134.4032634574));
#86823=CARTESIAN_POINT('Ctrl Pts',(-53.8760074307704,-3.25212818580093,
134.49391957842));
#86824=CARTESIAN_POINT('Ctrl Pts',(-53.8837637335123,-3.14916896186021,
134.584672049845));
#86825=CARTESIAN_POINT('Ctrl Pts',(-53.8915200362542,-3.04246265697053,
134.671063500558));
#86826=CARTESIAN_POINT('Ctrl Pts',(-53.8992763389961,-2.93242437667412,
134.752786929097));
#86827=CARTESIAN_POINT('Ctrl Pts',(-53.9070367815104,-2.82232736563432,
134.834553975889));
#86828=CARTESIAN_POINT('Ctrl Pts',(-53.9147972240246,-2.70889515881823,
134.911647816396));
#86829=CARTESIAN_POINT('Ctrl Pts',(-53.9225576665388,-2.59257091887731,
134.983805448293));
#86830=CARTESIAN_POINT('Ctrl Pts',(-53.9303305668043,-2.47605994493967,
135.056078914027));
#86831=CARTESIAN_POINT('Ctrl Pts',(-53.9381034670698,-2.35664800135264,
135.12340014428));
#86832=CARTESIAN_POINT('Ctrl Pts',(-53.9458763673353,-2.23480265526569,
135.185552253927));
#86833=CARTESIAN_POINT('Ctrl Pts',(-53.9533667030969,-2.11738669442517,
135.245444977833));
#86834=CARTESIAN_POINT('Ctrl Pts',(-53.9608570388586,-1.99771145989837,
135.300537748633));
#86835=CARTESIAN_POINT('Ctrl Pts',(-53.9683473746203,-1.87621011447327,
135.350679861619));
#86836=CARTESIAN_POINT('Ctrl Pts',(-53.9761217087393,-1.75010200860079,
135.402723128063));
#86837=CARTESIAN_POINT('Ctrl Pts',(-53.9838960428584,-1.62162711174686,
135.449597775056));
#86838=CARTESIAN_POINT('Ctrl Pts',(-53.9916703769775,-1.49124807972184,
135.491082523891));
#86839=CARTESIAN_POINT('Ctrl Pts',(-53.9994351299246,-1.36102972820148,
135.532516146481));
#86840=CARTESIAN_POINT('Ctrl Pts',(-54.0071998828717,-1.22891227968052,
135.568572970236));
#86841=CARTESIAN_POINT('Ctrl Pts',(-54.0149646358188,-1.09537938142757,
135.599079282226));
#86842=CARTESIAN_POINT('Ctrl Pts',(-54.0227216767038,-0.961979109931653,
135.629555294917));
#86843=CARTESIAN_POINT('Ctrl Pts',(-54.0304787175888,-0.827166565076972,
135.654491680145));
#86844=CARTESIAN_POINT('Ctrl Pts',(-54.0382357584738,-0.691441272809314,
135.673764280106));
#86845=CARTESIAN_POINT('Ctrl Pts',(-54.0459869497139,-0.55581833204016,
135.69302234645));
#86846=CARTESIAN_POINT('Ctrl Pts',(-54.0537381409541,-0.419284399413234,
135.70662507416));
#86847=CARTESIAN_POINT('Ctrl Pts',(-54.0614893321942,-0.282349582043312,
135.714499289337));
#86848=CARTESIAN_POINT('Ctrl Pts',(-54.0692372289713,-0.145472965623814,
135.722370157763));
#86849=CARTESIAN_POINT('Ctrl Pts',(-54.0769851257483,-0.00819619285073767,
135.724517333831));
#86850=CARTESIAN_POINT('Ctrl Pts',(-54.0847330225254,0.128965329089036,
135.720919475791));
#86851=CARTESIAN_POINT('Ctrl Pts',(-54.0924792986095,0.26609815979528,135.717322370346));
#86852=CARTESIAN_POINT('Ctrl Pts',(-54.1002255746936,0.403115397037173,
135.707982631359));
#86853=CARTESIAN_POINT('Ctrl Pts',(-54.1079718507777,0.5395018505838,135.692931044155));
#86854=CARTESIAN_POINT('Ctrl Pts',(-54.1157181840431,0.675889310904245,
135.677879345842));
#86855=CARTESIAN_POINT('Ctrl Pts',(-54.1234645173084,0.811645589632215,
135.657115758064));
#86856=CARTESIAN_POINT('Ctrl Pts',(-54.1312108505737,0.946261229910615,
135.630722886114));
#86857=CARTESIAN_POINT('Ctrl Pts',(-54.1389589185766,1.08090701642811,135.604324103664));
#86858=CARTESIAN_POINT('Ctrl Pts',(-54.1467069865796,1.21441127261649,135.572293603724));
#86859=CARTESIAN_POINT('Ctrl Pts',(-54.1544550545826,1.34627572541837,135.534764906171));
#86860=CARTESIAN_POINT('Ctrl Pts',(-54.1622113573245,1.47828032533025,135.497196322671));
#86861=CARTESIAN_POINT('Ctrl Pts',(-54.1699676600663,1.60864126378737,135.454117975627));
#86862=CARTESIAN_POINT('Ctrl Pts',(-54.1777239628081,1.73687587707863,135.405713163299));
#86863=CARTESIAN_POINT('Ctrl Pts',(-54.1854844053223,1.86517893304407,135.357282515865));
#86864=CARTESIAN_POINT('Ctrl Pts',(-54.1932448478364,1.99135304299268,135.30351989162));
#86865=CARTESIAN_POINT('Ctrl Pts',(-54.2010052903506,2.11493739538371,135.244655976673));
#86866=CARTESIAN_POINT('Ctrl Pts',(-54.208778190616,2.23872013634849,135.185697568145));
#86867=CARTESIAN_POINT('Ctrl Pts',(-54.2165510908815,2.35990446630394,135.121621687448));
#86868=CARTESIAN_POINT('Ctrl Pts',(-54.2243239911469,2.47805518218693,135.05270448036));
#86869=CARTESIAN_POINT('Ctrl Pts',(-54.231814326909,2.59191082194435,134.986292587341));
#86870=CARTESIAN_POINT('Ctrl Pts',(-54.239304662671,2.70294931782431,134.915385411484));
#86871=CARTESIAN_POINT('Ctrl Pts',(-54.246794998433,2.81080974262181,134.840265925336));
#86872=CARTESIAN_POINT('Ctrl Pts',(-54.2545693325521,2.92275972820834,134.762298261038));
#86873=CARTESIAN_POINT('Ctrl Pts',(-54.2623436666712,3.03164051620622,134.679545583393));
#86874=CARTESIAN_POINT('Ctrl Pts',(-54.2701180007903,3.13701586180466,134.592277531291));
#86875=CARTESIAN_POINT('Ctrl Pts',(-54.2778827537374,3.24226134170732,134.505117029264));
#86876=CARTESIAN_POINT('Ctrl Pts',(-54.2856475066844,3.3440096767891,134.41345247204));
#86877=CARTESIAN_POINT('Ctrl Pts',(-54.2934122596315,3.44185329427804,134.31759686968));
#86878=CARTESIAN_POINT('Ctrl Pts',(-54.3011693005165,3.53959973210662,134.221836472456));
#86879=CARTESIAN_POINT('Ctrl Pts',(-54.3089263414015,3.63344889270668,134.1218935857));
#86880=CARTESIAN_POINT('Ctrl Pts',(-54.3166833822865,3.72302631262759,134.018121364414));
#86881=CARTESIAN_POINT('Ctrl Pts',(-54.3244345735266,3.81253618151946,133.914427398567));
#86882=CARTESIAN_POINT('Ctrl Pts',(-54.3321857647668,3.89778046720273,133.806910140799));
#86883=CARTESIAN_POINT('Ctrl Pts',(-54.3399369560069,3.97842188104792,133.695959206392));
#86884=CARTESIAN_POINT('Ctrl Pts',(-54.347684852784,4.05902902014103,133.585055429092));
#86885=CARTESIAN_POINT('Ctrl Pts',(-54.355432749561,4.13503694903388,133.47072119339));
#86886=CARTESIAN_POINT('Ctrl Pts',(-54.3631806463381,4.20614912213341,133.353378590213));
#86887=CARTESIAN_POINT('Ctrl Pts',(-54.3709269224222,4.27724642009922,133.236060532579));
#86888=CARTESIAN_POINT('Ctrl Pts',(-54.3786731985063,4.343449796736,133.1157356933));
#86889=CARTESIAN_POINT('Ctrl Pts',(-54.3864194745904,4.40450667970366,132.992854156726));
#86890=CARTESIAN_POINT('Ctrl Pts',(-54.3941658078557,4.46556401337945,132.869971713069));
#86891=CARTESIAN_POINT('Ctrl Pts',(-54.4019121411211,4.52147460360996,132.744532884584));
#86892=CARTESIAN_POINT('Ctrl Pts',(-54.4096584743865,4.57203257469429,132.617010941935));
#86893=CARTESIAN_POINT('Ctrl Pts',(-54.4174065423894,4.62260186788564,132.48946044163));
#86894=CARTESIAN_POINT('Ctrl Pts',(-54.4251546103924,4.66781601262755,132.359826262256));
#86895=CARTESIAN_POINT('Ctrl Pts',(-54.4329026783953,4.70751801421561,132.228599785801));
#86896=CARTESIAN_POINT('Ctrl Pts',(-54.4406589811372,4.74726221156342,132.097233840286));
#86897=CARTESIAN_POINT('Ctrl Pts',(-54.448415283879,4.78148244963238,131.964272591924));
#86898=CARTESIAN_POINT('Ctrl Pts',(-54.4561715866209,4.8100720509136,131.830221196553));
#86899=CARTESIAN_POINT('Ctrl Pts',(-54.463932029135,4.83867691132587,131.696098253916));
#86900=CARTESIAN_POINT('Ctrl Pts',(-54.4716924716492,4.86164508131289,131.56088439015));
#86901=CARTESIAN_POINT('Ctrl Pts',(-54.4794529141634,4.87892156373866,131.425091990533));
#86902=CARTESIAN_POINT('Ctrl Pts',(-54.4872258144288,4.89622577990776,131.289081604902));
#86903=CARTESIAN_POINT('Ctrl Pts',(-54.4949987146943,4.90782001718698,131.152491217335));
#86904=CARTESIAN_POINT('Ctrl Pts',(-54.5027716149597,4.91370136695366,131.015836240033));
#86905=CARTESIAN_POINT('Ctrl Pts',(-54.5102619507218,4.91936891484217,130.884149015367));
#86906=CARTESIAN_POINT('Ctrl Pts',(-54.5177522864839,4.91973171888739,130.752402123454));
#86907=CARTESIAN_POINT('Ctrl Pts',(-54.5252426222461,4.91483276193648,130.621052176146));
#86908=CARTESIAN_POINT('Ctrl Pts',(-54.5330169563651,4.90974805954385,130.484722055665));
#86909=CARTESIAN_POINT('Ctrl Pts',(-54.5407912904842,4.89897861363779,130.348387721445));
#86910=CARTESIAN_POINT('Ctrl Pts',(-54.5485656246032,4.88251547807646,130.212561945006));
#86911=CARTESIAN_POINT('Ctrl Pts',(-54.5563303775503,4.86607263185836,130.076903561698));
#86912=CARTESIAN_POINT('Ctrl Pts',(-54.5640951304975,4.84395010424328,129.94175287352));
#86913=CARTESIAN_POINT('Ctrl Pts',(-54.5718598834446,4.81619093642229,129.807621972572));
#86914=CARTESIAN_POINT('Ctrl Pts',(-54.5796169243296,4.78845933939812,129.673624292327));
#86915=CARTESIAN_POINT('Ctrl Pts',(-54.5873739652145,4.75510232193858,129.540644764035));
#86916=CARTESIAN_POINT('Ctrl Pts',(-54.5951310060995,4.71621459670577,129.409189323309));
#86917=CARTESIAN_POINT('Ctrl Pts',(-54.6028821973396,4.67735619700906,129.277833014153));
#86918=CARTESIAN_POINT('Ctrl Pts',(-54.6106333885798,4.63297550162076,129.147998878285));
#86919=CARTESIAN_POINT('Ctrl Pts',(-54.6183845798199,4.58321799216971,129.020181282759));
#86920=CARTESIAN_POINT('Ctrl Pts',(-54.626132476597,4.5334816309875,128.892418013121));
#86921=CARTESIAN_POINT('Ctrl Pts',(-54.6338803733741,4.47837314254132,128.766669942722));
#86922=CARTESIAN_POINT('Ctrl Pts',(-54.6416282701511,4.41808735374489,128.643414714222));
#86923=CARTESIAN_POINT('Ctrl Pts',(-54.6493745462352,4.35781417543587,128.520185268059));
#86924=CARTESIAN_POINT('Ctrl Pts',(-54.6571208223193,4.29236602255315,128.399447977589));
#86925=CARTESIAN_POINT('Ctrl Pts',(-54.6648670984034,4.22198504228919,128.281658620661));
#86926=CARTESIAN_POINT('Ctrl Pts',(-54.6726134316687,4.15160354248891,128.163868394239));
#86927=CARTESIAN_POINT('Ctrl Pts',(-54.680359764934,4.07628934318438,128.049026480399));
#86928=CARTESIAN_POINT('Ctrl Pts',(-54.6881060981993,3.99632933954245,127.937561902551));
#86929=CARTESIAN_POINT('Ctrl Pts',(-54.6958541662023,3.9163514294121,127.826072362984));
#86930=CARTESIAN_POINT('Ctrl Pts',(-54.7036022342053,3.8317258725235,127.717961982038));
#86931=CARTESIAN_POINT('Ctrl Pts',(-54.7113503022083,3.74278122298893,127.613628447775));
#86932=CARTESIAN_POINT('Ctrl Pts',(-54.7191066049501,3.65374204202226,127.509184026589));
#86933=CARTESIAN_POINT('Ctrl Pts',(-54.7268629076919,3.56037485266949,127.408524768636));
#86934=CARTESIAN_POINT('Ctrl Pts',(-54.7346192104337,3.46304699504312,127.312013473793));
#86935=CARTESIAN_POINT('Ctrl Pts',(-54.7423796529479,3.36566719060865,127.215450667966));
#86936=CARTESIAN_POINT('Ctrl Pts',(-54.7501400954621,3.26432279447367,127.123040499916));
#86937=CARTESIAN_POINT('Ctrl Pts',(-54.7579005379763,3.15941516358818,127.035106197049));
#86938=CARTESIAN_POINT('Ctrl Pts',(-54.7656734382417,3.05433912566033,126.947030734233));
#86939=CARTESIAN_POINT('Ctrl Pts',(-54.7734463385071,2.94568873261387,126.863445733158));
#86940=CARTESIAN_POINT('Ctrl Pts',(-54.7812192387725,2.83389604314877,126.784632233816));
#86941=CARTESIAN_POINT('Ctrl Pts',(-54.7887095745346,2.7261672995333,126.708683803693));
#86942=CARTESIAN_POINT('Ctrl Pts',(-54.7961999102967,2.61552101254961,126.637166153199));
#86943=CARTESIAN_POINT('Ctrl Pts',(-54.8036902460588,2.50236457596035,126.570289929507));
#86944=CARTESIAN_POINT('Ctrl Pts',(-54.8114645801779,2.38491777868549,126.500878073468));
#86945=CARTESIAN_POINT('Ctrl Pts',(-54.819238914297,2.2643946935461,126.436246675518));
#86946=CARTESIAN_POINT('Ctrl Pts',(-54.8270132484161,2.14122189413659,126.376680427831));
#86947=CARTESIAN_POINT('Ctrl Pts',(-54.8347780013632,2.01820089419409,126.317187590222));
#86948=CARTESIAN_POINT('Ctrl Pts',(-54.8425427543104,1.89253702601445,126.262747651047));
#86949=CARTESIAN_POINT('Ctrl Pts',(-54.8503075072575,1.76468439199987,126.213601196824));
#86950=CARTESIAN_POINT('Ctrl Pts',(-54.8580645481425,1.6369587430238,126.164503555552));
#86951=CARTESIAN_POINT('Ctrl Pts',(-54.8658215890276,1.50704901696855,126.120689075813));
#86952=CARTESIAN_POINT('Ctrl Pts',(-54.8735786299126,1.37543206629944,126.082351543719));
#86953=CARTESIAN_POINT('Ctrl Pts',(-54.8813298211528,1.24391436899649,126.044042922255));
#86954=CARTESIAN_POINT('Ctrl Pts',(-54.8890810123929,1.11069238348038,126.011203136401));
#86955=CARTESIAN_POINT('Ctrl Pts',(-54.8968322036331,0.97626067112854,125.983977005808));
#86956=CARTESIAN_POINT('Ctrl Pts',(-54.9045801004102,0.841886095840717,
125.956762447047));
#86957=CARTESIAN_POINT('Ctrl Pts',(-54.9123279971873,0.706303198737797,
125.935156875512));
#86958=CARTESIAN_POINT('Ctrl Pts',(-54.9200758939644,0.570019142824407,
125.919254555328));
#86959=CARTESIAN_POINT('Ctrl Pts',(-54.9278221700485,0.43376359459757,125.903355561567));
#86960=CARTESIAN_POINT('Ctrl Pts',(-54.9355684461327,0.296807567374053,
125.893157491504));
#86961=CARTESIAN_POINT('Ctrl Pts',(-54.9433147222168,0.159665406438524,
125.888702978909));
#86962=CARTESIAN_POINT('Ctrl Pts',(-54.9510610554822,0.0225222331507177,
125.884248433431));
#86963=CARTESIAN_POINT('Ctrl Pts',(-54.9588073887475,-0.114806685831678,
125.885537542715));
#86964=CARTESIAN_POINT('Ctrl Pts',(-54.9665537220128,-0.251805327116809,
125.892560831364));
#86965=CARTESIAN_POINT('Ctrl Pts',(-54.9743017900158,-0.388834648297774,
125.899585692829));
#86966=CARTESIAN_POINT('Ctrl Pts',(-54.9820498580189,-0.525533154225138,
125.912347268917));
#86967=CARTESIAN_POINT('Ctrl Pts',(-54.9897979260219,-0.661388667148345,
125.930784097856));
#86968=CARTESIAN_POINT('Ctrl Pts',(-54.9975542287637,-0.797388568927388,
125.949240521677));
#86969=CARTESIAN_POINT('Ctrl Pts',(-55.0053105315057,-0.932543299927897,
125.973384194713));
#86970=CARTESIAN_POINT('Ctrl Pts',(-55.0130668342476,-1.0663490700338,126.003102165521));
#86971=CARTESIAN_POINT('Ctrl Pts',(-55.0208272767618,-1.2002262563082,126.032835997704));
#86972=CARTESIAN_POINT('Ctrl Pts',(-55.0285877192759,-1.33275266946667,
126.06814995532));
#86973=CARTESIAN_POINT('Ctrl Pts',(-55.0363481617901,-1.46343942590286,
126.108881077709));
#86974=CARTESIAN_POINT('Ctrl Pts',(-55.0441210620555,-1.59433597232213,
126.149677585312));
#86975=CARTESIAN_POINT('Ctrl Pts',(-55.051893962321,-1.72338659235167,126.195908503363));
#86976=CARTESIAN_POINT('Ctrl Pts',(-55.0596668625865,-1.85012130080695,
126.247362237623));
#86977=CARTESIAN_POINT('Ctrl Pts',(-55.0671571983483,-1.97224888338046,
126.296945499037));
#86978=CARTESIAN_POINT('Ctrl Pts',(-55.0746475341101,-2.09222572902183,
126.351378316933));
#86979=CARTESIAN_POINT('Ctrl Pts',(-55.0821378698719,-2.20965440801859,
126.410431799341));
#86980=CARTESIAN_POINT('Ctrl Pts',(-55.0899130101817,-2.33154807001562,
126.471730668459));
#86981=CARTESIAN_POINT('Ctrl Pts',(-55.0976881504915,-2.45108211634481,
126.538202733636));
#86982=CARTESIAN_POINT('Ctrl Pts',(-55.1054632908013,-2.56778630866249,
126.609642923186));
#86983=CARTESIAN_POINT('Ctrl Pts',(-55.1132286705009,-2.68434399505456,
126.680993429488));
#86984=CARTESIAN_POINT('Ctrl Pts',(-55.1209940502005,-2.79807856601499,
126.757299447498));
#86985=CARTESIAN_POINT('Ctrl Pts',(-55.1287594299001,-2.90854205076117,
126.838308903146));
#86986=CARTESIAN_POINT('Ctrl Pts',(-55.1367185626383,-3.02176169639659,
126.921339615808));
#86987=CARTESIAN_POINT('Ctrl Pts',(-55.1446776953764,-3.1315444928007,127.009311406704));
#86988=CARTESIAN_POINT('Ctrl Pts',(-55.1526368281145,-3.23743631109765,
127.101903434277));
#86989=CARTESIAN_POINT('Ctrl Pts',(-55.1603876305625,-3.34055641117398,
127.192071865636));
#86990=CARTESIAN_POINT('Ctrl Pts',(-55.1681384330106,-3.4399863653504,127.286621408679));
#86991=CARTESIAN_POINT('Ctrl Pts',(-55.1758892354586,-3.53533793702208,
127.385213248184));
#86992=CARTESIAN_POINT('Ctrl Pts',(-55.1836365277603,-3.63064632633007,
127.483760437888));
#86993=CARTESIAN_POINT('Ctrl Pts',(-55.191383820062,-3.7218797371152,127.586346001037));
#86994=CARTESIAN_POINT('Ctrl Pts',(-55.1991311123636,-3.8086857906305,127.692593336623));
#86995=CARTESIAN_POINT('Ctrl Pts',(-55.2068765738559,-3.89547133048362,
127.79881556426));
#86996=CARTESIAN_POINT('Ctrl Pts',(-55.2146220353483,-3.97783134877193,
127.908697539246));
#86997=CARTESIAN_POINT('Ctrl Pts',(-55.2223674968406,-4.05545313597058,
128.021828870317));
#86998=CARTESIAN_POINT('Ctrl Pts',(-55.2304850900719,-4.13680427237365,
128.140395611404));
#86999=CARTESIAN_POINT('Ctrl Pts',(-55.2386026833031,-4.21295029522901,
128.262531324154));
#87000=CARTESIAN_POINT('Ctrl Pts',(-55.2467202765344,-4.28358197502536,
128.387728968816));
#87001=CARTESIAN_POINT('Ctrl Pts',(-55.2544698307117,-4.3510113242947,128.507250346958));
#87002=CARTESIAN_POINT('Ctrl Pts',(-55.2622193848892,-4.41341520153701,
128.629561734039));
#87003=CARTESIAN_POINT('Ctrl Pts',(-55.2699689390666,-4.47057185358703,
128.75419712057));
#87004=CARTESIAN_POINT('Ctrl Pts',(-55.2777211340661,-4.52774798295818,
128.878874979208));
#87005=CARTESIAN_POINT('Ctrl Pts',(-55.2854733290657,-4.57967317347573,
129.005878054953));
#87006=CARTESIAN_POINT('Ctrl Pts',(-55.2932255240652,-4.6261740823844,129.134721009155));
#87007=CARTESIAN_POINT('Ctrl Pts',(-55.3009846094251,-4.67271632255723,
129.263678482456));
#87008=CARTESIAN_POINT('Ctrl Pts',(-55.308743694785,-4.71382453847262,129.394478726866));
#87009=CARTESIAN_POINT('Ctrl Pts',(-55.3165027801449,-4.74937539568687,
129.526621828398));
#87010=CARTESIAN_POINT('Ctrl Pts',(-55.317594725302,-4.75437850940002,129.545218481621));
#87011=CARTESIAN_POINT('Ctrl Pts',(-55.318686670459,-4.75927164097778,129.563841714487));
#87012=CARTESIAN_POINT('Ctrl Pts',(-55.3197786156161,-4.76405452823412,
129.582490119309));
#87013=CARTESIAN_POINT('Origin',(213.235140564004,0.,130.804360617566));
#87014=CARTESIAN_POINT('',(-57.4152011815765,-4.76405452823411,129.582490119308));
#87015=CARTESIAN_POINT('',(-57.0701182010014,-4.76405452823404,129.582490119308));
#87016=CARTESIAN_POINT('',(213.235140564004,-4.76405452823405,129.582490119308));
#87017=CARTESIAN_POINT('',(-55.7351405639628,-4.9182495025703,130.802148612358));
#87018=CARTESIAN_POINT('Ctrl Pts',(-55.7351405640085,-4.91824950257066,
130.802148613168));
#87019=CARTESIAN_POINT('Ctrl Pts',(-55.7430237908748,-4.91831241585365,
130.942032251313));
#87020=CARTESIAN_POINT('Ctrl Pts',(-55.7509070177411,-4.91240317315693,
131.08189431191));
#87021=CARTESIAN_POINT('Ctrl Pts',(-55.7587902446074,-4.90055374134223,
131.221201223454));
#87022=CARTESIAN_POINT('Ctrl Pts',(-55.7666765057547,-4.88869974864066,
131.360561754705));
#87023=CARTESIAN_POINT('Ctrl Pts',(-55.7745627669019,-4.87090104280418,
131.499366341054));
#87024=CARTESIAN_POINT('Ctrl Pts',(-55.7824490280492,-4.84724140196124,
131.63708737564));
#87025=CARTESIAN_POINT('Ctrl Pts',(-55.7903397817841,-4.82356828286713,
131.774886866138));
#87026=CARTESIAN_POINT('Ctrl Pts',(-55.798230535519,-4.79402763944753,131.911601209291));
#87027=CARTESIAN_POINT('Ctrl Pts',(-55.8061212892539,-4.7587541683001,132.046713960294));
#87028=CARTESIAN_POINT('Ctrl Pts',(-55.8140237851165,-4.72342820715993,
132.18202777082));
#87029=CARTESIAN_POINT('Ctrl Pts',(-55.8219262809793,-4.68235246769653,
132.315734867519));
#87030=CARTESIAN_POINT('Ctrl Pts',(-55.8298287768419,-4.63571156242695,
132.447333950424));
#87031=CARTESIAN_POINT('Ctrl Pts',(-55.8377374019982,-4.5890344817761,132.579035103538));
#87032=CARTESIAN_POINT('Ctrl Pts',(-55.8456460271544,-4.53678376848017,
132.708624639214));
#87033=CARTESIAN_POINT('Ctrl Pts',(-55.8535546523107,-4.47919160491059,
132.835622695437));
#87034=CARTESIAN_POINT('Ctrl Pts',(-55.8614779459022,-4.42149262291089,
132.962856299905));
#87035=CARTESIAN_POINT('Ctrl Pts',(-55.8694012394938,-4.35843255734479,
133.08748848667));
#87036=CARTESIAN_POINT('Ctrl Pts',(-55.8773245330854,-4.29028942379935,
133.209064283828));
#87037=CARTESIAN_POINT('Ctrl Pts',(-55.8841802704406,-4.23132765231517,
133.314259392962));
#87038=CARTESIAN_POINT('Ctrl Pts',(-55.8910360077956,-4.1685610800927,133.417166569318));
#87039=CARTESIAN_POINT('Ctrl Pts',(-55.8978917451508,-4.10219475032617,
133.51751031725));
#87040=CARTESIAN_POINT('Ctrl Pts',(-55.9056660792698,-4.02693602976367,
133.63129907297));
#87041=CARTESIAN_POINT('Ctrl Pts',(-55.913440413389,-3.94682002154035,133.74213434208));
#87042=CARTESIAN_POINT('Ctrl Pts',(-55.9212147475081,-3.86210581822375,
133.849573534809));
#87043=CARTESIAN_POINT('Ctrl Pts',(-55.9289795004551,-3.77749601759184,
133.956880318334));
#87044=CARTESIAN_POINT('Ctrl Pts',(-55.9367442534022,-3.68829953698645,
134.060799049036));
#87045=CARTESIAN_POINT('Ctrl Pts',(-55.9445090063493,-3.59481951570741,
134.160914760134));
#87046=CARTESIAN_POINT('Ctrl Pts',(-55.9522660472343,-3.50143234010321,
134.260931034896));
#87047=CARTESIAN_POINT('Ctrl Pts',(-55.9600230881193,-3.40377035551371,
134.357151522967));
#87048=CARTESIAN_POINT('Ctrl Pts',(-55.9677801290043,-3.30217762914935,
134.449193393983));
#87049=CARTESIAN_POINT('Ctrl Pts',(-55.9755313202444,-3.20066151465049,
134.541165855509));
#87050=CARTESIAN_POINT('Ctrl Pts',(-55.9832825114845,-3.09522084700842,
134.628965710673));
#87051=CARTESIAN_POINT('Ctrl Pts',(-55.9910337027246,-2.98623703530915,
134.712246418283));
#87052=CARTESIAN_POINT('Ctrl Pts',(-55.9987815995017,-2.87729954463678,
134.795491729372));
#87053=CARTESIAN_POINT('Ctrl Pts',(-56.0065294962788,-2.76482221508682,
134.874221476262));
#87054=CARTESIAN_POINT('Ctrl Pts',(-56.0142773930559,-2.64921989975699,
134.94812906974));
#87055=CARTESIAN_POINT('Ctrl Pts',(-56.02202366914,-2.53364176593942,135.022021203342));
#87056=CARTESIAN_POINT('Ctrl Pts',(-56.029769945224,-2.4149402757375,135.091092979413));
#87057=CARTESIAN_POINT('Ctrl Pts',(-56.0375162213081,-2.29355932284947,
135.155081097564));
#87058=CARTESIAN_POINT('Ctrl Pts',(-56.0452625545734,-2.17217747395497,
135.219069688059));
#87059=CARTESIAN_POINT('Ctrl Pts',(-56.0530088878387,-2.04811646875717,
135.277974363432));
#87060=CARTESIAN_POINT('Ctrl Pts',(-56.0607552211041,-1.92184450117899,
135.331577950077));
#87061=CARTESIAN_POINT('Ctrl Pts',(-56.068503289107,-1.79554425586936,135.385193540873));
#87062=CARTESIAN_POINT('Ctrl Pts',(-56.0762513571101,-1.66703242274066,
135.433505527923));
#87063=CARTESIAN_POINT('Ctrl Pts',(-56.083999425113,-1.53679647483696,135.476345169919));
#87064=CARTESIAN_POINT('Ctrl Pts',(-56.0917557278549,-1.40642211061765,
135.519230342397));
#87065=CARTESIAN_POINT('Ctrl Pts',(-56.0995120305967,-1.27432034316865,
135.556631429229));
#87066=CARTESIAN_POINT('Ctrl Pts',(-56.1072683333386,-1.14099362288777,
135.588429661281));
#87067=CARTESIAN_POINT('Ctrl Pts',(-56.1150287758527,-1.0075957421217,135.620244865006));
#87068=CARTESIAN_POINT('Ctrl Pts',(-56.1227892183669,-0.872971989357373,
135.646451180632));
#87069=CARTESIAN_POINT('Ctrl Pts',(-56.130549660881,-0.737633282538259,
135.666981331028));
#87070=CARTESIAN_POINT('Ctrl Pts',(-56.1383225611465,-0.602077318012338,
135.687544438244));
#87071=CARTESIAN_POINT('Ctrl Pts',(-56.1460954614119,-0.465804494828162,
135.70241312935));
#87072=CARTESIAN_POINT('Ctrl Pts',(-56.1538683616773,-0.329330006961362,
135.71157212809));
#87073=CARTESIAN_POINT('Ctrl Pts',(-56.1613586974394,-0.197816710484977,
135.720398174155));
#87074=CARTESIAN_POINT('Ctrl Pts',(-56.1688490332016,-0.0661164647181106,
135.723922435861));
#87075=CARTESIAN_POINT('Ctrl Pts',(-56.1763393689637,0.0653132185093781,
135.722176926253));
#87076=CARTESIAN_POINT('Ctrl Pts',(-56.1841137030828,0.201726098121702,
135.720365235117));
#87077=CARTESIAN_POINT('Ctrl Pts',(-56.1918880372019,0.338279608429306,
135.712870538652));
#87078=CARTESIAN_POINT('Ctrl Pts',(-56.199662371321,0.474461340259999,135.699671588189));
#87079=CARTESIAN_POINT('Ctrl Pts',(-56.2074271242681,0.610475240277306,
135.686488904252));
#87080=CARTESIAN_POINT('Ctrl Pts',(-56.2151918772151,0.746117888060793,
135.667615991243));
#87081=CARTESIAN_POINT('Ctrl Pts',(-56.2229566301623,0.880876306110258,
135.64308358916));
#87082=CARTESIAN_POINT('Ctrl Pts',(-56.2307136710473,1.01550088019879,135.618575553005));
#87083=CARTESIAN_POINT('Ctrl Pts',(-56.2384707119323,1.14924259011514,135.588419283556));
#87084=CARTESIAN_POINT('Ctrl Pts',(-56.2462277528172,1.281593373103,135.552697325143));
#87085=CARTESIAN_POINT('Ctrl Pts',(-56.2539789440574,1.41384434933568,135.517002304936));
#87086=CARTESIAN_POINT('Ctrl Pts',(-56.2617301352975,1.54470611049822,135.47575005136));
#87087=CARTESIAN_POINT('Ctrl Pts',(-56.2694813265376,1.67368094074449,135.429074140703));
#87088=CARTESIAN_POINT('Ctrl Pts',(-56.2772292233147,1.80260095324756,135.382418068554));
#87089=CARTESIAN_POINT('Ctrl Pts',(-56.2849771200917,1.92963526308168,135.330343056955));
#87090=CARTESIAN_POINT('Ctrl Pts',(-56.2927250168688,2.0543016898257,135.273032414608));
#87091=CARTESIAN_POINT('Ctrl Pts',(-56.3004712929529,2.17894203904075,135.215733760412));
#87092=CARTESIAN_POINT('Ctrl Pts',(-56.308217569037,2.30121513536269,135.153201817043));
#87093=CARTESIAN_POINT('Ctrl Pts',(-56.3159638451211,2.42065952133068,135.085667724548));
#87094=CARTESIAN_POINT('Ctrl Pts',(-56.3237101783865,2.54010478901016,135.018133133531));
#87095=CARTESIAN_POINT('Ctrl Pts',(-56.3314565116518,2.6567209643365,134.945596512133));
#87096=CARTESIAN_POINT('Ctrl Pts',(-56.3392028449172,2.77007226275375,134.868334377523));
#87097=CARTESIAN_POINT('Ctrl Pts',(-56.3469509129202,2.88344894540867,134.791054940594));
#87098=CARTESIAN_POINT('Ctrl Pts',(-56.3546989809232,2.99355897326287,134.709048104824));
#87099=CARTESIAN_POINT('Ctrl Pts',(-56.3624470489262,3.09999688838854,134.622632786294));
#87100=CARTESIAN_POINT('Ctrl Pts',(-56.370203351668,3.20654792699661,134.536125624535));
#87101=CARTESIAN_POINT('Ctrl Pts',(-56.3779596544098,3.30941875267354,134.445200867269));
#87102=CARTESIAN_POINT('Ctrl Pts',(-56.3857159571517,3.4082378548688,134.350217042626));
#87103=CARTESIAN_POINT('Ctrl Pts',(-56.3934763996659,3.50710969979443,134.255182522256));
#87104=CARTESIAN_POINT('Ctrl Pts',(-56.4012368421801,3.60192524206938,134.156084900034));
#87105=CARTESIAN_POINT('Ctrl Pts',(-56.4089972846943,3.69235171590876,134.053317660761));
#87106=CARTESIAN_POINT('Ctrl Pts',(-56.4167701849597,3.78292335035164,133.950385450393));
#87107=CARTESIAN_POINT('Ctrl Pts',(-56.4245430852252,3.8690915908621,133.843772155531));
#87108=CARTESIAN_POINT('Ctrl Pts',(-56.4323159854906,3.95056511016457,133.73390296627));
#87109=CARTESIAN_POINT('Ctrl Pts',(-56.4398063212526,4.02907686182065,133.628027798783));
#87110=CARTESIAN_POINT('Ctrl Pts',(-56.4472966570145,4.10322912279955,133.519129601613));
#87111=CARTESIAN_POINT('Ctrl Pts',(-56.4547869927765,4.17280153026225,133.407610596254));
#87112=CARTESIAN_POINT('Ctrl Pts',(-56.4625613268956,4.24501179670018,133.291863313911));
#87113=CARTESIAN_POINT('Ctrl Pts',(-56.4703356610147,4.31251680412911,133.172925911786));
#87114=CARTESIAN_POINT('Ctrl Pts',(-56.4781099951338,4.37502170576884,133.051218008802));
#87115=CARTESIAN_POINT('Ctrl Pts',(-56.4858747480809,4.43744957570352,132.929660099931));
#87116=CARTESIAN_POINT('Ctrl Pts',(-56.493639501028,4.49488942386328,132.805338828274));
#87117=CARTESIAN_POINT('Ctrl Pts',(-56.5014042539751,4.54708983580989,132.67870239205));
#87118=CARTESIAN_POINT('Ctrl Pts',(-56.5091612948601,4.59923840157152,132.552191732919));
#87119=CARTESIAN_POINT('Ctrl Pts',(-56.5169183357451,4.6461577390474,132.423370844359));
#87120=CARTESIAN_POINT('Ctrl Pts',(-56.5246753766301,4.68764267478816,132.292711791182));
#87121=CARTESIAN_POINT('Ctrl Pts',(-56.5324265678702,4.72909632641622,132.162151269014));
#87122=CARTESIAN_POINT('Ctrl Pts',(-56.5401777591103,4.76512361554327,132.02975571245));
#87123=CARTESIAN_POINT('Ctrl Pts',(-56.5479289503505,4.79556789611087,131.896016065173));
#87124=CARTESIAN_POINT('Ctrl Pts',(-56.5556768471276,4.82599923704705,131.762333260815));
#87125=CARTESIAN_POINT('Ctrl Pts',(-56.5634247439046,4.85085220239881,131.627307882381));
#87126=CARTESIAN_POINT('Ctrl Pts',(-56.5711726406817,4.87002038467275,131.491444684745));
#87127=CARTESIAN_POINT('Ctrl Pts',(-56.5789189167658,4.88918455737618,131.355609906762));
#87128=CARTESIAN_POINT('Ctrl Pts',(-56.5866651928499,4.90266625767106,131.218938045054));
#87129=CARTESIAN_POINT('Ctrl Pts',(-56.5944114689341,4.91041052119701,131.081942273692));
#87130=CARTESIAN_POINT('Ctrl Pts',(-56.6021578021994,4.91815484188936,130.944945491059));
#87131=CARTESIAN_POINT('Ctrl Pts',(-56.6099041354648,4.92016161923581,130.807625184344));
#87132=CARTESIAN_POINT('Ctrl Pts',(-56.6176504687301,4.91642794276504,130.670497455721));
#87133=CARTESIAN_POINT('Ctrl Pts',(-56.6253985367331,4.91269343016331,130.533339018294));
#87134=CARTESIAN_POINT('Ctrl Pts',(-56.6331466047362,4.90321591631798,130.39637363552));
#87135=CARTESIAN_POINT('Ctrl Pts',(-56.6408946727392,4.88804455444544,130.260114812569));
#87136=CARTESIAN_POINT('Ctrl Pts',(-56.648650975481,4.87285706826897,130.123711172121));
#87137=CARTESIAN_POINT('Ctrl Pts',(-56.6564072782229,4.85196368889586,129.988015980762));
#87138=CARTESIAN_POINT('Ctrl Pts',(-56.6641635809648,4.82546524566948,129.853535594054));
#87139=CARTESIAN_POINT('Ctrl Pts',(-56.6719240234789,4.79895265942614,129.718983431115));
#87140=CARTESIAN_POINT('Ctrl Pts',(-56.6796844659931,4.76682913985776,129.585647744679));
#87141=CARTESIAN_POINT('Ctrl Pts',(-56.6874449085073,4.72924586883788,129.454021188171));
#87142=CARTESIAN_POINT('Ctrl Pts',(-56.6952178087727,4.69160226581481,129.322183333029));
#87143=CARTESIAN_POINT('Ctrl Pts',(-56.702990709038,4.6484815201748,129.192060461829));
#87144=CARTESIAN_POINT('Ctrl Pts',(-56.7107636093035,4.60008388687645,129.06412750209));
#87145=CARTESIAN_POINT('Ctrl Pts',(-56.7182539450655,4.55344562945511,128.940845227682));
#87146=CARTESIAN_POINT('Ctrl Pts',(-56.7257442808275,4.50190760034834,128.819596694863));
#87147=CARTESIAN_POINT('Ctrl Pts',(-56.7332346165894,4.44568908839166,128.700784711673));
#87148=CARTESIAN_POINT('Ctrl Pts',(-56.7410089507085,4.38733903446656,128.577467936026));
#87149=CARTESIAN_POINT('Ctrl Pts',(-56.7487832848276,4.32376173499277,128.456385490379));
#87150=CARTESIAN_POINT('Ctrl Pts',(-56.7565576189467,4.25515085536902,128.338012251955));
#87151=CARTESIAN_POINT('Ctrl Pts',(-56.7643223718938,4.18662453252238,128.219784897968));
#87152=CARTESIAN_POINT('Ctrl Pts',(-56.7720871248408,4.11307716669244,128.104260442884));
#87153=CARTESIAN_POINT('Ctrl Pts',(-56.7798518777879,4.0347499440894,127.991892670874));
#87154=CARTESIAN_POINT('Ctrl Pts',(-56.7876089186729,3.95650051718817,127.87963650412));
#87155=CARTESIAN_POINT('Ctrl Pts',(-56.795365959558,3.87348090322022,127.770531099785));
#87156=CARTESIAN_POINT('Ctrl Pts',(-56.803123000443,3.78597736241983,127.665004238665));
#87157=CARTESIAN_POINT('Ctrl Pts',(-56.8108741916832,3.69853980872012,127.559556956172));
#87158=CARTESIAN_POINT('Ctrl Pts',(-56.8186253829233,3.60662530713444,127.45768314522));
#87159=CARTESIAN_POINT('Ctrl Pts',(-56.8263765741634,3.51056223146715,127.359779963626));
#87160=CARTESIAN_POINT('Ctrl Pts',(-56.8341244709405,3.41453998516973,127.261918393497));
#87161=CARTESIAN_POINT('Ctrl Pts',(-56.8418723677175,3.3143729450157,127.168024374652));
#87162=CARTESIAN_POINT('Ctrl Pts',(-56.8496202644946,3.21042825972758,127.078460263069));
#87163=CARTESIAN_POINT('Ctrl Pts',(-56.8573665405787,3.10650531742684,126.988914886367));
#87164=CARTESIAN_POINT('Ctrl Pts',(-56.8651128166628,2.99880659774137,126.903697870438));
#87165=CARTESIAN_POINT('Ctrl Pts',(-56.8728590927469,2.88773413897328,126.823132841476));
#87166=CARTESIAN_POINT('Ctrl Pts',(-56.8806054260123,2.77666086029354,126.742567217802));
#87167=CARTESIAN_POINT('Ctrl Pts',(-56.8883517592776,2.66221410931545,126.666653879171));
#87168=CARTESIAN_POINT('Ctrl Pts',(-56.896098092543,2.5448265242333,126.595674240077));
#87169=CARTESIAN_POINT('Ctrl Pts',(-56.9038461605459,2.4274126510157,126.524678705586));
#87170=CARTESIAN_POINT('Ctrl Pts',(-56.9115942285489,2.30705696769329,126.458619271447));
#87171=CARTESIAN_POINT('Ctrl Pts',(-56.9193422965518,2.18421806922206,126.397732145754));
#87172=CARTESIAN_POINT('Ctrl Pts',(-56.9270985992937,2.0612486161074,126.336780308499));
#87173=CARTESIAN_POINT('Ctrl Pts',(-56.9348549020356,1.93579102662994,126.281011934829));
#87174=CARTESIAN_POINT('Ctrl Pts',(-56.9426112047774,1.80832581278619,126.230615891708));
#87175=CARTESIAN_POINT('Ctrl Pts',(-56.9503716472916,1.6807925669199,126.180192950702));
#87176=CARTESIAN_POINT('Ctrl Pts',(-56.9581320898057,1.55124993067059,126.135148182076));
#87177=CARTESIAN_POINT('Ctrl Pts',(-56.9658925323198,1.42019410481406,126.095620683449));
#87178=CARTESIAN_POINT('Ctrl Pts',(-56.9736654325852,1.28892789651127,126.056029731771));
#87179=CARTESIAN_POINT('Ctrl Pts',(-56.9814383328508,1.15614402339869,126.02197384601));
#87180=CARTESIAN_POINT('Ctrl Pts',(-56.9892112331162,1.02235029814514,125.993541255921));
#87181=CARTESIAN_POINT('Ctrl Pts',(-56.9967015688783,0.893420311809538,
125.966142262098));
#87182=CARTESIAN_POINT('Ctrl Pts',(-57.0041919046403,0.763552923591962,
125.94396487197));
#87183=CARTESIAN_POINT('Ctrl Pts',(-57.0116822404024,0.633205558275497,
125.927042319211));
#87184=CARTESIAN_POINT('Ctrl Pts',(-57.0194565745215,0.497916032985787,
125.909478142721));
#87185=CARTESIAN_POINT('Ctrl Pts',(-57.0272309086405,0.361680858901798,
125.897519505895));
#87186=CARTESIAN_POINT('Ctrl Pts',(-57.0350052427596,0.225004244560835,
125.891260155289));
#87187=CARTESIAN_POINT('Ctrl Pts',(-57.0427699957067,0.0884960719324635,
125.885008518772));
#87188=CARTESIAN_POINT('Ctrl Pts',(-57.0505347486538,-0.0484520716775091,
125.8844422108));
#87189=CARTESIAN_POINT('Ctrl Pts',(-57.0582995016008,-0.18532803775502,
125.889603596011));
#87190=CARTESIAN_POINT('Ctrl Pts',(-57.0660565424858,-0.322068056693224,
125.894759854862));
#87191=CARTESIAN_POINT('Ctrl Pts',(-57.0738135833707,-0.458735652601401,
125.90563247124));
#87192=CARTESIAN_POINT('Ctrl Pts',(-57.0815706242557,-0.594816190732355,
125.922211832273));
#87193=CARTESIAN_POINT('Ctrl Pts',(-57.0893218154959,-0.730794109472061,
125.93877869068));
#87194=CARTESIAN_POINT('Ctrl Pts',(-57.097073006736,-0.866185465086569,
125.961043680792));
#87195=CARTESIAN_POINT('Ctrl Pts',(-57.1048241979762,-1.00047862339296,
125.988945205929));
#87196=CARTESIAN_POINT('Ctrl Pts',(-57.1125720947532,-1.13471470352413,
126.016834872173));
#87197=CARTESIAN_POINT('Ctrl Pts',(-57.1203199915304,-1.26785313271433,
126.050356229258));
#87198=CARTESIAN_POINT('Ctrl Pts',(-57.1280678883075,-1.3993905977649,126.089396246822));
#87199=CARTESIAN_POINT('Ctrl Pts',(-57.1358141643916,-1.53090054801376,
126.128428098055));
#87200=CARTESIAN_POINT('Ctrl Pts',(-57.1435604404757,-1.66080982566395,
126.172976202462));
#87201=CARTESIAN_POINT('Ctrl Pts',(-57.1513067165598,-1.78862884330984,
126.222877241695));
#87202=CARTESIAN_POINT('Ctrl Pts',(-57.1590530498252,-1.91644880448669,
126.272778649286));
#87203=CARTESIAN_POINT('Ctrl Pts',(-57.1667993830905,-2.04217811067544,
126.328032928369));
#87204=CARTESIAN_POINT('Ctrl Pts',(-57.1745457163558,-2.16534614838121,
126.388428199583));
#87205=CARTESIAN_POINT('Ctrl Pts',(-57.1822937843588,-2.28854176871487,
126.4488369959));
#87206=CARTESIAN_POINT('Ctrl Pts',(-57.1900418523619,-2.4091746282437,126.514388903186));
#87207=CARTESIAN_POINT('Ctrl Pts',(-57.1977899203649,-2.52679811663301,
126.584825768761));
#87208=CARTESIAN_POINT('Ctrl Pts',(-57.2055462231068,-2.64454661666551,
126.655337495475));
#87209=CARTESIAN_POINT('Ctrl Pts',(-57.2133025258485,-2.75927902046179,
126.730744350459));
#87210=CARTESIAN_POINT('Ctrl Pts',(-57.2210588285904,-2.87057670042268,
126.81074415257));
#87211=CARTESIAN_POINT('Ctrl Pts',(-57.2288192711045,-2.98193378330632,
126.890786652984));
#87212=CARTESIAN_POINT('Ctrl Pts',(-57.2365797136187,-3.08985218203316,
126.975426743976));
#87213=CARTESIAN_POINT('Ctrl Pts',(-57.2443401561329,-3.19394666119732,
127.064322143442));
#87214=CARTESIAN_POINT('Ctrl Pts',(-57.2521130563983,-3.29820824206064,
127.153360245695));
#87215=CARTESIAN_POINT('Ctrl Pts',(-57.2598859566637,-3.39863335010845,
127.246667040664));
#87216=CARTESIAN_POINT('Ctrl Pts',(-57.2676588569292,-3.49487326999634,
127.343862981508));
#87217=CARTESIAN_POINT('Ctrl Pts',(-57.2751491926912,-3.58761462638258,
127.43752560508));
#87218=CARTESIAN_POINT('Ctrl Pts',(-57.2826395284532,-3.67646958831234,
127.534799295745));
#87219=CARTESIAN_POINT('Ctrl Pts',(-57.2901298642152,-3.76116294608421,
127.635317172691));
#87220=CARTESIAN_POINT('Ctrl Pts',(-57.2978585046994,-3.84855081952744,
127.739033021732));
#87221=CARTESIAN_POINT('Ctrl Pts',(-57.3055871451837,-3.93179432220579,
127.84654304682));
#87222=CARTESIAN_POINT('Ctrl Pts',(-57.3133157856679,-4.01054278145833,
127.957479928005));
#87223=CARTESIAN_POINT('Ctrl Pts',(-57.3210349725339,-4.0891949161544,128.068281111985));
#87224=CARTESIAN_POINT('Ctrl Pts',(-57.3287541594,-4.16336271619009,128.182500495525));
#87225=CARTESIAN_POINT('Ctrl Pts',(-57.336473346266,-4.23273413835902,128.299735939801));
#87226=CARTESIAN_POINT('Ctrl Pts',(-57.3441832907805,-4.302022500605,128.416831015511));
#87227=CARTESIAN_POINT('Ctrl Pts',(-57.351893235295,-4.36652571901792,128.536934623359));
#87228=CARTESIAN_POINT('Ctrl Pts',(-57.3596031798095,-4.42597408949314,
128.659614380447));
#87229=CARTESIAN_POINT('Ctrl Pts',(-57.3673077977208,-4.48538138861153,
128.782209381233));
#87230=CARTESIAN_POINT('Ctrl Pts',(-57.3750124156322,-4.53974061357756,
128.907376636773));
#87231=CARTESIAN_POINT('Ctrl Pts',(-57.3827170335435,-4.58882720901201,
129.034657843558));
#87232=CARTESIAN_POINT('Ctrl Pts',(-57.3904178145022,-4.63788935898501,
129.161875663429));
#87233=CARTESIAN_POINT('Ctrl Pts',(-57.3981185954609,-4.68168396286949,
129.291204970892));
#87234=CARTESIAN_POINT('Ctrl Pts',(-57.4058193764196,-4.7200341787311,129.422166559515));
#87235=CARTESIAN_POINT('Ctrl Pts',(-57.4089466448052,-4.73560810795835,
129.475349741589));
#87236=CARTESIAN_POINT('Ctrl Pts',(-57.4120739131909,-4.75028473236229,
129.52880189419));
#87237=CARTESIAN_POINT('Ctrl Pts',(-57.4152011815765,-4.76405452823411,
129.582490119308));
#87238=CARTESIAN_POINT('Ctrl Pts',(-55.665415119611,-4.764054528234,129.582490119308));
#87239=CARTESIAN_POINT('Ctrl Pts',(-55.6739271886917,-4.8013074290267,129.727738614107));
#87240=CARTESIAN_POINT('Ctrl Pts',(-55.6824392577724,-4.83195755642185,
129.87486329597));
#87241=CARTESIAN_POINT('Ctrl Pts',(-55.6909513268531,-4.8558303914332,130.023275300758));
#87242=CARTESIAN_POINT('Ctrl Pts',(-55.699428429661,-4.87960516050402,130.171077651818));
#87243=CARTESIAN_POINT('Ctrl Pts',(-55.7079055324689,-4.89665810257531,
130.320156528335));
#87244=CARTESIAN_POINT('Ctrl Pts',(-55.7163826352768,-4.90686536188065,
130.469912739899));
#87245=CARTESIAN_POINT('Ctrl Pts',(-55.7226352781722,-4.91439415430214,
130.580371717865));
#87246=CARTESIAN_POINT('Ctrl Pts',(-55.7288879210675,-4.91819960239075,
130.691198813367));
#87247=CARTESIAN_POINT('Ctrl Pts',(-55.7351405639629,-4.9182495025703,130.802148612358));
#87248=CARTESIAN_POINT('',(-55.3898594360289,-4.9182491242873,130.801425664894));
#87249=CARTESIAN_POINT('Ctrl Pts',(-55.3197786156161,-4.76405452823412,
129.582490119309));
#87250=CARTESIAN_POINT('Ctrl Pts',(-55.3275521152037,-4.79810364862538,
129.715247122947));
#87251=CARTESIAN_POINT('Ctrl Pts',(-55.3353256147913,-4.82656139489736,
129.849280179693));
#87252=CARTESIAN_POINT('Ctrl Pts',(-55.3430991143789,-4.84936286713653,
129.98407844335));
#87253=CARTESIAN_POINT('Ctrl Pts',(-55.3489279074809,-4.86646006545832,
130.085154050354));
#87254=CARTESIAN_POINT('Ctrl Pts',(-55.3547567005828,-4.88037813522813,
130.186659715631));
#87255=CARTESIAN_POINT('Ctrl Pts',(-55.3605854936848,-4.89110893864667,
130.288379597769));
#87256=CARTESIAN_POINT('Ctrl Pts',(-55.3703434744535,-4.90907337340337,
130.458668821684));
#87257=CARTESIAN_POINT('Ctrl Pts',(-55.3801014552224,-4.91814677411089,
130.629912319547));
#87258=CARTESIAN_POINT('Ctrl Pts',(-55.389859435991,-4.9182491242869,130.801425664228));
#87259=CARTESIAN_POINT('Ctrl Pts',(-55.389859436029,-4.9182491242873,130.801425664894));
#87260=CARTESIAN_POINT('Ctrl Pts',(-55.3975287093647,-4.91832956626769,
130.936226373385));
#87261=CARTESIAN_POINT('Ctrl Pts',(-55.4051979827003,-4.91286385231857,
131.071249821404));
#87262=CARTESIAN_POINT('Ctrl Pts',(-55.412867256036,-4.90182346626275,131.205994490759));
#87263=CARTESIAN_POINT('Ctrl Pts',(-55.4205280170279,-4.89079533424426,
131.340589603187));
#87264=CARTESIAN_POINT('Ctrl Pts',(-55.4281887780199,-4.87420486859583,
131.474906155198));
#87265=CARTESIAN_POINT('Ctrl Pts',(-55.4358495390118,-4.8520755586004,131.608441357376));
#87266=CARTESIAN_POINT('Ctrl Pts',(-55.4435037431039,-4.82996518923872,
131.741862265824));
#87267=CARTESIAN_POINT('Ctrl Pts',(-55.4511579471961,-4.80232547147055,
131.874502760349));
#87268=CARTESIAN_POINT('Ctrl Pts',(-55.4588121512882,-4.76923177128743,
132.005864414581));
#87269=CARTESIAN_POINT('Ctrl Pts',(-55.4664622018516,-4.73615602929184,
132.137154785845));
#87270=CARTESIAN_POINT('Ctrl Pts',(-55.4741122524151,-4.69763228838224,
132.267167308161));
#87271=CARTESIAN_POINT('Ctrl Pts',(-55.4817623029785,-4.65378706511144,
132.395413418419));
#87272=CARTESIAN_POINT('Ctrl Pts',(-55.489410254756,-4.60995387074702,132.523624344446));
#87273=CARTESIAN_POINT('Ctrl Pts',(-55.4970582065333,-4.56080222634519,
132.650069441839));
#87274=CARTESIAN_POINT('Ctrl Pts',(-55.5047061583108,-4.50650846512339,
132.774275467571));
#87275=CARTESIAN_POINT('Ctrl Pts',(-55.5123537689327,-4.452217125807,132.898475952791));
#87276=CARTESIAN_POINT('Ctrl Pts',(-55.5200013795547,-4.3927842868615,133.020437196672));
#87277=CARTESIAN_POINT('Ctrl Pts',(-55.5276489901766,-4.32843414743316,
133.139706607743));
#87278=CARTESIAN_POINT('Ctrl Pts',(-55.5352980167735,-4.26407209340924,
133.258998101855));
#87279=CARTESIAN_POINT('Ctrl Pts',(-55.5429470433704,-4.19479111958725,
133.375596418511));
#87280=CARTESIAN_POINT('Ctrl Pts',(-55.5505960699673,-4.12086075596664,
133.489074697768));
#87281=CARTESIAN_POINT('Ctrl Pts',(-55.5582528693755,-4.04685526556292,
133.60266829173));
#87282=CARTESIAN_POINT('Ctrl Pts',(-55.5659096687836,-3.9681911697162,133.713135179273));
#87283=CARTESIAN_POINT('Ctrl Pts',(-55.5735664681918,-3.88518081679781,
133.820078290573));
#87284=CARTESIAN_POINT('Ctrl Pts',(-55.5812272718838,-3.80212705187374,
133.927077330017));
#87285=CARTESIAN_POINT('Ctrl Pts',(-55.5888880755759,-3.71472276315588,
134.030548617135));
#87286=CARTESIAN_POINT('Ctrl Pts',(-55.5965488792679,-3.62331890390447,
134.130130180105));
#87287=CARTESIAN_POINT('Ctrl Pts',(-55.6042216043421,-3.53177280626968,
134.229866707216));
#87288=CARTESIAN_POINT('Ctrl Pts',(-55.6118943294162,-3.43621498977593,
134.32570113535));
#87289=CARTESIAN_POINT('Ctrl Pts',(-55.6195670544903,-3.33703184835501,
134.417309759965));
#87290=CARTESIAN_POINT('Ctrl Pts',(-55.6260557421594,-3.25315442273412,
134.49478155091));
#87291=CARTESIAN_POINT('Ctrl Pts',(-55.6325444298286,-3.16668492983673,
134.569231755106));
#87292=CARTESIAN_POINT('Ctrl Pts',(-55.6390331174976,-3.07787329861358,
134.640488746315));
#87293=CARTESIAN_POINT('Ctrl Pts',(-55.6468074516167,-2.97146483360443,
134.725864354795));
#87294=CARTESIAN_POINT('Ctrl Pts',(-55.6545817857358,-2.86133284530761,
134.806944418968));
#87295=CARTESIAN_POINT('Ctrl Pts',(-55.6623561198549,-2.74785919161345,
134.883386595121));
#87296=CARTESIAN_POINT('Ctrl Pts',(-55.670120872802,-2.63452538405605,134.959734563124));
#87297=CARTESIAN_POINT('Ctrl Pts',(-55.677885625749,-2.51785842643888,135.031455799473));
#87298=CARTESIAN_POINT('Ctrl Pts',(-55.6856503786961,-2.39827368564984,
135.098247713336));
#87299=CARTESIAN_POINT('Ctrl Pts',(-55.6934074195811,-2.27880771811121,
135.164973288529));
#87300=CARTESIAN_POINT('Ctrl Pts',(-55.7011644604662,-2.15643007364254,
135.226779094832));
#87301=CARTESIAN_POINT('Ctrl Pts',(-55.7089215013512,-2.03158528013885,
135.283405639892));
#87302=CARTESIAN_POINT('Ctrl Pts',(-55.7166726925913,-1.90683463306543,
135.339989482434));
#87303=CARTESIAN_POINT('Ctrl Pts',(-55.7244238838314,-1.77962089477293,
135.391401676992));
#87304=CARTESIAN_POINT('Ctrl Pts',(-55.7321750750715,-1.65041307139816,
135.437428689185));
#87305=CARTESIAN_POINT('Ctrl Pts',(-55.7399229718486,-1.52126016479489,
135.483436138671));
#87306=CARTESIAN_POINT('Ctrl Pts',(-55.7476708686257,-1.39011522632476,
135.524062827211));
#87307=CARTESIAN_POINT('Ctrl Pts',(-55.7554187654028,-1.25746691026064,
135.559143476131));
#87308=CARTESIAN_POINT('Ctrl Pts',(-55.7631650414869,-1.12484634136466,
135.594216786935));
#87309=CARTESIAN_POINT('Ctrl Pts',(-55.770911317571,-0.990723398112361,
135.62374626575));
#87310=CARTESIAN_POINT('Ctrl Pts',(-55.7786575936551,-0.855601170929385,
135.647616722585));
#87311=CARTESIAN_POINT('Ctrl Pts',(-55.7864039269204,-0.720477946304455,
135.671487355627));
#87312=CARTESIAN_POINT('Ctrl Pts',(-55.7941502601859,-0.584355808033334,
135.689698815318));
#87313=CARTESIAN_POINT('Ctrl Pts',(-55.8018965934512,-0.447746902166392,
135.702187255382));
#87314=CARTESIAN_POINT('Ctrl Pts',(-55.8096446614542,-0.311107403682347,
135.714678492146));
#87315=CARTESIAN_POINT('Ctrl Pts',(-55.8173927294571,-0.173981309955912,
135.721444123399));
#87316=CARTESIAN_POINT('Ctrl Pts',(-55.8251407974601,-0.0368843373871096,
135.722472308871));
#87317=CARTESIAN_POINT('Ctrl Pts',(-55.832897100202,0.100358343475614,135.723501587111));
#87318=CARTESIAN_POINT('Ctrl Pts',(-55.8406534029438,0.237571449776515,
135.718781235569));
#87319=CARTESIAN_POINT('Ctrl Pts',(-55.8484097056857,0.37424026127967,135.708351572833));
#87320=CARTESIAN_POINT('Ctrl Pts',(-55.8561701481998,0.510982017042356,
135.697916343471));
#87321=CARTESIAN_POINT('Ctrl Pts',(-55.8639305907141,0.647178511093406,
135.681765777066));
#87322=CARTESIAN_POINT('Ctrl Pts',(-55.8716910332282,0.78232268235092,135.659991810643));
#87323=CARTESIAN_POINT('Ctrl Pts',(-55.8794639334937,0.917683799029857,
135.638182890715));
#87324=CARTESIAN_POINT('Ctrl Pts',(-55.8872368337591,1.05198883392483,135.610732609921));
#87325=CARTESIAN_POINT('Ctrl Pts',(-55.8950097340245,1.18474253183181,135.577783728476));
#87326=CARTESIAN_POINT('Ctrl Pts',(-55.9025000697865,1.31267029843313,135.546032621865));
#87327=CARTESIAN_POINT('Ctrl Pts',(-55.9099904055485,1.43915726414061,135.509175836042));
#87328=CARTESIAN_POINT('Ctrl Pts',(-55.9174807413105,1.5637775403749,135.467383549819));
#87329=CARTESIAN_POINT('Ctrl Pts',(-55.9252550754296,1.69312283226049,135.424006696361));
#87330=CARTESIAN_POINT('Ctrl Pts',(-55.9330294095487,1.82086681635337,135.375175290683));
#87331=CARTESIAN_POINT('Ctrl Pts',(-55.9408037436678,1.94651506567573,135.321025555504));
#87332=CARTESIAN_POINT('Ctrl Pts',(-55.9485684966149,2.07200846476013,135.266942555034));
#87333=CARTESIAN_POINT('Ctrl Pts',(-55.9563332495619,2.1954109124924,135.207554419546));
#87334=CARTESIAN_POINT('Ctrl Pts',(-55.964098002509,2.31624331468696,135.143047051231));
#87335=CARTESIAN_POINT('Ctrl Pts',(-55.971855043394,2.43695570443622,135.078603752543));
#87336=CARTESIAN_POINT('Ctrl Pts',(-55.9796120842791,2.55510278578551,135.009051522334));
#87337=CARTESIAN_POINT('Ctrl Pts',(-55.9873691251641,2.67022596228412,134.934624092557));
#87338=CARTESIAN_POINT('Ctrl Pts',(-55.9951203164042,2.78526232349981,134.860252789083));
#87339=CARTESIAN_POINT('Ctrl Pts',(-56.0028715076443,2.89727899176605,134.781013815149));
#87340=CARTESIAN_POINT('Ctrl Pts',(-56.0106226988844,3.00584280528774,134.69718633835));
#87341=CARTESIAN_POINT('Ctrl Pts',(-56.0183705956615,3.11436047629266,134.613394490466));
#87342=CARTESIAN_POINT('Ctrl Pts',(-56.0261184924385,3.21942790260524,134.525018257031));
#87343=CARTESIAN_POINT('Ctrl Pts',(-56.0338663892156,3.32064190102524,134.432379419565));
#87344=CARTESIAN_POINT('Ctrl Pts',(-56.0416126652997,3.42183472765869,134.339759960146));
#87345=CARTESIAN_POINT('Ctrl Pts',(-56.0493589413838,3.51917544146678,134.242879934026));
#87346=CARTESIAN_POINT('Ctrl Pts',(-56.0571052174679,3.61229519718496,134.142100342424));
#87347=CARTESIAN_POINT('Ctrl Pts',(-56.0648515507332,3.70541564029203,134.04132000689));
#87348=CARTESIAN_POINT('Ctrl Pts',(-56.0725978839986,3.79431479780925,133.936640335587));
#87349=CARTESIAN_POINT('Ctrl Pts',(-56.0803442172639,3.87866212660504,133.828457701017));
#87350=CARTESIAN_POINT('Ctrl Pts',(-56.0880922852668,3.96302834440007,133.720250839698));
#87351=CARTESIAN_POINT('Ctrl Pts',(-56.0958403532697,4.04284046473646,133.608539762386));
#87352=CARTESIAN_POINT('Ctrl Pts',(-56.1035884212727,4.11780976874678,133.493751955939));
#87353=CARTESIAN_POINT('Ctrl Pts',(-56.1113447240145,4.19285875102576,133.378842151644));
#87354=CARTESIAN_POINT('Ctrl Pts',(-56.1191010267564,4.26305442115808,133.260849413927));
#87355=CARTESIAN_POINT('Ctrl Pts',(-56.1268573294983,4.32815248145335,133.14022858468));
#87356=CARTESIAN_POINT('Ctrl Pts',(-56.1346177720125,4.39328528654363,133.019543376464));
#87357=CARTESIAN_POINT('Ctrl Pts',(-56.1423782145267,4.45331488943827,132.896227633092));
#87358=CARTESIAN_POINT('Ctrl Pts',(-56.1501386570409,4.50804456046034,132.770757653621));
#87359=CARTESIAN_POINT('Ctrl Pts',(-56.1579115573063,4.56286208840893,132.645086258599));
#87360=CARTESIAN_POINT('Ctrl Pts',(-56.1656844575717,4.61236254168788,132.517254081746));
#87361=CARTESIAN_POINT('Ctrl Pts',(-56.1734573578372,4.6563983309755,132.387754960675));
#87362=CARTESIAN_POINT('Ctrl Pts',(-56.1809476935992,4.69883330840324,132.262963458842));
#87363=CARTESIAN_POINT('Ctrl Pts',(-56.1884380293612,4.73619394523367,132.136624399281));
#87364=CARTESIAN_POINT('Ctrl Pts',(-56.1959283651233,4.7683932145393,132.009188079917));
#87365=CARTESIAN_POINT('Ctrl Pts',(-56.2037026992424,4.80181332892722,131.876919973772));
#87366=CARTESIAN_POINT('Ctrl Pts',(-56.2114770333615,4.82977882807532,131.743050774515));
#87367=CARTESIAN_POINT('Ctrl Pts',(-56.2192513674806,4.85213707015684,131.608070089272));
#87368=CARTESIAN_POINT('Ctrl Pts',(-56.2270161204276,4.87446775770323,131.47325575566));
#87369=CARTESIAN_POINT('Ctrl Pts',(-56.2347808733747,4.89120487462955,131.337333043576));
#87370=CARTESIAN_POINT('Ctrl Pts',(-56.2425456263218,4.90224586360402,131.200805513204));
#87371=CARTESIAN_POINT('Ctrl Pts',(-56.2503026672068,4.91327588651257,131.0644135839));
#87372=CARTESIAN_POINT('Ctrl Pts',(-56.2580597080919,4.91862100878843,130.927418418926));
#87373=CARTESIAN_POINT('Ctrl Pts',(-56.2658167489769,4.91822999315974,130.790332186294));
#87374=CARTESIAN_POINT('Ctrl Pts',(-56.273567940217,4.91783927239897,130.653349331456));
#87375=CARTESIAN_POINT('Ctrl Pts',(-56.2813191314571,4.91172102482053,130.516275935035));
#87376=CARTESIAN_POINT('Ctrl Pts',(-56.2890703226972,4.89987598749963,130.379627325223));
#87377=CARTESIAN_POINT('Ctrl Pts',(-56.2968182194743,4.88803598463561,130.243036794715));
#87378=CARTESIAN_POINT('Ctrl Pts',(-56.3045661162514,4.8704740668385,130.106871080414));
#87379=CARTESIAN_POINT('Ctrl Pts',(-56.3123140130284,4.84724302764511,129.971643322534));
#87380=CARTESIAN_POINT('Ctrl Pts',(-56.3200602891125,4.82401684788429,129.836443851385));
#87381=CARTESIAN_POINT('Ctrl Pts',(-56.3278065651966,4.79512397161675,129.702182331482));
#87382=CARTESIAN_POINT('Ctrl Pts',(-56.3355528412807,4.76066874951808,129.569364212769));
#87383=CARTESIAN_POINT('Ctrl Pts',(-56.343299174546,4.72621327307883,129.436545113623));
#87384=CARTESIAN_POINT('Ctrl Pts',(-56.3510455078113,4.68619546704952,129.305169815366));
#87385=CARTESIAN_POINT('Ctrl Pts',(-56.3587918410767,4.64077014420735,129.175730662317));
#87386=CARTESIAN_POINT('Ctrl Pts',(-56.3665399090796,4.59533464867928,129.046262522268));
#87387=CARTESIAN_POINT('Ctrl Pts',(-56.3742879770826,4.54448935607604,128.918731759051));
#87388=CARTESIAN_POINT('Ctrl Pts',(-56.3820360450855,4.48843786359724,128.793612347114));
#87389=CARTESIAN_POINT('Ctrl Pts',(-56.3897923478274,4.43232679892491,128.668359956776));
#87390=CARTESIAN_POINT('Ctrl Pts',(-56.3975486505692,4.37099864128637,128.54552439458));
#87391=CARTESIAN_POINT('Ctrl Pts',(-56.4053049533111,4.30470401317964,128.425557048245));
#87392=CARTESIAN_POINT('Ctrl Pts',(-56.4130653958252,4.2383740016338,128.305525671725));
#87393=CARTESIAN_POINT('Ctrl Pts',(-56.4208258383394,4.16707244092084,128.188365895236));
#87394=CARTESIAN_POINT('Ctrl Pts',(-56.4285862808536,4.09109371773113,128.074500684302));
#87395=CARTESIAN_POINT('Ctrl Pts',(-56.436359181119,4.01499302674978,127.960452686822));
#87396=CARTESIAN_POINT('Ctrl Pts',(-56.4441320813844,3.93420040008097,127.849710139489));
#87397=CARTESIAN_POINT('Ctrl Pts',(-56.4519049816498,3.84905154166185,127.742664144672));
#87398=CARTESIAN_POINT('Ctrl Pts',(-56.459395317412,3.76699805872237,127.639509541398));
#87399=CARTESIAN_POINT('Ctrl Pts',(-56.4668856531741,3.68089976659567,127.539787631828));
#87400=CARTESIAN_POINT('Ctrl Pts',(-56.4743759889362,3.59108847350101,127.443815031208));
#87401=CARTESIAN_POINT('Ctrl Pts',(-56.4821503230553,3.49787195793229,127.344203600268));
#87402=CARTESIAN_POINT('Ctrl Pts',(-56.4899246571744,3.40036004460926,127.248315861675));
#87403=CARTESIAN_POINT('Ctrl Pts',(-56.4976989912935,3.29888214723805,127.156544881933));
#87404=CARTESIAN_POINT('Ctrl Pts',(-56.5054637442406,3.19752931230587,127.064887001721));
#87405=CARTESIAN_POINT('Ctrl Pts',(-56.5132284971876,3.09222050562441,126.977336045254));
#87406=CARTESIAN_POINT('Ctrl Pts',(-56.5209932501348,2.9833239518934,126.894250483496));
#87407=CARTESIAN_POINT('Ctrl Pts',(-56.5287502910198,2.87453555575457,126.811247443489));
#87408=CARTESIAN_POINT('Ctrl Pts',(-56.5365073319048,2.76216681270894,126.732701207775));
#87409=CARTESIAN_POINT('Ctrl Pts',(-56.5442643727898,2.64662092921322,126.658931723042));
#87410=CARTESIAN_POINT('Ctrl Pts',(-56.55201556403,2.53116217976675,126.585217868452));
#87411=CARTESIAN_POINT('Ctrl Pts',(-56.5597667552701,2.41253138697458,126.516273804448));
#87412=CARTESIAN_POINT('Ctrl Pts',(-56.5675179465103,2.29116250944611,126.452377458383));
#87413=CARTESIAN_POINT('Ctrl Pts',(-56.5752658432873,2.16984521692886,126.388508269971));
#87414=CARTESIAN_POINT('Ctrl Pts',(-56.5830137400645,2.04579249953019,126.32968271418));
#87415=CARTESIAN_POINT('Ctrl Pts',(-56.5907616368416,1.91946461284274,126.276133739135));
#87416=CARTESIAN_POINT('Ctrl Pts',(-56.5985079129257,1.79316315122587,126.222595965381));
#87417=CARTESIAN_POINT('Ctrl Pts',(-56.6062541890097,1.6645878266771,126.174332729446));
#87418=CARTESIAN_POINT('Ctrl Pts',(-56.6140004650938,1.53422029263908,126.131529446193));
#87419=CARTESIAN_POINT('Ctrl Pts',(-56.6217467983592,1.40385179625754,126.088725846976));
#87420=CARTESIAN_POINT('Ctrl Pts',(-56.6294931316245,1.27169143544405,126.051382402824));
#87421=CARTESIAN_POINT('Ctrl Pts',(-56.6372394648899,1.13823711350541,126.019634989493));
#87422=CARTESIAN_POINT('Ctrl Pts',(-56.6449875328929,1.00475290539631,125.987880466549));
#87423=CARTESIAN_POINT('Ctrl Pts',(-56.6527356008959,0.869974539824291,
125.961724558599));
#87424=CARTESIAN_POINT('Ctrl Pts',(-56.6604836688989,0.73441083417581,125.941252168318));
#87425=CARTESIAN_POINT('Ctrl Pts',(-56.6682399716407,0.598703049808107,
125.920758019738));
#87426=CARTESIAN_POINT('Ctrl Pts',(-56.6759962743826,0.462208645221434,
125.905959513871));
#87427=CARTESIAN_POINT('Ctrl Pts',(-56.6837525771244,0.325442853270143,
125.896889780999));
#87428=CARTESIAN_POINT('Ctrl Pts',(-56.6915130196386,0.188604065297934,
125.887815207338));
#87429=CARTESIAN_POINT('Ctrl Pts',(-56.6992734621528,0.0514939919980021,
125.884475508752));
#87430=CARTESIAN_POINT('Ctrl Pts',(-56.7070339046669,-0.0853723905588257,
125.886851632579));
#87431=CARTESIAN_POINT('Ctrl Pts',(-56.7148068049324,-0.222458483183733,
125.88923157077));
#87432=CARTESIAN_POINT('Ctrl Pts',(-56.7225797051977,-0.359299712830921,
125.897345643882));
#87433=CARTESIAN_POINT('Ctrl Pts',(-56.7303526054631,-0.495385577822631,
125.911122815069));
#87434=CARTESIAN_POINT('Ctrl Pts',(-56.7378429412251,-0.626524378841732,
125.92439915138));
#87435=CARTESIAN_POINT('Ctrl Pts',(-56.7453332769872,-0.756961475594774,
125.942933955011));
#87436=CARTESIAN_POINT('Ctrl Pts',(-56.7528236127492,-0.886251140259517,
125.966619204583));
#87437=CARTESIAN_POINT('Ctrl Pts',(-56.7605979468683,-1.02044286185734,
125.991202487592));
#87438=CARTESIAN_POINT('Ctrl Pts',(-56.7683722809874,-1.15382350302958,
126.021412357054));
#87439=CARTESIAN_POINT('Ctrl Pts',(-56.7761466151065,-1.28588430964043,
126.057184129935));
#87440=CARTESIAN_POINT('Ctrl Pts',(-56.7839113680536,-1.4177823631101,126.092911817302));
#87441=CARTESIAN_POINT('Ctrl Pts',(-56.7916761210007,-1.54836344468064,
126.134187668342));
#87442=CARTESIAN_POINT('Ctrl Pts',(-56.7994408739478,-1.67712692813105,
126.180895647499));
#87443=CARTESIAN_POINT('Ctrl Pts',(-56.8071979148328,-1.8057625218741,126.227557235632));
#87444=CARTESIAN_POINT('Ctrl Pts',(-56.8149549557177,-1.93258374490037,
126.279640082603));
#87445=CARTESIAN_POINT('Ctrl Pts',(-56.8227119966027,-2.05710347406054,
126.336977898399));
#87446=CARTESIAN_POINT('Ctrl Pts',(-56.8304631878428,-2.18152930192365,
126.394272475303));
#87447=CARTESIAN_POINT('Ctrl Pts',(-56.838214379083,-2.30365673678873,126.45681397043));
#87448=CARTESIAN_POINT('Ctrl Pts',(-56.845965570323,-2.42301738527417,126.524387508637));
#87449=CARTESIAN_POINT('Ctrl Pts',(-56.8537134671001,-2.54232730230045,
126.591932326287));
#87450=CARTESIAN_POINT('Ctrl Pts',(-56.8614613638772,-2.65887243232339,
126.664504740991));
#87451=CARTESIAN_POINT('Ctrl Pts',(-56.8692092606543,-2.77220801009941,
126.741843440834));
#87452=CARTESIAN_POINT('Ctrl Pts',(-56.8769555367384,-2.8855198805158,126.819165963089));
#87453=CARTESIAN_POINT('Ctrl Pts',(-56.8847018128225,-2.99562321133926,
126.901252567156));
#87454=CARTESIAN_POINT('Ctrl Pts',(-56.8924480889065,-3.10210166234376,
126.987798245616));
#87455=CARTESIAN_POINT('Ctrl Pts',(-56.9001944221719,-3.20858089934814,
127.074344562937));
#87456=CARTESIAN_POINT('Ctrl Pts',(-56.9079407554373,-3.3114348997508,127.165349773736));
#87457=CARTESIAN_POINT('Ctrl Pts',(-56.9156870887026,-3.4102802185304,127.260468422027));
#87458=CARTESIAN_POINT('Ctrl Pts',(-56.9234351567056,-3.50914767303394,
127.35560837148));
#87459=CARTESIAN_POINT('Ctrl Pts',(-56.9311832247086,-3.60400437790277,
127.454863320417));
#87460=CARTESIAN_POINT('Ctrl Pts',(-56.9389312927115,-3.69450387388461,
127.55785107833));
#87461=CARTESIAN_POINT('Ctrl Pts',(-56.9466875954534,-3.7850995538076,127.660948292857));
#87462=CARTESIAN_POINT('Ctrl Pts',(-56.9544438981952,-3.87132851564963,
127.767785947264));
#87463=CARTESIAN_POINT('Ctrl Pts',(-56.9622002009371,-3.95288439002263,
127.877948469283));
#87464=CARTESIAN_POINT('Ctrl Pts',(-56.9699606434512,-4.03448379322138,
127.988169788358));
#87465=CARTESIAN_POINT('Ctrl Pts',(-56.9777210859654,-4.11140491994529,
128.101719187522));
#87466=CARTESIAN_POINT('Ctrl Pts',(-56.9854815284796,-4.18338544259421,
128.218153104393));
#87467=CARTESIAN_POINT('Ctrl Pts',(-56.993254428745,-4.25548151476821,128.334773931324));
#87468=CARTESIAN_POINT('Ctrl Pts',(-57.0010273290105,-4.32262094241365,
128.454288188086));
#87469=CARTESIAN_POINT('Ctrl Pts',(-57.0088002292759,-4.38458755221458,
128.576227978008));
#87470=CARTESIAN_POINT('Ctrl Pts',(-57.0162905650379,-4.44430151966453,
128.693734949418));
#87471=CARTESIAN_POINT('Ctrl Pts',(-57.0237809007999,-4.49921210133561,
128.813493887187));
#87472=CARTESIAN_POINT('Ctrl Pts',(-57.0312712365619,-4.54916925189624,
128.935071399681));
#87473=CARTESIAN_POINT('Ctrl Pts',(-57.0399825578534,-4.60726982350856,
129.076467033576));
#87474=CARTESIAN_POINT('Ctrl Pts',(-57.0486938791448,-4.65882662131957,
129.220700646112));
#87475=CARTESIAN_POINT('Ctrl Pts',(-57.0574052004363,-4.70358508809922,
129.367186173906));
#87476=CARTESIAN_POINT('Ctrl Pts',(-57.0616428672913,-4.72535807348324,
129.438444809089));
#87477=CARTESIAN_POINT('Ctrl Pts',(-57.0658805341464,-4.74552299645481,
129.510235958156));
#87478=CARTESIAN_POINT('Ctrl Pts',(-57.0701182010015,-4.76405452823404,
129.582490119308));
#87479=CARTESIAN_POINT('Origin',(213.235140564004,0.,130.804360617566));
#87480=CARTESIAN_POINT('',(-59.165034112149,-4.76405452823398,129.582490119308));
#87481=CARTESIAN_POINT('',(-58.8199570926743,-4.76405452823407,129.582490119308));
#87482=CARTESIAN_POINT('',(213.235140564004,-4.76405452823405,129.582490119308));
#87483=CARTESIAN_POINT('',(-57.4851405640492,-4.91824815608763,130.808619448461));
#87484=CARTESIAN_POINT('Ctrl Pts',(-57.4851405640492,-4.91824815608763,
130.808619448461));
#87485=CARTESIAN_POINT('Ctrl Pts',(-57.494480310666,-4.91810505791892,130.973874261755));
#87486=CARTESIAN_POINT('Ctrl Pts',(-57.5038200572828,-4.90962930027124,
131.138764540297));
#87487=CARTESIAN_POINT('Ctrl Pts',(-57.5131598038996,-4.89295343983749,
131.302547026536));
#87488=CARTESIAN_POINT('Ctrl Pts',(-57.5226232671053,-4.87605668684078,
131.46849901601));
#87489=CARTESIAN_POINT('Ctrl Pts',(-57.5320867303109,-4.8507412115729,131.633313665362));
#87490=CARTESIAN_POINT('Ctrl Pts',(-57.5415501935165,-4.81719403868288,
131.796239973223));
#87491=CARTESIAN_POINT('Ctrl Pts',(-57.5505592916871,-4.78525755123167,
131.951343772983));
#87492=CARTESIAN_POINT('Ctrl Pts',(-57.5595683898577,-4.74586126885286,
132.104736401066));
#87493=CARTESIAN_POINT('Ctrl Pts',(-57.5685774880283,-4.69920644601773,
132.255788135634));
#87494=CARTESIAN_POINT('Ctrl Pts',(-57.5763518221473,-4.65894601438298,
132.386137104151));
#87495=CARTESIAN_POINT('Ctrl Pts',(-57.5841261562665,-4.61319417433263,
132.515016120226));
#87496=CARTESIAN_POINT('Ctrl Pts',(-57.5919004903855,-4.56207524447303,
132.641927630294));
#87497=CARTESIAN_POINT('Ctrl Pts',(-57.5996652433326,-4.51101931412586,
132.768682733268));
#87498=CARTESIAN_POINT('Ctrl Pts',(-57.6074299962796,-4.45460959944137,
132.893474795645));
#87499=CARTESIAN_POINT('Ctrl Pts',(-57.6151947492267,-4.3930204521356,133.015820400067));
#87500=CARTESIAN_POINT('Ctrl Pts',(-57.6229517901117,-4.33149247603928,
133.138044489109));
#87501=CARTESIAN_POINT('Ctrl Pts',(-57.6307088309968,-4.26479547933942,
133.257826608766));
#87502=CARTESIAN_POINT('Ctrl Pts',(-57.6384658718818,-4.19315212162949,
133.37470268573));
#87503=CARTESIAN_POINT('Ctrl Pts',(-57.6462170631219,-4.12156279073292,
133.491490625535));
#87504=CARTESIAN_POINT('Ctrl Pts',(-57.653968254362,-4.04503472683967,133.605376552657));
#87505=CARTESIAN_POINT('Ctrl Pts',(-57.6617194456021,-3.96383662246492,
133.715920730788));
#87506=CARTESIAN_POINT('Ctrl Pts',(-57.6694673423792,-3.88267302945044,
133.826417924695));
#87507=CARTESIAN_POINT('Ctrl Pts',(-57.6772152391563,-3.79684357471622,
133.933575880107));
#87508=CARTESIAN_POINT('Ctrl Pts',(-57.6849631359334,-3.7066602718305,134.036983808062));
#87509=CARTESIAN_POINT('Ctrl Pts',(-57.6927094120175,-3.61649583334775,
134.140370105308));
#87510=CARTESIAN_POINT('Ctrl Pts',(-57.7004556881016,-3.52197961501504,
134.240007640895));
#87511=CARTESIAN_POINT('Ctrl Pts',(-57.7082019641857,-3.42346366282378,
134.335519012742));
#87512=CARTESIAN_POINT('Ctrl Pts',(-57.715948297451,-3.32494698341013,134.431031089634));
#87513=CARTESIAN_POINT('Ctrl Pts',(-57.7236946307164,-3.22243079192417,
134.522416669868));
#87514=CARTESIAN_POINT('Ctrl Pts',(-57.7314409639817,-3.11630341460103,
134.609335793654));
#87515=CARTESIAN_POINT('Ctrl Pts',(-57.7391890319847,-3.01015227078757,
134.696274382376));
#87516=CARTESIAN_POINT('Ctrl Pts',(-57.7469370999877,-2.90038863432754,
134.778744276628));
#87517=CARTESIAN_POINT('Ctrl Pts',(-57.7546851679907,-2.78743294051551,
134.856446582181));
#87518=CARTESIAN_POINT('Ctrl Pts',(-57.7624414707325,-2.6743571960479,134.934231470669));
#87519=CARTESIAN_POINT('Ctrl Pts',(-57.7701977734744,-2.55808293985622,
135.007238426546));
#87520=CARTESIAN_POINT('Ctrl Pts',(-57.7779540762162,-2.43905902038,135.075212307522));
#87521=CARTESIAN_POINT('Ctrl Pts',(-57.7857145187304,-2.31997157425404,
135.143222468205));
#87522=CARTESIAN_POINT('Ctrl Pts',(-57.7934749612445,-2.19813188771915,
135.20619402188));
#87523=CARTESIAN_POINT('Ctrl Pts',(-57.8012354037586,-2.07401140170014,
135.263918865657));
#87524=CARTESIAN_POINT('Ctrl Pts',(-57.8090083040241,-1.94969166645807,
135.321736374479));
#87525=CARTESIAN_POINT('Ctrl Pts',(-57.8167812042895,-1.82308417650453,
135.374290192622));
#87526=CARTESIAN_POINT('Ctrl Pts',(-57.8245541045549,-1.6946790855034,135.421420922528));
#87527=CARTESIAN_POINT('Ctrl Pts',(-57.8320444403169,-1.57094184299306,
135.466838331687));
#87528=CARTESIAN_POINT('Ctrl Pts',(-57.839534776079,-1.44553571822913,135.507219998651));
#87529=CARTESIAN_POINT('Ctrl Pts',(-57.847025111841,-1.31890879105788,135.542468115647));
#87530=CARTESIAN_POINT('Ctrl Pts',(-57.8547994459601,-1.18748076545568,
135.579052675712));
#87531=CARTESIAN_POINT('Ctrl Pts',(-57.8625737800792,-1.05432121209059,
135.610222613152));
#87532=CARTESIAN_POINT('Ctrl Pts',(-57.8703481141983,-0.919915934111412,
135.635813580875));
#87533=CARTESIAN_POINT('Ctrl Pts',(-57.8781128671453,-0.785676298625387,
135.661373010018));
#87534=CARTESIAN_POINT('Ctrl Pts',(-57.8858776200924,-0.650194373582241,
135.681367077378));
#87535=CARTESIAN_POINT('Ctrl Pts',(-57.8936423730395,-0.513971113057892,
135.695681171102));
#87536=CARTESIAN_POINT('Ctrl Pts',(-57.9013994139245,-0.377883151396122,
135.709981047866));
#87537=CARTESIAN_POINT('Ctrl Pts',(-57.9091564548095,-0.241055705841468,
135.718612137101));
#87538=CARTESIAN_POINT('Ctrl Pts',(-57.9169134956945,-0.103999567360767,
135.72151092567));
#87539=CARTESIAN_POINT('Ctrl Pts',(-57.9246646869346,0.0329532160197648,
135.72440752824));
#87540=CARTESIAN_POINT('Ctrl Pts',(-57.9324158781747,0.170133959760733,
135.721580426127));
#87541=CARTESIAN_POINT('Ctrl Pts',(-57.9401670694149,0.307027466384795,
135.713017989739));
#87542=CARTESIAN_POINT('Ctrl Pts',(-57.9479149661919,0.443862789616787,
135.704459192614));
#87543=CARTESIAN_POINT('Ctrl Pts',(-57.9556628629691,0.580410729160785,
135.690169933908));
#87544=CARTESIAN_POINT('Ctrl Pts',(-57.9634107597462,0.71615702567338,135.670190678006));
#87545=CARTESIAN_POINT('Ctrl Pts',(-57.9711570358303,0.851874926987096,
135.650215601333));
#87546=CARTESIAN_POINT('Ctrl Pts',(-57.9789033119143,0.986791132253789,
135.624552951778));
#87547=CARTESIAN_POINT('Ctrl Pts',(-57.9866495879984,1.12039783295732,135.593294920561));
#87548=CARTESIAN_POINT('Ctrl Pts',(-57.9943959212637,1.25400551991517,135.562036658605));
#87549=CARTESIAN_POINT('Ctrl Pts',(-58.0021422545291,1.38630330233558,135.525183021632));
#87550=CARTESIAN_POINT('Ctrl Pts',(-58.0098885877944,1.51679526260314,135.482876962931));
#87551=CARTESIAN_POINT('Ctrl Pts',(-58.0176366557974,1.64731644564044,135.440561430081));
#87552=CARTESIAN_POINT('Ctrl Pts',(-58.0253847238003,1.77603062997607,135.392791166342));
#87553=CARTESIAN_POINT('Ctrl Pts',(-58.0331327918033,1.90245909188332,135.339758336202));
#87554=CARTESIAN_POINT('Ctrl Pts',(-58.0408890945451,2.02902192346439,135.28666914214));
#87555=CARTESIAN_POINT('Ctrl Pts',(-58.0486453972871,2.15329381873653,135.228306360293));
#87556=CARTESIAN_POINT('Ctrl Pts',(-58.0564017000289,2.27481750571984,135.164909708927));
#87557=CARTESIAN_POINT('Ctrl Pts',(-58.0641621425431,2.3964060535539,135.10147922086));
#87558=CARTESIAN_POINT('Ctrl Pts',(-58.0719225850572,2.51524313177885,135.033009704825));
#87559=CARTESIAN_POINT('Ctrl Pts',(-58.0796830275714,2.63089883220604,134.959785312732));
#87560=CARTESIAN_POINT('Ctrl Pts',(-58.0874559278368,2.74674019343098,134.886443374344));
#87561=CARTESIAN_POINT('Ctrl Pts',(-58.0952288281023,2.85938964991657,134.808331529741));
#87562=CARTESIAN_POINT('Ctrl Pts',(-58.1030017283677,2.96844815595266,134.725776000807));
#87563=CARTESIAN_POINT('Ctrl Pts',(-58.1104920641298,3.07354211059357,134.646221573294));
#87564=CARTESIAN_POINT('Ctrl Pts',(-58.1179823998919,3.17530142432966,134.562541126215));
#87565=CARTESIAN_POINT('Ctrl Pts',(-58.125472735654,3.27340161060828,134.475058774343));
#87566=CARTESIAN_POINT('Ctrl Pts',(-58.1332470697731,3.37522129526569,134.384259502511));
#87567=CARTESIAN_POINT('Ctrl Pts',(-58.1410214038922,3.47342143760903,134.289076711545));
#87568=CARTESIAN_POINT('Ctrl Pts',(-58.1487957380113,3.56760117930796,134.189830287774));
#87569=CARTESIAN_POINT('Ctrl Pts',(-58.1565604909584,3.66166485289234,134.090706176351));
#87570=CARTESIAN_POINT('Ctrl Pts',(-58.1643252439054,3.75171771783988,133.987528677555));
#87571=CARTESIAN_POINT('Ctrl Pts',(-58.1720899968525,3.83739257003756,133.880657307731));
#87572=CARTESIAN_POINT('Ctrl Pts',(-58.1798470377375,3.92298232876423,133.773892084058));
#87573=CARTESIAN_POINT('Ctrl Pts',(-58.1876040786226,4.00420248510135,133.663440593516));
#87574=CARTESIAN_POINT('Ctrl Pts',(-58.1953611195076,4.08072350865371,133.549698248609));
#87575=CARTESIAN_POINT('Ctrl Pts',(-58.2031123107477,4.15718682710698,133.436041677689));
#87576=CARTESIAN_POINT('Ctrl Pts',(-58.2108635019878,4.22895784884965,133.319099515071));
#87577=CARTESIAN_POINT('Ctrl Pts',(-58.2186146932279,4.29574831275511,133.199298924905));
#87578=CARTESIAN_POINT('Ctrl Pts',(-58.226362590005,4.36251038893172,133.079549253186));
#87579=CARTESIAN_POINT('Ctrl Pts',(-58.2341104867821,4.42429592758238,132.956943911044));
#87580=CARTESIAN_POINT('Ctrl Pts',(-58.2418583835592,4.48086100280215,132.831937431417));
#87581=CARTESIAN_POINT('Ctrl Pts',(-58.2496046596433,4.5374142458276,132.706957100451));
#87582=CARTESIAN_POINT('Ctrl Pts',(-58.2573509357274,4.5887490364112,132.579576987005));
#87583=CARTESIAN_POINT('Ctrl Pts',(-58.2650972118115,4.63466845473061,132.450274156372));
#87584=CARTESIAN_POINT('Ctrl Pts',(-58.2728435450768,4.68058821201673,132.320970371255));
#87585=CARTESIAN_POINT('Ctrl Pts',(-58.2805898783422,4.72109238643315,132.189744209053));
#87586=CARTESIAN_POINT('Ctrl Pts',(-58.2883362116076,4.75603319304583,132.057090169044));
#87587=CARTESIAN_POINT('Ctrl Pts',(-58.2960842796105,4.79098182440989,131.924406422083));
#87588=CARTESIAN_POINT('Ctrl Pts',(-58.3038323476136,4.82036450925408,131.790294539021));
#87589=CARTESIAN_POINT('Ctrl Pts',(-58.3115804156165,4.8440841591374,131.655261153289));
#87590=CARTESIAN_POINT('Ctrl Pts',(-58.3193367183584,4.86782901854688,131.520084252468));
#87591=CARTESIAN_POINT('Ctrl Pts',(-58.3270930211003,4.88589875216386,131.383984278234));
#87592=CARTESIAN_POINT('Ctrl Pts',(-58.3348493238422,4.89824787507861,131.247475520032));
#87593=CARTESIAN_POINT('Ctrl Pts',(-58.3426097663563,4.91060358909209,131.110893902997));
#87594=CARTESIAN_POINT('Ctrl Pts',(-58.3503702088704,4.91723258963241,130.973903457567));
#87595=CARTESIAN_POINT('Ctrl Pts',(-58.3581306513846,4.91814156587027,130.837019468727));
#87596=CARTESIAN_POINT('Ctrl Pts',(-58.36590355165,4.91905200127748,130.699915741555));
#87597=CARTESIAN_POINT('Ctrl Pts',(-58.3736764519155,4.91422407701677,130.562919203419));
#87598=CARTESIAN_POINT('Ctrl Pts',(-58.3814493521809,4.90371655884486,130.426541913674));
#87599=CARTESIAN_POINT('Ctrl Pts',(-58.3889396879429,4.89359101542543,130.295122281925));
#87600=CARTESIAN_POINT('Ctrl Pts',(-58.3964300237048,4.87819168002817,130.164277963653));
#87601=CARTESIAN_POINT('Ctrl Pts',(-58.4039203594668,4.85761584668391,130.034457150536));
#87602=CARTESIAN_POINT('Ctrl Pts',(-58.4116946935859,4.83625987436435,129.89971414183));
#87603=CARTESIAN_POINT('Ctrl Pts',(-58.419469027705,4.80925947221593,129.765646957418));
#87604=CARTESIAN_POINT('Ctrl Pts',(-58.4272433618241,4.77666709594936,129.632765757141));
#87605=CARTESIAN_POINT('Ctrl Pts',(-58.4350081147711,4.74411488687367,129.500048321068));
#87606=CARTESIAN_POINT('Ctrl Pts',(-58.4427728677182,4.70598450816555,129.368514337008));
#87607=CARTESIAN_POINT('Ctrl Pts',(-58.4505376206653,4.66237994831585,129.238667071548));
#87608=CARTESIAN_POINT('Ctrl Pts',(-58.4582946615503,4.61881869712969,129.108948772223));
#87609=CARTESIAN_POINT('Ctrl Pts',(-58.4660517024353,4.56979420840062,128.980914225856));
#87610=CARTESIAN_POINT('Ctrl Pts',(-58.4738087433203,4.51546103463981,128.855054405821));
#87611=CARTESIAN_POINT('Ctrl Pts',(-58.4815599345604,4.46116883394798,128.729289497654));
#87612=CARTESIAN_POINT('Ctrl Pts',(-58.4893111258005,4.40157607092016,128.605696409035));
#87613=CARTESIAN_POINT('Ctrl Pts',(-58.4970623170406,4.33688631867345,128.48474855487));
#87614=CARTESIAN_POINT('Ctrl Pts',(-58.5048102138177,4.2722240612971,128.36385210677));
#87615=CARTESIAN_POINT('Ctrl Pts',(-58.5125581105949,4.20246930742585,128.245599001017));
#87616=CARTESIAN_POINT('Ctrl Pts',(-58.5203060073719,4.12787262058341,128.130440145537));
#87617=CARTESIAN_POINT('Ctrl Pts',(-58.528052283456,4.05329153775974,128.015305378807));
#87618=CARTESIAN_POINT('Ctrl Pts',(-58.5357985595401,3.97387074895792,127.903263902862));
#87619=CARTESIAN_POINT('Ctrl Pts',(-58.5435448356242,3.88990518274603,127.79473925737));
#87620=CARTESIAN_POINT('Ctrl Pts',(-58.5512911688896,3.8059389967194,127.686213810774));
#87621=CARTESIAN_POINT('Ctrl Pts',(-58.5590375021549,3.71742820558215,127.581205555652));
#87622=CARTESIAN_POINT('Ctrl Pts',(-58.5667838354203,3.6247089642163,127.480106116594));
#87623=CARTESIAN_POINT('Ctrl Pts',(-58.5745319034233,3.53196895901921,127.378984037018));
#87624=CARTESIAN_POINT('Ctrl Pts',(-58.5822799714262,3.43501889242421,127.281772803438));
#87625=CARTESIAN_POINT('Ctrl Pts',(-58.5900280394292,3.33423253081029,127.188827946854));
#87626=CARTESIAN_POINT('Ctrl Pts',(-58.5977843421711,3.23333905225187,127.09578430737));
#87627=CARTESIAN_POINT('Ctrl Pts',(-58.6055406449129,3.12860142177541,127.007016368217));
#87628=CARTESIAN_POINT('Ctrl Pts',(-58.6132969476547,3.02042773995131,126.922840383143));
#87629=CARTESIAN_POINT('Ctrl Pts',(-58.6210573901689,2.91219632257618,126.838619470812));
#87630=CARTESIAN_POINT('Ctrl Pts',(-58.628817832683,2.80052551778018,126.758995622983));
#87631=CARTESIAN_POINT('Ctrl Pts',(-58.6365782751972,2.6858524650723,126.684241735984));
#87632=CARTESIAN_POINT('Ctrl Pts',(-58.6443511754626,2.570995329,126.60936784741));
#87633=CARTESIAN_POINT('Ctrl Pts',(-58.652124075728,2.4531266505316,126.539379741636));
#87634=CARTESIAN_POINT('Ctrl Pts',(-58.6598969759935,2.33270900403111,126.474504757954));
#87635=CARTESIAN_POINT('Ctrl Pts',(-58.6673873117556,2.21666884229353,126.411988143339));
#87636=CARTESIAN_POINT('Ctrl Pts',(-58.6748776475177,2.09826209469348,126.354219490263));
#87637=CARTESIAN_POINT('Ctrl Pts',(-58.6823679832798,1.97791842738403,126.301359201053));
#87638=CARTESIAN_POINT('Ctrl Pts',(-58.6901423173988,1.85301189335193,126.246494697912));
#87639=CARTESIAN_POINT('Ctrl Pts',(-58.6979166515179,1.72562299724315,126.196744312983));
#87640=CARTESIAN_POINT('Ctrl Pts',(-58.705690985637,1.59620930457392,126.152339667646));
#87641=CARTESIAN_POINT('Ctrl Pts',(-58.7134557385841,1.46695510271487,126.107989747067));
#87642=CARTESIAN_POINT('Ctrl Pts',(-58.7212204915311,1.33568143561125,126.068972583302));
#87643=CARTESIAN_POINT('Ctrl Pts',(-58.7289852444783,1.2028679240148,126.035472715772));
#87644=CARTESIAN_POINT('Ctrl Pts',(-58.7367422853633,1.07018632467041,126.002006120783));
#87645=CARTESIAN_POINT('Ctrl Pts',(-58.7444993262484,0.935968301037668,
125.974046011868));
#87646=CARTESIAN_POINT('Ctrl Pts',(-58.7522563671334,0.800710462326672,
125.951727742722));
#87647=CARTESIAN_POINT('Ctrl Pts',(-58.7600075583735,0.665554622603999,
125.929426303956));
#87648=CARTESIAN_POINT('Ctrl Pts',(-58.7677587496135,0.529360912759822,
125.912758299918));
#87649=CARTESIAN_POINT('Ctrl Pts',(-58.7755099408537,0.392637666405466,
125.901808351101));
#87650=CARTESIAN_POINT('Ctrl Pts',(-58.7832578376307,0.255972531078022,
125.890863056304));
#87651=CARTESIAN_POINT('Ctrl Pts',(-58.791005734408,0.118778695783228,125.885631014141));
#87652=CARTESIAN_POINT('Ctrl Pts',(-58.7987536311851,-0.0184290421641127,
125.886145145171));
#87653=CARTESIAN_POINT('Ctrl Pts',(-58.8064999072692,-0.155608079210532,
125.886659168656));
#87654=CARTESIAN_POINT('Ctrl Pts',(-58.8142461833532,-0.292800622410291,
125.892916973076));
#87655=CARTESIAN_POINT('Ctrl Pts',(-58.8219924594373,-0.429490919750866,
125.904899360208));
#87656=CARTESIAN_POINT('Ctrl Pts',(-58.8297387927026,-0.566182226108165,
125.916881835792));
#87657=CARTESIAN_POINT('Ctrl Pts',(-58.837485125968,-0.702370889736662,
125.934588944269));
#87658=CARTESIAN_POINT('Ctrl Pts',(-58.8452314592334,-0.837545725852771,
125.957949551673));
#87659=CARTESIAN_POINT('Ctrl Pts',(-58.8529795272363,-0.972750833436009,
125.981315390524));
#87660=CARTESIAN_POINT('Ctrl Pts',(-58.8607275952393,-1.10694127654346,
126.010337181053));
#87661=CARTESIAN_POINT('Ctrl Pts',(-58.8684756632423,-1.23961590701895,
126.044892636209));
#87662=CARTESIAN_POINT('Ctrl Pts',(-58.8762319659841,-1.37243154567073,
126.079484817313));
#87663=CARTESIAN_POINT('Ctrl Pts',(-58.883988268726,-1.5037277745507,126.119622312767));
#87664=CARTESIAN_POINT('Ctrl Pts',(-58.8917445714679,-1.63301793209567,
126.165132718879));
#87665=CARTESIAN_POINT('Ctrl Pts',(-58.8995050139821,-1.76237709569076,
126.210667415265));
#87666=CARTESIAN_POINT('Ctrl Pts',(-58.9072654564963,-1.88972769163806,
126.261580591349));
#87667=CARTESIAN_POINT('Ctrl Pts',(-58.9150258990104,-2.01460383994363,
126.317651976414));
#87668=CARTESIAN_POINT('Ctrl Pts',(-58.9227987992759,-2.13968045052828,
126.373813372245));
#87669=CARTESIAN_POINT('Ctrl Pts',(-58.9305716995413,-2.26227432589723,
126.435149348929));
#87670=CARTESIAN_POINT('Ctrl Pts',(-58.9383445998068,-2.38194416632168,
126.501393611996));
#87671=CARTESIAN_POINT('Ctrl Pts',(-58.9458349355687,-2.49726370661558,
126.56522972924));
#87672=CARTESIAN_POINT('Ctrl Pts',(-58.9533252713306,-2.60986784986305,
126.633623311383));
#87673=CARTESIAN_POINT('Ctrl Pts',(-58.9608156070926,-2.7193893999931,126.706299569496));
#87674=CARTESIAN_POINT('Ctrl Pts',(-58.968571446223,-2.83279306454415,126.78155191925));
#87675=CARTESIAN_POINT('Ctrl Pts',(-58.9763272853535,-2.94325496047855,
126.861637362605));
#87676=CARTESIAN_POINT('Ctrl Pts',(-58.9840831244839,-3.05033395842733,
126.9462981758));
#87677=CARTESIAN_POINT('Ctrl Pts',(-58.9918266920159,-3.15724353170873,
127.030825035275));
#87678=CARTESIAN_POINT('Ctrl Pts',(-58.9995702595479,-3.26078056114886,
127.11991260563));
#87679=CARTESIAN_POINT('Ctrl Pts',(-59.0073138270799,-3.36053194376454,
127.213259377356));
#87680=CARTESIAN_POINT('Ctrl Pts',(-59.0150503122169,-3.4601920921144,127.306520772579));
#87681=CARTESIAN_POINT('Ctrl Pts',(-59.0227867973538,-3.55607319546732,
127.404033354081));
#87682=CARTESIAN_POINT('Ctrl Pts',(-59.0305232824907,-3.6477941619193,127.505454614848));
#87683=CARTESIAN_POINT('Ctrl Pts',(-59.0382543904089,-3.73945137801255,
127.606805383099));
#87684=CARTESIAN_POINT('Ctrl Pts',(-59.0459854983271,-3.82695394721599,
127.712059135335));
#87685=CARTESIAN_POINT('Ctrl Pts',(-59.0537166062452,-3.90995700446654,
127.820835976186));
#87686=CARTESIAN_POINT('Ctrl Pts',(-59.061444038016,-3.99292059370397,127.929561093571));
#87687=CARTESIAN_POINT('Ctrl Pts',(-59.0691714697868,-4.07138869102997,
128.04180565369));
#87688=CARTESIAN_POINT('Ctrl Pts',(-59.0768989015577,-4.14505645487896,
128.157156422879));
#87689=CARTESIAN_POINT('Ctrl Pts',(-59.0846259704071,-4.21872075889714,
128.272501774582));
#87690=CARTESIAN_POINT('Ctrl Pts',(-59.0923530392565,-4.28758495728074,
128.390952719827));
#87691=CARTESIAN_POINT('Ctrl Pts',(-59.100080108106,-4.351387403744,128.512066848208));
#87692=CARTESIAN_POINT('Ctrl Pts',(-59.1078067175771,-4.41518605711833,
128.63317377629));
#87693=CARTESIAN_POINT('Ctrl Pts',(-59.1155333270482,-4.47392337873462,
128.756943222097));
#87694=CARTESIAN_POINT('Ctrl Pts',(-59.1232599365194,-4.52738395536537,
128.882908670938));
#87695=CARTESIAN_POINT('Ctrl Pts',(-59.1309909096984,-4.58087472458491,
129.008945260482));
#87696=CARTESIAN_POINT('Ctrl Pts',(-59.1387218828775,-4.62908264408669,
129.137179967326));
#87697=CARTESIAN_POINT('Ctrl Pts',(-59.1464528560566,-4.67184062006425,
129.267126646039));
#87698=CARTESIAN_POINT('Ctrl Pts',(-59.1526466080874,-4.70609663084208,
129.37123482059));
#87699=CARTESIAN_POINT('Ctrl Pts',(-59.1588403601182,-4.7368554690376,129.476441400305));
#87700=CARTESIAN_POINT('Ctrl Pts',(-59.165034112149,-4.76405452823398,129.582490119308));
#87701=CARTESIAN_POINT('Ctrl Pts',(-57.4152011815765,-4.76405452823411,
129.582490119308));
#87702=CARTESIAN_POINT('Ctrl Pts',(-57.4229006030558,-4.79795614748395,
129.714672018235));
#87703=CARTESIAN_POINT('Ctrl Pts',(-57.4306000245351,-4.82635740057608,
129.848285643771));
#87704=CARTESIAN_POINT('Ctrl Pts',(-57.4382994460144,-4.84915170512526,
129.982831066557));
#87705=CARTESIAN_POINT('Ctrl Pts',(-57.4461062990135,-4.87226406302232,
130.119253827696));
#87706=CARTESIAN_POINT('Ctrl Pts',(-57.4539131520124,-4.88961172564464,
130.256634178774));
#87707=CARTESIAN_POINT('Ctrl Pts',(-57.4617200050115,-4.90113765442327,
130.394442631995));
#87708=CARTESIAN_POINT('Ctrl Pts',(-57.4695268580105,-4.91266358320189,
130.532251085217));
#87709=CARTESIAN_POINT('Ctrl Pts',(-57.4773337110095,-4.91836776813177,
130.670487216997));
#87710=CARTESIAN_POINT('Ctrl Pts',(-57.4851405640085,-4.91824815608826,
130.808619447741));
#87711=CARTESIAN_POINT('',(-57.139859435939,-4.91824920542422,130.801564934464));
#87712=CARTESIAN_POINT('Ctrl Pts',(-57.0701182010015,-4.76405452823404,
129.582490119308));
#87713=CARTESIAN_POINT('Ctrl Pts',(-57.0787834017356,-4.80194788990491,
129.730235761351));
#87714=CARTESIAN_POINT('Ctrl Pts',(-57.0874486024699,-4.83300862439036,
129.87991862542));
#87715=CARTESIAN_POINT('Ctrl Pts',(-57.0961138032041,-4.85705530084033,
130.030928741394));
#87716=CARTESIAN_POINT('Ctrl Pts',(-57.1047341945617,-4.88097762742078,
130.181157955764));
#87717=CARTESIAN_POINT('Ctrl Pts',(-57.1133545859192,-4.89795815486478,
130.332700521287));
#87718=CARTESIAN_POINT('Ctrl Pts',(-57.1219749772768,-4.90786633239802,
130.484937503478));
#87719=CARTESIAN_POINT('Ctrl Pts',(-57.1279364634976,-4.91471839530177,
130.590217952354));
#87720=CARTESIAN_POINT('Ctrl Pts',(-57.1338979497183,-4.91818910252655,
130.695830121914));
#87721=CARTESIAN_POINT('Ctrl Pts',(-57.139859435939,-4.91824920542422,130.801564934464));
#87722=CARTESIAN_POINT('Ctrl Pts',(-57.139859435991,-4.91824920542475,130.801564935387));
#87723=CARTESIAN_POINT('Ctrl Pts',(-57.1476908595179,-4.91832816075135,
130.940465549757));
#87724=CARTESIAN_POINT('Ctrl Pts',(-57.1555222830448,-4.91251855116177,
131.079373617091));
#87725=CARTESIAN_POINT('Ctrl Pts',(-57.1633537065717,-4.90084506944486,
131.217761957426));
#87726=CARTESIAN_POINT('Ctrl Pts',(-57.1711866138629,-4.8891693760361,131.356176517219));
#87727=CARTESIAN_POINT('Ctrl Pts',(-57.179019521154,-4.87162762925993,131.494070776241));
#87728=CARTESIAN_POINT('Ctrl Pts',(-57.1868524284452,-4.84829641842778,
131.630922715391));
#87729=CARTESIAN_POINT('Ctrl Pts',(-57.194688372281,-4.8249561629001,131.767827707257));
#87730=CARTESIAN_POINT('Ctrl Pts',(-57.2025243161168,-4.79582203705538,
131.903689201124));
#87731=CARTESIAN_POINT('Ctrl Pts',(-57.2103602599526,-4.76102170627262,
132.037995642564));
#87732=CARTESIAN_POINT('Ctrl Pts',(-57.2182007948159,-4.72620098620692,
132.172380773256));
#87733=CARTESIAN_POINT('Ctrl Pts',(-57.2260413296791,-4.68570754438162,
132.305208670745));
#87734=CARTESIAN_POINT('Ctrl Pts',(-57.2338818645424,-4.63971874720671,
132.435983432226));
#87735=CARTESIAN_POINT('Ctrl Pts',(-57.2417332379249,-4.5936663765037,132.566938972798));
#87736=CARTESIAN_POINT('Ctrl Pts',(-57.2495846113074,-4.54210360681127,
132.695835352532));
#87737=CARTESIAN_POINT('Ctrl Pts',(-57.25743598469,-4.48525600926085,132.822196486483));
#87738=CARTESIAN_POINT('Ctrl Pts',(-57.2652937880904,-4.42836185538808,
132.948661106069));
#87739=CARTESIAN_POINT('Ctrl Pts',(-57.2731515914908,-4.3661744177312,133.072586004796));
#87740=CARTESIAN_POINT('Ctrl Pts',(-57.2810093948912,-4.29896459324919,
133.193520823264));
#87741=CARTESIAN_POINT('Ctrl Pts',(-57.2888794534532,-4.23164994720188,
133.314644253695));
#87742=CARTESIAN_POINT('Ctrl Pts',(-57.2967495120151,-4.15929747147366,
133.432767971077));
#87743=CARTESIAN_POINT('Ctrl Pts',(-57.304619570577,-4.08222093126828,133.547471138638));
#87744=CARTESIAN_POINT('Ctrl Pts',(-57.306319333843,-4.06557405746394,133.572244554132));
#87745=CARTESIAN_POINT('Ctrl Pts',(-57.308019097109,-4.04870696780659,133.596858538697));
#87746=CARTESIAN_POINT('Ctrl Pts',(-57.3097188603751,-4.03162306031359,
133.621309066162));
#87747=CARTESIAN_POINT('Ctrl Pts',(-57.3174931944941,-3.95348511748049,
133.7331402686));
#87748=CARTESIAN_POINT('Ctrl Pts',(-57.3252675286132,-3.87056683763764,
133.841894995027));
#87749=CARTESIAN_POINT('Ctrl Pts',(-57.3330418627323,-3.78313852325258,
133.947137411483));
#87750=CARTESIAN_POINT('Ctrl Pts',(-57.3408066156794,-3.69581795645107,
134.052250126066));
#87751=CARTESIAN_POINT('Ctrl Pts',(-57.3485713686265,-3.60399866172716,
134.153858845474));
#87752=CARTESIAN_POINT('Ctrl Pts',(-57.3563361215736,-3.5079942690365,134.251556473752));
#87753=CARTESIAN_POINT('Ctrl Pts',(-57.3640931624586,-3.41208522926223,
134.349157067369));
#87754=CARTESIAN_POINT('Ctrl Pts',(-57.3718502033437,-3.31199963579226,
134.442854023233));
#87755=CARTESIAN_POINT('Ctrl Pts',(-57.3796072442287,-3.20809121308795,
134.532273415769));
#87756=CARTESIAN_POINT('Ctrl Pts',(-57.3873584354688,-3.10426114853378,
134.621625376446));
#87757=CARTESIAN_POINT('Ctrl Pts',(-57.3951096267088,-2.9966142879771,134.706705940454));
#87758=CARTESIAN_POINT('Ctrl Pts',(-57.4028608179489,-2.88554075954532,
134.787178412482));
#87759=CARTESIAN_POINT('Ctrl Pts',(-57.410608714726,-2.77451444032595,134.867616681564));
#87760=CARTESIAN_POINT('Ctrl Pts',(-57.4183566115031,-2.66006466589254,
134.943450525197));
#87761=CARTESIAN_POINT('Ctrl Pts',(-57.4261045082801,-2.54261397797426,
135.014384040483));
#87762=CARTESIAN_POINT('Ctrl Pts',(-57.4338507843642,-2.42518785820794,
135.085302718007));
#87763=CARTESIAN_POINT('Ctrl Pts',(-57.4415970604484,-2.3047624079933,135.151322904059));
#87764=CARTESIAN_POINT('Ctrl Pts',(-57.4493433365325,-2.18178809553241,
135.212192711543));
#87765=CARTESIAN_POINT('Ctrl Pts',(-57.4570896697978,-2.05881287530308,
135.273062968354));
#87766=CARTESIAN_POINT('Ctrl Pts',(-57.4648360030631,-1.93328910567397,
135.328782597298));
#87767=CARTESIAN_POINT('Ctrl Pts',(-57.4725823363285,-1.80569037006717,
135.379146443148));
#87768=CARTESIAN_POINT('Ctrl Pts',(-57.4803304043315,-1.67806305960806,
135.429521567633));
#87769=CARTESIAN_POINT('Ctrl Pts',(-57.4880784723345,-1.548360222116,135.474538378864));
#87770=CARTESIAN_POINT('Ctrl Pts',(-57.4958265403374,-1.41707347793118,
135.514040630119));
#87771=CARTESIAN_POINT('Ctrl Pts',(-57.5035828430793,-1.2856472006323,135.553584864837));
#87772=CARTESIAN_POINT('Ctrl Pts',(-57.5113391458211,-1.15263402886043,
135.587602718894));
#87773=CARTESIAN_POINT('Ctrl Pts',(-57.519095448563,-1.01853928021185,135.615988283665));
#87774=CARTESIAN_POINT('Ctrl Pts',(-57.5268558910771,-0.884372961158409,
135.644388998666));
#87775=CARTESIAN_POINT('Ctrl Pts',(-57.5346163335913,-0.749124300323084,
135.667151369573));
#87776=CARTESIAN_POINT('Ctrl Pts',(-57.5423767761054,-0.613305766086227,
135.684221179076));
#87777=CARTESIAN_POINT('Ctrl Pts',(-57.5501496763709,-0.477269203880809,
135.701318390554));
#87778=CARTESIAN_POINT('Ctrl Pts',(-57.5579225766363,-0.340661330027623,
135.712704747089));
#87779=CARTESIAN_POINT('Ctrl Pts',(-57.5656954769018,-0.203997560556797,
135.718378124432));
#87780=CARTESIAN_POINT('Ctrl Pts',(-57.5731858126638,-0.0723018633416816,
135.723845260219));
#87781=CARTESIAN_POINT('Ctrl Pts',(-57.5806761484258,0.0594454281349506,
135.724007567502));
#87782=CARTESIAN_POINT('Ctrl Pts',(-57.5881664841878,0.190787767961467,
135.718908723964));
#87783=CARTESIAN_POINT('Ctrl Pts',(-57.5959408183069,0.327109992523338,
135.713616556223));
#87784=CARTESIAN_POINT('Ctrl Pts',(-57.6037151524259,0.463427779607381,
135.702639645139));
#87785=CARTESIAN_POINT('Ctrl Pts',(-57.611489486545,0.599228344672425,135.685969824932));
#87786=CARTESIAN_POINT('Ctrl Pts',(-57.6192542394921,0.734861547677503,
135.669320548788));
#87787=CARTESIAN_POINT('Ctrl Pts',(-57.6270189924393,0.869978412631856,
135.64699237045));
#87788=CARTESIAN_POINT('Ctrl Pts',(-57.6347837453863,1.00406691352968,135.619029110376));
#87789=CARTESIAN_POINT('Ctrl Pts',(-57.6425407862713,1.13802223583827,135.591093623805));
#87790=CARTESIAN_POINT('Ctrl Pts',(-57.6502978271563,1.27095084643934,135.557534272768));
#87791=CARTESIAN_POINT('Ctrl Pts',(-57.6580548680413,1.40234695444476,135.518446539763));
#87792=CARTESIAN_POINT('Ctrl Pts',(-57.6658060592814,1.53364397562319,135.479388283122));
#87793=CARTESIAN_POINT('Ctrl Pts',(-57.6735572505215,1.66341042128189,135.434810053673));
#87794=CARTESIAN_POINT('Ctrl Pts',(-57.6813084417617,1.79115214633792,135.384858085218));
#87795=CARTESIAN_POINT('Ctrl Pts',(-57.6890563385388,1.91883957775318,135.334927347683));
#87796=CARTESIAN_POINT('Ctrl Pts',(-57.6968042353158,2.04450363680051,135.279627555894));
#87797=CARTESIAN_POINT('Ctrl Pts',(-57.7045521320929,2.1676669778647,135.219154263432));
#87798=CARTESIAN_POINT('Ctrl Pts',(-57.712298408177,2.29080455581303,135.158693620678));
#87799=CARTESIAN_POINT('Ctrl Pts',(-57.7200446842612,2.41144210552369,135.09306180198));
#87800=CARTESIAN_POINT('Ctrl Pts',(-57.7277909603453,2.52912421818262,135.022501647866));
#87801=CARTESIAN_POINT('Ctrl Pts',(-57.7355372936106,2.64680719954401,134.951940972893));
#87802=CARTESIAN_POINT('Ctrl Pts',(-57.7432836268759,2.76153436500908,134.876452090958));
#87803=CARTESIAN_POINT('Ctrl Pts',(-57.7510299601413,2.87287712826909,134.796322549795));
#87804=CARTESIAN_POINT('Ctrl Pts',(-57.7587780281442,2.98424482596878,134.716175064178));
#87805=CARTESIAN_POINT('Ctrl Pts',(-57.7665260961472,3.0922262960322,134.631385079688));
#87806=CARTESIAN_POINT('Ctrl Pts',(-57.7742741641501,3.19642435086389,134.542281755271));
#87807=CARTESIAN_POINT('Ctrl Pts',(-57.782030466892,3.30073314862851,134.453083730781));
#87808=CARTESIAN_POINT('Ctrl Pts',(-57.789786769634,3.40125020105201,134.35956346329));
#87809=CARTESIAN_POINT('Ctrl Pts',(-57.7975430723758,3.49761326770551,134.262088844606));
#87810=CARTESIAN_POINT('Ctrl Pts',(-57.80530351489,3.59402776622913,134.164562200783));
#87811=CARTESIAN_POINT('Ctrl Pts',(-57.8130639574041,3.68628359835076,134.063077289458));
#87812=CARTESIAN_POINT('Ctrl Pts',(-57.8208243999183,3.7740581478354,133.958035959014));
#87813=CARTESIAN_POINT('Ctrl Pts',(-57.8285973001837,3.86197360081913,133.852826006901));
#87814=CARTESIAN_POINT('Ctrl Pts',(-57.8363702004491,3.94539315770099,133.744048537527));
#87815=CARTESIAN_POINT('Ctrl Pts',(-57.8441431007145,4.02403643633555,133.632136036786));
#87816=CARTESIAN_POINT('Ctrl Pts',(-57.8516334364766,4.09982083370139,133.524291837337));
#87817=CARTESIAN_POINT('Ctrl Pts',(-57.8591237722386,4.17117001656507,133.413536840791));
#87818=CARTESIAN_POINT('Ctrl Pts',(-57.8666141080007,4.23787395798125,133.300278761008));
#87819=CARTESIAN_POINT('Ctrl Pts',(-57.8743884421198,4.30710699961025,133.182726466706));
#87820=CARTESIAN_POINT('Ctrl Pts',(-57.8821627762388,4.37155490709918,133.062105163146));
#87821=CARTESIAN_POINT('Ctrl Pts',(-57.8899371103579,4.43093363777566,132.93884185668));
#87822=CARTESIAN_POINT('Ctrl Pts',(-57.897701863305,4.49023918947333,132.815730461223));
#87823=CARTESIAN_POINT('Ctrl Pts',(-57.9054666162521,4.54448782659129,132.68998389024));
#87824=CARTESIAN_POINT('Ctrl Pts',(-57.9132313691992,4.59343965395904,132.56205661174));
#87825=CARTESIAN_POINT('Ctrl Pts',(-57.9209884100842,4.64234286168181,132.434256392417));
#87826=CARTESIAN_POINT('Ctrl Pts',(-57.9287454509691,4.68595959019541,132.304280138616));
#87827=CARTESIAN_POINT('Ctrl Pts',(-57.9365024918541,4.72409677930186,132.17260499716));
#87828=CARTESIAN_POINT('Ctrl Pts',(-57.9442536830942,4.7622052088574,132.041029152952));
#87829=CARTESIAN_POINT('Ctrl Pts',(-57.9520048743344,4.79484221550081,131.907757345141));
#87830=CARTESIAN_POINT('Ctrl Pts',(-57.9597560655746,4.82186373238449,131.773284354924));
#87831=CARTESIAN_POINT('Ctrl Pts',(-57.9675039623516,4.84887376440267,131.638868519314));
#87832=CARTESIAN_POINT('Ctrl Pts',(-57.9752518591287,4.87027297682982,131.503252899212));
#87833=CARTESIAN_POINT('Ctrl Pts',(-57.9829997559058,4.88596787746547,131.366944800489));
#87834=CARTESIAN_POINT('Ctrl Pts',(-57.9907460319899,4.90165949506622,131.230665214483));
#87835=CARTESIAN_POINT('Ctrl Pts',(-57.998492308074,4.91164912956055,131.093693826126));
#87836=CARTESIAN_POINT('Ctrl Pts',(-58.0062385841581,4.91589492997459,130.956545044989));
#87837=CARTESIAN_POINT('Ctrl Pts',(-58.0139849174234,4.92014076173016,130.819395251451));
#87838=CARTESIAN_POINT('Ctrl Pts',(-58.0217312506888,4.9186426627024,130.682068453299));
#87839=CARTESIAN_POINT('Ctrl Pts',(-58.0294775839542,4.91141089357604,130.545080658906));
#87840=CARTESIAN_POINT('Ctrl Pts',(-58.0372256519571,4.90417750494514,130.408062187047));
#87841=CARTESIAN_POINT('Ctrl Pts',(-58.0449737199599,4.89120791178008,130.271383260361));
#87842=CARTESIAN_POINT('Ctrl Pts',(-58.0527217879629,4.87256435522666,130.135555962473));
#87843=CARTESIAN_POINT('Ctrl Pts',(-58.0604780907047,4.85390098407946,129.999584305715));
#87844=CARTESIAN_POINT('Ctrl Pts',(-58.0682343934466,4.82955165650847,129.864466473782));
#87845=CARTESIAN_POINT('Ctrl Pts',(-58.0759906961885,4.79963009050997,129.730706084315));
#87846=CARTESIAN_POINT('Ctrl Pts',(-58.0837511387027,4.76969255447069,129.596874302899));
#87847=CARTESIAN_POINT('Ctrl Pts',(-58.0915115812168,4.73417695510684,129.464401785036));
#87848=CARTESIAN_POINT('Ctrl Pts',(-58.0992720237309,4.69324699688804,129.333777165768));
#87849=CARTESIAN_POINT('Ctrl Pts',(-58.1070449239964,4.65225133426672,129.202942856265));
#87850=CARTESIAN_POINT('Ctrl Pts',(-58.1148178242619,4.60582407667476,129.073962741261));
#87851=CARTESIAN_POINT('Ctrl Pts',(-58.1225907245274,4.55417753334568,128.947306483388));
#87852=CARTESIAN_POINT('Ctrl Pts',(-58.1300810602895,4.50440847195605,128.825254499514));
#87853=CARTESIAN_POINT('Ctrl Pts',(-58.1375713960515,4.44979313275573,128.705360630282));
#87854=CARTESIAN_POINT('Ctrl Pts',(-58.1450617318136,4.39056101226808,128.588021956609));
#87855=CARTESIAN_POINT('Ctrl Pts',(-58.1528360659327,4.32908308792936,128.46623435146));
#87856=CARTESIAN_POINT('Ctrl Pts',(-58.1606104000518,4.26243663729623,128.346813740717));
#87857=CARTESIAN_POINT('Ctrl Pts',(-58.1683847341709,4.19082738090478,128.230229904887));
#87858=CARTESIAN_POINT('Ctrl Pts',(-58.176149487118,4.11930637652203,128.113789748215));
#87859=CARTESIAN_POINT('Ctrl Pts',(-58.183914240065,4.04283493848531,128.00017974026));
#87860=CARTESIAN_POINT('Ctrl Pts',(-58.1916789930121,3.9616657544016,127.889847362681));
#87861=CARTESIAN_POINT('Ctrl Pts',(-58.1994360338971,3.88057718869581,127.779624568775));
#87862=CARTESIAN_POINT('Ctrl Pts',(-58.2071930747821,3.79480039241356,127.67267323976));
#87863=CARTESIAN_POINT('Ctrl Pts',(-58.2149501156671,3.70463244893746,127.569413712163));
#87864=CARTESIAN_POINT('Ctrl Pts',(-58.2227013069072,3.61453250180882,127.466232053378));
#87865=CARTESIAN_POINT('Ctrl Pts',(-58.2304524981473,3.52004825473804,127.366736947894));
#87866=CARTESIAN_POINT('Ctrl Pts',(-58.2382036893875,3.42151810950774,127.271317044553));
#87867=CARTESIAN_POINT('Ctrl Pts',(-58.2459515861645,3.32302984221768,127.175937697216));
#87868=CARTESIAN_POINT('Ctrl Pts',(-58.2536994829416,3.22049937721389,127.084630378483));
#87869=CARTESIAN_POINT('Ctrl Pts',(-58.2614473797186,3.1143029904755,126.997747957206));
#87870=CARTESIAN_POINT('Ctrl Pts',(-58.2691936558027,3.00812881773203,126.910883709858));
#87871=CARTESIAN_POINT('Ctrl Pts',(-58.2769399318869,2.89829055093085,126.828442766318));
#87872=CARTESIAN_POINT('Ctrl Pts',(-58.284686207971,2.78519835593871,126.750738387933));
#87873=CARTESIAN_POINT('Ctrl Pts',(-58.2924325412363,2.67210532612552,126.673033435952));
#87874=CARTESIAN_POINT('Ctrl Pts',(-58.3001788745017,2.55575864242525,126.600065340297));
#87875=CARTESIAN_POINT('Ctrl Pts',(-58.307925207767,2.4365979834481,126.532104383495));
#87876=CARTESIAN_POINT('Ctrl Pts',(-58.31567327577,2.31741063926789,126.464128207309));
#87877=CARTESIAN_POINT('Ctrl Pts',(-58.3234213437728,2.19540840539337,126.401161594914));
#87878=CARTESIAN_POINT('Ctrl Pts',(-58.3311694117758,2.07105575513923,126.343428974781));
#87879=CARTESIAN_POINT('Ctrl Pts',(-58.3389257145176,1.94657094140841,126.285634995731));
#87880=CARTESIAN_POINT('Ctrl Pts',(-58.3466820172595,1.81973107635018,126.233086286029));
#87881=CARTESIAN_POINT('Ctrl Pts',(-58.3544383200013,1.69102133510279,126.18595938914));
#87882=CARTESIAN_POINT('Ctrl Pts',(-58.3621987625155,1.56224289759094,126.138807339207));
#87883=CARTESIAN_POINT('Ctrl Pts',(-58.3699592050297,1.43159296752367,126.09708298708));
#87884=CARTESIAN_POINT('Ctrl Pts',(-58.3777196475439,1.29957113366506,126.060912722728));
#87885=CARTESIAN_POINT('Ctrl Pts',(-58.3854925478093,1.16733736663822,126.024684394656));
#87886=CARTESIAN_POINT('Ctrl Pts',(-58.3932654480747,1.03372767620185,125.994028058683));
#87887=CARTESIAN_POINT('Ctrl Pts',(-58.4010383483401,0.899251961154634,
125.96901895716));
#87888=CARTESIAN_POINT('Ctrl Pts',(-58.4085286841022,0.769664777072177,
125.944918999471));
#87889=CARTESIAN_POINT('Ctrl Pts',(-58.4160190198644,0.639273744424748,
125.926062866237));
#87890=CARTESIAN_POINT('Ctrl Pts',(-58.4235093556265,0.508536987110952,
125.912472107467));
#87891=CARTESIAN_POINT('Ctrl Pts',(-58.4312836897455,0.372843305908174,
125.898366050948));
#87892=CARTESIAN_POINT('Ctrl Pts',(-58.4390580238647,0.236347329424679,
125.889887840273));
#87893=CARTESIAN_POINT('Ctrl Pts',(-58.4468323579838,0.0995554942823636,
125.88711832477));
#87894=CARTESIAN_POINT('Ctrl Pts',(-58.4545971109309,-0.0370677571485767,
125.884352222448));
#87895=CARTESIAN_POINT('Ctrl Pts',(-58.4623618638779,-0.173985754621854,
125.887280824673));
#87896=CARTESIAN_POINT('Ctrl Pts',(-58.470126616825,-0.310685435319369,
125.895933412974));
#87897=CARTESIAN_POINT('Ctrl Pts',(-58.47788365771,-0.447249343966886,125.904577407402));
#87898=CARTESIAN_POINT('Ctrl Pts',(-58.4856406985951,-0.58359497969117,
125.918934049676));
#87899=CARTESIAN_POINT('Ctrl Pts',(-58.4933977394801,-0.71920812064433,
125.93898059729));
#87900=CARTESIAN_POINT('Ctrl Pts',(-58.5011489307201,-0.854718994672243,
125.959012027647));
#87901=CARTESIAN_POINT('Ctrl Pts',(-58.5089001219603,-0.989498088210454,
125.984724765824));
#87902=CARTESIAN_POINT('Ctrl Pts',(-58.5166513132004,-1.1230355055525,126.016044179008));
#87903=CARTESIAN_POINT('Ctrl Pts',(-58.5243992099774,-1.25651616593068,
126.047350280606));
#87904=CARTESIAN_POINT('Ctrl Pts',(-58.5321471067545,-1.38875581991871,
126.084258228547));
#87905=CARTESIAN_POINT('Ctrl Pts',(-58.5398950035315,-1.51925420260059,
126.126642185426));
#87906=CARTESIAN_POINT('Ctrl Pts',(-58.5476412796156,-1.64972528783386,
126.169017276496));
#87907=CARTESIAN_POINT('Ctrl Pts',(-58.5553875556997,-1.77845545463806,
126.216865977421));
#87908=CARTESIAN_POINT('Ctrl Pts',(-58.5631338317838,-1.90495944269964,
126.270012529454));
#87909=CARTESIAN_POINT('Ctrl Pts',(-58.5708801650492,-2.0314643645851,126.323159473802));
#87910=CARTESIAN_POINT('Ctrl Pts',(-58.5786264983145,-2.15574271448898,
126.381604195862));
#87911=CARTESIAN_POINT('Ctrl Pts',(-58.5863728315799,-2.27732943903889,
126.445122875875));
#87912=CARTESIAN_POINT('Ctrl Pts',(-58.5941208995829,-2.39894339209292,
126.508655780455));
#87913=CARTESIAN_POINT('Ctrl Pts',(-58.6018689675858,-2.51786417388733,
126.577264723053));
#87914=CARTESIAN_POINT('Ctrl Pts',(-58.6096170355888,-2.63365190722394,
126.650680238182));
#87915=CARTESIAN_POINT('Ctrl Pts',(-58.6173733383307,-2.74956270114128,
126.724173780195));
#87916=CARTESIAN_POINT('Ctrl Pts',(-58.6251296410725,-2.8623334641704,126.802483889793));
#87917=CARTESIAN_POINT('Ctrl Pts',(-58.6328859438143,-2.97155341628101,
126.885297801447));
#87918=CARTESIAN_POINT('Ctrl Pts',(-58.6406463863285,-3.08083166236861,
126.968155913379));
#87919=CARTESIAN_POINT('Ctrl Pts',(-58.6484068288427,-3.18655502001154,
127.055522368244));
#87920=CARTESIAN_POINT('Ctrl Pts',(-58.6561672713569,-3.2883471138192,127.147045164732));
#87921=CARTESIAN_POINT('Ctrl Pts',(-58.6639401716223,-3.39030261333251,
127.238714881738));
#87922=CARTESIAN_POINT('Ctrl Pts',(-58.6717130718878,-3.48831395829851,
127.334553999909));
#87923=CARTESIAN_POINT('Ctrl Pts',(-58.6794859721532,-3.58204223243934,
127.434174197274));
#87924=CARTESIAN_POINT('Ctrl Pts',(-58.6869763079152,-3.67236324772761,
127.530172949536));
#87925=CARTESIAN_POINT('Ctrl Pts',(-58.6944666436772,-3.7587069847742,127.629682417567));
#87926=CARTESIAN_POINT('Ctrl Pts',(-58.7019569794392,-3.84080768578747,
127.732328817064));
#87927=CARTESIAN_POINT('Ctrl Pts',(-58.7097173502063,-3.92586820915285,
127.838675734386));
#87928=CARTESIAN_POINT('Ctrl Pts',(-58.7174777209734,-4.00664976386243,
127.948734816506));
#87929=CARTESIAN_POINT('Ctrl Pts',(-58.7252380917405,-4.0828096513879,128.062126416584));
#87930=CARTESIAN_POINT('Ctrl Pts',(-58.7331313418183,-4.16027360977096,
128.177459598851));
#87931=CARTESIAN_POINT('Ctrl Pts',(-58.741024591896,-4.23295586205342,128.29624021107));
#87932=CARTESIAN_POINT('Ctrl Pts',(-58.7489178419738,-4.30053666294926,
128.418031329071));
#87933=CARTESIAN_POINT('Ctrl Pts',(-58.7566587308323,-4.36681297036912,
128.537471546864));
#87934=CARTESIAN_POINT('Ctrl Pts',(-58.7643996196907,-4.42818275921784,
128.659806752579));
#87935=CARTESIAN_POINT('Ctrl Pts',(-58.7721405085491,-4.48438690609844,
128.784594012507));
#87936=CARTESIAN_POINT('Ctrl Pts',(-58.7801099392367,-4.54225042295116,
128.913065488699));
#87937=CARTESIAN_POINT('Ctrl Pts',(-58.7880793699241,-4.59463830909258,
129.044135708188));
#87938=CARTESIAN_POINT('Ctrl Pts',(-58.7960488006117,-4.6413181232458,129.177292966443));
#87939=CARTESIAN_POINT('Ctrl Pts',(-58.8040182312992,-4.68799793739903,
129.310450224698));
#87940=CARTESIAN_POINT('Ctrl Pts',(-58.8119876619867,-4.72896949444375,
129.44569410505));
#87941=CARTESIAN_POINT('Ctrl Pts',(-58.8199570926742,-4.76405452823407,
129.582490119308));
#87942=CARTESIAN_POINT('Origin',(213.235140564004,0.,130.804360617566));
#87943=CARTESIAN_POINT('',(-60.9152461054369,-4.76405452823402,129.582490119308));
#87944=CARTESIAN_POINT('',(-60.5697319016605,-4.76405452823403,129.582490119308));
#87945=CARTESIAN_POINT('',(213.235140564004,-4.76405452823405,129.582490119308));
#87946=CARTESIAN_POINT('',(-59.2351405639695,-4.91824997905427,130.804814525752));
#87947=CARTESIAN_POINT('Ctrl Pts',(-59.2351405640084,-4.91824997905421,
130.804814526437));
#87948=CARTESIAN_POINT('Ctrl Pts',(-59.2365147863075,-4.91824775337627,
130.828930469497));
#87949=CARTESIAN_POINT('Ctrl Pts',(-59.2378890086065,-4.91806815542009,
130.853045470433));
#87950=CARTESIAN_POINT('Ctrl Pts',(-59.2392632309054,-4.91771121833615,
130.877157839702));
#87951=CARTESIAN_POINT('Ctrl Pts',(-59.2470375650245,-4.9156919321172,131.013567804266));
#87952=CARTESIAN_POINT('Ctrl Pts',(-59.2548118991436,-4.90798943313343,
131.150109750795));
#87953=CARTESIAN_POINT('Ctrl Pts',(-59.2625862332627,-4.89458325254077,
131.286271238374));
#87954=CARTESIAN_POINT('Ctrl Pts',(-59.2703509862099,-4.88119359386754,
131.422264919089));
#87955=CARTESIAN_POINT('Ctrl Pts',(-59.278115739157,-4.86211427769381,131.55787868844));
#87956=CARTESIAN_POINT('Ctrl Pts',(-59.2858804921042,-4.8373768246463,131.692599616302));
#87957=CARTESIAN_POINT('Ctrl Pts',(-59.2936375329892,-4.8126639411859,131.827186737439));
#87958=CARTESIAN_POINT('Ctrl Pts',(-59.3013945738742,-4.78230417454216,
131.960882399776));
#87959=CARTESIAN_POINT('Ctrl Pts',(-59.3091516147592,-4.74638084213209,
132.093178666765));
#87960=CARTESIAN_POINT('Ctrl Pts',(-59.3169028059993,-4.71048459978648,
132.22537516811));
#87961=CARTESIAN_POINT('Ctrl Pts',(-59.3246539972396,-4.66903324465619,
132.356173998829));
#87962=CARTESIAN_POINT('Ctrl Pts',(-59.3324051884797,-4.62216111031285,
132.485077646935));
#87963=CARTESIAN_POINT('Ctrl Pts',(-59.3401530852568,-4.57530889787697,
132.613926507552));
#87964=CARTESIAN_POINT('Ctrl Pts',(-59.3479009820339,-4.52304062198529,
132.74088142098));
#87965=CARTESIAN_POINT('Ctrl Pts',(-59.355648878811,-4.46554032492361,132.865460486321));
#87966=CARTESIAN_POINT('Ctrl Pts',(-59.3633951548951,-4.4080520556845,132.990013492407));
#87967=CARTESIAN_POINT('Ctrl Pts',(-59.3711414309793,-4.34533410588747,
133.112191284166));
#87968=CARTESIAN_POINT('Ctrl Pts',(-59.3788877070634,-4.27761831757293,
133.231532756427));
#87969=CARTESIAN_POINT('Ctrl Pts',(-59.3866340403288,-4.20990202939593,
133.35087510964));
#87970=CARTESIAN_POINT('Ctrl Pts',(-59.3943803735941,-4.1371880220269,133.467380761537));
#87971=CARTESIAN_POINT('Ctrl Pts',(-59.4021267068594,-4.05975347550475,
133.580614348879));
#87972=CARTESIAN_POINT('Ctrl Pts',(-59.4098747748624,-3.98230158805259,
133.693873294097));
#87973=CARTESIAN_POINT('Ctrl Pts',(-59.4176228428654,-3.90012727852677,
133.803858394002));
#87974=CARTESIAN_POINT('Ctrl Pts',(-59.4253709108685,-3.81355007967587,
133.91016467647));
#87975=CARTESIAN_POINT('Ctrl Pts',(-59.4331272136103,-3.72688086554775,
134.01658394252));
#87976=CARTESIAN_POINT('Ctrl Pts',(-59.4408835163522,-3.63579966168534,
134.119316277072));
#87977=CARTESIAN_POINT('Ctrl Pts',(-59.4486398190941,-3.54066556118018,
134.217990715625));
#87978=CARTESIAN_POINT('Ctrl Pts',(-59.4564002616083,-3.44548068474116,
134.316717819696));
#87979=CARTESIAN_POINT('Ctrl Pts',(-59.4641607041225,-3.34623888415661,
134.411382442465));
#87980=CARTESIAN_POINT('Ctrl Pts',(-59.4719211466367,-3.24333415018636,
134.501652417348));
#87981=CARTESIAN_POINT('Ctrl Pts',(-59.4796940469022,-3.1402642244017,134.592067301608));
#87982=CARTESIAN_POINT('Ctrl Pts',(-59.4874669471676,-3.03351991960272,
134.678073195052));
#87983=CARTESIAN_POINT('Ctrl Pts',(-59.4952398474331,-2.92352686874046,
134.759379417806));
#87984=CARTESIAN_POINT('Ctrl Pts',(-59.5027301831948,-2.81753234233684,
134.837729954562));
#87985=CARTESIAN_POINT('Ctrl Pts',(-59.5102205189566,-2.7085214241549,134.911716405154));
#87986=CARTESIAN_POINT('Ctrl Pts',(-59.5177108547184,-2.59689667057551,
134.981119019108));
#87987=CARTESIAN_POINT('Ctrl Pts',(-59.5254851888375,-2.48103963053278,
135.053153054268));
#87988=CARTESIAN_POINT('Ctrl Pts',(-59.5332595229566,-2.36199963500479,
135.120476981048));
#87989=CARTESIAN_POINT('Ctrl Pts',(-59.5410338570756,-2.2401967511368,135.182796591598));
#87990=CARTESIAN_POINT('Ctrl Pts',(-59.5487986100227,-2.11854397843751,
135.245039398798));
#87991=CARTESIAN_POINT('Ctrl Pts',(-59.5565633629697,-1.99413543707173,
135.302289984631));
#87992=CARTESIAN_POINT('Ctrl Pts',(-59.5643281159168,-1.86741970734935,
135.354297617031));
#87993=CARTESIAN_POINT('Ctrl Pts',(-59.5720851568018,-1.74082983347594,
135.406253594718));
#87994=CARTESIAN_POINT('Ctrl Pts',(-59.5798421976869,-1.61193769084453,
135.452976834399));
#87995=CARTESIAN_POINT('Ctrl Pts',(-59.5875992385719,-1.48121565595883,
135.494262881264));
#87996=CARTESIAN_POINT('Ctrl Pts',(-59.595350429812,-1.35059219957668,135.535517794));
#87997=CARTESIAN_POINT('Ctrl Pts',(-59.6031016210521,-1.21814196892384,
135.571343557909));
#87998=CARTESIAN_POINT('Ctrl Pts',(-59.6108528122922,-1.08435614550405,
135.601584274246));
#87999=CARTESIAN_POINT('Ctrl Pts',(-59.6186007090693,-0.950627184627884,
135.631812137472));
#88000=CARTESIAN_POINT('Ctrl Pts',(-59.6263486058464,-0.815564140568402,
135.656459588403));
#88001=CARTESIAN_POINT('Ctrl Pts',(-59.6340965026235,-0.679671929550312,
135.675420987822));
#88002=CARTESIAN_POINT('Ctrl Pts',(-59.6418427787076,-0.543808144253269,
135.694378420925));
#88003=CARTESIAN_POINT('Ctrl Pts',(-59.6495890547916,-0.407115923955601,
135.707652114301));
#88004=CARTESIAN_POINT('Ctrl Pts',(-59.6573353308757,-0.270108525782485,
135.715187884616));
#88005=CARTESIAN_POINT('Ctrl Pts',(-59.665081664141,-0.13310011625188,135.722723710558));
#88006=CARTESIAN_POINT('Ctrl Pts',(-59.6728279974064,0.00422308542152605,
135.72452150745));
#88007=CARTESIAN_POINT('Ctrl Pts',(-59.6805743306718,0.141344973232886,
135.720579150244));
#88008=CARTESIAN_POINT('Ctrl Pts',(-59.6883223986747,0.278497568540284,
135.716635910173));
#88009=CARTESIAN_POINT('Ctrl Pts',(-59.6960704666777,0.415448369547073,
135.706949969306));
#88010=CARTESIAN_POINT('Ctrl Pts',(-59.7038185346807,0.551683946481696,
135.691571262269));
#88011=CARTESIAN_POINT('Ctrl Pts',(-59.7115748374226,0.688064316208524,
135.676176210558));
#88012=CARTESIAN_POINT('Ctrl Pts',(-59.7193311401644,0.823727554267093,
135.655076350398));
#88013=CARTESIAN_POINT('Ctrl Pts',(-59.7270874429062,0.958167459128667,
135.628373281601));
#88014=CARTESIAN_POINT('Ctrl Pts',(-59.7348478854204,1.09267911861574,135.601655960571));
#88015=CARTESIAN_POINT('Ctrl Pts',(-59.7426083279345,1.22596576412376,135.569329563985));
#88016=CARTESIAN_POINT('Ctrl Pts',(-59.7503687704487,1.35753497286985,135.531546023274));
#88017=CARTESIAN_POINT('Ctrl Pts',(-59.7581416707141,1.4893153881898,135.493701829069));
#88018=CARTESIAN_POINT('Ctrl Pts',(-59.7659145709796,1.61937248627495,135.450383108503));
#88019=CARTESIAN_POINT('Ctrl Pts',(-59.773687471245,1.74723164491043,135.401790839062));
#88020=CARTESIAN_POINT('Ctrl Pts',(-59.7811778070071,1.87044280107329,135.354965021011));
#88021=CARTESIAN_POINT('Ctrl Pts',(-59.7886681427692,1.99161276138343,135.303242531957));
#88022=CARTESIAN_POINT('Ctrl Pts',(-59.7961584785313,2.11033905198889,135.246843273486));
#88023=CARTESIAN_POINT('Ctrl Pts',(-59.8039328126504,2.23356688598718,135.188305619989));
#88024=CARTESIAN_POINT('Ctrl Pts',(-59.8117071467694,2.35455243759627,135.124544127266));
#88025=CARTESIAN_POINT('Ctrl Pts',(-59.8194814808885,2.47282112486666,135.055753183175));
#88026=CARTESIAN_POINT('Ctrl Pts',(-59.8272462338356,2.59094405654997,134.987047017774));
#88027=CARTESIAN_POINT('Ctrl Pts',(-59.8350109867828,2.70635645128811,134.913323928556));
#88028=CARTESIAN_POINT('Ctrl Pts',(-59.8427757397299,2.81860489247843,134.834825792034));
#88029=CARTESIAN_POINT('Ctrl Pts',(-59.8505327806149,2.93074184693438,134.756405620968));
#88030=CARTESIAN_POINT('Ctrl Pts',(-59.8582898214998,3.03972078320653,134.673220063283));
#88031=CARTESIAN_POINT('Ctrl Pts',(-59.8660468623848,3.14511435663451,134.585556029892));
#88032=CARTESIAN_POINT('Ctrl Pts',(-59.8737980536249,3.25042845194907,134.49795810463));
#88033=CARTESIAN_POINT('Ctrl Pts',(-59.881549244865,3.35216226670846,134.405888674881));
#88034=CARTESIAN_POINT('Ctrl Pts',(-59.8893004361052,3.44991914328328,134.309676718477));
#88035=CARTESIAN_POINT('Ctrl Pts',(-59.8970483328823,3.54763447057779,134.213505654721));
#88036=CARTESIAN_POINT('Ctrl Pts',(-59.9047962296594,3.6413759435113,134.113195839846));
#88037=CARTESIAN_POINT('Ctrl Pts',(-59.9125441264365,3.73078176526413,134.009114973593));
#88038=CARTESIAN_POINT('Ctrl Pts',(-59.9202904025206,3.8201688852463,133.905055878813));
#88039=CARTESIAN_POINT('Ctrl Pts',(-59.9280366786046,3.90522190337754,133.79722759805));
#88040=CARTESIAN_POINT('Ctrl Pts',(-59.9357829546887,3.98561780567198,133.686032661642));
#88041=CARTESIAN_POINT('Ctrl Pts',(-59.9435292879541,4.06601430143071,133.574836904419));
#88042=CARTESIAN_POINT('Ctrl Pts',(-59.9512756212194,4.14175338368226,133.46027475879));
#88043=CARTESIAN_POINT('Ctrl Pts',(-59.9590219544847,4.21255429666111,133.342779290713));
#88044=CARTESIAN_POINT('Ctrl Pts',(-59.9667700224877,4.28337106501353,133.225257510341));
#88045=CARTESIAN_POINT('Ctrl Pts',(-59.9745180904906,4.34924726179517,133.104801435175));
#88046=CARTESIAN_POINT('Ctrl Pts',(-59.9822661584936,4.40994737708912,132.981870019108));
#88047=CARTESIAN_POINT('Ctrl Pts',(-59.9900224612354,4.47071200518795,132.85880795007));
#88048=CARTESIAN_POINT('Ctrl Pts',(-59.9977787639773,4.52628938918531,132.733265635899));
#88049=CARTESIAN_POINT('Ctrl Pts',(-60.0055350667191,4.57649139359088,132.605723875459));
#88050=CARTESIAN_POINT('Ctrl Pts',(-60.0132955092333,4.62672019231781,132.478114042142));
#88051=CARTESIAN_POINT('Ctrl Pts',(-60.0210559517474,4.67156776694264,132.348503005431));
#88052=CARTESIAN_POINT('Ctrl Pts',(-60.0288163942616,4.7108957751407,132.217387177211));
#88053=CARTESIAN_POINT('Ctrl Pts',(-60.036589294527,4.75028691614889,132.086060870223));
#88054=CARTESIAN_POINT('Ctrl Pts',(-60.0443621947924,4.78414068802326,131.953225323611));
#88055=CARTESIAN_POINT('Ctrl Pts',(-60.0521350950579,4.81236963391396,131.819388483727));
#88056=CARTESIAN_POINT('Ctrl Pts',(-60.05962543082,4.83957238651753,131.690416950085));
#88057=CARTESIAN_POINT('Ctrl Pts',(-60.0671157665822,4.86155211490772,131.560515962038));
#88058=CARTESIAN_POINT('Ctrl Pts',(-60.0746061023443,4.87827628156955,131.430142994416));
#88059=CARTESIAN_POINT('Ctrl Pts',(-60.0823804364634,4.89563455009333,131.294826896102));
#88060=CARTESIAN_POINT('Ctrl Pts',(-60.0901547705824,4.90738584632752,131.158573680767));
#88061=CARTESIAN_POINT('Ctrl Pts',(-60.0979291047015,4.91343719114534,131.021887699029));
#88062=CARTESIAN_POINT('Ctrl Pts',(-60.1056938576486,4.9194810782215,130.885370170548));
#88063=CARTESIAN_POINT('Ctrl Pts',(-60.1134586105958,4.91983897377632,130.748421323696));
#88064=CARTESIAN_POINT('Ctrl Pts',(-60.1212233635429,4.91446929262161,130.611553370868));
#88065=CARTESIAN_POINT('Ctrl Pts',(-60.1289804044279,4.90910494470992,130.47482135722));
#88066=CARTESIAN_POINT('Ctrl Pts',(-60.1367374453128,4.89802435610577,130.338170465841));
#88067=CARTESIAN_POINT('Ctrl Pts',(-60.1444944861978,4.88123792285803,130.202115316254));
#88068=CARTESIAN_POINT('Ctrl Pts',(-60.152245677438,4.86446414839018,130.066162766913));
#88069=CARTESIAN_POINT('Ctrl Pts',(-60.1599968686781,4.84199314146508,129.930805451605));
#88070=CARTESIAN_POINT('Ctrl Pts',(-60.1677480599182,4.81388727731124,129.796554910179));
#88071=CARTESIAN_POINT('Ctrl Pts',(-60.1754959566953,4.78579335889941,129.662361428816));
#88072=CARTESIAN_POINT('Ctrl Pts',(-60.1832438534725,4.75206942660643,129.529274167597));
#88073=CARTESIAN_POINT('Ctrl Pts',(-60.1909917502496,4.71282927662019,129.397796267125));
#88074=CARTESIAN_POINT('Ctrl Pts',(-60.1987380263337,4.67359733482741,129.266345868996));
#88075=CARTESIAN_POINT('Ctrl Pts',(-60.2064843024177,4.62885158220049,129.13650453641));
#88076=CARTESIAN_POINT('Ctrl Pts',(-60.2142305785018,4.57875608196576,129.008761607664));
#88077=CARTESIAN_POINT('Ctrl Pts',(-60.2219769117672,4.52866021193743,128.881017735948));
#88078=CARTESIAN_POINT('Ctrl Pts',(-60.2297232450325,4.47321465823772,128.755372662959));
#88079=CARTESIAN_POINT('Ctrl Pts',(-60.2374695782978,4.41263201617326,128.632296679202));
#88080=CARTESIAN_POINT('Ctrl Pts',(-60.2452176463008,4.35203580704625,128.509193133431));
#88081=CARTESIAN_POINT('Ctrl Pts',(-60.2529657143038,4.2863003929915,128.388660172438));
#88082=CARTESIAN_POINT('Ctrl Pts',(-60.2607137823068,4.21568460605508,128.271144013173));
#88083=CARTESIAN_POINT('Ctrl Pts',(-60.2684700850486,4.14499376781987,128.153502956337));
#88084=CARTESIAN_POINT('Ctrl Pts',(-60.2762263877906,4.06941239696825,128.038885441795));
#88085=CARTESIAN_POINT('Ctrl Pts',(-60.2839826905324,3.98924331137297,127.927709636796));
#88086=CARTESIAN_POINT('Ctrl Pts',(-60.2917431330466,3.90903143712277,127.816474493922));
#88087=CARTESIAN_POINT('Ctrl Pts',(-60.2995035755607,3.82422721070979,127.708685027972));
#88088=CARTESIAN_POINT('Ctrl Pts',(-60.3072640180749,3.73517350010559,127.604725953013));
#88089=CARTESIAN_POINT('Ctrl Pts',(-60.3150369183403,3.64597683257943,127.500599993718));
#88090=CARTESIAN_POINT('Ctrl Pts',(-60.3228098186058,3.55251731573888,127.400316999019));
#88091=CARTESIAN_POINT('Ctrl Pts',(-60.3305827188712,3.45517502667162,127.304225106252));
#88092=CARTESIAN_POINT('Ctrl Pts',(-60.3380730546332,3.36137137500331,127.211626395828));
#88093=CARTESIAN_POINT('Ctrl Pts',(-60.3455633903951,3.26396257485432,127.12291957079));
#88094=CARTESIAN_POINT('Ctrl Pts',(-60.3530537261571,3.16331592543335,127.03837928219));
#88095=CARTESIAN_POINT('Ctrl Pts',(-60.3608280602762,3.05885322770767,126.950633622851));
#88096=CARTESIAN_POINT('Ctrl Pts',(-60.3686023943952,2.95057140141032,126.867098733457));
#88097=CARTESIAN_POINT('Ctrl Pts',(-60.3763767285143,2.8388445135125,126.788125453809));
#88098=CARTESIAN_POINT('Ctrl Pts',(-60.3841414814614,2.7272553190187,126.70924950167));
#88099=CARTESIAN_POINT('Ctrl Pts',(-60.3919062344085,2.6122298268594,126.634924197119));
#88100=CARTESIAN_POINT('Ctrl Pts',(-60.3996709873556,2.49417649801723,126.565461390262));
#88101=CARTESIAN_POINT('Ctrl Pts',(-60.4074280282406,2.37624042140569,126.496067574845));
#88102=CARTESIAN_POINT('Ctrl Pts',(-60.4151850691257,2.25528282753555,126.431526843182));
#88103=CARTESIAN_POINT('Ctrl Pts',(-60.4229421100107,2.13174229970388,126.372108613206));
#88104=CARTESIAN_POINT('Ctrl Pts',(-60.4306933012508,2.00829493474525,126.312735190979));
#88105=CARTESIAN_POINT('Ctrl Pts',(-60.4384444924909,1.88226886373024,126.258476750307));
#88106=CARTESIAN_POINT('Ctrl Pts',(-60.446195683731,1.75412817495747,126.209557312927));
#88107=CARTESIAN_POINT('Ctrl Pts',(-60.4539435805081,1.6260419493957,126.160658667613));
#88108=CARTESIAN_POINT('Ctrl Pts',(-60.4616914772852,1.49584325814796,126.117094651436));
#88109=CARTESIAN_POINT('Ctrl Pts',(-60.4694393740623,1.36401691727227,126.079041484227));
#88110=CARTESIAN_POINT('Ctrl Pts',(-60.4771856501464,1.23221815162525,126.040996276921));
#88111=CARTESIAN_POINT('Ctrl Pts',(-60.4849319262304,1.09879278895285,126.008459734058));
#88112=CARTESIAN_POINT('Ctrl Pts',(-60.4926782023145,0.964241203603525,
125.981558323902));
#88113=CARTESIAN_POINT('Ctrl Pts',(-60.5004245355799,0.829688625024966,
125.954656715165));
#88114=CARTESIAN_POINT('Ctrl Pts',(-60.5081708688453,0.694010190558273,
125.93339039879));
#88115=CARTESIAN_POINT('Ctrl Pts',(-60.5159172021106,0.557716481881299,
125.91783471583));
#88116=CARTESIAN_POINT('Ctrl Pts',(-60.5236652701136,0.421392251173261,
125.902275549282));
#88117=CARTESIAN_POINT('Ctrl Pts',(-60.5314133381165,0.284452860444995,
125.892429605251));
#88118=CARTESIAN_POINT('Ctrl Pts',(-60.5391614061195,0.147413629699876,
125.88832031217));
#88119=CARTESIAN_POINT('Ctrl Pts',(-60.5469177088614,0.0102287520295327,
125.884206651683));
#88120=CARTESIAN_POINT('Ctrl Pts',(-60.5546740116033,-0.127055786213454,
125.885841833258));
#88121=CARTESIAN_POINT('Ctrl Pts',(-60.5624303143452,-0.26392448862483,
125.893197117253));
#88122=CARTESIAN_POINT('Ctrl Pts',(-60.5701907568593,-0.400866241983907,
125.900556326985));
#88123=CARTESIAN_POINT('Ctrl Pts',(-60.5779511993734,-0.537391328277675,
125.913641685197));
#88124=CARTESIAN_POINT('Ctrl Pts',(-60.5857116418876,-0.672990748154215,
125.932372674703));
#88125=CARTESIAN_POINT('Ctrl Pts',(-60.593484542153,-0.808807844257492,
125.951133732857));
#88126=CARTESIAN_POINT('Ctrl Pts',(-60.6012574424185,-0.943695919587552,
125.975558463103));
#88127=CARTESIAN_POINT('Ctrl Pts',(-60.609030342684,-1.07715663539498,126.005515272556));
#88128=CARTESIAN_POINT('Ctrl Pts',(-60.616520678446,-1.20576571801572,126.034383076529));
#88129=CARTESIAN_POINT('Ctrl Pts',(-60.624011014208,-1.33304911805222,126.068387653138));
#88130=CARTESIAN_POINT('Ctrl Pts',(-60.63150134997,-1.45857722960131,126.107368438757));
#88131=CARTESIAN_POINT('Ctrl Pts',(-60.6392756840891,-1.58886477765286,
126.147827192712));
#88132=CARTESIAN_POINT('Ctrl Pts',(-60.6470500182082,-1.71767401797561,
126.193775111706));
#88133=CARTESIAN_POINT('Ctrl Pts',(-60.6548243523273,-1.84450758677274,
126.245087120084));
#88134=CARTESIAN_POINT('Ctrl Pts',(-60.6625891052744,-1.97118484453177,
126.296335890999));
#88135=CARTESIAN_POINT('Ctrl Pts',(-60.6703538582214,-2.09589091641836,
126.352935452637));
#88136=CARTESIAN_POINT('Ctrl Pts',(-60.6781186111685,-2.21814265096764,
126.414710717807));
#88137=CARTESIAN_POINT('Ctrl Pts',(-60.6858756520535,-2.34027296337055,
126.476424626912));
#88138=CARTESIAN_POINT('Ctrl Pts',(-60.6936326929386,-2.45995344284691,
126.543303834373));
#88139=CARTESIAN_POINT('Ctrl Pts',(-60.7013897338236,-2.57672035547545,
126.615124974614));
#88140=CARTESIAN_POINT('Ctrl Pts',(-60.7091409250637,-2.69339921326718,
126.686891953975));
#88141=CARTESIAN_POINT('Ctrl Pts',(-60.7168921163037,-2.80716854582542,
126.763593244244));
#88142=CARTESIAN_POINT('Ctrl Pts',(-60.7246433075438,-2.91758902625588,
126.844959484014));
#88143=CARTESIAN_POINT('Ctrl Pts',(-60.7323912043209,-3.02796257503643,
126.926291140962));
#88144=CARTESIAN_POINT('Ctrl Pts',(-60.740139101098,-3.13498978854208,127.012283572473));
#88145=CARTESIAN_POINT('Ctrl Pts',(-60.7478869978751,-3.23826035311738,
127.102624140191));
#88146=CARTESIAN_POINT('Ctrl Pts',(-60.7556332739592,-3.34150931571683,
127.19294581061));
#88147=CARTESIAN_POINT('Ctrl Pts',(-60.7633795500433,-3.44100289833029,
127.287613550862));
#88148=CARTESIAN_POINT('Ctrl Pts',(-60.7711258261274,-3.53636423506873,
127.386274741022));
#88149=CARTESIAN_POINT('Ctrl Pts',(-60.7788721593927,-3.6317262757429,127.484936659477));
#88150=CARTESIAN_POINT('Ctrl Pts',(-60.7866184926581,-3.72295573796189,
127.587591805548));
#88151=CARTESIAN_POINT('Ctrl Pts',(-60.7943648259235,-3.80971325329529,
127.693851336087));
#88152=CARTESIAN_POINT('Ctrl Pts',(-60.8021128939264,-3.8964901973727,127.800134662712));
#88153=CARTESIAN_POINT('Ctrl Pts',(-60.8098609619293,-3.97879295455648,
127.910023677207));
#88154=CARTESIAN_POINT('Ctrl Pts',(-60.8176090299323,-4.05632327079427,
128.0230974899));
#88155=CARTESIAN_POINT('Ctrl Pts',(-60.8253653326742,-4.13393598717477,
128.136291478787));
#88156=CARTESIAN_POINT('Ctrl Pts',(-60.833121635416,-4.2067659088866,128.252676704494));
#88157=CARTESIAN_POINT('Ctrl Pts',(-60.8408779381578,-4.27455857700611,
128.371803930818));
#88158=CARTESIAN_POINT('Ctrl Pts',(-60.848638380672,-4.34238742811379,128.490994738929));
#88159=CARTESIAN_POINT('Ctrl Pts',(-60.8563988231862,-4.40517348960581,
128.612930116361));
#88160=CARTESIAN_POINT('Ctrl Pts',(-60.8641592657004,-4.46270937628829,
128.737138306036));
#88161=CARTESIAN_POINT('Ctrl Pts',(-60.8719321659658,-4.52033762468387,
128.861545885723));
#88162=CARTESIAN_POINT('Ctrl Pts',(-60.8797050662311,-4.57269870692403,
128.988233207032));
#88163=CARTESIAN_POINT('Ctrl Pts',(-60.8874779664966,-4.61963397156314,
129.11670987429));
#88164=CARTESIAN_POINT('Ctrl Pts',(-60.8949683022587,-4.66486302111027,
129.240516091081));
#88165=CARTESIAN_POINT('Ctrl Pts',(-60.9024586380208,-4.7050537945398,129.365983524651));
#88166=CARTESIAN_POINT('Ctrl Pts',(-60.9099489737829,-4.7401091660917,129.492663946825));
#88167=CARTESIAN_POINT('Ctrl Pts',(-60.9117146843342,-4.74837283295475,
129.522526554482));
#88168=CARTESIAN_POINT('Ctrl Pts',(-60.9134803948856,-4.75635509691311,
129.552470153443));
#88169=CARTESIAN_POINT('Ctrl Pts',(-60.9152461054369,-4.76405452823402,
129.582490119308));
#88170=CARTESIAN_POINT('Ctrl Pts',(-59.165034112149,-4.76405452823398,129.582490119308));
#88171=CARTESIAN_POINT('Ctrl Pts',(-59.1727742599865,-4.79804438416839,
129.715016051728));
#88172=CARTESIAN_POINT('Ctrl Pts',(-59.1805144078242,-4.82647343551534,
129.848857094792));
#88173=CARTESIAN_POINT('Ctrl Pts',(-59.1882545556616,-4.84926594987579,
129.983505691361));
#88174=CARTESIAN_POINT('Ctrl Pts',(-59.1960688903796,-4.87227692331144,
130.119444852341));
#88175=CARTESIAN_POINT('Ctrl Pts',(-59.2038832250975,-4.88954270213659,
130.256206719216));
#88176=CARTESIAN_POINT('Ctrl Pts',(-59.2116975598155,-4.90103911891263,
130.393266203364));
#88177=CARTESIAN_POINT('Ctrl Pts',(-59.2195118945334,-4.91253553568865,
130.530325687512));
#88178=CARTESIAN_POINT('Ctrl Pts',(-59.2273262292515,-4.91826263506064,
130.667682381086));
#88179=CARTESIAN_POINT('Ctrl Pts',(-59.2351405639694,-4.91824997905427,
130.804814525752));
#88180=CARTESIAN_POINT('',(-58.8898594360411,-4.91824840746026,130.808318522891));
#88181=CARTESIAN_POINT('Ctrl Pts',(-58.8199570926742,-4.76405452823407,
129.582490119308));
#88182=CARTESIAN_POINT('Ctrl Pts',(-58.8276862897791,-4.79808194527658,
129.715162501919));
#88183=CARTESIAN_POINT('Ctrl Pts',(-58.8354154868839,-4.82657252583923,
129.849294383098));
#88184=CARTESIAN_POINT('Ctrl Pts',(-58.8431446839888,-4.84941444227015,
129.984383404711));
#88185=CARTESIAN_POINT('Ctrl Pts',(-58.8509304759891,-4.87242361227952,
130.120461578102));
#88186=CARTESIAN_POINT('Ctrl Pts',(-58.8587162679895,-4.8897009621754,130.257510574267));
#88187=CARTESIAN_POINT('Ctrl Pts',(-58.8665020599899,-4.90118490255336,
130.395007941402));
#88188=CARTESIAN_POINT('Ctrl Pts',(-58.8742878519903,-4.91266884293131,
130.532505308536));
#88189=CARTESIAN_POINT('Ctrl Pts',(-58.8820736439906,-4.91835935506972,
130.670450640487));
#88190=CARTESIAN_POINT('Ctrl Pts',(-58.889859435991,-4.91824840746098,130.808318522003));
#88191=CARTESIAN_POINT('Ctrl Pts',(-58.8898594360411,-4.91824840746026,
130.808318522891));
#88192=CARTESIAN_POINT('Ctrl Pts',(-58.8989570390533,-4.91811876650329,
130.969415461274));
#88193=CARTESIAN_POINT('Ctrl Pts',(-58.9080546420654,-4.91007019755224,
131.130177591142));
#88194=CARTESIAN_POINT('Ctrl Pts',(-58.9171522450775,-4.89422441324256,
131.289902021898));
#88195=CARTESIAN_POINT('Ctrl Pts',(-58.9263092006774,-4.8782752513397,131.450668491779));
#88196=CARTESIAN_POINT('Ctrl Pts',(-58.9354661562772,-4.85442691080236,
131.610383603236));
#88197=CARTESIAN_POINT('Ctrl Pts',(-58.9446231118771,-4.82285244834712,
131.768350930781));
#88198=CARTESIAN_POINT('Ctrl Pts',(-58.9538470483144,-4.79104702660448,
131.927473749775));
#88199=CARTESIAN_POINT('Ctrl Pts',(-58.9630709847519,-4.75140211119584,
132.084823050191));
#88200=CARTESIAN_POINT('Ctrl Pts',(-58.9722949211893,-4.70414275297314,
132.239708666699));
#88201=CARTESIAN_POINT('Ctrl Pts',(-58.9749981485436,-4.69029261526219,
132.285100462076));
#88202=CARTESIAN_POINT('Ctrl Pts',(-58.9777013758979,-4.67578879778627,
132.33028080118));
#88203=CARTESIAN_POINT('Ctrl Pts',(-58.9804046032522,-4.66063772933524,
132.375232674227));
#88204=CARTESIAN_POINT('Ctrl Pts',(-58.9881789373714,-4.61706408459059,
132.504511804147));
#88205=CARTESIAN_POINT('Ctrl Pts',(-58.9959532714905,-4.56803833085984,
132.632181327229));
#88206=CARTESIAN_POINT('Ctrl Pts',(-59.0037276056097,-4.51369744313826,
132.757747024375));
#88207=CARTESIAN_POINT('Ctrl Pts',(-59.0114923585569,-4.45942352570428,
132.883157973022));
#88208=CARTESIAN_POINT('Ctrl Pts',(-59.0192571115041,-4.39984766146744,
133.006469899225));
#88209=CARTESIAN_POINT('Ctrl Pts',(-59.0270218644513,-4.33515648150296,
133.127203992265));
#88210=CARTESIAN_POINT('Ctrl Pts',(-59.0347789053364,-4.27052955373041,
133.247818170502));
#88211=CARTESIAN_POINT('Ctrl Pts',(-59.0425359462215,-4.20079760431519,
133.365859268386));
#88212=CARTESIAN_POINT('Ctrl Pts',(-59.0502929871065,-4.12619506284523,
133.480869045696));
#88213=CARTESIAN_POINT('Ctrl Pts',(-59.0580441783467,-4.05164877973211,
133.595792093239));
#88214=CARTESIAN_POINT('Ctrl Pts',(-59.0657953695868,-3.97223942725329,
133.707688043563));
#88215=CARTESIAN_POINT('Ctrl Pts',(-59.0735465608271,-3.8882468318813,133.816124160221));
#88216=CARTESIAN_POINT('Ctrl Pts',(-59.0812944576042,-3.8042899356028,133.924514188636));
#88217=CARTESIAN_POINT('Ctrl Pts',(-59.0890423543815,-3.71575390976769,
134.029446999701));
#88218=CARTESIAN_POINT('Ctrl Pts',(-59.0967902511586,-3.62296114909805,
134.130519900376));
#88219=CARTESIAN_POINT('Ctrl Pts',(-59.1045365272428,-3.53018779867356,
134.23157165878));
#88220=CARTESIAN_POINT('Ctrl Pts',(-59.112282803327,-3.43315974874112,134.328764824962));
#88221=CARTESIAN_POINT('Ctrl Pts',(-59.1200290794112,-3.33223856142256,
134.421731103467));
#88222=CARTESIAN_POINT('Ctrl Pts',(-59.1277754126766,-3.23131662912672,
134.514698068228));
#88223=CARTESIAN_POINT('Ctrl Pts',(-59.135521745942,-3.12650178965439,134.603437818162));
#88224=CARTESIAN_POINT('Ctrl Pts',(-59.1432680792074,-3.01819091808133,
134.687620413731));
#88225=CARTESIAN_POINT('Ctrl Pts',(-59.1510161472105,-2.90985579103955,
134.771821861409));
#88226=CARTESIAN_POINT('Ctrl Pts',(-59.1587642152136,-2.79802338262443,
134.851463884081));
#88227=CARTESIAN_POINT('Ctrl Pts',(-59.1665122832166,-2.68312161857887,
134.926258413778));
#88228=CARTESIAN_POINT('Ctrl Pts',(-59.1742685859586,-2.56809773557113,
135.00113243599));
#88229=CARTESIAN_POINT('Ctrl Pts',(-59.1820248887005,-2.44999830862501,
135.071148459976));
#88230=CARTESIAN_POINT('Ctrl Pts',(-59.1897811914424,-2.32927855088701,
135.13606288052));
#88231=CARTESIAN_POINT('Ctrl Pts',(-59.1975416339566,-2.2084943613795,135.201011947844));
#88232=CARTESIAN_POINT('Ctrl Pts',(-59.205302076471,-2.08508740596666,135.260853815656));
#88233=CARTESIAN_POINT('Ctrl Pts',(-59.2130625189852,-1.95953428254303,
135.315392479351));
#88234=CARTESIAN_POINT('Ctrl Pts',(-59.2208354192507,-1.8337796100996,135.370018693351));
#88235=CARTESIAN_POINT('Ctrl Pts',(-59.2286083195162,-1.70587225000887,
135.419324550496));
#88236=CARTESIAN_POINT('Ctrl Pts',(-59.2363812197817,-1.5763062639185,135.463163213173));
#88237=CARTESIAN_POINT('Ctrl Pts',(-59.2438715555428,-1.45145032779531,
135.505408230033));
#88238=CARTESIAN_POINT('Ctrl Pts',(-59.2513618913041,-1.325054558018,135.542576557053));
#88239=CARTESIAN_POINT('Ctrl Pts',(-59.2588522270652,-1.19756938443239,
135.574581852684));
#88240=CARTESIAN_POINT('Ctrl Pts',(-59.2666265611843,-1.06525057172689,
135.60780063883));
#88241=CARTESIAN_POINT('Ctrl Pts',(-59.2744008953034,-0.931338968758862,
135.635562379462));
#88242=CARTESIAN_POINT('Ctrl Pts',(-59.2821752294224,-0.796324414382764,
135.657715178028));
#88243=CARTESIAN_POINT('Ctrl Pts',(-59.2899399823695,-0.661476253378521,
135.67984067525));
#88244=CARTESIAN_POINT('Ctrl Pts',(-59.2977047353166,-0.525528227649034,
135.696370921565));
#88245=CARTESIAN_POINT('Ctrl Pts',(-59.3054694882636,-0.388984052867978,
135.707204126094));
#88246=CARTESIAN_POINT('Ctrl Pts',(-59.3132265291486,-0.252575495686064,
135.718026570932));
#88247=CARTESIAN_POINT('Ctrl Pts',(-59.3209835700337,-0.115572354984052,
135.723163203698));
#88248=CARTESIAN_POINT('Ctrl Pts',(-59.3287406109187,0.0215131238449157,
135.722563566612));
#88249=CARTESIAN_POINT('Ctrl Pts',(-59.3364918021588,0.158495225447929,
135.721964381717));
#88250=CARTESIAN_POINT('Ctrl Pts',(-59.3442429933989,0.295559152208349,
135.715637538848));
#88251=CARTESIAN_POINT('Ctrl Pts',(-59.351994184639,0.432189577653266,135.703584559321));
#88252=CARTESIAN_POINT('Ctrl Pts',(-59.3597420814161,0.568761931522634,
135.691536702632));
#88253=CARTESIAN_POINT('Ctrl Pts',(-59.3674899781933,0.704900761897533,
135.673767584134));
#88254=CARTESIAN_POINT('Ctrl Pts',(-59.3752378749703,0.840093009499151,
135.650330778214));
#88255=CARTESIAN_POINT('Ctrl Pts',(-59.3829841510544,0.975256977796978,
135.626898874769));
#88256=CARTESIAN_POINT('Ctrl Pts',(-59.3907304271384,1.10947437218832,135.597801708781));
#88257=CARTESIAN_POINT('Ctrl Pts',(-59.3984767032225,1.2422399021177,135.563144400014));
#88258=CARTESIAN_POINT('Ctrl Pts',(-59.4062230364878,1.37500641209207,135.528486835414));
#88259=CARTESIAN_POINT('Ctrl Pts',(-59.4139693697532,1.50632065793001,135.488269144885));
#88260=CARTESIAN_POINT('Ctrl Pts',(-59.4217157030186,1.63569053148172,135.442646890288));
#88261=CARTESIAN_POINT('Ctrl Pts',(-59.4294637710216,1.76508937651963,135.397014418903));
#88262=CARTESIAN_POINT('Ctrl Pts',(-59.4372118390245,1.89254261417908,135.345975105066));
#88263=CARTESIAN_POINT('Ctrl Pts',(-59.4449599070274,2.01757658040093,135.289733267048));
#88264=CARTESIAN_POINT('Ctrl Pts',(-59.4527162097693,2.14274343421001,135.233431654535));
#88265=CARTESIAN_POINT('Ctrl Pts',(-59.4604725125112,2.26548552314852,135.171916633098));
#88266=CARTESIAN_POINT('Ctrl Pts',(-59.468228815253,2.38535184142447,135.10543951188));
#88267=CARTESIAN_POINT('Ctrl Pts',(-59.4759892577672,2.50528213596359,135.038926909821));
#88268=CARTESIAN_POINT('Ctrl Pts',(-59.4837497002814,2.62233326794553,134.967447134438));
#88269=CARTESIAN_POINT('Ctrl Pts',(-59.4915101427955,2.73608272034308,134.891295215763));
#88270=CARTESIAN_POINT('Ctrl Pts',(-59.499283043061,2.85001477345983,134.815021051267));
#88271=CARTESIAN_POINT('Ctrl Pts',(-59.5070559433264,2.96063423993009,134.73405998685));
#88272=CARTESIAN_POINT('Ctrl Pts',(-59.5148288435918,3.06755052872188,134.64874832125));
#88273=CARTESIAN_POINT('Ctrl Pts',(-59.5223191793539,3.17058014111122,134.566537949581));
#88274=CARTESIAN_POINT('Ctrl Pts',(-59.529809515116,3.270170908261,134.480287997385));
#88275=CARTESIAN_POINT('Ctrl Pts',(-59.5372998508781,3.36600672024583,134.39033075433));
#88276=CARTESIAN_POINT('Ctrl Pts',(-59.5450741849972,3.46547617616961,134.296962755063));
#88277=CARTESIAN_POINT('Ctrl Pts',(-59.5528485191162,3.56121540719336,134.199305029842));
#88278=CARTESIAN_POINT('Ctrl Pts',(-59.5606228532352,3.65283184858071,134.097687590172));
#88279=CARTESIAN_POINT('Ctrl Pts',(-59.5683876061823,3.74433538089192,133.996195384914));
#88280=CARTESIAN_POINT('Ctrl Pts',(-59.5761523591294,3.83172597389976,133.890753462527));
#88281=CARTESIAN_POINT('Ctrl Pts',(-59.5839171120765,3.91464571742834,133.781730592816));
#88282=CARTESIAN_POINT('Ctrl Pts',(-59.5916741529615,3.9974831038988,133.672816006156));
#88283=CARTESIAN_POINT('Ctrl Pts',(-59.5994311938464,4.07585824255894,133.560327859232));
#88284=CARTESIAN_POINT('Ctrl Pts',(-59.6071882347314,4.14945180070211,133.444669844939));
#88285=CARTESIAN_POINT('Ctrl Pts',(-59.6149394259715,4.22298986137051,133.329099049254));
#88286=CARTESIAN_POINT('Ctrl Pts',(-59.6226906172117,4.29175330966586,133.210363472707));
#88287=CARTESIAN_POINT('Ctrl Pts',(-59.6304418084518,4.35546487896835,133.088897496361));
#88288=CARTESIAN_POINT('Ctrl Pts',(-59.6381897052288,4.41914936915441,132.967483146295));
#88289=CARTESIAN_POINT('Ctrl Pts',(-59.6459376020059,4.47778606970764,132.843341050065));
#88290=CARTESIAN_POINT('Ctrl Pts',(-59.6536854987829,4.53114273320537,132.716931817239));
#88291=CARTESIAN_POINT('Ctrl Pts',(-59.661431774867,4.58448823563932,132.5905490265));
#88292=CARTESIAN_POINT('Ctrl Pts',(-59.6691780509511,4.63255574592978,132.46190040241));
#88293=CARTESIAN_POINT('Ctrl Pts',(-59.6769243270352,4.6751605824233,132.331467880025));
#88294=CARTESIAN_POINT('Ctrl Pts',(-59.6846706603005,4.71776573341598,132.201034394817));
#88295=CARTESIAN_POINT('Ctrl Pts',(-59.6924169935658,4.75490800875374,132.068817356678));
#88296=CARTESIAN_POINT('Ctrl Pts',(-59.7001633268311,4.78645229056156,131.935314875119));
#88297=CARTESIAN_POINT('Ctrl Pts',(-59.7079113948341,4.81800363649258,131.801782496605));
#88298=CARTESIAN_POINT('Ctrl Pts',(-59.7156594628371,4.843954404426,131.666964482266));
#88299=CARTESIAN_POINT('Ctrl Pts',(-59.72340753084,4.86422046611703,131.531369778105));
#88300=CARTESIAN_POINT('Ctrl Pts',(-59.7311638335819,4.88450806681962,131.39563096228));
#88301=CARTESIAN_POINT('Ctrl Pts',(-59.7389201363237,4.89909883430244,131.259114194945));
#88302=CARTESIAN_POINT('Ctrl Pts',(-59.7466764390656,4.90796042241798,131.122334758777));
#88303=CARTESIAN_POINT('Ctrl Pts',(-59.7544368815797,4.91682674022992,130.985482319305));
#88304=CARTESIAN_POINT('Ctrl Pts',(-59.7621973240938,4.91995777675734,130.848367322324));
#88305=CARTESIAN_POINT('Ctrl Pts',(-59.769957766608,4.91737336834726,130.711504714312));
#88306=CARTESIAN_POINT('Ctrl Pts',(-59.7777306668734,4.91478481121536,130.574422402291));
#88307=CARTESIAN_POINT('Ctrl Pts',(-59.7855035671388,4.90646249844249,130.437593679342));
#88308=CARTESIAN_POINT('Ctrl Pts',(-59.7932764674042,4.89247824368927,130.301528938446));
#88309=CARTESIAN_POINT('Ctrl Pts',(-59.8007668031665,4.87900235182013,130.170410493602));
#88310=CARTESIAN_POINT('Ctrl Pts',(-59.8082571389287,4.86026906659534,130.040001754705));
#88311=CARTESIAN_POINT('Ctrl Pts',(-59.8157474746909,4.83638708758873,129.910748284669));
#88312=CARTESIAN_POINT('Ctrl Pts',(-59.82352180881,4.81159961608998,129.776594130035));
#88313=CARTESIAN_POINT('Ctrl Pts',(-59.8312961429291,4.7811867989801,129.643259617594));
#88314=CARTESIAN_POINT('Ctrl Pts',(-59.8390704770482,4.74521409345568,129.511253402456));
#88315=CARTESIAN_POINT('Ctrl Pts',(-59.8468352299953,4.7092857210759,129.379409873181));
#88316=CARTESIAN_POINT('Ctrl Pts',(-59.8545999829424,4.66781119565562,129.24889175764));
#88317=CARTESIAN_POINT('Ctrl Pts',(-59.8623647358895,4.62090731448351,129.120199504889));
#88318=CARTESIAN_POINT('Ctrl Pts',(-59.8701217767746,4.57405001890742,128.991635071098));
#88319=CARTESIAN_POINT('Ctrl Pts',(-59.8778788176595,4.52177423193532,128.864893256156));
#88320=CARTESIAN_POINT('Ctrl Pts',(-59.8856358585445,4.46424698470419,128.740460929582));
#88321=CARTESIAN_POINT('Ctrl Pts',(-59.8933870497847,4.40676311921778,128.616122438394));
#88322=CARTESIAN_POINT('Ctrl Pts',(-59.9011382410247,4.34403583934589,128.49409032246));
#88323=CARTESIAN_POINT('Ctrl Pts',(-59.9088894322648,4.27628073280018,128.374832647613));
#88324=CARTESIAN_POINT('Ctrl Pts',(-59.9166373290419,4.20855442398208,128.25562566046));
#88325=CARTESIAN_POINT('Ctrl Pts',(-59.9243852258191,4.13580473146711,128.139191108256));
#88326=CARTESIAN_POINT('Ctrl Pts',(-59.9321331225962,4.05829364372423,128.025973358056));
#88327=CARTESIAN_POINT('Ctrl Pts',(-59.9398793986803,3.98079876962997,127.912779290569));
#88328=CARTESIAN_POINT('Ctrl Pts',(-59.9476256747643,3.89854470209081,127.802801009081));
#88329=CARTESIAN_POINT('Ctrl Pts',(-59.9553719508484,3.81183708177263,127.696454389167));
#88330=CARTESIAN_POINT('Ctrl Pts',(-59.9631182841138,3.7251288213985,127.590106984226));
#88331=CARTESIAN_POINT('Ctrl Pts',(-59.9708646173791,3.63396718970146,127.487391597365));
#88332=CARTESIAN_POINT('Ctrl Pts',(-59.9786109506444,3.53869822580756,127.388691147438));
#88333=CARTESIAN_POINT('Ctrl Pts',(-59.9863590186474,3.44340792708988,127.289968594229));
#88334=CARTESIAN_POINT('Ctrl Pts',(-59.9941070866505,3.34400873733179,127.195263048339));
#88335=CARTESIAN_POINT('Ctrl Pts',(-60.0018551546534,3.2408833738499,127.10492038699));
#88336=CARTESIAN_POINT('Ctrl Pts',(-60.0096114573953,3.13764840750435,127.014481708386));
#88337=CARTESIAN_POINT('Ctrl Pts',(-60.0173677601372,3.030679651013,126.928415435118));
#88338=CARTESIAN_POINT('Ctrl Pts',(-60.025124062879,2.92039314240219,126.847027303791));
#88339=CARTESIAN_POINT('Ctrl Pts',(-60.0328845053932,2.81004777056107,126.765595733168));
#88340=CARTESIAN_POINT('Ctrl Pts',(-60.0406449479074,2.69638144202449,126.688847498374));
#88341=CARTESIAN_POINT('Ctrl Pts',(-60.0484053904216,2.57983811787982,126.617044251678));
#88342=CARTESIAN_POINT('Ctrl Pts',(-60.0561782906871,2.46310770804485,126.545125740036));
#88343=CARTESIAN_POINT('Ctrl Pts',(-60.0639511909524,2.34349141489891,126.478168270491));
#88344=CARTESIAN_POINT('Ctrl Pts',(-60.0717240912179,2.22145746354942,126.416387304049));
#88345=CARTESIAN_POINT('Ctrl Pts',(-60.0792144269798,2.10385975371761,126.356852231354));
#88346=CARTESIAN_POINT('Ctrl Pts',(-60.0867047627418,1.98401739007027,126.302123965985));
#88347=CARTESIAN_POINT('Ctrl Pts',(-60.0941950985038,1.86236399208234,126.252351893552));
#88348=CARTESIAN_POINT('Ctrl Pts',(-60.1019694326229,1.73609806853288,126.200692697865));
#88349=CARTESIAN_POINT('Ctrl Pts',(-60.1097437667419,1.60748109646445,126.154209301384));
#88350=CARTESIAN_POINT('Ctrl Pts',(-60.117518100861,1.47697640304071,126.113121573629));
#88351=CARTESIAN_POINT('Ctrl Pts',(-60.1252828538081,1.34663254498807,126.072084482826));
#88352=CARTESIAN_POINT('Ctrl Pts',(-60.1330476067553,1.21440596385744,126.036429946149));
#88353=CARTESIAN_POINT('Ctrl Pts',(-60.1408123597024,1.08078083339959,126.006330203672));
#88354=CARTESIAN_POINT('Ctrl Pts',(-60.1485694005874,0.947288421305109,
125.976260356682));
#88355=CARTESIAN_POINT('Ctrl Pts',(-60.1563264414724,0.812400603113867,
125.951734409972));
#88356=CARTESIAN_POINT('Ctrl Pts',(-60.1640834823574,0.676617280351525,
125.932875000382));
#88357=CARTESIAN_POINT('Ctrl Pts',(-60.1718346735975,0.540936352849304,
125.91402981282));
#88358=CARTESIAN_POINT('Ctrl Pts',(-60.1795858648377,0.404361650614417,
125.900842710442));
#88359=CARTESIAN_POINT('Ctrl Pts',(-60.1873370560778,0.267403501115037,
125.893385314218));
#88360=CARTESIAN_POINT('Ctrl Pts',(-60.1950849528549,0.130503562482486,
125.885931087587));
#88361=CARTESIAN_POINT('Ctrl Pts',(-60.2028328496319,-0.00677910969947318,
125.884201744739));
#88362=CARTESIAN_POINT('Ctrl Pts',(-60.210580746409,-0.143929045674341,
125.888217058605));
#88363=CARTESIAN_POINT('Ctrl Pts',(-60.2183270224931,-0.281050292839214,
125.892231532554));
#88364=CARTESIAN_POINT('Ctrl Pts',(-60.2260732985772,-0.418038468474032,
125.901988261618));
#88365=CARTESIAN_POINT('Ctrl Pts',(-60.2338195746613,-0.554378478434141,
125.917454892555));
#88366=CARTESIAN_POINT('Ctrl Pts',(-60.2415659079266,-0.690719494825046,
125.932921637662));
#88367=CARTESIAN_POINT('Ctrl Pts',(-60.249312241192,-0.826411947520334,
125.95409832468));
#88368=CARTESIAN_POINT('Ctrl Pts',(-60.2570585744574,-0.960946633444781,
125.980900798083));
#88369=CARTESIAN_POINT('Ctrl Pts',(-60.2648066424604,-1.09551144747953,
126.007709273713));
#88370=CARTESIAN_POINT('Ctrl Pts',(-60.2725547104634,-1.22891759546181,
126.040145966323));
#88371=CARTESIAN_POINT('Ctrl Pts',(-60.2803027784663,-1.36066721303082,
126.078075840081));
#88372=CARTESIAN_POINT('Ctrl Pts',(-60.2880590812082,-1.49255685566103,
126.116046026161));
#88373=CARTESIAN_POINT('Ctrl Pts',(-60.29581538395,-1.62278607462486,126.159520947523));
#88374=CARTESIAN_POINT('Ctrl Pts',(-60.3035716866918,-1.75087276634372,
126.208315837695));
#88375=CARTESIAN_POINT('Ctrl Pts',(-60.311332129206,-1.87902782178674,126.25713677117));
#88376=CARTESIAN_POINT('Ctrl Pts',(-60.3190925717202,-2.00503771237078,
126.311283176979));
#88377=CARTESIAN_POINT('Ctrl Pts',(-60.3268530142343,-2.12844233081867,
126.37052296753));
#88378=CARTESIAN_POINT('Ctrl Pts',(-60.3346259144998,-2.25204504931544,
126.429857855051));
#88379=CARTESIAN_POINT('Ctrl Pts',(-60.3423988147652,-2.3730337930136,126.494302282368));
#88380=CARTESIAN_POINT('Ctrl Pts',(-60.3501717150307,-2.49097420135859,
126.563578780373));
#88381=CARTESIAN_POINT('Ctrl Pts',(-60.3576620507927,-2.60462717878596,
126.630336903179));
#88382=CARTESIAN_POINT('Ctrl Pts',(-60.3651523865547,-2.71544934329007,
126.701581713584));
#88383=CARTESIAN_POINT('Ctrl Pts',(-60.3726427223167,-2.82308063060881,
126.777029141814));
#88384=CARTESIAN_POINT('Ctrl Pts',(-60.3803688363466,-2.93409989936158,
126.854851478795));
#88385=CARTESIAN_POINT('Ctrl Pts',(-60.3880949503766,-3.04208577092471,
126.937399034632));
#88386=CARTESIAN_POINT('Ctrl Pts',(-60.3958210644065,-3.14660570564304,
127.024406173963));
#88387=CARTESIAN_POINT('Ctrl Pts',(-60.4035349748601,-3.250960548701,127.1112758835));
#88388=CARTESIAN_POINT('Ctrl Pts',(-60.4112488853137,-3.35186005432657,
127.202590898686));
#88389=CARTESIAN_POINT('Ctrl Pts',(-60.4189627957674,-3.44890065211306,
127.298042412617));
#88390=CARTESIAN_POINT('Ctrl Pts',(-60.4266696585593,-3.54585259067578,
127.39340671916));
#88391=CARTESIAN_POINT('Ctrl Pts',(-60.4343765213512,-3.63895235232623,
127.492899732487));
#88392=CARTESIAN_POINT('Ctrl Pts',(-60.442083384143,-3.72782930482369,127.596172384841));
#88393=CARTESIAN_POINT('Ctrl Pts',(-60.4497849296654,-3.81664493759624,
127.699373785307));
#88394=CARTESIAN_POINT('Ctrl Pts',(-60.4574864751878,-3.90124329931633,
127.806349338136));
#88395=CARTESIAN_POINT('Ctrl Pts',(-60.4651880207102,-3.9812908597072,127.916713451981));
#88396=CARTESIAN_POINT('Ctrl Pts',(-60.4728859750974,-4.06130109491251,
128.027026104407));
#88397=CARTESIAN_POINT('Ctrl Pts',(-60.4805839294846,-4.13676451924996,
128.140723853293));
#88398=CARTESIAN_POINT('Ctrl Pts',(-60.4882818838717,-4.20738843157316,
128.257388758993));
#88399=CARTESIAN_POINT('Ctrl Pts',(-60.4959794064094,-4.27800838194788,
128.374047119879));
#88400=CARTESIAN_POINT('Ctrl Pts',(-60.503676928947,-4.34378914721932,128.493671972289));
#88401=CARTESIAN_POINT('Ctrl Pts',(-60.5113744514847,-4.40448196449461,
128.615817337907));
#88402=CARTESIAN_POINT('Ctrl Pts',(-60.5190716469134,-4.46517220260643,
128.737957512912));
#88403=CARTESIAN_POINT('Ctrl Pts',(-60.526768842342,-4.52077475164605,128.862617630379));
#88404=CARTESIAN_POINT('Ctrl Pts',(-60.5344660377707,-4.57108769168258,
128.989328833423));
#88405=CARTESIAN_POINT('Ctrl Pts',(-60.5421670668684,-4.62142569060738,
129.116103146314));
#88406=CARTESIAN_POINT('Ctrl Pts',(-60.5498680959661,-4.66646867744965,
129.244930214439));
#88407=CARTESIAN_POINT('Ctrl Pts',(-60.5575691250638,-4.70606359539469,
129.375323004835));
#88408=CARTESIAN_POINT('Ctrl Pts',(-60.5616233839294,-4.72690860780455,
129.443969171439));
#88409=CARTESIAN_POINT('Ctrl Pts',(-60.5656776427949,-4.74624448496707,
129.513049030915));
#88410=CARTESIAN_POINT('Ctrl Pts',(-60.5697319016604,-4.76405452823403,
129.582490119308));
#88411=CARTESIAN_POINT('Origin',(213.235140564004,0.,130.804360617566));
#88412=CARTESIAN_POINT('',(-62.6653842080088,-4.76405452823406,129.582490119308));
#88413=CARTESIAN_POINT('',(-62.3199210724795,-4.76405452823405,129.582490119308));
#88414=CARTESIAN_POINT('',(213.235140564004,-4.76405452823405,129.582490119308));
#88415=CARTESIAN_POINT('',(-60.9851405639584,-4.91824796096415,130.799882116478));
#88416=CARTESIAN_POINT('Ctrl Pts',(-60.9851405640084,-4.91824796096495,
130.799882117362));
#88417=CARTESIAN_POINT('Ctrl Pts',(-60.9928182880772,-4.91837153989948,
130.93559537294));
#88418=CARTESIAN_POINT('Ctrl Pts',(-61.0004960121458,-4.91287362247503,
131.071436499204));
#88419=CARTESIAN_POINT('Ctrl Pts',(-61.0081737362145,-4.9017493146528,131.206898465229));
#88420=CARTESIAN_POINT('Ctrl Pts',(-61.0158477996582,-4.89063031073562,
131.342295844996));
#88421=CARTESIAN_POINT('Ctrl Pts',(-61.0235218631019,-4.8738902832785,131.477314027108));
#88422=CARTESIAN_POINT('Ctrl Pts',(-61.0311959265456,-4.85157641150895,
131.611447592922));
#88423=CARTESIAN_POINT('Ctrl Pts',(-61.0388681933982,-4.82926776368656,
131.745549756447));
#88424=CARTESIAN_POINT('Ctrl Pts',(-61.0465404602509,-4.80138793153318,
131.878767321949));
#88425=CARTESIAN_POINT('Ctrl Pts',(-61.0542127271036,-4.76803571740963,
132.010602077642));
#88426=CARTESIAN_POINT('Ctrl Pts',(-61.0618849370681,-4.73468375058525,
132.14243585581));
#88427=CARTESIAN_POINT('Ctrl Pts',(-61.0695571470326,-4.69585958036707,
132.27288645754));
#88428=CARTESIAN_POINT('Ctrl Pts',(-61.0772293569972,-4.65171256107439,
132.40146841344));
#88429=CARTESIAN_POINT('Ctrl Pts',(-61.0849032494586,-4.60755586044814,
132.53007856705));
#88430=CARTESIAN_POINT('Ctrl Pts',(-61.0925771419201,-4.55807411889652,
132.656818882375));
#88431=CARTESIAN_POINT('Ctrl Pts',(-61.1002510343815,-4.50346556316825,
132.781222014796));
#88432=CARTESIAN_POINT('Ctrl Pts',(-61.1079330096527,-4.44879948896839,
132.905756179395));
#88433=CARTESIAN_POINT('Ctrl Pts',(-61.1156149849239,-4.38899597707964,
133.027947878844));
#88434=CARTESIAN_POINT('Ctrl Pts',(-61.1232969601951,-4.32430031971325,
133.147352253793));
#88435=CARTESIAN_POINT('Ctrl Pts',(-61.1309831423546,-4.25956923299425,
133.266822018288));
#88436=CARTESIAN_POINT('Ctrl Pts',(-61.1386693245141,-4.18994086992982,
133.383501076189));
#88437=CARTESIAN_POINT('Ctrl Pts',(-61.1463555066737,-4.11570429665684,
133.49697295598));
#88438=CARTESIAN_POINT('Ctrl Pts',(-61.1540537610474,-4.04135112455874,
133.610623059082));
#88439=CARTESIAN_POINT('Ctrl Pts',(-61.1617520154212,-3.96237551682344,
133.721055597784));
#88440=CARTESIAN_POINT('Ctrl Pts',(-61.1694502697949,-3.87910772298163,
133.827886098855));
#88441=CARTESIAN_POINT('Ctrl Pts',(-61.1757657123952,-3.81079704540008,
133.915526993105));
#88442=CARTESIAN_POINT('Ctrl Pts',(-61.1820811549954,-3.73959848333886,
134.000744235032));
#88443=CARTESIAN_POINT('Ctrl Pts',(-61.1883965975958,-3.6657123461508,134.083344615358));
#88444=CARTESIAN_POINT('Ctrl Pts',(-61.1961709317149,-3.57475822723578,
134.185026001075));
#88445=CARTESIAN_POINT('Ctrl Pts',(-61.2039452658339,-3.47942610258915,
134.2830811777));
#88446=CARTESIAN_POINT('Ctrl Pts',(-61.211719599953,-3.38003646820944,134.377109774178));
#88447=CARTESIAN_POINT('Ctrl Pts',(-61.2194843529001,-3.28076932267154,
134.471022488815));
#88448=CARTESIAN_POINT('Ctrl Pts',(-61.2272491058473,-3.17745489822238,
134.560918230894));
#88449=CARTESIAN_POINT('Ctrl Pts',(-61.2350138587944,-3.07045326961318,
134.646430343849));
#88450=CARTESIAN_POINT('Ctrl Pts',(-61.2427708996794,-2.96355791652997,
134.731857524969));
#88451=CARTESIAN_POINT('Ctrl Pts',(-61.2505279405644,-2.85298295063678,
134.812909498888));
#88452=CARTESIAN_POINT('Ctrl Pts',(-61.2582849814494,-2.73912428546976,
134.889257337344));
#88453=CARTESIAN_POINT('Ctrl Pts',(-61.2660361726895,-2.62535148200784,
134.9655476013));
#88454=CARTESIAN_POINT('Ctrl Pts',(-61.2737873639297,-2.50830023152952,
135.037140573869));
#88455=CARTESIAN_POINT('Ctrl Pts',(-61.2815385551698,-2.3883981363744,135.103748644328));
#88456=CARTESIAN_POINT('Ctrl Pts',(-61.2892864519469,-2.26854700280806,
135.17032840458));
#88457=CARTESIAN_POINT('Ctrl Pts',(-61.2970343487241,-2.14584777556872,
135.231927287224));
#88458=CARTESIAN_POINT('Ctrl Pts',(-61.3047822455012,-2.0207553582815,135.288302058361));
#88459=CARTESIAN_POINT('Ctrl Pts',(-61.3125285215853,-1.89568910763129,
135.34466503711));
#88460=CARTESIAN_POINT('Ctrl Pts',(-61.3202747976694,-1.76823101887653,
135.3958059174));
#88461=CARTESIAN_POINT('Ctrl Pts',(-61.3280210737535,-1.63885845643614,
135.441528505649));
#88462=CARTESIAN_POINT('Ctrl Pts',(-61.3357674070189,-1.50948493899706,
135.487251431411));
#88463=CARTESIAN_POINT('Ctrl Pts',(-61.3435137402843,-1.37819728829377,
135.527555855044));
#88464=CARTESIAN_POINT('Ctrl Pts',(-61.3512600735496,-1.24549022793658,
135.562294744329));
#88465=CARTESIAN_POINT('Ctrl Pts',(-61.3590081415526,-1.11275344875334,
135.597041413147));
#88466=CARTESIAN_POINT('Ctrl Pts',(-61.3667562095556,-0.978597005546652,
135.62621996851));
#88467=CARTESIAN_POINT('Ctrl Pts',(-61.3745042775585,-0.84352767891142,
135.6497340931));
#88468=CARTESIAN_POINT('Ctrl Pts',(-61.3822605803004,-0.708314798988495,
135.673273208782));
#88469=CARTESIAN_POINT('Ctrl Pts',(-61.3900168830423,-0.57218748329756,
135.691135800482));
#88470=CARTESIAN_POINT('Ctrl Pts',(-61.3977731857842,-0.435660089907948,
135.703277166004));
#88471=CARTESIAN_POINT('Ctrl Pts',(-61.4055336282984,-0.299059827737351,
135.715425011739));
#88472=CARTESIAN_POINT('Ctrl Pts',(-61.4132940708126,-0.162059452729946,
135.721845528465));
#88473=CARTESIAN_POINT('Ctrl Pts',(-61.4210545133268,-0.0251742390910713,
135.722546189521));
#88474=CARTESIAN_POINT('Ctrl Pts',(-61.4288274135922,0.111930714844648,
135.72324797534));
#88475=CARTESIAN_POINT('Ctrl Pts',(-61.4366003138577,0.248919747062051,
135.71821157126));
#88476=CARTESIAN_POINT('Ctrl Pts',(-61.4443732141231,0.385280888231227,
135.707496522236));
#88477=CARTESIAN_POINT('Ctrl Pts',(-61.451863549885,0.516684958442969,135.697170992234));
#88478=CARTESIAN_POINT('Ctrl Pts',(-61.4593538856468,0.647505690031206,
135.68157255189));
#88479=CARTESIAN_POINT('Ctrl Pts',(-61.4668442214087,0.777295039901073,
135.660799177194));
#88480=CARTESIAN_POINT('Ctrl Pts',(-61.4746185555278,0.912005392422351,
135.639238173683));
#88481=CARTESIAN_POINT('Ctrl Pts',(-61.4823928896469,1.0460313315711,135.612033775368));
#88482=CARTESIAN_POINT('Ctrl Pts',(-61.490167223766,1.17886277792507,135.579239214276));
#88483=CARTESIAN_POINT('Ctrl Pts',(-61.497931976713,1.31153052139307,135.54648506955));
#88484=CARTESIAN_POINT('Ctrl Pts',(-61.5056967296601,1.4430063251933,135.508154562664));
#88485=CARTESIAN_POINT('Ctrl Pts',(-61.5134614826072,1.57278708157492,135.464352447873));
#88486=CARTESIAN_POINT('Ctrl Pts',(-61.5212185234922,1.70243893787972,135.420593837961));
#88487=CARTESIAN_POINT('Ctrl Pts',(-61.5289755643773,1.83039872905795,135.371374559217));
#88488=CARTESIAN_POINT('Ctrl Pts',(-61.5367326052623,1.95617571750912,135.316849911152));
#88489=CARTESIAN_POINT('Ctrl Pts',(-61.5444837965024,2.08185785655506,135.262366380548));
#88490=CARTESIAN_POINT('Ctrl Pts',(-61.5522349877425,2.20536011201475,135.202585598886));
#88491=CARTESIAN_POINT('Ctrl Pts',(-61.5599861789826,2.32620937933313,135.137711859504));
#88492=CARTESIAN_POINT('Ctrl Pts',(-61.5677340757597,2.44700728248898,135.072865693191));
#88493=CARTESIAN_POINT('Ctrl Pts',(-61.5754819725368,2.56515409644669,135.002931058998));
#88494=CARTESIAN_POINT('Ctrl Pts',(-61.5832298693139,2.68019929511584,134.928159206363));
#88495=CARTESIAN_POINT('Ctrl Pts',(-61.590976145398,2.79522042880952,134.853402994387));
#88496=CARTESIAN_POINT('Ctrl Pts',(-61.5987224214821,2.90714091009121,134.773811789499));
#88497=CARTESIAN_POINT('Ctrl Pts',(-61.6064686975662,3.01553764861504,134.689681164482));
#88498=CARTESIAN_POINT('Ctrl Pts',(-61.6142150308315,3.12393518729883,134.605549918431));
#88499=CARTESIAN_POINT('Ctrl Pts',(-61.6219613640969,3.22880862246597,134.516879425099));
#88500=CARTESIAN_POINT('Ctrl Pts',(-61.6297076973622,3.32976684155063,134.424006434964));
#88501=CARTESIAN_POINT('Ctrl Pts',(-61.6374557653652,3.43074766952845,134.331112646568));
#88502=CARTESIAN_POINT('Ctrl Pts',(-61.6452038333682,3.52781124904164,134.23401475329));
#88503=CARTESIAN_POINT('Ctrl Pts',(-61.6529519013712,3.62060261831174,134.133087062135));
#88504=CARTESIAN_POINT('Ctrl Pts',(-61.660708204113,3.71349260735333,134.032052103829));
#88505=CARTESIAN_POINT('Ctrl Pts',(-61.6684645068548,3.8021010508708,133.927179504945));
#88506=CARTESIAN_POINT('Ctrl Pts',(-61.6762208095966,3.88611231654023,133.818877846864));
#88507=CARTESIAN_POINT('Ctrl Pts',(-61.6839812521108,3.97016842155167,133.710518384927));
#88508=CARTESIAN_POINT('Ctrl Pts',(-61.691741694625,4.04962223322311,133.598726535502));
#88509=CARTESIAN_POINT('Ctrl Pts',(-61.6995021371392,4.12420152079204,133.483939852893));
#88510=CARTESIAN_POINT('Ctrl Pts',(-61.7072750374046,4.19890052965431,133.368968904511));
#88511=CARTESIAN_POINT('Ctrl Pts',(-61.7150479376701,4.26870917831983,133.250993852549));
#88512=CARTESIAN_POINT('Ctrl Pts',(-61.7228208379355,4.33340083171799,133.130477616809));
#88513=CARTESIAN_POINT('Ctrl Pts',(-61.7303111736975,4.3957407805665,133.0143424498));
#88514=CARTESIAN_POINT('Ctrl Pts',(-61.7378015094595,4.45332917183307,132.895847925258));
#88515=CARTESIAN_POINT('Ctrl Pts',(-61.7452918452215,4.50600625725573,132.775423952944));
#88516=CARTESIAN_POINT('Ctrl Pts',(-61.7530661793406,4.56068061038311,132.650434069118));
#88517=CARTESIAN_POINT('Ctrl Pts',(-61.7608405134597,4.61023707348776,132.522969608907));
#88518=CARTESIAN_POINT('Ctrl Pts',(-61.7686148475788,4.65444472179399,132.393488489785));
#88519=CARTESIAN_POINT('Ctrl Pts',(-61.7763796005259,4.69859788812463,132.264166944571));
#88520=CARTESIAN_POINT('Ctrl Pts',(-61.7841443534729,4.73741523053368,132.132834051999));
#88521=CARTESIAN_POINT('Ctrl Pts',(-61.79190910642,4.77071293971553,131.999969713103));
#88522=CARTESIAN_POINT('Ctrl Pts',(-61.799666147305,4.80397757714325,131.867237336941));
#88523=CARTESIAN_POINT('Ctrl Pts',(-61.8074231881901,4.83173339669718,131.732976918205));
#88524=CARTESIAN_POINT('Ctrl Pts',(-61.8151802290751,4.8538458005935,131.597685271513));
#88525=CARTESIAN_POINT('Ctrl Pts',(-61.8229314203152,4.87594152935406,131.462495649305));
#88526=CARTESIAN_POINT('Ctrl Pts',(-61.8306826115553,4.89240225044825,131.326276731306));
#88527=CARTESIAN_POINT('Ctrl Pts',(-61.8384338027955,4.9031441170792,131.189536979317));
#88528=CARTESIAN_POINT('Ctrl Pts',(-61.8461816995726,4.91388141813024,131.05285534537));
#88529=CARTESIAN_POINT('Ctrl Pts',(-61.8539295963496,4.91890466857223,130.915653706666));
#88530=CARTESIAN_POINT('Ctrl Pts',(-61.8616774931267,4.91818173131711,130.778446910024));
#88531=CARTESIAN_POINT('Ctrl Pts',(-61.8694237692108,4.91745894528488,130.641268814085));
#88532=CARTESIAN_POINT('Ctrl Pts',(-61.8771700452949,4.91099236441548,130.504085953065));
#88533=CARTESIAN_POINT('Ctrl Pts',(-61.8849163213791,4.89880197179482,130.367414049163));
#88534=CARTESIAN_POINT('Ctrl Pts',(-61.8926626546444,4.88661148918747,130.23074113638));
#88535=CARTESIAN_POINT('Ctrl Pts',(-61.9004089879097,4.8686971452524,130.094579577661));
#88536=CARTESIAN_POINT('Ctrl Pts',(-61.9081553211751,4.84513085180934,129.959440448943));
#88537=CARTESIAN_POINT('Ctrl Pts',(-61.915903389178,4.8215592808583,129.824271056755));
#88538=CARTESIAN_POINT('Ctrl Pts',(-61.9236514571809,4.79233330892533,129.690124935263));
#88539=CARTESIAN_POINT('Ctrl Pts',(-61.9313995251839,4.757575985582,129.557503045943));
#88540=CARTESIAN_POINT('Ctrl Pts',(-61.9391558279257,4.7227817217417,129.424740204501));
#88541=CARTESIAN_POINT('Ctrl Pts',(-61.9469121306677,4.68244446225671,129.293505210095));
#88542=CARTESIAN_POINT('Ctrl Pts',(-61.9546684334095,4.63673735123466,129.164284461357));
#88543=CARTESIAN_POINT('Ctrl Pts',(-61.9624288759237,4.59100584495119,129.034994743614));
#88544=CARTESIAN_POINT('Ctrl Pts',(-61.9701893184378,4.53989892189582,128.907721776324));
#88545=CARTESIAN_POINT('Ctrl Pts',(-61.977949760952,4.48363756152041,128.782931103726));
#88546=CARTESIAN_POINT('Ctrl Pts',(-61.9857226612174,4.42728588541475,128.657940106062));
#88547=CARTESIAN_POINT('Ctrl Pts',(-61.9934955614829,4.36576341274733,128.53543971557));
#88548=CARTESIAN_POINT('Ctrl Pts',(-62.0012684617483,4.29933710926502,128.415870826213));
#88549=CARTESIAN_POINT('Ctrl Pts',(-62.0087587975104,4.23532556923152,128.300648567159));
#88550=CARTESIAN_POINT('Ctrl Pts',(-62.0162491332724,4.16676070194888,128.188148637693));
#88551=CARTESIAN_POINT('Ctrl Pts',(-62.0237394690345,4.09391785483666,128.078737815278));
#88552=CARTESIAN_POINT('Ctrl Pts',(-62.0315138031536,4.0183131490365,127.965178648278));
#88553=CARTESIAN_POINT('Ctrl Pts',(-62.0392881372726,3.93786016747144,127.854587738119));
#88554=CARTESIAN_POINT('Ctrl Pts',(-62.0470624713917,3.85281934859991,127.747406883936));
#88555=CARTESIAN_POINT('Ctrl Pts',(-62.0548272243388,3.76788333493756,127.640358120577));
#88556=CARTESIAN_POINT('Ctrl Pts',(-62.062591977286,3.67837097461425,127.536711354624));
#88557=CARTESIAN_POINT('Ctrl Pts',(-62.070356730233,3.58458666854186,127.436880628284));
#88558=CARTESIAN_POINT('Ctrl Pts',(-62.0781137711181,3.490895510364,127.337149055229));
#88559=CARTESIAN_POINT('Ctrl Pts',(-62.0858708120032,3.39294111607042,127.241226262332));
#88560=CARTESIAN_POINT('Ctrl Pts',(-62.0936278528882,3.29106871648181,127.149494030959));
#88561=CARTESIAN_POINT('Ctrl Pts',(-62.1013790441283,3.18927313966261,127.057830975576));
#88562=CARTESIAN_POINT('Ctrl Pts',(-62.1091302353684,3.0835657278569,126.970352452217));
#88563=CARTESIAN_POINT('Ctrl Pts',(-62.1168814266085,2.9743289431362,126.887403839591));
#88564=CARTESIAN_POINT('Ctrl Pts',(-62.1246293233856,2.86513858696298,126.804490482338));
#88565=CARTESIAN_POINT('Ctrl Pts',(-62.1323772201626,2.75242215213261,126.72610344242));
#88566=CARTESIAN_POINT('Ctrl Pts',(-62.1401251169397,2.63659542297332,126.652548044959));
#88567=CARTESIAN_POINT('Ctrl Pts',(-62.1478713930238,2.52079292226884,126.579008033702));
#88568=CARTESIAN_POINT('Ctrl Pts',(-62.1556176691079,2.40188175115738,126.510297864072));
#88569=CARTESIAN_POINT('Ctrl Pts',(-62.1633639451919,2.28030660267691,126.446679484178));
#88570=CARTESIAN_POINT('Ctrl Pts',(-62.1711102784573,2.15873055675664,126.383060634667));
#88571=CARTESIAN_POINT('Ctrl Pts',(-62.1788566117226,2.03449084063159,126.324533831162));
#88572=CARTESIAN_POINT('Ctrl Pts',(-62.1866029449879,1.90805630705779,126.271314821239));
#88573=CARTESIAN_POINT('Ctrl Pts',(-62.1943510129909,1.7815934593465,126.218083893288));
#88574=CARTESIAN_POINT('Ctrl Pts',(-62.2020990809939,1.6529351764055,126.17016327583));
#88575=CARTESIAN_POINT('Ctrl Pts',(-62.2098471489968,1.52256944261142,126.12772022569));
#88576=CARTESIAN_POINT('Ctrl Pts',(-62.2176034517387,1.39206515456409,126.085232066571));
#88577=CARTESIAN_POINT('Ctrl Pts',(-62.2253597544806,1.25985016295856,126.048233225318));
#88578=CARTESIAN_POINT('Ctrl Pts',(-62.2331160572224,1.1264272773577,126.016840941228));
#88579=CARTESIAN_POINT('Ctrl Pts',(-62.2408764997366,0.992933179945151,
125.985431902131));
#88580=CARTESIAN_POINT('Ctrl Pts',(-62.2486369422508,0.858230287738499,
125.959635456285));
#88581=CARTESIAN_POINT('Ctrl Pts',(-62.256397384765,0.722829721083129,125.939517325453));
#88582=CARTESIAN_POINT('Ctrl Pts',(-62.2641702850304,0.58721179741805,125.919366899211));
#88583=CARTESIAN_POINT('Ctrl Pts',(-62.2719431852958,0.450894350258999,
125.904913044574));
#88584=CARTESIAN_POINT('Ctrl Pts',(-62.2797160855613,0.314392617690945,
125.896169469654));
#88585=CARTESIAN_POINT('Ctrl Pts',(-62.2872064213233,0.182853066928855,
125.887743745707));
#88586=CARTESIAN_POINT('Ctrl Pts',(-62.2946967570852,0.0511427045500864,
125.884620350569));
#88587=CARTESIAN_POINT('Ctrl Pts',(-62.3021870928473,-0.0802810571713846,
125.886765878839));
#88588=CARTESIAN_POINT('Ctrl Pts',(-62.3099614269664,-0.216687790763728,
125.888992755464));
#88589=CARTESIAN_POINT('Ctrl Pts',(-62.3177357610855,-0.353217857286612,
125.896903039128));
#88590=CARTESIAN_POINT('Ctrl Pts',(-62.3255100952046,-0.489358785267645,
125.910516418801));
#88591=CARTESIAN_POINT('Ctrl Pts',(-62.3332748481517,-0.625331931722389,
125.924113021201));
#88592=CARTESIAN_POINT('Ctrl Pts',(-62.3410396010986,-0.760916508562987,
125.943398696353));
#88593=CARTESIAN_POINT('Ctrl Pts',(-62.3488043540457,-0.895599634227301,
125.968341143073));
#88594=CARTESIAN_POINT('Ctrl Pts',(-62.3565613949307,-1.03014899071269,
125.993258816604));
#88595=CARTESIAN_POINT('Ctrl Pts',(-62.3643184358159,-1.16379829583602,
126.023822010131));
#88596=CARTESIAN_POINT('Ctrl Pts',(-62.3720754767009,-1.29603974043084,
126.05994663334));
#88597=CARTESIAN_POINT('Ctrl Pts',(-62.379826667941,-1.42818146072253,126.096044014689));
#88598=CARTESIAN_POINT('Ctrl Pts',(-62.3875778591811,-1.55891705807206,
126.137694375373));
#88599=CARTESIAN_POINT('Ctrl Pts',(-62.3953290504212,-1.68774922549897,
126.184762624848));
#88600=CARTESIAN_POINT('Ctrl Pts',(-62.4030769471982,-1.81652663581871,
126.231810869061));
#88601=CARTESIAN_POINT('Ctrl Pts',(-62.4108248439753,-1.94340185881632,
126.284272288193));
#88602=CARTESIAN_POINT('Ctrl Pts',(-62.4185727407524,-2.06789327423267,
126.3419621068));
#88603=CARTESIAN_POINT('Ctrl Pts',(-62.4263190168365,-2.19235864872882,
126.399639857941));
#88604=CARTESIAN_POINT('Ctrl Pts',(-62.4340652929205,-2.31444085296472,
126.462543668912));
#88605=CARTESIAN_POINT('Ctrl Pts',(-62.4418115690046,-2.43367913512781,
126.530440996218));
#88606=CARTESIAN_POINT('Ctrl Pts',(-62.44955790227,-2.55291829748064,126.598338824726));
#88607=CARTESIAN_POINT('Ctrl Pts',(-62.4573042355354,-2.66931315612464,
126.671230049663));
#88608=CARTESIAN_POINT('Ctrl Pts',(-62.4650505688007,-2.78242877014554,
126.748836828761));
#88609=CARTESIAN_POINT('Ctrl Pts',(-62.4727986368036,-2.89556971562268,
126.826460987358));
#88610=CARTESIAN_POINT('Ctrl Pts',(-62.4805467048065,-3.00542963285425,
126.908802580325));
#88611=CARTESIAN_POINT('Ctrl Pts',(-62.4882947728094,-3.11160403646128,
126.995541458984));
#88612=CARTESIAN_POINT('Ctrl Pts',(-62.4960510755512,-3.21789128348912,
127.082372524757));
#88613=CARTESIAN_POINT('Ctrl Pts',(-62.5038073782931,-3.32048488899119,
127.173609964274));
#88614=CARTESIAN_POINT('Ctrl Pts',(-62.511563681035,-3.41901443537407,127.268894120312));
#88615=CARTESIAN_POINT('Ctrl Pts',(-62.5193241235491,-3.51759656994239,
127.364229132374));
#88616=CARTESIAN_POINT('Ctrl Pts',(-62.5270845660633,-3.6121100539642,127.463614881478));
#88617=CARTESIAN_POINT('Ctrl Pts',(-62.5348450085774,-3.70222332082832,
127.56665687182));
#88618=CARTESIAN_POINT('Ctrl Pts',(-62.5426179088429,-3.79248124550855,
127.669864274314));
#88619=CARTESIAN_POINT('Ctrl Pts',(-62.5503908091083,-3.8783245926976,127.776739341833));
#88620=CARTESIAN_POINT('Ctrl Pts',(-62.5581637093737,-3.95946333060175,
127.886855999554));
#88621=CARTESIAN_POINT('Ctrl Pts',(-62.5656540451359,-4.03765247100836,
127.992969639402));
#88622=CARTESIAN_POINT('Ctrl Pts',(-62.5731443808981,-4.11147293986799,
128.10209302614));
#88623=CARTESIAN_POINT('Ctrl Pts',(-62.5806347166602,-4.18070559958617,
128.21382326943));
#88624=CARTESIAN_POINT('Ctrl Pts',(-62.588633751821,-4.25464013295595,128.333141571435));
#88625=CARTESIAN_POINT('Ctrl Pts',(-62.5966327869818,-4.32356552374327,
128.455792831829));
#88626=CARTESIAN_POINT('Ctrl Pts',(-62.6046318221426,-4.3871773021134,128.58133151692));
#88627=CARTESIAN_POINT('Ctrl Pts',(-62.6126203547539,-4.45070555967966,
128.7067053726));
#88628=CARTESIAN_POINT('Ctrl Pts',(-62.6206088873652,-4.50893393109456,
128.834958788006));
#88629=CARTESIAN_POINT('Ctrl Pts',(-62.6285974199765,-4.56160153313018,
128.965617972321));
#88630=CARTESIAN_POINT('Ctrl Pts',(-62.63657358476,-4.61418759530553,129.096074870387));
#88631=CARTESIAN_POINT('Ctrl Pts',(-62.6445497495436,-4.6612299106076,129.228929782936));
#88632=CARTESIAN_POINT('Ctrl Pts',(-62.6525259143271,-4.702514088301,129.363685667471));
#88633=CARTESIAN_POINT('Ctrl Pts',(-62.656812012221,-4.72469868852751,129.436098528611));
#88634=CARTESIAN_POINT('Ctrl Pts',(-62.6610981101149,-4.74522136577641,
129.509059904719));
#88635=CARTESIAN_POINT('Ctrl Pts',(-62.6653842080088,-4.76405452823406,
129.582490119308));
#88636=CARTESIAN_POINT('Ctrl Pts',(-60.9152461054369,-4.76405452823402,
129.582490119308));
#88637=CARTESIAN_POINT('Ctrl Pts',(-60.9251020627235,-4.80703171165325,
129.75005750519));
#88638=CARTESIAN_POINT('Ctrl Pts',(-60.9349580200101,-4.84119281879953,
129.920005984769));
#88639=CARTESIAN_POINT('Ctrl Pts',(-60.9448139772968,-4.86631688391131,
130.091519086888));
#88640=CARTESIAN_POINT('Ctrl Pts',(-60.9545017912762,-4.89101233074943,
130.260106163723));
#88641=CARTESIAN_POINT('Ctrl Pts',(-60.9641896052557,-4.90697645570549,
130.430205070139));
#88642=CARTESIAN_POINT('Ctrl Pts',(-60.9738774192352,-4.91404468006025,
130.601018676807));
#88643=CARTESIAN_POINT('Ctrl Pts',(-60.9776318008096,-4.91678387502598,
130.667215185008));
#88644=CARTESIAN_POINT('Ctrl Pts',(-60.981386182384,-4.9181875312636,130.73351878516));
#88645=CARTESIAN_POINT('Ctrl Pts',(-60.9851405639584,-4.91824796096415,
130.799882116478));
#88646=CARTESIAN_POINT('',(-60.6398594359436,-4.91824984849176,130.805581400405));
#88647=CARTESIAN_POINT('Ctrl Pts',(-60.5697319016604,-4.76405452823403,
129.582490119308));
#88648=CARTESIAN_POINT('Ctrl Pts',(-60.5774417162904,-4.79792314311371,
129.714543334696));
#88649=CARTESIAN_POINT('Ctrl Pts',(-60.5851515309204,-4.82627074302898,
129.847903162596));
#88650=CARTESIAN_POINT('Ctrl Pts',(-60.5928613455504,-4.84902190340704,
129.982065267477));
#88651=CARTESIAN_POINT('Ctrl Pts',(-60.6006943606159,-4.87213662023907,
130.11837124099));
#88652=CARTESIAN_POINT('Ctrl Pts',(-60.6085273756815,-4.88947445874853,
130.255504925166));
#88653=CARTESIAN_POINT('Ctrl Pts',(-60.616360390747,-4.90101128615102,130.392934517859));
#88654=CARTESIAN_POINT('Ctrl Pts',(-60.6241934058126,-4.91254811355353,
130.530364110552));
#88655=CARTESIAN_POINT('Ctrl Pts',(-60.6320264208781,-4.91828397610615,
130.668089187314));
#88656=CARTESIAN_POINT('Ctrl Pts',(-60.6398594359436,-4.91824984849176,
130.805581400405));
#88657=CARTESIAN_POINT('Ctrl Pts',(-60.639859435991,-4.91824984849156,130.805581401237));
#88658=CARTESIAN_POINT('Ctrl Pts',(-60.643603072704,-4.91823353785304,130.871293121737));
#88659=CARTESIAN_POINT('Ctrl Pts',(-60.6473467094168,-4.91690034492517,
130.936986903404));
#88660=CARTESIAN_POINT('Ctrl Pts',(-60.6510903461297,-4.91425206892654,
131.002627270211));
#88661=CARTESIAN_POINT('Ctrl Pts',(-60.6588646802487,-4.9087524480947,131.138941283136));
#88662=CARTESIAN_POINT('Ctrl Pts',(-60.6666390143678,-4.89756809725561,
131.275242207376));
#88663=CARTESIAN_POINT('Ctrl Pts',(-60.6744133484869,-4.88069163100898,
131.411017246557));
#88664=CARTESIAN_POINT('Ctrl Pts',(-60.682178101434,-4.86383596349872,131.546624955137));
#88665=CARTESIAN_POINT('Ctrl Pts',(-60.6899428543811,-4.84130218614871,
131.681707683942));
#88666=CARTESIAN_POINT('Ctrl Pts',(-60.6977076073282,-4.81313489858287,
131.815753474246));
#88667=CARTESIAN_POINT('Ctrl Pts',(-60.7054646482132,-4.78499558716413,
131.949666128382));
#88668=CARTESIAN_POINT('Ctrl Pts',(-60.7132216890982,-4.7512339802709,132.082543513434));
#88669=CARTESIAN_POINT('Ctrl Pts',(-60.7209787299832,-4.71194633002055,
132.213879984409));
#88670=CARTESIAN_POINT('Ctrl Pts',(-60.7287299212233,-4.67268830689292,
132.34511741353));
#88671=CARTESIAN_POINT('Ctrl Pts',(-60.7364811124633,-4.62791264662451,
132.474815868444));
#88672=CARTESIAN_POINT('Ctrl Pts',(-60.7442323037035,-4.57776633485353,
132.602481427184));
#88673=CARTESIAN_POINT('Ctrl Pts',(-60.7519802004805,-4.52764133660268,
132.730092724656));
#88674=CARTESIAN_POINT('Ctrl Pts',(-60.7597280972577,-4.47215036954447,
132.855672481317));
#88675=CARTESIAN_POINT('Ctrl Pts',(-60.7674759940348,-4.41148971347016,
132.978743649703));
#88676=CARTESIAN_POINT('Ctrl Pts',(-60.7752222701188,-4.35084174629741,
133.101789074254));
#88677=CARTESIAN_POINT('Ctrl Pts',(-60.7829685462029,-4.28502641378575,
133.222326603813));
#88678=CARTESIAN_POINT('Ctrl Pts',(-60.790714822287,-4.21428724923702,133.339901199655));
#88679=CARTESIAN_POINT('Ctrl Pts',(-60.7984611555523,-4.14354756250775,
133.457476663405));
#88680=CARTESIAN_POINT('Ctrl Pts',(-60.8062074888176,-4.06788417277146,
133.572088814791));
#88681=CARTESIAN_POINT('Ctrl Pts',(-60.813953822083,-3.98758527966579,133.683309505597));
#88682=CARTESIAN_POINT('Ctrl Pts',(-60.821701890086,-3.90726840417987,133.794555103505));
#88683=CARTESIAN_POINT('Ctrl Pts',(-60.829449958089,-3.82231418845972,133.902407412605));
#88684=CARTESIAN_POINT('Ctrl Pts',(-60.837198026092,-3.73305239552146,134.006469746686));
#88685=CARTESIAN_POINT('Ctrl Pts',(-60.8449543288338,-3.64369573408743,
134.110642679453));
#88686=CARTESIAN_POINT('Ctrl Pts',(-60.8527106315756,-3.55002260504918,
134.211017293552));
#88687=CARTESIAN_POINT('Ctrl Pts',(-60.8604669343175,-3.45240145105574,
134.307231908842));
#88688=CARTESIAN_POINT('Ctrl Pts',(-60.8682273768316,-3.3547281937131,134.40349787677));
#88689=CARTESIAN_POINT('Ctrl Pts',(-60.8759878193458,-3.2531030022346,134.495599159301));
#88690=CARTESIAN_POINT('Ctrl Pts',(-60.8837482618599,-3.14792821550424,
134.58321375212));
#88691=CARTESIAN_POINT('Ctrl Pts',(-60.8915211621254,-3.0425845928691,134.670968991662));
#88692=CARTESIAN_POINT('Ctrl Pts',(-60.8992940623908,-2.9336802990924,134.754222911155));
#88693=CARTESIAN_POINT('Ctrl Pts',(-60.9070669626563,-2.82164824626189,
134.832695786946));
#88694=CARTESIAN_POINT('Ctrl Pts',(-60.9145572984184,-2.71368884074286,
134.908315976042));
#88695=CARTESIAN_POINT('Ctrl Pts',(-60.9220476341804,-2.60282539113857,
134.979496526034));
#88696=CARTESIAN_POINT('Ctrl Pts',(-60.9295379699425,-2.48946593046216,
135.046028030691));
#88697=CARTESIAN_POINT('Ctrl Pts',(-60.9373123040616,-2.37180841137968,
135.115082097569));
#88698=CARTESIAN_POINT('Ctrl Pts',(-60.9450866381807,-2.25108916875184,
135.179346365338));
#88699=CARTESIAN_POINT('Ctrl Pts',(-60.9528609722998,-2.12773564070224,
135.238537441486));
#88700=CARTESIAN_POINT('Ctrl Pts',(-60.9606257252469,-2.0045341348517,135.297655569922));
#88701=CARTESIAN_POINT('Ctrl Pts',(-60.9683904781941,-1.87870515229034,
135.351712779346));
#88702=CARTESIAN_POINT('Ctrl Pts',(-60.9761552311412,-1.75070352557956,
135.400469866488));
#88703=CARTESIAN_POINT('Ctrl Pts',(-60.9839122720262,-1.62282903188912,
135.449178527403));
#88704=CARTESIAN_POINT('Ctrl Pts',(-60.9916693129111,-1.49278655136236,
135.492597403677));
#88705=CARTESIAN_POINT('Ctrl Pts',(-60.9994263537961,-1.36105352407415,
135.530534161471));
#88706=CARTESIAN_POINT('Ctrl Pts',(-61.0071775450362,-1.22941983768637,
135.568442310861));
#88707=CARTESIAN_POINT('Ctrl Pts',(-61.0149287362764,-1.09609851623398,
135.600876462706));
#88708=CARTESIAN_POINT('Ctrl Pts',(-61.0226799275165,-0.96158455958484,
135.6276933033));
#88709=CARTESIAN_POINT('Ctrl Pts',(-61.0304278242936,-0.827127774955552,
135.654498746021));
#88710=CARTESIAN_POINT('Ctrl Pts',(-61.0381757210708,-0.691479745935739,
135.67569154978));
#88711=CARTESIAN_POINT('Ctrl Pts',(-61.0459236178479,-0.555147920088452,
135.691178994519));
#88712=CARTESIAN_POINT('Ctrl Pts',(-61.053669893932,-0.418844611920158,
135.706663199618));
#88713=CARTESIAN_POINT('Ctrl Pts',(-61.061416170016,-0.281858179650459,
135.716444375408));
#88714=CARTESIAN_POINT('Ctrl Pts',(-61.0691624461001,-0.144703095944134,
135.720481453807));
#88715=CARTESIAN_POINT('Ctrl Pts',(-61.0769087793655,-0.00754699979032486,
135.724518562007));
#88716=CARTESIAN_POINT('Ctrl Pts',(-61.0846551126309,0.129777359488358,
135.722811476705));
#88717=CARTESIAN_POINT('Ctrl Pts',(-61.0924014458962,0.266753989730087,
135.715371243849));
#88718=CARTESIAN_POINT('Ctrl Pts',(-61.1001495138992,0.403761294938243,
135.707929344805));
#88719=CARTESIAN_POINT('Ctrl Pts',(-61.1078975819022,0.540420325839154,
135.694751764598));
#88720=CARTESIAN_POINT('Ctrl Pts',(-61.1156456499051,0.676219094123127,
135.675901523608));
#88721=CARTESIAN_POINT('Ctrl Pts',(-61.123401952647,0.812162190954428,135.657031248358));
#88722=CARTESIAN_POINT('Ctrl Pts',(-61.1311582553888,0.947242810891693,
135.632476322644));
#88723=CARTESIAN_POINT('Ctrl Pts',(-61.1389145581307,1.08095750993771,135.602351230751));
#88724=CARTESIAN_POINT('Ctrl Pts',(-61.1466750006449,1.21474357654487,135.572210060189));
#88725=CARTESIAN_POINT('Ctrl Pts',(-61.1544354431591,1.34716189231044,135.53649290133));
#88726=CARTESIAN_POINT('Ctrl Pts',(-61.1621958856732,1.47772407188877,135.495364202073));
#88727=CARTESIAN_POINT('Ctrl Pts',(-61.1699687859387,1.60849584146835,135.454169479377));
#88728=CARTESIAN_POINT('Ctrl Pts',(-61.1777416862041,1.73740515273237,135.407545989768));
#88729=CARTESIAN_POINT('Ctrl Pts',(-61.1855145864695,1.8639826666933,135.355706756981));
#88730=CARTESIAN_POINT('Ctrl Pts',(-61.1930049222315,1.98595876919103,135.305752010881));
#88731=CARTESIAN_POINT('Ctrl Pts',(-61.2004952579934,2.10576938433685,135.250954276866));
#88732=CARTESIAN_POINT('Ctrl Pts',(-61.2079855937554,2.22301778092754,135.191543655482));
#88733=CARTESIAN_POINT('Ctrl Pts',(-61.2157599278745,2.34471168611271,135.129880462331));
#88734=CARTESIAN_POINT('Ctrl Pts',(-61.2235342619936,2.46403073401666,135.063052351033));
#88735=CARTESIAN_POINT('Ctrl Pts',(-61.2313085961127,2.58050545774597,134.991265756812));
#88736=CARTESIAN_POINT('Ctrl Pts',(-61.2390733490598,2.69683663678778,134.919567633153));
#88737=CARTESIAN_POINT('Ctrl Pts',(-61.2468381020068,2.81033013667362,134.842923388576));
#88738=CARTESIAN_POINT('Ctrl Pts',(-61.2546028549539,2.92053886080871,134.761586391389));
#88739=CARTESIAN_POINT('Ctrl Pts',(-61.2623598958389,3.03063812408547,134.680330179253));
#88740=CARTESIAN_POINT('Ctrl Pts',(-61.2701169367239,3.13745879156984,134.594390720583));
#88741=CARTESIAN_POINT('Ctrl Pts',(-61.2778739776089,3.24058097933402,134.504065738096));
#88742=CARTESIAN_POINT('Ctrl Pts',(-61.285625168849,3.34362540185424,134.413808870382));
#88743=CARTESIAN_POINT('Ctrl Pts',(-61.2933763600892,3.44297660318405,134.319173318109));
#88744=CARTESIAN_POINT('Ctrl Pts',(-61.3011275513293,3.53824644992244,134.220498074126));
#88745=CARTESIAN_POINT('Ctrl Pts',(-61.3088754481064,3.63347580443455,134.121864769753));
#88746=CARTESIAN_POINT('Ctrl Pts',(-61.3166233448835,3.72462698352099,134.019195469282));
#88747=CARTESIAN_POINT('Ctrl Pts',(-61.3243712416605,3.81134769136716,133.912866985263));
#88748=CARTESIAN_POINT('Ctrl Pts',(-61.3321175177446,3.89805025911073,133.806560742869));
#88749=CARTESIAN_POINT('Ctrl Pts',(-61.3398637938287,3.98032395204148,133.696597142177));
#88750=CARTESIAN_POINT('Ctrl Pts',(-61.3476100699127,4.05785613337724,133.583386825307));
#88751=CARTESIAN_POINT('Ctrl Pts',(-61.3553564031781,4.13538888703794,133.470175672745));
#88752=CARTESIAN_POINT('Ctrl Pts',(-61.3631027364434,4.20817983834974,133.353718078752));
#88753=CARTESIAN_POINT('Ctrl Pts',(-61.3708490697087,4.27595937421572,133.234454132754));
#88754=CARTESIAN_POINT('Ctrl Pts',(-61.3785971377117,4.34375408883881,133.115163478421));
#88755=CARTESIAN_POINT('Ctrl Pts',(-61.3863452057147,4.4065349616874,132.993065561358));
#88756=CARTESIAN_POINT('Ctrl Pts',(-61.3940932737177,4.4640782714028,132.868625195882));
#88757=CARTESIAN_POINT('Ctrl Pts',(-61.4018495764595,4.52168273883254,132.744052573704));
#88758=CARTESIAN_POINT('Ctrl Pts',(-61.4096058792014,4.57403835900126,132.617132885334));
#88759=CARTESIAN_POINT('Ctrl Pts',(-61.4173621819433,4.62096932700243,132.488351574015));
#88760=CARTESIAN_POINT('Ctrl Pts',(-61.4251226244574,4.66792534347429,132.359501528233));
#88761=CARTESIAN_POINT('Ctrl Pts',(-61.4328830669716,4.70945082033221,132.228788252095));
#88762=CARTESIAN_POINT('Ctrl Pts',(-61.4406435094857,4.74542012804259,132.096711526131));
#88763=CARTESIAN_POINT('Ctrl Pts',(-61.4484164097512,4.7814471768789,131.964422778881));
#88764=CARTESIAN_POINT('Ctrl Pts',(-61.4561893100165,4.81190014614841,131.830766589437));
#88765=CARTESIAN_POINT('Ctrl Pts',(-61.4639622102819,4.83670456956486,131.696252970516));
#88766=CARTESIAN_POINT('Ctrl Pts',(-61.471452546044,4.86060728971179,131.56662926046));
#88767=CARTESIAN_POINT('Ctrl Pts',(-61.4789428818062,4.87926496815599,131.436209682978));
#88768=CARTESIAN_POINT('Ctrl Pts',(-61.4864332175682,4.89265675209853,131.305452394234));
#88769=CARTESIAN_POINT('Ctrl Pts',(-61.4942075516873,4.90655628959947,131.169737403146));
#88770=CARTESIAN_POINT('Ctrl Pts',(-61.5019818858064,4.91482676681583,131.033228682329));
#88771=CARTESIAN_POINT('Ctrl Pts',(-61.5097562199255,4.91738810522468,130.896432790858));
#88772=CARTESIAN_POINT('Ctrl Pts',(-61.5175209728726,4.91994628701287,130.759805488098));
#88773=CARTESIAN_POINT('Ctrl Pts',(-61.5252857258198,4.91680932229427,130.622892106008));
#88774=CARTESIAN_POINT('Ctrl Pts',(-61.5330504787669,4.90794871036947,130.486205751372));
#88775=CARTESIAN_POINT('Ctrl Pts',(-61.5408075196518,4.89909689892936,130.349655155552));
#88776=CARTESIAN_POINT('Ctrl Pts',(-61.5485645605368,4.88453277843306,130.213331526079));
#88777=CARTESIAN_POINT('Ctrl Pts',(-61.5563216014218,4.86427987391699,130.077749049597));
#88778=CARTESIAN_POINT('Ctrl Pts',(-61.5640727926619,4.84404224227374,129.942268816915));
#88779=CARTESIAN_POINT('Ctrl Pts',(-61.5718239839022,4.81812442303516,129.807529009858));
#88780=CARTESIAN_POINT('Ctrl Pts',(-61.5795751751423,4.78660182490122,129.674039409965));
#88781=CARTESIAN_POINT('Ctrl Pts',(-61.5873230719194,4.75509262471238,129.540606546713));
#88782=CARTESIAN_POINT('Ctrl Pts',(-61.5950709686964,4.71798347326789,129.40842321347));
#88783=CARTESIAN_POINT('Ctrl Pts',(-61.6028188654734,4.67540096914463,129.27798948307));
#88784=CARTESIAN_POINT('Ctrl Pts',(-61.6105651415575,4.63282737236327,129.147583036595));
#88785=CARTESIAN_POINT('Ctrl Pts',(-61.6183114176416,4.58478282144526,129.018925836436));
#88786=CARTESIAN_POINT('Ctrl Pts',(-61.6260576937257,4.53144381342069,128.892502874869));
#88787=CARTESIAN_POINT('Ctrl Pts',(-61.633804026991,4.47810441165976,128.766078980076));
#88788=CARTESIAN_POINT('Ctrl Pts',(-61.6415503602565,4.41947062678487,128.641889717003));
#88789=CARTESIAN_POINT('Ctrl Pts',(-61.6492966935218,4.35576698602873,128.520399797867));
#88790=CARTESIAN_POINT('Ctrl Pts',(-61.6570447615248,4.29204907928385,128.398882671905));
#88791=CARTESIAN_POINT('Ctrl Pts',(-61.6647928295278,4.22325923894819,128.280066438951));
#88792=CARTESIAN_POINT('Ctrl Pts',(-61.6725408975308,4.14966759961328,128.164390565611));
#88793=CARTESIAN_POINT('Ctrl Pts',(-61.6802972002726,4.07599774620843,128.048591750577));
#88794=CARTESIAN_POINT('Ctrl Pts',(-61.6880535030144,3.99751610938801,127.93594029279));
#88795=CARTESIAN_POINT('Ctrl Pts',(-61.6958098057562,3.91453607945671,127.826846495831));
#88796=CARTESIAN_POINT('Ctrl Pts',(-61.7035702482704,3.83151176058484,127.717694472227));
#88797=CARTESIAN_POINT('Ctrl Pts',(-61.7113306907846,3.74398451393526,127.612104193882));
#88798=CARTESIAN_POINT('Ctrl Pts',(-61.7190911332987,3.65230691319044,127.510451500064));
#88799=CARTESIAN_POINT('Ctrl Pts',(-61.7268640335642,3.56048214342215,127.408635624318));
#88800=CARTESIAN_POINT('Ctrl Pts',(-61.7346369338296,3.46449397964875,127.310770243671));
#88801=CARTESIAN_POINT('Ctrl Pts',(-61.7424098340951,3.36473125916445,127.217193683048));
#88802=CARTESIAN_POINT('Ctrl Pts',(-61.7499001698571,3.26859516485716,127.127018866109));
#88803=CARTESIAN_POINT('Ctrl Pts',(-61.7573905056191,3.16895441158675,127.040826665518));
#88804=CARTESIAN_POINT('Ctrl Pts',(-61.7648808413811,3.06618318766209,126.958882269922));
#88805=CARTESIAN_POINT('Ctrl Pts',(-61.7726551755002,2.95951536154539,126.873830927661));
#88806=CARTESIAN_POINT('Ctrl Pts',(-61.7804295096194,2.84913710354739,126.793086442934));
#88807=CARTESIAN_POINT('Ctrl Pts',(-61.7882038437384,2.73543131176619,126.716989995625));
#88808=CARTESIAN_POINT('Ctrl Pts',(-61.7959685966855,2.62186565221118,126.640987330385));
#88809=CARTESIAN_POINT('Ctrl Pts',(-61.8037333496326,2.50498094021496,126.569621520331));
#88810=CARTESIAN_POINT('Ctrl Pts',(-61.8114981025797,2.38519346172388,126.503193890659));
#88811=CARTESIAN_POINT('Ctrl Pts',(-61.8192551434647,2.26552495784531,126.436832237845));
#88812=CARTESIAN_POINT('Ctrl Pts',(-61.8270121843497,2.14295976460758,126.375399193277));
#88813=CARTESIAN_POINT('Ctrl Pts',(-61.8347692252347,2.01794319765212,126.319152895113));
#88814=CARTESIAN_POINT('Ctrl Pts',(-61.8425204164749,1.8930209066623,126.262949012721));
#88815=CARTESIAN_POINT('Ctrl Pts',(-61.850271607715,1.76565127657975,126.21192425116));
#88816=CARTESIAN_POINT('Ctrl Pts',(-61.8580227989551,1.6363039612941,126.16629071633));
#88817=CARTESIAN_POINT('Ctrl Pts',(-61.8657706957322,1.5070116220679,126.120676576969));
#88818=CARTESIAN_POINT('Ctrl Pts',(-61.8735185925092,1.37574363738721,126.08044923669));
#88819=CARTESIAN_POINT('Ctrl Pts',(-61.8812664892863,1.24298916231292,126.045772486106));
#88820=CARTESIAN_POINT('Ctrl Pts',(-61.8890127653704,1.11026245661296,126.011102989151));
#88821=CARTESIAN_POINT('Ctrl Pts',(-61.8967590414545,0.976050257033153,
125.981981871217));
#88822=CARTESIAN_POINT('Ctrl Pts',(-61.9045053175386,0.840856002267571,
125.958522790528));
#88823=CARTESIAN_POINT('Ctrl Pts',(-61.912251650804,0.705660749528713,125.935063536669));
#88824=CARTESIAN_POINT('Ctrl Pts',(-61.9199979840693,0.56948381234757,125.917266470297));
#88825=CARTESIAN_POINT('Ctrl Pts',(-61.9277443173346,0.432837528728403,
125.905193878597));
#88826=CARTESIAN_POINT('Ctrl Pts',(-61.9354923853376,0.296160644121458,
125.893118583323));
#88827=CARTESIAN_POINT('Ctrl Pts',(-61.9432404533407,0.15901459329965,125.886770348067));
#88828=CARTESIAN_POINT('Ctrl Pts',(-61.9509885213436,0.0219151263119513,
125.886159443383));
#88829=CARTESIAN_POINT('Ctrl Pts',(-61.9587448240855,-0.115330051620767,
125.885547889421));
#88830=CARTESIAN_POINT('Ctrl Pts',(-61.9665011268274,-0.252528155233385,
125.890685848596));
#88831=CARTESIAN_POINT('Ctrl Pts',(-61.9742574295692,-0.389164589390033,
125.901531435873));
#88832=CARTESIAN_POINT('Ctrl Pts',(-61.9820178720834,-0.525873950525634,
125.912382811766));
#88833=CARTESIAN_POINT('Ctrl Pts',(-61.9897783145975,-0.662020656955246,
125.928947838641));
#88834=CARTESIAN_POINT('Ctrl Pts',(-61.9975387571116,-0.797097929770319,
125.951133036579));
#88835=CARTESIAN_POINT('Ctrl Pts',(-62.0053116573771,-0.932392040615496,
125.973353848165));
#88836=CARTESIAN_POINT('Ctrl Pts',(-62.0130845576424,-1.06661290420646,
126.001212780139));
#88837=CARTESIAN_POINT('Ctrl Pts',(-62.0208574579079,-1.19926570214619,
126.034565565558));
#88838=CARTESIAN_POINT('Ctrl Pts',(-62.0283477936699,-1.32709623674894,
126.066705893217));
#88839=CARTESIAN_POINT('Ctrl Pts',(-62.035838129432,-1.45347043720029,126.103947491135));
#88840=CARTESIAN_POINT('Ctrl Pts',(-62.0433284651941,-1.57796293485931,
126.146118885033));
#88841=CARTESIAN_POINT('Ctrl Pts',(-62.0511028340312,-1.70717618043334,
126.189889415614));
#88842=CARTESIAN_POINT('Ctrl Pts',(-62.0588772028683,-1.8347715093924,126.239109648032));
#88843=CARTESIAN_POINT('Ctrl Pts',(-62.0666515717054,-1.96025490507105,
126.293641853373));
#88844=CARTESIAN_POINT('Ctrl Pts',(-62.0744163512153,-2.08558352273938,
126.348106795741));
#88845=CARTESIAN_POINT('Ctrl Pts',(-62.0821811307252,-2.2088050351323,126.407870519972));
#88846=CARTESIAN_POINT('Ctrl Pts',(-62.0899459102351,-2.32944091129757,
126.47274566431));
#88847=CARTESIAN_POINT('Ctrl Pts',(-62.097702969562,-2.44995684445031,126.537556306109));
#88848=CARTESIAN_POINT('Ctrl Pts',(-62.1054600288888,-2.56789191527144,
126.607468070453));
#88849=CARTESIAN_POINT('Ctrl Pts',(-62.1132170882156,-2.68278823776849,
126.682245828554));
#88850=CARTESIAN_POINT('Ctrl Pts',(-62.1209682898026,-2.79759779635957,
126.756967118265));
#88851=CARTESIAN_POINT('Ctrl Pts',(-62.1287194913898,-2.9093728477812,126.836546875309));
#88852=CARTESIAN_POINT('Ctrl Pts',(-62.1364706929768,-3.01768108050096,
126.920704613375));
#88853=CARTESIAN_POINT('Ctrl Pts',(-62.144218557716,-3.12594268714839,127.004826122019));
#88854=CARTESIAN_POINT('Ctrl Pts',(-62.1519664224551,-3.23074013560302,
127.093521452251));
#88855=CARTESIAN_POINT('Ctrl Pts',(-62.1597142871944,-3.33167122921823,
127.186467600505));
#88856=CARTESIAN_POINT('Ctrl Pts',(-62.167460519711,-3.43258105994205,127.279394168035));
#88857=CARTESIAN_POINT('Ctrl Pts',(-62.1752067522277,-3.52962586860398,
127.376569507626));
#88858=CARTESIAN_POINT('Ctrl Pts',(-62.1829529847444,-3.62243791678548,
127.477631503025));
#88859=CARTESIAN_POINT('Ctrl Pts',(-62.1906992629046,-3.71525051184835,
127.578694093917));
#88860=CARTESIAN_POINT('Ctrl Pts',(-62.1984455410648,-3.80383003225941,
127.683643098332));
#88861=CARTESIAN_POINT('Ctrl Pts',(-62.206191819225,-3.88784714979851,127.792081148077));
#88862=CARTESIAN_POINT('Ctrl Pts',(-62.213939820567,-3.97188295718589,127.900543320177));
#88863=CARTESIAN_POINT('Ctrl Pts',(-62.221687821909,-4.05135410281197,128.012495773005));
#88864=CARTESIAN_POINT('Ctrl Pts',(-62.229435823251,-4.12597317726844,128.127510154249));
#88865=CARTESIAN_POINT('Ctrl Pts',(-62.2371918970811,-4.20066999585148,
128.242644366684));
#88866=CARTESIAN_POINT('Ctrl Pts',(-62.2449479709113,-4.27050443231383,
128.360846551381));
#88867=CARTESIAN_POINT('Ctrl Pts',(-62.2527040447415,-4.33523359464394,
128.481661165986));
#88868=CARTESIAN_POINT('Ctrl Pts',(-62.2604642535788,-4.39999726612839,
128.602540190666));
#88869=CARTESIAN_POINT('Ctrl Pts',(-62.2682244624161,-4.45965007018302,
128.72603406863));
#88870=CARTESIAN_POINT('Ctrl Pts',(-62.2759846712534,-4.51399674250588,
128.85166594836));
#88871=CARTESIAN_POINT('Ctrl Pts',(-62.283756953163,-4.56842796555643,128.977493281949));
#88872=CARTESIAN_POINT('Ctrl Pts',(-62.2915292350726,-4.61753642212146,
129.105464898438));
#88873=CARTESIAN_POINT('Ctrl Pts',(-62.2993015169822,-4.66117605574161,
129.235086632603));
#88874=CARTESIAN_POINT('Ctrl Pts',(-62.306174702148,-4.69976746119073,129.349713738361));
#88875=CARTESIAN_POINT('Ctrl Pts',(-62.3130478873137,-4.73408281986375,
129.465630883257));
#88876=CARTESIAN_POINT('Ctrl Pts',(-62.3199210724795,-4.76405452823405,
129.582490119308));
#88877=CARTESIAN_POINT('Origin',(213.235140564004,0.,130.804360617566));
#88878=CARTESIAN_POINT('',(-64.4150295539547,-4.76405452823403,129.582490119308));
#88879=CARTESIAN_POINT('',(-64.0701225287273,-4.76405452823399,129.582490119308));
#88880=CARTESIAN_POINT('',(213.235140564004,-4.76405452823405,129.582490119308));
#88881=CARTESIAN_POINT('',(-62.7351405640401,-4.91824977962896,130.805832921769));
#88882=CARTESIAN_POINT('Ctrl Pts',(-62.7351405640401,-4.91824977962896,
130.805832921769));
#88883=CARTESIAN_POINT('Ctrl Pts',(-62.7434671272577,-4.9182055325362,130.953640863794));
#88884=CARTESIAN_POINT('Ctrl Pts',(-62.7517936904754,-4.91149398221606,
131.101259344452));
#88885=CARTESIAN_POINT('Ctrl Pts',(-62.760120253693,-4.89819140610862,131.24809929249));
#88886=CARTESIAN_POINT('Ctrl Pts',(-62.7684782995291,-4.8848385331479,131.395494440308));
#88887=CARTESIAN_POINT('Ctrl Pts',(-62.7768363453653,-4.8648447801471,131.542104870886));
#88888=CARTESIAN_POINT('Ctrl Pts',(-62.7851943912014,-4.83833812578196,
131.687348297607));
#88889=CARTESIAN_POINT('Ctrl Pts',(-62.7935681368434,-4.81178168115064,
131.832864550494));
#88890=CARTESIAN_POINT('Ctrl Pts',(-62.8019418824853,-4.77868796388197,
131.977008386601));
#88891=CARTESIAN_POINT('Ctrl Pts',(-62.8103156281273,-4.73923506913203,
132.119211948329));
#88892=CARTESIAN_POINT('Ctrl Pts',(-62.8187159994217,-4.69965672764547,
132.261867668837));
#88893=CARTESIAN_POINT('Ctrl Pts',(-62.8271163707161,-4.6536788351441,132.402570489922));
#88894=CARTESIAN_POINT('Ctrl Pts',(-62.8355167420105,-4.6015289851969,132.540768997209));
#88895=CARTESIAN_POINT('Ctrl Pts',(-62.843371941498,-4.55276358421359,132.669998623563));
#88896=CARTESIAN_POINT('Ctrl Pts',(-62.8512271409856,-4.49860188638689,
132.797038484982));
#88897=CARTESIAN_POINT('Ctrl Pts',(-62.8590823404731,-4.43926593480472,
132.921457928174));
#88898=CARTESIAN_POINT('Ctrl Pts',(-62.8668566745922,-4.3805408173069,133.044596535133));
#88899=CARTESIAN_POINT('Ctrl Pts',(-62.8746310087113,-4.31659527900452,
133.165484912506));
#88900=CARTESIAN_POINT('Ctrl Pts',(-62.8824053428304,-4.24762442976221,
133.283648774717));
#88901=CARTESIAN_POINT('Ctrl Pts',(-62.8901700957775,-4.17873858092748,
133.401667010528));
#88902=CARTESIAN_POINT('Ctrl Pts',(-62.8979348487247,-4.10483993906106,
133.516967077629));
#88903=CARTESIAN_POINT('Ctrl Pts',(-62.9056996016718,-4.02617107041891,
133.629095928037));
#88904=CARTESIAN_POINT('Ctrl Pts',(-62.9134566425568,-3.94758033680614,
133.74111341049));
#88905=CARTESIAN_POINT('Ctrl Pts',(-62.9212136834419,-3.86422902805879,
133.849965626309));
#88906=CARTESIAN_POINT('Ctrl Pts',(-62.9289707243269,-3.77640470510279,
133.955225667957));
#88907=CARTESIAN_POINT('Ctrl Pts',(-62.936721915567,-3.68864661115214,134.06040633219));
#88908=CARTESIAN_POINT('Ctrl Pts',(-62.9444731068072,-3.59642246647058,
134.161999915144));
#88909=CARTESIAN_POINT('Ctrl Pts',(-62.9522242980474,-3.50006185215328,
134.259610260298));
#88910=CARTESIAN_POINT('Ctrl Pts',(-62.9599721948245,-3.40374219366731,
134.357179118452));
#88911=CARTESIAN_POINT('Ctrl Pts',(-62.9677200916015,-3.30328983638444,
134.450767828373));
#88912=CARTESIAN_POINT('Ctrl Pts',(-62.9754679883787,-3.19907303021354,
134.540015153234));
#88913=CARTESIAN_POINT('Ctrl Pts',(-62.9832142644628,-3.09487802395183,
134.62924380948));
#88914=CARTESIAN_POINT('Ctrl Pts',(-62.9909605405468,-2.98692043183581,
134.714132632834));
#88915=CARTESIAN_POINT('Ctrl Pts',(-62.998706816631,-2.87560327531221,134.794359222267));
#88916=CARTESIAN_POINT('Ctrl Pts',(-63.0064531498964,-2.76428529707065,
134.874586403914));
#88917=CARTESIAN_POINT('Ctrl Pts',(-63.0141994831618,-2.64960802211177,
134.950151054378));
#88918=CARTESIAN_POINT('Ctrl Pts',(-63.0219458164272,-2.53200494315482,
135.020773077269));
#88919=CARTESIAN_POINT('Ctrl Pts',(-63.0296938844302,-2.41437552780391,
135.091410915473));
#88920=CARTESIAN_POINT('Ctrl Pts',(-63.0374419524331,-2.29381933976595,
135.15710372233));
#88921=CARTESIAN_POINT('Ctrl Pts',(-63.0451900204361,-2.17079569080896,
135.217616686645));
#88922=CARTESIAN_POINT('Ctrl Pts',(-63.052946323178,-2.04764129085369,135.278193964859));
#88923=CARTESIAN_POINT('Ctrl Pts',(-63.0607026259199,-1.92201454274061,
135.333580230468));
#88924=CARTESIAN_POINT('Ctrl Pts',(-63.0684589286618,-1.7943965310866,135.383588079892));
#88925=CARTESIAN_POINT('Ctrl Pts',(-63.076219371176,-1.66671040585743,135.433622620012));
#88926=CARTESIAN_POINT('Ctrl Pts',(-63.0839798136902,-1.53703126885931,
135.478272896769));
#88927=CARTESIAN_POINT('Ctrl Pts',(-63.0917402562044,-1.40585574193498,
135.517401323455));
#88928=CARTESIAN_POINT('Ctrl Pts',(-63.0995131564698,-1.27446964040944,
135.556592562565));
#88929=CARTESIAN_POINT('Ctrl Pts',(-63.1072860567353,-1.14158272794049,
135.590244142148));
#88930=CARTESIAN_POINT('Ctrl Pts',(-63.1150589570007,-1.00770308338584,
135.618269378462));
#88931=CARTESIAN_POINT('Ctrl Pts',(-63.1225492927625,-0.87869030113794,
135.645275826844));
#88932=CARTESIAN_POINT('Ctrl Pts',(-63.1300396285242,-0.748756014115618,
135.667057842591));
#88933=CARTESIAN_POINT('Ctrl Pts',(-63.137529964286,-0.618357746135029,
135.683583584422));
#88934=CARTESIAN_POINT('Ctrl Pts',(-63.1453042984051,-0.483015388185867,
135.700735904778));
#88935=CARTESIAN_POINT('Ctrl Pts',(-63.1530786325242,-0.346744447157127,
135.712279833206));
#88936=CARTESIAN_POINT('Ctrl Pts',(-63.1608529666433,-0.210049414582917,
135.71812315822));
#88937=CARTESIAN_POINT('Ctrl Pts',(-63.1686177195904,-0.0735228464197539,
135.723959281858));
#88938=CARTESIAN_POINT('Ctrl Pts',(-63.1763824725374,0.063426386502673,
135.724108764167));
#88939=CARTESIAN_POINT('Ctrl Pts',(-63.1841472254845,0.200286009099147,
135.718530799505));
#88940=CARTESIAN_POINT('Ctrl Pts',(-63.1919042663694,0.337009700789261,
135.712958374956));
#88941=CARTESIAN_POINT('Ctrl Pts',(-63.1996613072545,0.473643571158825,
135.701669839789));
#88942=CARTESIAN_POINT('Ctrl Pts',(-63.2074183481395,0.609673017102681,
135.684676373203));
#88943=CARTESIAN_POINT('Ctrl Pts',(-63.2151695393796,0.745599882183011,
135.667695721522));
#88944=CARTESIAN_POINT('Ctrl Pts',(-63.2229207306197,0.880922843702231,
135.645018749826));
#88945=CARTESIAN_POINT('Ctrl Pts',(-63.2306719218598,1.01513045732638,135.616708611748));
#88946=CARTESIAN_POINT('Ctrl Pts',(-63.2384198186369,1.14928102913481,135.588410506234));
#88947=CARTESIAN_POINT('Ctrl Pts',(-63.246167715414,1.28231681415679,135.554484076837));
#88948=CARTESIAN_POINT('Ctrl Pts',(-63.2539156121911,1.41373484555055,135.515043885307));
#88949=CARTESIAN_POINT('Ctrl Pts',(-63.2616618882752,1.54512538712519,135.475611943815));
#88950=CARTESIAN_POINT('Ctrl Pts',(-63.2694081643592,1.67489847393822,135.430668646598));
#88951=CARTESIAN_POINT('Ctrl Pts',(-63.2771544404433,1.80256501793662,135.380378801382));
#88952=CARTESIAN_POINT('Ctrl Pts',(-63.2849007737086,1.93023250434044,135.330088584937));
#88953=CARTESIAN_POINT('Ctrl Pts',(-63.292647106974,2.05579305314045,135.27445188503));
#88954=CARTESIAN_POINT('Ctrl Pts',(-63.3003934402393,2.17877669790947,135.213682012423));
#88955=CARTESIAN_POINT('Ctrl Pts',(-63.3081415082423,2.30178788401303,135.152898530825));
#88956=CARTESIAN_POINT('Ctrl Pts',(-63.3158895762454,2.42222066732166,135.086979762243));
#88957=CARTESIAN_POINT('Ctrl Pts',(-63.3236376442484,2.5396292252973,135.016185217489));
#88958=CARTESIAN_POINT('Ctrl Pts',(-63.3313939469902,2.65716256648553,134.94531543145));
#88959=CARTESIAN_POINT('Ctrl Pts',(-63.3391502497319,2.7716649263213,134.869559719775));
#88960=CARTESIAN_POINT('Ctrl Pts',(-63.3469065524738,2.88271859887994,134.789221536365));
#88961=CARTESIAN_POINT('Ctrl Pts',(-63.3546669949879,2.99383154412738,134.708840474047));
#88962=CARTESIAN_POINT('Ctrl Pts',(-63.3624274375021,3.10149182766155,134.623872308619));
#88963=CARTESIAN_POINT('Ctrl Pts',(-63.3701878800163,3.20531525764995,134.534660493122));
#88964=CARTESIAN_POINT('Ctrl Pts',(-63.3779607802817,3.30930535422517,134.4453054669));
#88965=CARTESIAN_POINT('Ctrl Pts',(-63.3857336805471,3.40944600332291,134.351693444638));
#88966=CARTESIAN_POINT('Ctrl Pts',(-63.3935065808125,3.50538964642401,134.254205032789));
#88967=CARTESIAN_POINT('Ctrl Pts',(-63.4009969165746,3.5978454964321,134.160260570268));
#88968=CARTESIAN_POINT('Ctrl Pts',(-63.4084872523367,3.68640397913906,134.062716886227));
#88969=CARTESIAN_POINT('Ctrl Pts',(-63.4159775880989,3.77079100277721,133.961941697424));
#88970=CARTESIAN_POINT('Ctrl Pts',(-63.423751922218,3.85837758606461,133.857345586707));
#88971=CARTESIAN_POINT('Ctrl Pts',(-63.4315262563371,3.94174759222032,133.748936759917));
#88972=CARTESIAN_POINT('Ctrl Pts',(-63.4393005904562,4.02055075111479,133.637089817509));
#88973=CARTESIAN_POINT('Ctrl Pts',(-63.4470653434033,4.09925679215876,133.525380716462));
#88974=CARTESIAN_POINT('Ctrl Pts',(-63.4548300963504,4.17340696142413,133.410242247039));
#88975=CARTESIAN_POINT('Ctrl Pts',(-63.4625948492975,4.24269003077375,133.292083344333));
#88976=CARTESIAN_POINT('Ctrl Pts',(-63.4703518901825,4.31190428720207,133.174041798715));
#88977=CARTESIAN_POINT('Ctrl Pts',(-63.4781089310675,4.37626086726032,133.052986124905));
#88978=CARTESIAN_POINT('Ctrl Pts',(-63.4858659719525,4.43549102077797,132.9293553157));
#88979=CARTESIAN_POINT('Ctrl Pts',(-63.4936171631926,4.49467650837611,132.80581773745));
#88980=CARTESIAN_POINT('Ctrl Pts',(-63.5013683544327,4.54874309599145,132.679709240261));
#88981=CARTESIAN_POINT('Ctrl Pts',(-63.5091195456729,4.5974674684087,132.551494252817));
#88982=CARTESIAN_POINT('Ctrl Pts',(-63.5168674424499,4.64617113166797,132.423333760162));
#88983=CARTESIAN_POINT('Ctrl Pts',(-63.524615339227,4.68953695715384,132.293068922665));
#88984=CARTESIAN_POINT('Ctrl Pts',(-63.5323632360041,4.72738946304791,132.161184823999));
#88985=CARTESIAN_POINT('Ctrl Pts',(-63.5401095120882,4.76523405101375,132.029328312644));
#88986=CARTESIAN_POINT('Ctrl Pts',(-63.5478557881724,4.79756750551092,131.895853589396));
#88987=CARTESIAN_POINT('Ctrl Pts',(-63.5556020642565,4.82426411990756,131.761261220488));
#88988=CARTESIAN_POINT('Ctrl Pts',(-63.5633483975218,4.85096093137253,131.62666785805));
#88989=CARTESIAN_POINT('Ctrl Pts',(-63.5710947307872,4.87202074364083,131.490957216983));
#88990=CARTESIAN_POINT('Ctrl Pts',(-63.5788410640526,4.88736899276481,131.35463999303));
#88991=CARTESIAN_POINT('Ctrl Pts',(-63.5865891320555,4.90272067902274,131.21829224178));
#88992=CARTESIAN_POINT('Ctrl Pts',(-63.5943372000585,4.91235821321032,131.081338025775));
#88993=CARTESIAN_POINT('Ctrl Pts',(-63.6020852680615,4.91625895115228,130.944292700074));
#88994=CARTESIAN_POINT('Ctrl Pts',(-63.6098415708034,4.92016383484496,130.80710172097));
#88995=CARTESIAN_POINT('Ctrl Pts',(-63.6175978735453,4.91831973146611,130.669819830168));
#88996=CARTESIAN_POINT('Ctrl Pts',(-63.6253541762871,4.910756165122,130.532962479738));
#88997=CARTESIAN_POINT('Ctrl Pts',(-63.6331146188013,4.90318856187479,130.39603208442));
#88998=CARTESIAN_POINT('Ctrl Pts',(-63.6408750613154,4.88989545087465,130.259527069908));
#88999=CARTESIAN_POINT('Ctrl Pts',(-63.6486355038296,4.87095812382458,130.12395631243));
#89000=CARTESIAN_POINT('Ctrl Pts',(-63.656408404095,4.85199039689594,129.988167924738));
#89001=CARTESIAN_POINT('Ctrl Pts',(-63.6641813043605,4.82736041824475,129.853317175887));
#89002=CARTESIAN_POINT('Ctrl Pts',(-63.6719542046259,4.79720053899032,129.719902203789));
#89003=CARTESIAN_POINT('Ctrl Pts',(-63.6794445403879,4.76813704731518,129.59133720198));
#89004=CARTESIAN_POINT('Ctrl Pts',(-63.6869348761499,4.73393880641623,129.464105698514));
#89005=CARTESIAN_POINT('Ctrl Pts',(-63.6944252119119,4.69476703351866,129.338637054446));
#89006=CARTESIAN_POINT('Ctrl Pts',(-63.7021995460309,4.65411005094539,129.208411228601));
#89007=CARTESIAN_POINT('Ctrl Pts',(-63.7099738801501,4.60796615942195,129.079672062348));
#89008=CARTESIAN_POINT('Ctrl Pts',(-63.7177482142692,4.55646119136074,128.952916728564));
#89009=CARTESIAN_POINT('Ctrl Pts',(-63.7255129672163,4.50501969856954,128.8263176094));
#89010=CARTESIAN_POINT('Ctrl Pts',(-63.7332777201633,4.44823042105971,128.701697816819));
#89011=CARTESIAN_POINT('Ctrl Pts',(-63.7410424731104,4.38626918109586,128.579540235272));
#89012=CARTESIAN_POINT('Ctrl Pts',(-63.7487995139954,4.32436948190903,128.457503982358));
#89013=CARTESIAN_POINT('Ctrl Pts',(-63.7565565548804,4.25730821857601,128.337925420239));
#89014=CARTESIAN_POINT('Ctrl Pts',(-63.7643135957654,4.18530946213846,128.221267942373));
#89015=CARTESIAN_POINT('Ctrl Pts',(-63.7720647870055,4.1133650005232,128.10469843682));
#89016=CARTESIAN_POINT('Ctrl Pts',(-63.7798159782456,4.03649066151548,127.991045962311));
#89017=CARTESIAN_POINT('Ctrl Pts',(-63.7875671694858,3.95495647479197,127.880749435312));
#89018=CARTESIAN_POINT('Ctrl Pts',(-63.7953150662628,3.87345694227282,127.770499787279));
#89019=CARTESIAN_POINT('Ctrl Pts',(-63.80306296304,3.7873017331392,127.663603563551));
#89020=CARTESIAN_POINT('Ctrl Pts',(-63.8108108598171,3.69680410981446,127.560470601527));
#89021=CARTESIAN_POINT('Ctrl Pts',(-63.8185571359012,3.6063254166416,127.457359212695));
#89022=CARTESIAN_POINT('Ctrl Pts',(-63.8263034119853,3.51150637371691,127.358009813479));
#89023=CARTESIAN_POINT('Ctrl Pts',(-63.8340496880694,3.41270017408323,127.262798732703));
#89024=CARTESIAN_POINT('Ctrl Pts',(-63.8417960213347,3.31389324508463,127.167586949101));
#89025=CARTESIAN_POINT('Ctrl Pts',(-63.8495423546001,3.21109938217554,127.076513816182));
#89026=CARTESIAN_POINT('Ctrl Pts',(-63.8572886878655,3.10470794451307,126.989918110229));
#89027=CARTESIAN_POINT('Ctrl Pts',(-63.8650367558684,2.99829268122594,126.903303011769));
#89028=CARTESIAN_POINT('Ctrl Pts',(-63.8727848238713,2.88827854319387,126.821167582264));
#89029=CARTESIAN_POINT('Ctrl Pts',(-63.8805328918743,2.77508687349521,126.743809434899));
#89030=CARTESIAN_POINT('Ctrl Pts',(-63.8882891946162,2.66177490234284,126.666369070375));
#89031=CARTESIAN_POINT('Ctrl Pts',(-63.896045497358,2.54527897666502,126.593716351501));
#89032=CARTESIAN_POINT('Ctrl Pts',(-63.9038018000999,2.4260487193876,126.526105053243));
#89033=CARTESIAN_POINT('Ctrl Pts',(-63.9115622426141,2.30675482533191,126.4584576688));
#89034=CARTESIAN_POINT('Ctrl Pts',(-63.9193226851284,2.18472403940201,126.395857244901));
#89035=CARTESIAN_POINT('Ctrl Pts',(-63.9270831276425,2.06042843373263,126.338510448565));
#89036=CARTESIAN_POINT('Ctrl Pts',(-63.934856027908,1.9359332977226,126.28107159406));
#89037=CARTESIAN_POINT('Ctrl Pts',(-63.9426289281733,1.80916643846161,126.228903368991));
#89038=CARTESIAN_POINT('Ctrl Pts',(-63.9504018284387,1.68061849249453,126.182163678319));
#89039=CARTESIAN_POINT('Ctrl Pts',(-63.9578921642007,1.55674358815696,126.137123093134));
#89040=CARTESIAN_POINT('Ctrl Pts',(-63.9653824999627,1.43121513636299,126.09712330632));
#89041=CARTESIAN_POINT('Ctrl Pts',(-63.9728728357247,1.30448151257663,126.0622607614));
#89042=CARTESIAN_POINT('Ctrl Pts',(-63.9806471698438,1.17294274492381,126.026076392493));
#89043=CARTESIAN_POINT('Ctrl Pts',(-63.9884215039629,1.03968893777712,125.995311891306));
#89044=CARTESIAN_POINT('Ctrl Pts',(-63.9961958380819,0.905206392251208,
125.970130125551));
#89045=CARTESIAN_POINT('Ctrl Pts',(-64.003960591029,0.770889584443603,125.944979394072));
#89046=CARTESIAN_POINT('Ctrl Pts',(-64.0117253439761,0.635347431879937,
125.925397779699));
#89047=CARTESIAN_POINT('Ctrl Pts',(-64.0194900969232,0.499081235154803,
125.911498369023));
#89048=CARTESIAN_POINT('Ctrl Pts',(-64.0272471378082,0.362950379937272,
125.897612763438));
#89049=CARTESIAN_POINT('Ctrl Pts',(-64.0350041786931,0.226097298091355,
125.889398169859));
#89050=CARTESIAN_POINT('Ctrl Pts',(-64.0427612195781,0.0890329715300792,
125.886916546457));
#89051=CARTESIAN_POINT('Ctrl Pts',(-64.0505124108182,-0.0479279937563315,
125.884436794467));
#89052=CARTESIAN_POINT('Ctrl Pts',(-64.0582636020584,-0.185099497359099,
125.887681414481));
#89053=CARTESIAN_POINT('Ctrl Pts',(-64.0660147932985,-0.321966308790757,
125.896660467954));
#89054=CARTESIAN_POINT('Ctrl Pts',(-64.0737626900756,-0.458774948176515,
125.90563570509));
#89055=CARTESIAN_POINT('Ctrl Pts',(-64.0815105868526,-0.595278763651564,
125.920340502566));
#89056=CARTESIAN_POINT('Ctrl Pts',(-64.0892584836297,-0.730963621414174,
125.940732830958));
#89057=CARTESIAN_POINT('Ctrl Pts',(-64.0970047597138,-0.866620096829568,
125.961120893714));
#89058=CARTESIAN_POINT('Ctrl Pts',(-64.1047510357979,-1.00145756889593,
125.987194062921));
#89059=CARTESIAN_POINT('Ctrl Pts',(-64.112497311882,-1.13496851204762,126.018858602191));
#89060=CARTESIAN_POINT('Ctrl Pts',(-64.1202436451473,-1.26848044074658,
126.050523375201));
#89061=CARTESIAN_POINT('Ctrl Pts',(-64.1279899784126,-1.40066544057867,
126.087779510412));
#89062=CARTESIAN_POINT('Ctrl Pts',(-64.135736311678,-1.53102803132618,126.130482545794));
#89063=CARTESIAN_POINT('Ctrl Pts',(-64.1434843796809,-1.66141981587202,
126.173195144225));
#89064=CARTESIAN_POINT('Ctrl Pts',(-64.1512324476839,-1.78998800776162,
126.221356948396));
#89065=CARTESIAN_POINT('Ctrl Pts',(-64.1589805156869,-1.91625447036826,
126.27477433764));
#89066=CARTESIAN_POINT('Ctrl Pts',(-64.1667368184287,-2.04265513047413,
126.328248499521));
#89067=CARTESIAN_POINT('Ctrl Pts',(-64.1744931211706,-2.16674881389534,
126.386989251936));
#89068=CARTESIAN_POINT('Ctrl Pts',(-64.1822494239125,-2.28807898039,126.450755485954));
#89069=CARTESIAN_POINT('Ctrl Pts',(-64.1900098664266,-2.4094739044477,126.514555753931));
#89070=CARTESIAN_POINT('Ctrl Pts',(-64.1977703089408,-2.52810203457313,
126.583386652007));
#89071=CARTESIAN_POINT('Ctrl Pts',(-64.2055307514549,-2.64353432942961,
126.656962721098));
#89072=CARTESIAN_POINT('Ctrl Pts',(-64.2133036517203,-2.75915192645339,
126.730656901027));
#89073=CARTESIAN_POINT('Ctrl Pts',(-64.2210765519858,-2.87156311556875,
126.809111250017));
#89074=CARTESIAN_POINT('Ctrl Pts',(-64.2288494522512,-2.98036984582112,
126.891998333137));
#89075=CARTESIAN_POINT('Ctrl Pts',(-64.2363397880134,-3.08522117736238,
126.971872262007));
#89076=CARTESIAN_POINT('Ctrl Pts',(-64.2438301237754,-3.18672532526037,
127.055862041832));
#89077=CARTESIAN_POINT('Ctrl Pts',(-64.2513204595375,-3.28455879095931,
127.143642571713));
#89078=CARTESIAN_POINT('Ctrl Pts',(-64.2589772908735,-3.38456690403458,
127.23337429179));
#89079=CARTESIAN_POINT('Ctrl Pts',(-64.2666341222094,-3.48107626436257,
127.327370025791));
#89080=CARTESIAN_POINT('Ctrl Pts',(-64.2742909535454,-3.57369301393172,
127.425322099781));
#89081=CARTESIAN_POINT('Ctrl Pts',(-64.2819389498596,-3.66620289540336,
127.523161149379));
#89082=CARTESIAN_POINT('Ctrl Pts',(-64.2895869461738,-3.75482882032915,
127.624947174461));
#89083=CARTESIAN_POINT('Ctrl Pts',(-64.297234942488,-3.83921005965763,127.730332449132));
#89084=CARTESIAN_POINT('Ctrl Pts',(-64.3048758880061,-3.92351350672683,
127.835620567626));
#89085=CARTESIAN_POINT('Ctrl Pts',(-64.3125168335242,-4.00357979839632,
127.944501025308));
#89086=CARTESIAN_POINT('Ctrl Pts',(-64.3201577790423,-4.07908555363194,
128.056589865001));
#89087=CARTESIAN_POINT('Ctrl Pts',(-64.328063760285,-4.15721032015385,128.172566645889));
#89088=CARTESIAN_POINT('Ctrl Pts',(-64.3359697415278,-4.23045213663244,
128.291978101722));
#89089=CARTESIAN_POINT('Ctrl Pts',(-64.3438757227705,-4.29849852397049,
128.414361976997));
#89090=CARTESIAN_POINT('Ctrl Pts',(-64.3515082187794,-4.36419103750313,
128.532512325563));
#89091=CARTESIAN_POINT('Ctrl Pts',(-64.3591407147881,-4.42504138323864,
128.653432480606));
#89092=CARTESIAN_POINT('Ctrl Pts',(-64.3667732107969,-4.48081325641169,
128.776678289472));
#89093=CARTESIAN_POINT('Ctrl Pts',(-64.3744040968274,-4.53657336521397,
128.899898101194));
#89094=CARTESIAN_POINT('Ctrl Pts',(-64.3820349828578,-4.58725696986167,
129.025442221674));
#89095=CARTESIAN_POINT('Ctrl Pts',(-64.3896658688882,-4.63267495053891,
129.152844385387));
#89096=CARTESIAN_POINT('Ctrl Pts',(-64.3972978797951,-4.67809962632558,
129.28026532958));
#89097=CARTESIAN_POINT('Ctrl Pts',(-64.404929890702,-4.71825699590313,129.409544482713));
#89098=CARTESIAN_POINT('Ctrl Pts',(-64.4125619016089,-4.75300719352354,
129.54019857067));
#89099=CARTESIAN_POINT('Ctrl Pts',(-64.4133844523908,-4.75675244527613,
129.554279999997));
#89100=CARTESIAN_POINT('Ctrl Pts',(-64.4142070031727,-4.760434936853,129.568377387448));
#89101=CARTESIAN_POINT('Ctrl Pts',(-64.4150295539547,-4.76405452823403,
129.582490119308));
#89102=CARTESIAN_POINT('Ctrl Pts',(-62.6653842080088,-4.76405452823406,
129.582490119308));
#89103=CARTESIAN_POINT('Ctrl Pts',(-62.6733465228717,-4.799041029491,129.718901956715));
#89104=CARTESIAN_POINT('Ctrl Pts',(-62.6813088377347,-4.82819392202019,
129.856932659022));
#89105=CARTESIAN_POINT('Ctrl Pts',(-62.6892711525976,-4.85137405232088,
129.996058157488));
#89106=CARTESIAN_POINT('Ctrl Pts',(-62.6972258082262,-4.87453188482843,
130.135049826182));
#89107=CARTESIAN_POINT('Ctrl Pts',(-62.7051804638548,-4.89172834729019,
130.27513383785));
#89108=CARTESIAN_POINT('Ctrl Pts',(-62.7131351194834,-4.90287509196743,
130.415774854747));
#89109=CARTESIAN_POINT('Ctrl Pts',(-62.7204702676585,-4.91315372974815,
130.54546276917));
#89110=CARTESIAN_POINT('Ctrl Pts',(-62.7278054158335,-4.91828875835897,
130.675623958895));
#89111=CARTESIAN_POINT('Ctrl Pts',(-62.7351405640086,-4.91824977962913,
130.805832921208));
#89112=CARTESIAN_POINT('',(-62.3898594359577,-4.91824789635182,130.799811713202));
#89113=CARTESIAN_POINT('Ctrl Pts',(-62.3199210724795,-4.76405452823405,
129.582490119308));
#89114=CARTESIAN_POINT('Ctrl Pts',(-62.320539411322,-4.76675090131487,129.593003237027));
#89115=CARTESIAN_POINT('Ctrl Pts',(-62.3211577501644,-4.76941214013832,
129.603523977018));
#89116=CARTESIAN_POINT('Ctrl Pts',(-62.3217760890069,-4.77203820801996,
129.614052084581));
#89117=CARTESIAN_POINT('Ctrl Pts',(-62.3320725719393,-4.81576708491634,
129.789364506159));
#89118=CARTESIAN_POINT('Ctrl Pts',(-62.3423690548716,-4.84985192258178,
129.967171340743));
#89119=CARTESIAN_POINT('Ctrl Pts',(-62.352665537804,-4.87406213141582,130.14656019069));
#89120=CARTESIAN_POINT('Ctrl Pts',(-62.3627208266703,-4.89770521856867,
130.32174687506));
#89121=CARTESIAN_POINT('Ctrl Pts',(-62.3727761155366,-4.91193093972787,
130.498442635262));
#89122=CARTESIAN_POINT('Ctrl Pts',(-62.3828314044028,-4.9165688058078,130.67577508083));
#89123=CARTESIAN_POINT('Ctrl Pts',(-62.3851740815878,-4.91764933399519,
130.717089923189));
#89124=CARTESIAN_POINT('Ctrl Pts',(-62.3875167587727,-4.91820963078576,
130.758439214522));
#89125=CARTESIAN_POINT('Ctrl Pts',(-62.3898594359577,-4.91824789635182,
130.799811713202));
#89126=CARTESIAN_POINT('Ctrl Pts',(-62.389859435991,-4.91824789635236,130.799811713791));
#89127=CARTESIAN_POINT('Ctrl Pts',(-62.3975216442029,-4.91837305175083,
130.935128991462));
#89128=CARTESIAN_POINT('Ctrl Pts',(-62.4051838524148,-4.91290946822373,
131.070595210122));
#89129=CARTESIAN_POINT('Ctrl Pts',(-62.4128460606267,-4.90184711431266,
131.205705768782));
#89130=CARTESIAN_POINT('Ctrl Pts',(-62.4206534628014,-4.89057513584456,
131.343376586429));
#89131=CARTESIAN_POINT('Ctrl Pts',(-62.4284608649761,-4.87349000832848,
131.480677707847));
#89132=CARTESIAN_POINT('Ctrl Pts',(-62.4362682671508,-4.850636834558,131.617075427157));
#89133=CARTESIAN_POINT('Ctrl Pts',(-62.4439230751124,-4.82823032178836,
131.750807278591));
#89134=CARTESIAN_POINT('Ctrl Pts',(-62.4515778830739,-4.80027924671348,
131.88367030643));
#89135=CARTESIAN_POINT('Ctrl Pts',(-62.4592326910355,-4.76687835307637,
132.01516771594));
#89136=CARTESIAN_POINT('Ctrl Pts',(-62.4668867353449,-4.73348079154956,
132.146652007122));
#89137=CARTESIAN_POINT('Ctrl Pts',(-62.4745407796543,-4.69463459126161,
132.276770562044));
#89138=CARTESIAN_POINT('Ctrl Pts',(-62.4821948239637,-4.65048516148636,
132.405038856718));
#89139=CARTESIAN_POINT('Ctrl Pts',(-62.4898498570664,-4.60633002823537,
132.533323721824));
#89140=CARTESIAN_POINT('Ctrl Pts',(-62.497504890169,-4.55687043391876,132.659757472053));
#89141=CARTESIAN_POINT('Ctrl Pts',(-62.5051599232716,-4.50230082056917,
132.783873280724));
#89142=CARTESIAN_POINT('Ctrl Pts',(-62.5130819057339,-4.44582823395357,
132.912317305251));
#89143=CARTESIAN_POINT('Ctrl Pts',(-62.5210038881964,-4.38388293208794,
133.038278356155));
#89144=CARTESIAN_POINT('Ctrl Pts',(-62.5289258706588,-4.31673285920018,
133.161265470292));
#89145=CARTESIAN_POINT('Ctrl Pts',(-62.5365922686147,-4.25174922865379,
133.280284688639));
#89146=CARTESIAN_POINT('Ctrl Pts',(-62.5442586665705,-4.181891737911,133.396518584788));
#89147=CARTESIAN_POINT('Ctrl Pts',(-62.5519250645265,-4.10744755791259,
133.509551483567));
#89148=CARTESIAN_POINT('Ctrl Pts',(-62.559974839242,-4.02928061676058,133.628236865653));
#89149=CARTESIAN_POINT('Ctrl Pts',(-62.5680246139576,-3.94605672524618,
133.743392429204));
#89150=CARTESIAN_POINT('Ctrl Pts',(-62.5760743886732,-3.85815549910716,
133.854576873376));
#89151=CARTESIAN_POINT('Ctrl Pts',(-62.5841241633887,-3.77025427296802,
133.965761317548));
#89152=CARTESIAN_POINT('Ctrl Pts',(-62.5921739381043,-3.67767610052967,
134.072974313002));
#89153=CARTESIAN_POINT('Ctrl Pts',(-62.6002237128198,-3.58084349503747,
134.175820676138));
#89154=CARTESIAN_POINT('Ctrl Pts',(-62.6079980469389,-3.48732422831018,
134.275147926678));
#89155=CARTESIAN_POINT('Ctrl Pts',(-62.615772381058,-3.38952091736318,134.370738428404));
#89156=CARTESIAN_POINT('Ctrl Pts',(-62.6235467151771,-3.28776417073599,
134.462200119256));
#89157=CARTESIAN_POINT('Ctrl Pts',(-62.6313114681242,-3.18613283020502,
134.553549091749));
#89158=CARTESIAN_POINT('Ctrl Pts',(-62.6390762210712,-3.08055803631173,
134.640779118903));
#89159=CARTESIAN_POINT('Ctrl Pts',(-62.6468409740183,-2.97140910311259,
134.723532852163));
#89160=CARTESIAN_POINT('Ctrl Pts',(-62.6545980149033,-2.86236857817234,
134.806204393249));
#89161=CARTESIAN_POINT('Ctrl Pts',(-62.6623550557884,-2.7497612878884,134.884408253342));
#89162=CARTESIAN_POINT('Ctrl Pts',(-62.6701120966734,-2.63399141065753,
134.957825714456));
#89163=CARTESIAN_POINT('Ctrl Pts',(-62.6778632879135,-2.5183088363918,135.031187810891));
#89164=CARTESIAN_POINT('Ctrl Pts',(-62.6856144791536,-2.3994687510749,135.099770484225));
#89165=CARTESIAN_POINT('Ctrl Pts',(-62.6933656703938,-2.27790595722141,
135.163297129211));
#89166=CARTESIAN_POINT('Ctrl Pts',(-62.7011135671709,-2.15639483079794,
135.22679677368));
#89167=CARTESIAN_POINT('Ctrl Pts',(-62.7088614639479,-2.03216364324611,
135.285244483195));
#89168=CARTESIAN_POINT('Ctrl Pts',(-62.716609360725,-1.90567335704063,135.338408711573));
#89169=CARTESIAN_POINT('Ctrl Pts',(-62.7243556368091,-1.77920952987621,
135.39156181914));
#89170=CARTESIAN_POINT('Ctrl Pts',(-62.7321019128933,-1.65048790419101,
135.439433492463));
#89171=CARTESIAN_POINT('Ctrl Pts',(-62.7398481889774,-1.51999069553578,
135.481839783525));
#89172=CARTESIAN_POINT('Ctrl Pts',(-62.7475945222427,-1.38949252357979,
135.524246387621));
#89173=CARTESIAN_POINT('Ctrl Pts',(-62.7553408555081,-1.25721911432547,
135.561187408124));
#89174=CARTESIAN_POINT('Ctrl Pts',(-62.7630871887734,-1.12366878233238,
135.592528485353));
#89175=CARTESIAN_POINT('Ctrl Pts',(-62.7708352567764,-0.990088542668778,
135.623876581199));
#89176=CARTESIAN_POINT('Ctrl Pts',(-62.7785833247793,-0.855231191794881,
135.649622149014));
#89177=CARTESIAN_POINT('Ctrl Pts',(-62.7863313927823,-0.719605803154936,
135.66968183518));
#89178=CARTESIAN_POINT('Ctrl Pts',(-62.7940876955241,-0.583836270237611,
135.689762841019));
#89179=CARTESIAN_POINT('Ctrl Pts',(-62.8018439982661,-0.44729745632209,
135.704145836325));
#89180=CARTESIAN_POINT('Ctrl Pts',(-62.8096003010079,-0.310504692713374,
135.712799259161));
#89181=CARTESIAN_POINT('Ctrl Pts',(-62.8173607435221,-0.173638918687783,
135.721457300589));
#89182=CARTESIAN_POINT('Ctrl Pts',(-62.8251211860363,-0.036519315578075,
135.724379667806));
#89183=CARTESIAN_POINT('Ctrl Pts',(-62.8328816285504,0.100339200920041,
135.721586980797));
#89184=CARTESIAN_POINT('Ctrl Pts',(-62.8406545288159,0.237417414858382,
135.718789810719));
#89185=CARTESIAN_POINT('Ctrl Pts',(-62.8484274290813,0.37423331421897,135.710259277559));
#89186=CARTESIAN_POINT('Ctrl Pts',(-62.8562003293468,0.510276615900347,
135.696067971626));
#89187=CARTESIAN_POINT('Ctrl Pts',(-62.8636906651088,0.641374400893024,
135.682392555409));
#89188=CARTESIAN_POINT('Ctrl Pts',(-62.8711810008708,0.771754479904198,
135.663460831977));
#89189=CARTESIAN_POINT('Ctrl Pts',(-62.8786713366328,0.900971455956128,
135.639382178847));
#89190=CARTESIAN_POINT('Ctrl Pts',(-62.8864456707519,1.03508773293009,135.614390576265));
#89191=CARTESIAN_POINT('Ctrl Pts',(-62.894220004871,1.16837580784162,135.583774881943));
#89192=CARTESIAN_POINT('Ctrl Pts',(-62.9019943389901,1.30032712578436,135.547601327086));
#89193=CARTESIAN_POINT('Ctrl Pts',(-62.9097590919372,1.43211582552037,135.511472352903));
#89194=CARTESIAN_POINT('Ctrl Pts',(-62.9175238448843,1.56257067275564,135.469799249156));
#89195=CARTESIAN_POINT('Ctrl Pts',(-62.9252885978314,1.69119139676037,135.422699574596));
#89196=CARTESIAN_POINT('Ctrl Pts',(-62.9330456387164,1.8196843728486,135.375646680098));
#89197=CARTESIAN_POINT('Ctrl Pts',(-62.9408026796013,1.94634648617702,135.323178074193));
#89198=CARTESIAN_POINT('Ctrl Pts',(-62.9485597204863,2.07069112198224,135.265461528759));
#89199=CARTESIAN_POINT('Ctrl Pts',(-62.9563109117264,2.19494198853017,135.20778850782));
#89200=CARTESIAN_POINT('Ctrl Pts',(-62.9640621029666,2.31687850291183,135.144875588479));
#89201=CARTESIAN_POINT('Ctrl Pts',(-62.9718132942067,2.43603292792123,135.076939070513));
#89202=CARTESIAN_POINT('Ctrl Pts',(-62.9795611909838,2.55513670912177,135.009031427379));
#89203=CARTESIAN_POINT('Ctrl Pts',(-62.9873090877608,2.67146041384924,134.936104625539));
#89204=CARTESIAN_POINT('Ctrl Pts',(-62.9950569845379,2.78456007426379,134.85842132941));
#89205=CARTESIAN_POINT('Ctrl Pts',(-63.002803260622,2.89763607666753,134.780754282952));
#89206=CARTESIAN_POINT('Ctrl Pts',(-63.0105495367062,3.00748905411379,134.698332942439));
#89207=CARTESIAN_POINT('Ctrl Pts',(-63.0182958127903,3.11370359664268,134.611463581074));
#89208=CARTESIAN_POINT('Ctrl Pts',(-63.0260421460557,3.21991892322334,134.52459357846));
#89209=CARTESIAN_POINT('Ctrl Pts',(-63.033788479321,3.32249545865616,134.433275736993));
#89210=CARTESIAN_POINT('Ctrl Pts',(-63.0415348125864,3.42105081114509,134.337856678136));
#89211=CARTESIAN_POINT('Ctrl Pts',(-63.0492828805894,3.51962823442173,134.242416250842));
#89212=CARTESIAN_POINT('Ctrl Pts',(-63.0570309485923,3.61418240199828,134.142873050468));
#89213=CARTESIAN_POINT('Ctrl Pts',(-63.0647790165953,3.70436801948363,134.039610320252));
#89214=CARTESIAN_POINT('Ctrl Pts',(-63.0725353193371,3.79464948731646,133.936237841177));
#89215=CARTESIAN_POINT('Ctrl Pts',(-63.080291622079,3.88055287268232,133.829138230337));
#89216=CARTESIAN_POINT('Ctrl Pts',(-63.0880479248209,3.96177307247127,133.718727990555));
#89217=CARTESIAN_POINT('Ctrl Pts',(-63.095808367335,4.04303662192633,133.608258821503));
#89218=CARTESIAN_POINT('Ctrl Pts',(-63.1035688098493,4.11961178704503,133.494475826842));
#89219=CARTESIAN_POINT('Ctrl Pts',(-63.1113292523634,4.1912375914936,133.377823365334));
#89220=CARTESIAN_POINT('Ctrl Pts',(-63.1191021526289,4.26297837604221,133.260983642939));
#89221=CARTESIAN_POINT('Ctrl Pts',(-63.1268750528943,4.32975373241596,133.141265590436));
#89222=CARTESIAN_POINT('Ctrl Pts',(-63.1346479531597,4.39134891241674,133.019137760286));
#89223=CARTESIAN_POINT('Ctrl Pts',(-63.1421382889217,4.45070495247501,132.901449584385));
#89224=CARTESIAN_POINT('Ctrl Pts',(-63.1496286246837,4.50525077479246,132.781524072409));
#89225=CARTESIAN_POINT('Ctrl Pts',(-63.1571189604456,4.55483765382755,132.659795070673));
#89226=CARTESIAN_POINT('Ctrl Pts',(-63.1648932945647,4.60630463445315,132.533450676835));
#89227=CARTESIAN_POINT('Ctrl Pts',(-63.1726676286837,4.65259224396969,132.404763113887));
#89228=CARTESIAN_POINT('Ctrl Pts',(-63.1804419628028,4.69348131821857,132.274196043059));
#89229=CARTESIAN_POINT('Ctrl Pts',(-63.1882067157499,4.7343200003378,132.143789884476));
#89230=CARTESIAN_POINT('Ctrl Pts',(-63.1959714686969,4.76977326937909,132.011509196327));
#89231=CARTESIAN_POINT('Ctrl Pts',(-63.203736221644,4.79966962230043,131.877838413921));
#89232=CARTESIAN_POINT('Ctrl Pts',(-63.211493262529,4.82953628174255,131.74430039522));
#89233=CARTESIAN_POINT('Ctrl Pts',(-63.219250303414,4.85385692375506,131.609375408912));
#89234=CARTESIAN_POINT('Ctrl Pts',(-63.2270073442989,4.87250967240302,131.473563542574));
#89235=CARTESIAN_POINT('Ctrl Pts',(-63.234758535539,4.89114835486813,131.337854093021));
#89236=CARTESIAN_POINT('Ctrl Pts',(-63.2425097267792,4.90412759852797,131.201259480413));
#89237=CARTESIAN_POINT('Ctrl Pts',(-63.2502609180193,4.91137655912721,131.064290140621));
#89238=CARTESIAN_POINT('Ctrl Pts',(-63.2580088147964,4.91862243872484,130.927379016453));
#89239=CARTESIAN_POINT('Ctrl Pts',(-63.2657567115734,4.92014285871247,130.790093871477));
#89240=CARTESIAN_POINT('Ctrl Pts',(-63.2735046083505,4.91591883064088,130.652950204944));
#89241=CARTESIAN_POINT('Ctrl Pts',(-63.2812508844346,4.91169568614492,130.51583522591));
#89242=CARTESIAN_POINT('Ctrl Pts',(-63.2889971605186,4.90173049569564,130.378862056986));
#89243=CARTESIAN_POINT('Ctrl Pts',(-63.2967434366027,4.88605639638326,130.242545742485));
#89244=CARTESIAN_POINT('Ctrl Pts',(-63.304489769868,4.87038218136826,130.106228421728));
#89245=CARTESIAN_POINT('Ctrl Pts',(-63.3122361031334,4.84899901805933,129.970568353476));
#89246=CARTESIAN_POINT('Ctrl Pts',(-63.3199824363988,4.82199183680364,129.836074612142));
#89247=CARTESIAN_POINT('Ctrl Pts',(-63.3277305044017,4.79497860747696,129.701550751868));
#89248=CARTESIAN_POINT('Ctrl Pts',(-63.3354785724047,4.76233893098125,129.568194121493));
#89249=CARTESIAN_POINT('Ctrl Pts',(-63.3432266404076,4.72420860065541,129.4365023793));
#89250=CARTESIAN_POINT('Ctrl Pts',(-63.3509829431495,4.68603774496064,129.304670673555));
#89251=CARTESIAN_POINT('Ctrl Pts',(-63.3587392458913,4.64236468723968,129.174507766824));
#89252=CARTESIAN_POINT('Ctrl Pts',(-63.3664955486331,4.59337492743055,129.046495480944));
#89253=CARTESIAN_POINT('Ctrl Pts',(-63.3742559911473,4.54435902031156,128.918414871052));
#89254=CARTESIAN_POINT('Ctrl Pts',(-63.3820164336614,4.49002091160054,128.792487527998));
#89255=CARTESIAN_POINT('Ctrl Pts',(-63.3897768761755,4.43059338882702,128.669173205327));
#89256=CARTESIAN_POINT('Ctrl Pts',(-63.397549776441,4.37107046771821,128.545660927559));
#89257=CARTESIAN_POINT('Ctrl Pts',(-63.4053226767064,4.30644199075551,128.424770397412));
#89258=CARTESIAN_POINT('Ctrl Pts',(-63.4130955769718,4.23698608774719,128.306935552677));
#89259=CARTESIAN_POINT('Ctrl Pts',(-63.420585912734,4.17005508176039,128.193384301353));
#89260=CARTESIAN_POINT('Ctrl Pts',(-63.4280762484963,4.09864170138477,128.08267068765));
#89261=CARTESIAN_POINT('Ctrl Pts',(-63.4355665842585,4.02303056402202,127.975154343106));
#89262=CARTESIAN_POINT('Ctrl Pts',(-63.4433409183776,3.94455260740644,127.863561483682));
#89263=CARTESIAN_POINT('Ctrl Pts',(-63.4511152524967,3.86130369965797,127.75505963572));
#89264=CARTESIAN_POINT('Ctrl Pts',(-63.4588895866158,3.77355546852083,127.650083808455));
#89265=CARTESIAN_POINT('Ctrl Pts',(-63.4666543395629,3.68591537923628,127.545237354515));
#89266=CARTESIAN_POINT('Ctrl Pts',(-63.47441909251,3.59378724782314,127.443908572101));
#89267=CARTESIAN_POINT('Ctrl Pts',(-63.4821838454571,3.49748594184438,127.346503600698));
#89268=CARTESIAN_POINT('Ctrl Pts',(-63.4899408863421,3.40128028368033,127.249195373287));
#89269=CARTESIAN_POINT('Ctrl Pts',(-63.497697927227,3.30090997249661,127.155803477539));
#89270=CARTESIAN_POINT('Ctrl Pts',(-63.505454968112,3.196729869217,127.066700760683));
#89271=CARTESIAN_POINT('Ctrl Pts',(-63.5132061593522,3.09262832896409,126.977665236879));
#89272=CARTESIAN_POINT('Ctrl Pts',(-63.5209573505924,2.98472301105,126.892912706973));
#89273=CARTESIAN_POINT('Ctrl Pts',(-63.5287085418325,2.87340506657975,126.8127786773));
#89274=CARTESIAN_POINT('Ctrl Pts',(-63.5364564386095,2.7621344352051,126.732678706728));
#89275=CARTESIAN_POINT('Ctrl Pts',(-63.5442043353866,2.64745437876083,126.657193560096));
#89276=CARTESIAN_POINT('Ctrl Pts',(-63.5519522321636,2.52978833764556,126.586617852862));
#89277=CARTESIAN_POINT('Ctrl Pts',(-63.5596985082478,2.41214690972935,126.516056908544));
#89278=CARTESIAN_POINT('Ctrl Pts',(-63.5674447843318,2.29152107458051,126.450403561939));
#89279=CARTESIAN_POINT('Ctrl Pts',(-63.575191060416,2.16836206497228,126.389908327905));
#89280=CARTESIAN_POINT('Ctrl Pts',(-63.5829373936813,2.04520214623256,126.32941264731));
#89281=CARTESIAN_POINT('Ctrl Pts',(-63.5906837269467,1.91950936663725,126.274075327632));
#89282=CARTESIAN_POINT('Ctrl Pts',(-63.598430060212,1.79175793183678,126.224100081723));
#89283=CARTESIAN_POINT('Ctrl Pts',(-63.6061781282149,1.66397788798843,126.174113644204));
#89284=CARTESIAN_POINT('Ctrl Pts',(-63.6139261962179,1.53413863558321,126.129491812309));
#89285=CARTESIAN_POINT('Ctrl Pts',(-63.6216742642209,1.4027322682454,126.090389335714));
#89286=CARTESIAN_POINT('Ctrl Pts',(-63.6294305669628,1.2711862406561,126.051245300542));
#89287=CARTESIAN_POINT('Ctrl Pts',(-63.6371868697047,1.13807014634592,126.017632450394));
#89288=CARTESIAN_POINT('Ctrl Pts',(-63.6449431724465,1.00388962291999,125.989655155391));
#89289=CARTESIAN_POINT('Ctrl Pts',(-63.6527036149607,0.869637483308436,
125.961662928064));
#89290=CARTESIAN_POINT('Ctrl Pts',(-63.6604640574749,0.734320168108235,
125.939312312991));
#89291=CARTESIAN_POINT('Ctrl Pts',(-63.6682244999891,0.598450308344868,
125.922655967452));
#89292=CARTESIAN_POINT('Ctrl Pts',(-63.6759974002545,0.462362338220836,
125.905972883669));
#89293=CARTESIAN_POINT('Ctrl Pts',(-63.6837703005199,0.325720440973305,
125.895002367252));
#89294=CARTESIAN_POINT('Ctrl Pts',(-63.6915432007854,0.189040036710512,
125.889744973691));
#89295=CARTESIAN_POINT('Ctrl Pts',(-63.6990335365474,0.0573283094200115,
125.884678699629));
#89296=CARTESIAN_POINT('Ctrl Pts',(-63.7065238723094,-0.0744188658198374,
125.884917386534));
#89297=CARTESIAN_POINT('Ctrl Pts',(-63.7140142080714,-0.205745078151946,
125.890415967357));
#89298=CARTESIAN_POINT('Ctrl Pts',(-63.7217885421905,-0.342050563740365,
125.896123028543));
#89299=CARTESIAN_POINT('Ctrl Pts',(-63.7295628763096,-0.478334309468239,
125.907514793235));
#89300=CARTESIAN_POINT('Ctrl Pts',(-63.7373372104286,-0.614083508315742,
125.924597866436));
#89301=CARTESIAN_POINT('Ctrl Pts',(-63.7451019633757,-0.74966540840792,
125.941659886276));
#89302=CARTESIAN_POINT('Ctrl Pts',(-63.7528667163229,-0.884713688216192,
125.96439921045));
#89303=CARTESIAN_POINT('Ctrl Pts',(-63.76063146927,-1.01871645748081,125.992770460273));
#89304=CARTESIAN_POINT('Ctrl Pts',(-63.768388510155,-1.15258613330643,126.021113531371));
#89305=CARTESIAN_POINT('Ctrl Pts',(-63.7761455510401,-1.28541198507125,
126.055077315929));
#89306=CARTESIAN_POINT('Ctrl Pts',(-63.7839025919251,-1.41668851484582,
126.094564792437));
#89307=CARTESIAN_POINT('Ctrl Pts',(-63.7916537831653,-1.54786604796828,
126.134022491131));
#89308=CARTESIAN_POINT('Ctrl Pts',(-63.7994049744055,-1.67749621176206,
126.178995478521));
#89309=CARTESIAN_POINT('Ctrl Pts',(-63.8071561656456,-1.80508530851847,
126.229336017471));
#89310=CARTESIAN_POINT('Ctrl Pts',(-63.8149040624227,-1.93262017650468,
126.27965516035));
#89311=CARTESIAN_POINT('Ctrl Pts',(-63.8226519591998,-2.05811533994081,
126.335337174163));
#89312=CARTESIAN_POINT('Ctrl Pts',(-63.8303998559769,-2.18109405062049,
126.396185053362));
#89313=CARTESIAN_POINT('Ctrl Pts',(-63.8381461320611,-2.30404703680535,
126.457020204496));
#89314=CARTESIAN_POINT('Ctrl Pts',(-63.8458924081452,-2.42448426705172,
126.523018898396));
#89315=CARTESIAN_POINT('Ctrl Pts',(-63.8536386842294,-2.54195107377796,
126.59393690955));
#89316=CARTESIAN_POINT('Ctrl Pts',(-63.8613850174948,-2.65941874761765,
126.664855444206));
#89317=CARTESIAN_POINT('Ctrl Pts',(-63.8691313507602,-2.77391561948534,
126.74069316651));
#89318=CARTESIAN_POINT('Ctrl Pts',(-63.8768776840256,-2.88501398025388,
126.82116122559));
#89319=CARTESIAN_POINT('Ctrl Pts',(-63.8846257520287,-2.99613722073015,
126.901647304934));
#89320=CARTESIAN_POINT('Ctrl Pts',(-63.8923738200316,-3.10386011908522,
126.986765555134));
#89321=CARTESIAN_POINT('Ctrl Pts',(-63.9001218880346,-3.20778649141001,
127.076185609868));
#89322=CARTESIAN_POINT('Ctrl Pts',(-63.9078781907765,-3.31182331791933,
127.165700701299));
#89323=CARTESIAN_POINT('Ctrl Pts',(-63.9156344935184,-3.41205526122974,
127.259526474941));
#89324=CARTESIAN_POINT('Ctrl Pts',(-63.9233907962602,-3.50812120232632,
127.357293938157));
#89325=CARTESIAN_POINT('Ctrl Pts',(-63.9311512387744,-3.60423841670828,
127.455113582813));
#89326=CARTESIAN_POINT('Ctrl Pts',(-63.9389116812886,-3.69618493634622,
127.556878819085));
#89327=CARTESIAN_POINT('Ctrl Pts',(-63.9466721238028,-3.7836393695877,127.662186818521));
#89328=CARTESIAN_POINT('Ctrl Pts',(-63.9544450240683,-3.87123419244937,
127.767663867706));
#89329=CARTESIAN_POINT('Ctrl Pts',(-63.9622179243337,-3.95432228173845,
127.876694733667));
#89330=CARTESIAN_POINT('Ctrl Pts',(-63.9699908245991,-4.03262457294653,
127.988846079126));
#89331=CARTESIAN_POINT('Ctrl Pts',(-63.9774811603609,-4.10808037863444,
128.09692044068));
#89332=CARTESIAN_POINT('Ctrl Pts',(-63.9849714961226,-4.17909213089906,
128.207892086581));
#89333=CARTESIAN_POINT('Ctrl Pts',(-63.9924618318844,-4.24545104470866,
128.321352665609));
#89334=CARTESIAN_POINT('Ctrl Pts',(-64.0005366497677,-4.31698804398247,
128.443666743606));
#89335=CARTESIAN_POINT('Ctrl Pts',(-64.008611467651,-4.38332968069564,128.569235709413));
#89336=CARTESIAN_POINT('Ctrl Pts',(-64.0166862855343,-4.44417947166694,
128.697597250191));
#89337=CARTESIAN_POINT('Ctrl Pts',(-64.0247498264294,-4.50494428209864,
128.825779526047));
#89338=CARTESIAN_POINT('Ctrl Pts',(-64.0328133673244,-4.56023237056421,
128.95674629851));
#89339=CARTESIAN_POINT('Ctrl Pts',(-64.0408769082194,-4.60979166284431,
129.09000829448));
#89340=CARTESIAN_POINT('Ctrl Pts',(-64.0489271056746,-4.65926894506919,
129.223049770277));
#89341=CARTESIAN_POINT('Ctrl Pts',(-64.0569773031299,-4.70303620408986,
129.35837857463));
#89342=CARTESIAN_POINT('Ctrl Pts',(-64.0650275005851,-4.74088848545256,
129.495483453351));
#89343=CARTESIAN_POINT('Ctrl Pts',(-64.0667258432992,-4.74887414625427,
129.524408342851));
#89344=CARTESIAN_POINT('Ctrl Pts',(-64.0684241860133,-4.75659671139267,
129.553412204632));
#89345=CARTESIAN_POINT('Ctrl Pts',(-64.0701225287274,-4.764054528234,129.582490119308));
#89346=CARTESIAN_POINT('Origin',(213.235140564004,0.,130.804360617566));
#89347=CARTESIAN_POINT('',(-66.1650696236363,-4.76405452823402,129.582490119308));
#89348=CARTESIAN_POINT('',(-65.8197716842485,-4.76405452823398,129.582490119308));
#89349=CARTESIAN_POINT('',(213.235140564004,-4.76405452823405,129.582490119308));
#89350=CARTESIAN_POINT('',(-64.48514056398,-4.91824840200337,130.808325298039));
#89351=CARTESIAN_POINT('Ctrl Pts',(-64.4851405640085,-4.91824840200297,
130.808325298541));
#89352=CARTESIAN_POINT('Ctrl Pts',(-64.4978018550894,-4.91806869548702,
131.031254026103));
#89353=CARTESIAN_POINT('Ctrl Pts',(-64.5104631461705,-4.90272945504267,
131.253589797038));
#89354=CARTESIAN_POINT('Ctrl Pts',(-64.5231244372515,-4.87248571274956,
131.473737971195));
#89355=CARTESIAN_POINT('Ctrl Pts',(-64.5253389859512,-4.86719586989387,
131.512243432423));
#89356=CARTESIAN_POINT('Ctrl Pts',(-64.5275535346509,-4.86145014892634,
131.550682063995));
#89357=CARTESIAN_POINT('Ctrl Pts',(-64.5297680833505,-4.85525002522065,
131.589045430147));
#89358=CARTESIAN_POINT('Ctrl Pts',(-64.5375424174696,-4.83348404045158,
131.723722814499));
#89359=CARTESIAN_POINT('Ctrl Pts',(-64.5453167515887,-4.80607570897494,
131.857707197984));
#89360=CARTESIAN_POINT('Ctrl Pts',(-64.5530910857078,-4.77307903900955,
131.990488582782));
#89361=CARTESIAN_POINT('Ctrl Pts',(-64.5608558386549,-4.74012303449089,
132.12310632639));
#89362=CARTESIAN_POINT('Ctrl Pts',(-64.568620591602,-4.70159248819834,132.254523645437));
#89363=CARTESIAN_POINT('Ctrl Pts',(-64.576385344549,-4.65759291991145,132.384237592172));
#89364=CARTESIAN_POINT('Ctrl Pts',(-64.584142385434,-4.61363705261601,132.513822705187));
#89365=CARTESIAN_POINT('Ctrl Pts',(-64.591899426319,-4.5642230978478,132.641707444826));
#89366=CARTESIAN_POINT('Ctrl Pts',(-64.599656467204,-4.50950710175618,132.767401310397));
#89367=CARTESIAN_POINT('Ctrl Pts',(-64.6074076584441,-4.45483236742284,
132.893000389246));
#89368=CARTESIAN_POINT('Ctrl Pts',(-64.6151588496842,-4.39486370557697,
133.016411525519));
#89369=CARTESIAN_POINT('Ctrl Pts',(-64.6229100409244,-4.32980612930487,
133.137161926108));
#89370=CARTESIAN_POINT('Ctrl Pts',(-64.6306579377015,-4.26477620423823,
133.257861004555));
#89371=CARTESIAN_POINT('Ctrl Pts',(-64.6384058344785,-4.19466185168961,
133.375901253092));
#89372=CARTESIAN_POINT('Ctrl Pts',(-64.6461537312556,-4.11971500643078,
133.49083252851));
#89373=CARTESIAN_POINT('Ctrl Pts',(-64.6539000073397,-4.04478383843631,
133.605739762782));
#89374=CARTESIAN_POINT('Ctrl Pts',(-64.6616462834238,-3.96502240179397,
133.717538990196));
#89375=CARTESIAN_POINT('Ctrl Pts',(-64.6693925595079,-3.88072691281483,
133.825807570709));
#89376=CARTESIAN_POINT('Ctrl Pts',(-64.6771388927733,-3.79643080158565,
133.934076950435));
#89377=CARTESIAN_POINT('Ctrl Pts',(-64.6848852260386,-3.70760081141714,
134.038815322764));
#89378=CARTESIAN_POINT('Ctrl Pts',(-64.6926315593039,-3.61457428760482,
134.139632088059));
#89379=CARTESIAN_POINT('Ctrl Pts',(-64.7003796273069,-3.52152693114749,
134.24047143057));
#89380=CARTESIAN_POINT('Ctrl Pts',(-64.7081276953098,-3.42428143606292,
134.337387131221));
#89381=CARTESIAN_POINT('Ctrl Pts',(-64.7158757633128,-3.32321264911289,
134.430024798275));
#89382=CARTESIAN_POINT('Ctrl Pts',(-64.7236320660546,-3.22203644505322,
134.522760921744));
#89383=CARTESIAN_POINT('Ctrl Pts',(-64.7313883687965,-3.11702912064238,
134.611209664412));
#89384=CARTESIAN_POINT('Ctrl Pts',(-64.7391446715383,-3.00859973712811,
134.69505601611));
#89385=CARTESIAN_POINT('Ctrl Pts',(-64.7469051140525,-2.90011248158711,
134.778947119131));
#89386=CARTESIAN_POINT('Ctrl Pts',(-64.7546655565666,-2.78819984643927,
134.858230710632));
#89387=CARTESIAN_POINT('Ctrl Pts',(-64.7624259990808,-2.67329979977132,
134.932635226049));
#89388=CARTESIAN_POINT('Ctrl Pts',(-64.7701988993462,-2.55821530534812,
135.007159182199));
#89389=CARTESIAN_POINT('Ctrl Pts',(-64.7779717996116,-2.44013415312025,
135.076788212081));
#89390=CARTESIAN_POINT('Ctrl Pts',(-64.785744699877,-2.31951960725176,135.141296385372));
#89391=CARTESIAN_POINT('Ctrl Pts',(-64.7932350356391,-2.20328970393415,
135.203459524078));
#89392=CARTESIAN_POINT('Ctrl Pts',(-64.8007253714012,-2.08470767687764,
135.260867520164));
#89393=CARTESIAN_POINT('Ctrl Pts',(-64.8082157071633,-1.9642036784546,135.313361279802));
#89394=CARTESIAN_POINT('Ctrl Pts',(-64.8159900412824,-1.83913073430618,
135.367845356291));
#89395=CARTESIAN_POINT('Ctrl Pts',(-64.8237643754015,-1.71159100519587,
135.4172077828));
#89396=CARTESIAN_POINT('Ctrl Pts',(-64.8315387095206,-1.5820427594963,135.461218331693));
#89397=CARTESIAN_POINT('Ctrl Pts',(-64.8393034624677,-1.45265417043149,
135.505174641518));
#89398=CARTESIAN_POINT('Ctrl Pts',(-64.8470682154147,-1.3212623565535,135.543792072671));
#89399=CARTESIAN_POINT('Ctrl Pts',(-64.8548329683618,-1.18834749806699,
135.576887546389));
#89400=CARTESIAN_POINT('Ctrl Pts',(-64.8625900092468,-1.0555646524917,135.609950149215));
#89401=CARTESIAN_POINT('Ctrl Pts',(-64.8703470501318,-0.921262149594142,
135.637501615126));
#89402=CARTESIAN_POINT('Ctrl Pts',(-64.8781040910168,-0.785937008254221,
135.659408102561));
#89403=CARTESIAN_POINT('Ctrl Pts',(-64.8858552822569,-0.65071391665606,
135.681298070143));
#89404=CARTESIAN_POINT('Ctrl Pts',(-64.8936064734971,-0.514470105981229,
135.697551470172));
#89405=CARTESIAN_POINT('Ctrl Pts',(-64.9013576647372,-0.377714165042159,
135.708085229739));
#89406=CARTESIAN_POINT('Ctrl Pts',(-64.9091055615143,-0.241016349026072,
135.718614512176));
#89407=CARTESIAN_POINT('Ctrl Pts',(-64.9168534582913,-0.103807224667278,
135.723428959263));
#89408=CARTESIAN_POINT('Ctrl Pts',(-64.9246013550684,0.0333983129050693,
135.722497217458));
#89409=CARTESIAN_POINT('Ctrl Pts',(-64.9323476311525,0.170575150036766,
135.721565670552));
#89410=CARTESIAN_POINT('Ctrl Pts',(-64.9400939072366,0.307748011165861,
135.714890328209));
#89411=CARTESIAN_POINT('Ctrl Pts',(-64.9478401833207,0.444401205101536,
135.702491958333));
#89412=CARTESIAN_POINT('Ctrl Pts',(-64.955586516586,0.581055407780045,135.690093496935));
#89413=CARTESIAN_POINT('Ctrl Pts',(-64.9633328498514,0.717189546244628,
135.671971959031));
#89414=CARTESIAN_POINT('Ctrl Pts',(-64.9710791831168,0.85229265458679,135.648200034128));
#89415=CARTESIAN_POINT('Ctrl Pts',(-64.9788272511197,0.987426018333327,
135.624422785667));
#89416=CARTESIAN_POINT('Ctrl Pts',(-64.9865753191227,1.12152750753259,135.594992700016));
#89417=CARTESIAN_POINT('Ctrl Pts',(-64.9943233871257,1.25409634854941,135.560033588982));
#89418=CARTESIAN_POINT('Ctrl Pts',(-65.0020796898676,1.38680608530805,135.525037322988));
#89419=CARTESIAN_POINT('Ctrl Pts',(-65.0098359926094,1.5179795413033,135.484500392892));
#89420=CARTESIAN_POINT('Ctrl Pts',(-65.0175922953512,1.64713058196371,135.438596682816));
#89421=CARTESIAN_POINT('Ctrl Pts',(-65.0253527378654,1.77635055442337,135.392668472547));
#89422=CARTESIAN_POINT('Ctrl Pts',(-65.0331131803797,1.90354559829671,135.341367920882));
#89423=CARTESIAN_POINT('Ctrl Pts',(-65.0408736228938,2.028250506176,135.284916715496));
#89424=CARTESIAN_POINT('Ctrl Pts',(-65.0486465231592,2.15315560144404,135.228374889623));
#89425=CARTESIAN_POINT('Ctrl Pts',(-65.0564194234247,2.27556222335211,135.166666063457));
#89426=CARTESIAN_POINT('Ctrl Pts',(-65.0641923236901,2.39502988472424,135.1000578734));
#89427=CARTESIAN_POINT('Ctrl Pts',(-65.0716826594522,2.51015459568542,135.035871058827));
#89428=CARTESIAN_POINT('Ctrl Pts',(-65.0791729952142,2.62255005082217,134.967135065199));
#89429=CARTESIAN_POINT('Ctrl Pts',(-65.0866633309762,2.7318498921273,134.894125797791));
#89430=CARTESIAN_POINT('Ctrl Pts',(-65.0944376650953,2.84529387013583,134.818348361819));
#89431=CARTESIAN_POINT('Ctrl Pts',(-65.1022119992144,2.95576221648972,134.737727172878));
#89432=CARTESIAN_POINT('Ctrl Pts',(-65.1099863333335,3.06281352890933,134.652523341468));
#89433=CARTESIAN_POINT('Ctrl Pts',(-65.1177510862806,3.16973291015384,134.567424516165));
#89434=CARTESIAN_POINT('Ctrl Pts',(-65.1255158392277,3.27324333351046,134.477754526762));
#89435=CARTESIAN_POINT('Ctrl Pts',(-65.1332805921748,3.37293122049939,134.383818403919));
#89436=CARTESIAN_POINT('Ctrl Pts',(-65.1410376330598,3.47252009607348,134.289975579757));
#89437=CARTESIAN_POINT('Ctrl Pts',(-65.1487946739449,3.56829370797957,134.191875320732));
#89438=CARTESIAN_POINT('Ctrl Pts',(-65.1565517148299,3.65987080067712,134.08986343827));
#89439=CARTESIAN_POINT('Ctrl Pts',(-65.16430290607,3.7513788343767,133.987928483762));
#89440=CARTESIAN_POINT('Ctrl Pts',(-65.1720540973101,3.83869638775054,133.882088066942));
#89441=CARTESIAN_POINT('Ctrl Pts',(-65.1798052885502,3.92147866453274,133.772725175048));
#89442=CARTESIAN_POINT('Ctrl Pts',(-65.1875531853272,4.00422575663903,133.6634087653));
#89443=CARTESIAN_POINT('Ctrl Pts',(-65.1953010821043,4.0824411705606,133.550573169262));
#89444=CARTESIAN_POINT('Ctrl Pts',(-65.2030489788814,4.15582021428058,133.434634635435));
#89445=CARTESIAN_POINT('Ctrl Pts',(-65.2107952549654,4.22918390868647,133.31872035345));
#89446=CARTESIAN_POINT('Ctrl Pts',(-65.2185415310496,4.29771303619146,133.199704754854));
#89447=CARTESIAN_POINT('Ctrl Pts',(-65.2262878071337,4.36114632573639,133.078032930811));
#89448=CARTESIAN_POINT('Ctrl Pts',(-65.234034140399,4.42458008353146,132.956360208614));
#89449=CARTESIAN_POINT('Ctrl Pts',(-65.2417804736644,4.48291774756538,132.832031568524));
#89450=CARTESIAN_POINT('Ctrl Pts',(-65.2495268069298,4.53594428402451,132.705516191086));
#89451=CARTESIAN_POINT('Ctrl Pts',(-65.2572748749327,4.58898269540883,132.578972481406));
#89452=CARTESIAN_POINT('Ctrl Pts',(-65.2650229429357,4.63670746137042,132.450241420426));
#89453=CARTESIAN_POINT('Ctrl Pts',(-65.2727710109387,4.6789520679073,132.319811246497));
#89454=CARTESIAN_POINT('Ctrl Pts',(-65.2805273136805,4.72124157251472,132.189242449826));
#89455=CARTESIAN_POINT('Ctrl Pts',(-65.2882836164224,4.75803916221425,132.056971305385));
#89456=CARTESIAN_POINT('Ctrl Pts',(-65.2960399191643,4.78922836303293,131.923500800573));
#89457=CARTESIAN_POINT('Ctrl Pts',(-65.3038003616784,4.82043421046721,131.789959058534));
#89458=CARTESIAN_POINT('Ctrl Pts',(-65.3115608041926,4.84602563156959,131.655217064512));
#89459=CARTESIAN_POINT('Ctrl Pts',(-65.3193212467067,4.86593768249237,131.519786038278));
#89460=CARTESIAN_POINT('Ctrl Pts',(-65.3270941469722,4.885881698007,131.384137606138));
#89461=CARTESIAN_POINT('Ctrl Pts',(-65.3348670472376,4.90012808395764,131.247798320526));
#89462=CARTESIAN_POINT('Ctrl Pts',(-65.342639947503,4.90866391635209,131.111283439792));
#89463=CARTESIAN_POINT('Ctrl Pts',(-65.3501302832651,4.91688944973854,130.979731218833));
#89464=CARTESIAN_POINT('Ctrl Pts',(-65.3576206190271,4.91981240050838,130.848016255696));
#89465=CARTESIAN_POINT('Ctrl Pts',(-65.3651109547891,4.91746687013063,130.71659591129));
#89466=CARTESIAN_POINT('Ctrl Pts',(-65.3728852889082,4.91503240825569,130.580192724581));
#89467=CARTESIAN_POINT('Ctrl Pts',(-65.3806596230273,4.9069143582325,130.443674854263));
#89468=CARTESIAN_POINT('Ctrl Pts',(-65.3884339571464,4.8930938110057,130.307554801177));
#89469=CARTESIAN_POINT('Ctrl Pts',(-65.3961987100935,4.87929029636818,130.171602503891));
#89470=CARTESIAN_POINT('Ctrl Pts',(-65.4039634630406,4.85979830690382,130.03604743357));
#89471=CARTESIAN_POINT('Ctrl Pts',(-65.4117282159877,4.83465092427619,129.901402422025));
#89472=CARTESIAN_POINT('Ctrl Pts',(-65.4194852568727,4.80952851838354,129.766891141803));
#89473=CARTESIAN_POINT('Ctrl Pts',(-65.4272422977577,4.77876196875752,129.633288503421));
#89474=CARTESIAN_POINT('Ctrl Pts',(-65.4349993386427,4.74243613841335,129.501102187487));
#89475=CARTESIAN_POINT('Ctrl Pts',(-65.4427505298828,4.70613770166041,129.369015554282));
#89476=CARTESIAN_POINT('Ctrl Pts',(-65.4505017211229,4.66428843188234,129.238343493081));
#89477=CARTESIAN_POINT('Ctrl Pts',(-65.458252912363,4.61702417628389,129.109583104702));
#89478=CARTESIAN_POINT('Ctrl Pts',(-65.4660008091401,4.5697800092549,128.980877442923));
#89479=CARTESIAN_POINT('Ctrl Pts',(-65.4737487059172,4.51712556838073,128.854082204194));
#89480=CARTESIAN_POINT('Ctrl Pts',(-65.4814966026942,4.45924636183527,128.72967872702));
#89481=CARTESIAN_POINT('Ctrl Pts',(-65.4892428787783,4.40137926237209,128.605301272372));
#89482=CARTESIAN_POINT('Ctrl Pts',(-65.4969891548625,4.3382897359099,128.483314938397));
#89483=CARTESIAN_POINT('Ctrl Pts',(-65.5047354309466,4.27021102686079,128.364180122484));
#89484=CARTESIAN_POINT('Ctrl Pts',(-65.5124817642119,4.20213181527012,128.245044427145));
#89485=CARTESIAN_POINT('Ctrl Pts',(-65.5202280974773,4.12906354157955,128.128760631321));
#89486=CARTESIAN_POINT('Ctrl Pts',(-65.5279744307426,4.05128470964006,128.015763252593));
#89487=CARTESIAN_POINT('Ctrl Pts',(-65.5357224987456,3.97348845967044,127.902740568885));
#89488=CARTESIAN_POINT('Ctrl Pts',(-65.5434705667486,3.89097977396011,127.793006088756));
#89489=CARTESIAN_POINT('Ctrl Pts',(-65.5512186347516,3.80407941637344,127.686963809904));
#89490=CARTESIAN_POINT('Ctrl Pts',(-65.5589749374934,3.71708670005261,127.580808828056));
#89491=CARTESIAN_POINT('Ctrl Pts',(-65.5667312402352,3.62569323618477,127.478354189207));
#89492=CARTESIAN_POINT('Ctrl Pts',(-65.5744875429771,3.53025924528654,127.379969763185));
#89493=CARTESIAN_POINT('Ctrl Pts',(-65.5822479854913,3.43477431839377,127.281532826432));
#89494=CARTESIAN_POINT('Ctrl Pts',(-65.5900084280054,3.33524485094255,127.187170700047));
#89495=CARTESIAN_POINT('Ctrl Pts',(-65.5977688705196,3.23206584286858,127.097214349901));
#89496=CARTESIAN_POINT('Ctrl Pts',(-65.605541770785,3.12872120269104,127.007113593836));
#89497=CARTESIAN_POINT('Ctrl Pts',(-65.6133146710505,3.02171561997012,126.921432991711));
#89498=CARTESIAN_POINT('Ctrl Pts',(-65.6210875713159,2.91147561041485,126.840461926573));
#89499=CARTESIAN_POINT('Ctrl Pts',(-65.628577907078,2.80524310288459,126.762434363605));
#89500=CARTESIAN_POINT('Ctrl Pts',(-65.63606824284,2.69600750032462,126.688780047448));
#89501=CARTESIAN_POINT('Ctrl Pts',(-65.643558578602,2.58417202609608,126.619717502312));
#89502=CARTESIAN_POINT('Ctrl Pts',(-65.6513329127211,2.46809627587051,126.548036429786));
#89503=CARTESIAN_POINT('Ctrl Pts',(-65.6591072468402,2.34885192085261,126.481075131644));
#89504=CARTESIAN_POINT('Ctrl Pts',(-65.6668815809593,2.22685992170939,126.419126535834));
#89505=CARTESIAN_POINT('Ctrl Pts',(-65.6746463339064,2.10501826680254,126.357254286132));
#89506=CARTESIAN_POINT('Ctrl Pts',(-65.6824110868535,1.98043605059833,126.300382622285));
#89507=CARTESIAN_POINT('Ctrl Pts',(-65.6901758398006,1.85356261447099,126.248760909873));
#89508=CARTESIAN_POINT('Ctrl Pts',(-65.6979328806856,1.72681519082901,126.197190468873));
#89509=CARTESIAN_POINT('Ctrl Pts',(-65.7056899215706,1.59778143574751,126.150859748956));
#89510=CARTESIAN_POINT('Ctrl Pts',(-65.7134469624556,1.46693434583226,126.109971766233));
#89511=CARTESIAN_POINT('Ctrl Pts',(-65.7211981536957,1.33618592872536,126.069114617456));
#89512=CARTESIAN_POINT('Ctrl Pts',(-65.7289493449359,1.20362727027075,126.033692152431));
#89513=CARTESIAN_POINT('Ctrl Pts',(-65.736700536176,1.06975002419918,126.003858774193));
#89514=CARTESIAN_POINT('Ctrl Pts',(-65.7444484329531,0.935929679528493,
125.974038075937));
#89515=CARTESIAN_POINT('Ctrl Pts',(-65.7521963297302,0.800792242709317,
125.949801824617));
#89516=CARTESIAN_POINT('Ctrl Pts',(-65.7599442265073,0.664842949157073,
125.931254122171));
#89517=CARTESIAN_POINT('Ctrl Pts',(-65.7676905025914,0.528922093266312,
125.912710299506));
#89518=CARTESIAN_POINT('Ctrl Pts',(-65.7754367786755,0.392190105560796,
125.899852711712));
#89519=CARTESIAN_POINT('Ctrl Pts',(-65.7831830547596,0.255160405703753,
125.892733979693));
#89520=CARTESIAN_POINT('Ctrl Pts',(-65.790929388025,0.118129694324595,125.885615195126));
#89521=CARTESIAN_POINT('Ctrl Pts',(-65.7986757212904,-0.01919834315263,
125.88423537115));
#89522=CARTESIAN_POINT('Ctrl Pts',(-65.8064220545557,-0.156307596645724,
125.888595061955));
#89523=CARTESIAN_POINT('Ctrl Pts',(-65.8141701225587,-0.293447554805489,
125.892955729082));
#89524=CARTESIAN_POINT('Ctrl Pts',(-65.8219181905617,-0.430368240793513,
125.903058456214));
#89525=CARTESIAN_POINT('Ctrl Pts',(-65.8296662585647,-0.566556379200238,
125.918851746252));
#89526=CARTESIAN_POINT('Ctrl Pts',(-65.8374225613066,-0.702889259981121,
125.934661821586));
#89527=CARTESIAN_POINT('Ctrl Pts',(-65.8451788640484,-0.838487648940886,
125.956174496244));
#89528=CARTESIAN_POINT('Ctrl Pts',(-65.8529351667903,-0.972845656130369,
125.98328663018));
#89529=CARTESIAN_POINT('Ctrl Pts',(-65.8606956093045,-1.10727537423391,
126.010413234678));
#89530=CARTESIAN_POINT('Ctrl Pts',(-65.8684560518186,-1.24046301193602,
126.043145160232));
#89531=CARTESIAN_POINT('Ctrl Pts',(-65.8762164943327,-1.37191661116169,
126.081328977346));
#89532=CARTESIAN_POINT('Ctrl Pts',(-65.8839893945982,-1.50358123137457,
126.119574090513));
#89533=CARTESIAN_POINT('Ctrl Pts',(-65.8917622948637,-1.63350587975983,
126.163288459499));
#89534=CARTESIAN_POINT('Ctrl Pts',(-65.8995351951291,-1.76121654800737,
126.212269663161));
#89535=CARTESIAN_POINT('Ctrl Pts',(-65.9070255308911,-1.88428461177913,
126.259470276694));
#89536=CARTESIAN_POINT('Ctrl Pts',(-65.914515866653,-2.00529658537079,126.311561325851));
#89537=CARTESIAN_POINT('Ctrl Pts',(-65.922006202415,-2.12385066609942,126.368321685071));
#89538=CARTESIAN_POINT('Ctrl Pts',(-65.9297812304682,-2.24691074414967,
126.427239389067));
#89539=CARTESIAN_POINT('Ctrl Pts',(-65.9375562585214,-2.36771224722287,
126.491375015461));
#89540=CARTESIAN_POINT('Ctrl Pts',(-65.9453312865747,-2.48578106105976,
126.560532678196));
#89541=CARTESIAN_POINT('Ctrl Pts',(-65.9530965778673,-2.60370201590915,
126.629603733963));
#89542=CARTESIAN_POINT('Ctrl Pts',(-65.9608618691598,-2.71889675688229,
126.703684115817));
#89543=CARTESIAN_POINT('Ctrl Pts',(-65.9686271604524,-2.8309125142882,126.782530511887));
#89544=CARTESIAN_POINT('Ctrl Pts',(-65.9763845847619,-2.94281478901344,
126.861297029013));
#89545=CARTESIAN_POINT('Ctrl Pts',(-65.9841420090715,-3.05154417219573,
126.944819727021));
#89546=CARTESIAN_POINT('Ctrl Pts',(-65.991899433381,-3.1566741362209,127.032810344772));
#89547=CARTESIAN_POINT('Ctrl Pts',(-65.9996503662968,-3.26171612774944,
127.120727332189));
#89548=CARTESIAN_POINT('Ctrl Pts',(-66.0074012992125,-3.36316439949768,
127.213104544159));
#89549=CARTESIAN_POINT('Ctrl Pts',(-66.0151522321284,-3.46062334270266,
127.309611822239));
#89550=CARTESIAN_POINT('Ctrl Pts',(-66.0228996449348,-3.55803802463637,
127.406075271249));
#89551=CARTESIAN_POINT('Ctrl Pts',(-66.0306470577412,-3.65146670569653,
127.506664779914));
#89552=CARTESIAN_POINT('Ctrl Pts',(-66.0383944705476,-3.74054878273879,
127.611011612767));
#89553=CARTESIAN_POINT('Ctrl Pts',(-66.0461400426149,-3.82960969441067,
127.715333653434));
#89554=CARTESIAN_POINT('Ctrl Pts',(-66.0538856146823,-3.91432580411637,
127.823410944299));
#89555=CARTESIAN_POINT('Ctrl Pts',(-66.0616311867496,-3.99437541497384,
127.934840081526));
#89556=CARTESIAN_POINT('Ctrl Pts',(-66.0693765958471,-4.0744233415569,128.046266874242));
#89557=CARTESIAN_POINT('Ctrl Pts',(-66.0771220049447,-4.14980473803786,
128.161045054669));
#89558=CARTESIAN_POINT('Ctrl Pts',(-66.0848674140422,-4.22024026637581,
128.278740860643));
#89559=CARTESIAN_POINT('Ctrl Pts',(-66.0926173157467,-4.29071664977332,
128.396504934284));
#89560=CARTESIAN_POINT('Ctrl Pts',(-66.1003672174513,-4.35624123371674,
128.517189678217));
#89561=CARTESIAN_POINT('Ctrl Pts',(-66.1081171191558,-4.41657974103042,
128.64033509701));
#89562=CARTESIAN_POINT('Ctrl Pts',(-66.1158695639228,-4.47693804789723,
128.763520924893));
#89563=CARTESIAN_POINT('Ctrl Pts',(-66.1236220086897,-4.53210672686887,
128.889168680153));
#89564=CARTESIAN_POINT('Ctrl Pts',(-66.1313744534567,-4.58189937968992,
129.016797713247));
#89565=CARTESIAN_POINT('Ctrl Pts',(-66.1391346815246,-4.63174202334797,
129.144554883362));
#89566=CARTESIAN_POINT('Ctrl Pts',(-66.1468949095925,-4.67619773291773,
129.274296935016));
#89567=CARTESIAN_POINT('Ctrl Pts',(-66.1546551376604,-4.71512967005692,
129.405527083135));
#89568=CARTESIAN_POINT('Ctrl Pts',(-66.1581266329857,-4.73254565791201,
129.464232167798));
#89569=CARTESIAN_POINT('Ctrl Pts',(-66.1615981283111,-4.74885692234884,
129.523234884618));
#89570=CARTESIAN_POINT('Ctrl Pts',(-66.1650696236364,-4.76405452823402,
129.582490119308));
#89571=CARTESIAN_POINT('Ctrl Pts',(-64.4150295539547,-4.76405452823403,
129.582490119308));
#89572=CARTESIAN_POINT('Ctrl Pts',(-64.4226670803882,-4.79766306093323,
129.713529278222));
#89573=CARTESIAN_POINT('Ctrl Pts',(-64.4303046068217,-4.82584443848221,
129.845892000019));
#89574=CARTESIAN_POINT('Ctrl Pts',(-64.4379421332552,-4.8485150824566,129.979082144752));
#89575=CARTESIAN_POINT('Ctrl Pts',(-64.445808538376,-4.87186511226066,130.116263684571));
#89576=CARTESIAN_POINT('Ctrl Pts',(-64.4536749434968,-4.88936886737709,
130.254322558506));
#89577=CARTESIAN_POINT('Ctrl Pts',(-64.4615413486176,-4.90099259422966,
130.392711915629));
#89578=CARTESIAN_POINT('Ctrl Pts',(-64.4694077537384,-4.91261632108222,
130.531101272753));
#89579=CARTESIAN_POINT('Ctrl Pts',(-64.4772741588592,-4.91836005286657,
130.669820648485));
#89580=CARTESIAN_POINT('Ctrl Pts',(-64.48514056398,-4.91824840200337,130.808325298039));
#89581=CARTESIAN_POINT('',(-64.1398594360283,-4.91824993534877,130.805158077164));
#89582=CARTESIAN_POINT('Ctrl Pts',(-64.0701225287274,-4.764054528234,129.582490119308));
#89583=CARTESIAN_POINT('Ctrl Pts',(-64.0781582273743,-4.79934114512443,
129.720072103015));
#89584=CARTESIAN_POINT('Ctrl Pts',(-64.0861939260212,-4.82869690305613,
129.859313232665));
#89585=CARTESIAN_POINT('Ctrl Pts',(-64.0942296246681,-4.85197641295532,
129.999681830331));
#89586=CARTESIAN_POINT('Ctrl Pts',(-64.1022545812035,-4.87522480283589,
130.139862783439));
#89587=CARTESIAN_POINT('Ctrl Pts',(-64.1102795377389,-4.89241308219218,
130.281167856988));
#89588=CARTESIAN_POINT('Ctrl Pts',(-64.1183044942743,-4.90344656354808,
130.42305383697));
#89589=CARTESIAN_POINT('Ctrl Pts',(-64.1254894748465,-4.91332516523728,
130.550088544902));
#89590=CARTESIAN_POINT('Ctrl Pts',(-64.1326744554187,-4.91827061982955,
130.677588566443));
#89591=CARTESIAN_POINT('Ctrl Pts',(-64.139859435991,-4.91824993534888,130.805158076502));
#89592=CARTESIAN_POINT('Ctrl Pts',(-64.1398594360282,-4.91824993534877,
130.805158077163));
#89593=CARTESIAN_POINT('Ctrl Pts',(-64.1480802783964,-4.91822626875783,
130.951119339359));
#89594=CARTESIAN_POINT('Ctrl Pts',(-64.1563011207648,-4.91170069888442,
131.09692237697));
#89595=CARTESIAN_POINT('Ctrl Pts',(-64.164521963133,-4.89874086550328,131.24199173523));
#89596=CARTESIAN_POINT('Ctrl Pts',(-64.172757650151,-4.88575763011782,131.38732305008));
#89597=CARTESIAN_POINT('Ctrl Pts',(-64.180993337169,-4.86631695936606,131.531917728935));
#89598=CARTESIAN_POINT('Ctrl Pts',(-64.189229024187,-4.84053774569423,131.675209281232));
#89599=CARTESIAN_POINT('Ctrl Pts',(-64.1974879554785,-4.81468577317552,
131.818905257351));
#89600=CARTESIAN_POINT('Ctrl Pts',(-64.2057468867699,-4.78245953336674,
131.961290441817));
#89601=CARTESIAN_POINT('Ctrl Pts',(-64.2140058180614,-4.74402862355473,
132.101810224061));
#89602=CARTESIAN_POINT('Ctrl Pts',(-64.2222775043416,-4.70553836153289,
132.242547023275));
#89603=CARTESIAN_POINT('Ctrl Pts',(-64.2305491906217,-4.66082439267892,
132.381412370845));
#89604=CARTESIAN_POINT('Ctrl Pts',(-64.2388208769019,-4.61010499468608,
132.51787017414));
#89605=CARTESIAN_POINT('Ctrl Pts',(-64.2471120720283,-4.5592659745388,132.654649814386));
#89606=CARTESIAN_POINT('Ctrl Pts',(-64.2554032671548,-4.50239332614663,
132.789010268259));
#89607=CARTESIAN_POINT('Ctrl Pts',(-64.2636944622812,-4.43975267442496,
132.920436999088));
#89608=CARTESIAN_POINT('Ctrl Pts',(-64.2660994600866,-4.42158272092387,
132.958559488595));
#89609=CARTESIAN_POINT('Ctrl Pts',(-64.2685044578918,-4.40292774055166,
132.996435315707));
#89610=CARTESIAN_POINT('Ctrl Pts',(-64.2709094556971,-4.38379490299275,
133.034052370027));
#89611=CARTESIAN_POINT('Ctrl Pts',(-64.2786837898162,-4.32194658383872,
133.15565229341));
#89612=CARTESIAN_POINT('Ctrl Pts',(-64.2864581239353,-4.25493696664731,
133.274869502135));
#89613=CARTESIAN_POINT('Ctrl Pts',(-64.2942324580544,-4.18297320085201,
133.391234844013));
#89614=CARTESIAN_POINT('Ctrl Pts',(-64.3019972110015,-4.11109812396646,
133.507456776006));
#89615=CARTESIAN_POINT('Ctrl Pts',(-64.3097619639486,-4.03428125035618,
133.620833504975));
#89616=CARTESIAN_POINT('Ctrl Pts',(-64.3175267168957,-3.95277662843796,
133.730918320427));
#89617=CARTESIAN_POINT('Ctrl Pts',(-64.3252837577807,-3.87135295805923,
133.840893798088));
#89618=CARTESIAN_POINT('Ctrl Pts',(-64.3330407986656,-3.78525103603341,
133.947583556649));
#89619=CARTESIAN_POINT('Ctrl Pts',(-64.3407978395506,-3.69476922372682,
134.050568165752));
#89620=CARTESIAN_POINT('Ctrl Pts',(-64.3485490307907,-3.60435564445885,
134.15347511336));
#89621=CARTESIAN_POINT('Ctrl Pts',(-64.3563002220309,-3.50956900615667,
134.252682180442));
#89622=CARTESIAN_POINT('Ctrl Pts',(-64.364051413271,-3.41074889194883,134.347801749936));
#89623=CARTESIAN_POINT('Ctrl Pts',(-64.371799310048,-3.31197077892551,134.442880891075));
#89624=CARTESIAN_POINT('Ctrl Pts',(-64.3795472068252,-3.209162880766,134.533875719412));
#89625=CARTESIAN_POINT('Ctrl Pts',(-64.3872951036023,-3.10270254571794,
134.620434512985));
#89626=CARTESIAN_POINT('Ctrl Pts',(-64.3950413796864,-2.99626447987694,
134.706975200324));
#89627=CARTESIAN_POINT('Ctrl Pts',(-64.4027876557703,-2.88617579996529,
134.789081452102));
#89628=CARTESIAN_POINT('Ctrl Pts',(-64.4105339318544,-2.77284762340966,
134.866441256826));
#89629=CARTESIAN_POINT('Ctrl Pts',(-64.4182802651198,-2.65951861029118,
134.943801632603));
#89630=CARTESIAN_POINT('Ctrl Pts',(-64.4260265983852,-2.54295037571757,
135.016415270991));
#89631=CARTESIAN_POINT('Ctrl Pts',(-64.4337729316505,-2.42358341890949,
135.084013228945));
#89632=CARTESIAN_POINT('Ctrl Pts',(-64.4415209996535,-2.30418973069908,
135.151626324994));
#89633=CARTESIAN_POINT('Ctrl Pts',(-64.4492690676565,-2.18199641322166,
135.214221312899));
#89634=CARTESIAN_POINT('Ctrl Pts',(-64.4570171356595,-2.05746862072361,
135.271575178927));
#89635=CARTESIAN_POINT('Ctrl Pts',(-64.4647734384013,-1.93280847860578,
135.328990001327));
#89636=CARTESIAN_POINT('Ctrl Pts',(-64.4725297411432,-1.80580926086457,
135.381152410709));
#89637=CARTESIAN_POINT('Ctrl Pts',(-64.4802860438851,-1.67695667772851,
135.427887341131));
#89638=CARTESIAN_POINT('Ctrl Pts',(-64.4880464863992,-1.54803532208916,
135.474647215393));
#89639=CARTESIAN_POINT('Ctrl Pts',(-64.4958069289134,-1.41725900260808,
135.51597372081));
#89640=CARTESIAN_POINT('Ctrl Pts',(-64.5035673714276,-1.28512769042289,
135.551741988576));
#89641=CARTESIAN_POINT('Ctrl Pts',(-64.511340271693,-1.15278426932531,135.587567674739));
#89642=CARTESIAN_POINT('Ctrl Pts',(-64.5191131719584,-1.01908189041864,
135.617817206777));
#89643=CARTESIAN_POINT('Ctrl Pts',(-64.5268860722238,-0.884530679151612,
135.64241689464));
#89644=CARTESIAN_POINT('Ctrl Pts',(-64.5343764079859,-0.754870743326913,
135.666122321888));
#89645=CARTESIAN_POINT('Ctrl Pts',(-64.541866743748,-0.624422923058458,
135.684581502331));
#89646=CARTESIAN_POINT('Ctrl Pts',(-64.5493570795101,-0.493645405713664,
135.697774280431));
#89647=CARTESIAN_POINT('Ctrl Pts',(-64.5571314136292,-0.357909419051108,
135.711467266723));
#89648=CARTESIAN_POINT('Ctrl Pts',(-64.5649057477483,-0.221388270050871,
135.719529991327));
#89649=CARTESIAN_POINT('Ctrl Pts',(-64.5726800818674,-0.084588639066603,
135.72188314671));
#89650=CARTESIAN_POINT('Ctrl Pts',(-64.5804448348145,0.0520423985984248,
135.724233402039));
#89651=CARTESIAN_POINT('Ctrl Pts',(-64.5882095877615,0.188950848218802,
135.720888082093));
#89652=CARTESIAN_POINT('Ctrl Pts',(-64.5959743407086,0.325623560229994,
135.711819467065));
#89653=CARTESIAN_POINT('Ctrl Pts',(-64.6037313815936,0.462160526977055,
135.702759859113));
#89654=CARTESIAN_POINT('Ctrl Pts',(-64.6114884224786,0.598461834476933,
135.687988294124));
#89655=CARTESIAN_POINT('Ctrl Pts',(-64.6192454633636,0.734013332483941,
135.667529079612));
#89656=CARTESIAN_POINT('Ctrl Pts',(-64.6269966546037,0.869462610051866,
135.647085293552));
#89657=CARTESIAN_POINT('Ctrl Pts',(-64.6347478458438,1.00416281857292,135.620962453276));
#89658=CARTESIAN_POINT('Ctrl Pts',(-64.6424990370839,1.13760429185905,135.589236743198));
#89659=CARTESIAN_POINT('Ctrl Pts',(-64.650246933861,1.27098904895936,135.557524517393));
#89660=CARTESIAN_POINT('Ctrl Pts',(-64.6579948306382,1.40311575532449,135.520214248389));
#89661=CARTESIAN_POINT('Ctrl Pts',(-64.6657427274153,1.53348453136136,135.477433295641));
#89662=CARTESIAN_POINT('Ctrl Pts',(-64.6734890034994,1.66382603706071,135.434661291747));
#89663=CARTESIAN_POINT('Ctrl Pts',(-64.6812352795833,1.79240997260925,135.386421002107));
#89664=CARTESIAN_POINT('Ctrl Pts',(-64.6889815556674,1.91875161489029,135.332889661622));
#89665=CARTESIAN_POINT('Ctrl Pts',(-64.6967278889328,2.04509418979662,135.27935792598));
#89666=CARTESIAN_POINT('Ctrl Pts',(-64.7044742221981,2.16919407842172,135.220535214085));
#89667=CARTESIAN_POINT('Ctrl Pts',(-64.7122205554635,2.29058691077764,135.156646760121));
#89668=CARTESIAN_POINT('Ctrl Pts',(-64.7199686234664,2.41200692821669,135.09274399878));
#89669=CARTESIAN_POINT('Ctrl Pts',(-64.7277166914694,2.53071833715708,135.023773420022));
#89670=CARTESIAN_POINT('Ctrl Pts',(-64.7354647594724,2.64628208259835,134.950005826917));
#89671=CARTESIAN_POINT('Ctrl Pts',(-64.7432210622142,2.76196865056351,134.876159832737));
#89672=CARTESIAN_POINT('Ctrl Pts',(-64.7509773649561,2.87450054220997,134.797506850455));
#89673=CARTESIAN_POINT('Ctrl Pts',(-64.758733667698,2.98346793136081,134.714360894426));
#89674=CARTESIAN_POINT('Ctrl Pts',(-64.7664941102121,3.09249347968819,134.631170560896));
#89675=CARTESIAN_POINT('Ctrl Pts',(-64.7742545527263,3.19795043419182,134.543482725172));
#89676=CARTESIAN_POINT('Ctrl Pts',(-64.7820149952404,3.29946349259535,134.451650532493));
#89677=CARTESIAN_POINT('Ctrl Pts',(-64.7897878955058,3.40113950877214,134.359670922626));
#89678=CARTESIAN_POINT('Ctrl Pts',(-64.7975607957713,3.49885869844773,134.263533935556));
#89679=CARTESIAN_POINT('Ctrl Pts',(-64.8053336960367,3.59228332883262,134.163628923));
#89680=CARTESIAN_POINT('Ctrl Pts',(-64.8128240317988,3.68231173858146,134.067355709294));
#89681=CARTESIAN_POINT('Ctrl Pts',(-64.8203143675609,3.76835220309984,133.967583901549));
#89682=CARTESIAN_POINT('Ctrl Pts',(-64.827804703323,3.85014010349792,133.864688091209));
#89683=CARTESIAN_POINT('Ctrl Pts',(-64.835579037442,3.93502901699755,133.757890954948));
#89684=CARTESIAN_POINT('Ctrl Pts',(-64.8433533715611,4.01560543130416,133.647389945406));
#89685=CARTESIAN_POINT('Ctrl Pts',(-64.8511277056802,4.09152874963622,133.533568479456));
#89686=CARTESIAN_POINT('Ctrl Pts',(-64.8588924586272,4.16735849926379,133.41988728829));
#89687=CARTESIAN_POINT('Ctrl Pts',(-64.8666572115743,4.23854634804271,133.30289410503));
#89688=CARTESIAN_POINT('Ctrl Pts',(-64.8744219645214,4.30479160464176,133.183005673707));
#89689=CARTESIAN_POINT('Ctrl Pts',(-64.8821790054063,4.37097106551806,133.063236317265));
#89690=CARTESIAN_POINT('Ctrl Pts',(-64.8899360462913,4.43221751558849,132.94057777532));
#89691=CARTESIAN_POINT('Ctrl Pts',(-64.8976930871763,4.48827349468616,132.815475755841));
#89692=CARTESIAN_POINT('Ctrl Pts',(-64.9054442784164,4.54428720153394,132.690468076768));
#89693=CARTESIAN_POINT('Ctrl Pts',(-64.9131954696565,4.5951180691138,132.563020943177));
#89694=CARTESIAN_POINT('Ctrl Pts',(-64.9209466608966,4.64055470650643,132.433604331202));
#89695=CARTESIAN_POINT('Ctrl Pts',(-64.9286945576737,4.68597203211618,132.304242724739));
#89696=CARTESIAN_POINT('Ctrl Pts',(-64.9364424544508,4.72599955828581,132.172913672901));
#89697=CARTESIAN_POINT('Ctrl Pts',(-64.9441903512278,4.7604742390024,132.040106579443));
#89698=CARTESIAN_POINT('Ctrl Pts',(-64.9519366273119,4.79494170835893,131.907327266366));
#89699=CARTESIAN_POINT('Ctrl Pts',(-64.9596829033959,4.82385854444972,131.773070904818));
#89700=CARTESIAN_POINT('Ctrl Pts',(-64.96742917948,4.8471118553323,131.637841105878));
#89701=CARTESIAN_POINT('Ctrl Pts',(-64.9751755127453,4.87036533786557,131.502610308703));
#89702=CARTESIAN_POINT('Ctrl Pts',(-64.9829218460106,4.88795514551239,131.366406445107));
#89703=CARTESIAN_POINT('Ctrl Pts',(-64.990668179276,4.89981977085075,131.229741947293));
#89704=CARTESIAN_POINT('Ctrl Pts',(-64.9984162472789,4.91168705318969,131.093046844412));
#89705=CARTESIAN_POINT('Ctrl Pts',(-65.0061643152819,4.91782656815173,130.95589129147));
#89706=CARTESIAN_POINT('Ctrl Pts',(-65.0139123832849,4.91822883007871,130.818791053548));
#89707=CARTESIAN_POINT('Ctrl Pts',(-65.0216686860267,4.91863151953444,130.681545103863));
#89708=CARTESIAN_POINT('Ctrl Pts',(-65.0294249887685,4.91328477415181,130.544354978223));
#89709=CARTESIAN_POINT('Ctrl Pts',(-65.0371812915103,4.90223126204096,130.407735207427));
#89710=CARTESIAN_POINT('Ctrl Pts',(-65.0449417340245,4.89117185033789,130.271042518545));
#89711=CARTESIAN_POINT('Ctrl Pts',(-65.0527021765387,4.87439965053415,130.134921178923));
#89712=CARTESIAN_POINT('Ctrl Pts',(-65.0604626190529,4.8520089136721,129.99987782462));
#89713=CARTESIAN_POINT('Ctrl Pts',(-65.0682355193183,4.82958223321147,129.864617686736));
#89714=CARTESIAN_POINT('Ctrl Pts',(-65.0760084195836,4.80151907219228,129.730439375123));
#89715=CARTESIAN_POINT('Ctrl Pts',(-65.083781319849,4.76796445041862,129.597837488055));
#89716=CARTESIAN_POINT('Ctrl Pts',(-65.0912716556113,4.73562962366439,129.470056013582));
#89717=CARTESIAN_POINT('Ctrl Pts',(-65.0987619913735,4.69819574885011,129.343738634839));
#89718=CARTESIAN_POINT('Ctrl Pts',(-65.1062523271358,4.65583494739597,129.21931045902));
#89719=CARTESIAN_POINT('Ctrl Pts',(-65.1140266612549,4.61186802328036,129.090164551098));
#89720=CARTESIAN_POINT('Ctrl Pts',(-65.121800995374,4.56245391452202,128.962644836904));
#89721=CARTESIAN_POINT('Ctrl Pts',(-65.1295753294932,4.5077310997147,128.83724511634));
#89722=CARTESIAN_POINT('Ctrl Pts',(-65.1373400824403,4.45307572588598,128.711999939724));
#89723=CARTESIAN_POINT('Ctrl Pts',(-65.1451048353875,4.39312481851497,128.588869913132));
#89724=CARTESIAN_POINT('Ctrl Pts',(-65.1528695883346,4.32806646514757,128.468333277023));
#89725=CARTESIAN_POINT('Ctrl Pts',(-65.1606266292196,4.26307272865399,128.347916359601));
#89726=CARTESIAN_POINT('Ctrl Pts',(-65.1683836701047,4.19298182573539,128.230088048543));
#89727=CARTESIAN_POINT('Ctrl Pts',(-65.1761407109897,4.11802957961944,128.115305868425));
#89728=CARTESIAN_POINT('Ctrl Pts',(-65.1838919022299,4.04313385557522,128.000610246441));
#89729=CARTESIAN_POINT('Ctrl Pts',(-65.1916430934701,3.9633842981334,127.888956509165));
#89730=CARTESIAN_POINT('Ctrl Pts',(-65.1993942847103,3.87906204957123,127.780776539344));
#89731=CARTESIAN_POINT('Ctrl Pts',(-65.2071421814874,3.79477564021407,127.672642548897));
#89732=CARTESIAN_POINT('Ctrl Pts',(-65.2148900782645,3.70592064509094,127.567979697082));
#89733=CARTESIAN_POINT('Ctrl Pts',(-65.2226379750416,3.61282068308968,127.467189693813));
#89734=CARTESIAN_POINT('Ctrl Pts',(-65.2303842511257,3.51974019559346,127.366420773641));
#89735=CARTESIAN_POINT('Ctrl Pts',(-65.2381305272098,3.42241677252422,127.269523377659));
#89736=CARTESIAN_POINT('Ctrl Pts',(-65.2458768032939,3.32121309529373,127.176864699147));
#89737=CARTESIAN_POINT('Ctrl Pts',(-65.2536231365593,3.22000867100068,127.084205336649));
#89738=CARTESIAN_POINT('Ctrl Pts',(-65.2613694698248,3.11492422375067,126.995785018068));
#89739=CARTESIAN_POINT('Ctrl Pts',(-65.2691158030902,3.00635763100361,126.911932473463));
#89740=CARTESIAN_POINT('Ctrl Pts',(-65.2768638710932,2.89776672552087,126.828061150661));
#89741=CARTESIAN_POINT('Ctrl Pts',(-65.2846119390962,2.78569243218529,126.748759876268));
#89742=CARTESIAN_POINT('Ctrl Pts',(-65.2923600070992,2.67056355153748,126.67431541446));
#89743=CARTESIAN_POINT('Ctrl Pts',(-65.3001163098411,2.55531231054527,126.599791832192));
#89744=CARTESIAN_POINT('Ctrl Pts',(-65.307872612583,2.4370003259359,126.530135586547));
#89745=CARTESIAN_POINT('Ctrl Pts',(-65.3156289153249,2.31608355019785,126.465588896099));
#89746=CARTESIAN_POINT('Ctrl Pts',(-65.3233893578391,2.19510223753569,126.401007755139));
#89747=CARTESIAN_POINT('Ctrl Pts',(-65.3311498003534,2.07151371567519,126.341541772832));
#89748=CARTESIAN_POINT('Ctrl Pts',(-65.3389102428676,1.94579517687389,126.287385502275));
#89749=CARTESIAN_POINT('Ctrl Pts',(-65.346683143133,1.81987482351351,126.233142295265));
#89750=CARTESIAN_POINT('Ctrl Pts',(-65.3544560433985,1.69181798581307,126.184225972507));
#89751=CARTESIAN_POINT('Ctrl Pts',(-65.362228943664,1.56211917005494,126.140781867181));
#89752=CARTESIAN_POINT('Ctrl Pts',(-65.3697192794256,1.43713523294842,126.098917064514));
#89753=CARTESIAN_POINT('Ctrl Pts',(-65.3772096151873,1.31062692101751,126.062133614897));
#89754=CARTESIAN_POINT('Ctrl Pts',(-65.3846999509489,1.18304492481576,126.030516488526));
#89755=CARTESIAN_POINT('Ctrl Pts',(-65.3924742850679,1.05062561844378,125.997700589197));
#89756=CARTESIAN_POINT('Ctrl Pts',(-65.400248619187,0.916630138556373,125.970346558012));
#89757=CARTESIAN_POINT('Ctrl Pts',(-65.4080229533061,0.781548784059955,
125.948604799917));
#89758=CARTESIAN_POINT('Ctrl Pts',(-65.4157877062532,0.646633905260386,
125.926889836595));
#89759=CARTESIAN_POINT('Ctrl Pts',(-65.4235524592003,0.510636196849151,
125.910773445873));
#89760=CARTESIAN_POINT('Ctrl Pts',(-65.4313172121473,0.374059681983171,
125.900355885022));
#89761=CARTESIAN_POINT('Ctrl Pts',(-65.4390742530323,0.237618816837148,
125.889948671039));
#89762=CARTESIAN_POINT('Ctrl Pts',(-65.4468312939173,0.100600676581215,
125.885229052499));
#89763=CARTESIAN_POINT('Ctrl Pts',(-65.4545883348023,-0.0364823421880473,
125.886245927849));
#89764=CARTESIAN_POINT('Ctrl Pts',(-65.4623395260424,-0.173461985586505,
125.887262036366));
#89765=CARTESIAN_POINT('Ctrl Pts',(-65.4700907172825,-0.310506020742713,
125.894006025375));
#89766=CARTESIAN_POINT('Ctrl Pts',(-65.4778419085227,-0.44709912820108,
125.906474805089));
#89767=CARTESIAN_POINT('Ctrl Pts',(-65.4855898052997,-0.583634179945036,
125.91893828524));
#89768=CARTESIAN_POINT('Ctrl Pts',(-65.4933377020768,-0.719718296649652,
125.937121681203));
#89769=CARTESIAN_POINT('Ctrl Pts',(-65.5010855988538,-0.854838584474578,
125.960969857262));
#89770=CARTESIAN_POINT('Ctrl Pts',(-65.5088318749379,-0.989930608048148,
125.984813044798));
#89771=CARTESIAN_POINT('Ctrl Pts',(-65.516578151022,-1.12405881898928,126.01431858759));
#89772=CARTESIAN_POINT('Ctrl Pts',(-65.5243244271061,-1.25671824903137,
126.04937982843));
#89773=CARTESIAN_POINT('Ctrl Pts',(-65.5320707603714,-1.38937865833506,
126.084441328085));
#89774=CARTESIAN_POINT('Ctrl Pts',(-65.5398170936368,-1.52056988711839,
126.125058507722));
#89775=CARTESIAN_POINT('Ctrl Pts',(-65.5475634269021,-1.64980030298776,
126.171074308394));
#89776=CARTESIAN_POINT('Ctrl Pts',(-65.555311494905,-1.77905965911274,126.217100413985));
#89777=CARTESIAN_POINT('Ctrl Pts',(-65.563059562908,-1.90635696030263,126.268527415225));
#89778=CARTESIAN_POINT('Ctrl Pts',(-65.5708076309109,-2.03121916656682,
126.325149553118));
#89779=CARTESIAN_POINT('Ctrl Pts',(-65.5785639336528,-2.15621407786988,
126.381831869693));
#89780=CARTESIAN_POINT('Ctrl Pts',(-65.5863202363946,-2.27876836771029,
126.443720190894));
#89781=CARTESIAN_POINT('Ctrl Pts',(-65.5940765391365,-2.39843179728367,
126.510561836035));
#89782=CARTESIAN_POINT('Ctrl Pts',(-65.6018369816506,-2.51815909483241,
126.577439156574));
#89783=CARTESIAN_POINT('Ctrl Pts',(-65.6095974241648,-2.6349921247931,126.649274864249));
#89784=CARTESIAN_POINT('Ctrl Pts',(-65.617357866679,-2.74850927006552,126.725772644399));
#89785=CARTESIAN_POINT('Ctrl Pts',(-65.6251307669444,-2.86220864313711,
126.802393225576));
#89786=CARTESIAN_POINT('Ctrl Pts',(-65.6329036672098,-2.97258117959476,
126.883690602592));
#89787=CARTESIAN_POINT('Ctrl Pts',(-65.6406765674752,-3.07923731379335,
126.969327289439));
#89788=CARTESIAN_POINT('Ctrl Pts',(-65.6481669032373,-3.18201622886439,
127.051850867015));
#89789=CARTESIAN_POINT('Ctrl Pts',(-65.6556572389994,-3.2813440195308,127.138403539745));
#89790=CARTESIAN_POINT('Ctrl Pts',(-65.6631475747615,-3.37690558870681,
127.22865205737));
#89791=CARTESIAN_POINT('Ctrl Pts',(-65.6708054564397,-3.47460470567242,
127.320919278968));
#89792=CARTESIAN_POINT('Ctrl Pts',(-65.6784633381179,-3.56869624901928,
127.417360836562));
#89793=CARTESIAN_POINT('Ctrl Pts',(-65.6861212197961,-3.65879426432663,
127.517658989211));
#89794=CARTESIAN_POINT('Ctrl Pts',(-65.6937702152272,-3.74878772941223,
127.617840755345));
#89795=CARTESIAN_POINT('Ctrl Pts',(-65.7014192106583,-3.83479661182774,
127.721869923546));
#89796=CARTESIAN_POINT('Ctrl Pts',(-65.7090682060894,-3.91646911087059,
127.829389564581));
#89797=CARTESIAN_POINT('Ctrl Pts',(-65.7167100992922,-3.99806577554587,
127.936809371719));
#89798=CARTESIAN_POINT('Ctrl Pts',(-65.7243519924951,-4.07533382051231,
128.047712888317));
#89799=CARTESIAN_POINT('Ctrl Pts',(-65.7319938856979,-4.14795971669204,
128.16170792544));
#89800=CARTESIAN_POINT('Ctrl Pts',(-65.7396303820591,-4.2205343231654,128.27562245723));
#89801=CARTESIAN_POINT('Ctrl Pts',(-65.7472668784203,-4.28847308626001,
128.392623827514));
#89802=CARTESIAN_POINT('Ctrl Pts',(-65.7549033747815,-4.3515044086014,128.512288968506));
#89803=CARTESIAN_POINT('Ctrl Pts',(-65.7625365975673,-4.41450871098772,
128.631902812039));
#89804=CARTESIAN_POINT('Ctrl Pts',(-65.7701698203531,-4.47260956978139,
128.754177798339));
#89805=CARTESIAN_POINT('Ctrl Pts',(-65.7778030431388,-4.52558042577481,
128.87866467263));
#89806=CARTESIAN_POINT('Ctrl Pts',(-65.7854364070183,-4.57855226088996,
129.003153847956));
#89807=CARTESIAN_POINT('Ctrl Pts',(-65.7930697708978,-4.62639373549626,
129.129854626074));
#89808=CARTESIAN_POINT('Ctrl Pts',(-65.8007031347773,-4.66892581622505,
129.258296328771));
#89809=CARTESIAN_POINT('Ctrl Pts',(-65.8070593179343,-4.70434161710013,
129.36524773319));
#89810=CARTESIAN_POINT('Ctrl Pts',(-65.8134155010914,-4.73607689232854,
129.473405741533));
#89811=CARTESIAN_POINT('Ctrl Pts',(-65.8197716842484,-4.76405452823398,
129.582490119308));
#89812=CARTESIAN_POINT('Origin',(213.235140564004,0.,130.804360617566));
#89813=CARTESIAN_POINT('',(-67.9154119669996,-4.76405452823407,129.582490119308));
#89814=CARTESIAN_POINT('',(-67.5697761045558,-4.76405452823408,129.582490119308));
#89815=CARTESIAN_POINT('',(213.235140564004,-4.76405452823405,129.582490119308));
#89816=CARTESIAN_POINT('',(-66.235140564045,-4.91824885854051,130.801009801995));
#89817=CARTESIAN_POINT('Ctrl Pts',(-66.235140564045,-4.91824885854051,130.801009801996));
#89818=CARTESIAN_POINT('Ctrl Pts',(-66.2427998121925,-4.91834063041699,
130.935710419581));
#89819=CARTESIAN_POINT('Ctrl Pts',(-66.25045906034,-4.91289448446255,131.070628404356));
#89820=CARTESIAN_POINT('Ctrl Pts',(-66.2581183084876,-4.9018833561888,131.205262880991));
#89821=CARTESIAN_POINT('Ctrl Pts',(-66.2657694033577,-4.89088394927227,
131.339754039089));
#89822=CARTESIAN_POINT('Ctrl Pts',(-66.2734204982278,-4.87433137425639,
131.473961890991));
#89823=CARTESIAN_POINT('Ctrl Pts',(-66.2810715930979,-4.85225058466901,
131.60738448152));
#89824=CARTESIAN_POINT('Ctrl Pts',(-66.2887164947383,-4.83018766852416,
131.740699072242));
#89825=CARTESIAN_POINT('Ctrl Pts',(-66.2963613963786,-4.80260550492369,
131.873229270524));
#89826=CARTESIAN_POINT('Ctrl Pts',(-66.3040062980189,-4.76958091247342,
132.004477687634));
#89827=CARTESIAN_POINT('Ctrl Pts',(-66.3116475322512,-4.73657216256244,
132.135663142326));
#89828=CARTESIAN_POINT('Ctrl Pts',(-66.3192887664834,-4.69812627272704,
132.265567648643));
#89829=CARTESIAN_POINT('Ctrl Pts',(-66.3269300007157,-4.65437118034599,
132.393703871261));
#89830=CARTESIAN_POINT('Ctrl Pts',(-66.3345694738153,-4.61062617252976,
132.521810561361));
#89831=CARTESIAN_POINT('Ctrl Pts',(-66.3422089469151,-4.56157452489964,
132.648149396986));
#89832=CARTESIAN_POINT('Ctrl Pts',(-66.3498484200148,-4.50739392498528,
132.772248588845));
#89833=CARTESIAN_POINT('Ctrl Pts',(-66.357487894633,-4.45321331430047,132.896347805374));
#89834=CARTESIAN_POINT('Ctrl Pts',(-66.3651273692513,-4.39390391070185,
133.018207008109));
#89835=CARTESIAN_POINT('Ctrl Pts',(-66.3727668438696,-4.32969116860841,
133.137375286824));
#89836=CARTESIAN_POINT('Ctrl Pts',(-66.3804080824465,-4.26546359976,133.256571081557));
#89837=CARTESIAN_POINT('Ctrl Pts',(-66.3880493210234,-4.19633063253334,
133.373074362418));
#89838=CARTESIAN_POINT('Ctrl Pts',(-66.3956905596002,-4.12256291951449,
133.486460175216));
#89839=CARTESIAN_POINT('Ctrl Pts',(-66.4033397192723,-4.04871873707678,
133.599963526525));
#89840=CARTESIAN_POINT('Ctrl Pts',(-66.4109888789443,-3.97023043644532,
133.710342619686));
#89841=CARTESIAN_POINT('Ctrl Pts',(-66.4186380386163,-3.88741129824348,
133.817202541861));
#89842=CARTESIAN_POINT('Ctrl Pts',(-66.4262915254948,-3.80454530842361,
133.924122915767));
#89843=CARTESIAN_POINT('Ctrl Pts',(-66.4339450123733,-3.71734386289516,
134.027519848115));
#89844=CARTESIAN_POINT('Ctrl Pts',(-66.4415984992518,-3.62615863655848,
134.127033728935));
#89845=CARTESIAN_POINT('Ctrl Pts',(-66.4492633983006,-3.53483744326241,
134.226695995631));
#89846=CARTESIAN_POINT('Ctrl Pts',(-66.4569282973494,-3.43952089224874,
134.322463365574));
#89847=CARTESIAN_POINT('Ctrl Pts',(-66.4645931963983,-3.34059572849287,
134.414014789544));
#89848=CARTESIAN_POINT('Ctrl Pts',(-66.4693626142791,-3.2790403913808,134.470981880136));
#89849=CARTESIAN_POINT('Ctrl Pts',(-66.4741320321599,-3.21608850216308,
134.52631743402));
#89850=CARTESIAN_POINT('Ctrl Pts',(-66.4789014500408,-3.1518389214251,134.579952554718));
#89851=CARTESIAN_POINT('Ctrl Pts',(-66.4866757841598,-3.04710963995969,
134.667379859107));
#89852=CARTESIAN_POINT('Ctrl Pts',(-66.4944501182789,-2.93857406374783,
134.750584788941));
#89853=CARTESIAN_POINT('Ctrl Pts',(-66.502224452398,-2.82660732586373,134.829217644576));
#89854=CARTESIAN_POINT('Ctrl Pts',(-66.5099892053451,-2.71477857697762,
134.907753592244));
#89855=CARTESIAN_POINT('Ctrl Pts',(-66.5177539582921,-2.59952739694863,
134.981728454494));
#89856=CARTESIAN_POINT('Ctrl Pts',(-66.5255187112392,-2.48126319403188,
135.050831625879));
#89857=CARTESIAN_POINT('Ctrl Pts',(-66.5332757521242,-2.36311645278838,
135.11986616302));
#89858=CARTESIAN_POINT('Ctrl Pts',(-66.5410327930092,-2.24196297939929,
135.184038442426));
#89859=CARTESIAN_POINT('Ctrl Pts',(-66.5487898338942,-2.11824217514571,
135.243080382311));
#89860=CARTESIAN_POINT('Ctrl Pts',(-66.5565410251343,-1.99461466971319,
135.302077798209));
#89861=CARTESIAN_POINT('Ctrl Pts',(-66.5642922163745,-1.86842403841305,
135.35595240755));
#89862=CARTESIAN_POINT('Ctrl Pts',(-66.5720434076146,-1.7401350492394,135.404481602161));
#89863=CARTESIAN_POINT('Ctrl Pts',(-66.5797913043917,-1.6119005863082,135.452990170569));
#89864=CARTESIAN_POINT('Ctrl Pts',(-66.5875392011687,-1.48156990425189,
135.49615770493));
#89865=CARTESIAN_POINT('Ctrl Pts',(-66.5952870979458,-1.3496283532354,135.533809461844));
#89866=CARTESIAN_POINT('Ctrl Pts',(-66.6030333740299,-1.21771440154723,
135.571453342822));
#89867=CARTESIAN_POINT('Ctrl Pts',(-66.6107796501141,-1.08419062684762,
135.60358363407));
#89868=CARTESIAN_POINT('Ctrl Pts',(-66.6185259261982,-0.949557786093246,
135.630075390879));
#89869=CARTESIAN_POINT('Ctrl Pts',(-66.6262722594635,-0.814923951509823,
135.656567343244));
#89870=CARTESIAN_POINT('Ctrl Pts',(-66.6340185927289,-0.679181418144645,
135.677420602631));
#89871=CARTESIAN_POINT('Ctrl Pts',(-66.6417649259942,-0.542840994622834,
135.692561382373));
#89872=CARTESIAN_POINT('Ctrl Pts',(-66.6495129939972,-0.406470038608121,
135.707705552787));
#89873=CARTESIAN_POINT('Ctrl Pts',(-66.6572610620002,-0.269501314506633,
135.717134654811));
#89874=CARTESIAN_POINT('Ctrl Pts',(-66.6650091300032,-0.13245021124291,
135.72082682858));
#89875=CARTESIAN_POINT('Ctrl Pts',(-66.6727654327451,0.00474655156410364,
135.724522926435));
#89876=CARTESIAN_POINT('Ctrl Pts',(-66.6805217354869,0.142025476984417,
135.722469905523));
#89877=CARTESIAN_POINT('Ctrl Pts',(-66.6882780382287,0.278871158475106,
135.714698074347));
#89878=CARTESIAN_POINT('Ctrl Pts',(-66.6960384807429,0.41578987862635,135.706922095111));
#89879=CARTESIAN_POINT('Ctrl Pts',(-66.7037989232571,0.552274505215999,
135.69342126211));
#89880=CARTESIAN_POINT('Ctrl Pts',(-66.7115593657713,0.687816286316394,
135.674277641374));
#89881=CARTESIAN_POINT('Ctrl Pts',(-66.7193322660367,0.823575651116645,
135.655103289599));
#89882=CARTESIAN_POINT('Ctrl Pts',(-66.7271051663021,0.958388761177205,
135.630268119585));
#89883=CARTESIAN_POINT('Ctrl Pts',(-66.7348780665676,1.09175768058041,135.599905240379));
#89884=CARTESIAN_POINT('Ctrl Pts',(-66.7423684023296,1.22027830382709,135.570646128312));
#89885=CARTESIAN_POINT('Ctrl Pts',(-66.7498587380916,1.34745761606107,135.536254302324));
#89886=CARTESIAN_POINT('Ctrl Pts',(-66.7573490738536,1.47286650206953,135.496891632869));
#89887=CARTESIAN_POINT('Ctrl Pts',(-66.7651234079727,1.60303030410823,135.456036515837));
#89888=CARTESIAN_POINT('Ctrl Pts',(-66.7728977420918,1.73169909813534,135.409696758652));
#89889=CARTESIAN_POINT('Ctrl Pts',(-66.7806720762109,1.85837590334509,135.357998950193));
#89890=CARTESIAN_POINT('Ctrl Pts',(-66.788436829158,1.98489659071403,135.306364854661));
#89891=CARTESIAN_POINT('Ctrl Pts',(-66.796201582105,2.10942981537455,135.249385992802));
#89892=CARTESIAN_POINT('Ctrl Pts',(-66.8039663350521,2.23149296100489,135.187238921545));
#89893=CARTESIAN_POINT('Ctrl Pts',(-66.8117233759371,2.35343487179804,135.125153575634));
#89894=CARTESIAN_POINT('Ctrl Pts',(-66.8194804168222,2.47291123962067,135.057910411741));
#89895=CARTESIAN_POINT('Ctrl Pts',(-66.8272374577072,2.58945901254748,134.985734205854));
#89896=CARTESIAN_POINT('Ctrl Pts',(-66.8349886489473,2.70591889589228,134.913612428606));
#89897=CARTESIAN_POINT('Ctrl Pts',(-66.8427398401874,2.81945424913524,134.836565218898));
#89898=CARTESIAN_POINT('Ctrl Pts',(-66.8504910314275,2.92962656726045,134.754863274052));
#89899=CARTESIAN_POINT('Ctrl Pts',(-66.8582389282046,3.03975205921122,134.673196054712));
#89900=CARTESIAN_POINT('Ctrl Pts',(-66.8659868249817,3.14651704559254,134.586878267489));
#89901=CARTESIAN_POINT('Ctrl Pts',(-66.8737347217587,3.24951216621316,134.496223798147));
#89902=CARTESIAN_POINT('Ctrl Pts',(-66.8814809978428,3.35248574247486,134.405588291767));
#89903=CARTESIAN_POINT('Ctrl Pts',(-66.8892272739268,3.45169072820364,134.310618165768));
#89904=CARTESIAN_POINT('Ctrl Pts',(-66.8969735500109,3.54675133250987,134.211667185493));
#89905=CARTESIAN_POINT('Ctrl Pts',(-66.9047198832763,3.64181263853189,134.112715474785));
#89906=CARTESIAN_POINT('Ctrl Pts',(-66.9124662165416,3.73272923122931,134.009783133105));
#89907=CARTESIAN_POINT('Ctrl Pts',(-66.9202125498069,3.81916292724842,133.903260034719));
#89908=CARTESIAN_POINT('Ctrl Pts',(-66.9279606178099,3.90561597949447,133.796713081224));
#89909=CARTESIAN_POINT('Ctrl Pts',(-66.9357086858128,3.98758389109744,133.686574074445));
#89910=CARTESIAN_POINT('Ctrl Pts',(-66.9434567538158,4.06476969042986,133.573264809889));
#89911=CARTESIAN_POINT('Ctrl Pts',(-66.9512130565576,4.14203752374834,133.459835118898));
#89912=CARTESIAN_POINT('Ctrl Pts',(-66.9589693592995,4.21451287152458,133.343228763051));
#89913=CARTESIAN_POINT('Ctrl Pts',(-66.9667256620413,4.28194264333406,133.223895750954));
#89914=CARTESIAN_POINT('Ctrl Pts',(-66.9744861045555,4.34940840444312,133.104499047235));
#89915=CARTESIAN_POINT('Ctrl Pts',(-66.9822465470696,4.41182304576945,132.982373135426));
#89916=CARTESIAN_POINT('Ctrl Pts',(-66.9900069895838,4.46898061894604,132.857990401628));
#89917=CARTESIAN_POINT('Ctrl Pts',(-66.9977798898492,4.5262299465333,132.733407997622));
#89918=CARTESIAN_POINT('Ctrl Pts',(-67.0055527901146,4.578205193613,132.606561893998));
#89919=CARTESIAN_POINT('Ctrl Pts',(-67.0133256903801,4.6247492020701,132.477942967034));
#89920=CARTESIAN_POINT('Ctrl Pts',(-67.0208160261422,4.66960121858307,132.353999662036));
#89921=CARTESIAN_POINT('Ctrl Pts',(-67.0283063619043,4.70940992614292,132.228410482733));
#89922=CARTESIAN_POINT('Ctrl Pts',(-67.0357966976664,4.74407956369188,132.101623950842));
#89923=CARTESIAN_POINT('Ctrl Pts',(-67.0435710317855,4.78006371108571,131.970030269058));
#89924=CARTESIAN_POINT('Ctrl Pts',(-67.0513453659046,4.81062538703736,131.836729797883));
#89925=CARTESIAN_POINT('Ctrl Pts',(-67.0591197000237,4.83560246409114,131.702209085725));
#89926=CARTESIAN_POINT('Ctrl Pts',(-67.0668844529708,4.86054875912971,131.567854158322));
#89927=CARTESIAN_POINT('Ctrl Pts',(-67.0746492059179,4.87992407874462,131.43228236283));
#89928=CARTESIAN_POINT('Ctrl Pts',(-67.082413958865,4.89361609937007,131.295995171362));
#89929=CARTESIAN_POINT('Ctrl Pts',(-67.09017099975,4.90729452088759,131.159843342254));
#89930=CARTESIAN_POINT('Ctrl Pts',(-67.097928040635,4.91530083785992,131.022977917668));
#89931=CARTESIAN_POINT('Ctrl Pts',(-67.10568508152,4.91757386981557,130.885909973217));
#89932=CARTESIAN_POINT('Ctrl Pts',(-67.1134362727602,4.91984518766016,130.748945392768));
#89933=CARTESIAN_POINT('Ctrl Pts',(-67.1211874640003,4.91639181972575,130.611778985766));
#89934=CARTESIAN_POINT('Ctrl Pts',(-67.1289386552404,4.90720448866213,130.474925997415));
#89935=CARTESIAN_POINT('Ctrl Pts',(-67.1366865520175,4.89802106245932,130.338131175234));
#89936=CARTESIAN_POINT('Ctrl Pts',(-67.1444344487947,4.88310854644099,130.201649896027));
#89937=CARTESIAN_POINT('Ctrl Pts',(-67.1521823455718,4.86250975240698,130.065996229038));
#89938=CARTESIAN_POINT('Ctrl Pts',(-67.1599286216559,4.84191526719659,129.930370937871));
#89939=CARTESIAN_POINT('Ctrl Pts',(-67.1676748977398,4.81563692850278,129.795573300869));
#89940=CARTESIAN_POINT('Ctrl Pts',(-67.1754211738239,4.78376924497211,129.662110700359));
#89941=CARTESIAN_POINT('Ctrl Pts',(-67.1831675070893,4.75190132620147,129.528647114659));
#89942=CARTESIAN_POINT('Ctrl Pts',(-67.1909138403547,4.71444407106468,129.39651896539));
#89943=CARTESIAN_POINT('Ctrl Pts',(-67.19866017362,4.67154269546031,129.266221512351));
#89944=CARTESIAN_POINT('Ctrl Pts',(-67.206408241623,4.62863171239034,129.135894880101));
#89945=CARTESIAN_POINT('Ctrl Pts',(-67.214156309626,4.58027430508712,129.007400131158));
#89946=CARTESIAN_POINT('Ctrl Pts',(-67.221904377629,4.52666482163802,128.881215106939));
#89947=CARTESIAN_POINT('Ctrl Pts',(-67.2296606803708,4.47299836139194,128.754895971775));
#89948=CARTESIAN_POINT('Ctrl Pts',(-67.2374169831126,4.41406882753546,128.630891825478));
#89949=CARTESIAN_POINT('Ctrl Pts',(-67.2451732858545,4.35011802349843,128.509658840835));
#89950=CARTESIAN_POINT('Ctrl Pts',(-67.2529337283686,4.28613308699168,128.388361150497));
#89951=CARTESIAN_POINT('Ctrl Pts',(-67.2606941708829,4.21712173680047,128.269837906651));
#89952=CARTESIAN_POINT('Ctrl Pts',(-67.2684546133971,4.14337008460657,128.154517715716));
#89953=CARTESIAN_POINT('Ctrl Pts',(-67.2762275136625,4.0695000397132,128.039012402572));
#89954=CARTESIAN_POINT('Ctrl Pts',(-67.2840004139279,3.99087471087767,127.926720737791));
#89955=CARTESIAN_POINT('Ctrl Pts',(-67.2917733141934,3.9078221384177,127.818040273565));
#89956=CARTESIAN_POINT('Ctrl Pts',(-67.2992636499554,3.8277887361638,127.713310617965));
#89957=CARTESIAN_POINT('Ctrl Pts',(-67.3067539857174,3.7436445815651,127.611934405756));
#89958=CARTESIAN_POINT('Ctrl Pts',(-67.3142443214794,3.65571526745278,127.514234640371));
#89959=CARTESIAN_POINT('Ctrl Pts',(-67.3220186555985,3.56445208666996,127.412830558687));
#89960=CARTESIAN_POINT('Ctrl Pts',(-67.3297929897175,3.46882195736728,127.315065994442));
#89961=CARTESIAN_POINT('Ctrl Pts',(-67.3375673238366,3.36914659265055,127.221340341356));
#89962=CARTESIAN_POINT('Ctrl Pts',(-67.3453320767837,3.26959406891244,127.127730196761));
#89963=CARTESIAN_POINT('Ctrl Pts',(-67.3530968297308,3.1660065112925,127.038149324643));
#89964=CARTESIAN_POINT('Ctrl Pts',(-67.3608615826779,3.05874510885052,126.952963283924));
#89965=CARTESIAN_POINT('Ctrl Pts',(-67.3686186235629,2.95159023994586,126.867861851182));
#89966=CARTESIAN_POINT('Ctrl Pts',(-67.3763756644479,2.84076909190066,126.78714680485));
#89967=CARTESIAN_POINT('Ctrl Pts',(-67.3841327053329,2.72667857756171,126.711145866644));
#89968=CARTESIAN_POINT('Ctrl Pts',(-67.391883896573,2.6126740997679,126.635202241337));
#89969=CARTESIAN_POINT('Ctrl Pts',(-67.399635087813,2.49540548708247,126.563965864125));
#89970=CARTESIAN_POINT('Ctrl Pts',(-67.4073862790531,2.37530121525251,126.497723042924));
#89971=CARTESIAN_POINT('Ctrl Pts',(-67.4151341758302,2.25524799094115,126.431508376688));
#89972=CARTESIAN_POINT('Ctrl Pts',(-67.4228820726073,2.13236184622706,126.370283233607));
#89973=CARTESIAN_POINT('Ctrl Pts',(-67.4306299693844,2.00709842294861,126.314289461883));
#89974=CARTESIAN_POINT('Ctrl Pts',(-67.4383762454685,1.88186120207777,126.258307402849));
#89975=CARTESIAN_POINT('Ctrl Pts',(-67.4461225215526,1.75424804845261,126.207554698018));
#89976=CARTESIAN_POINT('Ctrl Pts',(-67.4538687976367,1.62473692142669,126.162226087131));
#89977=CARTESIAN_POINT('Ctrl Pts',(-67.461615130902,1.49522483837958,126.116897141639));
#89978=CARTESIAN_POINT('Ctrl Pts',(-67.4693614641674,1.36381512299099,126.076992499141));
#89979=CARTESIAN_POINT('Ctrl Pts',(-67.4771077974327,1.23100294409522,126.042657685407));
#89980=CARTESIAN_POINT('Ctrl Pts',(-67.4848558654357,1.09816102283176,126.00831518263));
#89981=CARTESIAN_POINT('Ctrl Pts',(-67.4926039334387,0.963916391542621,
125.979545088484));
#89982=CARTESIAN_POINT('Ctrl Pts',(-67.5003520014418,0.828776121632136,
125.956442177378));
#89983=CARTESIAN_POINT('Ctrl Pts',(-67.5081083041836,0.693492223035338,
125.933314712224));
#89984=CARTESIAN_POINT('Ctrl Pts',(-67.5158646069254,0.557311170292499,
125.915866527985));
#89985=CARTESIAN_POINT('Ctrl Pts',(-67.5236209096673,0.420747455148574,
125.904140761122));
#89986=CARTESIAN_POINT('Ctrl Pts',(-67.5313813521815,0.28411085183821,125.892408735865));
#89987=CARTESIAN_POINT('Ctrl Pts',(-67.5391417946956,0.147091569563719,
125.886405230893));
#89988=CARTESIAN_POINT('Ctrl Pts',(-67.5469022372098,0.0102048573974459,
125.886121204586));
#89989=CARTESIAN_POINT('Ctrl Pts',(-67.5546751374752,-0.126901597471801,
125.885836722335));
#89990=CARTESIAN_POINT('Ctrl Pts',(-67.5624480377406,-0.263874666083487,
125.891290050579));
#89991=CARTESIAN_POINT('Ctrl Pts',(-67.570220938006,-0.400202562713456,
125.902420086379));
#89992=CARTESIAN_POINT('Ctrl Pts',(-67.5777112737681,-0.531574596912417,
125.913145517342));
#89993=CARTESIAN_POINT('Ctrl Pts',(-67.5852016095302,-0.662347246264545,
125.929142058742));
#89994=CARTESIAN_POINT('Ctrl Pts',(-67.5926919452923,-0.792072767955476,
125.950310371353));
#89995=CARTESIAN_POINT('Ctrl Pts',(-67.6004662794114,-0.926716872229778,
125.97228128697));
#89996=CARTESIAN_POINT('Ctrl Pts',(-67.6082406135304,-1.06065938974916,
125.999893488132));
#89997=CARTESIAN_POINT('Ctrl Pts',(-67.6160149476495,-1.19339040547402,
126.033092190552));
#89998=CARTESIAN_POINT('Ctrl Pts',(-67.6237797005965,-1.32595784208378,
126.066249978538));
#89999=CARTESIAN_POINT('Ctrl Pts',(-67.6315444535437,-1.45731637201854,
126.104980475001));
#90000=CARTESIAN_POINT('Ctrl Pts',(-67.6393092064907,-1.58696320869375,
126.149177394883));
#90001=CARTESIAN_POINT('Ctrl Pts',(-67.6470662473757,-1.71648127830342,
126.19333041776));
#90002=CARTESIAN_POINT('Ctrl Pts',(-67.6548232882607,-1.84429067022652,
126.242938934112));
#90003=CARTESIAN_POINT('Ctrl Pts',(-67.6625803291456,-1.96990112181394,
126.29784615151));
#90004=CARTESIAN_POINT('Ctrl Pts',(-67.6703315203858,-2.0954168495827,126.352711962947));
#90005=CARTESIAN_POINT('Ctrl Pts',(-67.6780827116259,-2.21873658085227,
126.412868366091));
#90006=CARTESIAN_POINT('Ctrl Pts',(-67.6858339028661,-2.3393878350576,126.478109628582));
#90007=CARTESIAN_POINT('Ctrl Pts',(-67.6935817996431,-2.45998780926175,
126.543323161796));
#90008=CARTESIAN_POINT('Ctrl Pts',(-67.7013296964201,-2.57792121900156,
126.613617070318));
#90009=CARTESIAN_POINT('Ctrl Pts',(-67.7090775931972,-2.69273830499027,
126.688738734626));
#90010=CARTESIAN_POINT('Ctrl Pts',(-67.7168238692813,-2.80753137371962,
126.763844685101));
#90011=CARTESIAN_POINT('Ctrl Pts',(-67.7245701453654,-2.91920908834374,
126.843776168773));
#90012=CARTESIAN_POINT('Ctrl Pts',(-67.7323164214496,-3.02734926009838,
126.928236326488));
#90013=CARTESIAN_POINT('Ctrl Pts',(-67.7400627547149,-3.13549023011905,
127.012697107669));
#90014=CARTESIAN_POINT('Ctrl Pts',(-67.7478090879802,-3.2400932970392,127.101686388947));
#90015=CARTESIAN_POINT('Ctrl Pts',(-67.7555554212455,-3.34076837505722,
127.194866230991));
#90016=CARTESIAN_POINT('Ctrl Pts',(-67.7633034892485,-3.44146599856053,
127.288066940014));
#90017=CARTESIAN_POINT('Ctrl Pts',(-67.7710515572514,-3.53823359589458,
127.385459811688));
#90018=CARTESIAN_POINT('Ctrl Pts',(-67.7787996252544,-3.63071734618682,
127.486669460361));
#90019=CARTESIAN_POINT('Ctrl Pts',(-67.7865559279962,-3.72329938930995,
127.587986675853));
#90020=CARTESIAN_POINT('Ctrl Pts',(-67.7943122307381,-3.81158822628296,
127.693128482597));
#90021=CARTESIAN_POINT('Ctrl Pts',(-67.8020685334799,-3.8952694698251,127.801685340426));
#90022=CARTESIAN_POINT('Ctrl Pts',(-67.8098289759941,-3.97899537656674,
127.910300138319));
#90023=CARTESIAN_POINT('Ctrl Pts',(-67.8175894185082,-4.05810856427903,
128.022333300004));
#90024=CARTESIAN_POINT('Ctrl Pts',(-67.8253498610224,-4.13233813522523,
128.137346444626));
#90025=CARTESIAN_POINT('Ctrl Pts',(-67.8331227612879,-4.20668686606839,
128.252544218558));
#90026=CARTESIAN_POINT('Ctrl Pts',(-67.8408956615533,-4.2761361159087,128.370731197581));
#90027=CARTESIAN_POINT('Ctrl Pts',(-67.8486685618188,-4.34046065969393,
128.491443774238));
#90028=CARTESIAN_POINT('Ctrl Pts',(-67.8561588975809,-4.40244684428977,
128.607768144679));
#90029=CARTESIAN_POINT('Ctrl Pts',(-67.863649233343,-4.45967431223964,128.726437399618));
#90030=CARTESIAN_POINT('Ctrl Pts',(-67.8711395691052,-4.51198462451892,
128.847021145066));
#90031=CARTESIAN_POINT('Ctrl Pts',(-67.8797294403174,-4.57197377050905,
128.985305846391));
#90032=CARTESIAN_POINT('Ctrl Pts',(-67.8883193115296,-4.62565936726916,
129.126483064055));
#90033=CARTESIAN_POINT('Ctrl Pts',(-67.8969091827418,-4.67278164609967,
129.269989492194));
#90034=CARTESIAN_POINT('Ctrl Pts',(-67.9030767774944,-4.70661581106723,
129.373028230644));
#90035=CARTESIAN_POINT('Ctrl Pts',(-67.9092443722471,-4.73706726407475,
129.47726718594));
#90036=CARTESIAN_POINT('Ctrl Pts',(-67.9154119669996,-4.76405452823407,
129.582490119308));
#90037=CARTESIAN_POINT('Ctrl Pts',(-66.1650696236364,-4.76405452823402,
129.582490119308));
#90038=CARTESIAN_POINT('Ctrl Pts',(-66.1728438719774,-4.79808884234628,
129.715189393489));
#90039=CARTESIAN_POINT('Ctrl Pts',(-66.1806181203184,-4.82653451571629,
129.849155293682));
#90040=CARTESIAN_POINT('Ctrl Pts',(-66.1883923686595,-4.84932882642928,
129.983877226106));
#90041=CARTESIAN_POINT('Ctrl Pts',(-66.1924128545156,-4.861117001929,130.053549250984));
#90042=CARTESIAN_POINT('Ctrl Pts',(-66.1964333403718,-4.87139458023908,
130.12342340788));
#90043=CARTESIAN_POINT('Ctrl Pts',(-66.200453826228,-4.88015835202264,130.193428934246));
#90044=CARTESIAN_POINT('Ctrl Pts',(-66.2120160721548,-4.905361496178,130.394753137599));
#90045=CARTESIAN_POINT('Ctrl Pts',(-66.2235783180815,-4.91811032154685,
130.597668476328));
#90046=CARTESIAN_POINT('Ctrl Pts',(-66.2351405640084,-4.91824885854007,
130.801009801352));
#90047=CARTESIAN_POINT('',(-65.889859435952,-4.91824814305622,130.808634471095));
#90048=CARTESIAN_POINT('Ctrl Pts',(-65.8197716842484,-4.76405452823398,
129.582490119308));
#90049=CARTESIAN_POINT('Ctrl Pts',(-65.8274085485116,-4.79766926250685,
129.713553458063));
#90050=CARTESIAN_POINT('Ctrl Pts',(-65.8350454127747,-4.82585821990346,
129.845954040388));
#90051=CARTESIAN_POINT('Ctrl Pts',(-65.8426822770379,-4.84853448028878,
129.979196115209));
#90052=CARTESIAN_POINT('Ctrl Pts',(-65.8505451368569,-4.87188179280929,
130.116381184918));
#90053=CARTESIAN_POINT('Ctrl Pts',(-65.858407996676,-4.88938500251125,130.254457868088));
#90054=CARTESIAN_POINT('Ctrl Pts',(-65.866270856495,-4.90100668618583,130.392879725589));
#90055=CARTESIAN_POINT('Ctrl Pts',(-65.874133716314,-4.91262836986042,130.531301583091));
#90056=CARTESIAN_POINT('Ctrl Pts',(-65.8819965761329,-4.91836855425554,
130.670068150686));
#90057=CARTESIAN_POINT('Ctrl Pts',(-65.8898594359519,-4.91824814305622,
130.808634471095));
#90058=CARTESIAN_POINT('Ctrl Pts',(-65.8898594359911,-4.91824814305563,
130.808634471784));
#90059=CARTESIAN_POINT('Ctrl Pts',(-65.9014631194068,-4.91807044515766,
131.013124918148));
#90060=CARTESIAN_POINT('Ctrl Pts',(-65.9130668028225,-4.90513620346425,
131.217082535833));
#90061=CARTESIAN_POINT('Ctrl Pts',(-65.9246704862381,-4.87966224002228,
131.419242301958));
#90062=CARTESIAN_POINT('Ctrl Pts',(-65.9303120570168,-4.86727710655853,
131.517529939458));
#90063=CARTESIAN_POINT('Ctrl Pts',(-65.9359536277956,-4.85192848519588,
131.615393185222));
#90064=CARTESIAN_POINT('Ctrl Pts',(-65.9415951985743,-4.83364483722309,
131.712689109956));
#90065=CARTESIAN_POINT('Ctrl Pts',(-65.9493695326934,-4.80844916143868,
131.84676719866));
#90066=CARTESIAN_POINT('Ctrl Pts',(-65.9571438668125,-4.77763066080824,
131.980008527351));
#90067=CARTESIAN_POINT('Ctrl Pts',(-65.9649182009316,-4.74125634039637,
132.111904642504));
#90068=CARTESIAN_POINT('Ctrl Pts',(-65.9726829538787,-4.70492684808359,
132.243638207482));
#90069=CARTESIAN_POINT('Ctrl Pts',(-65.9804477068258,-4.66305526252321,
132.374029484283));
#90070=CARTESIAN_POINT('Ctrl Pts',(-65.9882124597729,-4.61575990365766,
132.502578381661));
#90071=CARTESIAN_POINT('Ctrl Pts',(-65.9959695006579,-4.56851151920922,
132.630999602461));
#90072=CARTESIAN_POINT('Ctrl Pts',(-66.003726541543,-4.51585021588766,132.757581720831));
#90073=CARTESIAN_POINT('Ctrl Pts',(-66.011483582428,-4.45794450591964,132.88183837789));
#90074=CARTESIAN_POINT('Ctrl Pts',(-66.0192347736681,-4.40008246309811,
133.006001332037));
#90075=CARTESIAN_POINT('Ctrl Pts',(-66.0269859649082,-4.33698404999113,
133.127841962465));
#90076=CARTESIAN_POINT('Ctrl Pts',(-66.0347371561483,-4.26886627794321,
133.246892861681));
#90077=CARTESIAN_POINT('Ctrl Pts',(-66.0424850529254,-4.20077745776532,
133.365893161088));
#90078=CARTESIAN_POINT('Ctrl Pts',(-66.0502329497024,-4.12767371549681,
133.482105748937));
#90079=CARTESIAN_POINT('Ctrl Pts',(-66.0579808464795,-4.04981839089362,
133.595087057631));
#90080=CARTESIAN_POINT('Ctrl Pts',(-66.0657271225636,-3.97197935194598,
133.708044733072));
#90081=CARTESIAN_POINT('Ctrl Pts',(-66.0734733986479,-3.88939092934408,
133.817772152061));
#90082=CARTESIAN_POINT('Ctrl Pts',(-66.081219674732,-3.8023600281203,133.923854371215));
#90083=CARTESIAN_POINT('Ctrl Pts',(-66.0889660079974,-3.71532848445418,
134.029937373444));
#90084=CARTESIAN_POINT('Ctrl Pts',(-66.0967123412627,-3.62385464470653,
134.132374819885));
#90085=CARTESIAN_POINT('Ctrl Pts',(-66.104458674528,-3.52828571187385,134.230784846684));
#90086=CARTESIAN_POINT('Ctrl Pts',(-66.112206742531,-3.43269537704155,134.329216911726));
#90087=CARTESIAN_POINT('Ctrl Pts',(-66.119954810534,-3.33300839658943,134.423619482005));
#90088=CARTESIAN_POINT('Ctrl Pts',(-66.127702878537,-3.22960853879268,134.513647846759));
#90089=CARTESIAN_POINT('Ctrl Pts',(-66.1354591812789,-3.12609878639644,
134.603771894732));
#90090=CARTESIAN_POINT('Ctrl Pts',(-66.1432154840207,-3.01886856924686,
134.689512193247));
#90091=CARTESIAN_POINT('Ctrl Pts',(-66.1509717867625,-2.90833485400029,
134.770564273394));
#90092=CARTESIAN_POINT('Ctrl Pts',(-66.1587322292767,-2.79774214358164,
134.851659613478));
#90093=CARTESIAN_POINT('Ctrl Pts',(-66.1664926717908,-2.68384274631323,
134.928061531575));
#90094=CARTESIAN_POINT('Ctrl Pts',(-66.174253114305,-2.56708141760555,134.999509727894));
#90095=CARTESIAN_POINT('Ctrl Pts',(-66.1820260145704,-2.45013265324744,
135.0710726192));
#90096=CARTESIAN_POINT('Ctrl Pts',(-66.1897989148359,-2.3303131186512,135.137665707753));
#90097=CARTESIAN_POINT('Ctrl Pts',(-66.1975718151014,-2.20809169254464,
135.19907495866));
#90098=CARTESIAN_POINT('Ctrl Pts',(-66.2050621508634,-2.09031332313426,
135.258251828616));
#90099=CARTESIAN_POINT('Ctrl Pts',(-66.2125524866254,-1.97030494057341,
135.312615081556));
#90100=CARTESIAN_POINT('Ctrl Pts',(-66.2200428223875,-1.84850061700697,
135.362016652352));
#90101=CARTESIAN_POINT('Ctrl Pts',(-66.2278171565065,-1.72207804549089,
135.41329129872));
#90102=CARTESIAN_POINT('Ctrl Pts',(-66.2355914906256,-1.59332018969813,
135.459383014073));
#90103=CARTESIAN_POINT('Ctrl Pts',(-66.2433658247447,-1.46269104385342,
135.500073340117));
#90104=CARTESIAN_POINT('Ctrl Pts',(-66.2511305776918,-1.3322228867563,135.540713518972));
#90105=CARTESIAN_POINT('Ctrl Pts',(-66.2588953306389,-1.19988839794507,
135.57596543827));
#90106=CARTESIAN_POINT('Ctrl Pts',(-66.266660083586,-1.0661722731674,135.605658332396));
#90107=CARTESIAN_POINT('Ctrl Pts',(-66.274417124471,-0.932588957130112,
135.635321735121));
#90108=CARTESIAN_POINT('Ctrl Pts',(-66.282174165356,-0.797627115184929,
135.659437016109));
#90109=CARTESIAN_POINT('Ctrl Pts',(-66.289931206241,-0.661787019806354,
135.677883060616));
#90110=CARTESIAN_POINT('Ctrl Pts',(-66.2976823974811,-0.526049362500386,
135.696315194818));
#90111=CARTESIAN_POINT('Ctrl Pts',(-66.3054335887212,-0.389435155866664,
135.7090865497));
#90112=CARTESIAN_POINT('Ctrl Pts',(-66.3131847799613,-0.252454942999151,
135.716127057886));
#90113=CARTESIAN_POINT('Ctrl Pts',(-66.3209326767384,-0.115532950375987,
135.723164573669));
#90114=CARTESIAN_POINT('Ctrl Pts',(-66.3286805735155,0.0217543494468244,
135.724476067275));
#90115=CARTESIAN_POINT('Ctrl Pts',(-66.3364284702926,0.158891428918405,
135.72004333478));
#90116=CARTESIAN_POINT('Ctrl Pts',(-66.3441747463767,0.295999822269294,
135.715611529517));
#90117=CARTESIAN_POINT('Ctrl Pts',(-66.3519210224609,0.432957667257184,
135.705437900761));
#90118=CARTESIAN_POINT('Ctrl Pts',(-66.359667298545,0.569249970595441,135.689556369373));
#90119=CARTESIAN_POINT('Ctrl Pts',(-66.3674136318104,0.705543280012333,
135.673674720752));
#90120=CARTESIAN_POINT('Ctrl Pts',(-66.3751599650757,0.841170649638669,
135.652085130674));
#90121=CARTESIAN_POINT('Ctrl Pts',(-66.3829062983411,0.975623134898289,
135.624873304112));
#90122=CARTESIAN_POINT('Ctrl Pts',(-66.390654366344,1.11010572985975,135.597655383651));
#90123=CARTESIAN_POINT('Ctrl Pts',(-66.398402434347,1.24341253377916,135.564812798861));
#90124=CARTESIAN_POINT('Ctrl Pts',(-66.40615050235,1.37504609560438,135.526482100275));
#90125=CARTESIAN_POINT('Ctrl Pts',(-66.4139068050918,1.50681955914575,135.488110663367));
#90126=CARTESIAN_POINT('Ctrl Pts',(-66.4216631078336,1.63691585219103,135.444239570432));
#90127=CARTESIAN_POINT('Ctrl Pts',(-66.4294194105755,1.76485343576031,135.395055054444));
#90128=CARTESIAN_POINT('Ctrl Pts',(-66.4371798530897,1.89285930347006,135.345844287199));
#90129=CARTESIAN_POINT('Ctrl Pts',(-66.4449402956039,2.01870380735118,135.291314601431));
#90130=CARTESIAN_POINT('Ctrl Pts',(-66.4527007381181,2.1419275486525,135.231699484066));
#90131=CARTESIAN_POINT('Ctrl Pts',(-66.4604736383835,2.26534909964264,135.171988667222));
#90132=CARTESIAN_POINT('Ctrl Pts',(-66.468246538649,2.38614113626038,135.10717629029));
#90133=CARTESIAN_POINT('Ctrl Pts',(-66.4760194389144,2.50387014448361,135.037541143136));
#90134=CARTESIAN_POINT('Ctrl Pts',(-66.4835097746765,2.61731940671614,134.970437408981));
#90135=CARTESIAN_POINT('Ctrl Pts',(-66.4910001104383,2.72792421320384,134.898855624029));
#90136=CARTESIAN_POINT('Ctrl Pts',(-66.4984904462003,2.83532536596307,134.823080952651));
#90137=CARTESIAN_POINT('Ctrl Pts',(-66.5062647803194,2.94679866607336,134.744433261576));
#90138=CARTESIAN_POINT('Ctrl Pts',(-66.5140391144386,3.05517369772571,134.661019328886));
#90139=CARTESIAN_POINT('Ctrl Pts',(-66.5218134485577,3.16001586556039,134.573111444021));
#90140=CARTESIAN_POINT('Ctrl Pts',(-66.5295782015048,3.26472882479324,134.485311897768));
#90141=CARTESIAN_POINT('Ctrl Pts',(-66.5373429544518,3.3659172865368,134.39302966788));
#90142=CARTESIAN_POINT('Ctrl Pts',(-66.5451077073989,3.46317559095159,134.296580239631));
#90143=CARTESIAN_POINT('Ctrl Pts',(-66.5528647482839,3.5603372970472,134.200226606315));
#90144=CARTESIAN_POINT('Ctrl Pts',(-66.5606217891689,3.6535763381209,134.099714284791));
#90145=CARTESIAN_POINT('Ctrl Pts',(-66.5683788300539,3.74252040741471,133.995398702983));
#90146=CARTESIAN_POINT('Ctrl Pts',(-66.5761300212941,3.83139740329399,133.891161786367));
#90147=CARTESIAN_POINT('Ctrl Pts',(-66.5838812125341,3.91598562153294,133.783127614483));
#90148=CARTESIAN_POINT('Ctrl Pts',(-66.5916324037742,3.99595015145007,133.671687848565));
#90149=CARTESIAN_POINT('Ctrl Pts',(-66.5993803005513,4.07588069430896,133.56029544752));
#90150=CARTESIAN_POINT('Ctrl Pts',(-66.6071281973284,4.15119123000632,133.44550064833));
#90151=CARTESIAN_POINT('Ctrl Pts',(-66.6148760941055,4.22158778783065,133.327727339257));
#90152=CARTESIAN_POINT('Ctrl Pts',(-66.6226223701896,4.29196962021257,133.209978665823));
#90153=CARTESIAN_POINT('Ctrl Pts',(-66.6303686462738,4.35743931880516,133.089253057139));
#90154=CARTESIAN_POINT('Ctrl Pts',(-66.6381149223579,4.41774705573912,132.966002126699));
#90155=CARTESIAN_POINT('Ctrl Pts',(-66.6458612556232,4.47805523785109,132.842750286449));
#90156=CARTESIAN_POINT('Ctrl Pts',(-66.6536075888885,4.533201210435,132.716973438423));
#90157=CARTESIAN_POINT('Ctrl Pts',(-66.6613539221539,4.58298198253718,132.58914609774));
#90158=CARTESIAN_POINT('Ctrl Pts',(-66.6691019901569,4.63277390269812,132.46129013101));
#90159=CARTESIAN_POINT('Ctrl Pts',(-66.6768500581599,4.67719808968219,132.331383122124));
#90160=CARTESIAN_POINT('Ctrl Pts',(-66.6845981261629,4.71610054287537,132.199917399639));
#90161=CARTESIAN_POINT('Ctrl Pts',(-66.6923544289047,4.75504434205875,132.06831195382));
#90162=CARTESIAN_POINT('Ctrl Pts',(-66.7001107316464,4.78845457324821,131.935144860621));
#90163=CARTESIAN_POINT('Ctrl Pts',(-66.7078670343883,4.8162276359383,131.800921915893));
#90164=CARTESIAN_POINT('Ctrl Pts',(-66.7156274769024,4.84401552194822,131.666627332339));
#90165=CARTESIAN_POINT('Ctrl Pts',(-66.7233879194166,4.86616018122114,131.531276160003));
#90166=CARTESIAN_POINT('Ctrl Pts',(-66.7311483619308,4.88260973667466,131.395381109453));
#90167=CARTESIAN_POINT('Ctrl Pts',(-66.7389212621962,4.89908569841491,131.259267908103));
#90168=CARTESIAN_POINT('Ctrl Pts',(-66.7466941624616,4.90984825642155,131.122609473826));
#90169=CARTESIAN_POINT('Ctrl Pts',(-66.7544670627271,4.91489763958616,130.985921226979));
#90170=CARTESIAN_POINT('Ctrl Pts',(-66.7619573984891,4.91976346495411,130.854201942202));
#90171=CARTESIAN_POINT('Ctrl Pts',(-66.7694477342512,4.91932428155204,130.722455282764));
#90172=CARTESIAN_POINT('Ctrl Pts',(-66.7769380700132,4.91362585095671,130.591137590409));
#90173=CARTESIAN_POINT('Ctrl Pts',(-66.7847124041323,4.90771136263336,130.454840947836));
#90174=CARTESIAN_POINT('Ctrl Pts',(-66.7924867382513,4.89611221047146,130.318574696249));
#90175=CARTESIAN_POINT('Ctrl Pts',(-66.8002610723704,4.87882256988073,130.182851652126));
#90176=CARTESIAN_POINT('Ctrl Pts',(-66.8080258253175,4.86155423722683,130.047295874525));
#90177=CARTESIAN_POINT('Ctrl Pts',(-66.8157905782647,4.83860941889166,129.912282356481));
#90178=CARTESIAN_POINT('Ctrl Pts',(-66.8235553312117,4.81003427251879,129.778322918602));
#90179=CARTESIAN_POINT('Ctrl Pts',(-66.8313123720967,4.78148750738413,129.644496531126));
#90180=CARTESIAN_POINT('Ctrl Pts',(-66.8390694129817,4.74732162382006,129.51172252027));
#90181=CARTESIAN_POINT('Ctrl Pts',(-66.8468264538667,4.7076344125075,129.380506235729));
#90182=CARTESIAN_POINT('Ctrl Pts',(-66.8545776451068,4.66797712962972,129.24938890241));
#90183=CARTESIAN_POINT('Ctrl Pts',(-66.8623288363469,4.62280691927656,129.119827329957));
#90184=CARTESIAN_POINT('Ctrl Pts',(-66.8700800275871,4.57227226973397,128.992314990679));
#90185=CARTESIAN_POINT('Ctrl Pts',(-66.8778279243642,4.5217590987655,128.864856847546));
#90186=CARTESIAN_POINT('Ctrl Pts',(-66.8855758211412,4.46588616715587,128.739446567977));
#90187=CARTESIAN_POINT('Ctrl Pts',(-66.8933237179183,4.40485120575558,128.616560599819));
#90188=CARTESIAN_POINT('Ctrl Pts',(-66.9010699940024,4.34382901155337,128.493700336756));
#90189=CARTESIAN_POINT('Ctrl Pts',(-66.9088162700866,4.2776471091168,128.373363684752));
#90190=CARTESIAN_POINT('Ctrl Pts',(-66.9165625461707,4.20655041560103,128.256004939191));
#90191=CARTESIAN_POINT('Ctrl Pts',(-66.924308879436,4.13545319726571,128.138645327315));
#90192=CARTESIAN_POINT('Ctrl Pts',(-66.9320552127014,4.05944131803315,128.024264000137));
#90193=CARTESIAN_POINT('Ctrl Pts',(-66.9398015459667,3.97880427934194,127.913288226706));
#90194=CARTESIAN_POINT('Ctrl Pts',(-66.9475496139697,3.89814918254502,127.802287601021));
#90195=CARTESIAN_POINT('Ctrl Pts',(-66.9552976819727,3.81286709499761,127.694694362895));
#90196=CARTESIAN_POINT('Ctrl Pts',(-66.9630457499757,3.72328898556474,127.590904193017));
#90197=CARTESIAN_POINT('Ctrl Pts',(-66.9708020527175,3.63361567145118,127.487003713712));
#90198=CARTESIAN_POINT('Ctrl Pts',(-66.9785583554593,3.53963747050244,127.386914673324));
#90199=CARTESIAN_POINT('Ctrl Pts',(-66.9863146582012,3.44172392449089,127.290997628906));
#90200=CARTESIAN_POINT('Ctrl Pts',(-66.9940751007153,3.34375811907158,127.195029390673));
#90201=CARTESIAN_POINT('Ctrl Pts',(-67.0018355432295,3.24185307369125,127.103237846874));
#90202=CARTESIAN_POINT('Ctrl Pts',(-67.0095959857437,3.13641210544066,127.015943775751));
#90203=CARTESIAN_POINT('Ctrl Pts',(-67.0173688860091,3.03080187398722,126.928509572436));
#90204=CARTESIAN_POINT('Ctrl Pts',(-67.0251417862746,2.92164468835486,126.845587505779));
#90205=CARTESIAN_POINT('Ctrl Pts',(-67.03291468654,2.80937431000866,126.7674559805));
#90206=CARTESIAN_POINT('Ctrl Pts',(-67.0404050223021,2.70118524270706,126.692164732966));
#90207=CARTESIAN_POINT('Ctrl Pts',(-67.0478953580641,2.59010565750581,126.621321942883));
#90208=CARTESIAN_POINT('Ctrl Pts',(-67.0553856938261,2.4765442228886,126.5551357736));
#90209=CARTESIAN_POINT('Ctrl Pts',(-67.0631600279452,2.35867707196212,126.486440135592));
#90210=CARTESIAN_POINT('Ctrl Pts',(-67.0709343620643,2.23776279017286,126.42254359334));
#90211=CARTESIAN_POINT('Ctrl Pts',(-67.0787086961834,2.11422967621388,126.363728237069));
#90212=CARTESIAN_POINT('Ctrl Pts',(-67.0864734491305,1.99084880577738,126.304985365468));
#90213=CARTESIAN_POINT('Ctrl Pts',(-67.0942382020775,1.86485587449695,126.251311386574));
#90214=CARTESIAN_POINT('Ctrl Pts',(-67.1020029550246,1.73670644087972,126.202944118192));
#90215=CARTESIAN_POINT('Ctrl Pts',(-67.1097599959096,1.60868428708672,126.154624888864));
#90216=CARTESIAN_POINT('Ctrl Pts',(-67.1175170367946,1.47851025678424,126.111602018282));
#90217=CARTESIAN_POINT('Ctrl Pts',(-67.1252740776796,1.34666237323368,126.074066386229));
#90218=CARTESIAN_POINT('Ctrl Pts',(-67.1330252689197,1.21491391719774,126.036559060089));
#90219=CARTESIAN_POINT('Ctrl Pts',(-67.1407764601597,1.08149449487975,126.004530842718));
#90220=CARTESIAN_POINT('Ctrl Pts',(-67.1485276513999,0.946899540052417,
125.978123540552));
#90221=CARTESIAN_POINT('Ctrl Pts',(-67.1562755481769,0.812361791671318,
125.951727462193));
#90222=CARTESIAN_POINT('Ctrl Pts',(-67.164023444954,0.676649887359797,125.930947622537));
#90223=CARTESIAN_POINT('Ctrl Pts',(-67.1717713417311,0.540271554538408,
125.915875196717));
#90224=CARTESIAN_POINT('Ctrl Pts',(-67.1795176178152,0.403921749124083,
125.900805923723));
#90225=CARTESIAN_POINT('Ctrl Pts',(-67.1872638938993,0.266906180831998,
125.891441732817));
#90226=CARTESIAN_POINT('Ctrl Pts',(-67.1950101699834,0.129739444941043,
125.887822126013));
#90227=CARTESIAN_POINT('Ctrl Pts',(-67.2027565032487,-0.00742830348359602,
125.884202492489));
#90228=CARTESIAN_POINT('Ctrl Pts',(-67.2105028365141,-0.144746830904619,
125.886327537996));
#90229=CARTESIAN_POINT('Ctrl Pts',(-67.2182491697795,-0.281700181170313,
125.894184646134));
#90230=CARTESIAN_POINT('Ctrl Pts',(-67.2259972377824,-0.41868420118923,
125.902043513816));
#90231=CARTESIAN_POINT('Ctrl Pts',(-67.2337453057854,-0.555302491073616,
125.915636976066));
#90232=CARTESIAN_POINT('Ctrl Pts',(-67.2414933737884,-0.691043256697624,
125.934900454481));
#90233=CARTESIAN_POINT('Ctrl Pts',(-67.2492496765302,-0.826928289222488,
125.95418440635));
#90234=CARTESIAN_POINT('Ctrl Pts',(-67.2570059792721,-0.961933546727675,
125.979150357268));
#90235=CARTESIAN_POINT('Ctrl Pts',(-67.2647622820139,-1.09555593599869,
126.009682291171));
#90236=CARTESIAN_POINT('Ctrl Pts',(-67.272522724528,-1.22924964356233,126.040230520887));
#90237=CARTESIAN_POINT('Ctrl Pts',(-67.2802831670421,-1.36155863522941,
126.076350550109));
#90238=CARTESIAN_POINT('Ctrl Pts',(-67.2880436095563,-1.49199502843927,
126.117876445224));
#90239=CARTESIAN_POINT('Ctrl Pts',(-67.2958165098217,-1.62264080972711,
126.159469001392));
#90240=CARTESIAN_POINT('Ctrl Pts',(-67.3035894100872,-1.75140761802711,
126.206484630644));
#90241=CARTESIAN_POINT('Ctrl Pts',(-67.3113623103526,-1.87782676489667,
126.258708881727));
#90242=CARTESIAN_POINT('Ctrl Pts',(-67.3188526461147,-1.99965025734861,
126.309034649738));
#90243=CARTESIAN_POINT('Ctrl Pts',(-67.3263429818768,-2.11929353208964,
126.364196792235));
#90244=CARTESIAN_POINT('Ctrl Pts',(-67.333833317639,-2.23636056010105,126.423964002221));
#90245=CARTESIAN_POINT('Ctrl Pts',(-67.3416084934216,-2.35787937448386,
126.486004019978));
#90246=CARTESIAN_POINT('Ctrl Pts',(-67.3493836692043,-2.47700710437234,
126.553202821404));
#90247=CARTESIAN_POINT('Ctrl Pts',(-67.357158844987,-2.59327476208843,126.625352473184));
#90248=CARTESIAN_POINT('Ctrl Pts',(-67.3649242526913,-2.7093963508775,126.697411482196));
#90249=CARTESIAN_POINT('Ctrl Pts',(-67.3726896603956,-2.8226646882478,126.774408760587));
#90250=CARTESIAN_POINT('Ctrl Pts',(-67.3804550681,-2.9326333414837,126.856089508977));
#90251=CARTESIAN_POINT('Ctrl Pts',(-67.388343444619,-3.04434339909278,126.939063709713));
#90252=CARTESIAN_POINT('Ctrl Pts',(-67.396231821138,-3.15264800295381,127.026870814925));
#90253=CARTESIAN_POINT('Ctrl Pts',(-67.404120197657,-3.25710679850231,127.11919598547));
#90254=CARTESIAN_POINT('Ctrl Pts',(-67.411871035762,-3.35974429444228,127.209911413187));
#90255=CARTESIAN_POINT('Ctrl Pts',(-67.4196218738671,-3.4586686846207,127.304988375594));
#90256=CARTESIAN_POINT('Ctrl Pts',(-67.4273727119721,-3.55349349238493,
127.404086060699));
#90257=CARTESIAN_POINT('Ctrl Pts',(-67.4351200140234,-3.64827503958724,
127.503138535888));
#90258=CARTESIAN_POINT('Ctrl Pts',(-67.4428673160746,-3.7389604562633,127.60620780199));
#90259=CARTESIAN_POINT('Ctrl Pts',(-67.450614618126,-3.8251993177929,127.712915447155));
#90260=CARTESIAN_POINT('Ctrl Pts',(-67.4583600634878,-3.91141751163871,
127.819597519164));
#90261=CARTESIAN_POINT('Ctrl Pts',(-67.4661055088497,-3.99319102630841,
127.929915930614));
#90262=CARTESIAN_POINT('Ctrl Pts',(-67.4738509542115,-4.07020927977448,
128.043458684984));
#90263=CARTESIAN_POINT('Ctrl Pts',(-67.4818447167402,-4.14969672043453,
128.160641593504));
#90264=CARTESIAN_POINT('Ctrl Pts',(-67.489838479269,-4.22411861333894,128.281258709124));
#90265=CARTESIAN_POINT('Ctrl Pts',(-67.4978322417977,-4.29318177250914,
128.404824551845));
#90266=CARTESIAN_POINT('Ctrl Pts',(-67.5055816027224,-4.36013339198612,
128.524612487724));
#90267=CARTESIAN_POINT('Ctrl Pts',(-67.513330963647,-4.42204900608833,128.647171103629));
#90268=CARTESIAN_POINT('Ctrl Pts',(-67.5210803245717,-4.47870852322668,
128.772033619645));
#90269=CARTESIAN_POINT('Ctrl Pts',(-67.5291962879024,-4.53804845691893,
128.902803061309));
#90270=CARTESIAN_POINT('Ctrl Pts',(-67.5373122512332,-4.5916226393496,129.036099274335));
#90271=CARTESIAN_POINT('Ctrl Pts',(-67.5454282145639,-4.63923546684187,
129.171364185942));
#90272=CARTESIAN_POINT('Ctrl Pts',(-67.5535441778946,-4.68684829433408,
129.306629097549));
#90273=CARTESIAN_POINT('Ctrl Pts',(-67.5616601412252,-4.72849966024031,
129.443862228621));
#90274=CARTESIAN_POINT('Ctrl Pts',(-67.5697761045559,-4.76405452823408,
129.582490119308));
#90275=CARTESIAN_POINT('Origin',(213.235140564004,0.,130.804360617566));
#90276=CARTESIAN_POINT('',(-69.6652100424012,-4.76405452823405,129.582490119308));
#90277=CARTESIAN_POINT('',(-69.3201134481353,-4.76405452823409,129.582490119308));
#90278=CARTESIAN_POINT('',(213.235140564004,-4.76405452823405,129.582490119308));
#90279=CARTESIAN_POINT('',(-67.9851405639607,-4.91824943552146,130.802004244757));
#90280=CARTESIAN_POINT('Ctrl Pts',(-67.9851405640084,-4.91824943552187,
130.802004245604));
#90281=CARTESIAN_POINT('Ctrl Pts',(-67.9930107492047,-4.91831633734571,
130.941642580585));
#90282=CARTESIAN_POINT('Ctrl Pts',(-68.0008809344009,-4.91243199672117,
131.081266340895));
#90283=CARTESIAN_POINT('Ctrl Pts',(-68.0087511195972,-4.9006266186085,131.220343558906));
#90284=CARTESIAN_POINT('Ctrl Pts',(-68.0166239464927,-4.88881727791327,
131.359467459451));
#90285=CARTESIAN_POINT('Ctrl Pts',(-68.0244967733882,-4.87108297174089,
131.498044080167));
#90286=CARTESIAN_POINT('Ctrl Pts',(-68.0323696002838,-4.84750573826796,
131.635547227154));
#90287=CARTESIAN_POINT('Ctrl Pts',(-68.0402465527333,-4.82391614974754,
131.773122429157));
#90288=CARTESIAN_POINT('Ctrl Pts',(-68.0481235051828,-4.79447759725055,
131.909622669071));
#90289=CARTESIAN_POINT('Ctrl Pts',(-68.0560004576324,-4.75932307605186,
132.044532750885));
#90290=CARTESIAN_POINT('Ctrl Pts',(-68.0638888171598,-4.72411764552476,
132.179638203917));
#90291=CARTESIAN_POINT('Ctrl Pts',(-68.0717771766871,-4.68317980188223,
132.313148535996));
#90292=CARTESIAN_POINT('Ctrl Pts',(-68.0796655362145,-4.63669250378297,
132.444563558626));
#90293=CARTESIAN_POINT('Ctrl Pts',(-68.0875597502083,-4.59017070442584,
132.576076112922));
#90294=CARTESIAN_POINT('Ctrl Pts',(-68.0954539642021,-4.53809137900341,
132.70548991166));
#90295=CARTESIAN_POINT('Ctrl Pts',(-68.1033481781959,-4.48068511658272,
132.832326087818));
#90296=CARTESIAN_POINT('Ctrl Pts',(-68.1112570938165,-4.42317194479173,
132.959398474716));
#90297=CARTESIAN_POINT('Ctrl Pts',(-68.1191660094372,-4.36031217509731,
133.083883310427));
#90298=CARTESIAN_POINT('Ctrl Pts',(-68.1270749250578,-4.29238232005271,
133.205326481755));
#90299=CARTESIAN_POINT('Ctrl Pts',(-68.1345790143446,-4.2279295275402,133.320553454027));
#90300=CARTESIAN_POINT('Ctrl Pts',(-68.1420831036313,-4.15891291511128,
133.433042176827));
#90301=CARTESIAN_POINT('Ctrl Pts',(-68.1495871929181,-4.08560303385224,
133.542431272658));
#90302=CARTESIAN_POINT('Ctrl Pts',(-68.1573615270372,-4.00965304320633,
133.655759798943));
#90303=CARTESIAN_POINT('Ctrl Pts',(-68.1651358611562,-3.92886383360519,
133.766105325651));
#90304=CARTESIAN_POINT('Ctrl Pts',(-68.1729101952753,-3.84349718698554,
133.873026848379));
#90305=CARTESIAN_POINT('Ctrl Pts',(-68.1806749482224,-3.7582357471284,133.979816599887));
#90306=CARTESIAN_POINT('Ctrl Pts',(-68.1884397011695,-3.6684083363175,134.083190440921));
#90307=CARTESIAN_POINT('Ctrl Pts',(-68.1962044541166,-3.57432061425678,
134.182735257685));
#90308=CARTESIAN_POINT('Ctrl Pts',(-68.2039614950016,-3.48032634144814,
134.282181205133));
#90309=CARTESIAN_POINT('Ctrl Pts',(-68.2117185358867,-3.38208044488746,
134.377805414241));
#90310=CARTESIAN_POINT('Ctrl Pts',(-68.2194755767717,-3.27992931580752,
134.469227156174));
#90311=CARTESIAN_POINT('Ctrl Pts',(-68.2272267680118,-3.17785521968835,
134.56057995626));
#90312=CARTESIAN_POINT('Ctrl Pts',(-68.2349779592519,-3.07188204297807,
134.647736337425));
#90313=CARTESIAN_POINT('Ctrl Pts',(-68.242729150492,-2.96239329719065,134.730352086642));
#90314=CARTESIAN_POINT('Ctrl Pts',(-68.2504770472691,-2.85295108704103,
134.812932721962));
#90315=CARTESIAN_POINT('Ctrl Pts',(-68.2582249440463,-2.73999659111978,
134.890976328743));
#90316=CARTESIAN_POINT('Ctrl Pts',(-68.2659728408234,-2.62394652113391,
134.964178848779));
#90317=CARTESIAN_POINT('Ctrl Pts',(-68.2737191169075,-2.50792072632093,
135.037366056426));
#90318=CARTESIAN_POINT('Ctrl Pts',(-68.2814653929915,-2.38880097587663,
135.105713983094));
#90319=CARTESIAN_POINT('Ctrl Pts',(-68.2892116690756,-2.26703275805912,
135.16896203538));
#90320=CARTESIAN_POINT('Ctrl Pts',(-68.2969580023409,-2.14526364137646,
135.232210554549));
#90321=CARTESIAN_POINT('Ctrl Pts',(-68.3047043356064,-2.02084636526339,
135.290358944003));
#90322=CARTESIAN_POINT('Ctrl Pts',(-68.3124506688717,-1.89425043696567,
135.343192884191));
#90323=CARTESIAN_POINT('Ctrl Pts',(-68.3201987368747,-1.76762615838722,
135.396038656173));
#90324=CARTESIAN_POINT('Ctrl Pts',(-68.3279468048776,-1.63882261750664,
135.443567460109));
#90325=CARTESIAN_POINT('Ctrl Pts',(-68.3356948728806,-1.50832830551248,
135.485613525206));
#90326=CARTESIAN_POINT('Ctrl Pts',(-68.3434511756225,-1.37769530261081,
135.527704277361));
#90327=CARTESIAN_POINT('Ctrl Pts',(-68.3512074783644,-1.24536831167013,
135.564300530284));
#90328=CARTESIAN_POINT('Ctrl Pts',(-68.3589637811063,-1.11185049676045,
135.595286575599));
#90329=CARTESIAN_POINT('Ctrl Pts',(-68.3667242236205,-0.978261419372801,
135.626289159099));
#90330=CARTESIAN_POINT('Ctrl Pts',(-68.3744846661345,-0.843480635593314,
135.651675496189));
#90331=CARTESIAN_POINT('Ctrl Pts',(-68.3822451086487,-0.708019463434344,
135.671381421086));
#90332=CARTESIAN_POINT('Ctrl Pts',(-68.3900180089141,-0.572340836976147,
135.691118979684));
#90333=CARTESIAN_POINT('Ctrl Pts',(-68.3977909091796,-0.43598002866856,
135.705157863953));
#90334=CARTESIAN_POINT('Ctrl Pts',(-68.405563809445,-0.299452315932775,
135.713485934054));
#90335=CARTESIAN_POINT('Ctrl Pts',(-68.413054145207,-0.167887729448603,
135.721511257829));
#90336=CARTESIAN_POINT('Ctrl Pts',(-68.4205444809689,-0.0361684706039233,
135.724233757462));
#90337=CARTESIAN_POINT('Ctrl Pts',(-68.4280348167309,0.0952481521205627,
135.721688230408));
#90338=CARTESIAN_POINT('Ctrl Pts',(-68.43580915085,0.231647476039649,135.719046188922));
#90339=CARTESIAN_POINT('Ctrl Pts',(-68.443583484969,0.368152833981991,135.71072039134));
#90340=CARTESIAN_POINT('Ctrl Pts',(-68.4513578190881,0.504251696922477,
135.696692708568));
#90341=CARTESIAN_POINT('Ctrl Pts',(-68.4591225720352,0.640182830177709,
135.682682313662));
#90342=CARTESIAN_POINT('Ctrl Pts',(-68.4668873249823,0.775708080038133,
135.662984055028));
#90343=CARTESIAN_POINT('Ctrl Pts',(-68.4746520779293,0.91031466563093,135.637631794733));
#90344=CARTESIAN_POINT('Ctrl Pts',(-68.4824091188143,1.04478755806548,135.612304714662));
#90345=CARTESIAN_POINT('Ctrl Pts',(-68.4901661596993,1.17834322028607,135.58133488019));
#90346=CARTESIAN_POINT('Ctrl Pts',(-68.4979232005843,1.31047410142037,135.54480792684));
#90347=CARTESIAN_POINT('Ctrl Pts',(-68.5056743918244,1.44250534162884,135.50830851875));
#90348=CARTESIAN_POINT('Ctrl Pts',(-68.5134255830644,1.57311356404928,135.4662604368));
#90349=CARTESIAN_POINT('Ctrl Pts',(-68.5211767743045,1.70180187517385,135.418800284541));
#90350=CARTESIAN_POINT('Ctrl Pts',(-68.5289246710816,1.83043549033384,135.371360304113));
#90351=CARTESIAN_POINT('Ctrl Pts',(-68.5366725678587,1.9571504511401,135.318512963443));
#90352=CARTESIAN_POINT('Ctrl Pts',(-68.5444204646357,2.08146570195725,135.260444503006));
#90353=CARTESIAN_POINT('Ctrl Pts',(-68.5521667407198,2.20575494870385,135.202388189239));
#90354=CARTESIAN_POINT('Ctrl Pts',(-68.5599130168039,2.32764512990048,135.139113093399));
#90355=CARTESIAN_POINT('Ctrl Pts',(-68.567659292888,2.44667620365112,135.070853160275));
#90356=CARTESIAN_POINT('Ctrl Pts',(-68.5754056261533,2.56570815606228,135.002592723271));
#90357=CARTESIAN_POINT('Ctrl Pts',(-68.5831519594186,2.68188061975816,134.92934757005));
#90358=CARTESIAN_POINT('Ctrl Pts',(-68.590898292684,2.79475950149538,134.851396865402));
#90359=CARTESIAN_POINT('Ctrl Pts',(-68.5986463606869,2.90766366167506,134.773428704235));
#90360=CARTESIAN_POINT('Ctrl Pts',(-68.6063944286899,3.01727245055912,134.69075311687));
#90361=CARTESIAN_POINT('Ctrl Pts',(-68.6141424966928,3.1231823590646,134.603691481617));
#90362=CARTESIAN_POINT('Ctrl Pts',(-68.6218987994347,3.22920482988147,134.516537316221));
#90363=CARTESIAN_POINT('Ctrl Pts',(-68.6296551021765,3.33152026479532,134.424988039666));
#90364=CARTESIAN_POINT('Ctrl Pts',(-68.6374114049183,3.42975934260136,134.32940443493));
#90365=CARTESIAN_POINT('Ctrl Pts',(-68.6451718474325,3.52805085356128,134.233769814347));
#90366=CARTESIAN_POINT('Ctrl Pts',(-68.6529322899467,3.62226140377021,134.134096859057));
#90367=CARTESIAN_POINT('Ctrl Pts',(-68.6606927324609,3.71206062886231,134.030781072211));
#90368=CARTESIAN_POINT('Ctrl Pts',(-68.6684656327263,3.80200400764254,133.927299433692));
#90369=CARTESIAN_POINT('Ctrl Pts',(-68.6762385329917,3.88752166626892,133.820163583591));
#90370=CARTESIAN_POINT('Ctrl Pts',(-68.6840114332571,3.9683248711163,133.709800477515));
#90371=CARTESIAN_POINT('Ctrl Pts',(-68.6915017690193,4.04619067593868,133.603449348329));
#90372=CARTESIAN_POINT('Ctrl Pts',(-68.6989921047816,4.11967866881516,133.494101782929));
#90373=CARTESIAN_POINT('Ctrl Pts',(-68.7064824405438,4.1885709394259,133.382161336764));
#90374=CARTESIAN_POINT('Ctrl Pts',(-68.7142567746629,4.26007528141438,133.265976634562));
#90375=CARTESIAN_POINT('Ctrl Pts',(-68.722031108782,4.3268550324068,133.14663051393));
#90376=CARTESIAN_POINT('Ctrl Pts',(-68.7298054429011,4.38861790542529,133.024544380834));
#90377=CARTESIAN_POINT('Ctrl Pts',(-68.7375701958482,4.45030466122261,132.902608707987));
#90378=CARTESIAN_POINT('Ctrl Pts',(-68.7453349487953,4.50698666628786,132.777940087056));
#90379=CARTESIAN_POINT('Ctrl Pts',(-68.7530997017424,4.55841523915072,132.650988238387));
#90380=CARTESIAN_POINT('Ctrl Pts',(-68.7608567426274,4.60979273243,132.524162480084));
#90381=CARTESIAN_POINT('Ctrl Pts',(-68.7686137835124,4.65592703128676,132.395058366953));
#90382=CARTESIAN_POINT('Ctrl Pts',(-68.7763708243974,4.69661583966551,132.264149204007));
#90383=CARTESIAN_POINT('Ctrl Pts',(-68.7841220156376,4.73727396429746,132.133338760679));
#90384=CARTESIAN_POINT('Ctrl Pts',(-68.7918732068777,4.7724946565911,132.000726348763));
#90385=CARTESIAN_POINT('Ctrl Pts',(-68.7996243981179,4.80212426190384,131.866803856396));
#90386=CARTESIAN_POINT('Ctrl Pts',(-68.8073722948949,4.83174127384384,131.73293828466));
#90387=CARTESIAN_POINT('Ctrl Pts',(-68.8151201916721,4.85577184092432,131.597764120879));
#90388=CARTESIAN_POINT('Ctrl Pts',(-68.8228680884492,4.87411263020959,131.461786758308));
#90389=CARTESIAN_POINT('Ctrl Pts',(-68.8306143645333,4.89244958299714,131.32583783927));
#90390=CARTESIAN_POINT('Ctrl Pts',(-68.8383606406174,4.90509907309294,131.189086442838));
#90391=CARTESIAN_POINT('Ctrl Pts',(-68.8461069167015,4.91200926099124,131.052046068161));
#90392=CARTESIAN_POINT('Ctrl Pts',(-68.8538532499669,4.91891949989897,130.915004681882));
#90393=CARTESIAN_POINT('Ctrl Pts',(-68.8615995832321,4.92009033238127,130.777674703572));
#90394=CARTESIAN_POINT('Ctrl Pts',(-68.8693459164975,4.91552198968117,130.640572243556));
#90395=CARTESIAN_POINT('Ctrl Pts',(-68.8770939845005,4.91095262393239,130.503439080395));
#90396=CARTESIAN_POINT('Ctrl Pts',(-68.8848420525035,4.90064153852303,130.36653392759));
#90397=CARTESIAN_POINT('Ctrl Pts',(-68.8925901205065,4.88464101161046,130.230369981586));
#90398=CARTESIAN_POINT('Ctrl Pts',(-68.9003464232484,4.86862347914747,130.094061318919));
#90399=CARTESIAN_POINT('Ctrl Pts',(-68.9081027259903,4.84690447173551,129.958495825609));
#90400=CARTESIAN_POINT('Ctrl Pts',(-68.9158590287322,4.81958789917982,129.824179234056));
#90401=CARTESIAN_POINT('Ctrl Pts',(-68.9236194712464,4.79225674694683,129.689790953694));
#90402=CARTESIAN_POINT('Ctrl Pts',(-68.9313799137605,4.75932217038413,129.55665328264));
#90403=CARTESIAN_POINT('Ctrl Pts',(-68.9391403562747,4.72093834748541,129.425257944905));
#90404=CARTESIAN_POINT('Ctrl Pts',(-68.9469132565401,4.68249290746666,129.293651679709));
#90405=CARTESIAN_POINT('Ctrl Pts',(-68.9546861568056,4.63858086590374,129.163793707602));
#90406=CARTESIAN_POINT('Ctrl Pts',(-68.962459057071,4.58940536506362,129.036157728295));
#90407=CARTESIAN_POINT('Ctrl Pts',(-68.9699493928329,4.54201751754565,128.913161638334));
#90408=CARTESIAN_POINT('Ctrl Pts',(-68.9774397285948,4.4897423690861,128.792229078583));
#90409=CARTESIAN_POINT('Ctrl Pts',(-68.9849300643567,4.43280165646442,128.673761514744));
#90410=CARTESIAN_POINT('Ctrl Pts',(-68.9927043984758,4.37370201941584,128.550802217212));
#90411=CARTESIAN_POINT('Ctrl Pts',(-69.0004787325948,4.30938883466821,128.430109028009));
#90412=CARTESIAN_POINT('Ctrl Pts',(-69.0082530667139,4.24005865474453,128.312155636665));
#90413=CARTESIAN_POINT('Ctrl Pts',(-69.016017819661,4.1708139180712,128.194347612335));
#90414=CARTESIAN_POINT('Ctrl Pts',(-69.0237825726081,4.09656468475564,128.079273001342));
#90415=CARTESIAN_POINT('Ctrl Pts',(-69.0315473255552,4.0175548988525,127.967384111282));
#90416=CARTESIAN_POINT('Ctrl Pts',(-69.0393043664402,3.93862358658277,127.855606350846));
#90417=CARTESIAN_POINT('Ctrl Pts',(-69.0470614073253,3.85494135521198,127.747008331936));
#90418=CARTESIAN_POINT('Ctrl Pts',(-69.0548184482103,3.76679706369379,127.642016084874));
#90419=CARTESIAN_POINT('Ctrl Pts',(-69.0625696394504,3.67871924247137,127.537103013282));
#90420=CARTESIAN_POINT('Ctrl Pts',(-69.0703208306905,3.586186309046,127.435790599475));
#90421=CARTESIAN_POINT('Ctrl Pts',(-69.0780720219306,3.4895290487504,127.338473995008));
#90422=CARTESIAN_POINT('Ctrl Pts',(-69.0858199187077,3.39291287036898,127.241198752694));
#90423=CARTESIAN_POINT('Ctrl Pts',(-69.0935678154847,3.29217612653519,127.147916218692));
#90424=CARTESIAN_POINT('Ctrl Pts',(-69.1013157122618,3.18768816493279,127.058986507327));
#90425=CARTESIAN_POINT('Ctrl Pts',(-69.1090619883459,3.0832220599596,126.970075398141));
#90426=CARTESIAN_POINT('Ctrl Pts',(-69.1168082644301,2.97500659551866,126.885515553761));
#90427=CARTESIAN_POINT('Ctrl Pts',(-69.1245545405142,2.86344577246775,126.805628147065));
#90428=CARTESIAN_POINT('Ctrl Pts',(-69.1323008737796,2.75188412590004,126.725740150659));
#90429=CARTESIAN_POINT('Ctrl Pts',(-69.1400472070448,2.63697738931614,126.650524888384));
#90430=CARTESIAN_POINT('Ctrl Pts',(-69.1477935403101,2.51915990594445,126.580261135927));
#90431=CARTESIAN_POINT('Ctrl Pts',(-69.1555416083131,2.4013160381641,126.50998164839));
#90432=CARTESIAN_POINT('Ctrl Pts',(-69.1632896763162,2.28056046222771,126.444656077385));
#90433=CARTESIAN_POINT('Ctrl Pts',(-69.1710377443192,2.1573532024603,126.38451783503));
#90434=CARTESIAN_POINT('Ctrl Pts',(-69.1787940470611,2.03401499655103,126.324315677036));
#90435=CARTESIAN_POINT('Ctrl Pts',(-69.1865503498029,1.90822025359245,126.26931203258));
#90436=CARTESIAN_POINT('Ctrl Pts',(-69.1943066525447,1.78045062636509,126.219692840117));
#90437=CARTESIAN_POINT('Ctrl Pts',(-69.2020670950589,1.65261280464061,126.170047164397));
#90438=CARTESIAN_POINT('Ctrl Pts',(-69.209827537573,1.52279836822426,126.125791793142));
#90439=CARTESIAN_POINT('Ctrl Pts',(-69.2175879800872,1.39150435542503,126.087062800878));
#90440=CARTESIAN_POINT('Ctrl Pts',(-69.2253608803526,1.25999957782091,126.048271637397));
#90441=CARTESIAN_POINT('Ctrl Pts',(-69.2331337806181,1.12701085704306,126.015024675736));
#90442=CARTESIAN_POINT('Ctrl Pts',(-69.2409066808835,0.993046533431332,
125.987407052818));
#90443=CARTESIAN_POINT('Ctrl Pts',(-69.2483970166455,0.863952150418478,
125.960793400057));
#90444=CARTESIAN_POINT('Ctrl Pts',(-69.2558873524076,0.733952168275309,
125.939406960477));
#90445=CARTESIAN_POINT('Ctrl Pts',(-69.2633776881696,0.603504205612691,
125.923278182664));
#90446=CARTESIAN_POINT('Ctrl Pts',(-69.2711520222887,0.468110268797287,
125.906537877338));
#90447=CARTESIAN_POINT('Ctrl Pts',(-69.2789263564076,0.331804823219269,
125.895408764251));
#90448=CARTESIAN_POINT('Ctrl Pts',(-69.2867006905267,0.195092638736001,
125.88998151896));
#90449=CARTESIAN_POINT('Ctrl Pts',(-69.2944654434738,0.0585489398019751,
125.884560962265));
#90450=CARTESIAN_POINT('Ctrl Pts',(-69.302230196421,-0.0784001137534861,
125.884828307005));
#90451=CARTESIAN_POINT('Ctrl Pts',(-69.3099949493681,-0.215242125019637,
125.890822799444));
#90452=CARTESIAN_POINT('Ctrl Pts',(-69.3177519902531,-0.351948222871249,
125.896811338068));
#90453=CARTESIAN_POINT('Ctrl Pts',(-69.325509031138,-0.488547101943895,
125.908515687449));
#90454=CARTESIAN_POINT('Ctrl Pts',(-69.333266072023,-0.624524195541667,
125.925923102164));
#90455=CARTESIAN_POINT('Ctrl Pts',(-69.3410172632631,-0.760398747754854,
125.943317389812));
#90456=CARTESIAN_POINT('Ctrl Pts',(-69.3487684545031,-0.895652061565506,
125.966406133015));
#90457=CARTESIAN_POINT('Ctrl Pts',(-69.3565196457432,-1.02977288722657,
125.995124621773));
#90458=CARTESIAN_POINT('Ctrl Pts',(-69.3642675425203,-1.1638367079593,126.023830904407));
#90459=CARTESIAN_POINT('Ctrl Pts',(-69.3720154392973,-1.29676861638737,
126.058162091826));
#90460=CARTESIAN_POINT('Ctrl Pts',(-69.3797633360744,-1.42806599668528,
126.098002091953));
#90461=CARTESIAN_POINT('Ctrl Pts',(-69.3875096121585,-1.55933591240186,
126.137833758411));
#90462=CARTESIAN_POINT('Ctrl Pts',(-69.3952558882426,-1.68897160617778,
126.18317183209));
#90463=CARTESIAN_POINT('Ctrl Pts',(-69.4030021643267,-1.81648449384346,
126.233850017411));
#90464=CARTESIAN_POINT('Ctrl Pts',(-69.4107484975921,-1.94399832278066,
126.284528576828));
#90465=CARTESIAN_POINT('Ctrl Pts',(-69.4184948308574,-2.06938895101667,
126.340547182149));
#90466=CARTESIAN_POINT('Ctrl Pts',(-69.4262411641227,-2.19218706354579,
126.401691093184));
#90467=CARTESIAN_POINT('Ctrl Pts',(-69.4339892321257,-2.31501267586012,
126.462848696973));
#90468=CARTESIAN_POINT('Ctrl Pts',(-69.4417373001286,-2.4352442672754,126.529133716189));
#90469=CARTESIAN_POINT('Ctrl Pts',(-69.4494853681315,-2.55243680718027,
126.600285284291));
#90470=CARTESIAN_POINT('Ctrl Pts',(-69.4572416708734,-2.66975390071147,
126.671512473126));
#90471=CARTESIAN_POINT('Ctrl Pts',(-69.4649979736152,-2.78402515585255,
126.747616339702));
#90472=CARTESIAN_POINT('Ctrl Pts',(-69.472754276357,-2.89483379222295,126.828292160169));
#90473=CARTESIAN_POINT('Ctrl Pts',(-69.4805147188711,-3.00570157049881,
126.909011039751));
#90474=CARTESIAN_POINT('Ctrl Pts',(-69.4882751613853,-3.11310274148995,
126.994306492482));
#90475=CARTESIAN_POINT('Ctrl Pts',(-69.4960356038994,-3.21665416049633,
127.083833897562));
#90476=CARTESIAN_POINT('Ctrl Pts',(-69.5038085041648,-3.32037180943349,
127.173505019981));
#90477=CARTESIAN_POINT('Ctrl Pts',(-69.5115814044303,-3.42022707189196,
127.267421402327));
#90478=CARTESIAN_POINT('Ctrl Pts',(-69.5193543046957,-3.51587354939758,
127.365201382063));
#90479=CARTESIAN_POINT('Ctrl Pts',(-69.5268446404579,-3.60804303653003,
127.459426813245));
#90480=CARTESIAN_POINT('Ctrl Pts',(-69.5343349762202,-3.69630421962132,
127.55723958703));
#90481=CARTESIAN_POINT('Ctrl Pts',(-69.5418253119825,-3.78038412737664,
127.658271154124));
#90482=CARTESIAN_POINT('Ctrl Pts',(-69.5495609560854,-3.86721765036528,
127.762611502943));
#90483=CARTESIAN_POINT('Ctrl Pts',(-69.5572966001884,-3.94987525363598,
127.870726382361));
#90484=CARTESIAN_POINT('Ctrl Pts',(-69.5650322442914,-4.02800816387792,
127.98224557841));
#90485=CARTESIAN_POINT('Ctrl Pts',(-69.5727583820808,-4.10604505678381,
128.093627728799));
#90486=CARTESIAN_POINT('Ctrl Pts',(-69.5804845198703,-4.17956809177795,
128.208405554353));
#90487=CARTESIAN_POINT('Ctrl Pts',(-69.5882106576597,-4.24826735672974,
128.326174279083));
#90488=CARTESIAN_POINT('Ctrl Pts',(-69.5959274543373,-4.31688356239112,
128.443800618203));
#90489=CARTESIAN_POINT('Ctrl Pts',(-69.6036442510148,-4.38068741280281,
128.564410317273));
#90490=CARTESIAN_POINT('Ctrl Pts',(-69.6113610476923,-4.43941153423827,
128.687568636248));
#90491=CARTESIAN_POINT('Ctrl Pts',(-69.6190724681238,-4.49809474292947,
128.810641151558));
#90492=CARTESIAN_POINT('Ctrl Pts',(-69.6267838885552,-4.55170509224803,
128.936258400123));
#90493=CARTESIAN_POINT('Ctrl Pts',(-69.6344953089866,-4.60002051692417,
129.063960000933));
#90494=CARTESIAN_POINT('Ctrl Pts',(-69.642202740298,-4.648310948017,129.191595541667));
#90495=CARTESIAN_POINT('Ctrl Pts',(-69.6499101716094,-4.69131176676075,
129.321312919831));
#90496=CARTESIAN_POINT('Ctrl Pts',(-69.6576176029209,-4.72884875237447,
129.452631155112));
#90497=CARTESIAN_POINT('Ctrl Pts',(-69.660148416081,-4.74117440191244,129.495750828137));
#90498=CARTESIAN_POINT('Ctrl Pts',(-69.6626792292411,-4.75291133001434,
129.539042958571));
#90499=CARTESIAN_POINT('Ctrl Pts',(-69.6652100424012,-4.76405452823405,
129.582490119308));
#90500=CARTESIAN_POINT('Ctrl Pts',(-67.9154119669996,-4.76405452823407,
129.582490119308));
#90501=CARTESIAN_POINT('Ctrl Pts',(-67.9239585741172,-4.80145152871823,
129.728300456617));
#90502=CARTESIAN_POINT('Ctrl Pts',(-67.9325051812348,-4.83219447185872,
129.876000973547));
#90503=CARTESIAN_POINT('Ctrl Pts',(-67.9410517883524,-4.85610720839616,
130.024998158204));
#90504=CARTESIAN_POINT('Ctrl Pts',(-67.9495613079844,-4.87991617705707,
130.173348778573));
#90505=CARTESIAN_POINT('Ctrl Pts',(-67.9580708276163,-4.89695398951606,
130.322984601923));
#90506=CARTESIAN_POINT('Ctrl Pts',(-67.9665803472483,-4.90709519897987,
130.473302056812));
#90507=CARTESIAN_POINT('Ctrl Pts',(-67.9727670861524,-4.9144682373931,130.582588466192));
#90508=CARTESIAN_POINT('Ctrl Pts',(-67.9789538250566,-4.91819684409512,
130.692234792326));
#90509=CARTESIAN_POINT('Ctrl Pts',(-67.9851405639607,-4.91824943552146,
130.802004244757));
#90510=CARTESIAN_POINT('',(-67.6398594360288,-4.91824920641527,130.801566678494));
#90511=CARTESIAN_POINT('Ctrl Pts',(-67.5697761045559,-4.76405452823408,
129.582490119308));
#90512=CARTESIAN_POINT('Ctrl Pts',(-67.5775493903736,-4.79810817533265,
129.715264772509));
#90513=CARTESIAN_POINT('Ctrl Pts',(-67.5853226761914,-4.82656962736789,
129.849318420193));
#90514=CARTESIAN_POINT('Ctrl Pts',(-67.5930959620091,-4.84937330309023,
129.984140141245));
#90515=CARTESIAN_POINT('Ctrl Pts',(-67.5994909551566,-4.86813362573884,
130.095056425874));
#90516=CARTESIAN_POINT('Ctrl Pts',(-67.6058859483039,-4.88306562724851,
130.206492331211));
#90517=CARTESIAN_POINT('Ctrl Pts',(-67.6122809414514,-4.89415924064579,
130.318162726064));
#90518=CARTESIAN_POINT('Ctrl Pts',(-67.6214737729647,-4.91010635997548,
130.478689422689));
#90519=CARTESIAN_POINT('Ctrl Pts',(-67.630666604478,-4.91815743186786,130.64001341048));
#90520=CARTESIAN_POINT('Ctrl Pts',(-67.639859435991,-4.9182492064149,130.80156667783));
#90521=CARTESIAN_POINT('Ctrl Pts',(-67.6398594360288,-4.91824920641527,
130.801566678494));
#90522=CARTESIAN_POINT('Ctrl Pts',(-67.6475324466333,-4.91832580815699,
130.93641087006));
#90523=CARTESIAN_POINT('Ctrl Pts',(-67.6552054572378,-4.91285267348217,
131.071479102557));
#90524=CARTESIAN_POINT('Ctrl Pts',(-67.6628784678423,-4.90180091895616,
131.206269579174));
#90525=CARTESIAN_POINT('Ctrl Pts',(-67.6705428620542,-4.89076157497681,
131.340908693082));
#90526=CARTESIAN_POINT('Ctrl Pts',(-67.678207256266,-4.87415610287449,131.475270274707));
#90527=CARTESIAN_POINT('Ctrl Pts',(-67.6858716504779,-4.85200762096918,
131.608851207043));
#90528=CARTESIAN_POINT('Ctrl Pts',(-67.6935293817549,-4.82987839353959,
131.742316012647));
#90529=CARTESIAN_POINT('Ctrl Pts',(-67.701187113032,-4.80221580742792,131.875001124938));
#90530=CARTESIAN_POINT('Ctrl Pts',(-67.708844844309,-4.76909486034099,132.006407736264));
#90531=CARTESIAN_POINT('Ctrl Pts',(-67.7164982782742,-4.73599249983397,
132.137740605752));
#90532=CARTESIAN_POINT('Ctrl Pts',(-67.7241517122395,-4.69743796800965,
132.267796012838));
#90533=CARTESIAN_POINT('Ctrl Pts',(-67.7318051462048,-4.6535574212547,132.396084962289));
#90534=CARTESIAN_POINT('Ctrl Pts',(-67.7394563818591,-4.60968947839604,
132.524337063052));
#90535=CARTESIAN_POINT('Ctrl Pts',(-67.7471076175133,-4.56049869176321,
132.650823335254));
#90536=CARTESIAN_POINT('Ctrl Pts',(-67.7547588531676,-4.50616105254587,
132.77507004085));
#90537=CARTESIAN_POINT('Ctrl Pts',(-67.7624096461324,-4.45182655722647,
132.899309557708));
#90538=CARTESIAN_POINT('Ctrl Pts',(-67.7700604390972,-4.39234596244396,
133.021309397682));
#90539=CARTESIAN_POINT('Ctrl Pts',(-67.7777112320619,-4.32794315310324,
133.140616409642));
#90540=CARTESIAN_POINT('Ctrl Pts',(-67.7853633373754,-4.26352929667955,
133.259943886461));
#90541=CARTESIAN_POINT('Ctrl Pts',(-67.793015442689,-4.19419173776662,133.376577263501));
#90542=CARTESIAN_POINT('Ctrl Pts',(-67.8006675480025,-4.12019973015244,
133.490089056212));
#90543=CARTESIAN_POINT('Ctrl Pts',(-67.8083273831058,-4.04613297935969,
133.603715513094));
#90544=CARTESIAN_POINT('Ctrl Pts',(-67.8159872182092,-3.96740260915268,
133.714213750862));
#90545=CARTESIAN_POINT('Ctrl Pts',(-67.8236470533126,-3.88432074757255,
133.821186000726));
#90546=CARTESIAN_POINT('Ctrl Pts',(-67.8313107955854,-3.80119650715437,
133.928212815564));
#90547=CARTESIAN_POINT('Ctrl Pts',(-67.8389745378581,-3.71371661445925,
134.031709754582));
#90548=CARTESIAN_POINT('Ctrl Pts',(-67.846638280131,-3.62223186484096,134.131314085806));
#90549=CARTESIAN_POINT('Ctrl Pts',(-67.8543141073698,-3.53060285279229,
134.231075483239));
#90550=CARTESIAN_POINT('Ctrl Pts',(-67.8619899346086,-3.43495665154634,
134.326931726454));
#90551=CARTESIAN_POINT('Ctrl Pts',(-67.8696657618474,-3.3356796100937,134.418558260378));
#90552=CARTESIAN_POINT('Ctrl Pts',(-67.8766866963198,-3.24487277182504,
134.502367323635));
#90553=CARTESIAN_POINT('Ctrl Pts',(-67.8837076307923,-3.15102880541874,
134.582637975888));
#90554=CARTESIAN_POINT('Ctrl Pts',(-67.8907285652647,-3.05446467201014,
134.659153560117));
#90555=CARTESIAN_POINT('Ctrl Pts',(-67.8985028993838,-2.94753847294181,
134.743879848256));
#90556=CARTESIAN_POINT('Ctrl Pts',(-67.9062772335028,-2.8369149677715,134.824288005531));
#90557=CARTESIAN_POINT('Ctrl Pts',(-67.914051567622,-2.72297809125792,134.90003801905));
#90558=CARTESIAN_POINT('Ctrl Pts',(-67.9218163205691,-2.60918163176197,
134.975694677448));
#90559=CARTESIAN_POINT('Ctrl Pts',(-67.9295810735162,-2.4920802481906,135.046704400084));
#90560=CARTESIAN_POINT('Ctrl Pts',(-67.9373458264633,-2.37209114169222,
135.112767130188));
#90561=CARTESIAN_POINT('Ctrl Pts',(-67.9451028673483,-2.25222121006596,
135.178764245858));
#90562=CARTESIAN_POINT('Ctrl Pts',(-67.9528599082333,-2.12946960348594,
135.239823959586));
#90563=CARTESIAN_POINT('Ctrl Pts',(-67.9606169491183,-2.00428242121468,
135.295689489794));
#90564=CARTESIAN_POINT('Ctrl Pts',(-67.9683681403585,-1.87918964357122,
135.351512891372));
#90565=CARTESIAN_POINT('Ctrl Pts',(-67.9761193315986,-1.7516653016332,135.402149747249));
#90566=CARTESIAN_POINT('Ctrl Pts',(-67.9838705228388,-1.62217969269224,
135.447389381974));
#90567=CARTESIAN_POINT('Ctrl Pts',(-67.9916184196159,-1.49274911858922,
135.492609788647));
#90568=CARTESIAN_POINT('Ctrl Pts',(-67.999366316393,-1.3613593037462,135.532437408005));
#90569=CARTESIAN_POINT('Ctrl Pts',(-68.0071142131701,-1.2284998994806,135.566709939012));
#90570=CARTESIAN_POINT('Ctrl Pts',(-68.0148604892543,-1.09566828653826,
135.600975300944));
#90571=CARTESIAN_POINT('Ctrl Pts',(-68.0226067653384,-0.961368073953953,
135.629687788222));
#90572=CARTESIAN_POINT('Ctrl Pts',(-68.0303530414225,-0.826103044026408,
135.652735275444));
#90573=CARTESIAN_POINT('Ctrl Pts',(-68.0380993746879,-0.690837015602955,
135.675782932797));
#90574=CARTESIAN_POINT('Ctrl Pts',(-68.0458457079532,-0.554606541035317,
135.69316544098));
#90575=CARTESIAN_POINT('Ctrl Pts',(-68.0535920412186,-0.417924145535406,
135.704822072478));
#90576=CARTESIAN_POINT('Ctrl Pts',(-68.0613401092216,-0.281211140961272,
135.716481314398));
#90577=CARTESIAN_POINT('Ctrl Pts',(-68.0690881772245,-0.144046403546104,
135.722412094846));
#90578=CARTESIAN_POINT('Ctrl Pts',(-68.0768362452275,-0.00694571220998101,
135.722605713084));
#90579=CARTESIAN_POINT('Ctrl Pts',(-68.0845925479694,0.130300691372787,
135.722799537101));
#90580=CARTESIAN_POINT('Ctrl Pts',(-68.0923488507113,0.267482521313254,
135.717244017892));
#90581=CARTESIAN_POINT('Ctrl Pts',(-68.1001051534531,0.404085312342746,
135.705982606546));
#90582=CARTESIAN_POINT('Ctrl Pts',(-68.1078655959673,0.540761012394842,
135.694715184645));
#90583=CARTESIAN_POINT('Ctrl Pts',(-68.1156260384815,0.676856669958941,
135.677735850756));
#90584=CARTESIAN_POINT('Ctrl Pts',(-68.1233864809957,0.811865792994566,
135.655139626825));
#90585=CARTESIAN_POINT('Ctrl Pts',(-68.1311593812611,0.947091644660035,
135.632507129429));
#90586=CARTESIAN_POINT('Ctrl Pts',(-68.1389322815266,1.08122709354346,135.604239804356));
#90587=CARTESIAN_POINT('Ctrl Pts',(-68.146705181792,1.21377776263872,135.570483423938));
#90588=CARTESIAN_POINT('Ctrl Pts',(-68.1541955175539,1.34150988103487,135.537954172977));
#90589=CARTESIAN_POINT('Ctrl Pts',(-68.1616858533158,1.46777014551341,135.500328107964));
#90590=CARTESIAN_POINT('Ctrl Pts',(-68.1691761890777,1.59213371131244,135.457777997063));
#90591=CARTESIAN_POINT('Ctrl Pts',(-68.1769505231968,1.72121255951112,135.413614585773));
#90592=CARTESIAN_POINT('Ctrl Pts',(-68.1847248573159,1.84865692617802,135.364006470938));
#90593=CARTESIAN_POINT('Ctrl Pts',(-68.192499191435,1.97397322272228,135.309092882471));
#90594=CARTESIAN_POINT('Ctrl Pts',(-68.2002639443821,2.09913507813072,135.254246970094));
#90595=CARTESIAN_POINT('Ctrl Pts',(-68.2080286973293,2.22217372706486,135.194108749205));
#90596=CARTESIAN_POINT('Ctrl Pts',(-68.2157934502764,2.34261121585499,135.128867034933));
#90597=CARTESIAN_POINT('Ctrl Pts',(-68.2235504911614,2.46292908443322,135.063690119652));
#90598=CARTESIAN_POINT('Ctrl Pts',(-68.2313075320465,2.58065059262441,134.993419983266));
#90599=CARTESIAN_POINT('Ctrl Pts',(-68.2390645729315,2.69531857526733,134.918293145005));
#90600=CARTESIAN_POINT('Ctrl Pts',(-68.2468157641717,2.80990008589334,134.843222960476));
#90601=CARTESIAN_POINT('Ctrl Pts',(-68.2545669554119,2.92143232862603,134.763303577402));
#90602=CARTESIAN_POINT('Ctrl Pts',(-68.2623181466521,3.02948384906819,134.678816794984));
#90603=CARTESIAN_POINT('Ctrl Pts',(-68.2700660434292,3.13748944473136,134.594365921704));
#90604=CARTESIAN_POINT('Ctrl Pts',(-68.2778139402063,3.24201695317114,134.50535175043));
#90605=CARTESIAN_POINT('Ctrl Pts',(-68.2855618369834,3.34266515743276,134.412098511009));
#90606=CARTESIAN_POINT('Ctrl Pts',(-68.2933081130676,3.44329230825992,134.318864778156));
#90607=CARTESIAN_POINT('Ctrl Pts',(-68.3010543891517,3.54004148235356,134.221394006444));
#90608=CARTESIAN_POINT('Ctrl Pts',(-68.3088006652359,3.6325460387999,134.12004943567));
#90609=CARTESIAN_POINT('Ctrl Pts',(-68.3165469985013,3.72505127809398,134.018704116793));
#90610=CARTESIAN_POINT('Ctrl Pts',(-68.3242933317666,3.81331157364519,133.913485230556));
#90611=CARTESIAN_POINT('Ctrl Pts',(-68.3320396650321,3.89699880127807,133.804791154229));
#90612=CARTESIAN_POINT('Ctrl Pts',(-68.3397877330351,3.980704770085,133.696072736617));
#90613=CARTESIAN_POINT('Ctrl Pts',(-68.3475358010381,4.05983539465274,133.583877890021));
#90614=CARTESIAN_POINT('Ctrl Pts',(-68.3552838690411,4.13410456369698,133.468635850893));
#90615=CARTESIAN_POINT('Ctrl Pts',(-68.363040171783,4.2084526668979,133.353271331154));
#90616=CARTESIAN_POINT('Ctrl Pts',(-68.3707964745248,4.27792878118196,133.2348534786));
#90617=CARTESIAN_POINT('Ctrl Pts',(-68.3785527772667,4.34229138213674,133.113838613807));
#90618=CARTESIAN_POINT('Ctrl Pts',(-68.3863132197809,4.40668833534957,132.992759159737));
#90619=CARTESIAN_POINT('Ctrl Pts',(-68.3940736622951,4.46596616810311,132.869080283888));
#90620=CARTESIAN_POINT('Ctrl Pts',(-68.4018341048093,4.51993105373295,132.743279474043));
#90621=CARTESIAN_POINT('Ctrl Pts',(-68.4096070050748,4.57398256858806,132.617276717569));
#90622=CARTESIAN_POINT('Ctrl Pts',(-68.4173799053403,4.62270395399424,132.48914558584));
#90623=CARTESIAN_POINT('Ctrl Pts',(-68.4251528056057,4.66595062949402,132.359380805739));
#90624=CARTESIAN_POINT('Ctrl Pts',(-68.4326431413674,4.70762517940513,132.234333302259));
#90625=CARTESIAN_POINT('Ctrl Pts',(-68.4401334771289,4.74421606231217,132.107769158674));
#90626=CARTESIAN_POINT('Ctrl Pts',(-68.4476238128906,4.77563899399134,131.980139194327));
#90627=CARTESIAN_POINT('Ctrl Pts',(-68.4553981470096,4.80825333567764,131.847670101082));
#90628=CARTESIAN_POINT('Ctrl Pts',(-68.4631724811287,4.83540341687729,131.71363314818));
#90629=CARTESIAN_POINT('Ctrl Pts',(-68.4709468152477,4.8569395789692,131.578518862851));
#90630=CARTESIAN_POINT('Ctrl Pts',(-68.4787115681948,4.87844919966604,131.443571093803));
#90631=CARTESIAN_POINT('Ctrl Pts',(-68.4864763211419,4.89435860636441,131.307549016472));
#90632=CARTESIAN_POINT('Ctrl Pts',(-68.494241074089,4.90456830894643,131.170956806005));
#90633=CARTESIAN_POINT('Ctrl Pts',(-68.501998114974,4.91476787110791,131.034500260848));
#90634=CARTESIAN_POINT('Ctrl Pts',(-68.5097551558589,4.91927896589805,130.897475096801));
#90635=CARTESIAN_POINT('Ctrl Pts',(-68.5175121967439,4.91805347470634,130.760393784284));
#90636=CARTESIAN_POINT('Ctrl Pts',(-68.525263387984,4.91682890766706,130.623415845849));
#90637=CARTESIAN_POINT('Ctrl Pts',(-68.5330145792241,4.90987636877563,130.486382232591));
#90638=CARTESIAN_POINT('Ctrl Pts',(-68.5407657704642,4.89719973204254,130.349808258665));
#90639=CARTESIAN_POINT('Ctrl Pts',(-68.5485136672413,4.88452848321827,130.213292332322));
#90640=CARTESIAN_POINT('Ctrl Pts',(-68.5562615640183,4.86613801145158,130.077236045234));
#90641=CARTESIAN_POINT('Ctrl Pts',(-68.5640094607954,4.84208423293126,129.94215220674));
#90642=CARTESIAN_POINT('Ctrl Pts',(-68.5717557368795,4.81803548594288,129.807096624874));
#90643=CARTESIAN_POINT('Ctrl Pts',(-68.5795020129636,4.78832585701402,129.673013471665));
#90644=CARTESIAN_POINT('Ctrl Pts',(-68.5872482890477,4.75306277170416,129.54040755248));
#90645=CARTESIAN_POINT('Ctrl Pts',(-68.594994622313,4.71779942609027,129.407800654429));
#90646=CARTESIAN_POINT('Ctrl Pts',(-68.6027409555783,4.67698264276923,129.276671389996));
#90647=CARTESIAN_POINT('Ctrl Pts',(-68.6104872888436,4.63077022868955,129.147511151989));
#90648=CARTESIAN_POINT('Ctrl Pts',(-68.6182353568466,4.58454746566014,129.018321989442));
#90649=CARTESIAN_POINT('Ctrl Pts',(-68.6259834248494,4.53292679914924,128.891103098802));
#90650=CARTESIAN_POINT('Ctrl Pts',(-68.6337314928524,4.47611470780124,128.766327206381));
#90651=CARTESIAN_POINT('Ctrl Pts',(-68.6414877955942,4.4192422358864,128.641418700657));
#90652=CARTESIAN_POINT('Ctrl Pts',(-68.6492440983361,4.35716747958491,128.518958736222));
#90653=CARTESIAN_POINT('Ctrl Pts',(-68.6570004010779,4.29014380447648,128.399397166823));
#90654=CARTESIAN_POINT('Ctrl Pts',(-68.6647608435921,4.22308435681443,128.279771783813));
#90655=CARTESIAN_POINT('Ctrl Pts',(-68.6725212861063,4.15107093234099,128.163048210861));
#90656=CARTESIAN_POINT('Ctrl Pts',(-68.6802817286204,4.07440048700341,128.049647613639));
#90657=CARTESIAN_POINT('Ctrl Pts',(-68.6880546288858,3.99760696346071,127.936064975711));
#90658=CARTESIAN_POINT('Ctrl Pts',(-68.6958275291512,3.91614171237452,127.825816287831));
#90659=CARTESIAN_POINT('Ctrl Pts',(-68.7036004294166,3.83034281221331,127.719290601598));
#90660=CARTESIAN_POINT('Ctrl Pts',(-68.7110907651789,3.7476629181841,127.616637392377));
#90661=CARTESIAN_POINT('Ctrl Pts',(-68.7185811009413,3.6609591856893,127.517441435162));
#90662=CARTESIAN_POINT('Ctrl Pts',(-68.7260714367036,3.57056534412745,127.422017319523));
#90663=CARTESIAN_POINT('Ctrl Pts',(-68.7338457708226,3.4767441925916,127.32297516954));
#90664=CARTESIAN_POINT('Ctrl Pts',(-68.7416201049417,3.37865039005745,127.227682790218));
#90665=CARTESIAN_POINT('Ctrl Pts',(-68.7493944390608,3.2766157368352,127.136531235544));
#90666=CARTESIAN_POINT('Ctrl Pts',(-68.7571591920079,3.17470683220396,127.045492017015));
#90667=CARTESIAN_POINT('Ctrl Pts',(-68.764923944955,3.06886702912894,126.95858372726));
#90668=CARTESIAN_POINT('Ctrl Pts',(-68.7726886979021,2.95946672760206,126.876162589116));
#90669=CARTESIAN_POINT('Ctrl Pts',(-68.7804457387871,2.85017508399679,126.793823312809));
#90670=CARTESIAN_POINT('Ctrl Pts',(-68.7882027796721,2.73733028965298,126.715962552808));
#90671=CARTESIAN_POINT('Ctrl Pts',(-68.7959598205571,2.62133749116316,126.642897795442));
#90672=CARTESIAN_POINT('Ctrl Pts',(-68.8037110117972,2.50543216374482,126.569888136777));
#90673=CARTESIAN_POINT('Ctrl Pts',(-68.8114622030374,2.38638388682055,126.501667489455));
#90674=CARTESIAN_POINT('Ctrl Pts',(-68.8192133942775,2.26462830278217,126.438511134048));
#90675=CARTESIAN_POINT('Ctrl Pts',(-68.8269612910546,2.14292446811527,126.375381621776));
#90676=CARTESIAN_POINT('Ctrl Pts',(-68.8347091878316,2.01851596127136,126.317312299988));
#90677=CARTESIAN_POINT('Ctrl Pts',(-68.8424570846087,1.89186444733695,126.264533310784));
#90678=CARTESIAN_POINT('Ctrl Pts',(-68.8502033606928,1.76523942616896,126.211765361807));
#90679=CARTESIAN_POINT('Ctrl Pts',(-68.8579496367769,1.63637269180727,126.164285694572));
#90680=CARTESIAN_POINT('Ctrl Pts',(-68.865695912861,1.50574701744352,126.122276788547));
#90681=CARTESIAN_POINT('Ctrl Pts',(-68.8734422461264,1.37512037883055,126.080267572422));
#90682=CARTESIAN_POINT('Ctrl Pts',(-68.8811885793917,1.24273514649838,126.043729317785));
#90683=CARTESIAN_POINT('Ctrl Pts',(-68.8889349126571,1.10909004164311,126.012794866997));
#90684=CARTESIAN_POINT('Ctrl Pts',(-68.8966829806601,0.975415007893047,
125.981853488653));
#90685=CARTESIAN_POINT('Ctrl Pts',(-68.904431048663,0.840479921016337,125.956518499477));
#90686=CARTESIAN_POINT('Ctrl Pts',(-68.912179116666,0.704794105798939,125.936871703256));
#90687=CARTESIAN_POINT('Ctrl Pts',(-68.9199354194078,0.568964082082815,
125.917204026187));
#90688=CARTESIAN_POINT('Ctrl Pts',(-68.9276917221497,0.432382123715796,
125.903236674684));
#90689=CARTESIAN_POINT('Ctrl Pts',(-68.9354480248915,0.295563655679571,
125.894999642048));
#90690=CARTESIAN_POINT('Ctrl Pts',(-68.9432084674057,0.15867216350743,125.886758213059));
#90691=CARTESIAN_POINT('Ctrl Pts',(-68.9509689099199,0.0215443008461921,
125.884253204283));
#90692=CARTESIAN_POINT('Ctrl Pts',(-68.9587293524341,-0.115305081753601,
125.887462428604));
#90693=CARTESIAN_POINT('Ctrl Pts',(-68.9665022526995,-0.252374147131448,
125.890676804656));
#90694=CARTESIAN_POINT('Ctrl Pts',(-68.9742751529649,-0.389163448761537,
125.899623718838));
#90695=CARTESIAN_POINT('Ctrl Pts',(-68.9820480532303,-0.525162926845925,
125.914229028052));
#90696=CARTESIAN_POINT('Ctrl Pts',(-68.9895383889923,-0.656218481339564,
125.928303397487));
#90697=CARTESIAN_POINT('Ctrl Pts',(-68.9970287247543,-0.786540334784979,
125.947631865341));
#90698=CARTESIAN_POINT('Ctrl Pts',(-69.0045190605163,-0.915683425175047,
125.972103698966));
#90699=CARTESIAN_POINT('Ctrl Pts',(-69.0122933946355,-1.04972301509146,
125.997503389601));
#90700=CARTESIAN_POINT('Ctrl Pts',(-69.0200677287547,-1.18291728898096,
126.028524625166));
#90701=CARTESIAN_POINT('Ctrl Pts',(-69.0278420628739,-1.31475789587773,
126.065099626892));
#90702=CARTESIAN_POINT('Ctrl Pts',(-69.0356068158211,-1.44643602100944,
126.101629553197));
#90703=CARTESIAN_POINT('Ctrl Pts',(-69.0433715687683,-1.5767634253954,126.143699523598));
#90704=CARTESIAN_POINT('Ctrl Pts',(-69.0511363217155,-1.70524019843139,
126.191190457237));
#90705=CARTESIAN_POINT('Ctrl Pts',(-69.0588933626006,-1.8335893665252,126.23863422221));
#90706=CARTESIAN_POINT('Ctrl Pts',(-69.0666504034856,-1.96009119677698,
126.291488100988));
#90707=CARTESIAN_POINT('Ctrl Pts',(-69.0744074443707,-2.08425958731718,
126.349582841383));
#90708=CARTESIAN_POINT('Ctrl Pts',(-69.082158635611,-2.20833434150801,126.407633772082));
#90709=CARTESIAN_POINT('Ctrl Pts',(-69.0899098268512,-2.33007880580415,
126.470917532822));
#90710=CARTESIAN_POINT('Ctrl Pts',(-69.0976610180914,-2.44902590350822,
126.539216401195));
#90711=CARTESIAN_POINT('Ctrl Pts',(-69.1054089148686,-2.5679224455229,126.607486240726));
#90712=CARTESIAN_POINT('Ctrl Pts',(-69.1131568116458,-2.68402364734899,
126.680766754119));
#90713=CARTESIAN_POINT('Ctrl Pts',(-69.120904708423,-2.79688634266317,126.758793926888));
#90714=CARTESIAN_POINT('Ctrl Pts',(-69.1286509845072,-2.90972542953453,
126.836804778054));
#90715=CARTESIAN_POINT('Ctrl Pts',(-69.1363972605914,-3.01932703594144,
126.919560091474));
#90716=CARTESIAN_POINT('Ctrl Pts',(-69.1441435366756,-3.12527668603847,
127.006752330999));
#90717=CARTESIAN_POINT('Ctrl Pts',(-69.1518898699411,-3.23122711823145,
127.093945214156));
#90718=CARTESIAN_POINT('Ctrl Pts',(-69.1596362032066,-3.3335252384397,127.185574840336));
#90719=CARTESIAN_POINT('Ctrl Pts',(-69.167382536472,-3.43178971163483,127.281293425811));
#90720=CARTESIAN_POINT('Ctrl Pts',(-69.1751306044752,-3.53007619047781,
127.377033446801));
#90721=CARTESIAN_POINT('Ctrl Pts',(-69.1828786724782,-3.62432694482605,
127.476863976462));
#90722=CARTESIAN_POINT('Ctrl Pts',(-69.1906267404813,-3.71419784834841,
127.580400722371));
#90723=CARTESIAN_POINT('Ctrl Pts',(-69.1983830432233,-3.80416426773626,
127.684047508366));
#90724=CARTESIAN_POINT('Ctrl Pts',(-69.2061393459651,-3.88974128082898,
127.791408083486));
#90725=CARTESIAN_POINT('Ctrl Pts',(-69.2138956487071,-3.97062505362117,
127.902065018207));
#90726=CARTESIAN_POINT('Ctrl Pts',(-69.2216560912214,-4.05155199651826,
128.012781013867));
#90727=CARTESIAN_POINT('Ctrl Pts',(-69.2294165337357,-4.12778049064987,
128.126796549957));
#90728=CARTESIAN_POINT('Ctrl Pts',(-69.23717697625,-4.19905091336629,128.243666475452));
#90729=CARTESIAN_POINT('Ctrl Pts',(-69.2449498765156,-4.27043574569225,
128.360724010926));
#90730=CARTESIAN_POINT('Ctrl Pts',(-69.2527227767811,-4.336846412196,128.48064475012));
#90731=CARTESIAN_POINT('Ctrl Pts',(-69.2604956770466,-4.39806959178665,
128.602959489125));
#90732=CARTESIAN_POINT('Ctrl Pts',(-69.2679860128077,-4.45706715457859,
128.720827779257));
#90733=CARTESIAN_POINT('Ctrl Pts',(-69.2754763485687,-4.51124771223012,
128.840918754452));
#90734=CARTESIAN_POINT('Ctrl Pts',(-69.2829666843298,-4.56046386036755,
128.962798117736));
#90735=CARTESIAN_POINT('Ctrl Pts',(-69.2917189477579,-4.61797165536622,
129.105210998539));
#90736=CARTESIAN_POINT('Ctrl Pts',(-69.300471211186,-4.66885543046119,129.250445070519));
#90737=CARTESIAN_POINT('Ctrl Pts',(-69.3092234746142,-4.7128622013437,129.397906589293));
#90738=CARTESIAN_POINT('Ctrl Pts',(-69.312853465788,-4.73111395886884,129.45906608432));
#90739=CARTESIAN_POINT('Ctrl Pts',(-69.3164834569616,-4.74818330114657,
129.520608445774));
#90740=CARTESIAN_POINT('Ctrl Pts',(-69.3201134481353,-4.76405452823409,
129.582490119308));
#90741=CARTESIAN_POINT('Origin',(213.235140564004,0.,130.804360617566));
#90742=CARTESIAN_POINT('',(-71.4150282010452,-4.76405452823412,129.582490119309));
#90743=CARTESIAN_POINT('',(-71.0699658330087,-4.76405452823398,129.582490119308));
#90744=CARTESIAN_POINT('',(213.235140564004,-4.76405452823405,129.582490119308));
#90745=CARTESIAN_POINT('',(-69.7351405640517,-4.91824821000367,130.808556722393));
#90746=CARTESIAN_POINT('Ctrl Pts',(-69.7351405640517,-4.91824821000367,
130.808556722393));
#90747=CARTESIAN_POINT('Ctrl Pts',(-69.7444187886688,-4.91810812104566,
130.972754781138));
#90748=CARTESIAN_POINT('Ctrl Pts',(-69.7536970132858,-4.90974152552505,
131.136595367194));
#90749=CARTESIAN_POINT('Ctrl Pts',(-69.7629752379029,-4.89327832969581,
131.299345718988));
#90750=CARTESIAN_POINT('Ctrl Pts',(-69.7725248542183,-4.87633357895065,
131.466856582214));
#90751=CARTESIAN_POINT('Ctrl Pts',(-69.7820744705337,-4.85081157199009,
131.633212407593));
#90752=CARTESIAN_POINT('Ctrl Pts',(-69.7916240868491,-4.81690610697297,
131.797637325793));
#90753=CARTESIAN_POINT('Ctrl Pts',(-69.8011737031644,-4.78300064195585,
131.962062243994));
#90754=CARTESIAN_POINT('Ctrl Pts',(-69.8107233194799,-4.74071184323133,
132.124556280918));
#90755=CARTESIAN_POINT('Ctrl Pts',(-69.8202729357953,-4.69028412933995,
132.284366647473));
#90756=CARTESIAN_POINT('Ctrl Pts',(-69.8280472699145,-4.64923097246828,
132.414468124253));
#90757=CARTESIAN_POINT('Ctrl Pts',(-69.8358216040337,-4.60269545694166,
132.543066248064));
#90758=CARTESIAN_POINT('Ctrl Pts',(-69.8435959381529,-4.55080492781291,
132.669664231323));
#90759=CARTESIAN_POINT('Ctrl Pts',(-69.8513606911001,-4.49897834912372,
132.796106193881));
#90760=CARTESIAN_POINT('Ctrl Pts',(-69.8591254440473,-4.44181003487559,
132.920552562208));
#90761=CARTESIAN_POINT('Ctrl Pts',(-69.8668901969945,-4.37947727625291,
133.042520989229));
#90762=CARTESIAN_POINT('Ctrl Pts',(-69.8746472378797,-4.31720642740474,
133.16436827549));
#90763=CARTESIAN_POINT('Ctrl Pts',(-69.8824042787648,-4.24978151868362,
133.283742172314));
#90764=CARTESIAN_POINT('Ctrl Pts',(-69.8901613196499,-4.17742803050364,
133.400179970384));
#90765=CARTESIAN_POINT('Ctrl Pts',(-69.8979125108902,-4.10512910465191,
133.516529961804));
#90766=CARTESIAN_POINT('Ctrl Pts',(-69.9056637021304,-4.02790920268156,
133.629947930839));
#90767=CARTESIAN_POINT('Ctrl Pts',(-69.9134148933707,-3.94603968892922,
133.739995784935));
#90768=CARTESIAN_POINT('Ctrl Pts',(-69.9211627901479,-3.86420497190416,
133.849996865758));
#90769=CARTESIAN_POINT('Ctrl Pts',(-69.9289106869252,-3.77772480649938,
133.956630367531));
#90770=CARTESIAN_POINT('Ctrl Pts',(-69.9366585837024,-3.68691370109126,
134.059487408216));
#90771=CARTESIAN_POINT('Ctrl Pts',(-69.9444048597866,-3.59612159140873,
134.162322933425));
#90772=CARTESIAN_POINT('Ctrl Pts',(-69.9521511358708,-3.50100060228079,
134.261383275912));
#90773=CARTESIAN_POINT('Ctrl Pts',(-69.959897411955,-3.40190507052986,134.356293183593));
#90774=CARTESIAN_POINT('Ctrl Pts',(-69.9676437452204,-3.30280880727835,
134.451203791877));
#90775=CARTESIAN_POINT('Ctrl Pts',(-69.975390078486,-3.19973822521254,134.541963633793));
#90776=CARTESIAN_POINT('Ctrl Pts',(-69.9831364117515,-3.09308371280454,
134.628235119702));
#90777=CARTESIAN_POINT('Ctrl Pts',(-69.9908844797546,-2.98640531585798,
134.714525925511));
#90778=CARTESIAN_POINT('Ctrl Pts',(-69.9986325477576,-2.87614169540752,
134.796326129377));
#90779=CARTESIAN_POINT('Ctrl Pts',(-70.0063806157607,-2.76271509841206,
134.873339401918));
#90780=CARTESIAN_POINT('Ctrl Pts',(-70.0141369185026,-2.64916795027937,
134.950434525081));
#90781=CARTESIAN_POINT('Ctrl Pts',(-70.0218932212446,-2.53245143431552,
135.022732333908));
#90782=CARTESIAN_POINT('Ctrl Pts',(-70.0296495239866,-2.41301594376746,
135.089980423105));
#90783=CARTESIAN_POINT('Ctrl Pts',(-70.0374099665009,-2.29351670690197,
135.157264404631));
#90784=CARTESIAN_POINT('Ctrl Pts',(-70.0451704090152,-2.17129595205114,
135.219493118833));
#90785=CARTESIAN_POINT('Ctrl Pts',(-70.0529308515295,-2.04682637818646,
135.276461336474));
#90786=CARTESIAN_POINT('Ctrl Pts',(-70.060703751795,-1.92215699471192,135.333521004556));
#90787=CARTESIAN_POINT('Ctrl Pts',(-70.0684766520606,-1.79523194049187,
135.385303153271));
#90788=CARTESIAN_POINT('Ctrl Pts',(-70.0762495523261,-1.66654233040697,
135.431651371718));
#90789=CARTESIAN_POINT('Ctrl Pts',(-70.0837398880869,-1.54253091182139,
135.476314715672));
#90790=CARTESIAN_POINT('Ctrl Pts',(-70.0912302238476,-1.41688129589539,
135.515932251774));
#90791=CARTESIAN_POINT('Ctrl Pts',(-70.0987205596083,-1.29004214955684,
135.550408901651));
#90792=CARTESIAN_POINT('Ctrl Pts',(-70.1064948937274,-1.15839385841048,
135.586192744193));
#90793=CARTESIAN_POINT('Ctrl Pts',(-70.1142692278464,-1.02504703192719,
135.61655152413));
#90794=CARTESIAN_POINT('Ctrl Pts',(-70.1220435619655,-0.890488464682378,
135.641323854636));
#90795=CARTESIAN_POINT('Ctrl Pts',(-70.1298083149126,-0.756095728846037,
135.666065655459));
#90796=CARTESIAN_POINT('Ctrl Pts',(-70.1375730678597,-0.620494604406137,
135.685234635443));
#90797=CARTESIAN_POINT('Ctrl Pts',(-70.1453378208068,-0.484186733831959,
135.698719234308));
#90798=CARTESIAN_POINT('Ctrl Pts',(-70.1530948616917,-0.348014246156439,
135.71219044008));
#90799=CARTESIAN_POINT('Ctrl Pts',(-70.1608519025767,-0.211136795807643,
135.719988461904));
#90800=CARTESIAN_POINT('Ctrl Pts',(-70.1686089434617,-0.0740655509111302,
135.722052897149));
#90801=CARTESIAN_POINT('Ctrl Pts',(-70.1763601347018,0.0629023274937205,
135.724115775587));
#90802=CARTESIAN_POINT('Ctrl Pts',(-70.184111325942,0.200063320220439,135.72045366773));
#90803=CARTESIAN_POINT('Ctrl Pts',(-70.1918625171822,0.336902168544469,
135.711058080354));
#90804=CARTESIAN_POINT('Ctrl Pts',(-70.1996104139592,0.47368285670748,135.701666486353));
#90805=CARTESIAN_POINT('Ctrl Pts',(-70.2073583107363,0.610141283560909,
135.686546286329));
#90806=CARTESIAN_POINT('Ctrl Pts',(-70.2151062075134,0.745763445607566,
135.66574107436));
#90807=CARTESIAN_POINT('Ctrl Pts',(-70.2228524835975,0.881357238421598,
135.644940214392));
#90808=CARTESIAN_POINT('Ctrl Pts',(-70.2305987596815,1.01611472817172,135.618456767071));
#90809=CARTESIAN_POINT('Ctrl Pts',(-70.2383450357656,1.14952867694443,135.586386013084));
#90810=CARTESIAN_POINT('Ctrl Pts',(-70.2460913690309,1.2829436105486,135.554315022358));
#90811=CARTESIAN_POINT('Ctrl Pts',(-70.2538377022963,1.41501460324895,135.516656734046));
#90812=CARTESIAN_POINT('Ctrl Pts',(-70.2615840355616,1.54524661681551,135.473557117578));
#90813=CARTESIAN_POINT('Ctrl Pts',(-70.2693321035646,1.67550779493854,135.430447849249));
#90814=CARTESIAN_POINT('Ctrl Pts',(-70.2770801715676,1.80392880334425,135.381894950809));
#90815=CARTESIAN_POINT('Ctrl Pts',(-70.2848282395705,1.93003209693533,135.328093497312));
#90816=CARTESIAN_POINT('Ctrl Pts',(-70.2925845423124,2.05626941460749,135.274234862991));
#90817=CARTESIAN_POINT('Ctrl Pts',(-70.3003408450543,2.18018373659078,135.215116684173));
#90818=CARTESIAN_POINT('Ctrl Pts',(-70.3080971477962,2.30131925861064,135.150981458225));
#90819=CARTESIAN_POINT('Ctrl Pts',(-70.3158575903103,2.42251943430592,135.086812001375));
#90820=CARTESIAN_POINT('Ctrl Pts',(-70.3236180328245,2.54093751737697,135.017620358898));
#90821=CARTESIAN_POINT('Ctrl Pts',(-70.3313784753387,2.65614533731364,134.943693294407));
#90822=CARTESIAN_POINT('Ctrl Pts',(-70.3391513756041,2.77153809907055,134.86964755563));
#90823=CARTESIAN_POINT('Ctrl Pts',(-70.3469242758695,2.88370997945372,134.790851429044));
#90824=CARTESIAN_POINT('Ctrl Pts',(-70.3546971761349,2.99226392595159,134.707633559592));
#90825=CARTESIAN_POINT('Ctrl Pts',(-70.362187511897,3.0968716630644,134.627440869306));
#90826=CARTESIAN_POINT('Ctrl Pts',(-70.3696778476591,3.19811970480336,134.543142534807));
#90827=CARTESIAN_POINT('Ctrl Pts',(-70.3771681834212,3.29568554360642,134.455064640102));
#90828=CARTESIAN_POINT('Ctrl Pts',(-70.3849425175403,3.39695062084092,134.363647245251));
#90829=CARTESIAN_POINT('Ctrl Pts',(-70.3927168516593,3.49456953909797,134.267868445663));
#90830=CARTESIAN_POINT('Ctrl Pts',(-70.4004911857783,3.58814339471309,134.16805056188));
#90831=CARTESIAN_POINT('Ctrl Pts',(-70.4082559387254,3.68160192891411,134.068355694718));
#90832=CARTESIAN_POINT('Ctrl Pts',(-70.4160206916725,3.77102505466988,133.964631930213));
#90833=CARTESIAN_POINT('Ctrl Pts',(-70.4237854446195,3.8560477631489,133.857241013326));
#90834=CARTESIAN_POINT('Ctrl Pts',(-70.4315424855045,3.94098602587525,133.749956758611));
#90835=CARTESIAN_POINT('Ctrl Pts',(-70.4392995263896,4.02153232781797,133.639012904335));
#90836=CARTESIAN_POINT('Ctrl Pts',(-70.4470565672745,4.09735955167546,133.524806861621));
#90837=CARTESIAN_POINT('Ctrl Pts',(-70.4548077585146,4.17312959363359,133.410686942572));
#90838=CARTESIAN_POINT('Ctrl Pts',(-70.4625589497547,4.24418742548935,133.293310056042));
#90839=CARTESIAN_POINT('Ctrl Pts',(-70.4703101409948,4.31024739172633,133.173105112993));
#90840=CARTESIAN_POINT('Ctrl Pts',(-70.4780580377718,4.37627928071545,133.052951260251));
#90841=CARTESIAN_POINT('Ctrl Pts',(-70.4858059345489,4.43731734110599,132.929972083592));
#90842=CARTESIAN_POINT('Ctrl Pts',(-70.493553831326,4.49312041838339,132.804623592379));
#90843=CARTESIAN_POINT('Ctrl Pts',(-70.50130010741,4.54891182286,132.679301321367));
#90844=CARTESIAN_POINT('Ctrl Pts',(-70.5090463834941,4.59947026342356,132.551611078539));
#90845=CARTESIAN_POINT('Ctrl Pts',(-70.5167926595782,4.64460172793202,132.422031119056));
#90846=CARTESIAN_POINT('Ctrl Pts',(-70.5245389928435,4.6897335255907,132.292450203043));
#90847=CARTESIAN_POINT('Ctrl Pts',(-70.5322853261088,4.72943813866297,132.160979911752));
#90848=CARTESIAN_POINT('Ctrl Pts',(-70.5400316593741,4.76357079511038,132.028115634909));
#90849=CARTESIAN_POINT('Ctrl Pts',(-70.547779727377,4.79771109532954,131.895221604032));
#90850=CARTESIAN_POINT('Ctrl Pts',(-70.55552779538,4.82627685868318,131.760933345011));
#90851=CARTESIAN_POINT('Ctrl Pts',(-70.5632758633829,4.8491740825506,131.625758072894));
#90852=CARTESIAN_POINT('Ctrl Pts',(-70.5710321661248,4.87209564186003,131.490439134889));
#90853=CARTESIAN_POINT('Ctrl Pts',(-70.5787884688667,4.88933656151407,131.354231686676));
#90854=CARTESIAN_POINT('Ctrl Pts',(-70.5865447716085,4.90085448807156,131.21765028505));
#90855=CARTESIAN_POINT('Ctrl Pts',(-70.5943052141227,4.91237856209326,131.080995985817));
#90856=CARTESIAN_POINT('Ctrl Pts',(-70.6020656566367,4.9181735400901,130.943967725896));
#90857=CARTESIAN_POINT('Ctrl Pts',(-70.6098260991509,4.91824924779478,130.807080740003));
#90858=CARTESIAN_POINT('Ctrl Pts',(-70.6175989994163,4.91832507703219,130.669974010967));
#90859=CARTESIAN_POINT('Ctrl Pts',(-70.6253718996817,4.91266330541031,130.533009400006));
#90860=CARTESIAN_POINT('Ctrl Pts',(-70.6331447999471,4.90132581464771,130.396698599262));
#90861=CARTESIAN_POINT('Ctrl Pts',(-70.6406351357094,4.8904004702313,130.265343039465));
#90862=CARTESIAN_POINT('Ctrl Pts',(-70.6481254714717,4.87420493364416,130.134594885555));
#90863=CARTESIAN_POINT('Ctrl Pts',(-70.6556158072341,4.85283922538445,130.004901728648));
#90864=CARTESIAN_POINT('Ctrl Pts',(-70.6633901413531,4.83066342980289,129.870291216283));
#90865=CARTESIAN_POINT('Ctrl Pts',(-70.6711644754722,4.80284742290493,129.736390874936));
#90866=CARTESIAN_POINT('Ctrl Pts',(-70.6789388095913,4.76944676491718,129.603710535685));
#90867=CARTESIAN_POINT('Ctrl Pts',(-70.6867035625384,4.7360872702553,129.471193713094));
#90868=CARTESIAN_POINT('Ctrl Pts',(-70.6944683154855,4.69715691331984,129.339894276492));
#90869=CARTESIAN_POINT('Ctrl Pts',(-70.7022330684326,4.65276274420152,129.210314850133));
#90870=CARTESIAN_POINT('Ctrl Pts',(-70.7099901093176,4.60841266799781,129.080864123887));
#90871=CARTESIAN_POINT('Ctrl Pts',(-70.7177471502026,4.55860970495447,128.953130375682));
#90872=CARTESIAN_POINT('Ctrl Pts',(-70.7255041910877,4.50351139341343,128.827603628987));
#90873=CARTESIAN_POINT('Ctrl Pts',(-70.7332553823278,4.44845463193781,128.702171542988));
#90874=CARTESIAN_POINT('Ctrl Pts',(-70.741006573568,4.38811062681534,128.578943502326));
#90875=CARTESIAN_POINT('Ctrl Pts',(-70.7487577648081,4.32268582920232,128.458391673928));
#90876=CARTESIAN_POINT('Ctrl Pts',(-70.7565056615852,4.25728883887346,128.337891083273));
#90877=CARTESIAN_POINT('Ctrl Pts',(-70.7642535583623,4.18681553717697,128.220064785461));
#90878=CARTESIAN_POINT('Ctrl Pts',(-70.7720014551394,4.11151922779875,128.105362154813));
#90879=CARTESIAN_POINT('Ctrl Pts',(-70.7797477312235,4.03623866878526,127.990683517484));
#90880=CARTESIAN_POINT('Ctrl Pts',(-70.7874940073077,3.95613732320112,127.879127574292));
#90881=CARTESIAN_POINT('Ctrl Pts',(-70.7952402833918,3.87151269235626,127.771116061744));
#90882=CARTESIAN_POINT('Ctrl Pts',(-70.8029866166572,3.7868874368316,127.66310375188));
#90883=CARTESIAN_POINT('Ctrl Pts',(-70.8107329499225,3.6977390705401,127.558636232625));
#90884=CARTESIAN_POINT('Ctrl Pts',(-70.8184792831879,3.60440612606566,127.458103075045));
#90885=CARTESIAN_POINT('Ctrl Pts',(-70.8262273511909,3.51105228032543,127.357547403761));
#90886=CARTESIAN_POINT('Ctrl Pts',(-70.8339754191939,3.41351225761958,127.260928133853));
#90887=CARTESIAN_POINT('Ctrl Pts',(-70.8417234871969,3.31216198162016,127.168598514511));
#90888=CARTESIAN_POINT('Ctrl Pts',(-70.8494797899388,3.21070398934133,127.076170766151));
#90889=CARTESIAN_POINT('Ctrl Pts',(-70.8572360926807,3.10542794376917,126.988042039347));
#90890=CARTESIAN_POINT('Ctrl Pts',(-70.8649923954226,2.99674386303928,126.904526097764));
#90891=CARTESIAN_POINT('Ctrl Pts',(-70.8727528379368,2.88800177434309,126.820965581209));
#90892=CARTESIAN_POINT('Ctrl Pts',(-70.8805132804509,2.77584834558633,126.74202298051));
#90893=CARTESIAN_POINT('Ctrl Pts',(-70.8882737229651,2.66072236937621,126.667968525948));
#90894=CARTESIAN_POINT('Ctrl Pts',(-70.8960466232305,2.54541158272867,126.593795192601));
#90895=CARTESIAN_POINT('Ctrl Pts',(-70.9038195234959,2.42711905062857,126.524525883645));
#90896=CARTESIAN_POINT('Ctrl Pts',(-70.9115924237614,2.30630872274831,126.46038511834));
#90897=CARTESIAN_POINT('Ctrl Pts',(-70.9190827595232,2.18989015459214,126.398576031416));
#90898=CARTESIAN_POINT('Ctrl Pts',(-70.9265730952851,2.07113394661053,126.341529224142));
#90899=CARTESIAN_POINT('Ctrl Pts',(-70.934063431047,1.95047073341027,126.289402480372));
#90900=CARTESIAN_POINT('Ctrl Pts',(-70.9418377651661,1.82523253780426,126.235299335269));
#90901=CARTESIAN_POINT('Ctrl Pts',(-70.9496120992851,1.6975431572031,126.186325324467));
#90902=CARTESIAN_POINT('Ctrl Pts',(-70.9573864334042,1.5678615585905,126.142709279725));
#90903=CARTESIAN_POINT('Ctrl Pts',(-70.9651511863513,1.43833978095839,126.099146987861));
#90904=CARTESIAN_POINT('Ctrl Pts',(-70.9729159392983,1.30683103750208,126.060929647065));
#90905=CARTESIAN_POINT('Ctrl Pts',(-70.9806806922454,1.17381606343087,126.028238873752));
#90906=CARTESIAN_POINT('Ctrl Pts',(-70.9884377331304,1.0409332017071,125.995580569376));
#90907=CARTESIAN_POINT('Ctrl Pts',(-70.9961947740153,0.906547463705026,
125.968438001702));
#90908=CARTESIAN_POINT('Ctrl Pts',(-71.0039518149003,0.771156273370085,
125.946943498917));
#90909=CARTESIAN_POINT('Ctrl Pts',(-71.0117030061404,0.635867182584781,
125.925465205304));
#90910=CARTESIAN_POINT('Ctrl Pts',(-71.0194541973806,0.499574533223449,
125.909626559854));
#90911=CARTESIAN_POINT('Ctrl Pts',(-71.0272053886207,0.362787164588129,
125.899509087121));
#90912=CARTESIAN_POINT('Ctrl Pts',(-71.0349532853977,0.226057934233588,
125.889395914584));
#90913=CARTESIAN_POINT('Ctrl Pts',(-71.0427011821748,0.08883479189768,125.884999107173));
#90914=CARTESIAN_POINT('Ctrl Pts',(-71.0504490789519,-0.0483672742460088,
125.886348451123));
#90915=CARTESIAN_POINT('Ctrl Pts',(-71.0581953550359,-0.185540640675194,
125.887697512819));
#90916=CARTESIAN_POINT('Ctrl Pts',(-71.0659416311199,-0.32269254898266,
125.894790331246));
#90917=CARTESIAN_POINT('Ctrl Pts',(-71.0736879072039,-0.459307373576597,
125.907604569009));
#90918=CARTESIAN_POINT('Ctrl Pts',(-71.0814342404693,-0.59592320663032,
125.920418901364));
#90919=CARTESIAN_POINT('Ctrl Pts',(-71.0891805737347,-0.732001558802787,
125.93895470082));
#90920=CARTESIAN_POINT('Ctrl Pts',(-71.096926907,-0.867031687794124,125.963137723001));
#90921=CARTESIAN_POINT('Ctrl Pts',(-71.1046749750029,-1.00209205584643,
125.987326160802));
#90922=CARTESIAN_POINT('Ctrl Pts',(-71.1124230430058,-1.13610334883913,
126.017164268939));
#90923=CARTESIAN_POINT('Ctrl Pts',(-71.1201711110088,-1.26856517229714,
126.052526711995));
#90924=CARTESIAN_POINT('Ctrl Pts',(-71.1279274137506,-1.40116777775763,
126.087926738676));
#90925=CARTESIAN_POINT('Ctrl Pts',(-71.1356837164925,-1.53221724569505,
126.128862727887));
#90926=CARTESIAN_POINT('Ctrl Pts',(-71.1434400192343,-1.66122797303317,
126.175159316681));
#90927=CARTESIAN_POINT('Ctrl Pts',(-71.1512004617484,-1.79030755728091,
126.22148061536));
#90928=CARTESIAN_POINT('Ctrl Pts',(-71.1589609042626,-1.91734587076247,
126.273168067364));
#90929=CARTESIAN_POINT('Ctrl Pts',(-71.1667213467767,-2.04187838296597,
126.329998570114));
#90930=CARTESIAN_POINT('Ctrl Pts',(-71.1744942470421,-2.16661080581352,
126.386920302233));
#90931=CARTESIAN_POINT('Ctrl Pts',(-71.1822671473075,-2.28882904030236,
126.449001406219));
#90932=CARTESIAN_POINT('Ctrl Pts',(-71.1900400475729,-2.40809341588997,
126.515972906217));
#90933=CARTESIAN_POINT('Ctrl Pts',(-71.1975303833351,-2.52302223102001,
126.580509823502));
#90934=CARTESIAN_POINT('Ctrl Pts',(-71.2050207190974,-2.63520795683101,
126.649587591853));
#90935=CARTESIAN_POINT('Ctrl Pts',(-71.2125110548596,-2.74428507677346,
126.722929192208));
#90936=CARTESIAN_POINT('Ctrl Pts',(-71.220259276429,-2.85711762798235,126.798795880678));
#90937=CARTESIAN_POINT('Ctrl Pts',(-71.2280074979985,-2.96698678927996,
126.879469506545));
#90938=CARTESIAN_POINT('Ctrl Pts',(-71.2357557195679,-3.07345350336626,
126.964690498253));
#90939=CARTESIAN_POINT('Ctrl Pts',(-71.2434916860282,-3.17975182252658,
127.049776698701));
#90940=CARTESIAN_POINT('Ctrl Pts',(-71.2512276524884,-3.28265810680815,
127.139395697583));
#90941=CARTESIAN_POINT('Ctrl Pts',(-71.2589636189487,-3.3817615476813,127.233244279903));
#90942=CARTESIAN_POINT('Ctrl Pts',(-71.2666925120404,-3.48077437348095,
127.32700705192));
#90943=CARTESIAN_POINT('Ctrl Pts',(-71.2744214051321,-3.57599098767044,
127.424991446448));
#90944=CARTESIAN_POINT('Ctrl Pts',(-71.2821502982237,-3.6670328127386,127.526853422639));
#90945=CARTESIAN_POINT('Ctrl Pts',(-71.2898738298731,-3.75801148316269,
127.628644738375));
#90946=CARTESIAN_POINT('Ctrl Pts',(-71.2975973615224,-3.84482086439671,
127.734307991986));
#90947=CARTESIAN_POINT('Ctrl Pts',(-71.3053208931718,-3.92711881451436,
127.843461956823));
#90948=CARTESIAN_POINT('Ctrl Pts',(-71.3130407711693,-4.00937783321157,
127.952564285881));
#90949=CARTESIAN_POINT('Ctrl Pts',(-71.3207606491669,-4.08712943133494,
128.065153725941));
#90950=CARTESIAN_POINT('Ctrl Pts',(-71.3284805271644,-4.16007168372777,
128.180815945039));
#90951=CARTESIAN_POINT('Ctrl Pts',(-71.3362000314408,-4.23301040496854,
128.296472564901));
#90952=CARTESIAN_POINT('Ctrl Pts',(-71.343919535717,-4.30114002466459,128.41520134041));
#90953=CARTESIAN_POINT('Ctrl Pts',(-71.3516390399934,-4.36420199213107,
128.536559031364));
#90954=CARTESIAN_POINT('Ctrl Pts',(-71.3593581195935,-4.42726049034381,
128.657910046019));
#90955=CARTESIAN_POINT('Ctrl Pts',(-71.3670771991937,-4.48525171412237,
128.781889336178));
#90956=CARTESIAN_POINT('Ctrl Pts',(-71.3747962787938,-4.53796349435114,
128.908029848308));
#90957=CARTESIAN_POINT('Ctrl Pts',(-71.3825195995503,-4.59070423643966,
129.034239666838));
#90958=CARTESIAN_POINT('Ctrl Pts',(-71.3902429203067,-4.63815959149372,
129.16261271424));
#90959=CARTESIAN_POINT('Ctrl Pts',(-71.3979662410631,-4.68016584382023,
129.292662652747));
#90960=CARTESIAN_POINT('Ctrl Pts',(-71.4036535610572,-4.71109852242625,
129.388429181008));
#90961=CARTESIAN_POINT('Ctrl Pts',(-71.4093408810511,-4.73907738275365,
129.485104608161));
#90962=CARTESIAN_POINT('Ctrl Pts',(-71.4150282010451,-4.76405452823412,
129.582490119309));
#90963=CARTESIAN_POINT('Ctrl Pts',(-69.6652100424012,-4.76405452823405,
129.582490119308));
#90964=CARTESIAN_POINT('Ctrl Pts',(-69.6729160059501,-4.79798397061735,
129.71478050021));
#90965=CARTESIAN_POINT('Ctrl Pts',(-69.6806219694989,-4.826405066055,129.848509029593));
#90966=CARTESIAN_POINT('Ctrl Pts',(-69.6883279330478,-4.84921000393715,
129.983175254681));
#90967=CARTESIAN_POINT('Ctrl Pts',(-69.6961300382079,-4.87229946217271,
130.11952161072));
#90968=CARTESIAN_POINT('Ctrl Pts',(-69.703932143368,-4.88963157798843,130.256828815998));
#90969=CARTESIAN_POINT('Ctrl Pts',(-69.7117342485281,-4.90114821834125,
130.394568957877));
#90970=CARTESIAN_POINT('Ctrl Pts',(-69.7195363536882,-4.91266485869405,
130.532309099757));
#90971=CARTESIAN_POINT('Ctrl Pts',(-69.7273384588484,-4.91836601148334,
130.670481758551));
#90972=CARTESIAN_POINT('Ctrl Pts',(-69.7351405640084,-4.91824821000432,
130.808556721627));
#90973=CARTESIAN_POINT('',(-69.3898594359379,-4.91824912971278,130.801434770766));
#90974=CARTESIAN_POINT('Ctrl Pts',(-69.3201134481353,-4.76405452823409,
129.582490119308));
#90975=CARTESIAN_POINT('Ctrl Pts',(-69.3288186313557,-4.80211576120071,
129.730890288985));
#90976=CARTESIAN_POINT('Ctrl Pts',(-69.3375238145761,-4.8332833158892,129.88124324352));
#90977=CARTESIAN_POINT('Ctrl Pts',(-69.3462289977965,-4.85737407892202,
130.032933291166));
#90978=CARTESIAN_POINT('Ctrl Pts',(-69.3548866098648,-4.88133319333549,
130.183794399301));
#90979=CARTESIAN_POINT('Ctrl Pts',(-69.3635442219332,-4.89829255583419,
130.335977826698));
#90980=CARTESIAN_POINT('Ctrl Pts',(-69.3722018340016,-4.90812000793932,
130.488859349477));
#90981=CARTESIAN_POINT('Ctrl Pts',(-69.3780877013137,-4.91480118961508,
130.592795671693));
#90982=CARTESIAN_POINT('Ctrl Pts',(-69.3839735686258,-4.91818703416645,
130.697054265705));
#90983=CARTESIAN_POINT('Ctrl Pts',(-69.389859435938,-4.91824912971278,130.801434770766));
#90984=CARTESIAN_POINT('Ctrl Pts',(-69.389859435991,-4.91824912971334,130.801434771708));
#90985=CARTESIAN_POINT('Ctrl Pts',(-69.3976795903753,-4.91833163184545,
130.940118099247));
#90986=CARTESIAN_POINT('Ctrl Pts',(-69.4054997447596,-4.91254396783923,
131.078815667496));
#90987=CARTESIAN_POINT('Ctrl Pts',(-69.4133198991439,-4.9009091403827,131.21700169673));
#90988=CARTESIAN_POINT('Ctrl Pts',(-69.4211412015346,-4.88927260492193,
131.35520801181));
#90989=CARTESIAN_POINT('Ctrl Pts',(-69.4289625039254,-4.87178722802085,
131.492902259086));
#90990=CARTESIAN_POINT('Ctrl Pts',(-69.4367838063161,-4.84852792659058,
131.62956362748));
#90991=CARTESIAN_POINT('Ctrl Pts',(-69.4446078276649,-4.82526053941436,
131.766272504141));
#90992=CARTESIAN_POINT('Ctrl Pts',(-69.4524318490137,-4.79621529426033,
131.901947411878));
#90993=CARTESIAN_POINT('Ctrl Pts',(-69.4602558703624,-4.76151821987119,
132.036077835248));
#90994=CARTESIAN_POINT('Ctrl Pts',(-69.4680841830829,-4.72680211459782,
132.170281827373));
#90995=CARTESIAN_POINT('Ctrl Pts',(-69.4759124958035,-4.68642810193007,
132.302939280281));
#90996=CARTESIAN_POINT('Ctrl Pts',(-69.483740808524,-4.64057196066345,132.433555185567));
#90997=CARTESIAN_POINT('Ctrl Pts',(-69.4915797216638,-4.59465372500422,
132.564347959536));
#90998=CARTESIAN_POINT('Ctrl Pts',(-69.4994186348035,-4.54323866303483,
132.693093306502));
#90999=CARTESIAN_POINT('Ctrl Pts',(-69.5072575479433,-4.48655081755768,
132.819315908378));
#91000=CARTESIAN_POINT('Ctrl Pts',(-69.5151026597042,-4.42981814616346,
132.945638320784));
#91001=CARTESIAN_POINT('Ctrl Pts',(-69.5229477714649,-4.36780455241388,
133.069433673841));
#91002=CARTESIAN_POINT('Ctrl Pts',(-69.5307928832258,-4.30077947142102,
133.190252274935));
#91003=CARTESIAN_POINT('Ctrl Pts',(-69.5386503213002,-4.2336490799887,133.311260707354));
#91004=CARTESIAN_POINT('Ctrl Pts',(-69.5465077593746,-4.16149167580229,
133.429282725199));
#91005=CARTESIAN_POINT('Ctrl Pts',(-69.554365197449,-4.08461966215346,133.543898038017));
#91006=CARTESIAN_POINT('Ctrl Pts',(-69.5567149010135,-4.06163170567629,
133.578172824088));
#91007=CARTESIAN_POINT('Ctrl Pts',(-69.5590646045779,-4.03822240922261,
133.612143192054));
#91008=CARTESIAN_POINT('Ctrl Pts',(-69.5614143081424,-4.01440079892208,
133.645798508514));
#91009=CARTESIAN_POINT('Ctrl Pts',(-69.5691886422613,-3.9355835555347,133.75715199114));
#91010=CARTESIAN_POINT('Ctrl Pts',(-69.5769629763802,-3.85200479108893,
133.865399955488));
#91011=CARTESIAN_POINT('Ctrl Pts',(-69.5847373104992,-3.76393745608926,
133.970108221079));
#91012=CARTESIAN_POINT('Ctrl Pts',(-69.5925020634461,-3.67597865620906,
134.074687443091));
#91013=CARTESIAN_POINT('Ctrl Pts',(-69.6002668163931,-3.58354254157078,
134.175735349814));
#91014=CARTESIAN_POINT('Ctrl Pts',(-69.6080315693401,-3.48694521442781,
134.272846761993));
#91015=CARTESIAN_POINT('Ctrl Pts',(-69.6157886102249,-3.39044382911221,
134.369861721747));
#91016=CARTESIAN_POINT('Ctrl Pts',(-69.6235456511098,-3.28978973003388,
134.462947692207));
#91017=CARTESIAN_POINT('Ctrl Pts',(-69.6313026919946,-3.18533891129155,
134.551732907947));
#91018=CARTESIAN_POINT('Ctrl Pts',(-69.6390538832347,-3.08096685972415,
134.640451170064));
#91019=CARTESIAN_POINT('Ctrl Pts',(-69.6468050744747,-2.97280408407458,
134.724874880731));
#91020=CARTESIAN_POINT('Ctrl Pts',(-69.6545562657147,-2.86124275480197,
134.804669725697));
#91021=CARTESIAN_POINT('Ctrl Pts',(-69.6623041624916,-2.74972884207,134.884430655725));
#91022=CARTESIAN_POINT('Ctrl Pts',(-69.6700520592686,-2.63481956599732,
134.95956640607));
#91023=CARTESIAN_POINT('Ctrl Pts',(-69.6777999560456,-2.51693926172928,
135.029783651449));
#91024=CARTESIAN_POINT('Ctrl Pts',(-69.6855462321295,-2.39908361548001,
135.099986208893));
#91025=CARTESIAN_POINT('Ctrl Pts',(-69.6932925082135,-2.27825851286104,
135.165272107847));
#91026=CARTESIAN_POINT('Ctrl Pts',(-69.7010387842975,-2.15491594703655,
135.22539220801));
#91027=CARTESIAN_POINT('Ctrl Pts',(-69.7087851175627,-2.03157247072508,
135.285512751967));
#91028=CARTESIAN_POINT('Ctrl Pts',(-69.716531450828,-1.90571184556632,135.340467249741));
#91029=CARTESIAN_POINT('Ctrl Pts',(-69.7242777840933,-1.77780889504602,
135.390053432746));
#91030=CARTESIAN_POINT('Ctrl Pts',(-69.7320258520962,-1.64987730154659,
135.439650720233));
#91031=CARTESIAN_POINT('Ctrl Pts',(-69.739773920099,-1.51990283704257,135.483877159422));
#91032=CARTESIAN_POINT('Ctrl Pts',(-69.7475219881019,-1.38837806388366,
135.522579499117));
#91033=CARTESIAN_POINT('Ctrl Pts',(-69.7552782908436,-1.25671350463086,
135.56132297212));
#91034=CARTESIAN_POINT('Ctrl Pts',(-69.7630345935854,-1.12349572095419,
135.594530506975));
#91035=CARTESIAN_POINT('Ctrl Pts',(-69.7707908963272,-0.989230665783423,
135.622099273032));
#91036=CARTESIAN_POINT('Ctrl Pts',(-69.7785513388412,-0.85489394931007,
135.64968275337));
#91037=CARTESIAN_POINT('Ctrl Pts',(-69.7863117813552,-0.71950923330896,
135.671621405558));
#91038=CARTESIAN_POINT('Ctrl Pts',(-69.7940722238693,-0.583589306701709,
135.687864132831));
#91039=CARTESIAN_POINT('Ctrl Pts',(-69.8018451241346,-0.447451189362046,
135.704132934372));
#91040=CARTESIAN_POINT('Ctrl Pts',(-69.8096180244,-0.310776534554623,135.714687509043));
#91041=CARTESIAN_POINT('Ctrl Pts',(-69.8173909246653,-0.174080761691003,
135.719528870119));
#91042=CARTESIAN_POINT('Ctrl Pts',(-69.8248812604285,-0.0423542244631702,
135.724194235527));
#91043=CARTESIAN_POINT('Ctrl Pts',(-69.8323715961918,0.0893916140735198,
135.723554556645));
#91044=CARTESIAN_POINT('Ctrl Pts',(-69.839861931955,0.220700482344392,135.717656289474));
#91045=CARTESIAN_POINT('Ctrl Pts',(-69.8476362660741,0.356987966243205,
135.711534387712));
#91046=CARTESIAN_POINT('Ctrl Pts',(-69.8554106001932,0.493236408100186,
135.699727874943));
#91047=CARTESIAN_POINT('Ctrl Pts',(-69.8631849343122,0.628932983167448,
135.682231707005));
#91048=CARTESIAN_POINT('Ctrl Pts',(-69.8709496872593,0.764462324333305,
135.66475710153));
#91049=CARTESIAN_POINT('Ctrl Pts',(-69.8787144402063,0.899440767925499,
135.641606842174));
#91050=CARTESIAN_POINT('Ctrl Pts',(-69.8864791931533,1.03335656417244,135.61282786543));
#91051=CARTESIAN_POINT('Ctrl Pts',(-69.8942362340383,1.16713935336285,135.584077472372));
#91052=CARTESIAN_POINT('Ctrl Pts',(-69.9019932749233,1.2998612158091,135.549709568929));
#91053=CARTESIAN_POINT('Ctrl Pts',(-69.9097503158083,1.43101695122329,135.509822714726));
#91054=CARTESIAN_POINT('Ctrl Pts',(-69.9175015070484,1.5620737810768,135.46996593951));
#91055=CARTESIAN_POINT('Ctrl Pts',(-69.9252526982883,1.6915664621274,135.424598610806));
#91056=CARTESIAN_POINT('Ctrl Pts',(-69.9330038895284,1.8190017486142,135.373869967708));
#91057=CARTESIAN_POINT('Ctrl Pts',(-69.9407517863054,1.94638287170496,135.323162885637));
#91058=CARTESIAN_POINT('Ctrl Pts',(-69.9484996830824,2.07170797695909,135.267099165631));
#91059=CARTESIAN_POINT('Ctrl Pts',(-69.9562475798595,2.19450091799564,135.205877263384));
#91060=CARTESIAN_POINT('Ctrl Pts',(-69.9639938559435,2.31726817339603,135.14466816744));
#91061=CARTESIAN_POINT('Ctrl Pts',(-69.9717401320276,2.4375039684628,135.078303209742));
#91062=CARTESIAN_POINT('Ctrl Pts',(-69.9794864081117,2.5547543810588,135.007027998523));
#91063=CARTESIAN_POINT('Ctrl Pts',(-69.987232741377,2.67200565917056,134.935752261167));
#91064=CARTESIAN_POINT('Ctrl Pts',(-69.9949790746423,2.7862711767559,134.859566401047));
#91065=CARTESIAN_POINT('Ctrl Pts',(-70.0027254079076,2.89712410583148,134.778760569497));
#91066=CARTESIAN_POINT('Ctrl Pts',(-70.0104734759105,3.00800185965223,134.697936642041));
#91067=CARTESIAN_POINT('Ctrl Pts',(-70.0182215439134,3.11546518836735,134.612490914657));
#91068=CARTESIAN_POINT('Ctrl Pts',(-70.0259696119163,3.2191189154243,134.522754957985));
#91069=CARTESIAN_POINT('Ctrl Pts',(-70.0337259146581,3.32288280689571,134.43292362887));
#91070=CARTESIAN_POINT('Ctrl Pts',(-70.0414822174,3.42282871255838,134.338793218266));
#91071=CARTESIAN_POINT('Ctrl Pts',(-70.0492385201418,3.51859663815677,134.240733816224));
#91072=CARTESIAN_POINT('Ctrl Pts',(-70.0569989626559,3.61441567798057,134.142622076926));
#91073=CARTESIAN_POINT('Ctrl Pts',(-70.0647594051701,3.70605203335514,134.040577458447));
#91074=CARTESIAN_POINT('Ctrl Pts',(-70.0725198476842,3.79318554018795,133.93500376558));
#91075=CARTESIAN_POINT('Ctrl Pts',(-70.0802927479495,3.88045892146129,133.829260596449));
#91076=CARTESIAN_POINT('Ctrl Pts',(-70.0880656482149,3.9632147734412,133.719977343951));
#91077=CARTESIAN_POINT('Ctrl Pts',(-70.0958385484803,4.04117535184151,133.607588192732));
#91078=CARTESIAN_POINT('Ctrl Pts',(-70.1033288842428,4.11630186685181,133.499284670242));
#91079=CARTESIAN_POINT('Ctrl Pts',(-70.1108192200053,4.18697553068549,133.388097402995));
#91080=CARTESIAN_POINT('Ctrl Pts',(-70.1183095557679,4.25298880215847,133.27443537579));
#91081=CARTESIAN_POINT('Ctrl Pts',(-70.126083889887,4.32150498687929,133.156463818284));
#91082=CARTESIAN_POINT('Ctrl Pts',(-70.1338582240061,4.38521744418695,133.03545243685));
#91083=CARTESIAN_POINT('Ctrl Pts',(-70.1416325581253,4.44384473598061,132.911829958979));
#91084=CARTESIAN_POINT('Ctrl Pts',(-70.1493973110724,4.50239977487689,132.788359834764));
#91085=CARTESIAN_POINT('Ctrl Pts',(-70.1571620640195,4.55588195182488,132.662285366721));
#91086=CARTESIAN_POINT('Ctrl Pts',(-70.1649268169667,4.60405414257455,132.534062474749));
#91087=CARTESIAN_POINT('Ctrl Pts',(-70.1726838578518,4.65217848802519,132.405966935561));
#91088=CARTESIAN_POINT('Ctrl Pts',(-70.1804408987369,4.69500320607329,132.275727582511));
#91089=CARTESIAN_POINT('Ctrl Pts',(-70.1881979396219,4.73233814462599,132.143822728795));
#91090=CARTESIAN_POINT('Ctrl Pts',(-70.1959491308621,4.7696449286113,132.012017345554));
#91091=CARTESIAN_POINT('Ctrl Pts',(-70.2037003221023,4.80147006724533,131.878549336237));
#91092=CARTESIAN_POINT('Ctrl Pts',(-70.2114515133426,4.82767250822328,131.743914349848));
#91093=CARTESIAN_POINT('Ctrl Pts',(-70.2191994101197,4.85386381246473,131.60933658692));
#91094=CARTESIAN_POINT('Ctrl Pts',(-70.2269473068968,4.87443709764183,131.473593216381));
#91095=CARTESIAN_POINT('Ctrl Pts',(-70.2346952036739,4.88930196140111,131.337192103816));
#91096=CARTESIAN_POINT('Ctrl Pts',(-70.2424414797581,4.90416371575131,131.200819523423));
#91097=CARTESIAN_POINT('Ctrl Pts',(-70.2501877558423,4.9133193814423,131.063789863088));
#91098=CARTESIAN_POINT('Ctrl Pts',(-70.2579340319265,4.91673023963269,130.926617777608));
#91099=CARTESIAN_POINT('Ctrl Pts',(-70.2656803651919,4.92014112300127,130.789444679554));
#91100=CARTESIAN_POINT('Ctrl Pts',(-70.2734266984572,4.91780710453085,130.652129545102));
#91101=CARTESIAN_POINT('Ctrl Pts',(-70.2811730317226,4.90974158580548,130.515188310607));
#91102=CARTESIAN_POINT('Ctrl Pts',(-70.2889210997256,4.90167426086311,130.378216409071));
#91103=CARTESIAN_POINT('Ctrl Pts',(-70.2966691677287,4.8878729045729,130.241618964322));
#91104=CARTESIAN_POINT('Ctrl Pts',(-70.3044172357317,4.86840287412582,130.105907671618));
#91105=CARTESIAN_POINT('Ctrl Pts',(-70.3121735384736,4.8489121506987,129.970052143337));
#91106=CARTESIAN_POINT('Ctrl Pts',(-70.3199298412155,4.82374077366935,129.835085036092));
#91107=CARTESIAN_POINT('Ctrl Pts',(-70.3276861439574,4.79300552459065,129.701509265958));
#91108=CARTESIAN_POINT('Ctrl Pts',(-70.3354465864716,4.76225387118414,129.567862202414));
#91109=CARTESIAN_POINT('Ctrl Pts',(-70.3432070289859,4.72593253202465,129.435608332494));
#91110=CARTESIAN_POINT('Ctrl Pts',(-70.3509674715001,4.68420818300894,129.30523528567));
#91111=CARTESIAN_POINT('Ctrl Pts',(-70.3587403717655,4.64241685436408,129.174652952458));
#91112=CARTESIAN_POINT('Ctrl Pts',(-70.366513272031,4.59520531839163,129.045957843051));
#91113=CARTESIAN_POINT('Ctrl Pts',(-70.3742861722965,4.54278873936122,128.919618318992));
#91114=CARTESIAN_POINT('Ctrl Pts',(-70.3817765080579,4.49227763501229,128.797871554874));
#91115=CARTESIAN_POINT('Ctrl Pts',(-70.3892668438194,4.43693347970021,128.678312366079));
#91116=CARTESIAN_POINT('Ctrl Pts',(-70.3967571795808,4.37698818284047,128.56133642916));
#91117=CARTESIAN_POINT('Ctrl Pts',(-70.4045315136999,4.31477004182549,128.439925314029));
#91118=CARTESIAN_POINT('Ctrl Pts',(-70.412305847819,4.24739787884373,128.320912611734));
#91119=CARTESIAN_POINT('Ctrl Pts',(-70.4200801819381,4.17508027030704,128.204766841802));
#91120=CARTESIAN_POINT('Ctrl Pts',(-70.4278449348851,4.10285178675966,128.088764211151));
#91121=CARTESIAN_POINT('Ctrl Pts',(-70.4356096878322,4.02569018919691,127.975621811474));
#91122=CARTESIAN_POINT('Ctrl Pts',(-70.4433744407793,3.94385088449194,127.865785577961));
#91123=CARTESIAN_POINT('Ctrl Pts',(-70.4511314816642,3.86209286373847,127.756058435343));
#91124=CARTESIAN_POINT('Ctrl Pts',(-70.4588885225492,3.77566661360599,127.649631235595));
#91125=CARTESIAN_POINT('Ctrl Pts',(-70.4666455634342,3.68487177068056,127.546922499022));
#91126=CARTESIAN_POINT('Ctrl Pts',(-70.4743967546743,3.59414539685198,127.444291215906));
#91127=CARTESIAN_POINT('Ctrl Pts',(-70.4821479459145,3.49905724540849,127.345373106266));
#91128=CARTESIAN_POINT('Ctrl Pts',(-70.4898991371546,3.39994807767874,127.250554751795));
#91129=CARTESIAN_POINT('Ctrl Pts',(-70.4976470339317,3.30088103398923,127.155776697654));
#91130=CARTESIAN_POINT('Ctrl Pts',(-70.5053949307087,3.19779665507245,127.065095202676));
#91131=CARTESIAN_POINT('Ctrl Pts',(-70.5131428274857,3.09107335794886,126.978860838677));
#91132=CARTESIAN_POINT('Ctrl Pts',(-70.5208891035698,2.98437238503833,126.892644513048));
#91133=CARTESIAN_POINT('Ctrl Pts',(-70.5286353796538,2.87403431186303,126.810873713653));
#91134=CARTESIAN_POINT('Ctrl Pts',(-70.5363816557379,2.760471203601,126.733859199241));
#91135=CARTESIAN_POINT('Ctrl Pts',(-70.5441279890032,2.64690725704221,126.656844116324));
#91136=CARTESIAN_POINT('Ctrl Pts',(-70.5518743222686,2.53011855146796,126.584585607887));
#91137=CARTESIAN_POINT('Ctrl Pts',(-70.559620655534,2.41054640262869,126.517351274997));
#91138=CARTESIAN_POINT('Ctrl Pts',(-70.567368723537,2.29094747643493,126.450101885444));
#91139=CARTESIAN_POINT('Ctrl Pts',(-70.5751167915398,2.1685642073369,126.387879101901));
#91140=CARTESIAN_POINT('Ctrl Pts',(-70.5828648595428,2.04386242620345,126.330904521296));
#91141=CARTESIAN_POINT('Ctrl Pts',(-70.5906211622846,1.91902811053372,126.273869387429));
#91142=CARTESIAN_POINT('Ctrl Pts',(-70.5983774650265,1.79187071661352,126.222093761593));
#91143=CARTESIAN_POINT('Ctrl Pts',(-70.6061337677683,1.66287648526213,126.175751230584));
#91144=CARTESIAN_POINT('Ctrl Pts',(-70.6138942102825,1.53381340580536,126.129383965169));
#91145=CARTESIAN_POINT('Ctrl Pts',(-70.6216546527966,1.40291190840469,126.088455689305));
#91146=CARTESIAN_POINT('Ctrl Pts',(-70.6294150953108,1.27067234193961,126.053089749479));
#91147=CARTESIAN_POINT('Ctrl Pts',(-70.6371879955762,1.13822049278277,126.017667037107));
#91148=CARTESIAN_POINT('Ctrl Pts',(-70.6449608958416,1.00442666400649,125.987824589233));
#91149=CARTESIAN_POINT('Ctrl Pts',(-70.652733796107,0.869801202983778,125.963634542917));
#91150=CARTESIAN_POINT('Ctrl Pts',(-70.6602241318692,0.740069716566674,
125.940323865715));
#91151=CARTESIAN_POINT('Ctrl Pts',(-70.6677144676315,0.609566317125854,
125.922261809065));
#91152=CARTESIAN_POINT('Ctrl Pts',(-70.6752048033937,0.478749251252998,
125.90946713385));
#91153=CARTESIAN_POINT('Ctrl Pts',(-70.6829791375128,0.342972216569107,
125.896187344635));
#91154=CARTESIAN_POINT('Ctrl Pts',(-70.6907534716319,0.206427159764203,
125.888540180794));
#91155=CARTESIAN_POINT('Ctrl Pts',(-70.6985278057511,0.069621000229875,
125.88660340733));
#91156=CARTESIAN_POINT('Ctrl Pts',(-70.7062925586982,-0.0670165579389881,
125.884669020767));
#91157=CARTESIAN_POINT('Ctrl Pts',(-70.7140573116453,-0.203914191406301,
125.888431027445));
#91158=CARTESIAN_POINT('Ctrl Pts',(-70.7218220645924,-0.340558668614846,
125.89791558519));
#91159=CARTESIAN_POINT('Ctrl Pts',(-70.7295791054775,-0.477067428602092,
125.907390722738));
#91160=CARTESIAN_POINT('Ctrl Pts',(-70.7373361463625,-0.613323145201315,
125.922577073601));
#91161=CARTESIAN_POINT('Ctrl Pts',(-70.7450931872475,-0.74881174453205,
125.94344876548));
#91162=CARTESIAN_POINT('Ctrl Pts',(-70.7528443784877,-0.884198170856636,
125.964304717854));
#91163=CARTESIAN_POINT('Ctrl Pts',(-70.7605955697279,-1.01881824651647,
125.990837418231));
#91164=CARTESIAN_POINT('Ctrl Pts',(-70.7683467609681,-1.15216253956335,
126.022969131301));
#91165=CARTESIAN_POINT('Ctrl Pts',(-70.7760946577453,-1.28545015772879,
126.055087187536));
#91166=CARTESIAN_POINT('Ctrl Pts',(-70.7838425545224,-1.41746269246836,
126.092799431967));
#91167=CARTESIAN_POINT('Ctrl Pts',(-70.7915904512995,-1.5477006541428,126.135976984266));
#91168=CARTESIAN_POINT('Ctrl Pts',(-70.7993367273837,-1.6779113728429,126.179145504751));
#91169=CARTESIAN_POINT('Ctrl Pts',(-70.8070830034678,-1.80634788595232,
126.227776936215));
#91170=CARTESIAN_POINT('Ctrl Pts',(-70.814829279552,-1.93252601204163,126.281692569247));
#91171=CARTESIAN_POINT('Ctrl Pts',(-70.8225756128174,-2.05870506954937,
126.335608600272));
#91172=CARTESIAN_POINT('Ctrl Pts',(-70.8303219460828,-2.18262534725211,
126.394808757078));
#91173=CARTESIAN_POINT('Ctrl Pts',(-70.8380682793482,-2.30382316284822,
126.459066393141));
#91174=CARTESIAN_POINT('Ctrl Pts',(-70.8458163473512,-2.42504811985448,
126.523338419255));
#91175=CARTESIAN_POINT('Ctrl Pts',(-70.8535644153542,-2.54354905621517,
126.592669995241));
#91176=CARTESIAN_POINT('Ctrl Pts',(-70.8613124833572,-2.65888774319492,
126.666788982949));
#91177=CARTESIAN_POINT('Ctrl Pts',(-70.8690687860991,-2.7743490135039,126.740986745199));
#91178=CARTESIAN_POINT('Ctrl Pts',(-70.876825088841,-2.88664099128814,126.819981871536));
#91179=CARTESIAN_POINT('Ctrl Pts',(-70.8845813915829,-2.99535480802067,
126.90345910169));
#91180=CARTESIAN_POINT('Ctrl Pts',(-70.8923418340972,-3.10412664859066,
126.986980886155));
#91181=CARTESIAN_POINT('Ctrl Pts',(-70.9001022766114,-3.20931622301673,
127.074989290409));
#91182=CARTESIAN_POINT('Ctrl Pts',(-70.9078627191256,-3.3105493056135,127.16713002856));
#91183=CARTESIAN_POINT('Ctrl Pts',(-70.9156356193911,-3.41194489654151,
127.259418679203));
#91184=CARTESIAN_POINT('Ctrl Pts',(-70.9234085196567,-3.50937102566989,
127.355852644575));
#91185=CARTESIAN_POINT('Ctrl Pts',(-70.9311814199222,-3.60249114682615,
127.456041546817));
#91186=CARTESIAN_POINT('Ctrl Pts',(-70.9386717556838,-3.69222611701703,
127.552588330097));
#91187=CARTESIAN_POINT('Ctrl Pts',(-70.9461620914453,-3.77796251193308,
127.652621553277));
#91188=CARTESIAN_POINT('Ctrl Pts',(-70.9536524272069,-3.85943685403772,
127.755765821238));
#91189=CARTESIAN_POINT('Ctrl Pts',(-70.9614213020186,-3.94394093827576,
127.862745659103));
#91190=CARTESIAN_POINT('Ctrl Pts',(-70.9691901768302,-4.02413301129352,
127.973418231407));
#91191=CARTESIAN_POINT('Ctrl Pts',(-70.9769590516418,-4.09967228073009,
128.087400873088));
#91192=CARTESIAN_POINT('Ctrl Pts',(-70.984715528078,-4.17509099677335,128.201201609459));
#91193=CARTESIAN_POINT('Ctrl Pts',(-70.9924720045142,-4.24587148194348,
128.318301572758));
#91194=CARTESIAN_POINT('Ctrl Pts',(-71.0002284809504,-4.31171306470087,
128.438285067169));
#91195=CARTESIAN_POINT('Ctrl Pts',(-71.0079778176759,-4.37749404134967,
128.558158118719));
#91196=CARTESIAN_POINT('Ctrl Pts',(-71.0157271544014,-4.4383449695204,128.680909082619));
#91197=CARTESIAN_POINT('Ctrl Pts',(-71.023476491127,-4.49400821765804,128.806093067381));
#91198=CARTESIAN_POINT('Ctrl Pts',(-71.0312247147739,-4.54966347058655,
128.9312590713));
#91199=CARTESIAN_POINT('Ctrl Pts',(-71.0389729384209,-4.60013233288696,
129.058857060701));
#91200=CARTESIAN_POINT('Ctrl Pts',(-71.0467211620678,-4.64520277425386,
129.188416853518));
#91201=CARTESIAN_POINT('Ctrl Pts',(-71.0544693857148,-4.6902732156207,129.317976646336));
#91202=CARTESIAN_POINT('Ctrl Pts',(-71.0622176093617,-4.72994507621285,
129.449497883561));
#91203=CARTESIAN_POINT('Ctrl Pts',(-71.0699658330086,-4.76405452823398,
129.582490119308));
#91204=CARTESIAN_POINT('Origin',(213.235140564004,0.,130.804360617566));
#91205=CARTESIAN_POINT('',(-73.1652357600351,-4.76405452823407,129.582490119308));
#91206=CARTESIAN_POINT('',(-72.8197282857816,-4.76405452823409,129.582490119308));
#91207=CARTESIAN_POINT('',(213.235140564004,-4.76405452823405,129.582490119308));
#91208=CARTESIAN_POINT('',(-71.4851405639545,-4.91824995845192,130.804999904443));
#91209=CARTESIAN_POINT('Ctrl Pts',(-71.4851405640084,-4.91824995845179,
130.804999905388));
#91210=CARTESIAN_POINT('Ctrl Pts',(-71.4870799355632,-4.91824553450007,
130.839034810544));
#91211=CARTESIAN_POINT('Ctrl Pts',(-71.489019307118,-4.91788782706535,130.873067104726));
#91212=CARTESIAN_POINT('Ctrl Pts',(-71.4909586786726,-4.9171769671839,130.907091994935));
#91213=CARTESIAN_POINT('Ctrl Pts',(-71.4987330127917,-4.91432735220566,
131.043487140169));
#91214=CARTESIAN_POINT('Ctrl Pts',(-71.5065073469109,-4.90579382634764,
131.179979669595));
#91215=CARTESIAN_POINT('Ctrl Pts',(-71.51428168103,-4.89155904051835,131.316057027191));
#91216=CARTESIAN_POINT('Ctrl Pts',(-71.5220464339771,-4.87734179779038,
131.451966681605));
#91217=CARTESIAN_POINT('Ctrl Pts',(-71.5298111869242,-4.8574373156064,131.587461797135));
#91218=CARTESIAN_POINT('Ctrl Pts',(-71.5375759398713,-4.83188023636037,
131.722029645032));
#91219=CARTESIAN_POINT('Ctrl Pts',(-71.5453329807564,-4.80634854076567,
131.856463838246));
#91220=CARTESIAN_POINT('Ctrl Pts',(-71.5530900216415,-4.775175493174,131.989972214996));
#91221=CARTESIAN_POINT('Ctrl Pts',(-71.5608470625266,-4.73844750141264,
132.122047355321));
#91222=CARTESIAN_POINT('Ctrl Pts',(-71.5685982537667,-4.70174720651567,
132.254022896755));
#91223=CARTESIAN_POINT('Ctrl Pts',(-71.5763494450069,-4.65950040977517,
132.384566977912));
#91224=CARTESIAN_POINT('Ctrl Pts',(-71.584100636247,-4.61184447077059,132.513182913746));
#91225=CARTESIAN_POINT('Ctrl Pts',(-71.5918485330241,-4.56420878681129,
132.641744184377));
#91226=CARTESIAN_POINT('Ctrl Pts',(-71.5995964298013,-4.51116866873738,
132.768378573794));
#91227=CARTESIAN_POINT('Ctrl Pts',(-71.6073443265784,-4.45291108889233,
132.892605310345));
#91228=CARTESIAN_POINT('Ctrl Pts',(-71.6150906026625,-4.39466569527709,
133.016806061341));
#91229=CARTESIAN_POINT('Ctrl Pts',(-71.6228368787467,-4.33120517660153,
133.138599807467));
#91230=CARTESIAN_POINT('Ctrl Pts',(-71.6305831548308,-4.26276417748866,
133.257526863384));
#91231=CARTESIAN_POINT('Ctrl Pts',(-71.6383294880962,-4.19432267315998,
133.376454797193));
#91232=CARTESIAN_POINT('Ctrl Pts',(-71.6460758213616,-4.12090081004148,
133.492515659709));
#91233=CARTESIAN_POINT('Ctrl Pts',(-71.653822154627,-4.04277841321618,133.605275783031));
#91234=CARTESIAN_POINT('Ctrl Pts',(-71.66157022263,-3.96463852142177,133.718061158202));
#91235=CARTESIAN_POINT('Ctrl Pts',(-71.6693182906329,-3.8817962238749,133.827544001991));
#91236=CARTESIAN_POINT('Ctrl Pts',(-71.6770663586359,-3.79457351258423,
133.933321294867));
#91237=CARTESIAN_POINT('Ctrl Pts',(-71.6848226613778,-3.70725809995791,
134.039211009108));
#91238=CARTESIAN_POINT('Ctrl Pts',(-71.6925789641197,-3.61555322273975,
134.141387003128));
#91239=CARTESIAN_POINT('Ctrl Pts',(-71.7003352668616,-3.51982022553436,
134.2394805052));
#91240=CARTESIAN_POINT('Ctrl Pts',(-71.7080957093758,-3.4240361327459,134.337626362727));
#91241=CARTESIAN_POINT('Ctrl Pts',(-71.71585615189,-3.32421992045408,134.431685118572));
#91242=CARTESIAN_POINT('Ctrl Pts',(-71.7236165944042,-3.22076759411128,
134.521327010637));
#91243=CARTESIAN_POINT('Ctrl Pts',(-71.7313894946697,-3.11714919691017,
134.611112803827));
#91244=CARTESIAN_POINT('Ctrl Pts',(-71.7391623949351,-3.00988332755102,
134.696467320899));
#91245=CARTESIAN_POINT('Ctrl Pts',(-71.7469352952005,-2.89939738054973,
134.777102478317));
#91246=CARTESIAN_POINT('Ctrl Pts',(-71.7544256309622,-2.79292787602493,
134.854806344651));
#91247=CARTESIAN_POINT('Ctrl Pts',(-71.7619159667239,-2.68346860103983,
134.928127844043));
#91248=CARTESIAN_POINT('Ctrl Pts',(-71.7694063024856,-2.57142344220033,
134.996849680569));
#91249=CARTESIAN_POINT('Ctrl Pts',(-71.7771806366047,-2.45513005710246,
135.068177126418));
#91250=CARTESIAN_POINT('Ctrl Pts',(-71.7849549707237,-2.33568244725872,
135.134775175601));
#91251=CARTESIAN_POINT('Ctrl Pts',(-71.7927293048428,-2.21350246295819,
135.196352182788));
#91252=CARTESIAN_POINT('Ctrl Pts',(-71.8004940577899,-2.09147305456877,
135.257853301816));
#91253=CARTESIAN_POINT('Ctrl Pts',(-71.808258810737,-1.96671831763929,135.314345516826));
#91254=CARTESIAN_POINT('Ctrl Pts',(-71.8160235636841,-1.83968835044573,
135.365580831032));
#91255=CARTESIAN_POINT('Ctrl Pts',(-71.8237806045691,-1.71278455120639,
135.416765257603));
#91256=CARTESIAN_POINT('Ctrl Pts',(-71.8315376454541,-1.58361037902625,
135.462703028554));
#91257=CARTESIAN_POINT('Ctrl Pts',(-71.8392946863391,-1.4526394462314,135.503192568355));
#91258=CARTESIAN_POINT('Ctrl Pts',(-71.8470458775792,-1.32176727963596,
135.543651574678));
#91259=CARTESIAN_POINT('Ctrl Pts',(-71.8547970688194,-1.18910142138563,
135.578670412671));
#91260=CARTESIAN_POINT('Ctrl Pts',(-71.8625482600595,-1.05513399288357,
135.608096176437));
#91261=CARTESIAN_POINT('Ctrl Pts',(-71.8702961568366,-0.921223504111953,
135.637509433469));
#91262=CARTESIAN_POINT('Ctrl Pts',(-71.8780440536136,-0.786012926428039,
135.661334260656));
#91263=CARTESIAN_POINT('Ctrl Pts',(-71.8857919503907,-0.650007809757516,
135.679468094305));
#91264=CARTESIAN_POINT('Ctrl Pts',(-71.8935382264748,-0.514031142425655,
135.697598134746));
#91265=CARTESIAN_POINT('Ctrl Pts',(-71.9012845025588,-0.377260653979112,
135.710039497848));
#91266=CARTESIAN_POINT('Ctrl Pts',(-71.9090307786429,-0.240209921862925,
135.716741125623));
#91267=CARTESIAN_POINT('Ctrl Pts',(-71.9167771119083,-0.103158178069368,
135.723442802868));
#91268=CARTESIAN_POINT('Ctrl Pts',(-71.9245234451736,0.0341734230231403,
135.724404641145));
#91269=CARTESIAN_POINT('Ctrl Pts',(-71.932269778439,0.171268772036229,135.71962765713));
#91270=CARTESIAN_POINT('Ctrl Pts',(-71.940017846442,0.308394822602178,135.714849603343));
#91271=CARTESIAN_POINT('Ctrl Pts',(-71.9477659144449,0.445284125156572,
135.704330183536));
#91272=CARTESIAN_POINT('Ctrl Pts',(-71.9555139824479,0.581423563406765,
135.688122456806));
#91273=CARTESIAN_POINT('Ctrl Pts',(-71.9632702851898,0.717707692272011,
135.67189750431));
#91274=CARTESIAN_POINT('Ctrl Pts',(-71.9710265879316,0.853239975967523,
135.649972214446));
#91275=CARTESIAN_POINT('Ctrl Pts',(-71.9787828906735,0.987514840810215,
135.622451266535));
#91276=CARTESIAN_POINT('Ctrl Pts',(-71.9865433331877,1.12186137219139,135.594915629865));
#91277=CARTESIAN_POINT('Ctrl Pts',(-71.9943037757019,1.25494876825523,135.561778478569));
#91278=CARTESIAN_POINT('Ctrl Pts',(-72.0020642182161,1.38628554019205,135.523194738782));
#91279=CARTESIAN_POINT('Ctrl Pts',(-72.0098371184815,1.51783314557453,135.484549060951));
#91280=CARTESIAN_POINT('Ctrl Pts',(-72.0176100187469,1.64762414065546,135.44043944851));
#91281=CARTESIAN_POINT('Ctrl Pts',(-72.0253829190123,1.77518513542065,135.391069764382));
#91282=CARTESIAN_POINT('Ctrl Pts',(-72.0328732547744,1.89810896672022,135.343494792626));
#91283=CARTESIAN_POINT('Ctrl Pts',(-72.0403635905365,2.01896183255949,135.291035665929));
#91284=CARTESIAN_POINT('Ctrl Pts',(-72.0478539262985,2.13734260514679,135.233914731777));
#91285=CARTESIAN_POINT('Ctrl Pts',(-72.0556282604176,2.26021182070693,135.174628040045));
#91286=CARTESIAN_POINT('Ctrl Pts',(-72.0634025945367,2.38080699643011,135.110131255283));
#91287=CARTESIAN_POINT('Ctrl Pts',(-72.0711769286558,2.49865474245378,135.04062165066));
#91288=CARTESIAN_POINT('Ctrl Pts',(-72.0789416816028,2.61635725166268,134.971197710413));
#91289=CARTESIAN_POINT('Ctrl Pts',(-72.0867064345499,2.73131873470714,134.896773439108));
#91290=CARTESIAN_POINT('Ctrl Pts',(-72.094471187497,2.84308725575626,134.817593468854));
#91291=CARTESIAN_POINT('Ctrl Pts',(-72.102228228382,2.95474476673477,134.738492141262));
#91292=CARTESIAN_POINT('Ctrl Pts',(-72.109985269267,3.06321530977931,134.654644739096));
#91293=CARTESIAN_POINT('Ctrl Pts',(-72.117742310152,3.16807329465536,134.56634076932));
#91294=CARTESIAN_POINT('Ctrl Pts',(-72.1254935013921,3.27285220530935,134.478103390255));
#91295=CARTESIAN_POINT('Ctrl Pts',(-72.1332446926322,3.37402368242551,134.385416383734));
#91296=CARTESIAN_POINT('Ctrl Pts',(-72.1409958838723,3.471193078305,134.28861113606));
#91297=CARTESIAN_POINT('Ctrl Pts',(-72.1487437806494,3.56832117459916,134.191847033199));
#91298=CARTESIAN_POINT('Ctrl Pts',(-72.1564916774265,3.66145029640585,134.09096844588));
#91299=CARTESIAN_POINT('Ctrl Pts',(-72.1642395742036,3.75022089190135,133.986345269391));
#91300=CARTESIAN_POINT('Ctrl Pts',(-72.1719858502877,3.83897291850182,133.881743977815));
#91301=CARTESIAN_POINT('Ctrl Pts',(-72.1797321263717,3.92336797944733,133.773399952997));
#91302=CARTESIAN_POINT('Ctrl Pts',(-72.1874784024558,4.00308551705314,133.661717684098));
#91303=CARTESIAN_POINT('Ctrl Pts',(-72.1952247357211,4.0828036431157,133.550034590786));
#91304=CARTESIAN_POINT('Ctrl Pts',(-72.2029710689865,4.15784394980044,133.435013522437));
#91305=CARTESIAN_POINT('Ctrl Pts',(-72.2107174022518,4.22792832273901,133.317089246026));
#91306=CARTESIAN_POINT('Ctrl Pts',(-72.2184654702547,4.29802839058697,133.199138561291));
#91307=CARTESIAN_POINT('Ctrl Pts',(-72.2262135382578,4.36317011651623,133.078283710789));
#91308=CARTESIAN_POINT('Ctrl Pts',(-72.2339616062607,4.42312078875598,132.954985073526));
#91309=CARTESIAN_POINT('Ctrl Pts',(-72.2417179090026,4.4831351772836,132.831555393005));
#91310=CARTESIAN_POINT('Ctrl Pts',(-72.2494742117444,4.53794731986127,132.705677089531));
#91311=CARTESIAN_POINT('Ctrl Pts',(-72.2572305144863,4.58737201124352,132.577832098295));
#91312=CARTESIAN_POINT('Ctrl Pts',(-72.2649909570004,4.63682308207178,132.449918872338));
#91313=CARTESIAN_POINT('Ctrl Pts',(-72.2727513995146,4.68088084660649,132.320037237103));
#91314=CARTESIAN_POINT('Ctrl Pts',(-72.2805118420287,4.71940998688618,132.188684437407));
#91315=CARTESIAN_POINT('Ctrl Pts',(-72.2882847422942,4.75800097756231,132.057120778536));
#91316=CARTESIAN_POINT('Ctrl Pts',(-72.2960576425596,4.79104551452926,131.924081615541));
#91317=CARTESIAN_POINT('Ctrl Pts',(-72.303830542825,4.81845923457119,131.790075417737));
#91318=CARTESIAN_POINT('Ctrl Pts',(-72.3113208785872,4.84487639683905,131.660940682762));
#91319=CARTESIAN_POINT('Ctrl Pts',(-72.3188112143493,4.86606497381129,131.530908304634));
#91320=CARTESIAN_POINT('Ctrl Pts',(-72.3263015501114,4.88199521335488,131.400435947772));
#91321=CARTESIAN_POINT('Ctrl Pts',(-72.3340758842305,4.89852945277239,131.265016691845));
#91322=CARTESIAN_POINT('Ctrl Pts',(-72.3418502183495,4.90945111928723,131.128694467491));
#91323=CARTESIAN_POINT('Ctrl Pts',(-72.3496245524686,4.91467030562071,130.991974181974));
#91324=CARTESIAN_POINT('Ctrl Pts',(-72.3573893054157,4.91988305977349,130.855422391991));
#91325=CARTESIAN_POINT('Ctrl Pts',(-72.3651540583628,4.91940730219587,130.718473903873));
#91326=CARTESIAN_POINT('Ctrl Pts',(-72.3729188113099,4.91320456645233,130.581641173664));
#91327=CARTESIAN_POINT('Ctrl Pts',(-72.3806758521949,4.90700799135338,130.444944347652));
#91328=CARTESIAN_POINT('Ctrl Pts',(-72.3884328930799,4.89509577528495,130.308363438786));
#91329=CARTESIAN_POINT('Ctrl Pts',(-72.3961899339649,4.87748144673841,130.172412993769));
#91330=CARTESIAN_POINT('Ctrl Pts',(-72.403941125205,4.85988040129402,130.03656507004));
#91331=CARTESIAN_POINT('Ctrl Pts',(-72.4116923164452,4.83658585230741,129.901347049987));
#91332=CARTESIAN_POINT('Ctrl Pts',(-72.4194435076854,4.80766328773967,129.767270084285));
#91333=CARTESIAN_POINT('Ctrl Pts',(-72.4271914044625,4.77875301603337,129.633250104871));
#91334=CARTESIAN_POINT('Ctrl Pts',(-72.4349393012395,4.74421956863301,129.500370596598));
#91335=CARTESIAN_POINT('Ctrl Pts',(-72.4426871980166,4.70417980237779,129.369133998038));
#91336=CARTESIAN_POINT('Ctrl Pts',(-72.4504334741007,4.66414841157861,129.237924851346));
#91337=CARTESIAN_POINT('Ctrl Pts',(-72.4581797501848,4.61861310694212,129.108358304516));
#91338=CARTESIAN_POINT('Ctrl Pts',(-72.4659260262689,4.56774092739604,128.980922688079));
#91339=CARTESIAN_POINT('Ctrl Pts',(-72.4736723595343,4.51686837232302,128.853486130941));
#91340=CARTESIAN_POINT('Ctrl Pts',(-72.4814186927997,4.46065900867942,128.728180898687));
#91341=CARTESIAN_POINT('Ctrl Pts',(-72.4891650260651,4.39932829062478,128.60547597898));
#91342=CARTESIAN_POINT('Ctrl Pts',(-72.4969130940681,4.33798383798115,128.482743580358));
#91343=CARTESIAN_POINT('Ctrl Pts',(-72.5046611620709,4.2715159235065,128.362613002684));
#91344=CARTESIAN_POINT('Ctrl Pts',(-72.5124092300739,4.20018609070058,128.24552887906));
#91345=CARTESIAN_POINT('Ctrl Pts',(-72.5201655328157,4.12878044769942,128.128320317036));
#91346=CARTESIAN_POINT('Ctrl Pts',(-72.5279218355576,4.05250276785224,128.014165011349));
#91347=CARTESIAN_POINT('Ctrl Pts',(-72.5356781382995,3.97165840892398,127.903479278158));
#91348=CARTESIAN_POINT('Ctrl Pts',(-72.5434385808136,3.89077090092719,127.792734468659));
#91349=CARTESIAN_POINT('Ctrl Pts',(-72.5511990233279,3.80531210066674,127.685463227196));
#91350=CARTESIAN_POINT('Ctrl Pts',(-72.558959465842,3.71562721162532,127.58204817357));
#91351=CARTESIAN_POINT('Ctrl Pts',(-72.5667323661075,3.62579835243816,127.47846710892));
#91352=CARTESIAN_POINT('Ctrl Pts',(-72.5745052663729,3.53173011613359,127.378754886839));
#91353=CARTESIAN_POINT('Ctrl Pts',(-72.5822781666383,3.43380469196813,127.283257324574));
#91354=CARTESIAN_POINT('Ctrl Pts',(-72.5897685024003,3.3394391036306,127.191231339242));
#91355=CARTESIAN_POINT('Ctrl Pts',(-72.5972588381623,3.24149212461839,127.10311911275));
#91356=CARTESIAN_POINT('Ctrl Pts',(-72.6047491739243,3.1403327192139,127.019193055207));
#91357=CARTESIAN_POINT('Ctrl Pts',(-72.6125235080434,3.03533782420661,126.932084915684));
#91358=CARTESIAN_POINT('Ctrl Pts',(-72.6202978421625,2.92654950353909,126.849210716208));
#91359=CARTESIAN_POINT('Ctrl Pts',(-72.6280721762816,2.81434395291338,126.77091901303));
#91360=CARTESIAN_POINT('Ctrl Pts',(-72.6358369292286,2.70227668560072,126.69272379738));
#91361=CARTESIAN_POINT('Ctrl Pts',(-72.6436016821758,2.58680088537269,126.619100062723));
#91362=CARTESIAN_POINT('Ctrl Pts',(-72.6513664351229,2.46832690396422,126.550357166972));
#91363=CARTESIAN_POINT('Ctrl Pts',(-72.6591234760079,2.34997059258428,126.481682547634));
#91364=CARTESIAN_POINT('Ctrl Pts',(-72.6668805168929,2.22862236202573,126.417879314967));
#91365=CARTESIAN_POINT('Ctrl Pts',(-72.6746375577779,2.10472242748314,126.359214212131));
#91366=CARTESIAN_POINT('Ctrl Pts',(-72.682388749018,1.98091592684482,126.300593349106));
#91367=CARTESIAN_POINT('Ctrl Pts',(-72.6901399402581,1.85456190427208,126.247103070181));
#91368=CARTESIAN_POINT('Ctrl Pts',(-72.6978911314983,1.72612580314898,126.198964567908));
#91369=CARTESIAN_POINT('Ctrl Pts',(-72.7056390282753,1.59774429079517,126.150846525783));
#91370=CARTESIAN_POINT('Ctrl Pts',(-72.7133869250524,1.4672828252962,126.108075873135));
#91371=CARTESIAN_POINT('Ctrl Pts',(-72.7211348218295,1.3352272864277,126.070825875317));
#91372=CARTESIAN_POINT('Ctrl Pts',(-72.7288810979135,1.20319937073114,126.033583669395));
#91373=CARTESIAN_POINT('Ctrl Pts',(-72.7366273739976,1.06957842095028,126.001859927412));
#91374=CARTESIAN_POINT('Ctrl Pts',(-72.7443736500817,0.934865572011036,
125.975778069367));
#91375=CARTESIAN_POINT('Ctrl Pts',(-72.752119983347,0.800151728652323,125.949696018792));
#91376=CARTESIAN_POINT('Ctrl Pts',(-72.7598663166124,0.664346353889069,
125.929256009573));
#91377=CARTESIAN_POINT('Ctrl Pts',(-72.7676126498777,0.527960478561605,
125.914530273313));
#91378=CARTESIAN_POINT('Ctrl Pts',(-72.7753607178807,0.391544060562809,
125.899801239326));
#91379=CARTESIAN_POINT('Ctrl Pts',(-72.7831087858837,0.254547271948345,
125.890789066658));
#91380=CARTESIAN_POINT('Ctrl Pts',(-72.7908568538867,0.117485565789411,
125.887514046406));
#91381=CARTESIAN_POINT('Ctrl Pts',(-72.7986131566285,-0.0197218111816969,
125.884235545423));
#91382=CARTESIAN_POINT('Ctrl Pts',(-72.8063694593703,-0.156993852045623,
125.886706386652));
#91383=CARTESIAN_POINT('Ctrl Pts',(-72.8141257621122,-0.293815244895422,
125.894894693011));
#91384=CARTESIAN_POINT('Ctrl Pts',(-72.8218862046264,-0.430709663442571,
125.903087369715));
#91385=CARTESIAN_POINT('Ctrl Pts',(-72.8296466471405,-0.567152565953215,
125.917003552436));
#91386=CARTESIAN_POINT('Ctrl Pts',(-72.8374070896547,-0.702635452636977,
125.936559627057));
#91387=CARTESIAN_POINT('Ctrl Pts',(-72.8451799899201,-0.83833582847805,
125.956147094825));
#91388=CARTESIAN_POINT('Ctrl Pts',(-72.8529528901856,-0.973072724378941,
125.981392474538));
#91389=CARTESIAN_POINT('Ctrl Pts',(-72.860725790451,-1.10634861186653,126.012161142218));
#91390=CARTESIAN_POINT('Ctrl Pts',(-72.8682161262131,-1.23477958514297,
126.041811291328));
#91391=CARTESIAN_POINT('Ctrl Pts',(-72.8757064619751,-1.36185363140396,
126.076590048094));
#91392=CARTESIAN_POINT('Ctrl Pts',(-72.8831967977372,-1.48714213010228,
126.116334236734));
#91393=CARTESIAN_POINT('Ctrl Pts',(-72.8909711318562,-1.61718098030739,
126.157585338366));
#91394=CARTESIAN_POINT('Ctrl Pts',(-72.8987454659753,-1.74570813606772,
126.204316504457));
#91395=CARTESIAN_POINT('Ctrl Pts',(-72.9065198000943,-1.8722270041725,126.256399634076));
#91396=CARTESIAN_POINT('Ctrl Pts',(-72.9142845530413,-1.99858994907999,
126.308418575892));
#91397=CARTESIAN_POINT('Ctrl Pts',(-72.9220493059884,-2.1229491728547,126.365776210127));
#91398=CARTESIAN_POINT('Ctrl Pts',(-72.9298140589354,-2.24482259878887,
126.428294511751));
#91399=CARTESIAN_POINT('Ctrl Pts',(-72.9375710998203,-2.36657497831796,
126.490750719316));
#91400=CARTESIAN_POINT('Ctrl Pts',(-72.9453281407052,-2.48584612767307,
126.558357216707));
#91401=CARTESIAN_POINT('Ctrl Pts',(-72.9530851815901,-2.60217368121453,
126.630887819608));
#91402=CARTESIAN_POINT('Ctrl Pts',(-72.9608363728302,-2.71841351124344,
126.703363726617));
#91403=CARTESIAN_POINT('Ctrl Pts',(-72.9685875640703,-2.83171383339463,
126.780756142008));
#91404=CARTESIAN_POINT('Ctrl Pts',(-72.9763387553104,-2.94163696859287,
126.862793035054));
#91405=CARTESIAN_POINT('Ctrl Pts',(-72.9840866520875,-3.0515133835262,126.944795060233));
#91406=CARTESIAN_POINT('Ctrl Pts',(-72.9918345488645,-3.15801515372683,
127.03143740353));
#91407=CARTESIAN_POINT('Ctrl Pts',(-72.9995824456416,-3.26073387625993,
127.122404934683));
#91408=CARTESIAN_POINT('Ctrl Pts',(-73.0073287217256,-3.36343111225064,
127.213353437391));
#91409=CARTESIAN_POINT('Ctrl Pts',(-73.0150749978097,-3.46234658207325,
127.308625069345));
#91410=CARTESIAN_POINT('Ctrl Pts',(-73.0228212738938,-3.55710557331878,
127.407864923065));
#91411=CARTESIAN_POINT('Ctrl Pts',(-73.030567607159,-3.65186526405352,127.50710550935));
#91412=CARTESIAN_POINT('Ctrl Pts',(-73.0383139404243,-3.74246814499035,
127.610314093088));
#91413=CARTESIAN_POINT('Ctrl Pts',(-73.0460602736896,-3.82857722098516,
127.717099772504));
#91414=CARTESIAN_POINT('Ctrl Pts',(-73.0538083416925,-3.91470558051061,
127.823909365832));
#91415=CARTESIAN_POINT('Ctrl Pts',(-73.0615564096954,-3.99633788719332,
127.934297344581));
#91416=CARTESIAN_POINT('Ctrl Pts',(-73.0693044776983,-4.07317845458179,
128.047841011318));
#91417=CARTESIAN_POINT('Ctrl Pts',(-73.0770607804401,-4.15010068903981,
128.161505353615));
#91418=CARTESIAN_POINT('Ctrl Pts',(-73.0848170831818,-4.22222079147901,
128.278331759377));
#91419=CARTESIAN_POINT('Ctrl Pts',(-73.0925733859236,-4.28928704231855,
128.397869451761));
#91420=CARTESIAN_POINT('Ctrl Pts',(-73.1003338284377,-4.3563890884355,128.517470945011));
#91421=CARTESIAN_POINT('Ctrl Pts',(-73.1080942709519,-4.41843173139561,
128.639786259838));
#91422=CARTESIAN_POINT('Ctrl Pts',(-73.115854713466,-4.4752104615666,128.764342385494));
#91423=CARTESIAN_POINT('Ctrl Pts',(-73.1236276137314,-4.53208033799584,
128.889098459701));
#91424=CARTESIAN_POINT('Ctrl Pts',(-73.1314005139968,-4.58366926842381,
129.016102170556));
#91425=CARTESIAN_POINT('Ctrl Pts',(-73.1391734142622,-4.62982158952197,
129.144862165715));
#91426=CARTESIAN_POINT('Ctrl Pts',(-73.1466637500247,-4.67429615750091,
129.268941410732));
#91427=CARTESIAN_POINT('Ctrl Pts',(-73.1541540857872,-4.7137224304112,129.394651172334));
#91428=CARTESIAN_POINT('Ctrl Pts',(-73.1616444215497,-4.74800601278444,
129.521542639417));
#91429=CARTESIAN_POINT('Ctrl Pts',(-73.1628415343781,-4.75348524863795,
129.541822558486));
#91430=CARTESIAN_POINT('Ctrl Pts',(-73.1640386472066,-4.75883489886877,
129.562138863632));
#91431=CARTESIAN_POINT('Ctrl Pts',(-73.1652357600351,-4.76405452823407,
129.582490119308));
#91432=CARTESIAN_POINT('Ctrl Pts',(-71.4150282010451,-4.76405452823412,
129.582490119309));
#91433=CARTESIAN_POINT('Ctrl Pts',(-71.4227606235564,-4.79801320159563,
129.71489447135));
#91434=CARTESIAN_POINT('Ctrl Pts',(-71.4304930460676,-4.826421244122,129.848611458346));
#91435=CARTESIAN_POINT('Ctrl Pts',(-71.4382254685788,-4.84920307574022,
129.983134343795));
#91436=CARTESIAN_POINT('Ctrl Pts',(-71.4460446511415,-4.8722405261997,130.119166615525));
#91437=CARTESIAN_POINT('Ctrl Pts',(-71.4538638337041,-4.88952469595008,
130.256022567493));
#91438=CARTESIAN_POINT('Ctrl Pts',(-71.4616830162667,-4.90103150184777,
130.393175403343));
#91439=CARTESIAN_POINT('Ctrl Pts',(-71.4695021988293,-4.91253830774546,
130.530328239193));
#91440=CARTESIAN_POINT('Ctrl Pts',(-71.4773213813919,-4.9182677949696,130.667777546891));
#91441=CARTESIAN_POINT('Ctrl Pts',(-71.4851405639546,-4.91824995845192,
130.804999904443));
#91442=CARTESIAN_POINT('',(-71.1398594360428,-4.9182484759593,130.808232467773));
#91443=CARTESIAN_POINT('Ctrl Pts',(-71.0699658330086,-4.76405452823398,
129.582490119308));
#91444=CARTESIAN_POINT('Ctrl Pts',(-71.0777030597182,-4.79811556922247,
129.715293601174));
#91445=CARTESIAN_POINT('Ctrl Pts',(-71.0854402864279,-4.82662987703852,
129.849563530845));
#91446=CARTESIAN_POINT('Ctrl Pts',(-71.0931775131375,-4.84948433727197,
129.984796876876));
#91447=CARTESIAN_POINT('Ctrl Pts',(-71.1009578336131,-4.8724660892081,130.120783427432));
#91448=CARTESIAN_POINT('Ctrl Pts',(-71.1087381540886,-4.88972465357151,
130.257743771572));
#91449=CARTESIAN_POINT('Ctrl Pts',(-71.1165184745642,-4.9011973749989,130.395157301592));
#91450=CARTESIAN_POINT('Ctrl Pts',(-71.1242987950398,-4.9126700964263,130.532570831613));
#91451=CARTESIAN_POINT('Ctrl Pts',(-71.1320791155154,-4.91835695415469,
130.670437145927));
#91452=CARTESIAN_POINT('Ctrl Pts',(-71.139859435991,-4.91824847596002,130.808232466857));
#91453=CARTESIAN_POINT('Ctrl Pts',(-71.1398594360427,-4.9182484759593,130.808232467773));
#91454=CARTESIAN_POINT('Ctrl Pts',(-71.1489049275806,-4.91812235791222,
130.96843491873));
#91455=CARTESIAN_POINT('Ctrl Pts',(-71.1579504191185,-4.91016493917958,
131.12830970416));
#91456=CARTESIAN_POINT('Ctrl Pts',(-71.1669959106564,-4.89449543925293,
131.287162292824));
#91457=CARTESIAN_POINT('Ctrl Pts',(-71.176096553043,-4.8787304015419,131.446983414271));
#91458=CARTESIAN_POINT('Ctrl Pts',(-71.1851971954297,-4.85515906191396,
131.605769743764));
#91459=CARTESIAN_POINT('Ctrl Pts',(-71.1942978378163,-4.82395190626533,
131.762833918466));
#91460=CARTESIAN_POINT('Ctrl Pts',(-71.2034625668571,-4.79252499006506,
131.921004137887));
#91461=CARTESIAN_POINT('Ctrl Pts',(-71.2126272958978,-4.75335441236356,
132.077427772717));
#91462=CARTESIAN_POINT('Ctrl Pts',(-71.2217920249387,-4.70666251969357,
132.231424382158));
#91463=CARTESIAN_POINT('Ctrl Pts',(-71.2252280336323,-4.68915695587144,
132.289160261361));
#91464=CARTESIAN_POINT('Ctrl Pts',(-71.228664042326,-4.67059465505894,132.346555214575));
#91465=CARTESIAN_POINT('Ctrl Pts',(-71.2321000510196,-4.65098903443619,
132.403574194314));
#91466=CARTESIAN_POINT('Ctrl Pts',(-71.2398743851383,-4.60662923825511,
132.532585683841));
#91467=CARTESIAN_POINT('Ctrl Pts',(-71.2476487192571,-4.5568272322371,132.659954407817));
#91468=CARTESIAN_POINT('Ctrl Pts',(-71.2554230533758,-4.50172299729148,
132.785186990108));
#91469=CARTESIAN_POINT('Ctrl Pts',(-71.2631878063226,-4.44668667339078,
132.910265234433));
#91470=CARTESIAN_POINT('Ctrl Pts',(-71.2709525592692,-4.38636127826588,
133.03321222075));
#91471=CARTESIAN_POINT('Ctrl Pts',(-71.278717312216,-4.32093635419087,133.153550283287));
#91472=CARTESIAN_POINT('Ctrl Pts',(-71.2864743531007,-4.25557641107269,
133.273768824365));
#91473=CARTESIAN_POINT('Ctrl Pts',(-71.2942313939854,-4.18512720396693,
133.391383257047));
#91474=CARTESIAN_POINT('Ctrl Pts',(-71.3019884348701,-4.1098259475563,133.505936776643));
#91475=CARTESIAN_POINT('Ctrl Pts',(-71.3097396261099,-4.03458147640898,
133.620403910539));
#91476=CARTESIAN_POINT('Ctrl Pts',(-71.3174908173498,-3.95449245279771,
133.731814400418));
#91477=CARTESIAN_POINT('Ctrl Pts',(-71.3252420085896,-3.86984133219999,
133.839737221234));
#91478=CARTESIAN_POINT('Ctrl Pts',(-71.3329899053664,-3.78522619058667,
133.947614171972));
#91479=CARTESIAN_POINT('Ctrl Pts',(-71.3407378021431,-3.69605304932102,
134.052006094952));
#91480=CARTESIAN_POINT('Ctrl Pts',(-71.3484856989199,-3.60264674845865,
134.152512267106));
#91481=CARTESIAN_POINT('Ctrl Pts',(-71.3562319750037,-3.50925998618094,
134.252997415536));
#91482=CARTESIAN_POINT('Ctrl Pts',(-71.3639782510876,-3.41164209157134,
134.349598143671));
#91483=CARTESIAN_POINT('Ctrl Pts',(-71.3717245271714,-3.31015686197168,
134.441948363812));
#91484=CARTESIAN_POINT('Ctrl Pts',(-71.3794708604364,-3.20867088323112,
134.534299265662));
#91485=CARTESIAN_POINT('Ctrl Pts',(-71.3872171937014,-3.1033178016973,134.622399333774));
#91486=CARTESIAN_POINT('Ctrl Pts',(-71.3949635269665,-2.99449649352841,
134.705921050617));
#91487=CARTESIAN_POINT('Ctrl Pts',(-71.4027115949692,-2.88565081558206,
134.789461471568));
#91488=CARTESIAN_POINT('Ctrl Pts',(-71.4104596629718,-2.77333567557318,
134.868421263047));
#91489=CARTESIAN_POINT('Ctrl Pts',(-71.4182077309745,-2.65798074486767,
134.942514967323));
#91490=CARTESIAN_POINT('Ctrl Pts',(-71.4259640337161,-2.54250321356905,
135.01668741927));
#91491=CARTESIAN_POINT('Ctrl Pts',(-71.4337203364577,-2.42397976732895,
135.08598324129));
#91492=CARTESIAN_POINT('Ctrl Pts',(-71.4414766391992,-2.30286709375386,
135.150161603691));
#91493=CARTESIAN_POINT('Ctrl Pts',(-71.4492370817131,-2.18168977869824,
135.214374220017));
#91494=CARTESIAN_POINT('Ctrl Pts',(-71.456997524227,-2.05792083530419,135.273463765935));
#91495=CARTESIAN_POINT('Ctrl Pts',(-71.4647579667409,-1.93203804577157,
135.327237141659));
#91496=CARTESIAN_POINT('Ctrl Pts',(-71.472530867006,-1.80595317800983,135.38109683918));
#91497=CARTESIAN_POINT('Ctrl Pts',(-71.4803037672712,-1.67774804900742,
135.4296231744));
#91498=CARTESIAN_POINT('Ctrl Pts',(-71.4880766675364,-1.54791760510034,
135.472672319918));
#91499=CARTESIAN_POINT('Ctrl Pts',(-71.4955670033018,-1.42280682479164,
135.514156520584));
#91500=CARTESIAN_POINT('Ctrl Pts',(-71.5030573390671,-1.29618714260848,
135.550554752058));
#91501=CARTESIAN_POINT('Ctrl Pts',(-71.5105476748325,-1.16850950563759,
135.581783416287));
#91502=CARTESIAN_POINT('Ctrl Pts',(-71.5183220089516,-1.03599093231318,
135.614196124796));
#91503=CARTESIAN_POINT('Ctrl Pts',(-71.5260963430708,-0.901912816821885,
135.641142193132));
#91504=CARTESIAN_POINT('Ctrl Pts',(-71.5338706771899,-0.766765913580014,
135.662472709343));
#91505=CARTESIAN_POINT('Ctrl Pts',(-71.541635430137,-0.631785566817964,
135.6837769376));
#91506=CARTESIAN_POINT('Ctrl Pts',(-71.549400183084,-0.495739435588995,
135.699479323429));
#91507=CARTESIAN_POINT('Ctrl Pts',(-71.5571649360311,-0.359131845864075,
135.709481144096));
#91508=CARTESIAN_POINT('Ctrl Pts',(-71.5649219769161,-0.222659936723285,
135.719473030814));
#91509=CARTESIAN_POINT('Ctrl Pts',(-71.5726790178012,-0.0856280662305558,
135.723775591406));
#91510=CARTESIAN_POINT('Ctrl Pts',(-71.5804360586862,0.051451222560865,
135.722341487211));
#91511=CARTESIAN_POINT('Ctrl Pts',(-71.5881872499263,0.188427138794287,
135.720908464485));
#91512=CARTESIAN_POINT('Ctrl Pts',(-71.5959384411664,0.3254500127893,135.713747391813));
#91513=CARTESIAN_POINT('Ctrl Pts',(-71.6036896324065,0.462004536881481,
135.70086292742));
#91514=CARTESIAN_POINT('Ctrl Pts',(-71.6114375291836,0.598501021658397,
135.687983939267));
#91515=CARTESIAN_POINT('Ctrl Pts',(-71.6191854259607,0.734529164028518,
135.669386434288));
#91516=CARTESIAN_POINT('Ctrl Pts',(-71.6269333227378,0.869576240341327,
135.645127109015));
#91517=CARTESIAN_POINT('Ctrl Pts',(-71.6346795988218,1.00459506771705,135.620872858269));
#91518=CARTESIAN_POINT('Ctrl Pts',(-71.642425874906,1.13863285266302,135.590959212009));
#91519=CARTESIAN_POINT('Ctrl Pts',(-71.6501721509901,1.27118495387946,135.555494363898));
#91520=CARTESIAN_POINT('Ctrl Pts',(-71.6579184842554,1.40373803356522,135.520029253993));
#91521=CARTESIAN_POINT('Ctrl Pts',(-71.6656648175208,1.53480502995698,135.479012961518));
#91522=CARTESIAN_POINT('Ctrl Pts',(-71.6734111507861,1.66389479097174,135.432604041056));
#91523=CARTESIAN_POINT('Ctrl Pts',(-71.6811592187891,1.79301346074362,135.386184727638));
#91524=CARTESIAN_POINT('Ctrl Pts',(-71.688907286792,1.92015364619997,135.334370515407));
#91525=CARTESIAN_POINT('Ctrl Pts',(-71.696655354795,2.04484293580088,135.277368602178));
#91526=CARTESIAN_POINT('Ctrl Pts',(-71.7044116575368,2.16966474666243,135.220306106638));
#91527=CARTESIAN_POINT('Ctrl Pts',(-71.7121679602786,2.29203010207884,135.158045058998));
#91528=CARTESIAN_POINT('Ctrl Pts',(-71.7199242630204,2.41148953440427,135.090839509146));
#91529=CARTESIAN_POINT('Ctrl Pts',(-71.7276847055346,2.53101272582576,135.023598089668));
#91530=CARTESIAN_POINT('Ctrl Pts',(-71.7354451480488,2.6476265714404,134.951407115176));
#91531=CARTESIAN_POINT('Ctrl Pts',(-71.743205590563,2.76091035798079,134.874564182217));
#91532=CARTESIAN_POINT('Ctrl Pts',(-71.7509784908284,2.87437599771219,134.797597894159));
#91533=CARTESIAN_POINT('Ctrl Pts',(-71.7587513910938,2.98450058168153,134.715964957672));
#91534=CARTESIAN_POINT('Ctrl Pts',(-71.7665242913592,3.09089557323945,134.630004042904));
#91535=CARTESIAN_POINT('Ctrl Pts',(-71.7740146271212,3.19342283886114,134.547168023909));
#91536=CARTESIAN_POINT('Ctrl Pts',(-71.7815049628832,3.29248673288394,134.460313432458));
#91537=CARTESIAN_POINT('Ctrl Pts',(-71.7889952986452,3.38777317398078,134.369774476315));
#91538=CARTESIAN_POINT('Ctrl Pts',(-71.7967696327644,3.48667242945431,134.275802708129));
#91539=CARTESIAN_POINT('Ctrl Pts',(-71.8045439668835,3.58181541636068,134.177564000405));
#91540=CARTESIAN_POINT('Ctrl Pts',(-71.8123183010026,3.67281158611053,134.075390748187));
#91541=CARTESIAN_POINT('Ctrl Pts',(-71.8200830539498,3.76369561121373,133.973343415371));
#91542=CARTESIAN_POINT('Ctrl Pts',(-71.8278478068969,3.85044273016745,133.867371475233));
#91543=CARTESIAN_POINT('Ctrl Pts',(-71.8356125598441,3.93269728423352,133.757845869448));
#91544=CARTESIAN_POINT('Ctrl Pts',(-71.8433696007291,4.0148701419168,133.648429046038));
#91545=CARTESIAN_POINT('Ctrl Pts',(-71.8511266416141,4.09255908118916,133.535465891543));
#91546=CARTESIAN_POINT('Ctrl Pts',(-71.8588836824992,4.1654472326537,133.419362035248));
#91547=CARTESIAN_POINT('Ctrl Pts',(-71.8666348737393,4.23828041859632,133.303345733773));
#91548=CARTESIAN_POINT('Ctrl Pts',(-71.8743860649795,4.3063198157089,133.184193774492));
#91549=CARTESIAN_POINT('Ctrl Pts',(-71.8821372562197,4.36929080670958,133.062342218222));
#91550=CARTESIAN_POINT('Ctrl Pts',(-71.8898851529968,4.43223503335927,132.940542452115));
#91551=CARTESIAN_POINT('Ctrl Pts',(-71.8976330497739,4.49011495933476,132.81604571771));
#91552=CARTESIAN_POINT('Ctrl Pts',(-71.905380946551,4.54270114537755,132.689314029798));
#91553=CARTESIAN_POINT('Ctrl Pts',(-71.9131272226352,4.59527633152385,132.562608851423));
#91554=CARTESIAN_POINT('Ctrl Pts',(-71.9208734987194,4.64255983054481,132.433670010315));
#91555=CARTESIAN_POINT('Ctrl Pts',(-71.9286197748035,4.68436989788417,132.302980556809));
#91556=CARTESIAN_POINT('Ctrl Pts',(-71.9363661080689,4.72618027385595,132.172290138583));
#91557=CARTESIAN_POINT('Ctrl Pts',(-71.9441124413343,4.7625170183942,132.039849454546));
#91558=CARTESIAN_POINT('Ctrl Pts',(-71.9518587745997,4.79324804826132,131.906157427481));
#91559=CARTESIAN_POINT('Ctrl Pts',(-71.9596068426028,4.82398596012951,131.772435461013));
#91560=CARTESIAN_POINT('Ctrl Pts',(-71.9673549106058,4.84911557173555,131.637461974848));
#91561=CARTESIAN_POINT('Ctrl Pts',(-71.9751029786089,4.86855585449216,131.501746417672));
#91562=CARTESIAN_POINT('Ctrl Pts',(-71.9828592813508,4.88801679861261,131.365886620388));
#91563=CARTESIAN_POINT('Ctrl Pts',(-71.9906155840927,4.90177627945069,131.229283564248));
#91564=CARTESIAN_POINT('Ctrl Pts',(-71.9983718868346,4.90980508813009,131.092452719283));
#91565=CARTESIAN_POINT('Ctrl Pts',(-72.0061323293488,4.91783818202642,130.955548843576));
#91566=CARTESIAN_POINT('Ctrl Pts',(-72.0138927718629,4.92013450263755,130.818417327509));
#91567=CARTESIAN_POINT('Ctrl Pts',(-72.0216532143772,4.91671702056835,130.681572987271));
#91568=CARTESIAN_POINT('Ctrl Pts',(-72.0294261146426,4.91329405245355,130.544508972349));
#91569=CARTESIAN_POINT('Ctrl Pts',(-72.0371990149082,4.90413897859954,130.407733444799));
#91570=CARTESIAN_POINT('Ctrl Pts',(-72.0449719151737,4.88932671824339,130.271756350993));
#91571=CARTESIAN_POINT('Ctrl Pts',(-72.0524622509352,4.87505292086205,130.140722367063));
#91572=CARTESIAN_POINT('Ctrl Pts',(-72.0599525866967,4.85552614771494,130.010430079174));
#91573=CARTESIAN_POINT('Ctrl Pts',(-72.0674429224582,4.83085780862984,129.881324380303));
#91574=CARTESIAN_POINT('Ctrl Pts',(-72.0752172565773,4.80525416196891,129.74732359961));
#91575=CARTESIAN_POINT('Ctrl Pts',(-72.0829915906964,4.77403026331621,129.614176688999));
#91576=CARTESIAN_POINT('Ctrl Pts',(-72.0907659248155,4.73725466498359,129.4823918957));
#91577=CARTESIAN_POINT('Ctrl Pts',(-72.0985306777626,4.70052438928919,129.350769515381));
#91578=CARTESIAN_POINT('Ctrl Pts',(-72.1062954307096,4.65825613148131,129.220506285248));
#91579=CARTESIAN_POINT('Ctrl Pts',(-72.1140601836566,4.61056973306006,129.092101934104));
#91580=CARTESIAN_POINT('Ctrl Pts',(-72.1218172245416,4.56293069744198,128.963825115972));
#91581=CARTESIAN_POINT('Ctrl Pts',(-72.1295742654266,4.5098843656183,128.837403866816));
#91582=CARTESIAN_POINT('Ctrl Pts',(-72.1373313063116,4.45160072934423,128.713324030368));
#91583=CARTESIAN_POINT('Ctrl Pts',(-72.1450824975517,4.39336104521358,128.589337763489));
#91584=CARTESIAN_POINT('Ctrl Pts',(-72.1528336887919,4.32989208340656,128.467689747284));
#91585=CARTESIAN_POINT('Ctrl Pts',(-72.160584880032,4.26141227689011,128.348846726571));
#91586=CARTESIAN_POINT('Ctrl Pts',(-72.168332776809,4.19296157611827,128.230054217312));
#91587=CARTESIAN_POINT('Ctrl Pts',(-72.176080673586,4.11950446131969,128.114064670398));
#91588=CARTESIAN_POINT('Ctrl Pts',(-72.1838285703631,4.04130562109771,128.001320849852));
#91589=CARTESIAN_POINT('Ctrl Pts',(-72.1915748464472,3.96312313838734,127.888600612884));
#91590=CARTESIAN_POINT('Ctrl Pts',(-72.1993211225312,3.88020112581105,127.779125072895));
#91591=CARTESIAN_POINT('Ctrl Pts',(-72.2070673986153,3.79284774992457,127.673308237232));
#91592=CARTESIAN_POINT('Ctrl Pts',(-72.2148137318806,3.70549372921544,127.567490620455));
#91593=CARTESIAN_POINT('Ctrl Pts',(-72.2225600651459,3.61370852881903,127.4653320634));
#91594=CARTESIAN_POINT('Ctrl Pts',(-72.2303063984112,3.51784051238584,127.367213371387));
#91595=CARTESIAN_POINT('Ctrl Pts',(-72.2380544664141,3.42195102697495,127.269072706373));
#91596=CARTESIAN_POINT('Ctrl Pts',(-72.2458025344171,3.3219771793156,127.174973986238));
#91597=CARTESIAN_POINT('Ctrl Pts',(-72.25355060242,3.21830378508636,127.085260752088));
#91598=CARTESIAN_POINT('Ctrl Pts',(-72.2613069051618,3.11452020554015,126.995452169645));
#91599=CARTESIAN_POINT('Ctrl Pts',(-72.2690632079037,3.00702952109897,126.910038640168));
#91600=CARTESIAN_POINT('Ctrl Pts',(-72.2768195106455,2.89624962318642,126.829323362056));
#91601=CARTESIAN_POINT('Ctrl Pts',(-72.2845799531597,2.78541059870654,126.748565003769));
#91602=CARTESIAN_POINT('Ctrl Pts',(-72.2923403956737,2.67127918785532,126.672510110146));
#91603=CARTESIAN_POINT('Ctrl Pts',(-72.3001008381879,2.5543009362462,126.601417626091));
#91604=CARTESIAN_POINT('Ctrl Pts',(-72.3078737384533,2.43713490076275,126.530211018069));
#91605=CARTESIAN_POINT('Ctrl Pts',(-72.3156466387187,2.31711323470843,126.463982927418));
#91606=CARTESIAN_POINT('Ctrl Pts',(-72.3234195389842,2.19470546608784,126.402945960933));
#91607=CARTESIAN_POINT('Ctrl Pts',(-72.3309098747465,2.07674752817853,126.34412784192));
#91608=CARTESIAN_POINT('Ctrl Pts',(-72.3384002105088,1.95657423844223,126.29013010502));
#91609=CARTESIAN_POINT('Ctrl Pts',(-72.3458905462711,1.83462011767261,126.241099493509));
#91610=CARTESIAN_POINT('Ctrl Pts',(-72.3536648803902,1.70804206935098,126.190209871462));
#91611=CARTESIAN_POINT('Ctrl Pts',(-72.3614392145093,1.57914452262869,126.144510264225));
#91612=CARTESIAN_POINT('Ctrl Pts',(-72.3692135486284,1.44839213449318,126.104217716841));
#91613=CARTESIAN_POINT('Ctrl Pts',(-72.3769783015756,1.31780088699037,126.06397482642));
#91614=CARTESIAN_POINT('Ctrl Pts',(-72.3847430545227,1.18535971642677,126.029125851069));
#91615=CARTESIAN_POINT('Ctrl Pts',(-72.3925078074698,1.05155383605675,125.999840080366));
#91616=CARTESIAN_POINT('Ctrl Pts',(-72.4002648483548,0.917880853573456,
125.970583396704));
#91617=CARTESIAN_POINT('Ctrl Pts',(-72.4080218892398,0.782846238141581,
125.946879004837));
#91618=CARTESIAN_POINT('Ctrl Pts',(-72.4157789301248,0.646950628550035,
125.928846496294));
#91619=CARTESIAN_POINT('Ctrl Pts',(-72.423530121365,0.51115749889498,125.910827586207));
#91620=CARTESIAN_POINT('Ctrl Pts',(-72.4312813126053,0.374505053437303,
125.898472097132));
#91621=CARTESIAN_POINT('Ctrl Pts',(-72.4390325038454,0.237504046167165,
125.891848542206));
#91622=CARTESIAN_POINT('Ctrl Pts',(-72.4467804006225,0.100561267979552,
125.885227802468));
#91623=CARTESIAN_POINT('Ctrl Pts',(-72.4545282973996,-0.0367293876737959,
125.884334170252));
#91624=CARTESIAN_POINT('Ctrl Pts',(-72.4622761941767,-0.173852340223402,
125.889184280312));
#91625=CARTESIAN_POINT('Ctrl Pts',(-72.4700224702608,-0.31094660960699,
125.894033375834));
#91626=CARTESIAN_POINT('Ctrl Pts',(-72.4777687463449,-0.447872855189297,
125.904623810035));
#91627=CARTESIAN_POINT('Ctrl Pts',(-72.485515022429,-0.584116189312538,
125.92092009475));
#91628=CARTESIAN_POINT('Ctrl Pts',(-72.4932613556944,-0.720360529153307,
125.93721649976));
#91629=CARTESIAN_POINT('Ctrl Pts',(-72.5010076889599,-0.85592155927776,
125.959218792897));
#91630=CARTESIAN_POINT('Ctrl Pts',(-72.5087540222252,-0.990290598323581,
125.986839720531));
#91631=CARTESIAN_POINT('Ctrl Pts',(-72.5165020902283,-1.12468972838423,
126.01446683368));
#91632=CARTESIAN_POINT('Ctrl Pts',(-72.5242501582312,-1.25789595330558,
126.047715006402));
#91633=CARTESIAN_POINT('Ctrl Pts',(-72.5319982262342,-1.3894122399525,126.086446174725));
#91634=CARTESIAN_POINT('Ctrl Pts',(-72.5397545289761,-1.52106830367375,
126.125218506995));
#91635=CARTESIAN_POINT('Ctrl Pts',(-72.547510831718,-1.65103046560631,126.169485365087));
#91636=CARTESIAN_POINT('Ctrl Pts',(-72.5552671344599,-1.7788177558298,126.219059051252));
#91637=CARTESIAN_POINT('Ctrl Pts',(-72.5630275769741,-1.90667324997769,
126.268659196385));
#91638=CARTESIAN_POINT('Ctrl Pts',(-72.5707880194884,-2.03235120134987,
126.323571656958));
#91639=CARTESIAN_POINT('Ctrl Pts',(-72.5785484620026,-2.15539292397695,
126.383561548872));
#91640=CARTESIAN_POINT('Ctrl Pts',(-72.5863213622681,-2.27863216410032,
126.443647741886));
#91641=CARTESIAN_POINT('Ctrl Pts',(-72.5940942625335,-2.39922637463695,
126.508827468021));
#91642=CARTESIAN_POINT('Ctrl Pts',(-72.601867162799,-2.5167428921132,126.578820619235));
#91643=CARTESIAN_POINT('Ctrl Pts',(-72.6093574985607,-2.62998738816753,
126.646269343097));
#91644=CARTESIAN_POINT('Ctrl Pts',(-72.6168478343224,-2.74037381200635,
126.718187439468));
#91645=CARTESIAN_POINT('Ctrl Pts',(-72.6243381700841,-2.8475438352521,126.794288652025));
#91646=CARTESIAN_POINT('Ctrl Pts',(-72.6320580407129,-2.95799799125557,
126.872721920482));
#91647=CARTESIAN_POINT('Ctrl Pts',(-72.6397779113418,-3.06539650939066,
126.955855338688));
#91648=CARTESIAN_POINT('Ctrl Pts',(-72.6474977819705,-3.16930886403994,
127.043421321749));
#91649=CARTESIAN_POINT('Ctrl Pts',(-72.6552054645287,-3.27305716268682,
127.130849056331));
#91650=CARTESIAN_POINT('Ctrl Pts',(-72.6629131470869,-3.37332995652509,
127.222695167493));
#91651=CARTESIAN_POINT('Ctrl Pts',(-72.6706208296451,-3.46972591784802,
127.318649052116));
#91652=CARTESIAN_POINT('Ctrl Pts',(-72.6783214714962,-3.56603382472385,
127.414515286113));
#91653=CARTESIAN_POINT('Ctrl Pts',(-72.6860221133473,-3.65847166227832,
127.514481553219));
#91654=CARTESIAN_POINT('Ctrl Pts',(-72.6937227551985,-3.74667126376606,
127.6181971717));
#91655=CARTESIAN_POINT('Ctrl Pts',(-72.7014180916617,-3.83481009978596,
127.721841334892));
#91656=CARTESIAN_POINT('Ctrl Pts',(-72.7091134281248,-3.9187162518825,127.829229409806));
#91657=CARTESIAN_POINT('Ctrl Pts',(-72.716808764588,-3.99805886377508,127.939974403333));
#91658=CARTESIAN_POINT('Ctrl Pts',(-72.7245005266803,-4.07736462218924,
128.050667957435));
#91659=CARTESIAN_POINT('Ctrl Pts',(-72.7321922887727,-4.15211082771811,
128.164715005133));
#91660=CARTESIAN_POINT('Ctrl Pts',(-72.7398840508651,-4.22200764339674,
128.281696446179));
#91661=CARTESIAN_POINT('Ctrl Pts',(-72.7475753563879,-4.29190031012319,
128.398670943412));
#91662=CARTESIAN_POINT('Ctrl Pts',(-72.7552666619107,-4.35694394839456,
128.518579151306));
#91663=CARTESIAN_POINT('Ctrl Pts',(-72.7629579674336,-4.41689283330309,
128.640974206955));
#91664=CARTESIAN_POINT('Ctrl Pts',(-72.7706489725695,-4.47683937688444,
128.763364482417));
#91665=CARTESIAN_POINT('Ctrl Pts',(-72.7783399777055,-4.53169139357884,
128.888241053135));
#91666=CARTESIAN_POINT('Ctrl Pts',(-72.7860309828414,-4.58125014194578,
129.015134472155));
#91667=CARTESIAN_POINT('Ctrl Pts',(-72.7937256911257,-4.63083275239513,
129.142088989191));
#91668=CARTESIAN_POINT('Ctrl Pts',(-72.80142039941,-4.67511686576179,129.271061921659));
#91669=CARTESIAN_POINT('Ctrl Pts',(-72.8091151076943,-4.71395272631355,
129.401565993759));
#91670=CARTESIAN_POINT('Ctrl Pts',(-72.8126528337234,-4.73180793662982,
129.461566663794));
#91671=CARTESIAN_POINT('Ctrl Pts',(-72.8161905597525,-4.74851219113345,
129.521890782841));
#91672=CARTESIAN_POINT('Ctrl Pts',(-72.8197282857817,-4.76405452823409,
129.582490119308));
#91673=CARTESIAN_POINT('Origin',(213.235140564004,0.,130.804360617566));
#91674=CARTESIAN_POINT('',(-74.915389332428,-4.7640545282341,129.582490119308));
#91675=CARTESIAN_POINT('',(-74.5699110322191,-4.76405452823404,129.582490119308));
#91676=CARTESIAN_POINT('',(213.235140564004,-4.76405452823405,129.582490119308));
#91677=CARTESIAN_POINT('',(-73.235140563966,-4.9182479362882,130.799855099079));
#91678=CARTESIAN_POINT('Ctrl Pts',(-73.2351405640085,-4.91824793628889,
130.79985509983));
#91679=CARTESIAN_POINT('Ctrl Pts',(-73.2428140903957,-4.91837216652081,
130.935465504126));
#91680=CARTESIAN_POINT('Ctrl Pts',(-73.2504876167828,-4.91288341773544,
131.071208978493));
#91681=CARTESIAN_POINT('Ctrl Pts',(-73.25816114317,-4.90177552888557,131.206579124001));
#91682=CARTESIAN_POINT('Ctrl Pts',(-73.2658307249217,-4.89067335013165,
131.341879681441));
#91683=CARTESIAN_POINT('Ctrl Pts',(-73.2735003066735,-4.87395780832335,
131.476806894329));
#91684=CARTESIAN_POINT('Ctrl Pts',(-73.2811698884252,-4.85167481683329,
131.610855834046));
#91685=CARTESIAN_POINT('Ctrl Pts',(-73.2888374871321,-4.82939758682722,
131.744870114107));
#91686=CARTESIAN_POINT('Ctrl Pts',(-73.296505085839,-4.80155583470916,131.878006178507));
#91687=CARTESIAN_POINT('Ctrl Pts',(-73.3041726845459,-4.76824711562812,
132.009766153809));
#91688=CARTESIAN_POINT('Ctrl Pts',(-73.3118400436167,-4.73493943754669,
132.141522011207));
#91689=CARTESIAN_POINT('Ctrl Pts',(-73.3195074026876,-4.69616523023003,
132.271901477481));
#91690=CARTESIAN_POINT('Ctrl Pts',(-73.3271747617585,-4.65207263555085,
132.400419280667));
#91691=CARTESIAN_POINT('Ctrl Pts',(-73.3348436241561,-4.60797139570735,
132.528962282132));
#91692=CARTESIAN_POINT('Ctrl Pts',(-73.3425124865538,-4.55854982451355,
132.655642516577));
#91693=CARTESIAN_POINT('Ctrl Pts',(-73.3501813489515,-4.50400498499601,
132.779992708222));
#91694=CARTESIAN_POINT('Ctrl Pts',(-73.3578581717088,-4.44940352736258,
132.904471976671));
#91695=CARTESIAN_POINT('Ctrl Pts',(-73.365534994466,-4.38966834096258,133.026616005201));
#91696=CARTESIAN_POINT('Ctrl Pts',(-73.3732118172233,-4.32504361823655,
133.14597987843));
#91697=CARTESIAN_POINT('Ctrl Pts',(-73.3808926932371,-4.26038477454887,
133.265406774138));
#91698=CARTESIAN_POINT('Ctrl Pts',(-73.3885735692509,-4.19083145789736,
133.382050248324));
#91699=CARTESIAN_POINT('Ctrl Pts',(-73.3962544452647,-4.11667170824701,
133.495493670579));
#91700=CARTESIAN_POINT('Ctrl Pts',(-73.4039475323815,-4.04239405897969,
133.60911744587));
#91701=CARTESIAN_POINT('Ctrl Pts',(-73.4116406194982,-3.9634955791439,133.719530680906));
#91702=CARTESIAN_POINT('Ctrl Pts',(-73.4193337066149,-3.880305609263,133.82634861245));
#91703=CARTESIAN_POINT('Ctrl Pts',(-73.4262531528642,-3.80548148257161,
133.922424599185));
#91704=CARTESIAN_POINT('Ctrl Pts',(-73.4331725991135,-3.72718626888421,
134.015592341138));
#91705=CARTESIAN_POINT('Ctrl Pts',(-73.4400920453628,-3.64568432271109,
134.105598094882));
#91706=CARTESIAN_POINT('Ctrl Pts',(-73.447866379482,-3.55411292550965,134.206723933142));
#91707=CARTESIAN_POINT('Ctrl Pts',(-73.4556407136011,-3.4581856774549,134.30419697933));
#91708=CARTESIAN_POINT('Ctrl Pts',(-73.4634150477202,-3.35822550577957,
134.397618820761));
#91709=CARTESIAN_POINT('Ctrl Pts',(-73.4711798006673,-3.25838852608214,
134.490925528123));
#91710=CARTESIAN_POINT('Ctrl Pts',(-73.4789445536145,-3.15452879491227,
134.580190700416));
#91711=CARTESIAN_POINT('Ctrl Pts',(-73.4867093065616,-3.0470086122924,134.665049879747));
#91712=CARTESIAN_POINT('Ctrl Pts',(-73.4944663474467,-2.93959522023339,
134.749824775744));
#91713=CARTESIAN_POINT('Ctrl Pts',(-73.5022233883317,-2.82852891666714,
134.830202146756));
#91714=CARTESIAN_POINT('Ctrl Pts',(-73.5099804292167,-2.71420761007415,
134.905855480651));
#91715=CARTESIAN_POINT('Ctrl Pts',(-73.5177316204569,-2.59997251406759,
134.98145176378));
#91716=CARTESIAN_POINT('Ctrl Pts',(-73.5254828116971,-2.48248762553258,
135.052330885712));
#91717=CARTESIAN_POINT('Ctrl Pts',(-73.5332340029373,-2.36218228965434,
135.118207843992));
#91718=CARTESIAN_POINT('Ctrl Pts',(-73.5409818997144,-2.24192808675326,
135.184056802808));
#91719=CARTESIAN_POINT('Ctrl Pts',(-73.5487297964914,-2.1188561629635,135.244907639145));
#91720=CARTESIAN_POINT('Ctrl Pts',(-73.5564776932685,-1.99342289411566,
135.300519892738));
#91721=CARTESIAN_POINT('Ctrl Pts',(-73.5642239693527,-1.86801586320364,
135.356120513446));
#91722=CARTESIAN_POINT('Ctrl Pts',(-73.5719702454369,-1.74024882689782,
135.406484572651));
#91723=CARTESIAN_POINT('Ctrl Pts',(-73.579716521521,-1.6106003350587,135.451418786258));
#91724=CARTESIAN_POINT('Ctrl Pts',(-73.5874628547864,-1.48095088618404,
135.496353331559));
#91725=CARTESIAN_POINT('Ctrl Pts',(-73.5952091880518,-1.34942032347004,
135.535857823251));
#91726=CARTESIAN_POINT('Ctrl Pts',(-73.6029555213172,-1.2165042563878,135.569788243361));
#91727=CARTESIAN_POINT('Ctrl Pts',(-73.6107035893202,-1.08355842367373,
135.603726261954));
#91728=CARTESIAN_POINT('Ctrl Pts',(-73.6184516573232,-0.949226847926304,
135.632087628358));
#91729=CARTESIAN_POINT('Ctrl Pts',(-73.6261997253262,-0.814016886661847,
135.654779111957));
#91730=CARTESIAN_POINT('Ctrl Pts',(-73.6339560280681,-0.678663222641723,
135.677494712335));
#91731=CARTESIAN_POINT('Ctrl Pts',(-73.64171233081,-0.542429694408645,135.694528327474));
#91732=CARTESIAN_POINT('Ctrl Pts',(-73.6494686335518,-0.405830922617038,
135.70583838705));
#91733=CARTESIAN_POINT('Ctrl Pts',(-73.657229076066,-0.269159243947644,
135.717154483146));
#91734=CARTESIAN_POINT('Ctrl Pts',(-73.6649895185803,-0.132122323731912,
135.722740920746));
#91735=CARTESIAN_POINT('Ctrl Pts',(-73.6727499610945,0.00476461886399771,
135.722608309672));
#91736=CARTESIAN_POINT('Ctrl Pts',(-73.68052286136,0.141871304532413,135.722475485719));
#91737=CARTESIAN_POINT('Ctrl Pts',(-73.6882957616255,0.27882714063965,135.71660528383));
#91738=CARTESIAN_POINT('Ctrl Pts',(-73.696068661891,0.415120529808438,135.70506036436));
#91739=CARTESIAN_POINT('Ctrl Pts',(-73.7035589976526,0.546459310971236,
135.693935131794));
#91740=CARTESIAN_POINT('Ctrl Pts',(-73.7110493334143,0.677182666616575,
135.677540637529));
#91741=CARTESIAN_POINT('Ctrl Pts',(-73.7185396691759,0.806843158358512,
135.655977583105));
#91742=CARTESIAN_POINT('Ctrl Pts',(-73.726314003295,0.941419767061309,135.633596958918));
#91743=CARTESIAN_POINT('Ctrl Pts',(-73.734088337414,1.0752776221262,135.605577210705));
#91744=CARTESIAN_POINT('Ctrl Pts',(-73.7418626715331,1.20790697761996,135.571974674504));
#91745=CARTESIAN_POINT('Ctrl Pts',(-73.7496274244803,1.3403728792865,135.538413550427));
#91746=CARTESIAN_POINT('Ctrl Pts',(-73.7573921774274,1.47161291846988,135.499283423181));
#91747=CARTESIAN_POINT('Ctrl Pts',(-73.7651569303745,1.60112463440961,135.454692107641));
#91748=CARTESIAN_POINT('Ctrl Pts',(-73.7729139712595,1.73050771748727,135.410145080825));
#91749=CARTESIAN_POINT('Ctrl Pts',(-73.7806710121444,1.85816552614729,135.360147786432));
#91750=CARTESIAN_POINT('Ctrl Pts',(-73.7884280530294,1.9836082772336,135.304858508354));
#91751=CARTESIAN_POINT('Ctrl Pts',(-73.7961792442696,2.10895643096535,135.249610924351));
#91752=CARTESIAN_POINT('Ctrl Pts',(-73.8039304355098,2.2320924956283,135.189079457005));
#91753=CARTESIAN_POINT('Ctrl Pts',(-73.81168162675,2.35254461902446,135.123471275792));
#91754=CARTESIAN_POINT('Ctrl Pts',(-73.8194295235271,2.47294554705551,135.057890979805));
#91755=CARTESIAN_POINT('Ctrl Pts',(-73.8271774203041,2.59066446005866,134.987238448148));
#91756=CARTESIAN_POINT('Ctrl Pts',(-73.8349253170813,2.70525236971734,134.911767668083));
#91757=CARTESIAN_POINT('Ctrl Pts',(-73.8426715931654,2.81981631005555,134.836312674879));
#91758=CARTESIAN_POINT('Ctrl Pts',(-73.8504178692497,2.93125022345547,134.756041652895));
#91759=CARTESIAN_POINT('Ctrl Pts',(-73.8581641453338,3.03913282664551,134.671252744909));
#91760=CARTESIAN_POINT('Ctrl Pts',(-73.8659104785992,3.14701622620056,134.58646321103));
#91761=CARTESIAN_POINT('Ctrl Pts',(-73.8736568118645,3.25134795584579,134.497155966189));
#91762=CARTESIAN_POINT('Ctrl Pts',(-73.8814031451299,3.35173896015751,134.403670135441));
#91763=CARTESIAN_POINT('Ctrl Pts',(-73.8891512131329,3.45215244633845,134.310163369188));
#91764=CARTESIAN_POINT('Ctrl Pts',(-73.8968992811359,3.54862316505258,134.21247642135));
#91765=CARTESIAN_POINT('Ctrl Pts',(-73.9046473491389,3.64079843961101,134.110985752749));
#91766=CARTESIAN_POINT('Ctrl Pts',(-73.9124036518808,3.73307167914802,134.009387218658));
#91767=CARTESIAN_POINT('Ctrl Pts',(-73.9201599546227,3.82104009168055,133.903977178074));
#91768=CARTESIAN_POINT('Ctrl Pts',(-73.9279162573646,3.90439053788344,133.795166126152));
#91769=CARTESIAN_POINT('Ctrl Pts',(-73.9356766998788,3.98778547072932,133.686296998495));
#91770=CARTESIAN_POINT('Ctrl Pts',(-73.943437142393,4.06655730158809,133.57402356241));
#91771=CARTESIAN_POINT('Ctrl Pts',(-73.9511975849072,4.14043646825831,133.458785021239));
#91772=CARTESIAN_POINT('Ctrl Pts',(-73.9589704851727,4.21443423232534,133.343361488933));
#91773=CARTESIAN_POINT('Ctrl Pts',(-73.9667433854382,4.28352343997149,133.224963677717));
#91774=CARTESIAN_POINT('Ctrl Pts',(-73.9745162857036,4.34748027824938,133.104055878407));
#91775=CARTESIAN_POINT('Ctrl Pts',(-73.9820066214654,4.40911212435572,132.987543382155));
#91776=CARTESIAN_POINT('Ctrl Pts',(-73.9894969572271,4.46597813883685,132.868700496163));
#91777=CARTESIAN_POINT('Ctrl Pts',(-73.9969872929888,4.51792119337332,132.747958094661));
#91778=CARTESIAN_POINT('Ctrl Pts',(-74.0047616271079,4.57183368461235,132.622637708301));
#91779=CARTESIAN_POINT('Ctrl Pts',(-74.012535961227,4.62061331720246,132.494873945455));
#91780=CARTESIAN_POINT('Ctrl Pts',(-74.0203102953461,4.66403195812012,132.365126120816));
#91781=CARTESIAN_POINT('Ctrl Pts',(-74.0280750482931,4.70739708944318,132.235538198775));
#91782=CARTESIAN_POINT('Ctrl Pts',(-74.0358398012402,4.74541425206288,132.103971447317));
#91783=CARTESIAN_POINT('Ctrl Pts',(-74.0436045541872,4.77790256137297,131.970906877483));
#91784=CARTESIAN_POINT('Ctrl Pts',(-74.0513615950722,4.81035860283625,131.837974469255));
#91785=CARTESIAN_POINT('Ctrl Pts',(-74.0591186359572,4.83729662686257,131.703547580502));
#91786=CARTESIAN_POINT('Ctrl Pts',(-74.0668756768422,4.85858506241349,131.568123835974));
#91787=CARTESIAN_POINT('Ctrl Pts',(-74.0746268680823,4.87985744418964,131.432802215544));
#91788=CARTESIAN_POINT('Ctrl Pts',(-74.0823780593223,4.89548865708745,131.296485620285));
#91789=CARTESIAN_POINT('Ctrl Pts',(-74.0901292505625,4.90539795101484,131.159683012975));
#91790=CARTESIAN_POINT('Ctrl Pts',(-74.0978771473395,4.91530303322795,131.022938550424));
#91791=CARTESIAN_POINT('Ctrl Pts',(-74.1056250441167,4.91949100528358,130.885708875797));
#91792=CARTESIAN_POINT('Ctrl Pts',(-74.1133729408938,4.91793286470779,130.748509022002));
#91793=CARTESIAN_POINT('Ctrl Pts',(-74.1211192169778,4.91637505006142,130.61133786746));
#91794=CARTESIAN_POINT('Ctrl Pts',(-74.1288654930619,4.90907351799069,130.474196912034));
#91795=CARTESIAN_POINT('Ctrl Pts',(-74.136611769146,4.89605139055868,130.337601746725));
#91796=CARTESIAN_POINT('Ctrl Pts',(-74.1443581024113,4.88302916700034,130.201005573103));
#91797=CARTESIAN_POINT('Ctrl Pts',(-74.1521044356767,4.86428630092153,130.064955586839));
#91798=CARTESIAN_POINT('Ctrl Pts',(-74.159850768942,4.83989781387392,129.929962416654));
#91799=CARTESIAN_POINT('Ctrl Pts',(-74.167598836945,4.81550386519363,129.794939015683));
#91800=CARTESIAN_POINT('Ctrl Pts',(-74.1753469049479,4.7854618492335,129.660973286394));
#91801=CARTESIAN_POINT('Ctrl Pts',(-74.1830949729508,4.74989786277997,129.528565431943));
#91802=CARTESIAN_POINT('Ctrl Pts',(-74.1908512756927,4.71429607849847,129.396016852849));
#91803=CARTESIAN_POINT('Ctrl Pts',(-74.1986075784345,4.67316070170972,129.265029834271));
#91804=CARTESIAN_POINT('Ctrl Pts',(-74.2063638811764,4.62666783415993,129.136089711853));
#91805=CARTESIAN_POINT('Ctrl Pts',(-74.2141243236905,4.58015015196686,129.007080770208));
#91806=CARTESIAN_POINT('Ctrl Pts',(-74.2218847662046,4.52826942912837,128.880121263338));
#91807=CARTESIAN_POINT('Ctrl Pts',(-74.2296452087188,4.471249474902,128.755675381692));
#91808=CARTESIAN_POINT('Ctrl Pts',(-74.2374181089842,4.41413798718311,128.631029728469));
#91809=CARTESIAN_POINT('Ctrl Pts',(-74.2451910092496,4.35187095973814,128.508906112379));
#91810=CARTESIAN_POINT('Ctrl Pts',(-74.252963909515,4.28471803721438,128.38974379412));
#91811=CARTESIAN_POINT('Ctrl Pts',(-74.2604542452772,4.2200062925709,128.274913326279));
#91812=CARTESIAN_POINT('Ctrl Pts',(-74.2679445810394,4.15075787663367,128.162832854982));
#91813=CARTESIAN_POINT('Ctrl Pts',(-74.2754349168016,4.07725036439922,128.053867474781));
#91814=CARTESIAN_POINT('Ctrl Pts',(-74.2832092509206,4.00095579249872,127.940770639074));
#91815=CARTESIAN_POINT('Ctrl Pts',(-74.2909835850395,3.91983110328264,127.830671518044));
#91816=CARTESIAN_POINT('Ctrl Pts',(-74.2987579191585,3.83413941974083,127.724010317277));
#91817=CARTESIAN_POINT('Ctrl Pts',(-74.3065226721056,3.74855334354026,127.617480566907));
#91818=CARTESIAN_POINT('Ctrl Pts',(-74.3142874250526,3.65841171439173,127.514380608434));
#91819=CARTESIAN_POINT('Ctrl Pts',(-74.3220521779996,3.56402144795968,127.415122623417));
#91820=CARTESIAN_POINT('Ctrl Pts',(-74.3298092188845,3.46972493127143,127.31596322283));
#91821=CARTESIAN_POINT('Ctrl Pts',(-74.3375662597694,3.37118844258138,127.220638483363));
#91822=CARTESIAN_POINT('Ctrl Pts',(-74.3453233006543,3.26875953032542,127.129528077789));
#91823=CARTESIAN_POINT('Ctrl Pts',(-74.3530744918943,3.16640786050911,127.03848637928));
#91824=CARTESIAN_POINT('Ctrl Pts',(-74.3608256831343,3.06016990061778,126.951652947715));
#91825=CARTESIAN_POINT('Ctrl Pts',(-74.3685768743743,2.95043020805505,126.869370827249));
#91826=CARTESIAN_POINT('Ctrl Pts',(-74.3763247711513,2.84073715778861,126.787123678879));
#91827=CARTESIAN_POINT('Ctrl Pts',(-74.3840726679282,2.7275456471735,126.709424228223));
#91828=CARTESIAN_POINT('Ctrl Pts',(-74.3918205647052,2.6112733114351,126.63657526375));
#91829=CARTESIAN_POINT('Ctrl Pts',(-74.3995668407892,2.49502529736279,126.563741537709));
#91830=CARTESIAN_POINT('Ctrl Pts',(-74.4073131168733,2.37569807109688,126.495756487169));
#91831=CARTESIAN_POINT('Ctrl Pts',(-74.4150593929573,2.25373791198869,126.432879348412));
#91832=CARTESIAN_POINT('Ctrl Pts',(-74.4228057262226,2.13177685259849,126.37000174551));
#91833=CARTESIAN_POINT('Ctrl Pts',(-74.4305520594878,2.00718316908452,126.312232308786));
#91834=CARTESIAN_POINT('Ctrl Pts',(-74.438298392753,1.8804270188328,126.25978392778));
#91835=CARTESIAN_POINT('Ctrl Pts',(-74.4460464607559,1.75364248242062,126.207323801323));
#91836=CARTESIAN_POINT('Ctrl Pts',(-74.4537945287587,1.62469487682233,126.160187251209));
#91837=CARTESIAN_POINT('Ctrl Pts',(-74.4615425967615,1.49407319551313,126.118538560664));
#91838=CARTESIAN_POINT('Ctrl Pts',(-74.4692988995033,1.36331268792573,126.076845605395));
#91839=CARTESIAN_POINT('Ctrl Pts',(-74.4770552022451,1.23087492351143,126.040652279824));
#91840=CARTESIAN_POINT('Ctrl Pts',(-74.4848115049868,1.0972634161861,126.010072760334));
#91841=CARTESIAN_POINT('Ctrl Pts',(-74.4925719475009,0.96358059637597,125.979476919634));
#91842=CARTESIAN_POINT('Ctrl Pts',(-74.500332390015,0.828723169616098,125.954500926474));
#91843=CARTESIAN_POINT('Ctrl Pts',(-74.5080928325291,0.693202646848998,
125.935207390063));
#91844=CARTESIAN_POINT('Ctrl Pts',(-74.5158657327944,0.557464574508172,
125.915882881955));
#91845=CARTESIAN_POINT('Ctrl Pts',(-74.5236386330597,0.421061668282188,
125.902259098105));
#91846=CARTESIAN_POINT('Ctrl Pts',(-74.531411533325,0.284509240154991,125.894346609972));
#91847=CARTESIAN_POINT('Ctrl Pts',(-74.5389018690881,0.152920836725796,
125.886721760712));
#91848=CARTESIAN_POINT('Ctrl Pts',(-74.5463922048511,0.0211939016250774,
125.884400181803));
#91849=CARTESIAN_POINT('Ctrl Pts',(-74.5538825406141,-0.110214364695965,
125.887345684061));
#91850=CARTESIAN_POINT('Ctrl Pts',(-74.5616568747333,-0.246605015360688,
125.890402865932));
#91851=CARTESIAN_POINT('Ctrl Pts',(-74.5694312088526,-0.38308440015906,
125.899144100303));
#91852=CARTESIAN_POINT('Ctrl Pts',(-74.5772055429719,-0.51913993726121,
125.913585956222));
#91853=CARTESIAN_POINT('Ctrl Pts',(-74.5849702959192,-0.655027798073519,
125.928010013845));
#91854=CARTESIAN_POINT('Ctrl Pts',(-74.5927350488664,-0.790492465470328,
125.948120673481));
#91855=CARTESIAN_POINT('Ctrl Pts',(-74.6004998018137,-0.925021264018458,
125.973882512491));
#91856=CARTESIAN_POINT('Ctrl Pts',(-74.6082568426989,-1.05941644666771,
125.999618764478));
#91857=CARTESIAN_POINT('Ctrl Pts',(-74.6160138835841,-1.19287722874811,
126.030994952995));
#91858=CARTESIAN_POINT('Ctrl Pts',(-74.6237709244693,-1.32489632238328,
126.067923898107));
#91859=CARTESIAN_POINT('Ctrl Pts',(-74.6315221157096,-1.45681585939281,
126.104824994815));
#91860=CARTESIAN_POINT('Ctrl Pts',(-74.63927330695,-1.58729549695094,126.147270408505));
#91861=CARTESIAN_POINT('Ctrl Pts',(-74.6470244981903,-1.7158387596256,126.195122023886));
#91862=CARTESIAN_POINT('Ctrl Pts',(-74.6547723949676,-1.84432738798479,
126.242953301055));
#91863=CARTESIAN_POINT('Ctrl Pts',(-74.6625202917448,-1.97088091273265,
126.296186073695));
#91864=CARTESIAN_POINT('Ctrl Pts',(-74.6702681885221,-2.09501884731395,
126.354632638026));
#91865=CARTESIAN_POINT('Ctrl Pts',(-74.6780144646064,-2.2191308149151,126.413066976596));
#91866=CARTESIAN_POINT('Ctrl Pts',(-74.6857607406907,-2.34082784390101,
126.476712771136));
#91867=CARTESIAN_POINT('Ctrl Pts',(-74.693507016775,-2.45965060655395,126.545334677732));
#91868=CARTESIAN_POINT('Ctrl Pts',(-74.7012533500405,-2.57847424632969,
126.613957090879));
#91869=CARTESIAN_POINT('Ctrl Pts',(-74.7089996833061,-2.69442323887346,
126.687555493855));
#91870=CARTESIAN_POINT('Ctrl Pts',(-74.7167460165716,-2.80706434263411,
126.765849401931));
#91871=CARTESIAN_POINT('Ctrl Pts',(-74.7244940845748,-2.9197306715888,126.844160843385));
#91872=CARTESIAN_POINT('Ctrl Pts',(-74.732242152578,-3.02908731672551,126.927169659255));
#91873=CARTESIAN_POINT('Ctrl Pts',(-74.7399902205811,-3.13473174899534,
127.01455324458));
#91874=CARTESIAN_POINT('Ctrl Pts',(-74.7477465233232,-3.24048846142483,
127.102029702219));
#91875=CARTESIAN_POINT('Ctrl Pts',(-74.7555028260651,-3.34252477791533,
127.193889967716));
#91876=CARTESIAN_POINT('Ctrl Pts',(-74.7632591288072,-3.44047247707194,
127.289772135679));
#91877=CARTESIAN_POINT('Ctrl Pts',(-74.7710195713215,-3.53847245386502,
127.385705478843));
#91878=CARTESIAN_POINT('Ctrl Pts',(-74.7787800138359,-3.63237919750787,
127.485664716967));
#91879=CARTESIAN_POINT('Ctrl Pts',(-74.7865404563503,-3.72186354894042,
127.589253343218));
#91880=CARTESIAN_POINT('Ctrl Pts',(-74.7943133566159,-3.81149154859769,
127.693008259127));
#91881=CARTESIAN_POINT('Ctrl Pts',(-74.8020862568816,-3.89668272643745,
127.800403899322));
#91882=CARTESIAN_POINT('Ctrl Pts',(-74.8098591571472,-3.97714964967791,
127.911012431369));
#91883=CARTESIAN_POINT('Ctrl Pts',(-74.8173494929076,-4.0546913975557,128.017600064645));
#91884=CARTESIAN_POINT('Ctrl Pts',(-74.8248398286679,-4.12784623364636,
128.1271707957));
#91885=CARTESIAN_POINT('Ctrl Pts',(-74.8323301644283,-4.19639747692351,
128.239320407712));
#91886=CARTESIAN_POINT('Ctrl Pts',(-74.8403463761326,-4.26976151510246,
128.359343736597));
#91887=CARTESIAN_POINT('Ctrl Pts',(-74.8483625878368,-4.33807319262493,
128.48268134349));
#91888=CARTESIAN_POINT('Ctrl Pts',(-74.8563787995411,-4.40102994931516,
128.60888380199));
#91889=CARTESIAN_POINT('Ctrl Pts',(-74.8643843410293,-4.4639029055492,128.734918274969));
#91890=CARTESIAN_POINT('Ctrl Pts',(-74.8723898825175,-4.52143497228248,
128.86380969095));
#91891=CARTESIAN_POINT('Ctrl Pts',(-74.8803954240057,-4.57336737440473,
128.995080672054));
#91892=CARTESIAN_POINT('Ctrl Pts',(-74.8883883634197,-4.62521802615655,
129.126145010468));
#91893=CARTESIAN_POINT('Ctrl Pts',(-74.8963813028338,-4.67148644927185,
129.259581118436));
#91894=CARTESIAN_POINT('Ctrl Pts',(-74.9043742422479,-4.71196051533489,
129.394888672324));
#91895=CARTESIAN_POINT('Ctrl Pts',(-74.9080459389746,-4.73055298653757,
129.457044567292));
#91896=CARTESIAN_POINT('Ctrl Pts',(-74.9117176357013,-4.74792338859597,
129.519595050684));
#91897=CARTESIAN_POINT('Ctrl Pts',(-74.915389332428,-4.7640545282341,129.582490119308));
#91898=CARTESIAN_POINT('Ctrl Pts',(-73.1652357600351,-4.76405452823407,
129.582490119308));
#91899=CARTESIAN_POINT('Ctrl Pts',(-73.1751882435279,-4.80744916394512,
129.75168514534));
#91900=CARTESIAN_POINT('Ctrl Pts',(-73.1851407270206,-4.84185311265486,
129.923297623253));
#91901=CARTESIAN_POINT('Ctrl Pts',(-73.1950932105134,-4.8670426185736,130.096491129957));
#91902=CARTESIAN_POINT('Ctrl Pts',(-73.2048632772353,-4.89177043185747,
130.266510212886));
#91903=CARTESIAN_POINT('Ctrl Pts',(-73.2146333439573,-4.90761850293709,
130.438053071438));
#91904=CARTESIAN_POINT('Ctrl Pts',(-73.2244034106792,-4.91442021846172,
130.610306555834));
#91905=CARTESIAN_POINT('Ctrl Pts',(-73.2279824617749,-4.9169118787639,130.673407867176));
#91906=CARTESIAN_POINT('Ctrl Pts',(-73.2315615128704,-4.91818999338173,
130.736604314292));
#91907=CARTESIAN_POINT('Ctrl Pts',(-73.235140563966,-4.9182479362882,130.799855099079));
#91908=CARTESIAN_POINT('',(-72.8898594359386,-4.91824980117577,130.805759093339));
#91909=CARTESIAN_POINT('Ctrl Pts',(-72.8197282857817,-4.76405452823409,
129.582490119308));
#91910=CARTESIAN_POINT('Ctrl Pts',(-72.827431657208,-4.79789784864164,129.714444711933));
#91911=CARTESIAN_POINT('Ctrl Pts',(-72.8351350286343,-4.82622855293165,
129.847704598932));
#91912=CARTESIAN_POINT('Ctrl Pts',(-72.8428384000606,-4.84897116631987,
129.981766130167));
#91913=CARTESIAN_POINT('Ctrl Pts',(-72.8506752393736,-4.87210781608252,
130.118150398848));
#91914=CARTESIAN_POINT('Ctrl Pts',(-72.8585120786865,-4.88946089590854,
130.255363917468));
#91915=CARTESIAN_POINT('Ctrl Pts',(-72.8663489179995,-4.90100615995804,
130.39287345792));
#91916=CARTESIAN_POINT('Ctrl Pts',(-72.8741857573126,-4.91255142400755,
130.530382998373));
#91917=CARTESIAN_POINT('Ctrl Pts',(-72.8820225966256,-4.91828891867964,
130.66818813263));
#91918=CARTESIAN_POINT('Ctrl Pts',(-72.8898594359387,-4.91824980117577,
130.805759093339));
#91919=CARTESIAN_POINT('Ctrl Pts',(-72.889859435991,-4.91824980117551,130.80575909426));
#91920=CARTESIAN_POINT('Ctrl Pts',(-72.8941682219596,-4.91822829389993,
130.881397218446));
#91921=CARTESIAN_POINT('Ctrl Pts',(-72.8984770079282,-4.91646201598752,
130.957008388749));
#91922=CARTESIAN_POINT('Ctrl Pts',(-72.9027857938971,-4.91295411382803,
131.03253804397));
#91923=CARTESIAN_POINT('Ctrl Pts',(-72.9105601280161,-4.90662481280411,
131.168816053557));
#91924=CARTESIAN_POINT('Ctrl Pts',(-72.9183344621351,-4.89461096677241,
131.305046370138));
#91925=CARTESIAN_POINT('Ctrl Pts',(-72.9261087962542,-4.87690831200657,
131.440716161882));
#91926=CARTESIAN_POINT('Ctrl Pts',(-72.9338735492012,-4.85922747418064,
131.576218752732));
#91927=CARTESIAN_POINT('Ctrl Pts',(-72.9416383021482,-4.83587182741818,
131.711161809267));
#91928=CARTESIAN_POINT('Ctrl Pts',(-72.9494030550952,-4.80688908695483,
131.845033653738));
#91929=CARTESIAN_POINT('Ctrl Pts',(-72.9571600959802,-4.77793513255782,
131.978772534806));
#91930=CARTESIAN_POINT('Ctrl Pts',(-72.9649171368652,-4.74336528883123,
132.111441941463));
#91931=CARTESIAN_POINT('Ctrl Pts',(-72.9726741777502,-4.70327888411369,
132.242536823999));
#91932=CARTESIAN_POINT('Ctrl Pts',(-72.9804253689903,-4.66322270886582,
132.373532846864));
#91933=CARTESIAN_POINT('Ctrl Pts',(-72.9881765602303,-4.61765836687906,
132.502956336613));
#91934=CARTESIAN_POINT('Ctrl Pts',(-72.9959277514704,-4.56673584771151,
132.630314275173));
#91935=CARTESIAN_POINT('Ctrl Pts',(-73.0036756482475,-4.51583497197294,
132.757618083211));
#91936=CARTESIAN_POINT('Ctrl Pts',(-73.0114235450245,-4.45958059341154,
132.882857723903));
#91937=CARTESIAN_POINT('Ctrl Pts',(-73.0191714418016,-4.39817189210529,
133.005557353434));
#91938=CARTESIAN_POINT('Ctrl Pts',(-73.0269177178857,-4.3367760361757,133.128231316847));
#91939=CARTESIAN_POINT('Ctrl Pts',(-73.0346639939697,-4.27022817691521,
133.248365976514));
#91940=CARTESIAN_POINT('Ctrl Pts',(-73.0424102700538,-4.1987746130634,133.365507784598));
#91941=CARTESIAN_POINT('Ctrl Pts',(-73.0501566033191,-4.12732052175752,
133.482650457395));
#91942=CARTESIAN_POINT('Ctrl Pts',(-73.0579029365845,-4.05096085719293,
133.596799900753));
#91943=CARTESIAN_POINT('Ctrl Pts',(-73.0656492698498,-3.9699864199273,133.707529728743));
#91944=CARTESIAN_POINT('Ctrl Pts',(-73.0733973378527,-3.88899384899776,
133.81828435391));
#91945=CARTESIAN_POINT('Ctrl Pts',(-73.0811454058556,-3.8033846796653,133.925617524333));
#91946=CARTESIAN_POINT('Ctrl Pts',(-73.0888934738586,-3.71349108357781,
134.02913456851));
#91947=CARTESIAN_POINT('Ctrl Pts',(-73.0966497766004,-3.62350194750678,
134.132761631834));
#91948=CARTESIAN_POINT('Ctrl Pts',(-73.1044060793422,-3.5292195452495,134.2325641713));
#91949=CARTESIAN_POINT('Ctrl Pts',(-73.112162382084,-3.43101451427831,134.328182756283));
#91950=CARTESIAN_POINT('Ctrl Pts',(-73.1199228245981,-3.3327570683252,134.423852375784));
#91951=CARTESIAN_POINT('Ctrl Pts',(-73.1276832671123,-3.23057311307851,
134.515333330507));
#91952=CARTESIAN_POINT('Ctrl Pts',(-73.1354437096265,-3.12486694009949,
134.602306071252));
#91953=CARTESIAN_POINT('Ctrl Pts',(-73.1432166098919,-3.01899107818746,
134.689418428361));
#91954=CARTESIAN_POINT('Ctrl Pts',(-73.1509895101572,-2.90958201191764,
134.772007874004));
#91955=CARTESIAN_POINT('Ctrl Pts',(-73.1587624104226,-2.79707434811417,
134.849797324971));
#91956=CARTESIAN_POINT('Ctrl Pts',(-73.166252746185,-2.68865662127357,134.92475893346));
#91957=CARTESIAN_POINT('Ctrl Pts',(-73.1737430819474,-2.57736192949597,
134.99526330736));
#91958=CARTESIAN_POINT('Ctrl Pts',(-73.1812334177098,-2.46359957294985,
135.061103528133));
#91959=CARTESIAN_POINT('Ctrl Pts',(-73.1890077518289,-2.34552388208411,
135.129440100884));
#91960=CARTESIAN_POINT('Ctrl Pts',(-73.196782085948,-2.22441568126635,135.192968325691));
#91961=CARTESIAN_POINT('Ctrl Pts',(-73.2045564200671,-2.1007041257914,135.251407417228));
#91962=CARTESIAN_POINT('Ctrl Pts',(-73.2123211730141,-1.97714503375216,
135.309774487807));
#91963=CARTESIAN_POINT('Ctrl Pts',(-73.2200859259612,-1.85098932093365,
135.363064738945));
#91964=CARTESIAN_POINT('Ctrl Pts',(-73.2278506789083,-1.72269326756848,
135.411041740498));
#91965=CARTESIAN_POINT('Ctrl Pts',(-73.2356077197933,-1.59452463965217,
135.458971090616));
#91966=CARTESIAN_POINT('Ctrl Pts',(-73.2433647606783,-1.46422026548786,
135.501597556949));
#91967=CARTESIAN_POINT('Ctrl Pts',(-73.2511218015633,-1.33225874709521,
135.538731715535));
#91968=CARTESIAN_POINT('Ctrl Pts',(-73.2588729928034,-1.20039674190991,
135.575837870964));
#91969=CARTESIAN_POINT('Ctrl Pts',(-73.2666241840436,-1.06688045470472,
135.607459857155));
#91970=CARTESIAN_POINT('Ctrl Pts',(-73.2743753752838,-0.932205748567533,
135.633457376261));
#91971=CARTESIAN_POINT('Ctrl Pts',(-73.2821232720609,-0.797588282772833,
135.659443845728));
#91972=CARTESIAN_POINT('Ctrl Pts',(-73.2898711688378,-0.661813760385015,
135.679810528779));
#91973=CARTESIAN_POINT('Ctrl Pts',(-73.2976190656149,-0.52539018397863,
135.694467796052));
#91974=CARTESIAN_POINT('Ctrl Pts',(-73.305365341699,-0.388995144443849,
135.70912199734));
#91975=CARTESIAN_POINT('Ctrl Pts',(-73.3131116177832,-0.251951709422492,
135.718069116613));
#91976=CARTESIAN_POINT('Ctrl Pts',(-73.3208578938673,-0.114774592040411,
135.721271218291));
#91977=CARTESIAN_POINT('Ctrl Pts',(-73.3286042271327,0.0224035379521743,
135.724473343606));
#91978=CARTESIAN_POINT('Ctrl Pts',(-73.336350560398,0.159714961415861,135.72193035758));
#91979=CARTESIAN_POINT('Ctrl Pts',(-73.3440968936634,0.296643762988791,
135.713656446947));
#91980=CARTESIAN_POINT('Ctrl Pts',(-73.3518449616663,0.433603228817248,
135.70538068343));
#91981=CARTESIAN_POINT('Ctrl Pts',(-73.3595930296693,0.570179512071966,
135.691371465064));
#91982=CARTESIAN_POINT('Ctrl Pts',(-73.3673410976723,0.705861017552133,
135.671694927679));
#91983=CARTESIAN_POINT('Ctrl Pts',(-73.3750974004141,0.841686726951139,
135.651997477835));
#91984=CARTESIAN_POINT('Ctrl Pts',(-73.3828537031559,0.976615371354942,
135.626620732993));
#91985=CARTESIAN_POINT('Ctrl Pts',(-73.3906100058978,1.11014421299232,135.595682239922));
#91986=CARTESIAN_POINT('Ctrl Pts',(-73.398370448412,1.24374432299296,135.564727234047));
#91987=CARTESIAN_POINT('Ctrl Pts',(-73.4061308909262,1.37594276486986,135.528204669071));
#91988=CARTESIAN_POINT('Ctrl Pts',(-73.4138913334404,1.50625216336704,135.486281962789));
#91989=CARTESIAN_POINT('Ctrl Pts',(-73.4216642337058,1.63677074607902,135.444291958456));
#91990=CARTESIAN_POINT('Ctrl Pts',(-73.4294371339712,1.76539385853742,135.396884625106));
#91991=CARTESIAN_POINT('Ctrl Pts',(-73.4372100342366,1.8916534671864,135.344275839526));
#91992=CARTESIAN_POINT('Ctrl Pts',(-73.4447003699987,2.01332322103189,135.293579515815));
#91993=CARTESIAN_POINT('Ctrl Pts',(-73.4521907057606,2.13279804700486,135.238053475853));
#91994=CARTESIAN_POINT('Ctrl Pts',(-73.4596810415227,2.24968262193993,135.177930230942));
#91995=CARTESIAN_POINT('Ctrl Pts',(-73.4674553756417,2.37099891105981,135.115527394925));
#91996=CARTESIAN_POINT('Ctrl Pts',(-73.4752297097608,2.48990894657635,135.047974192886));
#91997=CARTESIAN_POINT('Ctrl Pts',(-73.4830040438799,2.60594452692407,134.975479914001));
#91998=CARTESIAN_POINT('Ctrl Pts',(-73.490768796827,2.72183710378941,134.903074977837));
#91999=CARTESIAN_POINT('Ctrl Pts',(-73.498533549774,2.83486194563252,134.825741286154));
#92000=CARTESIAN_POINT('Ctrl Pts',(-73.506298302721,2.94457350646707,134.743734924168));
#92001=CARTESIAN_POINT('Ctrl Pts',(-73.514055343606,3.05417610023273,134.661810012056));
#92002=CARTESIAN_POINT('Ctrl Pts',(-73.521812384491,3.16047165069988,134.575221897923));
#92003=CARTESIAN_POINT('Ctrl Pts',(-73.529569425376,3.2630420940429,134.484270854923));
#92004=CARTESIAN_POINT('Ctrl Pts',(-73.5373206166161,3.36553518821685,134.393388398812));
#92005=CARTESIAN_POINT('Ctrl Pts',(-73.5450718078563,3.46430847533151,134.298149820955));
#92006=CARTESIAN_POINT('Ctrl Pts',(-73.5528229990964,3.55897589272276,134.198896470598));
#92007=CARTESIAN_POINT('Ctrl Pts',(-73.5605708958735,3.65360307393616,134.099685305562));
#92008=CARTESIAN_POINT('Ctrl Pts',(-73.5683187926505,3.74412758702922,133.996463044217));
#92009=CARTESIAN_POINT('Ctrl Pts',(-73.5760666894276,3.83019943647956,133.889608636655));
#92010=CARTESIAN_POINT('Ctrl Pts',(-73.5838129655116,3.91625328155449,133.782776580731));
#92011=CARTESIAN_POINT('Ctrl Pts',(-73.5915592415957,3.99785607049535,133.672314194089));
#92012=CARTESIAN_POINT('Ctrl Pts',(-73.5993055176798,4.07469767200758,133.558634014351));
#92013=CARTESIAN_POINT('Ctrl Pts',(-73.6070518509452,4.15153984074716,133.444952995451));
#92014=CARTESIAN_POINT('Ctrl Pts',(-73.6147981842105,4.22362053298201,133.328054459966));
#92015=CARTESIAN_POINT('Ctrl Pts',(-73.6225445174758,4.29067281955979,133.20838013038));
#92016=CARTESIAN_POINT('Ctrl Pts',(-73.6302925854788,4.35774012203214,133.088679000558));
#92017=CARTESIAN_POINT('Ctrl Pts',(-73.6380406534817,4.41977658701986,132.966201180694));
#92018=CARTESIAN_POINT('Ctrl Pts',(-73.6457887214846,4.47656132676596,132.841412838351));
#92019=CARTESIAN_POINT('Ctrl Pts',(-73.6535450242265,4.5334064180093,132.716491869472));
#92020=CARTESIAN_POINT('Ctrl Pts',(-73.6613013269683,4.58498847198252,132.589255829109));
#92021=CARTESIAN_POINT('Ctrl Pts',(-73.6690576297102,4.63113464206716,132.460191221688));
#92022=CARTESIAN_POINT('Ctrl Pts',(-73.6768180722243,4.67730544175221,132.331057728599));
#92023=CARTESIAN_POINT('Ctrl Pts',(-73.6845785147384,4.71803446042663,132.200094096911));
#92024=CARTESIAN_POINT('Ctrl Pts',(-73.6923389572526,4.75319911319038,132.067800862637));
#92025=CARTESIAN_POINT('Ctrl Pts',(-73.700111857518,4.78842021537651,131.935295259519));
#92026=CARTESIAN_POINT('Ctrl Pts',(-73.7078847577834,4.81805901726189,131.801456170549));
#92027=CARTESIAN_POINT('Ctrl Pts',(-73.7156576580489,4.84204415853208,131.666794052287));
#92028=CARTESIAN_POINT('Ctrl Pts',(-73.7231479938111,4.86515737950295,131.537027241214));
#92029=CARTESIAN_POINT('Ctrl Pts',(-73.7306383295734,4.88302081127843,131.406496505518));
#92030=CARTESIAN_POINT('Ctrl Pts',(-73.7381286653356,4.89561639037252,131.275660119811));
#92031=CARTESIAN_POINT('Ctrl Pts',(-73.7459029994547,4.90868953467592,131.139863032776));
#92032=CARTESIAN_POINT('Ctrl Pts',(-73.7536773335738,4.91612889133002,131.003306496408));
#92033=CARTESIAN_POINT('Ctrl Pts',(-73.7614516676929,4.91785746686445,130.866497547854));
#92034=CARTESIAN_POINT('Ctrl Pts',(-73.76921642064,4.91958391208402,130.729857204102));
#92035=CARTESIAN_POINT('Ctrl Pts',(-73.7769811735872,4.91561357486859,130.592965454294));
#92036=CARTESIAN_POINT('Ctrl Pts',(-73.7847459265343,4.90592107847343,130.4563355692));
#92037=CARTESIAN_POINT('Ctrl Pts',(-73.7925029674193,4.89623820880233,130.319841386834));
#92038=CARTESIAN_POINT('Ctrl Pts',(-73.8002600083042,4.88084451751945,130.183608939058));
#92039=CARTESIAN_POINT('Ctrl Pts',(-73.8080170491892,4.85976665922539,130.048152259783));
#92040=CARTESIAN_POINT('Ctrl Pts',(-73.8157682404293,4.8387046959082,129.912797729443));
#92041=CARTESIAN_POINT('Ctrl Pts',(-73.8235194316695,4.81196715741731,129.778218187925));
#92042=CARTESIAN_POINT('Ctrl Pts',(-73.8312706229097,4.77963255424048,129.644922948286));
#92043=CARTESIAN_POINT('Ctrl Pts',(-73.8390185196868,4.74731169413259,129.511684362681));
#92044=CARTESIAN_POINT('Ctrl Pts',(-73.8467664164639,4.70939859276699,129.379729372427));
#92045=CARTESIAN_POINT('Ctrl Pts',(-73.854514313241,4.66602289046028,129.249557270451));
#92046=CARTESIAN_POINT('Ctrl Pts',(-73.8622605893251,4.62265626141541,129.119412397673));
#92047=CARTESIAN_POINT('Ctrl Pts',(-73.8700068654092,4.57382942775682,128.991050042051));
#92048=CARTESIAN_POINT('Ctrl Pts',(-73.8777531414933,4.51972183553017,128.86495411249));
#92049=CARTESIAN_POINT('Ctrl Pts',(-73.8854994747586,4.46561384389348,128.738857252117));
#92050=CARTESIAN_POINT('Ctrl Pts',(-73.8932458080241,4.40622517007299,128.615027210473));
#92051=CARTESIAN_POINT('Ctrl Pts',(-73.9009921412894,4.34178316597662,128.493927324406));
#92052=CARTESIAN_POINT('Ctrl Pts',(-73.9087402092924,4.27732673054034,128.372800318859));
#92053=CARTESIAN_POINT('Ctrl Pts',(-73.9164882772954,4.20781489658678,128.254405030577));
#92054=CARTESIAN_POINT('Ctrl Pts',(-73.9242363452983,4.1335204688605,128.13917927364));
#92055=CARTESIAN_POINT('Ctrl Pts',(-73.9319926480402,4.05914708013222,128.023831053397));
#92056=CARTESIAN_POINT('Ctrl Pts',(-73.9397489507821,3.97998115599643,127.91165942278));
#92057=CARTESIAN_POINT('Ctrl Pts',(-73.947505253524,3.89633857858578,127.803072770071));
#92058=CARTESIAN_POINT('Ctrl Pts',(-73.9552656960382,3.81265135861313,127.694428161395));
#92059=CARTESIAN_POINT('Ctrl Pts',(-73.9630261385524,3.72448297564591,127.589372642587));
#92060=CARTESIAN_POINT('Ctrl Pts',(-73.9707865810666,3.63218828467451,127.488279899735));
#92061=CARTESIAN_POINT('Ctrl Pts',(-73.9785594813321,3.53974543407164,127.387024873837));
#92062=CARTESIAN_POINT('Ctrl Pts',(-73.9863323815975,3.44316331438664,127.289745613606));
#92063=CARTESIAN_POINT('Ctrl Pts',(-73.9941052818629,3.34283281518932,127.196778070736));
#92064=CARTESIAN_POINT('Ctrl Pts',(-74.0015956176248,3.24614958235809,127.107190132223));
#92065=CARTESIAN_POINT('Ctrl Pts',(-74.0090859533866,3.14598599881325,127.021606070122));
#92066=CARTESIAN_POINT('Ctrl Pts',(-74.0165762891484,3.04271786020936,126.940288790379));
#92067=CARTESIAN_POINT('Ctrl Pts',(-74.0243506232675,2.93553427873976,126.855888341255));
#92068=CARTESIAN_POINT('Ctrl Pts',(-74.0321249573865,2.82466655119882,126.775817256323));
#92069=CARTESIAN_POINT('Ctrl Pts',(-74.0398992915056,2.71049964544922,126.700414378332));
#92070=CARTESIAN_POINT('Ctrl Pts',(-74.0476640444527,2.59647344020756,126.62510442765));
#92071=CARTESIAN_POINT('Ctrl Pts',(-74.0554287973997,2.47915646987265,126.554451450257));
#92072=CARTESIAN_POINT('Ctrl Pts',(-74.0631935503468,2.35896684693005,126.488754231717));
#92073=CARTESIAN_POINT('Ctrl Pts',(-74.0709505912318,2.23889659801533,126.423122264579));
#92074=CARTESIAN_POINT('Ctrl Pts',(-74.0787076321169,2.11595971524768,126.362436447342));
#92075=CARTESIAN_POINT('Ctrl Pts',(-74.0864646730019,1.99060307737814,126.306952202619));
#92076=CARTESIAN_POINT('Ctrl Pts',(-74.094215864242,1.86534097192417,126.251509798997));
#92077=CARTESIAN_POINT('Ctrl Pts',(-74.1019670554821,1.7376630994995,126.201261317897));
#92078=CARTESIAN_POINT('Ctrl Pts',(-74.1097182467223,1.60804039644098,126.156416002372));
#92079=CARTESIAN_POINT('Ctrl Pts',(-74.1174661434994,1.47847278648923,126.111589747302));
#92080=CARTESIAN_POINT('Ctrl Pts',(-74.1252140402764,1.3469623586621,126.072162217823));
#92081=CARTESIAN_POINT('Ctrl Pts',(-74.1329619370535,1.2139992559975,126.038294223889));
#92082=CARTESIAN_POINT('Ctrl Pts',(-74.1407082131376,1.08106396634763,126.004433314409));
#92083=CARTESIAN_POINT('Ctrl Pts',(-74.1484544892217,0.94667698489861,125.976129723776));
#92084=CARTESIAN_POINT('Ctrl Pts',(-74.1562007653058,0.811342432886796,
125.95349404353));
#92085=CARTESIAN_POINT('Ctrl Pts',(-74.1639470985711,0.676006881866248,
125.930858196193));
#92086=CARTESIAN_POINT('Ctrl Pts',(-74.1716934318364,0.53972413193411,125.913890407228));
#92087=CARTESIAN_POINT('Ctrl Pts',(-74.1794397651018,0.403006890761979,
125.902649843918));
#92088=CARTESIAN_POINT('Ctrl Pts',(-74.1871878331047,0.266259032711431,
125.891406763362));
#92089=CARTESIAN_POINT('Ctrl Pts',(-74.1949359011077,0.129076879378445,
125.885893492662));
#92090=CARTESIAN_POINT('Ctrl Pts',(-74.2026839691107,-0.00802376622388518,
125.886117162665));
#92091=CARTESIAN_POINT('Ctrl Pts',(-74.2104402718526,-0.145270124023693,
125.886341070387));
#92092=CARTESIAN_POINT('Ctrl Pts',(-74.2181965745945,-0.282434409457219,
125.892314098165));
#92093=CARTESIAN_POINT('Ctrl Pts',(-74.2259528773363,-0.419002291888928,
125.903991229255));
#92094=CARTESIAN_POINT('Ctrl Pts',(-74.2337133198505,-0.555643064711471,
125.915674592782));
#92095=CARTESIAN_POINT('Ctrl Pts',(-74.2414737623646,-0.69168641263746,
125.933068076391));
#92096=CARTESIAN_POINT('Ctrl Pts',(-74.2492342048788,-0.826626135186591,
125.956075116987));
#92097=CARTESIAN_POINT('Ctrl Pts',(-74.2570071051442,-0.961782474958112,
125.979119090527));
#92098=CARTESIAN_POINT('Ctrl Pts',(-74.2647800054095,-1.09583126652113,
126.007794546833));
#92099=CARTESIAN_POINT('Ctrl Pts',(-74.272552905675,-1.22827857884026,126.041954209534));
#92100=CARTESIAN_POINT('Ctrl Pts',(-74.2800432414371,-1.35591109774303,
126.074872082454));
#92101=CARTESIAN_POINT('Ctrl Pts',(-74.2875335771992,-1.48205625659689,
126.112882265999));
#92102=CARTESIAN_POINT('Ctrl Pts',(-74.2950239129613,-1.60628973845464,
126.155810699728));
#92103=CARTESIAN_POINT('Ctrl Pts',(-74.3027983138802,-1.73523467846636,
126.20036716091));
#92104=CARTESIAN_POINT('Ctrl Pts',(-74.3105727147991,-1.86252854432281,
126.25036341917));
#92105=CARTESIAN_POINT('Ctrl Pts',(-74.318347115718,-1.98767816082537,126.305658739082));
#92106=CARTESIAN_POINT('Ctrl Pts',(-74.3261119198117,-2.11267329095542,
126.360885801706));
#92107=CARTESIAN_POINT('Ctrl Pts',(-74.3338767239053,-2.23552908409832,
126.421398754283));
#92108=CARTESIAN_POINT('Ctrl Pts',(-74.341641527999,-2.35576815425472,126.487007323486));
#92109=CARTESIAN_POINT('Ctrl Pts',(-74.3493986044432,-2.4758875606859,126.552550598059));
#92110=CARTESIAN_POINT('Ctrl Pts',(-74.3571556808874,-2.59339508567163,
126.623179211116));
#92111=CARTESIAN_POINT('Ctrl Pts',(-74.3649127573317,-2.70783428016457,
126.698655248976));
#92112=CARTESIAN_POINT('Ctrl Pts',(-74.3726639685936,-2.82218694634474,
126.774074218852));
#92113=CARTESIAN_POINT('Ctrl Pts',(-74.3804151798554,-2.93347557482508,
126.854333103745));
#92114=CARTESIAN_POINT('Ctrl Pts',(-74.3881663911174,-3.04126956814847,
126.939148789431));
#92115=CARTESIAN_POINT('Ctrl Pts',(-74.3959142270513,-3.14901662170038,
127.023927541436));
#92116=CARTESIAN_POINT('Ctrl Pts',(-74.4036620629853,-3.25327176059354,
127.113258905812));
#92117=CARTESIAN_POINT('Ctrl Pts',(-74.4114098989192,-3.35363476659757,
127.206817439956));
#92118=CARTESIAN_POINT('Ctrl Pts',(-74.4191560920303,-3.45397649199642,
127.30035613629));
#92119=CARTESIAN_POINT('Ctrl Pts',(-74.4269022851414,-3.5504274403712,127.39811995302));
#92120=CARTESIAN_POINT('Ctrl Pts',(-74.4346484782525,-3.64262209016361,
127.499744547468));
#92121=CARTESIAN_POINT('Ctrl Pts',(-74.4423947063997,-3.73481715695257,
127.601369601563));
#92122=CARTESIAN_POINT('Ctrl Pts',(-74.4501409345468,-3.82275562414257,
127.70685517861));
#92123=CARTESIAN_POINT('Ctrl Pts',(-74.4578871626939,-3.90611059478766,
127.815801920838));
#92124=CARTESIAN_POINT('Ctrl Pts',(-74.4656351033989,-3.9894839937832,127.924772749317));
#92125=CARTESIAN_POINT('Ctrl Pts',(-74.4733830441038,-4.06827164247307,
128.037205955102));
#92126=CARTESIAN_POINT('Ctrl Pts',(-74.4811309848088,-4.14218875059206,
128.152671454604));
#92127=CARTESIAN_POINT('Ctrl Pts',(-74.4888868507763,-4.21618146750984,
128.268255062187));
#92128=CARTESIAN_POINT('Ctrl Pts',(-74.4966427167438,-4.28529348184605,
128.386876829015));
#92129=CARTESIAN_POINT('Ctrl Pts',(-74.5043985827114,-4.34928469720025,
128.508079779951));
#92130=CARTESIAN_POINT('Ctrl Pts',(-74.5121585793053,-4.41330999305588,
128.629347281267));
#92131=CARTESIAN_POINT('Ctrl Pts',(-74.5199185758991,-4.47220888794963,
128.753198353049));
#92132=CARTESIAN_POINT('Ctrl Pts',(-74.527678572493,-4.52578903711485,128.879155004123));
#92133=CARTESIAN_POINT('Ctrl Pts',(-74.5354502962407,-4.5794501583059,129.005302004896));
#92134=CARTESIAN_POINT('Ctrl Pts',(-74.5432220199882,-4.62777633689152,
129.13356057663));
#92135=CARTESIAN_POINT('Ctrl Pts',(-74.5509937437359,-4.67062455285026,
129.263435782017));
#92136=CARTESIAN_POINT('Ctrl Pts',(-74.5572995065636,-4.70539041640939,
129.368812950451));
#92137=CARTESIAN_POINT('Ctrl Pts',(-74.5636052693913,-4.73655093449785,
129.475254024756));
#92138=CARTESIAN_POINT('Ctrl Pts',(-74.5699110322191,-4.76405452823404,
129.582490119308));
#92139=CARTESIAN_POINT('Origin',(213.235140564004,0.,130.804360617566));
#92140=CARTESIAN_POINT('',(-76.6650346057277,-4.76405452823402,129.582490119308));
#92141=CARTESIAN_POINT('',(-76.3201263474126,-4.76405452823413,129.582490119309));
#92142=CARTESIAN_POINT('',(213.235140564004,-4.76405452823405,129.582490119308));
#92143=CARTESIAN_POINT('',(-74.9851405640369,-4.91824982451843,130.8056744381));
#92144=CARTESIAN_POINT('Ctrl Pts',(-74.9851405640368,-4.91824982451843,
130.8056744381));
#92145=CARTESIAN_POINT('Ctrl Pts',(-74.9934406861383,-4.91821046334308,
130.95302187926));
#92146=CARTESIAN_POINT('Ctrl Pts',(-75.0017408082398,-4.91154523835553,
131.100187303183));
#92147=CARTESIAN_POINT('Ctrl Pts',(-75.0100409303413,-4.8983283466603,131.246585075058));
#92148=CARTESIAN_POINT('Ctrl Pts',(-75.0184356684995,-4.8849607908953,131.394651687431));
#92149=CARTESIAN_POINT('Ctrl Pts',(-75.0268304066577,-4.86489136275868,
131.541932729236));
#92150=CARTESIAN_POINT('Ctrl Pts',(-75.0352251448159,-4.83824912343897,
131.687835847576));
#92151=CARTESIAN_POINT('Ctrl Pts',(-75.0435702033672,-4.81176455145261,
131.832875519143));
#92152=CARTESIAN_POINT('Ctrl Pts',(-75.0519152619184,-4.7787849177952,131.976553268964));
#92153=CARTESIAN_POINT('Ctrl Pts',(-75.0602603204696,-4.73948666356753,
132.118304767203));
#92154=CARTESIAN_POINT('Ctrl Pts',(-75.0686798984314,-4.6998374851705,132.261322072989));
#92155=CARTESIAN_POINT('Ctrl Pts',(-75.0770994763931,-4.65375642235025,
132.402378272524));
#92156=CARTESIAN_POINT('Ctrl Pts',(-75.0855190543548,-4.60147351414362,
132.540915989886));
#92157=CARTESIAN_POINT('Ctrl Pts',(-75.0939386323165,-4.54919060593713,
132.679453707249));
#92158=CARTESIAN_POINT('Ctrl Pts',(-75.1023582102783,-4.49070603386983,
132.815472690386));
#92159=CARTESIAN_POINT('Ctrl Pts',(-75.11077778824,-4.42629631325821,132.948441775017));
#92160=CARTESIAN_POINT('Ctrl Pts',(-75.1185521223595,-4.36682270414599,
133.071220624052));
#92161=CARTESIAN_POINT('Ctrl Pts',(-75.1263264564791,-4.30214246873719,
133.191717507008));
#92162=CARTESIAN_POINT('Ctrl Pts',(-75.1341007905987,-4.23245360039246,
133.309459334788));
#92163=CARTESIAN_POINT('Ctrl Pts',(-75.1418655435463,-4.1628506173495,133.427056056287));
#92164=CARTESIAN_POINT('Ctrl Pts',(-75.1496302964939,-4.08825148041425,
133.541904145143));
#92165=CARTESIAN_POINT('Ctrl Pts',(-75.1573950494414,-4.00890150918022,
133.653552038337));
#92166=CARTESIAN_POINT('Ctrl Pts',(-75.1651520903268,-3.92963034945668,
133.765089041268));
#92167=CARTESIAN_POINT('Ctrl Pts',(-75.1729091312123,-3.84561797067704,
133.873431857237));
#92168=CARTESIAN_POINT('Ctrl Pts',(-75.1806661720977,-3.75715452714677,
133.978155337084));
#92169=CARTESIAN_POINT('Ctrl Pts',(-75.1884173633383,-3.66875779458705,
134.08279984414));
#92170=CARTESIAN_POINT('Ctrl Pts',(-75.1961685545787,-3.5759169296235,134.18383015026));
#92171=CARTESIAN_POINT('Ctrl Pts',(-75.2039197458193,-3.47896391876216,
134.280852112515));
#92172=CARTESIAN_POINT('Ctrl Pts',(-75.2116676425968,-3.38205211551686,
134.377832837847));
#92173=CARTESIAN_POINT('Ctrl Pts',(-75.2194155393744,-3.28103191833573,
134.470808331778));
#92174=CARTESIAN_POINT('Ctrl Pts',(-75.2271634361519,-3.17627376925593,
134.559419605816));
#92175=CARTESIAN_POINT('Ctrl Pts',(-75.2349097122365,-3.07153753332231,
134.648012344286));
#92176=CARTESIAN_POINT('Ctrl Pts',(-75.2426559883209,-2.96306519904072,
134.732242426343));
#92177=CARTESIAN_POINT('Ctrl Pts',(-75.2504022644054,-2.85126174293748,
134.811789910237));
#92178=CARTESIAN_POINT('Ctrl Pts',(-75.2581485976711,-2.73945746152668,
134.891337981333));
#92179=CARTESIAN_POINT('Ctrl Pts',(-75.2658949309369,-2.62432232778905,
134.966203158637));
#92180=CARTESIAN_POINT('Ctrl Pts',(-75.2736412642027,-2.5062915314385,135.036107989744));
#92181=CARTESIAN_POINT('Ctrl Pts',(-75.281389332206,-2.38823430290965,135.106028475554));
#92182=CARTESIAN_POINT('Ctrl Pts',(-75.2891374002094,-2.2672804577293,135.17098620554));
#92183=CARTESIAN_POINT('Ctrl Pts',(-75.2968854682128,-2.14389072851793,
135.23074916882));
#92184=CARTESIAN_POINT('Ctrl Pts',(-75.3046417709551,-2.02036985923383,
135.290575648889));
#92185=CARTESIAN_POINT('Ctrl Pts',(-75.3123980736973,-1.89440828676583,
135.345196162643));
#92186=CARTESIAN_POINT('Ctrl Pts',(-75.3201543764395,-1.76648822759623,
135.394426238476));
#92187=CARTESIAN_POINT('Ctrl Pts',(-75.3279148189541,-1.63849989363911,
135.443682589883));
#92188=CARTESIAN_POINT('Ctrl Pts',(-75.3356752614688,-1.50855136037819,
135.487542645658));
#92189=CARTESIAN_POINT('Ctrl Pts',(-75.3434357039834,-1.37714007798435,
135.525871844717));
#92190=CARTESIAN_POINT('Ctrl Pts',(-75.3512086042492,-1.24551784253424,
135.564262573208));
#92191=CARTESIAN_POINT('Ctrl Pts',(-75.358981504515,-1.11242854542716,135.597104608947));
#92192=CARTESIAN_POINT('Ctrl Pts',(-75.3667544047809,-0.978380783775875,
135.624314362618));
#92193=CARTESIAN_POINT('Ctrl Pts',(-75.3742447405384,-0.849205995991428,
135.650534973188));
#92194=CARTESIAN_POINT('Ctrl Pts',(-75.381735076296,-0.719141523111381,
135.671525638464));
#92195=CARTESIAN_POINT('Ctrl Pts',(-75.3892254120535,-0.588645074301121,
135.687257302834));
#92196=CARTESIAN_POINT('Ctrl Pts',(-75.3969997461725,-0.453200812889957,
135.70358543805));
#92197=CARTESIAN_POINT('Ctrl Pts',(-75.4047740802916,-0.316862125477234,
135.714299632698));
#92198=CARTESIAN_POINT('Ctrl Pts',(-75.4125484144106,-0.180134055567478,
135.719310747987));
#92199=CARTESIAN_POINT('Ctrl Pts',(-75.4203131673577,-0.0435744907845177,
135.724315687524));
#92200=CARTESIAN_POINT('Ctrl Pts',(-75.4280779203047,0.0933731147268622,
135.723631518211));
#92201=CARTESIAN_POINT('Ctrl Pts',(-75.4358426732518,0.230196246977213,
135.717220553528));
#92202=CARTESIAN_POINT('Ctrl Pts',(-75.4435997141367,0.366883484563744,
135.710815956305));
#92203=CARTESIAN_POINT('Ctrl Pts',(-75.4513567550218,0.503446106906145,
135.698695901137));
#92204=CARTESIAN_POINT('Ctrl Pts',(-75.4591137959067,0.639369588484622,
135.680874699553));
#92205=CARTESIAN_POINT('Ctrl Pts',(-75.4668649871469,0.775190569108495,
135.663066937076));
#92206=CARTESIAN_POINT('Ctrl Pts',(-75.474616178387,0.910372982243449,135.639566636256));
#92207=CARTESIAN_POINT('Ctrl Pts',(-75.4823673696271,1.04440577746549,135.610440062862));
#92208=CARTESIAN_POINT('Ctrl Pts',(-75.4901152664042,1.1783816051743,135.581325869039));
#92209=CARTESIAN_POINT('Ctrl Pts',(-75.4978631631813,1.31120840554609,135.546590241636));
#92210=CARTESIAN_POINT('Ctrl Pts',(-75.5056110599584,1.44238391842779,135.506350801984));
#92211=CARTESIAN_POINT('Ctrl Pts',(-75.5133573360425,1.57353199221965,135.466119779555));
#92212=CARTESIAN_POINT('Ctrl Pts',(-75.5211036121266,1.70302909203099,135.420387349419));
#92213=CARTESIAN_POINT('Ctrl Pts',(-75.5288498882107,1.83038714210187,135.369321293468));
#92214=CARTESIAN_POINT('Ctrl Pts',(-75.536596221476,1.95774613230111,135.318254860558));
#92215=CARTESIAN_POINT('Ctrl Pts',(-75.5443425547414,2.08296567837085,135.261854868771));
#92216=CARTESIAN_POINT('Ctrl Pts',(-75.5520888880068,2.2055771210745,135.200337485737));
#92217=CARTESIAN_POINT('Ctrl Pts',(-75.5598369560098,2.32821602176044,135.138806326311));
#92218=CARTESIAN_POINT('Ctrl Pts',(-75.5675850240127,2.44824530747384,135.072155670516));
#92219=CARTESIAN_POINT('Ctrl Pts',(-75.5753330920157,2.5652207436527,135.000647738204));
#92220=CARTESIAN_POINT('Ctrl Pts',(-75.5830893947575,2.68232050271731,134.929063806411));
#92221=CARTESIAN_POINT('Ctrl Pts',(-75.5908456974994,2.79635959457038,134.85261248995));
#92222=CARTESIAN_POINT('Ctrl Pts',(-75.5986020002413,2.9069221682364,134.771599779794));
#92223=CARTESIAN_POINT('Ctrl Pts',(-75.6063624427555,3.01754375247696,134.690543830716));
#92224=CARTESIAN_POINT('Ctrl Pts',(-75.6141228852696,3.12468481597546,134.604921880847));
#92225=CARTESIAN_POINT('Ctrl Pts',(-75.6218833277838,3.22796326471374,134.515079715552));
#92226=CARTESIAN_POINT('Ctrl Pts',(-75.6296562280493,3.33140750518657,134.425093327638));
#92227=CARTESIAN_POINT('Ctrl Pts',(-75.6374291283147,3.43097645596009,134.330873455235));
#92228=CARTESIAN_POINT('Ctrl Pts',(-75.6452020285801,3.52632488181411,134.232802813433));
#92229=CARTESIAN_POINT('Ctrl Pts',(-75.6526923643421,3.61820715221963,134.138297286485));
#92230=CARTESIAN_POINT('Ctrl Pts',(-75.6601827001042,3.70617021805039,134.040216329085));
#92231=CARTESIAN_POINT('Ctrl Pts',(-75.6676730358662,3.78994223101326,133.93892931965));
#92232=CARTESIAN_POINT('Ctrl Pts',(-75.6754473699852,3.87689048530829,133.833801982467));
#92233=CARTESIAN_POINT('Ctrl Pts',(-75.6832217041041,3.95959903151038,133.724887667353));
#92234=CARTESIAN_POINT('Ctrl Pts',(-75.690996038223,4.03771988627897,133.612563100018));
#92235=CARTESIAN_POINT('Ctrl Pts',(-75.6987607911699,4.11574446407592,133.500376962672));
#92236=CARTESIAN_POINT('Ctrl Pts',(-75.7065255441169,4.18919237896562,133.384789253375));
#92237=CARTESIAN_POINT('Ctrl Pts',(-75.7142902970638,4.25775489788121,133.266210794175));
#92238=CARTESIAN_POINT('Ctrl Pts',(-75.7220473379487,4.32624931953645,133.147750108772));
#92239=CARTESIAN_POINT('Ctrl Pts',(-75.7298043788335,4.38986780696952,133.026304921076));
#92240=CARTESIAN_POINT('Ctrl Pts',(-75.7375614197184,4.44834428726299,132.902315851711));
#92241=CARTESIAN_POINT('Ctrl Pts',(-75.7453126109584,4.5067766699877,132.778420283467));
#92242=CARTESIAN_POINT('Ctrl Pts',(-75.7530638021983,4.56007459765794,132.651985004114));
#92243=CARTESIAN_POINT('Ctrl Pts',(-75.7608149934383,4.60801758630512,132.523475793115));
#92244=CARTESIAN_POINT('Ctrl Pts',(-75.7685628902152,4.65594019790314,132.395021201959));
#92245=CARTESIAN_POINT('Ctrl Pts',(-75.7763107869921,4.69851226088147,132.264494797883));
#92246=CARTESIAN_POINT('Ctrl Pts',(-75.784058683769,4.73556124951496,132.13238272378));
#92247=CARTESIAN_POINT('Ctrl Pts',(-75.7918049598529,4.77260248829882,132.000298284674));
#92248=CARTESIAN_POINT('Ctrl Pts',(-75.7995512359368,4.80412284520769,131.866629211492));
#92249=CARTESIAN_POINT('Ctrl Pts',(-75.8072975120208,4.82999966302748,131.731876826402));
#92250=CARTESIAN_POINT('Ctrl Pts',(-75.8150438452859,4.85587667186404,131.597123446602));
#92251=CARTESIAN_POINT('Ctrl Pts',(-75.8227901785511,4.87610998475256,131.461287122887));
#92252=CARTESIAN_POINT('Ctrl Pts',(-75.8305365118163,4.89062814787684,131.324878995431));
#92253=CARTESIAN_POINT('Ctrl Pts',(-75.8382845798191,4.90514956224307,131.18844032032));
#92254=CARTESIAN_POINT('Ctrl Pts',(-75.8460326478219,4.91395323868608,131.051429975356));
#92255=CARTESIAN_POINT('Ctrl Pts',(-75.8537807158247,4.91701967056269,130.914363443891));
#92256=CARTESIAN_POINT('Ctrl Pts',(-75.8615370185664,4.92008936147959,130.777151236486));
#92257=CARTESIAN_POINT('Ctrl Pts',(-75.869293321308,4.9174096184353,130.639883114783));
#92258=CARTESIAN_POINT('Ctrl Pts',(-75.8770496240497,4.90901310269211,130.503074341581));
#92259=CARTESIAN_POINT('Ctrl Pts',(-75.8848100665637,4.90061210547565,130.366192549417));
#92260=CARTESIAN_POINT('Ctrl Pts',(-75.8925705090777,4.8864882960006,130.229770982968));
#92261=CARTESIAN_POINT('Ctrl Pts',(-75.9003309515917,4.86672606213781,130.09431801419));
#92262=CARTESIAN_POINT('Ctrl Pts',(-75.908103851857,4.84693210418281,129.958647604282));
#92263=CARTESIAN_POINT('Ctrl Pts',(-75.9158767521223,4.82148170708765,129.823949283577));
#92264=CARTESIAN_POINT('Ctrl Pts',(-75.9236496523875,4.79051025182633,129.690720375097));
#92265=CARTESIAN_POINT('Ctrl Pts',(-75.9311399881513,4.76066468696842,129.56233467299));
#92266=CARTESIAN_POINT('Ctrl Pts',(-75.9386303239151,4.72569258540207,129.435313701197));
#92267=CARTESIAN_POINT('Ctrl Pts',(-75.9461206596789,4.68575777500824,129.310085831441));
#92268=CARTESIAN_POINT('Ctrl Pts',(-75.953894993798,4.64430882414992,129.180109908971));
#92269=CARTESIAN_POINT('Ctrl Pts',(-75.9616693279171,4.59738211571997,129.05165401892));
#92270=CARTESIAN_POINT('Ctrl Pts',(-75.9694436620362,4.54510650623184,128.925214558977));
#92271=CARTESIAN_POINT('Ctrl Pts',(-75.9772084149834,4.49289532176025,128.798930924368));
#92272=CARTESIAN_POINT('Ctrl Pts',(-75.9849731679306,4.43534850037472,128.674659133153));
#92273=CARTESIAN_POINT('Ctrl Pts',(-75.9927379208778,4.37264480053699,128.552880990557));
#92274=CARTESIAN_POINT('Ctrl Pts',(-76.0004949617629,4.31000337889791,128.431223799729));
#92275=CARTESIAN_POINT('Ctrl Pts',(-76.008252002648,4.24221544940581,128.312055674066));
#92276=CARTESIAN_POINT('Ctrl Pts',(-76.016009043533,4.16950789975838,128.195838634459));
#92277=CARTESIAN_POINT('Ctrl Pts',(-76.0237602347732,4.09685517943981,128.079709235026));
#92278=CARTESIAN_POINT('Ctrl Pts',(-76.0315114260135,4.01929042986386,127.966526822155));
#92279=CARTESIAN_POINT('Ctrl Pts',(-76.0392626172537,3.93708634751327,127.856728660431));
#92280=CARTESIAN_POINT('Ctrl Pts',(-76.0470105140308,3.85491720409044,127.746977165854));
#92281=CARTESIAN_POINT('Ctrl Pts',(-76.054758410808,3.76811288355754,127.640607373877));
#92282=CARTESIAN_POINT('Ctrl Pts',(-76.0625063075852,3.67698913733047,127.538027207387));
#92283=CARTESIAN_POINT('Ctrl Pts',(-76.0702525836694,3.5858844522267,127.435468498456));
#92284=CARTESIAN_POINT('Ctrl Pts',(-76.0779988597536,3.49046239808624,127.33669813038));
#92285=CARTESIAN_POINT('Ctrl Pts',(-76.0857451358378,3.39107845222846,127.242090275027));
#92286=CARTESIAN_POINT('Ctrl Pts',(-76.0934914691032,3.29169377274112,127.1474817213));
#92287=CARTESIAN_POINT('Ctrl Pts',(-76.1012378023685,3.18834742635329,127.057036011175));
#92288=CARTESIAN_POINT('Ctrl Pts',(-76.108984135634,3.08143082723557,126.971089544519));
#92289=CARTESIAN_POINT('Ctrl Pts',(-76.116732203637,2.97449028488692,126.885123830747));
#92290=CARTESIAN_POINT('Ctrl Pts',(-76.1244802716402,2.86397820348854,126.803659610305));
#92291=CARTESIAN_POINT('Ctrl Pts',(-76.1322283396432,2.75031772996819,126.726991926029));
#92292=CARTESIAN_POINT('Ctrl Pts',(-76.1399846423851,2.63653645674385,126.650242758426));
#92293=CARTESIAN_POINT('Ctrl Pts',(-76.147740945127,2.5196004317433,126.578300529403));
#92294=CARTESIAN_POINT('Ctrl Pts',(-76.1554972478689,2.39996081436219,126.511416272245));
#92295=CARTESIAN_POINT('Ctrl Pts',(-76.1632576903832,2.28025734171468,126.444496316944));
#92296=CARTESIAN_POINT('Ctrl Pts',(-76.1710181328975,2.15784775018252,126.382639888916));
#92297=CARTESIAN_POINT('Ctrl Pts',(-76.1787785754117,2.03320536119487,126.326050777715));
#92298=CARTESIAN_POINT('Ctrl Pts',(-76.1865514756772,1.90836288517918,126.269370824648));
#92299=CARTESIAN_POINT('Ctrl Pts',(-76.1943243759428,1.78128081181966,126.217975231988));
#92300=CARTESIAN_POINT('Ctrl Pts',(-76.2020972762083,1.65245072978312,126.172018915129));
#92301=CARTESIAN_POINT('Ctrl Pts',(-76.2095876119696,1.52830394574665,126.127733226149));
#92302=CARTESIAN_POINT('Ctrl Pts',(-76.2170779477308,1.40253432966097,126.088498307759));
#92303=CARTESIAN_POINT('Ctrl Pts',(-76.224568283492,1.27559083576169,126.054407872304));
#92304=CARTESIAN_POINT('Ctrl Pts',(-76.2323426176111,1.14383424069293,126.019024887623));
#92305=CARTESIAN_POINT('Ctrl Pts',(-76.2401169517302,1.01039563017916,125.989072110177));
#92306=CARTESIAN_POINT('Ctrl Pts',(-76.2478912858494,0.875762287746976,
125.964709444407));
#92307=CARTESIAN_POINT('Ctrl Pts',(-76.2556560387965,0.741294868876446,
125.940376803445));
#92308=CARTESIAN_POINT('Ctrl Pts',(-76.2634207917437,0.605636028749181,
125.921620635428));
#92309=CARTESIAN_POINT('Ctrl Pts',(-76.2711855446908,0.469287747062014,
125.908550973293));
#92310=CARTESIAN_POINT('Ctrl Pts',(-76.2789425855759,0.333074888410762,
125.89549429213));
#92311=CARTESIAN_POINT('Ctrl Pts',(-76.2866996264608,0.196174337572018,
125.888112914302));
#92312=CARTESIAN_POINT('Ctrl Pts',(-76.2944566673459,0.0590974441484794,
125.886465686338));
#92313=CARTESIAN_POINT('Ctrl Pts',(-76.3022078585861,-0.077876078523613,
125.884819700562));
#92314=CARTESIAN_POINT('Ctrl Pts',(-76.3099590498262,-0.215025289734102,
125.888899262337));
#92315=CARTESIAN_POINT('Ctrl Pts',(-76.3177102410664,-0.35183490729462,
125.898711296578));
#92316=CARTESIAN_POINT('Ctrl Pts',(-76.3254581378435,-0.488586377117973,
125.908519160443));
#92317=CARTESIAN_POINT('Ctrl Pts',(-76.3332060346206,-0.624998151218251,
125.924054622943));
#92318=CARTESIAN_POINT('Ctrl Pts',(-76.3409539313978,-0.760556361164459,
125.945272525754));
#92319=CARTESIAN_POINT('Ctrl Pts',(-76.3487002074819,-0.896086215255443,
125.966485990237));
#92320=CARTESIAN_POINT('Ctrl Pts',(-76.3564464835661,-1.03076247431502,
125.993379470333));
#92321=CARTESIAN_POINT('Ctrl Pts',(-76.3641927596503,-1.16407819278082,
126.025856141938));
#92322=CARTESIAN_POINT('Ctrl Pts',(-76.3719390929156,-1.29739489535279,
126.058333053279));
#92323=CARTESIAN_POINT('Ctrl Pts',(-76.379685426181,-1.42935065743405,126.096393145834));
#92324=CARTESIAN_POINT('Ctrl Pts',(-76.3874317594463,-1.55945088736836,
126.139888944119));
#92325=CARTESIAN_POINT('Ctrl Pts',(-76.3951798274494,-1.68958025234729,
126.183394482988));
#92326=CARTESIAN_POINT('Ctrl Pts',(-76.4029278954524,-1.81785288759488,
126.23233802591));
#92327=CARTESIAN_POINT('Ctrl Pts',(-76.4106759634554,-1.94379184396714,
126.28652304525));
#92328=CARTESIAN_POINT('Ctrl Pts',(-76.4184322661973,-2.06986464976076,
126.340765653074));
#92329=CARTESIAN_POINT('Ctrl Pts',(-76.4261885689392,-2.1935984623812,126.400260710634));
#92330=CARTESIAN_POINT('Ctrl Pts',(-76.4339448716811,-2.31453821774371,
126.464764334373));
#92331=CARTESIAN_POINT('Ctrl Pts',(-76.4417053141953,-2.43554252229542,
126.529302385638));
#92332=CARTESIAN_POINT('Ctrl Pts',(-76.4494657567095,-2.55374946130381,
126.598854131537));
#92333=CARTESIAN_POINT('Ctrl Pts',(-76.4572261992238,-2.66873173905181,
126.673131506578));
#92334=CARTESIAN_POINT('Ctrl Pts',(-76.4649990994892,-2.78389859655938,
126.747528118254));
#92335=CARTESIAN_POINT('Ctrl Pts',(-76.4727719997547,-2.89583012906565,
126.826665292482));
#92336=CARTESIAN_POINT('Ctrl Pts',(-76.4805449000202,-3.00413028618033,
126.910213177348));
#92337=CARTESIAN_POINT('Ctrl Pts',(-76.4880352357818,-3.10849345978609,
126.99072388615));
#92338=CARTESIAN_POINT('Ctrl Pts',(-76.4955255715434,-3.2094844574116,127.075329994392));
#92339=CARTESIAN_POINT('Ctrl Pts',(-76.5030159073051,-3.30678176547625,
127.163704437972));
#92340=CARTESIAN_POINT('Ctrl Pts',(-76.5106725118287,-3.40623885695652,
127.254040597261));
#92341=CARTESIAN_POINT('Ctrl Pts',(-76.5183291163523,-3.50217156810879,
127.348619192693));
#92342=CARTESIAN_POINT('Ctrl Pts',(-76.5259857208759,-3.59418792836113,
127.447130181906));
#92343=CARTESIAN_POINT('Ctrl Pts',(-76.5336334799343,-3.68609798463603,
127.545527364074));
#92344=CARTESIAN_POINT('Ctrl Pts',(-76.5412812389926,-3.77410041135327,
127.647847617771));
#92345=CARTESIAN_POINT('Ctrl Pts',(-76.548928998051,-3.85783661147684,127.753741050716));
#92346=CARTESIAN_POINT('Ctrl Pts',(-76.5565696961159,-3.94149549996518,
127.859536714781));
#92347=CARTESIAN_POINT('Ctrl Pts',(-76.5642103941809,-4.02089574503894,
127.968898684209));
#92348=CARTESIAN_POINT('Ctrl Pts',(-76.5718510922459,-4.09571631903511,
128.081441063762));
#92349=CARTESIAN_POINT('Ctrl Pts',(-76.5796163850361,-4.17175697119375,
128.195818640404));
#92350=CARTESIAN_POINT('Ctrl Pts',(-76.5873816778263,-4.24306698472555,
128.313480961797));
#92351=CARTESIAN_POINT('Ctrl Pts',(-76.5951469706164,-4.30935250625322,
128.433988486581));
#92352=CARTESIAN_POINT('Ctrl Pts',(-76.602779193841,-4.37450212913653,128.552430939977));
#92353=CARTESIAN_POINT('Ctrl Pts',(-76.6104114170654,-4.4347978936474,128.673621490505));
#92354=CARTESIAN_POINT('Ctrl Pts',(-76.61804364029,-4.4900053734628,128.797115039971));
#92355=CARTESIAN_POINT('Ctrl Pts',(-76.625875467863,-4.54665668592162,128.923838297052));
#92356=CARTESIAN_POINT('Ctrl Pts',(-76.633707295436,-4.59794967749869,129.052986292388));
#92357=CARTESIAN_POINT('Ctrl Pts',(-76.6415391230089,-4.64368268703469,
129.184053805683));
#92358=CARTESIAN_POINT('Ctrl Pts',(-76.6493709505819,-4.68941569657056,
129.315121318978));
#92359=CARTESIAN_POINT('Ctrl Pts',(-76.6572027781548,-4.72958858089092,
129.448107913711));
#92360=CARTESIAN_POINT('Ctrl Pts',(-76.6650346057277,-4.76405452823403,
129.582490119308));
#92361=CARTESIAN_POINT('Ctrl Pts',(-74.915389332428,-4.7640545282341,129.582490119308));
#92362=CARTESIAN_POINT('Ctrl Pts',(-74.9233682696944,-4.79910898964202,
129.719166932312));
#92363=CARTESIAN_POINT('Ctrl Pts',(-74.9313472069608,-4.82830796905041,
129.857471997866));
#92364=CARTESIAN_POINT('Ctrl Pts',(-74.9393261442272,-4.85151083619154,
129.996879553506));
#92365=CARTESIAN_POINT('Ctrl Pts',(-74.9472967331157,-4.87468942612653,
130.136141246742));
#92366=CARTESIAN_POINT('Ctrl Pts',(-74.9552673220041,-4.89188435059366,
130.276502779105));
#92367=CARTESIAN_POINT('Ctrl Pts',(-74.9632379108926,-4.9030057590873,130.417427045933));
#92368=CARTESIAN_POINT('Ctrl Pts',(-74.9705387952646,-4.91319272501936,
130.546510579372));
#92369=CARTESIAN_POINT('Ctrl Pts',(-74.9778396796365,-4.918284447055,130.67606590687));
#92370=CARTESIAN_POINT('Ctrl Pts',(-74.9851405640085,-4.91824982451857,
130.805674437596));
#92371=CARTESIAN_POINT('',(-74.6398594359583,-4.91824789637572,130.799811739049));
#92372=CARTESIAN_POINT('Ctrl Pts',(-74.5699110322191,-4.76405452823404,
129.582490119308));
#92373=CARTESIAN_POINT('Ctrl Pts',(-74.5710978670709,-4.76923109837905,
129.602673487738));
#92374=CARTESIAN_POINT('Ctrl Pts',(-74.5722847019227,-4.77427818705792,
129.622885011757));
#92375=CARTESIAN_POINT('Ctrl Pts',(-74.5734715367745,-4.77919553909627,
129.643122889285));
#92376=CARTESIAN_POINT('Ctrl Pts',(-74.5838863897011,-4.82234686566057,
129.820716694929));
#92377=CARTESIAN_POINT('Ctrl Pts',(-74.5943012426276,-4.85561496466627,
130.000798665939));
#92378=CARTESIAN_POINT('Ctrl Pts',(-74.6047160955543,-4.87876862660314,
130.182428345873));
#92379=CARTESIAN_POINT('Ctrl Pts',(-74.6148654039255,-4.90133194617918,
130.3594270653));
#92380=CARTESIAN_POINT('Ctrl Pts',(-74.6250147122967,-4.91429008969093,
130.537895936914));
#92381=CARTESIAN_POINT('Ctrl Pts',(-74.6351640206679,-4.91747302611252,
130.716941512356));
#92382=CARTESIAN_POINT('Ctrl Pts',(-74.6367291590981,-4.91796387099888,
130.744552370221));
#92383=CARTESIAN_POINT('Ctrl Pts',(-74.6382942975283,-4.91822233695506,
130.77217689094));
#92384=CARTESIAN_POINT('Ctrl Pts',(-74.6398594359584,-4.91824789637572,
130.799811739049));
#92385=CARTESIAN_POINT('Ctrl Pts',(-74.639859435991,-4.91824789637626,130.799811739625));
#92386=CARTESIAN_POINT('Ctrl Pts',(-74.647518742692,-4.91837297631381,130.935048197454));
#92387=CARTESIAN_POINT('Ctrl Pts',(-74.6551780493929,-4.91291599175694,
131.070438329716));
#92388=CARTESIAN_POINT('Ctrl Pts',(-74.6628373560939,-4.90186575537136,
131.205478030324));
#92389=CARTESIAN_POINT('Ctrl Pts',(-74.6707157646144,-4.89049941636793,
131.344380671179));
#92390=CARTESIAN_POINT('Ctrl Pts',(-74.678594173135,-4.87321496953365,131.482912101015));
#92391=CARTESIAN_POINT('Ctrl Pts',(-74.6864725816555,-4.85005783070138,
131.620523653578));
#92392=CARTESIAN_POINT('Ctrl Pts',(-74.6941240345815,-4.82756778627012,
131.754170990316));
#92393=CARTESIAN_POINT('Ctrl Pts',(-74.7017754875075,-4.79953883076809,
131.886950297796));
#92394=CARTESIAN_POINT('Ctrl Pts',(-74.7094269404335,-4.76606506433638,
132.018365092439));
#92395=CARTESIAN_POINT('Ctrl Pts',(-74.7170774793527,-4.73259529652388,
132.149764188888));
#92396=CARTESIAN_POINT('Ctrl Pts',(-74.724728018272,-4.69368211011505,132.279798707484));
#92397=CARTESIAN_POINT('Ctrl Pts',(-74.7323785571913,-4.64947028911381,
132.407984355588));
#92398=CARTESIAN_POINT('Ctrl Pts',(-74.7400299369695,-4.60525360885936,
132.536184092379));
#92399=CARTESIAN_POINT('Ctrl Pts',(-74.7476813167477,-4.55573726714946,
132.662534175001));
#92400=CARTESIAN_POINT('Ctrl Pts',(-74.7553326965259,-4.5011151071118,132.786567936448));
#92401=CARTESIAN_POINT('Ctrl Pts',(-74.763381568531,-4.44365530410517,132.917045301203));
#92402=CARTESIAN_POINT('Ctrl Pts',(-74.7714304405361,-4.38054516848821,
133.044958770821));
#92403=CARTESIAN_POINT('Ctrl Pts',(-74.7794793125412,-4.31206593385308,
133.169793018757));
#92404=CARTESIAN_POINT('Ctrl Pts',(-74.7871418965388,-4.24687321030787,
133.288636119998));
#92405=CARTESIAN_POINT('Ctrl Pts',(-74.7948044805363,-4.17681500123564,
133.404688359622));
#92406=CARTESIAN_POINT('Ctrl Pts',(-74.8024670645338,-4.10217867923782,
133.517534616061));
#92407=CARTESIAN_POINT('Ctrl Pts',(-74.810134790174,-4.02749227579267,133.630456593056));
#92408=CARTESIAN_POINT('Ctrl Pts',(-74.8178025158143,-3.94822187912135,
133.74016798076));
#92409=CARTESIAN_POINT('Ctrl Pts',(-74.8254702414545,-3.86469534440186,
133.846286480808));
#92410=CARTESIAN_POINT('Ctrl Pts',(-74.8331485005768,-3.78105406571581,
133.952550760369));
#92411=CARTESIAN_POINT('Ctrl Pts',(-74.840826759699,-3.69314524463562,134.055212002915));
#92412=CARTESIAN_POINT('Ctrl Pts',(-74.8485050188213,-3.60133386345812,
134.153924390121));
#92413=CARTESIAN_POINT('Ctrl Pts',(-74.8496430660766,-3.58772587124415,
134.168555227597));
#92414=CARTESIAN_POINT('Ctrl Pts',(-74.8507811133319,-3.57403220584152,
134.183099387927));
#92415=CARTESIAN_POINT('Ctrl Pts',(-74.8519191605872,-3.56025411598836,
134.197555821513));
#92416=CARTESIAN_POINT('Ctrl Pts',(-74.8596934947062,-3.46613194879049,
134.296311953427));
#92417=CARTESIAN_POINT('Ctrl Pts',(-74.8674678288253,-3.367748563397,134.391305327569));
#92418=CARTESIAN_POINT('Ctrl Pts',(-74.8752421629444,-3.26543694881502,
134.482145901648));
#92419=CARTESIAN_POINT('Ctrl Pts',(-74.8830069158914,-3.16325142415417,
134.57287452284));
#92420=CARTESIAN_POINT('Ctrl Pts',(-74.8907716688385,-3.05714759238342,
134.659460270087));
#92421=CARTESIAN_POINT('Ctrl Pts',(-74.8985364217855,-2.9474969359988,134.741548049576));
#92422=CARTESIAN_POINT('Ctrl Pts',(-74.9062934626705,-2.8379551861919,134.823554298325));
#92423=CARTESIAN_POINT('Ctrl Pts',(-74.9140505035554,-2.72487393316754,
134.901071236943));
#92424=CARTESIAN_POINT('Ctrl Pts',(-74.9218075444404,-2.60865928796078,
134.973782613699));
#92425=CARTESIAN_POINT('Ctrl Pts',(-74.9295587356805,-2.49253228112216,
135.04643915824));
#92426=CARTESIAN_POINT('Ctrl Pts',(-74.9373099269205,-2.37327691543874,
135.114297147565));
#92427=CARTESIAN_POINT('Ctrl Pts',(-74.9450611181606,-2.25132966914383,
135.17708262832));
#92428=CARTESIAN_POINT('Ctrl Pts',(-74.9528090149377,-2.12943425368182,
135.239841423571));
#92429=CARTESIAN_POINT('Ctrl Pts',(-74.9605569117147,-2.00484958004986,
135.297531819686));
#92430=CARTESIAN_POINT('Ctrl Pts',(-74.9683048084917,-1.87803801166946,
135.349925080779));
#92431=CARTESIAN_POINT('Ctrl Pts',(-74.9760510845758,-1.75125296953507,
135.402307382332));
#92432=CARTESIAN_POINT('Ctrl Pts',(-74.9837973606599,-1.62224232030099,
135.449394603632));
#92433=CARTESIAN_POINT('Ctrl Pts',(-74.991543636744,-1.49148939032738,135.491005735456));
#92434=CARTESIAN_POINT('Ctrl Pts',(-74.9992899700093,-1.36073549516517,
135.532617174443));
#92435=CARTESIAN_POINT('Ctrl Pts',(-75.0070363032746,-1.22823966615429,
135.568752324729));
#92436=CARTESIAN_POINT('Ctrl Pts',(-75.01478263654,-1.09450102650723,135.599279862504));
#92437=CARTESIAN_POINT('Ctrl Pts',(-75.0225307045429,-0.960732437019272,
135.629814236709));
#92438=CARTESIAN_POINT('Ctrl Pts',(-75.0302787725459,-0.825720864161248,
135.654738412547));
#92439=CARTESIAN_POINT('Ctrl Pts',(-75.0380268405489,-0.68997587934256,
135.673972136817));
#92440=CARTESIAN_POINT('Ctrl Pts',(-75.0457831432907,-0.554086623138806,
135.693226302919));
#92441=CARTESIAN_POINT('Ctrl Pts',(-75.0535394460325,-0.417462785597245,
135.706777881227));
#92442=CARTESIAN_POINT('Ctrl Pts',(-75.0612957487743,-0.280619880601453,
135.714598447357));
#92443=CARTESIAN_POINT('Ctrl Pts',(-75.0690561912885,-0.14370393842663,
135.722423187559));
#92444=CARTESIAN_POINT('Ctrl Pts',(-75.0768166338027,-0.00656908654743849,
135.724510814688));
#92445=CARTESIAN_POINT('Ctrl Pts',(-75.0845770763168,0.130269894400301,
135.720885082787));
#92446=CARTESIAN_POINT('Ctrl Pts',(-75.0923499765822,0.26732854142788,135.717253530538));
#92447=CARTESIAN_POINT('Ctrl Pts',(-75.1001228768476,0.404089978129397,
135.707890318218));
#92448=CARTESIAN_POINT('Ctrl Pts',(-75.107895777113,0.540044372735581,135.692871141026));
#92449=CARTESIAN_POINT('Ctrl Pts',(-75.1153861128753,0.671056482655628,
135.678397948755));
#92450=CARTESIAN_POINT('Ctrl Pts',(-75.1228764486377,0.801318903257601,
135.658672915536));
#92451=CARTESIAN_POINT('Ctrl Pts',(-75.1303667844,0.930386911627887,135.633808128117));
#92452=CARTESIAN_POINT('Ctrl Pts',(-75.1381411185191,1.06434857275906,135.608000584728));
#92453=CARTESIAN_POINT('Ctrl Pts',(-75.1459154526382,1.19744781172977,135.576574095299));
#92454=CARTESIAN_POINT('Ctrl Pts',(-75.1536897867573,1.32917648622411,135.539597985531));
#92455=CARTESIAN_POINT('Ctrl Pts',(-75.1614545397044,1.46074281690008,135.502667445512));
#92456=CARTESIAN_POINT('Ctrl Pts',(-75.1692192926515,1.59094157109824,135.460200998189));
#92457=CARTESIAN_POINT('Ctrl Pts',(-75.1769840455986,1.71927320297116,135.412319245423));
#92458=CARTESIAN_POINT('Ctrl Pts',(-75.1847410864836,1.84747737405814,135.36448504949));
#92459=CARTESIAN_POINT('Ctrl Pts',(-75.1924981273685,1.97381774933448,135.311246387472));
#92460=CARTESIAN_POINT('Ctrl Pts',(-75.2002551682535,2.09780874432766,135.2527739903));
#92461=CARTESIAN_POINT('Ctrl Pts',(-75.2080063594936,2.22170623674717,135.194345687618));
#92462=CARTESIAN_POINT('Ctrl Pts',(-75.2157575507338,2.34325752313116,135.130691671734));
#92463=CARTESIAN_POINT('Ctrl Pts',(-75.223508741974,2.46199619161785,135.062031085669));
#92464=CARTESIAN_POINT('Ctrl Pts',(-75.231256638751,2.58068439300282,134.993399682185));
#92465=CARTESIAN_POINT('Ctrl Pts',(-75.2390045355282,2.69656201637946,134.919766136103));
#92466=CARTESIAN_POINT('Ctrl Pts',(-75.2467524323052,2.80918670104647,134.841395809531));
#92467=CARTESIAN_POINT('Ctrl Pts',(-75.2544987083893,2.92178782705705,134.763041876342));
#92468=CARTESIAN_POINT('Ctrl Pts',(-75.2622449844732,3.03113704708802,134.679953356652));
#92469=CARTESIAN_POINT('Ctrl Pts',(-75.2699912605573,3.13682082324802,134.592439046709));
#92470=CARTESIAN_POINT('Ctrl Pts',(-75.2777375938226,3.2425053795415,134.504924090755));
#92471=CARTESIAN_POINT('Ctrl Pts',(-75.285483927088,3.34452413684802,134.412983528711));
#92472=CARTESIAN_POINT('Ctrl Pts',(-75.2932302603533,3.44249682043959,134.316966303344));
#92473=CARTESIAN_POINT('Ctrl Pts',(-75.3009783283563,3.54049144433476,134.220927575586));
#92474=CARTESIAN_POINT('Ctrl Pts',(-75.3087263963593,3.6344379123272,134.120810641461));
#92475=CARTESIAN_POINT('Ctrl Pts',(-75.3164744643623,3.72399326933371,134.017000839013));
#92476=CARTESIAN_POINT('Ctrl Pts',(-75.3242307671041,3.81364380683923,133.913080706271));
#92477=CARTESIAN_POINT('Ctrl Pts',(-75.3319870698459,3.8988936548846,133.80546016145));
#92478=CARTESIAN_POINT('Ctrl Pts',(-75.3397433725878,3.97944025138362,133.694557556906));
#92479=CARTESIAN_POINT('Ctrl Pts',(-75.3475038151019,4.06002983802662,133.583595760301));
#92480=CARTESIAN_POINT('Ctrl Pts',(-75.3552642576161,4.13591095500109,133.469348739011));
#92481=CARTESIAN_POINT('Ctrl Pts',(-75.3630247001303,4.20682533574648,133.352262432201));
#92482=CARTESIAN_POINT('Ctrl Pts',(-75.3707976003957,4.27785355455113,133.234988168058));
#92483=CARTESIAN_POINT('Ctrl Pts',(-75.3785705006611,4.34389891596651,133.114865853107));
#92484=CARTESIAN_POINT('Ctrl Pts',(-75.3863434009265,4.40474952798511,132.99236533836));
#92485=CARTESIAN_POINT('Ctrl Pts',(-75.3938337366886,4.46338806698439,132.874318025882));
#92486=CARTESIAN_POINT('Ctrl Pts',(-75.4013240724508,4.5172028580651,132.754062699943));
#92487=CARTESIAN_POINT('Ctrl Pts',(-75.4088144082129,4.56604781938688,132.632034104153));
#92488=CARTESIAN_POINT('Ctrl Pts',(-75.416588742332,4.61674475226264,132.505378757065));
#92489=CARTESIAN_POINT('Ctrl Pts',(-75.424363076451,4.66224814645558,132.376411812581));
#92490=CARTESIAN_POINT('Ctrl Pts',(-75.4321374105701,4.70234166430523,132.245598257457));
#92491=CARTESIAN_POINT('Ctrl Pts',(-75.4399021635172,4.74238577047718,132.114945918349));
#92492=CARTESIAN_POINT('Ctrl Pts',(-75.4476669164643,4.77703315255691,131.982451866943));
#92493=CARTESIAN_POINT('Ctrl Pts',(-75.4554316694114,4.80611525957518,131.848601573562));
#92494=CARTESIAN_POINT('Ctrl Pts',(-75.4631887102964,4.83516848183493,131.714884222178));
#92495=CARTESIAN_POINT('Ctrl Pts',(-75.4709457511815,4.85866734655437,131.579813689065));
#92496=CARTESIAN_POINT('Ctrl Pts',(-75.4787027920665,4.87649302423167,131.44389079443));
#92497=CARTESIAN_POINT('Ctrl Pts',(-75.4864539833067,4.8943052594268,131.308070400307));
#92498=CARTESIAN_POINT('Ctrl Pts',(-75.4942051745467,4.90645277243412,131.17139931014));
#92499=CARTESIAN_POINT('Ctrl Pts',(-75.5019563657869,4.91286782747891,131.034388381592));
#92500=CARTESIAN_POINT('Ctrl Pts',(-75.509704262564,4.91928015595417,130.897435686343));
#92501=CARTESIAN_POINT('Ctrl Pts',(-75.5174521593412,4.91996485412807,130.760143829714));
#92502=CARTESIAN_POINT('Ctrl Pts',(-75.5252000561183,4.91490607189348,130.623028416993));
#92503=CARTESIAN_POINT('Ctrl Pts',(-75.5329463322024,4.90984834784707,130.48594168586));
#92504=CARTESIAN_POINT('Ctrl Pts',(-75.5406926082865,4.89904954747252,130.349031715674));
#92505=CARTESIAN_POINT('Ctrl Pts',(-75.5484388843706,4.88254594246699,130.21281333949));
#92506=CARTESIAN_POINT('Ctrl Pts',(-75.556185217636,4.86604221563561,130.076593957773));
#92507=CARTESIAN_POINT('Ctrl Pts',(-75.5639315509014,4.84383364716639,129.941066568371));
#92508=CARTESIAN_POINT('Ctrl Pts',(-75.5716778841667,4.8160082647134,129.806739719272));
#92509=CARTESIAN_POINT('Ctrl Pts',(-75.5794259521697,4.78817665095897,129.672382788608));
#92510=CARTESIAN_POINT('Ctrl Pts',(-75.5871740201726,4.75472579954021,129.539227315997));
#92511=CARTESIAN_POINT('Ctrl Pts',(-75.5949220881756,4.71579453066731,129.407770123889));
#92512=CARTESIAN_POINT('Ctrl Pts',(-75.6026783909175,4.6768218851784,129.276173217513));
#92513=CARTESIAN_POINT('Ctrl Pts',(-75.6104346936593,4.63235729805957,129.146278572697));
#92514=CARTESIAN_POINT('Ctrl Pts',(-75.6181909964012,4.58258919879826,129.018566873161));
#92515=CARTESIAN_POINT('Ctrl Pts',(-75.6259514389154,4.53279453680388,128.890787010045));
#92516=CARTESIAN_POINT('Ctrl Pts',(-75.6337118814296,4.4776908793719,128.765192771623));
#92517=CARTESIAN_POINT('Ctrl Pts',(-75.6414723239438,4.41751380836918,128.642242485879));
#92518=CARTESIAN_POINT('Ctrl Pts',(-75.6492452242093,4.35724013578982,128.519094829422));
#92519=CARTESIAN_POINT('Ctrl Pts',(-75.6570181244747,4.29187696127257,128.39859995098));
#92520=CARTESIAN_POINT('Ctrl Pts',(-75.6647910247401,4.2217050509751,128.281190087247));
#92521=CARTESIAN_POINT('Ctrl Pts',(-75.672281360502,4.15408406637082,128.168048367801));
#92522=CARTESIAN_POINT('Ctrl Pts',(-75.6797716962639,4.08199806393175,128.057771518885));
#92523=CARTESIAN_POINT('Ctrl Pts',(-75.6872620320258,4.00573384496549,127.950717432829));
#92524=CARTESIAN_POINT('Ctrl Pts',(-75.6950363661449,3.92657804495567,127.839604358559));
#92525=CARTESIAN_POINT('Ctrl Pts',(-75.702810700264,3.84267019807177,127.731611280616));
#92526=CARTESIAN_POINT('Ctrl Pts',(-75.7105850343831,3.75428457505002,127.627171546698));
#92527=CARTESIAN_POINT('Ctrl Pts',(-75.7183497873301,3.6660078794094,127.522860525419));
#92528=CARTESIAN_POINT('Ctrl Pts',(-75.7261145402773,3.57326463785824,127.422094430478));
#92529=CARTESIAN_POINT('Ctrl Pts',(-75.7338792932244,3.47637218441209,127.325277477147));
#92530=CARTESIAN_POINT('Ctrl Pts',(-75.7416363341094,3.37957596591663,127.228556683779));
#92531=CARTESIAN_POINT('Ctrl Pts',(-75.7493933749943,3.27863901138534,127.13577750094));
#92532=CARTESIAN_POINT('Ctrl Pts',(-75.7571504158793,3.17391844479411,127.04731060881));
#92533=CARTESIAN_POINT('Ctrl Pts',(-75.7649016071194,3.06927684879631,126.95891043025));
#92534=CARTESIAN_POINT('Ctrl Pts',(-75.7726527983595,2.96085761741198,126.874816320909));
#92535=CARTESIAN_POINT('Ctrl Pts',(-75.7804039895996,2.84905393682134,126.795361399858));
#92536=CARTESIAN_POINT('Ctrl Pts',(-75.7881518863767,2.73729777577787,126.715940249268));
#92537=CARTESIAN_POINT('Ctrl Pts',(-75.7958997831539,2.62216034457671,126.641154591255));
#92538=CARTESIAN_POINT('Ctrl Pts',(-75.8036476799309,2.504066869179,126.571296458215));
#92539=CARTESIAN_POINT('Ctrl Pts',(-75.811393956015,2.38599809639087,126.501452937991));
#92540=CARTESIAN_POINT('Ctrl Pts',(-75.819140232099,2.26497484560452,126.436535091487));
#92541=CARTESIAN_POINT('Ctrl Pts',(-75.8268865081831,2.14144986618793,126.376790682138));
#92542=CARTESIAN_POINT('Ctrl Pts',(-75.8346328414484,2.01792397493783,126.31704583177));
#92543=CARTESIAN_POINT('Ctrl Pts',(-75.8423791747138,1.89189667016723,126.26247466499));
#92544=CARTESIAN_POINT('Ctrl Pts',(-75.8501255079791,1.76384338879855,126.21327800425));
#92545=CARTESIAN_POINT('Ctrl Pts',(-75.8578735759821,1.63576143078589,126.164070326259));
#92546=CARTESIAN_POINT('Ctrl Pts',(-75.8656216439849,1.50565295824583,126.120239689486));
#92547=CARTESIAN_POINT('Ctrl Pts',(-75.8733697119879,1.37401099769051,126.081937845225));
#92548=CARTESIAN_POINT('Ctrl Pts',(-75.8811260147297,1.24222912649241,126.043595293308));
#92549=CARTESIAN_POINT('Ctrl Pts',(-75.8888823174716,1.10891088755632,126.010793381377));
#92550=CARTESIAN_POINT('Ctrl Pts',(-75.8966386202135,0.974562544449634,
125.98363339966));
#92551=CARTESIAN_POINT('Ctrl Pts',(-75.9043990627276,0.840142495586718,
125.956458921843));
#92552=CARTESIAN_POINT('Ctrl Pts',(-75.9121595052417,0.704691632965476,
125.93493243578));
#92553=CARTESIAN_POINT('Ctrl Pts',(-75.9199199477559,0.568722898653324,
125.919103477246));
#92554=CARTESIAN_POINT('Ctrl Pts',(-75.9276928480213,0.432535895258117,
125.903249108662));
#92555=CARTESIAN_POINT('Ctrl Pts',(-75.9354657482868,0.295829749021376,
125.893110573515));
#92556=CARTESIAN_POINT('Ctrl Pts',(-75.9432386485522,0.15911987388323,125.888685289777));
#92557=CARTESIAN_POINT('Ctrl Pts',(-75.9507289843144,0.0273797470562648,
125.884420876249));
#92558=CARTESIAN_POINT('Ctrl Pts',(-75.9582193200764,-0.104363534260139,
125.885461541182));
#92559=CARTESIAN_POINT('Ctrl Pts',(-75.9657096558385,-0.23565384200104,
125.891759440058));
#92560=CARTESIAN_POINT('Ctrl Pts',(-75.9734839899576,-0.37192206166341,
125.898296125685));
#92561=CARTESIAN_POINT('Ctrl Pts',(-75.9812583240767,-0.508133937464272,
125.910517277156));
#92562=CARTESIAN_POINT('Ctrl Pts',(-75.9890326581958,-0.643776631678409,
125.928426377751));
#92563=CARTESIAN_POINT('Ctrl Pts',(-75.9967974111429,-0.779252158393926,
125.946313406979));
#92564=CARTESIAN_POINT('Ctrl Pts',(-76.0045621640899,-0.914159515349397,
125.969874387057));
#92565=CARTESIAN_POINT('Ctrl Pts',(-76.012326917037,-1.04798709800216,125.999060824117));
#92566=CARTESIAN_POINT('Ctrl Pts',(-76.020083957922,-1.18168176121428,126.028218272797));
#92567=CARTESIAN_POINT('Ctrl Pts',(-76.0278409988071,-1.31429840482707,
126.062989976745));
#92568=CARTESIAN_POINT('Ctrl Pts',(-76.0355980396921,-1.44533213087425,
126.103275839139));
#92569=CARTESIAN_POINT('Ctrl Pts',(-76.0433492309323,-1.57626704336844,
126.14353132165));
#92570=CARTESIAN_POINT('Ctrl Pts',(-76.0511004221724,-1.70562104207544,
126.189292571394));
#92571=CARTESIAN_POINT('Ctrl Pts',(-76.0588516134125,-1.8329013377515,126.240408848696));
#92572=CARTESIAN_POINT('Ctrl Pts',(-76.0665995101897,-1.96012753590745,
126.291503400218));
#92573=CARTESIAN_POINT('Ctrl Pts',(-76.0743474069668,-2.08528142198677,
126.347948307052));
#92574=CARTESIAN_POINT('Ctrl Pts',(-76.0820953037439,-2.20788745584483,
126.409543665198));
#92575=CARTESIAN_POINT('Ctrl Pts',(-76.089841579828,-2.33046784316369,126.471126138922));
#92576=CARTESIAN_POINT('Ctrl Pts',(-76.0975878559121,-2.45050108920477,
126.537856745624));
#92577=CARTESIAN_POINT('Ctrl Pts',(-76.1053341319962,-2.56753402148043,
126.609488496626));
#92578=CARTESIAN_POINT('Ctrl Pts',(-76.1130804652616,-2.68456781766612,
126.681120776397));
#92579=CARTESIAN_POINT('Ctrl Pts',(-76.1208267985271,-2.79860092243051,
126.75765406856));
#92580=CARTESIAN_POINT('Ctrl Pts',(-76.1285731317924,-2.9092073928881,126.838796924008));
#92581=CARTESIAN_POINT('Ctrl Pts',(-76.1363211997954,-3.01983863289801,
126.919957950836));
#92582=CARTESIAN_POINT('Ctrl Pts',(-76.1440692677984,-3.12704139644846,
127.005730363849));
#92583=CARTESIAN_POINT('Ctrl Pts',(-76.1518173358014,-3.23042151800431,
127.095781391162));
#92584=CARTESIAN_POINT('Ctrl Pts',(-76.1595736385433,-3.33391151318373,
127.185928125778));
#92585=CARTESIAN_POINT('Ctrl Pts',(-76.1673299412852,-3.43357045531373,
127.280362301335));
#92586=CARTESIAN_POINT('Ctrl Pts',(-76.1750862440271,-3.52903947823306,
127.378712733797));
#92587=CARTESIAN_POINT('Ctrl Pts',(-76.1828466865413,-3.62455945584444,
127.477115658846));
#92588=CARTESIAN_POINT('Ctrl Pts',(-76.1906071290555,-3.71588479804903,
127.579438714207));
#92589=CARTESIAN_POINT('Ctrl Pts',(-76.1983675715697,-3.80269657128017,
127.685277122487));
#92590=CARTESIAN_POINT('Ctrl Pts',(-76.2061404718352,-3.8896477024765,127.791285431976));
#92591=CARTESIAN_POINT('Ctrl Pts',(-76.2139133721006,-3.97207055050816,
127.900820058631));
#92592=CARTESIAN_POINT('Ctrl Pts',(-76.221686272366,-4.04968869388416,128.013445974456));
#92593=CARTESIAN_POINT('Ctrl Pts',(-76.2291766081279,-4.12448522223826,
128.12197765455));
#92594=CARTESIAN_POINT('Ctrl Pts',(-76.2366669438898,-4.19482014291475,
128.233379513098));
#92595=CARTESIAN_POINT('Ctrl Pts',(-76.2441572796517,-4.26048716050001,
128.347241935509));
#92596=CARTESIAN_POINT('Ctrl Pts',(-76.2522516915477,-4.33145005258056,
128.470287066698));
#92597=CARTESIAN_POINT('Ctrl Pts',(-76.2603461034436,-4.39717110738405,
128.596568562782));
#92598=CARTESIAN_POINT('Ctrl Pts',(-76.2684405153396,-4.4573557375553,128.725619919118));
#92599=CARTESIAN_POINT('Ctrl Pts',(-76.2765234352285,-4.51745492085225,
128.854488055337));
#92600=CARTESIAN_POINT('Ctrl Pts',(-76.2846063551175,-4.57203318722553,
128.986117909908));
#92601=CARTESIAN_POINT('Ctrl Pts',(-76.2926892750064,-4.62084055069108,
129.120016333404));
#92602=CARTESIAN_POINT('Ctrl Pts',(-76.3007586197631,-4.66956594298494,
129.25368987668));
#92603=CARTESIAN_POINT('Ctrl Pts',(-76.3088279645198,-4.71253963181309,
129.389624072026));
#92604=CARTESIAN_POINT('Ctrl Pts',(-76.3168973092765,-4.7495588931892,129.527304086857));
#92605=CARTESIAN_POINT('Ctrl Pts',(-76.3179736553219,-4.75449678304108,
129.545668817075));
#92606=CARTESIAN_POINT('Ctrl Pts',(-76.3190500013673,-4.75932880030024,
129.564064577817));
#92607=CARTESIAN_POINT('Ctrl Pts',(-76.3201263474126,-4.76405452823413,
129.582490119309));
#92608=CARTESIAN_POINT('Origin',(213.235140564004,0.,130.804360617566));
#92609=CARTESIAN_POINT('',(-78.4150662180022,-4.76405452823401,129.582490119308));
#92610=CARTESIAN_POINT('',(-78.0697779892986,-4.76405452823406,129.582490119308));
#92611=CARTESIAN_POINT('',(213.235140564004,-4.76405452823405,129.582490119308));
#92612=CARTESIAN_POINT('',(-76.7351405639554,-4.9182483336571,130.808409194994));
#92613=CARTESIAN_POINT('Ctrl Pts',(-76.7351405640085,-4.91824833365633,
130.808409195929));
#92614=CARTESIAN_POINT('Ctrl Pts',(-76.74751275176,-4.91806897685328,131.026293405774));
#92615=CARTESIAN_POINT('Ctrl Pts',(-76.7598849395115,-4.90340809633497,
131.243600830494));
#92616=CARTESIAN_POINT('Ctrl Pts',(-76.7722571272631,-4.8745101616524,131.458832730377));
#92617=CARTESIAN_POINT('Ctrl Pts',(-76.7753259285481,-4.86734230897611,
131.512218917541));
#92618=CARTESIAN_POINT('Ctrl Pts',(-76.778394729833,-4.85929871632235,131.565477593643));
#92619=CARTESIAN_POINT('Ctrl Pts',(-76.781463531118,-4.85038346950786,131.618586176748));
#92620=CARTESIAN_POINT('Ctrl Pts',(-76.7892378652371,-4.82779806854749,
131.753128570112));
#92621=CARTESIAN_POINT('Ctrl Pts',(-76.7970121993562,-4.79957464391219,
131.886943628883));
#92622=CARTESIAN_POINT('Ctrl Pts',(-76.8047865334752,-4.76577030732162,
132.019521693453));
#92623=CARTESIAN_POINT('Ctrl Pts',(-76.8125512864222,-4.73200763155472,
132.151936367408));
#92624=CARTESIAN_POINT('Ctrl Pts',(-76.8203160393692,-4.69267782462236,
132.283116705224));
#92625=CARTESIAN_POINT('Ctrl Pts',(-76.8280807923163,-4.64788946593474,
132.412560410798));
#92626=CARTESIAN_POINT('Ctrl Pts',(-76.8358378332013,-4.60314559167637,
132.54187555106));
#92627=CARTESIAN_POINT('Ctrl Pts',(-76.8435948740863,-4.55295408172638,
132.669457124522));
#92628=CARTESIAN_POINT('Ctrl Pts',(-76.8513519149712,-4.49747396515987,
132.794815589478));
#92629=CARTESIAN_POINT('Ctrl Pts',(-76.8591031062113,-4.44203568658076,
132.92007952064));
#92630=CARTESIAN_POINT('Ctrl Pts',(-76.8668542974514,-4.38131689720084,
133.043123324124));
#92631=CARTESIAN_POINT('Ctrl Pts',(-76.8746054886915,-4.31552548433383,
133.163475463555));
#92632=CARTESIAN_POINT('Ctrl Pts',(-76.8823533854685,-4.24976203457241,
133.283776450116));
#92633=CARTESIAN_POINT('Ctrl Pts',(-76.8901012822456,-4.17893043658405,
133.401387705676));
#92634=CARTESIAN_POINT('Ctrl Pts',(-76.8978491790226,-4.1032853606222,133.515860628963));
#92635=CARTESIAN_POINT('Ctrl Pts',(-76.9055954551067,-4.02765610797952,
133.630309606982));
#92636=CARTESIAN_POINT('Ctrl Pts',(-76.9133417311908,-3.94721559550259,
133.741621232511));
#92637=CARTESIAN_POINT('Ctrl Pts',(-76.9210880072748,-3.86226260674418,
133.84937467649));
#92638=CARTESIAN_POINT('Ctrl Pts',(-76.9288343405402,-3.77730899088221,
133.95712891588));
#92639=CARTESIAN_POINT('Ctrl Pts',(-76.9365806738055,-3.68784307432745,
134.061324614286));
#92640=CARTESIAN_POINT('Ctrl Pts',(-76.9443270070708,-3.59420457381605,
134.161573232826));
#92641=CARTESIAN_POINT('Ctrl Pts',(-76.9520750750737,-3.50054510361182,
134.261844301348));
#92642=CARTESIAN_POINT('Ctrl Pts',(-76.9598231430766,-3.40271145688383,
134.358166245445));
#92643=CARTESIAN_POINT('Ctrl Pts',(-76.9675712110796,-3.30108063073189,
134.450186961745));
#92644=CARTESIAN_POINT('Ctrl Pts',(-76.9753275138214,-3.19934179012809,
134.542305478757));
#92645=CARTESIAN_POINT('Ctrl Pts',(-76.9830838165633,-3.09379799865874,
134.630113373286));
#92646=CARTESIAN_POINT('Ctrl Pts',(-76.9908401193051,-2.98486022754893,
134.713298131072));
#92647=CARTESIAN_POINT('Ctrl Pts',(-76.9986005618192,-2.87586431307063,
134.796527287069));
#92648=CARTESIAN_POINT('Ctrl Pts',(-77.0063610043333,-2.76347112968022,
134.875128165654));
#92649=CARTESIAN_POINT('Ctrl Pts',(-77.0141214468475,-2.64812029044048,
134.94883187333));
#92650=CARTESIAN_POINT('Ctrl Pts',(-77.0218943471129,-2.53258427979354,
135.022653896742));
#92651=CARTESIAN_POINT('Ctrl Pts',(-77.0296672473782,-2.41408146366862,
135.09156284307));
#92652=CARTESIAN_POINT('Ctrl Pts',(-77.0374401476436,-2.29307647294854,
135.155335606199));
#92653=CARTESIAN_POINT('Ctrl Pts',(-77.0449304834059,-2.17647031842908,
135.216790068757));
#92654=CARTESIAN_POINT('Ctrl Pts',(-77.0524208191683,-2.05754102965276,
135.273475158751));
#92655=CARTESIAN_POINT('Ctrl Pts',(-77.0599111549306,-1.93671971947156,
135.325234403762));
#92656=CARTESIAN_POINT('Ctrl Pts',(-77.0676854890497,-1.81131743259711,
135.378956116276));
#92657=CARTESIAN_POINT('Ctrl Pts',(-77.0754598231688,-1.68347958340171,
135.427541257682));
#92658=CARTESIAN_POINT('Ctrl Pts',(-77.0832341572879,-1.55366583322831,
135.47076239422));
#92659=CARTESIAN_POINT('Ctrl Pts',(-77.090998910235,-1.4240120669002,135.513930264569));
#92660=CARTESIAN_POINT('Ctrl Pts',(-77.0987636631821,-1.29238761214385,
135.551747160967));
#92661=CARTESIAN_POINT('Ctrl Pts',(-77.1065284161292,-1.15927375471972,
135.584032931032));
#92662=CARTESIAN_POINT('Ctrl Pts',(-77.1142854570142,-1.02629210785535,
135.616286634416));
#92663=CARTESIAN_POINT('Ctrl Pts',(-77.1220424978991,-0.891824379679084,
135.643020052407));
#92664=CARTESIAN_POINT('Ctrl Pts',(-77.1297995387841,-0.756368394593804,
135.664102371421));
#92665=CARTESIAN_POINT('Ctrl Pts',(-77.1375507300242,-0.621014557920387,
135.685168792093));
#92666=CARTESIAN_POINT('Ctrl Pts',(-77.1453019212643,-0.484674332468407,
135.700592536238));
#92667=CARTESIAN_POINT('Ctrl Pts',(-77.1530531125045,-0.347856803315691,
135.71029362841));
#92668=CARTESIAN_POINT('Ctrl Pts',(-77.1608010092816,-0.211097425262406,
135.719990597359));
#92669=CARTESIAN_POINT('Ctrl Pts',(-77.1685489060586,-0.0738615361646152,
135.723969724361));
#92670=CARTESIAN_POINT('Ctrl Pts',(-77.1762968028357,0.0633357875304305,
135.722202790767));
#92671=CARTESIAN_POINT('Ctrl Pts',(-77.1840430789198,0.200504412502617,
135.720436226778));
#92672=CARTESIAN_POINT('Ctrl Pts',(-77.191789355004,0.337634097432755,135.712925997974));
#92673=CARTESIAN_POINT('Ctrl Pts',(-77.1995356310881,0.474209287104718,
135.699696011032));
#92674=CARTESIAN_POINT('Ctrl Pts',(-77.2072819643534,0.610785484943892,
135.68646592643));
#92675=CARTESIAN_POINT('Ctrl Pts',(-77.2150282976188,0.746806790213627,
135.667516037135));
#92676=CARTESIAN_POINT('Ctrl Pts',(-77.2227746308841,0.881762688954109,
135.642922141704));
#92677=CARTESIAN_POINT('Ctrl Pts',(-77.2305226988871,1.01674881013221,135.61832273864));
#92678=CARTESIAN_POINT('Ctrl Pts',(-77.2382707668901,1.15066866545685,135.588076884433));
#92679=CARTESIAN_POINT('Ctrl Pts',(-77.246018834893,1.28302224424862,135.552311436947));
#92680=CARTESIAN_POINT('Ctrl Pts',(-77.2537751376349,1.41551648999914,135.516507977518));
#92681=CARTESIAN_POINT('Ctrl Pts',(-77.2615314403767,1.54644075585497,135.475173308419));
#92682=CARTESIAN_POINT('Ctrl Pts',(-77.2692877431186,1.67530997473362,135.42848426979));
#92683=CARTESIAN_POINT('Ctrl Pts',(-77.2770481856327,1.80424797499456,135.381770311815));
#92684=CARTESIAN_POINT('Ctrl Pts',(-77.284808628147,1.9311283812195,135.329696438297));
#92685=CARTESIAN_POINT('Ctrl Pts',(-77.2925690706611,2.05548734409571,135.272487164651));
#92686=CARTESIAN_POINT('Ctrl Pts',(-77.3003419709266,2.1800459390192,135.2151860536));
#92687=CARTESIAN_POINT('Ctrl Pts',(-77.308114871192,2.30207465387628,135.152733246904));
#92688=CARTESIAN_POINT('Ctrl Pts',(-77.3158877714574,2.42113463883094,135.085399057379));
#92689=CARTESIAN_POINT('Ctrl Pts',(-77.3233781072194,2.53586649343817,135.020512635247));
#92690=CARTESIAN_POINT('Ctrl Pts',(-77.3308684429814,2.6478414506437,134.951093732102));
#92691=CARTESIAN_POINT('Ctrl Pts',(-77.3383587787434,2.7566948387418,134.87742047823));
#92692=CARTESIAN_POINT('Ctrl Pts',(-77.3461331128625,2.86967543613508,134.800953880545));
#92693=CARTESIAN_POINT('Ctrl Pts',(-77.3539074469815,2.97965097170614,134.719661733149));
#92694=CARTESIAN_POINT('Ctrl Pts',(-77.3616817811006,3.08618164080724,134.633807828645));
#92695=CARTESIAN_POINT('Ctrl Pts',(-77.3694465340477,3.19258102037958,134.548059731406));
#92696=CARTESIAN_POINT('Ctrl Pts',(-77.3772112869949,3.29554367925083,134.457761306053));
#92697=CARTESIAN_POINT('Ctrl Pts',(-77.384976039942,3.39465790341201,134.363220095166));
#92698=CARTESIAN_POINT('Ctrl Pts',(-77.392733080827,3.4936736859285,134.268772783942));
#92699=CARTESIAN_POINT('Ctrl Pts',(-77.400490121712,3.58884835925057,134.170091341328));
#92700=CARTESIAN_POINT('Ctrl Pts',(-77.408247162597,3.67980277995377,134.067523893154));
#92701=CARTESIAN_POINT('Ctrl Pts',(-77.4159983538371,3.77068861122066,133.96503379189));
#92702=CARTESIAN_POINT('Ctrl Pts',(-77.4237495450771,3.85736026614413,133.858663809318));
#92703=CARTESIAN_POINT('Ctrl Pts',(-77.4315007363172,3.93947528619857,133.74879902445));
#92704=CARTESIAN_POINT('Ctrl Pts',(-77.4392486330943,4.02155540517911,133.638980935045));
#92705=CARTESIAN_POINT('Ctrl Pts',(-77.4469965298715,4.09908250765063,133.525671310165));
#92706=CARTESIAN_POINT('Ctrl Pts',(-77.4547444266485,4.17175444106424,133.409288245344));
#92707=CARTESIAN_POINT('Ctrl Pts',(-77.4624907027327,4.24441117307601,133.292929525351));
#92708=CARTESIAN_POINT('Ctrl Pts',(-77.4702369788167,4.31221454916572,133.173498975588));
#92709=CARTESIAN_POINT('Ctrl Pts',(-77.4779832549008,4.37490601251123,133.051443269404));
#92710=CARTESIAN_POINT('Ctrl Pts',(-77.4857295881662,4.43759793863097,132.929386662233));
#92711=CARTESIAN_POINT('Ctrl Pts',(-77.4934759214315,4.49517769808231,132.804705207746));
#92712=CARTESIAN_POINT('Ctrl Pts',(-77.5012222546968,4.54743311707082,132.677869386766));
#92713=CARTESIAN_POINT('Ctrl Pts',(-77.5089703226998,4.59970023829804,132.551005161783));
#92714=CARTESIAN_POINT('Ctrl Pts',(-77.5167183907029,4.64664049752387,132.421985971696));
#92715=CARTESIAN_POINT('Ctrl Pts',(-77.5244664587059,4.68809035587684,132.291301059425));
#92716=CARTESIAN_POINT('Ctrl Pts',(-77.5322227614477,4.72958426763247,132.160477253673));
#92717=CARTESIAN_POINT('Ctrl Pts',(-77.5399790641896,4.76557600355863,132.027984562538));
#92718=CARTESIAN_POINT('Ctrl Pts',(-77.5477353669314,4.79595215366741,131.894326673108));
#92719=CARTESIAN_POINT('Ctrl Pts',(-77.5554958094456,4.8263445164422,131.760597446437));
#92720=CARTESIAN_POINT('Ctrl Pts',(-77.5632562519597,4.85111525063289,131.625702166628));
#92721=CARTESIAN_POINT('Ctrl Pts',(-77.5710166944739,4.87020252553492,131.490152439312));
#92722=CARTESIAN_POINT('Ctrl Pts',(-77.5787895947393,4.88932044102506,131.35438511554));
#92723=CARTESIAN_POINT('Ctrl Pts',(-77.5865624950047,4.90273662709394,131.217961634185));
#92724=CARTESIAN_POINT('Ctrl Pts',(-77.5943353952701,4.91044129651265,131.081397322721));
#92725=CARTESIAN_POINT('Ctrl Pts',(-77.6018257310322,4.91786588179118,130.949797467962));
#92726=CARTESIAN_POINT('Ctrl Pts',(-77.6093160667943,4.91998699203978,130.818067152367));
#92727=CARTESIAN_POINT('Ctrl Pts',(-77.6168064025564,4.91684151218128,130.686663520784));
#92728=CARTESIAN_POINT('Ctrl Pts',(-77.6245807366755,4.91357677049793,130.550277680571));
#92729=CARTESIAN_POINT('Ctrl Pts',(-77.6323550707945,4.90462784785839,130.413811756488));
#92730=CARTESIAN_POINT('Ctrl Pts',(-77.6401294049136,4.88997895529572,130.277778354985));
#92731=CARTESIAN_POINT('Ctrl Pts',(-77.6478941578607,4.87534811618393,130.141912602492));
#92732=CARTESIAN_POINT('Ctrl Pts',(-77.6556589108078,4.85503132567286,130.006478696965));
#92733=CARTESIAN_POINT('Ctrl Pts',(-77.6634236637549,4.82906478656594,129.871989259335));
#92734=CARTESIAN_POINT('Ctrl Pts',(-77.6711807046399,4.80312403779173,129.737633398511));
#92735=CARTESIAN_POINT('Ctrl Pts',(-77.6789377455248,4.77154478101786,129.604220520198));
#92736=CARTESIAN_POINT('Ctrl Pts',(-77.6866947864098,4.73441496808316,129.47225777901));
#92737=CARTESIAN_POINT('Ctrl Pts',(-77.69444597765,4.69731315502918,129.340394551951));
#92738=CARTESIAN_POINT('Ctrl Pts',(-77.7021971688902,4.6546692226954,129.209979660183));
#92739=CARTESIAN_POINT('Ctrl Pts',(-77.7099483601303,4.60662204176346,129.081509368375));
#92740=CARTESIAN_POINT('Ctrl Pts',(-77.7176962569074,4.55859528216505,128.953093679868));
#92741=CARTESIAN_POINT('Ctrl Pts',(-77.7254441536844,4.50516997824864,128.826621312887));
#92742=CARTESIAN_POINT('Ctrl Pts',(-77.7331920504615,4.44653456479516,128.70257246778));
#92743=CARTESIAN_POINT('Ctrl Pts',(-77.7409383265456,4.3879114166063,128.578549571017));
#92744=CARTESIAN_POINT('Ctrl Pts',(-77.7486846026298,4.32408049360813,128.456949541021));
#92745=CARTESIAN_POINT('Ctrl Pts',(-77.7564308787139,4.25527783846084,128.338231346825));
#92746=CARTESIAN_POINT('Ctrl Pts',(-77.7641772119792,4.18647467542789,128.219512276279));
#92747=CARTESIAN_POINT('Ctrl Pts',(-77.7719235452446,4.11269990305261,128.103675422245));
#92748=CARTESIAN_POINT('Ctrl Pts',(-77.77966987851,4.03423466505778,127.991153598922));
#92749=CARTESIAN_POINT('Ctrl Pts',(-77.7874179465129,3.95575185531706,127.878606577118));
#92750=CARTESIAN_POINT('Ctrl Pts',(-77.7951660145158,3.87257671337463,127.769376383903));
#92751=CARTESIAN_POINT('Ctrl Pts',(-77.8029140825188,3.78503245640052,127.663865056911));
#92752=CARTESIAN_POINT('Ctrl Pts',(-77.8106703852607,3.69739515634819,127.558241591224));
#92753=CARTESIAN_POINT('Ctrl Pts',(-77.8184266880025,3.60537971532263,127.456345188578));
#92754=CARTESIAN_POINT('Ctrl Pts',(-77.8261829907443,3.50934859866901,127.358543519181));
#92755=CARTESIAN_POINT('Ctrl Pts',(-77.8339434332585,3.413266227317,127.260689650089));
#92756=CARTESIAN_POINT('Ctrl Pts',(-77.8417038757728,3.31316419486976,127.166935136134));
#92757=CARTESIAN_POINT('Ctrl Pts',(-77.8494643182869,3.20943950862779,127.077608532578));
#92758=CARTESIAN_POINT('Ctrl Pts',(-77.8572372185524,3.10554831431123,126.988138534029));
#92759=CARTESIAN_POINT('Ctrl Pts',(-77.8650101188178,2.99802315201168,126.903110892722));
#92760=CARTESIAN_POINT('Ctrl Pts',(-77.8727830190832,2.88729229109259,126.822812390017));
#92761=CARTESIAN_POINT('Ctrl Pts',(-77.8802733548452,2.78058677588241,126.745432940146));
#92762=CARTESIAN_POINT('Ctrl Pts',(-77.8877636906072,2.67090484247756,126.672444936751));
#92763=CARTESIAN_POINT('Ctrl Pts',(-77.8952540263692,2.55865103698725,126.604064445458));
#92764=CARTESIAN_POINT('Ctrl Pts',(-77.9030283604883,2.4421410943428,126.533091287054));
#92765=CARTESIAN_POINT('Ctrl Pts',(-77.9108026946074,2.32249133621925,126.466857103785));
#92766=CARTESIAN_POINT('Ctrl Pts',(-77.9185770287264,2.20012449861976,126.405652255663));
#92767=CARTESIAN_POINT('Ctrl Pts',(-77.9263417816735,2.07790846721136,126.344522837047));
#92768=CARTESIAN_POINT('Ctrl Pts',(-77.9341065346207,1.95298236526729,126.288410594211));
#92769=CARTESIAN_POINT('Ctrl Pts',(-77.9418712875677,1.8257970437956,126.237562152846));
#92770=CARTESIAN_POINT('Ctrl Pts',(-77.9496283284527,1.6987380445782,126.18676421487));
#92771=CARTESIAN_POINT('Ctrl Pts',(-77.9573853693377,1.56942465195114,126.141219818446));
#92772=CARTESIAN_POINT('Ctrl Pts',(-77.9651424102227,1.43833108957336,126.101129096658));
#92773=CARTESIAN_POINT('Ctrl Pts',(-77.9728936014628,1.30733638587056,126.061068607594));
#92774=CARTESIAN_POINT('Ctrl Pts',(-77.980644792703,1.17456455682217,126.026453721044));
#92775=CARTESIAN_POINT('Ctrl Pts',(-77.9883959839431,1.04050818694485,125.997435844346));
#92776=CARTESIAN_POINT('Ctrl Pts',(-77.9961438807202,0.906508794600613,
125.968430301018));
#92777=CARTESIAN_POINT('Ctrl Pts',(-78.0038917774972,0.771226328624115,
125.945017118674));
#92778=CARTESIAN_POINT('Ctrl Pts',(-78.0116396742743,0.635166648767972,
125.927297321812));
#92779=CARTESIAN_POINT('Ctrl Pts',(-78.0193859503584,0.499135429664119,
125.909581231549));
#92780=CARTESIAN_POINT('Ctrl Pts',(-78.0271322264427,0.362327707499512,
125.897556208394));
#92781=CARTESIAN_POINT('Ctrl Pts',(-78.0348785025268,0.22525721274329,125.891271746946));
#92782=CARTESIAN_POINT('Ctrl Pts',(-78.0426248357921,0.0881857061636275,
125.884987239108));
#92783=CARTESIAN_POINT('Ctrl Pts',(-78.0503711690574,-0.0491481863233042,
125.884443395439));
#92784=CARTESIAN_POINT('Ctrl Pts',(-78.0581175023228,-0.186228360824128,
125.889637628411));
#92785=CARTESIAN_POINT('Ctrl Pts',(-78.0658655703258,-0.323339233479397,
125.894833024596));
#92786=CARTESIAN_POINT('Ctrl Pts',(-78.0736136383287,-0.460195884476491,
125.905769039626));
#92787=CARTESIAN_POINT('Ctrl Pts',(-78.0813617063316,-0.596285361393116,
125.922391052904));
#92788=CARTESIAN_POINT('Ctrl Pts',(-78.0891180090735,-0.732519475825479,
125.939030732255));
#92789=CARTESIAN_POINT('Ctrl Pts',(-78.0968743118153,-0.867984398704479,
125.961368434214));
#92790=CARTESIAN_POINT('Ctrl Pts',(-78.1046306145572,-1.00217487729666,
125.98929794115));
#92791=CARTESIAN_POINT('Ctrl Pts',(-78.1123910570713,-1.13643697738766,
126.017242354905));
#92792=CARTESIAN_POINT('Ctrl Pts',(-78.1201514995856,-1.26942289890986,
126.050784424965));
#92793=CARTESIAN_POINT('Ctrl Pts',(-78.1279119420998,-1.40064162687198,
126.089767729991));
#92794=CARTESIAN_POINT('Ctrl Pts',(-78.1356848423652,-1.53207099878528,
126.128813614479));
#92795=CARTESIAN_POINT('Ctrl Pts',(-78.1434577426306,-1.66172713819609,
126.17331806175));
#92796=CARTESIAN_POINT('Ctrl Pts',(-78.151230642896,-1.78913727777151,126.22307576899));
#92797=CARTESIAN_POINT('Ctrl Pts',(-78.158720978658,-1.91191573784624,126.27102465824));
#92798=CARTESIAN_POINT('Ctrl Pts',(-78.1662113144201,-2.03260837636572,
126.323851376502));
#92799=CARTESIAN_POINT('Ctrl Pts',(-78.1737016501821,-2.15081474414552,
126.381332356423));
#92800=CARTESIAN_POINT('Ctrl Pts',(-78.1814767132349,-2.27351444572606,
126.440998339022));
#92801=CARTESIAN_POINT('Ctrl Pts',(-78.1892517762878,-2.39392383056797,
126.505868445645));
#92802=CARTESIAN_POINT('Ctrl Pts',(-78.1970268393407,-2.51156997926362,
126.575743905004));
#92803=CARTESIAN_POINT('Ctrl Pts',(-78.2047921581613,-2.62906868588906,
126.645531791734));
#92804=CARTESIAN_POINT('Ctrl Pts',(-78.2125574769819,-2.74381071431604,
126.720312350925));
#92805=CARTESIAN_POINT('Ctrl Pts',(-78.2203227958026,-2.85534477969413,
126.799839516164));
#92806=CARTESIAN_POINT('Ctrl Pts',(-78.2284371050609,-2.97189143028495,
126.882940806413));
#92807=CARTESIAN_POINT('Ctrl Pts',(-78.2365514143192,-3.08493467246098,
126.971225110819));
#92808=CARTESIAN_POINT('Ctrl Pts',(-78.2446657235775,-3.19398912335395,
127.064358406016));
#92809=CARTESIAN_POINT('Ctrl Pts',(-78.2524164511523,-3.29815712000958,
127.153318633711));
#92810=CARTESIAN_POINT('Ctrl Pts',(-78.260167178727,-3.39868566738597,127.246702473511));
#92811=CARTESIAN_POINT('Ctrl Pts',(-78.2679179063017,-3.49518270608593,
127.344175519399));
#92812=CARTESIAN_POINT('Ctrl Pts',(-78.2756651805459,-3.59163675060628,
127.441605136247));
#92813=CARTESIAN_POINT('Ctrl Pts',(-78.28341245479,-3.684062586047,127.543120056786));
#92814=CARTESIAN_POINT('Ctrl Pts',(-78.2911597290342,-3.77210358185438,
127.648347685042));
#92815=CARTESIAN_POINT('Ctrl Pts',(-78.2989052292268,-3.86012441711724,
127.753551217179));
#92816=CARTESIAN_POINT('Ctrl Pts',(-78.3066507294194,-3.94376216087564,
127.862465465105));
#92817=CARTESIAN_POINT('Ctrl Pts',(-78.314396229612,-4.02269946804459,127.974683594955));
#92818=CARTESIAN_POINT('Ctrl Pts',(-78.3221416334722,-4.10163579345397,
128.086900329125));
#92819=CARTESIAN_POINT('Ctrl Pts',(-78.3298870373324,-4.17587157524765,
128.202420542839));
#92820=CARTESIAN_POINT('Ctrl Pts',(-78.3376324411926,-4.24513215785856,
128.320807512675));
#92821=CARTESIAN_POINT('Ctrl Pts',(-78.3453822725759,-4.31443233205588,
128.439262156327));
#92822=CARTESIAN_POINT('Ctrl Pts',(-78.3531321039591,-4.37875142946373,
128.560586491384));
#92823=CARTESIAN_POINT('Ctrl Pts',(-78.3608819353423,-4.43786015067658,
128.684318083668));
#92824=CARTESIAN_POINT('Ctrl Pts',(-78.3686343747685,-4.49698876368704,
128.808091315218));
#92825=CARTESIAN_POINT('Ctrl Pts',(-78.3763868141946,-4.55090335005497,
128.934273060221));
#92826=CARTESIAN_POINT('Ctrl Pts',(-78.3841392536207,-4.59942270762946,
129.062380761471));
#92827=CARTESIAN_POINT('Ctrl Pts',(-78.3918991566564,-4.64798877689356,
129.19061179756));
#92828=CARTESIAN_POINT('Ctrl Pts',(-78.3996590596922,-4.69114912104015,
129.320772122251));
#92829=CARTESIAN_POINT('Ctrl Pts',(-78.407418962728,-4.72877228316011,129.452363666195));
#92830=CARTESIAN_POINT('Ctrl Pts',(-78.4099680478194,-4.74113128316439,
129.495590758245));
#92831=CARTESIAN_POINT('Ctrl Pts',(-78.4125171329109,-4.75289318270538,
129.538972202489));
#92832=CARTESIAN_POINT('Ctrl Pts',(-78.4150662180023,-4.76405452823401,
129.582490119308));
#92833=CARTESIAN_POINT('Ctrl Pts',(-76.6650346057277,-4.76405452823403,
129.582490119308));
#92834=CARTESIAN_POINT('Ctrl Pts',(-76.672671502873,-4.79766263469746,129.713527616335));
#92835=CARTESIAN_POINT('Ctrl Pts',(-76.6803084000183,-4.8258444961389,129.845891658541));
#92836=CARTESIAN_POINT('Ctrl Pts',(-76.6879452971636,-4.84851577964765,
129.979086240763));
#92837=CARTESIAN_POINT('Ctrl Pts',(-76.6958111749622,-4.87186682683677,
130.116274458343));
#92838=CARTESIAN_POINT('Ctrl Pts',(-76.7036770527608,-4.88937158334248,
130.254343344525));
#92839=CARTESIAN_POINT('Ctrl Pts',(-76.7115429305594,-4.9009954595654,130.392746031066));
#92840=CARTESIAN_POINT('Ctrl Pts',(-76.719408808358,-4.91261933578832,130.531148717607));
#92841=CARTESIAN_POINT('Ctrl Pts',(-76.7272746861567,-4.91836236347926,
130.669884739713));
#92842=CARTESIAN_POINT('Ctrl Pts',(-76.7351405639554,-4.9182483336571,130.808409194994));
#92843=CARTESIAN_POINT('',(-76.3898594360211,-4.91824995923563,130.804993846394));
#92844=CARTESIAN_POINT('Ctrl Pts',(-76.3201263474126,-4.76405452823413,
129.582490119309));
#92845=CARTESIAN_POINT('Ctrl Pts',(-76.3281810370973,-4.79941887244748,
129.720375160668));
#92846=CARTESIAN_POINT('Ctrl Pts',(-76.336235726782,-4.82882690419295,129.859929325067));
#92847=CARTESIAN_POINT('Ctrl Pts',(-76.3442904164667,-4.85213173058735,
130.000618910593));
#92848=CARTESIAN_POINT('Ctrl Pts',(-76.3523335468215,-4.87540311209611,
130.141106591715));
#92849=CARTESIAN_POINT('Ctrl Pts',(-76.3603766771764,-4.89258869526852,
130.282726105568));
#92850=CARTESIAN_POINT('Ctrl Pts',(-76.3684198075313,-4.90359226627961,
130.42493216768));
#92851=CARTESIAN_POINT('Ctrl Pts',(-76.3755663503513,-4.91336924215022,
130.551286170078));
#92852=CARTESIAN_POINT('Ctrl Pts',(-76.3827128931711,-4.91826629653936,
130.678102890917));
#92853=CARTESIAN_POINT('Ctrl Pts',(-76.3898594359911,-4.9182499592357,130.804993845861));
#92854=CARTESIAN_POINT('Ctrl Pts',(-76.3898594360212,-4.91824995923563,
130.804993846394));
#92855=CARTESIAN_POINT('Ctrl Pts',(-76.3980569668082,-4.91823121931258,
130.950545693764));
#92856=CARTESIAN_POINT('Ctrl Pts',(-76.4062544975953,-4.91174696503634,
131.09594676965));
#92857=CARTESIAN_POINT('Ctrl Pts',(-76.4144520283824,-4.89886280865999,
131.240624579438));
#92858=CARTESIAN_POINT('Ctrl Pts',(-76.4226634473724,-4.88595682403033,
131.385547501423));
#92859=CARTESIAN_POINT('Ctrl Pts',(-76.4308748663625,-4.86662931813862,
131.529744395062));
#92860=CARTESIAN_POINT('Ctrl Pts',(-76.4390862853525,-4.84099718955688,
131.672651624776));
#92861=CARTESIAN_POINT('Ctrl Pts',(-76.4473200301227,-4.81529537055134,
131.815947400662));
#92862=CARTESIAN_POINT('Ctrl Pts',(-76.455553774893,-4.78325470441282,131.957946186527));
#92863=CARTESIAN_POINT('Ctrl Pts',(-76.4637875196632,-4.74504281851426,
132.098096182883));
#92864=CARTESIAN_POINT('Ctrl Pts',(-76.4720334309119,-4.70677446935404,
132.238453269932));
#92865=CARTESIAN_POINT('Ctrl Pts',(-76.4802793421606,-4.66231679228311,
132.376955811759));
#92866=CARTESIAN_POINT('Ctrl Pts',(-76.4885252534092,-4.61188613012242,
132.513070477456));
#92867=CARTESIAN_POINT('Ctrl Pts',(-76.4967904872647,-4.5613372940174,132.649504100038));
#92868=CARTESIAN_POINT('Ctrl Pts',(-76.5050557211203,-4.50478760996428,
132.783538365348));
#92869=CARTESIAN_POINT('Ctrl Pts',(-76.5133209549758,-4.44250081567044,
132.914661440972));
#92870=CARTESIAN_POINT('Ctrl Pts',(-76.516415604472,-4.41917954007774,132.963756235749));
#92871=CARTESIAN_POINT('Ctrl Pts',(-76.5195102539682,-4.39505443429168,
133.012443189383));
#92872=CARTESIAN_POINT('Ctrl Pts',(-76.5226049034644,-4.37014091486708,
133.060696462848));
#92873=CARTESIAN_POINT('Ctrl Pts',(-76.5303792375834,-4.30755352837156,
133.181917644992));
#92874=CARTESIAN_POINT('Ctrl Pts',(-76.5381535717026,-4.23981944372601,
133.300724738339));
#92875=CARTESIAN_POINT('Ctrl Pts',(-76.5459279058216,-4.16714866238844,
133.416649860367));
#92876=CARTESIAN_POINT('Ctrl Pts',(-76.5536926587687,-4.09456744129409,
133.532432115043));
#92877=CARTESIAN_POINT('Ctrl Pts',(-76.5614574117157,-4.01706183459346,
133.645339137291));
#92878=CARTESIAN_POINT('Ctrl Pts',(-76.5692221646627,-3.93488860524996,
133.754925771358));
#92879=CARTESIAN_POINT('Ctrl Pts',(-76.5769792055477,-3.85279699151607,
133.864403562436));
#92880=CARTESIAN_POINT('Ctrl Pts',(-76.5847362464327,-3.76604721391699,
133.970567217445));
#92881=CARTESIAN_POINT('Ctrl Pts',(-76.5924932873177,-3.67494018148277,
134.072999130009));
#92882=CARTESIAN_POINT('Ctrl Pts',(-76.6002444785578,-3.58390185357053,
134.17535379787));
#92883=CARTESIAN_POINT('Ctrl Pts',(-76.6079956697979,-3.48851306986965,
134.273982033704));
#92884=CARTESIAN_POINT('Ctrl Pts',(-76.615746861038,-3.38911576675206,134.368498294768));
#92885=CARTESIAN_POINT('Ctrl Pts',(-76.6234947578151,-3.28976071013994,
134.4629743839));
#92886=CARTESIAN_POINT('Ctrl Pts',(-76.6312426545922,-3.18640080542552,
134.553341705457));
#92887=CARTESIAN_POINT('Ctrl Pts',(-76.6389905513692,-3.07941553489647,
134.639250841019));
#92888=CARTESIAN_POINT('Ctrl Pts',(-76.6467368274533,-2.97245264337967,
134.725142006242));
#92889=CARTESIAN_POINT('Ctrl Pts',(-76.6544831035374,-2.86186619909756,
134.80657659574));
#92890=CARTESIAN_POINT('Ctrl Pts',(-76.6622293796214,-2.74806921116227,
134.883245106389));
#92891=CARTESIAN_POINT('Ctrl Pts',(-76.6699757128868,-2.63427138320362,
134.959914182988));
#92892=CARTESIAN_POINT('Ctrl Pts',(-76.6777220461521,-2.51726328854291,
135.031816892083));
#92893=CARTESIAN_POINT('Ctrl Pts',(-76.6854683794175,-2.397487055372,135.098686977058));
#92894=CARTESIAN_POINT('Ctrl Pts',(-76.6932164474204,-2.2776839991443,135.165572037124));
#92895=CARTESIAN_POINT('Ctrl Pts',(-76.7009645154233,-2.15511191216886,
135.227422039882));
#92896=CARTESIAN_POINT('Ctrl Pts',(-76.7087125834262,-2.03023729762168,
135.284016807258));
#92897=CARTESIAN_POINT('Ctrl Pts',(-76.7164688861681,-1.90522996484762,
135.340671724226));
#92898=CARTESIAN_POINT('Ctrl Pts',(-76.7242251889098,-1.77791557271667,
135.392060086875));
#92899=CARTESIAN_POINT('Ctrl Pts',(-76.7319814916517,-1.64878088813436,
135.438009789161));
#92900=CARTESIAN_POINT('Ctrl Pts',(-76.7397419341658,-1.51957728048273,
135.483984016187));
#92901=CARTESIAN_POINT('Ctrl Pts',(-76.74750237668,-1.38855181781587,135.524513683345));
#92902=CARTESIAN_POINT('Ctrl Pts',(-76.7552628191941,-1.25620522211999,
135.559476967606));
#92903=CARTESIAN_POINT('Ctrl Pts',(-76.7630357194596,-1.12364617191951,
135.594496378035));
#92904=CARTESIAN_POINT('Ctrl Pts',(-76.770808619725,-0.989762132721141,
135.62393146529));
#92905=CARTESIAN_POINT('Ctrl Pts',(-76.7785815199905,-0.855063669094408,
135.647711645965));
#92906=CARTESIAN_POINT('Ctrl Pts',(-76.7860718557528,-0.725261833900718,
135.670627357175));
#92907=CARTESIAN_POINT('Ctrl Pts',(-76.7935621915151,-0.594704064254259,
135.688292122706));
#92908=CARTESIAN_POINT('Ctrl Pts',(-76.8010525272773,-0.463848661725816,
135.700688576508));
#92909=CARTESIAN_POINT('Ctrl Pts',(-76.8088268613964,-0.328031836842645,
135.713555045623));
#92910=CARTESIAN_POINT('Ctrl Pts',(-76.8166011955156,-0.191464137169983,
135.72078657786));
#92911=CARTESIAN_POINT('Ctrl Pts',(-76.8243755296346,-0.0546527164413332,
135.722306951462));
#92912=CARTESIAN_POINT('Ctrl Pts',(-76.8321402825817,0.0819900964384566,
135.72382545134));
#92913=CARTESIAN_POINT('Ctrl Pts',(-76.8399050355288,0.218875645550496,
135.719646792782));
#92914=CARTESIAN_POINT('Ctrl Pts',(-76.8476697884759,0.355490622099401,
135.709746380184));
#92915=CARTESIAN_POINT('Ctrl Pts',(-76.8554268293609,0.491969910727664,
135.699855800816));
#92916=CARTESIAN_POINT('Ctrl Pts',(-76.8631838702459,0.628178774171234,
135.684254804764));
#92917=CARTESIAN_POINT('Ctrl Pts',(-76.8709409111309,0.763603219677173,
135.662970828871));
#92918=CARTESIAN_POINT('Ctrl Pts',(-76.878692102371,0.898925540555123,135.64170290339));
#92919=CARTESIAN_POINT('Ctrl Pts',(-76.8864432936111,1.0334642362498,135.614760588708));
#92920=CARTESIAN_POINT('Ctrl Pts',(-76.8941944848512,1.16671011377224,135.582223170311));
#92921=CARTESIAN_POINT('Ctrl Pts',(-76.9019423816283,1.29989935824246,135.549699581184));
#92922=CARTESIAN_POINT('Ctrl Pts',(-76.9096902784053,1.43179649840839,135.511585710689));
#92923=CARTESIAN_POINT('Ctrl Pts',(-76.9174381751824,1.56190243921174,135.468011958831));
#92924=CARTESIAN_POINT('Ctrl Pts',(-76.9251844512665,1.69198116465704,135.424447321663));
#92925=CARTESIAN_POINT('Ctrl Pts',(-76.9329307273506,1.82026906550781,135.375425198891));
#92926=CARTESIAN_POINT('Ctrl Pts',(-76.9406770034347,1.94628250650731,135.321125772781));
#92927=CARTESIAN_POINT('Ctrl Pts',(-76.9484233367,2.07229687770957,135.266825945845));
#92928=CARTESIAN_POINT('Ctrl Pts',(-76.9561696699653,2.19603639650815,135.207248892552));
#92929=CARTESIAN_POINT('Ctrl Pts',(-76.9639160032307,2.31703807258324,135.142622669667));
#92930=CARTESIAN_POINT('Ctrl Pts',(-76.9716640712337,2.43806684614456,135.077981974188));
#92931=CARTESIAN_POINT('Ctrl Pts',(-76.9794121392367,2.55635621214841,135.008290043254));
#92932=CARTESIAN_POINT('Ctrl Pts',(-76.9871602072397,2.67146877218419,134.933820347572));
#92933=CARTESIAN_POINT('Ctrl Pts',(-76.9949165099815,2.78670367521847,134.859271504612));
#92934=CARTESIAN_POINT('Ctrl Pts',(-77.0026728127233,2.89875469888196,134.779934966023));
#92935=CARTESIAN_POINT('Ctrl Pts',(-77.0104291154651,3.00721393608535,134.696127235069));
#92936=CARTESIAN_POINT('Ctrl Pts',(-77.0181895579793,3.11573106124958,134.612274773406));
#92937=CARTESIAN_POINT('Ctrl Pts',(-77.0259500004935,3.22065228113544,134.523946615921));
#92938=CARTESIAN_POINT('Ctrl Pts',(-77.0337104430077,3.32160445011535,134.43149818588));
#92939=CARTESIAN_POINT('Ctrl Pts',(-77.0414833432731,3.42271867647901,134.338901349412));
#92940=CARTESIAN_POINT('Ctrl Pts',(-77.0492562435386,3.51985084251727,134.242171299094));
#92941=CARTESIAN_POINT('Ctrl Pts',(-77.057029143804,3.61266559179242,134.141699435304));
#92942=CARTESIAN_POINT('Ctrl Pts',(-77.0645194795661,3.70210629114568,134.044879976835));
#92943=CARTESIAN_POINT('Ctrl Pts',(-77.0720098153281,3.78753782222094,133.944586264901));
#92944=CARTESIAN_POINT('Ctrl Pts',(-77.0795001510902,3.86869785127562,133.84119449482));
#92945=CARTESIAN_POINT('Ctrl Pts',(-77.0872744852092,3.95293508749937,133.733882594351));
#92946=CARTESIAN_POINT('Ctrl Pts',(-77.0950488193283,4.03283735790277,133.622893140632));
#92947=CARTESIAN_POINT('Ctrl Pts',(-77.1028231534474,4.10806640598207,133.508611616741));
#92948=CARTESIAN_POINT('Ctrl Pts',(-77.1105879063945,4.18320274098303,133.394470934615));
#92949=CARTESIAN_POINT('Ctrl Pts',(-77.1183526593416,4.25367710010306,133.277046578327));
#92950=CARTESIAN_POINT('Ctrl Pts',(-77.1261174122887,4.31919133442124,133.156757114579));
#92951=CARTESIAN_POINT('Ctrl Pts',(-77.1338744531737,4.3846404990783,133.036587124023));
#92952=CARTESIAN_POINT('Ctrl Pts',(-77.1416314940587,4.44513915703453,132.913558030131));
#92953=CARTESIAN_POINT('Ctrl Pts',(-77.1493885349437,4.50043256604408,132.788117099847));
#92954=CARTESIAN_POINT('Ctrl Pts',(-77.1571397261838,4.55568427786385,132.662770765544));
#92955=CARTESIAN_POINT('Ctrl Pts',(-77.164890917424,4.60573839678961,132.535016571333));
#92956=CARTESIAN_POINT('Ctrl Pts',(-77.1726421086641,4.65038639669676,132.40532577144));
#92957=CARTESIAN_POINT('Ctrl Pts',(-77.1803900054412,4.69501542001298,132.275690093595));
#92958=CARTESIAN_POINT('Ctrl Pts',(-77.1881379022182,4.73424276735112,132.144119816067));
#92959=CARTESIAN_POINT('Ctrl Pts',(-77.1958857989953,4.76790837485868,132.011105326049));
#92960=CARTESIAN_POINT('Ctrl Pts',(-77.2036320750794,4.8015669402468,131.878118659796));
#92961=CARTESIAN_POINT('Ctrl Pts',(-77.2113783511636,4.82966598399625,131.743688760718));
#92962=CARTESIAN_POINT('Ctrl Pts',(-77.2191246272477,4.85209568187975,131.60831991777));
#92963=CARTESIAN_POINT('Ctrl Pts',(-77.2268709605131,4.87452554533422,131.472950075559));
#92964=CARTESIAN_POINT('Ctrl Pts',(-77.2346172937784,4.89128591550549,131.336641661353));
#92965=CARTESIAN_POINT('Ctrl Pts',(-77.2423636270438,4.9023184054314,131.199907472273));
#92966=CARTESIAN_POINT('Ctrl Pts',(-77.2501116950468,4.91335336600692,131.063142662519));
#92967=CARTESIAN_POINT('Ctrl Pts',(-77.2578597630497,4.91865786243756,130.925952277782));
#92968=CARTESIAN_POINT('Ctrl Pts',(-77.2656078310526,4.91822554884936,130.788852131327));
#92969=CARTESIAN_POINT('Ctrl Pts',(-77.2733641337945,4.91779277579313,130.651606273205));
#92970=CARTESIAN_POINT('Ctrl Pts',(-77.2811204365364,4.911611014239,130.514451236537));
#92971=CARTESIAN_POINT('Ctrl Pts',(-77.2888767392783,4.89972606360162,130.377901282854));
#92972=CARTESIAN_POINT('Ctrl Pts',(-77.2966371817924,4.88783476960823,130.241278448349));
#92973=CARTESIAN_POINT('Ctrl Pts',(-77.3043976243067,4.87023427132397,130.10526172788));
#92974=CARTESIAN_POINT('Ctrl Pts',(-77.3121580668208,4.84702190208244,129.970357174388));
#92975=CARTESIAN_POINT('Ctrl Pts',(-77.3199309670863,4.8237722702851,129.83523606013));
#92976=CARTESIAN_POINT('Ctrl Pts',(-77.3277038673517,4.79489284774365,129.701231062956));
#92977=CARTESIAN_POINT('Ctrl Pts',(-77.3354767676172,4.76053166233539,129.568835889201));
#92978=CARTESIAN_POINT('Ctrl Pts',(-77.3429671033792,4.72741959256741,129.441253613495));
#92979=CARTESIAN_POINT('Ctrl Pts',(-77.3504574391411,4.68921748157953,129.315166445745));
#92980=CARTESIAN_POINT('Ctrl Pts',(-77.3579477749031,4.64610003535104,129.190998437517));
#92981=CARTESIAN_POINT('Ctrl Pts',(-77.3657221090222,4.60134777804347,129.062122561518));
#92982=CARTESIAN_POINT('Ctrl Pts',(-77.3734964431412,4.55115833611975,128.934906007674));
#92983=CARTESIAN_POINT('Ctrl Pts',(-77.3812707772603,4.49567319150811,128.809841723784));
#92984=CARTESIAN_POINT('Ctrl Pts',(-77.3890355302074,4.44025642737835,128.684931570445));
#92985=CARTESIAN_POINT('Ctrl Pts',(-77.3968002831545,4.37955710333887,128.562168763357));
#92986=CARTESIAN_POINT('Ctrl Pts',(-77.4045650361016,4.31376621463617,128.442030389176));
#92987=CARTESIAN_POINT('Ctrl Pts',(-77.4123220769866,4.24804067037162,128.322011338123));
#92988=CARTESIAN_POINT('Ctrl Pts',(-77.4200791178717,4.17723381170246,128.204611873372));
#92989=CARTESIAN_POINT('Ctrl Pts',(-77.4278361587567,4.10158424256904,128.090288075498));
#92990=CARTESIAN_POINT('Ctrl Pts',(-77.4355873499968,4.02599172136406,127.976050490089));
#92991=CARTESIAN_POINT('Ctrl Pts',(-77.4433385412369,3.94556397350741,127.86488427969));
#92992=CARTESIAN_POINT('Ctrl Pts',(-77.451089732477,3.8605847650603,127.757219607655));
#92993=CARTESIAN_POINT('Ctrl Pts',(-77.4588376292541,3.77564167504356,127.649600695977));
#92994=CARTESIAN_POINT('Ctrl Pts',(-77.4665855260312,3.68615121371228,127.545480668898));
#92995=CARTESIAN_POINT('Ctrl Pts',(-77.4743334228083,3.59243943928063,127.445259258928));
#92996=CARTESIAN_POINT('Ctrl Pts',(-77.4820796988924,3.49874726733225,127.345058813118));
#92997=CARTESIAN_POINT('Ctrl Pts',(-77.4898259749765,3.40083580548928,127.24875564772));
#92998=CARTESIAN_POINT('Ctrl Pts',(-77.4975722510606,3.29906996365355,127.156714741467));
#92999=CARTESIAN_POINT('Ctrl Pts',(-77.505318584326,3.19730337060536,127.064673155789));
#93000=CARTESIAN_POINT('Ctrl Pts',(-77.5130649175913,3.09168263075157,126.976894154289));
#93001=CARTESIAN_POINT('Ctrl Pts',(-77.5208112508567,2.98260761525354,126.893704038942));
#93002=CARTESIAN_POINT('Ctrl Pts',(-77.5285593188596,2.87350817316222,126.810495293746));
#93003=CARTESIAN_POINT('Ctrl Pts',(-77.5363073868626,2.760953226939,126.731877716656));
#93004=CARTESIAN_POINT('Ctrl Pts',(-77.5440554548656,2.64537331479475,126.658135456305));
#93005=CARTESIAN_POINT('Ctrl Pts',(-77.5518117576074,2.52967056294429,126.584314821803));
#93006=CARTESIAN_POINT('Ctrl Pts',(-77.5595680603493,2.41093675304473,126.515380065358));
#93007=CARTESIAN_POINT('Ctrl Pts',(-77.5673243630912,2.28962930359001,126.451570625545));
#93008=CARTESIAN_POINT('Ctrl Pts',(-77.5750848056053,2.16825710869702,126.387727128712));
#93009=CARTESIAN_POINT('Ctrl Pts',(-77.5828452481195,2.04430889033384,126.329014566584));
#93010=CARTESIAN_POINT('Ctrl Pts',(-77.5906056906337,1.91826301621665,126.275624583846));
#93011=CARTESIAN_POINT('Ctrl Pts',(-77.5983785908991,1.79201480207251,126.222148894768));
#93012=CARTESIAN_POINT('Ctrl Pts',(-77.6061514911646,1.66366256942882,126.174012996633));
#93013=CARTESIAN_POINT('Ctrl Pts',(-77.61392439143,1.53370170009022,126.13135920973));
#93014=CARTESIAN_POINT('Ctrl Pts',(-77.621414727192,1.40846523570411,126.090255995419));
#93015=CARTESIAN_POINT('Ctrl Pts',(-77.628905062954,1.28173535637487,126.054243319314));
#93016=CARTESIAN_POINT('Ctrl Pts',(-77.636395398716,1.15396326154357,126.023403406556));
#93017=CARTESIAN_POINT('Ctrl Pts',(-77.6441697328351,1.02134664890106,125.991394189133));
#93018=CARTESIAN_POINT('Ctrl Pts',(-77.6519440669542,0.887187139887614,
125.964856333272));
#93019=CARTESIAN_POINT('Ctrl Pts',(-77.6597184010733,0.751975939883148,
125.943937256547));
#93020=CARTESIAN_POINT('Ctrl Pts',(-77.6674831540203,0.616931375598516,
125.923043960715));
#93021=CARTESIAN_POINT('Ctrl Pts',(-77.6752479069674,0.480838081865013,
125.907755725244));
#93022=CARTESIAN_POINT('Ctrl Pts',(-77.6830126599145,0.344200682795646,
125.898169737416));
#93023=CARTESIAN_POINT('Ctrl Pts',(-77.6907697007995,0.207698993917285,
125.888593270527));
#93024=CARTESIAN_POINT('Ctrl Pts',(-77.6985267416845,0.0706546626323717,
125.884707807741));
#93025=CARTESIAN_POINT('Ctrl Pts',(-77.7062837825695,-0.0664196262973008,
125.886559127495));
#93026=CARTESIAN_POINT('Ctrl Pts',(-77.7140349738096,-0.203390546439595,
125.888409051155));
#93027=CARTESIAN_POINT('Ctrl Pts',(-77.7217861650498,-0.340390989912295,
125.895987141153));
#93028=CARTESIAN_POINT('Ctrl Pts',(-77.72953735629,-0.476905665615885,125.909287170864));
#93029=CARTESIAN_POINT('Ctrl Pts',(-77.7372852530671,-0.613362318940467,
125.922581547709));
#93030=CARTESIAN_POINT('Ctrl Pts',(-77.7450331498441,-0.749333226829437,
125.941592989419));
#93031=CARTESIAN_POINT('Ctrl Pts',(-77.7527810466212,-0.884305840571931,
125.966263239171));
#93032=CARTESIAN_POINT('Ctrl Pts',(-77.7605273227053,-1.0192502209533,125.990928328439));
#93033=CARTESIAN_POINT('Ctrl Pts',(-77.7682735987894,-1.15319633819584,
126.021249801051));
#93034=CARTESIAN_POINT('Ctrl Pts',(-77.7760198748735,-1.28563988264154,
126.057117927892));
#93035=CARTESIAN_POINT('Ctrl Pts',(-77.7837662081388,-1.41808440475557,
126.092986319504));
#93036=CARTESIAN_POINT('Ctrl Pts',(-77.7915125414042,-1.5490259545688,126.134401344845));
#93037=CARTESIAN_POINT('Ctrl Pts',(-77.7992588746696,-1.67797386485884,
126.181202955172));
#93038=CARTESIAN_POINT('Ctrl Pts',(-77.8070069426725,-1.80695065213915,
126.228015046395));
#93039=CARTESIAN_POINT('Ctrl Pts',(-77.8147550106755,-1.93393254405191,
126.280215989616));
#93040=CARTESIAN_POINT('Ctrl Pts',(-77.8225030786785,-2.05844776188428,
126.337597150122));
#93041=CARTESIAN_POINT('Ctrl Pts',(-77.8302593814203,-2.18309531597174,
126.395039296008));
#93042=CARTESIAN_POINT('Ctrl Pts',(-77.8380156841621,-2.30527060338783,
126.457672493309));
#93043=CARTESIAN_POINT('Ctrl Pts',(-77.8457719869039,-2.42452493180908,
126.525241325289));
#93044=CARTESIAN_POINT('Ctrl Pts',(-77.8535324294181,-2.54384290985642,
126.59284622079));
#93045=CARTESIAN_POINT('Ctrl Pts',(-77.8612928719323,-2.66023649082991,
126.66539179333));
#93046=CARTESIAN_POINT('Ctrl Pts',(-77.8690533144465,-2.77328586919239,
126.742579167237));
#93047=CARTESIAN_POINT('Ctrl Pts',(-77.876826214712,-2.88651672445306,126.819890449168));
#93048=CARTESIAN_POINT('Ctrl Pts',(-77.8845991149773,-2.99639233575464,
126.901858188889));
#93049=CARTESIAN_POINT('Ctrl Pts',(-77.8923720152428,-3.10252519904289,
126.988142535249));
#93050=CARTESIAN_POINT('Ctrl Pts',(-77.8998623510048,-3.20479986541835,
127.071290228281));
#93051=CARTESIAN_POINT('Ctrl Pts',(-77.9073526867669,-3.30359894508477,
127.158445933845));
#93052=CARTESIAN_POINT('Ctrl Pts',(-77.914843022529,-3.39860937538332,127.249274489769));
#93053=CARTESIAN_POINT('Ctrl Pts',(-77.9225019334602,-3.49575808090294,
127.342147204948));
#93054=CARTESIAN_POINT('Ctrl Pts',(-77.9301608443915,-3.5892727087008,127.439173157499));
#93055=CARTESIAN_POINT('Ctrl Pts',(-77.9378197553226,-3.67876918681696,
127.540032151767));
#93056=CARTESIAN_POINT('Ctrl Pts',(-77.9454697647136,-3.76816164798992,
127.640773923051));
#93057=CARTESIAN_POINT('Ctrl Pts',(-77.9531197741044,-3.85354497834343,
127.745339581697));
#93058=CARTESIAN_POINT('Ctrl Pts',(-77.9607697834954,-3.93456950362442,
127.85336995617));
#93059=CARTESIAN_POINT('Ctrl Pts',(-77.9684126748289,-4.01551863851188,
127.961299812282));
#93060=CARTESIAN_POINT('Ctrl Pts',(-77.9760555661625,-4.09211679237984,
128.072687653498));
#93061=CARTESIAN_POINT('Ctrl Pts',(-77.983698457496,-4.16405278101098,128.187139285799));
#93062=CARTESIAN_POINT('Ctrl Pts',(-77.9913358822161,-4.23593731709264,
128.30150905604));
#93063=CARTESIAN_POINT('Ctrl Pts',(-77.9989733069363,-4.30316610786869,
128.418937917682));
#93064=CARTESIAN_POINT('Ctrl Pts',(-78.0066107316564,-4.365470096523,128.539001065781));
#93065=CARTESIAN_POINT('Ctrl Pts',(-78.0142448735701,-4.42774730495529,
128.659012606948));
#93066=CARTESIAN_POINT('Ctrl Pts',(-78.0218790154838,-4.48510373684876,
128.781655824646));
#93067=CARTESIAN_POINT('Ctrl Pts',(-78.0295131573976,-4.53731553191086,
128.906480003202));
#93068=CARTESIAN_POINT('Ctrl Pts',(-78.0371472564263,-4.5895270336716,129.031303480553));
#93069=CARTESIAN_POINT('Ctrl Pts',(-78.044781355455,-4.63659379080224,129.158307526332));
#93070=CARTESIAN_POINT('Ctrl Pts',(-78.0524154544837,-4.6783396088294,129.287020323842));
#93071=CARTESIAN_POINT('Ctrl Pts',(-78.0582029660887,-4.70998766649555,
129.384599200733));
#93072=CARTESIAN_POINT('Ctrl Pts',(-78.0639904776936,-4.73857855460141,
129.483159684766));
#93073=CARTESIAN_POINT('Ctrl Pts',(-78.0697779892986,-4.76405452823406,
129.582490119308));
#93074=CARTESIAN_POINT('Origin',(213.235140564004,0.,130.804360617566));
#93075=CARTESIAN_POINT('',(-80.1654084279177,-4.76405452823404,129.582490119308));
#93076=CARTESIAN_POINT('',(-79.8197738634776,-4.76405452823417,129.582490119309));
#93077=CARTESIAN_POINT('',(213.235140564004,-4.76405452823405,129.582490119308));
#93078=CARTESIAN_POINT('',(-78.4851405640458,-4.9182489417445,130.801134237387));
#93079=CARTESIAN_POINT('Ctrl Pts',(-78.485140564046,-4.9182489417445,130.801134237387));
#93080=CARTESIAN_POINT('Ctrl Pts',(-78.4928026403242,-4.91833732203731,
130.935859922949));
#93081=CARTESIAN_POINT('Ctrl Pts',(-78.5004647166025,-4.91288572166285,
131.070804853923));
#93082=CARTESIAN_POINT('Ctrl Pts',(-78.5081267928807,-4.90186657667286,
131.205467993461));
#93083=CARTESIAN_POINT('Ctrl Pts',(-78.5157805991188,-4.89085932516567,
131.339985784723));
#93084=CARTESIAN_POINT('Ctrl Pts',(-78.5234344053569,-4.87429651307583,
131.4742219915));
#93085=CARTESIAN_POINT('Ctrl Pts',(-78.5310882115949,-4.85220259044985,
131.607674431546));
#93086=CARTESIAN_POINT('Ctrl Pts',(-78.5387357066714,-4.83012688599015,
131.741016829624));
#93087=CARTESIAN_POINT('Ctrl Pts',(-78.5463832017478,-4.80252920910269,
131.873576351376));
#93088=CARTESIAN_POINT('Ctrl Pts',(-78.5540306968244,-4.76948587907409,
132.004855312187));
#93089=CARTESIAN_POINT('Ctrl Pts',(-78.5616743679513,-4.73645907158338,
132.13606863005));
#93090=CARTESIAN_POINT('Ctrl Pts',(-78.5693180390784,-4.69799212318942,
132.266002270696));
#93091=CARTESIAN_POINT('Ctrl Pts',(-78.5769617102053,-4.65421248287121,
132.394168538916));
#93092=CARTESIAN_POINT('Ctrl Pts',(-78.5846035112398,-4.6104435536333,132.522303450112));
#93093=CARTESIAN_POINT('Ctrl Pts',(-78.5922453122742,-4.56136464652823,
132.648671467787));
#93094=CARTESIAN_POINT('Ctrl Pts',(-78.5998871133087,-4.50715298291554,
132.772800368002));
#93095=CARTESIAN_POINT('Ctrl Pts',(-78.6075288055478,-4.45294209110812,
132.896927501008));
#93096=CARTESIAN_POINT('Ctrl Pts',(-78.6151704977868,-4.39359874940335,
133.018815211029));
#93097=CARTESIAN_POINT('Ctrl Pts',(-78.6228121900258,-4.32934797873513,
133.138012078586));
#93098=CARTESIAN_POINT('Ctrl Pts',(-78.6304555344611,-4.26508331652608,
133.257234717479));
#93099=CARTESIAN_POINT('Ctrl Pts',(-78.6380988788963,-4.19590930687053,
133.373765002907));
#93100=CARTESIAN_POINT('Ctrl Pts',(-78.6457422233316,-4.12209621223419,
133.487177398411));
#93101=CARTESIAN_POINT('Ctrl Pts',(-78.653393440683,-4.0482070874896,133.600706612709));
#93102=CARTESIAN_POINT('Ctrl Pts',(-78.6610446580344,-3.96966955657373,
133.711111186798));
#93103=CARTESIAN_POINT('Ctrl Pts',(-78.6686958753859,-3.88679657151321,
133.817995544722));
#93104=CARTESIAN_POINT('Ctrl Pts',(-78.6763513167103,-3.80387783513793,
133.92493890981));
#93105=CARTESIAN_POINT('Ctrl Pts',(-78.6840067580348,-3.71661913874972,
134.028357882526));
#93106=CARTESIAN_POINT('Ctrl Pts',(-78.6916621993592,-3.62537189640952,
134.127892124145));
#93107=CARTESIAN_POINT('Ctrl Pts',(-78.6993292101295,-3.5339867547656,134.227576788969));
#93108=CARTESIAN_POINT('Ctrl Pts',(-78.7069962208997,-3.43860131396968,
134.323364714613));
#93109=CARTESIAN_POINT('Ctrl Pts',(-78.71466323167,-3.33960217578401,134.414934030474));
#93110=CARTESIAN_POINT('Ctrl Pts',(-78.7199744537161,-3.27102180971564,
134.478367483709));
#93111=CARTESIAN_POINT('Ctrl Pts',(-78.7252856757622,-3.20070799148809,
134.539777330131));
#93112=CARTESIAN_POINT('Ctrl Pts',(-78.7305968978083,-3.12879742538389,
134.599068739861));
#93113=CARTESIAN_POINT('Ctrl Pts',(-78.7383712319274,-3.02353788949273,
134.685856907562));
#93114=CARTESIAN_POINT('Ctrl Pts',(-78.7461455660464,-2.9144978321693,134.768399608943));
#93115=CARTESIAN_POINT('Ctrl Pts',(-78.7539199001655,-2.80205450825847,
134.84634943438));
#93116=CARTESIAN_POINT('Ctrl Pts',(-78.7616846531126,-2.68974976069563,
134.924203193623));
#93117=CARTESIAN_POINT('Ctrl Pts',(-78.7694494060597,-2.57405041002116,
134.997475118645));
#93118=CARTESIAN_POINT('Ctrl Pts',(-78.7772141590067,-2.45536774764835,
135.065857101937));
#93119=CARTESIAN_POINT('Ctrl Pts',(-78.7849711998917,-2.33680296256829,
135.13417116728));
#93120=CARTESIAN_POINT('Ctrl Pts',(-78.7927282407768,-2.21526109899332,
135.197604762143));
#93121=CARTESIAN_POINT('Ctrl Pts',(-78.8004852816618,-2.0911831819534,135.255892484465));
#93122=CARTESIAN_POINT('Ctrl Pts',(-78.8082364729019,-1.96719883303608,
135.314136251562));
#93123=CARTESIAN_POINT('Ctrl Pts',(-78.815987664142,-1.84068258971744,135.367241704542));
#93124=CARTESIAN_POINT('Ctrl Pts',(-78.8237388553821,-1.71210056645969,
135.414989068529));
#93125=CARTESIAN_POINT('Ctrl Pts',(-78.8314867521592,-1.5835731939917,135.462716138612));
#93126=CARTESIAN_POINT('Ctrl Pts',(-78.8392346489363,-1.45298215362688,
135.505089513325));
#93127=CARTESIAN_POINT('Ctrl Pts',(-78.8469825457134,-1.32081385025044,
135.541937406969));
#93128=CARTESIAN_POINT('Ctrl Pts',(-78.8547288217975,-1.18867319363385,
135.578777592827));
#93129=CARTESIAN_POINT('Ctrl Pts',(-78.8624750978815,-1.05495630661775,
135.61009449166));
#93130=CARTESIAN_POINT('Ctrl Pts',(-78.8702213739656,-0.920164697454836,
135.635766209323));
#93131=CARTESIAN_POINT('Ctrl Pts',(-78.877967707231,-0.78537209329107,135.661438116488));
#93132=CARTESIAN_POINT('Ctrl Pts',(-78.8857140404963,-0.649505135211773,
135.681464686184));
#93133=CARTESIAN_POINT('Ctrl Pts',(-78.8934603737617,-0.51307507153837,
135.695775242546));
#93134=CARTESIAN_POINT('Ctrl Pts',(-78.9012084417646,-0.376614455298332,
135.710089003657));
#93135=CARTESIAN_POINT('Ctrl Pts',(-78.9089565097676,-0.239590871290205,
135.718684163482));
#93136=CARTESIAN_POINT('Ctrl Pts',(-78.9167045777706,-0.102519831956767,
135.721541999878));
#93137=CARTESIAN_POINT('Ctrl Pts',(-78.9244608805124,0.0346968881086265,
135.724402873616));
#93138=CARTESIAN_POINT('Ctrl Pts',(-78.9322171832543,0.171960772747315,
135.721514234959));
#93139=CARTESIAN_POINT('Ctrl Pts',(-78.9399734859961,0.308756609462109,
135.712909529272));
#93140=CARTESIAN_POINT('Ctrl Pts',(-78.9477339285103,0.445625458234173,
135.704300230995));
#93141=CARTESIAN_POINT('Ctrl Pts',(-78.9554943710244,0.582025372677596,
135.689968827472));
#93142=CARTESIAN_POINT('Ctrl Pts',(-78.9632548135386,0.717448109849961,
135.67000048013));
#93143=CARTESIAN_POINT('Ctrl Pts',(-78.971027713804,0.853088239621932,135.650000077825));
#93144=CARTESIAN_POINT('Ctrl Pts',(-78.9788006140696,0.987747673178774,
135.624344722283));
#93145=CARTESIAN_POINT('Ctrl Pts',(-78.986573514335,1.12092929410096,135.593170551164));
#93146=CARTESIAN_POINT('Ctrl Pts',(-78.9940638500969,1.24926942763691,135.563129639688));
#93147=CARTESIAN_POINT('Ctrl Pts',(-79.0015541858588,1.3762370307251,135.52796427433));
#93148=CARTESIAN_POINT('Ctrl Pts',(-79.0090445216208,1.50140398145464,135.48783893469));
#93149=CARTESIAN_POINT('Ctrl Pts',(-79.0168188557399,1.63131667516605,135.446192230601));
#93150=CARTESIAN_POINT('Ctrl Pts',(-79.0245931898589,1.75970100200358,135.399070088515));
#93151=CARTESIAN_POINT('Ctrl Pts',(-79.032367523978,1.8860607609518,135.346602120227));
#93152=CARTESIAN_POINT('Ctrl Pts',(-79.0401322769251,2.01226479278987,135.294198814022));
#93153=CARTESIAN_POINT('Ctrl Pts',(-79.0478970298721,2.13644886363297,135.236462938764));
#93154=CARTESIAN_POINT('Ctrl Pts',(-79.0556617828192,2.25813144085323,135.173573985935));
#93155=CARTESIAN_POINT('Ctrl Pts',(-79.0634188237041,2.37969316122237,135.1107474953));
#93156=CARTESIAN_POINT('Ctrl Pts',(-79.0711758645891,2.49875798719979,135.042778290705));
#93157=CARTESIAN_POINT('Ctrl Pts',(-79.0789329054741,2.61486424371473,134.969893962702));
#93158=CARTESIAN_POINT('Ctrl Pts',(-79.0866840967142,2.73088294359829,134.897064597339));
#93159=CARTESIAN_POINT('Ctrl Pts',(-79.0944352879544,2.84394718505944,134.819327693217));
#93160=CARTESIAN_POINT('Ctrl Pts',(-79.1021864791944,2.95362011901819,134.736956611948));
#93161=CARTESIAN_POINT('Ctrl Pts',(-79.1099343759715,3.06324643905482,134.654620540586));
#93162=CARTESIAN_POINT('Ctrl Pts',(-79.1176822727486,3.1694840064577,134.567654443856));
#93163=CARTESIAN_POINT('Ctrl Pts',(-79.1254301695256,3.2719253793318,134.476374693599));
#93164=CARTESIAN_POINT('Ctrl Pts',(-79.1331764456097,3.3743453236788,134.385114037098));
#93165=CARTESIAN_POINT('Ctrl Pts',(-79.1409227216938,3.47297036125623,134.28954178177));
#93166=CARTESIAN_POINT('Ctrl Pts',(-79.1486689977778,3.56742686160703,134.190013973949));
#93167=CARTESIAN_POINT('Ctrl Pts',(-79.1564153310432,3.66188405921439,134.090485431435));
#93168=CARTESIAN_POINT('Ctrl Pts',(-79.1641616643085,3.75217238905854,133.987001561748));
#93169=CARTESIAN_POINT('Ctrl Pts',(-79.1719079975739,3.83795604732683,133.879954290548));
#93170=CARTESIAN_POINT('Ctrl Pts',(-79.1796560655769,3.92375891625072,133.772883046854));
#93171=CARTESIAN_POINT('Ctrl Pts',(-79.1874041335798,4.00505486178291,133.662247118752));
#93172=CARTESIAN_POINT('Ctrl Pts',(-79.1951522015828,4.08154948538709,133.548470101686));
#93173=CARTESIAN_POINT('Ctrl Pts',(-79.2029085043246,4.15812540838744,133.434572161052));
#93174=CARTESIAN_POINT('Ctrl Pts',(-79.2106648070665,4.22988959737858,133.317526787637));
#93175=CARTESIAN_POINT('Ctrl Pts',(-79.2184211098083,4.29659170595529,133.197785522345));
#93176=CARTESIAN_POINT('Ctrl Pts',(-79.2261815523225,4.3633294154557,133.077980347534));
#93177=CARTESIAN_POINT('Ctrl Pts',(-79.2339419948366,4.42499948529468,132.955476762799));
#93178=CARTESIAN_POINT('Ctrl Pts',(-79.2417024373508,4.4813988464692,132.830748399153));
#93179=CARTESIAN_POINT('Ctrl Pts',(-79.2494753376162,4.53788874490518,132.705819810465));
#93180=CARTESIAN_POINT('Ctrl Pts',(-79.2572482378816,4.58909088076802,132.578659668924));
#93181=CARTESIAN_POINT('Ctrl Pts',(-79.265021138147,4.63485108695769,132.449759798381));
#93182=CARTESIAN_POINT('Ctrl Pts',(-79.2725114739093,4.6789477943906,132.325545762809));
#93183=CARTESIAN_POINT('Ctrl Pts',(-79.2800018096714,4.71799126740704,132.199716583479));
#93184=CARTESIAN_POINT('Ctrl Pts',(-79.2874921454337,4.75188847700245,132.072721356722));
#93185=CARTESIAN_POINT('Ctrl Pts',(-79.2952664795528,4.78707090960166,131.940911067346));
#93186=CARTESIAN_POINT('Ctrl Pts',(-79.3030408136719,4.81682058151303,131.807427028324));
#93187=CARTESIAN_POINT('Ctrl Pts',(-79.310815147791,4.84097833004299,131.672756765965));
#93188=CARTESIAN_POINT('Ctrl Pts',(-79.318579900738,4.86510630630679,131.53825247267));
#93189=CARTESIAN_POINT('Ctrl Pts',(-79.3263446536852,4.88365600294281,131.40256524594));
#93190=CARTESIAN_POINT('Ctrl Pts',(-79.3341094066322,4.8965181510694,131.266197232342));
#93191=CARTESIAN_POINT('Ctrl Pts',(-79.3418664475172,4.90936752432922,131.129964661377));
#93192=CARTESIAN_POINT('Ctrl Pts',(-79.3496234884022,4.91654055427657,130.993053035867));
#93193=CARTESIAN_POINT('Ctrl Pts',(-79.3573805292873,4.9179791726358,130.855973794376));
#93194=CARTESIAN_POINT('Ctrl Pts',(-79.3651317205274,4.91941670612174,130.718997925408));
#93195=CARTESIAN_POINT('Ctrl Pts',(-79.3728829117675,4.91512843131837,130.581855081413));
#93196=CARTESIAN_POINT('Ctrl Pts',(-79.3806341030077,4.90510820749114,130.445060554523));
#93197=CARTESIAN_POINT('Ctrl Pts',(-79.3883819997848,4.89509224252636,130.308324168955));
#93198=CARTESIAN_POINT('Ctrl Pts',(-79.3961298965618,4.87934920251789,130.171936195148));
#93199=CARTESIAN_POINT('Ctrl Pts',(-79.4038777933389,4.85792502775777,130.036410432212));
#93200=CARTESIAN_POINT('Ctrl Pts',(-79.411624069423,4.83650533447316,129.900913018345));
#93201=CARTESIAN_POINT('Ctrl Pts',(-79.4193703455071,4.8094069311796,129.766277842538));
#93202=CARTESIAN_POINT('Ctrl Pts',(-79.4271166215912,4.77672741335286,129.633011702416));
#93203=CARTESIAN_POINT('Ctrl Pts',(-79.4348629548566,4.7440476542932,129.499744578553));
#93204=CARTESIAN_POINT('Ctrl Pts',(-79.442609288122,4.70578679160541,129.367846890256));
#93205=CARTESIAN_POINT('Ctrl Pts',(-79.4503556213873,4.6620930532845,129.237813004176));
#93206=CARTESIAN_POINT('Ctrl Pts',(-79.4581036893903,4.61838953005391,129.10774999791));
#93207=CARTESIAN_POINT('Ctrl Pts',(-79.4658517573933,4.56925083469331,128.979551994941));
#93208=CARTESIAN_POINT('Ctrl Pts',(-79.4735998253963,4.51487422044557,128.85369564478));
#93209=CARTESIAN_POINT('Ctrl Pts',(-79.4813561281381,4.4604398140852,128.727705532992));
#93210=CARTESIAN_POINT('Ctrl Pts',(-79.4891124308801,4.40075652362129,128.604062405003));
#93211=CARTESIAN_POINT('Ctrl Pts',(-79.4968687336219,4.33606892485685,128.483220953222));
#93212=CARTESIAN_POINT('Ctrl Pts',(-79.5046291761361,4.27134680037325,128.36231500472));
#93213=CARTESIAN_POINT('Ctrl Pts',(-79.5123896186502,4.20161524417627,128.244214048511));
#93214=CARTESIAN_POINT('Ctrl Pts',(-79.5201500611643,4.12716297169562,128.129344941432));
#93215=CARTESIAN_POINT('Ctrl Pts',(-79.5279229614298,4.05259118181761,128.014291436264));
#93216=CARTESIAN_POINT('Ctrl Pts',(-79.5356958616953,3.97328375849158,127.90248046668));
#93217=CARTESIAN_POINT('Ctrl Pts',(-79.5434687619607,3.88957115597044,127.794307580634));
#93218=CARTESIAN_POINT('Ctrl Pts',(-79.5509590977227,3.80890171741095,127.690067051468));
#93219=CARTESIAN_POINT('Ctrl Pts',(-79.5584494334847,3.72414201603116,127.589204926877));
#93220=CARTESIAN_POINT('Ctrl Pts',(-79.5659397692466,3.63561960484334,127.492042222336));
#93221=CARTESIAN_POINT('Ctrl Pts',(-79.5737141033657,3.54374083952863,127.391195564319));
#93222=CARTESIAN_POINT('Ctrl Pts',(-79.5814884374847,3.44751736137916,127.294014939165));
#93223=CARTESIAN_POINT('Ctrl Pts',(-79.5892627716038,3.34727330876307,127.200897774835));
#93224=CARTESIAN_POINT('Ctrl Pts',(-79.5970275245509,3.24715279798331,127.107895369088));
#93225=CARTESIAN_POINT('Ctrl Pts',(-79.604792277498,3.14302185540678,127.018946723562));
#93226=CARTESIAN_POINT('Ctrl Pts',(-79.6125570304451,3.03524388866223,126.934415191744));
#93227=CARTESIAN_POINT('Ctrl Pts',(-79.6203140713301,2.92757296851336,126.849967617836));
#93228=CARTESIAN_POINT('Ctrl Pts',(-79.6280711122151,2.81626253833069,126.76992866675));
#93229=CARTESIAN_POINT('Ctrl Pts',(-79.6358281531001,2.70171149854224,126.694623638008));
#93230=CARTESIAN_POINT('Ctrl Pts',(-79.6435793443402,2.5872468425835,126.619375397374));
#93231=CARTESIAN_POINT('Ctrl Pts',(-79.6513305355804,2.46954676656517,126.548854187337));
#93232=CARTESIAN_POINT('Ctrl Pts',(-79.6590817268206,2.34904148113322,126.483343702254));
#93233=CARTESIAN_POINT('Ctrl Pts',(-79.6668296235977,2.22858741366232,126.417861060874));
#93234=CARTESIAN_POINT('Ctrl Pts',(-79.6745775203748,2.10533085091978,126.357385094995));
#93235=CARTESIAN_POINT('Ctrl Pts',(-79.6823254171519,1.97972889850062,126.302154874717));
#93236=CARTESIAN_POINT('Ctrl Pts',(-79.690071693236,1.85415321930225,126.246936207411));
#93237=CARTESIAN_POINT('Ctrl Pts',(-79.69781796932,1.72623348393338,126.196961260398));
#93238=CARTESIAN_POINT('Ctrl Pts',(-79.7055642454041,1.59644882832818,126.152421860335));
#93239=CARTESIAN_POINT('Ctrl Pts',(-79.7133105786695,1.46666321468231,126.107882131492));
#93240=CARTESIAN_POINT('Ctrl Pts',(-79.7210569119348,1.33501302312562,126.068778156571));
#93241=CARTESIAN_POINT('Ctrl Pts',(-79.7288032452002,1.20199429917472,126.035252444411));
#93242=CARTESIAN_POINT('Ctrl Pts',(-79.7365513132031,1.06894578660307,126.001719224401));
#93243=CARTESIAN_POINT('Ctrl Pts',(-79.7442993812062,0.934528510827687,
125.973766848473));
#93244=CARTESIAN_POINT('Ctrl Pts',(-79.7520474492092,0.799250110776796,
125.951487002591));
#93245=CARTESIAN_POINT('Ctrl Pts',(-79.7598037519511,0.663827935232313,
125.929183477423));
#93246=CARTESIAN_POINT('Ctrl Pts',(-79.767560054693,0.52754319355888,125.91256458918));
#93247=CARTESIAN_POINT('Ctrl Pts',(-79.7753163574348,0.390910630552998,
125.901670341664));
#93248=CARTESIAN_POINT('Ctrl Pts',(-79.783076799949,0.254205142633941,125.890770279561));
#93249=CARTESIAN_POINT('Ctrl Pts',(-79.7908372424631,0.117151853969851,
125.885600961082));
#93250=CARTESIAN_POINT('Ctrl Pts',(-79.7985976849773,-0.0197340509522312,
125.886150208308));
#93251=CARTESIAN_POINT('Ctrl Pts',(-79.8063705852427,-0.156839697280681,
125.886700337234));
#93252=CARTESIAN_POINT('Ctrl Pts',(-79.8141434855082,-0.293777032141836,
125.892987358387));
#93253=CARTESIAN_POINT('Ctrl Pts',(-79.8219163857736,-0.430034651244678,
125.904947054574));
#93254=CARTESIAN_POINT('Ctrl Pts',(-79.8294067215356,-0.561338962679421,
125.91647198568));
#93255=CARTESIAN_POINT('Ctrl Pts',(-79.8368970572976,-0.692011813627218,
125.933264280935));
#93256=CARTESIAN_POINT('Ctrl Pts',(-79.8443873930595,-0.821606074275422,
125.955221877417));
#93257=CARTESIAN_POINT('Ctrl Pts',(-79.8521617271786,-0.95611394070676,
125.978012002843));
#93258=CARTESIAN_POINT('Ctrl Pts',(-79.8599360612977,-1.08988589327567,
126.006439038537));
#93259=CARTESIAN_POINT('Ctrl Pts',(-79.8677103954168,-1.22241235987757,
126.040445097228));
#93260=CARTESIAN_POINT('Ctrl Pts',(-79.8754751483639,-1.35477549945361,
126.074409246491));
#93261=CARTESIAN_POINT('Ctrl Pts',(-79.8832399013109,-1.48589583209466,
126.113938642024));
#93262=CARTESIAN_POINT('Ctrl Pts',(-79.891004654258,-1.61527122751894,126.158923940132));
#93263=CARTESIAN_POINT('Ctrl Pts',(-79.898761695143,-1.74451812547697,126.203864558208));
#93264=CARTESIAN_POINT('Ctrl Pts',(-79.9065187360281,-1.87202316826902,
126.254250167474));
#93265=CARTESIAN_POINT('Ctrl Pts',(-79.9142757769132,-1.99729705676941,
126.30992099404));
#93266=CARTESIAN_POINT('Ctrl Pts',(-79.9220269681533,-2.12247647525617,
126.365549838803));
#93267=CARTESIAN_POINT('Ctrl Pts',(-79.9297781593934,-2.24542773259705,
126.426455809595));
#93268=CARTESIAN_POINT('Ctrl Pts',(-79.9375293506336,-2.36567960933227,
126.492430301746));
#93269=CARTESIAN_POINT('Ctrl Pts',(-79.9452772474107,-2.48588037581157,
126.558376752977));
#93270=CARTESIAN_POINT('Ctrl Pts',(-79.9530251441878,-2.60338370154532,
126.629387253254));
#93271=CARTESIAN_POINT('Ctrl Pts',(-79.9607730409649,-2.71774137334648,
126.705206449924));
#93272=CARTESIAN_POINT('Ctrl Pts',(-79.968519317049,-2.83207512398796,126.781009786851));
#93273=CARTESIAN_POINT('Ctrl Pts',(-79.9762655931331,-2.94326420385429,
126.861619603525));
#93274=CARTESIAN_POINT('Ctrl Pts',(-79.9840118692172,-3.05088823906931,
126.946736476309));
#93275=CARTESIAN_POINT('Ctrl Pts',(-79.9917582024826,-3.15851306874066,
127.031853977406));
#93276=CARTESIAN_POINT('Ctrl Pts',(-79.9995045357479,-3.26257249459517,
127.121478358478));
#93277=CARTESIAN_POINT('Ctrl Pts',(-80.0072508690133,-3.36267849519126,
127.21526931189));
#93278=CARTESIAN_POINT('Ctrl Pts',(-80.0149989370163,-3.46280691383196,
127.309081269136));
#93279=CARTESIAN_POINT('Ctrl Pts',(-80.0227470050192,-3.55897986023369,
127.407061388177));
#93280=CARTESIAN_POINT('Ctrl Pts',(-80.0304950730222,-3.6508458051584,127.508832136509));
#93281=CARTESIAN_POINT('Ctrl Pts',(-80.038251375764,-3.74280938630247,127.610711048003));
#93282=CARTESIAN_POINT('Ctrl Pts',(-80.046007678506,-3.83045655946711,127.716388345923));
#93283=CARTESIAN_POINT('Ctrl Pts',(-80.0537639812478,-3.91347543618363,
127.825452583926));
#93284=CARTESIAN_POINT('Ctrl Pts',(-80.061524423762,-3.99653862257453,127.934575032796));
#93285=CARTESIAN_POINT('Ctrl Pts',(-80.0692848662762,-4.07496836684843,
128.047087703195));
#93286=CARTESIAN_POINT('Ctrl Pts',(-80.0770453087904,-4.14849644483638,
128.162550573358));
#93287=CARTESIAN_POINT('Ctrl Pts',(-80.0848182090559,-4.22214255662263,
128.27819879477));
#93288=CARTESIAN_POINT('Ctrl Pts',(-80.0925911093213,-4.29087108204223,
128.396806341357));
#93289=CARTESIAN_POINT('Ctrl Pts',(-80.1003640095867,-4.354459622326,128.517908243246));
#93290=CARTESIAN_POINT('Ctrl Pts',(-80.1078543453488,-4.41573655900041,
128.634607785964));
#93291=CARTESIAN_POINT('Ctrl Pts',(-80.1153446811107,-4.47224059321952,
128.753623202075));
#93292=CARTESIAN_POINT('Ctrl Pts',(-80.1228350168728,-4.52381590882459,
128.874523141102));
#93293=CARTESIAN_POINT('Ctrl Pts',(-80.131461488494,-4.58321418021869,129.013761210818));
#93294=CARTESIAN_POINT('Ctrl Pts',(-80.1400879601153,-4.63623611515082,
129.155874571086));
#93295=CARTESIAN_POINT('Ctrl Pts',(-80.1487144317366,-4.68262360601552,
129.300293056954));
#93296=CARTESIAN_POINT('Ctrl Pts',(-80.1542790971303,-4.71254671669702,
129.39345287777));
#93297=CARTESIAN_POINT('Ctrl Pts',(-80.159843762524,-4.73971004719732,129.487571357225));
#93298=CARTESIAN_POINT('Ctrl Pts',(-80.1654084279176,-4.76405452823404,
129.582490119308));
#93299=CARTESIAN_POINT('Ctrl Pts',(-78.4150662180023,-4.76405452823401,
129.582490119308));
#93300=CARTESIAN_POINT('Ctrl Pts',(-78.4228402209491,-4.79809353827815,
129.715207702856));
#93301=CARTESIAN_POINT('Ctrl Pts',(-78.430614223896,-4.82654303296878,129.849194871298));
#93302=CARTESIAN_POINT('Ctrl Pts',(-78.4383882268428,-4.84933960771396,
129.983940949618));
#93303=CARTESIAN_POINT('Ctrl Pts',(-78.4429752425603,-4.86279062482549,
130.06344727131));
#93304=CARTESIAN_POINT('Ctrl Pts',(-78.4475622582779,-4.87427454369444,
130.143217716642));
#93305=CARTESIAN_POINT('Ctrl Pts',(-78.4521492739955,-4.88378684855164,
130.223147162445));
#93306=CARTESIAN_POINT('Ctrl Pts',(-78.4631463706665,-4.90659203225248,
130.41477324277));
#93307=CARTESIAN_POINT('Ctrl Pts',(-78.4741434673374,-4.91812209273009,
130.607767408421));
#93308=CARTESIAN_POINT('Ctrl Pts',(-78.4851405640086,-4.91824894174407,
130.801134236732));
#93309=CARTESIAN_POINT('',(-78.1398594359569,-4.91824809318944,130.80869147642));
#93310=CARTESIAN_POINT('Ctrl Pts',(-78.0697779892986,-4.76405452823406,
129.582490119308));
#93311=CARTESIAN_POINT('Ctrl Pts',(-78.0774154655189,-4.797673837549,129.713571296083));
#93312=CARTESIAN_POINT('Ctrl Pts',(-78.0850529417394,-4.82586675114046,
129.845993425159));
#93313=CARTESIAN_POINT('Ctrl Pts',(-78.0926904179597,-4.84854548498732,
129.979260779662));
#93314=CARTESIAN_POINT('Ctrl Pts',(-78.1005519209593,-4.87188944430299,
130.116437207704));
#93315=CARTESIAN_POINT('Ctrl Pts',(-78.1084134239588,-4.88939068370309,
130.254508754735));
#93316=CARTESIAN_POINT('Ctrl Pts',(-78.1162749269583,-4.90101084537413,
130.392929267247));
#93317=CARTESIAN_POINT('Ctrl Pts',(-78.1241364299578,-4.91263100704514,
130.531349779759));
#93318=CARTESIAN_POINT('Ctrl Pts',(-78.1319979329574,-4.91837011605548,
130.670118794076));
#93319=CARTESIAN_POINT('Ctrl Pts',(-78.1398594359569,-4.91824809318944,
130.80869147642));
#93320=CARTESIAN_POINT('Ctrl Pts',(-78.1398594359912,-4.91824809318891,
130.808691477025));
#93321=CARTESIAN_POINT('Ctrl Pts',(-78.1512629029101,-4.91807109345862,
131.009697442304));
#93322=CARTESIAN_POINT('Ctrl Pts',(-78.1626663698291,-4.90556839729258,
131.210182371441));
#93323=CARTESIAN_POINT('Ctrl Pts',(-78.174069836748,-4.8809497333259,131.408937133191));
#93324=CARTESIAN_POINT('Ctrl Pts',(-78.1804767732793,-4.86711795579357,
131.520605729495));
#93325=CARTESIAN_POINT('Ctrl Pts',(-78.1868837098105,-4.84946236679947,
131.631728881281));
#93326=CARTESIAN_POINT('Ctrl Pts',(-78.1932906463418,-4.82802602763092,
131.742096048814));
#93327=CARTESIAN_POINT('Ctrl Pts',(-78.2010649804609,-4.80201464728211,
131.876018280132));
#93328=CARTESIAN_POINT('Ctrl Pts',(-78.20883931458,-4.77038563986094,132.009069539209));
#93329=CARTESIAN_POINT('Ctrl Pts',(-78.2166136486991,-4.73320910429146,
132.140741789819));
#93330=CARTESIAN_POINT('Ctrl Pts',(-78.2243784016461,-4.6960783854796,132.272251766148));
#93331=CARTESIAN_POINT('Ctrl Pts',(-78.2321431545932,-4.65341384699147,
132.402385742874));
#93332=CARTESIAN_POINT('Ctrl Pts',(-78.2399079075403,-4.60533685077465,
132.530644358264));
#93333=CARTESIAN_POINT('Ctrl Pts',(-78.2476649484253,-4.55730760530798,
132.658775585389));
#93334=CARTESIAN_POINT('Ctrl Pts',(-78.2554219893103,-4.50387673639554,
132.785034794185));
#93335=CARTESIAN_POINT('Ctrl Pts',(-78.2631790301953,-4.44521571374638,
132.908936660564));
#93336=CARTESIAN_POINT('Ctrl Pts',(-78.2709302214354,-4.3865989278308,133.032745091582));
#93337=CARTESIAN_POINT('Ctrl Pts',(-78.2786814126755,-4.32276000529121,
133.154199366635));
#93338=CARTESIAN_POINT('Ctrl Pts',(-78.2864326039156,-4.25391879869345,
133.272833407901));
#93339=CARTESIAN_POINT('Ctrl Pts',(-78.2941805006927,-4.18510685144499,
133.391417026534));
#93340=CARTESIAN_POINT('Ctrl Pts',(-78.3019283974698,-4.11129704461234,
133.507182458003));
#93341=CARTESIAN_POINT('Ctrl Pts',(-78.3096762942469,-4.0327554131942,133.619687745957));
#93342=CARTESIAN_POINT('Ctrl Pts',(-78.317422570331,-3.95423021099219,133.732169500229));
#93343=CARTESIAN_POINT('Ctrl Pts',(-78.3251688464151,-3.8709753766189,133.841392147053));
#93344=CARTESIAN_POINT('Ctrl Pts',(-78.3329151224992,-3.78330033529861,
133.946942618951));
#93345=CARTESIAN_POINT('Ctrl Pts',(-78.3406614557645,-3.69562464678121,
134.052493869999));
#93346=CARTESIAN_POINT('Ctrl Pts',(-78.3484077890298,-3.60352893602056,
134.154372591285));
#93347=CARTESIAN_POINT('Ctrl Pts',(-78.3561541222952,-3.50736272409399,
134.252199039554));
#93348=CARTESIAN_POINT('Ctrl Pts',(-78.3639021902981,-3.41117497641089,
134.350047395378));
#93349=CARTESIAN_POINT('Ctrl Pts',(-78.3716502583012,-3.31091518768766,
134.443841393651));
#93350=CARTESIAN_POINT('Ctrl Pts',(-78.3793983263041,-3.20696921744136,
134.533238666106));
#93351=CARTESIAN_POINT('Ctrl Pts',(-78.387154629046,-3.10291277218105,134.622730951046));
#93352=CARTESIAN_POINT('Ctrl Pts',(-78.3949109317877,-2.99516261622621,
134.707816920224));
#93353=CARTESIAN_POINT('Ctrl Pts',(-78.4026672345296,-2.88413756189644,
134.788194648567));
#93354=CARTESIAN_POINT('Ctrl Pts',(-78.4104276770437,-2.77305325015197,
134.868615276923));
#93355=CARTESIAN_POINT('Ctrl Pts',(-78.418188119558,-2.65869088301477,134.94432244151));
#93356=CARTESIAN_POINT('Ctrl Pts',(-78.4259485620721,-2.54149679217376,
135.01505855471));
#93357=CARTESIAN_POINT('Ctrl Pts',(-78.4337214623376,-2.42411457097413,
135.085908219799));
#93358=CARTESIAN_POINT('Ctrl Pts',(-78.441494362603,-2.30389188532504,135.15177069902));
#93359=CARTESIAN_POINT('Ctrl Pts',(-78.4492672628685,-2.18129890815822,
135.212434815645));
#93360=CARTESIAN_POINT('Ctrl Pts',(-78.4567575986306,-2.0631624945035,135.270893638827));
#93361=CARTESIAN_POINT('Ctrl Pts',(-78.4642479343927,-1.94282541086829,
135.324525359456));
#93362=CARTESIAN_POINT('Ctrl Pts',(-78.4717382701548,-1.8207226226696,135.373184557466));
#93363=CARTESIAN_POINT('Ctrl Pts',(-78.4795126042738,-1.69399027014527,
135.423688683757));
#93364=CARTESIAN_POINT('Ctrl Pts',(-78.4872869383929,-1.56495422658384,
135.468995759522));
#93365=CARTESIAN_POINT('Ctrl Pts',(-78.495061272512,-1.43407980743096,135.508890154982));
#93366=CARTESIAN_POINT('Ctrl Pts',(-78.5028260254591,-1.3033666793031,135.548735384164));
#93367=CARTESIAN_POINT('Ctrl Pts',(-78.5105907784062,-1.17082005390523,
135.583181092731));
#93368=CARTESIAN_POINT('Ctrl Pts',(-78.5183555313533,-1.03692565750349,
135.612059468712));
#93369=CARTESIAN_POINT('Ctrl Pts',(-78.5261125722382,-0.903164246903833,
135.640909162282));
#93370=CARTESIAN_POINT('Ctrl Pts',(-78.5338696131232,-0.768058108928924,
135.664202445432));
#93371=CARTESIAN_POINT('Ctrl Pts',(-78.5416266540082,-0.63210824404421,
135.68182125096));
#93372=CARTESIAN_POINT('Ctrl Pts',(-78.5493778452483,-0.496260900009957,
135.69942677001));
#93373=CARTESIAN_POINT('Ctrl Pts',(-78.5571290364885,-0.35957148165881,
135.711366278817));
#93374=CARTESIAN_POINT('Ctrl Pts',(-78.5648802277286,-0.222550949145562,
135.717572819124));
#93375=CARTESIAN_POINT('Ctrl Pts',(-78.5726281245057,-0.0855886540139603,
135.723776721485));
#93376=CARTESIAN_POINT('Ctrl Pts',(-78.5803760212827,0.0517040856267704,
135.724252484031));
#93377=CARTESIAN_POINT('Ctrl Pts',(-78.5881239180598,0.188811640964827,
135.718985041338));
#93378=CARTESIAN_POINT('Ctrl Pts',(-78.5958701941439,0.325890516358004,
135.71371870048));
#93379=CARTESIAN_POINT('Ctrl Pts',(-78.603616470228,0.462783894068173,135.702711558942));
#93380=CARTESIAN_POINT('Ctrl Pts',(-78.6113627463122,0.598976996836243,
135.686000671868));
#93381=CARTESIAN_POINT('Ctrl Pts',(-78.6191090795775,0.735171104951045,
135.669289661437));
#93382=CARTESIAN_POINT('Ctrl Pts',(-78.6268554128428,0.870664539753861,
135.646874869069));
#93383=CARTESIAN_POINT('Ctrl Pts',(-78.6346017461082,1.00494888780859,135.61884509624));
#93384=CARTESIAN_POINT('Ctrl Pts',(-78.6423498141112,1.13926330791182,135.590809046337));
#93385=CARTESIAN_POINT('Ctrl Pts',(-78.6500978821142,1.27236771982945,135.557155593692));
#93386=CARTESIAN_POINT('Ctrl Pts',(-78.6578459501171,1.4037655129478,135.518024314433));
#93387=CARTESIAN_POINT('Ctrl Pts',(-78.665602252859,1.53530295720451,135.478851445984));
#93388=CARTESIAN_POINT('Ctrl Pts',(-78.6733585556009,1.665129784072,135.434189232817));
#93389=CARTESIAN_POINT('Ctrl Pts',(-78.6811148583427,1.79276559714513,135.384226835721));
#93390=CARTESIAN_POINT('Ctrl Pts',(-78.6888753008569,1.92046953329473,135.334237772188));
#93391=CARTESIAN_POINT('Ctrl Pts',(-78.696635743371,2.04597976789403,135.278943045515));
#93392=CARTESIAN_POINT('Ctrl Pts',(-78.7043961858852,2.16883833200463,135.218578934791));
#93393=CARTESIAN_POINT('Ctrl Pts',(-78.7121690861506,2.29189411958921,135.158117922239));
#93394=CARTESIAN_POINT('Ctrl Pts',(-78.7199419864161,2.41228938687595,135.092571450718));
#93395=CARTESIAN_POINT('Ctrl Pts',(-78.7277148866815,2.5295923249478,135.022220943853));
#93396=CARTESIAN_POINT('Ctrl Pts',(-78.7352052224436,2.64263100575247,134.954427855115));
#93397=CARTESIAN_POINT('Ctrl Pts',(-78.7426955582056,2.75279802434725,134.882174113557));
#93398=CARTESIAN_POINT('Ctrl Pts',(-78.7501858939676,2.85973592528007,134.805747064807));
#93399=CARTESIAN_POINT('Ctrl Pts',(-78.7579602280867,2.97072840922998,134.726422261274));
#93400=CARTESIAN_POINT('Ctrl Pts',(-78.7657345622058,3.07859366866015,134.642350164472));
#93401=CARTESIAN_POINT('Ctrl Pts',(-78.7735088963248,3.18289877376601,134.553805704303));
#93402=CARTESIAN_POINT('Ctrl Pts',(-78.7812736492719,3.28707533215155,134.465370367268));
#93403=CARTESIAN_POINT('Ctrl Pts',(-78.789038402219,3.38770017098097,134.372473884269));
#93404=CARTESIAN_POINT('Ctrl Pts',(-78.7968031551661,3.48436955837914,134.275434204101));
#93405=CARTESIAN_POINT('Ctrl Pts',(-78.8045601960511,3.58094293237893,134.178490905111));
#93406=CARTESIAN_POINT('Ctrl Pts',(-78.8123172369362,3.67356839891922,134.077412873341));
#93407=CARTESIAN_POINT('Ctrl Pts',(-78.8200742778212,3.76187582173067,133.972557796464));
#93408=CARTESIAN_POINT('Ctrl Pts',(-78.8278254690613,3.85011665122776,133.867781791616));
#93409=CARTESIAN_POINT('Ctrl Pts',(-78.8355766603014,3.93404566757502,133.759234708861));
#93410=CARTESIAN_POINT('Ctrl Pts',(-78.8433278515415,4.01333035044917,133.647310240873));
#93411=CARTESIAN_POINT('Ctrl Pts',(-78.8510757483186,4.09258133521822,133.53543334377));
#93412=CARTESIAN_POINT('Ctrl Pts',(-78.8588236450958,4.16719168706052,133.420182234855));
#93413=CARTESIAN_POINT('Ctrl Pts',(-78.8665715418728,4.23687002103937,133.301982584021));
#93414=CARTESIAN_POINT('Ctrl Pts',(-78.8743178179569,4.30653377981264,133.183807658006));
#93415=CARTESIAN_POINT('Ctrl Pts',(-78.882064094041,4.37126737435724,133.062685753451));
#93416=CARTESIAN_POINT('Ctrl Pts',(-78.8898103701251,4.4308237305321,132.939069996253));
#93417=CARTESIAN_POINT('Ctrl Pts',(-78.8975567033905,4.49038052633853,132.815453326551));
#93418=CARTESIAN_POINT('Ctrl Pts',(-78.9053030366558,4.54475983782165,132.689343119692));
#93419=CARTESIAN_POINT('Ctrl Pts',(-78.9130493699211,4.59376156629696,132.561215117664));
#93420=CARTESIAN_POINT('Ctrl Pts',(-78.9207974379241,4.64277426836968,132.433058422257));
#93421=CARTESIAN_POINT('Ctrl Pts',(-78.9285455059271,4.6864068514414,132.302883397612));
#93422=CARTESIAN_POINT('Ctrl Pts',(-78.9362935739301,4.72450831469506,132.171183300608));
#93423=CARTESIAN_POINT('Ctrl Pts',(-78.944049876672,4.76265027263722,132.039343231173));
#93424=CARTESIAN_POINT('Ctrl Pts',(-78.9518061794138,4.79524925891879,131.905975227691));
#93425=CARTESIAN_POINT('Ctrl Pts',(-78.9595624821557,4.82220475387671,131.771585707289));
#93426=CARTESIAN_POINT('Ctrl Pts',(-78.9673229246699,4.84917463579392,131.637124459152));
#93427=CARTESIAN_POINT('Ctrl Pts',(-78.975083367184,4.87049496377423,131.501640993734));
#93428=CARTESIAN_POINT('Ctrl Pts',(-78.9828438096982,4.88611698271115,131.365648327891));
#93429=CARTESIAN_POINT('Ctrl Pts',(-78.9906167099636,4.90176407949974,131.229437354548));
#93430=CARTESIAN_POINT('Ctrl Pts',(-78.9983896102291,4.91169455942326,131.09271593749));
#93431=CARTESIAN_POINT('Ctrl Pts',(-79.0061625104945,4.91591178887908,130.955999486131));
#93432=CARTESIAN_POINT('Ctrl Pts',(-79.0136528462565,4.91997571142159,130.824253022148));
#93433=CARTESIAN_POINT('Ctrl Pts',(-79.0211431820185,4.91873455684636,130.692511477106));
#93434=CARTESIAN_POINT('Ctrl Pts',(-79.0286335177804,4.91223686376402,130.561230905729));
#93435=CARTESIAN_POINT('Ctrl Pts',(-79.0364078518995,4.90549280867349,130.424972791586));
#93436=CARTESIAN_POINT('Ctrl Pts',(-79.0441821860186,4.89306438006664,130.288779672029));
#93437=CARTESIAN_POINT('Ctrl Pts',(-79.0519565201377,4.87494887512056,130.15316438949));
#93438=CARTESIAN_POINT('Ctrl Pts',(-79.0597212730848,4.8568556959153,130.017716240666));
#93439=CARTESIAN_POINT('Ctrl Pts',(-79.0674860260318,4.83308943708872,129.882844895731));
#93440=CARTESIAN_POINT('Ctrl Pts',(-79.0752507789789,4.80369937102654,129.749061884837));
#93441=CARTESIAN_POINT('Ctrl Pts',(-79.0830078198639,4.7743384955923,129.615411749115));
#93442=CARTESIAN_POINT('Ctrl Pts',(-79.0907648607489,4.73936501195307,129.482848175685));
#93443=CARTESIAN_POINT('Ctrl Pts',(-79.0985219016339,4.698879785185,129.351875909598));
#93444=CARTESIAN_POINT('Ctrl Pts',(-79.106273092874,4.65842508864131,129.221002410716));
#93445=CARTESIAN_POINT('Ctrl Pts',(-79.1140242841143,4.61246703712198,129.091718202631));
#93446=CARTESIAN_POINT('Ctrl Pts',(-79.1217754753544,4.56115712006781,128.964515844615));
#93447=CARTESIAN_POINT('Ctrl Pts',(-79.1295233721315,4.50986901109719,128.837367550995));
#93448=CARTESIAN_POINT('Ctrl Pts',(-79.1372712689084,4.45323370671615,128.712299709382));
#93449=CARTESIAN_POINT('Ctrl Pts',(-79.1450191656855,4.39145183438493,128.58978755515));
#93450=CARTESIAN_POINT('Ctrl Pts',(-79.1527654417696,4.32968288548955,128.46730102782));
#93451=CARTESIAN_POINT('Ctrl Pts',(-79.1605117178537,4.26276968589406,128.3473694734));
#93452=CARTESIAN_POINT('Ctrl Pts',(-79.1682579939378,4.19095991364083,128.230445687978));
#93453=CARTESIAN_POINT('Ctrl Pts',(-79.1760043272032,4.11914961130408,128.113521039451));
#93454=CARTESIAN_POINT('Ctrl Pts',(-79.1837506604685,4.04244286879164,127.999604537378));
#93455=CARTESIAN_POINT('Ctrl Pts',(-79.1914969937339,3.96113178308632,127.889121680614));
#93456=CARTESIAN_POINT('Ctrl Pts',(-79.1992450617368,3.87980248832723,127.77861408198));
#93457=CARTESIAN_POINT('Ctrl Pts',(-79.2069931297399,3.79386703028029,127.67154197358));
#93458=CARTESIAN_POINT('Ctrl Pts',(-79.2147411977429,3.70365878029909,127.568299014071));
#93459=CARTESIAN_POINT('Ctrl Pts',(-79.2224975004847,3.6133546559162,127.464946326716));
#93460=CARTESIAN_POINT('Ctrl Pts',(-79.2302538032266,3.5187689257682,127.365431212729));
#93461=CARTESIAN_POINT('Ctrl Pts',(-79.2380101059685,3.42027331959384,127.270111972978));
#93462=CARTESIAN_POINT('Ctrl Pts',(-79.2457705484826,3.32172514334882,127.174741858478));
#93463=CARTESIAN_POINT('Ctrl Pts',(-79.2535309909968,3.21926322485227,127.083572340298));
#93464=CARTESIAN_POINT('Ctrl Pts',(-79.2612914335109,3.11329282639065,126.996921735634));
#93465=CARTESIAN_POINT('Ctrl Pts',(-79.2690643337764,3.00715231483781,126.910132031727));
#93466=CARTESIAN_POINT('Ctrl Pts',(-79.2768372340418,2.89749238147942,126.827875972196));
#93467=CARTESIAN_POINT('Ctrl Pts',(-79.2846101343073,2.78474847447253,126.750429316172));
#93468=CARTESIAN_POINT('Ctrl Pts',(-79.2921004700693,2.67610309247011,126.675798041171));
#93469=CARTESIAN_POINT('Ctrl Pts',(-79.2995908058313,2.56459432514578,126.605632736604));
#93470=CARTESIAN_POINT('Ctrl Pts',(-79.3070811415933,2.45063210056094,126.540139074283));
#93471=CARTESIAN_POINT('Ctrl Pts',(-79.3148554757124,2.33234896359275,126.472162199848));
#93472=CARTESIAN_POINT('Ctrl Pts',(-79.3226298098315,2.21104796567604,126.409002881004));
#93473=CARTESIAN_POINT('Ctrl Pts',(-79.3304041439506,2.08715911473177,126.350940595573));
#93474=CARTESIAN_POINT('Ctrl Pts',(-79.3381688968977,1.96342294572437,126.292949866719));
#93475=CARTESIAN_POINT('Ctrl Pts',(-79.3459336498449,1.8371056200571,126.240043837013));
#93476=CARTESIAN_POINT('Ctrl Pts',(-79.3536984027919,1.70866413546114,126.192457546741));
#93477=CARTESIAN_POINT('Ctrl Pts',(-79.3614554436769,1.58035022075839,126.144918519843));
#93478=CARTESIAN_POINT('Ctrl Pts',(-79.369212484562,1.44991670985441,126.102688852645));
#93479=CARTESIAN_POINT('Ctrl Pts',(-79.376969525447,1.31784277909337,126.065956511531));
#93480=CARTESIAN_POINT('Ctrl Pts',(-79.3847207166871,1.18586844631073,126.029251870561));
#93481=CARTESIAN_POINT('Ctrl Pts',(-79.3924719079271,1.05225653109541,125.998036408491));
#93482=CARTESIAN_POINT('Ctrl Pts',(-79.4002230991673,0.917503321256874,
125.972448913283));
#93483=CARTESIAN_POINT('Ctrl Pts',(-79.4079709959444,0.782807385127366,
125.946872293444));
#93484=CARTESIAN_POINT('Ctrl Pts',(-79.4157188927214,0.646971502460888,
125.926918955671));
#93485=CARTESIAN_POINT('Ctrl Pts',(-79.4234667894985,0.510503946279892,
125.912676982729));
#93486=CARTESIAN_POINT('Ctrl Pts',(-79.4312130655826,0.374064936169748,
125.8984379889));
#93487=CARTESIAN_POINT('Ctrl Pts',(-79.4389593416668,0.23699490397085,125.889908024145));
#93488=CARTESIAN_POINT('Ctrl Pts',(-79.4467056177509,0.099808675887804,
125.887123457258));
#93489=CARTESIAN_POINT('Ctrl Pts',(-79.4544519510163,-0.0373785648730006,
125.884338869815));
#93490=CARTESIAN_POINT('Ctrl Pts',(-79.4621982842816,-0.174681612344805,
125.887299772803));
#93491=CARTESIAN_POINT('Ctrl Pts',(-79.469944617547,-0.311584596734984,
125.895990409281));
#93492=CARTESIAN_POINT('Ctrl Pts',(-79.47769268555,-0.448518239599112,125.904682991968));
#93493=CARTESIAN_POINT('Ctrl Pts',(-79.4854407535529,-0.585051251000035,
125.91910783667));
#93494=CARTESIAN_POINT('Ctrl Pts',(-79.4931888215558,-0.720672239401334,
125.939197250745));
#93495=CARTESIAN_POINT('Ctrl Pts',(-79.5009451242977,-0.856437367403201,
125.959308016089));
#93496=CARTESIAN_POINT('Ctrl Pts',(-79.5087014270396,-0.991288148744622,
125.985095319768));
#93497=CARTESIAN_POINT('Ctrl Pts',(-79.5164577297814,-1.12472220575496,
126.016440085395));
#93498=CARTESIAN_POINT('Ctrl Pts',(-79.5242181722956,-1.25822748053915,
126.047801580668));
#93499=CARTESIAN_POINT('Ctrl Pts',(-79.5319786148098,-1.39031414795729,
126.084726343056));
#93500=CARTESIAN_POINT('Ctrl Pts',(-79.539739057324,-1.52049534457306,126.12704547214));
#93501=CARTESIAN_POINT('Ctrl Pts',(-79.5475119575894,-1.65088551960258,
126.169432535647));
#93502=CARTESIAN_POINT('Ctrl Pts',(-79.5552848578548,-1.77936374467216,
126.217231133919));
#93503=CARTESIAN_POINT('Ctrl Pts',(-79.5630577581203,-1.90546264544854,
126.270223966637));
#93504=CARTESIAN_POINT('Ctrl Pts',(-79.5705480938823,-2.0269775335574,126.321290376404));
#93505=CARTESIAN_POINT('Ctrl Pts',(-79.5780384296443,-2.14628280396557,
126.377179799445));
#93506=CARTESIAN_POINT('Ctrl Pts',(-79.5855287654063,-2.26298384302322,
126.43765852231));
#93507=CARTESIAN_POINT('Ctrl Pts',(-79.5933039768102,-2.38412330573238,
126.500437397736));
#93508=CARTESIAN_POINT('Ctrl Pts',(-79.601079188214,-2.50284030305716,126.568360453214));
#93509=CARTESIAN_POINT('Ctrl Pts',(-79.6088543996178,-2.61866711537292,
126.641216901411));
#93510=CARTESIAN_POINT('Ctrl Pts',(-79.6166198354763,-2.73434830203286,
126.71398174933));
#93511=CARTESIAN_POINT('Ctrl Pts',(-79.6243852713348,-2.84714620647429,
126.791667441216));
#93512=CARTESIAN_POINT('Ctrl Pts',(-79.6321507071932,-2.95661595060341,
126.874016461752));
#93513=CARTESIAN_POINT('Ctrl Pts',(-79.6399683387051,-3.06682149951219,
126.95691899416));
#93514=CARTESIAN_POINT('Ctrl Pts',(-79.6477859702169,-3.1736536130799,127.044547616851));
#93515=CARTESIAN_POINT('Ctrl Pts',(-79.6556036017287,-3.27668541495413,
127.136593482929));
#93516=CARTESIAN_POINT('Ctrl Pts',(-79.6633544764349,-3.3788374012524,127.227853345217));
#93517=CARTESIAN_POINT('Ctrl Pts',(-79.6711053511411,-3.47725342455917,
127.323455045077));
#93518=CARTESIAN_POINT('Ctrl Pts',(-79.6788562258473,-3.57154877839179,
127.423055782733));
#93519=CARTESIAN_POINT('Ctrl Pts',(-79.6866035385961,-3.66580079827105,
127.522610748317));
#93520=CARTESIAN_POINT('Ctrl Pts',(-79.6943508513448,-3.75593564865222,
127.626160811545));
#93521=CARTESIAN_POINT('Ctrl Pts',(-79.7020981640935,-3.84160486831608,
127.7333257597));
#93522=CARTESIAN_POINT('Ctrl Pts',(-79.7098435942767,-3.92725327070679,
127.840464667207));
#93523=CARTESIAN_POINT('Ctrl Pts',(-79.7175890244597,-4.00843795881415,
127.951216405861));
#93524=CARTESIAN_POINT('Ctrl Pts',(-79.7253344546428,-4.08485048633842,
128.06516738474));
#93525=CARTESIAN_POINT('Ctrl Pts',(-79.733204405379,-4.16249147115516,128.180950313373));
#93526=CARTESIAN_POINT('Ctrl Pts',(-79.7410743561153,-4.2352052709196,128.300035912439));
#93527=CARTESIAN_POINT('Ctrl Pts',(-79.7489443068515,-4.30271412888976,
128.421959688345));
#93528=CARTESIAN_POINT('Ctrl Pts',(-79.7566934781813,-4.36918693465726,
128.542012311333));
#93529=CARTESIAN_POINT('Ctrl Pts',(-79.7644426495111,-4.43061327347606,
128.664816244655));
#93530=CARTESIAN_POINT('Ctrl Pts',(-79.7721918208409,-4.4867747180714,128.789903943479));
#93531=CARTESIAN_POINT('Ctrl Pts',(-79.7801221612803,-4.54424917001703,
128.917916087518));
#93532=CARTESIAN_POINT('Ctrl Pts',(-79.7880525017197,-4.59620932889364,
129.048319707534));
#93533=CARTESIAN_POINT('Ctrl Pts',(-79.7959828421592,-4.64247390309608,
129.18059366336));
#93534=CARTESIAN_POINT('Ctrl Pts',(-79.8039131825986,-4.68873847729852,
129.312867619186));
#93535=CARTESIAN_POINT('Ctrl Pts',(-79.8118435230381,-4.72930737185479,
129.447011483947));
#93536=CARTESIAN_POINT('Ctrl Pts',(-79.8197738634775,-4.76405452823417,
129.582490119309));
#93537=CARTESIAN_POINT('Origin',(213.235140564004,0.,130.804360617566));
#93538=CARTESIAN_POINT('',(-81.9152188971548,-4.76405452823409,129.582490119308));
#93539=CARTESIAN_POINT('',(-81.5701083236629,-4.76405452823402,129.582490119308));
#93540=CARTESIAN_POINT('',(213.235140564004,-4.76405452823405,129.582490119308));
#93541=CARTESIAN_POINT('',(-80.2351405639591,-4.91824936580377,130.801862964505));
#93542=CARTESIAN_POINT('Ctrl Pts',(-80.2351405640087,-4.91824936580422,
130.801862965385));
#93543=CARTESIAN_POINT('Ctrl Pts',(-80.2429981429322,-4.91832015776003,
130.941262876391));
#93544=CARTESIAN_POINT('Ctrl Pts',(-80.2508557218557,-4.91245999970312,
131.080655168156));
#93545=CARTESIAN_POINT('Ctrl Pts',(-80.2587133007792,-4.90069735131702,
131.219509426181));
#93546=CARTESIAN_POINT('Ctrl Pts',(-80.2665731437013,-4.88893131376744,
131.358403692184));
#93547=CARTESIAN_POINT('Ctrl Pts',(-80.2744329866233,-4.87125942953433,
131.496759241733));
#93548=CARTESIAN_POINT('Ctrl Pts',(-80.2822928295454,-4.84776201245914,
131.634051242473));
#93549=CARTESIAN_POINT('Ctrl Pts',(-80.290156443864,-4.82425332059426,131.771409120173));
#93550=CARTESIAN_POINT('Ctrl Pts',(-80.2980200581826,-4.79491359097808,
131.907702062928));
#93551=CARTESIAN_POINT('Ctrl Pts',(-80.3058836725012,-4.75987413255851,
132.042416070565));
#93552=CARTESIAN_POINT('Ctrl Pts',(-80.3138335865165,-4.72445013154641,
132.178608504984));
#93553=CARTESIAN_POINT('Ctrl Pts',(-80.3217835005318,-4.68320065663003,
132.313186761867));
#93554=CARTESIAN_POINT('Ctrl Pts',(-80.3297334145472,-4.63631250990897,
132.445637368441));
#93555=CARTESIAN_POINT('Ctrl Pts',(-80.3376137588887,-4.58983468121998,
132.576928900152));
#93556=CARTESIAN_POINT('Ctrl Pts',(-80.3454941032303,-4.53781668310194,
132.706129550449));
#93557=CARTESIAN_POINT('Ctrl Pts',(-80.3533744475718,-4.48048797077733,
132.832761614958));
#93558=CARTESIAN_POINT('Ctrl Pts',(-80.361359146424,-4.42240008988507,132.961070589327));
#93559=CARTESIAN_POINT('Ctrl Pts',(-80.3693438452763,-4.35886003026248,
133.086742111878));
#93560=CARTESIAN_POINT('Ctrl Pts',(-80.3773285441286,-4.29015297255464,
133.209307713571));
#93561=CARTESIAN_POINT('Ctrl Pts',(-80.3853132429809,-4.22144591484662,
133.331873315263));
#93562=CARTESIAN_POINT('Ctrl Pts',(-80.3932979418332,-4.14757212034963,
133.451332694959));
#93563=CARTESIAN_POINT('Ctrl Pts',(-80.4012826406855,-4.06885992385342,
133.567250767854));
#93564=CARTESIAN_POINT('Ctrl Pts',(-80.4090569748045,-3.99222147747906,
133.680114865273));
#93565=CARTESIAN_POINT('Ctrl Pts',(-80.4168313089237,-3.91076206017412,
133.789966560684));
#93566=CARTESIAN_POINT('Ctrl Pts',(-80.4246056430427,-3.82474613354405,
133.896366451396));
#93567=CARTESIAN_POINT('Ctrl Pts',(-80.4323703959898,-3.73883621385586,
134.002635213753));
#93568=CARTESIAN_POINT('Ctrl Pts',(-80.4401351489369,-3.64838120142737,
134.105460334563));
#93569=CARTESIAN_POINT('Ctrl Pts',(-80.447899901884,-3.55368926504029,134.204430568323));
#93570=CARTESIAN_POINT('Ctrl Pts',(-80.455656942769,-3.45909137801935,134.303302503451));
#93571=CARTESIAN_POINT('Ctrl Pts',(-80.463413983654,-3.36026521002513,134.398326890205));
#93572=CARTESIAN_POINT('Ctrl Pts',(-80.471171024539,-3.25755946347702,134.489125115388));
#93573=CARTESIAN_POINT('Ctrl Pts',(-80.4789222157791,-3.15493116813146,
134.579854868924));
#93574=CARTESIAN_POINT('Ctrl Pts',(-80.4866734070194,-3.0484294092288,134.666364546477));
#93575=CARTESIAN_POINT('Ctrl Pts',(-80.4944245982595,-2.93843978649981,
134.748312275943));
#93576=CARTESIAN_POINT('Ctrl Pts',(-80.5021724950366,-2.8284969122944,134.830225175438));
#93577=CARTESIAN_POINT('Ctrl Pts',(-80.5099203918136,-2.71506943557235,
134.907579750174));
#93578=CARTESIAN_POINT('Ctrl Pts',(-80.5176682885907,-2.59857591120857,
134.980074484222));
#93579=CARTESIAN_POINT('Ctrl Pts',(-80.5254145646748,-2.48210675477877,
135.052554053935));
#93580=CARTESIAN_POINT('Ctrl Pts',(-80.5331608407589,-2.36257315811835,
135.120175598543));
#93581=CARTESIAN_POINT('Ctrl Pts',(-80.540907116843,-2.24042218753757,135.182681241286));
#93582=CARTESIAN_POINT('Ctrl Pts',(-80.5486534501083,-2.11827031526657,
135.24518734543));
#93583=CARTESIAN_POINT('Ctrl Pts',(-80.5563997833736,-1.99350137856661,
135.302577294256));
#93584=CARTESIAN_POINT('Ctrl Pts',(-80.5641461166389,-1.86658618060849,
135.354639630205));
#93585=CARTESIAN_POINT('Ctrl Pts',(-80.5718941846418,-1.73964256087193,
135.406713625153));
#93586=CARTESIAN_POINT('Ctrl Pts',(-80.5796422526449,-1.61055208510356,
135.453457484778));
#93587=CARTESIAN_POINT('Ctrl Pts',(-80.5873903206479,-1.47980424453522,
135.494708414943));
#93588=CARTESIAN_POINT('Ctrl Pts',(-80.5951466233897,-1.34891744360548,
135.536003187087));
#93589=CARTESIAN_POINT('Ctrl Pts',(-80.6029029261314,-1.21637013259876,
135.571793250013));
#93590=CARTESIAN_POINT('Ctrl Pts',(-80.6106592288733,-1.08266617061231,
135.601965960392));
#93591=CARTESIAN_POINT('Ctrl Pts',(-80.6184196713874,-0.948890846795597,
135.632154774854));
#93592=CARTESIAN_POINT('Ctrl Pts',(-80.6261801139018,-0.813958026352576,
135.656720192708));
#93593=CARTESIAN_POINT('Ctrl Pts',(-80.6339405564159,-0.678379408417407,
135.675601161897));
#93594=CARTESIAN_POINT('Ctrl Pts',(-80.6417134566814,-0.542583147648625,
135.694512440494));
#93595=CARTESIAN_POINT('Ctrl Pts',(-80.6494863569467,-0.406139407117813,
135.707720997712));
#93596=CARTESIAN_POINT('Ctrl Pts',(-80.6572592572121,-0.269563528597922,
135.715217830574));
#93597=CARTESIAN_POINT('Ctrl Pts',(-80.6647495929741,-0.137952527276476,
135.722442134678));
#93598=CARTESIAN_POINT('Ctrl Pts',(-80.6722399287361,-0.00621913625590731,
135.724362771354));
#93599=CARTESIAN_POINT('Ctrl Pts',(-80.6797302644981,0.125179556277915,
135.72101732118));
#93600=CARTESIAN_POINT('Ctrl Pts',(-80.6875045986172,0.261560270176754,
135.717545027245));
#93601=CARTESIAN_POINT('Ctrl Pts',(-80.6952789327363,0.398012417497684,
135.708388437062));
#93602=CARTESIAN_POINT('Ctrl Pts',(-80.7030532668554,0.534023368354635,
135.693532541783));
#93603=CARTESIAN_POINT('Ctrl Pts',(-80.7108180198025,0.669866697870671,
135.678694955067));
#93604=CARTESIAN_POINT('Ctrl Pts',(-80.7185827727496,0.805269527871059,
135.658172080733));
#93605=CARTESIAN_POINT('Ctrl Pts',(-80.7263475256966,0.939719293111635,
135.632000901665));
#93606=CARTESIAN_POINT('Ctrl Pts',(-80.7341045665816,1.07403552094997,135.605855716181));
#93607=CARTESIAN_POINT('Ctrl Pts',(-80.7418616074666,1.20740018652085,135.574073464285));
#93608=CARTESIAN_POINT('Ctrl Pts',(-80.7496186483516,1.33930626964343,135.536742869518));
#93609=CARTESIAN_POINT('Ctrl Pts',(-80.7573698395917,1.47111288136246,135.499440426043));
#93610=CARTESIAN_POINT('Ctrl Pts',(-80.7651210308318,1.60146272530599,135.456598073826));
#93611=CARTESIAN_POINT('Ctrl Pts',(-80.7728722220719,1.72985974871705,135.408355438617));
#93612=CARTESIAN_POINT('Ctrl Pts',(-80.780620118849,1.85820219996823,135.360133307816));
#93613=CARTESIAN_POINT('Ctrl Pts',(-80.7883680156261,1.98459311627731,135.306515596352));
#93614=CARTESIAN_POINT('Ctrl Pts',(-80.7961159124032,2.10855258462038,135.247691469572));
#93615=CARTESIAN_POINT('Ctrl Pts',(-80.8038621884873,2.23248612331493,135.188879647532));
#93616=CARTESIAN_POINT('Ctrl Pts',(-80.8116084645714,2.3539888727009,135.124863743903));
#93617=CARTESIAN_POINT('Ctrl Pts',(-80.8193547406555,2.47260222349409,135.055880499546));
#93618=CARTESIAN_POINT('Ctrl Pts',(-80.8271010739208,2.59121644986393,134.986896745971));
#93619=CARTESIAN_POINT('Ctrl Pts',(-80.8348474071862,2.70694089711576,134.912945775053));
#93620=CARTESIAN_POINT('Ctrl Pts',(-80.8425937404515,2.81934317940427,134.834309388859));
#93621=CARTESIAN_POINT('Ctrl Pts',(-80.8503418084545,2.9317706334047,134.755655392592));
#93622=CARTESIAN_POINT('Ctrl Pts',(-80.8580898764575,3.04087412172568,134.672314117205));
#93623=CARTESIAN_POINT('Ctrl Pts',(-80.8658379444604,3.14625209908134,134.584609391328));
#93624=CARTESIAN_POINT('Ctrl Pts',(-80.8735942472023,3.2517420734052,134.496811451824));
#93625=CARTESIAN_POINT('Ctrl Pts',(-80.8813505499442,3.35349832621974,134.404641048372));
#93626=CARTESIAN_POINT('Ctrl Pts',(-80.889106852686,3.4511537393512,134.308461205429));
#93627=CARTESIAN_POINT('Ctrl Pts',(-80.8968672952002,3.54886127411726,134.212230028408));
#93628=CARTESIAN_POINT('Ctrl Pts',(-80.9046277377143,3.64246334125349,134.111985433467));
#93629=CARTESIAN_POINT('Ctrl Pts',(-80.9123881802285,3.73163199005489,134.008124927452));
#93630=CARTESIAN_POINT('Ctrl Pts',(-80.9201610804939,3.82094378028736,133.904097695332));
#93631=CARTESIAN_POINT('Ctrl Pts',(-80.9279339807593,3.90580768814124,133.79644325995));
#93632=CARTESIAN_POINT('Ctrl Pts',(-80.9357068810247,3.98593758434089,133.685590326603));
#93633=CARTESIAN_POINT('Ctrl Pts',(-80.9431972167869,4.06315455697952,133.578767176604));
#93634=CARTESIAN_POINT('Ctrl Pts',(-80.950687552549,4.13597555862536,133.468974294892));
#93635=CARTESIAN_POINT('Ctrl Pts',(-80.9581778883111,4.20418513955255,133.35661655592));
#93636=CARTESIAN_POINT('Ctrl Pts',(-80.9659522224301,4.27498090747135,133.239998739128));
#93637=CARTESIAN_POINT('Ctrl Pts',(-80.9737265565493,4.34103292747858,133.120248322405));
#93638=CARTESIAN_POINT('Ctrl Pts',(-80.9815008906683,4.40205148322949,132.997788483145));
#93639=CARTESIAN_POINT('Ctrl Pts',(-80.9892656436154,4.46299483906398,132.875479564691));
#93640=CARTESIAN_POINT('Ctrl Pts',(-80.9970303965624,4.51891690066217,132.750468214128));
#93641=CARTESIAN_POINT('Ctrl Pts',(-81.0047951495095,4.56957172873663,132.623205657263));
#93642=CARTESIAN_POINT('Ctrl Pts',(-81.0125521903944,4.62017624572146,132.496069499364));
#93643=CARTESIAN_POINT('Ctrl Pts',(-81.0203092312795,4.66552379643557,132.366686945663));
#93644=CARTESIAN_POINT('Ctrl Pts',(-81.0280662721644,4.70541496971352,132.235532523836));
#93645=CARTESIAN_POINT('Ctrl Pts',(-81.0358174634046,4.74527606074778,132.104477006578));
#93646=CARTESIAN_POINT('Ctrl Pts',(-81.0435686546447,4.7796888510925,131.971652653312));
#93647=CARTESIAN_POINT('Ctrl Pts',(-81.0513198458848,4.80850268321464,131.8375522784));
#93648=CARTESIAN_POINT('Ctrl Pts',(-81.0590677426619,4.83730426868938,131.703508899726));
#93649=CARTESIAN_POINT('Ctrl Pts',(-81.066815639439,4.8605115470373,131.568190959527));
#93650=CARTESIAN_POINT('Ctrl Pts',(-81.0745635362161,4.8780242637094,131.432104470712));
#93651=CARTESIAN_POINT('Ctrl Pts',(-81.0823098123002,4.89553331709871,131.296046448256));
#93652=CARTESIAN_POINT('Ctrl Pts',(-81.0900560883843,4.90735012826414,131.159220584475));
#93653=CARTESIAN_POINT('Ctrl Pts',(-81.0978023644684,4.91342598447547,131.022140684563));
#93654=CARTESIAN_POINT('Ctrl Pts',(-81.1055486977337,4.91950188553737,130.885059772759));
#93655=CARTESIAN_POINT('Ctrl Pts',(-81.1132950309991,4.91983672977018,130.747725211666));
#93656=CARTESIAN_POINT('Ctrl Pts',(-81.1210413642644,4.91443389012269,130.61065310064));
#93657=CARTESIAN_POINT('Ctrl Pts',(-81.1287894322674,4.90902984054669,130.473550293265));
#93658=CARTESIAN_POINT('Ctrl Pts',(-81.1365375002703,4.89788556565461,130.336710443499));
#93659=CARTESIAN_POINT('Ctrl Pts',(-81.1442855682733,4.88105646660766,130.200646420046));
#93660=CARTESIAN_POINT('Ctrl Pts',(-81.1520418710152,4.86420948139404,130.06443778613));
#93661=CARTESIAN_POINT('Ctrl Pts',(-81.159798173757,4.84166565074942,129.929007014297));
#93662=CARTESIAN_POINT('Ctrl Pts',(-81.1675544764989,4.81353196109052,129.794859195051));
#93663=CARTESIAN_POINT('Ctrl Pts',(-81.175314919013,4.78538325563429,129.660639777074));
#93664=CARTESIAN_POINT('Ctrl Pts',(-81.1830753615273,4.75163884248064,129.527705054868));
#93665=CARTESIAN_POINT('Ctrl Pts',(-81.1908358040414,4.71245589003037,129.396545804809));
#93666=CARTESIAN_POINT('Ctrl Pts',(-81.1986087043069,4.67321003762633,129.265176006278));
#93667=CARTESIAN_POINT('Ctrl Pts',(-81.2063816045722,4.62850832731785,129.1355877452));
#93668=CARTESIAN_POINT('Ctrl Pts',(-81.2141545048376,4.57855678115273,129.008253475923));
#93669=CARTESIAN_POINT('Ctrl Pts',(-81.2216448405997,4.53042109951067,128.88554812807));
#93670=CARTESIAN_POINT('Ctrl Pts',(-81.2291351763618,4.47741076877118,128.764936022581));
#93671=CARTESIAN_POINT('Ctrl Pts',(-81.2366255121239,4.41974996544118,128.646817267948));
#93672=CARTESIAN_POINT('Ctrl Pts',(-81.244399846243,4.35990293522789,128.524220004832));
#93673=CARTESIAN_POINT('Ctrl Pts',(-81.2521741803621,4.2948562483551,128.403920544404));
#93674=CARTESIAN_POINT('Ctrl Pts',(-81.2599485144812,4.22480933718678,128.286391370947));
#93675=CARTESIAN_POINT('Ctrl Pts',(-81.2677132674283,4.15484875257602,128.169007041692));
#93676=CARTESIAN_POINT('Ctrl Pts',(-81.2754780203754,4.07990040310759,128.054386538923));
#93677=CARTESIAN_POINT('Ctrl Pts',(-81.2832427733225,4.00021098164112,127.942980676898));
#93678=CARTESIAN_POINT('Ctrl Pts',(-81.2909998142075,3.92060070883148,127.831685464746));
#93679=CARTESIAN_POINT('Ctrl Pts',(-81.2987568550926,3.83625896093346,127.723598855399));
#93680=CARTESIAN_POINT('Ctrl Pts',(-81.3065138959776,3.74747718491634,127.619145112921));
#93681=CARTESIAN_POINT('Ctrl Pts',(-81.3142650872177,3.65876235992774,127.514770139823));
#93682=CARTESIAN_POINT('Ctrl Pts',(-81.3220162784578,3.56561442350507,127.41402287733));
#93683=CARTESIAN_POINT('Ctrl Pts',(-81.3297674696979,3.46836656025204,127.317296456094));
#93684=CARTESIAN_POINT('Ctrl Pts',(-81.337515366475,3.37116002993441,127.220611146165));
#93685=CARTESIAN_POINT('Ctrl Pts',(-81.345263263252,3.26985731525767,127.127943553625));
#93686=CARTESIAN_POINT('Ctrl Pts',(-81.3530111600291,3.16482994918056,127.0396515378));
#93687=CARTESIAN_POINT('Ctrl Pts',(-81.3607574361132,3.05982455256459,126.951377990763));
#93688=CARTESIAN_POINT('Ctrl Pts',(-81.3685037121973,2.95109635333172,126.867478451328));
#93689=CARTESIAN_POINT('Ctrl Pts',(-81.3762499882814,2.839051299925,126.788271627156));
#93690=CARTESIAN_POINT('Ctrl Pts',(-81.3839963215468,2.727005419427,126.709064218296));
#93691=CARTESIAN_POINT('Ctrl Pts',(-81.3917426548122,2.6116429551485,126.634549819506));
#93692=CARTESIAN_POINT('Ctrl Pts',(-81.3994889880775,2.49339993925729,126.565004557336));
#93693=CARTESIAN_POINT('Ctrl Pts',(-81.4072370560806,2.37513044366202,126.495443720986));
#93694=CARTESIAN_POINT('Ctrl Pts',(-81.4149851240835,2.25397944975393,126.430854433777));
#93695=CARTESIAN_POINT('Ctrl Pts',(-81.4227331920866,2.13040839418066,126.371467303205));
#93696=CARTESIAN_POINT('Ctrl Pts',(-81.4304894948284,2.00670600581951,126.312017055284));
#93697=CARTESIAN_POINT('Ctrl Pts',(-81.4382457975703,1.8805787707504,126.257780178224));
#93698=CARTESIAN_POINT('Ctrl Pts',(-81.4460021003122,1.75250946469014,126.208939675076));
#93699=CARTESIAN_POINT('Ctrl Pts',(-81.4537625428264,1.62437180418514,126.160073104282));
#93700=CARTESIAN_POINT('Ctrl Pts',(-81.4615229853405,1.49429037792357,126.116608770296));
#93701=CARTESIAN_POINT('Ctrl Pts',(-81.4692834278547,1.36276304332975,126.078679719512));
#93702=CARTESIAN_POINT('Ctrl Pts',(-81.4770563281201,1.231024569382,126.040689781648));
#93703=CARTESIAN_POINT('Ctrl Pts',(-81.4848292283855,1.09783592888468,126.008252976067));
#93704=CARTESIAN_POINT('Ctrl Pts',(-81.492602128651,0.963705971011835,125.981451343701));
#93705=CARTESIAN_POINT('Ctrl Pts',(-81.500092464413,0.834451974961738,125.95562401818));
#93706=CARTESIAN_POINT('Ctrl Pts',(-81.5075828001749,0.704324216090279,
125.935029321632));
#93707=CARTESIAN_POINT('Ctrl Pts',(-81.5150731359369,0.573780489878895,
125.919694916422));
#93708=CARTESIAN_POINT('Ctrl Pts',(-81.522847470056,0.438287158609339,125.903779102578));
#93709=CARTESIAN_POINT('Ctrl Pts',(-81.5306218041751,0.301916492385118,
125.893479925623));
#93710=CARTESIAN_POINT('Ctrl Pts',(-81.5383961382941,0.165173803679244,
125.888884986757));
#93711=CARTESIAN_POINT('Ctrl Pts',(-81.5461608912412,0.0285996381161548,
125.884295710743));
#93712=CARTESIAN_POINT('Ctrl Pts',(-81.5539256441882,-0.108345250687616,
125.88539669829));
#93713=CARTESIAN_POINT('Ctrl Pts',(-81.5616903971353,-0.245148236411733,
125.892224075827));
#93714=CARTESIAN_POINT('Ctrl Pts',(-81.5694474380203,-0.381815347482217,
125.899044672317));
#93715=CARTESIAN_POINT('Ctrl Pts',(-81.5772044789055,-0.518340447997844,
125.911580320992));
#93716=CARTESIAN_POINT('Ctrl Pts',(-81.5849615197905,-0.654209058381405,
125.929815144352));
#93717=CARTESIAN_POINT('Ctrl Pts',(-81.5927127110307,-0.789975209189526,
125.94803621669));
#93718=CARTESIAN_POINT('Ctrl Pts',(-81.6004639022708,-0.92508546933795,
125.971947857423));
#93719=CARTESIAN_POINT('Ctrl Pts',(-81.608215093511,-1.05902899246004,126.001482245628));
#93720=CARTESIAN_POINT('Ctrl Pts',(-81.6159629902881,-1.19291558601083,
126.03100408093));
#93721=CARTESIAN_POINT('Ctrl Pts',(-81.6237108870652,-1.32563604783668,
126.06614382653));
#93722=CARTESIAN_POINT('Ctrl Pts',(-81.6314587838422,-1.45668847810984,
126.106782332934));
#93723=CARTESIAN_POINT('Ctrl Pts',(-81.6392050599264,-1.58771349504011,
126.14741233864));
#93724=CARTESIAN_POINT('Ctrl Pts',(-81.6469513360104,-1.71707080124438,
126.193538701573));
#93725=CARTESIAN_POINT('Ctrl Pts',(-81.6546976120946,-1.8442728338938,126.244992155086));
#93726=CARTESIAN_POINT('Ctrl Pts',(-81.6624439453599,-1.97147580551956,
126.296445988416));
#93727=CARTESIAN_POINT('Ctrl Pts',(-81.6701902786253,-2.096523109407,126.353226844186));
#93728=CARTESIAN_POINT('Ctrl Pts',(-81.6779366118907,-2.21894674643024,
126.415117129332));
#93729=CARTESIAN_POINT('Ctrl Pts',(-81.6856846798936,-2.34139779937766,
126.477021274377));
#93730=CARTESIAN_POINT('Ctrl Pts',(-81.6934327478966,-2.46122366745418,
126.544036949308));
#93731=CARTESIAN_POINT('Ctrl Pts',(-81.7011808158995,-2.5779809162625,126.61590058339));
#93732=CARTESIAN_POINT('Ctrl Pts',(-81.7089371186414,-2.69486225606475,
126.687840594998));
#93733=CARTESIAN_POINT('Ctrl Pts',(-81.7166934213832,-2.80866812818763,
126.76463865311));
#93734=CARTESIAN_POINT('Ctrl Pts',(-81.7244497241251,-2.91898361491308,
126.845987502463));
#93735=CARTESIAN_POINT('Ctrl Pts',(-81.7322101666393,-3.02935798033532,
126.927379770146));
#93736=CARTESIAN_POINT('Ctrl Pts',(-81.7399706091535,-3.13623794380125,
127.013327423963));
#93737=CARTESIAN_POINT('Ctrl Pts',(-81.7477310516677,-3.23924246551425,
127.103483517187));
#93738=CARTESIAN_POINT('Ctrl Pts',(-81.7555039519331,-3.34241233922981,
127.193784336976));
#93739=CARTESIAN_POINT('Ctrl Pts',(-81.7632768521986,-3.44169405592559,
127.288306826595));
#93740=CARTESIAN_POINT('Ctrl Pts',(-81.771049752464,-3.53674354683358,127.386667221951));
#93741=CARTESIAN_POINT('Ctrl Pts',(-81.778540088226,-3.62833774933107,127.48145196918));
#93742=CARTESIAN_POINT('Ctrl Pts',(-81.7860304239879,-3.71600188302689,
127.57980020159));
#93743=CARTESIAN_POINT('Ctrl Pts',(-81.7935207597499,-3.79946522514793,
127.681341715063));
#93744=CARTESIAN_POINT('Ctrl Pts',(-81.8012637578307,-3.88574393392626,
127.786308403997));
#93745=CARTESIAN_POINT('Ctrl Pts',(-81.8090067559115,-3.96781483318949,
127.89503003215));
#93746=CARTESIAN_POINT('Ctrl Pts',(-81.8167497539922,-4.0453310506335,128.007133463172));
#93747=CARTESIAN_POINT('Ctrl Pts',(-81.8244831899834,-4.12275154068426,
128.119098453883));
#93748=CARTESIAN_POINT('Ctrl Pts',(-81.8322166259745,-4.19562831494933,
128.234436619325));
#93749=CARTESIAN_POINT('Ctrl Pts',(-81.8399500619657,-4.26365359300274,
128.352740520289));
#93750=CARTESIAN_POINT('Ctrl Pts',(-81.84767405617,-4.33159581868827,128.470899983487));
#93751=CARTESIAN_POINT('Ctrl Pts',(-81.8553980503743,-4.39469814749423,
128.592017632574));
#93752=CARTESIAN_POINT('Ctrl Pts',(-81.8631220445786,-4.45269553496809,
128.715656345685));
#93753=CARTESIAN_POINT('Ctrl Pts',(-81.8708406093801,-4.51065215452198,
128.839208149826));
#93754=CARTESIAN_POINT('Ctrl Pts',(-81.8785591741816,-4.56351080343583,
128.965277137834));
#93755=CARTESIAN_POINT('Ctrl Pts',(-81.8862777389832,-4.6110519036736,129.093400827235));
#93756=CARTESIAN_POINT('Ctrl Pts',(-81.8939921687289,-4.65856753478472,
129.221455877113));
#93757=CARTESIAN_POINT('Ctrl Pts',(-81.9017065984746,-4.70077115122349,
129.351563068366));
#93758=CARTESIAN_POINT('Ctrl Pts',(-81.9094210282204,-4.73749114772036,
129.483239620923));
#93759=CARTESIAN_POINT('Ctrl Pts',(-81.9113536511985,-4.74669026046447,
129.516227299798));
#93760=CARTESIAN_POINT('Ctrl Pts',(-81.9132862741767,-4.75554545824106,
129.549313384549));
#93761=CARTESIAN_POINT('Ctrl Pts',(-81.9152188971548,-4.76405452823409,
129.582490119308));
#93762=CARTESIAN_POINT('Ctrl Pts',(-80.1654084279176,-4.76405452823404,
129.582490119308));
#93763=CARTESIAN_POINT('Ctrl Pts',(-80.1739907747347,-4.80160086113247,
129.728882701434));
#93764=CARTESIAN_POINT('Ctrl Pts',(-80.1825731215518,-4.83243972327195,
129.877179793995));
#93765=CARTESIAN_POINT('Ctrl Pts',(-80.1911554683689,-4.85639332437589,
130.026783006355));
#93766=CARTESIAN_POINT('Ctrl Pts',(-80.1996984730164,-4.88023712024129,
130.175700425528));
#93767=CARTESIAN_POINT('Ctrl Pts',(-80.2082414776637,-4.89725853709734,
130.32591178946));
#93768=CARTESIAN_POINT('Ctrl Pts',(-80.2167844823112,-4.90733053367499,
130.476808948724));
#93769=CARTESIAN_POINT('Ctrl Pts',(-80.2229031761938,-4.9145443262912,130.584884920049));
#93770=CARTESIAN_POINT('Ctrl Pts',(-80.2290218700766,-4.91819424011381,
130.693312303923));
#93771=CARTESIAN_POINT('Ctrl Pts',(-80.2351405639592,-4.91824936580377,
130.801862964505));
#93772=CARTESIAN_POINT('',(-79.8898594360288,-4.91824928709222,130.801712501838));
#93773=CARTESIAN_POINT('Ctrl Pts',(-79.8197738634775,-4.76405452823417,
129.582490119309));
#93774=CARTESIAN_POINT('Ctrl Pts',(-79.827546945423,-4.79811264918998,129.715282216011));
#93775=CARTESIAN_POINT('Ctrl Pts',(-79.8353200273684,-4.82657777092677,
129.849356243151));
#93776=CARTESIAN_POINT('Ctrl Pts',(-79.8430931093139,-4.84938363127091,
129.984201206682));
#93777=CARTESIAN_POINT('Ctrl Pts',(-79.8500542026156,-4.86980715475825,
130.104960048412));
#93778=CARTESIAN_POINT('Ctrl Pts',(-79.8570152959173,-4.88569270901646,
130.226336888437));
#93779=CARTESIAN_POINT('Ctrl Pts',(-79.863976389219,-4.89702818777626,130.347963870618));
#93780=CARTESIAN_POINT('Ctrl Pts',(-79.8726040714764,-4.91107754823396,
130.498710155822));
#93781=CARTESIAN_POINT('Ctrl Pts',(-79.8812317537339,-4.91816766298115,
130.650115038787));
#93782=CARTESIAN_POINT('Ctrl Pts',(-79.8898594359913,-4.91824928709186,
130.80171250118));
#93783=CARTESIAN_POINT('Ctrl Pts',(-79.8898594360288,-4.91824928709222,
130.801712501838));
#93784=CARTESIAN_POINT('Ctrl Pts',(-79.8975364691867,-4.91832191735719,
130.936606058499));
#93785=CARTESIAN_POINT('Ctrl Pts',(-79.9052135023444,-4.91284074513111,
131.071724769537));
#93786=CARTESIAN_POINT('Ctrl Pts',(-79.9128905355022,-4.90177656295177,
131.206566521795));
#93787=CARTESIAN_POINT('Ctrl Pts',(-79.9205588524238,-4.89072494265981,
131.341255179421));
#93788=CARTESIAN_POINT('Ctrl Pts',(-79.9282271693454,-4.87410295193499,
131.475667107368));
#93789=CARTESIAN_POINT('Ctrl Pts',(-79.935895486267,-4.85193338151652,131.609298828751));
#93790=CARTESIAN_POINT('Ctrl Pts',(-79.9435570381454,-4.82978336924923,
131.742812659288));
#93791=CARTESIAN_POINT('Ctrl Pts',(-79.9512185900237,-4.80209557838459,
131.875547258887));
#93792=CARTESIAN_POINT('Ctrl Pts',(-79.9588801419021,-4.76894468128677,
132.007003411303));
#93793=CARTESIAN_POINT('Ctrl Pts',(-79.9665372570022,-4.73581298175884,
132.138383437915));
#93794=CARTESIAN_POINT('Ctrl Pts',(-79.9741943721024,-4.6972245660148,132.268486101928));
#93795=CARTESIAN_POINT('Ctrl Pts',(-79.9818514872026,-4.6533052723407,132.396821953017));
#93796=CARTESIAN_POINT('Ctrl Pts',(-79.9895063075543,-4.60939914076901,
132.525119343341));
#93797=CARTESIAN_POINT('Ctrl Pts',(-79.997161127906,-4.56016543717282,132.651650594194));
#93798=CARTESIAN_POINT('Ctrl Pts',(-80.0048159482576,-4.50577985147171,
132.775941453487));
#93799=CARTESIAN_POINT('Ctrl Pts',(-80.0124702272485,-4.45139811200396,
132.900223522737));
#93800=CARTESIAN_POINT('Ctrl Pts',(-80.0201245062393,-4.39186537579566,
133.022265147927));
#93801=CARTESIAN_POINT('Ctrl Pts',(-80.0277787852301,-4.32740525268059,
133.141612602606));
#93802=CARTESIAN_POINT('Ctrl Pts',(-80.035434275585,-4.26293492812495,133.260978945178));
#93803=CARTESIAN_POINT('Ctrl Pts',(-80.0430897659398,-4.19353585685992,
133.377649916452));
#93804=CARTESIAN_POINT('Ctrl Pts',(-80.0507452562946,-4.11947705388346,
133.49119739434));
#93805=CARTESIAN_POINT('Ctrl Pts',(-80.0584084351493,-4.04534387277225,
133.604858909308));
#93806=CARTESIAN_POINT('Ctrl Pts',(-80.066071614004,-3.96654183206233,133.715390328504));
#93807=CARTESIAN_POINT('Ctrl Pts',(-80.0737347928587,-3.88338287503102,
133.822393173457));
#93808=CARTESIAN_POINT('Ctrl Pts',(-80.0814017837352,-3.80018255086408,
133.929449246605));
#93809=CARTESIAN_POINT('Ctrl Pts',(-80.0890687746115,-3.71262125321013,
134.032972943804));
#93810=CARTESIAN_POINT('Ctrl Pts',(-80.096735765488,-3.62104965329249,134.132600763783));
#93811=CARTESIAN_POINT('Ctrl Pts',(-80.1044150067211,-3.52933173981188,
134.232387769594));
#93812=CARTESIAN_POINT('Ctrl Pts',(-80.1120942479542,-3.433591005632,134.328266177521));
#93813=CARTESIAN_POINT('Ctrl Pts',(-80.1197734891873,-3.33421378696513,
134.419910573702));
#93814=CARTESIAN_POINT('Ctrl Pts',(-80.1273236638021,-3.23650682205786,
134.510014683292));
#93815=CARTESIAN_POINT('Ctrl Pts',(-80.134873838417,-3.13528498592989,134.596025828627));
#93816=CARTESIAN_POINT('Ctrl Pts',(-80.1424240130319,-3.030942861091,134.677675533152));
#93817=CARTESIAN_POINT('Ctrl Pts',(-80.150198347151,-2.92350289015378,134.761749361386));
#93818=CARTESIAN_POINT('Ctrl Pts',(-80.15797268127,-2.81239196730528,134.841482632209));
#93819=CARTESIAN_POINT('Ctrl Pts',(-80.1657470153891,-2.69799608994582,
134.916537676149));
#93820=CARTESIAN_POINT('Ctrl Pts',(-80.1735117683362,-2.58374119528136,
134.991500221455));
#93821=CARTESIAN_POINT('Ctrl Pts',(-80.1812765212833,-2.46620972499101,
135.061795799086));
#93822=CARTESIAN_POINT('Ctrl Pts',(-80.1890412742304,-2.34582069902412,
135.127126897453));
#93823=CARTESIAN_POINT('Ctrl Pts',(-80.1967983151154,-2.22555124513501,
135.192393108052));
#93824=CARTESIAN_POINT('Ctrl Pts',(-80.2045553560003,-2.10243022504993,
135.252704466614));
#93825=CARTESIAN_POINT('Ctrl Pts',(-80.2123123968853,-1.97690529286855,
135.307806911853));
#93826=CARTESIAN_POINT('Ctrl Pts',(-80.2200635881254,-1.85147502001514,
135.362867803909));
#93827=CARTESIAN_POINT('Ctrl Pts',(-80.2278147793656,-1.72364479989424,
135.412727444737));
#93828=CARTESIAN_POINT('Ctrl Pts',(-80.2355659706057,-1.5938862035252,135.457178025622));
#93829=CARTESIAN_POINT('Ctrl Pts',(-80.2433138673828,-1.46418275802087,
135.501609713825));
#93830=CARTESIAN_POINT('Ctrl Pts',(-80.25106176416,-1.33255293550377,135.540636788173));
#93831=CARTESIAN_POINT('Ctrl Pts',(-80.258809660937,-1.1994873661917,135.574099931286));
#93832=CARTESIAN_POINT('Ctrl Pts',(-80.2665559370211,-1.06644963132817,
135.607556074631));
#93833=CARTESIAN_POINT('Ctrl Pts',(-80.2743022131051,-0.931977125956554,
135.635450506419));
#93834=CARTESIAN_POINT('Ctrl Pts',(-80.2820484891892,-0.796574305580768,
135.657674169995));
#93835=CARTESIAN_POINT('Ctrl Pts',(-80.2897948224546,-0.661170485692306,
135.67989799762));
#93836=CARTESIAN_POINT('Ctrl Pts',(-80.2975411557199,-0.524836722899564,
135.696450910181));
#93837=CARTESIAN_POINT('Ctrl Pts',(-80.3052874889853,-0.388085902584176,
135.707275301172));
#93838=CARTESIAN_POINT('Ctrl Pts',(-80.3130355569882,-0.251304457870929,
135.71810211621));
#93839=CARTESIAN_POINT('Ctrl Pts',(-80.3207836249912,-0.114106159457105,
135.723197826087));
#93840=CARTESIAN_POINT('Ctrl Pts',(-80.3285316929941,0.0229931703295307,
135.722556869915));
#93841=CARTESIAN_POINT('Ctrl Pts',(-80.336287995736,0.160238210915554,135.721915232527));
#93842=CARTESIAN_POINT('Ctrl Pts',(-80.3440442984779,0.297383681171619,
135.715524751514));
#93843=CARTESIAN_POINT('Ctrl Pts',(-80.3518006012197,0.433915389860011,
135.703432008855));
#93844=CARTESIAN_POINT('Ctrl Pts',(-80.3595610437339,0.570519969632221,
135.691332811935));
#93845=CARTESIAN_POINT('Ctrl Pts',(-80.367321486248,0.706509747633785,135.673525339737));
#93846=CARTESIAN_POINT('Ctrl Pts',(-80.3750819287622,0.841378819633916,
135.65010769561));
#93847=CARTESIAN_POINT('Ctrl Pts',(-80.3828548290276,0.976464395441904,
135.626652459401));
#93848=CARTESIAN_POINT('Ctrl Pts',(-80.3906277292929,1.11042528787508,135.597569137508));
#93849=CARTESIAN_POINT('Ctrl Pts',(-80.3984006295584,1.24276801644454,135.563006508973));
#93850=CARTESIAN_POINT('Ctrl Pts',(-80.4058909653205,1.37029975348108,135.529700319042));
#93851=CARTESIAN_POINT('Ctrl Pts',(-80.4133813010827,1.4963286381162,135.491306369086));
#93852=CARTESIAN_POINT('Ctrl Pts',(-80.4208716368449,1.62043088514817,135.448000010215));
#93853=CARTESIAN_POINT('Ctrl Pts',(-80.4286459709639,1.74923850659444,135.403051677585));
#93854=CARTESIAN_POINT('Ctrl Pts',(-80.436420305083,1.87637853333625,135.352668691841));
#93855=CARTESIAN_POINT('Ctrl Pts',(-80.4441946392021,2.0013582334598,135.29699328493));
#93856=CARTESIAN_POINT('Ctrl Pts',(-80.4519593921492,2.12618390727271,135.241386492982));
#93857=CARTESIAN_POINT('Ctrl Pts',(-80.4597241450963,2.24885419816539,135.180500415137));
#93858=CARTESIAN_POINT('Ctrl Pts',(-80.4674888980434,2.36889231069481,135.114526772464));
#93859=CARTESIAN_POINT('Ctrl Pts',(-80.4752459389284,2.48881119967895,135.048618655744));
#93860=CARTESIAN_POINT('Ctrl Pts',(-80.4830029798134,2.60610277249812,134.977633217067));
#93861=CARTESIAN_POINT('Ctrl Pts',(-80.4907600206984,2.72031131222097,134.901809754176));
#93862=CARTESIAN_POINT('Ctrl Pts',(-80.4985112119386,2.83443372639576,134.826043470347));
#93863=CARTESIAN_POINT('Ctrl Pts',(-80.5062624031788,2.94547741072523,134.745446639576));
#93864=CARTESIAN_POINT('Ctrl Pts',(-80.5140135944189,3.05301263419777,134.66030368223));
#93865=CARTESIAN_POINT('Ctrl Pts',(-80.521761491196,3.16050215233159,134.575196912912));
#93866=CARTESIAN_POINT('Ctrl Pts',(-80.5295093879731,3.26448586959285,134.485548102252));
#93867=CARTESIAN_POINT('Ctrl Pts',(-80.5372572847502,3.3645645501395,134.391683916412));
#93868=CARTESIAN_POINT('Ctrl Pts',(-80.5450035608343,3.46462229638362,134.297839364936));
#93869=CARTESIAN_POINT('Ctrl Pts',(-80.5527498369184,3.56077634568605,134.199781459449));
#93870=CARTESIAN_POINT('Ctrl Pts',(-80.5604961130025,3.65266227506975,134.097875664865));
#93871=CARTESIAN_POINT('Ctrl Pts',(-80.5682424462679,3.74454888273413,133.995969118036));
#93872=CARTESIAN_POINT('Ctrl Pts',(-80.5759887795332,3.83216704580072,133.890214915791));
#93873=CARTESIAN_POINT('Ctrl Pts',(-80.5837351127986,3.91519107120897,133.781013425407));
#93874=CARTESIAN_POINT('Ctrl Pts',(-80.5914831808015,3.99823368927219,133.671787480105));
#93875=CARTESIAN_POINT('Ctrl Pts',(-80.5992312488045,4.07667988585684,133.559113021649));
#93876=CARTESIAN_POINT('Ctrl Pts',(-80.6069793168075,4.1502461678637,133.443421020178));
#93877=CARTESIAN_POINT('Ctrl Pts',(-80.6147356195494,4.22389063699063,133.32760605987));
#93878=CARTESIAN_POINT('Ctrl Pts',(-80.6224919222911,4.29264462096392,133.208767480497));
#93879=CARTESIAN_POINT('Ctrl Pts',(-80.630248225033,4.35626937759889,133.08736306441));
#93880=CARTESIAN_POINT('Ctrl Pts',(-80.6380086675472,4.41992809268218,132.96589385113));
#93881=CARTESIAN_POINT('Ctrl Pts',(-80.6457691100614,4.4784519587335,132.841856425771));
#93882=CARTESIAN_POINT('Ctrl Pts',(-80.6535295525756,4.53165005928323,132.715729447148));
#93883=CARTESIAN_POINT('Ctrl Pts',(-80.661302452841,4.58493355814667,132.589399998302));
#93884=CARTESIAN_POINT('Ctrl Pts',(-80.6690753531064,4.63287407029189,132.460974659645));
#93885=CARTESIAN_POINT('Ctrl Pts',(-80.6768482533718,4.67533002948314,132.330949028996));
#93886=CARTESIAN_POINT('Ctrl Pts',(-80.6843385891338,4.71624260761744,132.205650157537));
#93887=CARTESIAN_POINT('Ctrl Pts',(-80.6918289248958,4.75206238071695,132.078865619797));
#93888=CARTESIAN_POINT('Ctrl Pts',(-80.6993192606578,4.78270781038475,131.951046739826));
#93889=CARTESIAN_POINT('Ctrl Pts',(-80.7070935947769,4.81451517083294,131.818381568172));
#93890=CARTESIAN_POINT('Ctrl Pts',(-80.7148679288959,4.84084882802785,131.684181828415));
#93891=CARTESIAN_POINT('Ctrl Pts',(-80.722642263015,4.86156211209968,131.548938949709));
#93892=CARTESIAN_POINT('Ctrl Pts',(-80.7304070159621,4.88224986890008,131.413862745765));
#93893=CARTESIAN_POINT('Ctrl Pts',(-80.7381717689091,4.89733097584156,131.277746343533));
#93894=CARTESIAN_POINT('Ctrl Pts',(-80.7459365218562,4.9067090137068,131.141094514447));
#93895=CARTESIAN_POINT('Ctrl Pts',(-80.7536935627412,4.91607773717265,131.004578409883));
#93896=CARTESIAN_POINT('Ctrl Pts',(-80.7614506036261,4.91975463731667,130.86752832428));
#93897=CARTESIAN_POINT('Ctrl Pts',(-80.7692076445111,4.91769471597277,130.730457011474));
#93898=CARTESIAN_POINT('Ctrl Pts',(-80.7769588357512,4.91563634803158,130.593489065211));
#93899=CARTESIAN_POINT('Ctrl Pts',(-80.7847100269913,4.90784977545585,130.456500312946));
#93900=CARTESIAN_POINT('Ctrl Pts',(-80.7924612182315,4.89434200904784,130.320006035705));
#93901=CARTESIAN_POINT('Ctrl Pts',(-80.8002091150085,4.88083998380091,130.183569772174));
#93902=CARTESIAN_POINT('Ctrl Pts',(-80.8079570117856,4.86162163953014,130.047627953916));
#93903=CARTESIAN_POINT('Ctrl Pts',(-80.8157049085627,4.83674601300432,129.91269304039));
#93904=CARTESIAN_POINT('Ctrl Pts',(-80.8234511846467,4.81187558992331,129.77778635234));
#93905=CARTESIAN_POINT('Ctrl Pts',(-80.8311974607308,4.78135030923411,129.643886534325));
#93906=CARTESIAN_POINT('Ctrl Pts',(-80.8389437368149,4.74528066739942,129.51149772843));
#93907=CARTESIAN_POINT('Ctrl Pts',(-80.8466900700802,4.70921075930687,129.379107945271));
#93908=CARTESIAN_POINT('Ctrl Pts',(-80.8544364033455,4.66759651117477,129.248229573706));
#93909=CARTESIAN_POINT('Ctrl Pts',(-80.8621827366108,4.62059871827531,129.11935303682));
#93910=CARTESIAN_POINT('Ctrl Pts',(-80.8699308046138,4.57359040054592,128.990447638927));
#93911=CARTESIAN_POINT('Ctrl Pts',(-80.8776788726167,4.52119627295,128.863545335007));
#93912=CARTESIAN_POINT('Ctrl Pts',(-80.8854269406196,4.46362568792565,128.73911758572));
#93913=CARTESIAN_POINT('Ctrl Pts',(-80.8931832433614,4.40599391619835,128.61455759314));
#93914=CARTESIAN_POINT('Ctrl Pts',(-80.9009395461033,4.3431748614365,128.492477764265));
#93915=CARTESIAN_POINT('Ctrl Pts',(-80.9086958488452,4.27542462291296,128.373326402198));
#93916=CARTESIAN_POINT('Ctrl Pts',(-80.9164562913593,4.20763822404721,128.254111445462));
#93917=CARTESIAN_POINT('Ctrl Pts',(-80.9242167338734,4.13491560429727,128.137828401283));
#93918=CARTESIAN_POINT('Ctrl Pts',(-80.9319771763876,4.05755627786348,128.024896619873));
#93919=CARTESIAN_POINT('Ctrl Pts',(-80.939750076653,3.98007276737126,127.911783550343));
#93920=CARTESIAN_POINT('Ctrl Pts',(-80.9475229769183,3.8979379105921,127.802032807222));
#93921=CARTESIAN_POINT('Ctrl Pts',(-80.9552958771837,3.81149214799814,127.696031376921));
#93922=CARTESIAN_POINT('Ctrl Pts',(-80.962786212946,3.7281889066154,127.59388336561));
#93923=CARTESIAN_POINT('Ctrl Pts',(-80.9702765487083,3.64088294659379,127.495217036496));
#93924=CARTESIAN_POINT('Ctrl Pts',(-80.9777668844705,3.5499099061446,127.400344941815));
#93925=CARTESIAN_POINT('Ctrl Pts',(-80.9855412185896,3.45548759521866,127.301875742832));
#93926=CARTESIAN_POINT('Ctrl Pts',(-80.9933155527087,3.35681553837506,127.207182253876));
#93927=CARTESIAN_POINT('Ctrl Pts',(-81.0010898868278,3.25422791023313,127.116653501924));
#93928=CARTESIAN_POINT('Ctrl Pts',(-81.008854639775,3.15176671217408,127.026236318567));
#93929=CARTESIAN_POINT('Ctrl Pts',(-81.0166193927221,3.04539983463761,126.939973915944));
#93930=CARTESIAN_POINT('Ctrl Pts',(-81.0243841456692,2.93549983918251,126.858220255559));
#93931=CARTESIAN_POINT('Ctrl Pts',(-81.0321411865543,2.82570899795221,126.776547794063));
#93932=CARTESIAN_POINT('Ctrl Pts',(-81.0398982274394,2.7123923338149,126.699375394933));
#93933=CARTESIAN_POINT('Ctrl Pts',(-81.0476552683244,2.59595691848611,126.627018072375));
#93934=CARTESIAN_POINT('Ctrl Pts',(-81.0554064595647,2.47960930800865,126.554715315036));
#93935=CARTESIAN_POINT('Ctrl Pts',(-81.0631576508049,2.36014795832808,126.487220612334));
#93936=CARTESIAN_POINT('Ctrl Pts',(-81.0709088420451,2.23801017947578,126.424806587866));
#93937=CARTESIAN_POINT('Ctrl Pts',(-81.0786567388222,2.11592431243879,126.362419091023));
#93938=CARTESIAN_POINT('Ctrl Pts',(-81.0864046355994,1.9911646261518,126.305108155018));
#93939=CARTESIAN_POINT('Ctrl Pts',(-81.0941525323765,1.86419417808803,126.253101107399));
#93940=CARTESIAN_POINT('Ctrl Pts',(-81.1018988084606,1.73725028950484,126.201104938534));
#93941=CARTESIAN_POINT('Ctrl Pts',(-81.1096450845448,1.60809692053365,126.154410599377));
#93942=CARTESIAN_POINT('Ctrl Pts',(-81.1173913606289,1.47721794622575,126.113197627235));
#93943=CARTESIAN_POINT('Ctrl Pts',(-81.1251376938944,1.34633800579881,126.071984350869));
#93944=CARTESIAN_POINT('Ctrl Pts',(-81.1328840271597,1.21373280753077,126.036252639686));
#93945=CARTESIAN_POINT('Ctrl Pts',(-81.1406303604251,1.07990187202671,126.006132297728));
#93946=CARTESIAN_POINT('Ctrl Pts',(-81.1483784284282,0.946040966012017,
125.976005210528));
#93947=CARTESIAN_POINT('Ctrl Pts',(-81.1561264964312,0.810954157898682,
125.951492078924));
#93948=CARTESIAN_POINT('Ctrl Pts',(-81.1638745644343,0.675151260998935,
125.932671604783));
#93949=CARTESIAN_POINT('Ctrl Pts',(-81.1716308671762,0.539204031165215,
125.913831128018));
#93950=CARTESIAN_POINT('Ctrl Pts',(-81.179387169918,0.402539580111882,125.900695448445));
#93951=CARTESIAN_POINT('Ctrl Pts',(-81.1871434726599,0.265673505848731,
125.893291421272));
#93952=CARTESIAN_POINT('Ctrl Pts',(-81.1949039151741,0.128734382040788,
125.885883442346));
#93953=CARTESIAN_POINT('Ctrl Pts',(-81.2026643576884,-0.00840618865881398,
125.884213216204));
#93954=CARTESIAN_POINT('Ctrl Pts',(-81.2104248002026,-0.145233500297805,
125.8882554221));
#93955=CARTESIAN_POINT('Ctrl Pts',(-81.218197700468,-0.282280459284768,
125.892304116903));
#93956=CARTESIAN_POINT('Ctrl Pts',(-81.2259706007335,-0.419012764120642,
125.902083540625));
#93957=CARTESIAN_POINT('Ctrl Pts',(-81.2337435009989,-0.554920815787799,
125.917516446661));
#93958=CARTESIAN_POINT('Ctrl Pts',(-81.2412338367602,-0.685888267431147,
125.932388327688));
#93959=CARTESIAN_POINT('Ctrl Pts',(-81.2487241725215,-0.816090048431828,
125.95250974354));
#93960=CARTESIAN_POINT('Ctrl Pts',(-81.2562145082828,-0.945081779089869,
125.977767254403));
#93961=CARTESIAN_POINT('Ctrl Pts',(-81.2639888424019,-1.07896427043575,
126.003982411469));
#93962=CARTESIAN_POINT('Ctrl Pts',(-81.271763176521,-1.21196724147693,126.035813863631));
#93963=CARTESIAN_POINT('Ctrl Pts',(-81.2795375106402,-1.34358276325477,
126.073190738901));
#93964=CARTESIAN_POINT('Ctrl Pts',(-81.2873022635873,-1.47503608066449,
126.110521550513));
#93965=CARTESIAN_POINT('Ctrl Pts',(-81.2950670165344,-1.60510497853336,
126.153384081356));
#93966=CARTESIAN_POINT('Ctrl Pts',(-81.3028317694815,-1.73329028039838,
126.20165620968));
#93967=CARTESIAN_POINT('Ctrl Pts',(-81.3105888103664,-1.86134826681414,
126.249880393445));
#93968=CARTESIAN_POINT('Ctrl Pts',(-81.3183458512514,-1.98752601671655,
126.303503345507));
#93969=CARTESIAN_POINT('Ctrl Pts',(-81.3261028921363,-2.11133846752849,
126.362352857776));
#93970=CARTESIAN_POINT('Ctrl Pts',(-81.3338540833765,-2.23505755040899,
126.42115799117));
#93971=CARTESIAN_POINT('Ctrl Pts',(-81.3416052746167,-2.35641453284803,
126.485181672517));
#93972=CARTESIAN_POINT('Ctrl Pts',(-81.3493564658569,-2.47494367214014,
126.554203340213));
#93973=CARTESIAN_POINT('Ctrl Pts',(-81.357104362634,-2.59342243338602,126.62319567186));
#93974=CARTESIAN_POINT('Ctrl Pts',(-81.364852259411,-2.70907540484057,126.697181568502));
#93975=CARTESIAN_POINT('Ctrl Pts',(-81.3726001561881,-2.82146103552243,
126.775894322867));
#93976=CARTESIAN_POINT('Ctrl Pts',(-81.3803464322722,-2.93382315755311,
126.85459061222));
#93977=CARTESIAN_POINT('Ctrl Pts',(-81.3880927083564,-3.04291897821407,
126.938011568461));
#93978=CARTESIAN_POINT('Ctrl Pts',(-81.3958389844405,-3.14833590139897,
127.025847138106));
#93979=CARTESIAN_POINT('Ctrl Pts',(-81.4035853177059,-3.25375360274751,
127.113683356132));
#93980=CARTESIAN_POINT('Ctrl Pts',(-81.4113316509712,-3.35549205206618,
127.205934002319));
#93981=CARTESIAN_POINT('Ctrl Pts',(-81.4190779842366,-3.45317203845016,
127.302248978088));
#93982=CARTESIAN_POINT('Ctrl Pts',(-81.4268260522395,-3.55087389958968,
127.398585522928));
#93983=CARTESIAN_POINT('Ctrl Pts',(-81.4345741202425,-3.64451521091992,
127.498987934051));
#93984=CARTESIAN_POINT('Ctrl Pts',(-81.4423221882455,-3.73375419178265,
127.60306983136));
#93985=CARTESIAN_POINT('Ctrl Pts',(-81.4500784909873,-3.82308801689633,
127.707262348149));
#93986=CARTESIAN_POINT('Ctrl Pts',(-81.4578347937292,-3.90800991015203,
127.815141865692));
#93987=CARTESIAN_POINT('Ctrl Pts',(-81.4655910964711,-3.98821858418567,
127.926289112677));
#93988=CARTESIAN_POINT('Ctrl Pts',(-81.4733515389853,-4.06847006800367,
128.037495682294));
#93989=CARTESIAN_POINT('Ctrl Pts',(-81.4811119814996,-4.14400310486857,
128.151973130418));
#93990=CARTESIAN_POINT('Ctrl Pts',(-81.4888724240137,-4.21456078670153,
128.269274733873));
#93991=CARTESIAN_POINT('Ctrl Pts',(-81.4966453242792,-4.28523173398918,
128.386764640276));
#93992=CARTESIAN_POINT('Ctrl Pts',(-81.5044182245446,-4.3509111784808,128.507087418191));
#93993=CARTESIAN_POINT('Ctrl Pts',(-81.51219112481,-4.41138865921522,128.629772573856));
#93994=CARTESIAN_POINT('Ctrl Pts',(-81.5196814605727,-4.46966763119614,
128.747997815097));
#93995=CARTESIAN_POINT('Ctrl Pts',(-81.5271717963353,-4.52311615716766,
128.868416377742));
#93996=CARTESIAN_POINT('Ctrl Pts',(-81.534662132098,-4.57158947917601,128.990593075573));
#93997=CARTESIAN_POINT('Ctrl Pts',(-81.5434568423525,-4.62850399351063,
129.134045744628));
#93998=CARTESIAN_POINT('Ctrl Pts',(-81.552251552607,-4.67871160297205,129.280302977208));
#93999=CARTESIAN_POINT('Ctrl Pts',(-81.5610462628615,-4.72196086392718,
129.428763052128));
#94000=CARTESIAN_POINT('Ctrl Pts',(-81.5640669497953,-4.73681552925252,
129.47975409055));
#94001=CARTESIAN_POINT('Ctrl Pts',(-81.567087636729,-4.75084972363613,129.531004786592));
#94002=CARTESIAN_POINT('Ctrl Pts',(-81.5701083236628,-4.76405452823403,
129.582490119308));
#94003=CARTESIAN_POINT('Origin',(213.235140564004,0.,130.804360617566));
#94004=CARTESIAN_POINT('',(-83.6650228471445,-4.76405452823415,129.582490119309));
#94005=CARTESIAN_POINT('',(-83.3199745081269,-4.76405452823405,129.582490119308));
#94006=CARTESIAN_POINT('',(213.235140564004,-4.76405452823405,129.582490119308));
#94007=CARTESIAN_POINT('',(-81.9851405640544,-4.91824826795288,130.808488241399));
#94008=CARTESIAN_POINT('Ctrl Pts',(-81.9851405640544,-4.91824826795288,
130.8084882414));
#94009=CARTESIAN_POINT('Ctrl Pts',(-81.9943597297253,-4.91811131641968,
130.971672113781));
#94010=CARTESIAN_POINT('Ctrl Pts',(-82.0035788953962,-4.90984909429807,
131.134505591539));
#94011=CARTESIAN_POINT('Ctrl Pts',(-82.0127980610671,-4.89358889978316,
131.296265834472));
#94012=CARTESIAN_POINT('Ctrl Pts',(-82.0220872629018,-4.87720517981175,
131.459254937725));
#94013=CARTESIAN_POINT('Ctrl Pts',(-82.0313764647366,-4.85270160936032,
131.62115440444));
#94014=CARTESIAN_POINT('Ctrl Pts',(-82.0406656665714,-4.82025706733785,
131.781245906267));
#94015=CARTESIAN_POINT('Ctrl Pts',(-82.0500289215405,-4.78755387876324,
131.942613650949));
#94016=CARTESIAN_POINT('Ctrl Pts',(-82.0593921765095,-4.74678266151788,
132.102144461393));
#94017=CARTESIAN_POINT('Ctrl Pts',(-82.0687554314786,-4.69817465004165,
132.259124522881));
#94018=CARTESIAN_POINT('Ctrl Pts',(-82.0698264155067,-4.69261478820944,
132.277080152535));
#94019=CARTESIAN_POINT('Ctrl Pts',(-82.0708973995348,-4.68695244725871,
132.295002433936));
#94020=CARTESIAN_POINT('Ctrl Pts',(-82.0719683835628,-4.68118801245724,
132.31289031715));
#94021=CARTESIAN_POINT('Ctrl Pts',(-82.0797427176819,-4.6393436515898,132.44273948123));
#94022=CARTESIAN_POINT('Ctrl Pts',(-82.087517051801,-4.59202618497923,132.571051947522));
#94023=CARTESIAN_POINT('Ctrl Pts',(-82.09529138592,-4.53936597940594,132.697331712832));
#94024=CARTESIAN_POINT('Ctrl Pts',(-82.1030561388671,-4.48677067282964,
132.823455849617));
#94025=CARTESIAN_POINT('Ctrl Pts',(-82.1108208918142,-4.42884587741305,
132.947551912483));
#94026=CARTESIAN_POINT('Ctrl Pts',(-82.1185856447613,-4.3657718172393,133.069138642517));
#94027=CARTESIAN_POINT('Ctrl Pts',(-82.1263426856463,-4.30276040311129,
133.190604610896));
#94028=CARTESIAN_POINT('Ctrl Pts',(-82.1340997265313,-4.23461008082681,
133.309565861439));
#94029=CARTESIAN_POINT('Ctrl Pts',(-82.1418567674163,-4.16154914326525,
133.425561065965));
#94030=CARTESIAN_POINT('Ctrl Pts',(-82.1496079586564,-4.08854330152494,
133.541468797605));
#94031=CARTESIAN_POINT('Ctrl Pts',(-82.1573591498966,-4.01063442289286,
133.654414605805));
#94032=CARTESIAN_POINT('Ctrl Pts',(-82.1651103411367,-3.92809653347163,
133.763962058002));
#94033=CARTESIAN_POINT('Ctrl Pts',(-82.1728582379138,-3.84559372485506,
133.873462949608));
#94034=CARTESIAN_POINT('Ctrl Pts',(-82.1806061346908,-3.75846605333776,
133.979568046395));
#94035=CARTESIAN_POINT('Ctrl Pts',(-82.1883540314679,-3.66703051045002,
134.081870388403));
#94036=CARTESIAN_POINT('Ctrl Pts',(-82.196100307552,-3.57561409390672,134.184151330965));
#94037=CARTESIAN_POINT('Ctrl Pts',(-82.2038465836361,-3.47989185873097,
134.282630809634));
#94038=CARTESIAN_POINT('Ctrl Pts',(-82.2115928597202,-3.38022041944603,
134.376935736225));
#94039=CARTESIAN_POINT('Ctrl Pts',(-82.2193391929856,-3.28054824440958,
134.471241358953));
#94040=CARTESIAN_POINT('Ctrl Pts',(-82.2270855262509,-3.17692709108684,
134.561372099411));
#94041=CARTESIAN_POINT('Ctrl Pts',(-82.2348318595163,-3.06974939572087,
134.646992750619));
#94042=CARTESIAN_POINT('Ctrl Pts',(-82.2425799275192,-2.96254769865299,
134.732632575978));
#94043=CARTESIAN_POINT('Ctrl Pts',(-82.2503279955222,-2.85178818007577,
134.813760058322));
#94044=CARTESIAN_POINT('Ctrl Pts',(-82.2580760635252,-2.73789488296588,
134.890081444095));
#94045=CARTESIAN_POINT('Ctrl Pts',(-82.265832366267,-2.62388053870433,134.966483945144));
#94046=CARTESIAN_POINT('Ctrl Pts',(-82.2735886690088,-2.50672608794671,
135.0380699279));
#94047=CARTESIAN_POINT('Ctrl Pts',(-82.2813449717507,-2.38688345205788,
135.104589733415));
#94048=CARTESIAN_POINT('Ctrl Pts',(-82.2891054142648,-2.26697685254588,
135.171145042552));
#94049=CARTESIAN_POINT('Ctrl Pts',(-82.2968658567791,-2.14437955831906,
135.232628611376));
#94050=CARTESIAN_POINT('Ctrl Pts',(-82.3046262992932,-2.01956550887947,
135.288838091904));
#94051=CARTESIAN_POINT('Ctrl Pts',(-82.3123991995587,-1.89455109684725,
135.34513780488));
#94052=CARTESIAN_POINT('Ctrl Pts',(-82.3201720998241,-1.7673131816202,135.396146365363));
#94053=CARTESIAN_POINT('Ctrl Pts',(-82.3279450000896,-1.63834382109731,
135.441710354902));
#94054=CARTESIAN_POINT('Ctrl Pts',(-82.3354353358516,-1.51406282168399,
135.485617978653));
#94055=CARTESIAN_POINT('Ctrl Pts',(-82.3429256716135,-1.38817437054623,
135.524469915866));
#94056=CARTESIAN_POINT('Ctrl Pts',(-82.3504160073755,-1.2611277050684,135.558173821091));
#94057=CARTESIAN_POINT('Ctrl Pts',(-82.3581903414946,-1.12926402665379,
135.593155620127));
#94058=CARTESIAN_POINT('Ctrl Pts',(-82.3659646756136,-0.99573486826807,
135.622702117604));
#94059=CARTESIAN_POINT('Ctrl Pts',(-82.3737390097327,-0.861027997874883,
135.646654892946));
#94060=CARTESIAN_POINT('Ctrl Pts',(-82.3815037626798,-0.726487141660357,
135.670578148632));
#94061=CARTESIAN_POINT('Ctrl Pts',(-82.3892685156269,-0.590771842573108,
135.688921330927));
#94062=CARTESIAN_POINT('Ctrl Pts',(-82.397033268574,-0.454384412887237,
135.701575935257));
#94063=CARTESIAN_POINT('Ctrl Pts',(-82.404790309459,-0.318132445119255,
135.714217970855));
#94064=CARTESIAN_POINT('Ctrl Pts',(-82.412547350344,-0.181210062020253,
135.721182636309));
#94065=CARTESIAN_POINT('Ctrl Pts',(-82.420304391229,-0.0441287899329816,
135.722412641732));
#94066=CARTESIAN_POINT('Ctrl Pts',(-82.4280555824691,0.0928491081004854,
135.723641719598));
#94067=CARTESIAN_POINT('Ctrl Pts',(-82.4358067737092,0.229985267261336,
135.719144741698));
#94068=CARTESIAN_POINT('Ctrl Pts',(-82.4435579649493,0.366764386670902,
135.70891635149));
#94069=CARTESIAN_POINT('Ctrl Pts',(-82.4513058617264,0.503485371306202,
135.698692308622));
#94070=CARTESIAN_POINT('Ctrl Pts',(-82.4590537585035,0.639849228951849,
135.682741727565));
#94071=CARTESIAN_POINT('Ctrl Pts',(-82.4668016552806,0.775342231003463,
135.661111330473));
#94072=CARTESIAN_POINT('Ctrl Pts',(-82.4745479313647,0.910806890839939,
135.639485457994));
#94073=CARTESIAN_POINT('Ctrl Pts',(-82.4822942074486,1.04540067158514,135.612182194261));
#94074=CARTESIAN_POINT('Ctrl Pts',(-82.4900404835327,1.17861692472409,135.579299905898));
#94075=CARTESIAN_POINT('Ctrl Pts',(-82.4977868167981,1.31183416123534,135.546417374804));
#94076=CARTESIAN_POINT('Ctrl Pts',(-82.5055331500635,1.4436734702766,135.507955830594));
#94077=CARTESIAN_POINT('Ctrl Pts',(-82.5132794833288,1.57364071134718,135.464064253431));
#94078=CARTESIAN_POINT('Ctrl Pts',(-82.5210275513318,1.70363705768009,135.420162847053));
#94079=CARTESIAN_POINT('Ctrl Pts',(-82.5287756193348,1.83176013146819,135.370829113058));
#94080=CARTESIAN_POINT('Ctrl Pts',(-82.5365236873378,1.9575335839392,135.316261029837));
#94081=CARTESIAN_POINT('Ctrl Pts',(-82.5442799900796,2.08344070993205,135.261634951008));
#94082=CARTESIAN_POINT('Ctrl Pts',(-82.5520362928215,2.20699286693559,135.201763565864));
#94083=CARTESIAN_POINT('Ctrl Pts',(-82.5597925955633,2.32773573527054,135.136892141888));
#94084=CARTESIAN_POINT('Ctrl Pts',(-82.5675530380775,2.44854304771014,135.07198609408));
#94085=CARTESIAN_POINT('Ctrl Pts',(-82.5753134805917,2.56653774760186,135.00207488908));
#94086=CARTESIAN_POINT('Ctrl Pts',(-82.5830739231058,2.68129341798007,134.927447891587));
#94087=CARTESIAN_POINT('Ctrl Pts',(-82.5908468233713,2.7962333043479,134.852701096213));
#94088=CARTESIAN_POINT('Ctrl Pts',(-82.5986197236367,2.90792345205854,134.773223607462));
#94089=CARTESIAN_POINT('Ctrl Pts',(-82.6063926239022,3.01596881651194,134.68934648116));
#94090=CARTESIAN_POINT('Ctrl Pts',(-82.6138829596642,3.1200864598182,134.608518499673));
#94091=CARTESIAN_POINT('Ctrl Pts',(-82.6213732954263,3.22081947777635,134.523605401459));
#94092=CARTESIAN_POINT('Ctrl Pts',(-82.6288636311884,3.31784735376558,134.434935227681));
#94093=CARTESIAN_POINT('Ctrl Pts',(-82.6366379653074,3.41855407116322,134.342903097314));
#94094=CARTESIAN_POINT('Ctrl Pts',(-82.6444122994266,3.5155881480297,134.246531838222));
#94095=CARTESIAN_POINT('Ctrl Pts',(-82.6521866335457,3.60855265014795,134.146146193214));
#94096=CARTESIAN_POINT('Ctrl Pts',(-82.6599513864927,3.70140258182582,134.045884264542));
#94097=CARTESIAN_POINT('Ctrl Pts',(-82.6677161394397,3.79019265478353,133.941618077851));
#94098=CARTESIAN_POINT('Ctrl Pts',(-82.6754808923868,3.87456006899657,133.833711593309));
#94099=CARTESIAN_POINT('Ctrl Pts',(-82.6832379332718,3.95884368830444,133.72591228301));
#94100=CARTESIAN_POINT('Ctrl Pts',(-82.6909949741569,4.03871315118027,133.614480176064));
#94101=CARTESIAN_POINT('Ctrl Pts',(-82.6987520150419,4.11384376553748,133.499814667489));
#94102=CARTESIAN_POINT('Ctrl Pts',(-82.706503206282,4.18891772331408,133.385235629066));
#94103=CARTESIAN_POINT('Ctrl Pts',(-82.7142543975221,4.2592597322091,133.267428368066));
#94104=CARTESIAN_POINT('Ctrl Pts',(-82.7220055887622,4.32458675290145,133.146823526371));
#94105=CARTESIAN_POINT('Ctrl Pts',(-82.7297534855393,4.38988600786726,133.026269944952));
#94106=CARTESIAN_POINT('Ctrl Pts',(-82.7375013823165,4.45017432820992,132.902921490813));
#94107=CARTESIAN_POINT('Ctrl Pts',(-82.7452492790935,4.50521333974134,132.777235632846));
#94108=CARTESIAN_POINT('Ctrl Pts',(-82.7529955551776,4.56024083829805,132.651576065651));
#94109=CARTESIAN_POINT('Ctrl Pts',(-82.7607418312618,4.61002105537983,132.523580425049));
#94110=CARTESIAN_POINT('Ctrl Pts',(-82.7684881073459,4.65436289371413,132.393728138348));
#94111=CARTESIAN_POINT('Ctrl Pts',(-82.7762344406112,4.69870505936975,132.263874893107));
#94112=CARTESIAN_POINT('Ctrl Pts',(-82.7839807738764,4.73760863982853,132.132165344406));
#94113=CARTESIAN_POINT('Ctrl Pts',(-82.7917271071418,4.77093188131216,131.999095754062));
#94114=CARTESIAN_POINT('Ctrl Pts',(-82.7994751751448,4.80426258530472,131.865996363706));
#94115=CARTESIAN_POINT('Ctrl Pts',(-82.8072232431478,4.83201036865254,131.731536704826));
#94116=CARTESIAN_POINT('Ctrl Pts',(-82.8149713111508,4.85408431803855,131.596224555293));
#94117=CARTESIAN_POINT('Ctrl Pts',(-82.8227276138926,4.87618172788062,131.460768594397));
#94118=CARTESIAN_POINT('Ctrl Pts',(-82.8304839166344,4.89259319470256,131.32445871942));
#94119=CARTESIAN_POINT('Ctrl Pts',(-82.8382402193763,4.90327949810117,131.187809735443));
#94120=CARTESIAN_POINT('Ctrl Pts',(-82.8460006618904,4.9139715051017,131.051087817788));
#94121=CARTESIAN_POINT('Ctrl Pts',(-82.8537611044047,4.91893224581936,130.914026821007));
#94122=CARTESIAN_POINT('Ctrl Pts',(-82.8615215469189,4.91817468218478,130.777141910458));
#94123=CARTESIAN_POINT('Ctrl Pts',(-82.8692944471843,4.9174159024418,130.640037260098));
#94124=CARTESIAN_POINT('Ctrl Pts',(-82.8770673474496,4.91092049325699,130.503109651584));
#94125=CARTESIAN_POINT('Ctrl Pts',(-82.8848402477151,4.89875345001772,130.366870390887));
#94126=CARTESIAN_POINT('Ctrl Pts',(-82.8923305834772,4.88702870944704,130.235583770481));
#94127=CARTESIAN_POINT('Ctrl Pts',(-82.8998209192393,4.8700375718024,130.104936625863));
#94128=CARTESIAN_POINT('Ctrl Pts',(-82.9073112550014,4.847882780343,129.975375931004));
#94129=CARTESIAN_POINT('Ctrl Pts',(-82.9150855891205,4.82488798323177,129.840902903022));
#94130=CARTESIAN_POINT('Ctrl Pts',(-82.9228599232395,4.79625740231677,129.707174366468));
#94131=CARTESIAN_POINT('Ctrl Pts',(-82.9306342573586,4.76204970028167,129.574699804761));
#94132=CARTESIAN_POINT('Ctrl Pts',(-82.9383990103057,4.72788415618218,129.442388506113));
#94133=CARTESIAN_POINT('Ctrl Pts',(-82.9461637632528,4.68815526359836,129.311328482318));
#94134=CARTESIAN_POINT('Ctrl Pts',(-82.9539285161999,4.64297313025405,129.182021696675));
#94135=CARTESIAN_POINT('Ctrl Pts',(-82.9616855570848,4.59783587244154,129.052843340353));
#94136=CARTESIAN_POINT('Ctrl Pts',(-82.96944259797,4.54725628055144,128.925415123531));
#94137=CARTESIAN_POINT('Ctrl Pts',(-82.977199638855,4.49139487291884,128.800226101617));
#94138=CARTESIAN_POINT('Ctrl Pts',(-82.9849508300951,4.43557559080819,128.675131485718));
#94139=CARTESIAN_POINT('Ctrl Pts',(-82.9927020213352,4.37448257966063,128.552273059273));
#94140=CARTESIAN_POINT('Ctrl Pts',(-83.0004532125753,4.30832516102148,128.432121723734));
#94141=CARTESIAN_POINT('Ctrl Pts',(-83.0082011093524,4.24219586104996,128.312021455718));
#94142=CARTESIAN_POINT('Ctrl Pts',(-83.0159490061295,4.1710066229427,128.194626331944));
#94143=CARTESIAN_POINT('Ctrl Pts',(-83.0236969029066,4.0950134811615,128.080384176477));
#94144=CARTESIAN_POINT('Ctrl Pts',(-83.0314431789907,4.01903623550754,127.966165918007));
#94145=CARTESIAN_POINT('Ctrl Pts',(-83.0391894550748,3.93825730132652,127.855099641315));
#94146=CARTESIAN_POINT('Ctrl Pts',(-83.0469357311589,3.85297674164616,127.747605264118));
#94147=CARTESIAN_POINT('Ctrl Pts',(-83.0546820644242,3.76769555244396,127.640110093421));
#94148=CARTESIAN_POINT('Ctrl Pts',(-83.0624283976896,3.67791291442427,127.536187181117));
#94149=CARTESIAN_POINT('Ctrl Pts',(-83.070174730955,3.5839697253284,127.436224030307));
#94150=CARTESIAN_POINT('Ctrl Pts',(-83.077922798958,3.49000549830656,127.336238493443));
#94151=CARTESIAN_POINT('Ctrl Pts',(-83.0856708669609,3.39187913387172,127.24021476747));
#94152=CARTESIAN_POINT('Ctrl Pts',(-83.0934189349639,3.28996869905902,127.148503806679));
#94153=CARTESIAN_POINT('Ctrl Pts',(-83.1011752377057,3.18794995262359,127.056695374387));
#94154=CARTESIAN_POINT('Ctrl Pts',(-83.1089315404476,3.08213939299894,126.969209125574));
#94155=CARTESIAN_POINT('Ctrl Pts',(-83.1166878431895,2.97294894069247,126.886356322196));
#94156=CARTESIAN_POINT('Ctrl Pts',(-83.1244482857036,2.86370021015395,126.803459297783));
#94157=CARTESIAN_POINT('Ctrl Pts',(-83.1322087282178,2.75106831332362,126.72520086946));
#94158=CARTESIAN_POINT('Ctrl Pts',(-83.139969170732,2.63549367964732,126.65184859145));
#94159=CARTESIAN_POINT('Ctrl Pts',(-83.1477420709974,2.5197335153088,126.578378561851));
#94160=CARTESIAN_POINT('Ctrl Pts',(-83.1555149712629,2.40102151295096,126.509830616513));
#94161=CARTESIAN_POINT('Ctrl Pts',(-83.1632878715283,2.27982298036273,126.446426446343));
#94162=CARTESIAN_POINT('Ctrl Pts',(-83.1707782072903,2.16303031971576,126.385327177465));
#94163=CARTESIAN_POINT('Ctrl Pts',(-83.1782685430522,2.04392905190227,126.329004329881));
#94164=CARTESIAN_POINT('Ctrl Pts',(-83.1857588788141,1.9229507640255,126.277613063125));
#94165=CARTESIAN_POINT('Ctrl Pts',(-83.1935332129332,1.79738554759209,126.224273280871));
#94166=CARTESIAN_POINT('Ctrl Pts',(-83.2013075470523,1.66940041407463,126.176077458946));
#94167=CARTESIAN_POINT('Ctrl Pts',(-83.2090818811714,1.53945571491708,126.133251631007));
#94168=CARTESIAN_POINT('Ctrl Pts',(-83.2168466341185,1.40967116098809,126.090478582074));
#94169=CARTESIAN_POINT('Ctrl Pts',(-83.2246113870656,1.27793221428302,126.053062480406));
#94170=CARTESIAN_POINT('Ctrl Pts',(-83.2323761400127,1.1447207066549,126.021182012678));
#94171=CARTESIAN_POINT('Ctrl Pts',(-83.2401331808977,1.01164150657411,125.989333209081));
#94172=CARTESIAN_POINT('Ctrl Pts',(-83.2478902217827,0.87709303391469,125.963009188427));
#94173=CARTESIAN_POINT('Ctrl Pts',(-83.2556472626677,0.741573508925192,
125.942339248489));
#94174=CARTESIAN_POINT('Ctrl Pts',(-83.2633984539079,0.606156180263492,
125.921684895914));
#94175=CARTESIAN_POINT('Ctrl Pts',(-83.271149645148,0.469769641758475,125.906676195959));
#94176=CARTESIAN_POINT('Ctrl Pts',(-83.2789008363881,0.332923219547658,
125.897391574217));
#94177=CARTESIAN_POINT('Ctrl Pts',(-83.2866487331652,0.196134960716965,
125.888110898687));
#94178=CARTESIAN_POINT('Ctrl Pts',(-83.2943966299423,0.0588875961929768,
125.884549488956));
#94179=CARTESIAN_POINT('Ctrl Pts',(-83.3021445267193,-0.0783037140750059,
125.886733995824));
#94180=CARTESIAN_POINT('Ctrl Pts',(-83.3098908028034,-0.215466326878383,
125.888918045741));
#94181=CARTESIAN_POINT('Ctrl Pts',(-83.3176370788876,-0.352572518080116,
125.896845615349));
#94182=CARTESIAN_POINT('Ctrl Pts',(-83.3253833549717,-0.489106807615796,
125.910491228908));
#94183=CARTESIAN_POINT('Ctrl Pts',(-83.3331296882371,-0.62564210501677,
125.924136943196));
#94184=CARTESIAN_POINT('Ctrl Pts',(-83.3408760215024,-0.761605103300574,
125.943500746779));
#94185=CARTESIAN_POINT('Ctrl Pts',(-83.3486223547678,-0.896485521576785,
125.968505287627));
#94186=CARTESIAN_POINT('Ctrl Pts',(-83.3563704227708,-1.03139614538729,
125.993515428067));
#94187=CARTESIAN_POINT('Ctrl Pts',(-83.3641184907737,-1.16522332242821,
126.024168748151));
#94188=CARTESIAN_POINT('Ctrl Pts',(-83.3718665587766,-1.29746743044787,
126.06033686874));
#94189=CARTESIAN_POINT('Ctrl Pts',(-83.3796228615185,-1.42985208907943,
126.096543429238));
#94190=CARTESIAN_POINT('Ctrl Pts',(-83.3873791642604,-1.56064993998876,
126.138276395307));
#94191=CARTESIAN_POINT('Ctrl Pts',(-83.3951354670022,-1.68937645658072,
126.185357451249));
#94192=CARTESIAN_POINT('Ctrl Pts',(-83.4028959095164,-1.81817167839047,
126.232463635767));
#94193=CARTESIAN_POINT('Ctrl Pts',(-83.4106563520306,-1.94489300195566,
126.284923448395));
#94194=CARTESIAN_POINT('Ctrl Pts',(-83.4184167945448,-2.06907726345978,
126.342510962957));
#94195=CARTESIAN_POINT('Ctrl Pts',(-83.4261896948102,-2.19346087656504,
126.40019092211));
#94196=CARTESIAN_POINT('Ctrl Pts',(-83.4339625950757,-2.31529894133267,
126.46301485296));
#94197=CARTESIAN_POINT('Ctrl Pts',(-83.4417354953411,-2.43415343269864,
126.530711108238));
#94198=CARTESIAN_POINT('Ctrl Pts',(-83.4492258311031,-2.54868726392673,
126.595946434119));
#94199=CARTESIAN_POINT('Ctrl Pts',(-83.4567161668651,-2.66045041520976,
126.665705828973));
#94200=CARTESIAN_POINT('Ctrl Pts',(-83.4642065026271,-2.76907906306409,
126.739710053864));
#94201=CARTESIAN_POINT('Ctrl Pts',(-83.4719474395665,-2.88134205628105,
126.816190208604));
#94202=CARTESIAN_POINT('Ctrl Pts',(-83.4796883765059,-2.99061989283231,
126.897451418079));
#94203=CARTESIAN_POINT('Ctrl Pts',(-83.4874293134452,-3.09647557227514,
126.983232238042));
#94204=CARTESIAN_POINT('Ctrl Pts',(-83.4951580116616,-3.20216388976515,
127.068877435188));
#94205=CARTESIAN_POINT('Ctrl Pts',(-83.502886709878,-3.3044405208091,127.159027766624));
#94206=CARTESIAN_POINT('Ctrl Pts',(-83.5106154080944,-3.40289693775067,
127.253378289597));
#94207=CARTESIAN_POINT('Ctrl Pts',(-83.5183370415297,-3.50126335595945,
127.347642567024));
#94208=CARTESIAN_POINT('Ctrl Pts',(-83.526058674965,-3.59581622232154,127.44609912865));
#94209=CARTESIAN_POINT('Ctrl Pts',(-83.5337803084002,-3.68617946093688,
127.548402380078));
#94210=CARTESIAN_POINT('Ctrl Pts',(-83.5414965952463,-3.77648013052249,
127.65063479501));
#94211=CARTESIAN_POINT('Ctrl Pts',(-83.5492128820924,-3.86259668317436,
127.756708306345));
#94212=CARTESIAN_POINT('Ctrl Pts',(-83.5569291689385,-3.94418968735834,
127.866240338776));
#94213=CARTESIAN_POINT('Ctrl Pts',(-83.5646418232168,-4.02574428030597,
127.975720807218));
#94214=CARTESIAN_POINT('Ctrl Pts',(-83.5723544774951,-4.10277932737506,
128.088656240637));
#94215=CARTESIAN_POINT('Ctrl Pts',(-83.5800671317734,-4.17499580640857,
128.204631193381));
#94216=CARTESIAN_POINT('Ctrl Pts',(-83.5877793978067,-4.24720865015867,
128.320600308098));
#94217=CARTESIAN_POINT('Ctrl Pts',(-83.5954916638401,-4.31460319117812,
128.439608308166));
#94218=CARTESIAN_POINT('Ctrl Pts',(-83.6032039298734,-4.37692395977381,
128.561211110097));
#94219=CARTESIAN_POINT('Ctrl Pts',(-83.6109158038908,-4.4392415605924,128.682807730933));
#94220=CARTESIAN_POINT('Ctrl Pts',(-83.6186276779081,-4.49648572694092,
128.806998537271));
#94221=CARTESIAN_POINT('Ctrl Pts',(-83.6263395519254,-4.5484475173092,128.933315924144));
#94222=CARTESIAN_POINT('Ctrl Pts',(-83.6340555416557,-4.60043703891545,
129.059700724735));
#94223=CARTESIAN_POINT('Ctrl Pts',(-83.6417715313859,-4.64713840675758,
129.188214005921));
#94224=CARTESIAN_POINT('Ctrl Pts',(-83.6494875211162,-4.68839126405798,
129.318369225396));
#94225=CARTESIAN_POINT('Ctrl Pts',(-83.6546659631256,-4.71607734668912,
129.405720463517));
#94226=CARTESIAN_POINT('Ctrl Pts',(-83.6598444051351,-4.74131034347372,
129.493810888119));
#94227=CARTESIAN_POINT('Ctrl Pts',(-83.6650228471445,-4.76405452823415,
129.582490119309));
#94228=CARTESIAN_POINT('Ctrl Pts',(-81.9152188971548,-4.76405452823409,
129.582490119308));
#94229=CARTESIAN_POINT('Ctrl Pts',(-81.9229317503212,-4.79801314726194,
129.714894259504));
#94230=CARTESIAN_POINT('Ctrl Pts',(-81.9306446034876,-4.82645499448301,
129.848743097592));
#94231=CARTESIAN_POINT('Ctrl Pts',(-81.9383574566541,-4.84927101642369,
129.983535622958));
#94232=CARTESIAN_POINT('Ctrl Pts',(-81.9461546412132,-4.87233650595616,
130.119801953302));
#94233=CARTESIAN_POINT('Ctrl Pts',(-81.9539518257724,-4.88965231265043,
130.257032331246));
#94234=CARTESIAN_POINT('Ctrl Pts',(-81.9617490103315,-4.90115921366017,
130.394700484219));
#94235=CARTESIAN_POINT('Ctrl Pts',(-81.9695461948906,-4.91266611466992,
130.532368637192));
#94236=CARTESIAN_POINT('Ctrl Pts',(-81.9773433794496,-4.91836409580708,
130.670474149571));
#94237=CARTESIAN_POINT('Ctrl Pts',(-81.9851405640087,-4.91824826795356,
130.808488240592));
#94238=CARTESIAN_POINT('',(-81.6398594359374,-4.91824905295598,130.801308471165));
#94239=CARTESIAN_POINT('Ctrl Pts',(-81.5701083236628,-4.76405452823403,
129.582490119308));
#94240=CARTESIAN_POINT('Ctrl Pts',(-81.5788549634402,-4.80229009242161,
129.73157000377));
#94241=CARTESIAN_POINT('Ctrl Pts',(-81.5876016032175,-4.83356823313081,
129.882618677574));
#94242=CARTESIAN_POINT('Ctrl Pts',(-81.5963482429949,-4.85770413863388,
130.035014425011));
#94243=CARTESIAN_POINT('Ctrl Pts',(-81.6050443608007,-4.88170063133802,
130.186529910561));
#94244=CARTESIAN_POINT('Ctrl Pts',(-81.6137404786066,-4.89863706784531,
130.33937676233));
#94245=CARTESIAN_POINT('Ctrl Pts',(-81.6224365964124,-4.90837967686126,
130.492925214512));
#94246=CARTESIAN_POINT('Ctrl Pts',(-81.6282442095874,-4.91488617846839,
130.595470975022));
#94247=CARTESIAN_POINT('Ctrl Pts',(-81.6340518227623,-4.9181851465564,130.698329272967));
#94248=CARTESIAN_POINT('Ctrl Pts',(-81.6398594359373,-4.91824905295597,
130.801308471165));
#94249=CARTESIAN_POINT('Ctrl Pts',(-81.6398594359913,-4.91824905295657,
130.801308472121));
#94250=CARTESIAN_POINT('Ctrl Pts',(-81.6476687247406,-4.91833498556877,
130.939780899548));
#94251=CARTESIAN_POINT('Ctrl Pts',(-81.6554780134899,-4.9125685830178,131.078274297816));
#94252=CARTESIAN_POINT('Ctrl Pts',(-81.6632873022392,-4.90097117585682,
131.21626424212));
#94253=CARTESIAN_POINT('Ctrl Pts',(-81.6710974148324,-4.88937254522282,
131.354268743727));
#94254=CARTESIAN_POINT('Ctrl Pts',(-81.6789075274256,-4.87194171643958,
131.49176930486));
#94255=CARTESIAN_POINT('Ctrl Pts',(-81.6867176400188,-4.84875195097137,
131.628246277383));
#94256=CARTESIAN_POINT('Ctrl Pts',(-81.6945301641732,-4.82555502510229,
131.764765390471));
#94257=CARTESIAN_POINT('Ctrl Pts',(-81.7023426883276,-4.79659568558305,
131.900259909069));
#94258=CARTESIAN_POINT('Ctrl Pts',(-81.710155212482,-4.7619983407032,132.034220311043));
#94259=CARTESIAN_POINT('Ctrl Pts',(-81.7179717371523,-4.7273832797523,132.16824930938));
#94260=CARTESIAN_POINT('Ctrl Pts',(-81.7257882618226,-4.6871245600809,132.300742257428));
#94261=CARTESIAN_POINT('Ctrl Pts',(-81.733604786493,-4.64139638868414,132.431204994146));
#94262=CARTESIAN_POINT('Ctrl Pts',(-81.7414316799484,-4.59560755790249,
132.561840792438));
#94263=CARTESIAN_POINT('Ctrl Pts',(-81.7492585734038,-4.54433491332346,
132.690440640849));
#94264=CARTESIAN_POINT('Ctrl Pts',(-81.7570854668591,-4.48780098528893,
132.816529939204));
#94265=CARTESIAN_POINT('Ctrl Pts',(-81.7649183325838,-4.43122391934212,
132.942715449325));
#94266=CARTESIAN_POINT('Ctrl Pts',(-81.7727511983086,-4.36937774052998,
133.066386251551));
#94267=CARTESIAN_POINT('Ctrl Pts',(-81.7805840640333,-4.30253043869562,
133.187093268662));
#94268=CARTESIAN_POINT('Ctrl Pts',(-81.7884293310176,-4.23557730193732,
133.307991393232));
#94269=CARTESIAN_POINT('Ctrl Pts',(-81.796274598002,-4.1636074284083,133.425916037209));
#94270=CARTESIAN_POINT('Ctrl Pts',(-81.8041198649863,-4.08693187737184,
133.540447402049));
#94271=CARTESIAN_POINT('Ctrl Pts',(-81.8071164952938,-4.05764437440562,
133.584194563199));
#94272=CARTESIAN_POINT('Ctrl Pts',(-81.8101131256012,-4.02767073475177,
133.627446999452));
#94273=CARTESIAN_POINT('Ctrl Pts',(-81.8131097559086,-3.99702978244563,
133.670182660321));
#94274=CARTESIAN_POINT('Ctrl Pts',(-81.8208840900277,-3.91753615910348,
133.781054296896));
#94275=CARTESIAN_POINT('Ctrl Pts',(-81.8286584241468,-3.83330000709396,
133.888791488001));
#94276=CARTESIAN_POINT('Ctrl Pts',(-81.8364327582659,-3.74459691484425,
133.992961722728));
#94277=CARTESIAN_POINT('Ctrl Pts',(-81.844197511213,-3.65600314122812,134.09700357695));
#94278=CARTESIAN_POINT('Ctrl Pts',(-81.85196226416,-3.56295363192653,134.197486926625));
#94279=CARTESIAN_POINT('Ctrl Pts',(-81.8597270171071,-3.46576694977739,
134.294008524208));
#94280=CARTESIAN_POINT('Ctrl Pts',(-81.8674840579921,-3.36867679481105,
134.390434255179));
#94281=CARTESIAN_POINT('Ctrl Pts',(-81.8752410988771,-3.26745791989503,
134.482905790904));
#94282=CARTESIAN_POINT('Ctrl Pts',(-81.8829981397621,-3.16246857557404,
134.57105353988));
#94283=CARTESIAN_POINT('Ctrl Pts',(-81.8907493310022,-3.05755840453444,
134.659134815952));
#94284=CARTESIAN_POINT('Ctrl Pts',(-81.8985005222424,-2.94888372179954,
134.742898544929));
#94285=CARTESIAN_POINT('Ctrl Pts',(-81.9062517134825,-2.83683872562821,
134.822012806006));
#94286=CARTESIAN_POINT('Ctrl Pts',(-81.9139996102596,-2.72484135156899,
134.901093441411));
#94287=CARTESIAN_POINT('Ctrl Pts',(-81.9217475070366,-2.60947683185872,
134.975528314288));
#94288=CARTESIAN_POINT('Ctrl Pts',(-81.9294954038137,-2.49117127933511,
135.045026687833));
#94289=CARTESIAN_POINT('Ctrl Pts',(-81.9372416798978,-2.37289047378271,
135.114510523817));
#94290=CARTESIAN_POINT('Ctrl Pts',(-81.944987955982,-2.25167019597342,135.179059716482));
#94291=CARTESIAN_POINT('Ctrl Pts',(-81.9527342320661,-2.1279639472848,135.238427881552));
#94292=CARTESIAN_POINT('Ctrl Pts',(-81.9604805653315,-2.00425678542459,
135.297796484866));
#94293=CARTESIAN_POINT('Ctrl Pts',(-81.9682268985968,-1.87806396854338,
135.351983815112));
#94294=CARTESIAN_POINT('Ctrl Pts',(-81.9759732318621,-1.74986154259587,
135.400790497837));
#94295=CARTESIAN_POINT('Ctrl Pts',(-81.9837212998651,-1.62163040660414,
135.449608110479));
#94296=CARTESIAN_POINT('Ctrl Pts',(-81.9914693678681,-1.49138913133547,
135.493042538798));
#94297=CARTESIAN_POINT('Ctrl Pts',(-81.9992174358711,-1.3596312028971,135.530943532803));
#94298=CARTESIAN_POINT('Ctrl Pts',(-82.0069737386129,-1.22773324056462,
135.568884808435));
#94299=CARTESIAN_POINT('Ctrl Pts',(-82.0147300413549,-1.0943157814127,135.60128079357));
#94300=CARTESIAN_POINT('Ctrl Pts',(-82.0224863440967,-0.959885394956362,
135.628031739341));
#94301=CARTESIAN_POINT('Ctrl Pts',(-82.0302467866109,-0.82538325895515,
135.654796962898));
#94302=CARTESIAN_POINT('Ctrl Pts',(-82.0380072291249,-0.689867504514324,
135.675911083419));
#94303=CARTESIAN_POINT('Ctrl Pts',(-82.0457676716391,-0.553851222095246,
135.691326126579));
#94304=CARTESIAN_POINT('Ctrl Pts',(-82.0535405719045,-0.417616594264671,
135.706765915335));
#94305=CARTESIAN_POINT('Ctrl Pts',(-82.06131347217,-0.280880223027997,135.716488317037));
#94306=CARTESIAN_POINT('Ctrl Pts',(-82.0690863724354,-0.144157512079178,
135.720497482444));
#94307=CARTESIAN_POINT('Ctrl Pts',(-82.076576708198,-0.0124050160477781,
135.72436090459));
#94308=CARTESIAN_POINT('Ctrl Pts',(-82.0840670439605,0.119334487624514,
135.722919263247));
#94309=CARTESIAN_POINT('Ctrl Pts',(-82.0915573797231,0.25060501860766,135.716221791006));
#94310=CARTESIAN_POINT('Ctrl Pts',(-82.0993317138421,0.386852711662048,
135.70927038207));
#94311=CARTESIAN_POINT('Ctrl Pts',(-82.1071060479612,0.523026759557225,
135.696634705111));
#94312=CARTESIAN_POINT('Ctrl Pts',(-82.1148803820803,0.658614316341515,
135.678312837768));
#94313=CARTESIAN_POINT('Ctrl Pts',(-82.1226451350273,0.794034773579877,
135.660013550489));
#94314=CARTESIAN_POINT('Ctrl Pts',(-82.1304098879745,0.928869794135261,
135.636042067955));
#94315=CARTESIAN_POINT('Ctrl Pts',(-82.1381746409216,1.06260792343337,135.606448440957));
#94316=CARTESIAN_POINT('Ctrl Pts',(-82.1459316818066,1.19621322213645,135.576884206766));
#94317=CARTESIAN_POINT('Ctrl Pts',(-82.1536887226916,1.32872341837167,135.541709024433));
#94318=CARTESIAN_POINT('Ctrl Pts',(-82.1614457635766,1.45963392117172,135.501024527052));
#94319=CARTESIAN_POINT('Ctrl Pts',(-82.1691969548168,1.59044570334346,135.460370710167));
#94320=CARTESIAN_POINT('Ctrl Pts',(-82.1769481460569,1.7196598213891,135.414215963309));
#94321=CARTESIAN_POINT('Ctrl Pts',(-82.184699337297,1.84678394714717,135.362712525335));
#94322=CARTESIAN_POINT('Ctrl Pts',(-82.1924472340741,1.97385404176047,135.311230977696));
#94323=CARTESIAN_POINT('Ctrl Pts',(-82.2001951308512,2.09883554925481,135.254405406932));
#94324=CARTESIAN_POINT('Ctrl Pts',(-82.2079430276283,2.22125354012725,135.1924371635));
#94325=CARTESIAN_POINT('Ctrl Pts',(-82.2156893037124,2.34364592379502,135.130481882487));
#94326=CARTESIAN_POINT('Ctrl Pts',(-82.2234355797966,2.4634755088373,135.063386244966));
#94327=CARTESIAN_POINT('Ctrl Pts',(-82.2311818558807,2.58028987661407,134.991398617769));
#94328=CARTESIAN_POINT('Ctrl Pts',(-82.2389281891461,2.6971051066878,134.919410459176));
#94329=CARTESIAN_POINT('Ctrl Pts',(-82.2466745224114,2.81090474224335,134.842530443964));
#94330=CARTESIAN_POINT('Ctrl Pts',(-82.2544208556768,2.92126372943901,134.761051316315));
#94331=CARTESIAN_POINT('Ctrl Pts',(-82.2621689236798,3.03164743076482,134.679553941979));
#94332=CARTESIAN_POINT('Ctrl Pts',(-82.2699169916828,3.13858863603834,134.593455637922));
#94333=CARTESIAN_POINT('Ctrl Pts',(-82.2776650596858,3.2416941943933,134.50309037419));
#94334=CARTESIAN_POINT('Ctrl Pts',(-82.2854213624277,3.34490933456251,134.412629069181));
#94335=CARTESIAN_POINT('Ctrl Pts',(-82.2931776651695,3.4442803899321,134.317892003498));
#94336=CARTESIAN_POINT('Ctrl Pts',(-82.3009339679114,3.53944962575954,134.219251451723));
#94337=CARTESIAN_POINT('Ctrl Pts',(-82.3086944104256,3.6346696562739,134.120558252515));
#94338=CARTESIAN_POINT('Ctrl Pts',(-82.3164548529398,3.72568313928251,134.01795770818));
#94339=CARTESIAN_POINT('Ctrl Pts',(-82.324215295454,3.81217237469915,133.91185556496));
#94340=CARTESIAN_POINT('Ctrl Pts',(-82.3319881957195,3.8988004503144,133.805583097161));
#94341=CARTESIAN_POINT('Ctrl Pts',(-82.3397610959849,3.98088953084325,133.695798111066));
#94342=CARTESIAN_POINT('Ctrl Pts',(-82.3475339962503,4.05816452015065,133.582936473988));
#94343=CARTESIAN_POINT('Ctrl Pts',(-82.355024332012,4.13263036894901,133.474177641704));
#94344=CARTESIAN_POINT('Ctrl Pts',(-82.3625146677737,4.20262589489997,133.362562223861));
#94345=CARTESIAN_POINT('Ctrl Pts',(-82.3700050035353,4.26794605027134,133.248500461043));
#94346=CARTESIAN_POINT('Ctrl Pts',(-82.3777793376544,4.33574283919023,133.130114011815));
#94347=CARTESIAN_POINT('Ctrl Pts',(-82.3855536717735,4.398717485427,133.008717036632));
#94348=CARTESIAN_POINT('Ctrl Pts',(-82.3933280058925,4.4565911658811,132.884739968235));
#94349=CARTESIAN_POINT('Ctrl Pts',(-82.4010927588396,4.51439352219653,132.760915690495));
#94350=CARTESIAN_POINT('Ctrl Pts',(-82.4088575117866,4.56710725717209,132.63451799713));
#94351=CARTESIAN_POINT('Ctrl Pts',(-82.4166222647337,4.61449802626495,132.506004243034));
#94352=CARTESIAN_POINT('Ctrl Pts',(-82.4243793056187,4.66184172617772,132.377618130611));
#94353=CARTESIAN_POINT('Ctrl Pts',(-82.4321363465037,4.70387284687444,132.247120504383));
#94354=CARTESIAN_POINT('Ctrl Pts',(-82.4398933873887,4.7404041514135,132.114990826191));
#94355=CARTESIAN_POINT('Ctrl Pts',(-82.4476445786287,4.77690790741148,131.982960788019));
#94356=CARTESIAN_POINT('Ctrl Pts',(-82.4553957698688,4.80791999874377,131.849301522906));
#94357=CARTESIAN_POINT('Ctrl Pts',(-82.4631469611089,4.8333023928751,131.714509529298));
#94358=CARTESIAN_POINT('Ctrl Pts',(-82.4708948578859,4.85867399881194,131.579774825884));
#94359=CARTESIAN_POINT('Ctrl Pts',(-82.4786427546629,4.87842059438907,131.44390873493));
#94360=CARTESIAN_POINT('Ctrl Pts',(-82.48639065144,4.89245487044994,131.307419662918));
#94361=CARTESIAN_POINT('Ctrl Pts',(-82.494136927524,4.9064862108428,131.170959141478));
#94362=CARTESIAN_POINT('Ctrl Pts',(-82.5018832036081,4.91480756846505,131.03387628685));
#94363=CARTESIAN_POINT('Ctrl Pts',(-82.5096294796922,4.91738335804249,130.89668597999));
#94364=CARTESIAN_POINT('Ctrl Pts',(-82.5173758129575,4.91995916663382,130.759494660423));
#94365=CARTESIAN_POINT('Ctrl Pts',(-82.5251221462228,4.91678931521013,130.622196277936));
#94366=CARTESIAN_POINT('Ctrl Pts',(-82.5328684794881,4.90789034575819,130.485306677748));
#94367=CARTESIAN_POINT('Ctrl Pts',(-82.540616547491,4.89898938344374,130.348386422082));
#94368=CARTESIAN_POINT('Ctrl Pts',(-82.548364615494,4.88435677544462,130.211875520943));
#94369=CARTESIAN_POINT('Ctrl Pts',(-82.5561126834969,4.86406099257518,130.076285262257));
#94370=CARTESIAN_POINT('Ctrl Pts',(-82.5638689862388,4.84374363910614,129.94055089663));
#94371=CARTESIAN_POINT('Ctrl Pts',(-82.5716252889806,4.81775114535535,129.805739515331));
#94372=CARTESIAN_POINT('Ctrl Pts',(-82.5793815917225,4.78620335210486,129.672353314233));
#94373=CARTESIAN_POINT('Ctrl Pts',(-82.5871420342366,4.75463872084722,129.538895920903));
#94374=CARTESIAN_POINT('Ctrl Pts',(-82.5949024767508,4.71751298779507,129.406865599642));
#94375=CARTESIAN_POINT('Ctrl Pts',(-82.6026629192649,4.67499579409606,129.276748956284));
#94376=CARTESIAN_POINT('Ctrl Pts',(-82.6104358195303,4.63241034802323,129.14642343814));
#94377=CARTESIAN_POINT('Ctrl Pts',(-82.6182087197958,4.58441628311373,129.018018103176));
#94378=CARTESIAN_POINT('Ctrl Pts',(-82.6259816200612,4.53123161070032,128.89199999449));
#94379=CARTESIAN_POINT('Ctrl Pts',(-82.6334719558235,4.47998033509123,128.770562961471));
#94380=CARTESIAN_POINT('Ctrl Pts',(-82.6409622915858,4.42390941445499,128.6513428834));
#94381=CARTESIAN_POINT('Ctrl Pts',(-82.6484526273481,4.3632531625059,128.534734017796));
#94382=CARTESIAN_POINT('Ctrl Pts',(-82.6562269614672,4.30029711033031,128.413703891615));
#94383=CARTESIAN_POINT('Ctrl Pts',(-82.6640012955862,4.23220173149967,128.295103507828));
#94384=CARTESIAN_POINT('Ctrl Pts',(-82.6717756297053,4.15917845057275,128.179400107617));
#94385=CARTESIAN_POINT('Ctrl Pts',(-82.6795403826524,4.08624516431329,128.063839301506));
#94386=CARTESIAN_POINT('Ctrl Pts',(-82.6873051355995,4.00839626647538,127.951168702641));
#94387=CARTESIAN_POINT('Ctrl Pts',(-82.6950698885466,3.92588987373413,127.841832683215));
#94388=CARTESIAN_POINT('Ctrl Pts',(-82.7028269294317,3.84346542750507,127.732605257864));
#94389=CARTESIAN_POINT('Ctrl Pts',(-82.7105839703167,3.75639292607726,127.62670613108));
#94390=CARTESIAN_POINT('Ctrl Pts',(-82.7183410112018,3.66497454813711,127.524551991441));
#94391=CARTESIAN_POINT('Ctrl Pts',(-82.7260922024419,3.57362510950677,127.422474887033));
#94392=CARTESIAN_POINT('Ctrl Pts',(-82.7338433936822,3.47793657721598,127.324137438683));
#94393=CARTESIAN_POINT('Ctrl Pts',(-82.7415945849224,3.37825205951236,127.22992414661));
#94394=CARTESIAN_POINT('Ctrl Pts',(-82.7493424816995,3.27860991038807,127.1357508977));
#94395=CARTESIAN_POINT('Ctrl Pts',(-82.7570903784765,3.17497543738677,127.045698586713));
#94396=CARTESIAN_POINT('Ctrl Pts',(-82.7648382752536,3.06772918454784,126.960115475438));
#94397=CARTESIAN_POINT('Ctrl Pts',(-82.7725845513377,2.96050536531304,126.874550266305));
#94398=CARTESIAN_POINT('Ctrl Pts',(-82.7803308274219,2.84967157438043,126.793452641103));
#94399=CARTESIAN_POINT('Ctrl Pts',(-82.7880771035061,2.73564176097019,126.717130844463));
#94400=CARTESIAN_POINT('Ctrl Pts',(-82.7958234367714,2.62161110581824,126.640808484434));
#94401=CARTESIAN_POINT('Ctrl Pts',(-82.8035697700368,2.50438470601706,126.569262240779));
#94402=CARTESIAN_POINT('Ctrl Pts',(-82.8113161033021,2.38440549810417,126.502757023194));
#94403=CARTESIAN_POINT('Ctrl Pts',(-82.8190641713051,2.26439942168004,126.436236912228));
#94404=CARTESIAN_POINT('Ctrl Pts',(-82.826812239308,2.14163965231658,126.374760263225));
#94405=CARTESIAN_POINT('Ctrl Pts',(-82.834560307311,2.01659336117531,126.318545833364));
#94406=CARTESIAN_POINT('Ctrl Pts',(-82.8423166100528,1.8914141693469,126.262271658138));
#94407=CARTESIAN_POINT('Ctrl Pts',(-82.8500729127948,1.76394395842746,126.211271034733));
#94408=CARTESIAN_POINT('Ctrl Pts',(-82.8578292155367,1.63467001689946,126.165714586842));
#94409=CARTESIAN_POINT('Ctrl Pts',(-82.8655896580509,1.50532707797614,126.120133824103));
#94410=CARTESIAN_POINT('Ctrl Pts',(-82.8733501005651,1.3741788638437,126.080003141114));
#94411=CARTESIAN_POINT('Ctrl Pts',(-82.8811105430793,1.24172646495639,126.045442836313));
#94412=CARTESIAN_POINT('Ctrl Pts',(-82.8888834433448,1.10906144172018,126.010827052242));
#94413=CARTESIAN_POINT('Ctrl Pts',(-82.8966563436102,0.975088432382155,
125.981799598291));
#94414=CARTESIAN_POINT('Ctrl Pts',(-82.9044292438757,0.840318213978551,
125.958429503553));
#94415=CARTESIAN_POINT('Ctrl Pts',(-82.9119195796375,0.710447232484356,
125.935908970626));
#94416=CARTESIAN_POINT('Ctrl Pts',(-82.9194099153993,0.579836302111344,
125.91864165986));
#94417=CARTESIAN_POINT('Ctrl Pts',(-82.9269002511611,0.448943775163659,
125.906643542311));
#94418=CARTESIAN_POINT('Ctrl Pts',(-82.9346745852802,0.31308841826842,125.894190512489));
#94419=CARTESIAN_POINT('Ctrl Pts',(-82.9424489193992,0.176499340871205,
125.887374678848));
#94420=CARTESIAN_POINT('Ctrl Pts',(-82.9502232535183,0.0396839263492316,
125.886270719192));
#94421=CARTESIAN_POINT('Ctrl Pts',(-82.9579880064654,-0.0969628754018883,
125.885168120067));
#94422=CARTESIAN_POINT('Ctrl Pts',(-82.9657527594125,-0.233835072070384,
125.889763391795));
#94423=CARTESIAN_POINT('Ctrl Pts',(-82.9735175123596,-0.37041928237792,
125.90007956753));
#94424=CARTESIAN_POINT('Ctrl Pts',(-82.9812745532446,-0.506867835322649,
125.910385497094));
#94425=CARTESIAN_POINT('Ctrl Pts',(-82.9890315941297,-0.64302858379119,
125.92640099381));
#94426=CARTESIAN_POINT('Ctrl Pts',(-82.9967886350147,-0.778387620919688,
125.948097056545));
#94427=CARTESIAN_POINT('Ctrl Pts',(-83.0045398262549,-0.913644582744795,
125.969776758111));
#94428=CARTESIAN_POINT('Ctrl Pts',(-83.012291017495,-1.04810065212751,125.997128437508));
#94429=CARTESIAN_POINT('Ctrl Pts',(-83.0200422087351,-1.18124687975515,
126.030071259811));
#94430=CARTESIAN_POINT('Ctrl Pts',(-83.0277901055122,-1.31433651668442,
126.063000080536));
#94431=CARTESIAN_POINT('Ctrl Pts',(-83.0355380022893,-1.44611704040084,
126.101515224015));
#94432=CARTESIAN_POINT('Ctrl Pts',(-83.0432858990664,-1.57608975505062,
126.145484771772));
#94433=CARTESIAN_POINT('Ctrl Pts',(-83.0510321751505,-1.70603528221039,
126.189445122047));
#94434=CARTESIAN_POINT('Ctrl Pts',(-83.0587784512346,-1.83417338236171,
126.238857481993));
#94435=CARTESIAN_POINT('Ctrl Pts',(-83.0665247273187,-1.96002097090085,
126.29354019816));
#94436=CARTESIAN_POINT('Ctrl Pts',(-83.074271060584,-2.08586948841779,126.348223317982));
#94437=CARTESIAN_POINT('Ctrl Pts',(-83.0820173938494,-2.20942710200628,
126.408176715849));
#94438=CARTESIAN_POINT('Ctrl Pts',(-83.0897637271148,-2.3302315176174,126.473170926869));
#94439=CARTESIAN_POINT('Ctrl Pts',(-83.0975117951177,-2.45106298653962,
126.538179692891));
#94440=CARTESIAN_POINT('Ctrl Pts',(-83.1052598631206,-2.56913968636999,
126.608231333157));
#94441=CARTESIAN_POINT('Ctrl Pts',(-83.1130079311236,-2.68402505307463,
126.683051046936));
#94442=CARTESIAN_POINT('Ctrl Pts',(-83.1207642338654,-2.79903252131463,
126.757950279997));
#94443=CARTESIAN_POINT('Ctrl Pts',(-83.1285205366073,-2.91084155283274,
126.837627495877));
#94444=CARTESIAN_POINT('Ctrl Pts',(-83.1362768393492,-3.01904520575611,
126.921764951249));
#94445=CARTESIAN_POINT('Ctrl Pts',(-83.1440372818633,-3.12730661022699,
127.005947313315));
#94446=CARTESIAN_POINT('Ctrl Pts',(-83.1517977243776,-3.23195850359698,
127.094594405772));
#94447=CARTESIAN_POINT('Ctrl Pts',(-83.1595581668917,-3.33262882375305,
127.187349671275));
#94448=CARTESIAN_POINT('Ctrl Pts',(-83.1673310671572,-3.43346074884413,
127.280253835764));
#94449=CARTESIAN_POINT('Ctrl Pts',(-83.1751039674226,-3.53029805197323,
127.377279074937));
#94450=CARTESIAN_POINT('Ctrl Pts',(-83.182876867688,-3.62280656954413,127.478032969518));
#94451=CARTESIAN_POINT('Ctrl Pts',(-83.1903672034502,-3.71195216948843,
127.57512420625));
#94452=CARTESIAN_POINT('Ctrl Pts',(-83.1978575392124,-3.79707804529234,
127.675677477826));
#94453=CARTESIAN_POINT('Ctrl Pts',(-83.2053478749746,-3.8779230094375,127.779315792216));
#94454=CARTESIAN_POINT('Ctrl Pts',(-83.2131256248477,-3.96187010200848,
127.886930846092));
#94455=CARTESIAN_POINT('Ctrl Pts',(-83.2209033747207,-4.04147175796609,
127.998219251153));
#94456=CARTESIAN_POINT('Ctrl Pts',(-83.2286811245938,-4.116389092648,128.112795292253));
#94457=CARTESIAN_POINT('Ctrl Pts',(-83.2364463580136,-4.1911858655564,128.227186950248));
#94458=CARTESIAN_POINT('Ctrl Pts',(-83.2442115914335,-4.26131311791541,
128.3448553847));
#94459=CARTESIAN_POINT('Ctrl Pts',(-83.2519768248532,-4.32647231475834,
128.465382128539));
#94460=CARTESIAN_POINT('Ctrl Pts',(-83.2597348559254,-4.39157107566005,
128.58579708237));
#94461=CARTESIAN_POINT('Ctrl Pts',(-83.2674928869975,-4.4517107608616,128.709064732525));
#94462=CARTESIAN_POINT('Ctrl Pts',(-83.2752509180696,-4.50663606226283,
128.834737693042));
#94463=CARTESIAN_POINT('Ctrl Pts',(-83.2830025719219,-4.56151621422867,
128.960307348468));
#94464=CARTESIAN_POINT('Ctrl Pts',(-83.2907542257741,-4.61119035866945,
129.088278022726));
#94465=CARTESIAN_POINT('Ctrl Pts',(-83.2985058796263,-4.65544934868352,
129.218178274851));
#94466=CARTESIAN_POINT('Ctrl Pts',(-83.3056620891265,-4.6963085783192,129.338100221321));
#94467=CARTESIAN_POINT('Ctrl Pts',(-83.3128182986267,-4.73255301784986,
129.459666208422));
#94468=CARTESIAN_POINT('Ctrl Pts',(-83.3199745081269,-4.76405452823405,
129.582490119308));
#94469=CARTESIAN_POINT('Origin',(213.235140564004,0.,130.804360617566));
#94470=CARTESIAN_POINT('',(-85.4152252782566,-4.76405452823408,129.582490119308));
#94471=CARTESIAN_POINT('',(-85.069725199937,-4.76405452823396,129.582490119308));
#94472=CARTESIAN_POINT('',(213.235140564004,-4.76405452823405,129.582490119308));
#94473=CARTESIAN_POINT('',(-83.7351405639751,-4.91824993107876,130.80518399099));
#94474=CARTESIAN_POINT('Ctrl Pts',(-83.7351405640088,-4.91824993107866,
130.805183991582));
#94475=CARTESIAN_POINT('Ctrl Pts',(-83.7376450848192,-4.91824257246219,
130.849139125296));
#94476=CARTESIAN_POINT('Ctrl Pts',(-83.7401496056296,-4.91764597711713,
130.893088715047));
#94477=CARTESIAN_POINT('Ctrl Pts',(-83.74265412644,-4.91646050823067,130.937022343426));
#94478=CARTESIAN_POINT('Ctrl Pts',(-83.7504284605591,-4.91278067008646,
131.073397615159));
#94479=CARTESIAN_POINT('Ctrl Pts',(-83.7582027946782,-4.903416433567,131.2098356697));
#94480=CARTESIAN_POINT('Ctrl Pts',(-83.7659771287973,-4.88835356997622,
131.345823854915));
#94481=CARTESIAN_POINT('Ctrl Pts',(-83.7737418817444,-4.87330927001864,
131.481644446846));
#94482=CARTESIAN_POINT('Ctrl Pts',(-83.7815066346914,-4.85258035939235,
131.617015887731));
#94483=CARTESIAN_POINT('Ctrl Pts',(-83.7892713876385,-4.82620460097485,
131.751425669201));
#94484=CARTESIAN_POINT('Ctrl Pts',(-83.7970284285235,-4.79985503933245,
131.885701952982));
#94485=CARTESIAN_POINT('Ctrl Pts',(-83.8047854694086,-4.76786986592196,
132.019018096942));
#94486=CARTESIAN_POINT('Ctrl Pts',(-83.8125425102936,-4.73033857577903,
132.150867216509));
#94487=CARTESIAN_POINT('Ctrl Pts',(-83.8202937015337,-4.692835588274,132.282616907629));
#94488=CARTESIAN_POINT('Ctrl Pts',(-83.8280448927738,-4.64979491539434,
132.412901401863));
#94489=CARTESIAN_POINT('Ctrl Pts',(-83.8357960840139,-4.60135693763739,
132.541224859514));
#94490=CARTESIAN_POINT('Ctrl Pts',(-83.8435439807909,-4.55293954731305,
132.669493776272));
#94491=CARTESIAN_POINT('Ctrl Pts',(-83.8512918775679,-4.49912955247868,
132.795802949193));
#94492=CARTESIAN_POINT('Ctrl Pts',(-83.859039774345,-4.44011684860706,132.919672753686));
#94493=CARTESIAN_POINT('Ctrl Pts',(-83.8667860504291,-4.38111648892092,
133.043516647286));
#94494=CARTESIAN_POINT('Ctrl Pts',(-83.8745323265132,-4.31691575292055,
133.164921834666));
#94495=CARTESIAN_POINT('Ctrl Pts',(-83.8822786025973,-4.24775207911664,
133.283430067352));
#94496=CARTESIAN_POINT('Ctrl Pts',(-83.8900249358627,-4.17858789476211,
133.401939174839));
#94497=CARTESIAN_POINT('Ctrl Pts',(-83.8977712691281,-4.10446089656903,
133.517550947295));
#94498=CARTESIAN_POINT('Ctrl Pts',(-83.9055176023934,-4.02565354429549,
133.62983342823));
#94499=CARTESIAN_POINT('Ctrl Pts',(-83.9132656703964,-3.94682854366193,
133.742141054048));
#94500=CARTESIAN_POINT('Ctrl Pts',(-83.9210137383994,-3.86332132784651,
133.851117584795));
#94501=CARTESIAN_POINT('Ctrl Pts',(-83.9287618064024,-3.7754563361864,133.956361968462));
#94502=CARTESIAN_POINT('Ctrl Pts',(-83.9365181091442,-3.68749796056742,
134.061718207112));
#94503=CARTESIAN_POINT('Ctrl Pts',(-83.944274411886,-3.59517280815231,134.163334074431));
#94504=CARTESIAN_POINT('Ctrl Pts',(-83.9520307146279,-3.49884446166895,
134.260843005131));
#94505=CARTESIAN_POINT('Ctrl Pts',(-83.959791157142,-3.40246470184669,134.358403979284));
#94506=CARTESIAN_POINT('Ctrl Pts',(-83.9675515996562,-3.30207777657493,
134.451853382821));
#94507=CARTESIAN_POINT('Ctrl Pts',(-83.9753120421704,-3.19808169132444,
134.540863870357));
#94508=CARTESIAN_POINT('Ctrl Pts',(-83.9830849424358,-3.09391866232556,
134.630017245429));
#94509=CARTESIAN_POINT('Ctrl Pts',(-83.9908578427013,-2.98613520318335,
134.714717223287));
#94510=CARTESIAN_POINT('Ctrl Pts',(-83.9986307429667,-2.87516045414131,
134.794678327403));
#94511=CARTESIAN_POINT('Ctrl Pts',(-84.0061210787287,-2.76821991675548,
134.871732643975));
#94512=CARTESIAN_POINT('Ctrl Pts',(-84.0136114144907,-2.65831634101399,
134.944386475219));
#94513=CARTESIAN_POINT('Ctrl Pts',(-84.0211017502528,-2.54585492878171,
135.012424987808));
#94514=CARTESIAN_POINT('Ctrl Pts',(-84.0288760843718,-2.42912950792289,
135.083043201281));
#94515=CARTESIAN_POINT('Ctrl Pts',(-84.0366504184909,-2.30927870993854,
135.148912905052));
#94516=CARTESIAN_POINT('Ctrl Pts',(-84.04442475261,-2.18672615262975,135.209745027116));
#94517=CARTESIAN_POINT('Ctrl Pts',(-84.0521895055571,-2.064324630395,135.270502179026));
#94518=CARTESIAN_POINT('Ctrl Pts',(-84.0599542585042,-1.93922832073468,
135.326233929872));
#94519=CARTESIAN_POINT('Ctrl Pts',(-84.0677190114513,-1.8118888232123,135.376695027342));
#94520=CARTESIAN_POINT('Ctrl Pts',(-84.0754760523363,-1.68467580107403,
135.427106006138));
#94521=CARTESIAN_POINT('Ctrl Pts',(-84.0832330932213,-1.55522438594163,
135.472256606118));
#94522=CARTESIAN_POINT('Ctrl Pts',(-84.0909901341063,-1.42400940841375,
135.5119481385));
#94523=CARTESIAN_POINT('Ctrl Pts',(-84.0987413253464,-1.29289338112131,
135.551609739187));
#94524=CARTESIAN_POINT('Ctrl Pts',(-84.1064925165865,-1.16001681125566,
135.585820353627));
#94525=CARTESIAN_POINT('Ctrl Pts',(-84.1142437078267,-1.02587274188369,
135.614430074441));
#94526=CARTESIAN_POINT('Ctrl Pts',(-84.1219916046037,-0.891785687319422,
135.64302763536));
#94527=CARTESIAN_POINT('Ctrl Pts',(-84.1297395013808,-0.75643258628915,
135.666028955964));
#94528=CARTESIAN_POINT('Ctrl Pts',(-84.1374873981579,-0.6203196036862,135.683334551887));
#94529=CARTESIAN_POINT('Ctrl Pts',(-84.145233674242,-0.484235092984954,
135.700636527852));
#94530=CARTESIAN_POINT('Ctrl Pts',(-84.1529799503261,-0.347391404470298,
135.712245099661));
#94531=CARTESIAN_POINT('Ctrl Pts',(-84.1607262264102,-0.210302416876331,
135.718112336564));
#94532=CARTESIAN_POINT('Ctrl Pts',(-84.1684725596755,-0.0732124173227867,
135.723979616778));
#94533=CARTESIAN_POINT('Ctrl Pts',(-84.1762188929409,0.0641224943156463,
135.724105460799));
#94534=CARTESIAN_POINT('Ctrl Pts',(-84.1839652262063,0.201186224411701,
135.718494026989));
#94535=CARTESIAN_POINT('Ctrl Pts',(-84.1917132942092,0.338280648979591,
135.712881336537));
#94536=CARTESIAN_POINT('Ctrl Pts',(-84.1994613622121,0.475103380597773,
135.701528827593));
#94537=CARTESIAN_POINT('Ctrl Pts',(-84.2072094302151,0.611141635466226,
135.684492681752));
#94538=CARTESIAN_POINT('Ctrl Pts',(-84.214965732957,0.747324473411385,135.667438429693));
#94539=CARTESIAN_POINT('Ctrl Pts',(-84.2227220356988,0.882720780545246,
135.644688522574));
#94540=CARTESIAN_POINT('Ctrl Pts',(-84.2304783384407,1.01682562976458,135.616350715348));
#94541=CARTESIAN_POINT('Ctrl Pts',(-84.2382387809549,1.15100205477976,135.587997783382));
#94542=CARTESIAN_POINT('Ctrl Pts',(-84.245999223469,1.28388526979703,135.554051105286));
#94543=CARTESIAN_POINT('Ctrl Pts',(-84.2537596659832,1.41498473819222,135.514668596158));
#94544=CARTESIAN_POINT('Ctrl Pts',(-84.2615325662486,1.54629465909254,135.475222866729));
#94545=CARTESIAN_POINT('Ctrl Pts',(-84.269305466514,1.67581474171641,135.430323996911));
#94546=CARTESIAN_POINT('Ctrl Pts',(-84.2770783667795,1.80307284579192,135.380178727507));
#94547=CARTESIAN_POINT('Ctrl Pts',(-84.2845687025416,1.9257047972415,135.331856364954));
#94548=CARTESIAN_POINT('Ctrl Pts',(-84.2920590383037,2.04623609036355,135.278662544507));
#94549=CARTESIAN_POINT('Ctrl Pts',(-84.2995493740658,2.16426695829061,135.22082205131));
#94550=CARTESIAN_POINT('Ctrl Pts',(-84.3073237081849,2.28677300244897,135.160788518234));
#94551=CARTESIAN_POINT('Ctrl Pts',(-84.315098042304,2.40697333358794,135.095558831384));
#94552=CARTESIAN_POINT('Ctrl Pts',(-84.3228723764231,2.52439577147361,135.025333141934));
#94553=CARTESIAN_POINT('Ctrl Pts',(-84.3306371293702,2.6416734966986,134.955193999369));
#94554=CARTESIAN_POINT('Ctrl Pts',(-84.3384018823172,2.7561798081096,134.880071303797));
#94555=CARTESIAN_POINT('Ctrl Pts',(-84.3461666352643,2.8674642673941,134.800212433852));
#94556=CARTESIAN_POINT('Ctrl Pts',(-84.3539236761493,2.9786381973848,134.720432880863));
#94557=CARTESIAN_POINT('Ctrl Pts',(-84.3616807170344,3.08659632778562,134.635926741212));
#94558=CARTESIAN_POINT('Ctrl Pts',(-84.3694377579194,3.19091483855833,134.546986107188));
#94559=CARTESIAN_POINT('Ctrl Pts',(-84.3771889491595,3.29515468193073,134.458112543988));
#94560=CARTESIAN_POINT('Ctrl Pts',(-84.3849401403995,3.39576007245741,134.364811395245));
#94561=CARTESIAN_POINT('Ctrl Pts',(-84.3926913316397,3.49233838699389,134.267416443456));
#94562=CARTESIAN_POINT('Ctrl Pts',(-84.4004392284168,3.58887565317052,134.170062887119));
#94563=CARTESIAN_POINT('Ctrl Pts',(-84.4081871251939,3.68138897291665,134.068619265448));
#94564=CARTESIAN_POINT('Ctrl Pts',(-84.415935021971,3.76952105272785,133.963457655573));
#94565=CARTESIAN_POINT('Ctrl Pts',(-84.4236812980551,3.85763469720762,133.858318043239));
#94566=CARTESIAN_POINT('Ctrl Pts',(-84.4314275741392,3.94136867367733,133.749462289095));
#94567=CARTESIAN_POINT('Ctrl Pts',(-84.4391738502233,4.02040489263177,133.637296826132));
#94568=CARTESIAN_POINT('Ctrl Pts',(-84.4469201834886,4.09944169501374,133.525130535188));
#94569=CARTESIAN_POINT('Ctrl Pts',(-84.454666516754,4.17378044548553,133.409654806267));
#94570=CARTESIAN_POINT('Ctrl Pts',(-84.4624128500193,4.2431456813816,133.291306091249));
#94571=CARTESIAN_POINT('Ctrl Pts',(-84.4701609180223,4.31252645114139,133.172930872857));
#94572=CARTESIAN_POINT('Ctrl Pts',(-84.4779089860252,4.37693129236773,133.05168172534));
#94573=CARTESIAN_POINT('Ctrl Pts',(-84.4856570540282,4.43613030005905,132.928020435757));
#94574=CARTESIAN_POINT('Ctrl Pts',(-84.4934133567701,4.49539222516014,132.804227717484));
#94575=CARTESIAN_POINT('Ctrl Pts',(-84.501169659512,4.54943709523391,132.678018089174));
#94576=CARTESIAN_POINT('Ctrl Pts',(-84.5089259622539,4.59808264214261,132.549874604484));
#94577=CARTESIAN_POINT('Ctrl Pts',(-84.516686404768,4.64675415264437,132.421662725758));
#94578=CARTESIAN_POINT('Ctrl Pts',(-84.5244468472822,4.69002047451208,132.291515304811));
#94579=CARTESIAN_POINT('Ctrl Pts',(-84.5322072897963,4.72774931916171,132.159930400966));
#94580=CARTESIAN_POINT('Ctrl Pts',(-84.5399801900618,4.76553872950219,132.02813426535));
#94581=CARTESIAN_POINT('Ctrl Pts',(-84.5477530903272,4.79777280708402,131.894896415787));
#94582=CARTESIAN_POINT('Ctrl Pts',(-84.5555259905927,4.82437028545145,131.760725825712));
#94583=CARTESIAN_POINT('Ctrl Pts',(-84.5630163263546,4.85000087848501,131.631432674544));
#94584=CARTESIAN_POINT('Ctrl Pts',(-84.5705066621165,4.87039751888811,131.501273724736));
#94585=CARTESIAN_POINT('Ctrl Pts',(-84.5779969978785,4.88553324101221,131.370706813337));
#94586=CARTESIAN_POINT('Ctrl Pts',(-84.5857713319976,4.90124283864115,131.235189417808));
#94587=CARTESIAN_POINT('Ctrl Pts',(-84.5935456661167,4.91133447073031,131.098803235904));
#94588=CARTESIAN_POINT('Ctrl Pts',(-84.6013200002357,4.91572130518057,130.96205371283));
#94589=CARTESIAN_POINT('Ctrl Pts',(-84.6090847531828,4.92010273324944,130.82547272132));
#94590=CARTESIAN_POINT('Ctrl Pts',(-84.61684950613,4.91879334016872,130.688529666612));
#94591=CARTESIAN_POINT('Ctrl Pts',(-84.624614259077,4.91175777968097,130.55173722941));
#94592=CARTESIAN_POINT('Ctrl Pts',(-84.632371299962,4.90472920701109,130.415080656385));
#94593=CARTESIAN_POINT('Ctrl Pts',(-84.640128340847,4.89198580488988,130.278574791087));
#94594=CARTESIAN_POINT('Ctrl Pts',(-84.647885381732,4.87354423374991,130.142734088334));
#94595=CARTESIAN_POINT('Ctrl Pts',(-84.6556365729722,4.85511656954221,130.006995824113));
#94596=CARTESIAN_POINT('Ctrl Pts',(-84.6633877642123,4.8309993416822,129.871922109868));
#94597=CARTESIAN_POINT('Ctrl Pts',(-84.6711389554524,4.80126114843691,129.738023688162));
#94598=CARTESIAN_POINT('Ctrl Pts',(-84.6788868522295,4.771535594717,129.604182176858));
#94599=CARTESIAN_POINT('Ctrl Pts',(-84.6866347490066,4.73619391185903,129.471515345431));
#94600=CARTESIAN_POINT('Ctrl Pts',(-84.6943826457837,4.69535601302328,129.340524911803));
#94601=CARTESIAN_POINT('Ctrl Pts',(-84.7021289218678,4.65452665659561,129.20956187855));
#94602=CARTESIAN_POINT('Ctrl Pts',(-84.7098751979518,4.60820348727698,129.080274918612));
#94603=CARTESIAN_POINT('Ctrl Pts',(-84.7176214740359,4.55655651350683,128.953151336658));
#94604=CARTESIAN_POINT('Ctrl Pts',(-84.7253678073012,4.50490915849052,128.826026816307));
#94605=CARTESIAN_POINT('Ctrl Pts',(-84.7331141405666,4.44793806776186,128.701066068019));
#94606=CARTESIAN_POINT('Ctrl Pts',(-84.740860473832,4.38586154634956,128.578736759239));
#94607=CARTESIAN_POINT('Ctrl Pts',(-84.7486085418349,4.32377112333078,128.456380055659));
#94608=CARTESIAN_POINT('Ctrl Pts',(-84.7563566098379,4.25657317142948,128.336656312788));
#94609=CARTESIAN_POINT('Ctrl Pts',(-84.7641046778409,4.18453193590752,128.2200085634));
#94610=CARTESIAN_POINT('Ctrl Pts',(-84.7718609805827,4.11241413410304,128.103236839396));
#94611=CARTESIAN_POINT('Ctrl Pts',(-84.7796172833246,4.03544297175806,127.98954797263));
#94612=CARTESIAN_POINT('Ctrl Pts',(-84.7873735860664,3.95392633521457,127.879356412749));
#94613=CARTESIAN_POINT('Ctrl Pts',(-84.7951340285806,3.87236619078753,127.769106040314));
#94614=CARTESIAN_POINT('Ctrl Pts',(-84.8028944710948,3.78625598338683,127.662356998312));
#94615=CARTESIAN_POINT('Ctrl Pts',(-84.8106549136089,3.69594323921468,127.559489798103));
#94616=CARTESIAN_POINT('Ctrl Pts',(-84.8184278138744,3.605485517008,127.456457466332));
#94617=CARTESIAN_POINT('Ctrl Pts',(-84.8262007141398,3.51081204697257,127.357319711741));
#94618=CARTESIAN_POINT('Ctrl Pts',(-84.8339736144053,3.41230711637157,127.262420018677));
#94619=CARTESIAN_POINT('Ctrl Pts',(-84.8414639501674,3.31738308811578,127.170970168492));
#94620=CARTESIAN_POINT('Ctrl Pts',(-84.8489542859295,3.21890155970101,127.083455805576));
#94621=CARTESIAN_POINT('Ctrl Pts',(-84.8564446216916,3.11723314681125,127.000147089));
#94622=CARTESIAN_POINT('Ctrl Pts',(-84.8642189558106,3.01170994514667,126.913679697116));
#94623=CARTESIAN_POINT('Ctrl Pts',(-84.8719932899298,2.90241916130007,126.831469258493));
#94624=CARTESIAN_POINT('Ctrl Pts',(-84.8797676240489,2.78973910576426,126.753862032914));
#94625=CARTESIAN_POINT('Ctrl Pts',(-84.8875323769959,2.67719791832639,126.676350451304));
#94626=CARTESIAN_POINT('Ctrl Pts',(-84.895297129943,2.56127608902775,126.603431014697));
#94627=CARTESIAN_POINT('Ctrl Pts',(-84.9030618828901,2.44238584514977,126.535410577344));
#94628=CARTESIAN_POINT('Ctrl Pts',(-84.9108189237751,2.32361368473807,126.467457698848));
#94629=CARTESIAN_POINT('Ctrl Pts',(-84.9185759646601,2.20187931409443,126.40439432943));
#94630=CARTESIAN_POINT('Ctrl Pts',(-84.926333005545,2.07762456399858,126.346484527591));
#94631=CARTESIAN_POINT('Ctrl Pts',(-84.9340841967852,1.95346351537617,126.288618395984));
#94632=CARTESIAN_POINT('Ctrl Pts',(-84.9418353880253,1.82678622334068,126.23589826091));
#94633=CARTESIAN_POINT('Ctrl Pts',(-84.9495865792654,1.69805946911441,126.188542477534));
#94634=CARTESIAN_POINT('Ctrl Pts',(-84.9573344760425,1.56938742719277,126.141206821629));
#94635=CARTESIAN_POINT('Ctrl Pts',(-84.9650823728196,1.4386680217402,126.099231117392));
#94636=CARTESIAN_POINT('Ctrl Pts',(-84.9728302695966,1.30638817824548,126.062785669277));
#94637=CARTESIAN_POINT('Ctrl Pts',(-84.9805765456808,1.17413600484203,126.026347844764));
#94638=CARTESIAN_POINT('Ctrl Pts',(-84.9883228217649,1.04032441932584,125.995438079196));
#94639=CARTESIAN_POINT('Ctrl Pts',(-84.996069097849,0.905455298630496,125.970176739735));
#94640=CARTESIAN_POINT('Ctrl Pts',(-85.0038154311144,0.770585182362128,
125.9449152138));
#94641=CARTESIAN_POINT('Ctrl Pts',(-85.0115617643797,0.634657899619902,
125.92530226915));
#94642=CARTESIAN_POINT('Ctrl Pts',(-85.0193080976451,0.498184911470203,
125.911407025258));
#94643=CARTESIAN_POINT('Ctrl Pts',(-85.0270561656481,0.361681361141231,
125.897508669622));
#94644=CARTESIAN_POINT('Ctrl Pts',(-85.034804233651,0.224632251107003,125.889330602264));
#94645=CARTESIAN_POINT('Ctrl Pts',(-85.042552301654,0.0875531484062345,
125.886889976199));
#94646=CARTESIAN_POINT('Ctrl Pts',(-85.0503086043958,-0.0496716435959595,
125.884446756208));
#94647=CARTESIAN_POINT('Ctrl Pts',(-85.0580649071377,-0.186926100415,125.887753165533));
#94648=CARTESIAN_POINT('Ctrl Pts',(-85.0658212098795,-0.323695113736321,
125.896774190834));
#94649=CARTESIAN_POINT('Ctrl Pts',(-85.0735816523937,-0.460537124798459,
125.905800030928));
#94650=CARTESIAN_POINT('Ctrl Pts',(-85.0813420949078,-0.596892787583985,
125.920546522489));
#94651=CARTESIAN_POINT('Ctrl Pts',(-85.089102537422,-0.732254120706716,
125.940926957567));
#94652=CARTESIAN_POINT('Ctrl Pts',(-85.0968754376874,-0.867832747858191,
125.961340109129));
#94653=CARTESIAN_POINT('Ctrl Pts',(-85.1046483379529,-1.00241347160462,
125.987405202831));
#94654=CARTESIAN_POINT('Ctrl Pts',(-85.1124212382183,-1.1354995921853,126.018984588595));
#94655=CARTESIAN_POINT('Ctrl Pts',(-85.1199115739803,-1.26374769705952,
126.049415984143));
#94656=CARTESIAN_POINT('Ctrl Pts',(-85.1274019097423,-1.39060768076853,
126.084967632327));
#94657=CARTESIAN_POINT('Ctrl Pts',(-85.1348922455044,-1.51565192400376,
126.125473751252));
#94658=CARTESIAN_POINT('Ctrl Pts',(-85.1426665796235,-1.6454372577271,126.167515671988));
#94659=CARTESIAN_POINT('Ctrl Pts',(-85.1504409137426,-1.77367756630603,
126.215028353537));
#94660=CARTESIAN_POINT('Ctrl Pts',(-85.1582152478616,-1.89987704551724,
126.267880674436));
#94661=CARTESIAN_POINT('Ctrl Pts',(-85.1659800008087,-2.02592099514908,
126.320667859574));
#94662=CARTESIAN_POINT('Ctrl Pts',(-85.1737447537559,-2.14992876263638,
126.378781440998));
#94663=CARTESIAN_POINT('Ctrl Pts',(-85.181509506703,-2.27141936389203,126.442040462438));
#94664=CARTESIAN_POINT('Ctrl Pts',(-85.189266547588,-2.39278929897012,126.505236654127));
#94665=CARTESIAN_POINT('Ctrl Pts',(-85.1970235884729,-2.51164669856962,
126.573567936267));
#94666=CARTESIAN_POINT('Ctrl Pts',(-85.2047806293579,-2.62753058246556,
126.646805314181));
#94667=CARTESIAN_POINT('Ctrl Pts',(-85.2125318205981,-2.74332707742305,
126.719987463218));
#94668=CARTESIAN_POINT('Ctrl Pts',(-85.2202830118382,-2.85615419078308,
126.798068135926));
#94669=CARTESIAN_POINT('Ctrl Pts',(-85.2280342030784,-2.9655759075078,126.880772642344));
#94670=CARTESIAN_POINT('Ctrl Pts',(-85.2357820998554,-3.07495111708415,
126.96344199714));
#94671=CARTESIAN_POINT('Ctrl Pts',(-85.2435299966326,-3.18092349751863,
127.05073104166));
#94672=CARTESIAN_POINT('Ctrl Pts',(-85.2512778934097,-3.28308657173051,
127.142322165416));
#94673=CARTESIAN_POINT('Ctrl Pts',(-85.2590241694938,-3.38522827562965,
127.233894130284));
#94674=CARTESIAN_POINT('Ctrl Pts',(-85.2667704455778,-3.48356196731321,
127.329766123617));
#94675=CARTESIAN_POINT('Ctrl Pts',(-85.2745167216619,-3.57771510173734,
127.429580963529));
#94676=CARTESIAN_POINT('Ctrl Pts',(-85.2822630549272,-3.67186893117813,
127.529396540251));
#94677=CARTESIAN_POINT('Ctrl Pts',(-85.2900093881926,-3.76184187351027,
127.633154737226));
#94678=CARTESIAN_POINT('Ctrl Pts',(-85.2977557214579,-3.84729931936343,
127.740462608538));
#94679=CARTESIAN_POINT('Ctrl Pts',(-85.3055037894609,-3.93277590281919,
127.847794510704));
#94680=CARTESIAN_POINT('Ctrl Pts',(-85.3132518574639,-4.01373473408586,
127.958677363241));
#94681=CARTESIAN_POINT('Ctrl Pts',(-85.3209999254669,-4.0898827052696,128.072686676621));
#94682=CARTESIAN_POINT('Ctrl Pts',(-85.3287562282087,-4.1661116074234,128.186817160457));
#94683=CARTESIAN_POINT('Ctrl Pts',(-85.3365125309506,-4.23751921815287,
128.304080417231));
#94684=CARTESIAN_POINT('Ctrl Pts',(-85.3442688336925,-4.30385656654757,
128.424024146164));
#94685=CARTESIAN_POINT('Ctrl Pts',(-85.3520292762067,-4.37022932118248,
128.544031892677));
#94686=CARTESIAN_POINT('Ctrl Pts',(-85.3597897187208,-4.43152624659729,
128.666722612464));
#94687=CARTESIAN_POINT('Ctrl Pts',(-85.367550161235,-4.48754571629947,128.791622058631));
#94688=CARTESIAN_POINT('Ctrl Pts',(-85.3753230615004,-4.5436551134276,128.916722004478));
#94689=CARTESIAN_POINT('Ctrl Pts',(-85.3830959617658,-4.59446998039584,
129.044037398712));
#94690=CARTESIAN_POINT('Ctrl Pts',(-85.3908688620313,-4.6398376477609,129.173075950526));
#94691=CARTESIAN_POINT('Ctrl Pts',(-85.3983591977933,-4.68355608614274,
129.297423625952));
#94692=CARTESIAN_POINT('Ctrl Pts',(-85.4058495335553,-4.72221639757264,
129.423371057348));
#94693=CARTESIAN_POINT('Ctrl Pts',(-85.4133398693172,-4.75572692037172,
129.550468867313));
#94694=CARTESIAN_POINT('Ctrl Pts',(-85.4139683389637,-4.75853858957919,
129.561132890694));
#94695=CARTESIAN_POINT('Ctrl Pts',(-85.4145968086102,-4.76131447935733,
129.571806710324));
#94696=CARTESIAN_POINT('Ctrl Pts',(-85.4152252782566,-4.76405452823408,
129.582490119308));
#94697=CARTESIAN_POINT('Ctrl Pts',(-83.6650228471445,-4.76405452823415,
129.582490119309));
#94698=CARTESIAN_POINT('Ctrl Pts',(-83.6727478526518,-4.7979834497542,129.714778469372));
#94699=CARTESIAN_POINT('Ctrl Pts',(-83.6804728581592,-4.82637148214606,
129.848377264129));
#94700=CARTESIAN_POINT('Ctrl Pts',(-83.6881978636665,-4.84914314726169,
129.982780554599));
#94701=CARTESIAN_POINT('Ctrl Pts',(-83.6960216470513,-4.87220598844752,
130.118902429184));
#94702=CARTESIAN_POINT('Ctrl Pts',(-83.7038454304361,-4.88950779304398,
130.255849098009));
#94703=CARTESIAN_POINT('Ctrl Pts',(-83.7116692138208,-4.9010245141228,130.393092123189));
#94704=CARTESIAN_POINT('Ctrl Pts',(-83.7194929972056,-4.91254123520162,
130.530335148369));
#94705=CARTESIAN_POINT('Ctrl Pts',(-83.7273167805903,-4.91827291838221,
130.667874113824));
#94706=CARTESIAN_POINT('Ctrl Pts',(-83.7351405639751,-4.91824993107876,
130.805183990989));
#94707=CARTESIAN_POINT('',(-83.3898594360444,-4.91824854697785,130.808141179725));
#94708=CARTESIAN_POINT('Ctrl Pts',(-83.3199745081269,-4.76405452823405,
129.582490119308));
#94709=CARTESIAN_POINT('Ctrl Pts',(-83.3277201319047,-4.79815063006876,
129.715430302881));
#94710=CARTESIAN_POINT('Ctrl Pts',(-83.3354657556824,-4.82668962234322,
129.849844006803));
#94711=CARTESIAN_POINT('Ctrl Pts',(-83.3432113794602,-4.8495570910012,129.985227488203));
#94712=CARTESIAN_POINT('Ctrl Pts',(-83.3509860555487,-4.87251033103457,
130.121118766403));
#94713=CARTESIAN_POINT('Ctrl Pts',(-83.3587607316373,-4.88974931916973,
130.257986727359));
#94714=CARTESIAN_POINT('Ctrl Pts',(-83.3665354077258,-4.90121034433255,
130.395312670367));
#94715=CARTESIAN_POINT('Ctrl Pts',(-83.3743100838143,-4.91267136949533,
130.532638613375));
#94716=CARTESIAN_POINT('Ctrl Pts',(-83.3820847599029,-4.91835440890207,
130.670422141569));
#94717=CARTESIAN_POINT('Ctrl Pts',(-83.3898594359914,-4.91824854697857,
130.808141178786));
#94718=CARTESIAN_POINT('Ctrl Pts',(-83.3898594360443,-4.91824854697785,
130.808141179725));
#94719=CARTESIAN_POINT('Ctrl Pts',(-83.3988547443525,-4.91812606459202,
130.967482248801));
#94720=CARTESIAN_POINT('Ctrl Pts',(-83.4078500526607,-4.91025620410759,
131.126502818401));
#94721=CARTESIAN_POINT('Ctrl Pts',(-83.4168453609689,-4.89475572259842,
131.284516299184));
#94722=CARTESIAN_POINT('Ctrl Pts',(-83.4258919752923,-4.87916683189729,
131.443431032237));
#94723=CARTESIAN_POINT('Ctrl Pts',(-83.4349385896156,-4.85586013639439,
131.601327047096));
#94724=CARTESIAN_POINT('Ctrl Pts',(-83.443985203939,-4.82500359745644,131.757525528288));
#94725=CARTESIAN_POINT('Ctrl Pts',(-83.4530931965809,-4.79393770699704,
131.914783765073));
#94726=CARTESIAN_POINT('Ctrl Pts',(-83.4622011892227,-4.75521925941508,
132.070321249573));
#94727=CARTESIAN_POINT('Ctrl Pts',(-83.4713091818646,-4.70906796023881,
132.223466677151));
#94728=CARTESIAN_POINT('Ctrl Pts',(-83.4754712875057,-4.68797806807494,
132.293449984462));
#94729=CARTESIAN_POINT('Ctrl Pts',(-83.4796333931467,-4.66533667133282,
132.362934075846));
#94730=CARTESIAN_POINT('Ctrl Pts',(-83.4837954987878,-4.64116799542365,
132.431856454966));
#94731=CARTESIAN_POINT('Ctrl Pts',(-83.4915698329069,-4.59602369156994,
132.560595523544));
#94732=CARTESIAN_POINT('Ctrl Pts',(-83.499344167026,-4.54544727869063,132.687658728732));
#94733=CARTESIAN_POINT('Ctrl Pts',(-83.507118501145,-4.48958173842214,132.812553555639));
#94734=CARTESIAN_POINT('Ctrl Pts',(-83.5148832540921,-4.43378504743918,
132.937294460834));
#94735=CARTESIAN_POINT('Ctrl Pts',(-83.5226480070392,-4.37271235679831,
133.05987195143));
#94736=CARTESIAN_POINT('Ctrl Pts',(-83.5304127599863,-4.306556112949,133.179809524304));
#94737=CARTESIAN_POINT('Ctrl Pts',(-83.5381698008712,-4.24046557641391,
133.299627973489));
#94738=CARTESIAN_POINT('Ctrl Pts',(-83.5459268417562,-4.16930172213016,
133.416811382731));
#94739=CARTESIAN_POINT('Ctrl Pts',(-83.5536838826411,-4.09330454108528,
133.530904399798));
#94740=CARTESIAN_POINT('Ctrl Pts',(-83.5614350738812,-4.01736467010568,
133.644911378434));
#94741=CARTESIAN_POINT('Ctrl Pts',(-83.5691862651213,-3.93659894307991,
133.75583227952));
#94742=CARTESIAN_POINT('Ctrl Pts',(-83.5769374563614,-3.85129243402407,
133.86323780538));
#94743=CARTESIAN_POINT('Ctrl Pts',(-83.5846853531385,-3.76602218251008,
133.970597681027));
#94744=CARTESIAN_POINT('Ctrl Pts',(-83.5924332499156,-3.67621523014584,
134.074444847647));
#94745=CARTESIAN_POINT('Ctrl Pts',(-83.6001811466927,-3.58219885028352,
134.174380566992));
#94746=CARTESIAN_POINT('Ctrl Pts',(-83.6079274227768,-3.4882021366211,134.274295381938));
#94747=CARTESIAN_POINT('Ctrl Pts',(-83.6156736988608,-3.38999801458852,
134.370300092455));
#94748=CARTESIAN_POINT('Ctrl Pts',(-83.6234199749449,-3.2879525032671,134.462030832164));
#94749=CARTESIAN_POINT('Ctrl Pts',(-83.6311663082103,-3.18590623866902,
134.553762249009));
#94750=CARTESIAN_POINT('Ctrl Pts',(-83.6389126414756,-3.0800188189575,134.641219370721));
#94751=CARTESIAN_POINT('Ctrl Pts',(-83.646658974741,-2.97069110659266,134.72407711391));
#94752=CARTESIAN_POINT('Ctrl Pts',(-83.654407042744,-2.86133891104451,134.806953412516));
#94753=CARTESIAN_POINT('Ctrl Pts',(-83.6621551107469,-2.74854520130655,
134.885228046916));
#94754=CARTESIAN_POINT('Ctrl Pts',(-83.6699031787499,-2.6327413784461,134.958618180202));
#94755=CARTESIAN_POINT('Ctrl Pts',(-83.6776594814917,-2.51681447790479,
135.032086313395));
#94756=CARTESIAN_POINT('Ctrl Pts',(-83.6854157842335,-2.39787140428618,
135.100659365664));
#94757=CARTESIAN_POINT('Ctrl Pts',(-83.6931720869753,-2.27637030273414,
135.164099291768));
#94758=CARTESIAN_POINT('Ctrl Pts',(-83.7009325294894,-2.15480435238587,
135.22757307767));
#94759=CARTESIAN_POINT('Ctrl Pts',(-83.7086929720037,-2.03067800729966,
135.285908112105));
#94760=CARTESIAN_POINT('Ctrl Pts',(-83.7164534145178,-1.90447021627643,
135.338914207261));
#94761=CARTESIAN_POINT('Ctrl Pts',(-83.7242263147832,-1.77805982530285,
135.392005392507));
#94762=CARTESIAN_POINT('Ctrl Pts',(-83.7319992150486,-1.64956167806223,
135.439750407634));
#94763=CARTESIAN_POINT('Ctrl Pts',(-83.739772115314,-1.51947158723861,135.482008440786));
#94764=CARTESIAN_POINT('Ctrl Pts',(-83.7472624510759,-1.39411059889536,
135.522730287991));
#94765=CARTESIAN_POINT('Ctrl Pts',(-83.7547527868379,-1.26727169637365,
135.558357075127));
#94766=CARTESIAN_POINT('Ctrl Pts',(-83.7622431225998,-1.13940632728965,
135.588807950731));
#94767=CARTESIAN_POINT('Ctrl Pts',(-83.7700174567189,-1.00669290387129,
135.620413380539));
#94768=CARTESIAN_POINT('Ctrl Pts',(-83.7777917908379,-0.872453244171115,
135.646542778081));
#94769=CARTESIAN_POINT('Ctrl Pts',(-83.785566124957,-0.737178999982175,
135.667050221529));
#94770=CARTESIAN_POINT('Ctrl Pts',(-83.7933308779041,-0.602071469209758,
135.687532391384));
#94771=CARTESIAN_POINT('Ctrl Pts',(-83.8010956308511,-0.465932273721789,
135.702406334869));
#94772=CARTESIAN_POINT('Ctrl Pts',(-83.8088603837982,-0.329266331098542,
135.711576401053));
#94773=CARTESIAN_POINT('Ctrl Pts',(-83.8166174246832,-0.192736127016161,
135.720737359398));
#94774=CARTESIAN_POINT('Ctrl Pts',(-83.8243744655681,-0.0556806044995665,
135.724205688384));
#94775=CARTESIAN_POINT('Ctrl Pts',(-83.8321315064531,0.081387414730357,
135.721937170221));
#94776=CARTESIAN_POINT('Ctrl Pts',(-83.8398826976932,0.218352069900932,
135.719670362765));
#94777=CARTESIAN_POINT('Ctrl Pts',(-83.8476338889332,0.355328813697248,
135.711675325645));
#94778=CARTESIAN_POINT('Ctrl Pts',(-83.8553850801734,0.491802376358289,
135.697959853824));
#94779=CARTESIAN_POINT('Ctrl Pts',(-83.8631329769504,0.628217934114462,
135.684250211445));
#94780=CARTESIAN_POINT('Ctrl Pts',(-83.8708808737275,0.764130347906118,
135.664825009123));
#94781=CARTESIAN_POINT('Ctrl Pts',(-83.8786287705045,0.899027248710216,
135.639744063434));
#94782=CARTESIAN_POINT('Ctrl Pts',(-83.8863750465886,1.03389593199071,135.614668364139));
#94783=CARTESIAN_POINT('Ctrl Pts',(-83.8941213226727,1.16774914067108,135.583939346068));
#94784=CARTESIAN_POINT('Ctrl Pts',(-83.9018675987568,1.30008290140695,135.547668272776));
#94785=CARTESIAN_POINT('Ctrl Pts',(-83.9096139320221,1.43241763900075,135.511396931738));
#94786=CARTESIAN_POINT('Ctrl Pts',(-83.9173602652875,1.56323252921032,135.469583557192));
#94787=CARTESIAN_POINT('Ctrl Pts',(-83.9251065985528,1.69203739421934,135.422389690565));
#94788=CARTESIAN_POINT('Ctrl Pts',(-83.9328546665557,1.82087110418464,135.375185255198));
#94789=CARTESIAN_POINT('Ctrl Pts',(-83.9406027345587,1.94769352621084,135.32259806457));
#94790=CARTESIAN_POINT('Ctrl Pts',(-83.9483508025616,2.07203351878264,135.264838188358));
#94791=CARTESIAN_POINT('Ctrl Pts',(-83.9561071053035,2.19650566137838,135.207016924263));
#94792=CARTESIAN_POINT('Ctrl Pts',(-83.9638634080453,2.31848974897926,135.144012157526));
#94793=CARTESIAN_POINT('Ctrl Pts',(-83.9716197107872,2.43753786874083,135.076080669366));
#94794=CARTESIAN_POINT('Ctrl Pts',(-83.9793801533013,2.55664952806839,135.008112924126));
#94795=CARTESIAN_POINT('Ctrl Pts',(-83.9871405958155,2.67282176614634,134.935213425589));
#94796=CARTESIAN_POINT('Ctrl Pts',(-83.9949010383297,2.78563568905678,134.857682325789));
#94797=CARTESIAN_POINT('Ctrl Pts',(-84.0026739385951,2.89863071089142,134.780026766185));
#94798=CARTESIAN_POINT('Ctrl Pts',(-84.0104468388605,3.0082563316525,134.697724982568));
#94799=CARTESIAN_POINT('Ctrl Pts',(-84.0182197391259,3.11412608347067,134.611118003945));
#94800=CARTESIAN_POINT('Ctrl Pts',(-84.0257100748881,3.2161472031436,134.527659407141));
#94801=CARTESIAN_POINT('Ctrl Pts',(-84.0332004106503,3.31468055319453,134.440203394861));
#94802=CARTESIAN_POINT('Ctrl Pts',(-84.0406907464125,3.40941409253309,134.34908608058));
#94803=CARTESIAN_POINT('Ctrl Pts',(-84.0484650805316,3.5077394828064,134.254514025635));
#94804=CARTESIAN_POINT('Ctrl Pts',(-84.0562394146507,3.60228270003551,134.155697975682));
#94805=CARTESIAN_POINT('Ctrl Pts',(-84.0640137487698,3.69265522625002,134.052972696985));
#94806=CARTESIAN_POINT('Ctrl Pts',(-84.0717785017169,3.7829163764028,133.950374018014));
#94807=CARTESIAN_POINT('Ctrl Pts',(-84.0795432546639,3.86901680685477,133.843875986957));
#94808=CARTESIAN_POINT('Ctrl Pts',(-84.087308007611,3.95060312348455,133.73385170361));
#94809=CARTESIAN_POINT('Ctrl Pts',(-84.095065048496,4.03210840743449,133.623936697934));
#94810=CARTESIAN_POINT('Ctrl Pts',(-84.102822089381,4.10910826852633,133.510502721761));
#94811=CARTESIAN_POINT('Ctrl Pts',(-84.110579130266,4.18128831241459,133.393957325736));
#94812=CARTESIAN_POINT('Ctrl Pts',(-84.1183303215061,4.25341392477017,133.277499817501));
#94813=CARTESIAN_POINT('Ctrl Pts',(-84.1260815127463,4.32072674947453,133.157935890709));
#94814=CARTESIAN_POINT('Ctrl Pts',(-84.1338327039864,4.38295482875981,133.035703269771));
#94815=CARTESIAN_POINT('Ctrl Pts',(-84.1415806007634,4.44515645945148,132.913522600959));
#94816=CARTESIAN_POINT('Ctrl Pts',(-84.1493284975406,4.50227746608728,132.788675841654));
#94817=CARTESIAN_POINT('Ctrl Pts',(-84.1570763943177,4.55409122607484,132.661626394747));
#94818=CARTESIAN_POINT('Ctrl Pts',(-84.1648226704018,4.6058941477408,132.534603523846));
#94819=CARTESIAN_POINT('Ctrl Pts',(-84.1725689464858,4.65239188338515,132.405379243598));
#94820=CARTESIAN_POINT('Ctrl Pts',(-84.1803152225699,4.69340563228344,132.274437701718));
#94821=CARTESIAN_POINT('Ctrl Pts',(-84.1880615558352,4.73441968393585,132.143495193259));
#94822=CARTESIAN_POINT('Ctrl Pts',(-84.1958078891006,4.76994955120377,132.010835770965));
#94823=CARTESIAN_POINT('Ctrl Pts',(-84.2035542223659,4.79986619038137,131.876959152403));
#94824=CARTESIAN_POINT('Ctrl Pts',(-84.2113022903689,4.82978952918292,131.7430525531));
#94825=CARTESIAN_POINT('Ctrl Pts',(-84.2190503583718,4.85409705327559,131.607928596603));
#94826=CARTESIAN_POINT('Ctrl Pts',(-84.2267984263748,4.87271083673212,131.472097215405));
#94827=CARTESIAN_POINT('Ctrl Pts',(-84.2345547291166,4.89134440313919,131.336121470998));
#94828=CARTESIAN_POINT('Ctrl Pts',(-84.2423110318584,4.90427208747126,131.199437187933));
#94829=CARTESIAN_POINT('Ctrl Pts',(-84.2500673346003,4.91146781920559,131.06256000449));
#94830=CARTESIAN_POINT('Ctrl Pts',(-84.2578277771145,4.91866739151862,130.925609765573));
#94831=CARTESIAN_POINT('Ctrl Pts',(-84.2655882196287,4.92012891112413,130.78846681188));
#94832=CARTESIAN_POINT('Ctrl Pts',(-84.2733486621429,4.91587848203368,130.651645810235));
#94833=CARTESIAN_POINT('Ctrl Pts',(-84.2811215624083,4.91162122977712,130.514605171371));
#94834=CARTESIAN_POINT('Ctrl Pts',(-84.2888944626737,4.90163373408856,130.377887907488));
#94835=CARTESIAN_POINT('Ctrl Pts',(-84.2966673629391,4.88599401700529,130.242003499456));
#94836=CARTESIAN_POINT('Ctrl Pts',(-84.3041576987012,4.87092284303194,130.111058831928));
#94837=CARTESIAN_POINT('Ctrl Pts',(-84.3116480344633,4.8506033055318,129.980887823054));
#94838=CARTESIAN_POINT('Ctrl Pts',(-84.3191383702254,4.82514952045834,129.851934679385));
#94839=CARTESIAN_POINT('Ctrl Pts',(-84.3269127043446,4.79873064738741,129.718092238079));
#94840=CARTESIAN_POINT('Ctrl Pts',(-84.3346870384637,4.76669682420443,129.585137863104));
#94841=CARTESIAN_POINT('Ctrl Pts',(-84.3424613725828,4.72911969579625,129.453579374976));
#94842=CARTESIAN_POINT('Ctrl Pts',(-84.3502261255299,4.69158887784058,129.322183020928));
#94843=CARTESIAN_POINT('Ctrl Pts',(-84.357990878477,4.64852845391031,129.192179503152));
#94844=CARTESIAN_POINT('Ctrl Pts',(-84.3657556314241,4.60006130527624,129.064067811685));
#94845=CARTESIAN_POINT('Ctrl Pts',(-84.3735126723091,4.55164229489746,128.936083362557));
#94846=CARTESIAN_POINT('Ctrl Pts',(-84.3812697131942,4.49782738387271,128.80998736377));
#94847=CARTESIAN_POINT('Ctrl Pts',(-84.3890267540792,4.43878951827638,128.686264615271));
#94848=CARTESIAN_POINT('Ctrl Pts',(-84.3967779453193,4.37979617359383,128.562635167058));
#94849=CARTESIAN_POINT('Ctrl Pts',(-84.4045291365595,4.31558788171681,128.441375758293));
#94850=CARTESIAN_POINT('Ctrl Pts',(-84.4122803277997,4.2463859127734,128.322951795485));
#94851=CARTESIAN_POINT('Ctrl Pts',(-84.4200282245768,4.17721335651271,128.20457816602));
#94852=CARTESIAN_POINT('Ctrl Pts',(-84.4277761213537,4.10305154140986,128.089037922431));
#94853=CARTESIAN_POINT('Ctrl Pts',(-84.4355240181308,4.02416784639441,127.976772209303));
#94854=CARTESIAN_POINT('Ctrl Pts',(-84.443270294215,3.94530065214742,127.864529979742));
#94855=CARTESIAN_POINT('Ctrl Pts',(-84.4510165702991,3.86171376723845,127.755561237907));
#94856=CARTESIAN_POINT('Ctrl Pts',(-84.4587628463832,3.77371787269385,127.650278107578));
#94857=CARTESIAN_POINT('Ctrl Pts',(-84.4665091796486,3.68572132858368,127.544994200073));
#94858=CARTESIAN_POINT('Ctrl Pts',(-84.4742555129139,3.59331596062078,127.443396258346));
#94859=CARTESIAN_POINT('Ctrl Pts',(-84.4820018461793,3.49685244407135,127.345862960072));
#94860=CARTESIAN_POINT('Ctrl Pts',(-84.4897499141823,3.4003673251861,127.248307819891));
#94861=CARTESIAN_POINT('Ctrl Pts',(-84.4974979821853,3.29982252419184,127.154819412375));
#94862=CARTESIAN_POINT('Ctrl Pts',(-84.5052460501883,3.19560494086963,127.065738929779));
#94863=CARTESIAN_POINT('Ctrl Pts',(-84.5130023529302,3.0912765938598,126.976563771387));
#94864=CARTESIAN_POINT('Ctrl Pts',(-84.520758655672,2.9832679645739,126.891806150731));
#94865=CARTESIAN_POINT('Ctrl Pts',(-84.5285149584139,2.8719987823477,126.811766716768));
#94866=CARTESIAN_POINT('Ctrl Pts',(-84.5362754009281,2.7606702124084,126.731684563348));
#94867=CARTESIAN_POINT('Ctrl Pts',(-84.5440358434422,2.64607794842242,126.656325829138));
#94868=CARTESIAN_POINT('Ctrl Pts',(-84.5517962859564,2.52866910401943,126.585946742082));
#94869=CARTESIAN_POINT('Ctrl Pts',(-84.5595691862219,2.41107178451633,126.515454676267));
#94870=CARTESIAN_POINT('Ctrl Pts',(-84.5673420864874,2.29064919299887,126.449958418617));
#94871=CARTESIAN_POINT('Ctrl Pts',(-84.5751149867528,2.16787214297028,126.389667713837));
#94872=CARTESIAN_POINT('Ctrl Pts',(-84.5826053225147,2.04955834797027,126.331568728041));
#94873=CARTESIAN_POINT('Ctrl Pts',(-84.5900956582766,1.92905858522301,126.278303520521));
#94874=CARTESIAN_POINT('Ctrl Pts',(-84.5975859940384,1.80680826073937,126.230016186784));
#94875=CARTESIAN_POINT('Ctrl Pts',(-84.6053603281575,1.6799227780427,126.179898024111));
#94876=CARTESIAN_POINT('Ctrl Pts',(-84.6131346622766,1.55074943301358,126.134983899535));
#94877=CARTESIAN_POINT('Ctrl Pts',(-84.6209089963956,1.41975419524518,126.095488025577));
#94878=CARTESIAN_POINT('Ctrl Pts',(-84.6286737493427,1.28892039739995,126.056040826754));
#94879=CARTESIAN_POINT('Ctrl Pts',(-84.6364385022899,1.15626954506074,126.021998704071));
#94880=CARTESIAN_POINT('Ctrl Pts',(-84.644203255237,1.02228787300575,125.993527990338));
#94881=CARTESIAN_POINT('Ctrl Pts',(-84.651960296122,0.88843927343626,125.965085554119));
#94882=CARTESIAN_POINT('Ctrl Pts',(-84.6597173370069,0.753262864522192,
125.942203595472));
#94883=CARTESIAN_POINT('Ctrl Pts',(-84.6674743778919,0.617260003764343,
125.924998656177));
#94884=CARTESIAN_POINT('Ctrl Pts',(-84.675225569132,0.481359703821925,125.90780669126));
#94885=CARTESIAN_POINT('Ctrl Pts',(-84.6829767603722,0.344634578849199,
125.896283273327));
#94886=CARTESIAN_POINT('Ctrl Pts',(-84.6907279516123,0.207595790432129,
125.890493805137));
#94887=CARTESIAN_POINT('Ctrl Pts',(-84.6984758483894,0.0706152471555784,
125.884706797625));
#94888=CARTESIAN_POINT('Ctrl Pts',(-84.7062237451666,-0.0666783046123071,
125.884648909155));
#94889=CARTESIAN_POINT('Ctrl Pts',(-84.7139716419437,-0.203769192594108,
125.890333635686));
#94890=CARTESIAN_POINT('Ctrl Pts',(-84.7217179180278,-0.340831404117481,
125.896017173094));
#94891=CARTESIAN_POINT('Ctrl Pts',(-84.7294641941118,-0.477690645794539,
125.90744092));
#94892=CARTESIAN_POINT('Ctrl Pts',(-84.7372104701959,-0.613832255533716,
125.924566254628));
#94893=CARTESIAN_POINT('Ctrl Pts',(-84.7449568034612,-0.749974870239143,
125.94169171567));
#94894=CARTESIAN_POINT('Ctrl Pts',(-84.7527031367266,-0.885399454527858,
125.964518799622));
#94895=CARTESIAN_POINT('Ctrl Pts',(-84.760449469992,-1.01959786759984,125.992957157983));
#94896=CARTESIAN_POINT('Ctrl Pts',(-84.768197537995,-1.15382633347579,126.021401884917));
#94897=CARTESIAN_POINT('Ctrl Pts',(-84.7759456059979,-1.28682769932916,
126.055460305726));
#94898=CARTESIAN_POINT('Ctrl Pts',(-84.7836936740009,-1.41810578166829,
126.094991333416));
#94899=CARTESIAN_POINT('Ctrl Pts',(-84.7914499767427,-1.54952338791573,
126.134564375152));
#94900=CARTESIAN_POINT('Ctrl Pts',(-84.7992062794846,-1.67921367702035,
126.179621529649));
#94901=CARTESIAN_POINT('Ctrl Pts',(-84.8069625822265,-1.80669683054255,
126.229972174833));
#94902=CARTESIAN_POINT('Ctrl Pts',(-84.8147230247407,-1.93424802566257,
126.280349693673));
#94903=CARTESIAN_POINT('Ctrl Pts',(-84.8224834672548,-2.05958938077981,
126.336026174206));
#94904=CARTESIAN_POINT('Ctrl Pts',(-84.830243909769,-2.18226364822946,126.396763944535));
#94905=CARTESIAN_POINT('Ctrl Pts',(-84.8380168100344,-2.3051348433034,126.457599216524));
#94906=CARTESIAN_POINT('Ctrl Pts',(-84.8457897102998,-2.42533005201508,
126.523511826218));
#94907=CARTESIAN_POINT('Ctrl Pts',(-84.8535626105653,-2.54241832400425,
126.594219037017));
#94908=CARTESIAN_POINT('Ctrl Pts',(-84.8610529463274,-2.65525014238096,
126.662355862604));
#94909=CARTESIAN_POINT('Ctrl Pts',(-84.8685432820896,-2.76519673515625,
126.734944579998));
#94910=CARTESIAN_POINT('Ctrl Pts',(-84.8760336178517,-2.87190152311498,
126.81169675693));
#94911=CARTESIAN_POINT('Ctrl Pts',(-84.8841041004386,-2.98687088637196,
126.89439359818));
#94912=CARTESIAN_POINT('Ctrl Pts',(-84.8921745830254,-3.09847089327534,
126.982208319673));
#94913=CARTESIAN_POINT('Ctrl Pts',(-84.9002450656123,-3.20621148892957,
127.074831029165));
#94914=CARTESIAN_POINT('Ctrl Pts',(-84.9079464759637,-3.30902498610363,
127.163217998096));
#94915=CARTESIAN_POINT('Ctrl Pts',(-84.9156478863152,-3.4083238454004,127.255982692074));
#94916=CARTESIAN_POINT('Ctrl Pts',(-84.9233492966666,-3.50371041895164,
127.352810768204));
#94917=CARTESIAN_POINT('Ctrl Pts',(-84.9310437533059,-3.59901086661893,
127.449551416897));
#94918=CARTESIAN_POINT('Ctrl Pts',(-84.9387382099451,-3.69040577616813,
127.550347870198));
#94919=CARTESIAN_POINT('Ctrl Pts',(-84.9464326665844,-3.77753108436507,
127.654846056692));
#94920=CARTESIAN_POINT('Ctrl Pts',(-84.9541219091619,-3.86459735307908,
127.759273431169));
#94921=CARTESIAN_POINT('Ctrl Pts',(-84.9618111517394,-3.94739952192053,
127.867397244793));
#94922=CARTESIAN_POINT('Ctrl Pts',(-84.9695003943169,-4.0256112273304,127.97882751585));
#94923=CARTESIAN_POINT('Ctrl Pts',(-84.9771861581981,-4.10378754892108,
128.090207374651));
#94924=CARTESIAN_POINT('Ctrl Pts',(-84.9848719220792,-4.1773773117728,128.204890389145));
#94925=CARTESIAN_POINT('Ctrl Pts',(-84.9925576859603,-4.2460955201551,128.322454919072));
#94926=CARTESIAN_POINT('Ctrl Pts',(-85.0002430415961,-4.31481007842572,
128.440013204312));
#94927=CARTESIAN_POINT('Ctrl Pts',(-85.0079283972319,-4.37865338911832,
128.560452361462));
#94928=CARTESIAN_POINT('Ctrl Pts',(-85.0156137528677,-4.43738487790799,
128.683323487336));
#94929=CARTESIAN_POINT('Ctrl Pts',(-85.0232989048597,-4.49611481045222,
128.806191357416));
#94930=CARTESIAN_POINT('Ctrl Pts',(-85.0309840568516,-4.54973302457026,
128.931490706482));
#94931=CARTESIAN_POINT('Ctrl Pts',(-85.0386692088436,-4.59804617841052,
129.05875057987));
#94932=CARTESIAN_POINT('Ctrl Pts',(-85.0463579175028,-4.64638169144558,
129.186069348778));
#94933=CARTESIAN_POINT('Ctrl Pts',(-85.054046626162,-4.68940710720134,129.315350079358));
#94934=CARTESIAN_POINT('Ctrl Pts',(-85.0617353348212,-4.72697827914892,
129.446104599374));
#94935=CARTESIAN_POINT('Ctrl Pts',(-85.0643986231931,-4.73999254068507,
129.491396599392));
#94936=CARTESIAN_POINT('Ctrl Pts',(-85.0670619115651,-4.75235281418266,
129.53686531382));
#94937=CARTESIAN_POINT('Ctrl Pts',(-85.069725199937,-4.76405452823396,129.582490119308));
#94938=CARTESIAN_POINT('Origin',(213.235140564004,0.,130.804360617566));
#94939=CARTESIAN_POINT('',(-87.1653941590426,-4.76405452823403,129.582490119308));
#94940=CARTESIAN_POINT('',(-86.8199013756722,-4.76405452823401,129.582490119308));
#94941=CARTESIAN_POINT('',(213.235140564004,-4.76405452823405,129.582490119308));
#94942=CARTESIAN_POINT('',(-85.4851405639742,-4.91824791732384,130.799834444828));
#94943=CARTESIAN_POINT('Ctrl Pts',(-85.4851405640089,-4.91824791732441,
130.79983444544));
#94944=CARTESIAN_POINT('Ctrl Pts',(-85.4928102058359,-4.91837262725987,
130.93534727246));
#94945=CARTESIAN_POINT('Ctrl Pts',(-85.5004798476629,-4.91289243297851,
131.070998262037));
#94946=CARTESIAN_POINT('Ctrl Pts',(-85.5081494894899,-4.90179993215824,
131.206281614272));
#94947=CARTESIAN_POINT('Ctrl Pts',(-85.5158149080154,-4.89071353944266,
131.341490472497));
#94948=CARTESIAN_POINT('Ctrl Pts',(-85.5234803265409,-4.87402101912933,
131.476331698243));
#94949=CARTESIAN_POINT('Ctrl Pts',(-85.5311457450664,-4.85176704392226,
131.61030082255));
#94950=CARTESIAN_POINT('Ctrl Pts',(-85.5388089982247,-4.82951935513341,
131.744232102565));
#94951=CARTESIAN_POINT('Ctrl Pts',(-85.5464722513831,-4.80171340041526,
131.8772913765));
#94952=CARTESIAN_POINT('Ctrl Pts',(-85.5541355045414,-4.76844551204447,
132.008981081099));
#94953=CARTESIAN_POINT('Ctrl Pts',(-85.5617983391458,-4.73517944070992,
132.140663593028));
#94954=CARTESIAN_POINT('Ctrl Pts',(-85.5694611737501,-4.69645212696236,
132.270976296331));
#94955=CARTESIAN_POINT('Ctrl Pts',(-85.5771240083544,-4.65241052363223,
132.399434089885));
#94956=CARTESIAN_POINT('Ctrl Pts',(-85.5847881706427,-4.60836128953188,
132.527914140392));
#94957=CARTESIAN_POINT('Ctrl Pts',(-85.592452332931,-4.55899606467394,132.654538263487));
#94958=CARTESIAN_POINT('Ctrl Pts',(-85.6001164952193,-4.50451077086627,
132.77883922663));
#94959=CARTESIAN_POINT('Ctrl Pts',(-85.607788497958,-4.44996973851463,132.903267349859));
#94960=CARTESIAN_POINT('Ctrl Pts',(-85.6154605006967,-4.39029833615977,
133.025367198979));
#94961=CARTESIAN_POINT('Ctrl Pts',(-85.6231325034355,-4.32573967813694,
133.144693777501));
#94962=CARTESIAN_POINT('Ctrl Pts',(-85.6308084083052,-4.26114818431489,
133.26408104786));
#94963=CARTESIAN_POINT('Ctrl Pts',(-85.6384843131749,-4.19166468913342,
133.380691894912));
#94964=CARTESIAN_POINT('Ctrl Pts',(-85.6461602180447,-4.1175762274804,133.494109504245));
#94965=CARTESIAN_POINT('Ctrl Pts',(-85.6538484765497,-4.04336852752947,
133.60770964838));
#94966=CARTESIAN_POINT('Ctrl Pts',(-85.6615367350547,-3.96454128652445,
133.718105961257));
#94967=CARTESIAN_POINT('Ctrl Pts',(-85.6692249935597,-3.88142295689908,
133.824913363697));
#94968=CARTESIAN_POINT('Ctrl Pts',(-85.6767458267499,-3.80011467469848,
133.929394847598));
#94969=CARTESIAN_POINT('Ctrl Pts',(-85.68426665994,-3.71470056573458,134.030441917186));
#94970=CARTESIAN_POINT('Ctrl Pts',(-85.6917874931301,-3.62552120709613,
134.12772924584));
#94971=CARTESIAN_POINT('Ctrl Pts',(-85.6995618272492,-3.53333592482057,
134.228295789385));
#94972=CARTESIAN_POINT('Ctrl Pts',(-85.7073361613683,-3.43681710797767,
134.325183093237));
#94973=CARTESIAN_POINT('Ctrl Pts',(-85.7151104954874,-3.33629010306817,
134.417994717841));
#94974=CARTESIAN_POINT('Ctrl Pts',(-85.7228752484345,-3.23588698870785,
134.510691960412));
#94975=CARTESIAN_POINT('Ctrl Pts',(-85.7306400013816,-3.13148579937848,
134.599323255166));
#94976=CARTESIAN_POINT('Ctrl Pts',(-85.7384047543287,-3.02345104694852,
134.683526356382));
#94977=CARTESIAN_POINT('Ctrl Pts',(-85.7461617952137,-2.91552359615741,
134.767645825892));
#94978=CARTESIAN_POINT('Ctrl Pts',(-85.7539188360988,-2.80397007052181,
134.847345615583));
#94979=CARTESIAN_POINT('Ctrl Pts',(-85.7616758769838,-2.68919035872191,
134.922301641556));
#94980=CARTESIAN_POINT('Ctrl Pts',(-85.7694270682239,-2.574497203196,134.997201142606));
#94981=CARTESIAN_POINT('Ctrl Pts',(-85.777178259464,-2.45658303005188,135.067363787449));
#94982=CARTESIAN_POINT('Ctrl Pts',(-85.7849294507041,-2.33587891141086,
135.132507192455));
#94983=CARTESIAN_POINT('Ctrl Pts',(-85.7926773474812,-2.21522609523998,
135.197622909777));
#94984=CARTESIAN_POINT('Ctrl Pts',(-85.8004252442582,-2.09178603537643,
135.257723444957));
#94985=CARTESIAN_POINT('Ctrl Pts',(-85.8081731410353,-1.96601656294511,
135.312571120274));
#94986=CARTESIAN_POINT('Ctrl Pts',(-85.8159194171194,-1.84027339877615,
135.367407322639));
#94987=CARTESIAN_POINT('Ctrl Pts',(-85.8236656932035,-1.71220214937502,
135.4169926945));
#94988=CARTESIAN_POINT('Ctrl Pts',(-85.8314119692876,-1.58228253231092,
135.461136868412));
#94989=CARTESIAN_POINT('Ctrl Pts',(-85.8391583025529,-1.4523619562099,135.505281368186));
#94990=CARTESIAN_POINT('Ctrl Pts',(-85.8469046358182,-1.32059335539978,
135.543984464083));
#94991=CARTESIAN_POINT('Ctrl Pts',(-85.8546509690836,-1.18747320684742,
135.577105157715));
#94992=CARTESIAN_POINT('Ctrl Pts',(-85.8623990370865,-1.05432324696095,
135.610233268496));
#94993=CARTESIAN_POINT('Ctrl Pts',(-85.8701471050894,-0.919821516380451,
135.637776395001));
#94994=CARTESIAN_POINT('Ctrl Pts',(-85.8778951730924,-0.784475930743299,
135.659644396768));
#94995=CARTESIAN_POINT('Ctrl Pts',(-85.8856514758342,-0.648986498206545,
135.681535640108));
#94996=CARTESIAN_POINT('Ctrl Pts',(-85.8934077785761,-0.51265180561555,
135.6977396475));
#94997=CARTESIAN_POINT('Ctrl Pts',(-85.901164081318,-0.375986717140373,
135.708217982033));
#94998=CARTESIAN_POINT('Ctrl Pts',(-85.9089245238322,-0.23924868639257,
135.718701909168));
#94999=CARTESIAN_POINT('Ctrl Pts',(-85.9166849663464,-0.10218029892303,
135.723454060636));
#95000=CARTESIAN_POINT('Ctrl Pts',(-85.9244454088605,0.0347033002329159,
135.722488182346));
#95001=CARTESIAN_POINT('Ctrl Pts',(-85.9322183091259,0.17180663709381,135.721520753544));
#95002=CARTESIAN_POINT('Ctrl Pts',(-85.9399912093913,0.308724202140494,
135.714816971369));
#95003=CARTESIAN_POINT('Ctrl Pts',(-85.9477641096567,0.444944788905772,
135.702442609257));
#95004=CARTESIAN_POINT('Ctrl Pts',(-85.9552544454188,0.576213414224647,
135.690518086376));
#95005=CARTESIAN_POINT('Ctrl Pts',(-85.962744781181,0.706834549936867,135.673328145693));
#95006=CARTESIAN_POINT('Ctrl Pts',(-85.9702351169431,0.836361378945249,
135.650976210566));
#95007=CARTESIAN_POINT('Ctrl Pts',(-85.9780094510622,0.970799257042992,
135.627776795025));
#95008=CARTESIAN_POINT('Ctrl Pts',(-85.9857837851813,1.10448406787116,135.598942735196));
#95009=CARTESIAN_POINT('Ctrl Pts',(-85.9935581193003,1.23690641787442,135.564533469041));
#95010=CARTESIAN_POINT('Ctrl Pts',(-86.0013228722474,1.36916556916623,135.530166609232));
#95011=CARTESIAN_POINT('Ctrl Pts',(-86.0090876251945,1.50016498058434,135.490238311607));
#95012=CARTESIAN_POINT('Ctrl Pts',(-86.0168523781416,1.62940285697743,135.444859447668));
#95013=CARTESIAN_POINT('Ctrl Pts',(-86.0246094190266,1.75851237248976,135.399525654655));
#95014=CARTESIAN_POINT('Ctrl Pts',(-86.0323664599116,1.88586346822408,135.348752197281));
#95015=CARTESIAN_POINT('Ctrl Pts',(-86.0401235007966,2.01096733361788,135.292700337955));
#95016=CARTESIAN_POINT('Ctrl Pts',(-86.0478746920367,2.13597685721379,135.236690747772));
#95017=CARTESIAN_POINT('Ctrl Pts',(-86.0556258832769,2.25874216822816,135.175410837758));
#95018=CARTESIAN_POINT('Ctrl Pts',(-86.063377074517,2.3787926843047,135.109070645849));
#95019=CARTESIAN_POINT('Ctrl Pts',(-86.0711249712941,2.49879217570929,135.042758650291));
#95020=CARTESIAN_POINT('Ctrl Pts',(-86.0788728680711,2.61607882563935,134.971390839226));
#95021=CARTESIAN_POINT('Ctrl Pts',(-86.0866207648482,2.73020520018958,134.89522392833));
#95022=CARTESIAN_POINT('Ctrl Pts',(-86.0943670409323,2.84430770196254,134.819072949911));
#95023=CARTESIAN_POINT('Ctrl Pts',(-86.1021133170164,2.95525091825526,134.738125085304));
#95024=CARTESIAN_POINT('Ctrl Pts',(-86.1098595931005,3.06261538848128,134.652681036234));
#95025=CARTESIAN_POINT('Ctrl Pts',(-86.1176059263659,3.16998065124757,134.567236356435));
#95026=CARTESIAN_POINT('Ctrl Pts',(-86.1253522596313,3.2737668093194,134.477295669401));
#95027=CARTESIAN_POINT('Ctrl Pts',(-86.1330985928966,3.37358687883183,134.383200462191));
#95028=CARTESIAN_POINT('Ctrl Pts',(-86.1408466608996,3.47342930235659,134.289084183012));
#95029=CARTESIAN_POINT('Ctrl Pts',(-86.1485947289026,3.56930358551315,134.190811800441));
#95030=CARTESIAN_POINT('Ctrl Pts',(-86.1563427969056,3.66085934977078,134.088761915169));
#95031=CARTESIAN_POINT('Ctrl Pts',(-86.1640990996475,3.75251242058432,133.986603570064));
#95032=CARTESIAN_POINT('Ctrl Pts',(-86.1718554023893,3.83983754243001,133.880659993789));
#95033=CARTESIAN_POINT('Ctrl Pts',(-86.1796117051311,3.92252408058497,133.77134358006));
#95034=CARTESIAN_POINT('Ctrl Pts',(-86.1873721476453,4.00525475103477,133.661968820871));
#95035=CARTESIAN_POINT('Ctrl Pts',(-86.1951325901594,4.08334168216125,133.549217958461));
#95036=CARTESIAN_POINT('Ctrl Pts',(-86.2028930326735,4.15651799031273,133.433531828938));
#95037=CARTESIAN_POINT('Ctrl Pts',(-86.210665932939,4.22981176757055,133.31765998977));
#95038=CARTESIAN_POINT('Ctrl Pts',(-86.2184388332043,4.29817897407176,133.198843806574));
#95039=CARTESIAN_POINT('Ctrl Pts',(-86.2262117334697,4.36139862728571,133.077548923978));
#95040=CARTESIAN_POINT('Ctrl Pts',(-86.2337020692318,4.42232008686481,132.960663415888));
#95041=CARTESIAN_POINT('Ctrl Pts',(-86.2411924049939,4.47846161737434,132.841476572204));
#95042=CARTESIAN_POINT('Ctrl Pts',(-86.248682740756,4.52966871625975,132.720420215657));
#95043=CARTESIAN_POINT('Ctrl Pts',(-86.2564570748751,4.58281734786325,132.594773970558));
#95044=CARTESIAN_POINT('Ctrl Pts',(-86.2642314089941,4.63081834239162,132.466715639409));
#95045=CARTESIAN_POINT('Ctrl Pts',(-86.2720057431132,4.67344636702702,132.336705917106));
#95046=CARTESIAN_POINT('Ctrl Pts',(-86.2797704960603,4.71602185643184,132.206856420166));
#95047=CARTESIAN_POINT('Ctrl Pts',(-86.2875352490074,4.75323743052242,132.075060685075));
#95048=CARTESIAN_POINT('Ctrl Pts',(-86.2953000019545,4.78491513609461,131.941800815059));
#95049=CARTESIAN_POINT('Ctrl Pts',(-86.3030570428395,4.81656137892306,131.808673300624));
#95050=CARTESIAN_POINT('Ctrl Pts',(-86.3108140837245,4.84268060922345,131.674084923091));
#95051=CARTESIAN_POINT('Ctrl Pts',(-86.3185711246095,4.86314428757814,131.538534098901));
#95052=CARTESIAN_POINT('Ctrl Pts',(-86.3263223158496,4.88359253411395,131.403085494641));
#95053=CARTESIAN_POINT('Ctrl Pts',(-86.3340735070898,4.89839365959494,131.266676273383));
#95054=CARTESIAN_POINT('Ctrl Pts',(-86.34182469833,4.90747001362606,131.129815880023));
#95055=CARTESIAN_POINT('Ctrl Pts',(-86.3495725951071,4.91654250996454,130.993013655983));
#95056=CARTESIAN_POINT('Ctrl Pts',(-86.3573204918842,4.91989504844671,130.85576103053));
#95057=CARTESIAN_POINT('Ctrl Pts',(-86.3650683886613,4.9175017622875,130.718573203574));
#95058=CARTESIAN_POINT('Ctrl Pts',(-86.3728146647454,4.91510897675215,130.581414073355));
#95059=CARTESIAN_POINT('Ctrl Pts',(-86.3805609408294,4.90697276404083,130.444320105332));
#95060=CARTESIAN_POINT('Ctrl Pts',(-86.3883072169135,4.89311938433697,130.307806740201));
#95061=CARTESIAN_POINT('Ctrl Pts',(-86.3960535501788,4.87926590237063,130.171292367361));
#95062=CARTESIAN_POINT('Ctrl Pts',(-86.4037998834442,4.85969520867153,130.035358994933));
#95063=CARTESIAN_POINT('Ctrl Pts',(-86.4115462167096,4.8344854317433,129.900516785501));
#95064=CARTESIAN_POINT('Ctrl Pts',(-86.4192942847126,4.80927000926015,129.76564437909));
#95065=CARTESIAN_POINT('Ctrl Pts',(-86.4270423527155,4.77841306249044,129.631864006154));
#95066=CARTESIAN_POINT('Ctrl Pts',(-86.4347904207185,4.74204373076291,129.499675092992));
#95067=CARTESIAN_POINT('Ctrl Pts',(-86.4425467234604,4.70563574527696,129.367345687882));
#95068=CARTESIAN_POINT('Ctrl Pts',(-86.4503030262024,4.66370377547049,129.236611498904));
#95069=CARTESIAN_POINT('Ctrl Pts',(-86.4580593289442,4.61642687420275,129.107956780728));
#95070=CARTESIAN_POINT('Ctrl Pts',(-86.4658197714584,4.56912473982932,128.979233395655));
#95071=CARTESIAN_POINT('Ctrl Pts',(-86.4735802139725,4.51647213966634,128.852592053736));
#95072=CARTESIAN_POINT('Ctrl Pts',(-86.4813406564867,4.45869570448371,128.728495574429));
#95073=CARTESIAN_POINT('Ctrl Pts',(-86.4891135567521,4.40082652143816,128.604199884437));
#95074=CARTESIAN_POINT('Ctrl Pts',(-86.4968864570175,4.3378172465426,128.482457568084));
#95075=CARTESIAN_POINT('Ctrl Pts',(-86.504659357283,4.26994019335295,128.363706236526));
#95076=CARTESIAN_POINT('Ctrl Pts',(-86.5121496930449,4.20453064201928,128.249271814988));
#95077=CARTESIAN_POINT('Ctrl Pts',(-86.5196400288069,4.13460124345565,128.137614955049));
#95078=CARTESIAN_POINT('Ctrl Pts',(-86.5271303645689,4.06043178994989,128.029099054818));
#95079=CARTESIAN_POINT('Ctrl Pts',(-86.5349046986879,3.9834501790708,127.916468741247));
#95080=CARTESIAN_POINT('Ctrl Pts',(-86.5426790328071,3.90165678830704,127.806865489107));
#95081=CARTESIAN_POINT('Ctrl Pts',(-86.5504533669261,3.81531741542974,127.700727894124));
#95082=CARTESIAN_POINT('Ctrl Pts',(-86.5582181198732,3.72908444811291,127.594721104241));
#95083=CARTESIAN_POINT('Ctrl Pts',(-86.5659828728202,3.63831689036867,127.492171773653));
#95084=CARTESIAN_POINT('Ctrl Pts',(-86.5737476257673,3.54332416124115,127.393490207998));
#95085=CARTESIAN_POINT('Ctrl Pts',(-86.5815046666522,3.44842578023163,127.294906654267));
#95086=CARTESIAN_POINT('Ctrl Pts',(-86.5892617075373,3.34931084844771,127.20018350052));
#95087=CARTESIAN_POINT('Ctrl Pts',(-86.5970187484222,3.24632921906197,127.109698296871));
#95088=CARTESIAN_POINT('Ctrl Pts',(-86.6047699396623,3.14342524892417,127.019281328818));
#95089=CARTESIAN_POINT('Ctrl Pts',(-86.6125211309025,3.03666067763057,126.933096206691));
#95090=CARTESIAN_POINT('Ctrl Pts',(-86.6202723221426,2.92642214366695,126.851483627378));
#95091=CARTESIAN_POINT('Ctrl Pts',(-86.6280202189197,2.81623046402053,126.769905735588));
#95092=CARTESIAN_POINT('Ctrl Pts',(-86.6357681156966,2.70256807197049,126.692896753375));
#95093=CARTESIAN_POINT('Ctrl Pts',(-86.6435160124737,2.58585443816379,126.620756921334));
#95094=CARTESIAN_POINT('Ctrl Pts',(-86.6512622885578,2.46916521833323,126.54863217939));
#95095=CARTESIAN_POINT('Ctrl Pts',(-86.6590085646419,2.34942635862366,126.48137476715));
#95096=CARTESIAN_POINT('Ctrl Pts',(-86.666754840726,2.22708570816272,126.419241199466));
#95097=CARTESIAN_POINT('Ctrl Pts',(-86.6745011739913,2.10474415461105,126.357107173126));
#95098=CARTESIAN_POINT('Ctrl Pts',(-86.6822475072567,1.97980112056938,126.300097243851));
#95099=CARTESIAN_POINT('Ctrl Pts',(-86.6899938405221,1.85272805063187,126.248421435257));
#95100=CARTESIAN_POINT('Ctrl Pts',(-86.697741908525,1.72562652356157,126.196734054223));
#95101=CARTESIAN_POINT('Ctrl Pts',(-86.705489976528,1.596394373502,126.150383318115));
#95102=CARTESIAN_POINT('Ctrl Pts',(-86.7132380445309,1.46552158490703,126.109530530473));
#95103=CARTESIAN_POINT('Ctrl Pts',(-86.7209943472728,1.33450970315441,126.068634324002));
#95104=CARTESIAN_POINT('Ctrl Pts',(-86.7287506500146,1.2018540734575,126.033247855273));
#95105=CARTESIAN_POINT('Ctrl Pts',(-86.7365069527565,1.06805889542725,126.00348223352));
#95106=CARTESIAN_POINT('Ctrl Pts',(-86.7442673952706,0.934192306881998,
125.973700724959));
#95107=CARTESIAN_POINT('Ctrl Pts',(-86.7520278377849,0.799185342756793,
125.949546109981));
#95108=CARTESIAN_POINT('Ctrl Pts',(-86.759788280299,0.663549885637091,125.931077882923));
#95109=CARTESIAN_POINT('Ctrl Pts',(-86.7675611805645,0.527696694440839,
125.912580009028));
#95110=CARTESIAN_POINT('Ctrl Pts',(-86.7753340808298,0.391213383603855,
125.899786800802));
#95111=CARTESIAN_POINT('Ctrl Pts',(-86.7831069810952,0.254615319914042,
125.892705692659));
#95112=CARTESIAN_POINT('Ctrl Pts',(-86.7905973168574,0.122982939906159,
125.885882000633));
#95113=CARTESIAN_POINT('Ctrl Pts',(-86.7980876526196,-0.0087556866946793,
125.88436232398));
#95114=CARTESIAN_POINT('Ctrl Pts',(-86.8055779883818,-0.140143588202138,
125.88810769108));
#95115=CARTESIAN_POINT('Ctrl Pts',(-86.8133523225008,-0.276513101926866,
125.891995064911));
#95116=CARTESIAN_POINT('Ctrl Pts',(-86.8211266566199,-0.41293674770034,
125.90156692608));
#95117=CARTESIAN_POINT('Ctrl Pts',(-86.828900990739,-0.54890185232917,125.916836723097));
#95118=CARTESIAN_POINT('Ctrl Pts',(-86.8366657436861,-0.684699392118095,
125.932087701453));
#95119=CARTESIAN_POINT('Ctrl Pts',(-86.8444304966332,-0.820039130371874,
125.953022600364));
#95120=CARTESIAN_POINT('Ctrl Pts',(-86.8521952495803,-0.954408616783686,
125.979602877046));
#95121=CARTESIAN_POINT('Ctrl Pts',(-86.8599522904653,-1.08864464552732,
126.006156753822));
#95122=CARTESIAN_POINT('Ctrl Pts',(-86.8677093313503,-1.22191195911997,
126.038344774671));
#95123=CARTESIAN_POINT('Ctrl Pts',(-86.8754663722353,-1.35370380977322,
126.076076673268));
#95124=CARTESIAN_POINT('Ctrl Pts',(-86.8832175634754,-1.48539627516723,
126.113780117947));
#95125=CARTESIAN_POINT('Ctrl Pts',(-86.8909687547155,-1.61561511795681,
126.157019011809));
#95126=CARTESIAN_POINT('Ctrl Pts',(-86.8987199459557,-1.74386471265541,
126.205652219934));
#95127=CARTESIAN_POINT('Ctrl Pts',(-86.9064678427328,-1.87205979785491,
126.254264757647));
#95128=CARTESIAN_POINT('Ctrl Pts',(-86.9142157395099,-1.99828693486013,
126.30826691123));
#95129=CARTESIAN_POINT('Ctrl Pts',(-86.921963636287,-2.12206678862434,126.367468055522));
#95130=CARTESIAN_POINT('Ctrl Pts',(-86.9297099123711,-2.24582075031153,
126.426656816211));
#95131=CARTESIAN_POINT('Ctrl Pts',(-86.9374561884552,-2.36712809451514,
126.491042235897));
#95132=CARTESIAN_POINT('Ctrl Pts',(-86.9452024645393,-2.48553093463297,
126.560386178967));
#95133=CARTESIAN_POINT('Ctrl Pts',(-86.9529487978047,-2.60393464877382,
126.629730633918));
#95134=CARTESIAN_POINT('Ctrl Pts',(-86.96069513107,-2.71943347868095,126.704033487711));
#95135=CARTESIAN_POINT('Ctrl Pts',(-86.9684414643354,-2.83159589822037,
126.783011623549));
#95136=CARTESIAN_POINT('Ctrl Pts',(-86.9761895323384,-2.94378343575612,
126.862007445993));
#95137=CARTESIAN_POINT('Ctrl Pts',(-86.9839376003414,-3.05263275654347,
126.945680408838));
#95138=CARTESIAN_POINT('Ctrl Pts',(-86.9916856683444,-3.15774330277944,
127.033705462788));
#95139=CARTESIAN_POINT('Ctrl Pts',(-86.9994419710863,-3.26296556175435,
127.121824070813));
#95140=CARTESIAN_POINT('Ctrl Pts',(-87.0071982738281,-3.36444080823806,
127.214303758369));
#95141=CARTESIAN_POINT('Ctrl Pts',(-87.0149545765699,-3.46180303067885,
127.3107803853));
#95142=CARTESIAN_POINT('Ctrl Pts',(-87.0227150190841,-3.55921721826955,
127.407308504711));
#95143=CARTESIAN_POINT('Ctrl Pts',(-87.0304754615983,-3.65251374178303,
127.507837527821));
#95144=CARTESIAN_POINT('Ctrl Pts',(-87.0382359041124,-3.74136586190748,
127.611968951455));
#95145=CARTESIAN_POINT('Ctrl Pts',(-87.0460088043779,-3.83036061534283,
127.716267536095));
#95146=CARTESIAN_POINT('Ctrl Pts',(-87.0537817046434,-3.91489646704285,
127.824179769374));
#95147=CARTESIAN_POINT('Ctrl Pts',(-87.0615546049088,-3.99468859388868,
127.935276077097));
#95148=CARTESIAN_POINT('Ctrl Pts',(-87.0690449406707,-4.07158007593813,
128.042333754199));
#95149=CARTESIAN_POINT('Ctrl Pts',(-87.0765352764325,-4.14406656851509,
128.152347769435));
#95150=CARTESIAN_POINT('Ctrl Pts',(-87.0840256121944,-4.21193385519023,
128.264912594471));
#95151=CARTESIAN_POINT('Ctrl Pts',(-87.092059552798,-4.28472655332906,128.385646717364));
#95152=CARTESIAN_POINT('Ctrl Pts',(-87.1000934934016,-4.35242294254361,
128.50967647454));
#95153=CARTESIAN_POINT('Ctrl Pts',(-87.1081274340052,-4.41472236966481,
128.636548480576));
#95154=CARTESIAN_POINT('Ctrl Pts',(-87.1161505265311,-4.47693767505077,
128.763249173748));
#95155=CARTESIAN_POINT('Ctrl Pts',(-87.124173619057,-4.53377037157371,128.892784159149));
#95156=CARTESIAN_POINT('Ctrl Pts',(-87.1321967115828,-4.58496378813763,
129.024672407804));
#95157=CARTESIAN_POINT('Ctrl Pts',(-87.1402069690404,-4.63607530722921,
129.156349666161));
#95158=CARTESIAN_POINT('Ctrl Pts',(-87.148217226498,-4.68156539790506,129.290372355991));
#95159=CARTESIAN_POINT('Ctrl Pts',(-87.1562274839556,-4.72122418707915,
129.426236806786));
#95160=CARTESIAN_POINT('Ctrl Pts',(-87.159283042318,-4.73635225824825,129.478063075913));
#95161=CARTESIAN_POINT('Ctrl Pts',(-87.1623386006803,-4.7506323121341,129.530157102445));
#95162=CARTESIAN_POINT('Ctrl Pts',(-87.1653941590427,-4.76405452823403,
129.582490119308));
#95163=CARTESIAN_POINT('Ctrl Pts',(-85.4152252782566,-4.76405452823408,
129.582490119308));
#95164=CARTESIAN_POINT('Ctrl Pts',(-85.4252802492457,-4.80789294130721,
129.75341542654));
#95165=CARTESIAN_POINT('Ctrl Pts',(-85.4353352202348,-4.84255315743214,
129.926797078868));
#95166=CARTESIAN_POINT('Ctrl Pts',(-85.4453901912239,-4.86780846451807,
130.101776946203));
#95167=CARTESIAN_POINT('Ctrl Pts',(-85.4552467903679,-4.89256551637552,
130.273304682329));
#95168=CARTESIAN_POINT('Ctrl Pts',(-85.4651033895119,-4.90828512320806,
130.446368405372));
#95169=CARTESIAN_POINT('Ctrl Pts',(-85.4749599886558,-4.91479857163483,
130.620137755911));
#95170=CARTESIAN_POINT('Ctrl Pts',(-85.4783535137619,-4.91704108453822,
130.679964745436));
#95171=CARTESIAN_POINT('Ctrl Pts',(-85.481747038868,-4.9181927379082,130.739875167581));
#95172=CARTESIAN_POINT('Ctrl Pts',(-85.4851405639742,-4.91824791732385,
130.799834444828));
#95173=CARTESIAN_POINT('',(-85.1398594359628,-4.91824974829331,130.805934120905));
#95174=CARTESIAN_POINT('Ctrl Pts',(-85.069725199937,-4.76405452823396,129.582490119308));
#95175=CARTESIAN_POINT('Ctrl Pts',(-85.0774224301562,-4.79787391781389,
129.714351405999));
#95176=CARTESIAN_POINT('Ctrl Pts',(-85.0851196603755,-4.82618868007886,
129.847516930377));
#95177=CARTESIAN_POINT('Ctrl Pts',(-85.0928168905947,-4.84892324497919,
129.981483696757));
#95178=CARTESIAN_POINT('Ctrl Pts',(-85.1006573148227,-4.87208074818226,
130.117942689271));
#95179=CARTESIAN_POINT('Ctrl Pts',(-85.1084977390507,-4.88944832579167,
130.255232597457));
#95180=CARTESIAN_POINT('Ctrl Pts',(-85.1163381632788,-4.90100157360506,
130.392818835944));
#95181=CARTESIAN_POINT('Ctrl Pts',(-85.1241785875068,-4.91255482141848,
130.530405074431));
#95182=CARTESIAN_POINT('Ctrl Pts',(-85.1320190117348,-4.91829378588438,
130.668287211764));
#95183=CARTESIAN_POINT('Ctrl Pts',(-85.1398594359628,-4.91824974829331,
130.805934120905));
#95184=CARTESIAN_POINT('Ctrl Pts',(-85.1398594359914,-4.91824974829315,
130.805934121408));
#95185=CARTESIAN_POINT('Ctrl Pts',(-85.1447333712156,-4.91822237267818,
130.891501190161));
#95186=CARTESIAN_POINT('Ctrl Pts',(-85.1496073064404,-4.91596211462244,
130.977029819251));
#95187=CARTESIAN_POINT('Ctrl Pts',(-85.1544812416651,-4.91147410740755,
131.062440362539));
#95188=CARTESIAN_POINT('Ctrl Pts',(-85.1622555757842,-4.90431536072584,
131.198677318959));
#95189=CARTESIAN_POINT('Ctrl Pts',(-85.1700299099032,-4.89147246467867,
131.334831979816));
#95190=CARTESIAN_POINT('Ctrl Pts',(-85.1778042440223,-4.87294427737159,
131.470391496829));
#95191=CARTESIAN_POINT('Ctrl Pts',(-85.1855689969693,-4.85443892439945,
131.605783948852));
#95192=CARTESIAN_POINT('Ctrl Pts',(-85.1933337499163,-4.830262273676,131.740582332754));
#95193=CARTESIAN_POINT('Ctrl Pts',(-85.2010985028634,-4.80046515428053,
131.874275270722));
#95194=CARTESIAN_POINT('Ctrl Pts',(-85.2088555437484,-4.77069762980412,
132.00783542298));
#95195=CARTESIAN_POINT('Ctrl Pts',(-85.2166125846333,-4.73532083024184,
132.14029193513));
#95196=CARTESIAN_POINT('Ctrl Pts',(-85.2243696255183,-4.69443715647294,
132.271140371458));
#95197=CARTESIAN_POINT('Ctrl Pts',(-85.2321208167584,-4.65358431340052,
132.401890133961));
#95198=CARTESIAN_POINT('Ctrl Pts',(-85.2398720079985,-4.60723297809819,
132.53103386271));
#95199=CARTESIAN_POINT('Ctrl Pts',(-85.2476231992386,-4.55553613848605,
132.658079461794));
#95200=CARTESIAN_POINT('Ctrl Pts',(-85.2553710960156,-4.50386127140973,
132.78507106311));
#95201=CARTESIAN_POINT('Ctrl Pts',(-85.2631189927927,-4.44684556587112,
132.909965947032));
#95202=CARTESIAN_POINT('Ctrl Pts',(-85.2708668895697,-4.3846910948542,133.032289491028));
#95203=CARTESIAN_POINT('Ctrl Pts',(-85.2786131656538,-4.32254962521273,
133.154587447576));
#95204=CARTESIAN_POINT('Ctrl Pts',(-85.2863594417378,-4.25527170515766,
133.274314785718));
#95205=CARTESIAN_POINT('Ctrl Pts',(-85.2941057178219,-4.18310638973966,
133.391019465311));
#95206=CARTESIAN_POINT('Ctrl Pts',(-85.3018520510872,-4.1109405416136,133.507725006392));
#95207=CARTESIAN_POINT('Ctrl Pts',(-85.3095983843526,-4.03388743175491,
133.621407511873));
#95208=CARTESIAN_POINT('Ctrl Pts',(-85.3173447176179,-3.95224045086554,
133.731642373913));
#95209=CARTESIAN_POINT('Ctrl Pts',(-85.3250927856209,-3.8705751857008,133.841901922286));
#95210=CARTESIAN_POINT('Ctrl Pts',(-85.3328408536239,-3.78431423503414,
133.948711976761));
#95211=CARTESIAN_POINT('Ctrl Pts',(-85.3405889216268,-3.69379216683655,
134.051679895173));
#95212=CARTESIAN_POINT('Ctrl Pts',(-85.3483452243687,-3.60317389070803,
134.154757249113));
#95213=CARTESIAN_POINT('Ctrl Pts',(-85.3561015271104,-3.5082857088998,134.253984015726));
#95214=CARTESIAN_POINT('Ctrl Pts',(-85.3638578298523,-3.40950043997338,
134.349003027221));
#95215=CARTESIAN_POINT('Ctrl Pts',(-85.3716182723664,-3.31066244637429,
134.444072753223));
#95216=CARTESIAN_POINT('Ctrl Pts',(-85.3793787148806,-3.20792351382213,
134.534929990277));
#95217=CARTESIAN_POINT('Ctrl Pts',(-85.3871391573947,-3.10168987157424,
134.62125765614));
#95218=CARTESIAN_POINT('Ctrl Pts',(-85.3949120576601,-2.99528569365313,
134.707723902836));
#95219=CARTESIAN_POINT('Ctrl Pts',(-85.4026849579255,-2.88537590908218,
134.789645814247));
#95220=CARTESIAN_POINT('Ctrl Pts',(-85.4104578581909,-2.77239680331742,
134.866748957872));
#95221=CARTESIAN_POINT('Ctrl Pts',(-85.417948193953,-2.6635247726235,134.941049208016));
#95222=CARTESIAN_POINT('Ctrl Pts',(-85.4254385297151,-2.55180296274842,
135.010874793252));
#95223=CARTESIAN_POINT('Ctrl Pts',(-85.4329288654771,-2.43764192584907,
135.076021290401));
#95224=CARTESIAN_POINT('Ctrl Pts',(-85.4407031995962,-2.31915243853834,
135.143637836789));
#95225=CARTESIAN_POINT('Ctrl Pts',(-85.4484775337152,-2.1976597672397,135.206427664572));
#95226=CARTESIAN_POINT('Ctrl Pts',(-85.4562518678343,-2.07359476851667,
135.264112606016));
#95227=CARTESIAN_POINT('Ctrl Pts',(-85.4640166207813,-1.94968266881657,
135.321726455925));
#95228=CARTESIAN_POINT('Ctrl Pts',(-85.4717813737284,-1.82320490048748,
135.374247774086));
#95229=CARTESIAN_POINT('Ctrl Pts',(-85.4795461266754,-1.69461917452559,
135.421442912244));
#95230=CARTESIAN_POINT('Ctrl Pts',(-85.4873031675604,-1.56616116171946,
135.468591175526));
#95231=CARTESIAN_POINT('Ctrl Pts',(-85.4950602084454,-1.43559972239451,
135.510423652379));
#95232=CARTESIAN_POINT('Ctrl Pts',(-85.5028172493303,-1.3034146027804,135.546753835737));
#95233=CARTESIAN_POINT('Ctrl Pts',(-85.5105684405704,-1.17132916499342,
135.583056622222));
#95234=CARTESIAN_POINT('Ctrl Pts',(-85.5183196318105,-1.03762285953132,
135.613865270995));
#95235=CARTESIAN_POINT('Ctrl Pts',(-85.5260708230506,-0.90279239432758,
135.639042505265));
#95236=CARTESIAN_POINT('Ctrl Pts',(-85.5338187198277,-0.768019235668091,
135.664209038539));
#95237=CARTESIAN_POINT('Ctrl Pts',(-85.5415666166046,-0.632123251088051,
135.683748846188));
#95238=CARTESIAN_POINT('Ctrl Pts',(-85.5493145133817,-0.495612979349267,
135.697575392865));
#95239=CARTESIAN_POINT('Ctrl Pts',(-85.5570607894658,-0.359131262616511,
135.711399047325));
#95240=CARTESIAN_POINT('Ctrl Pts',(-85.5648070655498,-0.222035903038514,
135.719511778543));
#95241=CARTESIAN_POINT('Ctrl Pts',(-85.5725533416339,-0.0848418351293324,
135.721878784844));
#95242=CARTESIAN_POINT('Ctrl Pts',(-85.5802996748992,0.0523532455151055,
135.724245808619));
#95243=CARTESIAN_POINT('Ctrl Pts',(-85.5880460081645,0.18964664503765,135.7208670161));
#95244=CARTESIAN_POINT('Ctrl Pts',(-85.5957923414298,0.326522543993857,
135.711759734284));
#95245=CARTESIAN_POINT('Ctrl Pts',(-85.6035404094328,0.46342909535879,135.702650412955));
#95246=CARTESIAN_POINT('Ctrl Pts',(-85.6112884774358,0.599917570082481,
135.687810075547));
#95247=CARTESIAN_POINT('Ctrl Pts',(-85.6190365454387,0.735476785030354,
135.667307970888));
#95248=CARTESIAN_POINT('Ctrl Pts',(-85.6267928481806,0.871180073925235,
135.646784076348));
#95249=CARTESIAN_POINT('Ctrl Pts',(-85.6345491509224,1.00595174296484,135.620586452722));
#95250=CARTESIAN_POINT('Ctrl Pts',(-85.6423054536642,1.13928977923307,135.588835704912));
#95251=CARTESIAN_POINT('Ctrl Pts',(-85.6500658961784,1.272698982026,135.557068010772));
#95252=CARTESIAN_POINT('Ctrl Pts',(-85.6578263386926,1.40467265135236,135.519741393037));
#95253=CARTESIAN_POINT('Ctrl Pts',(-85.6655867812067,1.53472444010577,135.477026233191));
#95254=CARTESIAN_POINT('Ctrl Pts',(-85.6733596814721,1.66498499953558,135.434242503178));
#95255=CARTESIAN_POINT('Ctrl Pts',(-85.6811325817374,1.79331714701117,135.386053082784));
#95256=CARTESIAN_POINT('Ctrl Pts',(-85.6889054820028,1.91925417175156,135.332676693848));
#95257=CARTESIAN_POINT('Ctrl Pts',(-85.6963958177651,2.04061306843187,135.281240671095));
#95258=CARTESIAN_POINT('Ctrl Pts',(-85.7038861535275,2.15974767805275,135.224988382724));
#95259=CARTESIAN_POINT('Ctrl Pts',(-85.7113764892898,2.27626410013549,135.16415474217));
#95260=CARTESIAN_POINT('Ctrl Pts',(-85.7191508234089,2.39719827777097,135.101014575648));
#95261=CARTESIAN_POINT('Ctrl Pts',(-85.726925157528,2.51569489464556,135.032738786076));
#95262=CARTESIAN_POINT('Ctrl Pts',(-85.7346994916471,2.63128703187111,134.95953950883));
#95263=CARTESIAN_POINT('Ctrl Pts',(-85.7424642445942,2.74673671211829,134.886430443151));
#95264=CARTESIAN_POINT('Ctrl Pts',(-85.7502289975413,2.85928870774192,134.80841016999));
#95265=CARTESIAN_POINT('Ctrl Pts',(-85.7579937504884,2.96849903987399,134.725737481981));
#95266=CARTESIAN_POINT('Ctrl Pts',(-85.7657507913734,3.0776009027646,134.643146905651));
#95267=CARTESIAN_POINT('Ctrl Pts',(-85.7735078322584,3.18336739739423,134.555913344608));
#95268=CARTESIAN_POINT('Ctrl Pts',(-85.7812648731434,3.28538229553097,134.464339611319));
#95269=CARTESIAN_POINT('Ctrl Pts',(-85.7890160643835,3.38732026343959,134.372834934494));
#95270=CARTESIAN_POINT('Ctrl Pts',(-85.7967672556236,3.48551197625884,134.276996860153));
#95271=CARTESIAN_POINT('Ctrl Pts',(-85.8045184468638,3.57957345636716,134.177169081291));
#95272=CARTESIAN_POINT('Ctrl Pts',(-85.8122663436409,3.67359495783713,134.077383731897));
#95273=CARTESIAN_POINT('Ctrl Pts',(-85.8200142404179,3.76348945051798,133.973612334616));
#95274=CARTESIAN_POINT('Ctrl Pts',(-85.827762137195,3.84890925214866,133.86623596304));
#95275=CARTESIAN_POINT('Ctrl Pts',(-85.8355084132791,3.93431118579828,133.758882052287));
#95276=CARTESIAN_POINT('Ctrl Pts',(-85.8432546893632,4.01524004692808,133.647924972919));
#95277=CARTESIAN_POINT('Ctrl Pts',(-85.8510009654473,4.09138822122309,133.533779142772));
#95278=CARTESIAN_POINT('Ctrl Pts',(-85.8587472987127,4.16753695762672,133.419632470026));
#95279=CARTESIAN_POINT('Ctrl Pts',(-85.866493631978,4.23890471980806,133.302297324768));
#95280=CARTESIAN_POINT('Ctrl Pts',(-85.8742399652434,4.30522727245043,133.182217046169));
#95281=CARTESIAN_POINT('Ctrl Pts',(-85.8819880332464,4.37156467756852,133.062109876425));
#95282=CARTESIAN_POINT('Ctrl Pts',(-85.8897361012494,4.43285443591132,132.93925669222));
#95283=CARTESIAN_POINT('Ctrl Pts',(-85.8974841692524,4.48887850150865,132.814124997088));
#95284=CARTESIAN_POINT('Ctrl Pts',(-85.9052404719942,4.54496211014951,132.6888603105));
#95285=CARTESIAN_POINT('Ctrl Pts',(-85.912996774736,4.59576868653493,132.561312632923));
#95286=CARTESIAN_POINT('Ctrl Pts',(-85.9207530774779,4.64112834873941,132.431969511934));
#95287=CARTESIAN_POINT('Ctrl Pts',(-85.9285135199921,4.68651222076149,132.302557356627));
#95288=CARTESIAN_POINT('Ctrl Pts',(-85.9362739625062,4.7264432720234,132.171348222295));
#95289=CARTESIAN_POINT('Ctrl Pts',(-85.9440344050204,4.76080196680109,132.038843381886));
#95290=CARTESIAN_POINT('Ctrl Pts',(-85.9518073052858,4.79521581720586,131.906125832943));
#95291=CARTESIAN_POINT('Ctrl Pts',(-85.9595802055512,4.82403935343005,131.772108803901));
#95292=CARTESIAN_POINT('Ctrl Pts',(-85.9673531058166,4.84720432377537,131.637303176254));
#95293=CARTESIAN_POINT('Ctrl Pts',(-85.9748434415787,4.86952718909967,131.507398072726));
#95294=CARTESIAN_POINT('Ctrl Pts',(-85.9823337773408,4.88659571226928,131.376761015686));
#95295=CARTESIAN_POINT('Ctrl Pts',(-85.9898241131028,4.89839461978055,131.245850381213));
#95296=CARTESIAN_POINT('Ctrl Pts',(-85.9975984472219,4.91064088645626,131.109976230245));
#95297=CARTESIAN_POINT('Ctrl Pts',(-86.005372781341,4.91724884688008,130.973376938477));
#95298=CARTESIAN_POINT('Ctrl Pts',(-86.01314711546,4.91814459548718,130.836560002346));
#95299=CARTESIAN_POINT('Ctrl Pts',(-86.0209118684071,4.91903924016418,130.699911680862));
#95300=CARTESIAN_POINT('Ctrl Pts',(-86.0286766213543,4.91423567757437,130.563046635911));
#95301=CARTESIAN_POINT('Ctrl Pts',(-86.0364413743013,4.90371165586805,130.426478283229));
#95302=CARTESIAN_POINT('Ctrl Pts',(-86.0441984151863,4.89319808676846,130.290045572161));
#95303=CARTESIAN_POINT('Ctrl Pts',(-86.0519554560713,4.87697539511814,130.153909354224));
#95304=CARTESIAN_POINT('Ctrl Pts',(-86.0597124969563,4.85507336409417,130.018583491554));
#95305=CARTESIAN_POINT('Ctrl Pts',(-86.0674636881964,4.83318784956213,129.88335967917));
#95306=CARTESIAN_POINT('Ctrl Pts',(-86.0752148794366,4.80563158258861,129.748945390085));
#95307=CARTESIAN_POINT('Ctrl Pts',(-86.0829660706767,4.77248617253988,129.615849450006));
#95308=CARTESIAN_POINT('Ctrl Pts',(-86.0907139674538,4.73935485017465,129.482810079252));
#95309=CARTESIAN_POINT('Ctrl Pts',(-86.0984618642309,4.70063920377225,129.351088321627));
#95310=CARTESIAN_POINT('Ctrl Pts',(-86.1062097610079,4.65647191058508,129.221182671651));
#95311=CARTESIAN_POINT('Ctrl Pts',(-86.113956037092,4.61231385624351,129.091304195136));
#95312=CARTESIAN_POINT('Ctrl Pts',(-86.121702313176,4.56270654914106,128.963241440567));
#95313=CARTESIAN_POINT('Ctrl Pts',(-86.1294485892601,4.5078323776895,128.837477215543));
#95314=CARTESIAN_POINT('Ctrl Pts',(-86.1371949225255,4.4529578011692,128.711712062156));
#95315=CARTESIAN_POINT('Ctrl Pts',(-86.1449412557909,4.39281643907293,128.58824583051));
#95316=CARTESIAN_POINT('Ctrl Pts',(-86.1526875890563,4.32763845955921,128.467540464913));
#95317=CARTESIAN_POINT('Ctrl Pts',(-86.1604356570593,4.26244588388899,128.346808068187));
#95318=CARTESIAN_POINT('Ctrl Pts',(-86.1681837250622,4.19221463210468,128.228838111759));
#95319=CARTESIAN_POINT('Ctrl Pts',(-86.1759317930652,4.11722016899497,128.114066740957));
#95320=CARTESIAN_POINT('Ctrl Pts',(-86.183688095807,4.04214600087753,127.999173389776));
#95321=CARTESIAN_POINT('Ctrl Pts',(-86.1914443985488,3.96229872294989,127.887485742891));
#95322=CARTESIAN_POINT('Ctrl Pts',(-86.1992007012906,3.8779966974675,127.77941025815));
#95323=CARTESIAN_POINT('Ctrl Pts',(-86.2069611438048,3.79364967745559,127.671277090269));
#95324=CARTESIAN_POINT('Ctrl Pts',(-86.214721586319,3.70484342528343,127.566760223868));
#95325=CARTESIAN_POINT('Ctrl Pts',(-86.2224820288331,3.61193506410006,127.466231178011));
#95326=CARTESIAN_POINT('Ctrl Pts',(-86.2302549290986,3.5188775581673,127.365540754005));
#95327=CARTESIAN_POINT('Ctrl Pts',(-86.238027829364,3.42170506145758,127.268851218909));
#95328=CARTESIAN_POINT('Ctrl Pts',(-86.2458007296295,3.32081050133173,127.176496138738));
#95329=CARTESIAN_POINT('Ctrl Pts',(-86.2532910653915,3.22358371260424,127.087498398359));
#95330=CARTESIAN_POINT('Ctrl Pts',(-86.2607814011535,3.12290101037792,127.002525646093));
#95331=CARTESIAN_POINT('Ctrl Pts',(-86.2682717369156,3.01913978372785,126.921838495438));
#95332=CARTESIAN_POINT('Ctrl Pts',(-86.2760460710347,2.91144441863196,126.838092066942));
#95333=CARTESIAN_POINT('Ctrl Pts',(-86.2838204051537,2.80009132979206,126.758697348867));
#95334=CARTESIAN_POINT('Ctrl Pts',(-86.2915947392728,2.68546754057026,126.683990834277));
#95335=CARTESIAN_POINT('Ctrl Pts',(-86.2993594922199,2.57098501492446,126.609376388789));
#95336=CARTESIAN_POINT('Ctrl Pts',(-86.3071242451671,2.45324013347387,126.539438862129));
#95337=CARTESIAN_POINT('Ctrl Pts',(-86.3148889981142,2.33265281974991,126.474474489154));
#95338=CARTESIAN_POINT('Ctrl Pts',(-86.3226460389993,2.21218527504593,126.409574639711));
#95339=CARTESIAN_POINT('Ctrl Pts',(-86.3304030798843,2.08888125821942,126.34963829854));
#95340=CARTESIAN_POINT('Ctrl Pts',(-86.3381601207693,1.96318919457174,126.294918163247));
#95341=CARTESIAN_POINT('Ctrl Pts',(-86.3459113120094,1.83759191628716,126.240239292833));
#95342=CARTESIAN_POINT('Ctrl Pts',(-86.3536625032496,1.70961053267106,126.19076895417));
#95343=CARTESIAN_POINT('Ctrl Pts',(-86.3614136944897,1.57971724505676,126.14671351971));
#95344=CARTESIAN_POINT('Ctrl Pts',(-86.3691615912668,1.44987916555454,126.102676809984));
#95345=CARTESIAN_POINT('Ctrl Pts',(-86.3769094880439,1.31813116774786,126.064050552307));
#95346=CARTESIAN_POINT('Ctrl Pts',(-86.384657384821,1.18496436448925,126.030992570014));
#95347=CARTESIAN_POINT('Ctrl Pts',(-86.3924036609051,1.05182541685513,125.997941502738));
#95348=CARTESIAN_POINT('Ctrl Pts',(-86.4001499369893,0.917268633295511,
125.970456488204));
#95349=CARTESIAN_POINT('Ctrl Pts',(-86.4078962130734,0.781798798908662,
125.948645047176));
#95350=CARTESIAN_POINT('Ctrl Pts',(-86.4156425463388,0.646327964514085,
125.926833445141));
#95351=CARTESIAN_POINT('Ctrl Pts',(-86.4233888796041,0.5099444518374,125.91069556233));
#95352=CARTESIAN_POINT('Ctrl Pts',(-86.4311352128695,0.373161319218978,
125.900287443934));
#95353=CARTESIAN_POINT('Ctrl Pts',(-86.4388832808725,0.23634755496658,125.889876994712));
#95354=CARTESIAN_POINT('Ctrl Pts',(-86.4466313488755,0.0991343824571351,
125.885198892865));
#95355=CARTESIAN_POINT('Ctrl Pts',(-86.4543794168785,-0.0379623614454079,
125.886257129268));
#95356=CARTESIAN_POINT('Ctrl Pts',(-86.4621357196204,-0.175204813399029,
125.887316490377));
#95357=CARTESIAN_POINT('Ctrl Pts',(-86.4698920223623,-0.312330197981408,
125.894124365426));
#95358=CARTESIAN_POINT('Ctrl Pts',(-86.4776483251042,-0.448824468116052,
125.906632607629));
#95359=CARTESIAN_POINT('Ctrl Pts',(-86.4854087676184,-0.585391589352429,
125.919147525858));
#95360=CARTESIAN_POINT('Ctrl Pts',(-86.4931692101326,-0.721326537639481,
125.937368821679));
#95361=CARTESIAN_POINT('Ctrl Pts',(-86.5009296526468,-0.856123709682584,
125.9611968524));
#95362=CARTESIAN_POINT('Ctrl Pts',(-86.5087025529123,-0.991137270112981,
125.985063133991));
#95363=CARTESIAN_POINT('Ctrl Pts',(-86.5164754531777,-1.12500902242117,
126.014554052049));
#95364=CARTESIAN_POINT('Ctrl Pts',(-86.5242483534431,-1.25724594123624,
126.049519326235));
#95365=CARTESIAN_POINT('Ctrl Pts',(-86.531738689205,-1.38467571496373,126.083213524631));
#95366=CARTESIAN_POINT('Ctrl Pts',(-86.5392290249669,-1.51058715785964,
126.121990885321));
#95367=CARTESIAN_POINT('Ctrl Pts',(-86.5467193607287,-1.63455702039369,
126.165674768149));
#95368=CARTESIAN_POINT('Ctrl Pts',(-86.5544937938774,-1.7632288769528,126.211015516217));
#95369=CARTESIAN_POINT('Ctrl Pts',(-86.562268227026,-1.89021656238627,126.261785955074));
#95370=CARTESIAN_POINT('Ctrl Pts',(-86.5700426601747,-2.01502776123146,
126.317842347909));
#95371=CARTESIAN_POINT('Ctrl Pts',(-86.5778074890018,-2.13968477174234,
126.373829490213));
#95372=CARTESIAN_POINT('Ctrl Pts',(-86.5855723178289,-2.26217029233569,
126.4350894347));
#95373=CARTESIAN_POINT('Ctrl Pts',(-86.593337146656,-2.38200809965312,126.501429003458));
#95374=CARTESIAN_POINT('Ctrl Pts',(-86.6010942403688,-2.50172652776018,
126.567702486517));
#95375=CARTESIAN_POINT('Ctrl Pts',(-86.6088513340816,-2.61880215171673,
126.639045335571));
#95376=CARTESIAN_POINT('Ctrl Pts',(-86.6166084277944,-2.73277997633288,
126.715216860805));
#95377=CARTESIAN_POINT('Ctrl Pts',(-86.6243596488841,-2.8466715123427,126.791330719255));
#95378=CARTESIAN_POINT('Ctrl Pts',(-86.6321108699738,-2.95746959339661,
126.872265761093));
#95379=CARTESIAN_POINT('Ctrl Pts',(-86.6398620910635,-3.06474535206361,
126.957736254634));
#95380=CARTESIAN_POINT('Ctrl Pts',(-86.6476098988209,-3.17197387071528,
127.043169110338));
#95381=CARTESIAN_POINT('Ctrl Pts',(-86.6553577065785,-3.27568284748481,
127.133133201471));
#95382=CARTESIAN_POINT('Ctrl Pts',(-86.663105514336,-3.3754740572554,127.227300658424));
#95383=CARTESIAN_POINT('Ctrl Pts',(-86.6708516686727,-3.47524397108448,
127.321448019573));
#95384=CARTESIAN_POINT('Ctrl Pts',(-86.6785978230093,-3.57109749695532,
127.419796693971));
#95385=CARTESIAN_POINT('Ctrl Pts',(-86.686343977346,-3.66267134356729,127.521980125985));
#95386=CARTESIAN_POINT('Ctrl Pts',(-86.6940901561138,-3.75424547899967,
127.624163880282));
#95387=CARTESIAN_POINT('Ctrl Pts',(-86.7018363348816,-3.8415396474482,127.730182125101));
#95388=CARTESIAN_POINT('Ctrl Pts',(-86.7095825136493,-3.92422939519156,
127.839633527864));
#95389=CARTESIAN_POINT('Ctrl Pts',(-86.7173303943538,-4.00693731095241,
127.949108978529));
#95390=CARTESIAN_POINT('Ctrl Pts',(-86.7250782750582,-4.08503855757133,
128.062018776099));
#95391=CARTESIAN_POINT('Ctrl Pts',(-86.7328261557626,-4.15825097429988,
128.177931121609));
#95392=CARTESIAN_POINT('Ctrl Pts',(-86.7405818164013,-4.23153690633054,
128.293959859002));
#95393=CARTESIAN_POINT('Ctrl Pts',(-86.74833747704,-4.2999239947759,128.412996835063));
#95394=CARTESIAN_POINT('Ctrl Pts',(-86.7560931376787,-4.36317494708238,
128.534583658556));
#95395=CARTESIAN_POINT('Ctrl Pts',(-86.7638529245643,-4.42645955081553,
128.65623516993));
#95396=CARTESIAN_POINT('Ctrl Pts',(-86.7716127114498,-4.48460240798662,
128.780438878062));
#95397=CARTESIAN_POINT('Ctrl Pts',(-86.7793724983354,-4.53741409986099,
128.90671566951));
#95398=CARTESIAN_POINT('Ctrl Pts',(-86.787143673959,-4.59030330140581,129.033177792504));
#95399=CARTESIAN_POINT('Ctrl Pts',(-86.7949148495828,-4.63784557115586,
129.161718710619));
#95400=CARTESIAN_POINT('Ctrl Pts',(-86.8026860252064,-4.67990092905662,
129.291842731154));
#95401=CARTESIAN_POINT('Ctrl Pts',(-86.8084244753616,-4.71095576384141,
129.387929892481));
#95402=CARTESIAN_POINT('Ctrl Pts',(-86.8141629255169,-4.7390197636557,129.484879952173));
#95403=CARTESIAN_POINT('Ctrl Pts',(-86.8199013756722,-4.76405452823401,
129.582490119308));
#95404=CARTESIAN_POINT('Origin',(213.235140564004,0.,130.804360617566));
#95405=CARTESIAN_POINT('',(-88.9150399778173,-4.76405452823403,129.582490119308));
#95406=CARTESIAN_POINT('',(-88.5701298338732,-4.76405452823396,129.582490119308));
#95407=CARTESIAN_POINT('',(213.235140564004,-4.76405452823405,129.582490119308));
#95408=CARTESIAN_POINT('',(-87.2351405640591,-4.91824986470146,130.805514248378));
#95409=CARTESIAN_POINT('Ctrl Pts',(-87.235140564059,-4.91824986470146,130.805514248378));
#95410=CARTESIAN_POINT('Ctrl Pts',(-87.2434150306343,-4.9182154076984,130.95241406143));
#95411=CARTESIAN_POINT('Ctrl Pts',(-87.2516894972096,-4.91159524424352,
131.099139306973));
#95412=CARTESIAN_POINT('Ctrl Pts',(-87.2599639637848,-4.89846150369965,
131.245107664377));
#95413=CARTESIAN_POINT('Ctrl Pts',(-87.2685064031367,-4.88490242033887,
131.395803280715));
#95414=CARTESIAN_POINT('Ctrl Pts',(-87.2770488424886,-4.86440086237666,
131.545691795828));
#95415=CARTESIAN_POINT('Ctrl Pts',(-87.2855912818405,-4.83709249482959,
131.694146692397));
#95416=CARTESIAN_POINT('Ctrl Pts',(-87.2939087439399,-4.81050333186161,
131.838691818775));
#95417=CARTESIAN_POINT('Ctrl Pts',(-87.3022262060394,-4.77746153715247,
131.98187763293));
#95418=CARTESIAN_POINT('Ctrl Pts',(-87.3105436681389,-4.73814257228153,
132.123143399996));
#95419=CARTESIAN_POINT('Ctrl Pts',(-87.319198596117,-4.69722831201058,132.270140768316));
#95420=CARTESIAN_POINT('Ctrl Pts',(-87.327853524095,-4.64951700377619,132.415058660253));
#95421=CARTESIAN_POINT('Ctrl Pts',(-87.336508452073,-4.59526078202615,132.557289996541));
#95422=CARTESIAN_POINT('Ctrl Pts',(-87.3451633800511,-4.54100456027611,
132.699521332828));
#95423=CARTESIAN_POINT('Ctrl Pts',(-87.3538183080292,-4.48020363982355,
132.839065813765));
#95424=CARTESIAN_POINT('Ctrl Pts',(-87.3624732360073,-4.41316267366985,
132.975346172153));
#95425=CARTESIAN_POINT('Ctrl Pts',(-87.3702475701264,-4.35294277676666,
133.097760713634));
#95426=CARTESIAN_POINT('Ctrl Pts',(-87.3780219042455,-4.2875302410094,133.217861637103));
#95427=CARTESIAN_POINT('Ctrl Pts',(-87.3857962383646,-4.2171259359179,133.335177067471));
#95428=CARTESIAN_POINT('Ctrl Pts',(-87.3935609913117,-4.14680839784021,
133.452347917055));
#95429=CARTESIAN_POINT('Ctrl Pts',(-87.4013257442588,-4.07151153014495,
133.566739771915));
#95430=CARTESIAN_POINT('Ctrl Pts',(-87.4090904972059,-3.99148339667264,
133.677902570729));
#95431=CARTESIAN_POINT('Ctrl Pts',(-87.4168475380909,-3.91153474827069,
133.788954961083));
#95432=CARTESIAN_POINT('Ctrl Pts',(-87.4246045789759,-3.82686441257948,
133.896784362512));
#95433=CARTESIAN_POINT('Ctrl Pts',(-87.4323616198609,-3.73776512653218,
134.000967399981));
#95434=CARTESIAN_POINT('Ctrl Pts',(-87.440112811101,-3.6487330309497,134.105071872211));
#95435=CARTESIAN_POINT('Ctrl Pts',(-87.4478640023411,-3.55527888597019,
134.205535157772));
#95436=CARTESIAN_POINT('Ctrl Pts',(-87.4556151935812,-3.45773707120855,
134.301965141936));
#95437=CARTESIAN_POINT('Ctrl Pts',(-87.4633630903583,-3.36023671432006,
134.398354140783));
#95438=CARTESIAN_POINT('Ctrl Pts',(-87.4711109871354,-3.25865242059542,
134.490712973477));
#95439=CARTESIAN_POINT('Ctrl Pts',(-87.4788588839125,-3.15335681047315,
134.578684913164));
#95440=CARTESIAN_POINT('Ctrl Pts',(-87.4866051599966,-3.0480832259226,134.666638451018));
#95441=CARTESIAN_POINT('Ctrl Pts',(-87.4943514360806,-2.93910016897346,
134.750206670598));
#95442=CARTESIAN_POINT('Ctrl Pts',(-87.5020977121647,-2.82681455622494,
134.829072101289));
#95443=CARTESIAN_POINT('Ctrl Pts',(-87.5098440454301,-2.71452811460937,
134.907938114147));
#95444=CARTESIAN_POINT('Ctrl Pts',(-87.5175903786955,-2.59893938848384,
134.982101044134));
#95445=CARTESIAN_POINT('Ctrl Pts',(-87.5253367119608,-2.48048524843065,
135.051286093109));
#95446=CARTESIAN_POINT('Ctrl Pts',(-87.5330847799638,-2.36200458139394,
135.120486635596));
#95447=CARTESIAN_POINT('Ctrl Pts',(-87.5408328479669,-2.24065756107677,
135.184706881681));
#95448=CARTESIAN_POINT('Ctrl Pts',(-87.5485809159699,-2.11690632387932,
135.243717629389));
#95449=CARTESIAN_POINT('Ctrl Pts',(-87.5563372187118,-1.99302356239449,
135.302791094422));
#95450=CARTESIAN_POINT('Ctrl Pts',(-87.5640935214537,-1.866731833141,135.356643832343));
#95451=CARTESIAN_POINT('Ctrl Pts',(-87.5718498241955,-1.7385144665978,135.405094310351));
#95452=CARTESIAN_POINT('Ctrl Pts',(-87.5796102667097,-1.61022866658553,
135.453570647839));
#95453=CARTESIAN_POINT('Ctrl Pts',(-87.5873707092238,-1.48001555237063,
135.496638857385));
#95454=CARTESIAN_POINT('Ctrl Pts',(-87.595131151738,-1.34837338401885,135.534167408522));
#95455=CARTESIAN_POINT('Ctrl Pts',(-87.6029040520034,-1.21651989197179,
135.57175620382));
#95456=CARTESIAN_POINT('Ctrl Pts',(-87.6106769522689,-1.0832331419167,135.603787478749));
#95457=CARTESIAN_POINT('Ctrl Pts',(-87.6184498525343,-0.949022230375064,
135.630180741519));
#95458=CARTESIAN_POINT('Ctrl Pts',(-87.6259401882964,-0.819690223524848,
135.655614542707));
#95459=CARTESIAN_POINT('Ctrl Pts',(-87.6334305240584,-0.689500384223107,
135.675813079727));
#95460=CARTESIAN_POINT('Ctrl Pts',(-87.6409208598204,-0.558910590025547,
135.690750083711));
#95461=CARTESIAN_POINT('Ctrl Pts',(-87.6486951939395,-0.423369444088893,
135.706253428742));
#95462=CARTESIAN_POINT('Ctrl Pts',(-87.6564695280586,-0.28696806237198,
135.716137492594));
#95463=CARTESIAN_POINT('Ctrl Pts',(-87.6642438621777,-0.150212021635176,
135.720316212469));
#95464=CARTESIAN_POINT('Ctrl Pts',(-87.6720086151248,-0.0136245204967136,
135.724489782445));
#95465=CARTESIAN_POINT('Ctrl Pts',(-87.6797733680718,0.123316382960341,
135.722971986863));
#95466=CARTESIAN_POINT('Ctrl Pts',(-87.6875381210189,0.260097954833687,
135.715728259719));
#95467=CARTESIAN_POINT('Ctrl Pts',(-87.6952951619039,0.396743673321566,
135.708491727147));
#95468=CARTESIAN_POINT('Ctrl Pts',(-87.703052202789,0.533229987259395,135.695540601093));
#95469=CARTESIAN_POINT('Ctrl Pts',(-87.710809243674,0.669042467778677,135.676892324883));
#95470=CARTESIAN_POINT('Ctrl Pts',(-87.7185604349141,0.804752531050118,
135.658258111483));
#95471=CARTESIAN_POINT('Ctrl Pts',(-87.7263116261543,0.939789386567182,
135.63393535235));
#95472=CARTESIAN_POINT('Ctrl Pts',(-87.7340628173944,1.073642396753,135.603993422937));
#95473=CARTESIAN_POINT('Ctrl Pts',(-87.7418107141715,1.20743851583903,135.574064219642));
#95474=CARTESIAN_POINT('Ctrl Pts',(-87.7495586109486,1.34005140961509,135.538520681376));
#95475=CARTESIAN_POINT('Ctrl Pts',(-87.7573065077257,1.47097954322825,135.497483484688));
#95476=CARTESIAN_POINT('Ctrl Pts',(-87.7650527838098,1.60188028949799,135.456454872097));
#95477=CARTESIAN_POINT('Ctrl Pts',(-87.7727990598939,1.73109660374572,135.409935003676));
#95478=CARTESIAN_POINT('Ctrl Pts',(-87.780545335978,1.8581414405904,135.35809462926));
#95479=CARTESIAN_POINT('Ctrl Pts',(-87.7882916692433,1.98518721525138,135.306253872171));
#95480=CARTESIAN_POINT('Ctrl Pts',(-87.7960380025087,2.11006111853508,135.249092678427));
#95481=CARTESIAN_POINT('Ctrl Pts',(-87.8037843357741,2.23229581576175,135.186830064514));
#95482=CARTESIAN_POINT('Ctrl Pts',(-87.811532403777,2.35455788660119,135.124553507321));
#95483=CARTESIAN_POINT('Ctrl Pts',(-87.8192804717799,2.47417922699072,135.057173434077));
#95484=CARTESIAN_POINT('Ctrl Pts',(-87.8270285397829,2.59071720680562,134.98495476396));
#95485=CARTESIAN_POINT('Ctrl Pts',(-87.8347848425248,2.70737904457244,134.91265933898));
#95486=CARTESIAN_POINT('Ctrl Pts',(-87.8425411452667,2.82095064268278,134.835515250664));
#95487=CARTESIAN_POINT('Ctrl Pts',(-87.8502974480085,2.93101802051978,134.753831015719));
#95488=CARTESIAN_POINT('Ctrl Pts',(-87.8580578905227,3.04114414463041,134.672103183438));
#95489=CARTESIAN_POINT('Ctrl Pts',(-87.8658183330368,3.14776201794214,134.585830621882));
#95490=CARTESIAN_POINT('Ctrl Pts',(-87.873578775551,3.25049165840981,134.495361435922));
#95491=CARTESIAN_POINT('Ctrl Pts',(-87.8813516758164,3.35338620961626,134.404747020794));
#95492=CARTESIAN_POINT('Ctrl Pts',(-87.8891245760819,3.45237977250185,134.309922789603));
#95493=CARTESIAN_POINT('Ctrl Pts',(-87.8968974763473,3.54712944793814,134.211273551891));
#95494=CARTESIAN_POINT('Ctrl Pts',(-87.9043878121093,3.63843473401178,134.116210462453));
#95495=CARTESIAN_POINT('Ctrl Pts',(-87.9118781478713,3.72579912346444,134.017595866117));
#95496=CARTESIAN_POINT('Ctrl Pts',(-87.9193684836333,3.80895302155096,133.915800789274));
#95497=CARTESIAN_POINT('Ctrl Pts',(-87.9271428177524,3.89525972495811,133.810146121152));
#95498=CARTESIAN_POINT('Ctrl Pts',(-87.9349171518714,3.97730374641448,133.700730353569));
#95499=CARTESIAN_POINT('Ctrl Pts',(-87.9426914859905,4.05473940226316,133.587932323528));
#95500=CARTESIAN_POINT('Ctrl Pts',(-87.9504562389376,4.13207962558642,133.475273306979));
#95501=CARTESIAN_POINT('Ctrl Pts',(-87.9582209918847,4.20482256446318,133.359240640946));
#95502=CARTESIAN_POINT('Ctrl Pts',(-87.9659857448318,4.27266199233714,133.240247019215));
#95503=CARTESIAN_POINT('Ctrl Pts',(-87.9737427857168,4.34043404113496,133.121371583626));
#95504=CARTESIAN_POINT('Ctrl Pts',(-87.9814998266019,4.40331207853759,132.999541382236));
#95505=CARTESIAN_POINT('Ctrl Pts',(-87.9892568674869,4.46103271874009,132.875198647164));
#95506=CARTESIAN_POINT('Ctrl Pts',(-87.997008058727,4.5187098313589,132.750949679917));
#95507=CARTESIAN_POINT('Ctrl Pts',(-88.0047592499672,4.57123712411015,132.6241923035));
#95508=CARTESIAN_POINT('Ctrl Pts',(-88.0125104412073,4.61839695244212,132.495393630896));
#95509=CARTESIAN_POINT('Ctrl Pts',(-88.0202583379844,4.66553673658896,132.366649701165));
#95510=CARTESIAN_POINT('Ctrl Pts',(-88.0280062347614,4.70731345953583,132.235866567206));
#95511=CARTESIAN_POINT('Ctrl Pts',(-88.0357541315385,4.74355755804388,132.103531413122));
#95512=CARTESIAN_POINT('Ctrl Pts',(-88.0435004076226,4.77979407506785,131.971223940698));
#95513=CARTESIAN_POINT('Ctrl Pts',(-88.0512466837067,4.81050016638838,131.837365470733));
#95514=CARTESIAN_POINT('Ctrl Pts',(-88.0589929597908,4.83555622875427,131.702458062755));
#95515=CARTESIAN_POINT('Ctrl Pts',(-88.0667392930562,4.86061247607836,131.567549658922));
#95516=CARTESIAN_POINT('Ctrl Pts',(-88.0744856263215,4.88001853983181,131.431592686018));
#95517=CARTESIAN_POINT('Ctrl Pts',(-88.0822319595869,4.89370607897761,131.295098709706));
#95518=CARTESIAN_POINT('Ctrl Pts',(-88.0899800275899,4.90739668335288,131.158574166515));
#95519=CARTESIAN_POINT('Ctrl Pts',(-88.0977280955928,4.91536617582449,131.021512769555));
#95520=CARTESIAN_POINT('Ctrl Pts',(-88.1054761635958,4.91759818800414,130.884430111372));
#95521=CARTESIAN_POINT('Ctrl Pts',(-88.1132324663377,4.91983257239291,130.747201760109));
#95522=CARTESIAN_POINT('Ctrl Pts',(-88.1209887690795,4.91631728897776,130.60995249402));
#95523=CARTESIAN_POINT('Ctrl Pts',(-88.1287450718213,4.90708813496676,130.473197367539));
#95524=CARTESIAN_POINT('Ctrl Pts',(-88.1365055143355,4.89785405507839,130.33636925073));
#95525=CARTESIAN_POINT('Ctrl Pts',(-88.1442659568497,4.88290007048621,130.200036187492));
#95526=CARTESIAN_POINT('Ctrl Pts',(-88.1520263993639,4.86231366210198,130.064706026668));
#95527=CARTESIAN_POINT('Ctrl Pts',(-88.1597992996293,4.84169420658744,129.929158621856));
#95528=CARTESIAN_POINT('Ctrl Pts',(-88.1675721998948,4.81542433411614,129.794617720587));
#95529=CARTESIAN_POINT('Ctrl Pts',(-88.1753451001602,4.78364245050019,129.661579812568));
#95530=CARTESIAN_POINT('Ctrl Pts',(-88.1828354359222,4.7530159184075,129.533378167607));
#95531=CARTESIAN_POINT('Ctrl Pts',(-88.1903257716842,4.71727125209247,129.406572434357));
#95532=CARTESIAN_POINT('Ctrl Pts',(-88.1978161074462,4.67657488402088,129.281589979339));
#95533=CARTESIAN_POINT('Ctrl Pts',(-88.2055904415653,4.63433550078439,129.151868776552));
#95534=CARTESIAN_POINT('Ctrl Pts',(-88.2133647756844,4.58662771433529,129.023700922686));
#95535=CARTESIAN_POINT('Ctrl Pts',(-88.2211391098034,4.53358340051323,128.897582021847));
#95536=CARTESIAN_POINT('Ctrl Pts',(-88.2289038627505,4.48060445906725,128.771618551282));
#95537=CARTESIAN_POINT('Ctrl Pts',(-88.2366686156977,4.4223022262262,128.647699366372));
#95538=CARTESIAN_POINT('Ctrl Pts',(-88.2444333686447,4.35885839002497,128.526305175262));
#95539=CARTESIAN_POINT('Ctrl Pts',(-88.2521904095297,4.29547756713627,128.405031554575));
#95540=CARTESIAN_POINT('Ctrl Pts',(-88.2599474504147,4.22696548339365,128.28627828119));
#95541=CARTESIAN_POINT('Ctrl Pts',(-88.2677044912997,4.15355183474339,128.170505986308));
#95542=CARTESIAN_POINT('Ctrl Pts',(-88.2754556825398,4.08019354789676,128.054820996214));
#95543=CARTESIAN_POINT('Ctrl Pts',(-88.28320687378,4.00194126194501,127.942112838998));
#95544=CARTESIAN_POINT('Ctrl Pts',(-88.2909580650201,3.91907033007207,127.832817111163));
#95545=CARTESIAN_POINT('Ctrl Pts',(-88.2987059617972,3.83623462055573,127.723567836926));
#95546=CARTESIAN_POINT('Ctrl Pts',(-88.3064538585743,3.74878440519206,127.617728418273));
#95547=CARTESIAN_POINT('Ctrl Pts',(-88.3142017553514,3.65703791268919,127.515704848463));
#95548=CARTESIAN_POINT('Ctrl Pts',(-88.3219480314355,3.56531061157473,127.413702619785));
#95549=CARTESIAN_POINT('Ctrl Pts',(-88.3296943075194,3.46928908212053,127.315514942824));
#95550=CARTESIAN_POINT('Ctrl Pts',(-88.3374405836035,3.36933107275015,127.221513818622));
#95551=CARTESIAN_POINT('Ctrl Pts',(-88.3451869168689,3.2693723255126,127.127512000526));
#95552=CARTESIAN_POINT('Ctrl Pts',(-88.3529332501342,3.16547732518568,127.037697064694));
#95553=CARTESIAN_POINT('Ctrl Pts',(-88.3606795833996,3.05803952644947,126.952403022112));
#95554=CARTESIAN_POINT('Ctrl Pts',(-88.3684276514025,2.95057766776329,126.867089878521));
#95555=CARTESIAN_POINT('Ctrl Pts',(-88.3761757194055,2.83957173806734,126.78629988583));
#95556=CARTESIAN_POINT('Ctrl Pts',(-88.3839237874084,2.72544667245893,126.710325505591));
#95557=CARTESIAN_POINT('Ctrl Pts',(-88.3916800901502,2.61120031337254,126.634270378877));
#95558=CARTESIAN_POINT('Ctrl Pts',(-88.3994363928921,2.49382852215972,126.563041305552));
#95559=CARTESIAN_POINT('Ctrl Pts',(-88.4071926956339,2.37378397796804,126.496886567912));
#95560=CARTESIAN_POINT('Ctrl Pts',(-88.4149531381481,2.25367536238832,126.430696521497));
#95561=CARTESIAN_POINT('Ctrl Pts',(-88.4227135806623,2.13089150118981,126.369586381453));
#95562=CARTESIAN_POINT('Ctrl Pts',(-88.4304740231765,2.00590694755695,126.313757052315));
#95563=CARTESIAN_POINT('Ctrl Pts',(-88.4382469234419,1.880721757623,126.257838100983));
#95564=CARTESIAN_POINT('Ctrl Pts',(-88.4460198237073,1.75332917924145,126.207217045214));
#95565=CARTESIAN_POINT('Ctrl Pts',(-88.4537927239727,1.6242217349851,126.162045805093));
#95566=CARTESIAN_POINT('Ctrl Pts',(-88.4612830597348,1.49980767152809,126.11851665333));
#95567=CARTESIAN_POINT('Ctrl Pts',(-88.468773395497,1.37380155156294,126.080048057218));
#95568=CARTESIAN_POINT('Ctrl Pts',(-88.4762637312591,1.246652891461,126.046730994454));
#95569=CARTESIAN_POINT('Ctrl Pts',(-88.4840380653782,1.1146833512666,126.012150705129));
#95570=CARTESIAN_POINT('Ctrl Pts',(-88.4918123994972,0.981064882003765,
125.983010761335));
#95571=CARTESIAN_POINT('Ctrl Pts',(-88.4995867336163,0.846285731554575,
125.959468098318));
#95572=CARTESIAN_POINT('Ctrl Pts',(-88.5073514865634,0.71167268436312,125.935954449529));
#95573=CARTESIAN_POINT('Ctrl Pts',(-88.5151162395104,0.575902183562834,
125.918024422884));
#95574=CARTESIAN_POINT('Ctrl Pts',(-88.5228809924575,0.439476869351736,
125.905784993591));
#95575=CARTESIAN_POINT('Ctrl Pts',(-88.5306380333425,0.303187054685602,
125.893557720671));
#95576=CARTESIAN_POINT('Ctrl Pts',(-88.5383950742276,0.166244107755559,
125.887009832112));
#95577=CARTESIAN_POINT('Ctrl Pts',(-88.5461521151126,0.0291597269057145,
125.886197060625));
#95578=CARTESIAN_POINT('Ctrl Pts',(-88.5539033063528,-0.107821277545984,
125.885384902055));
#95579=CARTESIAN_POINT('Ctrl Pts',(-88.5616544975928,-0.244943114247928,
125.890299254421));
#95580=CARTESIAN_POINT('Ctrl Pts',(-88.569405688833,-0.381690468404819,
125.900943905841));
#95581=CARTESIAN_POINT('Ctrl Pts',(-88.5771535856101,-0.518379701288525,
125.911584032999));
#95582=CARTESIAN_POINT('Ctrl Pts',(-88.5849014823872,-0.654694379224354,
125.92794958485));
#95583=CARTESIAN_POINT('Ctrl Pts',(-88.5926493791643,-0.790120918193643,
125.949992275842));
#95584=CARTESIAN_POINT('Ctrl Pts',(-88.6003956552484,-0.925519128850438,
125.972030355978));
#95585=CARTESIAN_POINT('Ctrl Pts',(-88.6081419313325,-1.06002918442376,
125.999743150414));
#95586=CARTESIAN_POINT('Ctrl Pts',(-88.6158882074166,-1.19314473813956,
126.03303075092));
#95587=CARTESIAN_POINT('Ctrl Pts',(-88.623634540682,-1.32626127448395,126.066318597147));
#95588=CARTESIAN_POINT('Ctrl Pts',(-88.6313808739474,-1.45798290914398,
126.105181236712));
#95589=CARTESIAN_POINT('Ctrl Pts',(-88.6391272072127,-1.58781595735216,
126.149468186147));
#95590=CARTESIAN_POINT('Ctrl Pts',(-88.6468752752157,-1.71767808077147,
126.193765053338));
#95591=CARTESIAN_POINT('Ctrl Pts',(-88.6546233432187,-1.84565040618618,
126.243488521388));
#95592=CARTESIAN_POINT('Ctrl Pts',(-88.6623714112216,-1.97125718960859,
126.298439162978));
#95593=CARTESIAN_POINT('Ctrl Pts',(-88.6701277139635,-2.09699746941498,
126.353448206764));
#95594=CARTESIAN_POINT('Ctrl Pts',(-88.6778840167053,-2.22036682623198,
126.413695364854));
#95595=CARTESIAN_POINT('Ctrl Pts',(-88.6856403194471,-2.34091168899455,
126.478933988108));
#95596=CARTESIAN_POINT('Ctrl Pts',(-88.6934007619613,-2.46152089017991,
126.544207431178));
#95597=CARTESIAN_POINT('Ctrl Pts',(-88.7011612044755,-2.57930225786841,
126.614477447632));
#95598=CARTESIAN_POINT('Ctrl Pts',(-88.7089216469896,-2.69383025779619,
126.689453376244));
#95599=CARTESIAN_POINT('Ctrl Pts',(-88.7166945472551,-2.80854210823678,
126.764549662873));
#95600=CARTESIAN_POINT('Ctrl Pts',(-88.7244674475205,-2.91998983646938,
126.84436672988));
#95601=CARTESIAN_POINT('Ctrl Pts',(-88.7322403477859,-3.02777940734386,
126.928572320592));
#95602=CARTESIAN_POINT('Ctrl Pts',(-88.7397306835478,-3.13165055581004,
127.009716825979));
#95603=CARTESIAN_POINT('Ctrl Pts',(-88.7472210193098,-3.2321246609155,127.094936127536));
#95604=CARTESIAN_POINT('Ctrl Pts',(-88.7547113550717,-3.32888220596853,
127.183901210076));
#95605=CARTESIAN_POINT('Ctrl Pts',(-88.7623680314278,-3.42778848080405,
127.274841972366));
#95606=CARTESIAN_POINT('Ctrl Pts',(-88.7700247077838,-3.52314454494613,
127.370003713737));
#95607=CARTESIAN_POINT('Ctrl Pts',(-88.7776813841399,-3.61456031361364,
127.469074002933));
#95608=CARTESIAN_POINT('Ctrl Pts',(-88.7853292035122,-3.70587033561802,
127.568029690976));
#95609=CARTESIAN_POINT('Ctrl Pts',(-88.7929770228845,-3.79324885201695,
127.670884646024));
#95610=CARTESIAN_POINT('Ctrl Pts',(-88.8006248422568,-3.87633939608425,
127.777286791432));
#95611=CARTESIAN_POINT('Ctrl Pts',(-88.8082655891791,-3.95935310076816,
127.88359053966));
#95612=CARTESIAN_POINT('Ctrl Pts',(-88.8159063361015,-4.03808647091666,
127.993434639985));
#95613=CARTESIAN_POINT('Ctrl Pts',(-88.8235470830237,-4.11222082990317,
128.106431243285));
#95614=CARTESIAN_POINT('Ctrl Pts',(-88.8311825833212,-4.18630428350404,
128.2193502559));
#95615=CARTESIAN_POINT('Ctrl Pts',(-88.8388180836185,-4.25579478629175,
128.335417129918));
#95616=CARTESIAN_POINT('Ctrl Pts',(-88.8464535839159,-4.32041515927868,
128.454212555427));
#95617=CARTESIAN_POINT('Ctrl Pts',(-88.8540858257332,-4.38500795526401,
128.572957284515));
#95618=CARTESIAN_POINT('Ctrl Pts',(-88.8617180675505,-4.44473456326938,
128.694427894813));
#95619=CARTESIAN_POINT('Ctrl Pts',(-88.8693503093677,-4.49936248964123,
128.818178287237));
#95620=CARTESIAN_POINT('Ctrl Pts',(-88.8769831125742,-4.55399443416758,
128.941937782116));
#95621=CARTESIAN_POINT('Ctrl Pts',(-88.8846159157806,-4.6035267735283,129.06797702981));
#95622=CARTESIAN_POINT('Ctrl Pts',(-88.8922487189871,-4.64777422352981,
129.195827798631));
#95623=CARTESIAN_POINT('Ctrl Pts',(-88.8998458052638,-4.69181462206964,
129.323080302725));
#95624=CARTESIAN_POINT('Ctrl Pts',(-88.9074428915406,-4.73061939022566,
129.452127023663));
#95625=CARTESIAN_POINT('Ctrl Pts',(-88.9150399778173,-4.76405452823403,
129.582490119308));
#95626=CARTESIAN_POINT('Ctrl Pts',(-87.1653941590427,-4.76405452823403,
129.582490119308));
#95627=CARTESIAN_POINT('Ctrl Pts',(-87.1733902600484,-4.79917917091089,
129.719440568014));
#95628=CARTESIAN_POINT('Ctrl Pts',(-87.181386361054,-4.82842565015031,129.858028792729));
#95629=CARTESIAN_POINT('Ctrl Pts',(-87.1893824620597,-4.85165185218374,
129.997727263618));
#95630=CARTESIAN_POINT('Ctrl Pts',(-87.197369497904,-4.87485172272489,130.137267358669));
#95631=CARTESIAN_POINT('Ctrl Pts',(-87.2053565337483,-4.89204486357648,
130.277914841835));
#95632=CARTESIAN_POINT('Ctrl Pts',(-87.2133435695926,-4.90313991537456,
130.419130773498));
#95633=CARTESIAN_POINT('Ctrl Pts',(-87.2206092343981,-4.91323288715235,
130.547592401148));
#95634=CARTESIAN_POINT('Ctrl Pts',(-87.2278748992035,-4.91828012077182,
130.676524083358));
#95635=CARTESIAN_POINT('Ctrl Pts',(-87.2351405640089,-4.91824986470167,
130.805514247488));
#95636=CARTESIAN_POINT('',(-86.8898594360246,-4.9182479024669,130.799818329603));
#95637=CARTESIAN_POINT('Ctrl Pts',(-86.8199013756722,-4.76405452823401,
129.582490119308));
#95638=CARTESIAN_POINT('Ctrl Pts',(-86.8216565786288,-4.77171183841665,
129.612345855494));
#95639=CARTESIAN_POINT('Ctrl Pts',(-86.8234117815855,-4.77908585800606,
129.642263334497));
#95640=CARTESIAN_POINT('Ctrl Pts',(-86.8251669845421,-4.78617577532478,
129.672236724083));
#95641=CARTESIAN_POINT('Ctrl Pts',(-86.8359490597836,-4.82972858595405,
129.85636092496));
#95642=CARTESIAN_POINT('Ctrl Pts',(-86.846731135025,-4.86267186386441,130.043083385357));
#95643=CARTESIAN_POINT('Ctrl Pts',(-86.8575132102665,-4.88475779004073,
130.231364635786));
#95644=CARTESIAN_POINT('Ctrl Pts',(-86.8682952855081,-4.90684371621709,
130.419645886214));
#95645=CARTESIAN_POINT('Ctrl Pts',(-86.8790773607497,-4.91807212000454,
130.609486579959));
#95646=CARTESIAN_POINT('Ctrl Pts',(-86.8898594359914,-4.91824790246636,
130.799818329018));
#95647=CARTESIAN_POINT('Ctrl Pts',(-86.8898594360245,-4.9182479024669,130.799818329603));
#95648=CARTESIAN_POINT('Ctrl Pts',(-86.8975161444314,-4.91837273139357,
130.934979202668));
#95649=CARTESIAN_POINT('Ctrl Pts',(-86.9051728528383,-4.91292173440832,
131.070298365521));
#95650=CARTESIAN_POINT('Ctrl Pts',(-86.9128295612452,-4.90188259609975,
131.205272174589));
#95651=CARTESIAN_POINT('Ctrl Pts',(-86.920778938208,-4.89042149988227,131.345405196689));
#95652=CARTESIAN_POINT('Ctrl Pts',(-86.9287283151711,-4.87293651889991,
131.485165501218));
#95653=CARTESIAN_POINT('Ctrl Pts',(-86.9366776921339,-4.84947337498785,
131.623989221132));
#95654=CARTESIAN_POINT('Ctrl Pts',(-86.9443260986553,-4.82689856645291,
131.757556952248));
#95655=CARTESIAN_POINT('Ctrl Pts',(-86.9519745051767,-4.7987900901287,131.890257291798));
#95656=CARTESIAN_POINT('Ctrl Pts',(-86.9596229116981,-4.76524142747747,
132.021594038218));
#95657=CARTESIAN_POINT('Ctrl Pts',(-86.9672702572283,-4.7316974187152,132.152912565532));
#95658=CARTESIAN_POINT('Ctrl Pts',(-86.9749176027584,-4.69271482354635,
132.282867486452));
#95659=CARTESIAN_POINT('Ctrl Pts',(-86.9825649482887,-4.64843782494699,
132.410974712519));
#95660=CARTESIAN_POINT('Ctrl Pts',(-86.9902129898755,-4.60415679628284,
132.539093598826));
#95661=CARTESIAN_POINT('Ctrl Pts',(-86.9978610314625,-4.5545805375101,132.665364076015));
#95662=CARTESIAN_POINT('Ctrl Pts',(-87.0055090730494,-4.49990231636308,
132.789319611019));
#95663=CARTESIAN_POINT('Ctrl Pts',(-87.0131595680623,-4.44520655491211,
132.913314909894));
#95664=CARTESIAN_POINT('Ctrl Pts',(-87.0208100630751,-4.38540573883924,
133.034993422437));
#95665=CARTESIAN_POINT('Ctrl Pts',(-87.0284605580881,-4.32074000539837,
133.153911397662));
#95666=CARTESIAN_POINT('Ctrl Pts',(-87.0361193562716,-4.25600408949026,
133.272958435938));
#95667=CARTESIAN_POINT('Ctrl Pts',(-87.0437781544552,-4.18639291050616,
133.389238604206));
#95668=CARTESIAN_POINT('Ctrl Pts',(-87.0514369526387,-4.11219115716434,
133.502335218899));
#95669=CARTESIAN_POINT('Ctrl Pts',(-87.0591006870272,-4.03794157973197,
133.615504725977));
#95670=CARTESIAN_POINT('Ctrl Pts',(-87.0667644214155,-3.95909577203372,
133.725486269763));
#95671=CARTESIAN_POINT('Ctrl Pts',(-87.0744281558039,-3.87597913792231,
133.831895718088));
#95672=CARTESIAN_POINT('Ctrl Pts',(-87.0821026387063,-3.79274593135937,
133.93845440742));
#95673=CARTESIAN_POINT('Ctrl Pts',(-87.0897771216088,-3.70523020533087,
134.041430700128));
#95674=CARTESIAN_POINT('Ctrl Pts',(-87.0974516045112,-3.61379480714271,
134.140476645879));
#95675=CARTESIAN_POINT('Ctrl Pts',(-87.0995059391258,-3.58931903387138,
134.166989639312));
#95676=CARTESIAN_POINT('Ctrl Pts',(-87.1015602737403,-3.56456258369106,
134.193221227023));
#95677=CARTESIAN_POINT('Ctrl Pts',(-87.1036146083549,-3.53953281040988,
134.219165230795));
#95678=CARTESIAN_POINT('Ctrl Pts',(-87.111388942474,-3.44481123047191,134.317346584641));
#95679=CARTESIAN_POINT('Ctrl Pts',(-87.1191632765931,-3.34585141626337,
134.411739311184));
#95680=CARTESIAN_POINT('Ctrl Pts',(-87.1269376107121,-3.24298872491999,
134.501955402361));
#95681=CARTESIAN_POINT('Ctrl Pts',(-87.1347023636592,-3.14025280265087,
134.592060310268));
#95682=CARTESIAN_POINT('Ctrl Pts',(-87.1424671166063,-3.0336238647186,134.677998569143));
#95683=CARTESIAN_POINT('Ctrl Pts',(-87.1502318695533,-2.92347554829333,
134.759417353067));
#95684=CARTESIAN_POINT('Ctrl Pts',(-87.1579889104383,-2.81343663272846,
134.840755270707));
#95685=CARTESIAN_POINT('Ctrl Pts',(-87.1657459513234,-2.69988560722988,
134.917582415432));
#95686=CARTESIAN_POINT('Ctrl Pts',(-87.1735029922084,-2.58323050042245,
134.989585013484));
#95687=CARTESIAN_POINT('Ctrl Pts',(-87.1812541834485,-2.46666336413866,
135.061533313816));
#95688=CARTESIAN_POINT('Ctrl Pts',(-87.1890053746886,-2.34699713713889,
135.12866410463));
#95689=CARTESIAN_POINT('Ctrl Pts',(-87.1967565659287,-2.22466995720138,
135.190706094615));
#95690=CARTESIAN_POINT('Ctrl Pts',(-87.2045044627058,-2.10239476957835,
135.252721715099));
#95691=CARTESIAN_POINT('Ctrl Pts',(-87.2122523594829,-1.97746122639522,
135.309652660074));
#95692=CARTESIAN_POINT('Ctrl Pts',(-87.22000025626,-1.85033307488721,135.361273012431));
#95693=CARTESIAN_POINT('Ctrl Pts',(-87.2277465323441,-1.72323151584793,
135.412882566924));
#95694=CARTESIAN_POINT('Ctrl Pts',(-87.2354928084281,-1.59393662360072,
135.459183591368));
#95695=CARTESIAN_POINT('Ctrl Pts',(-87.2432390845122,-1.46293281740536,
135.499998022036));
#95696=CARTESIAN_POINT('Ctrl Pts',(-87.2509854177776,-1.33192804416949,
135.540812753987));
#95697=CARTESIAN_POINT('Ctrl Pts',(-87.258731751043,-1.19921470508263,135.576140695054));
#95698=CARTESIAN_POINT('Ctrl Pts',(-87.2664780843084,-1.06529271351499,
135.605853562165));
#95699=CARTESIAN_POINT('Ctrl Pts',(-87.2742261523114,-0.931340731045698,
135.635573083266));
#95700=CARTESIAN_POINT('Ctrl Pts',(-87.2819742203143,-0.796179939105779,
135.659674943551));
#95701=CARTESIAN_POINT('Ctrl Pts',(-87.2897222883173,-0.660320388187454,
135.678081993214));
#95702=CARTESIAN_POINT('Ctrl Pts',(-87.2974785910592,-0.524316444122219,
135.696508606107));
#95703=CARTESIAN_POINT('Ctrl Pts',(-87.305234893801,-0.38761264559977,135.709228265258));
#95704=CARTESIAN_POINT('Ctrl Pts',(-87.3129911965429,-0.250724669979703,
135.716215684887));
#95705=CARTESIAN_POINT('Ctrl Pts',(-87.320751639057,-0.11376363312543,135.723206833912));
#95706=CARTESIAN_POINT('Ctrl Pts',(-87.3285120815712,0.023381385941645,
135.724459643595));
#95707=CARTESIAN_POINT('Ctrl Pts',(-87.3362725240853,0.160195760720989,
135.720001001153));
#95708=CARTESIAN_POINT('Ctrl Pts',(-87.3440454243508,0.297229762080538,
135.715535201302));
#95709=CARTESIAN_POINT('Ctrl Pts',(-87.3518183246162,0.433931668378921,
135.705339656776));
#95710=CARTESIAN_POINT('Ctrl Pts',(-87.3595912248817,0.569792118071048,
135.689493164865));
#95711=CARTESIAN_POINT('Ctrl Pts',(-87.3670815606435,0.700713698202832,
135.674222732851));
#95712=CARTESIAN_POINT('Ctrl Pts',(-87.3745718964054,0.830853633460133,
135.653705120765));
#95713=CARTESIAN_POINT('Ctrl Pts',(-87.3820622321673,0.959767891472947,
135.628055120434));
#95714=CARTESIAN_POINT('Ctrl Pts',(-87.3898365662864,1.09356997276304,135.601432592544));
#95715=CARTESIAN_POINT('Ctrl Pts',(-87.3976109004055,1.22647544375197,135.56919647253));
#95716=CARTESIAN_POINT('Ctrl Pts',(-87.4053852345246,1.35797659354375,135.531419178012));
#95717=CARTESIAN_POINT('Ctrl Pts',(-87.4131499874716,1.48931567992064,135.493688440634));
#95718=CARTESIAN_POINT('Ctrl Pts',(-87.4209147404187,1.61925351651872,135.450430223343));
#95719=CARTESIAN_POINT('Ctrl Pts',(-87.4286794933657,1.74729130088375,135.401768166648));
#95720=CARTESIAN_POINT('Ctrl Pts',(-87.4364365342506,1.87520191631599,135.353154441793));
#95721=CARTESIAN_POINT('Ctrl Pts',(-87.4441935751356,2.00121587195041,135.299147696441));
#95722=CARTESIAN_POINT('Ctrl Pts',(-87.4519506160206,2.12484863159888,135.239921614249));
#95723=CARTESIAN_POINT('Ctrl Pts',(-87.4597018072607,2.24838815882208,135.180740194905));
#95724=CARTESIAN_POINT('Ctrl Pts',(-87.4674529985008,2.36954971308005,135.116347441203));
#95725=CARTESIAN_POINT('Ctrl Pts',(-87.4752041897409,2.48786822513832,135.046965331282));
#95726=CARTESIAN_POINT('Ctrl Pts',(-87.482952086518,2.60613644867287,134.977612710609));
#95727=CARTESIAN_POINT('Ctrl Pts',(-87.490699983295,2.72156369681083,134.903275148803));
#95728=CARTESIAN_POINT('Ctrl Pts',(-87.4984478800721,2.8337092323813,134.82422069583));
#95729=CARTESIAN_POINT('Ctrl Pts',(-87.5061941561562,2.945831309523,134.745182779344));
#95730=CARTESIAN_POINT('Ctrl Pts',(-87.5139404322402,3.05467272016352,134.661430159353));
#95731=CARTESIAN_POINT('Ctrl Pts',(-87.5216867083243,3.15982181380379,134.573274143705));
#95732=CARTESIAN_POINT('Ctrl Pts',(-87.5294330415897,3.26497168363092,134.485117477309));
#95733=CARTESIAN_POINT('Ctrl Pts',(-87.537179374855,3.36642888246945,134.392557601578));
#95734=CARTESIAN_POINT('Ctrl Pts',(-87.5449257081203,3.46381526675065,134.295945767655));
#95735=CARTESIAN_POINT('Ctrl Pts',(-87.5526737761233,3.56122346003751,134.199312298182));
#95736=CARTESIAN_POINT('Ctrl Pts',(-87.5604218441263,3.65455874722492,134.098625340176));
#95737=CARTESIAN_POINT('Ctrl Pts',(-87.5681699121293,3.74348052524587,133.994272312207));
#95738=CARTESIAN_POINT('Ctrl Pts',(-87.5759262148711,3.83249681039056,133.889808376597));
#95739=CARTESIAN_POINT('Ctrl Pts',(-87.583682517613,3.91708996215104,133.781670885714));
#95740=CARTESIAN_POINT('Ctrl Pts',(-87.5914388203548,3.99695997067645,133.670280025943));
#95741=CARTESIAN_POINT('Ctrl Pts',(-87.599199262869,4.07687260823024,133.558829713516));
#95742=CARTESIAN_POINT('Ctrl Pts',(-87.606959705383,4.15205686525745,133.444122899062));
#95743=CARTESIAN_POINT('Ctrl Pts',(-87.6147201478972,4.22225719454089,133.326607085627));
#95744=CARTESIAN_POINT('Ctrl Pts',(-87.6224930481626,4.29257021562499,133.208902625377));
#95745=CARTESIAN_POINT('Ctrl Pts',(-87.630265948428,4.357883134747,133.088380499153));
#95746=CARTESIAN_POINT('Ctrl Pts',(-87.6380388486934,4.41798692394173,132.96551183911));
#95747=CARTESIAN_POINT('Ctrl Pts',(-87.6455291844556,4.47590578900855,132.847109764343));
#95748=CARTESIAN_POINT('Ctrl Pts',(-87.6530195202179,4.52898755472494,132.726529080548));
#95749=CARTESIAN_POINT('Ctrl Pts',(-87.6605098559801,4.57708878836483,132.604205412521));
#95750=CARTESIAN_POINT('Ctrl Pts',(-87.6682841900992,4.62701379489702,132.477243805443));
#95751=CARTESIAN_POINT('Ctrl Pts',(-87.6760585242182,4.67173128762119,132.348002258342));
#95752=CARTESIAN_POINT('Ctrl Pts',(-87.6838328583374,4.71102776339145,132.216947066267));
#95753=CARTESIAN_POINT('Ctrl Pts',(-87.6915976112844,4.75027580976704,132.086053388005));
#95754=CARTESIAN_POINT('Ctrl Pts',(-87.6993623642315,4.78411602101374,131.953350882958));
#95755=CARTESIAN_POINT('Ctrl Pts',(-87.7071271171785,4.81238280448082,131.819326038473));
#95756=CARTESIAN_POINT('Ctrl Pts',(-87.7148841580635,4.84062151298023,131.685434309352));
#95757=CARTESIAN_POINT('Ctrl Pts',(-87.7226411989485,4.86329772964747,131.550223234525));
#95758=CARTESIAN_POINT('Ctrl Pts',(-87.7303982398335,4.8802956758171,131.414194348267));
#95759=CARTESIAN_POINT('Ctrl Pts',(-87.7381494310736,4.89728080370324,131.278268042452));
#95760=CARTESIAN_POINT('Ctrl Pts',(-87.7459006223137,4.90859613592757,131.141525539124));
#95761=CARTESIAN_POINT('Ctrl Pts',(-87.7536518135538,4.91417704770595,131.004478098812));
#95762=CARTESIAN_POINT('Ctrl Pts',(-87.7613997103309,4.91975558744796,130.867488907316));
#95763=CARTESIAN_POINT('Ctrl Pts',(-87.7691476071078,4.9196045384368,130.730195426436));
#95764=CARTESIAN_POINT('Ctrl Pts',(-87.7768955038849,4.91371118949469,130.593113348389));
#95765=CARTESIAN_POINT('Ctrl Pts',(-87.784641779969,4.90781907331414,130.456059944958));
#95766=CARTESIAN_POINT('Ctrl Pts',(-87.7923880560532,4.89618706316837,130.31921824676));
#95767=CARTESIAN_POINT('Ctrl Pts',(-87.8001343321373,4.87885456401745,130.183102856515));
#95768=CARTESIAN_POINT('Ctrl Pts',(-87.8078806654027,4.86152193692189,130.046986461496));
#95769=CARTESIAN_POINT('Ctrl Pts',(-87.8156269986681,4.83848878623959,129.911596772963));
#95770=CARTESIAN_POINT('Ctrl Pts',(-87.8233733319334,4.80984623366961,129.77744179363));
#95771=CARTESIAN_POINT('Ctrl Pts',(-87.8311213999364,4.78119726679885,129.643256771221));
#95772=CARTESIAN_POINT('Ctrl Pts',(-87.8388694679392,4.74693647999147,129.5103073905));
#95773=CARTESIAN_POINT('Ctrl Pts',(-87.8466175359422,4.70720571518489,129.379089619674));
#95774=CARTESIAN_POINT('Ctrl Pts',(-87.854373838684,4.66743272404841,129.247732389039));
#95775=CARTESIAN_POINT('Ctrl Pts',(-87.8621301414259,4.62217825518426,129.118110819433));
#95776=CARTESIAN_POINT('Ctrl Pts',(-87.8698864441678,4.57163366064695,128.990704438645));
#95777=CARTESIAN_POINT('Ctrl Pts',(-87.877646886682,4.52106208893767,128.863230057235));
#95778=CARTESIAN_POINT('Ctrl Pts',(-87.8854073291962,4.46519492467207,128.737973577387));
#95779=CARTESIAN_POINT('Ctrl Pts',(-87.8931677717103,4.40427053532475,128.615391884539));
#95780=CARTESIAN_POINT('Ctrl Pts',(-87.9009406719758,4.34324834473903,128.492613412676));
#95781=CARTESIAN_POINT('Ctrl Pts',(-87.9087135722412,4.27715289472485,128.372518650919));
#95782=CARTESIAN_POINT('Ctrl Pts',(-87.9164864725066,4.20626757738537,128.255538118855));
#95783=CARTESIAN_POINT('Ctrl Pts',(-87.9239768082687,4.13795911987975,128.142810123786));
#95784=CARTESIAN_POINT('Ctrl Pts',(-87.9314671440308,4.06520316654555,128.032974125998));
#95785=CARTESIAN_POINT('Ctrl Pts',(-87.9389574797929,3.98828869196884,127.92638626535));
#95786=CARTESIAN_POINT('Ctrl Pts',(-87.946731813912,3.90845798171169,127.81575709357));
#95787=CARTESIAN_POINT('Ctrl Pts',(-87.9545061480312,3.82389430492806,127.708276787368));
#95788=CARTESIAN_POINT('Ctrl Pts',(-87.9622804821502,3.73487456518304,127.60437701685));
#95789=CARTESIAN_POINT('Ctrl Pts',(-87.9700452350973,3.64596453431157,127.500605293515));
#95790=CARTESIAN_POINT('Ctrl Pts',(-87.9778099880444,3.55260961925711,127.400405619971));
#95791=CARTESIAN_POINT('Ctrl Pts',(-87.9855747409915,3.45512960872882,127.3041802723));
#95792=CARTESIAN_POINT('Ctrl Pts',(-87.9933317818765,3.35774641672068,127.208050497));
#95793=CARTESIAN_POINT('Ctrl Pts',(-88.0010888227616,3.25624655909695,127.115887465035));
#95794=CARTESIAN_POINT('Ctrl Pts',(-88.0088458636466,3.15098940965234,127.028059675803));
#95795=CARTESIAN_POINT('Ctrl Pts',(-88.0165970548867,3.04581163544361,126.940298118191));
#95796=CARTESIAN_POINT('Ctrl Pts',(-88.0243482461268,2.93688250810477,126.856865545554));
#95797=CARTESIAN_POINT('Ctrl Pts',(-88.032099437367,2.82459723432153,126.778092677356));
#95798=CARTESIAN_POINT('Ctrl Pts',(-88.0398473341441,2.71235968477449,126.699353289728));
#95799=CARTESIAN_POINT('Ctrl Pts',(-88.0475952309212,2.59676914527587,126.625269891544));
#95800=CARTESIAN_POINT('Ctrl Pts',(-88.0553431276983,2.47825261159246,126.556131921317));
#95801=CARTESIAN_POINT('Ctrl Pts',(-88.0630894037824,2.35976086901298,126.487008413263));
#95802=CARTESIAN_POINT('Ctrl Pts',(-88.0708356798666,2.23834468714888,126.422828472414));
#95803=CARTESIAN_POINT('Ctrl Pts',(-88.0785819559507,2.11445831518612,126.363837101601));
#95804=CARTESIAN_POINT('Ctrl Pts',(-88.086328289216,1.99057102872246,126.304845295327));
#95805=CARTESIAN_POINT('Ctrl Pts',(-88.0940746224814,1.86421386876416,126.251042303599));
#95806=CARTESIAN_POINT('Ctrl Pts',(-88.1018209557468,1.73586348588816,126.202626051029));
#95807=CARTESIAN_POINT('Ctrl Pts',(-88.1095690237498,1.60748435983365,126.154198955975));
#95808=CARTESIAN_POINT('Ctrl Pts',(-88.1173170917527,1.47711148837441,126.111161138483));
#95809=CARTESIAN_POINT('Ctrl Pts',(-88.1250651597557,1.34523881264115,126.073661345845));
#95810=CARTESIAN_POINT('Ctrl Pts',(-88.1328214624976,1.21322598105863,126.036121697981));
#95811=CARTESIAN_POINT('Ctrl Pts',(-88.1405777652395,1.07971053765166,126.004131939754));
#95812=CARTESIAN_POINT('Ctrl Pts',(-88.1483340679814,0.945199353190114,
125.977790277746));
#95813=CARTESIAN_POINT('Ctrl Pts',(-88.1560945104956,0.810616376059364,
125.9514345564));
#95814=CARTESIAN_POINT('Ctrl Pts',(-88.1638549530098,0.67503698519777,125.930732997019));
#95815=CARTESIAN_POINT('Ctrl Pts',(-88.171615395524,0.53897441470745,125.915732012038));
#95816=CARTESIAN_POINT('Ctrl Pts',(-88.1793882957895,0.402693424499912,
125.900706946143));
#95817=CARTESIAN_POINT('Ctrl Pts',(-88.1871611960548,0.265928094969845,
125.891400767954));
#95818=CARTESIAN_POINT('Ctrl Pts',(-88.1949340963203,0.12919381479039,125.887807758019));
#95819=CARTESIAN_POINT('Ctrl Pts',(-88.2024244320822,-0.00256982988834706,
125.884345363046));
#95820=CARTESIAN_POINT('Ctrl Pts',(-88.2099147678441,-0.134304335479741,
125.886187967444));
#95821=CARTESIAN_POINT('Ctrl Pts',(-88.217405103606,-0.265553873613018,
125.893284951003));
#95822=CARTESIAN_POINT('Ctrl Pts',(-88.2251794377251,-0.401779777880308,
125.90065101885));
#95823=CARTESIAN_POINT('Ctrl Pts',(-88.2329537718442,-0.537914736372974,
125.913701104242));
#95824=CARTESIAN_POINT('Ctrl Pts',(-88.2407281059633,-0.67344589966379,
125.932435568602));
#95825=CARTESIAN_POINT('Ctrl Pts',(-88.2484928589103,-0.808810032907883,
125.951146944409));
#95826=CARTESIAN_POINT('Ctrl Pts',(-88.2562576118575,-0.943571467969517,
125.975528707329));
#95827=CARTESIAN_POINT('Ctrl Pts',(-88.2640223648046,-1.07721890498082,
126.005529250113));
#95828=CARTESIAN_POINT('Ctrl Pts',(-88.2717794056896,-1.21073360147394,
126.035499995935));
#95829=CARTESIAN_POINT('Ctrl Pts',(-88.2795364465746,-1.3431361227756,126.071078330794));
#95830=CARTESIAN_POINT('Ctrl Pts',(-88.2872934874596,-1.47392218959192,
126.112161086266));
#95831=CARTESIAN_POINT('Ctrl Pts',(-88.2950446786997,-1.60460962961841,
126.153212860913));
#95832=CARTESIAN_POINT('Ctrl Pts',(-88.3027958699398,-1.7336826699805,126.199760677313));
#95833=CARTESIAN_POINT('Ctrl Pts',(-88.31054706118,-1.86064944815984,126.251650798836));
#95834=CARTESIAN_POINT('Ctrl Pts',(-88.3182949579571,-1.98756226207099,
126.303518865673));
#95835=CARTESIAN_POINT('Ctrl Pts',(-88.3260428547341,-2.11237023316926,
126.360724573941));
#95836=CARTESIAN_POINT('Ctrl Pts',(-88.3337907515112,-2.23459904699309,
126.423065128595));
#95837=CARTESIAN_POINT('Ctrl Pts',(-88.3415370275953,-2.35680229318368,
126.485392642949));
#95838=CARTESIAN_POINT('Ctrl Pts',(-88.3492833036794,-2.47642710714252,
126.552852689725));
#95839=CARTESIAN_POINT('Ctrl Pts',(-88.3570295797635,-2.59302182826836,
126.625195526232));
#95840=CARTESIAN_POINT('Ctrl Pts',(-88.3647759130289,-2.70961741007011,
126.697538896758));
#95841=CARTESIAN_POINT('Ctrl Pts',(-88.3725222462942,-2.8231825221929,126.774764922812));
#95842=CARTESIAN_POINT('Ctrl Pts',(-88.3802685795596,-2.93329300377644,
126.85657956785));
#95843=CARTESIAN_POINT('Ctrl Pts',(-88.3880166475625,-3.04342814383873,
126.938412534711));
#95844=CARTESIAN_POINT('Ctrl Pts',(-88.3957647155655,-3.15010680014675,
127.024835932209));
#95845=CARTESIAN_POINT('Ctrl Pts',(-88.4035127835685,-3.25293684014523,
127.115514595227));
#95846=CARTESIAN_POINT('Ctrl Pts',(-88.4112690863104,-3.35587616913378,
127.206289632607));
#95847=CARTESIAN_POINT('Ctrl Pts',(-88.4190253890522,-3.45495841718359,
127.301328710784));
#95848=CARTESIAN_POINT('Ctrl Pts',(-88.426781691794,-3.54982698428493,127.400258468079));
#95849=CARTESIAN_POINT('Ctrl Pts',(-88.4345421343082,-3.64474618559723,
127.499241027165));
#95850=CARTESIAN_POINT('Ctrl Pts',(-88.4423025768223,-3.73544696627377,
127.602118109995));
#95851=CARTESIAN_POINT('Ctrl Pts',(-88.4500630193365,-3.82161286265189,
127.708483005238));
#95852=CARTESIAN_POINT('Ctrl Pts',(-88.457835919602,-3.90791708017656,127.815018646854));
#95853=CARTESIAN_POINT('Ctrl Pts',(-88.4656088198673,-3.9896716327417,127.925052975355));
#95854=CARTESIAN_POINT('Ctrl Pts',(-88.4733817201328,-4.06660275211667,
128.038149288152));
#95855=CARTESIAN_POINT('Ctrl Pts',(-88.4808720558949,-4.1407372315256,128.147134265108));
#95856=CARTESIAN_POINT('Ctrl Pts',(-88.4883623916571,-4.21039271432896,
128.258962208267));
#95857=CARTESIAN_POINT('Ctrl Pts',(-88.4958527274192,-4.27536540237552,
128.37322225485));
#95858=CARTESIAN_POINT('Ctrl Pts',(-88.5039673523599,-4.3457533010789,128.497005413998));
#95859=CARTESIAN_POINT('Ctrl Pts',(-88.5120819773005,-4.41085202937009,
128.624006454679));
#95860=CARTESIAN_POINT('Ctrl Pts',(-88.5201966022411,-4.47036889127372,
128.753754600206));
#95861=CARTESIAN_POINT('Ctrl Pts',(-88.5285188075131,-4.53140825483455,
128.886821834817));
#95862=CARTESIAN_POINT('Ctrl Pts',(-88.5368410127851,-4.58657609156948,
129.022778347369));
#95863=CARTESIAN_POINT('Ctrl Pts',(-88.5451632180572,-4.63560448481789,
129.161085192436));
#95864=CARTESIAN_POINT('Ctrl Pts',(-88.5534854233292,-4.68463287806617,
129.299392037503));
#95865=CARTESIAN_POINT('Ctrl Pts',(-88.5618076286012,-4.72752162291951,
129.440048875951));
#95866=CARTESIAN_POINT('Ctrl Pts',(-88.5701298338733,-4.76405452823397,
129.582490119308));
#95867=CARTESIAN_POINT('Origin',(213.235140564004,0.,130.804360617566));
#95868=CARTESIAN_POINT('',(-90.6650630979317,-4.76405452823406,129.582490119308));
#95869=CARTESIAN_POINT('',(-90.3197845579208,-4.76405452823393,129.582490119308));
#95870=CARTESIAN_POINT('',(213.235140564004,-4.76405452823405,129.582490119308));
#95871=CARTESIAN_POINT('',(-88.98514056396,-4.91824826917725,130.808486782246));
#95872=CARTESIAN_POINT('Ctrl Pts',(-88.985140564009,-4.91824826917653,130.808486783108));
#95873=CARTESIAN_POINT('Ctrl Pts',(-88.9972482442412,-4.9180693451276,131.021758132721));
#95874=CARTESIAN_POINT('Ctrl Pts',(-89.0093559244733,-4.90401532505547,
131.234467650703));
#95875=CARTESIAN_POINT('Ctrl Pts',(-89.0214636047054,-4.87632108299787,
131.445200502413));
#95876=CARTESIAN_POINT('Ctrl Pts',(-89.0253620627651,-4.86740402877369,
131.513052739048));
#95877=CARTESIAN_POINT('Ctrl Pts',(-89.0292605208248,-4.85707316178395,
131.580700345055));
#95878=CARTESIAN_POINT('Ctrl Pts',(-89.0331589788845,-4.84533718105517,
131.648096751902));
#95879=CARTESIAN_POINT('Ctrl Pts',(-89.0409333130037,-4.82193320081409,
131.782499168762));
#95880=CARTESIAN_POINT('Ctrl Pts',(-89.0487076471227,-4.79289572884961,
131.916139944255));
#95881=CARTESIAN_POINT('Ctrl Pts',(-89.0564819812418,-4.75828497826597,
132.04850977587));
#95882=CARTESIAN_POINT('Ctrl Pts',(-89.0642467341889,-4.72371688233916,
132.180716473498));
#95883=CARTESIAN_POINT('Ctrl Pts',(-89.072011487136,-4.68358927214729,132.311654969149));
#95884=CARTESIAN_POINT('Ctrl Pts',(-89.0797762400831,-4.63801378270779,
132.440823636981));
#95885=CARTESIAN_POINT('Ctrl Pts',(-89.0875332809681,-4.5924835594869,132.569864012671));
#95886=CARTESIAN_POINT('Ctrl Pts',(-89.0952903218531,-4.54151635421954,
132.697137692376));
#95887=CARTESIAN_POINT('Ctrl Pts',(-89.1030473627381,-4.48527417301372,
132.822156111514));
#95888=CARTESIAN_POINT('Ctrl Pts',(-89.1107985539783,-4.42907440447432,
132.947080253289));
#95889=CARTESIAN_POINT('Ctrl Pts',(-89.1185497452184,-4.36760773751705,
133.069752164552));
#95890=CARTESIAN_POINT('Ctrl Pts',(-89.1263009364585,-4.30108492597971,
133.189701583133));
#95891=CARTESIAN_POINT('Ctrl Pts',(-89.1340488332356,-4.23459038841173,
133.309600020011));
#95892=CARTESIAN_POINT('Ctrl Pts',(-89.1417967300127,-4.16304416967384,
133.426777924466));
#95893=CARTESIAN_POINT('Ctrl Pts',(-89.1495446267898,-4.08670366606434,
133.540788253787));
#95894=CARTESIAN_POINT('Ctrl Pts',(-89.1572909028739,-4.01037913124248,
133.654774734606));
#95895=CARTESIAN_POINT('Ctrl Pts',(-89.165037178958,-3.92926252368292,133.765594633558));
#95896=CARTESIAN_POINT('Ctrl Pts',(-89.1727834550421,-3.84365518310861,
133.872828948161));
#95897=CARTESIAN_POINT('Ctrl Pts',(-89.1805297883074,-3.75804721060048,
133.980064054342));
#95898=CARTESIAN_POINT('Ctrl Pts',(-89.1882761215728,-3.66794868285102,
134.083713217816));
#95899=CARTESIAN_POINT('Ctrl Pts',(-89.1960224548381,-3.57370167544866,
134.183389974851));
#95900=CARTESIAN_POINT('Ctrl Pts',(-89.2037705228411,-3.47943356208258,
134.283089053805));
#95901=CARTESIAN_POINT('Ctrl Pts',(-89.2115185908439,-3.38101538897182,
134.378813672103));
#95902=CARTESIAN_POINT('Ctrl Pts',(-89.2192666588469,-3.27882628958447,
134.470214027787));
#95903=CARTESIAN_POINT('Ctrl Pts',(-89.2270229615887,-3.17652858240609,
134.561711524857));
#95904=CARTESIAN_POINT('Ctrl Pts',(-89.2347792643307,-3.07045223484165,
134.648875317493));
#95905=CARTESIAN_POINT('Ctrl Pts',(-89.2425355670725,-2.9610101128649,134.731395398926));
#95906=CARTESIAN_POINT('Ctrl Pts',(-89.2502960095867,-2.85150957833211,
134.813959523811));
#95907=CARTESIAN_POINT('Ctrl Pts',(-89.2580564521008,-2.73864001146899,
134.891874776896));
#95908=CARTESIAN_POINT('Ctrl Pts',(-89.265816894615,-2.62284265402436,134.964874945715));
#95909=CARTESIAN_POINT('Ctrl Pts',(-89.2735897948804,-2.50685940838154,
135.037992300885));
#95910=CARTESIAN_POINT('Ctrl Pts',(-89.281362695146,-2.38793931952346,135.106178610214));
#95911=CARTESIAN_POINT('Ctrl Pts',(-89.2891355954114,-2.26654836783466,
135.169213600058));
#95912=CARTESIAN_POINT('Ctrl Pts',(-89.2966259311736,-2.14957028300346,
135.229957109246));
#95913=CARTESIAN_POINT('Ctrl Pts',(-89.3041162669356,-2.03029813948232,
135.285917192658));
#95914=CARTESIAN_POINT('Ctrl Pts',(-89.3116066026978,-1.90916399462772,
135.33694000508));
#95915=CARTESIAN_POINT('Ctrl Pts',(-89.3193809368168,-1.78343701185497,
135.389897362942));
#95916=CARTESIAN_POINT('Ctrl Pts',(-89.3271552709359,-1.65530577965287,
135.437703418906));
#95917=CARTESIAN_POINT('Ctrl Pts',(-89.334929605055,-1.52523133530176,135.480133541513));
#95918=CARTESIAN_POINT('Ctrl Pts',(-89.3426943580021,-1.39531719607823,
135.522511372786));
#95919=CARTESIAN_POINT('Ctrl Pts',(-89.3504591109492,-1.26346497783599,
135.559526333108));
#95920=CARTESIAN_POINT('Ctrl Pts',(-89.3582238638963,-1.13015705405705,
135.591001203161));
#95921=CARTESIAN_POINT('Ctrl Pts',(-89.3659809047813,-0.996981533586957,
135.622444811929));
#95922=CARTESIAN_POINT('Ctrl Pts',(-89.3737379456663,-0.862353562882643,
135.648359191384));
#95923=CARTESIAN_POINT('Ctrl Pts',(-89.3814949865514,-0.726771753422879,
135.668616560763));
#95924=CARTESIAN_POINT('Ctrl Pts',(-89.3892461777915,-0.591292187260485,
135.688858653902));
#95925=CARTESIAN_POINT('Ctrl Pts',(-89.3969973690316,-0.454860599168647,
135.703452170629));
#95926=CARTESIAN_POINT('Ctrl Pts',(-89.4047485602717,-0.317986551626253,
135.712320235929));
#95927=CARTESIAN_POINT('Ctrl Pts',(-89.4124964570488,-0.181170679205113,
135.721184532065));
#95928=CARTESIAN_POINT('Ctrl Pts',(-89.420244353826,-0.0439131106949756,
135.724328191534));
#95929=CARTESIAN_POINT('Ctrl Pts',(-89.4279922506031,0.0932709152251658,
135.721726131627));
#95930=CARTESIAN_POINT('Ctrl Pts',(-89.4357385266872,0.23042624520443,135.719124616015));
#95931=CARTESIAN_POINT('Ctrl Pts',(-89.4434848027712,0.36750767254513,135.710779779043));
#95932=CARTESIAN_POINT('Ctrl Pts',(-89.4512310788553,0.503999797109908,
135.696718665278));
#95933=CARTESIAN_POINT('Ctrl Pts',(-89.4589774121207,0.640492929228357,
135.682657447717));
#95934=CARTESIAN_POINT('Ctrl Pts',(-89.4667237453861,0.776396360983598,
135.662879909228));
#95935=CARTESIAN_POINT('Ctrl Pts',(-89.4744700786514,0.911200049281774,
135.637464954603));
#95936=CARTESIAN_POINT('Ctrl Pts',(-89.4822181466544,1.04603392593147,135.612044308476));
#95937=CARTESIAN_POINT('Ctrl Pts',(-89.4899662146574,1.17976718493234,135.580983806484));
#95938=CARTESIAN_POINT('Ctrl Pts',(-89.4977142826604,1.31190059708888,135.544413347848));
#95939=CARTESIAN_POINT('Ctrl Pts',(-89.5054705854023,1.44417444220809,135.507804021694));
#95940=CARTESIAN_POINT('Ctrl Pts',(-89.5132268881441,1.57484466647749,135.465673145264));
#95941=CARTESIAN_POINT('Ctrl Pts',(-89.520983190886,1.70342728827788,135.418200508162));
#95942=CARTESIAN_POINT('Ctrl Pts',(-89.5287436334001,1.83207853849507,135.370702533484));
#95943=CARTESIAN_POINT('Ctrl Pts',(-89.5365040759143,1.95863960547145,135.317857267727));
#95944=CARTESIAN_POINT('Ctrl Pts',(-89.5442645184285,2.08264801517743,135.259892045732));
#95945=CARTESIAN_POINT('Ctrl Pts',(-89.5520374186939,2.20685549419162,135.201833772817));
#95946=CARTESIAN_POINT('Ctrl Pts',(-89.5598103189593,2.32850178017859,135.138639299804));
#95947=CARTESIAN_POINT('Ctrl Pts',(-89.5675832192248,2.44714967690405,135.070581605903));
#95948=CARTESIAN_POINT('Ctrl Pts',(-89.5750735549867,2.56148442372623,135.004997980603));
#95949=CARTESIAN_POINT('Ctrl Pts',(-89.5825638907487,2.67303473372726,134.934898740284));
#95950=CARTESIAN_POINT('Ctrl Pts',(-89.5900542265106,2.78143763501597,134.860564229938));
#95951=CARTESIAN_POINT('Ctrl Pts',(-89.5978285606297,2.89395066525651,134.783411304038));
#95952=CARTESIAN_POINT('Ctrl Pts',(-89.6056028947488,3.00342931486091,134.701451210497));
#95953=CARTESIAN_POINT('Ctrl Pts',(-89.6133772288678,3.10943539311046,134.614950414247));
#95954=CARTESIAN_POINT('Ctrl Pts',(-89.6211419818149,3.21531082834259,134.528556222498));
#95955=CARTESIAN_POINT('Ctrl Pts',(-89.6289067347621,3.31772190740933,134.437632707237));
#95956=CARTESIAN_POINT('Ctrl Pts',(-89.6366714877092,3.41625879602881,134.342489911565));
#95957=CARTESIAN_POINT('Ctrl Pts',(-89.6444285285941,3.51469781642138,134.247441613059));
#95958=CARTESIAN_POINT('Ctrl Pts',(-89.6521855694791,3.60927002442683,134.148182643533));
#95959=CARTESIAN_POINT('Ctrl Pts',(-89.6599426103641,3.69959840278609,134.045063430322));
#95960=CARTESIAN_POINT('Ctrl Pts',(-89.6676938016043,3.7898586638127,133.942021980111));
#95961=CARTESIAN_POINT('Ctrl Pts',(-89.6754449928444,3.87588120863602,133.835126373364));
#95962=CARTESIAN_POINT('Ctrl Pts',(-89.6831961840846,3.95732592916066,133.724763766601));
#95963=CARTESIAN_POINT('Ctrl Pts',(-89.6909440808617,4.03873603350658,133.61444806689));
#95964=CARTESIAN_POINT('Ctrl Pts',(-89.6986919776387,4.11557195173285,133.500668611897));
#95965=CARTESIAN_POINT('Ctrl Pts',(-89.7064398744158,4.18753408195496,133.383845328698));
#95966=CARTESIAN_POINT('Ctrl Pts',(-89.7141861504999,4.25948115925054,133.267046482412));
#95967=CARTESIAN_POINT('Ctrl Pts',(-89.7219324265841,4.32655627144583,133.147205407026));
#95968=CARTESIAN_POINT('Ctrl Pts',(-89.7296787026682,4.38850358553658,133.024770341521));
#95969=CARTESIAN_POINT('Ctrl Pts',(-89.7374250359335,4.45045135690841,132.902334372227));
#95970=CARTESIAN_POINT('Ctrl Pts',(-89.7451713691989,4.50727107813781,132.777304723459));
#95971=CARTESIAN_POINT('Ctrl Pts',(-89.7529177024643,4.55875344331177,132.650153158886));
#95972=CARTESIAN_POINT('Ctrl Pts',(-89.7606657704672,4.61024733760439,132.522973119602));
#95973=CARTESIAN_POINT('Ctrl Pts',(-89.7684138384702,4.65640135070579,132.39367058126));
#95974=CARTESIAN_POINT('Ctrl Pts',(-89.7761619064732,4.69705492493503,132.262735773225));
#95975=CARTESIAN_POINT('Ctrl Pts',(-89.783918209215,4.7377517062668,132.131661806117));
#95976=CARTESIAN_POINT('Ctrl Pts',(-89.7916745119568,4.77293625473262,131.998952477852));
#95977=CARTESIAN_POINT('Ctrl Pts',(-89.7994308146987,4.80249822853209,131.865112156545));
#95978=CARTESIAN_POINT('Ctrl Pts',(-89.8071912572129,4.83207598044706,131.731200400629));
#95979=CARTESIAN_POINT('Ctrl Pts',(-89.8149516997271,4.85602510983729,131.596156833627));
#95980=CARTESIAN_POINT('Ctrl Pts',(-89.8227121422413,4.87428690143246,131.460493428073));
#95981=CARTESIAN_POINT('Ctrl Pts',(-89.8304850425067,4.89257800847671,131.324612243577));
#95982=CARTESIAN_POINT('Ctrl Pts',(-89.8382579427722,4.90516349752205,131.1881096217));
#95983=CARTESIAN_POINT('Ctrl Pts',(-89.8460308430376,4.91203671846552,131.051500939947));
#95984=CARTESIAN_POINT('Ctrl Pts',(-89.8535211787996,4.91866008051508,130.919858327872));
#95985=CARTESIAN_POINT('Ctrl Pts',(-89.8610115145615,4.91997927164379,130.788117541136));
#95986=CARTESIAN_POINT('Ctrl Pts',(-89.8685018503236,4.91603395886155,130.656735491588));
#95987=CARTESIAN_POINT('Ctrl Pts',(-89.8762761844426,4.91193905834601,130.520372051698));
#95988=CARTESIAN_POINT('Ctrl Pts',(-89.8840505185617,4.90215959469573,130.383963130644));
#95989=CARTESIAN_POINT('Ctrl Pts',(-89.8918248526808,4.88668289961727,130.248021421492));
#95990=CARTESIAN_POINT('Ctrl Pts',(-89.8995896056279,4.87122527818231,130.112247248347));
#95991=CARTESIAN_POINT('Ctrl Pts',(-89.907354358575,4.85008443947064,129.976939526167));
#95992=CARTESIAN_POINT('Ctrl Pts',(-89.9151191115221,4.82329970608404,129.842610646009));
#95993=CARTESIAN_POINT('Ctrl Pts',(-89.9228761524071,4.79654157567223,129.708415183189));
#95994=CARTESIAN_POINT('Ctrl Pts',(-89.9306331932921,4.76415078193144,129.575197008606));
#95995=CARTESIAN_POINT('Ctrl Pts',(-89.9383902341771,4.72621836226506,129.443462732092));
#95996=CARTESIAN_POINT('Ctrl Pts',(-89.9461414254172,4.68831454773138,129.31182779742));
#95997=CARTESIAN_POINT('Ctrl Pts',(-89.9538926166574,4.64487753302853,129.181674907658));
#95998=CARTESIAN_POINT('Ctrl Pts',(-89.9616438078975,4.59604920716909,129.053499472935));
#95999=CARTESIAN_POINT('Ctrl Pts',(-89.9693917046746,4.54724163465076,128.92537851619));
#96000=CARTESIAN_POINT('Ctrl Pts',(-89.9771396014517,4.49304744738668,128.799233707439));
#96001=CARTESIAN_POINT('Ctrl Pts',(-89.9848874982287,4.43365799978234,128.675544091074));
#96002=CARTESIAN_POINT('Ctrl Pts',(-89.9926337743128,4.37428097517015,128.55188034791));
#96003=CARTESIAN_POINT('Ctrl Pts',(-90.0003800503969,4.30971102091436,128.430671127827));
#96004=CARTESIAN_POINT('Ctrl Pts',(-90.0081263264809,4.24018696917661,128.312373954495));
#96005=CARTESIAN_POINT('Ctrl Pts',(-90.0158726597463,4.17066240422801,128.19407590792));
#96006=CARTESIAN_POINT('Ctrl Pts',(-90.0236189930117,4.09618386691946,128.078690288053));
#96007=CARTESIAN_POINT('Ctrl Pts',(-90.0313653262771,4.0170351304277,127.966648189675));
#96008=CARTESIAN_POINT('Ctrl Pts',(-90.0391133942801,3.93786866912529,127.854581000245));
#96009=CARTESIAN_POINT('Ctrl Pts',(-90.046861462283,3.85403015303628,127.745859141509));
#96010=CARTESIAN_POINT('Ctrl Pts',(-90.054609530286,3.7658452406594,127.640882676138));
#96011=CARTESIAN_POINT('Ctrl Pts',(-90.0623658330278,3.67756660430836,127.53579464053));
#96012=CARTESIAN_POINT('Ctrl Pts',(-90.0701221357696,3.58493259579151,127.434460249894));
#96013=CARTESIAN_POINT('Ctrl Pts',(-90.0778784385115,3.48830791185131,127.3372449612));
#96014=CARTESIAN_POINT('Ctrl Pts',(-90.0856388810256,3.39163165640772,127.23997778578));
#96015=CARTESIAN_POINT('Ctrl Pts',(-90.0933993235398,3.29096076828217,127.146834358362));
#96016=CARTESIAN_POINT('Ctrl Pts',(-90.101159766054,3.18669424742868,127.058140811427));
#96017=CARTESIAN_POINT('Ctrl Pts',(-90.1089326663194,3.08226034869956,126.969304885737));
#96018=CARTESIAN_POINT('Ctrl Pts',(-90.1167055665849,2.9742195912059,126.884933355977));
#96019=CARTESIAN_POINT('Ctrl Pts',(-90.1244784668503,2.86300198209583,126.805310391198));
#96020=CARTESIAN_POINT('Ctrl Pts',(-90.1319688026124,2.75582741321686,126.728581921746));
#96021=CARTESIAN_POINT('Ctrl Pts',(-90.1394591383744,2.64570321327045,126.656262935709));
#96022=CARTESIAN_POINT('Ctrl Pts',(-90.1469494741364,2.53303523612335,126.588567032124));
#96023=CARTESIAN_POINT('Ctrl Pts',(-90.1547238082555,2.41609541837882,126.518304417778));
#96024=CARTESIAN_POINT('Ctrl Pts',(-90.1624981423746,2.29604469081544,126.452799803714));
#96025=CARTESIAN_POINT('Ctrl Pts',(-90.1702724764937,2.17330754910786,126.392340971249));
#96026=CARTESIAN_POINT('Ctrl Pts',(-90.1780372294408,2.0507216699581,126.331956648891));
#96027=CARTESIAN_POINT('Ctrl Pts',(-90.1858019823878,1.92545631145703,126.276605906326));
#96028=CARTESIAN_POINT('Ctrl Pts',(-90.1935667353348,1.79796381754005,126.226532620217));
#96029=CARTESIAN_POINT('Ctrl Pts',(-90.2013237762198,1.67059795096502,126.176509067601));
#96030=CARTESIAN_POINT('Ctrl Pts',(-90.2090808171048,1.54100971254757,126.131752682333));
#96031=CARTESIAN_POINT('Ctrl Pts',(-90.2168378579898,1.40967453542727,126.092460707056));
#96032=CARTESIAN_POINT('Ctrl Pts',(-90.2245890492299,1.27843839918586,126.053198362163));
#96033=CARTESIAN_POINT('Ctrl Pts',(-90.2323402404701,1.14545831945303,126.019392336755));
#96034=CARTESIAN_POINT('Ctrl Pts',(-90.2400914317102,1.01122779327843,125.991191036863));
#96035=CARTESIAN_POINT('Ctrl Pts',(-90.2478393284873,0.877054318657992,
125.963001723277));
#96036=CARTESIAN_POINT('Ctrl Pts',(-90.2555872252643,0.741631836466278,
125.940412477493));
#96037=CARTESIAN_POINT('Ctrl Pts',(-90.2633351220414,0.605466812048298,
125.923521242826));
#96038=CARTESIAN_POINT('Ctrl Pts',(-90.2710813981255,0.469330270418419,
125.906633541442));
#96039=CARTESIAN_POINT('Ctrl Pts',(-90.2788276742095,0.332451883255404,
125.895441528519));
#96040=CARTESIAN_POINT('Ctrl Pts',(-90.2865739502936,0.195345672797809,
125.889991570514));
#96041=CARTESIAN_POINT('Ctrl Pts',(-90.2943202835589,0.0582384502531272,
125.884541572279));
#96042=CARTESIAN_POINT('Ctrl Pts',(-90.3020666168243,-0.0790962082852262,
125.88483372907));
#96043=CARTESIAN_POINT('Ctrl Pts',(-90.3098129500896,-0.216142224237108,
125.890862311735));
#96044=CARTESIAN_POINT('Ctrl Pts',(-90.3175610180925,-0.353218930693866,
125.896892244459));
#96045=CARTESIAN_POINT('Ctrl Pts',(-90.3253090860955,-0.490006475426297,
125.90866114215));
#96046=CARTESIAN_POINT('Ctrl Pts',(-90.3330571540984,-0.625992248007013,
125.926111262732));
#96047=CARTESIAN_POINT('Ctrl Pts',(-90.3408134568403,-0.762122547885265,
125.943579929511));
#96048=CARTESIAN_POINT('Ctrl Pts',(-90.3485697595821,-0.897448984980592,
125.966741831039));
#96049=CARTESIAN_POINT('Ctrl Pts',(-90.356326062324,-1.03146696249758,125.995487676036));
#96050=CARTESIAN_POINT('Ctrl Pts',(-90.3640865048381,-1.16555646944436,
126.024248863557));
#96051=CARTESIAN_POINT('Ctrl Pts',(-90.3718469473523,-1.29833574694426,
126.05859983521));
#96052=CARTESIAN_POINT('Ctrl Pts',(-90.3796073898664,-1.42931474128445,
126.098381183607));
#96053=CARTESIAN_POINT('Ctrl Pts',(-90.3873802901318,-1.56050399473413,
126.138226392555));
#96054=CARTESIAN_POINT('Ctrl Pts',(-90.3951531903973,-1.68988682071423,
126.183519268983));
#96055=CARTESIAN_POINT('Ctrl Pts',(-90.4029260906627,-1.81699171038766,
126.234051636011));
#96056=CARTESIAN_POINT('Ctrl Pts',(-90.4104164264249,-1.939476017167,126.282747024215));
#96057=CARTESIAN_POINT('Ctrl Pts',(-90.4179067621871,-2.05984484830673,
126.336307454068));
#96058=CARTESIAN_POINT('Ctrl Pts',(-90.4253970979493,-2.17769912295971,
126.394506924714));
#96059=CARTESIAN_POINT('Ctrl Pts',(-90.4331721961499,-2.30003390044828,
126.454918982846));
#96060=CARTESIAN_POINT('Ctrl Pts',(-90.4409472943505,-2.4200467036457,126.520521173735));
#96061=CARTESIAN_POINT('Ctrl Pts',(-90.448722392551,-2.53726582552732,126.591111848135));
#96062=CARTESIAN_POINT('Ctrl Pts',(-90.4564877390489,-2.65433792855479,
126.661613986126));
#96063=CARTESIAN_POINT('Ctrl Pts',(-90.4642530855467,-2.76862299067614,
126.73709195787));
#96064=CARTESIAN_POINT('Ctrl Pts',(-90.4720184320446,-2.87967122861419,
126.817296951459));
#96065=CARTESIAN_POINT('Ctrl Pts',(-90.4800619597899,-2.99469759391117,
126.900375161996));
#96066=CARTESIAN_POINT('Ctrl Pts',(-90.4881054875353,-3.10625051128023,
126.988525230945));
#96067=CARTESIAN_POINT('Ctrl Pts',(-90.4961490152806,-3.21385903343552,
127.081419149358));
#96068=CARTESIAN_POINT('Ctrl Pts',(-90.5038997764408,-3.31755084385011,
127.170931934998));
#96069=CARTESIAN_POINT('Ctrl Pts',(-90.511650537601,-3.41758002234671,127.264849021001));
#96070=CARTESIAN_POINT('Ctrl Pts',(-90.5194012987613,-3.51355624691792,
127.362833985061));
#96071=CARTESIAN_POINT('Ctrl Pts',(-90.5271485806756,-3.60948938863803,
127.460774964565));
#96072=CARTESIAN_POINT('Ctrl Pts',(-90.5348958625898,-3.70137292352647,
127.562779910086));
#96073=CARTESIAN_POINT('Ctrl Pts',(-90.5426431445041,-3.78885215464494,
127.668474393108));
#96074=CARTESIAN_POINT('Ctrl Pts',(-90.5503886264776,-3.87631106154699,
127.77414431993));
#96075=CARTESIAN_POINT('Ctrl Pts',(-90.5581341084511,-3.95936745262888,
127.883501776978));
#96076=CARTESIAN_POINT('Ctrl Pts',(-90.5658795904246,-4.03770609206386,
127.996138301472));
#96077=CARTESIAN_POINT('Ctrl Pts',(-90.5736249501833,-4.11604349540499,
128.10877304869));
#96078=CARTESIAN_POINT('Ctrl Pts',(-90.581370309942,-4.1896630736576,128.224686438558));
#96079=CARTESIAN_POINT('Ctrl Pts',(-90.5891156697007,-4.25829243351487,
128.343440339871));
#96080=CARTESIAN_POINT('Ctrl Pts',(-90.596865332462,-4.32695992101522,128.462260215956));
#96081=CARTESIAN_POINT('Ctrl Pts',(-90.6046149952232,-4.39063145769388,
128.583923416421));
#96082=CARTESIAN_POINT('Ctrl Pts',(-90.6123646579845,-4.44908014600279,
128.707966351941));
#96083=CARTESIAN_POINT('Ctrl Pts',(-90.6201169107451,-4.50754836833084,
128.832050743602));
#96084=CARTESIAN_POINT('Ctrl Pts',(-90.6278691635057,-4.5607901095426,128.958516096289));
#96085=CARTESIAN_POINT('Ctrl Pts',(-90.6356214162662,-4.6086266685323,129.086878945875));
#96086=CARTESIAN_POINT('Ctrl Pts',(-90.6433808915753,-4.65650779545359,
129.215361387398));
#96087=CARTESIAN_POINT('Ctrl Pts',(-90.6511403668844,-4.69897356303453,
129.345744484816));
#96088=CARTESIAN_POINT('Ctrl Pts',(-90.6588998421936,-4.73589510125555,
129.4775295611));
#96089=CARTESIAN_POINT('Ctrl Pts',(-90.6609542607729,-4.74567054238756,
129.512421315814));
#96090=CARTESIAN_POINT('Ctrl Pts',(-90.6630086793523,-4.75505761478963,
129.547411290336));
#96091=CARTESIAN_POINT('Ctrl Pts',(-90.6650630979317,-4.76405452823406,
129.582490119308));
#96092=CARTESIAN_POINT('Ctrl Pts',(-88.9150399778173,-4.76405452823403,
129.582490119308));
#96093=CARTESIAN_POINT('Ctrl Pts',(-88.9226765403677,-4.7976634032,129.713530612715));
#96094=CARTESIAN_POINT('Ctrl Pts',(-88.9303131029181,-4.82584657930655,
129.84590081179));
#96095=CARTESIAN_POINT('Ctrl Pts',(-88.9379496654685,-4.84851894198989,
129.979104819849));
#96096=CARTESIAN_POINT('Ctrl Pts',(-88.9458148152171,-4.87186996235847,
130.116296057869));
#96097=CARTESIAN_POINT('Ctrl Pts',(-88.9536799649657,-4.889375011302,130.254371347012));
#96098=CARTESIAN_POINT('Ctrl Pts',(-88.9615451147143,-4.9009986377072,130.392783874185));
#96099=CARTESIAN_POINT('Ctrl Pts',(-88.9694102644628,-4.91262226411238,
130.531196401358));
#96100=CARTESIAN_POINT('Ctrl Pts',(-88.9772754142115,-4.91836449822501,
130.669945701738));
#96101=CARTESIAN_POINT('Ctrl Pts',(-88.9851405639601,-4.91824826917725,
130.808486782245));
#96102=CARTESIAN_POINT('',(-88.6398594360367,-4.91824997771658,130.804828795773));
#96103=CARTESIAN_POINT('Ctrl Pts',(-88.5701298338733,-4.76405452823397,
129.582490119308));
#96104=CARTESIAN_POINT('Ctrl Pts',(-88.5782041209728,-4.79949911971491,
129.720688043545));
#96105=CARTESIAN_POINT('Ctrl Pts',(-88.5862784080723,-4.8289610107534,129.860565217491));
#96106=CARTESIAN_POINT('Ctrl Pts',(-88.5943526951718,-4.85229179860094,
130.001585827397));
#96107=CARTESIAN_POINT('Ctrl Pts',(-88.6024145699402,-4.87558672080988,
130.142389651045));
#96108=CARTESIAN_POINT('Ctrl Pts',(-88.6104764447087,-4.89276927693621,
130.28433306948));
#96109=CARTESIAN_POINT('Ctrl Pts',(-88.6185383194771,-4.90374172190632,
130.426868647671));
#96110=CARTESIAN_POINT('Ctrl Pts',(-88.6256453583152,-4.91341460753055,
130.552522533289));
#96111=CARTESIAN_POINT('Ctrl Pts',(-88.6327523971533,-4.91826199021932,
130.678636265036));
#96112=CARTESIAN_POINT('Ctrl Pts',(-88.6398594359915,-4.91824997771666,
130.804828794969));
#96113=CARTESIAN_POINT('Ctrl Pts',(-88.6398594360368,-4.91824997771658,
130.804828795773));
#96114=CARTESIAN_POINT('Ctrl Pts',(-88.6480343427133,-4.91823616025208,
130.949982379278));
#96115=CARTESIAN_POINT('Ctrl Pts',(-88.6562092493898,-4.91179212857453,
131.094992640823));
#96116=CARTESIAN_POINT('Ctrl Pts',(-88.6643841560662,-4.89898148010898,
131.239289945215));
#96117=CARTESIAN_POINT('Ctrl Pts',(-88.6725720466721,-4.88615048492125,
131.383816432164));
#96118=CARTESIAN_POINT('Ctrl Pts',(-88.6807599372779,-4.86693271592382,
131.527627381295));
#96119=CARTESIAN_POINT('Ctrl Pts',(-88.6889478278838,-4.84144309063563,
131.670161901139));
#96120=CARTESIAN_POINT('Ctrl Pts',(-88.6971571696266,-4.81588668606677,
131.813069841643));
#96121=CARTESIAN_POINT('Ctrl Pts',(-88.7053665113696,-4.78402562367715,
131.95469434762));
#96122=CARTESIAN_POINT('Ctrl Pts',(-88.7135758531125,-4.74602557556677,
132.094486308561));
#96123=CARTESIAN_POINT('Ctrl Pts',(-88.7217967973305,-4.70797182100498,
132.234475841098));
#96124=CARTESIAN_POINT('Ctrl Pts',(-88.7300177415486,-4.66376185868199,
132.372627352328));
#96125=CARTESIAN_POINT('Ctrl Pts',(-88.7382386857666,-4.61361011382306,
132.508410141532));
#96126=CARTESIAN_POINT('Ctrl Pts',(-88.7464787748588,-4.56334157595128,
132.644509140693));
#96127=CARTESIAN_POINT('Ctrl Pts',(-88.754718863951,-4.50710371254321,132.778228090842));
#96128=CARTESIAN_POINT('Ctrl Pts',(-88.7629589530432,-4.44515839478008,
132.909057723521));
#96129=CARTESIAN_POINT('Ctrl Pts',(-88.7667394191062,-4.41673853560815,
132.969080980654));
#96130=CARTESIAN_POINT('Ctrl Pts',(-88.7705198851692,-4.38711794729714,
133.028496445633));
#96131=CARTESIAN_POINT('Ctrl Pts',(-88.7743003512322,-4.35632498955899,
133.087256946321));
#96132=CARTESIAN_POINT('Ctrl Pts',(-88.7820746853513,-4.29300085491992,
133.208094895332));
#96133=CARTESIAN_POINT('Ctrl Pts',(-88.7898490194703,-4.22454481273088,
133.32648747086));
#96134=CARTESIAN_POINT('Ctrl Pts',(-88.7976233535894,-4.15116970869277,
133.441968077392));
#96135=CARTESIAN_POINT('Ctrl Pts',(-88.8053881065365,-4.07788503291266,
133.557306364398));
#96136=CARTESIAN_POINT('Ctrl Pts',(-88.8131528594836,-3.99969356511958,
133.669739496114));
#96137=CARTESIAN_POINT('Ctrl Pts',(-88.8209176124307,-3.91685477330913,
133.778823888024));
#96138=CARTESIAN_POINT('Ctrl Pts',(-88.8286746533157,-3.83409825815476,
133.887799935779));
#96139=CARTESIAN_POINT('Ctrl Pts',(-88.8364316942006,-3.74670383952713,
133.993433553302));
#96140=CARTESIAN_POINT('Ctrl Pts',(-88.8441887350856,-3.65497496296968,
134.095308973673));
#96141=CARTESIAN_POINT('Ctrl Pts',(-88.8519399263257,-3.56331525987146,
134.197107568998));
#96142=CARTESIAN_POINT('Ctrl Pts',(-88.8596911175658,-3.46732786543789,
134.295153318878));
#96143=CARTESIAN_POINT('Ctrl Pts',(-88.8674423088059,-3.36735705661374,
134.389062769178));
#96144=CARTESIAN_POINT('Ctrl Pts',(-88.875190205583,-3.26742873805002,134.482932305458));
#96145=CARTESIAN_POINT('Ctrl Pts',(-88.8829381023602,-3.16352065681897,
134.57266877164));
#96146=CARTESIAN_POINT('Ctrl Pts',(-88.8906859991373,-3.05601441518644,
134.657925065797));
#96147=CARTESIAN_POINT('Ctrl Pts',(-88.8984322752214,-2.94853066154209,
134.743163526176));
#96148=CARTESIAN_POINT('Ctrl Pts',(-88.9061785513054,-2.83745055070981,
134.823923435804));
#96149=CARTESIAN_POINT('Ctrl Pts',(-88.9139248273895,-2.723188968183,134.899897811399));
#96150=CARTESIAN_POINT('Ctrl Pts',(-88.9216711606549,-2.60892654220331,
134.975872747818));
#96151=CARTESIAN_POINT('Ctrl Pts',(-88.9294174939203,-2.49148292323219,
135.04706186324));
#96152=CARTESIAN_POINT('Ctrl Pts',(-88.9371638271856,-2.37130185204952,
135.113201597338));
#96153=CARTESIAN_POINT('Ctrl Pts',(-88.9449118951886,-2.25109386714939,
135.179356142972));
#96154=CARTESIAN_POINT('Ctrl Pts',(-88.9526599631916,-2.1281475526282,135.240458868709));
#96155=CARTESIAN_POINT('Ctrl Pts',(-88.9604080311945,-2.00293074330515,
135.296292440293));
#96156=CARTESIAN_POINT('Ctrl Pts',(-88.9681643339364,-1.87758085206688,
135.35218535246));
#96157=CARTESIAN_POINT('Ctrl Pts',(-88.9759206366782,-1.74995600322717,
135.40279776416));
#96158=CARTESIAN_POINT('Ctrl Pts',(-88.9836769394201,-1.62054400233121,
135.447960535626));
#96159=CARTESIAN_POINT('Ctrl Pts',(-88.9914373819342,-1.49106293035351,
135.493147411824));
#96160=CARTESIAN_POINT('Ctrl Pts',(-88.9991978244484,-1.35979317969662,
135.532878738879));
#96161=CARTESIAN_POINT('Ctrl Pts',(-89.0069582669626,-1.22723620464085,
135.567035744059));
#96162=CARTESIAN_POINT('Ctrl Pts',(-89.014731167228,-1.09446643736122,135.601247581096));
#96163=CARTESIAN_POINT('Ctrl Pts',(-89.0225040674935,-0.960405698992884,
135.629867132839));
#96164=CARTESIAN_POINT('Ctrl Pts',(-89.0302769677589,-0.825564974306989,
135.652826925142));
#96165=CARTESIAN_POINT('Ctrl Pts',(-89.0377673035208,-0.695626049608546,
135.674952071162));
#96166=CARTESIAN_POINT('Ctrl Pts',(-89.0452576392827,-0.564963168459875,
135.691821767204));
#96167=CARTESIAN_POINT('Ctrl Pts',(-89.0527479750446,-0.434034729652507,
135.703421437351));
#96168=CARTESIAN_POINT('Ctrl Pts',(-89.0605223091637,-0.298142099291189,
135.715460912518));
#96169=CARTESIAN_POINT('Ctrl Pts',(-89.0682966432828,-0.161532909512511,
135.721860984421));
#96170=CARTESIAN_POINT('Ctrl Pts',(-89.0760709774019,-0.0247147686370575,
135.722548519905));
#96171=CARTESIAN_POINT('Ctrl Pts',(-89.083835730349,0.111934756107555,135.723235208062));
#96172=CARTESIAN_POINT('Ctrl Pts',(-89.091600483296,0.248792332366639,135.718223365735));
#96173=CARTESIAN_POINT('Ctrl Pts',(-89.0993652362431,0.385344511134806,
135.707491522431));
#96174=CARTESIAN_POINT('Ctrl Pts',(-89.1071222771281,0.521761064353973,
135.696770338144));
#96175=CARTESIAN_POINT('Ctrl Pts',(-89.1148793180131,0.657872436471643,
135.68034048913));
#96176=CARTESIAN_POINT('Ctrl Pts',(-89.1226363588981,0.793164811273817,
135.658232540542));
#96177=CARTESIAN_POINT('Ctrl Pts',(-89.1303875501382,0.928355161043546,
135.63614126373));
#96178=CARTESIAN_POINT('Ctrl Pts',(-89.1381387413784,1.06272735853112,135.608380473));
#96179=CARTESIAN_POINT('Ctrl Pts',(-89.1458899326185,1.19577270281499,135.575032551969));
#96180=CARTESIAN_POINT('Ctrl Pts',(-89.1536378293955,1.32876149927861,135.541698804695));
#96181=CARTESIAN_POINT('Ctrl Pts',(-89.1613857261727,1.46042418574826,135.502782745032));
#96182=CARTESIAN_POINT('Ctrl Pts',(-89.1691336229498,1.59026247019454,135.458417808705));
#96183=CARTESIAN_POINT('Ctrl Pts',(-89.1768798990338,1.72007359527036,135.414062152566));
#96184=CARTESIAN_POINT('Ctrl Pts',(-89.1846261751177,1.84806070766761,135.364260013196));
#96185=CARTESIAN_POINT('Ctrl Pts',(-89.1923724512018,1.97374127791077,135.309194513546));
#96186=CARTESIAN_POINT('Ctrl Pts',(-89.2001187844671,2.09942277589953,135.254128607415));
#96187=CARTESIAN_POINT('Ctrl Pts',(-89.2078651177326,2.22279733965769,135.193799420375));
#96188=CARTESIAN_POINT('Ctrl Pts',(-89.2156114509979,2.34340337568982,135.128437823318));
#96189=CARTESIAN_POINT('Ctrl Pts',(-89.2233595190009,2.46403642060733,135.063061588985));
#96190=CARTESIAN_POINT('Ctrl Pts',(-89.2311075870038,2.58189936041836,134.992650888336));
#96191=CARTESIAN_POINT('Ctrl Pts',(-89.2388556550067,2.69655646951008,134.91748184958));
#96192=CARTESIAN_POINT('Ctrl Pts',(-89.2466119577486,2.81133543754193,134.842232920275));
#96193=CARTESIAN_POINT('Ctrl Pts',(-89.2543682604904,2.92290144113071,134.762215765223));
#96194=CARTESIAN_POINT('Ctrl Pts',(-89.2621245632322,3.03084850738987,134.677749364871));
#96195=CARTESIAN_POINT('Ctrl Pts',(-89.2698850057464,3.13885318824882,134.593237882258));
#96196=CARTESIAN_POINT('Ctrl Pts',(-89.2776454482605,3.24323478562238,134.504272676044));
#96197=CARTESIAN_POINT('Ctrl Pts',(-89.2854058907747,3.34362232435879,134.411211434352));
#96198=CARTESIAN_POINT('Ctrl Pts',(-89.2931787910401,3.4441710140841,134.318000802494));
#96199=CARTESIAN_POINT('Ctrl Pts',(-89.3009516913055,3.54071255721653,134.220681273296));
#96200=CARTESIAN_POINT('Ctrl Pts',(-89.3087245915709,3.63291398609695,134.119646281294));
#96201=CARTESIAN_POINT('Ctrl Pts',(-89.3162149273331,3.72176366079819,134.022284165741));
#96202=CARTESIAN_POINT('Ctrl Pts',(-89.3237052630953,3.80658309273496,133.921472266038));
#96203=CARTESIAN_POINT('Ctrl Pts',(-89.3311955988575,3.88711224303279,133.817588367432));
#96204=CARTESIAN_POINT('Ctrl Pts',(-89.3389699329766,3.9706946805387,133.709765679238));
#96205=CARTESIAN_POINT('Ctrl Pts',(-89.3467442670956,4.04991984623069,133.598291894098));
#96206=CARTESIAN_POINT('Ctrl Pts',(-89.3545186012147,4.12445183641704,133.483554547011));
#96207=CARTESIAN_POINT('Ctrl Pts',(-89.3622833541618,4.1988919725866,133.36895860345));
#96208=CARTESIAN_POINT('Ctrl Pts',(-89.3700481071089,4.2686502305942,133.251107425337));
#96209=CARTESIAN_POINT('Ctrl Pts',(-89.377812860056,4.33343101497726,133.130421386534));
#96210=CARTESIAN_POINT('Ctrl Pts',(-89.385569900941,4.39814745817201,133.009855214807));
#96211=CARTESIAN_POINT('Ctrl Pts',(-89.393326941826,4.45789608221385,132.886460127857));
#96212=CARTESIAN_POINT('Ctrl Pts',(-89.401083982711,4.51242487221753,132.760684935028));
#96213=CARTESIAN_POINT('Ctrl Pts',(-89.4088351739511,4.56691254163658,132.63500459025));
#96214=CARTESIAN_POINT('Ctrl Pts',(-89.4165863651913,4.61618805713429,132.5069480694));
#96215=CARTESIAN_POINT('Ctrl Pts',(-89.4243375564314,4.66004576510778,132.376987887329));
#96216=CARTESIAN_POINT('Ctrl Pts',(-89.4320854532085,4.70388483238538,132.247082941801));
#96217=CARTESIAN_POINT('Ctrl Pts',(-89.4398333499855,4.74231054730809,132.115276313968));
#96218=CARTESIAN_POINT('Ctrl Pts',(-89.4475812467626,4.77516583411507,131.982059356293));
#96219=CARTESIAN_POINT('Ctrl Pts',(-89.4553275228466,4.80801424830433,131.848870264734));
#96220=CARTESIAN_POINT('Ctrl Pts',(-89.4630737989308,4.83529445849214,131.714271809476));
#96221=CARTESIAN_POINT('Ctrl Pts',(-89.4708200750149,4.85689971223601,131.578768938661));
#96222=CARTESIAN_POINT('Ctrl Pts',(-89.4785664082802,4.87850512546497,131.443265067595));
#96223=CARTESIAN_POINT('Ctrl Pts',(-89.4863127415455,4.8944354370992,131.306857153738));
#96224=CARTESIAN_POINT('Ctrl Pts',(-89.4940590748109,4.90463538279991,131.170058340128));
#96225=CARTESIAN_POINT('Ctrl Pts',(-89.5018071428139,4.91483761270772,131.033228891373));
#96226=CARTESIAN_POINT('Ctrl Pts',(-89.5095552108169,4.91930689404716,130.89600875848));
#96227=CARTESIAN_POINT('Ctrl Pts',(-89.5173032788199,4.9180400209636,130.758913783789));
#96228=CARTESIAN_POINT('Ctrl Pts',(-89.5250595815617,4.91677180143226,130.621673102928));
#96229=CARTESIAN_POINT('Ctrl Pts',(-89.5328158843034,4.90975525277446,130.484558237562));
#96230=CARTESIAN_POINT('Ctrl Pts',(-89.5405721870453,4.89703930401219,130.348083160902));
#96231=CARTESIAN_POINT('Ctrl Pts',(-89.5483326295595,4.88431656836516,130.211535243384));
#96232=CARTESIAN_POINT('Ctrl Pts',(-89.5560930720736,4.86588842379378,130.075628182218));
#96233=CARTESIAN_POINT('Ctrl Pts',(-89.5638535145878,4.84185528231614,129.940867428475));
#96234=CARTESIAN_POINT('Ctrl Pts',(-89.5716264148532,4.81778356070624,129.805890344806));
#96235=CARTESIAN_POINT('Ctrl Pts',(-89.5793993151186,4.7880889467807,129.672063627676));
#96236=CARTESIAN_POINT('Ctrl Pts',(-89.5871722153841,4.75292247100479,129.539880073185));
#96237=CARTESIAN_POINT('Ctrl Pts',(-89.5946625511461,4.71903438520224,129.41250172385));
#96238=CARTESIAN_POINT('Ctrl Pts',(-89.6021528869083,4.68006545363289,129.286649439295));
#96239=CARTESIAN_POINT('Ctrl Pts',(-89.6096432226703,4.6361929603614,129.162746199746));
#96240=CARTESIAN_POINT('Ctrl Pts',(-89.6174175567894,4.59065702817282,129.034145131209));
#96241=CARTESIAN_POINT('Ctrl Pts',(-89.6251918909085,4.53969411287146,128.907236451772));
#96242=CARTESIAN_POINT('Ctrl Pts',(-89.6329662250276,4.48344869447733,128.782512238857));
#96243=CARTESIAN_POINT('Ctrl Pts',(-89.6407309779746,4.42727259353472,128.657941737387));
#96244=CARTESIAN_POINT('Ctrl Pts',(-89.6484957309217,4.36582710206212,128.535550698823));
#96245=CARTESIAN_POINT('Ctrl Pts',(-89.6562604838688,4.2993061159292,128.415815038341));
#96246=CARTESIAN_POINT('Ctrl Pts',(-89.6640175247538,4.2328511993775,128.296198301006));
#96247=CARTESIAN_POINT('Ctrl Pts',(-89.6717745656389,4.16133100873153,128.179232032841));
#96248=CARTESIAN_POINT('Ctrl Pts',(-89.6795316065239,4.08498691980275,128.065370853522));
#96249=CARTESIAN_POINT('Ctrl Pts',(-89.687282797764,4.00870040254521,127.951595537803));
#96250=CARTESIAN_POINT('Ctrl Pts',(-89.6950339890041,3.92759744455299,127.840920973586));
#96251=CARTESIAN_POINT('Ctrl Pts',(-89.7027851802443,3.84196442515621,127.733775588889));
#96252=CARTESIAN_POINT('Ctrl Pts',(-89.7105330770214,3.75636780207689,127.626675743839));
#96253=CARTESIAN_POINT('Ctrl Pts',(-89.7182809737985,3.66624519063893,127.523102399702));
#96254=CARTESIAN_POINT('Ctrl Pts',(-89.7260288705756,3.57192507630068,127.423453296773));
#96255=CARTESIAN_POINT('Ctrl Pts',(-89.7337751466597,3.47762469169703,127.323825038287));
#96256=CARTESIAN_POINT('Ctrl Pts',(-89.7415214227438,3.37912881922449,127.228119672023));
#96257=CARTESIAN_POINT('Ctrl Pts',(-89.7492676988279,3.27680458375309,127.136699948639));
#96258=CARTESIAN_POINT('Ctrl Pts',(-89.7570140320933,3.17447959294757,127.045279550415));
#96259=CARTESIAN_POINT('Ctrl Pts',(-89.7647603653587,3.06832647430463,126.958145118679));
#96260=CARTESIAN_POINT('Ctrl Pts',(-89.772506698624,2.95874707786966,126.875620515231));
#96261=CARTESIAN_POINT('Ctrl Pts',(-89.780254766627,2.84914314188848,126.79307743097));
#96262=CARTESIAN_POINT('Ctrl Pts',(-89.7880028346301,2.73611171354127,126.715146464385));
#96263=CARTESIAN_POINT('Ctrl Pts',(-89.7957509026331,2.62008505275539,126.642109138039));
#96264=CARTESIAN_POINT('Ctrl Pts',(-89.803507205375,2.50393507745386,126.568994186753));
#96265=CARTESIAN_POINT('Ctrl Pts',(-89.8112635081168,2.38478384198821,126.50078347391));
#96266=CARTESIAN_POINT('Ctrl Pts',(-89.8190198108586,2.26309021390805,126.437713649214));
#96267=CARTESIAN_POINT('Ctrl Pts',(-89.8267802533728,2.14133163427447,126.374610162254));
#96268=CARTESIAN_POINT('Ctrl Pts',(-89.834540695887,2.01702831235432,126.31665319592));
#96269=CARTESIAN_POINT('Ctrl Pts',(-89.8423011384012,1.89065977359634,126.264031479386));
#96270=CARTESIAN_POINT('Ctrl Pts',(-89.8500740386666,1.76408837684147,126.211325289802));
#96271=CARTESIAN_POINT('Ctrl Pts',(-89.8578469389321,1.63544550539274,126.163971599985));
#96272=CARTESIAN_POINT('Ctrl Pts',(-89.8656198391975,1.50522739822047,126.122109712056));
#96273=CARTESIAN_POINT('Ctrl Pts',(-89.8731101749595,1.37974304724494,126.081769609198));
#96274=CARTESIAN_POINT('Ctrl Pts',(-89.8806005107214,1.25279629654676,126.046529041071));
#96275=CARTESIAN_POINT('Ctrl Pts',(-89.8880908464834,1.12483883773506,126.016467484713));
#96276=CARTESIAN_POINT('Ctrl Pts',(-89.8958651806025,0.992029832979374,
125.985266135308));
#96277=CARTESIAN_POINT('Ctrl Pts',(-89.9036395147215,0.85771126616984,125.959545438143));
#96278=CARTESIAN_POINT('Ctrl Pts',(-89.9114138488406,0.722375230958079,
125.939449817952));
#96279=CARTESIAN_POINT('Ctrl Pts',(-89.9191786017877,0.587205985314387,
125.919378963817));
#96280=CARTESIAN_POINT('Ctrl Pts',(-89.9269433547348,0.451022149245679,
125.904919450109));
#96281=CARTESIAN_POINT('Ctrl Pts',(-89.9347081076819,0.314328929122017,
125.896165390518));
#96282=CARTESIAN_POINT('Ctrl Pts',(-89.9424651485669,0.177771474631618,
125.887420025583));
#96283=CARTESIAN_POINT('Ctrl Pts',(-89.9502221894519,0.0407060305458466,
125.884368862527));
#96284=CARTESIAN_POINT('Ctrl Pts',(-89.9579792303369,-0.0963544492060208,
125.887054558084));
#96285=CARTESIAN_POINT('Ctrl Pts',(-89.965730421577,-0.233311570584119,
125.889738228337));
#96286=CARTESIAN_POINT('Ctrl Pts',(-89.9734816128173,-0.370263345771275,
125.898150138515));
#96287=CARTESIAN_POINT('Ctrl Pts',(-89.9812328040574,-0.506694531118351,
125.912280925387));
#96288=CARTESIAN_POINT('Ctrl Pts',(-89.9889807008345,-0.643067729572047,
125.926405706297));
#96289=CARTESIAN_POINT('Ctrl Pts',(-89.9967285976115,-0.778920390193332,
125.946244489279));
#96290=CARTESIAN_POINT('Ctrl Pts',(-90.0044764943886,-0.913740328393507,
125.971735898558));
#96291=CARTESIAN_POINT('Ctrl Pts',(-90.0122227704727,-1.04853206516899,
125.997221975584));
#96292=CARTESIAN_POINT('Ctrl Pts',(-90.0199690465567,-1.18229112529025,
126.028358254444));
#96293=CARTESIAN_POINT('Ctrl Pts',(-90.0277153226408,-1.31451387639524,
126.065031938179));
#96294=CARTESIAN_POINT('Ctrl Pts',(-90.0354616559061,-1.44673760353836,
126.10170589263));
#96295=CARTESIAN_POINT('Ctrl Pts',(-90.0432079891715,-1.57742462229343,
126.143917229027));
#96296=CARTESIAN_POINT('Ctrl Pts',(-90.0509543224368,-1.70608524879114,
126.191502914758));
#96297=CARTESIAN_POINT('Ctrl Pts',(-90.0587023904398,-1.83477468794392,
126.239099256973));
#96298=CARTESIAN_POINT('Ctrl Pts',(-90.0664504584427,-1.9614364652183,126.292072207849));
#96299=CARTESIAN_POINT('Ctrl Pts',(-90.0741985264457,-2.08560008066112,
126.350210264688));
#96300=CARTESIAN_POINT('Ctrl Pts',(-90.0819548291875,-2.2098956586725,126.408410111345));
#96301=CARTESIAN_POINT('Ctrl Pts',(-90.0897111319294,-2.33168741641451,
126.47178586385));
#96302=CARTESIAN_POINT('Ctrl Pts',(-90.0974674346713,-2.45052822467107,
126.540079378882));
#96303=CARTESIAN_POINT('Ctrl Pts',(-90.1052278771855,-2.56943246184523,
126.60840934422));
#96304=CARTESIAN_POINT('Ctrl Pts',(-90.1129883196996,-2.68538228082437,
126.681662093423));
#96305=CARTESIAN_POINT('Ctrl Pts',(-90.1207487622138,-2.7979597031904,126.75953620088));
#96306=CARTESIAN_POINT('Ctrl Pts',(-90.1285216624792,-2.91071784482865,
126.837535318767));
#96307=CARTESIAN_POINT('Ctrl Pts',(-90.1362945627447,-3.0200924594925,126.920170383848));
#96308=CARTESIAN_POINT('Ctrl Pts',(-90.1440674630101,-3.12569811907768,
127.007099192421));
#96309=CARTESIAN_POINT('Ctrl Pts',(-90.1515577987722,-3.22746474693347,
127.090867919843));
#96310=CARTESIAN_POINT('Ctrl Pts',(-90.1590481345343,-3.32573145456485,
127.178623428655));
#96311=CARTESIAN_POINT('Ctrl Pts',(-90.1665384702964,-3.42018722534059,
127.270028657193));
#96312=CARTESIAN_POINT('Ctrl Pts',(-90.1741987121588,-3.51678557185298,
127.363507264871));
#96313=CARTESIAN_POINT('Ctrl Pts',(-90.1818589540213,-3.60972311669065,
127.46111811559));
#96314=CARTESIAN_POINT('Ctrl Pts',(-90.1895191958837,-3.69861766985977,
127.562538538133));
#96315=CARTESIAN_POINT('Ctrl Pts',(-90.1971705196152,-3.7874087310932,127.663840885997));
#96316=CARTESIAN_POINT('Ctrl Pts',(-90.2048218433467,-3.87216589474051,
127.768943689028));
#96317=CARTESIAN_POINT('Ctrl Pts',(-90.2124731670783,-3.9525416122317,127.87748551499));
#96318=CARTESIAN_POINT('Ctrl Pts',(-90.2201173554329,-4.03284237392931,
127.985926118358));
#96319=CARTESIAN_POINT('Ctrl Pts',(-90.2277615437875,-4.10876957591086,
128.097799045613));
#96320=CARTESIAN_POINT('Ctrl Pts',(-90.2354057321421,-4.18001437723478,
128.212708081324));
#96321=CARTESIAN_POINT('Ctrl Pts',(-90.2430443833342,-4.25120757150529,
128.327533881253));
#96322=CARTESIAN_POINT('Ctrl Pts',(-90.2506830345264,-4.31772490130267,
128.445391072843));
#96323=CARTESIAN_POINT('Ctrl Pts',(-90.2583216857185,-4.37929984730207,
128.565853099169));
#96324=CARTESIAN_POINT('Ctrl Pts',(-90.2659570433207,-4.44084824376795,
128.686263185367));
#96325=CARTESIAN_POINT('Ctrl Pts',(-90.273592400923,-4.49745831256911,128.809275513571));
#96326=CARTESIAN_POINT('Ctrl Pts',(-90.2812277585251,-4.5489088876211,128.934437893328));
#96327=CARTESIAN_POINT('Ctrl Pts',(-90.2888628943485,-4.60035796822437,
129.059596637581));
#96328=CARTESIAN_POINT('Ctrl Pts',(-90.2964980301717,-4.64664769166659,
129.186904939655));
#96329=CARTESIAN_POINT('Ctrl Pts',(-90.304133165995,-4.68760469495257,129.315889829691));
#96330=CARTESIAN_POINT('Ctrl Pts',(-90.3093502966369,-4.71559084238847,
129.404025920222));
#96331=CARTESIAN_POINT('Ctrl Pts',(-90.3145674272788,-4.74108810602048,
129.492944387662));
#96332=CARTESIAN_POINT('Ctrl Pts',(-90.3197845579208,-4.76405452823393,
129.582490119308));
#96333=CARTESIAN_POINT('Origin',(213.235140564004,0.,130.804360617566));
#96334=CARTESIAN_POINT('',(-92.4154045049002,-4.764054528234,129.582490119308));
#96335=CARTESIAN_POINT('',(-92.069771887517,-4.76405452823417,129.582490119309));
#96336=CARTESIAN_POINT('',(213.235140564004,-4.76405452823405,129.582490119308));
#96337=CARTESIAN_POINT('',(-90.7351405640466,-4.91824902519036,130.801264052685));
#96338=CARTESIAN_POINT('Ctrl Pts',(-90.7351405640468,-4.91824902519036,
130.801264052685));
#96339=CARTESIAN_POINT('Ctrl Pts',(-90.7428057530588,-4.91833386882775,
130.93602051764));
#96340=CARTESIAN_POINT('Ctrl Pts',(-90.7504709420708,-4.9128761986244,131.070997929296));
#96341=CARTESIAN_POINT('Ctrl Pts',(-90.7581361310829,-4.90184799165934,
131.205695053125));
#96342=CARTESIAN_POINT('Ctrl Pts',(-90.7657929371722,-4.89083184553285,
131.340244867398));
#96343=CARTESIAN_POINT('Ctrl Pts',(-90.7734497432615,-4.87425731142311,
131.474514605884));
#96344=CARTESIAN_POINT('Ctrl Pts',(-90.7811065493508,-4.85214837645269,
131.608001828174));
#96345=CARTESIAN_POINT('Ctrl Pts',(-90.7887569299817,-4.8300579949156,131.741377030311));
#96346=CARTESIAN_POINT('Ctrl Pts',(-90.7964073106126,-4.80244251677769,
131.873970627672));
#96347=CARTESIAN_POINT('Ctrl Pts',(-90.8040576912435,-4.76937780208517,
132.005284613278));
#96348=CARTESIAN_POINT('Ctrl Pts',(-90.8117040952299,-4.73633027433065,
132.136530342274));
#96349=CARTESIAN_POINT('Ctrl Pts',(-90.8193504992163,-4.69783924039402,
132.266497393015));
#96350=CARTESIAN_POINT('Ctrl Pts',(-90.8269969032026,-4.65403170005497,
132.394697687933));
#96351=CARTESIAN_POINT('Ctrl Pts',(-90.8346413310321,-4.61023548145241,
132.522864850428));
#96352=CARTESIAN_POINT('Ctrl Pts',(-90.8422857588617,-4.56112561799244,
132.649265784427));
#96353=CARTESIAN_POINT('Ctrl Pts',(-90.8499301866912,-4.50687890279669,
132.773427812465));
#96354=CARTESIAN_POINT('Ctrl Pts',(-90.8575743981105,-4.45263372330044,
132.897586325533));
#96355=CARTESIAN_POINT('Ctrl Pts',(-90.8652186095297,-4.39325214244064,
133.019505690027));
#96356=CARTESIAN_POINT('Ctrl Pts',(-90.872862820949,-4.32895878409133,133.138733961343));
#96357=CARTESIAN_POINT('Ctrl Pts',(-90.8805085753086,-4.26465244849602,
133.257986298203));
#96358=CARTESIAN_POINT('Ctrl Pts',(-90.8881543296682,-4.19543255524392,
133.374546107872));
#96359=CARTESIAN_POINT('Ctrl Pts',(-90.8958000840277,-4.12156901147522,
133.487987258168));
#96360=CARTESIAN_POINT('Ctrl Pts',(-90.9034536646853,-4.0476298599804,133.601544528365));
#96361=CARTESIAN_POINT('Ctrl Pts',(-90.9111072453428,-3.96903778608739,
133.711976427007));
#96362=CARTESIAN_POINT('Ctrl Pts',(-90.9187608260003,-3.88610544629988,
133.818886703494));
#96363=CARTESIAN_POINT('Ctrl Pts',(-90.9264185292908,-3.80312843466327,
133.925854567645));
#96364=CARTESIAN_POINT('Ctrl Pts',(-90.9340762325813,-3.71580676153998,
134.029296725865));
#96365=CARTESIAN_POINT('Ctrl Pts',(-90.9417339358718,-3.62449161161779,
134.128852100457));
#96366=CARTESIAN_POINT('Ctrl Pts',(-90.9494033679423,-3.53303660053156,
134.228559957201));
#96367=CARTESIAN_POINT('Ctrl Pts',(-90.9570728000127,-3.43757618066661,
134.324368856597));
#96368=CARTESIAN_POINT('Ctrl Pts',(-90.9647422320831,-3.33849684065856,
134.415956097048));
#96369=CARTESIAN_POINT('Ctrl Pts',(-90.9705922699137,-3.26292176782947,
134.485816396549));
#96370=CARTESIAN_POINT('Ctrl Pts',(-90.9764423077442,-3.18524185082494,
134.553221231407));
#96371=CARTESIAN_POINT('Ctrl Pts',(-90.9822923455748,-3.10563999061448,
134.618044310689));
#96372=CARTESIAN_POINT('Ctrl Pts',(-90.990066679694,-2.99985410072831,134.704190125736));
#96373=CARTESIAN_POINT('Ctrl Pts',(-90.9978410138131,-2.89031360281266,
134.786067540014));
#96374=CARTESIAN_POINT('Ctrl Pts',(-91.0056153479322,-2.77739785950375,
134.863331446794));
#96375=CARTESIAN_POINT('Ctrl Pts',(-91.0133801008793,-2.66462127475689,
134.940500132714));
#96376=CARTESIAN_POINT('Ctrl Pts',(-91.0211448538265,-2.5484780407179,135.01306640539));
#96377=CARTESIAN_POINT('Ctrl Pts',(-91.0289096067736,-2.4293813167176,135.080724666672));
#96378=CARTESIAN_POINT('Ctrl Pts',(-91.0366666476586,-2.31040288126287,
135.148315728814));
#96379=CARTESIAN_POINT('Ctrl Pts',(-91.0444236885437,-2.18847713128068,
135.211008288578));
#96380=CARTESIAN_POINT('Ctrl Pts',(-91.0521807294287,-2.06404669920747,
135.268539633465));
#96381=CARTESIAN_POINT('Ctrl Pts',(-91.0599319206688,-1.93971010109084,
135.326027593517));
#96382=CARTESIAN_POINT('Ctrl Pts',(-91.0676831119089,-1.8128729338595,135.378361922294));
#96383=CARTESIAN_POINT('Ctrl Pts',(-91.0754343031491,-1.68400264117168,
135.425325686361));
#96384=CARTESIAN_POINT('Ctrl Pts',(-91.0831821999262,-1.55518712179581,
135.472269489576));
#96385=CARTESIAN_POINT('Ctrl Pts',(-91.0909300967033,-1.42434056222138,
135.51384713448));
#96386=CARTESIAN_POINT('Ctrl Pts',(-91.0986779934804,-1.29195040402995,
135.549889799441));
#96387=CARTESIAN_POINT('Ctrl Pts',(-91.1064242695645,-1.15958793900563,
135.585924925053));
#96388=CARTESIAN_POINT('Ctrl Pts',(-91.1141705456486,-1.0256828946015,135.616427271012));
#96389=CARTESIAN_POINT('Ctrl Pts',(-91.1219168217328,-0.890737511782772,
135.641277998254));
#96390=CARTESIAN_POINT('Ctrl Pts',(-91.1296631549981,-0.755791132827696,
135.666128908938));
#96391=CARTESIAN_POINT('Ctrl Pts',(-91.1374094882635,-0.61980478463389,
135.685328046851));
#96392=CARTESIAN_POINT('Ctrl Pts',(-91.1451558215289,-0.483290136274591,
135.69880784955));
#96393=CARTESIAN_POINT('Ctrl Pts',(-91.1529038895319,-0.346744916406505,
135.712290670958));
#96394=CARTESIAN_POINT('Ctrl Pts',(-91.1606519575349,-0.209671549949994,
135.720051570087));
#96395=CARTESIAN_POINT('Ctrl Pts',(-91.1684000255379,-0.0725856537635758,
135.722074963212));
#96396=CARTESIAN_POINT('Ctrl Pts',(-91.1761563282797,0.0646459389448387,
135.724100506823));
#96397=CARTESIAN_POINT('Ctrl Pts',(-91.1839126310217,0.201889696438832,
135.720376357459));
#96398=CARTESIAN_POINT('Ctrl Pts',(-91.1916689337636,0.338630619358337,
135.710939096112));
#96399=CARTESIAN_POINT('Ctrl Pts',(-91.1994293762778,0.475444525025594,
135.701496797815));
#96400=CARTESIAN_POINT('Ctrl Pts',(-91.2071898187919,0.611754672973703,
135.686335354825));
#96401=CARTESIAN_POINT('Ctrl Pts',(-91.2149502613061,0.747053348078596,
135.665543020812));
#96402=CARTESIAN_POINT('Ctrl Pts',(-91.2227231615715,0.882569216628018,
135.644717309098));
#96403=CARTESIAN_POINT('Ctrl Pts',(-91.230496061837,1.0170699838269,135.618242718698));
#96404=CARTESIAN_POINT('Ctrl Pts',(-91.2382689621025,1.15005937117471,135.586258410835));
#96405=CARTESIAN_POINT('Ctrl Pts',(-91.2457592978643,1.27821425930877,135.555436813128));
#96406=CARTESIAN_POINT('Ctrl Pts',(-91.2532496336261,1.40496544841964,135.519499211466));
#96407=CARTESIAN_POINT('Ctrl Pts',(-91.260739969388,1.52988582576255,135.4786126885));
#96408=CARTESIAN_POINT('Ctrl Pts',(-91.2685143035071,1.65954259718496,135.436175940588));
#96409=CARTESIAN_POINT('Ctrl Pts',(-91.2762886376263,1.78763769950532,135.388273159727));
#96410=CARTESIAN_POINT('Ctrl Pts',(-91.2840629717454,1.91367572988546,135.335036975832));
#96411=CARTESIAN_POINT('Ctrl Pts',(-91.2918277246925,2.03955842965785,135.281866400775));
#96412=CARTESIAN_POINT('Ctrl Pts',(-91.2995924776396,2.16338874499898,135.223375651541));
#96413=CARTESIAN_POINT('Ctrl Pts',(-91.3073572305868,2.28468624481829,135.159747147512));
#96414=CARTESIAN_POINT('Ctrl Pts',(-91.3151142714718,2.40586327025045,135.096181840211));
#96415=CARTESIAN_POINT('Ctrl Pts',(-91.3228713123569,2.52451214239294,135.027489113537));
#96416=CARTESIAN_POINT('Ctrl Pts',(-91.3306283532419,2.64017258013704,134.953899364173));
#96417=CARTESIAN_POINT('Ctrl Pts',(-91.3383795444821,2.75574579744518,134.880365109412));
#96418=CARTESIAN_POINT('Ctrl Pts',(-91.3461307357222,2.86833473748875,134.801941391445));
#96419=CARTESIAN_POINT('Ctrl Pts',(-91.3538819269624,2.97750422331127,134.718904226042));
#96420=CARTESIAN_POINT('Ctrl Pts',(-91.3616298237395,3.08662730919027,134.63590235365));
#96421=CARTESIAN_POINT('Ctrl Pts',(-91.3693777205167,3.19233352094263,134.548291169973));
#96422=CARTESIAN_POINT('Ctrl Pts',(-91.3771256172938,3.29421735006745,134.456389521205));
#96423=CARTESIAN_POINT('Ctrl Pts',(-91.3848718933779,3.39607986729158,134.36450709628));
#96424=CARTESIAN_POINT('Ctrl Pts',(-91.392618169462,3.49412130213105,134.268336253087));
#96425=CARTESIAN_POINT('Ctrl Pts',(-91.4003644455462,3.58797019840641,134.168235305756));
#96426=CARTESIAN_POINT('Ctrl Pts',(-91.4081107788116,3.68181978745312,134.068133619503));
#96427=CARTESIAN_POINT('Ctrl Pts',(-91.4158571120769,3.77147650877684,133.964102056441));
#96428=CARTESIAN_POINT('Ctrl Pts',(-91.4236034453423,3.85660695054932,133.856534579101));
#96429=CARTESIAN_POINT('Ctrl Pts',(-91.4313515133453,3.94175645669388,133.748943012772));
#96430=CARTESIAN_POINT('Ctrl Pts',(-91.4390995813483,4.02237742370374,133.637814263001));
#96431=CARTESIAN_POINT('Ctrl Pts',(-91.4468476493513,4.09817803704285,133.523573709473));
#96432=CARTESIAN_POINT('Ctrl Pts',(-91.4546039520932,4.17405921217595,133.409211739725));
#96433=CARTESIAN_POINT('Ctrl Pts',(-91.4623602548352,4.24510958313337,133.291731685901));
#96434=CARTESIAN_POINT('Ctrl Pts',(-91.4701165575771,4.31108155680585,133.171586604469));
#96435=CARTESIAN_POINT('Ctrl Pts',(-91.4778770000913,4.37708874170706,133.051377397989));
#96436=CARTESIAN_POINT('Ctrl Pts',(-91.4856374426056,4.43801195485126,132.928500679741));
#96437=CARTESIAN_POINT('Ctrl Pts',(-91.4933978851198,4.49365101412424,132.803431308102));
#96438=CARTESIAN_POINT('Ctrl Pts',(-91.5011707853853,4.54937939015457,132.678161164005));
#96439=CARTESIAN_POINT('Ctrl Pts',(-91.5089436856507,4.59980651748605,132.550691696511));
#96440=CARTESIAN_POINT('Ctrl Pts',(-91.5167165859162,4.64478122574641,132.42151565882));
#96441=CARTESIAN_POINT('Ctrl Pts',(-91.5242069216778,4.68812099007425,132.297035495482));
#96442=CARTESIAN_POINT('Ctrl Pts',(-91.5316972574393,4.72639778177273,132.170970978784));
#96443=CARTESIAN_POINT('Ctrl Pts',(-91.5391875932009,4.75952130733774,132.043771763029));
#96444=CARTESIAN_POINT('Ctrl Pts',(-91.54696192732,4.79390072144421,131.91174975034));
#96445=CARTESIAN_POINT('Ctrl Pts',(-91.5547362614391,4.8228372869302,131.778087089771));
#96446=CARTESIAN_POINT('Ctrl Pts',(-91.5625105955582,4.84617481176206,131.643272267469));
#96447=CARTESIAN_POINT('Ctrl Pts',(-91.5702753485052,4.86948357518022,131.508623592387));
#96448=CARTESIAN_POINT('Ctrl Pts',(-91.5780401014523,4.88720696147164,131.372825962359));
#96449=CARTESIAN_POINT('Ctrl Pts',(-91.5858048543994,4.89923876048785,131.236382179798));
#96450=CARTESIAN_POINT('Ctrl Pts',(-91.5935618952843,4.91125860935166,131.100073915126));
#96451=CARTESIAN_POINT('Ctrl Pts',(-91.6013189361692,4.91759808647479,130.963121162003));
#96452=CARTESIAN_POINT('Ctrl Pts',(-91.6090759770542,4.91820223792918,130.826035702995));
#96453=CARTESIAN_POINT('Ctrl Pts',(-91.6168271682943,4.91880593378827,130.689053621199));
#96454=CARTESIAN_POINT('Ctrl Pts',(-91.6245783595346,4.91368291101969,130.55193942209));
#96455=CARTESIAN_POINT('Ctrl Pts',(-91.6323295507746,4.90283016573214,130.415208425632));
#96456=CARTESIAN_POINT('Ctrl Pts',(-91.6400774475517,4.89198203315083,130.278535543495));
#96457=CARTESIAN_POINT('Ctrl Pts',(-91.6478253443288,4.87540905251657,130.142245928994));
#96458=CARTESIAN_POINT('Ctrl Pts',(-91.6555732411058,4.85316029091126,130.00685309207));
#96459=CARTESIAN_POINT('Ctrl Pts',(-91.6633195171899,4.83091618326719,129.871488576409));
#96460=CARTESIAN_POINT('Ctrl Pts',(-91.6710657932739,4.80299871951531,129.737020850752));
#96461=CARTESIAN_POINT('Ctrl Pts',(-91.678812069358,4.76950857834417,129.603956109243));
#96462=CARTESIAN_POINT('Ctrl Pts',(-91.6865584026234,4.73601818995646,129.470890385481));
#96463=CARTESIAN_POINT('Ctrl Pts',(-91.6943047358886,4.69695513748856,129.339228045675));
#96464=CARTESIAN_POINT('Ctrl Pts',(-91.702051069154,4.65247065553931,129.209462545009));
#96465=CARTESIAN_POINT('Ctrl Pts',(-91.7097991371569,4.60797621159882,129.07966798426));
#96466=CARTESIAN_POINT('Ctrl Pts',(-91.71754720516,4.55805804903395,128.951771477689));
#96467=CARTESIAN_POINT('Ctrl Pts',(-91.7252952731629,4.50291631893379,128.82624846524));
#96468=CARTESIAN_POINT('Ctrl Pts',(-91.7330515759048,4.4477159835466,128.700592045439));
#96469=CARTESIAN_POINT('Ctrl Pts',(-91.7408078786465,4.38728114806209,128.577314517401));
#96470=CARTESIAN_POINT('Ctrl Pts',(-91.7485641813884,4.32185915159361,128.456869076306));
#96471=CARTESIAN_POINT('Ctrl Pts',(-91.7563246239026,4.25640223743562,128.336359349853));
#96472=CARTESIAN_POINT('Ctrl Pts',(-91.7640850664167,4.18595305916165,128.218685057556));
#96473=CARTESIAN_POINT('Ctrl Pts',(-91.7718455089309,4.11080292525089,128.104271290849));
#96474=CARTESIAN_POINT('Ctrl Pts',(-91.7796184091963,4.03553215367387,127.989673857008));
#96475=CARTESIAN_POINT('Ctrl Pts',(-91.7873913094617,3.95554557462359,127.878347725819));
#96476=CARTESIAN_POINT('Ctrl Pts',(-91.7951642097271,3.8711760440431,127.770686426337));
#96477=CARTESIAN_POINT('Ctrl Pts',(-91.8026545454893,3.78987355841094,127.666938886272));
#96478=CARTESIAN_POINT('Ctrl Pts',(-91.8101448812516,3.70450145104887,127.56659458678));
#96479=CARTESIAN_POINT('Ctrl Pts',(-91.8176352170138,3.61538922301267,127.469972543477));
#96480=CARTESIAN_POINT('Ctrl Pts',(-91.8254095511329,3.52289827776763,127.369687046038));
#96481=CARTESIAN_POINT('Ctrl Pts',(-91.833183885252,3.42608501636788,127.273093961039));
#96482=CARTESIAN_POINT('Ctrl Pts',(-91.8409582193711,3.32527599043282,127.180588735955));
#96483=CARTESIAN_POINT('Ctrl Pts',(-91.8487229723181,3.2245912026132,127.088197515295));
#96484=CARTESIAN_POINT('Ctrl Pts',(-91.8564877252652,3.1199207336899,126.999884392384));
#96485=CARTESIAN_POINT('Ctrl Pts',(-91.8642524782123,3.01163019639435,126.916010501814));
#96486=CARTESIAN_POINT('Ctrl Pts',(-91.8720095190973,2.90344721478708,126.832219915976));
#96487=CARTESIAN_POINT('Ctrl Pts',(-91.8797665599822,2.79165162711616,126.752860026009));
#96488=CARTESIAN_POINT('Ctrl Pts',(-91.8875236008672,2.67664430660942,126.678253697188));
#96489=CARTESIAN_POINT('Ctrl Pts',(-91.8952747921073,2.56172371401755,126.603703629579));
#96490=CARTESIAN_POINT('Ctrl Pts',(-91.9030259833474,2.44359653608789,126.533900199907));
#96491=CARTESIAN_POINT('Ctrl Pts',(-91.9107771745875,2.32269470242368,126.469124478457));
#96492=CARTESIAN_POINT('Ctrl Pts',(-91.9185250713646,2.20184425526378,126.404376288417));
#96493=CARTESIAN_POINT('Ctrl Pts',(-91.9262729681418,2.07822184181082,126.344651740699));
#96494=CARTESIAN_POINT('Ctrl Pts',(-91.9340208649188,1.9522860144783,126.290187118444));
#96495=CARTESIAN_POINT('Ctrl Pts',(-91.941767141003,1.82637653020564,126.235733889014));
#96496=CARTESIAN_POINT('Ctrl Pts',(-91.949513417087,1.69815495320619,126.186538551658));
#96497=CARTESIAN_POINT('Ctrl Pts',(-91.9572596931712,1.56810157824014,126.142790012843));
#96498=CARTESIAN_POINT('Ctrl Pts',(-91.9650060264365,1.4380472432505,126.099041151086));
#96499=CARTESIAN_POINT('Ctrl Pts',(-91.9727523597018,1.30616145387334,126.060739292754));
#96500=CARTESIAN_POINT('Ctrl Pts',(-91.9804986929671,1.17294111392645,126.028023924476));
#96501=CARTESIAN_POINT('Ctrl Pts',(-91.9882467609701,1.03969094020721,125.995301229817));
#96502=CARTESIAN_POINT('Ctrl Pts',(-91.995994828973,0.905106000826217,125.968167607892));
#96503=CARTESIAN_POINT('Ctrl Pts',(-92.003742896976,0.769694483424782,125.946711652821));
#96504=CARTESIAN_POINT('Ctrl Pts',(-92.0114991997179,0.634139049051788,
125.925232894106));
#96505=CARTESIAN_POINT('Ctrl Pts',(-92.0192555024598,0.497755668529646,
125.909443917677));
#96506=CARTESIAN_POINT('Ctrl Pts',(-92.0270118052017,0.361059320632334,
125.899381593199));
#96507=CARTESIAN_POINT('Ctrl Pts',(-92.0347722477158,0.224290013777929,
125.889313898154));
#96508=CARTESIAN_POINT('Ctrl Pts',(-92.04253269023,0.0872077972854539,125.88497895772));
#96509=CARTESIAN_POINT('Ctrl Pts',(-92.0502931327442,-0.0496722280336851,
125.886361458125));
#96510=CARTESIAN_POINT('Ctrl Pts',(-92.0580660330096,-0.186771985321104,
125.887746177843));
#96511=CARTESIAN_POINT('Ctrl Pts',(-92.065838933275,-0.323668512168345,
125.894866658936));
#96512=CARTESIAN_POINT('Ctrl Pts',(-92.0736118335404,-0.459850804667805,
125.90765557234));
#96513=CARTESIAN_POINT('Ctrl Pts',(-92.0811021693025,-0.591082527813524,
125.919979576528));
#96514=CARTESIAN_POINT('Ctrl Pts',(-92.0885925050647,-0.721650738231154,
125.937567003394));
#96515=CARTESIAN_POINT('Ctrl Pts',(-92.0960828408268,-0.851108935678263,
125.9603130701));
#96516=CARTESIAN_POINT('Ctrl Pts',(-92.1038571749458,-0.985475580027133,
125.983921560839));
#96517=CARTESIAN_POINT('Ctrl Pts',(-92.1116315090648,-1.11907201067563,
126.013162377689));
#96518=CARTESIAN_POINT('Ctrl Pts',(-92.1194058431838,-1.25138901733661,
126.047974532544));
#96519=CARTESIAN_POINT('Ctrl Pts',(-92.1271705961309,-1.38354295511239,
126.08274378453));
#96520=CARTESIAN_POINT('Ctrl Pts',(-92.1349353490778,-1.51442023174586,
126.123070614355));
#96521=CARTESIAN_POINT('Ctrl Pts',(-92.1427001020249,-1.64351939186472,
126.168842623742));
#96522=CARTESIAN_POINT('Ctrl Pts',(-92.1504571429097,-1.77249032887706,
126.214569171724));
#96523=CARTESIAN_POINT('Ctrl Pts',(-92.1582141837946,-1.89968629778918,
126.265730006846));
#96524=CARTESIAN_POINT('Ctrl Pts',(-92.1659712246795,-2.02461898113001,
126.322162379676));
#96525=CARTESIAN_POINT('Ctrl Pts',(-92.1737224159196,-2.14945745176335,
126.378552196414));
#96526=CARTESIAN_POINT('Ctrl Pts',(-92.1814736071597,-2.27203567916957,
126.44020547796));
#96527=CARTESIAN_POINT('Ctrl Pts',(-92.1892247983997,-2.39188372245534,
126.50691075506));
#96528=CARTESIAN_POINT('Ctrl Pts',(-92.1969726951767,-2.51168082712517,
126.573587680638));
#96529=CARTESIAN_POINT('Ctrl Pts',(-92.2047205919537,-2.62874971472295,
126.645312141349));
#96530=CARTESIAN_POINT('Ctrl Pts',(-92.2124684887307,-2.7426437347701,126.721826060869));
#96531=CARTESIAN_POINT('Ctrl Pts',(-92.2202147648147,-2.85651393064383,
126.798323975327));
#96532=CARTESIAN_POINT('Ctrl Pts',(-92.2279610408988,-2.96721025559948,
126.879609137975));
#96533=CARTESIAN_POINT('Ctrl Pts',(-92.2357073169828,-3.07431416622612,
126.965379571788));
#96534=CARTESIAN_POINT('Ctrl Pts',(-92.2434536502481,-3.18141886746964,
127.05115063874));
#96535=CARTESIAN_POINT('Ctrl Pts',(-92.2511999835133,-3.28493079629746,
127.141406798538));
#96536=CARTESIAN_POINT('Ctrl Pts',(-92.2589463167786,-3.3844640100063,127.235805387859));
#96537=CARTESIAN_POINT('Ctrl Pts',(-92.2666943847815,-3.4840195134881,127.330225117089));
#96538=CARTESIAN_POINT('Ctrl Pts',(-92.2744424527843,-3.57959424523284,
127.428788852805));
#96539=CARTESIAN_POINT('Ctrl Pts',(-92.2821905207872,-3.67083898066302,
127.53111692964));
#96540=CARTESIAN_POINT('Ctrl Pts',(-92.289946823529,-3.76218069208396,127.633553761973));
#96541=CARTESIAN_POINT('Ctrl Pts',(-92.2977031262709,-3.84918295364231,
127.739762635156));
#96542=CARTESIAN_POINT('Ctrl Pts',(-92.3054594290127,-3.93153638723861,
127.849330211916));
#96543=CARTESIAN_POINT('Ctrl Pts',(-92.3132198715268,-4.01393377534204,
127.95895626819));
#96544=CARTESIAN_POINT('Ctrl Pts',(-92.3209803140407,-4.09167716993482,
128.071944278102));
#96545=CARTESIAN_POINT('Ctrl Pts',(-92.3287407565548,-4.16450103035498,
128.187852595283));
#96546=CARTESIAN_POINT('Ctrl Pts',(-92.3365136568202,-4.23744179410088,
128.303946978785));
#96547=CARTESIAN_POINT('Ctrl Pts',(-92.3442865570856,-4.30544704833943,
128.422970697889));
#96548=CARTESIAN_POINT('Ctrl Pts',(-92.3520594573509,-4.36829722882561,
128.544457437531));
#96549=CARTESIAN_POINT('Ctrl Pts',(-92.3595497931137,-4.42886264694771,
128.661527828193));
#96550=CARTESIAN_POINT('Ctrl Pts',(-92.3670401288763,-4.48464115366571,
128.780884995329));
#96551=CARTESIAN_POINT('Ctrl Pts',(-92.3745304646391,-4.53547956146055,
128.902096647957));
#96552=CARTESIAN_POINT('Ctrl Pts',(-92.3831948267737,-4.59428632118831,
129.042306871712));
#96553=CARTESIAN_POINT('Ctrl Pts',(-92.3918591889083,-4.6466417660541,129.185375286934));
#96554=CARTESIAN_POINT('Ctrl Pts',(-92.4005235510429,-4.69228942413747,
129.330724630415));
#96555=CARTESIAN_POINT('Ctrl Pts',(-92.4054838689954,-4.71842255365836,
129.413936636866));
#96556=CARTESIAN_POINT('Ctrl Pts',(-92.4104441869478,-4.74235801714723,
129.497895751871));
#96557=CARTESIAN_POINT('Ctrl Pts',(-92.4154045049002,-4.764054528234,129.582490119308));
#96558=CARTESIAN_POINT('Ctrl Pts',(-90.6650630979317,-4.76405452823406,
129.582490119308));
#96559=CARTESIAN_POINT('Ctrl Pts',(-90.6728368653943,-4.7980981811203,129.715225805227));
#96560=CARTESIAN_POINT('Ctrl Pts',(-90.680610632857,-4.82655146086384,129.849234029403));
#96561=CARTESIAN_POINT('Ctrl Pts',(-90.6883844003196,-4.84935028061991,
129.984004037565));
#96562=CARTESIAN_POINT('Ctrl Pts',(-90.6935378408002,-4.86446423420885,
130.073346717156));
#96563=CARTESIAN_POINT('Ctrl Pts',(-90.6986912812809,-4.87709428164181,
130.163024053761));
#96564=CARTESIAN_POINT('Ctrl Pts',(-90.7038447217616,-4.88723437455985,
130.252886927694));
#96565=CARTESIAN_POINT('Ctrl Pts',(-90.7142766691775,-4.90776064560362,
130.434793515931));
#96566=CARTESIAN_POINT('Ctrl Pts',(-90.7247086165934,-4.91813355712363,
130.617867092848));
#96567=CARTESIAN_POINT('Ctrl Pts',(-90.735140564009,-4.91824902518994,130.801264052022));
#96568=CARTESIAN_POINT('',(-90.3898594359623,-4.9182480484996,130.808741933566));
#96569=CARTESIAN_POINT('Ctrl Pts',(-90.3197845579208,-4.76405452823393,
129.582490119308));
#96570=CARTESIAN_POINT('Ctrl Pts',(-90.3274229448282,-4.79767960507908,
129.713593783595));
#96571=CARTESIAN_POINT('Ctrl Pts',(-90.3350613317357,-4.82587730052624,
129.846042274493));
#96572=CARTESIAN_POINT('Ctrl Pts',(-90.3426997186431,-4.84855894226438,
129.979339862743));
#96573=CARTESIAN_POINT('Ctrl Pts',(-90.3505596715296,-4.87189850827637,
130.116504001748));
#96574=CARTESIAN_POINT('Ctrl Pts',(-90.3584196244162,-4.88939706813633,
130.254566794181));
#96575=CARTESIAN_POINT('Ctrl Pts',(-90.3662795773027,-4.90101530917749,
130.392982443974));
#96576=CARTESIAN_POINT('Ctrl Pts',(-90.3741395301893,-4.91263355021866,
130.531398093767));
#96577=CARTESIAN_POINT('Ctrl Pts',(-90.3819994830757,-4.91837149578089,
130.670166137992));
#96578=CARTESIAN_POINT('Ctrl Pts',(-90.3898594359622,-4.9182480484996,130.808741933566));
#96579=CARTESIAN_POINT('Ctrl Pts',(-90.3898594359916,-4.91824804849914,
130.808741934084));
#96580=CARTESIAN_POINT('Ctrl Pts',(-90.4010783904105,-4.91807184520559,
131.006538989173));
#96581=CARTESIAN_POINT('Ctrl Pts',(-90.4122973448293,-4.90596017356694,
131.203826077175));
#96582=CARTESIAN_POINT('Ctrl Pts',(-90.4235162992482,-4.8821162522506,131.399443773109));
#96583=CARTESIAN_POINT('Ctrl Pts',(-90.4306728975352,-4.86690615689988,
131.524228776714));
#96584=CARTESIAN_POINT('Ctrl Pts',(-90.4378294958223,-4.84692287525181,
131.648335290403));
#96585=CARTESIAN_POINT('Ctrl Pts',(-90.4449860941093,-4.82222831375912,
131.77146823954));
#96586=CARTESIAN_POINT('Ctrl Pts',(-90.4527604282283,-4.79540219270726,
131.905229650933));
#96587=CARTESIAN_POINT('Ctrl Pts',(-90.4605347623474,-4.76296385051995,
132.038085910132));
#96588=CARTESIAN_POINT('Ctrl Pts',(-90.4683090964665,-4.72498647738317,
132.169529417036));
#96589=CARTESIAN_POINT('Ctrl Pts',(-90.4760738494135,-4.68705590796465,
132.300810931565));
#96590=CARTESIAN_POINT('Ctrl Pts',(-90.4838386023605,-4.64359999749885,
132.430682786054));
#96591=CARTESIAN_POINT('Ctrl Pts',(-90.4916033553075,-4.59474314544142,
132.558646366787));
#96592=CARTESIAN_POINT('Ctrl Pts',(-90.4993603961925,-4.54593481869822,
132.686482852287));
#96593=CARTESIAN_POINT('Ctrl Pts',(-90.5071174370776,-4.49173636409581,
132.812414472927));
#96594=CARTESIAN_POINT('Ctrl Pts',(-90.5148744779625,-4.43232220247175,
132.935956957396));
#96595=CARTESIAN_POINT('Ctrl Pts',(-90.5226256692026,-4.37295284552907,
133.059406277516));
#96596=CARTESIAN_POINT('Ctrl Pts',(-90.5303768604427,-4.30837577913205,
133.180469696662));
#96597=CARTESIAN_POINT('Ctrl Pts',(-90.5381280516828,-4.23881368892118,
133.298682483949));
#96598=CARTESIAN_POINT('Ctrl Pts',(-90.5458759484599,-4.16928116445436,
133.416845027647));
#96599=CARTESIAN_POINT('Ctrl Pts',(-90.5536238452369,-4.0947680281073,133.532159013008));
#96600=CARTESIAN_POINT('Ctrl Pts',(-90.561371742014,-4.01554300026345,133.644184111295));
#96601=CARTESIAN_POINT('Ctrl Pts',(-90.569118018098,-3.93633454458753,133.756185776347));
#96602=CARTESIAN_POINT('Ctrl Pts',(-90.5768642941821,-3.85241638348156,
133.86489960372));
#96603=CARTESIAN_POINT('Ctrl Pts',(-90.5846105702662,-3.76410045089587,
133.969914417151));
#96604=CARTESIAN_POINT('Ctrl Pts',(-90.5923569035315,-3.67578386638214,
134.074930005776));
#96605=CARTESIAN_POINT('Ctrl Pts',(-90.6001032367967,-3.58306969724902,
134.176246226755));
#96606=CARTESIAN_POINT('Ctrl Pts',(-90.607849570062,-3.48630976970296,134.273485471499));
#96607=CARTESIAN_POINT('Ctrl Pts',(-90.615597638065,-3.38952817344214,134.370746492297));
#96608=CARTESIAN_POINT('Ctrl Pts',(-90.6233457060679,-3.28869929161189,
134.463928442994));
#96609=CARTESIAN_POINT('Ctrl Pts',(-90.6310937740708,-3.184211060673,134.5526913105));
#96610=CARTESIAN_POINT('Ctrl Pts',(-90.6388500768127,-3.07961177839841,
134.641548516238));
#96611=CARTESIAN_POINT('Ctrl Pts',(-90.6466063795545,-2.97134567635988,
134.725977003188));
#96612=CARTESIAN_POINT('Ctrl Pts',(-90.6543626822963,-2.85983339702102,
134.805677401299));
#96613=CARTESIAN_POINT('Ctrl Pts',(-90.6621231248104,-2.7482616002211,134.885420337912));
#96614=CARTESIAN_POINT('Ctrl Pts',(-90.6698835673247,-2.63344050095503,
134.960429943632));
#96615=CARTESIAN_POINT('Ctrl Pts',(-90.6776440098388,-2.51581799065118,
135.030451352562));
#96616=CARTESIAN_POINT('Ctrl Pts',(-90.6854169101042,-2.39800666225207,
135.100585166073));
#96617=CARTESIAN_POINT('Ctrl Pts',(-90.6931898103695,-2.27738528044665,
135.165714595404));
#96618=CARTESIAN_POINT('Ctrl Pts',(-90.7009627106349,-2.15442529494813,
135.225631329815));
#96619=CARTESIAN_POINT('Ctrl Pts',(-90.7084530463972,-2.03593521463467,
135.283369940011));
#96620=CARTESIAN_POINT('Ctrl Pts',(-90.7159433821596,-1.91527388905724,
135.336268140986));
#96621=CARTESIAN_POINT('Ctrl Pts',(-90.7234337179219,-1.79287716078718,
135.384183163127));
#96622=CARTESIAN_POINT('Ctrl Pts',(-90.731208052041,-1.66583972336827,135.433914897893));
#96623=CARTESIAN_POINT('Ctrl Pts',(-90.7389823861601,-1.53653027351599,
135.478435655201));
#96624=CARTESIAN_POINT('Ctrl Pts',(-90.7467567202791,-1.40541543065441,
135.517532641774));
#96625=CARTESIAN_POINT('Ctrl Pts',(-90.7545214732262,-1.27446217511859,
135.556581444805));
#96626=CARTESIAN_POINT('Ctrl Pts',(-90.7622862261733,-1.14170832469778,
135.590219666243));
#96627=CARTESIAN_POINT('Ctrl Pts',(-90.7700509791204,-1.00764061817782,
135.618282453979));
#96628=CARTESIAN_POINT('Ctrl Pts',(-90.7778080200054,-0.873706069594,135.64631736936));
#96629=CARTESIAN_POINT('Ctrl Pts',(-90.7855650608904,-0.73846064199694,
135.668787791529));
#96630=CARTESIAN_POINT('Ctrl Pts',(-90.7933221017754,-0.602406045278277,
135.685578705207));
#96631=CARTESIAN_POINT('Ctrl Pts',(-90.8010732930155,-0.466454048389164,
135.702356956726));
#96632=CARTESIAN_POINT('Ctrl Pts',(-90.8088244842557,-0.329694483397402,
135.713464177035));
#96633=CARTESIAN_POINT('Ctrl Pts',(-90.8165756754958,-0.192638708584791,
135.718836519476));
#96634=CARTESIAN_POINT('Ctrl Pts',(-90.8243235722729,-0.0556411861327437,
135.724206578528));
#96635=CARTESIAN_POINT('Ctrl Pts',(-90.8320714690499,0.0816519058931658,
135.723846592386));
#96636=CARTESIAN_POINT('Ctrl Pts',(-90.839819365827,0.218724856527024,135.717744634681));
#96637=CARTESIAN_POINT('Ctrl Pts',(-90.8475656419111,0.355769134454561,
135.711643953374));
#96638=CARTESIAN_POINT('Ctrl Pts',(-90.8553119179952,0.492592972252758,
135.699803706927));
#96639=CARTESIAN_POINT('Ctrl Pts',(-90.8630581940793,0.628681827765329,
135.682264083394));
#96640=CARTESIAN_POINT('Ctrl Pts',(-90.8708045273446,0.764771687855103,
135.664724330387));
#96641=CARTESIAN_POINT('Ctrl Pts',(-90.87855086061,0.900126167075165,135.641485166318));
#96642=CARTESIAN_POINT('Ctrl Pts',(-90.8862971938754,1.03423740196892,135.612638485875));
#96643=CARTESIAN_POINT('Ctrl Pts',(-90.8940452618784,1.16837867014369,135.583785345417));
#96644=CARTESIAN_POINT('Ctrl Pts',(-90.9017933298814,1.3012757578266,135.549322271957));
#96645=CARTESIAN_POINT('Ctrl Pts',(-90.9095413978843,1.43243291324453,135.509391862048));
#96646=CARTESIAN_POINT('Ctrl Pts',(-90.9172977006262,1.56372946404785,135.469419013624));
#96647=CARTESIAN_POINT('Ctrl Pts',(-90.925054003368,1.69328201395639,135.423967335201));
#96648=CARTESIAN_POINT('Ctrl Pts',(-90.9328103061098,1.82061132694102,135.37322890837));
#96649=CARTESIAN_POINT('Ctrl Pts',(-90.940570748624,1.94800859941416,135.322463400913));
#96650=CARTESIAN_POINT('Ctrl Pts',(-90.9483311911382,2.07317991390372,135.266405682301));
#96651=CARTESIAN_POINT('Ctrl Pts',(-90.9560916336523,2.19566874825433,135.205294815034));
#96652=CARTESIAN_POINT('Ctrl Pts',(-90.9638645339178,2.3183542125559,135.144085847177));
#96653=CARTESIAN_POINT('Ctrl Pts',(-90.9716374341832,2.43834824922074,135.077807709916));
#96654=CARTESIAN_POINT('Ctrl Pts',(-90.9794103344487,2.55522077043769,135.006744450205));
#96655=CARTESIAN_POINT('Ctrl Pts',(-90.9869006702107,2.66784468112461,134.938264518981));
#96656=CARTESIAN_POINT('Ctrl Pts',(-90.9943910059728,2.77756982954708,134.865341498206));
#96657=CARTESIAN_POINT('Ctrl Pts',(-91.0018813417348,2.88404051603024,134.788264904117));
#96658=CARTESIAN_POINT('Ctrl Pts',(-91.0096556758539,2.99454807095201,134.708265927535));
#96659=CARTESIAN_POINT('Ctrl Pts',(-91.017430009973,3.10189956117272,134.623538781946));
#96660=CARTESIAN_POINT('Ctrl Pts',(-91.025204344092,3.20566373848533,134.53436102752));
#96661=CARTESIAN_POINT('Ctrl Pts',(-91.0329690970391,3.30930003572306,134.445293176708));
#96662=CARTESIAN_POINT('Ctrl Pts',(-91.0407338499863,3.40935752294812,134.35178588291));
#96663=CARTESIAN_POINT('Ctrl Pts',(-91.0484986029334,3.50543441121012,134.254159546664));
#96664=CARTESIAN_POINT('Ctrl Pts',(-91.0562556438184,3.60141587455225,134.156630174271));
#96665=CARTESIAN_POINT('Ctrl Pts',(-91.0640126847033,3.69342433428844,134.054990177737));
#96666=CARTESIAN_POINT('Ctrl Pts',(-91.0717697255883,3.78109183835352,133.949599491235));
#96667=CARTESIAN_POINT('Ctrl Pts',(-91.0795209168284,3.86869323167196,133.844288280669));
#96668=CARTESIAN_POINT('Ctrl Pts',(-91.0872721080687,3.95195993610689,133.735232309295));
#96669=CARTESIAN_POINT('Ctrl Pts',(-91.0950232993088,4.03056183401493,133.62282728664));
#96670=CARTESIAN_POINT('Ctrl Pts',(-91.1027711960859,4.10913032401948,133.510470039119));
#96671=CARTESIAN_POINT('Ctrl Pts',(-91.1105190928628,4.18303772729247,133.394766891152));
#96672=CARTESIAN_POINT('Ctrl Pts',(-91.1182669896399,4.25199525546935,133.276145278487));
#96673=CARTESIAN_POINT('Ctrl Pts',(-91.126013265724,4.32093835921788,133.157548478907));
#96674=CARTESIAN_POINT('Ctrl Pts',(-91.1337595418081,4.38493345098744,133.036034766697));
#96675=CARTESIAN_POINT('Ctrl Pts',(-91.1415058178922,4.44373621952061,132.912058763369));
#96676=CARTESIAN_POINT('Ctrl Pts',(-91.1492521511576,4.50253942212255,132.788081844878));
#96677=CARTESIAN_POINT('Ctrl Pts',(-91.156998484423,4.55615005745953,132.661642952245));
#96678=CARTESIAN_POINT('Ctrl Pts',(-91.1647448176884,4.60437092653096,132.533219036702));
#96679=CARTESIAN_POINT('Ctrl Pts',(-91.1724928856914,4.65260259433161,132.404766361514));
#96680=CARTESIAN_POINT('Ctrl Pts',(-91.1802409536943,4.69544195666949,132.274328144793));
#96681=CARTESIAN_POINT('Ctrl Pts',(-91.1879890216973,4.73274101811986,132.142398553465));
#96682=CARTESIAN_POINT('Ctrl Pts',(-91.1957453244391,4.77007972145655,132.010328745799));
#96683=CARTESIAN_POINT('Ctrl Pts',(-91.2035016271809,4.80186625486287,131.876764774035));
#96684=CARTESIAN_POINT('Ctrl Pts',(-91.2112579299227,4.82800318324298,131.74221365781));
#96685=CARTESIAN_POINT('Ctrl Pts',(-91.2190183724369,4.8541540616888,131.607590727604));
#96686=CARTESIAN_POINT('Ctrl Pts',(-91.2267788149511,4.87464926834414,131.471979989492));
#96687=CARTESIAN_POINT('Ctrl Pts',(-91.2345392574652,4.88944317188505,131.335894747615));
#96688=CARTESIAN_POINT('Ctrl Pts',(-91.2423121577307,4.90426082391327,131.199591049626));
#96689=CARTESIAN_POINT('Ctrl Pts',(-91.2500850579961,4.91335885777632,131.06281171605));
#96690=CARTESIAN_POINT('Ctrl Pts',(-91.2578579582616,4.91674377725259,130.926072126257));
#96691=CARTESIAN_POINT('Ctrl Pts',(-91.2653482940236,4.92000564637981,130.79430336498));
#96692=CARTESIAN_POINT('Ctrl Pts',(-91.2728386297856,4.91796256662295,130.662571816062));
#96693=CARTESIAN_POINT('Ctrl Pts',(-91.2803289655477,4.9106658518279,130.531333230311));
#96694=CARTESIAN_POINT('Ctrl Pts',(-91.2881032996668,4.90309247987363,130.395118693693));
#96695=CARTESIAN_POINT('Ctrl Pts',(-91.2958776337859,4.88983523536181,130.259003752851));
#96696=CARTESIAN_POINT('Ctrl Pts',(-91.3036519679049,4.87089453733705,130.123501257169));
#96697=CARTESIAN_POINT('Ctrl Pts',(-91.311416720852,4.85197718202983,129.988165756203));
#96698=CARTESIAN_POINT('Ctrl Pts',(-91.3191814737991,4.82739036337932,129.853441582085));
#96699=CARTESIAN_POINT('Ctrl Pts',(-91.3269462267462,4.79718646668753,129.719839955554));
#96700=CARTESIAN_POINT('Ctrl Pts',(-91.3347032676312,4.76701256893165,129.586371024042));
#96701=CARTESIAN_POINT('Ctrl Pts',(-91.3424603085162,4.73123278117247,129.454022800229));
#96702=CARTESIAN_POINT('Ctrl Pts',(-91.3502173494012,4.68995103914371,129.323299405821));
#96703=CARTESIAN_POINT('Ctrl Pts',(-91.3579685406414,4.64870042799779,129.192674590942));
#96704=CARTESIAN_POINT('Ctrl Pts',(-91.3657197318814,4.60195623830484,129.063672537898));
#96705=CARTESIAN_POINT('Ctrl Pts',(-91.3734709231216,4.54987295504699,128.936784874676));
#96706=CARTESIAN_POINT('Ctrl Pts',(-91.3812188198986,4.49781180857398,128.809951142096));
#96707=CARTESIAN_POINT('Ctrl Pts',(-91.3889667166757,4.44041623006354,128.685230372873));
#96708=CARTESIAN_POINT('Ctrl Pts',(-91.3967146134528,4.37788973615141,128.5630965723));
#96709=CARTESIAN_POINT('Ctrl Pts',(-91.4044608895368,4.31537632143389,128.440988319486));
#96710=CARTESIAN_POINT('Ctrl Pts',(-91.412207165621,4.24773430417261,128.321466306758));
#96711=CARTESIAN_POINT('Ctrl Pts',(-91.4199534417051,4.17521411411934,128.204981814129));
#96712=CARTESIAN_POINT('Ctrl Pts',(-91.4276997749704,4.1026933887384,128.088496461638));
#96713=CARTESIAN_POINT('Ctrl Pts',(-91.4354461082358,4.02529462534275,127.975049005887));
#96714=CARTESIAN_POINT('Ctrl Pts',(-91.4431924415012,3.94331250563561,127.865063159771));
#96715=CARTESIAN_POINT('Ctrl Pts',(-91.4509405095041,3.8613120266013,127.755052683089));
#96716=CARTESIAN_POINT('Ctrl Pts',(-91.458688577507,3.77472638242484,127.648505672012));
#96717=CARTESIAN_POINT('Ctrl Pts',(-91.46643664551,3.6838913345952,127.545813748578));
#96718=CARTESIAN_POINT('Ctrl Pts',(-91.4741929482519,3.59295974619566,127.443012682945));
#96719=CARTESIAN_POINT('Ctrl Pts',(-91.4819492509938,3.49776999175757,127.344075182929));
#96720=CARTESIAN_POINT('Ctrl Pts',(-91.4897055537357,3.39869597521147,127.249357279933));
#96721=CARTESIAN_POINT('Ctrl Pts',(-91.4974659962499,3.29956907987941,127.15458882314));
#96722=CARTESIAN_POINT('Ctrl Pts',(-91.505226438764,3.19655408503046,127.064044708901));
#96723=CARTESIAN_POINT('Ctrl Pts',(-91.5129868812782,3.09005818312961,126.978040781565));
#96724=CARTESIAN_POINT('Ctrl Pts',(-91.5207597815437,2.98339132455306,126.89189879309));
#96725=CARTESIAN_POINT('Ctrl Pts',(-91.5285326818091,2.87323270695781,126.810311788713));
#96726=CARTESIAN_POINT('Ctrl Pts',(-91.5363055820745,2.76001944905717,126.733552871759));
#96727=CARTESIAN_POINT('Ctrl Pts',(-91.5437959178365,2.65092177824852,126.65958433478));
#96728=CARTESIAN_POINT('Ctrl Pts',(-91.5512862535985,2.5389879607995,126.590099115731));
#96729=CARTESIAN_POINT('Ctrl Pts',(-91.5587765893605,2.42462916915919,126.525300387263));
#96730=CARTESIAN_POINT('Ctrl Pts',(-91.5665509234796,2.30593442917507,126.45804479531));
#96731=CARTESIAN_POINT('Ctrl Pts',(-91.5743252575987,2.18425120998468,126.395625040265));
#96732=CARTESIAN_POINT('Ctrl Pts',(-91.5820995917178,2.06001121280276,126.338317977193));
#96733=CARTESIAN_POINT('Ctrl Pts',(-91.5898643446648,1.93592433031373,126.281081539955));
#96734=CARTESIAN_POINT('Ctrl Pts',(-91.597629097612,1.80928729099459,126.228945419889));
#96735=CARTESIAN_POINT('Ctrl Pts',(-91.6053938505591,1.68055851486637,126.182141871054));
#96736=CARTESIAN_POINT('Ctrl Pts',(-91.6131508914441,1.55195759397336,126.135384808163));
#96737=CARTESIAN_POINT('Ctrl Pts',(-91.6209079323291,1.42126943572979,126.093949909185));
#96738=CARTESIAN_POINT('Ctrl Pts',(-91.6286649732141,1.28897435180654,126.05802222014));
#96739=CARTESIAN_POINT('Ctrl Pts',(-91.6364161644542,1.156779032635,126.022121624444));
#96740=CARTESIAN_POINT('Ctrl Pts',(-91.6441673556943,1.02297957556137,125.991720074376));
#96741=CARTESIAN_POINT('Ctrl Pts',(-91.6519185469345,0.888073104041771,
125.966953334281));
#96742=CARTESIAN_POINT('Ctrl Pts',(-91.6596664437115,0.753223971371501,
125.942197120712));
#96743=CARTESIAN_POINT('Ctrl Pts',(-91.6674143404886,0.617269143798842,
125.923071024201));
#96744=CARTESIAN_POINT('Ctrl Pts',(-91.6751622372657,0.480717421113914,
125.909660031878));
#96745=CARTESIAN_POINT('Ctrl Pts',(-91.6829085133498,0.344194262105658,
125.896251844845));
#96746=CARTESIAN_POINT('Ctrl Pts',(-91.6906547894339,0.207074845180411,
125.888556422322));
#96747=CARTESIAN_POINT('Ctrl Pts',(-91.698401065518,0.0698742083914101,
125.886606998534));
#96748=CARTESIAN_POINT('Ctrl Pts',(-91.7061473987833,-0.0673274411813373,
125.884657560356));
#96749=CARTESIAN_POINT('Ctrl Pts',(-91.7138937320486,-0.204609920888443,
125.888454211106));
#96750=CARTESIAN_POINT('Ctrl Pts',(-91.7216400653139,-0.341457466412116,
125.897978053891));
#96751=CARTESIAN_POINT('Ctrl Pts',(-91.7293881333169,-0.478335657994589,
125.907504029475));
#96752=CARTESIAN_POINT('Ctrl Pts',(-91.7371362013198,-0.61477833163074,
125.922759722111));
#96753=CARTESIAN_POINT('Ctrl Pts',(-91.7448842693228,-0.750274517323372,
125.943674327426));
#96754=CARTESIAN_POINT('Ctrl Pts',(-91.7526405720646,-0.885914709974768,
125.964611161033));
#96755=CARTESIAN_POINT('Ctrl Pts',(-91.7603968748065,-1.02060601820641,
125.991218861914));
#96756=CARTESIAN_POINT('Ctrl Pts',(-91.7681531775484,-1.15384679850733,
126.023375297773));
#96757=CARTESIAN_POINT('Ctrl Pts',(-91.7759136200625,-1.2871586934245,126.055548896491));
#96758=CARTESIAN_POINT('Ctrl Pts',(-91.7836740625767,-1.41901814207316,
126.093277023784));
#96759=CARTESIAN_POINT('Ctrl Pts',(-91.7914345050908,-1.54893931818225,
126.136387818685));
#96760=CARTESIAN_POINT('Ctrl Pts',(-91.7992074053563,-1.67906905529709,
126.179567818862));
#96761=CARTESIAN_POINT('Ctrl Pts',(-91.8069803056217,-1.80725393632791,
126.22814761496));
#96762=CARTESIAN_POINT('Ctrl Pts',(-91.8147532058871,-1.93302791836956,
126.281907065643));
#96763=CARTESIAN_POINT('Ctrl Pts',(-91.8222435416493,-2.05422969936048,
126.333712224882));
#96764=CARTESIAN_POINT('Ctrl Pts',(-91.8297338774114,-2.17319254453902,
126.390326857467));
#96765=CARTESIAN_POINT('Ctrl Pts',(-91.8372242131735,-2.28952327024669,
126.45151485215));
#96766=CARTESIAN_POINT('Ctrl Pts',(-91.8449994603469,-2.41027889121765,
126.515030266921));
#96767=CARTESIAN_POINT('Ctrl Pts',(-91.8527747075203,-2.52858075501139,
126.583675067432));
#96768=CARTESIAN_POINT('Ctrl Pts',(-91.8605499546937,-2.64396242739829,
126.657235620052));
#96769=CARTESIAN_POINT('Ctrl Pts',(-91.8683154188557,-2.75919892366504,
126.730703616936));
#96770=CARTESIAN_POINT('Ctrl Pts',(-91.8760808830178,-2.87152221321195,
126.809074849936));
#96771=CARTESIAN_POINT('Ctrl Pts',(-91.8838463471797,-2.98048898906497,
126.892089097264));
#96772=CARTESIAN_POINT('Ctrl Pts',(-91.8916025221625,-3.08932541702299,
126.975004041551));
#96773=CARTESIAN_POINT('Ctrl Pts',(-91.8993586971453,-3.19481301885132,
127.062550703165));
#96774=CARTESIAN_POINT('Ctrl Pts',(-91.9071148721281,-3.29653663340567,
127.154425099353));
#96775=CARTESIAN_POINT('Ctrl Pts',(-91.9148657790816,-3.39819115681903,
127.246237094034));
#96776=CARTESIAN_POINT('Ctrl Pts',(-91.9226166860351,-3.49608648998639,
127.342370714792));
#96777=CARTESIAN_POINT('Ctrl Pts',(-91.9303675929886,-3.58983974795637,
127.44248113631));
#96778=CARTESIAN_POINT('Ctrl Pts',(-91.9381149140952,-3.68354963231496,
127.542545243165));
#96779=CARTESIAN_POINT('Ctrl Pts',(-91.9458622352018,-3.77312098801117,
127.646582205093));
#96780=CARTESIAN_POINT('Ctrl Pts',(-91.9536095563085,-3.85820737238423,
127.754209976339));
#96781=CARTESIAN_POINT('Ctrl Pts',(-91.9613549709857,-3.94327281904472,
127.861811262978));
#96782=CARTESIAN_POINT('Ctrl Pts',(-91.969100385663,-4.02385524938429,127.973001293432));
#96783=CARTESIAN_POINT('Ctrl Pts',(-91.9768458003403,-4.09964841115681,
128.087364856178));
#96784=CARTESIAN_POINT('Ctrl Pts',(-91.984593776484,-4.17546663829348,128.201766239807));
#96785=CARTESIAN_POINT('Ctrl Pts',(-91.9923417526278,-4.24649221036113,
128.319342930459));
#96786=CARTESIAN_POINT('Ctrl Pts',(-92.0000897287715,-4.31246207454953,
128.439650504662));
#96787=CARTESIAN_POINT('Ctrl Pts',(-92.0078387166846,-4.3784405534115,128.559973789227));
#96788=CARTESIAN_POINT('Ctrl Pts',(-92.0155877045976,-4.43936182826284,
128.683028320924));
#96789=CARTESIAN_POINT('Ctrl Pts',(-92.0233366925106,-4.49500920693038,
128.808345764888));
#96790=CARTESIAN_POINT('Ctrl Pts',(-92.0310930625346,-4.55070959834326,
128.933782593123));
#96791=CARTESIAN_POINT('Ctrl Pts',(-92.0388494325587,-4.60112590169011,
129.061486280616));
#96792=CARTESIAN_POINT('Ctrl Pts',(-92.0466058025827,-4.64608972588001,
129.190968748995));
#96793=CARTESIAN_POINT('Ctrl Pts',(-92.0543278308942,-4.69085447051105,
129.319877927331));
#96794=CARTESIAN_POINT('Ctrl Pts',(-92.0620498592056,-4.7302148646397,129.450549784542));
#96795=CARTESIAN_POINT('Ctrl Pts',(-92.0697718875171,-4.76405452823417,
129.582490119309));
#96796=CARTESIAN_POINT('Origin',(213.235140564004,0.,130.804360617566));
#96797=CARTESIAN_POINT('',(-94.1652277315646,-4.76405452823406,129.582490119308));
#96798=CARTESIAN_POINT('',(-93.8201028328085,-4.76405452823393,129.582490119308));
#96799=CARTESIAN_POINT('',(213.235140564004,-4.76405452823405,129.582490119308));
#96800=CARTESIAN_POINT('',(-92.4851405639578,-4.91824929378548,130.801724962307));
#96801=CARTESIAN_POINT('Ctrl Pts',(-92.485140564009,-4.91824929378596,130.801724963215));
#96802=CARTESIAN_POINT('Ctrl Pts',(-92.4929859638921,-4.91832387304165,
130.940893201087));
#96803=CARTESIAN_POINT('Ctrl Pts',(-92.5008313637752,-4.91248718749969,
131.08006072528));
#96804=CARTESIAN_POINT('Ctrl Pts',(-92.5086767636583,-4.90076596850035,
131.218698625102));
#96805=CARTESIAN_POINT('Ctrl Pts',(-92.5165240638458,-4.88904191039983,
131.357370105649));
#96806=CARTESIAN_POINT('Ctrl Pts',(-92.5243713640332,-4.87143051122289,
131.495511330634));
#96807=CARTESIAN_POINT('Ctrl Pts',(-92.5322186642207,-4.84801037639572,
131.632598779485));
#96808=CARTESIAN_POINT('Ctrl Pts',(-92.5400693938123,-4.82458000656991,
131.769746137891));
#96809=CARTESIAN_POINT('Ctrl Pts',(-92.547920123404,-4.7953359082831,131.905838431539));
#96810=CARTESIAN_POINT('Ctrl Pts',(-92.5557708529956,-4.76040771941291,
132.040362805045));
#96811=CARTESIAN_POINT('Ctrl Pts',(-92.5638714559503,-4.72436783462716,
132.179168826166));
#96812=CARTESIAN_POINT('Ctrl Pts',(-92.5719720589049,-4.68227613829448,
132.316305040936));
#96813=CARTESIAN_POINT('Ctrl Pts',(-92.5800726618596,-4.63433002919282,
132.451226806126));
#96814=CARTESIAN_POINT('Ctrl Pts',(-92.5879396713312,-4.58776652070624,
132.582257892405));
#96815=CARTESIAN_POINT('Ctrl Pts',(-92.5958066808029,-4.53568179255408,
132.711200161232));
#96816=CARTESIAN_POINT('Ctrl Pts',(-92.6036736902745,-4.47830470860807,
132.837577280728));
#96817=CARTESIAN_POINT('Ctrl Pts',(-92.6118910899708,-4.41837209585412,
132.969583134682));
#96818=CARTESIAN_POINT('Ctrl Pts',(-92.6201084896671,-4.35266507332881,
133.098789662325));
#96819=CARTESIAN_POINT('Ctrl Pts',(-92.6283258893634,-4.28149618872812,
133.224685688379));
#96820=CARTESIAN_POINT('Ctrl Pts',(-92.6365432890597,-4.21032730412744,
133.350581714433));
#96821=CARTESIAN_POINT('Ctrl Pts',(-92.6447606887559,-4.13369686372427,
133.473166887299));
#96822=CARTESIAN_POINT('Ctrl Pts',(-92.6529780884522,-4.05196604076127,
133.591967883129));
#96823=CARTESIAN_POINT('Ctrl Pts',(-92.6607524225715,-3.97464197852288,
133.704363369464));
#96824=CARTESIAN_POINT('Ctrl Pts',(-92.6685267566907,-3.89251537202124,
133.813717162985));
#96825=CARTESIAN_POINT('Ctrl Pts',(-92.6763010908099,-3.80585335273085,
133.919591478996));
#96826=CARTESIAN_POINT('Ctrl Pts',(-92.6840658437571,-3.71929813663427,
134.025335314375));
#96827=CARTESIAN_POINT('Ctrl Pts',(-92.6918305967042,-3.62821887443087,
134.12760790474));
#96828=CARTESIAN_POINT('Ctrl Pts',(-92.6995953496514,-3.53292623256085,
134.225999888118));
#96829=CARTESIAN_POINT('Ctrl Pts',(-92.7073523905365,-3.43772823668586,
134.324294147191));
#96830=CARTESIAN_POINT('Ctrl Pts',(-92.7151094314216,-3.33832545929679,
134.41871519043));
#96831=CARTESIAN_POINT('Ctrl Pts',(-92.7228664723067,-3.23506890107839,
134.508886534303));
#96832=CARTESIAN_POINT('Ctrl Pts',(-92.730617663547,-3.1318902094339,134.598989879264));
#96833=CARTESIAN_POINT('Ctrl Pts',(-92.7383688547872,-3.02486381479887,
134.684849647559));
#96834=CARTESIAN_POINT('Ctrl Pts',(-92.7461200460275,-2.91437739083234,
134.766126320672));
#96835=CARTESIAN_POINT('Ctrl Pts',(-92.7538679428047,-2.80393792654287,
134.847368449031));
#96836=CARTESIAN_POINT('Ctrl Pts',(-92.7616158395819,-2.69004167211494,
134.924031125321));
#96837=CARTESIAN_POINT('Ctrl Pts',(-92.7693637363591,-2.57310901008165,
134.995815387063));
#96838=CARTESIAN_POINT('Ctrl Pts',(-92.7771100124433,-2.4562008078408,135.067584633084));
#96839=CARTESIAN_POINT('Ctrl Pts',(-92.7848562885275,-2.33625779432396,
135.134477289891));
#96840=CARTESIAN_POINT('Ctrl Pts',(-92.7926025646117,-2.21372859732735,
135.196238206921));
#96841=CARTESIAN_POINT('Ctrl Pts',(-92.8003488978771,-2.09119849584788,
135.257999579855));
#96842=CARTESIAN_POINT('Ctrl Pts',(-92.8080952311427,-1.9660825219171,135.314628961446));
#96843=CARTESIAN_POINT('Ctrl Pts',(-92.8158415644081,-1.83885275718515,
135.365917763968));
#96844=CARTESIAN_POINT('Ctrl Pts',(-92.8235896324112,-1.71159450022936,
135.417218052262));
#96845=CARTESIAN_POINT('Ctrl Pts',(-92.8313377004143,-1.5822218730646,135.463175235465));
#96846=CARTESIAN_POINT('Ctrl Pts',(-92.8390857684174,-1.45122534882768,
135.503629502129));
#96847=CARTESIAN_POINT('Ctrl Pts',(-92.8468420711594,-1.32008959992611,
135.544126764069));
#96848=CARTESIAN_POINT('Ctrl Pts',(-92.8545983739013,-1.1873268804404,135.579109310784));
#96849=CARTESIAN_POINT('Ctrl Pts',(-92.8623546766433,-1.05344172582442,
135.608467568165));
#96850=CARTESIAN_POINT('Ctrl Pts',(-92.8701151191575,-0.919485112670212,
135.637841494932));
#96851=CARTESIAN_POINT('Ctrl Pts',(-92.8778755616718,-0.784405255546721,
135.661585083268));
#96852=CARTESIAN_POINT('Ctrl Pts',(-92.8856360041861,-0.64871421574871,
135.679640397105));
#96853=CARTESIAN_POINT('Ctrl Pts',(-92.8934089044516,-0.512805352647534,
135.697724694936));
#96854=CARTESIAN_POINT('Ctrl Pts',(-92.9011818047172,-0.376283735864319,
135.710102435652));
#96855=CARTESIAN_POINT('Ctrl Pts',(-92.9089547049827,-0.239664752427623,
135.716767753476));
#96856=CARTESIAN_POINT('Ctrl Pts',(-92.9164450407436,-0.108012213183497,
135.723190770208));
#96857=CARTESIAN_POINT('Ctrl Pts',(-92.9239353765044,0.0237304285630812,
135.724309472757));
#96858=CARTESIAN_POINT('Ctrl Pts',(-92.9314257122653,0.155106321858892,
135.720164223429));
#96859=CARTESIAN_POINT('Ctrl Pts',(-92.9392000463844,0.291463372101913,
135.715861805713));
#96860=CARTESIAN_POINT('Ctrl Pts',(-92.9469743805035,0.427857252518841,
135.70587476223));
#96861=CARTESIAN_POINT('Ctrl Pts',(-92.9547487146226,0.56377525135831,135.690191204934));
#96862=CARTESIAN_POINT('Ctrl Pts',(-92.9625134675698,0.699525743411182,
135.674526976219));
#96863=CARTESIAN_POINT('Ctrl Pts',(-92.9702782205169,0.8348011361504,135.653180246668));
#96864=CARTESIAN_POINT('Ctrl Pts',(-92.9780429734641,0.969089098953742,
135.626191118609));
#96865=CARTESIAN_POINT('Ctrl Pts',(-92.9858000143491,1.1032436850593,135.599228796532));
#96866=CARTESIAN_POINT('Ctrl Pts',(-92.9935570552341,1.23641241210438,135.566635304915));
#96867=CARTESIAN_POINT('Ctrl Pts',(-93.0013140961192,1.36808880938738,135.52850245203));
#96868=CARTESIAN_POINT('Ctrl Pts',(-93.0090652873593,1.49966590847509,135.490398355425));
#96869=CARTESIAN_POINT('Ctrl Pts',(-93.0168164785995,1.62975254378082,135.446763320479));
#96870=CARTESIAN_POINT('Ctrl Pts',(-93.0245676698397,1.75785352167992,135.397739989969));
#96871=CARTESIAN_POINT('Ctrl Pts',(-93.0323155666168,1.88590005324603,135.348737495682));
#96872=CARTESIAN_POINT('Ctrl Pts',(-93.040063463394,2.01196224159648,135.294351400248));
#96873=CARTESIAN_POINT('Ctrl Pts',(-93.0478113601711,2.13556133410218,135.234773786875));
#96874=CARTESIAN_POINT('Ctrl Pts',(-93.0555576362552,2.25913457234221,135.175208635854));
#96875=CARTESIAN_POINT('Ctrl Pts',(-93.0633039123394,2.38024538758876,135.110454296569));
#96876=CARTESIAN_POINT('Ctrl Pts',(-93.0710501884235,2.49843662016344,135.040750297178));
#96877=CARTESIAN_POINT('Ctrl Pts',(-93.0787965216889,2.61662872519879,134.971045783249));
#96878=CARTESIAN_POINT('Ctrl Pts',(-93.0865428549543,2.73190086779516,134.896391734913));
#96879=CARTESIAN_POINT('Ctrl Pts',(-93.0942891882197,2.84382238552751,134.817072581073));
#96880=CARTESIAN_POINT('Ctrl Pts',(-93.1020372562227,2.95576896730729,134.737735664259));
#96881=CARTESIAN_POINT('Ctrl Pts',(-93.1097853242257,3.06436311219457,134.653731789092));
#96882=CARTESIAN_POINT('Ctrl Pts',(-93.1175333922287,3.16920525357997,134.565387222521));
#96883=CARTESIAN_POINT('Ctrl Pts',(-93.1252896949706,3.27415882244158,134.476948762293));
#96884=CARTESIAN_POINT('Ctrl Pts',(-93.1330459977124,3.3753521225419,134.384160647352));
#96885=CARTESIAN_POINT('Ctrl Pts',(-93.1408023004543,3.47242025234193,134.28738813018));
#96886=CARTESIAN_POINT('Ctrl Pts',(-93.1485627429686,3.56954019032549,134.190563962602));
#96887=CARTESIAN_POINT('Ctrl Pts',(-93.1563231854829,3.66253030592995,134.08975144261));
#96888=CARTESIAN_POINT('Ctrl Pts',(-93.1640836279971,3.75106507426348,133.985350066015));
#96889=CARTESIAN_POINT('Ctrl Pts',(-93.1718565282626,3.83974196646688,133.880781095061));
#96890=CARTESIAN_POINT('Ctrl Pts',(-93.179629428528,3.92394897888479,133.77261206357));
#96891=CARTESIAN_POINT('Ctrl Pts',(-93.1874023287935,4.00340259719374,133.661273410649));
#96892=CARTESIAN_POINT('Ctrl Pts',(-93.1948926645551,4.07996787634084,133.553982198214));
#96893=CARTESIAN_POINT('Ctrl Pts',(-93.2023830003167,4.15211918834305,133.44374806861));
#96894=CARTESIAN_POINT('Ctrl Pts',(-93.2098733360783,4.21964355205206,133.330977200296));
#96895=CARTESIAN_POINT('Ctrl Pts',(-93.2176476701974,4.28972812253835,133.213930590228));
#96896=CARTESIAN_POINT('Ctrl Pts',(-93.2254220043165,4.35504996397883,133.093780314809));
#96897=CARTESIAN_POINT('Ctrl Pts',(-93.2331963384355,4.41532194139743,132.970951307178));
#96898=CARTESIAN_POINT('Ctrl Pts',(-93.2409610913826,4.47551963899051,132.848273675322));
#96899=CARTESIAN_POINT('Ctrl Pts',(-93.2487258443297,4.53067968490899,132.722924227468));
#96900=CARTESIAN_POINT('Ctrl Pts',(-93.2564905972767,4.58055889116168,132.595355678168));
#96901=CARTESIAN_POINT('Ctrl Pts',(-93.2642476381617,4.63038855668341,132.467913831749));
#96902=CARTESIAN_POINT('Ctrl Pts',(-93.2720046790466,4.67494767888497,132.338257631794));
#96903=CARTESIAN_POINT('Ctrl Pts',(-93.2797617199315,4.71403973888023,132.206862811061));
#96904=CARTESIAN_POINT('Ctrl Pts',(-93.2875129111716,4.753102319249,132.075567076184));
#96905=CARTESIAN_POINT('Ctrl Pts',(-93.2952641024116,4.78670593246589,131.942535703424));
#96906=CARTESIAN_POINT('Ctrl Pts',(-93.3030152936517,4.8147029236901,131.808262415109));
#96907=CARTESIAN_POINT('Ctrl Pts',(-93.3107631904288,4.84268801544614,131.674046196523));
#96908=CARTESIAN_POINT('Ctrl Pts',(-93.3185110872058,4.86507114510722,131.538589494163));
#96909=CARTESIAN_POINT('Ctrl Pts',(-93.3262589839829,4.88175514022601,131.402398921838));
#96910=CARTESIAN_POINT('Ctrl Pts',(-93.3340052600669,4.89843564541268,131.266236837646));
#96911=CARTESIAN_POINT('Ctrl Pts',(-93.341751536151,4.90941933977151,131.129341576648));
#96912=CARTESIAN_POINT('Ctrl Pts',(-93.349497812235,4.91466063915287,130.992227231049));
#96913=CARTESIAN_POINT('Ctrl Pts',(-93.3572441455003,4.9199019772243,130.855111873303));
#96914=CARTESIAN_POINT('Ctrl Pts',(-93.3649904787656,4.91940082079996,130.71777781841));
#96915=CARTESIAN_POINT('Ctrl Pts',(-93.3727368120309,4.91316368440942,130.580741135632));
#96916=CARTESIAN_POINT('Ctrl Pts',(-93.3804848800338,4.9069251512554,130.443673764439));
#96917=CARTESIAN_POINT('Ctrl Pts',(-93.3882329480367,4.89494809983603,130.306904288363));
#96918=CARTESIAN_POINT('Ctrl Pts',(-93.3959810160396,4.87729105226344,130.170945229364));
#96919=CARTESIAN_POINT('Ctrl Pts',(-93.4037373187814,4.85961523857064,130.03484167146));
#96920=CARTESIAN_POINT('Ctrl Pts',(-93.4114936215232,4.83624742006354,129.899550639542));
#96921=CARTESIAN_POINT('Ctrl Pts',(-93.419249924265,4.80729765580588,129.765576563499));
#96922=CARTESIAN_POINT('Ctrl Pts',(-93.4270103667791,4.7783324401873,129.631530981458));
#96923=CARTESIAN_POINT('Ctrl Pts',(-93.4347708092933,4.74377944085467,129.498804134045));
#96924=CARTESIAN_POINT('Ctrl Pts',(-93.4425312518074,4.70379881079189,129.367885831817));
#96925=CARTESIAN_POINT('Ctrl Pts',(-93.4503041520727,4.66375400027242,129.236757367908));
#96926=CARTESIAN_POINT('Ctrl Pts',(-93.4580770523382,4.61826427765711,129.107443619798));
#96927=CARTESIAN_POINT('Ctrl Pts',(-93.4658499526036,4.56753853714037,128.980415778971));
#96928=CARTESIAN_POINT('Ctrl Pts',(-93.4733402883661,4.51865680505869,128.858005720113));
#96929=CARTESIAN_POINT('Ctrl Pts',(-93.4808306241285,4.46491325635545,128.737718538211));
#96930=CARTESIAN_POINT('Ctrl Pts',(-93.488320959891,4.40653449895807,128.619952969714));
#96931=CARTESIAN_POINT('Ctrl Pts',(-93.4960952940101,4.34594229323363,128.497722283901));
#96932=CARTESIAN_POINT('Ctrl Pts',(-93.5038696281292,4.28016451456443,128.377821009989));
#96933=CARTESIAN_POINT('Ctrl Pts',(-93.5116439622483,4.20940346776533,128.260720409505));
#96934=CARTESIAN_POINT('Ctrl Pts',(-93.5194087151954,4.13872962763252,128.143764125046));
#96935=CARTESIAN_POINT('Ctrl Pts',(-93.5271734681424,4.06308493925008,128.029601977805));
#96936=CARTESIAN_POINT('Ctrl Pts',(-93.5349382210895,3.98271883514135,127.918683272));
#96937=CARTESIAN_POINT('Ctrl Pts',(-93.5426952619745,3.90243255177997,127.807874732217));
#96938=CARTESIAN_POINT('Ctrl Pts',(-93.5504523028595,3.81743441266948,127.700303537624));
#96939=CARTESIAN_POINT('Ctrl Pts',(-93.5582093437446,3.72801844199509,127.596392170302));
#96940=CARTESIAN_POINT('Ctrl Pts',(-93.5659605349847,3.63866990059985,127.492559163349));
#96941=CARTESIAN_POINT('Ctrl Pts',(-93.573711726225,3.5449104128099,127.392380785397));
#96942=CARTESIAN_POINT('Ctrl Pts',(-93.5814629174651,3.44707555015369,127.296248131623));
#96943=CARTESIAN_POINT('Ctrl Pts',(-93.5892108142422,3.34928226992381,127.20015633679));
#96944=CARTESIAN_POINT('Ctrl Pts',(-93.5969587110193,3.24741733821374,127.108107119542));
#96945=CARTESIAN_POINT('Ctrl Pts',(-93.6047066077964,3.14185445948987,127.020456070952));
#96946=CARTESIAN_POINT('Ctrl Pts',(-93.6124528838805,3.03631366224456,126.932823357072));
#96947=CARTESIAN_POINT('Ctrl Pts',(-93.6201991599646,2.92707675718301,126.849587231511));
#96948=CARTESIAN_POINT('Ctrl Pts',(-93.6279454360487,2.81455162529098,126.7710639249));
#96949=CARTESIAN_POINT('Ctrl Pts',(-93.6356917693141,2.70202566276414,126.692540038647));
#96950=CARTESIAN_POINT('Ctrl Pts',(-93.6434381025795,2.58621174558976,126.6187292645));
#96951=CARTESIAN_POINT('Ctrl Pts',(-93.6511844358448,2.46754757871762,126.549905069642));
#96952=CARTESIAN_POINT('Ctrl Pts',(-93.6589325038479,2.34885683782791,126.481065462082));
#96953=CARTESIAN_POINT('Ctrl Pts',(-93.6666805718508,2.2273149152436,126.41721485205));
#96954=CARTESIAN_POINT('Ctrl Pts',(-93.6744286398538,2.10338464283626,126.358581033873));
#96955=CARTESIAN_POINT('Ctrl Pts',(-93.6821849425957,1.97932265586078,126.299884898977));
#96956=CARTESIAN_POINT('Ctrl Pts',(-93.6899412453376,1.85286760237231,126.246416799079));
#96957=CARTESIAN_POINT('Ctrl Pts',(-93.6976975480794,1.72450336313443,126.198356795049));
#96958=CARTESIAN_POINT('Ctrl Pts',(-93.7054579905936,1.59607061203674,126.150271139948));
#96959=CARTESIAN_POINT('Ctrl Pts',(-93.7132184331078,1.46572701614474,126.107599453819));
#96960=CARTESIAN_POINT('Ctrl Pts',(-93.720978875622,1.33397123354978,126.07047174999));
#96961=CARTESIAN_POINT('Ctrl Pts',(-93.7287517758875,1.20200394487588,126.033284445474));
#96962=CARTESIAN_POINT('Ctrl Pts',(-93.736524676153,1.06862032001299,126.00165899793));
#96963=CARTESIAN_POINT('Ctrl Pts',(-93.7442975764185,0.934329698113822,
125.97567434926));
#96964=CARTESIAN_POINT('Ctrl Pts',(-93.7517879121804,0.804920878580893,
125.950634308022));
#96965=CARTESIAN_POINT('Ctrl Pts',(-93.7592782479422,0.674670164913171,
125.930832117648));
#96966=CARTESIAN_POINT('Ctrl Pts',(-93.7667685837041,0.544035512498864,
125.916292653264));
#96967=CARTESIAN_POINT('Ctrl Pts',(-93.7745429178232,0.408447807531721,
125.901201920668));
#96968=CARTESIAN_POINT('Ctrl Pts',(-93.7823172519422,0.272016973927845,
125.891733061484));
#96969=CARTESIAN_POINT('Ctrl Pts',(-93.7900915860612,0.135248848051348,
125.887970599311));
#96970=CARTESIAN_POINT('Ctrl Pts',(-93.7978563390082,-0.00135072333332237,
125.884212774035));
#96971=CARTESIAN_POINT('Ctrl Pts',(-93.8056210919553,-0.138286372840629,
125.886147363591));
#96972=CARTESIAN_POINT('Ctrl Pts',(-93.8133858449023,-0.275045263736215,
125.893807373236));
#96973=CARTESIAN_POINT('Ctrl Pts',(-93.8211428857872,-0.411668323773028,
125.901459774852));
#96974=CARTESIAN_POINT('Ctrl Pts',(-93.8288999266721,-0.548114586741336,
125.914826258307));
#96975=CARTESIAN_POINT('Ctrl Pts',(-93.836656967557,-0.683869679246917,
125.933887814613));
#96976=CARTESIAN_POINT('Ctrl Pts',(-93.8444081587971,-0.819522397781403,
125.95293499645));
#96977=CARTESIAN_POINT('Ctrl Pts',(-93.8521593500371,-0.954484597703345,
125.977668648658));
#96978=CARTESIAN_POINT('Ctrl Pts',(-93.8599105412771,-1.08824585495615,
126.008017841901));
#96979=CARTESIAN_POINT('Ctrl Pts',(-93.8676584380541,-1.2219502601066,126.038354135928));
#96980=CARTESIAN_POINT('Ctrl Pts',(-93.8754063348312,-1.35445435732335,
126.07430113759));
#96981=CARTESIAN_POINT('Ctrl Pts',(-93.8831542316082,-1.48525698137443,
126.115736644397));
#96982=CARTESIAN_POINT('Ctrl Pts',(-93.8909005076922,-1.61603224433669,
126.157163483789));
#96983=CARTESIAN_POINT('Ctrl Pts',(-93.8986467837762,-1.7451063695853,126.204076426745));
#96984=CARTESIAN_POINT('Ctrl Pts',(-93.9063930598602,-1.87199283369897,
126.25630324182));
#96985=CARTESIAN_POINT('Ctrl Pts',(-93.9141393931255,-1.99888023445917,
126.308530442421));
#96986=CARTESIAN_POINT('Ctrl Pts',(-93.9218857263907,-2.12357958032309,
126.366071444604));
#96987=CARTESIAN_POINT('Ctrl Pts',(-93.929632059656,-2.2456242053865,126.428705810491));
#96988=CARTESIAN_POINT('Ctrl Pts',(-93.9373801276589,-2.36769616149799,
126.491354202909));
#96989=CARTESIAN_POINT('Ctrl Pts',(-93.9451281956619,-2.48711186604396,
126.559098050264));
#96990=CARTESIAN_POINT('Ctrl Pts',(-93.9528762636648,-2.6034294972728,126.631671087391));
#96991=CARTESIAN_POINT('Ctrl Pts',(-93.9606325664066,-2.71987075226446,
126.704321256006));
#96992=CARTESIAN_POINT('Ctrl Pts',(-93.9683888691484,-2.83320702425014,
126.781810659872));
#96993=CARTESIAN_POINT('Ctrl Pts',(-93.9761451718902,-2.94302527354926,
126.863829523697));
#96994=CARTESIAN_POINT('Ctrl Pts',(-93.9839056144043,-3.05290213615429,
126.945892163458));
#96995=CARTESIAN_POINT('Ctrl Pts',(-93.9916660569184,-3.15925693161789,
127.032488833536));
#96996=CARTESIAN_POINT('Ctrl Pts',(-93.9994264994325,-3.26171073916644,
127.123270274134));
#96997=CARTESIAN_POINT('Ctrl Pts',(-94.0071993996978,-3.36432901466257,
127.214197445161));
#96998=CARTESIAN_POINT('Ctrl Pts',(-94.0149722999632,-3.46303350667502,
127.309322539484));
#96999=CARTESIAN_POINT('Ctrl Pts',(-94.0227452002286,-3.55748248889155,
127.408259705677));
#97000=CARTESIAN_POINT('Ctrl Pts',(-94.0302355359913,-3.64849801271059,
127.503600256681));
#97001=CARTESIAN_POINT('Ctrl Pts',(-94.0377258717539,-3.73556184859653,
127.602480303399));
#97002=CARTESIAN_POINT('Ctrl Pts',(-94.0452162075166,-3.81840553232964,
127.704528000605));
#97003=CARTESIAN_POINT('Ctrl Pts',(-94.0529669144684,-3.90412894123516,
127.810122972741));
#97004=CARTESIAN_POINT('Ctrl Pts',(-94.0607176214202,-3.98561230062312,
127.919453344993));
#97005=CARTESIAN_POINT('Ctrl Pts',(-94.068468328372,-4.06251064084263,128.032143029508));
#97006=CARTESIAN_POINT('Ctrl Pts',(-94.0765316119714,-4.14251019822082,
128.149377352856));
#97007=CARTESIAN_POINT('Ctrl Pts',(-94.0845948955708,-4.21754685391524,
128.270247352509));
#97008=CARTESIAN_POINT('Ctrl Pts',(-94.0926581791702,-4.28727613769913,
128.394288755232));
#97009=CARTESIAN_POINT('Ctrl Pts',(-94.1003894614796,-4.35413435637868,
128.513222821072));
#97010=CARTESIAN_POINT('Ctrl Pts',(-94.1081207437889,-4.41611330721045,
128.635071952975));
#97011=CARTESIAN_POINT('Ctrl Pts',(-94.1158520260983,-4.47295211812505,
128.759395480587));
#97012=CARTESIAN_POINT('Ctrl Pts',(-94.1235778857442,-4.52975106272427,
128.883631808609));
#97013=CARTESIAN_POINT('Ctrl Pts',(-94.1313037453902,-4.58141687585617,
129.010338723938));
#97014=CARTESIAN_POINT('Ctrl Pts',(-94.1390296050361,-4.62773442138493,
129.139050680158));
#97015=CARTESIAN_POINT('Ctrl Pts',(-94.1467512564063,-4.67402673774634,
129.267692526976));
#97016=CARTESIAN_POINT('Ctrl Pts',(-94.1544729077765,-4.7149764535067,129.398336871008));
#97017=CARTESIAN_POINT('Ctrl Pts',(-94.1621945591467,-4.75041662047909,
129.530498382324));
#97018=CARTESIAN_POINT('Ctrl Pts',(-94.1632056166193,-4.75505708453684,
129.547803344334));
#97019=CARTESIAN_POINT('Ctrl Pts',(-94.164216674092,-4.75960315778423,129.565134293483));
#97020=CARTESIAN_POINT('Ctrl Pts',(-94.1652277315646,-4.76405452823406,
129.582490119308));
#97021=CARTESIAN_POINT('Ctrl Pts',(-92.4154045049002,-4.764054528234,129.582490119308));
#97022=CARTESIAN_POINT('Ctrl Pts',(-92.424023850493,-4.80175568549997,129.729486359293));
#97023=CARTESIAN_POINT('Ctrl Pts',(-92.4326431960858,-4.83269371092977,
129.878401800015));
#97024=CARTESIAN_POINT('Ctrl Pts',(-92.4412625416786,-4.85668916151153,
130.028632926326));
#97025=CARTESIAN_POINT('Ctrl Pts',(-92.4498401457289,-4.88056840754981,
130.17813651725));
#97026=CARTESIAN_POINT('Ctrl Pts',(-92.4584177497793,-4.89757206130976,
130.32894286188));
#97027=CARTESIAN_POINT('Ctrl Pts',(-92.4669953538296,-4.90757148331663,
130.480439024218));
#97028=CARTESIAN_POINT('Ctrl Pts',(-92.4730437572057,-4.91462246602353,
130.587264880759));
#97029=CARTESIAN_POINT('Ctrl Pts',(-92.4790921605817,-4.91819179696133,
130.694433345267));
#97030=CARTESIAN_POINT('Ctrl Pts',(-92.4851405639579,-4.91824929378548,
130.801724962307));
#97031=CARTESIAN_POINT('',(-92.1398594360289,-4.91824936578745,130.801862932376));
#97032=CARTESIAN_POINT('Ctrl Pts',(-92.0697718875171,-4.76405452823417,
129.582490119309));
#97033=CARTESIAN_POINT('Ctrl Pts',(-92.0775447754838,-4.79811707026865,
129.71529945373));
#97034=CARTESIAN_POINT('Ctrl Pts',(-92.0853176634505,-4.82658582570716,
129.849393649157));
#97035=CARTESIAN_POINT('Ctrl Pts',(-92.0930905514173,-4.84939385186018,
129.984261640588));
#97036=CARTESIAN_POINT('Ctrl Pts',(-92.1006176466071,-4.87148064697149,
130.114864862183));
#97037=CARTESIAN_POINT('Ctrl Pts',(-92.1081447417968,-4.88825931939402,
130.246193359425));
#97038=CARTESIAN_POINT('Ctrl Pts',(-92.1156718369866,-4.89971567372624,
130.377781927121));
#97039=CARTESIAN_POINT('Ctrl Pts',(-92.1237343699882,-4.91198697262083,
130.51873101079));
#97040=CARTESIAN_POINT('Ctrl Pts',(-92.1317969029898,-4.91817743232996,
130.660217143608));
#97041=CARTESIAN_POINT('Ctrl Pts',(-92.1398594359916,-4.91824936578712,
130.80186293172));
#97042=CARTESIAN_POINT('Ctrl Pts',(-92.1398594360288,-4.91824936578745,
130.801862932376));
#97043=CARTESIAN_POINT('Ctrl Pts',(-92.1475407774203,-4.91831789825695,
130.93681179459));
#97044=CARTESIAN_POINT('Ctrl Pts',(-92.1552221188117,-4.91282807124698,
131.0719867331));
#97045=CARTESIAN_POINT('Ctrl Pts',(-92.1629034602031,-4.90175039741188,
131.20688528013));
#97046=CARTESIAN_POINT('Ctrl Pts',(-92.1705759898489,-4.89068543146713,
131.341629076626));
#97047=CARTESIAN_POINT('Ctrl Pts',(-92.1782485194948,-4.8740454003861,131.47609671642));
#97048=CARTESIAN_POINT('Ctrl Pts',(-92.1859210491406,-4.85185281164743,
131.609784330036));
#97049=CARTESIAN_POINT('Ctrl Pts',(-92.193586715678,-4.82968007426798,131.743352359547));
#97050=CARTESIAN_POINT('Ctrl Pts',(-92.2012523822153,-4.80196472494574,
131.876141357745));
#97051=CARTESIAN_POINT('Ctrl Pts',(-92.2089180487527,-4.76878115459254,
132.007651672175));
#97052=CARTESIAN_POINT('Ctrl Pts',(-92.2166347742547,-4.7353765573092,132.140037941808));
#97053=CARTESIAN_POINT('Ctrl Pts',(-92.2243514997566,-4.69643065403239,
132.271128020614));
#97054=CARTESIAN_POINT('Ctrl Pts',(-92.2320682252585,-4.65207195115217,
132.4004212755));
#97055=CARTESIAN_POINT('Ctrl Pts',(-92.23972692109,-4.60804682511228,132.528742246872));
#97056=CARTESIAN_POINT('Ctrl Pts',(-92.2473856169216,-4.55869017428788,
132.65529294547));
#97057=CARTESIAN_POINT('Ctrl Pts',(-92.255044312753,-4.50417778488755,132.779598715777));
#97058=CARTESIAN_POINT('Ctrl Pts',(-92.2627023841936,-4.4496698397213,132.903894351802));
#97059=CARTESIAN_POINT('Ctrl Pts',(-92.2703604556343,-4.39000715277736,
133.025945056422));
#97060=CARTESIAN_POINT('Ctrl Pts',(-92.278018527075,-4.32541343863651,133.145296679778));
#97061=CARTESIAN_POINT('Ctrl Pts',(-92.2856777243033,-4.26081022878763,
133.26466584862));
#97062=CARTESIAN_POINT('Ctrl Pts',(-92.2933369215316,-4.19127474119288,
133.381334794752));
#97063=CARTESIAN_POINT('Ctrl Pts',(-92.3009961187599,-4.11707610984384,
133.494874949112));
#97064=CARTESIAN_POINT('Ctrl Pts',(-92.3087563972632,-4.04189825155601,
133.609913535124));
#97065=CARTESIAN_POINT('Ctrl Pts',(-92.3165166757665,-3.96193351289705,
133.72173979682));
#97066=CARTESIAN_POINT('Ctrl Pts',(-92.3242769542698,-3.87750578463183,
133.829940223633));
#97067=CARTESIAN_POINT('Ctrl Pts',(-92.3319475927844,-3.79405329206241,
133.936890813209));
#97068=CARTESIAN_POINT('Ctrl Pts',(-92.3396182312991,-3.70624068100972,
134.040298626305));
#97069=CARTESIAN_POINT('Ctrl Pts',(-92.3472888698137,-3.61441924797575,
134.139800103205));
#97070=CARTESIAN_POINT('Ctrl Pts',(-92.3550939683113,-3.52098826075632,
134.241045759143));
#97071=CARTESIAN_POINT('Ctrl Pts',(-92.362899066809,-3.42340690801974,134.33824654365));
#97072=CARTESIAN_POINT('Ctrl Pts',(-92.3707041653066,-3.322081168469,134.431061566446));
#97073=CARTESIAN_POINT('Ctrl Pts',(-92.3785092638042,-3.22075542891826,
134.523876589241));
#97074=CARTESIAN_POINT('Ctrl Pts',(-92.3863143623019,-3.11568567483839,
134.612305625749));
#97075=CARTESIAN_POINT('Ctrl Pts',(-92.3941194607995,-3.00730873746807,
134.696053979079));
#97076=CARTESIAN_POINT('Ctrl Pts',(-92.4018937949185,-2.89935897588927,
134.779472232022));
#97077=CARTESIAN_POINT('Ctrl Pts',(-92.4096681290376,-2.78776475261839,
134.858527661847));
#97078=CARTESIAN_POINT('Ctrl Pts',(-92.4174424631567,-2.67291411339402,
134.932884955016));
#97079=CARTESIAN_POINT('Ctrl Pts',(-92.4252072161037,-2.55820501731832,
135.007150609467));
#97080=CARTESIAN_POINT('Ctrl Pts',(-92.4329719690508,-2.44024781548098,
135.076729437264));
#97081=CARTESIAN_POINT('Ctrl Pts',(-92.4407367219978,-2.31946333110538,
135.141326483025));
#97082=CARTESIAN_POINT('Ctrl Pts',(-92.4484937628828,-2.19879881158243,
135.20585937009));
#97083=CARTESIAN_POINT('Ctrl Pts',(-92.4562508037678,-2.07531294028713,
135.265420138627));
#97084=CARTESIAN_POINT('Ctrl Pts',(-92.4640078446527,-1.94945490956833,
135.319757457054));
#97085=CARTESIAN_POINT('Ctrl Pts',(-92.4717590358928,-1.82369178936936,
135.374053799287));
#97086=CARTESIAN_POINT('Ctrl Pts',(-92.4795102271329,-1.69556042786087,
135.423134377499));
#97087=CARTESIAN_POINT('Ctrl Pts',(-92.487261418373,-1.56553365231574,135.466794257412));
#97088=CARTESIAN_POINT('Ctrl Pts',(-92.4950093151501,-1.43556214161862,
135.510435580711));
#97089=CARTESIAN_POINT('Ctrl Pts',(-92.5027572119271,-1.30369718901858,
135.548660663888));
#97090=CARTESIAN_POINT('Ctrl Pts',(-92.5105051087042,-1.17043038545329,
135.581313179117));
#97091=CARTESIAN_POINT('Ctrl Pts',(-92.5182513847883,-1.03719145843076,
135.613958864144));
#97092=CARTESIAN_POINT('Ctrl Pts',(-92.5259976608723,-0.902551643199964,
135.641034206805));
#97093=CARTESIAN_POINT('Ctrl Pts',(-92.5337439369564,-0.767016049777256,
135.662433223228));
#97094=CARTESIAN_POINT('Ctrl Pts',(-92.5414902702217,-0.631479455861401,
135.683832397613));
#97095=CARTESIAN_POINT('Ctrl Pts',(-92.5492366034871,-0.495047456740555,
135.699555101177));
#97096=CARTESIAN_POINT('Ctrl Pts',(-92.5569829367524,-0.358233278960902,
135.709546850559));
#97097=CARTESIAN_POINT('Ctrl Pts',(-92.5647310047553,-0.221388462595671,
135.719540837524));
#97098=CARTESIAN_POINT('Ctrl Pts',(-92.5724790727582,-0.0841616871169833,
135.723801288006));
#97099=CARTESIAN_POINT('Ctrl Pts',(-92.5802271407611,0.0529312008536751,
135.722325781175));
#97100=CARTESIAN_POINT('Ctrl Pts',(-92.5879834435029,0.19016979277803,135.720848706159));
#97101=CARTESIAN_POINT('Ctrl Pts',(-92.5957397462448,0.327273821374372,
135.713623500143));
#97102=CARTESIAN_POINT('Ctrl Pts',(-92.6034960489866,0.463729388489498,
135.700699874271));
#97103=CARTESIAN_POINT('Ctrl Pts',(-92.6112564915008,0.600257786049763,
135.687769350671));
#97104=CARTESIAN_POINT('Ctrl Pts',(-92.619016934015,0.736136645338421,135.669134400028));
#97105=CARTESIAN_POINT('Ctrl Pts',(-92.6267773765292,0.870860668680839,
135.644896203454));
#97106=CARTESIAN_POINT('Ctrl Pts',(-92.6345502767946,1.0058009629854,135.620619097575));
#97107=CARTESIAN_POINT('Ctrl Pts',(-92.6423231770599,1.13958233499793,135.590720856553));
#97108=CARTESIAN_POINT('Ctrl Pts',(-92.6500960773253,1.27171221903285,135.555353260632));
#97109=CARTESIAN_POINT('Ctrl Pts',(-92.6575864130876,1.39903884897194,135.521271365906));
#97110=CARTESIAN_POINT('Ctrl Pts',(-92.6650767488499,1.52483168371457,135.482110953708));
#97111=CARTESIAN_POINT('Ctrl Pts',(-92.6725670846121,1.64866801332278,135.438049951601));
#97112=CARTESIAN_POINT('Ctrl Pts',(-92.6803414187312,1.77719963500352,135.392318363208));
#97113=CARTESIAN_POINT('Ctrl Pts',(-92.6881157528502,1.90403061060044,135.341162373514));
#97114=CARTESIAN_POINT('Ctrl Pts',(-92.6958900869693,2.02866908313515,135.284727211231));
#97115=CARTESIAN_POINT('Ctrl Pts',(-92.7036548399164,2.15315394989138,135.228361600242));
#97116=CARTESIAN_POINT('Ctrl Pts',(-92.7114195928634,2.27545133714997,135.166729921597));
#97117=CARTESIAN_POINT('Ctrl Pts',(-92.7191843458105,2.39508562536236,135.100026795202));
#97118=CARTESIAN_POINT('Ctrl Pts',(-92.7269413866955,2.51460109111315,135.033389919292));
#97119=CARTESIAN_POINT('Ctrl Pts',(-92.7346984275805,2.63145838227722,134.961691808717));
#97120=CARTESIAN_POINT('Ctrl Pts',(-92.7424554684655,2.74520324703989,134.885174530861));
#97121=CARTESIAN_POINT('Ctrl Pts',(-92.7502066597056,2.85886233591539,134.80871495528));
#97122=CARTESIAN_POINT('Ctrl Pts',(-92.7579578509456,2.96941334707704,134.727443663357));
#97123=CARTESIAN_POINT('Ctrl Pts',(-92.7657090421858,3.07642828882265,134.641647686086));
#97124=CARTESIAN_POINT('Ctrl Pts',(-92.7734569389628,3.18339774636316,134.555888174394));
#97125=CARTESIAN_POINT('Ctrl Pts',(-92.7812048357399,3.28683381929068,134.465608046319));
#97126=CARTESIAN_POINT('Ctrl Pts',(-92.788952732517,3.38633926766975,134.371136392231));
#97127=CARTESIAN_POINT('Ctrl Pts',(-92.7966990086011,3.4858239016541,134.276684499577));
#97128=CARTESIAN_POINT('Ctrl Pts',(-92.8044452846851,3.58137926314151,134.178043093886));
#97129=CARTESIAN_POINT('Ctrl Pts',(-92.8121915607692,3.67264316059553,134.075579851648));
#97130=CARTESIAN_POINT('Ctrl Pts',(-92.8199378940345,3.76390773173878,133.973115853051));
#97131=CARTESIAN_POINT('Ctrl Pts',(-92.8276842273,3.85088051559807,133.86683025356));
#97132=CARTESIAN_POINT('Ctrl Pts',(-92.8354305605653,3.93323826229641,133.757125395619));
#97133=CARTESIAN_POINT('Ctrl Pts',(-92.8431786285683,4.01561445244121,133.647395970035));
#97134=CARTESIAN_POINT('Ctrl Pts',(-92.8509266965711,4.09337331419015,133.534246074912));
#97135=CARTESIAN_POINT('Ctrl Pts',(-92.8586747645741,4.16623398313402,133.418108398106));
#97136=CARTESIAN_POINT('Ctrl Pts',(-92.8664310673159,4.239172089264,133.301847288796));
#97137=CARTESIAN_POINT('Ctrl Pts',(-92.8741873700578,4.30720139522228,133.182592386212));
#97138=CARTESIAN_POINT('Ctrl Pts',(-92.8819436727996,4.37008594989862,133.060802917515));
#97139=CARTESIAN_POINT('Ctrl Pts',(-92.8897041153138,4.43300406795539,132.938948446111));
#97140=CARTESIAN_POINT('Ctrl Pts',(-92.897464557828,4.49077179868117,132.814557067495));
#97141=CARTESIAN_POINT('Ctrl Pts',(-92.9052250003422,4.54320114287566,132.688108593775));
#97142=CARTESIAN_POINT('Ctrl Pts',(-92.9129979006076,4.59571465130776,132.56145713374));
#97143=CARTESIAN_POINT('Ctrl Pts',(-92.920770800873,4.64287251373869,132.432742347004));
#97144=CARTESIAN_POINT('Ctrl Pts',(-92.9285437011385,4.68453618340016,132.302460683955));
#97145=CARTESIAN_POINT('Ctrl Pts',(-92.9360340369007,4.72468527372622,132.176915087514));
#97146=CARTESIAN_POINT('Ctrl Pts',(-92.9435243726629,4.75973260970269,132.049914853668));
#97147=CARTESIAN_POINT('Ctrl Pts',(-92.9510147084252,4.78959940178096,131.921911794452));
#97148=CARTESIAN_POINT('Ctrl Pts',(-92.9587890425443,4.82059860235787,131.789055460344));
#97149=CARTESIAN_POINT('Ctrl Pts',(-92.9665633766633,4.84611485974488,131.654697906551));
#97150=CARTESIAN_POINT('Ctrl Pts',(-92.9743377107824,4.86600449825838,131.519331445942));
#97151=CARTESIAN_POINT('Ctrl Pts',(-92.9821024637295,4.88586962456994,131.384131812399));
#97152=CARTESIAN_POINT('Ctrl Pts',(-92.9898672166766,4.90012187291857,131.247926129111));
#97153=CARTESIAN_POINT('Ctrl Pts',(-92.9976319696237,4.90866789856035,131.111219745087));
#97154=CARTESIAN_POINT('Ctrl Pts',(-93.0053890105087,4.91720543616898,130.974649139772));
#97155=CARTESIAN_POINT('Ctrl Pts',(-93.0131460513937,4.92004800541794,130.837579211055));
#97156=CARTESIAN_POINT('Ctrl Pts',(-93.0209030922787,4.91715373025298,130.700522977188));
#97157=CARTESIAN_POINT('Ctrl Pts',(-93.0286542835189,4.91426163768341,130.563570098493));
#97158=CARTESIAN_POINT('Ctrl Pts',(-93.036405474759,4.90564131995753,130.426631283388));
#97159=CARTESIAN_POINT('Ctrl Pts',(-93.0441566659992,4.89130292440958,130.290221760678));
#97160=CARTESIAN_POINT('Ctrl Pts',(-93.0519045627763,4.87697062306229,130.153870215654));
#97161=CARTESIAN_POINT('Ctrl Pts',(-93.0596524595533,4.85692511842995,130.018047903598));
#97162=CARTESIAN_POINT('Ctrl Pts',(-93.0674003563304,4.83122856567375,129.883266915102));
#97163=CARTESIAN_POINT('Ctrl Pts',(-93.0751466324145,4.80553738808243,129.748514119884));
#97164=CARTESIAN_POINT('Ctrl Pts',(-93.0828929084987,4.77419758675797,129.61480259877));
#97165=CARTESIAN_POINT('Ctrl Pts',(-93.0906391845828,4.73732272497176,129.48263581188));
#97166=CARTESIAN_POINT('Ctrl Pts',(-93.0983855178482,4.70044759098376,129.350468049365));
#97167=CARTESIAN_POINT('Ctrl Pts',(-93.1061318511135,4.65803742007127,129.219845420412));
#97168=CARTESIAN_POINT('Ctrl Pts',(-93.1138781843789,4.61025598987186,129.091257360214));
#97169=CARTESIAN_POINT('Ctrl Pts',(-93.1216262523819,4.56246385935238,128.962640503611));
#97170=CARTESIAN_POINT('Ctrl Pts',(-93.1293743203848,4.50929821215446,128.836059488822));
#97171=CARTESIAN_POINT('Ctrl Pts',(-93.1371223883878,4.45097126675221,128.711984493384));
#97172=CARTESIAN_POINT('Ctrl Pts',(-93.1448786911296,4.39258233077837,128.587777629564));
#97173=CARTESIAN_POINT('Ctrl Pts',(-93.1526349938715,4.3290213053387,128.466082459962));
#97174=CARTESIAN_POINT('Ctrl Pts',(-93.1603912966134,4.26054701390939,128.347345720426));
#97175=CARTESIAN_POINT('Ctrl Pts',(-93.1681517391275,4.19203617568902,128.228545607517));
#97176=CARTESIAN_POINT('Ctrl Pts',(-93.1759121816417,4.11860705542509,128.11270740102));
#97177=CARTESIAN_POINT('Ctrl Pts',(-93.1836726241559,4.04056171447239,128.000248620152));
#97178=CARTESIAN_POINT('Ctrl Pts',(-93.1914455244213,3.96239108820964,127.887609310465));
#97179=CARTESIAN_POINT('Ctrl Pts',(-93.1992184246868,3.87958966927376,127.778360578957));
#97180=CARTESIAN_POINT('Ctrl Pts',(-93.2069913249523,3.79250024752544,127.67288733251));
#97181=CARTESIAN_POINT('Ctrl Pts',(-93.2144816607142,3.70857674562457,127.571248304245));
#97182=CARTESIAN_POINT('Ctrl Pts',(-93.221971996476,3.62067179323408,127.473115259353));
#97183=CARTESIAN_POINT('Ctrl Pts',(-93.2294623322379,3.52912292494078,127.378798701156));
#97184=CARTESIAN_POINT('Ctrl Pts',(-93.237236666357,3.43410295347847,127.280906101986));
#97185=CARTESIAN_POINT('Ctrl Pts',(-93.245011000476,3.33485629865505,127.186815012297));
#97186=CARTESIAN_POINT('Ctrl Pts',(-93.2527853345951,3.23171949701599,127.096912417644));
#97187=CARTESIAN_POINT('Ctrl Pts',(-93.2605500875422,3.12870980226791,127.007120619904));
#97188=CARTESIAN_POINT('Ctrl Pts',(-93.2683148404893,3.02181979173525,126.921507300897));
#97189=CARTESIAN_POINT('Ctrl Pts',(-93.2760795934364,2.91142417473824,126.840424147685));
#97190=CARTESIAN_POINT('Ctrl Pts',(-93.2838366343214,2.80113820422434,126.759421527404));
#97191=CARTESIAN_POINT('Ctrl Pts',(-93.2915936752062,2.68735386928573,126.682940348799));
#97192=CARTESIAN_POINT('Ctrl Pts',(-93.2993507160912,2.57048015167668,126.611293142276));
#97193=CARTESIAN_POINT('Ctrl Pts',(-93.3071019073313,2.45369456944706,126.539699965469));
#97194=CARTESIAN_POINT('Ctrl Pts',(-93.3148530985715,2.33382457369807,126.472933708431));
#97195=CARTESIAN_POINT('Ctrl Pts',(-93.3226042898116,2.21130912589593,126.411264327678));
#97196=CARTESIAN_POINT('Ctrl Pts',(-93.3303521865887,2.08884575042714,126.349621158056));
#97197=CARTESIAN_POINT('Ctrl Pts',(-93.3381000833658,1.96373950771476,126.293070731511));
#97198=CARTESIAN_POINT('Ctrl Pts',(-93.3458479801428,1.83645483045995,126.241837552618));
#97199=CARTESIAN_POINT('Ctrl Pts',(-93.353594256227,1.70919677841534,126.190615090602));
#97200=CARTESIAN_POINT('Ctrl Pts',(-93.361340532311,1.57976156066156,126.144707809798));
#97201=CARTESIAN_POINT('Ctrl Pts',(-93.3690868083952,1.44863413617935,126.104292298701));
#97202=CARTESIAN_POINT('Ctrl Pts',(-93.3768331416605,1.31750574374517,126.063876489267));
#97203=CARTESIAN_POINT('Ctrl Pts',(-93.3845794749259,1.18468549327806,126.02895264559));
#97204=CARTESIAN_POINT('Ctrl Pts',(-93.3923258081912,1.0506736862822,125.999647528582));
#97205=CARTESIAN_POINT('Ctrl Pts',(-93.4000738761942,0.916631868270413,
125.970335848896));
#97206=CARTESIAN_POINT('Ctrl Pts',(-93.4078219441971,0.781398344614256,
125.946645483206));
#97207=CARTESIAN_POINT('Ctrl Pts',(-93.4155700122001,0.645483398260895,
125.928652028543));
#97208=CARTESIAN_POINT('Ctrl Pts',(-93.4233263149419,0.509423999885697,
125.910639450223));
#97209=CARTESIAN_POINT('Ctrl Pts',(-93.4310826176839,0.372682120299041,
125.898335929327));
#97210=CARTESIAN_POINT('Ctrl Pts',(-93.4388389204257,0.235773511433159,
125.891765181973));
#97211=CARTESIAN_POINT('Ctrl Pts',(-93.4465993629399,0.0987918303201126,
125.885190927614));
#97212=CARTESIAN_POINT('Ctrl Pts',(-93.4543598054541,-0.0383563666225004,
125.884355545996));
#97213=CARTESIAN_POINT('Ctrl Pts',(-93.4621202479683,-0.175156537113291,
125.88923058368));
#97214=CARTESIAN_POINT('Ctrl Pts',(-93.4698931482337,-0.312176311382302,
125.894113447208));
#97215=CARTESIAN_POINT('Ctrl Pts',(-93.477666048499,-0.44884655275655,125.904725018088));
#97216=CARTESIAN_POINT('Ctrl Pts',(-93.4854389487645,-0.584658141882119,
125.920984949073));
#97217=CARTESIAN_POINT('Ctrl Pts',(-93.4929292845266,-0.715532637655331,
125.936653790611));
#97218=CARTESIAN_POINT('Ctrl Pts',(-93.5004196202887,-0.845609521563356,
125.957567408858));
#97219=CARTESIAN_POINT('Ctrl Pts',(-93.5079099560508,-0.97444511267973,
125.983609661037));
#97220=CARTESIAN_POINT('Ctrl Pts',(-93.5156842901699,-1.1081655443907,126.010639313123));
#97221=CARTESIAN_POINT('Ctrl Pts',(-93.5234586242889,-1.24097228411011,
126.043279802357));
#97222=CARTESIAN_POINT('Ctrl Pts',(-93.531232958408,-1.37235784370795,126.081457166159));
#97223=CARTESIAN_POINT('Ctrl Pts',(-93.5389977113552,-1.50358148234658,
126.119587479772));
#97224=CARTESIAN_POINT('Ctrl Pts',(-93.5467624643023,-1.63338705394936,
126.163240982771));
#97225=CARTESIAN_POINT('Ctrl Pts',(-93.5545272172494,-1.76127613469166,
126.21229251704));
#97226=CARTESIAN_POINT('Ctrl Pts',(-93.5622842581345,-1.8890381941957,126.261295332634));
#97227=CARTESIAN_POINT('Ctrl Pts',(-93.5700412990195,-2.01488718818781,
126.315685370965));
#97228=CARTESIAN_POINT('Ctrl Pts',(-93.5777983399045,-2.13833911135747,
126.37528747442));
#97229=CARTESIAN_POINT('Ctrl Pts',(-93.5855495311446,-2.26169793847139,
126.434844631465));
#97230=CARTESIAN_POINT('Ctrl Pts',(-93.5933007223848,-2.38266294212549,
126.499605860998));
#97231=CARTESIAN_POINT('Ctrl Pts',(-93.6010519136249,-2.50076973086457,
126.569347770396));
#97232=CARTESIAN_POINT('Ctrl Pts',(-93.608799810402,-2.61882632106767,126.639060037623));
#97233=CARTESIAN_POINT('Ctrl Pts',(-93.6165477071791,-2.73402677658734,
126.713748575941));
#97234=CARTESIAN_POINT('Ctrl Pts',(-93.6242956039561,-2.84593117814597,
126.793143995174));
#97235=CARTESIAN_POINT('Ctrl Pts',(-93.6320418800403,-2.95781217171647,
126.872522806596));
#97236=CARTESIAN_POINT('Ctrl Pts',(-93.6397881561243,-3.06639816404589,
126.956606314466));
#97237=CARTESIAN_POINT('Ctrl Pts',(-93.6475344322085,-3.17127845405589,
127.045081959453));
#97238=CARTESIAN_POINT('Ctrl Pts',(-93.6552807654738,-3.27615951826795,
127.133558257548));
#97239=CARTESIAN_POINT('Ctrl Pts',(-93.6630270987391,-3.37733452674099,
127.226426505361));
#97240=CARTESIAN_POINT('Ctrl Pts',(-93.6707734320044,-3.47442640674552,
127.323334302439));
#97241=CARTESIAN_POINT('Ctrl Pts',(-93.6785215000074,-3.57154002980351,
127.420263801346));
#97242=CARTESIAN_POINT('Ctrl Pts',(-93.6862695680104,-3.66456842820272,
127.521234373485));
#97243=CARTESIAN_POINT('Ctrl Pts',(-93.6940176360134,-3.75317217962262,
127.625857565403));
#97244=CARTESIAN_POINT('Ctrl Pts',(-93.7017739387553,-3.84187010016406,
127.730591952095));
#97245=CARTESIAN_POINT('Ctrl Pts',(-93.7095302414971,-3.9261337267703,127.838986414549));
#97246=CARTESIAN_POINT('Ctrl Pts',(-93.717286544239,-4.00566432988292,127.950619855197));
#97247=CARTESIAN_POINT('Ctrl Pts',(-93.7250469867532,-4.08523738087325,
128.062312877975));
#97248=CARTESIAN_POINT('Ctrl Pts',(-93.7328074292674,-4.1600721615665,128.177247996132));
#97249=CARTESIAN_POINT('Ctrl Pts',(-93.7405678717816,-4.22991448797448,
128.294976930896));
#97250=CARTESIAN_POINT('Ctrl Pts',(-93.748340772047,-4.29986893148494,128.412894854598));
#97251=CARTESIAN_POINT('Ctrl Pts',(-93.7561136723125,-4.3648147201874,128.533615212631));
#97252=CARTESIAN_POINT('Ctrl Pts',(-93.7638865725779,-4.42454426104911,
128.656666238815));
#97253=CARTESIAN_POINT('Ctrl Pts',(-93.7713769083399,-4.48210248265039,
128.77524405025));
#97254=CARTESIAN_POINT('Ctrl Pts',(-93.7788672441018,-4.53481699637019,
128.895985738155));
#97255=CARTESIAN_POINT('Ctrl Pts',(-93.7863575798638,-4.58254569603886,
129.018455243193));
#97256=CARTESIAN_POINT('Ctrl Pts',(-93.7951963202617,-4.63886648048808,
129.162971616836));
#97257=CARTESIAN_POINT('Ctrl Pts',(-93.8040350606597,-4.68839467034822,
129.310276098878));
#97258=CARTESIAN_POINT('Ctrl Pts',(-93.8128738010576,-4.73088032785859,
129.459758674246));
#97259=CARTESIAN_POINT('Ctrl Pts',(-93.8152834783079,-4.74246305545977,
129.50051162602));
#97260=CARTESIAN_POINT('Ctrl Pts',(-93.8176931555582,-4.75352260960667,
129.541426328424));
#97261=CARTESIAN_POINT('Ctrl Pts',(-93.8201028328085,-4.76405452823393,
129.582490119308));
#97262=CARTESIAN_POINT('Origin',(213.235140564004,0.,130.804360617566));
#97263=CARTESIAN_POINT('',(-95.9150180446607,-4.76405452823415,129.582490119309));
#97264=CARTESIAN_POINT('',(-95.5699831042333,-4.76405452823397,129.582490119308));
#97265=CARTESIAN_POINT('',(213.235140564004,-4.76405452823405,129.582490119308));
#97266=CARTESIAN_POINT('',(-94.2351405640567,-4.91824832960019,130.808414120368));
#97267=CARTESIAN_POINT('Ctrl Pts',(-94.2351405640567,-4.91824832960019,
130.808414120368));
#97268=CARTESIAN_POINT('Ctrl Pts',(-94.2443029884524,-4.9181146402537,130.970623803505));
#97269=CARTESIAN_POINT('Ctrl Pts',(-94.2534654128481,-4.90995233268537,
131.132490188506));
#97270=CARTESIAN_POINT('Ctrl Pts',(-94.2626278372439,-4.89388613611978,
131.293299825643));
#97271=CARTESIAN_POINT('Ctrl Pts',(-94.2718551523956,-4.87770615442514,
131.455248359919));
#97272=CARTESIAN_POINT('Ctrl Pts',(-94.2810824675474,-4.85351003632696,
131.616125071655));
#97273=CARTESIAN_POINT('Ctrl Pts',(-94.2903097826992,-4.82147397135044,
131.775221990827));
#97274=CARTESIAN_POINT('Ctrl Pts',(-94.2996077942268,-4.78919245754591,
131.935537853473));
#97275=CARTESIAN_POINT('Ctrl Pts',(-94.3089058057544,-4.74895046713222,
132.094046497661));
#97276=CARTESIAN_POINT('Ctrl Pts',(-94.318203817282,-4.70097636774123,132.250045317782));
#97277=CARTESIAN_POINT('Ctrl Pts',(-94.3200238219645,-4.69158585609541,
132.28058072659));
#97278=CARTESIAN_POINT('Ctrl Pts',(-94.3218438266471,-4.68189923651167,
132.31102004001));
#97279=CARTESIAN_POINT('Ctrl Pts',(-94.3236638313296,-4.67191843243465,
132.341358087693));
#97280=CARTESIAN_POINT('Ctrl Pts',(-94.3314381654491,-4.62928441812665,
132.470950127476));
#97281=CARTESIAN_POINT('Ctrl Pts',(-94.3392124995686,-4.58118675379454,
132.598972181592));
#97282=CARTESIAN_POINT('Ctrl Pts',(-94.3469868336881,-4.52775882311562,
132.724929049619));
#97283=CARTESIAN_POINT('Ctrl Pts',(-94.3547515866357,-4.47439673758627,
132.850730687063));
#97284=CARTESIAN_POINT('Ctrl Pts',(-94.3625163395831,-4.4157176074208,132.974471846052));
#97285=CARTESIAN_POINT('Ctrl Pts',(-94.3702810925306,-4.35190458292287,
133.095672373664));
#97286=CARTESIAN_POINT('Ctrl Pts',(-94.3780381334161,-4.28815493842031,
133.216752523204));
#97287=CARTESIAN_POINT('Ctrl Pts',(-94.3857951743015,-4.21928172790127,
133.335296719322));
#97288=CARTESIAN_POINT('Ctrl Pts',(-94.3935522151869,-4.14551604825105,
133.450845032066));
#97289=CARTESIAN_POINT('Ctrl Pts',(-94.4013034064275,-4.07180599587357,
133.566306208929));
#97290=CARTESIAN_POINT('Ctrl Pts',(-94.409054597668,-3.99321102751453,133.678775671053));
#97291=CARTESIAN_POINT('Ctrl Pts',(-94.4168057889085,-3.91000782088841,
133.787818662032));
#97292=CARTESIAN_POINT('Ctrl Pts',(-94.424553685686,-3.82683997784474,133.896815306832));
#97293=CARTESIAN_POINT('Ctrl Pts',(-94.4323015824634,-3.73906802875495,
134.002388066874));
#97294=CARTESIAN_POINT('Ctrl Pts',(-94.4400494792409,-3.64701143655703,
134.104131919357));
#97295=CARTESIAN_POINT('Ctrl Pts',(-94.4477957553253,-3.55497410061344,
134.205854489219));
#97296=CARTESIAN_POINT('Ctrl Pts',(-94.4555420314098,-3.45865416640367,
134.303749454879));
#97297=CARTESIAN_POINT('Ctrl Pts',(-94.4632883074943,-3.35841051293748,
134.397445905879));
#97298=CARTESIAN_POINT('Ctrl Pts',(-94.47103464076,-3.25816611949555,134.491143048525));
#97299=CARTESIAN_POINT('Ctrl Pts',(-94.4787809740257,-3.15399823462587,
134.580641347699));
#97300=CARTESIAN_POINT('Ctrl Pts',(-94.4865273072914,-3.04630132780064,
134.665607991504));
#97301=CARTESIAN_POINT('Ctrl Pts',(-94.4942753752947,-2.93858030299999,
134.750593662999));
#97302=CARTESIAN_POINT('Ctrl Pts',(-94.502023443298,-2.82732899052071,134.831045417611));
#97303=CARTESIAN_POINT('Ctrl Pts',(-94.5097715113014,-2.71297321364428,
134.906672088499));
#97304=CARTESIAN_POINT('Ctrl Pts',(-94.5175278140436,-2.59849589808718,
134.982379136313));
#97305=CARTESIAN_POINT('Ctrl Pts',(-94.5252841167858,-2.48090785372675,
135.053250640351));
#97306=CARTESIAN_POINT('Ctrl Pts',(-94.533040419528,-2.36066251329971,135.119039697266));
#97307=CARTESIAN_POINT('Ctrl Pts',(-94.5408008620426,-2.24035299431363,
135.184863867782));
#97308=CARTESIAN_POINT('Ctrl Pts',(-94.5485613045571,-2.1173837035878,135.245600012929));
#97309=CARTESIAN_POINT('Ctrl Pts',(-94.5563217470716,-1.99222980359294,
135.301048673477));
#97310=CARTESIAN_POINT('Ctrl Pts',(-94.5640946473374,-1.86687499544717,
135.356586345138));
#97311=CARTESIAN_POINT('Ctrl Pts',(-94.5718675476033,-1.73932893404993,
135.406819427243));
#97312=CARTESIAN_POINT('Ctrl Pts',(-94.5796404478691,-1.61008460208522,
135.451597499481));
#97313=CARTESIAN_POINT('Ctrl Pts',(-94.5871307836269,-1.48553862721053,
135.494747775977));
#97314=CARTESIAN_POINT('Ctrl Pts',(-94.5946211193847,-1.35941600579462,
135.532832674595));
#97315=CARTESIAN_POINT('Ctrl Pts',(-94.6021114551425,-1.23216652903071,
135.565762586234));
#97316=CARTESIAN_POINT('Ctrl Pts',(-94.6098857892615,-1.10009234960476,
135.599941045501));
#97317=CARTESIAN_POINT('Ctrl Pts',(-94.6176601233806,-0.966385807288509,
135.628674165663));
#97318=CARTESIAN_POINT('Ctrl Pts',(-94.6254344574997,-0.831535625359408,
135.65180649826));
#97319=CARTESIAN_POINT('Ctrl Pts',(-94.6331992104467,-0.696851634227995,
135.674910322325));
#97320=CARTESIAN_POINT('Ctrl Pts',(-94.6409639633938,-0.561027189474129,
135.692427027217));
#97321=CARTESIAN_POINT('Ctrl Pts',(-94.6487287163409,-0.424565254563363,
135.70425116809));
#97322=CARTESIAN_POINT('Ctrl Pts',(-94.6564857572259,-0.288238855569757,
135.71606356506));
#97323=CARTESIAN_POINT('Ctrl Pts',(-94.6642427981108,-0.151276613429885,
135.722194616066));
#97324=CARTESIAN_POINT('Ctrl Pts',(-94.6719998389958,-0.0141903937488982,
135.722590146088));
#97325=CARTESIAN_POINT('Ctrl Pts',(-94.679751030236,0.122792448147638,135.722985377838));
#97326=CARTESIAN_POINT('Ctrl Pts',(-94.6875022214762,0.259898692112635,
135.717653696532));
#97327=CARTESIAN_POINT('Ctrl Pts',(-94.6952534127164,0.39661301420797,135.70659288251));
#97328=CARTESIAN_POINT('Ctrl Pts',(-94.7030013094935,0.533269229069254,
135.69553676963));
#97329=CARTESIAN_POINT('Ctrl Pts',(-94.7107492062706,0.669533464494266,
135.678756398594));
#97330=CARTESIAN_POINT('Ctrl Pts',(-94.7184971030477,0.804892285807843,
135.656301617903));
#97331=CARTESIAN_POINT('Ctrl Pts',(-94.7262433791318,0.940222792973999,
135.633851534267));
#97332=CARTESIAN_POINT('Ctrl Pts',(-94.7339896552158,1.07464787729224,135.605729465855));
#97333=CARTESIAN_POINT('Ctrl Pts',(-94.7417359312999,1.20766149842017,135.57203686158));
#97334=CARTESIAN_POINT('Ctrl Pts',(-94.7494822645652,1.34067610142462,135.538344008593));
#97335=CARTESIAN_POINT('Ctrl Pts',(-94.7572285978306,1.47227884145251,135.499080633691));
#97336=CARTESIAN_POINT('Ctrl Pts',(-94.764974931096,1.60197649404298,135.454398722252));
#97337=CARTESIAN_POINT('Ctrl Pts',(-94.7727229990989,1.73170319152331,135.409706804609));
#97338=CARTESIAN_POINT('Ctrl Pts',(-94.780471067102,1.85952358304612,135.359594063137));
#97339=CARTESIAN_POINT('Ctrl Pts',(-94.788219135105,1.98496253381547,135.304261372233));
#97340=CARTESIAN_POINT('Ctrl Pts',(-94.7959754378469,2.11053480259426,135.248869873086));
#97341=CARTESIAN_POINT('Ctrl Pts',(-94.8037317405888,2.23372021634751,135.188247500172));
#97342=CARTESIAN_POINT('Ctrl Pts',(-94.8114880433307,2.35406595682623,135.122642282003));
#97343=CARTESIAN_POINT('Ctrl Pts',(-94.8192484858449,2.47447592945051,135.057002048354));
#97344=CARTESIAN_POINT('Ctrl Pts',(-94.827008928359,2.59204287382563,134.986373871417));
#97345=CARTESIAN_POINT('Ctrl Pts',(-94.8347693708731,2.70634214233155,134.911049706253));
#97346=CARTESIAN_POINT('Ctrl Pts',(-94.8425422711386,2.82082489417029,134.835604624052));
#97347=CARTESIAN_POINT('Ctrl Pts',(-94.8503151714041,2.93202917048863,134.755448718204));
#97348=CARTESIAN_POINT('Ctrl Pts',(-94.8580880716695,3.03956194923661,134.670915443151));
#97349=CARTESIAN_POINT('Ctrl Pts',(-94.8655784074316,3.14318564061895,134.589455165572));
#97350=CARTESIAN_POINT('Ctrl Pts',(-94.8730687431937,3.24339990209743,134.503930450129));
#97351=CARTESIAN_POINT('Ctrl Pts',(-94.8805590789558,3.33988621986936,134.414671282983));
#97352=CARTESIAN_POINT('Ctrl Pts',(-94.8883334130748,3.44003084570447,134.322027827387));
#97353=CARTESIAN_POINT('Ctrl Pts',(-94.8961077471939,3.5364764855459,134.225067679864));
#97354=CARTESIAN_POINT('Ctrl Pts',(-94.9038820813129,3.62882818933252,134.12411799346));
#97355=CARTESIAN_POINT('Ctrl Pts',(-94.9116468342599,3.72106607789793,134.023292718523));
#97356=CARTESIAN_POINT('Ctrl Pts',(-94.919411587207,3.80921980790795,133.918487973268));
#97357=CARTESIAN_POINT('Ctrl Pts',(-94.927176340154,3.89292880158878,133.810069919588));
#97358=CARTESIAN_POINT('Ctrl Pts',(-94.9349333810389,3.97655465431699,133.701759548248));
#97359=CARTESIAN_POINT('Ctrl Pts',(-94.9426904219239,4.05574431853306,133.589843317792));
#97360=CARTESIAN_POINT('Ctrl Pts',(-94.9504474628088,4.13017553939704,133.47472259233));
#97361=CARTESIAN_POINT('Ctrl Pts',(-94.9581986540489,4.20455063109848,133.359688680303));
#97362=CARTESIAN_POINT('Ctrl Pts',(-94.9659498452889,4.27417421048338,133.241455410226));
#97363=CARTESIAN_POINT('Ctrl Pts',(-94.973701036529,4.33876586491409,133.120455138944));
#97364=CARTESIAN_POINT('Ctrl Pts',(-94.981448933306,4.40333006616854,132.999506296005));
#97365=CARTESIAN_POINT('Ctrl Pts',(-94.9891968300829,4.46286641245744,132.875793135111));
#97366=CARTESIAN_POINT('Ctrl Pts',(-94.9969447268599,4.51713931875218,132.749774567728));
#97367=CARTESIAN_POINT('Ctrl Pts',(-95.004691002944,4.5714008723249,132.623782360712));
#97368=CARTESIAN_POINT('Ctrl Pts',(-95.012437279028,4.62040102130089,132.495486065263));
#97369=CARTESIAN_POINT('Ctrl Pts',(-95.020183555112,4.66395159035826,132.36536626307));
#97370=CARTESIAN_POINT('Ctrl Pts',(-95.0279298883773,4.70750248089598,132.235245500361));
#97371=CARTESIAN_POINT('Ctrl Pts',(-95.0356762216425,4.74560358715529,132.103301574798));
#97372=CARTESIAN_POINT('Ctrl Pts',(-95.0434225549078,4.7781161788708,131.970031601898));
#97373=CARTESIAN_POINT('Ctrl Pts',(-95.0511706229106,4.81063605155575,131.836731784111));
#97374=CARTESIAN_POINT('Ctrl Pts',(-95.0589186909136,4.83756482669407,131.702105707825));
#97375=CARTESIAN_POINT('Ctrl Pts',(-95.0666667589165,4.85881468364112,131.566661694919));
#97376=CARTESIAN_POINT('Ctrl Pts',(-95.0744230616583,4.8800871251891,131.431073730503));
#97377=CARTESIAN_POINT('Ctrl Pts',(-95.0821793644,4.89566853104698,131.294666479777));
#97378=CARTESIAN_POINT('Ctrl Pts',(-95.0899356671418,4.90552281530287,131.157954977028));
#97379=CARTESIAN_POINT('Ctrl Pts',(-95.0976961096558,4.91538235908697,131.021170507233));
#97380=CARTESIAN_POINT('Ctrl Pts',(-95.10545655217,4.91950867870449,130.884081852439));
#97381=CARTESIAN_POINT('Ctrl Pts',(-95.1132169946841,4.91791787180366,130.747204089556));
#97382=CARTESIAN_POINT('Ctrl Pts',(-95.1209898949494,4.91632451119835,130.610106598336));
#97383=CARTESIAN_POINT('Ctrl Pts',(-95.1287627952148,4.90899570514173,130.473221066174));
#97384=CARTESIAN_POINT('Ctrl Pts',(-95.1365356954802,4.8959995602815,130.337058393921));
#97385=CARTESIAN_POINT('Ctrl Pts',(-95.144026031243,4.88347585802091,130.205845577764));
#97386=CARTESIAN_POINT('Ctrl Pts',(-95.1515163670057,4.86568974893018,130.0753042836));
#97387=CARTESIAN_POINT('Ctrl Pts',(-95.1590067027684,4.84274669522234,129.945880851693));
#97388=CARTESIAN_POINT('Ctrl Pts',(-95.1667810368876,4.81893374866204,129.811550291041));
#97389=CARTESIAN_POINT('Ctrl Pts',(-95.1745553710066,4.78948965464658,129.677998514639));
#97390=CARTESIAN_POINT('Ctrl Pts',(-95.1823297051257,4.75447617614294,129.54573463937));
#97391=CARTESIAN_POINT('Ctrl Pts',(-95.1900944580729,4.71950584862231,129.413633767508));
#97392=CARTESIAN_POINT('Ctrl Pts',(-95.19785921102,4.67897989255844,129.282818012996));
#97393=CARTESIAN_POINT('Ctrl Pts',(-95.2056239639671,4.6330114692282,129.153788659577));
#97394=CARTESIAN_POINT('Ctrl Pts',(-95.2133810048521,4.58708870238405,129.02488745993));
#97395=CARTESIAN_POINT('Ctrl Pts',(-95.2211380457372,4.53573435589198,128.897769496389));
#97396=CARTESIAN_POINT('Ctrl Pts',(-95.2288950866223,4.47911192213214,128.772922838181));
#97397=CARTESIAN_POINT('Ctrl Pts',(-95.2366462778624,4.42253218778998,128.648170327809));
#97398=CARTESIAN_POINT('Ctrl Pts',(-95.2443974691026,4.36069243444075,128.525686068144));
#97399=CARTESIAN_POINT('Ctrl Pts',(-95.2521486603428,4.29380484626233,128.405939677715));
#97400=CARTESIAN_POINT('Ctrl Pts',(-95.2598965571199,4.22694568709327,128.286244182697));
#97401=CARTESIAN_POINT('Ctrl Pts',(-95.2676444538971,4.15504315051818,128.169284583081));
#97402=CARTESIAN_POINT('Ctrl Pts',(-95.2753923506743,4.07835599228737,128.055507136081));
#97403=CARTESIAN_POINT('Ctrl Pts',(-95.2831386267584,4.00168487535666,127.941753488869));
#97404=CARTESIAN_POINT('Ctrl Pts',(-95.2908849028425,3.92023134587071,127.831180994277));
#97405=CARTESIAN_POINT('Ctrl Pts',(-95.2986311789267,3.8342980174561,127.724207735673));
#97406=CARTESIAN_POINT('Ctrl Pts',(-95.3063775121921,3.74836405470131,127.617233687417));
#97407=CARTESIAN_POINT('Ctrl Pts',(-95.3141238454575,3.65795047188117,127.513859232965));
#97408=CARTESIAN_POINT('Ctrl Pts',(-95.3218701787229,3.56340051926233,127.414469793097));
#97409=CARTESIAN_POINT('Ctrl Pts',(-95.329618246726,3.46882939283728,127.315058095653));
#97410=CARTESIAN_POINT('Ctrl Pts',(-95.3373663147289,3.37012032278139,127.219633471809));
#97411=CARTESIAN_POINT('Ctrl Pts',(-95.345114382732,3.26765350548347,127.128544567952));
#97412=CARTESIAN_POINT('Ctrl Pts',(-95.3528706854739,3.16507778523262,127.037358853724));
#97413=CARTESIAN_POINT('Ctrl Pts',(-95.3606269882158,3.05873663240364,126.950518324737));
#97414=CARTESIAN_POINT('Ctrl Pts',(-95.3683832909577,2.94904385461191,126.868331729705));
#97415=CARTESIAN_POINT('Ctrl Pts',(-95.3761437334719,2.83929253048188,126.786101269212));
#97416=CARTESIAN_POINT('Ctrl Pts',(-95.3839041759861,2.72618633919327,126.708529913162));
#97417=CARTESIAN_POINT('Ctrl Pts',(-95.3916646185004,2.61016733071024,126.635882529799));
#97418=CARTESIAN_POINT('Ctrl Pts',(-95.3994375187658,2.49396207821512,126.563118526407));
#97419=CARTESIAN_POINT('Ctrl Pts',(-95.4072104190314,2.37483500451532,126.495294484757));
#97420=CARTESIAN_POINT('Ctrl Pts',(-95.4149833192969,2.25325275827421,126.432629259188));
#97421=CARTESIAN_POINT('Ctrl Pts',(-95.4224736550584,2.13609033293938,126.372242072416));
#97422=CARTESIAN_POINT('Ctrl Pts',(-95.42996399082,2.01664841864358,126.316645271589));
#97423=CARTESIAN_POINT('Ctrl Pts',(-95.4374543265815,1.89535953899379,126.265991386174));
#97424=CARTESIAN_POINT('Ctrl Pts',(-95.4452286607005,1.76947195460049,126.213416943295));
#97425=CARTESIAN_POINT('Ctrl Pts',(-95.4530029948194,1.64119581070522,126.166001096162));
#97426=CARTESIAN_POINT('Ctrl Pts',(-95.4607773289384,1.51099282615369,126.123967071953));
#97427=CARTESIAN_POINT('Ctrl Pts',(-95.4685420818854,1.38095030514368,126.081984850923));
#97428=CARTESIAN_POINT('Ctrl Pts',(-95.4763068348325,1.24898603682646,126.045371374849));
#97429=CARTESIAN_POINT('Ctrl Pts',(-95.4840715877795,1.11558293184436,126.01430239405));
#97430=CARTESIAN_POINT('Ctrl Pts',(-95.4918286286644,0.982312324706775,
125.9832642714));
#97431=CARTESIAN_POINT('Ctrl Pts',(-95.4995856695494,0.847606103134692,
125.957759773211));
#97432=CARTESIAN_POINT('Ctrl Pts',(-95.5073427104344,0.71196326521803,125.937915162053));
#97433=CARTESIAN_POINT('Ctrl Pts',(-95.5150939016744,0.576422716620774,
125.918085515871));
#97434=CARTESIAN_POINT('Ctrl Pts',(-95.5228450929144,0.439947342827352,
125.903907317563));
#97435=CARTESIAN_POINT('Ctrl Pts',(-95.5305962841545,0.303046937937487,
125.895455890857));
#97436=CARTESIAN_POINT('Ctrl Pts',(-95.5383441809315,0.166204719371452,
125.887008056233));
#97437=CARTESIAN_POINT('Ctrl Pts',(-95.5460920777085,0.0289382184125221,
125.884282176149));
#97438=CARTESIAN_POINT('Ctrl Pts',(-95.5538399744855,-0.108237252303732,
125.887301764988));
#97439=CARTESIAN_POINT('Ctrl Pts',(-95.5615862505695,-0.245384028868673,
125.890320722195));
#97440=CARTESIAN_POINT('Ctrl Pts',(-95.5693325266535,-0.382439422442771,
125.899082749224));
#97441=CARTESIAN_POINT('Ctrl Pts',(-95.5770788027375,-0.518888117590341,
125.913559232933));
#97442=CARTESIAN_POINT('Ctrl Pts',(-95.5848251360028,-0.655337819970996,
125.928035823505));
#97443=CARTESIAN_POINT('Ctrl Pts',(-95.5925714692681,-0.791180426205342,
125.948226913683));
#97444=CARTESIAN_POINT('Ctrl Pts',(-95.6003178025333,-0.925906135721069,
125.974052046643));
#97445=CARTESIAN_POINT('Ctrl Pts',(-95.6080658705362,-1.0606620161255,125.999882962962));
#97446=CARTESIAN_POINT('Ctrl Pts',(-95.6158139385392,-1.19430011819792,
126.031350359121));
#97447=CARTESIAN_POINT('Ctrl Pts',(-95.6235620065421,-1.32632161042376,
126.068322817018));
#97448=CARTESIAN_POINT('Ctrl Pts',(-95.6313183092839,-1.45848341666278,
126.105334569683));
#97449=CARTESIAN_POINT('Ctrl Pts',(-95.6390746120257,-1.58902480378018,
126.147862966179));
#97450=CARTESIAN_POINT('Ctrl Pts',(-95.6468309147674,-1.71746233961627,
126.19572674466));
#97451=CARTESIAN_POINT('Ctrl Pts',(-95.6545913572815,-1.8459684264324,126.24361606948));
#97452=CARTESIAN_POINT('Ctrl Pts',(-95.6623517997955,-1.97236806437471,
126.296846298812));
#97453=CARTESIAN_POINT('Ctrl Pts',(-95.6701122423096,-2.09619947348481,
126.355188691256));
#97454=CARTESIAN_POINT('Ctrl Pts',(-95.677885142575,-2.22022966776605,126.413624740089));
#97455=CARTESIAN_POINT('Ctrl Pts',(-95.6856580428404,-2.34168304805709,
126.477189169837));
#97456=CARTESIAN_POINT('Ctrl Pts',(-95.6934309431057,-2.4601232510035,126.545607671882));
#97457=CARTESIAN_POINT('Ctrl Pts',(-95.7009212788685,-2.57425785425245,
126.611538989049));
#97458=CARTESIAN_POINT('Ctrl Pts',(-95.7084116146312,-2.68559428959815,
126.681977425453));
#97459=CARTESIAN_POINT('Ctrl Pts',(-95.7159019503939,-2.79377044010429,
126.756641532637));
#97460=CARTESIAN_POINT('Ctrl Pts',(-95.7236359322541,-2.9054653510155,126.833734318442));
#97461=CARTESIAN_POINT('Ctrl Pts',(-95.7313699141143,-3.01415319167601,
126.915582540708));
#97462=CARTESIAN_POINT('Ctrl Pts',(-95.7391038959745,-3.11939900417275,
127.001922858014));
#97463=CARTESIAN_POINT('Ctrl Pts',(-95.7468256553064,-3.22447848968136,
127.088126725949));
#97464=CARTESIAN_POINT('Ctrl Pts',(-95.7545474146384,-3.32612647623596,
127.1788083035));
#97465=CARTESIAN_POINT('Ctrl Pts',(-95.7622691739704,-3.42393670427249,
127.273660898299));
#97466=CARTESIAN_POINT('Ctrl Pts',(-95.7699838766338,-3.52165754667375,
127.368426810348));
#97467=CARTESIAN_POINT('Ctrl Pts',(-95.7776985792971,-3.61554732379551,
127.467355885301));
#97468=CARTESIAN_POINT('Ctrl Pts',(-95.7854132819605,-3.70523244929159,
127.570100955879));
#97469=CARTESIAN_POINT('Ctrl Pts',(-95.7931226519618,-3.79485558141093,
127.672775005606));
#97470=CARTESIAN_POINT('Ctrl Pts',(-95.8008320219632,-3.88027958457348,
127.779259506873));
#97471=CARTESIAN_POINT('Ctrl Pts',(-95.8085413919645,-3.96116772555666,
127.889170518703));
#97472=CARTESIAN_POINT('Ctrl Pts',(-95.8162471491015,-4.04201795969688,
127.999030022618));
#97473=CARTESIAN_POINT('Ctrl Pts',(-95.8239529062385,-4.11833632781777,
128.112312523592));
#97474=CARTESIAN_POINT('Ctrl Pts',(-95.8316586633755,-4.18982669797117,
128.22860144725));
#97475=CARTESIAN_POINT('Ctrl Pts',(-95.8393640142852,-4.26131329934031,
128.344884240461));
#97476=CARTESIAN_POINT('Ctrl Pts',(-95.8470693651949,-4.32797219364736,
128.464172809372));
#97477=CARTESIAN_POINT('Ctrl Pts',(-95.8547747161047,-4.38955097814496,
128.586022213993));
#97478=CARTESIAN_POINT('Ctrl Pts',(-95.8624797057105,-4.45112687521296,
128.707865905095));
#97479=CARTESIAN_POINT('Ctrl Pts',(-95.8701846953162,-4.50762296300028,
128.832269837348));
#97480=CARTESIAN_POINT('Ctrl Pts',(-95.877889684922,-4.55883351165112,128.958765842013));
#97481=CARTESIAN_POINT('Ctrl Pts',(-95.8855986625547,-4.61007056637895,
129.085327319769));
#97482=CARTESIAN_POINT('Ctrl Pts',(-95.8933076401875,-4.65601647346959,
129.213982664105));
#97483=CARTESIAN_POINT('Ctrl Pts',(-95.9010166178202,-4.69651421639679,
129.344245116079));
#97484=CARTESIAN_POINT('Ctrl Pts',(-95.9056837601004,-4.72103221829949,
129.423108154227));
#97485=CARTESIAN_POINT('Ctrl Pts',(-95.9103509023805,-4.7435542697273,129.502559922525));
#97486=CARTESIAN_POINT('Ctrl Pts',(-95.9150180446607,-4.76405452823415,
129.582490119309));
#97487=CARTESIAN_POINT('Ctrl Pts',(-94.1652277315646,-4.76405452823406,
129.582490119308));
#97488=CARTESIAN_POINT('Ctrl Pts',(-94.1729478262758,-4.79804369541448,
129.715013366287));
#97489=CARTESIAN_POINT('Ctrl Pts',(-94.1806679209871,-4.82650721410582,
129.848987986936));
#97490=CARTESIAN_POINT('Ctrl Pts',(-94.1883880156982,-4.84933477376199,
129.983912377588));
#97491=CARTESIAN_POINT('Ctrl Pts',(-94.1961801070834,-4.87237522049178,
130.120095056867));
#97492=CARTESIAN_POINT('Ctrl Pts',(-94.2039721984684,-4.88967394969018,
130.257244916243));
#97493=CARTESIAN_POINT('Ctrl Pts',(-94.2117642898536,-4.90117065471659,
130.394837387645));
#97494=CARTESIAN_POINT('Ctrl Pts',(-94.2195563812387,-4.912667359743,130.532429859047));
#97495=CARTESIAN_POINT('Ctrl Pts',(-94.2273484726239,-4.9183620243331,130.670464531076));
#97496=CARTESIAN_POINT('Ctrl Pts',(-94.2351405640091,-4.91824832960088,
130.808414119523));
#97497=CARTESIAN_POINT('',(-93.8898594359371,-4.9182489755649,130.801186211347));
#97498=CARTESIAN_POINT('Ctrl Pts',(-93.8201028328085,-4.76405452823393,
129.582490119308));
#97499=CARTESIAN_POINT('Ctrl Pts',(-93.8288924822948,-4.80247123866298,
129.732276290216));
#97500=CARTESIAN_POINT('Ctrl Pts',(-93.8376821317811,-4.83386392063157,
129.884047727739));
#97501=CARTESIAN_POINT('Ctrl Pts',(-93.8464717812675,-4.85804604657392,
130.037176368596));
#97502=CARTESIAN_POINT('Ctrl Pts',(-93.8552077517182,-4.88208049049494,
130.189369841584));
#97503=CARTESIAN_POINT('Ctrl Pts',(-93.8639437221688,-4.8989920902913,130.342903811076));
#97504=CARTESIAN_POINT('Ctrl Pts',(-93.8726796926194,-4.90864545612675,
130.497142700533));
#97505=CARTESIAN_POINT('Ctrl Pts',(-93.8784062737253,-4.91497340591942,
130.59824898462));
#97506=CARTESIAN_POINT('Ctrl Pts',(-93.8841328548312,-4.91818344564875,
130.699657792874));
#97507=CARTESIAN_POINT('Ctrl Pts',(-93.8898594359371,-4.9182489755649,130.801186211347));
#97508=CARTESIAN_POINT('Ctrl Pts',(-93.8898594359916,-4.91824897556552,
130.801186212314));
#97509=CARTESIAN_POINT('Ctrl Pts',(-93.8976582558575,-4.91833821831731,
130.93945402557));
#97510=CARTESIAN_POINT('Ctrl Pts',(-93.9054570757235,-4.91259240001704,
131.077749479743));
#97511=CARTESIAN_POINT('Ctrl Pts',(-93.9132558955893,-4.90103119738631,
131.215549460734));
#97512=CARTESIAN_POINT('Ctrl Pts',(-93.9210552260816,-4.88946923778778,
131.353358464156));
#97513=CARTESIAN_POINT('Ctrl Pts',(-93.928854556574,-4.87209116707281,131.490671547624));
#97514=CARTESIAN_POINT('Ctrl Pts',(-93.9366538870663,-4.84896860855516,
131.626970182151));
#97515=CARTESIAN_POINT('Ctrl Pts',(-93.9444553313755,-4.82583978323616,
131.763305757074));
#97516=CARTESIAN_POINT('Ctrl Pts',(-93.9522567756846,-4.79696343420705,
131.89862595763));
#97517=CARTESIAN_POINT('Ctrl Pts',(-93.9600582199938,-4.76246236580466,
132.032422210807));
#97518=CARTESIAN_POINT('Ctrl Pts',(-93.967863382338,-4.72794485478284,132.166282228992));
#97519=CARTESIAN_POINT('Ctrl Pts',(-93.9756685446822,-4.68779738267569,
132.298616482816));
#97520=CARTESIAN_POINT('Ctrl Pts',(-93.9834737070264,-4.64219260075093,
132.428931613255));
#97521=CARTESIAN_POINT('Ctrl Pts',(-93.9912890127563,-4.59652855203957,
132.559416097842));
#97522=CARTESIAN_POINT('Ctrl Pts',(-93.9991043184861,-4.54539315719707,
132.68787585688));
#97523=CARTESIAN_POINT('Ctrl Pts',(-94.006919624216,-4.48900745015003,132.813836961044));
#97524=CARTESIAN_POINT('Ctrl Pts',(-94.0147406807408,-4.43258025238576,
132.939890752111));
#97525=CARTESIAN_POINT('Ctrl Pts',(-94.0225617372657,-4.37089521509931,
133.063441882653));
#97526=CARTESIAN_POINT('Ctrl Pts',(-94.0303827937905,-4.30421889949876,
133.184041841532));
#97527=CARTESIAN_POINT('Ctrl Pts',(-94.038216330487,-4.23743618754821,133.30483424349));
#97528=CARTESIAN_POINT('Ctrl Pts',(-94.0460498671836,-4.16564648951891,
133.422665742289));
#97529=CARTESIAN_POINT('Ctrl Pts',(-94.0538834038801,-4.08915953845766,
133.537116979107));
#97530=CARTESIAN_POINT('Ctrl Pts',(-94.0575240038123,-4.05361258187441,
133.590307661826));
#97531=CARTESIAN_POINT('Ctrl Pts',(-94.0611646037445,-4.01705164262998,
133.642768717421));
#97532=CARTESIAN_POINT('Ctrl Pts',(-94.0648052036766,-3.97951065453995,
133.694460618068));
#97533=CARTESIAN_POINT('Ctrl Pts',(-94.0725795377957,-3.89934359690934,
133.8048463002));
#97534=CARTESIAN_POINT('Ctrl Pts',(-94.0803538719147,-3.8144531787387,133.912068725817));
#97535=CARTESIAN_POINT('Ctrl Pts',(-94.0881282060338,-3.72511761616584,
134.015697069611));
#97536=CARTESIAN_POINT('Ctrl Pts',(-94.0958929589809,-3.63589215168971,
134.119197700732));
#97537=CARTESIAN_POINT('Ctrl Pts',(-94.103657711928,-3.54223269570981,134.219112769909));
#97538=CARTESIAN_POINT('Ctrl Pts',(-94.1114224648751,-3.44446025984409,
134.315040976251));
#97539=CARTESIAN_POINT('Ctrl Pts',(-94.1191795057601,-3.34678493294002,
134.410873905346));
#97540=CARTESIAN_POINT('Ctrl Pts',(-94.1269365466451,-3.24500503289072,
134.502727579765));
#97541=CARTESIAN_POINT('Ctrl Pts',(-94.1346935875301,-3.13948105341171,
134.590234595628));
#97542=CARTESIAN_POINT('Ctrl Pts',(-94.1424447787702,-3.03403665038606,
134.677675621771));
#97543=CARTESIAN_POINT('Ctrl Pts',(-94.1501959700104,-2.92485408754741,
134.76077626516));
#97544=CARTESIAN_POINT('Ctrl Pts',(-94.1579471612506,-2.81232957634721,
134.839207010739));
#97545=CARTESIAN_POINT('Ctrl Pts',(-94.1656950580277,-2.69985289106641,
134.917604421159));
#97546=CARTESIAN_POINT('Ctrl Pts',(-94.1734429548046,-2.58403740259514,
134.991335658353));
#97547=CARTESIAN_POINT('Ctrl Pts',(-94.1811908515817,-2.46531098567366,
135.060112584777));
#97548=CARTESIAN_POINT('Ctrl Pts',(-94.1889371276658,-2.34660940375914,
135.12887512455));
#97549=CARTESIAN_POINT('Ctrl Pts',(-94.19668340375,-2.2249984426239,135.192685219029));
#97550=CARTESIAN_POINT('Ctrl Pts',(-94.2044296798341,-2.10093309505414,
135.251299249097));
#97551=CARTESIAN_POINT('Ctrl Pts',(-94.2121760130994,-1.976866831662,135.309913711841));
#97552=CARTESIAN_POINT('Ctrl Pts',(-94.2199223463648,-1.8503464991821,135.363331866627));
#97553=CARTESIAN_POINT('Ctrl Pts',(-94.2276686796302,-1.72184934839801,
135.411357240521));
#97554=CARTESIAN_POINT('Ctrl Pts',(-94.2354167476332,-1.59332342156811,
135.459393369365));
#97555=CARTESIAN_POINT('Ctrl Pts',(-94.2431648156361,-1.46282016167545,
135.502034177335));
#97556=CARTESIAN_POINT('Ctrl Pts',(-94.2509128836391,-1.33083396029842,
135.539132421214));
#97557=CARTESIAN_POINT('Ctrl Pts',(-94.2586691863809,-1.19870748241608,
135.576270093548));
#97558=CARTESIAN_POINT('Ctrl Pts',(-94.2664254891228,-1.06509529162429,
135.607853328517));
#97559=CARTESIAN_POINT('Ctrl Pts',(-94.2741817918646,-0.930504555252162,
135.633785462737));
#97560=CARTESIAN_POINT('Ctrl Pts',(-94.2819422343788,-0.795841983751215,
135.659731437718));
#97561=CARTESIAN_POINT('Ctrl Pts',(-94.2897026768929,-0.660200212458831,
135.680020244181));
#97562=CARTESIAN_POINT('Ctrl Pts',(-94.2974631194071,-0.524092614363329,
135.694607032019));
#97563=CARTESIAN_POINT('Ctrl Pts',(-94.3052360196725,-0.3877665242683,135.709217235863));
#97564=CARTESIAN_POINT('Ctrl Pts',(-94.3130089199379,-0.250973503421118,
135.718107104329));
#97565=CARTESIAN_POINT('Ctrl Pts',(-94.3207818202033,-0.114228920699665,
135.721283925507));
#97566=CARTESIAN_POINT('Ctrl Pts',(-94.3282721559654,0.0175446520010466,
135.724345261234));
#97567=CARTESIAN_POINT('Ctrl Pts',(-94.3357624917274,0.149272939156129,
135.72210171085));
#97568=CARTESIAN_POINT('Ctrl Pts',(-94.3432528274895,0.28050026857667,135.714605281718));
#97569=CARTESIAN_POINT('Ctrl Pts',(-94.3510271616085,0.41670312207732,135.706824623196));
#97570=CARTESIAN_POINT('Ctrl Pts',(-94.3588014957276,0.552797730030421,
135.693360250267));
#97571=CARTESIAN_POINT('Ctrl Pts',(-94.3665758298467,0.688271244284175,
135.674213362444));
#97572=CARTESIAN_POINT('Ctrl Pts',(-94.3743405827937,0.823577799539594,
135.655090071448));
#97573=CARTESIAN_POINT('Ctrl Pts',(-94.3821053357407,0.958264400696356,
135.63029825401));
#97574=CARTESIAN_POINT('Ctrl Pts',(-94.3898700886878,1.09181990732962,135.599891073361));
#97575=CARTESIAN_POINT('Ctrl Pts',(-94.3976271295728,1.22524276475018,135.569514093553));
#97576=CARTESIAN_POINT('Ctrl Pts',(-94.4053841704578,1.35753638455871,135.53353293576));
#97577=CARTESIAN_POINT('Ctrl Pts',(-94.4131412113428,1.4881968038063,135.492052302782));
#97578=CARTESIAN_POINT('Ctrl Pts',(-94.4208924025829,1.6187586910166,135.450602950671));
#97579=CARTESIAN_POINT('Ctrl Pts',(-94.428643593823,1.74768945797974,135.403662495943));
#97580=CARTESIAN_POINT('Ctrl Pts',(-94.4363947850632,1.87449771237708,135.351386171573));
#97581=CARTESIAN_POINT('Ctrl Pts',(-94.4441426818402,2.00125206988272,135.299132066036));
#97582=CARTESIAN_POINT('Ctrl Pts',(-94.4518905786173,2.12588534838054,135.24154675021));
#97583=CARTESIAN_POINT('Ctrl Pts',(-94.4596384753943,2.24792385284434,135.178834461849));
#97584=CARTESIAN_POINT('Ctrl Pts',(-94.4673847514784,2.36993682948418,135.116135291546));
#97585=CARTESIAN_POINT('Ctrl Pts',(-94.4751310275626,2.48935576417221,135.048311460457));
#97586=CARTESIAN_POINT('Ctrl Pts',(-94.4828773036467,2.60572975853007,134.975614084812));
#97587=CARTESIAN_POINT('Ctrl Pts',(-94.490623636912,2.72210461193449,134.902916172532));
#97588=CARTESIAN_POINT('Ctrl Pts',(-94.4983699701774,2.835434148573,134.825344851047));
#97589=CARTESIAN_POINT('Ctrl Pts',(-94.5061163034428,2.94529510449609,134.743195446539));
#97590=CARTESIAN_POINT('Ctrl Pts',(-94.5138643714458,3.05518066301839,134.661027645242));
#97591=CARTESIAN_POINT('Ctrl Pts',(-94.5216124394487,3.16159578210479,134.574279954917));
#97592=CARTESIAN_POINT('Ctrl Pts',(-94.5293605074517,3.26414935114367,134.483288732646));
#97593=CARTESIAN_POINT('Ctrl Pts',(-94.5371168101935,3.36681191533599,134.392200803822));
#97594=CARTESIAN_POINT('Ctrl Pts',(-94.5448731129353,3.46560443818187,134.29686059358));
#97595=CARTESIAN_POINT('Ctrl Pts',(-94.5526294156772,3.56017145770785,134.197642547236));
#97596=CARTESIAN_POINT('Ctrl Pts',(-94.5603898581913,3.65478895049952,134.098371545233));
#97597=CARTESIAN_POINT('Ctrl Pts',(-94.5681503007055,3.74517618860425,133.995218876946));
#97598=CARTESIAN_POINT('Ctrl Pts',(-94.5759107432196,3.83101794771462,133.888592215029));
#97599=CARTESIAN_POINT('Ctrl Pts',(-94.583683643485,3.91699750763739,133.781794386529));
#97600=CARTESIAN_POINT('Ctrl Pts',(-94.5914565437505,3.99841677487503,133.671511734964));
#97601=CARTESIAN_POINT('Ctrl Pts',(-94.5992294440159,4.07500331163742,133.558181794158));
#97602=CARTESIAN_POINT('Ctrl Pts',(-94.606719779778,4.1488057348801,133.448971682159));
#97603=CARTESIAN_POINT('Ctrl Pts',(-94.6142101155402,4.21812052925243,133.33693224965));
#97604=CARTESIAN_POINT('Ctrl Pts',(-94.6217004513024,4.28274514807211,133.222474977799));
#97605=CARTESIAN_POINT('Ctrl Pts',(-94.6294747854214,4.34982002895534,133.103678023699));
#97606=CARTESIAN_POINT('Ctrl Pts',(-94.6372491195405,4.41205453057355,132.981899953175));
#97607=CARTESIAN_POINT('Ctrl Pts',(-94.6450234536596,4.46917245515842,132.857572888266));
#97608=CARTESIAN_POINT('Ctrl Pts',(-94.6527882066067,4.52621998700617,132.733399045353));
#97609=CARTESIAN_POINT('Ctrl Pts',(-94.6605529595537,4.57816332668305,132.606682810378));
#97610=CARTESIAN_POINT('Ctrl Pts',(-94.6683177125009,4.62477091803712,132.477882956281));
#97611=CARTESIAN_POINT('Ctrl Pts',(-94.6760747533859,4.67133221807454,132.349211028015));
#97612=CARTESIAN_POINT('Ctrl Pts',(-94.6838317942709,4.71256818394173,132.218459964242));
#97613=CARTESIAN_POINT('Ctrl Pts',(-94.691588835156,4.74829450078647,132.086110357687));
#97614=CARTESIAN_POINT('Ctrl Pts',(-94.6993400263961,4.78399387613743,131.953860557001));
#97615=CARTESIAN_POINT('Ctrl Pts',(-94.7070912176363,4.81419177100366,131.820014988882));
#97616=CARTESIAN_POINT('Ctrl Pts',(-94.7148424088764,4.8387531777343,131.68507098282));
#97617=CARTESIAN_POINT('Ctrl Pts',(-94.7225903056535,4.86330414521205,131.55018433156));
#97618=CARTESIAN_POINT('Ctrl Pts',(-94.7303382024306,4.88222331947136,131.414200554757));
#97619=CARTESIAN_POINT('Ctrl Pts',(-94.7380860992077,4.89542648778786,131.277628580949));
#97620=CARTESIAN_POINT('Ctrl Pts',(-94.7458323752918,4.90862689428618,131.141085175054));
#97621=CARTESIAN_POINT('Ctrl Pts',(-94.7535786513759,4.91611363548783,131.003954205787));
#97622=CARTESIAN_POINT('Ctrl Pts',(-94.76132492746,4.91785426100443,130.866750761183));
#97623=CARTESIAN_POINT('Ctrl Pts',(-94.7690712607254,4.91959489936993,130.729546303775));
#97624=CARTESIAN_POINT('Ctrl Pts',(-94.7768175939907,4.91558933245176,130.592269760894));
#97625=CARTESIAN_POINT('Ctrl Pts',(-94.7845639272561,4.90585724202649,130.455436867506));
#97626=CARTESIAN_POINT('Ctrl Pts',(-94.7923119952591,4.89612297216703,130.318573331339));
#97627=CARTESIAN_POINT('Ctrl Pts',(-94.800060063262,4.88065965467418,130.182154032268));
#97628=CARTESIAN_POINT('Ctrl Pts',(-94.8078081312649,4.85953887144842,130.046689831946));
#97629=CARTESIAN_POINT('Ctrl Pts',(-94.8155644340068,4.83839564080288,129.91108165866));
#97630=CARTESIAN_POINT('Ctrl Pts',(-94.8233207367487,4.81158299349032,129.77643099879));
#97631=CARTESIAN_POINT('Ctrl Pts',(-94.8310770394906,4.77922382508127,129.643239309401));
#97632=CARTESIAN_POINT('Ctrl Pts',(-94.8388374820048,4.74684738560964,129.509976531596));
#97633=CARTESIAN_POINT('Ctrl Pts',(-94.8465979245189,4.70891863437051,129.378174651425));
#97634=CARTESIAN_POINT('Ctrl Pts',(-94.8543583670331,4.66561017147632,129.248319233053));
#97635=CARTESIAN_POINT('Ctrl Pts',(-94.8621312672986,4.62223218599287,129.118255359236));
#97636=CARTESIAN_POINT('Ctrl Pts',(-94.8699041675641,4.57345737058193,128.990144556821));
#97637=CARTESIAN_POINT('Ctrl Pts',(-94.8776770678295,4.51950657556094,128.864452533155));
#97638=CARTESIAN_POINT('Ctrl Pts',(-94.8851674035915,4.46751702783325,128.743329731151));
#97639=CARTESIAN_POINT('Ctrl Pts',(-94.8926577393534,4.41072141960972,128.624453181565));
#97640=CARTESIAN_POINT('Ctrl Pts',(-94.9001480751154,4.34935646022077,128.508215708281));
#97641=CARTESIAN_POINT('Ctrl Pts',(-94.9079224092344,4.28566482974465,128.387571055867));
#97642=CARTESIAN_POINT('Ctrl Pts',(-94.9156967433535,4.21684875836493,128.269387385369));
#97643=CARTESIAN_POINT('Ctrl Pts',(-94.9234710774726,4.14312251095284,128.154130642312));
#97644=CARTESIAN_POINT('Ctrl Pts',(-94.9312358304197,4.06948712455159,128.039015942889));
#97645=CARTESIAN_POINT('Ctrl Pts',(-94.9390005833668,3.99095381115865,127.926821319887));
#97646=CARTESIAN_POINT('Ctrl Pts',(-94.9467653363139,3.9077833876865,127.817989566035));
#97647=CARTESIAN_POINT('Ctrl Pts',(-94.9545223771989,3.82469557025121,127.709265905415));
#97648=CARTESIAN_POINT('Ctrl Pts',(-94.962279418084,3.73698004403296,127.603898775727));
#97649=CARTESIAN_POINT('Ctrl Pts',(-94.970036458969,3.64494151862112,127.502303018382));
#97650=CARTESIAN_POINT('Ctrl Pts',(-94.9777876502091,3.55297240017737,127.400783875187));
#97651=CARTESIAN_POINT('Ctrl Pts',(-94.9855388414492,3.45668703281444,127.303030732059));
#97652=CARTESIAN_POINT('Ctrl Pts',(-94.9932900326893,3.35643085898491,127.209425993494));
#97653=CARTESIAN_POINT('Ctrl Pts',(-95.0010379294664,3.25621729670381,127.11586103944));
#97654=CARTESIAN_POINT('Ctrl Pts',(-95.0087858262434,3.15203656983306,127.026441249366));
#97655=CARTESIAN_POINT('Ctrl Pts',(-95.0165337230204,3.0442713353298,126.94151256213));
#97656=CARTESIAN_POINT('Ctrl Pts',(-95.0242799991045,2.93652864299044,126.856601640143));
#97657=CARTESIAN_POINT('Ctrl Pts',(-95.0320262751887,2.82520324128915,126.776180194236));
#97658=CARTESIAN_POINT('Ctrl Pts',(-95.0397725512728,2.71071094814917,126.700553943503));
#97659=CARTESIAN_POINT('Ctrl Pts',(-95.0475188845381,2.59621780985325,126.624927134514));
#97660=CARTESIAN_POINT('Ctrl Pts',(-95.0552652178034,2.47855805969385,126.554095806813));
#97661=CARTESIAN_POINT('Ctrl Pts',(-95.0630115510687,2.35817623858243,126.488322168909));
#97662=CARTESIAN_POINT('Ctrl Pts',(-95.0707596190717,2.23776745879667,126.422533801455));
#97663=CARTESIAN_POINT('Ctrl Pts',(-95.0785076870747,2.11463573807559,126.361805565031));
#97664=CARTESIAN_POINT('Ctrl Pts',(-95.0862557550777,1.98924957056218,126.306353368959));
#97665=CARTESIAN_POINT('Ctrl Pts',(-95.0940120578196,1.86373014113764,126.250842237634));
#97666=CARTESIAN_POINT('Ctrl Pts',(-95.1017683605614,1.73595183667613,126.200618506506));
#97667=CARTESIAN_POINT('Ctrl Pts',(-95.1095246633032,1.6064029752666,126.155849829845));
#97668=CARTESIAN_POINT('Ctrl Pts',(-95.1172851058174,1.4767849697291,126.111057258794));
#97669=CARTESIAN_POINT('Ctrl Pts',(-95.1250455483315,1.34539489861243,126.071725655737));
#97670=CARTESIAN_POINT('Ctrl Pts',(-95.1328059908457,1.21273457537751,126.037972266604));
#97671=CARTESIAN_POINT('Ctrl Pts',(-95.1405788911111,1.07986129401471,126.004164693535));
#97672=CARTESIAN_POINT('Ctrl Pts',(-95.1483517913766,0.945714068535662,
125.975953309129));
#97673=CARTESIAN_POINT('Ctrl Pts',(-95.156124691642,0.810804086712758,125.953404031956));
#97674=CARTESIAN_POINT('Ctrl Pts',(-95.163615027404,0.680798422546853,125.931674477807));
#97675=CARTESIAN_POINT('Ctrl Pts',(-95.171105363166,0.550084801065957,125.915202552769));
#97676=CARTESIAN_POINT('Ctrl Pts',(-95.178595698928,0.419121663302422,125.90400143748));
#97677=CARTESIAN_POINT('Ctrl Pts',(-95.1863700330471,0.283193018365383,
125.892375628501));
#97678=CARTESIAN_POINT('Ctrl Pts',(-95.1941443671662,0.146564981733707,
125.886391377625));
#97679=CARTESIAN_POINT('Ctrl Pts',(-95.2019187012853,0.00974538196894736,
125.886120272683));
#97680=CARTESIAN_POINT('Ctrl Pts',(-95.2096834542324,-0.12690559986702,
125.885849501855));
#97681=CARTESIAN_POINT('Ctrl Pts',(-95.2174482071795,-0.263747287887186,
125.891277868353));
#97682=CARTESIAN_POINT('Ctrl Pts',(-95.2252129601266,-0.400266170115626,
125.902425279808));
#97683=CARTESIAN_POINT('Ctrl Pts',(-95.2329700010116,-0.536649459865659,
125.913561619497));
#97684=CARTESIAN_POINT('Ctrl Pts',(-95.2407270418965,-0.672710194716023,
125.930405668606));
#97685=CARTESIAN_POINT('Ctrl Pts',(-95.2484840827815,-0.807934653862507,
125.952925298242));
#97686=CARTESIAN_POINT('Ctrl Pts',(-95.2562352740216,-0.943057139191905,
125.97542794565));
#97687=CARTESIAN_POINT('Ctrl Pts',(-95.2639864652617,-1.07734421997863,
126.003597590541));
#97688=CARTESIAN_POINT('Ctrl Pts',(-95.2717376565018,-1.2102874484048,126.037350301368));
#97689=CARTESIAN_POINT('Ctrl Pts',(-95.2794855532788,-1.34317417241305,
126.071088666394));
#97690=CARTESIAN_POINT('Ctrl Pts',(-95.287233450056,-1.47471780193109,126.110405281727));
#97691=CARTESIAN_POINT('Ctrl Pts',(-95.2949813468331,-1.60442045337004,
126.155165195635));
#97692=CARTESIAN_POINT('Ctrl Pts',(-95.3027276229172,-1.73409597381037,
126.199915746733));
#97693=CARTESIAN_POINT('Ctrl Pts',(-95.3104738990013,-1.86193091279937,
126.250107204168));
#97694=CARTESIAN_POINT('Ctrl Pts',(-95.3182201750854,-1.98744330045985,
126.305554977181));
#97695=CARTESIAN_POINT('Ctrl Pts',(-95.3259665083507,-2.11295661462409,
126.361003159498));
#97696=CARTESIAN_POINT('Ctrl Pts',(-95.3337128416161,-2.23614698562669,
126.42170757683));
#97697=CARTESIAN_POINT('Ctrl Pts',(-95.3414591748815,-2.35655352480187,
126.487435954424));
#97698=CARTESIAN_POINT('Ctrl Pts',(-95.3492072428845,-2.47698702818748,
126.553179051433));
#97699=CARTESIAN_POINT('Ctrl Pts',(-95.3569553108874,-2.5946351161138,126.62394816019));
#97700=CARTESIAN_POINT('Ctrl Pts',(-95.3647033788904,-2.70906290542555,
126.699465827569));
#97701=CARTESIAN_POINT('Ctrl Pts',(-95.3724596816323,-2.82361230995271,
126.775063756022));
#97702=CARTESIAN_POINT('Ctrl Pts',(-95.3802159843742,-2.93493425208004,
126.855420108978));
#97703=CARTESIAN_POINT('Ctrl Pts',(-95.387972287116,-3.04262373166821,126.940214671825));
#97704=CARTESIAN_POINT('Ctrl Pts',(-95.3957327296302,-3.15037068837468,
127.025054492083));
#97705=CARTESIAN_POINT('Ctrl Pts',(-95.4034931721443,-3.25448102277499,
127.114336987894));
#97706=CARTESIAN_POINT('Ctrl Pts',(-95.4112536146585,-3.35458485011532,
127.207703343669));
#97707=CARTESIAN_POINT('Ctrl Pts',(-95.419026514924,-3.45484937300583,127.301219579406));
#97708=CARTESIAN_POINT('Ctrl Pts',(-95.4267994151894,-3.55109426179414,
127.398832497076));
#97709=CARTESIAN_POINT('Ctrl Pts',(-95.4345723154549,-3.64298774784284,
127.500147650524));
#97710=CARTESIAN_POINT('Ctrl Pts',(-95.4420626512169,-3.73154067420819,
127.597779742948));
#97711=CARTESIAN_POINT('Ctrl Pts',(-95.4495529869789,-3.81605287652075,
127.698849336869));
#97712=CARTESIAN_POINT('Ctrl Pts',(-95.457043322741,-3.89626546695886,127.802977857323));
#97713=CARTESIAN_POINT('Ctrl Pts',(-95.4648303242939,-3.97965499529767,
127.911230541345));
#97714=CARTESIAN_POINT('Ctrl Pts',(-95.4726173258466,-4.05866526764973,
128.023137238951));
#97715=CARTESIAN_POINT('Ctrl Pts',(-95.4804043273994,-4.13295930852,128.13830915208));
#97716=CARTESIAN_POINT('Ctrl Pts',(-95.4881786918195,-4.20713278133153,
128.25329415851));
#97717=CARTESIAN_POINT('Ctrl Pts',(-95.4959530562395,-4.27660505651125,
128.371533503499));
#97718=CARTESIAN_POINT('Ctrl Pts',(-95.5037274206595,-4.34107973569718,
128.492605918032));
#97719=CARTESIAN_POINT('Ctrl Pts',(-95.511494515971,-4.40549413041293,128.613565128645));
#97720=CARTESIAN_POINT('Ctrl Pts',(-95.5192616112825,-4.46492004108336,
128.73735179959));
#97721=CARTESIAN_POINT('Ctrl Pts',(-95.527028706594,-4.51910448149372,128.863516021045));
#97722=CARTESIAN_POINT('Ctrl Pts',(-95.5347892209818,-4.57324301237752,
128.989573345767));
#97723=CARTESIAN_POINT('Ctrl Pts',(-95.5425497353695,-4.62214876099844,
129.118003854856));
#97724=CARTESIAN_POINT('Ctrl Pts',(-95.5503102497573,-4.66561506002151,
129.248333890867));
#97725=CARTESIAN_POINT('Ctrl Pts',(-95.556867867916,-4.70234399028569,129.358462494213));
#97726=CARTESIAN_POINT('Ctrl Pts',(-95.5634254860746,-4.73518976908424,
129.469946861467));
#97727=CARTESIAN_POINT('Ctrl Pts',(-95.5699831042333,-4.76405452823397,
129.582490119308));
#97728=CARTESIAN_POINT('Origin',(213.235140564004,0.,130.804360617566));
#97729=CARTESIAN_POINT('',(-97.6652146800015,-4.76405452823416,129.582490119309));
#97730=CARTESIAN_POINT('',(-97.3196997604543,-4.76048812747127,129.583439530431));
#97731=CARTESIAN_POINT('',(213.235140564004,-4.76405452823405,129.582490119308));
#97732=CARTESIAN_POINT('',(-95.9851405639689,-4.91824989715129,130.805366436304));
#97733=CARTESIAN_POINT('Ctrl Pts',(-95.9851405640092,-4.91824989715114,
130.805366437011));
#97734=CARTESIAN_POINT('Ctrl Pts',(-95.9882102340752,-4.91823887890383,
130.85924339672));
#97735=CARTESIAN_POINT('Ctrl Pts',(-95.9912799041412,-4.91734259694869,
130.913110294248));
#97736=CARTESIAN_POINT('Ctrl Pts',(-95.9943495742066,-4.91556186802578,
130.966947776071));
#97737=CARTESIAN_POINT('Ctrl Pts',(-96.0021239083257,-4.91105194307381,
131.103298120867));
#97738=CARTESIAN_POINT('Ctrl Pts',(-96.0098982424448,-4.90085734288855,
131.239676644761));
#97739=CARTESIAN_POINT('Ctrl Pts',(-96.0176725765639,-4.8849669596966,131.375570618505));
#97740=CARTESIAN_POINT('Ctrl Pts',(-96.025437329511,-4.86909615998181,131.511297115071));
#97741=CARTESIAN_POINT('Ctrl Pts',(-96.0332020824581,-4.84754358903086,
131.646539865074));
#97742=CARTESIAN_POINT('Ctrl Pts',(-96.0409668354052,-4.82035012880556,
131.780786599515));
#97743=CARTESIAN_POINT('Ctrl Pts',(-96.0487238762902,-4.79318367750824,
131.914899998206));
#97744=CARTESIAN_POINT('Ctrl Pts',(-96.0564809171752,-4.76038756350126,
132.048018969298));
#97745=CARTESIAN_POINT('Ctrl Pts',(-96.0642379580601,-4.72205436571241,
132.179637182391));
#97746=CARTESIAN_POINT('Ctrl Pts',(-96.0719891493003,-4.68375007528626,
132.311156141165));
#97747=CARTESIAN_POINT('Ctrl Pts',(-96.0797403405404,-4.63991712115529,
132.441176220737));
#97748=CARTESIAN_POINT('Ctrl Pts',(-96.0874915317805,-4.59069889953289,
132.569202445132));
#97749=CARTESIAN_POINT('Ctrl Pts',(-96.0952394285576,-4.54150159696756,
132.697174254968));
#97750=CARTESIAN_POINT('Ctrl Pts',(-96.1029873253346,-4.48692371932166,
132.823153530961));
#97751=CARTESIAN_POINT('Ctrl Pts',(-96.1107352221117,-4.4271580781607,132.946661813354));
#97752=CARTESIAN_POINT('Ctrl Pts',(-96.1184814981958,-4.36740493868348,
133.070144260478));
#97753=CARTESIAN_POINT('Ctrl Pts',(-96.1262277742798,-4.30246636433993,
133.191156390399));
#97754=CARTESIAN_POINT('Ctrl Pts',(-96.1339740503639,-4.23258257873011,
133.309241408488));
#97755=CARTESIAN_POINT('Ctrl Pts',(-96.1417203836292,-4.16269827725396,
133.427327298254));
#97756=CARTESIAN_POINT('Ctrl Pts',(-96.1494667168946,-4.08786889078945,
133.542485696614));
#97757=CARTESIAN_POINT('Ctrl Pts',(-96.1572130501599,-4.00837950330312,
133.654286374494));
#97758=CARTESIAN_POINT('Ctrl Pts',(-96.1649611181629,-3.92887231471971,
133.766112089359));
#97759=CARTESIAN_POINT('Ctrl Pts',(-96.1727091861658,-3.84470327502629,
133.874578268899));
#97760=CARTESIAN_POINT('Ctrl Pts',(-96.1804572541687,-3.75619925886632,
133.979285843487));
#97761=CARTESIAN_POINT('Ctrl Pts',(-96.1882135569105,-3.66760117958464,
134.084104702533));
#97762=CARTESIAN_POINT('Ctrl Pts',(-96.1959698596524,-3.5746591731151,134.185156677737));
#97763=CARTESIAN_POINT('Ctrl Pts',(-96.2037261623942,-3.47773904683619,
134.282077423836));
#97764=CARTESIAN_POINT('Ctrl Pts',(-96.2114866049084,-3.38076719136742,
134.379049899455));
#97765=CARTESIAN_POINT('Ctrl Pts',(-96.2192470474225,-3.27981327299003,
134.471886487885));
#97766=CARTESIAN_POINT('Ctrl Pts',(-96.2270074899367,-3.17527728244498,
134.560262272574));
#97767=CARTESIAN_POINT('Ctrl Pts',(-96.2347803902021,-3.07057348144764,
134.648779925918));
#97768=CARTESIAN_POINT('Ctrl Pts',(-96.2425532904675,-2.96227642647806,
134.732822225973));
#97769=CARTESIAN_POINT('Ctrl Pts',(-96.2503261907329,-2.85081698760548,
134.8121063138));
#97770=CARTESIAN_POINT('Ctrl Pts',(-96.2578165264951,-2.74340938008197,
134.888508225332));
#97771=CARTESIAN_POINT('Ctrl Pts',(-96.2653068622573,-2.63306557610413,
134.96049169621));
#97772=CARTESIAN_POINT('Ctrl Pts',(-96.2727971980195,-2.52019207778084,
135.027844363668));
#97773=CARTESIAN_POINT('Ctrl Pts',(-96.2805715321388,-2.40303894646081,
135.097750727985));
#97774=CARTESIAN_POINT('Ctrl Pts',(-96.2883458662582,-2.28278940144744,
135.16288964552));
#97775=CARTESIAN_POINT('Ctrl Pts',(-96.2961202003775,-2.15986881235654,
135.222974628306));
#97776=CARTESIAN_POINT('Ctrl Pts',(-96.3038849533248,-2.03709971190629,
135.282985561721));
#97777=CARTESIAN_POINT('Ctrl Pts',(-96.3116497062722,-1.91166646500117,
135.337954783245));
#97778=CARTESIAN_POINT('Ctrl Pts',(-96.3194144592195,-1.78402215575809,
135.387639794123));
#97779=CARTESIAN_POINT('Ctrl Pts',(-96.3271715001047,-1.65650462464206,
135.437275457149));
#97780=CARTESIAN_POINT('Ctrl Pts',(-96.3349285409899,-1.52678076342298,
135.481637213087));
#97781=CARTESIAN_POINT('Ctrl Pts',(-96.3426855818751,-1.39532660337702,
135.520529267265));
#97782=CARTESIAN_POINT('Ctrl Pts',(-96.3504367731155,-1.26397157393589,
135.559391992643));
#97783=CARTESIAN_POINT('Ctrl Pts',(-96.3581879643559,-1.13088921624073,
135.592793115844));
#97784=CARTESIAN_POINT('Ctrl Pts',(-96.3659391555963,-0.996573476752261,
135.62058573356));
#97785=CARTESIAN_POINT('Ctrl Pts',(-96.3736870523736,-0.862314825035884,
135.648366538673));
#97786=CARTESIAN_POINT('Ctrl Pts',(-96.3814349491509,-0.726824216213565,
135.670543500372));
#97787=CARTESIAN_POINT('Ctrl Pts',(-96.3891828459282,-0.590608411390184,
135.687020217302));
#97788=CARTESIAN_POINT('Ctrl Pts',(-96.3969291220126,-0.454421099976698,
135.703493487659));
#97789=CARTESIAN_POINT('Ctrl Pts',(-96.404675398097,-0.31750928218268,135.714268838013));
#97790=CARTESIAN_POINT('Ctrl Pts',(-96.4124216741813,-0.180387118989354,
135.71930146663));
#97791=CARTESIAN_POINT('Ctrl Pts',(-96.4201680074469,-0.0432639435915556,
135.724334132397));
#97792=CARTESIAN_POINT('Ctrl Pts',(-96.4279143407125,0.094069189601743,
135.723623977498));
#97793=CARTESIAN_POINT('Ctrl Pts',(-96.435660673978,0.231096221838379,135.717178301823));
#97794=CARTESIAN_POINT('Ctrl Pts',(-96.4434087419813,0.368153940328618,
135.710731182685));
#97795=CARTESIAN_POINT('Ctrl Pts',(-96.4511568099844,0.50490503099862,135.698546005271));
#97796=CARTESIAN_POINT('Ctrl Pts',(-96.4589048779876,0.64083706154235,135.680682071598));
#97797=CARTESIAN_POINT('Ctrl Pts',(-96.4666611807297,0.776913562265933,
135.662799151924));
#97798=CARTESIAN_POINT('Ctrl Pts',(-96.4744174834719,0.912168875681759,
135.639225470552));
#97799=CARTESIAN_POINT('Ctrl Pts',(-96.482173786214,1.04609873997669,135.610071854076));
#97800=CARTESIAN_POINT('Ctrl Pts',(-96.4899342287284,1.18010008667275,135.580902677437));
#97801=CARTESIAN_POINT('Ctrl Pts',(-96.4976946712429,1.31277419661058,135.546147730444));
#97802=CARTESIAN_POINT('Ctrl Pts',(-96.5054551137573,1.44363150352852,135.505967911303));
#97803=CARTESIAN_POINT('Ctrl Pts',(-96.5132280140229,1.57469887421212,135.465723591949));
#97804=CARTESIAN_POINT('Ctrl Pts',(-96.5210009142885,1.70394324496737,135.420037128494));
#97805=CARTESIAN_POINT('Ctrl Pts',(-96.5287738145542,1.83089374275992,135.369118131961));
#97806=CARTESIAN_POINT('Ctrl Pts',(-96.5362641503141,1.95322927014955,135.320050169225));
#97807=CARTESIAN_POINT('Ctrl Pts',(-96.5437544860739,2.07343452418635,135.266123626158));
#97808=CARTESIAN_POINT('Ctrl Pts',(-96.5512448218338,2.19111111374094,135.207565717234));
#97809=CARTESIAN_POINT('Ctrl Pts',(-96.5590191559527,2.31324944698682,135.146787567379));
#97810=CARTESIAN_POINT('Ctrl Pts',(-96.5667934900716,2.43305047947014,135.080827395553));
#97811=CARTESIAN_POINT('Ctrl Pts',(-96.5745678241904,2.55004325808241,135.009888223516));
#97812=CARTESIAN_POINT('Ctrl Pts',(-96.5823325771373,2.66689185355067,134.939036477669));
#97813=CARTESIAN_POINT('Ctrl Pts',(-96.5900973300841,2.78093875025133,134.86321814153));
#97814=CARTESIAN_POINT('Ctrl Pts',(-96.5978620830309,2.89173502408148,134.782683331097));
#97815=CARTESIAN_POINT('Ctrl Pts',(-96.6056191239157,3.00242125349081,134.702228508974));
#97816=CARTESIAN_POINT('Ctrl Pts',(-96.6133761648005,3.10986297081719,134.617066763246));
#97817=CARTESIAN_POINT('Ctrl Pts',(-96.6211332056853,3.21363814192348,134.527492760705));
#97818=CARTESIAN_POINT('Ctrl Pts',(-96.6288843969252,3.31733505536585,134.437986306616));
#97819=CARTESIAN_POINT('Ctrl Pts',(-96.6366355881651,3.41737063133081,134.344074472963));
#97820=CARTESIAN_POINT('Ctrl Pts',(-96.644386779405,3.51335428577712,134.246093426067));
#97821=CARTESIAN_POINT('Ctrl Pts',(-96.6521346761819,3.60929714460997,134.148154023729));
#97822=CARTESIAN_POINT('Ctrl Pts',(-96.6598825729588,3.7011912341784,134.046149126742));
#97823=CARTESIAN_POINT('Ctrl Pts',(-96.6676304697357,3.78868153253689,133.940452980287));
#97824=CARTESIAN_POINT('Ctrl Pts',(-96.6753767458196,3.87615352981104,133.834778943187));
#97825=CARTESIAN_POINT('Ctrl Pts',(-96.6831230219035,3.95922331901052,133.72541549341));
#97826=CARTESIAN_POINT('Ctrl Pts',(-96.6908692979874,4.03757529059656,133.612770992718));
#97827=CARTESIAN_POINT('Ctrl Pts',(-96.6986156312526,4.11592784055916,133.500125660511));
#97828=CARTESIAN_POINT('Ctrl Pts',(-96.7063619645176,4.18956228016758,133.384199550018));
#97829=CARTESIAN_POINT('Ctrl Pts',(-96.7141082977828,4.25820580866642,133.265430781852));
#97830=CARTESIAN_POINT('Ctrl Pts',(-96.7218563657855,4.32686470940744,133.146635416245));
#97831=CARTESIAN_POINT('Ctrl Pts',(-96.7296044337884,4.39053027938544,133.024996464649));
#97832=CARTESIAN_POINT('Ctrl Pts',(-96.7373525017912,4.44897542888738,132.900977105066));
#97833=CARTESIAN_POINT('Ctrl Pts',(-96.7451088045329,4.50748269458981,132.776825936231));
#97834=CARTESIAN_POINT('Ctrl Pts',(-96.7528651072745,4.56075828950776,132.650289659834));
#97835=CARTESIAN_POINT('Ctrl Pts',(-96.7606214100161,4.60862288936522,132.521852430099));
#97836=CARTESIAN_POINT('Ctrl Pts',(-96.7683818525301,4.65651303600081,132.393346649548));
#97837=CARTESIAN_POINT('Ctrl Pts',(-96.7761422950441,4.6989863119534,132.262938265555));
#97838=CARTESIAN_POINT('Ctrl Pts',(-96.783902737558,4.73591346291848,132.131126133491));
#97839=CARTESIAN_POINT('Ctrl Pts',(-96.7916756378232,4.77289989262452,131.999102404891));
#97840=CARTESIAN_POINT('Ctrl Pts',(-96.7994485380884,4.8043223163777,131.865670805942));
#97841=CARTESIAN_POINT('Ctrl Pts',(-96.8072214383537,4.83010256749374,131.731340795342));
#97842=CARTESIAN_POINT('Ctrl Pts',(-96.8147117741174,4.85494564155144,131.601894018952));
#97843=CARTESIAN_POINT('Ctrl Pts',(-96.8222021098811,4.87454958958725,131.47161332052));
#97844=CARTESIAN_POINT('Ctrl Pts',(-96.8296924456448,4.8888902334363,131.340956692758));
#97845=CARTESIAN_POINT('Ctrl Pts',(-96.8374667797639,4.90377460715241,131.205346179271));
#97846=CARTESIAN_POINT('Ctrl Pts',(-96.845241113883,4.91303583086735,131.068901093659));
#97847=CARTESIAN_POINT('Ctrl Pts',(-96.8530154480021,4.9165901508792,130.932127400329));
#97848=CARTESIAN_POINT('Ctrl Pts',(-96.8607802009493,4.92014009050929,130.795522268353));
#97849=CARTESIAN_POINT('Ctrl Pts',(-96.8685449538964,4.91799711044606,130.658589721529));
#97850=CARTESIAN_POINT('Ctrl Pts',(-96.8763097068435,4.91012898591992,130.521842646228));
#97851=CARTESIAN_POINT('Ctrl Pts',(-96.8840667477285,4.90226867612598,130.385231390049));
#97852=CARTESIAN_POINT('Ctrl Pts',(-96.8918237886136,4.88869456016397,130.248805626594));
#97853=CARTESIAN_POINT('Ctrl Pts',(-96.8995808294986,4.86942642979025,130.113079699733));
#97854=CARTESIAN_POINT('Ctrl Pts',(-96.9073320207387,4.8501728296635,129.977456124849));
#97855=CARTESIAN_POINT('Ctrl Pts',(-96.9150832119789,4.82523381660316,129.842531721617));
#97856=CARTESIAN_POINT('Ctrl Pts',(-96.9228344032191,4.79468109664022,129.708816805562));
#97857=CARTESIAN_POINT('Ctrl Pts',(-96.9305822999961,4.76414136239833,129.575158721913));
#97858=CARTESIAN_POINT('Ctrl Pts',(-96.9383301967732,4.72799275368204,129.442709483349));
#97859=CARTESIAN_POINT('Ctrl Pts',(-96.9460780935503,4.68635823552932,129.311970068552));
#97860=CARTESIAN_POINT('Ctrl Pts',(-96.9538243696344,4.64473242642025,129.181258001622));
#97861=CARTESIAN_POINT('Ctrl Pts',(-96.9615706457184,4.59762310894182,129.052255419351));
#97862=CARTESIAN_POINT('Ctrl Pts',(-96.9693169218025,4.54520325474541,128.92544858249));
#97863=CARTESIAN_POINT('Ctrl Pts',(-96.9770632550679,4.49278301359748,128.798640809571));
#97864=CARTESIAN_POINT('Ctrl Pts',(-96.9848095883333,4.43505230686832,128.674029175715));
#97865=CARTESIAN_POINT('Ctrl Pts',(-96.9925559215987,4.37223228236641,128.552080010818));
#97866=CARTESIAN_POINT('Ctrl Pts',(-97.0003039896016,4.30939818975567,128.430103536251));
#97867=CARTESIAN_POINT('Ctrl Pts',(-97.0080520576045,4.24147269047217,128.310791064589));
#97868=CARTESIAN_POINT('Ctrl Pts',(-97.0158001256075,4.16872272174816,128.194584011862));
#97869=CARTESIAN_POINT('Ctrl Pts',(-97.0235564283493,4.09589543349176,128.078253452896));
#97870=CARTESIAN_POINT('Ctrl Pts',(-97.0313127310912,4.01823364084334,127.965035237833));
#97871=CARTESIAN_POINT('Ctrl Pts',(-97.039069033833,3.93604774731314,127.855341934449));
#97872=CARTESIAN_POINT('Ctrl Pts',(-97.0468294763472,3.85381798869699,127.745590084447));
#97873=CARTESIAN_POINT('Ctrl Pts',(-97.0545899188613,3.76705956500141,127.63936719753));
#97874=CARTESIAN_POINT('Ctrl Pts',(-97.0623503613754,3.67612231227041,127.537051662519));
#97875=CARTESIAN_POINT('Ctrl Pts',(-97.0701232616408,3.5850390789883,127.434571881529));
#97876=CARTESIAN_POINT('Ctrl Pts',(-97.0778961619063,3.48976388338215,127.336012268014));
#97877=CARTESIAN_POINT('Ctrl Pts',(-97.0856690621717,3.39068309648188,127.241713960692));
#97878=CARTESIAN_POINT('Ctrl Pts',(-97.0931593979342,3.29520414574868,127.150843634359));
#97879=CARTESIAN_POINT('Ctrl Pts',(-97.1006497336967,3.19619171719632,127.063930377892));
#97880=CARTESIAN_POINT('Ctrl Pts',(-97.1081400694592,3.09401806417718,126.981242089316));
#97881=CARTESIAN_POINT('Ctrl Pts',(-97.1159144035785,2.98797046605325,126.89541864915));
#97882=CARTESIAN_POINT('Ctrl Pts',(-97.1236887376978,2.87818126883451,126.813875017716));
#97883=CARTESIAN_POINT('Ctrl Pts',(-97.131463071817,2.76503088378618,126.736955145498));
#97884=CARTESIAN_POINT('Ctrl Pts',(-97.1392278247643,2.65201994647519,126.660130070148));
#97885=CARTESIAN_POINT('Ctrl Pts',(-97.1469925777114,2.53565638362885,126.587917633646));
#97886=CARTESIAN_POINT('Ctrl Pts',(-97.1547573306587,2.41635428279995,126.520622175213));
#97887=CARTESIAN_POINT('Ctrl Pts',(-97.1625143715438,2.29717067449977,126.453393555578));
#97888=CARTESIAN_POINT('Ctrl Pts',(-97.170271412429,2.17505467468009,126.391072386244));
#97889=CARTESIAN_POINT('Ctrl Pts',(-97.1780284533142,2.0504497133336,126.333920031271));
#97890=CARTESIAN_POINT('Ctrl Pts',(-97.1857796445544,1.92593871755757,126.276810775334));
#97891=CARTESIAN_POINT('Ctrl Pts',(-97.1935308357946,1.79894285013012,126.224862737674));
#97892=CARTESIAN_POINT('Ctrl Pts',(-97.2012820270349,1.66993021281508,126.178291427981));
#97893=CARTESIAN_POINT('Ctrl Pts',(-97.2090299238122,1.54097240931225,126.131739912337));
#97894=CARTESIAN_POINT('Ctrl Pts',(-97.2167778205895,1.40999990775853,126.090560711937));
#97895=CARTESIAN_POINT('Ctrl Pts',(-97.2245257173667,1.27750066131269,126.054921164026));
#97896=CARTESIAN_POINT('Ctrl Pts',(-97.232271993451,1.14502913085285,126.019289071139));
#97897=CARTESIAN_POINT('Ctrl Pts',(-97.2400182695353,1.01103186803643,125.98919442736));
#97898=CARTESIAN_POINT('Ctrl Pts',(-97.2477645456196,0.87601147320753,125.964754542552));
#97899=CARTESIAN_POINT('Ctrl Pts',(-97.2555108788851,0.740990081688564,
125.940314477335));
#97900=CARTESIAN_POINT('Ctrl Pts',(-97.2632572121506,0.604945927800174,
125.92152932402));
#97901=CARTESIAN_POINT('Ctrl Pts',(-97.2710035454161,0.468390883882421,
125.90846508739));
#97902=CARTESIAN_POINT('Ctrl Pts',(-97.2787516134193,0.331805259409576,
125.895397925116));
#97903=CARTESIAN_POINT('Ctrl Pts',(-97.2864996814225,0.194708906357857,
125.888054266113));
#97904=CARTESIAN_POINT('Ctrl Pts',(-97.2942477494257,0.0576174866290085,
125.886448124675));
#97905=CARTESIAN_POINT('Ctrl Pts',(-97.3020040521677,-0.0796196354923194,
125.884840276211));
#97906=CARTESIAN_POINT('Ctrl Pts',(-97.3097603549097,-0.216851422255191,
125.888982131115));
#97907=CARTESIAN_POINT('Ctrl Pts',(-97.3175166576517,-0.353562988024938,
125.898835541083));
#97908=CARTESIAN_POINT('Ctrl Pts',(-97.3252771001661,-0.490347520873641,
125.908694210114));
#97909=CARTESIAN_POINT('Ctrl Pts',(-97.3330375426805,-0.626610891227336,
125.924270464082));
#97910=CARTESIAN_POINT('Ctrl Pts',(-97.3407979851948,-0.76184565492745,
125.945474504415));
#97911=CARTESIAN_POINT('Ctrl Pts',(-97.3485708854604,-0.897297509475828,
125.966712583357));
#97912=CARTESIAN_POINT('Ctrl Pts',(-97.356343785726,-1.03171707413186,125.993596425201));
#97913=CARTESIAN_POINT('Ctrl Pts',(-97.3641166859917,-1.1646084962526,126.025985358866));
#97914=CARTESIAN_POINT('Ctrl Pts',(-97.3716070217516,-1.29266898040746,
126.0571968732));
#97915=CARTESIAN_POINT('Ctrl Pts',(-97.3790973575117,-1.41931020068542,
126.093520095413));
#97916=CARTESIAN_POINT('Ctrl Pts',(-97.3865876932717,-1.54410555486253,
126.134786643643));
#97917=CARTESIAN_POINT('Ctrl Pts',(-97.3943620273906,-1.67363256285817,
126.177617825602));
#97918=CARTESIAN_POINT('Ctrl Pts',(-97.4021363615096,-1.80158127226142,
126.225910262007));
#97919=CARTESIAN_POINT('Ctrl Pts',(-97.4099106956286,-1.9274566862086,126.279529815725));
#97920=CARTESIAN_POINT('Ctrl Pts',(-97.4176754485756,-2.05317696995756,
126.333083288134));
#97921=CARTESIAN_POINT('Ctrl Pts',(-97.4254402015226,-2.17682868600184,
126.391950663325));
#97922=CARTESIAN_POINT('Ctrl Pts',(-97.4332049544696,-2.29793196069802,
126.455948060494));
#97923=CARTESIAN_POINT('Ctrl Pts',(-97.4409619953545,-2.41891495391452,
126.519881894546));
#97924=CARTESIAN_POINT('Ctrl Pts',(-97.4487190362394,-2.53735419945096,
126.588935429391));
#97925=CARTESIAN_POINT('Ctrl Pts',(-97.4564760771243,-2.65279011957886,
126.662876868477));
#97926=CARTESIAN_POINT('Ctrl Pts',(-97.4642272683644,-2.76813898858159,
126.736762547749));
#97927=CARTESIAN_POINT('Ctrl Pts',(-97.4719784596044,-2.8804887122988,126.815528584465));
#97928=CARTESIAN_POINT('Ctrl Pts',(-97.4797296508445,-2.98940495588678,
126.898897639606));
#97929=CARTESIAN_POINT('Ctrl Pts',(-97.4874775476214,-3.09827490716565,
126.982231260674));
#97930=CARTESIAN_POINT('Ctrl Pts',(-97.4952254443983,-3.20371397098678,
127.070163771886));
#97931=CARTESIAN_POINT('Ctrl Pts',(-97.5029733411752,-3.30531761118572,
127.162375094299));
#97932=CARTESIAN_POINT('Ctrl Pts',(-97.5107196172593,-3.40689999809344,
127.254567128092));
#97933=CARTESIAN_POINT('Ctrl Pts',(-97.5184658933432,-3.50464826784564,
127.351035930229));
#97934=CARTESIAN_POINT('Ctrl Pts',(-97.5262121694272,-3.59819205656837,
127.451422057653));
#97935=CARTESIAN_POINT('Ctrl Pts',(-97.5339585026925,-3.69173653580997,
127.551808926106));
#97936=CARTESIAN_POINT('Ctrl Pts',(-97.5417048359577,-3.78107620555669,
127.656112891517));
#97937=CARTESIAN_POINT('Ctrl Pts',(-97.549451169223,-3.86587885461105,127.76393897839));
#97938=CARTESIAN_POINT('Ctrl Pts',(-97.5571992372258,-3.95070049463058,
127.871789212166));
#97939=CARTESIAN_POINT('Ctrl Pts',(-97.5649473052287,-4.03098285052187,
127.983162829684));
#97940=CARTESIAN_POINT('Ctrl Pts',(-97.5726953732315,-4.10643540380995,
128.097633565047));
#97941=CARTESIAN_POINT('Ctrl Pts',(-97.5804516759733,-4.18196814896966,
128.212225961271));
#97942=CARTESIAN_POINT('Ctrl Pts',(-97.588207978715,-4.25266062195452,128.329921723821));
#97943=CARTESIAN_POINT('Ctrl Pts',(-97.5959642814567,-4.31826660975013,
128.450267044741));
#97944=CARTESIAN_POINT('Ctrl Pts',(-97.6037247239708,-4.38390761343679,
128.570676597582));
#97945=CARTESIAN_POINT('Ctrl Pts',(-97.611485166485,-4.44445654992704,128.693738175975));
#97946=CARTESIAN_POINT('Ctrl Pts',(-97.619245608999,-4.49971468333945,128.818976314455));
#97947=CARTESIAN_POINT('Ctrl Pts',(-97.6270185092643,-4.5550615220132,128.944415496313));
#97948=CARTESIAN_POINT('Ctrl Pts',(-97.6347914095296,-4.60510044255946,
129.072037856203));
#97949=CARTESIAN_POINT('Ctrl Pts',(-97.6425643097949,-4.6496817750774,129.201350183098));
#97950=CARTESIAN_POINT('Ctrl Pts',(-97.6500546455582,-4.69264246387257,
129.325961681215));
#97951=CARTESIAN_POINT('Ctrl Pts',(-97.6575449813215,-4.73053538126077,
129.452142115407));
#97952=CARTESIAN_POINT('Ctrl Pts',(-97.6650353170848,-4.7632716027491,129.57944155863));
#97953=CARTESIAN_POINT('Ctrl Pts',(-97.6650951047238,-4.76353290230253,
129.580457659028));
#97954=CARTESIAN_POINT('Ctrl Pts',(-97.6651548923626,-4.76379387748142,
129.58147384598));
#97955=CARTESIAN_POINT('Ctrl Pts',(-97.6652146800015,-4.76405452823416,
129.582490119309));
#97956=CARTESIAN_POINT('Ctrl Pts',(-95.9150180446607,-4.76405452823415,
129.582490119309));
#97957=CARTESIAN_POINT('Ctrl Pts',(-95.9227359398604,-4.79795511176593,
129.714667979986));
#97958=CARTESIAN_POINT('Ctrl Pts',(-95.9304538350601,-4.82632412144731,
129.84815437457));
#97959=CARTESIAN_POINT('Ctrl Pts',(-95.9381717302599,-4.84908613199551,
129.982444109039));
#97960=CARTESIAN_POINT('Ctrl Pts',(-95.9459998692114,-4.87217327904473,
130.118652061334));
#97961=CARTESIAN_POINT('Ctrl Pts',(-95.9538280081629,-4.88949196545971,
130.255686058514));
#97962=CARTESIAN_POINT('Ctrl Pts',(-95.9616561471144,-4.90101813305355,
130.393016088029));
#97963=CARTESIAN_POINT('Ctrl Pts',(-95.9694842860659,-4.9125443006474,130.530346117543));
#97964=CARTESIAN_POINT('Ctrl Pts',(-95.9773124250174,-4.9182779953861,130.667971759409));
#97965=CARTESIAN_POINT('Ctrl Pts',(-95.9851405639689,-4.91824989715129,
130.805366436304));
#97966=CARTESIAN_POINT('',(-95.6398613041516,-4.91378236373845,130.808074515593));
#97967=CARTESIAN_POINT('Ctrl Pts',(-95.5699831042333,-4.76405452823397,
129.582490119308));
#97968=CARTESIAN_POINT('Ctrl Pts',(-95.5777374979323,-4.79818715094222,
129.715572697213));
#97969=CARTESIAN_POINT('Ctrl Pts',(-95.5854918916312,-4.82675179822305,
129.850135990574));
#97970=CARTESIAN_POINT('Ctrl Pts',(-95.5932462853303,-4.84963274388358,
129.985675505968));
#97971=CARTESIAN_POINT('Ctrl Pts',(-95.6010151437738,-4.87255637077067,
130.121467851505));
#97972=CARTESIAN_POINT('Ctrl Pts',(-95.6087840022174,-4.88977498398199,
130.258239682372));
#97973=CARTESIAN_POINT('Ctrl Pts',(-95.616552860661,-4.90122382829593,130.395474267287));
#97974=CARTESIAN_POINT('Ctrl Pts',(-95.6243217191045,-4.91267267260987,
130.532708852202));
#97975=CARTESIAN_POINT('Ctrl Pts',(-95.6320905775481,-4.91835172324539,
130.67040579917));
#97976=CARTESIAN_POINT('Ctrl Pts',(-95.6398594359917,-4.91824862012079,
130.808044797249));
#97977=CARTESIAN_POINT('Ctrl Pts',(-95.639861537601,-4.91322425034186,130.808078229263));
#97978=CARTESIAN_POINT('Ctrl Pts',(-95.671738007252,-4.91712121886186,131.372252204815));
#97979=CARTESIAN_POINT('Ctrl Pts',(-95.7964303515077,-4.56637019745189,
133.574446779133));
#97980=CARTESIAN_POINT('Ctrl Pts',(-96.0139385703665,-1.31322884073256,
136.471556559328));
#97981=CARTESIAN_POINT('Ctrl Pts',(-96.29238619418,4.05814018332094,134.972475069326));
#97982=CARTESIAN_POINT('Ctrl Pts',(-96.5708338179925,5.70027663007168,129.643100021867));
#97983=CARTESIAN_POINT('Ctrl Pts',(-96.8492814418056,2.10413732778126,125.380866731122));
#97984=CARTESIAN_POINT('Ctrl Pts',(-97.0989034226261,-2.85314803968669,
126.027847816815));
#97985=CARTESIAN_POINT('Ctrl Pts',(-97.2557095288423,-4.46971273000384,
128.48961976286));
#97986=CARTESIAN_POINT('Ctrl Pts',(-97.3196997604543,-4.76048812747127,
129.583439530431));
#97987=CARTESIAN_POINT('Origin',(213.235140564004,0.,130.804360617566));
#97988=CARTESIAN_POINT('',(-99.4153986790351,-4.76405452823397,129.582490119308));
#97989=CARTESIAN_POINT('',(-99.0698920977623,-4.76405452823408,129.582490119308));
#97990=CARTESIAN_POINT('',(213.235140564004,-4.76405452823405,129.582490119308));
#97991=CARTESIAN_POINT('',(-97.7351405639562,-4.91824790420648,130.799820213553));
#97992=CARTESIAN_POINT('Ctrl Pts',(-97.7351405640093,-4.91824790420734,
130.799820214491));
#97993=CARTESIAN_POINT('Ctrl Pts',(-97.7428066318137,-4.91837292102423,
130.935240723974));
#97994=CARTESIAN_POINT('Ctrl Pts',(-97.750472699618,-4.91290066797459,131.070804378959));
#97995=CARTESIAN_POINT('Ctrl Pts',(-97.7581387674224,-4.9018225276731,131.206005945805));
#97996=CARTESIAN_POINT('Ctrl Pts',(-97.7658614413172,-4.89066258660654,
131.342205838301));
#97997=CARTESIAN_POINT('Ctrl Pts',(-97.773584115212,-4.87381359281784,131.478037863531));
#97998=CARTESIAN_POINT('Ctrl Pts',(-97.7813067891068,-4.85132026448249,
131.612985842204));
#97999=CARTESIAN_POINT('Ctrl Pts',(-97.7889660047495,-4.8290117668574,131.74682493515));
#98000=CARTESIAN_POINT('Ctrl Pts',(-97.7966252203921,-4.80115142974561,
131.879794056288));
#98001=CARTESIAN_POINT('Ctrl Pts',(-97.8042844360347,-4.76783479633275,
132.011396001214));
#98002=CARTESIAN_POINT('Ctrl Pts',(-97.8119430718726,-4.7345206849984,132.142987983836));
#98003=CARTESIAN_POINT('Ctrl Pts',(-97.8196017077106,-4.69575119701223,
132.273212607617));
#98004=CARTESIAN_POINT('Ctrl Pts',(-97.8272603435484,-4.6516725183478,132.401585036534));
#98005=CARTESIAN_POINT('Ctrl Pts',(-97.8349201488105,-4.6075871091537,132.529977067092));
#98006=CARTESIAN_POINT('Ctrl Pts',(-97.8425799540726,-4.55819102745045,
132.656515961451));
#98007=CARTESIAN_POINT('Ctrl Pts',(-97.8502397593348,-4.50367945960312,
132.780734668106));
#98008=CARTESIAN_POINT('Ctrl Pts',(-97.858010024465,-4.44838179597548,132.906744697319));
#98009=CARTESIAN_POINT('Ctrl Pts',(-97.8657802895951,-4.3878201249069,133.030366707881));
#98010=CARTESIAN_POINT('Ctrl Pts',(-97.8735505547254,-4.32224705533296,
133.151137866298));
#98011=CARTESIAN_POINT('Ctrl Pts',(-97.8812219175975,-4.25750861939675,
133.270371813296));
#98012=CARTESIAN_POINT('Ctrl Pts',(-97.8888932804697,-4.18788587560084,
133.38682674569));
#98013=CARTESIAN_POINT('Ctrl Pts',(-97.8965646433418,-4.11366578001135,
133.500086292197));
#98014=CARTESIAN_POINT('Ctrl Pts',(-97.9043843596011,-4.03801037197998,
133.615536119314));
#98015=CARTESIAN_POINT('Ctrl Pts',(-97.9122040758604,-3.95757823358253,
133.727665346258));
#98016=CARTESIAN_POINT('Ctrl Pts',(-97.9200237921197,-3.87271585389831,
133.836068878178));
#98017=CARTESIAN_POINT('Ctrl Pts',(-97.927843508379,-3.78785347421433,133.944472410098));
#98018=CARTESIAN_POINT('Ctrl Pts',(-97.9356632246383,-3.69856118665766,
134.049149962176));
#98019=CARTESIAN_POINT('Ctrl Pts',(-97.9434829408976,-3.60522374645677,
134.149737248154));
#98020=CARTESIAN_POINT('Ctrl Pts',(-97.9512572750166,-3.51242799506625,
134.249740770455));
#98021=CARTESIAN_POINT('Ctrl Pts',(-97.9590316091357,-3.41532118597507,
134.346038741776));
#98022=CARTESIAN_POINT('Ctrl Pts',(-97.9668059432548,-3.31423107289613,
134.438236710383));
#98023=CARTESIAN_POINT('Ctrl Pts',(-97.9745706962019,-3.2132655443466,134.530321053235));
#98024=CARTESIAN_POINT('Ctrl Pts',(-97.9823354491489,-3.10832676548148,
134.618315186184));
#98025=CARTESIAN_POINT('Ctrl Pts',(-97.990100202096,-2.99978144650823,134.70185908911));
#98026=CARTESIAN_POINT('Ctrl Pts',(-97.997857242981,-2.89134393627599,134.785320015054));
#98027=CARTESIAN_POINT('Ctrl Pts',(-98.005614283866,-2.77930732222756,134.864339270119));
#98028=CARTESIAN_POINT('Ctrl Pts',(-98.013371324751,-2.66407345842478,134.938595210646));
#98029=CARTESIAN_POINT('Ctrl Pts',(-98.0211225159912,-2.54892649337556,
135.01279515419));
#98030=CARTESIAN_POINT('Ctrl Pts',(-98.0288737072314,-2.43058740497435,
135.082238722042));
#98031=CARTESIAN_POINT('Ctrl Pts',(-98.0366248984715,-2.30948897630498,
135.146646159861));
#98032=CARTESIAN_POINT('Ctrl Pts',(-98.0443727952486,-2.18844201769804,
135.211026222802));
#98033=CARTESIAN_POINT('Ctrl Pts',(-98.0521206920256,-2.06463839587678,
135.270374229777));
#98034=CARTESIAN_POINT('Ctrl Pts',(-98.0598685888026,-1.9385373802953,135.324455294417));
#98035=CARTESIAN_POINT('Ctrl Pts',(-98.0676148648867,-1.81246274232786,
135.378525046464));
#98036=CARTESIAN_POINT('Ctrl Pts',(-98.0753611409709,-1.68409202555793,
135.427329893577));
#98037=CARTESIAN_POINT('Ctrl Pts',(-98.0831074170549,-1.55390609748732,
135.470682392014));
#98038=CARTESIAN_POINT('Ctrl Pts',(-98.0908537503203,-1.42371920841394,
135.51403521047));
#98039=CARTESIAN_POINT('Ctrl Pts',(-98.0986000835856,-1.29171745224094,
135.551935476415));
#98040=CARTESIAN_POINT('Ctrl Pts',(-98.1063464168509,-1.15839815503381,
135.584245216269));
#98041=CARTESIAN_POINT('Ctrl Pts',(-98.1140944848539,-1.02504900189462,
135.616562191665));
#98042=CARTESIAN_POINT('Ctrl Pts',(-98.1218425528568,-0.890382100491075,
135.643286057649));
#98043=CARTESIAN_POINT('Ctrl Pts',(-98.1295906208598,-0.754905905760631,
135.664329767257));
#98044=CARTESIAN_POINT('Ctrl Pts',(-98.1373469236016,-0.619285725317686,
135.68539584237));
#98045=CARTESIAN_POINT('Ctrl Pts',(-98.1451032263436,-0.482854920300665,
135.70076964157));
#98046=CARTESIAN_POINT('Ctrl Pts',(-98.1528595290854,-0.346128579316764,
135.710415862779));
#98047=CARTESIAN_POINT('Ctrl Pts',(-98.1606199715996,-0.209329263367929,
135.720067232467));
#98048=CARTESIAN_POINT('Ctrl Pts',(-98.1683804141137,-0.0722344877634435,
135.723984921709));
#98049=CARTESIAN_POINT('Ctrl Pts',(-98.1761408566278,0.0646406956810316,
135.722185811995));
#98050=CARTESIAN_POINT('Ctrl Pts',(-98.1839137568933,0.20173560332118,135.72038381419));
#98051=CARTESIAN_POINT('Ctrl Pts',(-98.1916866571587,0.338609823777876,
135.712846700142));
#98052=CARTESIAN_POINT('Ctrl Pts',(-98.1994595574241,0.474752560436986,
135.699643353921));
#98053=CARTESIAN_POINT('Ctrl Pts',(-98.2069498931862,0.605946165696418,
135.686919982593));
#98054=CARTESIAN_POINT('Ctrl Pts',(-98.2144402289483,0.736460241253026,
135.668935232472));
#98055=CARTESIAN_POINT('Ctrl Pts',(-98.2219305647104,0.865848607855436,
135.645795244903));
#98056=CARTESIAN_POINT('Ctrl Pts',(-98.2297048988295,1.00014277370338,135.621777897671));
#98057=CARTESIAN_POINT('Ctrl Pts',(-98.2374792329486,1.13364958655527,135.592130594683));
#98058=CARTESIAN_POINT('Ctrl Pts',(-98.2452535670676,1.2658600241094,135.556915873622));
#98059=CARTESIAN_POINT('Ctrl Pts',(-98.2530183200147,1.39790752411522,135.521744551557));
#98060=CARTESIAN_POINT('Ctrl Pts',(-98.2607830729618,1.52866145353691,135.481019563112));
#98061=CARTESIAN_POINT('Ctrl Pts',(-98.2685478259089,1.65762070142654,135.434854832302));
#98062=CARTESIAN_POINT('Ctrl Pts',(-98.2763048667939,1.78645186517316,135.388735952953));
#98063=CARTESIAN_POINT('Ctrl Pts',(-98.2840619076788,1.91349152894031,135.337188214028));
#98064=CARTESIAN_POINT('Ctrl Pts',(-98.2918189485638,2.03825187287204,135.280375850475));
#98065=CARTESIAN_POINT('Ctrl Pts',(-98.2995701398039,2.16291813405775,135.223606329568));
#98066=CARTESIAN_POINT('Ctrl Pts',(-98.3073213310441,2.2853081423093,135.161580247636));
#98067=CARTESIAN_POINT('Ctrl Pts',(-98.3150725222842,2.40495260254972,135.094510503291));
#98068=CARTESIAN_POINT('Ctrl Pts',(-98.3228204190612,2.52454621070309,135.027469265377));
#98069=CARTESIAN_POINT('Ctrl Pts',(-98.3305683158383,2.6413962514606,134.955388819464));
#98070=CARTESIAN_POINT('Ctrl Pts',(-98.3383162126154,2.75505686190805,134.87852860013));
#98071=CARTESIAN_POINT('Ctrl Pts',(-98.3460624886995,2.86869369700605,134.801684458298));
#98072=CARTESIAN_POINT('Ctrl Pts',(-98.3538087647836,2.9791421051503,134.720062750621));
#98073=CARTESIAN_POINT('Ctrl Pts',(-98.3615550408677,3.08598446398274,134.633966726627));
#98074=CARTESIAN_POINT('Ctrl Pts',(-98.369301374133,3.19282761150135,134.547870067092));
#98075=CARTESIAN_POINT('Ctrl Pts',(-98.3770477073983,3.29606435216587,134.457299270648));
#98076=CARTESIAN_POINT('Ctrl Pts',(-98.3847940406637,3.39530978800992,134.362598173709));
#98077=CARTESIAN_POINT('Ctrl Pts',(-98.3925421086667,3.49457744918081,134.267875869116));
#98078=CARTESIAN_POINT('Ctrl Pts',(-98.4002901766696,3.58985174412298,134.169021693331));
#98079=CARTESIAN_POINT('Ctrl Pts',(-98.4080382446726,3.68078460544728,134.066416372884));
#98080=CARTESIAN_POINT('Ctrl Pts',(-98.4157945474144,3.77181411129909,133.96370200228));
#98081=CARTESIAN_POINT('Ctrl Pts',(-98.4235508501563,3.85849270659342,133.857228816091));
#98082=CARTESIAN_POINT('Ctrl Pts',(-98.4313071528981,3.94051227272033,133.747411091316));
#98083=CARTESIAN_POINT('Ctrl Pts',(-98.4390675954123,4.02257561515924,133.637534753514));
#98084=CARTESIAN_POINT('Ctrl Pts',(-98.4468280379265,4.09997475301399,133.524310642803));
#98085=CARTESIAN_POINT('Ctrl Pts',(-98.4545884804407,4.17244549107215,133.408181211718));
#98086=CARTESIAN_POINT('Ctrl Pts',(-98.4623613807061,4.24503256559269,133.291865359361));
#98087=CARTESIAN_POINT('Ctrl Pts',(-98.4701342809715,4.31267523757678,133.172635206964));
#98088=CARTESIAN_POINT('Ctrl Pts',(-98.4779071812369,4.37515536309906,133.050957735708));
#98089=CARTESIAN_POINT('Ctrl Pts',(-98.485397516999,4.43536417868101,132.933703547019));
#98090=CARTESIAN_POINT('Ctrl Pts',(-98.4928878527611,4.49077914487141,132.81417716216));
#98091=CARTESIAN_POINT('Ctrl Pts',(-98.5003781885232,4.54124839060584,132.692811336362));
#98092=CARTESIAN_POINT('Ctrl Pts',(-98.5081525226422,4.59363119313158,132.566843888391));
#98093=CARTESIAN_POINT('Ctrl Pts',(-98.5159268567614,4.6408517709036,132.438495734188));
#98094=CARTESIAN_POINT('Ctrl Pts',(-98.5237011908804,4.68268759965953,132.308228931779));
#98095=CARTESIAN_POINT('Ctrl Pts',(-98.5314659438275,4.72447186949562,132.178122671562));
#98096=CARTESIAN_POINT('Ctrl Pts',(-98.5392306967745,4.76088447602025,132.046102836578));
#98097=CARTESIAN_POINT('Ctrl Pts',(-98.5469954497215,4.79175040402551,131.912652604373));
#98098=CARTESIAN_POINT('Ctrl Pts',(-98.5547524906065,4.82258567555586,131.779334916821));
#98099=CARTESIAN_POINT('Ctrl Pts',(-98.5625095314916,4.84788514427261,131.644590037731));
#98100=CARTESIAN_POINT('Ctrl Pts',(-98.5702665723765,4.86752330714199,131.508917156766));
#98101=CARTESIAN_POINT('Ctrl Pts',(-98.5780177636167,4.88714666072008,131.373346587775));
#98102=CARTESIAN_POINT('Ctrl Pts',(-98.5857689548568,4.90111715032316,131.236849795212));
#98103=CARTESIAN_POINT('Ctrl Pts',(-98.5935201460969,4.90936022813055,131.099936687216));
#98104=CARTESIAN_POINT('Ctrl Pts',(-98.601268042874,4.91759980240997,130.963081770944));
#98105=CARTESIAN_POINT('Ctrl Pts',(-98.6090159396511,4.92011678308943,130.825811280611));
#98106=CARTESIAN_POINT('Ctrl Pts',(-98.6167638364282,4.91688844003116,130.68864056404));
#98107=CARTESIAN_POINT('Ctrl Pts',(-98.6245101125123,4.91366077227266,130.551498540627));
#98108=CARTESIAN_POINT('Ctrl Pts',(-98.6322563885964,4.90469018041137,130.414456640073));
#98109=CARTESIAN_POINT('Ctrl Pts',(-98.6400026646805,4.89000606177802,130.278030133674));
#98110=CARTESIAN_POINT('Ctrl Pts',(-98.6477489979459,4.87532183474981,130.141602620205));
#98111=CARTESIAN_POINT('Ctrl Pts',(-98.6554953312112,4.85492403862992,130.005790898674));
#98112=CARTESIAN_POINT('Ctrl Pts',(-98.6632416644765,4.82889390597889,129.871104646623));
#98113=CARTESIAN_POINT('Ctrl Pts',(-98.6709897324795,4.8028579440601,129.73638823252));
#98114=CARTESIAN_POINT('Ctrl Pts',(-98.6787378004826,4.77118720989687,129.602798173217));
#98115=CARTESIAN_POINT('Ctrl Pts',(-98.6864858684856,4.73401388057493,129.470833099656));
#98116=CARTESIAN_POINT('Ctrl Pts',(-98.6942421712274,4.69680104299638,129.338727772044));
#98117=CARTESIAN_POINT('Ctrl Pts',(-98.7019984739692,4.65407403397733,129.208251257071));
#98118=CARTESIAN_POINT('Ctrl Pts',(-98.709754776711,4.60601485085524,129.079886710486));
#98119=CARTESIAN_POINT('Ctrl Pts',(-98.7175152192252,4.55793001709981,128.951453651876));
#98120=CARTESIAN_POINT('Ctrl Pts',(-98.7252756617395,4.50450749067418,128.825135167649));
#98121=CARTESIAN_POINT('Ctrl Pts',(-98.7330361042537,4.44597671546269,128.701392689122));
#98122=CARTESIAN_POINT('Ctrl Pts',(-98.7408090045191,4.38735198145487,128.577451568184));
#98123=CARTESIAN_POINT('Ctrl Pts',(-98.7485819047844,4.3236027939411,128.456095062774));
#98124=CARTESIAN_POINT('Ctrl Pts',(-98.7563548050498,4.2550041252953,128.337759118292));
#98125=CARTESIAN_POINT('Ctrl Pts',(-98.7638451408119,4.1888991910442,128.223724983462));
#98126=CARTESIAN_POINT('Ctrl Pts',(-98.771335476574,4.11829140111115,128.112495872362));
#98127=CARTESIAN_POINT('Ctrl Pts',(-98.7788258123361,4.04346275470753,128.004433473194));
#98128=CARTESIAN_POINT('Ctrl Pts',(-98.7866001464551,3.96579695743217,127.892273855316));
#98129=CARTESIAN_POINT('Ctrl Pts',(-98.7943744805743,3.88333789600536,127.783170533456));
#98130=CARTESIAN_POINT('Ctrl Pts',(-98.8021488146934,3.7963540331303,127.677560477225));
#98131=CARTESIAN_POINT('Ctrl Pts',(-98.8099135676405,3.70947737009226,127.57208057595));
#98132=CARTESIAN_POINT('Ctrl Pts',(-98.8176783205875,3.61808724717833,127.47008567325));
#98133=CARTESIAN_POINT('Ctrl Pts',(-98.8254430735346,3.52249557534673,127.371984183641));
#98134=CARTESIAN_POINT('Ctrl Pts',(-98.8332001144196,3.42699884651094,127.273980129814));
#98135=CARTESIAN_POINT('Ctrl Pts',(-98.8409571553047,3.32730914437406,127.17986207179));
#98136=CARTESIAN_POINT('Ctrl Pts',(-98.8487141961897,3.22377861388139,127.090005423029));
#98137=CARTESIAN_POINT('Ctrl Pts',(-98.8564653874299,3.12032615656697,127.000216535867));
#98138=CARTESIAN_POINT('Ctrl Pts',(-98.8642165786699,3.013038930072,126.914682916799));
#98139=CARTESIAN_POINT('Ctrl Pts',(-98.8719677699101,2.90230563963737,126.833742902823));
#98140=CARTESIAN_POINT('Ctrl Pts',(-98.8797156666871,2.79161941380553,126.752837290513));
#98141=CARTESIAN_POINT('Ctrl Pts',(-98.8874635634643,2.67749035212375,126.676521630339));
#98142=CARTESIAN_POINT('Ctrl Pts',(-98.8952114602414,2.56033974511689,126.605093603899));
#98143=CARTESIAN_POINT('Ctrl Pts',(-98.9029577363255,2.44321364349122,126.533680518661));
#98144=CARTESIAN_POINT('Ctrl Pts',(-98.9107040124095,2.32306758730672,126.46715323697));
#98145=CARTESIAN_POINT('Ctrl Pts',(-98.9184502884936,2.20035097887212,126.405765542741));
#98146=CARTESIAN_POINT('Ctrl Pts',(-98.926196621759,2.0776334645719,126.344377395362));
#98147=CARTESIAN_POINT('Ctrl Pts',(-98.9339429550244,1.95234570981431,126.28812908606));
#98148=CARTESIAN_POINT('Ctrl Pts',(-98.9416892882897,1.8249604289321,126.237227764743));
#98149=CARTESIAN_POINT('Ctrl Pts',(-98.9494373562927,1.6975466209993,126.186315044428));
#98150=CARTESIAN_POINT('Ctrl Pts',(-98.9571854242956,1.5680347152251,126.14075183987));
#98151=CARTESIAN_POINT('Ctrl Pts',(-98.9649334922986,1.43691566888555,126.100696468946));
#98152=CARTESIAN_POINT('Ctrl Pts',(-98.9726897950404,1.30565726766303,126.060598526697));
#98153=CARTESIAN_POINT('Ctrl Pts',(-98.9804460977824,1.17278868828855,126.026020226068));
#98154=CARTESIAN_POINT('Ctrl Pts',(-98.9882024005242,1.03881479738488,125.997069605027));
#98155=CARTESIAN_POINT('Ctrl Pts',(-98.9959628430384,0.904769400581384,
125.968103532169));
#98156=CARTESIAN_POINT('Ctrl Pts',(-99.0037232855526,0.769617901824807,
125.94477119043));
#98157=CARTESIAN_POINT('Ctrl Pts',(-99.0114837280667,0.63387253637551,125.927128957072));
#98158=CARTESIAN_POINT('Ctrl Pts',(-99.0192566283322,0.497909260415057,
125.909458402834));
#98159=CARTESIAN_POINT('Ctrl Pts',(-99.0270295285976,0.361350602407642,
125.897496244289));
#98160=CARTESIAN_POINT('Ctrl Pts',(-99.0348024288631,0.224711964847995,
125.891246778527));
#98161=CARTESIAN_POINT('Ctrl Pts',(-99.042292764625,0.093040485936713,125.885224496588));
#98162=CARTESIAN_POINT('Ctrl Pts',(-99.049783100387,-0.0387049505519755,
125.884506778503));
#98163=CARTESIAN_POINT('Ctrl Pts',(-99.057273436149,-0.170067618629719,
125.889051871659));
#98164=CARTESIAN_POINT('Ctrl Pts',(-99.065047770268,-0.306410942195046,
125.893769293402));
#98165=CARTESIAN_POINT('Ctrl Pts',(-99.0728221043871,-0.442773793718309,
125.90417142668));
#98166=CARTESIAN_POINT('Ctrl Pts',(-99.0805964385061,-0.578643427639874,
125.920268598966));
#98167=CARTESIAN_POINT('Ctrl Pts',(-99.0883611914533,-0.714345614381386,
125.936345932926));
#98168=CARTESIAN_POINT('Ctrl Pts',(-99.0961259444003,-0.84955540843205,
125.958104295363));
#98169=CARTESIAN_POINT('Ctrl Pts',(-99.1038906973475,-0.98376060360043,
125.985502024776));
#98170=CARTESIAN_POINT('Ctrl Pts',(-99.1116477382324,-1.11783250427664,
126.012872542378));
#98171=CARTESIAN_POINT('Ctrl Pts',(-99.1194047791175,-1.25090141111581,
126.045871202821));
#98172=CARTESIAN_POINT('Ctrl Pts',(-99.1271618200025,-1.38246113519507,
126.084404656736));
#98173=CARTESIAN_POINT('Ctrl Pts',(-99.1349130112426,-1.5139216490632,126.122909052273));
#98174=CARTESIAN_POINT('Ctrl Pts',(-99.1426642024828,-1.6438748717794,126.166939824075));
#98175=CARTESIAN_POINT('Ctrl Pts',(-99.1504153937229,-1.77182604616822,
126.216352822823));
#98176=CARTESIAN_POINT('Ctrl Pts',(-99.1581632905,-1.89972283789489,126.265744819729));
#98177=CARTESIAN_POINT('Ctrl Pts',(-99.165911187277,-2.02561890976725,126.320514353188));
#98178=CARTESIAN_POINT('Ctrl Pts',(-99.1736590840542,-2.14903609600899,
126.380467883723));
#98179=CARTESIAN_POINT('Ctrl Pts',(-99.1814053601383,-2.27242746603561,
126.440408873271));
#98180=CARTESIAN_POINT('Ctrl Pts',(-99.1891516362224,-2.3933406303705,126.505531532279));
#98181=CARTESIAN_POINT('Ctrl Pts',(-99.1968979123065,-2.51131916049412,
126.575594942261));
#98182=CARTESIAN_POINT('Ctrl Pts',(-99.2046442455719,-2.62929856150861,
126.645658869436));
#98183=CARTESIAN_POINT('Ctrl Pts',(-99.2123905788372,-2.74434294892905,
126.720663420728));
#98184=CARTESIAN_POINT('Ctrl Pts',(-99.2201369121026,-2.85602252802894,
126.800322857768));
#98185=CARTESIAN_POINT('Ctrl Pts',(-99.2278849801056,-2.96772711699608,
126.880000133986));
#98186=CARTESIAN_POINT('Ctrl Pts',(-99.2356330481085,-3.07606507998314,
126.964334143274));
#98187=CARTESIAN_POINT('Ctrl Pts',(-99.2433811161115,-3.18063784527585,
127.052997404053));
#98188=CARTESIAN_POINT('Ctrl Pts',(-99.2511374188534,-3.28532175174808,
127.1417548972));
#98189=CARTESIAN_POINT('Ctrl Pts',(-99.2588937215952,-3.38623216802364,
127.23485057995));
#98190=CARTESIAN_POINT('Ctrl Pts',(-99.2666500243371,-3.48300530595665,
127.331918090874));
#98191=CARTESIAN_POINT('Ctrl Pts',(-99.2744104668513,-3.57983009462716,
127.429037409652));
#98192=CARTESIAN_POINT('Ctrl Pts',(-99.2821709093654,-3.67251294087485,
127.530132492611));
#98193=CARTESIAN_POINT('Ctrl Pts',(-99.2899313518796,-3.76072953724353,
127.634802855006));
#98194=CARTESIAN_POINT('Ctrl Pts',(-99.2977042521451,-3.84908774672421,
127.739641243559));
#98195=CARTESIAN_POINT('Ctrl Pts',(-99.3054771524106,-3.93296513977772,
127.848066071197));
#98196=CARTESIAN_POINT('Ctrl Pts',(-99.313250052676,-4.01207951350237,127.959646037888));
#98197=CARTESIAN_POINT('Ctrl Pts',(-99.320740388438,-4.08831788046484,128.067169791736));
#98198=CARTESIAN_POINT('Ctrl Pts',(-99.3282307242,-4.1601333434996,128.177623014523));
#98199=CARTESIAN_POINT('Ctrl Pts',(-99.335721059962,-4.22731415871232,128.290598881432));
#98200=CARTESIAN_POINT('Ctrl Pts',(-99.3437732964471,-4.29953466104291,
128.41204983188));
#98201=CARTESIAN_POINT('Ctrl Pts',(-99.3518255329323,-4.36661414793408,
128.536777810003));
#98202=CARTESIAN_POINT('Ctrl Pts',(-99.3598777694174,-4.42825387018387,
128.664325402038));
#98203=CARTESIAN_POINT('Ctrl Pts',(-99.3679189691167,-4.48980910604086,
128.791698171157));
#98204=CARTESIAN_POINT('Ctrl Pts',(-99.3759601688161,-4.54593927038731,
128.921882544925));
#98205=CARTESIAN_POINT('Ctrl Pts',(-99.3840013685154,-4.59638979165394,
129.054393776257));
#98206=CARTESIAN_POINT('Ctrl Pts',(-99.3920295010243,-4.64675832931226,
129.18668967287));
#98207=CARTESIAN_POINT('Ctrl Pts',(-99.4000576335332,-4.69146549368572,
129.321304563779));
#98208=CARTESIAN_POINT('Ctrl Pts',(-99.4080857660421,-4.73030365966211,
129.457731362765));
#98209=CARTESIAN_POINT('Ctrl Pts',(-99.4105234037064,-4.74209636189924,
129.499155579824));
#98210=CARTESIAN_POINT('Ctrl Pts',(-99.4129610413707,-4.75334829840962,
129.540746691713));
#98211=CARTESIAN_POINT('Ctrl Pts',(-99.4153986790351,-4.76405452823397,
129.582490119308));
#98212=CARTESIAN_POINT('Ctrl Pts',(-97.6652146800015,-4.76405452823416,
129.582490119309));
#98213=CARTESIAN_POINT('Ctrl Pts',(-97.6753787325341,-4.80836582721425,
129.755259201514));
#98214=CARTESIAN_POINT('Ctrl Pts',(-97.6855427850666,-4.84329698735637,
129.93052638174));
#98215=CARTESIAN_POINT('Ctrl Pts',(-97.6957068375993,-4.86861814770353,
130.107409834259));
#98216=CARTESIAN_POINT('Ctrl Pts',(-97.7056546069463,-4.89340049332051,
130.280529343561));
#98217=CARTESIAN_POINT('Ctrl Pts',(-97.7156023762933,-4.908977520003,130.4551973254));
#98218=CARTESIAN_POINT('Ctrl Pts',(-97.7255501456403,-4.91517833945882,
130.63056489318));
#98219=CARTESIAN_POINT('Ctrl Pts',(-97.7287469517456,-4.91717102915664,
130.686920855184));
#98220=CARTESIAN_POINT('Ctrl Pts',(-97.7319437578509,-4.91819577127258,
130.743348874851));
#98221=CARTESIAN_POINT('Ctrl Pts',(-97.7351405639562,-4.91824790420648,
130.799820213553));
#98222=CARTESIAN_POINT('',(-97.3898584762948,-4.92178906768926,130.806090568707));
#98223=CARTESIAN_POINT('Ctrl Pts',(-97.3196997604543,-4.76048812747127,
129.583439530431));
#98224=CARTESIAN_POINT('Ctrl Pts',(-97.3430856516127,-4.86675500017061,
129.983187263592));
#98225=CARTESIAN_POINT('Ctrl Pts',(-97.366471542771,-4.92374838532847,130.394849645968));
#98226=CARTESIAN_POINT('Ctrl Pts',(-97.3898574339294,-4.92563332792477,
130.806073603889));
#98227=CARTESIAN_POINT('Ctrl Pts',(-97.3898594359918,-4.91824969023367,
130.806106188069));
#98228=CARTESIAN_POINT('Ctrl Pts',(-97.3952985204717,-4.91821579607926,
130.901605003017));
#98229=CARTESIAN_POINT('Ctrl Pts',(-97.4007376049514,-4.9154006230219,130.997051187051));
#98230=CARTESIAN_POINT('Ctrl Pts',(-97.4061766894311,-4.9098121045098,131.092333117831));
#98231=CARTESIAN_POINT('Ctrl Pts',(-97.4139510235502,-4.90182417744125,
131.228523972774));
#98232=CARTESIAN_POINT('Ctrl Pts',(-97.4217253576694,-4.88815270727774,
131.364597932649));
#98233=CARTESIAN_POINT('Ctrl Pts',(-97.4294996917885,-4.86879967399904,
131.500042151723));
#98234=CARTESIAN_POINT('Ctrl Pts',(-97.4372644447356,-4.84947049160423,
131.635319447902));
#98235=CARTESIAN_POINT('Ctrl Pts',(-97.4450291976826,-4.82447373279531,
131.769968164168));
#98236=CARTESIAN_POINT('Ctrl Pts',(-97.4527939506297,-4.79386333861176,
131.903477241594));
#98237=CARTESIAN_POINT('Ctrl Pts',(-97.4605509915147,-4.76328334710323,
132.036853715921));
#98238=CARTESIAN_POINT('Ctrl Pts',(-97.4683080323997,-4.72710090260625,
132.16909242534));
#98239=CARTESIAN_POINT('Ctrl Pts',(-97.4760650732847,-4.68542147474618,
132.299689566823));
#98240=CARTESIAN_POINT('Ctrl Pts',(-97.4838162645248,-4.64377347766694,
132.430188223987));
#98241=CARTESIAN_POINT('Ctrl Pts',(-97.4915674557649,-4.59663686661538,
132.559047406268));
#98242=CARTESIAN_POINT('Ctrl Pts',(-97.499318647005,-4.54416762220457,132.685775958156));
#98243=CARTESIAN_POINT('Ctrl Pts',(-97.5070665437821,-4.49172067862222,
132.812450647029));
#98244=CARTESIAN_POINT('Ctrl Pts',(-97.5148144405592,-4.43394575884481,
132.936996146156));
#98245=CARTESIAN_POINT('Ctrl Pts',(-97.5225623373363,-4.37104782127443,
133.058939071875));
#98246=CARTESIAN_POINT('Ctrl Pts',(-97.5303086134204,-4.30816304059667,
133.180856489761));
#98247=CARTESIAN_POINT('Ctrl Pts',(-97.5380548895045,-4.24015755275567,
133.300172069839));
#98248=CARTESIAN_POINT('Ctrl Pts',(-97.5458011655886,-4.16728315988435,
133.416435296407));
#98249=CARTESIAN_POINT('Ctrl Pts',(-97.5535474988539,-4.09440822907092,
133.532699381204));
#98250=CARTESIAN_POINT('Ctrl Pts',(-97.5612938321193,-4.01666452915023,
133.645910736262));
#98251=CARTESIAN_POINT('Ctrl Pts',(-97.5690401653846,-3.93434803009684,
133.755646547559));
#98252=CARTESIAN_POINT('Ctrl Pts',(-97.5767882333876,-3.85201309683413,
133.865406933429));
#98253=CARTESIAN_POINT('Ctrl Pts',(-97.5845363013905,-3.76510356126534,
133.971689914071));
#98254=CARTESIAN_POINT('Ctrl Pts',(-97.5922843693935,-3.67395637528701,
134.074104891204));
#98255=CARTESIAN_POINT('Ctrl Pts',(-97.6000406721353,-3.58271231699489,
134.176628716193));
#98256=CARTESIAN_POINT('Ctrl Pts',(-97.6077969748772,-3.4872218717525,134.275276033069));
#98257=CARTESIAN_POINT('Ctrl Pts',(-97.6155532776191,-3.3878600253956,134.369691950111));
#98258=CARTESIAN_POINT('Ctrl Pts',(-97.6233137201332,-3.2884451466293,134.464158259771));
#98259=CARTESIAN_POINT('Ctrl Pts',(-97.6310741626475,-3.18515504380116,
134.554388412408));
#98260=CARTESIAN_POINT('Ctrl Pts',(-97.6388346051616,-3.07839786881164,
134.640067804487));
#98261=CARTESIAN_POINT('Ctrl Pts',(-97.6466075054271,-2.97146931772736,
134.725884736732));
#98262=CARTESIAN_POINT('Ctrl Pts',(-97.6543804056925,-2.86106288760271,
134.807136078266));
#98263=CARTESIAN_POINT('Ctrl Pts',(-97.6621533059579,-2.74761652635889,
134.883550057465));
#98264=CARTESIAN_POINT('Ctrl Pts',(-97.66964364172,-2.63829422609949,134.957186196045));
#98265=CARTESIAN_POINT('Ctrl Pts',(-97.6771339774821,-2.52614943801408,
135.026330405208));
#98266=CARTESIAN_POINT('Ctrl Pts',(-97.6846243132442,-2.41159395103489,
135.090780764709));
#98267=CARTESIAN_POINT('Ctrl Pts',(-97.6923986473633,-2.29269505794933,
135.157674779179));
#98268=CARTESIAN_POINT('Ctrl Pts',(-97.7001729814824,-2.17082241812403,
135.219723883238));
#98269=CARTESIAN_POINT('Ctrl Pts',(-97.7079473156015,-2.04640857342569,
135.276652537053));
#98270=CARTESIAN_POINT('Ctrl Pts',(-97.7157120685486,-1.92214805767176,
135.33351103139));
#98271=CARTESIAN_POINT('Ctrl Pts',(-97.7234768214958,-1.79535292051091,
135.385261470379));
#98272=CARTESIAN_POINT('Ctrl Pts',(-97.7312415744429,-1.66648228674226,
135.43167299631));
#98273=CARTESIAN_POINT('Ctrl Pts',(-97.7389986153279,-1.53773964910417,
135.478038425659));
#98274=CARTESIAN_POINT('Ctrl Pts',(-97.7467556562129,-1.40692598261968,
135.519075362914));
#98275=CARTESIAN_POINT('Ctrl Pts',(-97.7545126970979,-1.27452215995131,
135.554600224817));
#98276=CARTESIAN_POINT('Ctrl Pts',(-97.762263888338,-1.1422181840354,135.590098297145));
#98277=CARTESIAN_POINT('Ctrl Pts',(-97.7700150795781,-1.00832681485096,
135.620092466873));
#98278=CARTESIAN_POINT('Ctrl Pts',(-97.7777662708182,-0.873345586771444,
135.644448483356));
#98279=CARTESIAN_POINT('Ctrl Pts',(-97.7855141675953,-0.738421729314418,
135.668794147883));
#98280=CARTESIAN_POINT('Ctrl Pts',(-97.7932620643724,-0.602409318216158,
135.687506356074));
#98281=CARTESIAN_POINT('Ctrl Pts',(-97.8010099611495,-0.465817409581646,
135.700501669806));
#98282=CARTESIAN_POINT('Ctrl Pts',(-97.8087562372336,-0.32925407302984,
135.713494265199));
#98283=CARTESIAN_POINT('Ctrl Pts',(-97.8165025133178,-0.192111869012933,
135.720772307739));
#98284=CARTESIAN_POINT('Ctrl Pts',(-97.8242487894019,-0.0549059343520972,
135.722304130954));
#98285=CARTESIAN_POINT('Ctrl Pts',(-97.8319951226672,0.0823010131315924,
135.723835965476));
#98286=CARTESIAN_POINT('Ctrl Pts',(-97.8397414559326,0.219571301257105,
135.719621491666));
#98287=CARTESIAN_POINT('Ctrl Pts',(-97.847487789198,0.356389225611277,135.70968117614));
#98288=CARTESIAN_POINT('Ctrl Pts',(-97.8552358572009,0.493237789390792,
135.699738634549));
#98289=CARTESIAN_POINT('Ctrl Pts',(-97.8629839252039,0.629633397953496,
135.684067728012));
#98290=CARTESIAN_POINT('Ctrl Pts',(-97.8707319932069,0.76506529917312,135.662740815791));
#98291=CARTESIAN_POINT('Ctrl Pts',(-97.8784882959488,0.900641139029206,
135.641391237073));
#98292=CARTESIAN_POINT('Ctrl Pts',(-97.8862445986906,1.03525083869141,135.614373705427));
#98293=CARTESIAN_POINT('Ctrl Pts',(-97.8940009014325,1.16839312870102,135.581811879411));
#98294=CARTESIAN_POINT('Ctrl Pts',(-97.9017613439467,1.30160648076001,135.549232674168));
#98295=CARTESIAN_POINT('Ctrl Pts',(-97.9095217864608,1.43335048720379,135.511103386825));
#98296=CARTESIAN_POINT('Ctrl Pts',(-97.917282228975,1.56313984709728,135.46759735624));
#98297=CARTESIAN_POINT('Ctrl Pts',(-97.9250551292404,1.69313755639307,135.424021485912));
#98298=CARTESIAN_POINT('Ctrl Pts',(-97.9328280295059,1.82117398349192,135.375051764149));
#98299=CARTESIAN_POINT('Ctrl Pts',(-97.9406009297713,1.94678375768187,135.320909749738));
#98300=CARTESIAN_POINT('Ctrl Pts',(-97.9480912655332,2.06782730018638,135.268735933928));
#98301=CARTESIAN_POINT('Ctrl Pts',(-97.9555816012951,2.18661727886674,135.211759481601));
#98302=CARTESIAN_POINT('Ctrl Pts',(-97.963071937057,2.30276123052712,135.150217699625));
#98303=CARTESIAN_POINT('Ctrl Pts',(-97.9708462711761,2.42330881541743,135.086342542279));
#98304=CARTESIAN_POINT('Ctrl Pts',(-97.9786206052953,2.54138762271405,135.017346695159));
#98305=CARTESIAN_POINT('Ctrl Pts',(-97.9863949394143,2.65653203350798,134.943445131978));
#98306=CARTESIAN_POINT('Ctrl Pts',(-97.9941596923614,2.77153453910637,134.869634645869));
#98307=CARTESIAN_POINT('Ctrl Pts',(-98.0019244453084,2.88360951785468,134.790930682299));
#98308=CARTESIAN_POINT('Ctrl Pts',(-98.0096891982555,2.99231457445502,134.707594731734));
#98309=CARTESIAN_POINT('Ctrl Pts',(-98.0174462391405,3.10091166366068,134.62434155161));
#98310=CARTESIAN_POINT('Ctrl Pts',(-98.0252032800256,3.20614518323624,134.53646577613));
#98311=CARTESIAN_POINT('Ctrl Pts',(-98.0329603209106,3.30760075596693,134.44427274585));
#98312=CARTESIAN_POINT('Ctrl Pts',(-98.0407115121507,3.40897982026089,134.352149239051));
#98313=CARTESIAN_POINT('Ctrl Pts',(-98.0484627033908,3.50658632025427,134.255715219542));
#98314=CARTESIAN_POINT('Ctrl Pts',(-98.0562138946309,3.60003837759656,134.15531671133));
#98315=CARTESIAN_POINT('Ctrl Pts',(-98.0639617914079,3.69345071532169,134.054960875162));
#98316=CARTESIAN_POINT('Ctrl Pts',(-98.0717096881851,3.78271185651674,133.950644187232));
#98317=CARTESIAN_POINT('Ctrl Pts',(-98.0794575849622,3.86747644506555,133.842749830515));
#98318=CARTESIAN_POINT('Ctrl Pts',(-98.0872038610463,3.95222330268974,133.734878042971));
#98319=CARTESIAN_POINT('Ctrl Pts',(-98.0949501371303,4.03247523715973,133.623430382432));
#98320=CARTESIAN_POINT('Ctrl Pts',(-98.1026964132144,4.10792716253893,133.508823131593));
#98321=CARTESIAN_POINT('Ctrl Pts',(-98.1104427464797,4.18337964488699,133.394215034749));
#98322=CARTESIAN_POINT('Ctrl Pts',(-98.118189079745,4.25403183245597,133.276447627614));
#98323=CARTESIAN_POINT('Ctrl Pts',(-98.1259354130104,4.31962219355627,133.155965849623));
#98324=CARTESIAN_POINT('Ctrl Pts',(-98.1336834810133,4.38522724316325,133.035457090572));
#98325=CARTESIAN_POINT('Ctrl Pts',(-98.1414315490163,4.4457680237467,132.912233094398));
#98326=CARTESIAN_POINT('Ctrl Pts',(-98.1491796170193,4.50102933920304,132.786762683277));
#98327=CARTESIAN_POINT('Ctrl Pts',(-98.1569359197612,4.55634938704299,132.66115892071));
#98328=CARTESIAN_POINT('Ctrl Pts',(-98.164692222503,4.60637860318453,132.533304332244));
#98329=CARTESIAN_POINT('Ctrl Pts',(-98.1724485252448,4.65095007669019,132.403687490546));
#98330=CARTESIAN_POINT('Ctrl Pts',(-98.180208967759,4.69554533933328,132.274001468436));
#98331=CARTESIAN_POINT('Ctrl Pts',(-98.1879694102731,4.734676943523,132.142551693463));
#98332=CARTESIAN_POINT('Ctrl Pts',(-98.1957298527873,4.76822840714074,132.009840156935));
#98333=CARTESIAN_POINT('Ctrl Pts',(-98.2035027530527,4.80183373054652,131.876915580066));
#98334=CARTESIAN_POINT('Ctrl Pts',(-98.2112756533181,4.8298409330431,131.742725577002));
#98335=CARTESIAN_POINT('Ctrl Pts',(-98.2190485535836,4.85218487407739,131.607781435242));
#98336=CARTESIAN_POINT('Ctrl Pts',(-98.2265388893457,4.8737165565744,131.477742852936));
#98337=CARTESIAN_POINT('Ctrl Pts',(-98.2340292251079,4.88998953865862,131.347004315352));
#98338=CARTESIAN_POINT('Ctrl Pts',(-98.24151956087,4.90099133737466,131.216024283049));
#98339=CARTESIAN_POINT('Ctrl Pts',(-98.2492938949891,4.91241027263277,131.080078103012));
#98340=CARTESIAN_POINT('Ctrl Pts',(-98.2570682291081,4.91818659196586,130.943441117583));
#98341=CARTESIAN_POINT('Ctrl Pts',(-98.2648425632272,4.9182494804533,130.806621263677));
#98342=CARTESIAN_POINT('Ctrl Pts',(-98.2726073161743,4.9183122914363,130.669970028014));
#98343=CARTESIAN_POINT('Ctrl Pts',(-98.2803720691214,4.91267568146981,130.533136759504));
#98344=CARTESIAN_POINT('Ctrl Pts',(-98.2881368220685,4.90132052442372,130.396634999824));
#98345=CARTESIAN_POINT('Ctrl Pts',(-98.2958938629535,4.8899766454797,130.260268815617));
#98346=CARTESIAN_POINT('Ctrl Pts',(-98.3036509038384,4.87292555459962,130.124233872098));
#98347=CARTESIAN_POINT('Ctrl Pts',(-98.3114079447234,4.85020016243341,129.989043840582));
#98348=CARTESIAN_POINT('Ctrl Pts',(-98.3191591359635,4.82749190766217,129.853955756921));
#98349=CARTESIAN_POINT('Ctrl Pts',(-98.3269103272037,4.79911793331346,129.71971170104));
#98350=CARTESIAN_POINT('Ctrl Pts',(-98.3346615184439,4.76516294460801,129.586819992439));
#98351=CARTESIAN_POINT('Ctrl Pts',(-98.342409415221,4.73122238767848,129.453984766359));
#98352=CARTESIAN_POINT('Ctrl Pts',(-98.350157311998,4.69170563086144,129.322501122362));
#98353=CARTESIAN_POINT('Ctrl Pts',(-98.3579052087751,4.64674838342874,129.192866738086));
#98354=CARTESIAN_POINT('Ctrl Pts',(-98.3656514848592,4.60180054008315,129.063259470528));
#98355=CARTESIAN_POINT('Ctrl Pts',(-98.3733977609433,4.55141459775355,128.935501062424));
#98356=CARTESIAN_POINT('Ctrl Pts',(-98.3811440370274,4.4957758804594,128.810073202177));
#98357=CARTESIAN_POINT('Ctrl Pts',(-98.3888903702928,4.44013675245279,128.684644416049));
#98358=CARTESIAN_POINT('Ctrl Pts',(-98.3966367035582,4.37924493064071,128.561546569488));
#98359=CARTESIAN_POINT('Ctrl Pts',(-98.4043830368235,4.3133333909033,128.441240197143));
#98360=CARTESIAN_POINT('Ctrl Pts',(-98.4121311048265,4.24740709073367,128.320906883021));
#98361=CARTESIAN_POINT('Ctrl Pts',(-98.4198791728294,4.17645902356311,128.203366629866));
#98362=CARTESIAN_POINT('Ctrl Pts',(-98.4276272408324,4.10076730401701,128.089053898095));
#98363=CARTESIAN_POINT('Ctrl Pts',(-98.4353835435742,4.02499513841053,127.974619673392));
#98364=CARTESIAN_POINT('Ctrl Pts',(-98.4431398463161,3.94446946546042,127.863420148863));
#98365=CARTESIAN_POINT('Ctrl Pts',(-98.450896149058,3.85951111574793,127.755859836868));
#98366=CARTESIAN_POINT('Ctrl Pts',(-98.4586565915721,3.77450742120614,127.648242116695));
#98367=CARTESIAN_POINT('Ctrl Pts',(-98.4664170340864,3.68506659057689,127.544267775613));
#98368=CARTESIAN_POINT('Ctrl Pts',(-98.4741774766005,3.59154800193454,127.444306151891));
#98369=CARTESIAN_POINT('Ctrl Pts',(-98.481950376866,3.49787928895151,127.344184060897));
#98370=CARTESIAN_POINT('Ctrl Pts',(-98.4897232771314,3.40012001597915,127.248087833803));
#98371=CARTESIAN_POINT('Ctrl Pts',(-98.4974961773969,3.29866513360926,127.156348638582));
#98372=CARTESIAN_POINT('Ctrl Pts',(-98.5049865131589,3.20089839176322,127.067944394185));
#98373=CARTESIAN_POINT('Ctrl Pts',(-98.5124768489209,3.09970030169355,126.983586100453));
#98374=CARTESIAN_POINT('Ctrl Pts',(-98.5199671846829,2.99544983191148,126.903532068783));
#98375=CARTESIAN_POINT('Ctrl Pts',(-98.527741518802,2.88724667388123,126.82044276417));
#98376=CARTESIAN_POINT('Ctrl Pts',(-98.535515852921,2.77541234997262,126.741727354952));
#98377=CARTESIAN_POINT('Ctrl Pts',(-98.5432901870401,2.66033592470592,126.66771997204));
#98378=CARTESIAN_POINT('Ctrl Pts',(-98.5510549399872,2.54540132084868,126.593803796613));
#98379=CARTESIAN_POINT('Ctrl Pts',(-98.5588196929343,2.42723289136294,126.524584312247));
#98380=CARTESIAN_POINT('Ctrl Pts',(-98.5665844458814,2.30625235526557,126.460355192117));
#98381=CARTESIAN_POINT('Ctrl Pts',(-98.5743414867664,2.18539197874218,126.396189865255));
#98382=CARTESIAN_POINT('Ctrl Pts',(-98.5820985276514,2.0617253969332,126.337005221114));
#98383=CARTESIAN_POINT('Ctrl Pts',(-98.5898555685364,1.93570256507375,126.283051222925));
#98384=CARTESIAN_POINT('Ctrl Pts',(-98.5976067597765,1.80977476801229,126.229137911867));
#98385=CARTESIAN_POINT('Ctrl Pts',(-98.6053579510166,1.68149461560239,126.180447548782));
#98386=CARTESIAN_POINT('Ctrl Pts',(-98.6131091422567,1.55133555667627,126.137183627876));
#98387=CARTESIAN_POINT('Ctrl Pts',(-98.6208570390338,1.42123181882212,126.093938095291));
#98388=CARTESIAN_POINT('Ctrl Pts',(-98.6286049358109,1.28925113300718,126.056114540726));
#98389=CARTESIAN_POINT('Ctrl Pts',(-98.636352832588,1.15588556370023,126.02386779505));
#98390=CARTESIAN_POINT('Ctrl Pts',(-98.6440991086721,1.02254789159534,125.991627794697));
#98391=CARTESIAN_POINT('Ctrl Pts',(-98.6518453847561,0.887826291977052,
125.96496237473));
#98392=CARTESIAN_POINT('Ctrl Pts',(-98.6595916608402,0.752226195100541,
125.94397598115));
#98393=CARTESIAN_POINT('Ctrl Pts',(-98.6673379941055,0.616625097255102,
125.922989432654));
#98394=CARTESIAN_POINT('Ctrl Pts',(-98.6750843273709,0.480145875576691,
125.907682053992));
#98395=CARTESIAN_POINT('Ctrl Pts',(-98.6828306606363,0.34330192006288,125.898106766186));
#98396=CARTESIAN_POINT('Ctrl Pts',(-98.6905787286392,0.206427319293855,
125.888529334061));
#98397=CARTESIAN_POINT('Ctrl Pts',(-98.6983267966421,0.0691882120934057,
125.884686574414));
#98398=CARTESIAN_POINT('Ctrl Pts',(-98.706074864645,-0.067899549938197,
125.886579338003));
#98399=CARTESIAN_POINT('Ctrl Pts',(-98.7138311673869,-0.205133010474839,
125.888474113244));
#98400=CARTESIAN_POINT('Ctrl Pts',(-98.7215874701289,-0.342214412973249,
125.896116583295));
#98401=CARTESIAN_POINT('Ctrl Pts',(-98.7293437728707,-0.478630012964187,
125.909455473113));
#98402=CARTESIAN_POINT('Ctrl Pts',(-98.7371042153849,-0.615118422068234,
125.922801482299));
#98403=CARTESIAN_POINT('Ctrl Pts',(-98.744864657899,-0.75093993359559,125.941849915134));
#98404=CARTESIAN_POINT('Ctrl Pts',(-98.7526251004132,-0.885589560172638,
125.966498053022));
#98405=CARTESIAN_POINT('Ctrl Pts',(-98.7603980006786,-1.0204553382839,125.99118575829));
#98406=CARTESIAN_POINT('Ctrl Pts',(-98.7681709009441,-1.15414509066939,
126.021491045303));
#98407=CARTESIAN_POINT('Ctrl Pts',(-98.7759438012095,-1.28616671589187,
126.057260635321));
#98408=CARTESIAN_POINT('Ctrl Pts',(-98.7834341369716,-1.41338902249583,
126.091729910644));
#98409=CARTESIAN_POINT('Ctrl Pts',(-98.7909244727336,-1.53906208374758,
126.131273011571));
#98410=CARTESIAN_POINT('Ctrl Pts',(-98.7984148084957,-1.66276373321742,
126.175710724779));
#98411=CARTESIAN_POINT('Ctrl Pts',(-98.8061892740224,-1.79115773849947,
126.221834086988));
#98412=CARTESIAN_POINT('Ctrl Pts',(-98.8139637395492,-1.91783453747899,
126.273376832534));
#98413=CARTESIAN_POINT('Ctrl Pts',(-98.8217382050759,-2.04230269266731,
126.330192228466));
#98414=CARTESIAN_POINT('Ctrl Pts',(-98.829503058786,-2.16661696395553,126.386937381734));
#98415=CARTESIAN_POINT('Ctrl Pts',(-98.8372679124961,-2.28872767236615,
126.448942054039));
#98416=CARTESIAN_POINT('Ctrl Pts',(-98.8450327662062,-2.40815977482729,
126.516010169969));
#98417=CARTESIAN_POINT('Ctrl Pts',(-98.8527898773389,-2.52747278781919,
126.583011410192));
#98418=CARTESIAN_POINT('Ctrl Pts',(-98.8605469884715,-2.64411217150775,
126.655065856078));
#98419=CARTESIAN_POINT('Ctrl Pts',(-98.8683040996042,-2.75762440141954,
126.731930050546));
#98420=CARTESIAN_POINT('Ctrl Pts',(-98.8760553306746,-2.87105058654408,
126.808735980251));
#98421=CARTESIAN_POINT('Ctrl Pts',(-98.883806561745,-2.98135401381862,126.890344183093));
#98422=CARTESIAN_POINT('Ctrl Pts',(-98.8915577928154,-3.08810756172547,
126.976466320473));
#98423=CARTESIAN_POINT('Ctrl Pts',(-98.8993055730249,-3.19481358277658,
127.062550116136));
#98424=CARTESIAN_POINT('Ctrl Pts',(-98.9070533532344,-3.29797256497424,
127.153143603344));
#98425=CARTESIAN_POINT('Ctrl Pts',(-98.9148011334439,-3.39718829094002,
127.247916497606));
#98426=CARTESIAN_POINT('Ctrl Pts',(-98.922547249637,-3.49638270801475,127.342669037178));
#98427=CARTESIAN_POINT('Ctrl Pts',(-98.9302933658301,-3.59163527116042,
127.44159892824));
#98428=CARTESIAN_POINT('Ctrl Pts',(-98.9380394820231,-3.68258493265018,
127.544337415759));
#98429=CARTESIAN_POINT('Ctrl Pts',(-98.9457856120448,-3.77353475650647,
127.647076086691));
#98430=CARTESIAN_POINT('Ctrl Pts',(-98.9535317420665,-3.86018140440898,
127.753623074815));
#98431=CARTESIAN_POINT('Ctrl Pts',(-98.9612778720882,-3.94220287772239,
127.86357508758));
#98432=CARTESIAN_POINT('Ctrl Pts',(-98.9690256934281,-4.02424225990282,
127.973551107667));
#98433=CARTESIAN_POINT('Ctrl Pts',(-98.976773514768,-4.10165422457565,128.086933318308));
#98434=CARTESIAN_POINT('Ctrl Pts',(-98.9845213361079,-4.17415925078712,
128.203288221117));
#98435=CARTESIAN_POINT('Ctrl Pts',(-98.9922767939493,-4.24673574028139,
128.319757807056));
#98436=CARTESIAN_POINT('Ctrl Pts',(-99.0000322517909,-4.31439542526681,
128.43920560458));
#98437=CARTESIAN_POINT('Ctrl Pts',(-99.0077877096324,-4.37690382517589,
128.56117182309));
#98438=CARTESIAN_POINT('Ctrl Pts',(-99.0155472893426,-4.4394454470335,128.683202864176));
#98439=CARTESIAN_POINT('Ctrl Pts',(-99.0233068690528,-4.49683016518702,
128.807754638531));
#98440=CARTESIAN_POINT('Ctrl Pts',(-99.0310664487631,-4.54887149333015,
128.934346927865));
#98441=CARTESIAN_POINT('Ctrl Pts',(-99.0388370862935,-4.6009869831765,129.061119618049));
#98442=CARTESIAN_POINT('Ctrl Pts',(-99.046607723824,-4.64774373928055,129.189938264582));
#98443=CARTESIAN_POINT('Ctrl Pts',(-99.0543783613544,-4.68900482500524,
129.320306436083));
#98444=CARTESIAN_POINT('Ctrl Pts',(-99.0595496068237,-4.71646347325353,
129.407064544871));
#98445=CARTESIAN_POINT('Ctrl Pts',(-99.064720852293,-4.74148929291332,129.494508609268));
#98446=CARTESIAN_POINT('Ctrl Pts',(-99.0698920977623,-4.76405452823408,
129.582490119308));
#98447=CARTESIAN_POINT('Origin',(213.235140564004,0.,130.804360617566));
#98448=CARTESIAN_POINT('',(-101.165045656948,-4.76405452823419,129.582490119309));
#98449=CARTESIAN_POINT('',(-100.820132980931,-4.76405452823394,129.582490119308));
#98450=CARTESIAN_POINT('',(213.235140564004,-4.76405452823405,129.582490119308));
#98451=CARTESIAN_POINT('',(-99.4851405640526,-4.91824989996933,130.805352560943));
#98452=CARTESIAN_POINT('Ctrl Pts',(-99.4851405640525,-4.91824989996933,
130.805352560944));
#98453=CARTESIAN_POINT('Ctrl Pts',(-99.4933901351786,-4.91822036007165,
130.951817169788));
#98454=CARTESIAN_POINT('Ctrl Pts',(-99.5016397063047,-4.9116440396768,131.098114664302));
#98455=CARTESIAN_POINT('Ctrl Pts',(-99.5098892774308,-4.89859101298216,
131.243665921461));
#98456=CARTESIAN_POINT('Ctrl Pts',(-99.5185792279595,-4.88484118835586,
131.396987009887));
#98457=CARTESIAN_POINT('Ctrl Pts',(-99.5272691784882,-4.86390433493261,
131.549479585931));
#98458=CARTESIAN_POINT('Ctrl Pts',(-99.5359591290169,-4.83592288046644,
131.700481678964));
#98459=CARTESIAN_POINT('Ctrl Pts',(-99.5442498456649,-4.80922695054012,
131.844546430823));
#98460=CARTESIAN_POINT('Ctrl Pts',(-99.5525405623128,-4.77611938693527,
131.987254339953));
#98461=CARTESIAN_POINT('Ctrl Pts',(-99.5608312789607,-4.73677468896852,
132.128048121642));
#98462=CARTESIAN_POINT('Ctrl Pts',(-99.5691354981031,-4.6973659131193,132.269071204047));
#98463=CARTESIAN_POINT('Ctrl Pts',(-99.5774397172456,-4.65169981408719,
132.408173642682));
#98464=CARTESIAN_POINT('Ctrl Pts',(-99.585743936388,-4.59999944278608,132.544816933843));
#98465=CARTESIAN_POINT('Ctrl Pts',(-99.5940676315148,-4.5481778179863,132.681780696147));
#98466=CARTESIAN_POINT('Ctrl Pts',(-99.6023913266416,-4.49029374540701,
132.816273497092));
#98467=CARTESIAN_POINT('Ctrl Pts',(-99.6107150217685,-4.42661743930218,
132.947778707572));
#98468=CARTESIAN_POINT('Ctrl Pts',(-99.6118662424373,-4.41781059587682,
132.965966725521));
#98469=CARTESIAN_POINT('Ctrl Pts',(-99.6130174631061,-4.40889302351978,
132.98409763851));
#98470=CARTESIAN_POINT('Ctrl Pts',(-99.6141686837749,-4.39986550271429,
133.002170122624));
#98471=CARTESIAN_POINT('Ctrl Pts',(-99.621943017894,-4.33890154948689,133.124215820442));
#98472=CARTESIAN_POINT('Ctrl Pts',(-99.629717352013,-4.2727591372625,133.243916334047));
#98473=CARTESIAN_POINT('Ctrl Pts',(-99.6374916861321,-4.20164200427695,
133.360801019843));
#98474=CARTESIAN_POINT('Ctrl Pts',(-99.6452564390792,-4.13061251680189,
133.47754165571));
#98475=CARTESIAN_POINT('Ctrl Pts',(-99.6530211920263,-4.05462070849437,
133.591473037749));
#98476=CARTESIAN_POINT('Ctrl Pts',(-99.6607859449734,-3.97391737824988,
133.702146623009));
#98477=CARTESIAN_POINT('Ctrl Pts',(-99.6685429858584,-3.89329420369071,
133.812710285705));
#98478=CARTESIAN_POINT('Ctrl Pts',(-99.6763000267434,-3.8079690485726,133.920022276938));
#98479=CARTESIAN_POINT('Ctrl Pts',(-99.6840570676283,-3.71823722160899,
134.023661011493));
#98480=CARTESIAN_POINT('Ctrl Pts',(-99.6918082588684,-3.62857306211422,
134.127221591272));
#98481=CARTESIAN_POINT('Ctrl Pts',(-99.6995594501086,-3.53450910008951,
134.227114133576));
#98482=CARTESIAN_POINT('Ctrl Pts',(-99.7073106413487,-3.43638209586812,
134.322948566402));
#98483=CARTESIAN_POINT('Ctrl Pts',(-99.7150585381258,-3.33829679824102,
134.418742267039));
#98484=CARTESIAN_POINT('Ctrl Pts',(-99.7228064349029,-3.23615217220895,
134.510481016108));
#98485=CARTESIAN_POINT('Ctrl Pts',(-99.7305543316799,-3.13032300280422,
134.597810361614));
#98486=CARTESIAN_POINT('Ctrl Pts',(-99.738300607764,-3.02451597058032,134.685121439703));
#98487=CARTESIAN_POINT('Ctrl Pts',(-99.746046883848,-2.9150262293628,134.768024700156));
#98488=CARTESIAN_POINT('Ctrl Pts',(-99.7537931599321,-2.80226262074539,
134.846205155258));
#98489=CARTESIAN_POINT('Ctrl Pts',(-99.7615394931974,-2.68949817973248,
134.924386187471));
#98490=CARTESIAN_POINT('Ctrl Pts',(-99.7692858264628,-2.57346014439362,
134.997844122007));
#98491=CARTESIAN_POINT('Ctrl Pts',(-99.7770321597281,-2.4545870499912,135.066306825171));
#98492=CARTESIAN_POINT('Ctrl Pts',(-99.7847802277311,-2.33568733478367,
135.134784860082));
#98493=CARTESIAN_POINT('Ctrl Pts',(-99.7925282957342,-2.21395163588035,
135.198265242559));
#98494=CARTESIAN_POINT('Ctrl Pts',(-99.8002763637371,-2.08984347633659,
135.256521588029));
#98495=CARTESIAN_POINT('Ctrl Pts',(-99.808032666479,-1.9656034131638,135.314839849036));
#98496=CARTESIAN_POINT('Ctrl Pts',(-99.8157889692208,-1.83898620690269,
135.367922815589));
#98497=CARTESIAN_POINT('Ctrl Pts',(-99.8235452719626,-1.71047628411891,
135.41559190042));
#98498=CARTESIAN_POINT('Ctrl Pts',(-99.8313057144768,-1.58189777171998,
135.463286427676));
#98499=CARTESIAN_POINT('Ctrl Pts',(-99.8390661569911,-1.45142490163688,
135.505561195083));
#98500=CARTESIAN_POINT('Ctrl Pts',(-99.8468265995052,-1.31955672536704,
135.542287707659));
#98501=CARTESIAN_POINT('Ctrl Pts',(-99.8545994997707,-1.18747686259395,
135.579073176894));
#98502=CARTESIAN_POINT('Ctrl Pts',(-99.862372400036,-1.05399759857168,135.610292504079));
#98503=CARTESIAN_POINT('Ctrl Pts',(-99.8701453003014,-0.9196285103657,135.635868297931));
#98504=CARTESIAN_POINT('Ctrl Pts',(-99.8776356360634,-0.790144076970954,
135.660514347254));
#98505=CARTESIAN_POINT('Ctrl Pts',(-99.8851259718256,-0.65983369555726,
135.679920007538));
#98506=CARTESIAN_POINT('Ctrl Pts',(-99.8926163075877,-0.52915539510297,
135.694061797631));
#98507=CARTESIAN_POINT('Ctrl Pts',(-99.9003906417068,-0.393522387168712,
135.708739777995));
#98508=CARTESIAN_POINT('Ctrl Pts',(-99.9081649758259,-0.257063365551851,
135.717793344791));
#98509=CARTESIAN_POINT('Ctrl Pts',(-99.9159393099449,-0.120284421534253,
135.721139514409));
#98510=CARTESIAN_POINT('Ctrl Pts',(-99.923704062892,0.0163259546591279,
135.724481560171));
#98511=CARTESIAN_POINT('Ctrl Pts',(-99.9314688158392,0.153255081665827,
135.722130194562));
#98512=CARTESIAN_POINT('Ctrl Pts',(-99.9392335687862,0.28999002467024,135.714053973377));
#98513=CARTESIAN_POINT('Ctrl Pts',(-99.9469906096713,0.426589160601637,
135.705985773608));
#98514=CARTESIAN_POINT('Ctrl Pts',(-99.9547476505562,0.562994108583869,
135.692204056576));
#98515=CARTESIAN_POINT('Ctrl Pts',(-99.9625046914412,0.69869055546209,135.672729396758));
#98516=CARTESIAN_POINT('Ctrl Pts',(-99.9702558826814,0.83428467259434,135.653269422932));
#98517=CARTESIAN_POINT('Ctrl Pts',(-99.9780070739216,0.969170966652728,
135.628125106777));
#98518=CARTESIAN_POINT('Ctrl Pts',(-99.9857582651617,1.10283923182938,135.597368930853));
#98519=CARTESIAN_POINT('Ctrl Pts',(-99.9935061619388,1.23645068442743,135.566625827125));
#98520=CARTESIAN_POINT('Ctrl Pts',(-100.001254058716,1.36884475758745,135.530275695073));
#98521=CARTESIAN_POINT('Ctrl Pts',(-100.009001955493,1.49952066034119,135.488442261999));
#98522=CARTESIAN_POINT('Ctrl Pts',(-100.016748231577,1.63016922851311,135.446617579576));
#98523=CARTESIAN_POINT('Ctrl Pts',(-100.024494507661,1.75909996903882,135.399311996679));
#98524=CARTESIAN_POINT('Ctrl Pts',(-100.032240783745,1.88582688496382,135.346699224765));
#98525=CARTESIAN_POINT('Ctrl Pts',(-100.039987117011,2.01255473635794,135.294086064475));
#98526=CARTESIAN_POINT('Ctrl Pts',(-100.047733450276,2.13707836960651,135.236165786902));
#98527=CARTESIAN_POINT('Ctrl Pts',(-100.055479783541,2.25893179190393,135.173160249276));
#98528=CARTESIAN_POINT('Ctrl Pts',(-100.063227851544,2.38081250243057,135.110140601995));
#98529=CARTESIAN_POINT('Ctrl Pts',(-100.070975919547,2.50002146488317,135.042033608097));
#98530=CARTESIAN_POINT('Ctrl Pts',(-100.07872398755,2.61611766997616,134.969106876264));
#98531=CARTESIAN_POINT('Ctrl Pts',(-100.086480290292,2.73233726349732,134.896102637032));
#98532=CARTESIAN_POINT('Ctrl Pts',(-100.094236593034,2.84543715942706,134.818268635465));
#98533=CARTESIAN_POINT('Ctrl Pts',(-100.101992895776,2.9550052628474,134.73591590257));
#98534=CARTESIAN_POINT('Ctrl Pts',(-100.10975333829,3.06463184606387,134.653519215542));
#98535=CARTESIAN_POINT('Ctrl Pts',(-100.117513780804,3.17072257842416,134.56659923916));
#98536=CARTESIAN_POINT('Ctrl Pts',(-100.125274223318,3.27289960393646,134.475506384905));
#98537=CARTESIAN_POINT('Ctrl Pts',(-100.133047123584,3.37524065308097,134.384267300314));
#98538=CARTESIAN_POINT('Ctrl Pts',(-100.140820023849,3.47365515983561,134.288842224081));
#98539=CARTESIAN_POINT('Ctrl Pts',(-100.148592924115,3.56780257387002,134.189618045944));
#98540=CARTESIAN_POINT('Ctrl Pts',(-100.156083259877,3.65852749226177,134.094000916611));
#98541=CARTESIAN_POINT('Ctrl Pts',(-100.163573595639,3.74528996801761,133.994856335539));
#98542=CARTESIAN_POINT('Ctrl Pts',(-100.171063931401,3.8278226699303,133.892556963343));
#98543=CARTESIAN_POINT('Ctrl Pts',(-100.17883826552,3.91348462432068,133.786378879357));
#98544=CARTESIAN_POINT('Ctrl Pts',(-100.186612599639,3.99486108085797,133.67646571375));
#98545=CARTESIAN_POINT('Ctrl Pts',(-100.194386933758,4.07160866837837,133.563198400779));
#98546=CARTESIAN_POINT('Ctrl Pts',(-100.202151686705,4.14826167135627,133.45007067965));
#98547=CARTESIAN_POINT('Ctrl Pts',(-100.209916439652,4.22029693870276,133.333597356518));
#98548=CARTESIAN_POINT('Ctrl Pts',(-100.217681192599,4.28741076171937,133.21419298161));
#98549=CARTESIAN_POINT('Ctrl Pts',(-100.225438233484,4.35445792634083,133.09490720081));
#98550=CARTESIAN_POINT('Ctrl Pts',(-100.233195274369,4.4165931837437,132.972696500191));
#98551=CARTESIAN_POINT('Ctrl Pts',(-100.240952315254,4.47355584499542,132.848004706983));
#98552=CARTESIAN_POINT('Ctrl Pts',(-100.248703506494,4.53047555026125,132.723406944825));
#98553=CARTESIAN_POINT('Ctrl Pts',(-100.256454697734,4.58223026167519,132.59633216839));
#98554=CARTESIAN_POINT('Ctrl Pts',(-100.264205888974,4.62860518216726,132.467248806866));
#98555=CARTESIAN_POINT('Ctrl Pts',(-100.271953785752,4.67496039208097,132.338220309215));
#98556=CARTESIAN_POINT('Ctrl Pts',(-100.279701682529,4.71594022694488,132.207185291596));
#98557=CARTESIAN_POINT('Ctrl Pts',(-100.287449579306,4.75137809228967,132.07463196126));
#98558=CARTESIAN_POINT('Ctrl Pts',(-100.29519585539,4.78680854479707,131.942106358223));
#98559=CARTESIAN_POINT('Ctrl Pts',(-100.302942131474,4.81669923270472,131.808063451651));
#98560=CARTESIAN_POINT('Ctrl Pts',(-100.310688407558,4.84093361115626,131.673006019832));
#98561=CARTESIAN_POINT('Ctrl Pts',(-100.318434740823,4.86516816850043,131.53794759105));
#98562=CARTESIAN_POINT('Ctrl Pts',(-100.326181074089,4.88374626402124,131.401875006896));
#98563=CARTESIAN_POINT('Ctrl Pts',(-100.333927407354,4.89660267199325,131.265300239565));
#98564=CARTESIAN_POINT('Ctrl Pts',(-100.341675475357,4.90946195906866,131.128694887262));
#98565=CARTESIAN_POINT('Ctrl Pts',(-100.34942354336,4.9165969722581,130.99158751717));
#98566=CARTESIAN_POINT('Ctrl Pts',(-100.357171611363,4.91799448203471,130.85449381192));
#98567=CARTESIAN_POINT('Ctrl Pts',(-100.364927914105,4.91939347710135,130.717254401848));
#98568=CARTESIAN_POINT('Ctrl Pts',(-100.372684216847,4.91504278357763,130.580029077198));
#98569=CARTESIAN_POINT('Ctrl Pts',(-100.380440519588,4.90498133329089,130.443332664953));
#98570=CARTESIAN_POINT('Ctrl Pts',(-100.388200962103,4.89491451290518,130.306563293717));
#98571=CARTESIAN_POINT('Ctrl Pts',(-100.395961404617,4.87913090732387,130.170323785564));
#98572=CARTESIAN_POINT('Ctrl Pts',(-100.403721847131,4.85772108725793,130.035121447405));
#98573=CARTESIAN_POINT('Ctrl Pts',(-100.411494747396,4.83627689824814,129.899702070451));
#98574=CARTESIAN_POINT('Ctrl Pts',(-100.419267647662,4.80918852384349,129.765323574084));
#98575=CARTESIAN_POINT('Ctrl Pts',(-100.427040547927,4.77659738956548,129.632481596295));
#98576=CARTESIAN_POINT('Ctrl Pts',(-100.434530883689,4.7451910251106,129.504468759007));
#98577=CARTESIAN_POINT('Ctrl Pts',(-100.442021219451,4.70867511857131,129.377882963102));
#98578=CARTESIAN_POINT('Ctrl Pts',(-100.449511555213,4.6672187008311,129.253150554063));
#98579=CARTESIAN_POINT('Ctrl Pts',(-100.457285889332,4.62419045041181,129.123688877823));
#98580=CARTESIAN_POINT('Ctrl Pts',(-100.465060223451,4.57570335377249,128.995813809448));
#98581=CARTESIAN_POINT('Ctrl Pts',(-100.47283455757,4.52189230119232,128.870020141094));
#98582=CARTESIAN_POINT('Ctrl Pts',(-100.480599310517,4.46814756592537,128.744381502194));
#98583=CARTESIAN_POINT('Ctrl Pts',(-100.488364063465,4.40909208203862,128.620819515459));
#98584=CARTESIAN_POINT('Ctrl Pts',(-100.496128816412,4.34491046040765,128.499813774141));
#98585=CARTESIAN_POINT('Ctrl Pts',(-100.503885857297,4.28079258486808,128.378928217431));
#98586=CARTESIAN_POINT('Ctrl Pts',(-100.511642898182,4.21155888561439,128.260594196769));
#98587=CARTESIAN_POINT('Ctrl Pts',(-100.519399939067,4.13744185832994,128.145270936596));
#98588=CARTESIAN_POINT('Ctrl Pts',(-100.527151130307,4.0633807232722,128.030034642591));
#98589=CARTESIAN_POINT('Ctrl Pts',(-100.534902321547,3.98444380061046,127.917804917471));
#98590=CARTESIAN_POINT('Ctrl Pts',(-100.542653512787,3.90090909002651,127.809015673516));
#98591=CARTESIAN_POINT('Ctrl Pts',(-100.550401409564,3.81740988392304,127.700272667891));
#98592=CARTESIAN_POINT('Ctrl Pts',(-100.558149306341,3.72931701422712,127.594967544479));
#98593=CARTESIAN_POINT('Ctrl Pts',(-100.565897203118,3.63695117514703,127.49350435187));
#98594=CARTESIAN_POINT('Ctrl Pts',(-100.573643479202,3.5446046570093,127.392062383174));
#98595=CARTESIAN_POINT('Ctrl Pts',(-100.581389755287,3.44798721035295,127.294461035707));
#98596=CARTESIAN_POINT('Ctrl Pts',(-100.589136031371,3.3474588414492,127.201070125904));
#98597=CARTESIAN_POINT('Ctrl Pts',(-100.596882364636,3.24692973046774,127.107678526709));
#98598=CARTESIAN_POINT('Ctrl Pts',(-100.604628697901,3.14248992606727,127.018497693296));
#98599=CARTESIAN_POINT('Ctrl Pts',(-100.612375031167,3.03453490885772,126.93385923539));
#98600=CARTESIAN_POINT('Ctrl Pts',(-100.62012309917,2.92655571587073,126.849201823289));
#98601=CARTESIAN_POINT('Ctrl Pts',(-100.627871167173,2.81506005124071,126.76908905205));
#98602=CARTESIAN_POINT('Ctrl Pts',(-100.635619235176,2.70047462248842,126.693810791108));
#98603=CARTESIAN_POINT('Ctrl Pts',(-100.643375537918,2.58576741097871,126.618452523534));
#98604=CARTESIAN_POINT('Ctrl Pts',(-100.651131840659,2.46796420280636,126.547939245325));
#98605=CARTESIAN_POINT('Ctrl Pts',(-100.658888143401,2.34751918009664,126.482516478593));
#98606=CARTESIAN_POINT('Ctrl Pts',(-100.666648585915,2.22700987225176,126.41705879376));
#98607=CARTESIAN_POINT('Ctrl Pts',(-100.67440902843,2.10385629118612,126.356697206158));
#98608=CARTESIAN_POINT('Ctrl Pts',(-100.682169470944,1.97853420425474,126.301629727862));
#98609=CARTESIAN_POINT('Ctrl Pts',(-100.689942371209,1.85301093918384,126.246473850361));
#98610=CARTESIAN_POINT('Ctrl Pts',(-100.697715271475,1.72531257635716,126.196629207267));
#98611=CARTESIAN_POINT('Ctrl Pts',(-100.70548817174,1.59593255400286,126.152244717723));
#98612=CARTESIAN_POINT('Ctrl Pts',(-100.712978507502,1.4712558213501,126.109473716172));
#98613=CARTESIAN_POINT('Ctrl Pts',(-100.720468843264,1.34501786672497,126.071772867811));
#98614=CARTESIAN_POINT('Ctrl Pts',(-100.727959179026,1.21766875197736,126.039230412319));
#98615=CARTESIAN_POINT('Ctrl Pts',(-100.735733513145,1.08549115683662,126.005454099735));
#98616=CARTESIAN_POINT('Ctrl Pts',(-100.743507847264,0.95169778010567,125.977128069385));
#98617=CARTESIAN_POINT('Ctrl Pts',(-100.751282181383,0.81677781592988,125.954406281502));
#98618=CARTESIAN_POINT('Ctrl Pts',(-100.759046934331,0.682024128552159,
125.931712496192));
#98619=CARTESIAN_POINT('Ctrl Pts',(-100.766811687278,0.546146998103354,
125.914609275325));
#98620=CARTESIAN_POINT('Ctrl Pts',(-100.774576440225,0.409649706657167,
125.903200532409));
#98621=CARTESIAN_POINT('Ctrl Pts',(-100.78233348111,0.273287986245119,125.891803120818));
#98622=CARTESIAN_POINT('Ctrl Pts',(-100.790090521995,0.136307717694797,
125.886088964163));
#98623=CARTESIAN_POINT('Ctrl Pts',(-100.79784756288,-0.000779070869449877,
125.88611067927));
#98624=CARTESIAN_POINT('Ctrl Pts',(-100.80559875412,-0.137762481220248,
125.886132378001));
#98625=CARTESIAN_POINT('Ctrl Pts',(-100.81334994536,-0.274851862314551,
125.891881338856));
#98626=CARTESIAN_POINT('Ctrl Pts',(-100.8211011366,-0.41153188584531,125.903358213013));
#98627=CARTESIAN_POINT('Ctrl Pts',(-100.828849033377,-0.548153816719824,
125.914830209193));
#98628=CARTESIAN_POINT('Ctrl Pts',(-100.836596930154,-0.684366347300932,
125.932025243963));
#98629=CARTESIAN_POINT('Ctrl Pts',(-100.844344826931,-0.819656197013348,
125.954891906336));
#98630=CARTESIAN_POINT('Ctrl Pts',(-100.852091103016,-0.954917747005717,
125.977753785497));
#98631=CARTESIAN_POINT('Ctrl Pts',(-100.8598373791,-1.08925661477345,126.006284867366));
#98632=CARTESIAN_POINT('Ctrl Pts',(-100.867583655184,-1.22216707109371,
126.040382163287));
#98633=CARTESIAN_POINT('Ctrl Pts',(-100.875329988449,-1.35507850852894,
126.074479710907));
#98634=CARTESIAN_POINT('Ctrl Pts',(-100.883076321715,-1.48656113477474,
126.114143457415));
#98635=CARTESIAN_POINT('Ctrl Pts',(-100.89082265498,-1.61612219024604,126.159219916931));
#98636=CARTESIAN_POINT('Ctrl Pts',(-100.898570722983,-1.74571226001758,
126.204306471008));
#98637=CARTESIAN_POINT('Ctrl Pts',(-100.906318790986,-1.87337953353842,
126.254808021665));
#98638=CARTESIAN_POINT('Ctrl Pts',(-100.914066858989,-1.99864948960598,
126.310522249289));
#98639=CARTESIAN_POINT('Ctrl Pts',(-100.921823161731,-2.12405258407306,
126.366295690657));
#98640=CARTESIAN_POINT('Ctrl Pts',(-100.929579464473,-2.24705291358996,
126.427292716799));
#98641=CARTESIAN_POINT('Ctrl Pts',(-100.937335767215,-2.36719841691857,
126.493263922125));
#98642=CARTESIAN_POINT('Ctrl Pts',(-100.945096209729,-2.48740804552015,
126.559270338271));
#98643=CARTESIAN_POINT('Ctrl Pts',(-100.952856652243,-2.60475947745769,
126.6302560214));
#98644=CARTESIAN_POINT('Ctrl Pts',(-100.960617094757,-2.71882895568887,
126.705927725324));
#98645=CARTESIAN_POINT('Ctrl Pts',(-100.968389995023,-2.83308154837312,
126.781720904186));
#98646=CARTESIAN_POINT('Ctrl Pts',(-100.976162895288,-2.94404134259594,
126.862214906322));
#98647=CARTESIAN_POINT('Ctrl Pts',(-100.983935795553,-3.05131633304839,
126.947075082611));
#98648=CARTESIAN_POINT('Ctrl Pts',(-100.991426131315,-3.15469160738822,
127.028850377742));
#98649=CARTESIAN_POINT('Ctrl Pts',(-100.998916467077,-3.25464509686574,
127.11467971478));
#98650=CARTESIAN_POINT('Ctrl Pts',(-101.00640680284,-3.35085929351795,127.204232139644));
#98651=CARTESIAN_POINT('Ctrl Pts',(-101.01406385016,-3.44921491869811,127.295777722733));
#98652=CARTESIAN_POINT('Ctrl Pts',(-101.021720897481,-3.54399429620978,
127.391522944431));
#98653=CARTESIAN_POINT('Ctrl Pts',(-101.029377944801,-3.6348092257146,127.491152964074));
#98654=CARTESIAN_POINT('Ctrl Pts',(-101.037026122495,-3.7255189587235,127.590667576161));
#98655=CARTESIAN_POINT('Ctrl Pts',(-101.044674300189,-3.81227310359175,
127.694057745953));
#98656=CARTESIAN_POINT('Ctrl Pts',(-101.052322477882,-3.89471732244525,
127.8009691944));
#98657=CARTESIAN_POINT('Ctrl Pts',(-101.059963570359,-3.97708516556853,
127.907781600852));
#98658=CARTESIAN_POINT('Ctrl Pts',(-101.067604662836,-4.055150776805,128.018108482406));
#98659=CARTESIAN_POINT('Ctrl Pts',(-101.075245755313,-4.12859782843107,
128.131560020145));
#98660=CARTESIAN_POINT('Ctrl Pts',(-101.082881533129,-4.20199379492717,
128.244932648161));
#98661=CARTESIAN_POINT('Ctrl Pts',(-101.090517310945,-4.27077737290134,
128.361425272055));
#98662=CARTESIAN_POINT('Ctrl Pts',(-101.09815308876,-4.33467393107329,128.48061687658));
#98663=CARTESIAN_POINT('Ctrl Pts',(-101.105785602063,-4.39854317164236,
128.599757523291));
#98664=CARTESIAN_POINT('Ctrl Pts',(-101.113418115366,-4.4575293583208,128.721594500147));
#98665=CARTESIAN_POINT('Ctrl Pts',(-101.121050628668,-4.51140270703491,
128.84568027676));
#98666=CARTESIAN_POINT('Ctrl Pts',(-101.128683508868,-4.56527864545375,
128.969772018207));
#98667=CARTESIAN_POINT('Ctrl Pts',(-101.136316389067,-4.61404108335767,
129.096112409849));
#98668=CARTESIAN_POINT('Ctrl Pts',(-101.143949269266,-4.65750759204066,
129.224232112481));
#98669=CARTESIAN_POINT('Ctrl Pts',(-101.150981398493,-4.69755303990952,
129.342268067705));
#98670=CARTESIAN_POINT('Ctrl Pts',(-101.158013527721,-4.73310382814636,
129.461813809409));
#98671=CARTESIAN_POINT('Ctrl Pts',(-101.165045656948,-4.76405452823419,
129.582490119309));
#98672=CARTESIAN_POINT('Ctrl Pts',(-99.4153986790351,-4.76405452823397,
129.582490119308));
#98673=CARTESIAN_POINT('Ctrl Pts',(-99.4234124993472,-4.79925163865272,
129.71972311864));
#98674=CARTESIAN_POINT('Ctrl Pts',(-99.4314263196594,-4.82854706849966,
129.858603556017));
#98675=CARTESIAN_POINT('Ctrl Pts',(-99.4394401399715,-4.85179721396206,
129.998602057518));
#98676=CARTESIAN_POINT('Ctrl Pts',(-99.4474441489718,-4.87501889429581,
130.138429159002));
#98677=CARTESIAN_POINT('Ctrl Pts',(-99.455448157972,-4.89220998763033,130.279371249564));
#98678=CARTESIAN_POINT('Ctrl Pts',(-99.4634521669723,-4.90327761995071,
130.420887483969));
#98679=CARTESIAN_POINT('Ctrl Pts',(-99.4706816326513,-4.91327424389314,
130.548709274227));
#98680=CARTESIAN_POINT('Ctrl Pts',(-99.4779110983303,-4.91827578707414,
130.676999116505));
#98681=CARTESIAN_POINT('Ctrl Pts',(-99.4851405640093,-4.91824989996949,
130.805352560176));
#98682=CARTESIAN_POINT('',(-99.1398594360355,-4.91824791462173,130.799831509598));
#98683=CARTESIAN_POINT('Ctrl Pts',(-99.0698920977623,-4.76405452823408,
129.582490119308));
#98684=CARTESIAN_POINT('Ctrl Pts',(-99.0722155426109,-4.77419310704967,
129.622020284236));
#98685=CARTESIAN_POINT('Ctrl Pts',(-99.0745389874596,-4.78383510064487,
129.661658926553));
#98686=CARTESIAN_POINT('Ctrl Pts',(-99.0768624323083,-4.79297865804362,
129.701392510122));
#98687=CARTESIAN_POINT('Ctrl Pts',(-99.0873847719171,-4.8343876961091,129.881336639384));
#98688=CARTESIAN_POINT('Ctrl Pts',(-99.0979071115259,-4.86567686657927,
130.063689892457));
#98689=CARTESIAN_POINT('Ctrl Pts',(-99.1084294511346,-4.88662244155525,
130.247490636162));
#98690=CARTESIAN_POINT('Ctrl Pts',(-99.1189061127537,-4.90747709076822,
130.43049349187));
#98691=CARTESIAN_POINT('Ctrl Pts',(-99.1293827743728,-4.91807764454407,
130.614931896228));
#98692=CARTESIAN_POINT('Ctrl Pts',(-99.1398594359919,-4.91824791462102,
130.799831508829));
#98693=CARTESIAN_POINT('Ctrl Pts',(-99.1398594360355,-4.91824791462173,
130.799831509599));
#98694=CARTESIAN_POINT('Ctrl Pts',(-99.1475138473507,-4.91837231655715,
130.934922031593));
#98695=CARTESIAN_POINT('Ctrl Pts',(-99.1551682586658,-4.91292669612711,
131.070175337922));
#98696=CARTESIAN_POINT('Ctrl Pts',(-99.162822669981,-4.90189763815913,131.205088215205));
#98697=CARTESIAN_POINT('Ctrl Pts',(-99.1708429777369,-4.8903413687717,131.346450202625));
#98698=CARTESIAN_POINT('Ctrl Pts',(-99.1788632854928,-4.87265462096077,
131.48743796528));
#98699=CARTESIAN_POINT('Ctrl Pts',(-99.1868835932486,-4.84888341719431,
131.627472195032));
#98700=CARTESIAN_POINT('Ctrl Pts',(-99.1945292598886,-4.82622260352458,
131.760965206953));
#98701=CARTESIAN_POINT('Ctrl Pts',(-99.2021749265287,-4.7980329603097,131.893591305512));
#98702=CARTESIAN_POINT('Ctrl Pts',(-99.2098205931686,-4.76440737574616,
132.02485454235));
#98703=CARTESIAN_POINT('Ctrl Pts',(-99.2174650551137,-4.73078708942197,
132.156097096602));
#98704=CARTESIAN_POINT('Ctrl Pts',(-99.2251095170586,-4.69173266446441,
132.285976826505));
#98705=CARTESIAN_POINT('Ctrl Pts',(-99.2327539790036,-4.64738770754741,
132.414009821038));
#98706=CARTESIAN_POINT('Ctrl Pts',(-99.2403989952572,-4.60303953512731,
132.542052099388));
#98707=CARTESIAN_POINT('Ctrl Pts',(-99.2480440115109,-4.55340019985477,
132.668246996029));
#98708=CARTESIAN_POINT('Ctrl Pts',(-99.2556890277645,-4.49866241804575,
132.792128086603));
#98709=CARTESIAN_POINT('Ctrl Pts',(-99.2633363575497,-4.44390807151249,
132.91604666602));
#98710=CARTESIAN_POINT('Ctrl Pts',(-99.2709836873348,-4.38405237314869,
133.03764967938));
#98711=CARTESIAN_POINT('Ctrl Pts',(-99.27863101712,-4.31933494023983,133.156493423452));
#98712=CARTESIAN_POINT('Ctrl Pts',(-99.2862865694172,-4.25454792227538,
133.275464949918));
#98713=CARTESIAN_POINT('Ctrl Pts',(-99.2939421217144,-4.18488892867429,
133.391670932161));
#98714=CARTESIAN_POINT('Ctrl Pts',(-99.3015976740116,-4.11064217079655,
133.504694672117));
#98715=CARTESIAN_POINT('Ctrl Pts',(-99.3092580406042,-4.0363487218619,133.617789488549));
#98716=CARTESIAN_POINT('Ctrl Pts',(-99.3169184071968,-3.95746199965463,
133.727697753534));
#98717=CARTESIAN_POINT('Ctrl Pts',(-99.3245787737895,-3.87430697435425,
133.834035275177));
#98718=CARTESIAN_POINT('Ctrl Pts',(-99.3322500063426,-3.79103399657552,
133.940523632854));
#98719=CARTESIAN_POINT('Ctrl Pts',(-99.3399212388958,-3.70348089295842,
134.043430834714));
#98720=CARTESIAN_POINT('Ctrl Pts',(-99.347592471449,-3.61201015730344,134.142408802664));
#98721=CARTESIAN_POINT('Ctrl Pts',(-99.3501649996731,-3.58133567995954,
134.175600811165));
#98722=CARTESIAN_POINT('Ctrl Pts',(-99.3527375278972,-3.55022091423936,
134.208351277801));
#98723=CARTESIAN_POINT('Ctrl Pts',(-99.3553100561213,-3.51868034615613,
134.240648103222));
#98724=CARTESIAN_POINT('Ctrl Pts',(-99.3630843902404,-3.42336286342179,
134.338251040852));
#98725=CARTESIAN_POINT('Ctrl Pts',(-99.3708587243596,-3.32383028739127,
134.43203962204));
#98726=CARTESIAN_POINT('Ctrl Pts',(-99.3786330584786,-3.22042033090212,
134.521627887324));
#98727=CARTESIAN_POINT('Ctrl Pts',(-99.3863978114257,-3.11713781794233,
134.611105743078));
#98728=CARTESIAN_POINT('Ctrl Pts',(-99.3941625643728,-3.00998772502323,
134.696393329106));
#98729=CARTESIAN_POINT('Ctrl Pts',(-99.4019273173199,-2.89934583014384,
134.777140100463));
#98730=CARTESIAN_POINT('Ctrl Pts',(-99.4096843582049,-2.78881382635423,
134.857806672988));
#98731=CARTESIAN_POINT('Ctrl Pts',(-99.4174413990899,-2.67479723605721,
134.933941176963));
#98732=CARTESIAN_POINT('Ctrl Pts',(-99.4251984399749,-2.55770599034775,
135.005232328228));
#98733=CARTESIAN_POINT('Ctrl Pts',(-99.432949631215,-2.44070304405735,135.076469718281));
#98734=CARTESIAN_POINT('Ctrl Pts',(-99.4407008224552,-2.32063039001773,
135.142870823028));
#98735=CARTESIAN_POINT('Ctrl Pts',(-99.4484520136953,-2.19792780931666,
135.204167023254));
#98736=CARTESIAN_POINT('Ctrl Pts',(-99.4561999104724,-2.07527738048576,
135.265437170959));
#98737=CARTESIAN_POINT('Ctrl Pts',(-99.4639478072495,-1.94999959721095,
135.321606555199));
#98738=CARTESIAN_POINT('Ctrl Pts',(-99.4716957040266,-1.82255957335685,
135.372452086009));
#98739=CARTESIAN_POINT('Ctrl Pts',(-99.4794419801107,-1.69514620720846,
135.423286981031));
#98740=CARTESIAN_POINT('Ctrl Pts',(-99.4871882561947,-1.56557186301867,
135.468800092917));
#98741=CARTESIAN_POINT('Ctrl Pts',(-99.4949345322788,-1.43432203499653,
135.508816310037));
#98742=CARTESIAN_POINT('Ctrl Pts',(-99.5026808655442,-1.30307123811817,
135.548832822548));
#98743=CARTESIAN_POINT('Ctrl Pts',(-99.5104271988096,-1.17014530669805,
135.583352245306));
#98744=CARTESIAN_POINT('Ctrl Pts',(-99.5181735320749,-1.03604492573959,
135.612249340732));
#98745=CARTESIAN_POINT('Ctrl Pts',(-99.5259216000778,-0.901914513931145,
135.641152907462));
#98746=CARTESIAN_POINT('Ctrl Pts',(-99.5336696680808,-0.766609511344383,
135.664431559092));
#98747=CARTESIAN_POINT('Ctrl Pts',(-99.5414177360837,-0.630640428654262,
135.682011252067));
#98748=CARTESIAN_POINT('Ctrl Pts',(-99.5491740388256,-0.494526836404078,
135.699609628948));
#98749=CARTESIAN_POINT('Ctrl Pts',(-99.5569303415675,-0.357748142510617,
135.711496897611));
#98750=CARTESIAN_POINT('Ctrl Pts',(-99.5646866443093,-0.220820168700871,
135.717650911818));
#98751=CARTESIAN_POINT('Ctrl Pts',(-99.5724470868235,-0.0838191123086806,
135.723808210609));
#98752=CARTESIAN_POINT('Ctrl Pts',(-99.5802075293377,0.0533309919872466,
135.724226156423));
#98753=CARTESIAN_POINT('Ctrl Pts',(-99.5879679718518,0.190115690891329,
135.718934768658));
#98754=CARTESIAN_POINT('Ctrl Pts',(-99.5957408721173,0.327119968737268,
135.713634886687));
#98755=CARTESIAN_POINT('Ctrl Pts',(-99.6035137723827,0.46375727909287,135.702607387757));
#98756=CARTESIAN_POINT('Ctrl Pts',(-99.6112866726481,0.599518749511796,
135.685934168326));
#98757=CARTESIAN_POINT('Ctrl Pts',(-99.6187770084102,0.730344948519594,
135.66986706242));
#98758=CARTESIAN_POINT('Ctrl Pts',(-99.6262673441724,0.860357576060504,
135.648557631752));
#98759=CARTESIAN_POINT('Ctrl Pts',(-99.6337576799345,0.989113306761833,
135.622123368977));
#98760=CARTESIAN_POINT('Ctrl Pts',(-99.6415320140535,1.12275085012585,135.594686843095));
#98761=CARTESIAN_POINT('Ctrl Pts',(-99.6493063481726,1.2554576282722,135.561642287017));
#98762=CARTESIAN_POINT('Ctrl Pts',(-99.6570806822917,1.38672638053822,135.523065207601));
#98763=CARTESIAN_POINT('Ctrl Pts',(-99.6648454352388,1.5178333557989,135.484535670988));
#98764=CARTESIAN_POINT('Ctrl Pts',(-99.6726101881859,1.64750545990355,135.440487286681));
#98765=CARTESIAN_POINT('Ctrl Pts',(-99.680374941133,1.77524465227443,135.391046729245));
#98766=CARTESIAN_POINT('Ctrl Pts',(-99.688131982018,1.90285697227898,135.341655276868));
#98767=CARTESIAN_POINT('Ctrl Pts',(-99.695889022903,2.02853983877989,135.286882449421));
#98768=CARTESIAN_POINT('Ctrl Pts',(-99.7036460637881,2.15180978182806,135.22690487685));
#98769=CARTESIAN_POINT('Ctrl Pts',(-99.7113972550282,2.27498676605311,135.166972533834));
#98770=CARTESIAN_POINT('Ctrl Pts',(-99.7191484462683,2.39575409849983,135.101843428409));
#98771=CARTESIAN_POINT('Ctrl Pts',(-99.7268996375084,2.51364806979434,135.031742365613));
#98772=CARTESIAN_POINT('Ctrl Pts',(-99.7346475342855,2.63149193300629,134.961671097638));
#98773=CARTESIAN_POINT('Ctrl Pts',(-99.7423954310626,2.74646452870675,134.886632274712));
#98774=CARTESIAN_POINT('Ctrl Pts',(-99.7501433278397,2.85812675958685,134.806896624729));
#98775=CARTESIAN_POINT('Ctrl Pts',(-99.7578896039238,2.96976563313541,134.727177653724));
#98776=CARTESIAN_POINT('Ctrl Pts',(-99.7656358800078,3.07809520122745,134.642764036915));
#98777=CARTESIAN_POINT('Ctrl Pts',(-99.773382156092,3.18270571601008,134.553969582215));
#98778=CARTESIAN_POINT('Ctrl Pts',(-99.7811284893573,3.28731700300333,134.465174472055));
#98779=CARTESIAN_POINT('Ctrl Pts',(-99.7888748226226,3.3882088838396,134.371998712478));
#98780=CARTESIAN_POINT('Ctrl Pts',(-99.7966211558879,3.48500536012169,134.274795849986));
#98781=CARTESIAN_POINT('Ctrl Pts',(-99.8043692238909,3.58182351330364,134.177571219587));
#98782=CARTESIAN_POINT('Ctrl Pts',(-99.812117291894,3.67454416111241,134.076317968692));
#98783=CARTESIAN_POINT('Ctrl Pts',(-99.819865359897,3.7628290651184,133.97142558204));
#98784=CARTESIAN_POINT('Ctrl Pts',(-99.8276216626388,3.85120779937109,133.866421714512));
#98785=CARTESIAN_POINT('Ctrl Pts',(-99.8353779653807,3.93514112021633,133.75777128464));
#98786=CARTESIAN_POINT('Ctrl Pts',(-99.8431342681226,4.01433158115551,133.645896297271));
#98787=CARTESIAN_POINT('Ctrl Pts',(-99.8508947106368,4.0935643084283,133.533961598853));
#98788=CARTESIAN_POINT('Ctrl Pts',(-99.8586551531509,4.16804891952822,133.418799241737));
#98789=CARTESIAN_POINT('Ctrl Pts',(-99.8664155956651,4.23753259605088,133.300858276268));
#98790=CARTESIAN_POINT('Ctrl Pts',(-99.8741884959306,4.30712781393937,133.182727981492));
#98791=CARTESIAN_POINT('Ctrl Pts',(-99.881961396196,4.37170587057351,133.061810509987));
#98792=CARTESIAN_POINT('Ctrl Pts',(-99.8897342964615,4.43106060977608,132.93857825759));
#98793=CARTESIAN_POINT('Ctrl Pts',(-99.8972246322234,4.48825765470259,132.819825807973));
#98794=CARTESIAN_POINT('Ctrl Pts',(-99.9047149679853,4.54060442808771,132.698924234489));
#98795=CARTESIAN_POINT('Ctrl Pts',(-99.9122053037473,4.58796015163464,132.576310026977));
#98796=CARTESIAN_POINT('Ctrl Pts',(-99.9199796378664,4.63711138183367,132.449046864519));
#98797=CARTESIAN_POINT('Ctrl Pts',(-99.9277539719854,4.68104131606582,132.319535503895));
#98798=CARTESIAN_POINT('Ctrl Pts',(-99.9355283061045,4.71953929361126,132.188243531168));
#98799=CARTESIAN_POINT('Ctrl Pts',(-99.9432930590516,4.75798982583993,132.057113364064));
#98800=CARTESIAN_POINT('Ctrl Pts',(-99.9510578119986,4.7910216122923,131.924207322716));
#98801=CARTESIAN_POINT('Ctrl Pts',(-99.9588225649457,4.81847202477224,131.790012893466));
#98802=CARTESIAN_POINT('Ctrl Pts',(-99.9665796058306,4.84589517311553,131.655951748015));
#98803=CARTESIAN_POINT('Ctrl Pts',(-99.9743366467156,4.86774790145498,131.520605141769));
#98804=CARTESIAN_POINT('Ctrl Pts',(-99.9820936876006,4.88391748625177,131.384475304489));
#98805=CARTESIAN_POINT('Ctrl Pts',(-99.9898448788407,4.9000748774389,131.248448123779));
#98806=CARTESIAN_POINT('Ctrl Pts',(-99.9975960700808,4.91055760958646,131.111639274334));
#98807=CARTESIAN_POINT('Ctrl Pts',(-100.005347261321,4.91530417129558,130.974560400598));
#98808=CARTESIAN_POINT('Ctrl Pts',(-100.013095158098,4.92004871558936,130.837539789041));
#98809=CARTESIAN_POINT('Ctrl Pts',(-100.020843054875,4.91906192499011,130.700249771369));
#98810=CARTESIAN_POINT('Ctrl Pts',(-100.028590951652,4.91233422772049,130.563206107623));
#98811=CARTESIAN_POINT('Ctrl Pts',(-100.036337227736,4.90560793774011,130.426191110458));
#98812=CARTESIAN_POINT('Ctrl Pts',(-100.04408350382,4.89314314885131,130.289422754967));
#98813=CARTESIAN_POINT('Ctrl Pts',(-100.051829779904,4.87498239781686,130.153415394467));
#98814=CARTESIAN_POINT('Ctrl Pts',(-100.05957611317,4.85682151272385,130.017407029991));
#98815=CARTESIAN_POINT('Ctrl Pts',(-100.067322446435,4.83296463333027,129.88216005924));
#98816=CARTESIAN_POINT('Ctrl Pts',(-100.075068779701,4.80350597200363,129.748181920836));
#98817=CARTESIAN_POINT('Ctrl Pts',(-100.082816847703,4.77404071361408,129.614173778957));
#98818=CARTESIAN_POINT('Ctrl Pts',(-100.090564915706,4.73897126096355,129.481435416614));
#98819=CARTESIAN_POINT('Ctrl Pts',(-100.098312983709,4.6984424724607,129.350461929391));
#98820=CARTESIAN_POINT('Ctrl Pts',(-100.106069286451,4.65787060947907,129.219349241987));
#98821=CARTESIAN_POINT('Ctrl Pts',(-100.113825589193,4.61182793579019,129.090005550765));
#98822=CARTESIAN_POINT('Ctrl Pts',(-100.121581891935,4.56050871892502,128.962909209815));
#98823=CARTESIAN_POINT('Ctrl Pts',(-100.129342334449,4.50916211144861,128.835745033721));
#98824=CARTESIAN_POINT('Ctrl Pts',(-100.137102776963,4.45253351052727,128.710830953871));
#98825=CARTESIAN_POINT('Ctrl Pts',(-100.144863219478,4.39086406041055,128.588622396229));
#98826=CARTESIAN_POINT('Ctrl Pts',(-100.152636119743,4.32909561301774,128.46621765856));
#98827=CARTESIAN_POINT('Ctrl Pts',(-100.160409020008,4.26227033669737,128.346527463646));
#98828=CARTESIAN_POINT('Ctrl Pts',(-100.168181920274,4.1906742389969,128.229980598006));
#98829=CARTESIAN_POINT('Ctrl Pts',(-100.175672256036,4.12168083978695,128.117670504495));
#98830=CARTESIAN_POINT('Ctrl Pts',(-100.183162591798,4.04825763155853,128.008279427853));
#98831=CARTESIAN_POINT('Ctrl Pts',(-100.19065292756,3.9706957514681,127.902161742269));
#98832=CARTESIAN_POINT('Ctrl Pts',(-100.198427261679,3.89019308912041,127.792020572384));
#98833=CARTESIAN_POINT('Ctrl Pts',(-100.206201595798,3.80497671597569,127.685057020646));
#98834=CARTESIAN_POINT('Ctrl Pts',(-100.213975929917,3.71532615816712,127.581701063574));
#98835=CARTESIAN_POINT('Ctrl Pts',(-100.221740682864,3.62578608665876,127.478472483481));
#98836=CARTESIAN_POINT('Ctrl Pts',(-100.229505435811,3.53182295740176,127.378842944271));
#98837=CARTESIAN_POINT('Ctrl Pts',(-100.237270188759,3.43375900194902,127.283212767925));
#98838=CARTESIAN_POINT('Ctrl Pts',(-100.245027229644,3.33579244499904,127.187677572817));
#98839=CARTESIAN_POINT('Ctrl Pts',(-100.252784270529,3.23373344539835,127.096134106863));
#98840=CARTESIAN_POINT('Ctrl Pts',(-100.260541311414,3.1279436134437,127.008948675021));
#98841=CARTESIAN_POINT('Ctrl Pts',(-100.268292502654,3.02223355842469,126.921828990391));
#98842=CARTESIAN_POINT('Ctrl Pts',(-100.276043693894,2.91279857153971,126.839061046082));
#98843=CARTESIAN_POINT('Ctrl Pts',(-100.283794885134,2.80003586533546,126.760973149695));
#98844=CARTESIAN_POINT('Ctrl Pts',(-100.291542781911,2.68732108628953,126.682918442747));
#98845=CARTESIAN_POINT('Ctrl Pts',(-100.299290678688,2.57128172174446,126.609540049579));
#98846=CARTESIAN_POINT('Ctrl Pts',(-100.307038575465,2.45234652145019,126.541124804099));
#98847=CARTESIAN_POINT('Ctrl Pts',(-100.314784851549,2.33343619983524,126.472723869612));
#98848=CARTESIAN_POINT('Ctrl Pts',(-100.322531127633,2.2116315860155,126.40928421263));
#98849=CARTESIAN_POINT('Ctrl Pts',(-100.330277403718,2.08738841216248,126.351048066299));
#98850=CARTESIAN_POINT('Ctrl Pts',(-100.338023736983,1.96314432117509,126.292811490083));
#98851=CARTESIAN_POINT('Ctrl Pts',(-100.345770070248,1.83646198824102,126.239778667097));
#98852=CARTESIAN_POINT('Ctrl Pts',(-100.353516403513,1.70781925992925,126.192144616779));
#98853=CARTESIAN_POINT('Ctrl Pts',(-100.361264471516,1.57914772297059,126.144499899146));
#98854=CARTESIAN_POINT('Ctrl Pts',(-100.369012539519,1.44851528360887,126.102256495718));
#98855=CARTESIAN_POINT('Ctrl Pts',(-100.376760607522,1.31641677929023,126.065560144271));
#98856=CARTESIAN_POINT('Ctrl Pts',(-100.384516910264,1.18417787910866,126.028824791505));
#98857=CARTESIAN_POINT('Ctrl Pts',(-100.392273213006,1.05047017869606,125.997648372375));
#98858=CARTESIAN_POINT('Ctrl Pts',(-100.400029515748,0.915801137242447,
125.972126006175));
#98859=CARTESIAN_POINT('Ctrl Pts',(-100.407789958262,0.781060218866975,
125.94659001792));
#98860=CARTESIAN_POINT('Ctrl Pts',(-100.415550400776,0.645357323710639,
125.926714152326));
#98861=CARTESIAN_POINT('Ctrl Pts',(-100.42331084329,0.509205958892165,125.912541696763));
#98862=CARTESIAN_POINT('Ctrl Pts',(-100.431083743556,0.372836031815564,
125.898346490316));
#98863=CARTESIAN_POINT('Ctrl Pts',(-100.438856643821,0.236016586882788,
125.889873013928));
#98864=CARTESIAN_POINT('Ctrl Pts',(-100.446629544087,0.0992629684021214,
125.887112410936));
#98865=CARTESIAN_POINT('Ctrl Pts',(-100.454119879849,-0.0325193115866818,
125.884452162817));
#98866=CARTESIAN_POINT('Ctrl Pts',(-100.461610215611,-0.164240159991098,
125.887096638402));
#98867=CARTESIAN_POINT('Ctrl Pts',(-100.469100551373,-0.295444065025355,
125.894992443662));
#98868=CARTESIAN_POINT('Ctrl Pts',(-100.476874885492,-0.431622605996199,
125.903187620778));
#98869=CARTESIAN_POINT('Ctrl Pts',(-100.484649219611,-0.567675602649322,
125.917066156513));
#98870=CARTESIAN_POINT('Ctrl Pts',(-100.49242355373,-0.703090212859308,
125.936625290427));
#98871=CARTESIAN_POINT('Ctrl Pts',(-100.500188306677,-0.838337936663458,
125.956160319455));
#98872=CARTESIAN_POINT('Ctrl Pts',(-100.507953059624,-0.972948456195941,
125.981361961743));
#98873=CARTESIAN_POINT('Ctrl Pts',(-100.515717812571,-1.10641079521007,
126.012175498568));
#98874=CARTESIAN_POINT('Ctrl Pts',(-100.523474853456,-1.23974057754796,
126.042958430955));
#98875=CARTESIAN_POINT('Ctrl Pts',(-100.531231894341,-1.37192407031433,
126.079342078358));
#98876=CARTESIAN_POINT('Ctrl Pts',(-100.538988935226,-1.50245763157392,
126.121220204571));
#98877=CARTESIAN_POINT('Ctrl Pts',(-100.546740126466,-1.63289275645972,
126.163066750164));
#98878=CARTESIAN_POINT('Ctrl Pts',(-100.554491317707,-1.76168005562612,
126.210399408372));
#98879=CARTESIAN_POINT('Ctrl Pts',(-100.562242508947,-1.88832861150635,
126.263061451307));
#98880=CARTESIAN_POINT('Ctrl Pts',(-100.569990405724,-2.01492333837238,
126.315701111469));
#98881=CARTESIAN_POINT('Ctrl Pts',(-100.577738302501,-2.13938076968501,
126.373665501392));
#98882=CARTESIAN_POINT('Ctrl Pts',(-100.585486199278,-2.26122783424161,
126.436748942503));
#98883=CARTESIAN_POINT('Ctrl Pts',(-100.593232475362,-2.38304941101935,
126.499819187917));
#98884=CARTESIAN_POINT('Ctrl Pts',(-100.600978751446,-2.50226136015605,
126.568006175011));
#98885=CARTESIAN_POINT('Ctrl Pts',(-100.60872502753,-2.61841354967332,126.641057416334));
#98886=CARTESIAN_POINT('Ctrl Pts',(-100.616471360796,-2.73456659659919,
126.714109196905));
#98887=CARTESIAN_POINT('Ctrl Pts',(-100.624217694061,-2.84765950788361,
126.79202509521));
#98888=CARTESIAN_POINT('Ctrl Pts',(-100.631964027326,-2.95726992040894,
126.874508498167));
#98889=CARTESIAN_POINT('Ctrl Pts',(-100.639712095329,-3.06690487942601,
126.95701037271));
#98890=CARTESIAN_POINT('Ctrl Pts',(-100.647460163332,-3.17305547547524,
127.044081552243));
#98891=CARTESIAN_POINT('Ctrl Pts',(-100.655208231335,-3.27533162351188,
127.135384490835));
#98892=CARTESIAN_POINT('Ctrl Pts',(-100.662964534077,-3.37771647185616,
127.226784467277));
#98893=CARTESIAN_POINT('Ctrl Pts',(-100.670720836819,-3.47621835429782,
127.322424926367));
#98894=CARTESIAN_POINT('Ctrl Pts',(-100.678477139561,-3.57048295019262,
127.421930342618));
#98895=CARTESIAN_POINT('Ctrl Pts',(-100.686237582075,-3.66479785794024,
127.521488867906));
#98896=CARTESIAN_POINT('Ctrl Pts',(-100.693998024589,-3.75487071613825,
127.624916166058));
#98897=CARTESIAN_POINT('Ctrl Pts',(-100.701758467103,-3.84038754275462,
127.731803606874));
#98898=CARTESIAN_POINT('Ctrl Pts',(-100.709531367369,-3.92604164857291,
127.838862632898));
#98899=CARTESIAN_POINT('Ctrl Pts',(-100.717304267634,-4.00712487622633,
127.949392585884));
#98900=CARTESIAN_POINT('Ctrl Pts',(-100.7250771679,-4.08336612088915,128.062955104827));
#98901=CARTESIAN_POINT('Ctrl Pts',(-100.732567503662,-4.15683580426816,
128.172389340159));
#98902=CARTESIAN_POINT('Ctrl Pts',(-100.740057839424,-4.22580926808501,
128.284639224097));
#98903=CARTESIAN_POINT('Ctrl Pts',(-100.747548175186,-4.29008521900273,
128.399292660897));
#98904=CARTESIAN_POINT('Ctrl Pts',(-100.755683650374,-4.3598972301696,128.523821149328));
#98905=CARTESIAN_POINT('Ctrl Pts',(-100.763819125561,-4.42437184426201,
128.651549076575));
#98906=CARTESIAN_POINT('Ctrl Pts',(-100.771954600749,-4.48321825173858,
128.782001309783));
#98907=CARTESIAN_POINT('Ctrl Pts',(-100.78007251136,-4.54193760919861,128.912171895238));
#98908=CARTESIAN_POINT('Ctrl Pts',(-100.788190421971,-4.59505284665445,
129.045054753809));
#98909=CARTESIAN_POINT('Ctrl Pts',(-100.796308332581,-4.6423186290701,129.180149791137));
#98910=CARTESIAN_POINT('Ctrl Pts',(-100.804249882031,-4.68855756496666,
129.312309896222));
#98911=CARTESIAN_POINT('Ctrl Pts',(-100.812191431481,-4.72919843798944,
129.44658675246));
#98912=CARTESIAN_POINT('Ctrl Pts',(-100.820132980931,-4.76405452823393,
129.582490119308));
#98913=CARTESIAN_POINT('Origin',(213.235140564004,0.,130.804360617566));
#98914=CARTESIAN_POINT('',(-102.915060258535,-4.76405452823397,129.582490119308));
#98915=CARTESIAN_POINT('',(-102.569791376202,-4.76405452823412,129.582490119309));
#98916=CARTESIAN_POINT('',(213.235140564004,-4.76405452823405,129.582490119308));
#98917=CARTESIAN_POINT('',(-101.235140563964,-4.91824820892467,130.808557986892));
#98918=CARTESIAN_POINT('Ctrl Pts',(-101.235140564009,-4.918248208924,130.808557987678));
#98919=CARTESIAN_POINT('Ctrl Pts',(-101.247006338631,-4.91806979539947,
131.017613175562));
#98920=CARTESIAN_POINT('Ctrl Pts',(-101.258872113253,-4.90455922343421,
131.226120353833));
#98921=CARTESIAN_POINT('Ctrl Pts',(-101.270737887874,-4.87794266429464,
131.432738232026));
#98922=CARTESIAN_POINT('Ctrl Pts',(-101.2754434008,-4.86738755372939,131.514674989427));
#98923=CARTESIAN_POINT('Ctrl Pts',(-101.280148913726,-4.85477182893646,
131.596315055863));
#98924=CARTESIAN_POINT('Ctrl Pts',(-101.284854426652,-4.84011134684747,
131.677576062126));
#98925=CARTESIAN_POINT('Ctrl Pts',(-101.292628760771,-4.81588965456829,
131.81183352215));
#98926=CARTESIAN_POINT('Ctrl Pts',(-101.30040309489,-4.78603921126845,131.945295062255));
#98927=CARTESIAN_POINT('Ctrl Pts',(-101.308177429009,-4.7506233292055,132.077451755902));
#98928=CARTESIAN_POINT('Ctrl Pts',(-101.315942181957,-4.71525109405207,
132.209445578234));
#98929=CARTESIAN_POINT('Ctrl Pts',(-101.323706934904,-4.67432716754392,
132.340137379745));
#98930=CARTESIAN_POINT('Ctrl Pts',(-101.331471687851,-4.62796623616901,
132.46902622344));
#98931=CARTESIAN_POINT('Ctrl Pts',(-101.339228728736,-4.58165135112484,
132.597787052918));
#98932=CARTESIAN_POINT('Ctrl Pts',(-101.346985769621,-4.52991033914884,
132.724748122692));
#98933=CARTESIAN_POINT('Ctrl Pts',(-101.354742810506,-4.47290817737871,
132.849421863406));
#98934=CARTESIAN_POINT('Ctrl Pts',(-101.362494001746,-4.41594900138195,
132.974001586684));
#98935=CARTESIAN_POINT('Ctrl Pts',(-101.370245192986,-4.35373673451711,
133.096297060072));
#98936=CARTESIAN_POINT('Ctrl Pts',(-101.377996384226,-4.28648498933653,
133.215839313033));
#98937=CARTESIAN_POINT('Ctrl Pts',(-101.385744281003,-4.21926182794175,
133.335330757348));
#98938=CARTESIAN_POINT('Ctrl Pts',(-101.39349217778,-4.14700363962606,133.452070968626));
#98939=CARTESIAN_POINT('Ctrl Pts',(-101.401240074557,-4.06997053719467,
133.565614479287));
#98940=CARTESIAN_POINT('Ctrl Pts',(-101.408986350641,-3.99295354842767,
133.679134239092));
#98941=CARTESIAN_POINT('Ctrl Pts',(-101.416732626726,-3.91116385159159,
133.789458304995));
#98942=CARTESIAN_POINT('Ctrl Pts',(-101.42447890281,-3.82490533141331,133.896169516613));
#98943=CARTESIAN_POINT('Ctrl Pts',(-101.432225236075,-3.7386461744941,134.002881515949));
#98944=CARTESIAN_POINT('Ctrl Pts',(-101.43997156934,-3.64791837418422,134.105980303733));
#98945=CARTESIAN_POINT('Ctrl Pts',(-101.447717902606,-3.55306635224864,
134.205081505704));
#98946=CARTESIAN_POINT('Ctrl Pts',(-101.455465970609,-3.45819308886053,
134.304204900702));
#98947=CARTESIAN_POINT('Ctrl Pts',(-101.463214038612,-3.35919403628882,
134.399328646091));
#98948=CARTESIAN_POINT('Ctrl Pts',(-101.470962106615,-3.25645045032094,
134.490105254285));
#98949=CARTESIAN_POINT('Ctrl Pts',(-101.478718409356,-3.1535976672471,134.580978340939));
#98950=CARTESIAN_POINT('Ctrl Pts',(-101.486474712098,-3.04699269428558,
134.667494801797));
#98951=CARTESIAN_POINT('Ctrl Pts',(-101.49423101484,-2.93705027685989,134.749347149064));
#98952=CARTESIAN_POINT('Ctrl Pts',(-101.501991457354,-2.82704917985571,
134.831243183393));
#98953=CARTESIAN_POINT('Ctrl Pts',(-101.509751899869,-2.71370741194373,
134.908469923798));
#98954=CARTESIAN_POINT('Ctrl Pts',(-101.517512342383,-2.59746782720842,
134.980763848711));
#98955=CARTESIAN_POINT('Ctrl Pts',(-101.525285242648,-2.48104164437242,
135.05317382625));
#98956=CARTESIAN_POINT('Ctrl Pts',(-101.533058142914,-2.3617086894097,135.120634971909));
#98957=CARTESIAN_POINT('Ctrl Pts',(-101.540831043179,-2.23993627493946,
135.182929852683));
#98958=CARTESIAN_POINT('Ctrl Pts',(-101.548321378941,-2.12259059446142,
135.242960157628));
#98959=CARTESIAN_POINT('Ctrl Pts',(-101.555811714703,-2.0029800158675,135.298193160838));
#98960=CARTESIAN_POINT('Ctrl Pts',(-101.563302050465,-1.88153752500862,
135.348477650003));
#98961=CARTESIAN_POINT('Ctrl Pts',(-101.571076384584,-1.75549050519735,
135.400668690858));
#98962=CARTESIAN_POINT('Ctrl Pts',(-101.578850718703,-1.62707063793868,
135.447693889908));
#98963=CARTESIAN_POINT('Ctrl Pts',(-101.586625052822,-1.49674031936641,
135.489331426321));
#98964=CARTESIAN_POINT('Ctrl Pts',(-101.594389805769,-1.36657062126383,
135.530917648191));
#98965=CARTESIAN_POINT('Ctrl Pts',(-101.602154558716,-1.23449552536829,
135.567129300836));
#98966=CARTESIAN_POINT('Ctrl Pts',(-101.609919311664,-1.10099847500883,
135.597792104562));
#98967=CARTESIAN_POINT('Ctrl Pts',(-101.617676352549,-0.967634015801769,
135.62842445356));
#98968=CARTESIAN_POINT('Ctrl Pts',(-101.625433393434,-0.832850791259232,
135.653518834212));
#98969=CARTESIAN_POINT('Ctrl Pts',(-101.633190434319,-0.697148181459653,
135.672950503312));
#98970=CARTESIAN_POINT('Ctrl Pts',(-101.640941625559,-0.561547906053921,
135.692367518839));
#98971=CARTESIAN_POINT('Ctrl Pts',(-101.648692816799,-0.425030010845373,
135.706130267382));
#98972=CARTESIAN_POINT('Ctrl Pts',(-101.656444008039,-0.288104516831927,
135.7141649772));
#98973=CARTESIAN_POINT('Ctrl Pts',(-101.664191904816,-0.151237219805858,
135.722196272052));
#98974=CARTESIAN_POINT('Ctrl Pts',(-101.671939801593,-0.0139630580134921,
135.724504347499));
#98975=CARTESIAN_POINT('Ctrl Pts',(-101.67968769837,0.123202586726795,135.721067257699));
#98976=CARTESIAN_POINT('Ctrl Pts',(-101.687433974454,0.260339539371152,
135.717630886864));
#98977=CARTESIAN_POINT('Ctrl Pts',(-101.695180250538,0.397367629518935,
135.708451750946));
#98978=CARTESIAN_POINT('Ctrl Pts',(-101.702926526622,0.533771631209913,
135.693560031398));
#98979=CARTESIAN_POINT('Ctrl Pts',(-101.710672859888,0.670176639804059,
135.678668201923));
#98980=CARTESIAN_POINT('Ctrl Pts',(-101.718419193153,0.805957162092814,
135.658063747102));
#98981=CARTESIAN_POINT('Ctrl Pts',(-101.726165526418,0.940603644748119,
135.631828675046));
#98982=CARTESIAN_POINT('Ctrl Pts',(-101.733913594421,1.07528028054982,135.605587727827));
#98983=CARTESIAN_POINT('Ctrl Pts',(-101.741661662424,1.2088219876912,135.573713729009));
#98984=CARTESIAN_POINT('Ctrl Pts',(-101.749409730427,1.34073033695971,135.536339614355));
#98985=CARTESIAN_POINT('Ctrl Pts',(-101.757166033169,1.47277887999138,135.498925778048));
#98986=CARTESIAN_POINT('Ctrl Pts',(-101.764922335911,1.60319022064089,135.456000255462));
#98987=CARTESIAN_POINT('Ctrl Pts',(-101.772678638653,1.73148148068647,135.407745779003));
#98988=CARTESIAN_POINT('Ctrl Pts',(-101.780439081167,1.85984121364067,135.359465547677));
#98989=CARTESIAN_POINT('Ctrl Pts',(-101.788199523681,1.98607825160179,135.305850847885));
#98990=CARTESIAN_POINT('Ctrl Pts',(-101.795959966195,2.10973151296049,135.247131825463));
#98991=CARTESIAN_POINT('Ctrl Pts',(-101.803732866461,2.23358327351175,135.188318542055));
#98992=CARTESIAN_POINT('Ctrl Pts',(-101.811505766726,2.35484262298096,135.124384744419));
#98993=CARTESIAN_POINT('Ctrl Pts',(-101.819278666992,2.47307403493597,135.055606068046));
#98994=CARTESIAN_POINT('Ctrl Pts',(-101.826769002754,2.58700743726043,134.989327669802));
#98995=CARTESIAN_POINT('Ctrl Pts',(-101.834259338516,2.69812896652249,134.918550689858));
#98996=CARTESIAN_POINT('Ctrl Pts',(-101.841749674278,2.80607736409552,134.843557677529));
#98997=CARTESIAN_POINT('Ctrl Pts',(-101.849524008397,2.91811865797165,134.765721282344));
#98998=CARTESIAN_POINT('Ctrl Pts',(-101.857298342516,3.02709636483782,134.68309627972));
#98999=CARTESIAN_POINT('Ctrl Pts',(-101.865072676635,3.13257392414164,134.595951797043));
#99000=CARTESIAN_POINT('Ctrl Pts',(-101.872837429582,3.23792149178041,134.508914712153));
#99001=CARTESIAN_POINT('Ctrl Pts',(-101.880602182529,3.33977719616249,134.417369476188));
#99002=CARTESIAN_POINT('Ctrl Pts',(-101.888366935476,3.43773309791964,134.321628621282));
#99003=CARTESIAN_POINT('Ctrl Pts',(-101.896123976361,3.53559170849424,134.225982857544));
#99004=CARTESIAN_POINT('Ctrl Pts',(-101.903881017247,3.62955794677515,134.126150039184));
#99005=CARTESIAN_POINT('Ctrl Pts',(-101.911638058132,3.71925693563923,134.022482882055));
#99006=CARTESIAN_POINT('Ctrl Pts',(-101.919389249372,3.80888828179817,133.918893901136));
#99007=CARTESIAN_POINT('Ctrl Pts',(-101.927140440612,3.8942585289241,133.81147663127));
#99008=CARTESIAN_POINT('Ctrl Pts',(-101.934891631852,3.9750299319547,133.70062029214));
#99009=CARTESIAN_POINT('Ctrl Pts',(-101.942639528629,4.05576700498424,133.589811069912));
#99010=CARTESIAN_POINT('Ctrl Pts',(-101.950387425406,4.1319088917817,133.475566000946));
#99011=CARTESIAN_POINT('Ctrl Pts',(-101.958135322183,4.20315855222879,133.358306828301));
#99012=CARTESIAN_POINT('Ctrl Pts',(-101.965881598267,4.27439330878288,133.241072183746));
#99013=CARTESIAN_POINT('Ctrl Pts',(-101.973627874351,4.34073767159088,133.120825023492));
#99014=CARTESIAN_POINT('Ctrl Pts',(-101.981374150435,4.40193854094643,132.998015135541));
#99015=CARTESIAN_POINT('Ctrl Pts',(-101.989120483701,4.46313986207299,132.875204341035));
#99016=CARTESIAN_POINT('Ctrl Pts',(-101.996866816966,4.51919743960488,132.749831131006));
#99017=CARTESIAN_POINT('Ctrl Pts',(-102.004613150232,4.56990484326638,132.622368534488));
#99018=CARTESIAN_POINT('Ctrl Pts',(-102.012361218234,4.62062360249929,132.494877393605));
#99019=CARTESIAN_POINT('Ctrl Pts',(-102.020109286237,4.66598965922242,132.365296298362));
#99020=CARTESIAN_POINT('Ctrl Pts',(-102.02785735424,4.70584544289486,132.2341164464));
#99021=CARTESIAN_POINT('Ctrl Pts',(-102.035613656982,4.74574358576852,132.102797174931));
#99022=CARTESIAN_POINT('Ctrl Pts',(-102.043369959724,4.78011964299761,131.969876127129));
#99023=CARTESIAN_POINT('Ctrl Pts',(-102.051126262466,4.80886634505797,131.835858333448));
#99024=CARTESIAN_POINT('Ctrl Pts',(-102.05888670498,4.83762839009877,131.701769010435));
#99025=CARTESIAN_POINT('Ctrl Pts',(-102.066647147494,4.86075502724483,131.56658216033));
#99026=CARTESIAN_POINT('Ctrl Pts',(-102.074407590008,4.87819065883584,131.430810103596));
#99027=CARTESIAN_POINT('Ctrl Pts',(-102.082180490274,4.89565427965054,131.294820093503));
#99028=CARTESIAN_POINT('Ctrl Pts',(-102.089953390539,4.9074086053125,131.158243389259));
#99029=CARTESIAN_POINT('Ctrl Pts',(-102.097726290805,4.91345012309112,131.021595399302));
#99030=CARTESIAN_POINT('Ctrl Pts',(-102.105216626567,4.91927201648083,130.889914907975));
#99031=CARTESIAN_POINT('Ctrl Pts',(-102.112706962329,4.91978923960662,130.7581685318));
#99032=CARTESIAN_POINT('Ctrl Pts',(-102.120197298091,4.91504424009559,130.626812932695));
#99033=CARTESIAN_POINT('Ctrl Pts',(-102.12797163221,4.91011933248587,130.490476946125));
#99034=CARTESIAN_POINT('Ctrl Pts',(-102.135745966329,4.89950969020642,130.354130082783));
#99035=CARTESIAN_POINT('Ctrl Pts',(-102.143520300448,4.88320576610674,130.218285103351));
#99036=CARTESIAN_POINT('Ctrl Pts',(-102.151285053395,4.86692193513642,130.082607540717));
#99037=CARTESIAN_POINT('Ctrl Pts',(-102.159049806342,4.84495783160567,129.947431015761));
#99038=CARTESIAN_POINT('Ctrl Pts',(-102.166814559289,4.8173558964575,129.813267670681));
#99039=CARTESIAN_POINT('Ctrl Pts',(-102.174571600174,4.78978137594045,129.679237578526));
#99040=CARTESIAN_POINT('Ctrl Pts',(-102.182328641059,4.7565802454855,129.546219044122));
#99041=CARTESIAN_POINT('Ctrl Pts',(-102.190085681944,4.71784662468719,129.414718113744));
#99042=CARTESIAN_POINT('Ctrl Pts',(-102.197836873184,4.67914221321358,129.283316349241));
#99043=CARTESIAN_POINT('Ctrl Pts',(-102.205588064425,4.63491372571621,129.153430284348));
#99044=CARTESIAN_POINT('Ctrl Pts',(-102.213339255665,4.58530606428086,129.025554456297));
#99045=CARTESIAN_POINT('Ctrl Pts',(-102.221087152442,4.53571948742489,128.897732978884));
#99046=CARTESIAN_POINT('Ctrl Pts',(-102.228835049219,4.48075842499837,128.771920402704));
#99047=CARTESIAN_POINT('Ctrl Pts',(-102.236582945996,4.42061714394063,128.648594598445));
#99048=CARTESIAN_POINT('Ctrl Pts',(-102.24432922208,4.36048844314255,128.525294591286));
#99049=CARTESIAN_POINT('Ctrl Pts',(-102.252075498164,4.29518185029251,128.404480672567));
#99050=CARTESIAN_POINT('Ctrl Pts',(-102.259821774248,4.22493897820357,128.286608903644));
#99051=CARTESIAN_POINT('Ctrl Pts',(-102.267568107513,4.15469558759761,128.168736264618));
#99052=CARTESIAN_POINT('Ctrl Pts',(-102.275314440779,4.07951604518537,128.053806154576));
#99053=CARTESIAN_POINT('Ctrl Pts',(-102.283060774044,3.99968674308219,127.942247932902));
#99054=CARTESIAN_POINT('Ctrl Pts',(-102.290808842047,3.91983956376019,127.830664728538));
#99055=CARTESIAN_POINT('Ctrl Pts',(-102.29855691005,3.83534078019137,127.72245523301));
#99056=CARTESIAN_POINT('Ctrl Pts',(-102.306304978053,3.7465184801358,127.618017519201));
#99057=CARTESIAN_POINT('Ctrl Pts',(-102.314061280795,3.65760177868286,127.513468807746));
#99058=CARTESIAN_POINT('Ctrl Pts',(-102.321817583537,3.56435263526141,127.412700184105));
#99059=CARTESIAN_POINT('Ctrl Pts',(-102.329573886279,3.46713796449722,127.316074878461));
#99060=CARTESIAN_POINT('Ctrl Pts',(-102.337334328793,3.36987140733617,127.219398000983));
#99061=CARTESIAN_POINT('Ctrl Pts',(-102.345094771307,3.26863539392902,127.126869111567));
#99062=CARTESIAN_POINT('Ctrl Pts',(-102.352855213821,3.16383090209819,127.038811907825));
#99063=CARTESIAN_POINT('Ctrl Pts',(-102.360628114087,3.05885816879296,126.950613346843));
#99064=CARTESIAN_POINT('Ctrl Pts',(-102.368401014352,2.95030581959511,126.866901055049));
#99065=CARTESIAN_POINT('Ctrl Pts',(-102.376173914617,2.8386055835034,126.787956578652));
#99066=CARTESIAN_POINT('Ctrl Pts',(-102.383664250379,2.73096593235044,126.711881932823));
#99067=CARTESIAN_POINT('Ctrl Pts',(-102.391154586141,2.62040354655705,126.640234643952));
#99068=CARTESIAN_POINT('Ctrl Pts',(-102.398644921903,2.50732557270838,126.573225836571));
#99069=CARTESIAN_POINT('Ctrl Pts',(-102.406419256022,2.3899602131111,126.503676369892));
#99070=CARTESIAN_POINT('Ctrl Pts',(-102.414193590142,2.26951296463109,126.438903752329));
#99071=CARTESIAN_POINT('Ctrl Pts',(-102.421967924261,2.14641006688465,126.379193175844));
#99072=CARTESIAN_POINT('Ctrl Pts',(-102.429732677208,2.02345888245767,126.319556187309));
#99073=CARTESIAN_POINT('Ctrl Pts',(-102.437497430155,1.8978589091528,126.264968996056));
#99074=CARTESIAN_POINT('Ctrl Pts',(-102.445262183102,1.77006396707104,126.215672720686));
#99075=CARTESIAN_POINT('Ctrl Pts',(-102.453019223987,1.64239595272735,126.166425407071));
#99076=CARTESIAN_POINT('Ctrl Pts',(-102.460776264872,1.5125376704593,126.122458691424));
#99077=CARTESIAN_POINT('Ctrl Pts',(-102.468533305757,1.38096574526973,126.083966918637));
#99078=CARTESIAN_POINT('Ctrl Pts',(-102.476284496997,1.24949303949224,126.045504172795));
#99079=CARTESIAN_POINT('Ctrl Pts',(-102.484035688237,1.11630963669997,126.012508261224));
#99080=CARTESIAN_POINT('Ctrl Pts',(-102.491786879477,0.981909928188809,
125.985124583149));
#99081=CARTESIAN_POINT('Ctrl Pts',(-102.499534776254,0.847567343139183,
125.957752543868));
#99082=CARTESIAN_POINT('Ctrl Pts',(-102.507282673032,0.712009862861705,
125.935988071697));
#99083=CARTESIAN_POINT('Ctrl Pts',(-102.515030569809,0.575744539526512,
125.919926025138));
#99084=CARTESIAN_POINT('Ctrl Pts',(-102.522776845893,0.43950771995942,125.903867338413));
#99085=CARTESIAN_POINT('Ctrl Pts',(-102.530523121977,0.302563739876156,
125.893508750446));
#99086=CARTESIAN_POINT('Ctrl Pts',(-102.538269398061,0.165426894237428,
125.888893497834));
#99087=CARTESIAN_POINT('Ctrl Pts',(-102.546015731326,0.0282890362854728,
125.884278211154));
#99088=CARTESIAN_POINT('Ctrl Pts',(-102.553762064592,-0.109041299318828,
125.885406357579));
#99089=CARTESIAN_POINT('Ctrl Pts',(-102.561508397857,-0.24604807843205,
125.892269066546));
#99090=CARTESIAN_POINT('Ctrl Pts',(-102.56925646586,-0.383085539263329,
125.899133312369));
#99091=CARTESIAN_POINT('Ctrl Pts',(-102.577004533863,-0.519798909019114,
125.911734656619));
#99092=CARTESIAN_POINT('Ctrl Pts',(-102.584752601866,-0.655675938261888,
125.930012237886));
#99093=CARTESIAN_POINT('Ctrl Pts',(-102.592508904608,-0.791697379228114,
125.948309244785));
#99094=CARTESIAN_POINT('Ctrl Pts',(-102.60026520735,-0.926880315969279,
125.97229448761));
#99095=CARTESIAN_POINT('Ctrl Pts',(-102.608021510092,-1.06072082632601,
126.001855605481));
#99096=CARTESIAN_POINT('Ctrl Pts',(-102.615781952606,-1.19463277139335,
126.031432501012));
#99097=CARTESIAN_POINT('Ctrl Pts',(-102.62354239512,-1.3272004846867,126.066591101371));
#99098=CARTESIAN_POINT('Ctrl Pts',(-102.631302837634,-1.45793489193086,
126.107169019026));
#99099=CARTESIAN_POINT('Ctrl Pts',(-102.6390757379,-1.58887916565159,126.147812075958));
#99100=CARTESIAN_POINT('Ctrl Pts',(-102.646848638165,-1.71798388387347,
126.193891703199));
#99101=CARTESIAN_POINT('Ctrl Pts',(-102.654621538431,-1.84477881372711,
126.245196857519));
#99102=CARTESIAN_POINT('Ctrl Pts',(-102.662111874193,-1.9669644285041,126.294636940251));
#99103=CARTESIAN_POINT('Ctrl Pts',(-102.669602209955,-2.08700499194705,
126.348929096992));
#99104=CARTESIAN_POINT('Ctrl Pts',(-102.677092545717,-2.20450280633424,
126.407844901756));
#99105=CARTESIAN_POINT('Ctrl Pts',(-102.684867679213,-2.32646812557258,
126.469000804729));
#99106=CARTESIAN_POINT('Ctrl Pts',(-102.69264281271,-2.44607989834717,126.535332656813));
#99107=CARTESIAN_POINT('Ctrl Pts',(-102.700417946207,-2.56286764750348,
126.606635938186));
#99108=CARTESIAN_POINT('Ctrl Pts',(-102.708183320531,-2.67950880731297,
126.677849721288));
#99109=CARTESIAN_POINT('Ctrl Pts',(-102.715948694856,-2.79333266624636,
126.754022314974));
#99110=CARTESIAN_POINT('Ctrl Pts',(-102.72371406918,-2.90389095927734,126.834902170986));
#99111=CARTESIAN_POINT('Ctrl Pts',(-102.73168682707,-3.01740184313235,126.917942019832));
#99112=CARTESIAN_POINT('Ctrl Pts',(-102.73965958496,-3.12746990584699,127.005943931496));
#99113=CARTESIAN_POINT('Ctrl Pts',(-102.74763234285,-3.23363833206806,127.098585907754));
#99114=CARTESIAN_POINT('Ctrl Pts',(-102.75538313854,-3.33685102105582,127.188648724197));
#99115=CARTESIAN_POINT('Ctrl Pts',(-102.763133934231,-3.43637799670921,
127.283096407964));
#99116=CARTESIAN_POINT('Ctrl Pts',(-102.770884729922,-3.53183068472812,
127.381590529331));
#99117=CARTESIAN_POINT('Ctrl Pts',(-102.778632020455,-3.6272402059904,127.480040108509));
#99118=CARTESIAN_POINT('Ctrl Pts',(-102.786379310989,-3.71857883439708,
127.582532204005));
#99119=CARTESIAN_POINT('Ctrl Pts',(-102.794126601522,-3.80549381601036,
127.688690564623));
#99120=CARTESIAN_POINT('Ctrl Pts',(-102.801872066229,-3.89238831412471,
127.794823906601));
#99121=CARTESIAN_POINT('Ctrl Pts',(-102.809617530937,-3.97486099342078,
127.904621491454));
#99122=CARTESIAN_POINT('Ctrl Pts',(-102.817362995644,-4.05259873568158,
128.017673238248));
#99123=CARTESIAN_POINT('Ctrl Pts',(-102.825504434218,-4.13431068937647,
128.136504565612));
#99124=CARTESIAN_POINT('Ctrl Pts',(-102.833645872793,-4.2107905216308,128.258931186203));
#99125=CARTESIAN_POINT('Ctrl Pts',(-102.841787311367,-4.28172584201632,
128.384441842832));
#99126=CARTESIAN_POINT('Ctrl Pts',(-102.849536903174,-4.34924705128524,
128.503911681915));
#99127=CARTESIAN_POINT('Ctrl Pts',(-102.857286494982,-4.41174482490943,
128.626175246942));
#99128=CARTESIAN_POINT('Ctrl Pts',(-102.865036086789,-4.46899709010937,
128.750766677398));
#99129=CARTESIAN_POINT('Ctrl Pts',(-102.872788327524,-4.52626892499603,
128.875400695082));
#99130=CARTESIAN_POINT('Ctrl Pts',(-102.880540568259,-4.57829152778495,
129.002363803426));
#99131=CARTESIAN_POINT('Ctrl Pts',(-102.888292808993,-4.6248912238265,129.131170780676));
#99132=CARTESIAN_POINT('Ctrl Pts',(-102.896051980615,-4.67153258229963,
129.26009291773));
#99133=CARTESIAN_POINT('Ctrl Pts',(-102.903811152236,-4.71274123686296,
129.390861842772));
#99134=CARTESIAN_POINT('Ctrl Pts',(-102.911570323857,-4.74839351052368,
129.522977719398));
#99135=CARTESIAN_POINT('Ctrl Pts',(-102.912733635416,-4.75373875922984,
129.542785494502));
#99136=CARTESIAN_POINT('Ctrl Pts',(-102.913896946976,-4.75895920425979,
129.562623528465));
#99137=CARTESIAN_POINT('Ctrl Pts',(-102.915060258535,-4.76405452823397,
129.582490119308));
#99138=CARTESIAN_POINT('Ctrl Pts',(-101.165045656948,-4.76405452823419,
129.582490119309));
#99139=CARTESIAN_POINT('Ctrl Pts',(-101.172682180364,-4.79766536477147,
129.713538260852));
#99140=CARTESIAN_POINT('Ctrl Pts',(-101.18031870378,-4.82585068438517,129.845919443598));
#99141=CARTESIAN_POINT('Ctrl Pts',(-101.187955227196,-4.84852456437522,
129.979137853005));
#99142=CARTESIAN_POINT('Ctrl Pts',(-101.195819449991,-4.8718745148893,130.116328455962));
#99143=CARTESIAN_POINT('Ctrl Pts',(-101.203683672785,-4.88937914754242,
130.254406536086));
#99144=CARTESIAN_POINT('Ctrl Pts',(-101.21154789558,-4.90100212544491,130.392825407791));
#99145=CARTESIAN_POINT('Ctrl Pts',(-101.219412118375,-4.9126251033474,130.531244279497));
#99146=CARTESIAN_POINT('Ctrl Pts',(-101.22727634117,-4.91836645518236,130.670003478117));
#99147=CARTESIAN_POINT('Ctrl Pts',(-101.235140563964,-4.91824820892467,
130.808557986892));
#99148=CARTESIAN_POINT('',(-100.889859436022,-4.918249990696,130.804663138373));
#99149=CARTESIAN_POINT('Ctrl Pts',(-100.820132980931,-4.76405452823393,
129.582490119308));
#99150=CARTESIAN_POINT('Ctrl Pts',(-100.82822748962,-4.79958196870859,129.721011070514));
#99151=CARTESIAN_POINT('Ctrl Pts',(-100.83632199831,-4.82909935154331,129.861221551865));
#99152=CARTESIAN_POINT('Ctrl Pts',(-100.844416506999,-4.85245675817816,
130.002583545986));
#99153=CARTESIAN_POINT('Ctrl Pts',(-100.852497712237,-4.87577577655068,
130.143713209463));
#99154=CARTESIAN_POINT('Ctrl Pts',(-100.860578917475,-4.8929549507117,130.285990279047));
#99155=CARTESIAN_POINT('Ctrl Pts',(-100.868660122712,-4.90389499969728,
130.42886508571));
#99156=CARTESIAN_POINT('Ctrl Pts',(-100.875726560472,-4.9134612924681,130.55379891662));
#99157=CARTESIAN_POINT('Ctrl Pts',(-100.882792998232,-4.91825770855033,
130.679189440182));
#99158=CARTESIAN_POINT('Ctrl Pts',(-100.889859435992,-4.91824999069603,
130.804663137836));
#99159=CARTESIAN_POINT('Ctrl Pts',(-100.889859436022,-4.91824999069599,
130.804663138372));
#99160=CARTESIAN_POINT('Ctrl Pts',(-100.898012385779,-4.91824108615426,
130.949429254983));
#99161=CARTESIAN_POINT('Ctrl Pts',(-100.906165335536,-4.91183621813621,
131.094059493338));
#99162=CARTESIAN_POINT('Ctrl Pts',(-100.914318285293,-4.89909698201659,
131.237986981266));
#99163=CARTESIAN_POINT('Ctrl Pts',(-100.922483363176,-4.88633879532363,
131.382128572174));
#99164=CARTESIAN_POINT('Ctrl Pts',(-100.93064844106,-4.86722746182756,131.52556500171));
#99165=CARTESIAN_POINT('Ctrl Pts',(-100.938813518944,-4.84187593075419,
131.667738016901));
#99166=CARTESIAN_POINT('Ctrl Pts',(-100.946999214543,-4.81646038428944,
131.810270034521));
#99167=CARTESIAN_POINT('Ctrl Pts',(-100.955184910142,-4.7847731895604,131.951531936429));
#99168=CARTESIAN_POINT('Ctrl Pts',(-100.963370605741,-4.74697807774749,
132.090977185112));
#99169=CARTESIAN_POINT('Ctrl Pts',(-100.971567362971,-4.70913189201404,
132.230610871274));
#99170=CARTESIAN_POINT('Ctrl Pts',(-100.979764120201,-4.66516141326116,
132.368422693961));
#99171=CARTESIAN_POINT('Ctrl Pts',(-100.987960877431,-4.61527916584051,
132.503884457898));
#99172=CARTESIAN_POINT('Ctrl Pts',(-100.996176610845,-4.56528143680963,
132.639659827246));
#99173=CARTESIAN_POINT('Ctrl Pts',(-101.004392344259,-4.50934469907841,
132.773073958039));
#99174=CARTESIAN_POINT('Ctrl Pts',(-101.012608077673,-4.44772897719346,
132.90362001267));
#99175=CARTESIAN_POINT('Ctrl Pts',(-101.017070651448,-4.41426091162266,
132.974529251136));
#99176=CARTESIAN_POINT('Ctrl Pts',(-101.021533225223,-4.37911811220072,
133.044592757345));
#99177=CARTESIAN_POINT('Ctrl Pts',(-101.025995798998,-4.34234763903753,
133.11373283621));
#99178=CARTESIAN_POINT('Ctrl Pts',(-101.033770133118,-4.27828910275458,
133.234183074393));
#99179=CARTESIAN_POINT('Ctrl Pts',(-101.041544467237,-4.20911363968645,
133.352156745023));
#99180=CARTESIAN_POINT('Ctrl Pts',(-101.049318801356,-4.13503693188983,
133.467188556883));
#99181=CARTESIAN_POINT('Ctrl Pts',(-101.057083554303,-4.06105151701534,
133.582078602316));
#99182=CARTESIAN_POINT('Ctrl Pts',(-101.06484830725,-3.98217708554418,133.694033677248));
#99183=CARTESIAN_POINT('Ctrl Pts',(-101.072613060197,-3.89867580088949,
133.80261178484));
#99184=CARTESIAN_POINT('Ctrl Pts',(-101.080370101082,-3.81525745088788,
133.911082051124));
#99185=CARTESIAN_POINT('Ctrl Pts',(-101.088127141967,-3.7272216296641,134.01618171687));
#99186=CARTESIAN_POINT('Ctrl Pts',(-101.095884182852,-3.63487430803071,
134.117496870019));
#99187=CARTESIAN_POINT('Ctrl Pts',(-101.103635374092,-3.54259662623079,
134.218735620623));
#99188=CARTESIAN_POINT('Ctrl Pts',(-101.111386565332,-3.446014177913,134.316195251428));
#99189=CARTESIAN_POINT('Ctrl Pts',(-101.119137756573,-3.34547356783761,
134.409494411117));
#99190=CARTESIAN_POINT('Ctrl Pts',(-101.12688565335,-3.24497569020364,134.502753916173));
#99191=CARTESIAN_POINT('Ctrl Pts',(-101.134633550127,-3.14052328280892,
134.591856201764));
#99192=CARTESIAN_POINT('Ctrl Pts',(-101.142381446904,-3.03250005375704,
134.676456495313));
#99193=CARTESIAN_POINT('Ctrl Pts',(-101.150127722988,-2.92449942083597,
134.761039092304));
#99194=CARTESIAN_POINT('Ctrl Pts',(-101.157873999072,-2.81292975956872,
134.841121329476));
#99195=CARTESIAN_POINT('Ctrl Pts',(-101.165620275156,-2.6982078164562,134.916398754757));
#99196=CARTESIAN_POINT('Ctrl Pts',(-101.173366608422,-2.58348502649221,
134.991676735719));
#99197=CARTESIAN_POINT('Ctrl Pts',(-101.181112941687,-2.46561023512771,
135.062149619528));
#99198=CARTESIAN_POINT('Ctrl Pts',(-101.188859274952,-2.34502877928759,
135.12755655192));
#99199=CARTESIAN_POINT('Ctrl Pts',(-101.196607342955,-2.22442032006698,
135.19297813174));
#99200=CARTESIAN_POINT('Ctrl Pts',(-101.204355410958,-2.1011043338218,135.253331316272));
#99201=CARTESIAN_POINT('Ctrl Pts',(-101.212103478961,-1.97554996967867,
135.30840162313));
#99202=CARTESIAN_POINT('Ctrl Pts',(-101.219859781703,-1.8498621648627,135.363530459365));
#99203=CARTESIAN_POINT('Ctrl Pts',(-101.227616084445,-1.72193158850011,
135.413365044655));
#99204=CARTESIAN_POINT('Ctrl Pts',(-101.235372387187,-1.59224706669994,
135.45773921178));
#99205=CARTESIAN_POINT('Ctrl Pts',(-101.243132829701,-1.46249332836542,
135.502137062733));
#99206=CARTESIAN_POINT('Ctrl Pts',(-101.250893272215,-1.33098415396787,
135.541068577429));
#99207=CARTESIAN_POINT('Ctrl Pts',(-101.258653714729,-1.19822171150016,
135.574418037827));
#99208=CARTESIAN_POINT('Ctrl Pts',(-101.266426614995,-1.06524614697407,
135.60782103374));
#99209=CARTESIAN_POINT('Ctrl Pts',(-101.27419951526,-0.93101367710583,135.635623989463));
#99210=CARTESIAN_POINT('Ctrl Pts',(-101.281972415526,-0.796035687933511,
135.657762542612));
#99211=CARTESIAN_POINT('Ctrl Pts',(-101.289462751288,-0.66596448865701,
135.679096303589));
#99212=CARTESIAN_POINT('Ctrl Pts',(-101.29695308705,-0.535201337759194,
135.695170305031));
#99213=CARTESIAN_POINT('Ctrl Pts',(-101.304443422812,-0.404204714266281,
135.705972761694));
#99214=CARTESIAN_POINT('Ctrl Pts',(-101.312217756931,-0.268241313977503,
135.717184796786));
#99215=CARTESIAN_POINT('Ctrl Pts',(-101.31999209105,-0.131595696195883,
135.722753171198));
#99216=CARTESIAN_POINT('Ctrl Pts',(-101.327766425169,0.00522409498051373,
135.722607843086));
#99217=CARTESIAN_POINT('Ctrl Pts',(-101.335531178116,0.141875267992222,
135.722462694077));
#99218=CARTESIAN_POINT('Ctrl Pts',(-101.343295931063,0.278699800091174,
135.716617853696));
#99219=CARTESIAN_POINT('Ctrl Pts',(-101.351060684011,0.415184121088017,
135.705054977358));
#99220=CARTESIAN_POINT('Ctrl Pts',(-101.358817724896,0.551532883932784,
135.693503585431));
#99221=CARTESIAN_POINT('Ctrl Pts',(-101.366574765781,0.687541721067824,
135.676245492269));
#99222=CARTESIAN_POINT('Ctrl Pts',(-101.374331806666,0.822697011857725,
135.653314390204));
#99223=CARTESIAN_POINT('Ctrl Pts',(-101.382082997906,0.957750380991672,
135.630400580661));
#99224=CARTESIAN_POINT('Ctrl Pts',(-101.389834189146,1.09195110106149,135.601822342568));
#99225=CARTESIAN_POINT('Ctrl Pts',(-101.397585380386,1.22479098206313,135.567665154624));
#99226=CARTESIAN_POINT('Ctrl Pts',(-101.405333277163,1.3575744025719,135.533522484395));
#99227=CARTESIAN_POINT('Ctrl Pts',(-101.41308117394,1.48899775653647,135.493805677614));
#99228=CARTESIAN_POINT('Ctrl Pts',(-101.420829070717,1.61856357342074,135.448651200776));
#99229=CARTESIAN_POINT('Ctrl Pts',(-101.428575346801,1.74810228792925,135.403506169281));
#99230=CARTESIAN_POINT('Ctrl Pts',(-101.436321622886,1.87578386926455,135.352925858749));
#99231=CARTESIAN_POINT('Ctrl Pts',(-101.44406789897,2.00112691161267,135.297096326031));
#99232=CARTESIAN_POINT('Ctrl Pts',(-101.451814232235,2.12647087921449,135.241266381193));
#99233=CARTESIAN_POINT('Ctrl Pts',(-101.459560565501,2.24947591624303,135.180187295925));
#99234=CARTESIAN_POINT('Ctrl Pts',(-101.467306898766,2.36968184313177,135.114092746693));
#99235=CARTESIAN_POINT('Ctrl Pts',(-101.475054966769,2.48991468930455,135.047983396045));
#99236=CARTESIAN_POINT('Ctrl Pts',(-101.482803034772,2.60734683546902,134.976856534775));
#99237=CARTESIAN_POINT('Ctrl Pts',(-101.490551102775,2.72154424495612,134.90099093836));
#99238=CARTESIAN_POINT('Ctrl Pts',(-101.498307405517,2.83586302480883,134.825044711086));
#99239=CARTESIAN_POINT('Ctrl Pts',(-101.506063708259,2.9469398742037,134.744349904637));
#99240=CARTESIAN_POINT('Ctrl Pts',(-101.513820011,3.05437076950047,134.659227964819));
#99241=CARTESIAN_POINT('Ctrl Pts',(-101.521580453515,3.16185900390074,134.57406059286));
#99242=CARTESIAN_POINT('Ctrl Pts',(-101.529340896029,3.26569711086327,134.484461634554));
#99243=CARTESIAN_POINT('Ctrl Pts',(-101.537101338543,3.36551629945877,134.39079102963));
#99244=CARTESIAN_POINT('Ctrl Pts',(-101.544874238808,3.46549572667732,134.296970056335));
#99245=CARTESIAN_POINT('Ctrl Pts',(-101.552647139074,3.56144306952175,134.199064654467));
#99246=CARTESIAN_POINT('Ctrl Pts',(-101.560420039339,3.65302776144976,134.097470278142));
#99247=CARTESIAN_POINT('Ctrl Pts',(-101.567910375101,3.74128311913701,133.999569113298));
#99248=CARTESIAN_POINT('Ctrl Pts',(-101.575400710863,3.82548730891585,133.898242761453));
#99249=CARTESIAN_POINT('Ctrl Pts',(-101.582891046625,3.90538259641576,133.793870583783));
#99250=CARTESIAN_POINT('Ctrl Pts',(-101.590665380744,3.98830713802593,133.685541103273));
#99251=CARTESIAN_POINT('Ctrl Pts',(-101.598439714863,4.06685226328891,133.573587117414));
#99252=CARTESIAN_POINT('Ctrl Pts',(-101.606214048982,4.14068443377205,133.458398198765));
#99253=CARTESIAN_POINT('Ctrl Pts',(-101.613978801929,4.21442561270363,133.343351240164));
#99254=CARTESIAN_POINT('Ctrl Pts',(-101.621743554876,4.28346518468094,133.225077607244));
#99255=CARTESIAN_POINT('Ctrl Pts',(-101.629508307824,4.34751011865313,133.103999465452));
#99256=CARTESIAN_POINT('Ctrl Pts',(-101.637265348709,4.41149144229402,132.983041580179));
#99257=CARTESIAN_POINT('Ctrl Pts',(-101.645022389594,4.47048781841425,132.85928507262));
#99258=CARTESIAN_POINT('Ctrl Pts',(-101.652779430479,4.52424996882774,132.733180277893));
#99259=CARTESIAN_POINT('Ctrl Pts',(-101.660530621719,4.57797157678532,132.607170579772));
#99260=CARTESIAN_POINT('Ctrl Pts',(-101.668281812959,4.62646666293253,132.478816477464));
#99261=CARTESIAN_POINT('Ctrl Pts',(-101.676033004199,4.6695324538088,132.348591728937));
#99262=CARTESIAN_POINT('Ctrl Pts',(-101.683780900976,4.7125799405752,132.218422329402));
#99263=CARTESIAN_POINT('Ctrl Pts',(-101.691528797753,4.75020259920362,132.086384235407));
#99264=CARTESIAN_POINT('Ctrl Pts',(-101.69927669453,4.78224634784539,131.952969746478));
#99265=CARTESIAN_POINT('Ctrl Pts',(-101.707022970614,4.81428339362574,131.819583164983));
#99266=CARTESIAN_POINT('Ctrl Pts',(-101.714769246698,4.84074375937369,131.68482114114));
#99267=CARTESIAN_POINT('Ctrl Pts',(-101.722515522782,4.8615237683873,131.549189263568));
#99268=CARTESIAN_POINT('Ctrl Pts',(-101.730261856048,4.88230393079419,131.413556384792));
#99269=CARTESIAN_POINT('Ctrl Pts',(-101.738008189313,4.89740359358778,131.27705402593));
#99270=CARTESIAN_POINT('Ctrl Pts',(-101.745754522578,4.90677061710056,131.140195656921));
#99271=CARTESIAN_POINT('Ctrl Pts',(-101.753502590581,4.91613973829328,131.00330663943));
#99272=CARTESIAN_POINT('Ctrl Pts',(-101.761250658584,4.9197736389307,130.866061843124));
#99273=CARTESIAN_POINT('Ctrl Pts',(-101.768998726587,4.9176722532963,130.728977120302));
#99274=CARTESIAN_POINT('Ctrl Pts',(-101.776755029329,4.91556863428424,130.591746702205));
#99275=CARTESIAN_POINT('Ctrl Pts',(-101.784511332071,4.90771755852357,130.454677088984));
#99276=CARTESIAN_POINT('Ctrl Pts',(-101.792267634813,4.89417108283057,130.31828194648));
#99277=CARTESIAN_POINT('Ctrl Pts',(-101.800028077327,4.88061737697558,130.181814005781));
#99278=CARTESIAN_POINT('Ctrl Pts',(-101.807788519841,4.86136226897875,130.046021640005));
#99279=CARTESIAN_POINT('Ctrl Pts',(-101.815548962355,4.83650924582193,129.91140967962));
#99280=CARTESIAN_POINT('Ctrl Pts',(-101.823321862621,4.81161632638598,129.776581628166));
#99281=CARTESIAN_POINT('Ctrl Pts',(-101.831094762886,4.7811076214212,129.642938150079));
#99282=CARTESIAN_POINT('Ctrl Pts',(-101.838867663151,4.74513715838434,129.510971112962));
#99283=CARTESIAN_POINT('Ctrl Pts',(-101.846357998914,4.71047431228261,129.383801410048));
#99284=CARTESIAN_POINT('Ctrl Pts',(-101.853848334676,4.67074000413977,129.258188672191));
#99285=CARTESIAN_POINT('Ctrl Pts',(-101.861338670438,4.62611408953649,129.1345547926));
#99286=CARTESIAN_POINT('Ctrl Pts',(-101.869113004557,4.57979616981786,129.006233296887));
#99287=CARTESIAN_POINT('Ctrl Pts',(-101.876887338676,4.52806166958869,128.879637194505));
#99288=CARTESIAN_POINT('Ctrl Pts',(-101.884661672795,4.47105806160708,128.755257674267));
#99289=CARTESIAN_POINT('Ctrl Pts',(-101.892426425742,4.41412470547775,128.631031440671));
#99290=CARTESIAN_POINT('Ctrl Pts',(-101.900191178689,4.35193532345734,128.509016705876));
#99291=CARTESIAN_POINT('Ctrl Pts',(-101.907955931636,4.28468670485385,128.389688195943));
#99292=CARTESIAN_POINT('Ctrl Pts',(-101.915712972521,4.2175048785264,128.270478204767));
#99293=CARTESIAN_POINT('Ctrl Pts',(-101.923470013406,4.14527400611062,128.153949467417));
#99294=CARTESIAN_POINT('Ctrl Pts',(-101.931227054291,4.06823822634483,128.04055512582));
#99295=CARTESIAN_POINT('Ctrl Pts',(-101.938978245531,3.99126053985992,127.927246295778));
#99296=CARTESIAN_POINT('Ctrl Pts',(-101.946729436771,3.90948537703234,127.817067478829));
#99297=CARTESIAN_POINT('Ctrl Pts',(-101.954480628012,3.82320171984922,127.710445351784));
#99298=CARTESIAN_POINT('Ctrl Pts',(-101.962228524789,3.73695473552198,127.603868541986));
#99299=CARTESIAN_POINT('Ctrl Pts',(-101.969976421566,3.6462033135042,127.500845718739));
#99300=CARTESIAN_POINT('Ctrl Pts',(-101.977724318343,3.55127835432622,127.401772615384));
#99301=CARTESIAN_POINT('Ctrl Pts',(-101.985470594427,3.45637325140336,127.302720235986));
#99302=CARTESIAN_POINT('Ctrl Pts',(-101.993216870511,3.3572966181027,127.207616215254));
#99303=CARTESIAN_POINT('Ctrl Pts',(-102.000963146595,3.25441778065853,127.11682106233));
#99304=CARTESIAN_POINT('Ctrl Pts',(-102.00870947986,3.15153818378629,127.026025239176));
#99305=CARTESIAN_POINT('Ctrl Pts',(-102.016455813126,3.04485661989751,126.939538606003));
#99306=CARTESIAN_POINT('Ctrl Pts',(-102.024202146391,2.93477690303093,126.857682572433));
#99307=CARTESIAN_POINT('Ctrl Pts',(-102.031950214394,2.82467253457515,126.775808207772));
#99308=CARTESIAN_POINT('Ctrl Pts',(-102.039698282397,2.71116881252626,126.698566739455));
#99309=CARTESIAN_POINT('Ctrl Pts',(-102.0474463504,2.59469970251056,126.626237053537));
#99310=CARTESIAN_POINT('Ctrl Pts',(-102.055202653141,2.47810680773858,126.553830494769));
#99311=CARTESIAN_POINT('Ctrl Pts',(-102.062958955883,2.3585425619003,126.486346353103));
#99312=CARTESIAN_POINT('Ctrl Pts',(-102.070715258625,2.23646726459749,126.4240184806));
#99313=CARTESIAN_POINT('Ctrl Pts',(-102.078475701139,2.11432681203256,126.361657341834));
#99314=CARTESIAN_POINT('Ctrl Pts',(-102.086236143653,1.98967299266106,126.30445811891));
#99315=CARTESIAN_POINT('Ctrl Pts',(-102.093996586168,1.86298647189528,126.252606618498));
#99316=CARTESIAN_POINT('Ctrl Pts',(-102.101769486433,1.73609658267967,126.200671881454));
#99317=CARTESIAN_POINT('Ctrl Pts',(-102.109542386698,1.60716783933513,126.154102154663));
#99318=CARTESIAN_POINT('Ctrl Pts',(-102.117315286964,1.47669731960939,126.113033716916));
#99319=CARTESIAN_POINT('Ctrl Pts',(-102.124805622726,1.35096973190967,126.073458220327));
#99320=CARTESIAN_POINT('Ctrl Pts',(-102.132295958488,1.22381081389744,126.038991066028));
#99321=CARTESIAN_POINT('Ctrl Pts',(-102.13978629425,1.09567273261236,126.009708980011));
#99322=CARTESIAN_POINT('Ctrl Pts',(-102.147560628369,0.962676257029962,
125.979316654803));
#99323=CARTESIAN_POINT('Ctrl Pts',(-102.155334962488,0.828203609648187,
125.954414069423));
#99324=CARTESIAN_POINT('Ctrl Pts',(-102.163109296607,0.692747754155644,
125.935142650416));
#99325=CARTESIAN_POINT('Ctrl Pts',(-102.170874049555,0.557458835899325,
125.915894981711));
#99326=CARTESIAN_POINT('Ctrl Pts',(-102.178638802502,0.421189503837876,
125.902264725568));
#99327=CARTESIAN_POINT('Ctrl Pts',(-102.186403555449,0.284445527877808,
125.894342918599));
#99328=CARTESIAN_POINT('Ctrl Pts',(-102.194160596334,0.147837367962416,
125.88642897968));
#99329=CARTESIAN_POINT('Ctrl Pts',(-102.201917637219,0.0107558900865783,
125.884212229418));
#99330=CARTESIAN_POINT('Ctrl Pts',(-102.209674678104,-0.12628570166064,
125.887732201257));
#99331=CARTESIAN_POINT('Ctrl Pts',(-102.217425869344,-0.263223949277679,
125.891249518658));
#99332=CARTESIAN_POINT('Ctrl Pts',(-102.225177060584,-0.400121981380527,
125.90049493731));
#99333=CARTESIAN_POINT('Ctrl Pts',(-102.232928251824,-0.536464620862973,
125.91545595772));
#99334=CARTESIAN_POINT('Ctrl Pts',(-102.240676148601,-0.672749311086765,
125.930410619297));
#99335=CARTESIAN_POINT('Ctrl Pts',(-102.248424045378,-0.808478690370066,
125.951076008417));
#99336=CARTESIAN_POINT('Ctrl Pts',(-102.256171942155,-0.943140957225522,
125.97738763263));
#99337=CARTESIAN_POINT('Ctrl Pts',(-102.26391821824,-1.07777505563737,126.003693753018));
#99338=CARTESIAN_POINT('Ctrl Pts',(-102.271664494324,-1.21134210214581,
126.035643684359));
#99339=CARTESIAN_POINT('Ctrl Pts',(-102.279410770408,-1.34333916034705,
126.07312156603));
#99340=CARTESIAN_POINT('Ctrl Pts',(-102.287157103673,-1.47533719292078,
126.110599724355));
#99341=CARTESIAN_POINT('Ctrl Pts',(-102.294903436938,-1.6057648379625,126.15360580765));
#99342=CARTESIAN_POINT('Ctrl Pts',(-102.302649770204,-1.7341334131014,126.20197380548));
#99343=CARTESIAN_POINT('Ctrl Pts',(-102.310397838207,-1.86253073549282,
126.250352634988));
#99344=CARTESIAN_POINT('Ctrl Pts',(-102.31814590621,-1.98886770463073,126.304095630587));
#99345=CARTESIAN_POINT('Ctrl Pts',(-102.325893974213,-2.11267511675619,
126.362988429431));
#99346=CARTESIAN_POINT('Ctrl Pts',(-102.333650276955,-2.2366141128724,126.421943820242));
#99347=CARTESIAN_POINT('Ctrl Pts',(-102.341406579696,-2.35801782790125,
126.486059779539));
#99348=CARTESIAN_POINT('Ctrl Pts',(-102.349162882438,-2.4764407123026,126.555075446981));
#99349=CARTESIAN_POINT('Ctrl Pts',(-102.356923324952,-2.59492680256331,
126.624127950163));
#99350=CARTESIAN_POINT('Ctrl Pts',(-102.364683767467,-2.71042856298488,
126.698085161621));
#99351=CARTESIAN_POINT('Ctrl Pts',(-102.372444209981,-2.82252985775665,
126.776643116974));
#99352=CARTESIAN_POINT('Ctrl Pts',(-102.380217110246,-2.93481110747836,
126.855327180531));
#99353=CARTESIAN_POINT('Ctrl Pts',(-102.387990010512,-3.04368067258819,
126.938626508899));
#99354=CARTESIAN_POINT('Ctrl Pts',(-102.395762910777,-3.14875521521399,
127.026196558507));
#99355=CARTESIAN_POINT('Ctrl Pts',(-102.403253246539,-3.2500100335474,127.110583216236));
#99356=CARTESIAN_POINT('Ctrl Pts',(-102.410743582301,-3.34774072783208,
127.198935276479));
#99357=CARTESIAN_POINT('Ctrl Pts',(-102.418233918063,-3.44163833898923,
127.290913790574));
#99358=CARTESIAN_POINT('Ctrl Pts',(-102.425895793646,-3.53768634499599,
127.384998749344));
#99359=CARTESIAN_POINT('Ctrl Pts',(-102.43355766923,-3.63004660103402,127.48319505752));
#99360=CARTESIAN_POINT('Ctrl Pts',(-102.441219544813,-3.71833879881601,
127.585177547326));
#99361=CARTESIAN_POINT('Ctrl Pts',(-102.448872484318,-3.80652802103169,
127.68704109452));
#99362=CARTESIAN_POINT('Ctrl Pts',(-102.456525423823,-3.89065835611075,
127.792681743424));
#99363=CARTESIAN_POINT('Ctrl Pts',(-102.464178363328,-3.97038438058634,
127.901735782542));
#99364=CARTESIAN_POINT('Ctrl Pts',(-102.471824148583,-4.05003587423122,
128.010687873919));
#99365=CARTESIAN_POINT('Ctrl Pts',(-102.479469933838,-4.12529100819736,
128.123046687155));
#99366=CARTESIAN_POINT('Ctrl Pts',(-102.487115719093,-4.19584328337776,
128.238413968893));
#99367=CARTESIAN_POINT('Ctrl Pts',(-102.49475589586,-4.266343805663,128.35369662415));
#99368=CARTESIAN_POINT('Ctrl Pts',(-102.502396072628,-4.33214812334253,
128.47198301457));
#99369=CARTESIAN_POINT('Ctrl Pts',(-102.510036249396,-4.39299225161995,
128.592844816197));
#99370=CARTESIAN_POINT('Ctrl Pts',(-102.517673120172,-4.4538100519486,128.713654319542));
#99371=CARTESIAN_POINT('Ctrl Pts',(-102.525309990948,-4.50967175179214,
128.837036657736));
#99372=CARTESIAN_POINT('Ctrl Pts',(-102.532946861724,-4.56035887464973,
128.962538151392));
#99373=CARTESIAN_POINT('Ctrl Pts',(-102.540583337081,-4.61104337304876,
129.088033146879));
#99374=CARTESIAN_POINT('Ctrl Pts',(-102.548219812438,-4.65655366963076,
129.215646708699));
#99375=CARTESIAN_POINT('Ctrl Pts',(-102.555856287795,-4.69671922554291,
129.344904698768));
#99376=CARTESIAN_POINT('Ctrl Pts',(-102.560501317264,-4.72115067881412,
129.423528297335));
#99377=CARTESIAN_POINT('Ctrl Pts',(-102.565146346733,-4.74360557052034,
129.502759943539));
#99378=CARTESIAN_POINT('Ctrl Pts',(-102.569791376202,-4.76405452823412,
129.582490119309));
#99379=CARTESIAN_POINT('Origin',(213.235140564004,0.,130.804360617566));
#99380=CARTESIAN_POINT('',(-104.665400201108,-4.76405452823405,129.582490119308));
#99381=CARTESIAN_POINT('',(-104.319770171817,-4.76405452823413,129.582490119309));
#99382=CARTESIAN_POINT('',(213.235140564004,-4.76405452823405,129.582490119308));
#99383=CARTESIAN_POINT('',(-102.985140564047,-4.91824910835199,130.801399081676));
#99384=CARTESIAN_POINT('Ctrl Pts',(-102.985140564047,-4.91824910835199,
130.801399081677));
#99385=CARTESIAN_POINT('Ctrl Pts',(-102.992809150511,-4.91833027429495,
130.936192088233));
#99386=CARTESIAN_POINT('Ctrl Pts',(-103.000477736976,-4.91286591839689,
131.071207562454));
#99387=CARTESIAN_POINT('Ctrl Pts',(-103.008146323441,-4.90182760008308,
131.205944035505));
#99388=CARTESIAN_POINT('Ctrl Pts',(-103.015806418068,-4.89080150509054,
131.340531307641));
#99389=CARTESIAN_POINT('Ctrl Pts',(-103.023466512696,-4.87421375603655,
131.474839795842));
#99390=CARTESIAN_POINT('Ctrl Pts',(-103.031126607324,-4.85208791853538,
131.608366770094));
#99391=CARTESIAN_POINT('Ctrl Pts',(-103.038780165911,-4.82998096009431,
131.741779811313));
#99392=CARTESIAN_POINT('Ctrl Pts',(-103.046433724498,-4.80234537868109,
131.87441227058));
#99393=CARTESIAN_POINT('Ctrl Pts',(-103.054087283084,-4.76925661605141,
132.005765791831));
#99394=CARTESIAN_POINT('Ctrl Pts',(-103.061736716309,-4.73618568867177,
132.137048511918));
#99395=CARTESIAN_POINT('Ctrl Pts',(-103.069386149533,-4.69766752323498,
132.267053276107));
#99396=CARTESIAN_POINT('Ctrl Pts',(-103.077035582757,-4.65382871039418,
132.395291601868));
#99397=CARTESIAN_POINT('Ctrl Pts',(-103.084682936707,-4.61000181385035,
132.523495069797));
#99398=CARTESIAN_POINT('Ctrl Pts',(-103.092330290657,-4.56085727503352,
132.649932673786));
#99399=CARTESIAN_POINT('Ctrl Pts',(-103.099977644607,-4.50657149761993,
132.774131263946));
#99400=CARTESIAN_POINT('Ctrl Pts',(-103.107624677276,-4.45228800086938,
132.898324636254));
#99401=CARTESIAN_POINT('Ctrl Pts',(-103.115271709944,-4.39286385612323,
133.020278813433));
#99402=CARTESIAN_POINT('Ctrl Pts',(-103.122918742612,-4.3285233274563,133.139541309968));
#99403=CARTESIAN_POINT('Ctrl Pts',(-103.130567211507,-4.26417071467739,
133.25882620578));
#99404=CARTESIAN_POINT('Ctrl Pts',(-103.138215680402,-4.19490007299654,
133.375418062055));
#99405=CARTESIAN_POINT('Ctrl Pts',(-103.145864149297,-4.12098098982155,
133.488890137618));
#99406=CARTESIAN_POINT('Ctrl Pts',(-103.153520399481,-4.04698670391944,
133.602477655758));
#99407=CARTESIAN_POINT('Ctrl Pts',(-103.161176649664,-3.96833475199176,
133.712938717368));
#99408=CARTESIAN_POINT('Ctrl Pts',(-103.168832899848,-3.88533752884895,
133.819876385958));
#99409=CARTESIAN_POINT('Ctrl Pts',(-103.176493173238,-3.80229669232332,
133.926870248156));
#99410=CARTESIAN_POINT('Ctrl Pts',(-103.184153446628,-3.71490629724936,
134.03033672405));
#99411=CARTESIAN_POINT('Ctrl Pts',(-103.191813720019,-3.62351733110619,
134.129913987108));
#99412=CARTESIAN_POINT('Ctrl Pts',(-103.199485883508,-3.53198651312275,
134.229645811691));
#99413=CARTESIAN_POINT('Ctrl Pts',(-103.207158046997,-3.43644501090141,
134.325476081341));
#99414=CARTESIAN_POINT('Ctrl Pts',(-103.214830210487,-3.33727923066267,
134.417081254301));
#99415=CARTESIAN_POINT('Ctrl Pts',(-103.221216071439,-3.25473942495501,
134.493328051933));
#99416=CARTESIAN_POINT('Ctrl Pts',(-103.22760193239,-3.16968944572114,134.566648390191));
#99417=CARTESIAN_POINT('Ctrl Pts',(-103.233987793342,-3.08236747520497,
134.636878564073));
#99418=CARTESIAN_POINT('Ctrl Pts',(-103.241762127461,-2.97605915125946,
134.722378834299));
#99419=CARTESIAN_POINT('Ctrl Pts',(-103.24953646158,-2.86602227181567,134.803587927477));
#99420=CARTESIAN_POINT('Ctrl Pts',(-103.257310795699,-2.75263829324372,
134.880163052556));
#99421=CARTESIAN_POINT('Ctrl Pts',(-103.265075548646,-2.63939405029195,
134.956643805637));
#99422=CARTESIAN_POINT('Ctrl Pts',(-103.272840301594,-2.52281123661999,
135.028501736997));
#99423=CARTESIAN_POINT('Ctrl Pts',(-103.280605054541,-2.40330486416648,
135.095433769165));
#99424=CARTESIAN_POINT('Ctrl Pts',(-103.288362095426,-2.28391718712685,
135.162299323495));
#99425=CARTESIAN_POINT('Ctrl Pts',(-103.296119136311,-2.16161206874099,
135.224248525064));
#99426=CARTESIAN_POINT('Ctrl Pts',(-103.303876177196,-2.03683373244994,
135.281021360671));
#99427=CARTESIAN_POINT('Ctrl Pts',(-103.311627368436,-1.91214949247241,
135.337751383441));
#99428=CARTESIAN_POINT('Ctrl Pts',(-103.319378559676,-1.78499610132625,
135.389312648746));
#99429=CARTESIAN_POINT('Ctrl Pts',(-103.327129750916,-1.65584231454443,
135.435491072635));
#99430=CARTESIAN_POINT('Ctrl Pts',(-103.334877647693,-1.52674342156781,
135.481649869461));
#99431=CARTESIAN_POINT('Ctrl Pts',(-103.34262554447,-1.39564619135186,135.52243024388));
#99432=CARTESIAN_POINT('Ctrl Pts',(-103.350373441247,-1.26303908411213,
135.557666344584));
#99433=CARTESIAN_POINT('Ctrl Pts',(-103.358119717331,-1.13045971542056,
135.592895074656));
#99434=CARTESIAN_POINT('Ctrl Pts',(-103.365865993416,-0.996371475529762,
135.622581737465));
#99435=CARTESIAN_POINT('Ctrl Pts',(-103.3736122695,-0.861277319506663,135.646610553433));
#99436=CARTESIAN_POINT('Ctrl Pts',(-103.381358602765,-0.726182166249009,
135.670639546776));
#99437=CARTESIAN_POINT('Ctrl Pts',(-103.38910493603,-0.59008146696587,135.689010541475));
#99438=CARTESIAN_POINT('Ctrl Pts',(-103.396851269296,-0.453487292522191,
135.701659091012));
#99439=CARTESIAN_POINT('Ctrl Pts',(-103.404599337299,-0.316862528760408,
135.714310473105));
#99440=CARTESIAN_POINT('Ctrl Pts',(-103.412347405302,-0.179744459160507,
135.721236823955));
#99441=CARTESIAN_POINT('Ctrl Pts',(-103.420095473305,-0.0426487858903845,
135.722425698831));
#99442=CARTESIAN_POINT('Ctrl Pts',(-103.427851776046,0.0945925942929355,
135.723615837258));
#99443=CARTESIAN_POINT('Ctrl Pts',(-103.435608078788,0.231811139023357,
135.719056315188));
#99444=CARTESIAN_POINT('Ctrl Pts',(-103.44336438153,0.368492081161458,135.708786847883));
#99445=CARTESIAN_POINT('Ctrl Pts',(-103.451124824044,0.505245974033762,
135.698511899454));
#99446=CARTESIAN_POINT('Ctrl Pts',(-103.458885266558,0.641461304463368,
135.68252097881));
#99447=CARTESIAN_POINT('Ctrl Pts',(-103.466645709073,0.776630903958121,
135.660905428593));
#99448=CARTESIAN_POINT('Ctrl Pts',(-103.474418609338,0.912017489693777,
135.639255179176));
#99449=CARTESIAN_POINT('Ctrl Pts',(-103.482191509604,1.04635460655848,135.611962334943));
#99450=CARTESIAN_POINT('Ctrl Pts',(-103.489964409869,1.17914683236046,135.579169075529));
#99451=CARTESIAN_POINT('Ctrl Pts',(-103.497454745631,1.30711172627074,135.547567933695));
#99452=CARTESIAN_POINT('Ctrl Pts',(-103.504945081393,1.43364180459688,135.510859427408));
#99453=CARTESIAN_POINT('Ctrl Pts',(-103.512435417155,1.55831097958705,135.469213236181));
#99454=CARTESIAN_POINT('Ctrl Pts',(-103.520209751274,1.68770702423953,135.425988016955));
#99455=CARTESIAN_POINT('Ctrl Pts',(-103.527984085393,1.81550815543012,135.377306372377));
#99456=CARTESIAN_POINT('Ctrl Pts',(-103.535758419512,1.94121978685523,135.32330394556));
#99457=CARTESIAN_POINT('Ctrl Pts',(-103.543523172459,2.06677648993011,135.269368071908));
#99458=CARTESIAN_POINT('Ctrl Pts',(-103.551287925407,2.19024846118948,135.210124616096));
#99459=CARTESIAN_POINT('Ctrl Pts',(-103.559052678354,2.31115638888255,135.145758918647));
#99460=CARTESIAN_POINT('Ctrl Pts',(-103.566809719239,2.43194422911701,135.081457150116));
#99461=CARTESIAN_POINT('Ctrl Pts',(-103.574566760124,2.55017275084561,135.012043446798));
#99462=CARTESIAN_POINT('Ctrl Pts',(-103.582323801009,2.66538308397759,134.93775100297));
#99463=CARTESIAN_POINT('Ctrl Pts',(-103.590074992249,2.7805065361013,134.863514583651));
#99464=CARTESIAN_POINT('Ctrl Pts',(-103.597826183489,2.8926160027019,134.78440695786));
#99465=CARTESIAN_POINT('Ctrl Pts',(-103.605577374729,3.00127799507205,134.700706785298));
#99466=CARTESIAN_POINT('Ctrl Pts',(-103.613325271506,3.10989380319664,134.617042187542));
#99467=CARTESIAN_POINT('Ctrl Pts',(-103.621073168283,3.21506474231533,134.528789163384));
#99468=CARTESIAN_POINT('Ctrl Pts',(-103.62882106506,3.31638725234764,134.436269021555));
#99469=CARTESIAN_POINT('Ctrl Pts',(-103.636567341144,3.41768856789512,134.343768232945));
#99470=CARTESIAN_POINT('Ctrl Pts',(-103.644313617229,3.5151427670346,134.247002365534));
#99471=CARTESIAN_POINT('Ctrl Pts',(-103.652059893313,3.60838058162866,134.146331987974));
#99472=CARTESIAN_POINT('Ctrl Pts',(-103.659806226578,3.70161908448321,134.045660867287));
#99473=CARTESIAN_POINT('Ctrl Pts',(-103.667552559843,3.79064087502338,133.941085465779));
#99474=CARTESIAN_POINT('Ctrl Pts',(-103.675298893109,3.87511494576002,133.833001768255));
#99475=CARTESIAN_POINT('Ctrl Pts',(-103.683046961112,3.95960793387923,133.724893866136));
#99476=CARTESIAN_POINT('Ctrl Pts',(-103.690795029115,4.03955093492755,133.613276412616));
#99477=CARTESIAN_POINT('Ctrl Pts',(-103.698543097118,4.11465472918241,133.498576555852));
#99478=CARTESIAN_POINT('Ctrl Pts',(-103.706299399859,4.18983834464345,133.383754794717));
#99479=CARTESIAN_POINT('Ctrl Pts',(-103.714055702601,4.26017226476969,133.265844413753));
#99480=CARTESIAN_POINT('Ctrl Pts',(-103.721812005343,4.3254116589225,133.145299968202));
#99481=CARTESIAN_POINT('Ctrl Pts',(-103.729572447857,4.39068587330446,133.024691184451));
#99482=CARTESIAN_POINT('Ctrl Pts',(-103.737332890372,4.4508599722224,132.901445885934));
#99483=CARTESIAN_POINT('Ctrl Pts',(-103.745093332886,4.50573666786875,132.776040140796));
#99484=CARTESIAN_POINT('Ctrl Pts',(-103.752866233151,4.56070145645852,132.650433083222));
#99485=CARTESIAN_POINT('Ctrl Pts',(-103.760639133417,4.61035170666361,132.522659013206));
#99486=CARTESIAN_POINT('Ctrl Pts',(-103.768412033682,4.65453925044116,132.393211595035));
#99487=CARTESIAN_POINT('Ctrl Pts',(-103.775902369444,4.69712046570032,132.268469916573));
#99488=CARTESIAN_POINT('Ctrl Pts',(-103.783392705206,4.73462915772616,132.142174733856));
#99489=CARTESIAN_POINT('Ctrl Pts',(-103.790883040968,4.76697777186086,132.0147762425));
#99490=CARTESIAN_POINT('Ctrl Pts',(-103.798657375087,4.80055289353287,131.882547398621));
#99491=CARTESIAN_POINT('Ctrl Pts',(-103.806431709206,4.82867528033846,131.748711069425));
#99492=CARTESIAN_POINT('Ctrl Pts',(-103.814206043325,4.85119171669166,131.613756682791));
#99493=CARTESIAN_POINT('Ctrl Pts',(-103.821970796272,4.87368040354941,131.478968615378));
#99494=CARTESIAN_POINT('Ctrl Pts',(-103.829735549219,4.89057682274961,131.343065614082));
#99495=CARTESIAN_POINT('Ctrl Pts',(-103.837500302166,4.90177782681263,131.206551118533));
#99496=CARTESIAN_POINT('Ctrl Pts',(-103.845257343052,4.91296770588052,131.070172211105));
#99497=CARTESIAN_POINT('Ctrl Pts',(-103.853014383937,4.91847339526769,130.933183405202));
#99498=CARTESIAN_POINT('Ctrl Pts',(-103.860771424822,4.91824305743001,130.796096808429));
#99499=CARTESIAN_POINT('Ctrl Pts',(-103.868522616062,4.91801289329189,130.659113589724));
#99500=CARTESIAN_POINT('Ctrl Pts',(-103.876273807302,4.91205531239327,130.522033116316));
#99501=CARTESIAN_POINT('Ctrl Pts',(-103.884024998542,4.90037044779738,130.385370716907));
#99502=CARTESIAN_POINT('Ctrl Pts',(-103.891772895319,4.88869054958068,130.248766402664));
#99503=CARTESIAN_POINT('Ctrl Pts',(-103.899520792096,4.87128824243807,130.11258019773));
#99504=CARTESIAN_POINT('Ctrl Pts',(-103.907268688873,4.84821571842312,129.977325303849));
#99505=CARTESIAN_POINT('Ctrl Pts',(-103.915014964957,4.82514802068279,129.842098702376));
#99506=CARTESIAN_POINT('Ctrl Pts',(-103.922761241041,4.79641253096411,129.70780340962));
#99507=CARTESIAN_POINT('Ctrl Pts',(-103.930507517126,4.7621130074377,129.574944997488));
#99508=CARTESIAN_POINT('Ctrl Pts',(-103.938253850391,4.72781323071985,129.442085604624));
#99509=CARTESIAN_POINT('Ctrl Pts',(-103.946000183656,4.68794943596679,129.310663492103));
#99510=CARTESIAN_POINT('Ctrl Pts',(-103.953746516922,4.6426758587771,129.181171185359));
#99511=CARTESIAN_POINT('Ctrl Pts',(-103.961494584925,4.59739214288389,129.051649879711));
#99512=CARTESIAN_POINT('Ctrl Pts',(-103.969242652928,4.54669636284973,128.924059608791));
#99513=CARTESIAN_POINT('Ctrl Pts',(-103.976990720931,4.49079156019326,128.798874585354));
#99514=CARTESIAN_POINT('Ctrl Pts',(-103.984747023672,4.43482734124717,128.673556513785));
#99515=CARTESIAN_POINT('Ctrl Pts',(-103.992503326414,4.37364320017627,128.55064915379));
#99516=CARTESIAN_POINT('Ctrl Pts',(-104.000259629156,4.30748923023899,128.430604186532));
#99517=CARTESIAN_POINT('Ctrl Pts',(-104.00802007167,4.24129995193592,128.31049514766));
#99518=CARTESIAN_POINT('Ctrl Pts',(-104.015780514185,4.17013576210445,128.193251879739));
#99519=CARTESIAN_POINT('Ctrl Pts',(-104.023540956699,4.09429055147871,128.07929769305));
#99520=CARTESIAN_POINT('Ctrl Pts',(-104.031313856964,4.01832358738785,127.965160576984));
#99521=CARTESIAN_POINT('Ctrl Pts',(-104.03908675723,3.93766081654446,127.85432340942));
#99522=CARTESIAN_POINT('Ctrl Pts',(-104.046859657495,3.85263748424759,127.747177685933));
#99523=CARTESIAN_POINT('Ctrl Pts',(-104.054349993257,3.77070496424125,127.643926979379));
#99524=CARTESIAN_POINT('Ctrl Pts',(-104.061840329019,3.68472361439727,127.544104223287));
#99525=CARTESIAN_POINT('Ctrl Pts',(-104.069330664781,3.59502487160512,127.448026421596));
#99526=CARTESIAN_POINT('Ctrl Pts',(-104.0771049989,3.50192517371625,127.348305800851));
#99527=CARTESIAN_POINT('Ctrl Pts',(-104.084879333019,3.40452571651778,127.252303835299));
#99528=CARTESIAN_POINT('Ctrl Pts',(-104.092653667138,3.30315545277988,127.160413977277));
#99529=CARTESIAN_POINT('Ctrl Pts',(-104.100418420085,3.20191011883204,127.068637365293));
#99530=CARTESIAN_POINT('Ctrl Pts',(-104.108183173032,3.09670400216443,126.980963037472));
#99531=CARTESIAN_POINT('Ctrl Pts',(-104.115947925979,2.98790490706331,126.897749896129));
#99532=CARTESIAN_POINT('Ctrl Pts',(-104.123704966864,2.87921387275754,126.814619403251));
#99533=CARTESIAN_POINT('Ctrl Pts',(-104.131462007749,2.76693727022471,126.735941515112));
#99534=CARTESIAN_POINT('Ctrl Pts',(-104.139219048634,2.65147793063793,126.662036650776));
#99535=CARTESIAN_POINT('Ctrl Pts',(-104.146970239874,2.53610565983744,126.588187518674));
#99536=CARTESIAN_POINT('Ctrl Pts',(-104.154721431115,2.41755575724214,126.519104455958));
#99537=CARTESIAN_POINT('Ctrl Pts',(-104.162472622355,2.29626185540724,126.45506589843));
#99538=CARTESIAN_POINT('Ctrl Pts',(-104.170220519132,2.17501950671576,126.391054558997));
#99539=CARTESIAN_POINT('Ctrl Pts',(-104.177968415909,2.05103582342604,126.332083642556));
#99540=CARTESIAN_POINT('Ctrl Pts',(-104.185716312686,1.92477078777817,126.27838663653));
#99541=CARTESIAN_POINT('Ctrl Pts',(-104.19346258877,1.79853216405381,126.22470086276));
#99542=CARTESIAN_POINT('Ctrl Pts',(-104.201208864854,1.67001349672181,126.176286958012));
#99543=CARTESIAN_POINT('Ctrl Pts',(-104.208955140938,1.5396962215709,126.133330901563));
#99544=CARTESIAN_POINT('Ctrl Pts',(-104.216701474203,1.40937798444764,126.090374528023));
#99545=CARTESIAN_POINT('Ctrl Pts',(-104.224447807469,1.27726148432534,126.052876205568));
#99546=CARTESIAN_POINT('Ctrl Pts',(-104.232194140734,1.14384446491003,126.020972393452));
#99547=CARTESIAN_POINT('Ctrl Pts',(-104.239942208737,1.01039756767809,125.989061436698));
#99548=CARTESIAN_POINT('Ctrl Pts',(-104.24769027674,0.875649951786629,125.962747574221));
#99549=CARTESIAN_POINT('Ctrl Pts',(-104.255438344743,0.740110334758956,
125.94211630502));
#99550=CARTESIAN_POINT('Ctrl Pts',(-104.263194647485,0.604426664613549,
125.921463108661));
#99551=CARTESIAN_POINT('Ctrl Pts',(-104.270950950227,0.467949698978643,
125.906504629113));
#99552=CARTESIAN_POINT('Ctrl Pts',(-104.278707252969,0.331194631522968,
125.897274600534));
#99553=CARTESIAN_POINT('Ctrl Pts',(-104.286467695483,0.194366573769804,
125.888039645611));
#99554=CARTESIAN_POINT('Ctrl Pts',(-104.294228137997,0.0572605090805218,
125.884539243853));
#99555=CARTESIAN_POINT('Ctrl Pts',(-104.301988580511,-0.0796085644963637,
125.886754946209));
#99556=CARTESIAN_POINT('Ctrl Pts',(-104.309761480777,-0.216697352460448,
125.888974205407));
#99557=CARTESIAN_POINT('Ctrl Pts',(-104.317534381042,-0.353547998542257,
125.896927882589));
#99558=CARTESIAN_POINT('Ctrl Pts',(-104.325307281307,-0.48964991815302,
125.910545539311));
#99559=CARTESIAN_POINT('Ctrl Pts',(-104.332797617069,-0.620804190168828,
125.923668159911));
#99560=CARTESIAN_POINT('Ctrl Pts',(-104.340287952832,-0.751262921802112,
125.942050066679));
#99561=CARTESIAN_POINT('Ctrl Pts',(-104.347778288594,-0.880580258925905,
125.965583760747));
#99562=CARTESIAN_POINT('Ctrl Pts',(-104.355552622713,-1.01480070218907,
125.990009741977));
#99563=CARTESIAN_POINT('Ctrl Pts',(-104.363326956832,-1.14821666045444,
126.020063256455));
#99564=CARTESIAN_POINT('Ctrl Pts',(-104.371101290951,-1.28031930412125,
126.055680217498));
#99565=CARTESIAN_POINT('Ctrl Pts',(-104.378866043898,-1.41225914308646,
126.091253283819));
#99566=CARTESIAN_POINT('Ctrl Pts',(-104.386630796845,-1.54288851400916,
126.132376053612));
#99567=CARTESIAN_POINT('Ctrl Pts',(-104.394395549792,-1.67170665500806,
126.178933078181));
#99568=CARTESIAN_POINT('Ctrl Pts',(-104.402152590677,-1.8003968520133,126.225443861657));
#99569=CARTESIAN_POINT('Ctrl Pts',(-104.409909631562,-1.92727903375607,
126.277378026853));
#99570=CARTESIAN_POINT('Ctrl Pts',(-104.417666672447,-2.05186588251464,
126.334569854826));
#99571=CARTESIAN_POINT('Ctrl Pts',(-104.425417863688,-2.17635877936091,
126.391718553997));
#99572=CARTESIAN_POINT('Ctrl Pts',(-104.433169054928,-2.29855943465286,
126.454116861713));
#99573=CARTESIAN_POINT('Ctrl Pts',(-104.440920246168,-2.41799920347746,
126.521550451976));
#99574=CARTESIAN_POINT('Ctrl Pts',(-104.448668142945,-2.53738820721431,
126.588955381164));
#99575=CARTESIAN_POINT('Ctrl Pts',(-104.456416039722,-2.65401831864758,
126.661391144535));
#99576=CARTESIAN_POINT('Ctrl Pts',(-104.464163936499,-2.7674444665579,126.738596951658));
#99577=CARTESIAN_POINT('Ctrl Pts',(-104.471910212583,-2.88084688816326,
126.81578660899));
#99578=CARTESIAN_POINT('Ctrl Pts',(-104.479656488667,-2.99104635631646,
126.897744105563));
#99579=CARTESIAN_POINT('Ctrl Pts',(-104.487402764751,-3.09762617358104,
126.984164922154));
#99580=CARTESIAN_POINT('Ctrl Pts',(-104.495149098017,-3.20420677759376,
127.070586376684));
#99581=CARTESIAN_POINT('Ctrl Pts',(-104.502895431282,-3.3071673737233,127.161470970737));
#99582=CARTESIAN_POINT('Ctrl Pts',(-104.510641764547,-3.4061241123059,127.256473697994));
#99583=CARTESIAN_POINT('Ctrl Pts',(-104.51838983255,-3.50510301156412,127.351497700454));
#99584=CARTESIAN_POINT('Ctrl Pts',(-104.526137900553,-3.60007598709598,
127.450641400534));
#99585=CARTESIAN_POINT('Ctrl Pts',(-104.533885968556,-3.69069613192513,
127.553523014072));
#99586=CARTESIAN_POINT('Ctrl Pts',(-104.541642271298,-3.78141258892249,
127.656513971412));
#99587=CARTESIAN_POINT('Ctrl Pts',(-104.54939857404,-3.86776671497381,127.763250484252));
#99588=CARTESIAN_POINT('Ctrl Pts',(-104.557154876782,-3.94945165381305,
127.873317339705));
#99589=CARTESIAN_POINT('Ctrl Pts',(-104.564915319296,-4.03118019036386,
127.983442941153));
#99590=CARTESIAN_POINT('Ctrl Pts',(-104.57267576181,-4.10823435446561,128.09690210377));
#99591=CARTESIAN_POINT('Ctrl Pts',(-104.580436204324,-4.18035129880294,
128.213251572949));
#99592=CARTESIAN_POINT('Ctrl Pts',(-104.58820910459,-4.25258401166136,128.329787816625));
#99593=CARTESIAN_POINT('Ctrl Pts',(-104.595982004855,-4.31986347475862,
128.449223297781));
#99594=CARTESIAN_POINT('Ctrl Pts',(-104.603754905121,-4.38197296650989,
128.571090373445));
#99595=CARTESIAN_POINT('Ctrl Pts',(-104.611245240883,-4.44182462179129,
128.688527273943));
#99596=CARTESIAN_POINT('Ctrl Pts',(-104.618735576645,-4.49687553410252,
128.808221769257));
#99597=CARTESIAN_POINT('Ctrl Pts',(-104.626225912407,-4.54697515024065,
128.92974064392));
#99598=CARTESIAN_POINT('Ctrl Pts',(-104.634929516994,-4.605189796778,129.070942890192));
#99599=CARTESIAN_POINT('Ctrl Pts',(-104.643633121581,-4.65687583065861,
129.214986364832));
#99600=CARTESIAN_POINT('Ctrl Pts',(-104.652336726168,-4.7017783882902,129.361286451105));
#99601=CARTESIAN_POINT('Ctrl Pts',(-104.656691217814,-4.72424354168428,
129.434481699951));
#99602=CARTESIAN_POINT('Ctrl Pts',(-104.661045709461,-4.74501143990967,
129.508241406951));
#99603=CARTESIAN_POINT('Ctrl Pts',(-104.665400201108,-4.76405452823405,
129.582490119308));
#99604=CARTESIAN_POINT('Ctrl Pts',(-102.915060258535,-4.76405452823397,
129.582490119308));
#99605=CARTESIAN_POINT('Ctrl Pts',(-102.92283380042,-4.7981027709504,129.715243700905));
#99606=CARTESIAN_POINT('Ctrl Pts',(-102.930607342304,-4.82655979954569,
129.849272768635));
#99607=CARTESIAN_POINT('Ctrl Pts',(-102.938380884189,-4.84936084534268,
129.984066490952));
#99608=CARTESIAN_POINT('Ctrl Pts',(-102.944100645969,-4.86613782451462,
130.083247532556));
#99609=CARTESIAN_POINT('Ctrl Pts',(-102.949820407749,-4.87985373792882,
130.182842392454));
#99610=CARTESIAN_POINT('Ctrl Pts',(-102.955540169529,-4.89050080230448,
130.282647128034));
#99611=CARTESIAN_POINT('Ctrl Pts',(-102.965406967689,-4.90886737756294,
130.454813945338));
#99612=CARTESIAN_POINT('Ctrl Pts',(-102.975273765849,-4.91814467604707,
130.627967458999));
#99613=CARTESIAN_POINT('Ctrl Pts',(-102.985140564009,-4.91824910835159,
130.80139908101));
#99614=CARTESIAN_POINT('',(-102.639859435943,-4.91824800921729,130.808785810233));
#99615=CARTESIAN_POINT('Ctrl Pts',(-102.569791376202,-4.76405452823412,
129.582490119309));
#99616=CARTESIAN_POINT('Ctrl Pts',(-102.577430973814,-4.79768656643153,
129.713620925803));
#99617=CARTESIAN_POINT('Ctrl Pts',(-102.585070571426,-4.82588986934994,
129.846100596011));
#99618=CARTESIAN_POINT('Ctrl Pts',(-102.592710169038,-4.84857485260586,
129.979433371575));
#99619=CARTESIAN_POINT('Ctrl Pts',(-102.600568380189,-4.871908985819,130.116581577134));
#99620=CARTESIAN_POINT('Ctrl Pts',(-102.60842659134,-4.88940415632356,130.254631994833));
#99621=CARTESIAN_POINT('Ctrl Pts',(-102.616284802491,-4.9010200776338,130.393039257641));
#99622=CARTESIAN_POINT('Ctrl Pts',(-102.624143013642,-4.91263599894403,
130.531446520449));
#99623=CARTESIAN_POINT('Ctrl Pts',(-102.632001224793,-4.91837269262525,
130.670210166371));
#99624=CARTESIAN_POINT('Ctrl Pts',(-102.639859435943,-4.91824800921729,
130.808785810233));
#99625=CARTESIAN_POINT('Ctrl Pts',(-102.639859435992,-4.91824800921652,
130.80878581109));
#99626=CARTESIAN_POINT('Ctrl Pts',(-102.650907811304,-4.91807270858805,
131.0036184127));
#99627=CARTESIAN_POINT('Ctrl Pts',(-102.661956186616,-4.90631686207873,
131.197951502016));
#99628=CARTESIAN_POINT('Ctrl Pts',(-102.673004561928,-4.88317768197775,
131.390670082554));
#99629=CARTESIAN_POINT('Ctrl Pts',(-102.680896888577,-4.86664837675505,
131.528337200658));
#99630=CARTESIAN_POINT('Ctrl Pts',(-102.688789215226,-4.84431127361759,
131.665181352765));
#99631=CARTESIAN_POINT('Ctrl Pts',(-102.696681541875,-4.81625191044857,
131.800804593713));
#99632=CARTESIAN_POINT('Ctrl Pts',(-102.704455875994,-4.78861204274581,
131.934400228606));
#99633=CARTESIAN_POINT('Ctrl Pts',(-102.712230210113,-4.7553655678073,132.067056564891));
#99634=CARTESIAN_POINT('Ctrl Pts',(-102.720004544232,-4.71658876436888,
132.198266457402));
#99635=CARTESIAN_POINT('Ctrl Pts',(-102.727769297179,-4.67785974987522,
132.329314645447));
#99636=CARTESIAN_POINT('Ctrl Pts',(-102.735534050127,-4.6336140777068,132.458919565251));
#99637=CARTESIAN_POINT('Ctrl Pts',(-102.743298803074,-4.58397918021763,
132.58658336959));
#99638=CARTESIAN_POINT('Ctrl Pts',(-102.751055843959,-4.53439358080839,
132.714120376438));
#99639=CARTESIAN_POINT('Ctrl Pts',(-102.758812884844,-4.47942954885954,
132.839719742481));
#99640=CARTESIAN_POINT('Ctrl Pts',(-102.766569925729,-4.41926444987399,
132.962898267129));
#99641=CARTESIAN_POINT('Ctrl Pts',(-102.774321116969,-4.35914472185735,
133.085983901894));
#99642=CARTESIAN_POINT('Ctrl Pts',(-102.782072308209,-4.29383190452954,
133.206651979083));
#99643=CARTESIAN_POINT('Ctrl Pts',(-102.789823499449,-4.22355150835399,
133.324439131974));
#99644=CARTESIAN_POINT('Ctrl Pts',(-102.797571396226,-4.15330098322189,
133.442176222183));
#99645=CARTESIAN_POINT('Ctrl Pts',(-102.805319293003,-4.07808727847184,
133.557034488432));
#99646=CARTESIAN_POINT('Ctrl Pts',(-102.81306718978,-3.99818178991451,133.668575245923));
#99647=CARTESIAN_POINT('Ctrl Pts',(-102.820813465864,-3.91829301586261,
133.780092671493));
#99648=CARTESIAN_POINT('Ctrl Pts',(-102.828559741948,-3.83371463764168,
133.888293650986));
#99649=CARTESIAN_POINT('Ctrl Pts',(-102.836306018033,-3.74476108636928,
133.992768914587));
#99650=CARTESIAN_POINT('Ctrl Pts',(-102.844052351298,-3.6558068784621,134.097244949401));
#99651=CARTESIAN_POINT('Ctrl Pts',(-102.851798684563,-3.56247768651339,
134.197994915762));
#99652=CARTESIAN_POINT('Ctrl Pts',(-102.859545017829,-3.46512762882175,
134.294643353746));
#99653=CARTESIAN_POINT('Ctrl Pts',(-102.867293085832,-3.36775577025954,
134.391313435478));
#99654=CARTESIAN_POINT('Ctrl Pts',(-102.875041153835,-3.26636153157214,
134.483879885707));
#99655=CARTESIAN_POINT('Ctrl Pts',(-102.882789221838,-3.16133491178896,
134.572005059124));
#99656=CARTESIAN_POINT('Ctrl Pts',(-102.89054552458,-3.05619666846459,134.660223893025));
#99657=CARTESIAN_POINT('Ctrl Pts',(-102.898301827321,-2.94741863218222,
134.743991769218));
#99658=CARTESIAN_POINT('Ctrl Pts',(-102.906058130063,-2.83542325996239,
134.82301188377));
#99659=CARTESIAN_POINT('Ctrl Pts',(-102.913818572577,-2.7233681124403,134.902074173737));
#99660=CARTESIAN_POINT('Ctrl Pts',(-102.921579015091,-2.60809253578269,
134.976383441081));
#99661=CARTESIAN_POINT('Ctrl Pts',(-102.929339457606,-2.49004596456064,
135.045687551071));
#99662=CARTESIAN_POINT('Ctrl Pts',(-102.937112357871,-2.37180989450277,
135.115102914171));
#99663=CARTESIAN_POINT('Ctrl Pts',(-102.944885258137,-2.25079428620926,
135.179496880217));
#99664=CARTESIAN_POINT('Ctrl Pts',(-102.952658158402,-2.12747184870504,
135.238664012178));
#99665=CARTESIAN_POINT('Ctrl Pts',(-102.960148494165,-2.00863249242518,
135.295680269864));
#99666=CARTESIAN_POINT('Ctrl Pts',(-102.967638829927,-1.88765139605412,
135.347842991023));
#99667=CARTESIAN_POINT('Ctrl Pts',(-102.97512916569,-1.76496526316726,135.395012061785));
#99668=CARTESIAN_POINT('Ctrl Pts',(-102.982903499809,-1.63762744827224,
135.443969562199));
#99669=CARTESIAN_POINT('Ctrl Pts',(-102.990677833928,-1.50804938373783,
135.487702351316));
#99670=CARTESIAN_POINT('Ctrl Pts',(-102.998452168047,-1.3766989756758,135.526000480249));
#99671=CARTESIAN_POINT('Ctrl Pts',(-103.006216920994,-1.24551044525223,
135.56425141016));
#99672=CARTESIAN_POINT('Ctrl Pts',(-103.013981673941,-1.11255428905039,
135.597080897992));
#99673=CARTESIAN_POINT('Ctrl Pts',(-103.021746426889,-0.978318240339559,
135.624327057607));
#99674=CARTESIAN_POINT('Ctrl Pts',(-103.029503467774,-0.84421551676507,
135.651546155952));
#99675=CARTESIAN_POINT('Ctrl Pts',(-103.037260508659,-0.708835811114473,
135.673192884491));
#99676=CARTESIAN_POINT('Ctrl Pts',(-103.045017549544,-0.57268152411455,
135.689155284124));
#99677=CARTESIAN_POINT('Ctrl Pts',(-103.052768740784,-0.436629912121395,
135.705105646388));
#99678=CARTESIAN_POINT('Ctrl Pts',(-103.060519932024,-0.299805268164579,
135.715380166616));
#99679=CARTESIAN_POINT('Ctrl Pts',(-103.068271123264,-0.162719329704358,
135.719918112117));
#99680=CARTESIAN_POINT('Ctrl Pts',(-103.076019020041,-0.0256916564250546,
135.724454128871));
#99681=CARTESIAN_POINT('Ctrl Pts',(-103.083766916818,0.111596700540384,
135.723258407377));
#99682=CARTESIAN_POINT('Ctrl Pts',(-103.091514813595,0.24862996718179,135.71632216077));
#99683=CARTESIAN_POINT('Ctrl Pts',(-103.09926108968,0.385634569417911,135.709387365077));
#99684=CARTESIAN_POINT('Ctrl Pts',(-103.107007365764,0.522383797246825,
135.696714452466));
#99685=CARTESIAN_POINT('Ctrl Pts',(-103.114753641848,0.658363362681601,
135.678346742411));
#99686=CARTESIAN_POINT('Ctrl Pts',(-103.122499975113,0.794343931886825,
135.659978896769));
#99687=CARTESIAN_POINT('Ctrl Pts',(-103.130246308379,0.92955443991439,135.635916222134));
#99688=CARTESIAN_POINT('Ctrl Pts',(-103.137992641644,1.06348759210629,135.606253703));
#99689=CARTESIAN_POINT('Ctrl Pts',(-103.145740709647,1.1974507376988,135.57658454115));
#99690=CARTESIAN_POINT('Ctrl Pts',(-103.15348877765,1.33013557659674,135.541313123917));
#99691=CARTESIAN_POINT('Ctrl Pts',(-103.161236845653,1.4610472342378,135.500585062993));
#99692=CARTESIAN_POINT('Ctrl Pts',(-103.168993148395,1.59209802634665,135.459813715801));
#99693=CARTESIAN_POINT('Ctrl Pts',(-103.176749451137,1.72137149867967,135.413574256348));
#99694=CARTESIAN_POINT('Ctrl Pts',(-103.184505753879,1.84838959334207,135.362061679914));
#99695=CARTESIAN_POINT('Ctrl Pts',(-103.192266196393,1.97547548138603,135.310521609666));
#99696=CARTESIAN_POINT('Ctrl Pts',(-103.200026638907,2.10030323749682,135.253702976353));
#99697=CARTESIAN_POINT('Ctrl Pts',(-103.207787081421,2.22241780321864,135.191847617027));
#99698=CARTESIAN_POINT('Ctrl Pts',(-103.215559981687,2.34472839808219,135.129892961986));
#99699=CARTESIAN_POINT('Ctrl Pts',(-103.223332881952,2.46431675770193,135.062885614945));
#99700=CARTESIAN_POINT('Ctrl Pts',(-103.231105782218,2.58075453130965,134.991112235661));
#99701=CARTESIAN_POINT('Ctrl Pts',(-103.238596117979,2.6929594985498,134.921947999505));
#99702=CARTESIAN_POINT('Ctrl Pts',(-103.246086453741,2.80223871088605,134.848358401708));
#99703=CARTESIAN_POINT('Ctrl Pts',(-103.253576789502,2.90823823760139,134.770635118386));
#99704=CARTESIAN_POINT('Ctrl Pts',(-103.261351123621,3.01825676859669,134.689964933148));
#99705=CARTESIAN_POINT('Ctrl Pts',(-103.26912545774,3.12509051165878,134.604585878365));
#99706=CARTESIAN_POINT('Ctrl Pts',(-103.276899791859,3.22830991615819,134.514778134199));
#99707=CARTESIAN_POINT('Ctrl Pts',(-103.284664544806,3.33140211196653,134.42508107005));
#99708=CARTESIAN_POINT('Ctrl Pts',(-103.292429297753,3.43088853991979,134.330966430403));
#99709=CARTESIAN_POINT('Ctrl Pts',(-103.3001940507,3.5263693688808,134.232757055658));
#99710=CARTESIAN_POINT('Ctrl Pts',(-103.307951091585,3.62175536493645,134.134645223848));
#99711=CARTESIAN_POINT('Ctrl Pts',(-103.31570813247,3.71314340846088,134.032447028859));
#99712=CARTESIAN_POINT('Ctrl Pts',(-103.323465173355,3.80016774522769,133.926524638022));
#99713=CARTESIAN_POINT('Ctrl Pts',(-103.331216364596,3.88712645626532,133.820682124084));
#99714=CARTESIAN_POINT('Ctrl Pts',(-103.338967555836,3.9697277633093,133.711121305202));
#99715=CARTESIAN_POINT('Ctrl Pts',(-103.346718747076,4.04764396362877,133.598239893089));
#99716=CARTESIAN_POINT('Ctrl Pts',(-103.354466643853,4.12552704748452,133.485406458589));
#99717=CARTESIAN_POINT('Ctrl Pts',(-103.36221454063,4.1987287635222,133.369255558992));
#99718=CARTESIAN_POINT('Ctrl Pts',(-103.369962437407,4.26696293065056,133.250216380066));
#99719=CARTESIAN_POINT('Ctrl Pts',(-103.377708713491,4.33518282466211,133.131202101569));
#99720=CARTESIAN_POINT('Ctrl Pts',(-103.385454989575,4.39843704229483,133.00930108444));
#99721=CARTESIAN_POINT('Ctrl Pts',(-103.393201265659,4.45648404422802,132.884969428958));
#99722=CARTESIAN_POINT('Ctrl Pts',(-103.400947598925,4.5145314746509,132.760636855688));
#99723=CARTESIAN_POINT('Ctrl Pts',(-103.40869393219,4.56737144727976,132.633873962522));
#99724=CARTESIAN_POINT('Ctrl Pts',(-103.416440265455,4.61480967010514,132.505158892261));
#99725=CARTESIAN_POINT('Ctrl Pts',(-103.424188333458,4.66225851639168,132.376414997152));
#99726=CARTESIAN_POINT('Ctrl Pts',(-103.431936401461,4.70430307056754,132.245718421791));
#99727=CARTESIAN_POINT('Ctrl Pts',(-103.439684469464,4.74079834808433,132.113564224841));
#99728=CARTESIAN_POINT('Ctrl Pts',(-103.447440772206,4.77733241321632,131.981269572837));
#99729=CARTESIAN_POINT('Ctrl Pts',(-103.455197074948,4.80830531588587,131.847514582053));
#99730=CARTESIAN_POINT('Ctrl Pts',(-103.462953377689,4.83362270917481,131.712806855848));
#99731=CARTESIAN_POINT('Ctrl Pts',(-103.470713820204,4.85895361511892,131.578027232074));
#99732=CARTESIAN_POINT('Ctrl Pts',(-103.478474262718,4.87862294099198,131.442294246375));
#99733=CARTESIAN_POINT('Ctrl Pts',(-103.486234705232,4.89258818094349,131.306121471153));
#99734=CARTESIAN_POINT('Ctrl Pts',(-103.494007605497,4.90657583913795,131.169730099303));
#99735=CARTESIAN_POINT('Ctrl Pts',(-103.501780505763,4.91484108980973,131.032897917616));
#99736=CARTESIAN_POINT('Ctrl Pts',(-103.509553406028,4.91739357387722,130.896140256327));
#99737=CARTESIAN_POINT('Ctrl Pts',(-103.51704374179,4.91985326871964,130.764354080491));
#99738=CARTESIAN_POINT('Ctrl Pts',(-103.524534077553,4.91700833948822,130.632637409056));
#99739=CARTESIAN_POINT('Ctrl Pts',(-103.532024413315,4.90891287336266,130.501445672021));
#99740=CARTESIAN_POINT('Ctrl Pts',(-103.539798747434,4.90051046517871,130.365279760408));
#99741=CARTESIAN_POINT('Ctrl Pts',(-103.547573081553,4.88642489601396,130.229248042071));
#99742=CARTESIAN_POINT('Ctrl Pts',(-103.555347415672,4.86665970676502,130.093863354341));
#99743=CARTESIAN_POINT('Ctrl Pts',(-103.563112168619,4.84691887634537,129.95864551614));
#99744=CARTESIAN_POINT('Ctrl Pts',(-103.570876921566,4.82151240894448,129.824073505093));
#99745=CARTESIAN_POINT('Ctrl Pts',(-103.578641674513,4.79049580083954,129.690658213582));
#99746=CARTESIAN_POINT('Ctrl Pts',(-103.586398715398,4.75950999886703,129.557375432021));
#99747=CARTESIAN_POINT('Ctrl Pts',(-103.594155756284,4.72292523282126,129.425247462038));
#99748=CARTESIAN_POINT('Ctrl Pts',(-103.601912797169,4.68084850524219,129.294777783313));
#99749=CARTESIAN_POINT('Ctrl Pts',(-103.609663988409,4.63880350805062,129.164406492787));
#99750=CARTESIAN_POINT('Ctrl Pts',(-103.617415179649,4.59127491230719,129.035691375002));
#99751=CARTESIAN_POINT('Ctrl Pts',(-103.625166370889,4.5384201928109,128.909123108443));
#99752=CARTESIAN_POINT('Ctrl Pts',(-103.632914267666,4.48558793798041,128.782608636774));
#99753=CARTESIAN_POINT('Ctrl Pts',(-103.640662164443,4.42743421215485,128.658239561515));
#99754=CARTESIAN_POINT('Ctrl Pts',(-103.64841006122,4.36416541360402,128.536488640315));
#99755=CARTESIAN_POINT('Ctrl Pts',(-103.656156337304,4.30090984952192,128.414763186782));
#99756=CARTESIAN_POINT('Ctrl Pts',(-103.663902613388,4.23254152109466,128.295655144678));
#99757=CARTESIAN_POINT('Ctrl Pts',(-103.671648889472,4.15931360050365,128.179614261217));
#99758=CARTESIAN_POINT('Ctrl Pts',(-103.679395222738,4.08608513936066,128.063572521169));
#99759=CARTESIAN_POINT('Ctrl Pts',(-103.687141556003,4.00799722312143,127.950598315578));
#99760=CARTESIAN_POINT('Ctrl Pts',(-103.694887889269,3.92534710729005,127.841113555678));
#99761=CARTESIAN_POINT('Ctrl Pts',(-103.702635957271,3.84267848253841,127.731604277425));
#99762=CARTESIAN_POINT('Ctrl Pts',(-103.710384025275,3.75544586069529,127.625586311809));
#99763=CARTESIAN_POINT('Ctrl Pts',(-103.718132093277,3.66398738094329,127.523449229737));
#99764=CARTESIAN_POINT('Ctrl Pts',(-103.725888396019,3.57243169803076,127.421203595158));
#99765=CARTESIAN_POINT('Ctrl Pts',(-103.733644698761,3.47664144659419,127.322847375278));
#99766=CARTESIAN_POINT('Ctrl Pts',(-103.741401001503,3.37699269090074,127.228734318845));
#99767=CARTESIAN_POINT('Ctrl Pts',(-103.749161444017,3.27729074966573,127.13457103144));
#99768=CARTESIAN_POINT('Ctrl Pts',(-103.756921886531,3.17372649572347,127.044655676286));
#99769=CARTESIAN_POINT('Ctrl Pts',(-103.764682329046,3.06670903662881,126.959301613187));
#99770=CARTESIAN_POINT('Ctrl Pts',(-103.772455229311,2.95951978360825,126.873810532167));
#99771=CARTESIAN_POINT('Ctrl Pts',(-103.780228129576,2.84886656374427,126.79289560618));
#99772=CARTESIAN_POINT('Ctrl Pts',(-103.788001029842,2.73518815010882,126.716827272625));
#99773=CARTESIAN_POINT('Ctrl Pts',(-103.795491365604,2.62564223314736,126.643524214599));
#99774=CARTESIAN_POINT('Ctrl Pts',(-103.802981701366,2.51328751332149,126.574721655867));
#99775=CARTESIAN_POINT('Ctrl Pts',(-103.810472037128,2.39853639223181,126.510620262393));
#99776=CARTESIAN_POINT('Ctrl Pts',(-103.818246371247,2.27943444750834,126.444088445102));
#99777=CARTESIAN_POINT('Ctrl Pts',(-103.826020705366,2.15737351606003,126.382410566844));
#99778=CARTESIAN_POINT('Ctrl Pts',(-103.833795039485,2.03278697639856,126.325860849666));
#99779=CARTESIAN_POINT('Ctrl Pts',(-103.841559792432,1.9083539785126,126.26938082496));
#99780=CARTESIAN_POINT('Ctrl Pts',(-103.84932454538,1.7814019181233,126.218016546457));
#99781=CARTESIAN_POINT('Ctrl Pts',(-103.857089298327,1.65239062055459,126.171997473381));
#99782=CARTESIAN_POINT('Ctrl Pts',(-103.864846339212,1.52350745882537,126.126024107097));
#99783=CARTESIAN_POINT('Ctrl Pts',(-103.872603380097,1.39256949593961,126.085385511725));
#99784=CARTESIAN_POINT('Ctrl Pts',(-103.880360420982,1.26005816109676,126.050263806062));
#99785=CARTESIAN_POINT('Ctrl Pts',(-103.888111612222,1.12764675408248,126.015168585951));
#99786=CARTESIAN_POINT('Ctrl Pts',(-103.895862803462,0.993664713138639,
125.985582074425));
#99787=CARTESIAN_POINT('Ctrl Pts',(-103.903613994702,0.858609978946894,
125.961637007184));
#99788=CARTESIAN_POINT('Ctrl Pts',(-103.911361891479,0.723612646619699,
125.937702117235));
#99789=CARTESIAN_POINT('Ctrl Pts',(-103.919109788256,0.587543911996632,
125.91940397071));
#99790=CARTESIAN_POINT('Ctrl Pts',(-103.926857685033,0.450913082781708,
125.906824455956));
#99791=CARTESIAN_POINT('Ctrl Pts',(-103.934603961118,0.314310833790836,
125.894247572565));
#99792=CARTESIAN_POINT('Ctrl Pts',(-103.942350237202,0.177147113149288,
125.88738697743));
#99793=CARTESIAN_POINT('Ctrl Pts',(-103.950096513286,0.0399371516740185,
125.886272768979));
#99794=CARTESIAN_POINT('Ctrl Pts',(-103.957842846551,-0.0972738226542039,
125.885158552304));
#99795=CARTESIAN_POINT('Ctrl Pts',(-103.965589179817,-0.23453064754495,
125.88979081013));
#99796=CARTESIAN_POINT('Ctrl Pts',(-103.973335513082,-0.371317683267096,
125.900147506312));
#99797=CARTESIAN_POINT('Ctrl Pts',(-103.981083581085,-0.508135351497291,
125.910506521805));
#99798=CARTESIAN_POINT('Ctrl Pts',(-103.988831649088,-0.644482631436312,
125.92659249707));
#99799=CARTESIAN_POINT('Ctrl Pts',(-103.996579717091,-0.779848993560361,
125.948331518627));
#99800=CARTESIAN_POINT('Ctrl Pts',(-104.004336019833,-0.91535922466514,
125.970093644675));
#99801=CARTESIAN_POINT('Ctrl Pts',(-104.012092322575,-1.0498860687521,125.997520756801));
#99802=CARTESIAN_POINT('Ctrl Pts',(-104.019848625317,-1.18292863505851,
126.030487671324));
#99803=CARTESIAN_POINT('Ctrl Pts',(-104.027609067831,-1.3160422101884,126.063472181283));
#99804=CARTESIAN_POINT('Ctrl Pts',(-104.035369510345,-1.44766955396821,
126.102002275452));
#99805=CARTESIAN_POINT('Ctrl Pts',(-104.043129952859,-1.57732589529462,
126.145903138686));
#99806=CARTESIAN_POINT('Ctrl Pts',(-104.050902853125,-1.70719037249047,
126.189874475483));
#99807=CARTESIAN_POINT('Ctrl Pts',(-104.05867575339,-1.83507715954553,126.239233669264));
#99808=CARTESIAN_POINT('Ctrl Pts',(-104.066448653655,-1.96052156225215,
126.293757745838));
#99809=CARTESIAN_POINT('Ctrl Pts',(-104.073938989417,-2.08140574494126,
126.346299734888));
#99810=CARTESIAN_POINT('Ctrl Pts',(-104.081429325179,-2.20002175667112,
126.403637479136));
#99811=CARTESIAN_POINT('Ctrl Pts',(-104.088919660941,-2.31597785834425,
126.465532478292));
#99812=CARTESIAN_POINT('Ctrl Pts',(-104.096694944032,-2.4363451616712,126.529782086809));
#99813=CARTESIAN_POINT('Ctrl Pts',(-104.104470227123,-2.55422750628298,
126.599146096603));
#99814=CARTESIAN_POINT('Ctrl Pts',(-104.112245510215,-2.66915976063969,
126.673408035572));
#99815=CARTESIAN_POINT('Ctrl Pts',(-104.120011002829,-2.78394729466695,
126.747576465436));
#99816=CARTESIAN_POINT('Ctrl Pts',(-104.127776495444,-2.8957918048788,126.826630341773));
#99817=CARTESIAN_POINT('Ctrl Pts',(-104.135541988059,-3.00425157186128,
126.910306745896));
#99818=CARTESIAN_POINT('Ctrl Pts',(-104.143298171535,-3.1125813191387,126.993882840183));
#99819=CARTESIAN_POINT('Ctrl Pts',(-104.15105435501,-3.21753409680233,127.082070188469));
#99820=CARTESIAN_POINT('Ctrl Pts',(-104.158810538486,-3.31869660073135,
127.174562285042));
#99821=CARTESIAN_POINT('Ctrl Pts',(-104.166561443349,-3.41979025667306,
127.266991434431));
#99822=CARTESIAN_POINT('Ctrl Pts',(-104.174312348213,-3.51709848335758,
127.363719241173));
#99823=CARTESIAN_POINT('Ctrl Pts',(-104.182063253076,-3.61024050260019,
127.464398555523));
#99824=CARTESIAN_POINT('Ctrl Pts',(-104.189810561528,-3.70333930404406,
127.565031154778));
#99825=CARTESIAN_POINT('Ctrl Pts',(-104.19755786998,-3.79227547989826,127.669611326847));
#99826=CARTESIAN_POINT('Ctrl Pts',(-104.205305178432,-3.87670492154576,
127.777754925745));
#99827=CARTESIAN_POINT('Ctrl Pts',(-104.213050569898,-3.96111347206215,
127.885871765706));
#99828=CARTESIAN_POINT('Ctrl Pts',(-104.220795961364,-4.04101726819991,
127.997549969224));
#99829=CARTESIAN_POINT('Ctrl Pts',(-104.22854135283,-4.11611259387954,128.112372471789));
#99830=CARTESIAN_POINT('Ctrl Pts',(-104.236289194533,-4.1912316757932,128.227231298188));
#99831=CARTESIAN_POINT('Ctrl Pts',(-104.244037036236,-4.26153902828456,
128.345236087324));
#99832=CARTESIAN_POINT('Ctrl Pts',(-104.251784877939,-4.32677432210976,
128.465940846004));
#99833=CARTESIAN_POINT('Ctrl Pts',(-104.259533727165,-4.39201809907846,
128.58666130103));
#99834=CARTESIAN_POINT('Ctrl Pts',(-104.26728257639,-4.45218832466746,128.710082077126));
#99835=CARTESIAN_POINT('Ctrl Pts',(-104.275031425616,-4.50707117204207,
128.8357335547));
#99836=CARTESIAN_POINT('Ctrl Pts',(-104.282787377523,-4.56200432563929,
128.961500205803));
#99837=CARTESIAN_POINT('Ctrl Pts',(-104.290543329429,-4.61164026750674,
129.089501282152));
#99838=CARTESIAN_POINT('Ctrl Pts',(-104.298299281335,-4.65581360460957,
129.219247769333));
#99839=CARTESIAN_POINT('Ctrl Pts',(-104.305456244829,-4.69657545626425,
129.338973998096));
#99840=CARTESIAN_POINT('Ctrl Pts',(-104.312613208323,-4.73268634054227,
129.460186031577));
#99841=CARTESIAN_POINT('Ctrl Pts',(-104.319770171817,-4.76405452823413,
129.582490119309));
#99842=CARTESIAN_POINT('Origin',(213.235140564004,0.,130.804360617566));
#99843=CARTESIAN_POINT('',(-106.415236531453,-4.76405452823412,129.582490119309));
#99844=CARTESIAN_POINT('',(-106.070096981463,-4.76405452823408,129.582490119308));
#99845=CARTESIAN_POINT('',(213.235140564004,-4.76405452823405,129.582490119308));
#99846=CARTESIAN_POINT('',(-104.735140563956,-4.91824921984811,130.801590425618));
#99847=CARTESIAN_POINT('Ctrl Pts',(-104.735140564009,-4.91824921984864,
130.80159042655));
#99848=CARTESIAN_POINT('Ctrl Pts',(-104.742974204282,-4.91832747923958,
130.940533620822));
#99849=CARTESIAN_POINT('Ctrl Pts',(-104.750807844555,-4.91251356494721,
131.07948295469));
#99850=CARTESIAN_POINT('Ctrl Pts',(-104.758641484828,-4.90083249721782,
131.217910973283));
#99851=CARTESIAN_POINT('Ctrl Pts',(-104.766476674903,-4.88914911851372,
131.356366378384));
#99852=CARTESIAN_POINT('Ctrl Pts',(-104.774311864978,-4.87159630597743,
131.49429988545));
#99853=CARTESIAN_POINT('Ctrl Pts',(-104.782147055053,-4.84825097285308,
131.631189237492));
#99854=CARTESIAN_POINT('Ctrl Pts',(-104.789985344041,-4.8248964063682,131.768132730923));
#99855=CARTESIAN_POINT('Ctrl Pts',(-104.797823633028,-4.79574482004112,
131.904030873771));
#99856=CARTESIAN_POINT('Ctrl Pts',(-104.805661922015,-4.7609241962113,132.038371906181));
#99857=CARTESIAN_POINT('Ctrl Pts',(-104.813912889865,-4.72427029786459,
132.179785873083));
#99858=CARTESIAN_POINT('Ctrl Pts',(-104.822163857716,-4.68133437221187,
132.319473861166));
#99859=CARTESIAN_POINT('Ctrl Pts',(-104.830414825566,-4.63232475084333,
132.456858867255));
#99860=CARTESIAN_POINT('Ctrl Pts',(-104.838268951371,-4.58567231698785,
132.587636145885));
#99861=CARTESIAN_POINT('Ctrl Pts',(-104.846123077176,-4.53351697905264,
132.71632647103));
#99862=CARTESIAN_POINT('Ctrl Pts',(-104.853977202981,-4.47608702524996,
132.842454826598));
#99863=CARTESIAN_POINT('Ctrl Pts',(-104.861837876973,-4.41860919061258,
132.968688338631));
#99864=CARTESIAN_POINT('Ctrl Pts',(-104.869698550966,-4.35584814706225,
133.092355288183));
#99865=CARTESIAN_POINT('Ctrl Pts',(-104.877559224958,-4.28807735207693,
133.213006644923));
#99866=CARTESIAN_POINT('Ctrl Pts',(-104.885432015159,-4.22020209720895,
133.333843970068));
#99867=CARTESIAN_POINT('Ctrl Pts',(-104.89330480536,-4.14730187255067,133.451656102214));
#99868=CARTESIAN_POINT('Ctrl Pts',(-104.901177595561,-4.0696927951611,133.566023814901));
#99869=CARTESIAN_POINT('Ctrl Pts',(-104.902342909114,-4.05820526565772,
133.582952278915));
#99870=CARTESIAN_POINT('Ctrl Pts',(-104.903508222666,-4.04661463849552,
133.599805339595));
#99871=CARTESIAN_POINT('Ctrl Pts',(-104.904673536219,-4.03492201057254,
133.616581702598));
#99872=CARTESIAN_POINT('Ctrl Pts',(-104.912447870338,-3.9569151977443,133.728504412989));
#99873=CARTESIAN_POINT('Ctrl Pts',(-104.920222204457,-3.87412444528042,
133.837356252472));
#99874=CARTESIAN_POINT('Ctrl Pts',(-104.927996538576,-3.7868195446258,133.942701070567));
#99875=CARTESIAN_POINT('Ctrl Pts',(-104.935761291523,-3.6996222394588,134.047916060588));
#99876=CARTESIAN_POINT('Ctrl Pts',(-104.94352604447,-3.60792210245885,134.149632330757));
#99877=CARTESIAN_POINT('Ctrl Pts',(-104.951290797418,-3.5120322862127,134.2474424178));
#99878=CARTESIAN_POINT('Ctrl Pts',(-104.959047838303,-3.41623770908385,
134.345155358485));
#99879=CARTESIAN_POINT('Ctrl Pts',(-104.966804879188,-3.31626200571,134.438969559399));
#99880=CARTESIAN_POINT('Ctrl Pts',(-104.974561920073,-3.21245846203479,
134.528510680628));
#99881=CARTESIAN_POINT('Ctrl Pts',(-104.982313111313,-3.10873319741892,
134.6179842782));
#99882=CARTESIAN_POINT('Ctrl Pts',(-104.990064302553,-3.00118613295721,
134.70319095567));
#99883=CARTESIAN_POINT('Ctrl Pts',(-104.997815493793,-2.89020700187156,
134.783793560692));
#99884=CARTESIAN_POINT('Ctrl Pts',(-105.00556339057,-2.77927503987724,134.864361907456));
#99885=CARTESIAN_POINT('Ctrl Pts',(-105.013311287347,-2.66491422821539,
134.940329844535));
#99886=CARTESIAN_POINT('Ctrl Pts',(-105.021059184124,-2.54754676149983,
135.011400973977));
#99887=CARTESIAN_POINT('Ctrl Pts',(-105.028805460208,-2.43020384552816,
135.082457236871));
#99888=CARTESIAN_POINT('Ctrl Pts',(-105.036551736292,-2.30985585969123,
135.148618527145));
#99889=CARTESIAN_POINT('Ctrl Pts',(-105.044298012377,-2.18695297664713,
135.209632429888));
#99890=CARTESIAN_POINT('Ctrl Pts',(-105.052044345642,-2.06404918636203,
135.270646783021));
#99891=CARTESIAN_POINT('Ctrl Pts',(-105.059790678907,-1.93859081142382,
135.326513498956));
#99892=CARTESIAN_POINT('Ctrl Pts',(-105.067537012173,-1.81105119446872,
135.377026867525));
#99893=CARTESIAN_POINT('Ctrl Pts',(-105.075285080176,-1.68348301590087,
135.427551548213));
#99894=CARTESIAN_POINT('Ctrl Pts',(-105.083033148178,-1.55383303129568,
135.472720352035));
#99895=CARTESIAN_POINT('Ctrl Pts',(-105.090781216181,-1.42259267752029,
135.512376456151));
#99896=CARTESIAN_POINT('Ctrl Pts',(-105.098537518923,-1.29121283993458,
135.552074707247));
#99897=CARTESIAN_POINT('Ctrl Pts',(-105.106293821665,-1.15823963154555,
135.586248441461));
#99898=CARTESIAN_POINT('Ctrl Pts',(-105.114050124407,-1.02417824546788,
135.614791157966));
#99899=CARTESIAN_POINT('Ctrl Pts',(-105.121810566921,-0.890045306791942,
135.643349108577));
#99900=CARTESIAN_POINT('Ctrl Pts',(-105.129571009435,-0.754823418425915,
135.66626998757));
#99901=CARTESIAN_POINT('Ctrl Pts',(-105.13733145195,-0.619024984850516,
135.683498977013));
#99902=CARTESIAN_POINT('Ctrl Pts',(-105.145104352215,-0.483008555573924,
135.70075562396));
#99903=CARTESIAN_POINT('Ctrl Pts',(-105.15287725248,-0.346414121401026,
135.712302089516));
#99904=CARTESIAN_POINT('Ctrl Pts',(-105.160650152746,-0.209757095518095,
135.71813564532));
#99905=CARTESIAN_POINT('Ctrl Pts',(-105.168140488508,-0.0780678967427983,
135.723757136677));
#99906=CARTESIAN_POINT('Ctrl Pts',(-105.17563082427,0.0536791139996607,
135.724073863646));
#99907=CARTESIAN_POINT('Ctrl Pts',(-105.183121160032,0.185027339917025,
135.719128968769));
#99908=CARTESIAN_POINT('Ctrl Pts',(-105.190895494151,0.321355673741123,
135.713996586699));
#99909=CARTESIAN_POINT('Ctrl Pts',(-105.19866982827,0.457686233126234,135.70317945999));
#99910=CARTESIAN_POINT('Ctrl Pts',(-105.20644416239,0.593506243454455,135.686668821836));
#99911=CARTESIAN_POINT('Ctrl Pts',(-105.214208915337,0.729158867757792,
135.670178531568));
#99912=CARTESIAN_POINT('Ctrl Pts',(-105.221973668284,0.864301810554518,
135.648008737812));
#99913=CARTESIAN_POINT('Ctrl Pts',(-105.229738421231,0.99842299482897,135.620202660854));
#99914=CARTESIAN_POINT('Ctrl Pts',(-105.237495462116,1.13241096805315,135.592424201283));
#99915=CARTESIAN_POINT('Ctrl Pts',(-105.245252503001,1.26537882195526,135.559020677709));
#99916=CARTESIAN_POINT('Ctrl Pts',(-105.253009543886,1.39682065408044,135.520086979733));
#99917=CARTESIAN_POINT('Ctrl Pts',(-105.260760735126,1.52816336489773,135.481182641961));
#99918=CARTESIAN_POINT('Ctrl Pts',(-105.268511926366,1.65798197115636,135.436756541199));
#99919=CARTESIAN_POINT('Ctrl Pts',(-105.276263117606,1.78578215671355,135.386954331967));
#99920=CARTESIAN_POINT('Ctrl Pts',(-105.284011014384,1.91352802378217,135.337173290002));
#99921=CARTESIAN_POINT('Ctrl Pts',(-105.291758911161,2.03925681289221,135.282020825895));
#99922=CARTESIAN_POINT('Ctrl Pts',(-105.299506807938,2.16249094954978,135.2216919336));
#99923=CARTESIAN_POINT('Ctrl Pts',(-105.307253084022,2.28569930828292,135.161375660808));
#99924=CARTESIAN_POINT('Ctrl Pts',(-105.314999360106,2.40641370158378,135.095885285364));
#99925=CARTESIAN_POINT('Ctrl Pts',(-105.32274563619,2.52417843631995,135.025463113848));
#99926=CARTESIAN_POINT('Ctrl Pts',(-105.330491969456,2.64194404036848,134.955040422491));
#99927=CARTESIAN_POINT('Ctrl Pts',(-105.338238302721,2.75675960685744,134.879686063073));
#99928=CARTESIAN_POINT('Ctrl Pts',(-105.345984635986,2.86819621274039,134.799687080788));
#99929=CARTESIAN_POINT('Ctrl Pts',(-105.353732703989,2.97965777407843,134.719670183286));
#99930=CARTESIAN_POINT('Ctrl Pts',(-105.361480771992,3.08773855153675,134.635006821134));
#99931=CARTESIAN_POINT('Ctrl Pts',(-105.369228839995,3.19204097198851,134.546025687511));
#99932=CARTESIAN_POINT('Ctrl Pts',(-105.376985142737,3.29645424629409,134.456949983681));
#99933=CARTESIAN_POINT('Ctrl Pts',(-105.384741445479,3.39708084392467,134.363547595549));
#99934=CARTESIAN_POINT('Ctrl Pts',(-105.392497748221,3.49355809349757,134.266185990091));
#99935=CARTESIAN_POINT('Ctrl Pts',(-105.400258190735,3.59008683588344,134.168772419813));
#99936=CARTESIAN_POINT('Ctrl Pts',(-105.408018633249,3.68246155417312,134.067395710417));
#99937=CARTESIAN_POINT('Ctrl Pts',(-105.415779075763,3.7703591613504,133.962457331874));
#99938=CARTESIAN_POINT('Ctrl Pts',(-105.423551976029,3.85839786956991,133.857350496929));
#99939=CARTESIAN_POINT('Ctrl Pts',(-105.431324876294,3.94194486623019,133.748670877576));
#99940=CARTESIAN_POINT('Ctrl Pts',(-105.43909777656,4.02071926246565,133.636850630777));
#99941=CARTESIAN_POINT('Ctrl Pts',(-105.446588112322,4.09663001097658,133.529095331608));
#99942=CARTESIAN_POINT('Ctrl Pts',(-105.454078448084,4.1681089597507,133.418424038867));
#99943=CARTESIAN_POINT('Ctrl Pts',(-105.461568783846,4.23494560410924,133.305244219963));
#99944=CARTESIAN_POINT('Ctrl Pts',(-105.469343117965,4.30431638015387,133.187773153823));
#99945=CARTESIAN_POINT('Ctrl Pts',(-105.477117452084,4.36890562250306,133.067227471921));
#99946=CARTESIAN_POINT('Ctrl Pts',(-105.484891786203,4.42842878818928,132.944033847393));
#99947=CARTESIAN_POINT('Ctrl Pts',(-105.49265653915,4.4878785968932,132.820992047997));
#99948=CARTESIAN_POINT('Ctrl Pts',(-105.500421292097,4.54227458315621,132.695309147722));
#99949=CARTESIAN_POINT('Ctrl Pts',(-105.508186045044,4.59137631929478,132.567439333086));
#99950=CARTESIAN_POINT('Ctrl Pts',(-105.515943085929,4.6404292868968,132.439696520552));
#99951=CARTESIAN_POINT('Ctrl Pts',(-105.523700126814,4.6841983294311,132.309771478801));
#99952=CARTESIAN_POINT('Ctrl Pts',(-105.531457167699,4.72248982757289,132.178141128045));
#99953=CARTESIAN_POINT('Ctrl Pts',(-105.539208358939,4.76075244979813,132.046610040759));
#99954=CARTESIAN_POINT('Ctrl Pts',(-105.546959550179,4.79354564069304,131.913376578031));
#99955=CARTESIAN_POINT('Ctrl Pts',(-105.554710741419,4.82072475358047,131.778935351856));
#99956=CARTESIAN_POINT('Ctrl Pts',(-105.562458638196,4.84789231461993,131.644551266789));
#99957=CARTESIAN_POINT('Ctrl Pts',(-105.570206534974,4.86945046617891,131.508960821663));
#99958=CARTESIAN_POINT('Ctrl Pts',(-105.577954431751,4.88530512151254,131.37267121242));
#99959=CARTESIAN_POINT('Ctrl Pts',(-105.585700707835,4.90115646039411,131.236410112025));
#99960=CARTESIAN_POINT('Ctrl Pts',(-105.593446983919,4.91130663094113,131.099450526513));
#99961=CARTESIAN_POINT('Ctrl Pts',(-105.601193260003,4.91571317927373,130.962306816047));
#99962=CARTESIAN_POINT('Ctrl Pts',(-105.608939593268,4.92011976013443,130.825162093218));
#99963=CARTESIAN_POINT('Ctrl Pts',(-105.616685926534,4.91878262162284,130.687833633488));
#99964=CARTESIAN_POINT('Ctrl Pts',(-105.624432259799,4.91171141960792,130.550837456902));
#99965=CARTESIAN_POINT('Ctrl Pts',(-105.632180327802,4.90463863404629,130.413810600971));
#99966=CARTESIAN_POINT('Ctrl Pts',(-105.639928395805,4.89182924991284,130.277116566627));
#99967=CARTESIAN_POINT('Ctrl Pts',(-105.647676463808,4.87334490810206,130.141267510095));
#99968=CARTESIAN_POINT('Ctrl Pts',(-105.65543276655,4.85484092091291,130.005274071569));
#99969=CARTESIAN_POINT('Ctrl Pts',(-105.663189069291,4.83064998044537,129.870127792824));
#99970=CARTESIAN_POINT('Ctrl Pts',(-105.670945372033,4.80088521433196,129.736332424442));
#99971=CARTESIAN_POINT('Ctrl Pts',(-105.678705814547,4.77110456186667,129.602465645442));
#99972=CARTESIAN_POINT('Ctrl Pts',(-105.686466257061,4.73574425672799,129.469951591065));
#99973=CARTESIAN_POINT('Ctrl Pts',(-105.694226699576,4.69496743054843,129.339279087893));
#99974=CARTESIAN_POINT('Ctrl Pts',(-105.701999599841,4.65412514578738,129.208396817617));
#99975=CARTESIAN_POINT('Ctrl Pts',(-105.709772500106,4.6078490965022,129.079362374245));
#99976=CARTESIAN_POINT('Ctrl Pts',(-105.717545400372,4.55635104129327,128.952645668929));
#99977=CARTESIAN_POINT('Ctrl Pts',(-105.725035736134,4.5067250701064,128.83053543503));
#99978=CARTESIAN_POINT('Ctrl Pts',(-105.732526071896,4.45225029493123,128.710577634012));
#99979=CARTESIAN_POINT('Ctrl Pts',(-105.740016407658,4.39315574671854,128.59316961551));
#99980=CARTESIAN_POINT('Ctrl Pts',(-105.747790741777,4.33182061074958,128.471310036302));
#99981=CARTESIAN_POINT('Ctrl Pts',(-105.755565075896,4.26531417770391,128.351811391892));
#99982=CARTESIAN_POINT('Ctrl Pts',(-105.763339410015,4.19384161735086,128.235143703587));
#99983=CARTESIAN_POINT('Ctrl Pts',(-105.771104162962,4.12245714054114,128.118619797782));
#99984=CARTESIAN_POINT('Ctrl Pts',(-105.77886891591,4.04611891628644,128.004920236391));
#99985=CARTESIAN_POINT('Ctrl Pts',(-105.786633668857,3.965079107531,127.894492796939));
#99986=CARTESIAN_POINT('Ctrl Pts',(-105.794390709742,3.88411978865586,127.784175035577));
#99987=CARTESIAN_POINT('Ctrl Pts',(-105.802147750627,3.79846840797045,127.677123241827));
#99988=CARTESIAN_POINT('Ctrl Pts',(-105.809904791512,3.70842155598071,127.573758100134));
#99989=CARTESIAN_POINT('Ctrl Pts',(-105.817655982752,3.6184426090219,127.470470906898));
#99990=CARTESIAN_POINT('Ctrl Pts',(-105.825407173992,3.52407504415699,127.370865125633));
#99991=CARTESIAN_POINT('Ctrl Pts',(-105.833158365232,3.4256568074044,127.275329801551));
#99992=CARTESIAN_POINT('Ctrl Pts',(-105.840906262009,3.3272804010285,127.179835082531));
#99993=CARTESIAN_POINT('Ctrl Pts',(-105.848654158786,3.22485702692788,127.088407651494));
#99994=CARTESIAN_POINT('Ctrl Pts',(-105.856402055563,3.11876254722884,127.001400818081));
#99995=CARTESIAN_POINT('Ctrl Pts',(-105.864148331647,3.01269026020783,126.914412184621));
#99996=CARTESIAN_POINT('Ctrl Pts',(-105.871894607732,2.90294869713193,126.831842557279));
#99997=CARTESIAN_POINT('Ctrl Pts',(-105.879640883816,2.78994765641538,126.754005677939));
#99998=CARTESIAN_POINT('Ctrl Pts',(-105.887387217081,2.67694578155067,126.676168224025));
#99999=CARTESIAN_POINT('Ctrl Pts',(-105.895133550346,2.56068470300772,126.603063809605));
#100000=CARTESIAN_POINT('Ctrl Pts',(-105.902879883612,2.44160378229905,
126.534963232365));
#100001=CARTESIAN_POINT('Ctrl Pts',(-105.910627951615,2.32249619424367,
126.466847404472));
#100002=CARTESIAN_POINT('Ctrl Pts',(-105.918376019618,2.20056784676347,
126.403737837624));
#100003=CARTESIAN_POINT('Ctrl Pts',(-105.926124087621,2.07628294980358,
126.34585950454));
#100004=CARTESIAN_POINT('Ctrl Pts',(-105.933880390363,1.95186596137635,
126.287919657675));
#100005=CARTESIAN_POINT('Ctrl Pts',(-105.941636693104,1.82508777530703,
126.23522231622));
#100006=CARTESIAN_POINT('Ctrl Pts',(-105.949392995846,1.69643335947566,
126.187944592189));
#100007=CARTESIAN_POINT('Ctrl Pts',(-105.957153438361,1.56771027690885,
126.140641634613));
#100008=CARTESIAN_POINT('Ctrl Pts',(-105.964913880875,1.43710934131709,
126.098764177556));
#100009=CARTESIAN_POINT('Ctrl Pts',(-105.972674323389,1.30512999298075,
126.062439196462));
#100010=CARTESIAN_POINT('Ctrl Pts',(-105.980447223654,1.17293877967788,
126.026055903285));
#100011=CARTESIAN_POINT('Ctrl Pts',(-105.98822012392,1.0393651130295,125.99524298567));
#100012=CARTESIAN_POINT('Ctrl Pts',(-105.995993024185,0.904918803293208,
125.970076283567));
#100013=CARTESIAN_POINT('Ctrl Pts',(-106.003483359947,0.775359955566745,
125.945824454477));
#100014=CARTESIAN_POINT('Ctrl Pts',(-106.010973695709,0.644991113588729,
125.926815504056));
#100015=CARTESIAN_POINT('Ctrl Pts',(-106.018464031471,0.514270375684464,
125.913071519261));
#100016=CARTESIAN_POINT('Ctrl Pts',(-106.02623836559,0.378593321269518,
125.898806427106));
#100017=CARTESIAN_POINT('Ctrl Pts',(-106.034012699709,0.242107375778195,
125.890168236567));
#100018=CARTESIAN_POINT('Ctrl Pts',(-106.041787033828,0.105318880721756,
125.887238390504));
#100019=CARTESIAN_POINT('Ctrl Pts',(-106.049551786775,-0.0313010347389233,
125.884312155215));
#100020=CARTESIAN_POINT('Ctrl Pts',(-106.057316539722,-0.168222370750725,
125.887080275094));
#100021=CARTESIAN_POINT('Ctrl Pts',(-106.06508129267,-0.304932099168563,
125.895572633002));
#100022=CARTESIAN_POINT('Ctrl Pts',(-106.072838333555,-0.441506045557609,
125.904056556182));
#100023=CARTESIAN_POINT('Ctrl Pts',(-106.08059537444,-0.577868414915769,
125.918253379118));
#100024=CARTESIAN_POINT('Ctrl Pts',(-106.088352415325,-0.71350495909208,
125.938140962038));
#100025=CARTESIAN_POINT('Ctrl Pts',(-106.096103606565,-0.849039218695514,
125.958013547576));
#100026=CARTESIAN_POINT('Ctrl Pts',(-106.103854797805,-0.98384835732093,
125.983568294745));
#100027=CARTESIAN_POINT('Ctrl Pts',(-106.111605989045,-1.1174223921357,
126.014731168428));
#100028=CARTESIAN_POINT('Ctrl Pts',(-106.119353885822,-1.25093965442192,
126.045880797057));
#100029=CARTESIAN_POINT('Ctrl Pts',(-106.127101782599,-1.38322247704346,
126.082633722755));
#100030=CARTESIAN_POINT('Ctrl Pts',(-106.134849679376,-1.513770447935,126.124864694557));
#100031=CARTESIAN_POINT('Ctrl Pts',(-106.14259595546,-1.64429111100569,
126.16708683255));
#100032=CARTESIAN_POINT('Ctrl Pts',(-106.150342231544,-1.77307727241129,
126.214784617155));
#100033=CARTESIAN_POINT('Ctrl Pts',(-106.158088507629,-1.89964346616637,
126.267782858511));
#100034=CARTESIAN_POINT('Ctrl Pts',(-106.165834840894,-2.0262105942045,
126.320781491088));
#100035=CARTESIAN_POINT('Ctrl Pts',(-106.173581174159,-2.15055736126741,
126.379080507483));
#100036=CARTESIAN_POINT('Ctrl Pts',(-106.181327507425,-2.27221845196502,
126.442456633175));
#100037=CARTESIAN_POINT('Ctrl Pts',(-106.189075575428,-2.39390678782019,
126.50584695151));
#100038=CARTESIAN_POINT('Ctrl Pts',(-106.196823643431,-2.51290790384352,
126.574316461017));
#100039=CARTESIAN_POINT('Ctrl Pts',(-106.204571711434,-2.62878160730095,
126.647596211972));
#100040=CARTESIAN_POINT('Ctrl Pts',(-106.212328014175,-2.74477846270917,
126.720953845517));
#100041=CARTESIAN_POINT('Ctrl Pts',(-106.220084316917,-2.85764093484098,
126.799131723742));
#100042=CARTESIAN_POINT('Ctrl Pts',(-106.227840619659,-2.96695787735862,
126.881817562802));
#100043=CARTESIAN_POINT('Ctrl Pts',(-106.235601062173,-3.07633316561995,
126.964547533783));
#100044=CARTESIAN_POINT('Ctrl Pts',(-106.243361504688,-3.18215885206609,
127.051790011254));
#100045=CARTESIAN_POINT('Ctrl Pts',(-106.251121947202,-3.28405814898742,
127.143193435291));
#100046=CARTESIAN_POINT('Ctrl Pts',(-106.258894847467,-3.38612102370636,
127.234743588218));
#100047=CARTESIAN_POINT('Ctrl Pts',(-106.266667747733,-3.4842446335043,
127.330467762354));
#100048=CARTESIAN_POINT('Ctrl Pts',(-106.274440647998,-3.57808960718752,
127.429978033235));
#100049=CARTESIAN_POINT('Ctrl Pts',(-106.28193098376,-3.66852307969486,
127.525870855117));
#100050=CARTESIAN_POINT('Ctrl Pts',(-106.289421319522,-3.7549833915705,
127.625279052087));
#100051=CARTESIAN_POINT('Ctrl Pts',(-106.296911655284,-3.83720434709623,
127.727829151592));
#100052=CARTESIAN_POINT('Ctrl Pts',(-106.304670430773,-3.92237194902209,
127.834054456276));
#100053=CARTESIAN_POINT('Ctrl Pts',(-106.312429206263,-4.00326690146727,
127.943995672536));
#100054=CARTESIAN_POINT('Ctrl Pts',(-106.320187981752,-4.07954613905818,
128.0572737311));
#100055=CARTESIAN_POINT('Ctrl Pts',(-106.328108694227,-4.15741743583502,
128.172916068324));
#100056=CARTESIAN_POINT('Ctrl Pts',(-106.336029406702,-4.23047789099962,
128.292035822503));
#100057=CARTESIAN_POINT('Ctrl Pts',(-106.343950119177,-4.29840385481742,
128.414191719059));
#100058=CARTESIAN_POINT('Ctrl Pts',(-106.351689422288,-4.36477409925469,
128.533549859278));
#100059=CARTESIAN_POINT('Ctrl Pts',(-106.359428725399,-4.42624226601099,
128.655806220943));
#100060=CARTESIAN_POINT('Ctrl Pts',(-106.36716802851,-4.48254895009903,
128.780518239201));
#100061=CARTESIAN_POINT('Ctrl Pts',(-106.375179445667,-4.54083537828252,
128.90961513442));
#100062=CARTESIAN_POINT('Ctrl Pts',(-106.383190862824,-4.59359046755274,
129.041343187705));
#100063=CARTESIAN_POINT('Ctrl Pts',(-106.391202279981,-4.64057775253825,
129.175182547143));
#100064=CARTESIAN_POINT('Ctrl Pts',(-106.399213697139,-4.68756503752376,
129.309021906581));
#100065=CARTESIAN_POINT('Ctrl Pts',(-106.407225114296,-4.72878432796288,
129.444972143751));
#100066=CARTESIAN_POINT('Ctrl Pts',(-106.415236531453,-4.76405452823412,
129.582490119309));
#100067=CARTESIAN_POINT('Ctrl Pts',(-104.665400201108,-4.76405452823405,
129.582490119308));
#100068=CARTESIAN_POINT('Ctrl Pts',(-104.674057866373,-4.80191628057872,
129.730112517068));
#100069=CARTESIAN_POINT('Ctrl Pts',(-104.682715531638,-4.8329568645889,
129.87966918857));
#100070=CARTESIAN_POINT('Ctrl Pts',(-104.691373196903,-4.85699517168876,
130.030551232322));
#100071=CARTESIAN_POINT('Ctrl Pts',(-104.699986564182,-4.8809104839014,
130.180661269963));
#100072=CARTESIAN_POINT('Ctrl Pts',(-104.708599931462,-4.8978948960219,
130.332082940685));
#100073=CARTESIAN_POINT('Ctrl Pts',(-104.717213298742,-4.90781816629195,
130.484198300741));
#100074=CARTESIAN_POINT('Ctrl Pts',(-104.723189053814,-4.91470270177198,
130.589732420529));
#100075=CARTESIAN_POINT('Ctrl Pts',(-104.729164808885,-4.9181895210244,
130.695600047087));
#100076=CARTESIAN_POINT('Ctrl Pts',(-104.735140563956,-4.91824921984811,
130.801590425618));
#100077=CARTESIAN_POINT('',(-104.389859436028,-4.9182494419762,130.802017755898));
#100078=CARTESIAN_POINT('Ctrl Pts',(-104.319770171817,-4.76405452823413,
129.582490119309));
#100079=CARTESIAN_POINT('Ctrl Pts',(-104.327703023973,-4.79882335101448,
129.718053231639));
#100080=CARTESIAN_POINT('Ctrl Pts',(-104.33563587613,-4.82776451325459,
129.85495775685));
#100081=CARTESIAN_POINT('Ctrl Pts',(-104.343568728286,-4.85080669696491,
129.992660271884));
#100082=CARTESIAN_POINT('Ctrl Pts',(-104.351501580442,-4.87384888067523,
130.130362786918));
#100083=CARTESIAN_POINT('Ctrl Pts',(-104.359434432598,-4.89099209668079,
130.268862857689));
#100084=CARTESIAN_POINT('Ctrl Pts',(-104.367367284754,-4.90222159891013,
130.407615790657));
#100085=CARTESIAN_POINT('Ctrl Pts',(-104.3748646685,-4.91283466541256,130.538751977723));
#100086=CARTESIAN_POINT('Ctrl Pts',(-104.382362052246,-4.91818670614076,
130.670319667333));
#100087=CARTESIAN_POINT('Ctrl Pts',(-104.389859435992,-4.9182494419759,
130.802017755259));
#100088=CARTESIAN_POINT('Ctrl Pts',(-104.389859436028,-4.9182494419762,
130.802017755897));
#100089=CARTESIAN_POINT('Ctrl Pts',(-104.397545371812,-4.91831375554012,
130.937027924903));
#100090=CARTESIAN_POINT('Ctrl Pts',(-104.405231307596,-4.91281465613365,
131.072264896961));
#100091=CARTESIAN_POINT('Ctrl Pts',(-104.41291724338,-4.90172242161412,
131.207225810832));
#100092=CARTESIAN_POINT('Ctrl Pts',(-104.420594276387,-4.89064303545788,
131.342030396702));
#100093=CARTESIAN_POINT('Ctrl Pts',(-104.428271309393,-4.87398343223574,
131.476559165036));
#100094=CARTESIAN_POINT('Ctrl Pts',(-104.4359483424,-4.85176588145133,131.610307820604));
#100095=CARTESIAN_POINT('Ctrl Pts',(-104.443618418405,-4.82956846442449,
131.743935271858));
#100096=CARTESIAN_POINT('Ctrl Pts',(-104.451288494411,-4.80182318464016,
131.876783624039));
#100097=CARTESIAN_POINT('Ctrl Pts',(-104.458958570417,-4.76860419642255,
132.008352760548));
#100098=CARTESIAN_POINT('Ctrl Pts',(-104.466744251173,-4.73488452570238,
132.141904930498));
#100099=CARTESIAN_POINT('Ctrl Pts',(-104.474529931929,-4.69552482911067,
132.274138591999));
#100100=CARTESIAN_POINT('Ctrl Pts',(-104.482315612685,-4.65065684970194,
132.404539960271));
#100101=CARTESIAN_POINT('Ctrl Pts',(-104.48997848367,-4.60649660883172,
132.532884403426));
#100102=CARTESIAN_POINT('Ctrl Pts',(-104.497641354654,-4.55700073228512,
132.659453546734));
#100103=CARTESIAN_POINT('Ctrl Pts',(-104.505304225638,-4.50234520281099,
132.783772332502));
#100104=CARTESIAN_POINT('Ctrl Pts',(-104.512966394213,-4.44769468328114,
132.908079722713));
#100105=CARTESIAN_POINT('Ctrl Pts',(-104.520628562788,-4.38788561240711,
133.030136799074));
#100106=CARTESIAN_POINT('Ctrl Pts',(-104.528290731363,-4.32314190563217,
133.149488999183));
#100107=CARTESIAN_POINT('Ctrl Pts',(-104.535953944915,-4.25838936902452,
133.268857476704));
#100108=CARTESIAN_POINT('Ctrl Pts',(-104.543617158466,-4.18870104925746,
133.385519992526));
#100109=CARTESIAN_POINT('Ctrl Pts',(-104.551280372018,-4.11434629046257,
133.499047550153));
#100110=CARTESIAN_POINT('Ctrl Pts',(-104.559158250064,-4.03790868136313,
133.615755279592));
#100111=CARTESIAN_POINT('Ctrl Pts',(-104.56703612811,-3.95653959196402,
133.729149450618));
#100112=CARTESIAN_POINT('Ctrl Pts',(-104.574914006155,-3.87057790563903,
133.838797919419));
#100113=CARTESIAN_POINT('Ctrl Pts',(-104.582588618686,-3.7868342082679,
133.945617231383));
#100114=CARTESIAN_POINT('Ctrl Pts',(-104.590263231216,-3.69873231707316,
134.048881501605));
#100115=CARTESIAN_POINT('Ctrl Pts',(-104.597937843746,-3.60662432917995,
134.148227243295));
#100116=CARTESIAN_POINT('Ctrl Pts',(-104.60591735455,-3.51085705994149,
134.251519809009));
#100117=CARTESIAN_POINT('Ctrl Pts',(-104.613896865353,-3.41075917559361,
134.350575735485));
#100118=CARTESIAN_POINT('Ctrl Pts',(-104.621876376157,-3.30676506649801,
134.445031964651));
#100119=CARTESIAN_POINT('Ctrl Pts',(-104.62985588696,-3.20277095740268,
134.539488193817));
#100120=CARTESIAN_POINT('Ctrl Pts',(-104.637835397764,-3.09488103853637,
134.629344477018));
#100121=CARTESIAN_POINT('Ctrl Pts',(-104.645814908567,-2.98356317691055,
134.714288216881));
#100122=CARTESIAN_POINT('Ctrl Pts',(-104.653589242686,-2.87510762480794,
134.797047803437));
#100123=CARTESIAN_POINT('Ctrl Pts',(-104.661363576805,-2.76303423627931,
134.875422462838));
#100124=CARTESIAN_POINT('Ctrl Pts',(-104.669137910924,-2.64773309102237,
134.949079249899));
#100125=CARTESIAN_POINT('Ctrl Pts',(-104.676902663871,-2.5325740441222,
135.022645261552));
#100126=CARTESIAN_POINT('Ctrl Pts',(-104.684667416819,-2.41419548168438,
135.091504761247));
#100127=CARTESIAN_POINT('Ctrl Pts',(-104.692432169766,-2.29302001461254,
135.155365360736));
#100128=CARTESIAN_POINT('Ctrl Pts',(-104.700189210651,-2.17196490072286,
135.219162532977));
#100129=CARTESIAN_POINT('Ctrl Pts',(-104.707946251535,-2.04811875403068,
135.277970504442));
#100130=CARTESIAN_POINT('Ctrl Pts',(-104.71570329242,-1.92193228848902,
135.331540682569));
#100131=CARTESIAN_POINT('Ctrl Pts',(-104.723454483661,-1.79584098114279,
135.385070463008));
#100132=CARTESIAN_POINT('Ctrl Pts',(-104.731205674901,-1.66741322620109,
135.433370159905));
#100133=CARTESIAN_POINT('Ctrl Pts',(-104.738956866141,-1.53712308966951,
135.476237721012));
#100134=CARTESIAN_POINT('Ctrl Pts',(-104.746704762918,-1.40688832992137,
135.519087062263));
#100135=CARTESIAN_POINT('Ctrl Pts',(-104.754452659695,-1.27479313354236,
135.556508737822));
#100136=CARTESIAN_POINT('Ctrl Pts',(-104.762200556472,-1.14133003397393,
135.588349415217));
#100137=CARTESIAN_POINT('Ctrl Pts',(-104.769946832556,-1.00789485200844,
135.620183432228));
#100138=CARTESIAN_POINT('Ctrl Pts',(-104.77769310864,-0.873092716044913,
135.646438682476));
#100139=CARTESIAN_POINT('Ctrl Pts',(-104.785439384725,-0.737429371895126,
135.667012258797));
#100140=CARTESIAN_POINT('Ctrl Pts',(-104.79318571799,-0.601765026309906,
135.687585986988));
#100141=CARTESIAN_POINT('Ctrl Pts',(-104.800932051255,-0.465239846398554,
135.702477898943));
#100142=CARTESIAN_POINT('Ctrl Pts',(-104.80867838452,-0.328367380854038,
135.711636636468));
#100143=CARTESIAN_POINT('Ctrl Pts',(-104.816426452523,-0.191464263670057,
135.720797425029));
#100144=CARTESIAN_POINT('Ctrl Pts',(-104.824174520526,-0.0542140961134072,
135.724222458242));
#100145=CARTESIAN_POINT('Ctrl Pts',(-104.831922588529,0.0828672700156155,
135.721912455428));
#100146=CARTESIAN_POINT('Ctrl Pts',(-104.839678891271,0.220094327852036,
135.719599997516));
#100147=CARTESIAN_POINT('Ctrl Pts',(-104.847435194013,0.357151834348657,
135.711540334229));
#100148=CARTESIAN_POINT('Ctrl Pts',(-104.855191496755,0.493526203479473,
135.697786304033));
#100149=CARTESIAN_POINT('Ctrl Pts',(-104.862951939269,0.629973359717618,
135.684024932898));
#100150=CARTESIAN_POINT('Ctrl Pts',(-104.870712381783,0.765736265252047,
135.664563194333));
#100151=CARTESIAN_POINT('Ctrl Pts',(-104.878472824297,0.900310247688287,
135.639505343467));
#100152=CARTESIAN_POINT('Ctrl Pts',(-104.886245724563,1.03510026022768,
135.614407267514));
#100153=CARTESIAN_POINT('Ctrl Pts',(-104.894018624828,1.16869715450211,
135.583695215254));
#100154=CARTESIAN_POINT('Ctrl Pts',(-104.901791525094,1.30060929788147,
135.547523962504));
#100155=CARTESIAN_POINT('Ctrl Pts',(-104.909281860856,1.42772610258021,
135.512667625902));
#100156=CARTESIAN_POINT('Ctrl Pts',(-104.916772196617,1.55327822612299,
135.472742202568));
#100157=CARTESIAN_POINT('Ctrl Pts',(-104.924262532379,1.67684404949931,
135.427928189924));
#100158=CARTESIAN_POINT('Ctrl Pts',(-104.932036866498,1.80509490862829,
135.381415040368));
#100159=CARTESIAN_POINT('Ctrl Pts',(-104.939811200617,1.93161213331215,
135.329487942329));
#100160=CARTESIAN_POINT('Ctrl Pts',(-104.947585534736,2.05590475973382,
135.2722951159));
#100161=CARTESIAN_POINT('Ctrl Pts',(-104.955350287684,2.1800442066011,135.215172774518));
#100162=CARTESIAN_POINT('Ctrl Pts',(-104.963115040631,2.30196415845116,
135.152797778857));
#100163=CARTESIAN_POINT('Ctrl Pts',(-104.970879793578,2.42119018925418,
135.085367640447));
#100164=CARTESIAN_POINT('Ctrl Pts',(-104.978636834463,2.54029780308294,
135.018004474602));
#100165=CARTESIAN_POINT('Ctrl Pts',(-104.986393875348,2.65671648240282,
134.945596348927));
#100166=CARTESIAN_POINT('Ctrl Pts',(-104.994150916233,2.76999345734827,
134.868388091482));
#100167=CARTESIAN_POINT('Ctrl Pts',(-105.001902107473,2.8831850092459,134.791238057386));
#100168=CARTESIAN_POINT('Ctrl Pts',(-105.009653298713,2.99323925073205,
134.709295315848));
#100169=CARTESIAN_POINT('Ctrl Pts',(-105.017404489953,3.09972994527334,
134.622849497853));
#100170=CARTESIAN_POINT('Ctrl Pts',(-105.02515238673,3.20617537842858,134.536440421636));
#100171=CARTESIAN_POINT('Ctrl Pts',(-105.032900283507,3.30905997416121,
134.445532321508));
#100172=CARTESIAN_POINT('Ctrl Pts',(-105.040648180284,3.40798850316221,
134.350456699853));
#100173=CARTESIAN_POINT('Ctrl Pts',(-105.048394456368,3.50689633844732,
134.25540096597));
#100174=CARTESIAN_POINT('Ctrl Pts',(-105.056140732452,3.60184947128084,
134.156179715268));
#100175=CARTESIAN_POINT('Ctrl Pts',(-105.063887008536,3.69248795498802,
134.05316282219));
#100176=CARTESIAN_POINT('Ctrl Pts',(-105.071633341802,3.78312710776778,
133.950145168664));
#100177=CARTESIAN_POINT('Ctrl Pts',(-105.079379675067,3.86945128961112,
133.843332110378));
#100178=CARTESIAN_POINT('Ctrl Pts',(-105.087126008332,3.95113970580277,
133.733127950033));
#100179=CARTESIAN_POINT('Ctrl Pts',(-105.094874076335,4.0328464155494,133.622899110231));
#100180=CARTESIAN_POINT('Ctrl Pts',(-105.102622144338,4.10991506107959,
133.509277971251));
#100181=CARTESIAN_POINT('Ctrl Pts',(-105.110370212341,4.1820674170817,133.392698922634));
#100182=CARTESIAN_POINT('Ctrl Pts',(-105.118126515083,4.2542964574661,133.275995972418));
#100183=CARTESIAN_POINT('Ctrl Pts',(-105.125882817825,4.32159856455811,
133.156329165658));
#100184=CARTESIAN_POINT('Ctrl Pts',(-105.133639120567,4.38374058706518,
133.034159157304));
#100185=CARTESIAN_POINT('Ctrl Pts',(-105.141399563081,4.44591577664072,
132.911923943138));
#100186=CARTESIAN_POINT('Ctrl Pts',(-105.149160005595,4.50292523143581,
132.787183220634));
#100187=CARTESIAN_POINT('Ctrl Pts',(-105.156920448109,4.55458387648579,
132.660417937412));
#100188=CARTESIAN_POINT('Ctrl Pts',(-105.164693348375,4.60632544857885,
132.533449159305));
#100189=CARTESIAN_POINT('Ctrl Pts',(-105.17246624864,4.65269891384318,132.404449694061));
#100190=CARTESIAN_POINT('Ctrl Pts',(-105.180239148906,4.69356875011187,
132.273916826247));
#100191=CARTESIAN_POINT('Ctrl Pts',(-105.187729484668,4.73295286488795,
132.148129156969));
#100192=CARTESIAN_POINT('Ctrl Pts',(-105.19521982043,4.76722646504752,132.020917933062));
#100193=CARTESIAN_POINT('Ctrl Pts',(-105.202710156192,4.79631351280986,
131.892735437808));
#100194=CARTESIAN_POINT('Ctrl Pts',(-105.210484490311,4.82650340482854,
131.759692864288));
#100195=CARTESIAN_POINT('Ctrl Pts',(-105.21825882443,4.85120131689324,131.625182475128));
#100196=CARTESIAN_POINT('Ctrl Pts',(-105.226033158549,4.87026657283051,
131.489697448672));
#100197=CARTESIAN_POINT('Ctrl Pts',(-105.233797911496,4.88930833254364,
131.354379395403));
#100198=CARTESIAN_POINT('Ctrl Pts',(-105.241562664443,4.90273119417715,
131.218089478209));
#100199=CARTESIAN_POINT('Ctrl Pts',(-105.249327417391,4.91044489091943,
131.081333604955));
#100200=CARTESIAN_POINT('Ctrl Pts',(-105.257084458276,4.91815092630938,
130.944713559562));
#100201=CARTESIAN_POINT('Ctrl Pts',(-105.26484149916,4.92015905933097,130.807628866907));
#100202=CARTESIAN_POINT('Ctrl Pts',(-105.272598540045,4.91643053759352,
130.67059279065));
#100203=CARTESIAN_POINT('Ctrl Pts',(-105.280349731286,4.9127048275633,130.533660054363));
#100204=CARTESIAN_POINT('Ctrl Pts',(-105.288100922526,4.9032510841166,130.396776250738));
#100205=CARTESIAN_POINT('Ctrl Pts',(-105.295852113766,4.88808259074364,
130.260456537264));
#100206=CARTESIAN_POINT('Ctrl Pts',(-105.303600010543,4.87292054438506,
130.124194763305));
#100207=CARTESIAN_POINT('Ctrl Pts',(-105.31134790732,4.85204862218518,129.988496990399));
#100208=CARTESIAN_POINT('Ctrl Pts',(-105.319095804097,4.82553209539436,
129.853874921293));
#100209=CARTESIAN_POINT('Ctrl Pts',(-105.326842080181,4.79902111528932,
129.719281012223));
#100210=CARTESIAN_POINT('Ctrl Pts',(-105.334588356266,4.7668679546381,129.585762742739));
#100211=CARTESIAN_POINT('Ctrl Pts',(-105.34233463235,4.72918923931268,129.453822872344));
#100212=CARTESIAN_POINT('Ctrl Pts',(-105.350080965615,4.6915102458515,129.321882027999));
#100213=CARTESIAN_POINT('Ctrl Pts',(-105.35782729888,4.64830572368379,129.191519981928));
#100214=CARTESIAN_POINT('Ctrl Pts',(-105.365573632146,4.59974242674365,
129.063225163296));
#100215=CARTESIAN_POINT('Ctrl Pts',(-105.373321700149,4.5511682543898,128.93490161393));
#100216=CARTESIAN_POINT('Ctrl Pts',(-105.381069768152,4.49723305766329,
128.808646578779));
#100217=CARTESIAN_POINT('Ctrl Pts',(-105.388817836155,4.43815191321042,
128.684928934834));
#100218=CARTESIAN_POINT('Ctrl Pts',(-105.396574138896,4.3790079766144,128.561079802306));
#100219=CARTESIAN_POINT('Ctrl Pts',(-105.404330441638,4.31470733577502,
128.439773801437));
#100220=CARTESIAN_POINT('Ctrl Pts',(-105.41208674438,4.24551152878097,128.321456084265));
#100221=CARTESIAN_POINT('Ctrl Pts',(-105.419847186894,4.17627878990128,
128.203075217364));
#100222=CARTESIAN_POINT('Ctrl Pts',(-105.427607629408,4.10214589006745,
128.087686140979));
#100223=CARTESIAN_POINT('Ctrl Pts',(-105.435368071923,4.02341742659575,
127.975704527854));
#100224=CARTESIAN_POINT('Ctrl Pts',(-105.443140972188,3.94456258120508,
127.863543151902));
#100225=CARTESIAN_POINT('Ctrl Pts',(-105.450913872453,3.8610976683509,127.754800480259));
#100226=CARTESIAN_POINT('Ctrl Pts',(-105.458686772719,3.77336781458023,
127.649859326016));
#100227=CARTESIAN_POINT('Ctrl Pts',(-105.466177108481,3.6888271619723,127.548733047061));
#100228=CARTESIAN_POINT('Ctrl Pts',(-105.473667444243,3.60032647455756,
127.451136922741));
#100229=CARTESIAN_POINT('Ctrl Pts',(-105.481157780005,3.50820517079095,
127.357379395955));
#100230=CARTESIAN_POINT('Ctrl Pts',(-105.488932114124,3.41259105979224,
127.260067024045));
#100231=CARTESIAN_POINT('Ctrl Pts',(-105.496706448243,3.31277348461028,
127.166581820203));
#100232=CARTESIAN_POINT('Ctrl Pts',(-105.504480782362,3.20909133124621,
127.077308714222));
#100233=CARTESIAN_POINT('Ctrl Pts',(-105.512245535309,3.10553695687011,
126.988145629365));
#100234=CARTESIAN_POINT('Ctrl Pts',(-105.520010288257,2.99812777418872,
126.903184566408));
#100235=CARTESIAN_POINT('Ctrl Pts',(-105.527775041204,2.88724062639873,
126.822774924934));
#100236=CARTESIAN_POINT('Ctrl Pts',(-105.535532082089,2.77646361328686,
126.742445147449));
#100237=CARTESIAN_POINT('Ctrl Pts',(-105.543289122974,2.66221582386565,
126.666658023405));
#100238=CARTESIAN_POINT('Ctrl Pts',(-105.551046163859,2.54490813477318,
126.59572358783));
#100239=CARTESIAN_POINT('Ctrl Pts',(-105.558797355099,2.42768890832237,
126.524842644465));
#100240=CARTESIAN_POINT('Ctrl Pts',(-105.566548546339,2.30741470832992,
126.45880730714));
#100241=CARTESIAN_POINT('Ctrl Pts',(-105.574299737579,2.18452613143105,
126.397884855282));
#100242=CARTESIAN_POINT('Ctrl Pts',(-105.582047634356,2.06168978545502,
126.336988297091));
#100243=CARTESIAN_POINT('Ctrl Pts',(-105.589795531133,1.93624162217422,
126.281200475503));
#100244=CARTESIAN_POINT('Ctrl Pts',(-105.59754342791,1.808647432308,126.230743063801));
#100245=CARTESIAN_POINT('Ctrl Pts',(-105.605289703994,1.68107993239568,
126.180296206702));
#100246=CARTESIAN_POINT('Ctrl Pts',(-105.613035980078,1.5513676621287,126.135177685362));
#100247=CARTESIAN_POINT('Ctrl Pts',(-105.620782256162,1.41999664644693,
126.095561132922));
#100248=CARTESIAN_POINT('Ctrl Pts',(-105.628528589428,1.288624661014,126.055944288043));
#100249=CARTESIAN_POINT('Ctrl Pts',(-105.636274922693,1.1555942800487,126.021829605987));
#100250=CARTESIAN_POINT('Ctrl Pts',(-105.644021255959,1.02140656741542,
125.993340799841));
#100251=CARTESIAN_POINT('Ctrl Pts',(-105.651769323961,0.887188804374838,
125.964845613825));
#100252=CARTESIAN_POINT('Ctrl Pts',(-105.659517391965,0.75181357630323,
125.941978891905));
#100253=CARTESIAN_POINT('Ctrl Pts',(-105.667265459967,0.615791616874018,
125.924813123475));
#100254=CARTESIAN_POINT('Ctrl Pts',(-105.675021762709,0.479625091687086,
125.907629111062));
#100255=CARTESIAN_POINT('Ctrl Pts',(-105.682778065451,0.342810850586459,
125.896158204755));
#100256=CARTESIAN_POINT('Ctrl Pts',(-105.690534368193,0.205864780315405,
125.890420980704));
#100257=CARTESIAN_POINT('Ctrl Pts',(-105.698294810707,0.0688456178032804,
125.884680694523));
#100258=CARTESIAN_POINT('Ctrl Pts',(-105.706055253221,-0.068305123305999,
125.884680188385));
#100259=CARTESIAN_POINT('Ctrl Pts',(-105.713815695736,-0.205073083468483,
125.890387877213));
#100260=CARTESIAN_POINT('Ctrl Pts',(-105.721588596001,-0.342060595702309,
125.896104728529));
#100261=CARTESIAN_POINT('Ctrl Pts',(-105.729361496266,-0.47866370924976,
125.907548053352));
#100262=CARTESIAN_POINT('Ctrl Pts',(-105.737134396532,-0.614373803286218,
125.924634406769));
#100263=CARTESIAN_POINT('Ctrl Pts',(-105.744624732294,-0.745150493571723,
125.941099628202));
#100264=CARTESIAN_POINT('Ctrl Pts',(-105.752115068056,-0.875097660325476,
125.962804673881));
#100265=CARTESIAN_POINT('Ctrl Pts',(-105.759605403818,-1.00377233783546,
125.989630702369));
#100266=CARTESIAN_POINT('Ctrl Pts',(-105.767379737937,-1.13732575485286,
126.01747384788));
#100267=CARTESIAN_POINT('Ctrl Pts',(-105.775154072056,-1.26993134204901,
126.050922164682));
#100268=CARTESIAN_POINT('Ctrl Pts',(-105.782928406175,-1.40108207092772,
126.089898602338));
#100269=CARTESIAN_POINT('Ctrl Pts',(-105.790693159122,-1.53207116825331,
126.128827005019));
#100270=CARTESIAN_POINT('Ctrl Pts',(-105.798457912069,-1.66160860359512,
126.173269862577));
#100271=CARTESIAN_POINT('Ctrl Pts',(-105.806222665016,-1.78919672423613,
126.223098985168));
#100272=CARTESIAN_POINT('Ctrl Pts',(-105.813979705901,-1.91665812255705,
126.272878616772));
#100273=CARTESIAN_POINT('Ctrl Pts',(-105.821736746786,-2.04217369725687,
126.328033725928));
#100274=CARTESIAN_POINT('Ctrl Pts',(-105.829493787671,-2.16526051822668,
126.388386211989));
#100275=CARTESIAN_POINT('Ctrl Pts',(-105.837244978912,-2.28825451846816,
126.448693185772));
#100276=CARTESIAN_POINT('Ctrl Pts',(-105.844996170152,-2.40882306093549,
126.514189563741));
#100277=CARTESIAN_POINT('Ctrl Pts',(-105.852747361392,-2.52650312263188,
126.584649130529));
#100278=CARTESIAN_POINT('Ctrl Pts',(-105.860495258169,-2.64413316716267,
126.655078750122));
#100279=CARTESIAN_POINT('Ctrl Pts',(-105.868243154946,-2.75887683795299,
126.730467162505));
#100280=CARTESIAN_POINT('Ctrl Pts',(-105.875991051723,-2.87029586373044,
126.810542304579));
#100281=CARTESIAN_POINT('Ctrl Pts',(-105.883737327807,-2.98169158304962,
126.890600696659));
#100282=CARTESIAN_POINT('Ctrl Pts',(-105.891483603891,-3.08976372335384,
126.975343640412));
#100283=CARTESIAN_POINT('Ctrl Pts',(-105.899229879975,-3.19410349381147,
127.064456082244));
#100284=CARTESIAN_POINT('Ctrl Pts',(-105.906976213241,-3.29844403448201,
127.153569181885));
#100285=CARTESIAN_POINT('Ctrl Pts',(-105.914722546506,-3.3990518530336,
127.247051590059));
#100286=CARTESIAN_POINT('Ctrl Pts',(-105.922468879771,-3.4955520288846,
127.344548617491));
#100287=CARTESIAN_POINT('Ctrl Pts',(-105.930216947774,-3.59207381528024,
127.442067478707));
#100288=CARTESIAN_POINT('Ctrl Pts',(-105.937965015777,-3.68448585354708,
127.543602470361));
#100289=CARTESIAN_POINT('Ctrl Pts',(-105.94571308378,-3.77245109227978,
127.648763080037));
#100290=CARTESIAN_POINT('Ctrl Pts',(-105.953469386522,-3.86050982151513,
127.754035455661));
#100291=CARTESIAN_POINT('Ctrl Pts',(-105.961225689264,-3.94411205905247,
127.862940846428));
#100292=CARTESIAN_POINT('Ctrl Pts',(-105.968981992006,-4.02296164420858,
127.975056344122));
#100293=CARTESIAN_POINT('Ctrl Pts',(-105.97674243452,-4.10185331376239,
128.087231681233));
#100294=CARTESIAN_POINT('Ctrl Pts',(-105.984502877034,-4.17598706525354,
128.202620210459));
#100295=CARTESIAN_POINT('Ctrl Pts',(-105.992263319548,-4.24511144820341,
128.320772114043));
#100296=CARTESIAN_POINT('Ctrl Pts',(-106.000036219814,-4.31434679574956,
128.439113685552));
#100297=CARTESIAN_POINT('Ctrl Pts',(-106.007809120079,-4.37855652207327,
128.560227150366));
#100298=CARTESIAN_POINT('Ctrl Pts',(-106.015582020345,-4.43753590976266,
128.683639487368));
#100299=CARTESIAN_POINT('Ctrl Pts',(-106.023072356107,-4.49437124815023,
128.802565475065));
#100300=CARTESIAN_POINT('Ctrl Pts',(-106.030562691869,-4.54634979626853,
128.923625814116));
#100301=CARTESIAN_POINT('Ctrl Pts',(-106.038053027631,-4.59333210499773,
129.046383588223));
#100302=CARTESIAN_POINT('Ctrl Pts',(-106.046937466579,-4.64905877290856,
129.19198907029));
#100303=CARTESIAN_POINT('Ctrl Pts',(-106.055821905528,-4.69790417122911,
129.340366392219));
#100304=CARTESIAN_POINT('Ctrl Pts',(-106.064706344476,-4.73961983046872,
129.490896904657));
#100305=CARTESIAN_POINT('Ctrl Pts',(-106.066503223472,-4.74805682827102,
129.521341721442));
#100306=CARTESIAN_POINT('Ctrl Pts',(-106.068300102468,-4.75620233512269,
129.551874537541));
#100307=CARTESIAN_POINT('Ctrl Pts',(-106.070096981463,-4.76405452823408,
129.582490119308));
#100308=CARTESIAN_POINT('Origin',(213.235140564004,0.,130.804360617566));
#100309=CARTESIAN_POINT('',(-108.165013787364,-4.76405452823416,129.582490119309));
#100310=CARTESIAN_POINT('',(-107.819991607676,-4.76405452823401,129.582490119308));
#100311=CARTESIAN_POINT('',(213.235140564004,-4.76405452823405,129.582490119308));
#100312=CARTESIAN_POINT('',(-106.48514056406,-4.91824839459279,130.808334480353));
#100313=CARTESIAN_POINT('Ctrl Pts',(-106.485140564059,-4.91824839459279,
130.808334480353));
#100314=CARTESIAN_POINT('Ctrl Pts',(-106.49424843149,-4.91811808858843,
130.969607612091));
#100315=CARTESIAN_POINT('Ctrl Pts',(-106.50335629892,-4.91005153646411,
131.130544562526));
#100316=CARTESIAN_POINT('Ctrl Pts',(-106.512464166351,-4.89417093461805,
131.290440780955));
#100317=CARTESIAN_POINT('Ctrl Pts',(-106.521632239911,-4.87818535654372,
131.451393968262));
#100318=CARTESIAN_POINT('Ctrl Pts',(-106.530800313471,-4.85428218621434,
131.611292547037));
#100319=CARTESIAN_POINT('Ctrl Pts',(-106.539968387031,-4.82263498104052,
131.769438283945));
#100320=CARTESIAN_POINT('Ctrl Pts',(-106.549204021272,-4.79075456365281,
131.928749416573));
#100321=CARTESIAN_POINT('Ctrl Pts',(-106.558439655513,-4.7510156272781,
132.086281709925));
#100322=CARTESIAN_POINT('Ctrl Pts',(-106.567675289754,-4.70364375126848,
132.24134305436));
#100323=CARTESIAN_POINT('Ctrl Pts',(-106.570236619535,-4.69050605074448,
132.284346407354));
#100324=CARTESIAN_POINT('Ctrl Pts',(-106.572797949316,-4.67678156078555,
132.327159843967));
#100325=CARTESIAN_POINT('Ctrl Pts',(-106.575359279097,-4.66247573275551,
132.369768904233));
#100326=CARTESIAN_POINT('Ctrl Pts',(-106.583133613216,-4.61905364483081,
132.499099017622));
#100327=CARTESIAN_POINT('Ctrl Pts',(-106.590907947335,-4.57017756505967,
132.626825915645));
#100328=CARTESIAN_POINT('Ctrl Pts',(-106.598682281454,-4.51598388907358,
132.752455218998));
#100329=CARTESIAN_POINT('Ctrl Pts',(-106.606447034401,-4.4618570019497,
132.877929695462));
#100330=CARTESIAN_POINT('Ctrl Pts',(-106.614211787348,-4.40242571141989,
133.001311365288));
#100331=CARTESIAN_POINT('Ctrl Pts',(-106.621976540295,-4.3378760872215,
133.122121199337));
#100332=CARTESIAN_POINT('Ctrl Pts',(-106.62973358118,-4.27339057462002,
133.242811043356));
#100333=CARTESIAN_POINT('Ctrl Pts',(-106.637490622065,-4.20379702799861,
133.360933792337));
#100334=CARTESIAN_POINT('Ctrl Pts',(-106.64524766295,-4.12932933968496,
133.476030931605));
#100335=CARTESIAN_POINT('Ctrl Pts',(-106.65299885419,-4.05491780803404,
133.591041275225));
#100336=CARTESIAN_POINT('Ctrl Pts',(-106.66075004543,-3.97563966232488,
133.703030223665));
#100337=CARTESIAN_POINT('Ctrl Pts',(-106.66850123667,-3.89177422163134,
133.811564712792));
#100338=CARTESIAN_POINT('Ctrl Pts',(-106.676249133448,-3.80794442598738,
133.920053071866));
#100339=CARTESIAN_POINT('Ctrl Pts',(-106.683997030225,-3.71953145175937,
134.02508958312));
#100340=CARTESIAN_POINT('Ctrl Pts',(-106.691744927002,-3.62685722145508,
134.126271175916));
#100341=CARTESIAN_POINT('Ctrl Pts',(-106.699491203086,-3.53420237660195,
134.227431603705));
#100342=CARTESIAN_POINT('Ctrl Pts',(-106.70723747917,-3.43728831254272,
134.324738428817));
#100343=CARTESIAN_POINT('Ctrl Pts',(-106.714983755254,-3.33647615947514,
134.417822932266));
#100344=CARTESIAN_POINT('Ctrl Pts',(-106.72273008852,-3.23566326223529,
134.510908122843));
#100345=CARTESIAN_POINT('Ctrl Pts',(-106.730476421785,-3.1309525058131,
134.599770664338));
#100346=CARTESIAN_POINT('Ctrl Pts',(-106.73822275505,-3.0227403782926,134.684080152267));
#100347=CARTESIAN_POINT('Ctrl Pts',(-106.745970823053,-2.91450401741658,
134.768408520721));
#100348=CARTESIAN_POINT('Ctrl Pts',(-106.753718891056,-2.8027650335091,
134.848181566432));
#100349=CARTESIAN_POINT('Ctrl Pts',(-106.761466959059,-2.68795101437728,
134.923110720062));
#100350=CARTESIAN_POINT('Ctrl Pts',(-106.769223261801,-2.57301496953946,
134.998119509287));
#100351=CARTESIAN_POINT('Ctrl Pts',(-106.776979564543,-2.45499768886047,
135.06827390844));
#100352=CARTESIAN_POINT('Ctrl Pts',(-106.784735867285,-2.33435409964669,
135.133329778921));
#100353=CARTESIAN_POINT('Ctrl Pts',(-106.792496309799,-2.21364611931651,
135.198420371679));
#100354=CARTESIAN_POINT('Ctrl Pts',(-106.800256752313,-2.09030938878064,
135.258406842552));
#100355=CARTESIAN_POINT('Ctrl Pts',(-106.808017194827,-1.96482027587102,
135.313092628456));
#100356=CARTESIAN_POINT('Ctrl Pts',(-106.815790095093,-1.83912971669696,
135.367866200838));
#100357=CARTESIAN_POINT('Ctrl Pts',(-106.823562995358,-1.71128023541256,
135.417321943166));
#100358=CARTESIAN_POINT('Ctrl Pts',(-106.831335895624,-1.58176572121906,
135.461312438841));
#100359=CARTESIAN_POINT('Ctrl Pts',(-106.838826231386,-1.45695938584211,
135.503703769193));
#100360=CARTESIAN_POINT('Ctrl Pts',(-106.846316567148,-1.33060726752646,
135.541020218017));
#100361=CARTESIAN_POINT('Ctrl Pts',(-106.85380690291,-1.20315969460859,
135.573174915876));
#100362=CARTESIAN_POINT('Ctrl Pts',(-106.861581237029,-1.07087990822838,
135.606548768878));
#100363=CARTESIAN_POINT('Ctrl Pts',(-106.869355571148,-0.93700093652646,
135.634467447008));
#100364=CARTESIAN_POINT('Ctrl Pts',(-106.877129905267,-0.802012439984278,
135.656778479685));
#100365=CARTESIAN_POINT('Ctrl Pts',(-106.884894658214,-0.667190304699816,
135.679062016008));
#100366=CARTESIAN_POINT('Ctrl Pts',(-106.892659411162,-0.531261747303075,
135.695751594409));
#100367=CARTESIAN_POINT('Ctrl Pts',(-106.900424164109,-0.39473036381357,
135.706744833678));
#100368=CARTESIAN_POINT('Ctrl Pts',(-106.908181204994,-0.258334585218901,
135.717727154307));
#100369=CARTESIAN_POINT('Ctrl Pts',(-106.915938245879,-0.121337559224111,
135.723024363676));
#100370=CARTESIAN_POINT('Ctrl Pts',(-106.923695286764,0.0157485282706149,
135.72258540364));
#100371=CARTESIAN_POINT('Ctrl Pts',(-106.931446478004,0.1527312380802,135.722146774629));
#100372=CARTESIAN_POINT('Ctrl Pts',(-106.939197669244,0.289802486326624,
135.715980587483));
#100373=CARTESIAN_POINT('Ctrl Pts',(-106.946948860484,0.426446945107832,
135.704087759511));
#100374=CARTESIAN_POINT('Ctrl Pts',(-106.954696757261,0.563033326349133,
135.692199986307));
#100375=CARTESIAN_POINT('Ctrl Pts',(-106.962444654038,0.699192890232504,
135.674590447095));
#100376=CARTESIAN_POINT('Ctrl Pts',(-106.970192550815,0.834412515037491,
135.651312114873));
#100377=CARTESIAN_POINT('Ctrl Pts',(-106.9779388269,0.969603854811967,135.628038651977));
#100378=CARTESIAN_POINT('Ctrl Pts',(-106.985685102984,1.10385526153267,
135.599098820959));
#100379=CARTESIAN_POINT('Ctrl Pts',(-106.993431379068,1.2366613217813,135.564597149264));
#100380=CARTESIAN_POINT('Ctrl Pts',(-107.001177712333,1.36946836237391,
135.530095222885));
#100381=CARTESIAN_POINT('Ctrl Pts',(-107.008924045599,1.50082965680052,
135.490031472211));
#100382=CARTESIAN_POINT('Ctrl Pts',(-107.016670378864,1.6302529149167,135.4445608822));
#100383=CARTESIAN_POINT('Ctrl Pts',(-107.024418446867,1.75970515647435,
135.399080109365));
#100384=CARTESIAN_POINT('Ctrl Pts',(-107.03216651487,1.88721812930065,135.348190217363));
#100385=CARTESIAN_POINT('Ctrl Pts',(-107.039914582873,2.01231793018225,
135.292094969148));
#100386=CARTESIAN_POINT('Ctrl Pts',(-107.047670885615,2.13755068862111,
135.235940102235));
#100387=CARTESIAN_POINT('Ctrl Pts',(-107.055427188357,2.26036479444397,
135.174568987935));
#100388=CARTESIAN_POINT('Ctrl Pts',(-107.063183491099,2.38030894761148,
135.108232406597));
#100389=CARTESIAN_POINT('Ctrl Pts',(-107.070943933613,2.50031711858497,
135.041860419429));
#100390=CARTESIAN_POINT('Ctrl Pts',(-107.078704376127,2.61745195095748,
134.970517887709));
#100391=CARTESIAN_POINT('Ctrl Pts',(-107.086464818641,2.73129058219,134.894499346037));
#100392=CARTESIAN_POINT('Ctrl Pts',(-107.094237718907,2.8453119572995,134.818358772653));
#100393=CARTESIAN_POINT('Ctrl Pts',(-107.102010619172,2.95602624151052,
134.737527419915));
#100394=CARTESIAN_POINT('Ctrl Pts',(-107.109783519438,3.06304244988668,
134.652341128521));
#100395=CARTESIAN_POINT('Ctrl Pts',(-107.117273855199,3.16616834952791,
134.570251573394));
#100396=CARTESIAN_POINT('Ctrl Pts',(-107.124764190961,3.26586014104743,
134.484118409874));
#100397=CARTESIAN_POINT('Ctrl Pts',(-107.132254526723,3.3618013252633,134.394273556894));
#100398=CARTESIAN_POINT('Ctrl Pts',(-107.140028860842,3.4613801486418,134.301022209004));
#100399=CARTESIAN_POINT('Ctrl Pts',(-107.147803194961,3.55723377763119,
134.203476765943));
#100400=CARTESIAN_POINT('Ctrl Pts',(-107.15557752908,3.64896926096127,134.101966778868));
#100401=CARTESIAN_POINT('Ctrl Pts',(-107.163342282027,3.74059168850678,
134.000581893781));
#100402=CARTESIAN_POINT('Ctrl Pts',(-107.171107034974,3.82810580900147,
133.895242473538));
#100403=CARTESIAN_POINT('Ctrl Pts',(-107.178871787922,3.91115328028357,
133.786316868189));
#100404=CARTESIAN_POINT('Ctrl Pts',(-107.186628828807,3.99411826764643,
133.677499449286));
#100405=CARTESIAN_POINT('Ctrl Pts',(-107.194385869692,4.07262519880145,
133.565103242415));
#100406=CARTESIAN_POINT('Ctrl Pts',(-107.202142910576,4.14635426809657,
133.449531565905));
#100407=CARTESIAN_POINT('Ctrl Pts',(-107.209894101817,4.22002773772709,
133.334047042895));
#100408=CARTESIAN_POINT('Ctrl Pts',(-107.217645293057,4.28893030767497,
133.215392144917));
#100409=CARTESIAN_POINT('Ctrl Pts',(-107.225396484297,4.35278420237677,
133.094000927754));
#100410=CARTESIAN_POINT('Ctrl Pts',(-107.233144381074,4.41661095746987,
132.972661305097));
#100411=CARTESIAN_POINT('Ctrl Pts',(-107.240892277851,4.47539312356383,
132.848588021683));
#100412=CARTESIAN_POINT('Ctrl Pts',(-107.248640174628,4.52889791351924,
132.722241414545));
#100413=CARTESIAN_POINT('Ctrl Pts',(-107.256386450712,4.58239151142601,
132.595921236394));
#100414=CARTESIAN_POINT('Ctrl Pts',(-107.264132726796,4.63060977657732,
132.467329040163));
#100415=CARTESIAN_POINT('Ctrl Pts',(-107.27187900288,4.67336746257489,132.336946544112));
#100416=CARTESIAN_POINT('Ctrl Pts',(-107.279625336146,4.71612546420004,
132.206563085606));
#100417=CARTESIAN_POINT('Ctrl Pts',(-107.287371669411,4.75342268440877,
132.074389672409));
#100418=CARTESIAN_POINT('Ctrl Pts',(-107.295118002677,4.78512342158928,
131.940924255317));
#100419=CARTESIAN_POINT('Ctrl Pts',(-107.30286607068,4.81683125793005,131.80742894957));
#100420=CARTESIAN_POINT('Ctrl Pts',(-107.310614138682,4.84294002700223,
131.672641444495));
#100421=CARTESIAN_POINT('Ctrl Pts',(-107.318362206685,4.86336500408786,
131.53707058714));
#100422=CARTESIAN_POINT('Ctrl Pts',(-107.326118509427,4.88381168908217,
131.401355643465));
#100423=CARTESIAN_POINT('Ctrl Pts',(-107.333874812169,4.89856245659972,
131.264856071609));
#100424=CARTESIAN_POINT('Ctrl Pts',(-107.341631114911,4.90758435655711,
131.128087115981));
#100425=CARTESIAN_POINT('Ctrl Pts',(-107.349391557425,4.91661107177417,
130.991245162643));
#100426=CARTESIAN_POINT('Ctrl Pts',(-107.357151999939,4.9199028173875,130.854133929705));
#100427=CARTESIAN_POINT('Ctrl Pts',(-107.364912442454,4.91747882616643,
130.717268386542));
#100428=CARTESIAN_POINT('Ctrl Pts',(-107.372685342719,4.91505094373946,
130.580183134658));
#100429=CARTESIAN_POINT('Ctrl Pts',(-107.380458242984,4.90688901238055,
130.44334475119));
#100430=CARTESIAN_POINT('Ctrl Pts',(-107.38823114325,4.89306424747406,130.307263712938));
#100431=CARTESIAN_POINT('Ctrl Pts',(-107.395721479012,4.87974204759436,
130.176129563193));
#100432=CARTESIAN_POINT('Ctrl Pts',(-107.403211814774,4.86116162613072,
130.045698956764));
#100433=CARTESIAN_POINT('Ctrl Pts',(-107.410702150536,4.83743116034206,
129.916417583666));
#100434=CARTESIAN_POINT('Ctrl Pts',(-107.418476484655,4.81280094673047,
129.782234468014));
#100435=CARTESIAN_POINT('Ctrl Pts',(-107.426250818774,4.78254443067672,
129.648864400575));
#100436=CARTESIAN_POINT('Ctrl Pts',(-107.434025152893,4.74672647314242,
129.516816112833));
#100437=CARTESIAN_POINT('Ctrl Pts',(-107.44178990584,4.71095265803954,129.384930562803));
#100438=CARTESIAN_POINT('Ctrl Pts',(-107.449554658787,4.66963114020049,
129.254363925003));
#100439=CARTESIAN_POINT('Ctrl Pts',(-107.457319411734,4.62287813026192,
129.125616785039));
#100440=CARTESIAN_POINT('Ctrl Pts',(-107.465076452619,4.57617155607191,
128.99699751855));
#100441=CARTESIAN_POINT('Ctrl Pts',(-107.472833493504,4.52404435793295,
128.870194518694));
#100442=CARTESIAN_POINT('Ctrl Pts',(-107.480590534389,4.46666299621196,
128.745694850432));
#100443=CARTESIAN_POINT('Ctrl Pts',(-107.48834172563,4.40932490622228,128.621289068338));
#100444=CARTESIAN_POINT('Ctrl Pts',(-107.49609291687,4.34674070216743,128.499183514154));
#100445=CARTESIAN_POINT('Ctrl Pts',(-107.50384410811,4.27912542299531,128.379846506084));
#100446=CARTESIAN_POINT('Ctrl Pts',(-107.511592004887,4.21153888212043,
128.260560219425));
#100447=CARTESIAN_POINT('Ctrl Pts',(-107.519339901664,4.13892571145353,
128.144040477949));
#100448=CARTESIAN_POINT('Ctrl Pts',(-107.527087798441,4.06154737844507,
128.03073195548));
#100449=CARTESIAN_POINT('Ctrl Pts',(-107.534834074525,3.984185231316,127.917447134711));
#100450=CARTESIAN_POINT('Ctrl Pts',(-107.542580350609,3.90206012481772,
127.807372519526));
#100451=CARTESIAN_POINT('Ctrl Pts',(-107.550326626693,3.81547721196221,
127.70092434345));
#100452=CARTESIAN_POINT('Ctrl Pts',(-107.558072959959,3.72889365997118,
127.594475381599));
#100453=CARTESIAN_POINT('Ctrl Pts',(-107.565819293224,3.63785248266103,
127.491653215577));
#100454=CARTESIAN_POINT('Ctrl Pts',(-107.573565626489,3.54269927010443,
127.392841169563));
#100455=CARTESIAN_POINT('Ctrl Pts',(-107.581313694492,3.44752474864576,
127.294006995277));
#100456=CARTESIAN_POINT('Ctrl Pts',(-107.589061762495,3.34823663067146,
127.199185009557));
#100457=CARTESIAN_POINT('Ctrl Pts',(-107.596809830498,3.24521722783572,
127.108721537967));
#100458=CARTESIAN_POINT('Ctrl Pts',(-107.60456613324,3.14208833475255,127.018161920723));
#100459=CARTESIAN_POINT('Ctrl Pts',(-107.612322435982,3.03522052923194,
126.931970329471));
#100460=CARTESIAN_POINT('Ctrl Pts',(-107.620078738724,2.92502949066337,
126.850452988239));
#100461=CARTESIAN_POINT('Ctrl Pts',(-107.627839181238,2.81477963981943,
126.768892138747));
#100462=CARTESIAN_POINT('Ctrl Pts',(-107.635599623752,2.70120334526599,
126.692010729404));
#100463=CARTESIAN_POINT('Ctrl Pts',(-107.643360066266,2.58474426110525,
126.620070932663));
#100464=CARTESIAN_POINT('Ctrl Pts',(-107.651132966531,2.46809822648417,
126.548015651774));
#100465=CARTESIAN_POINT('Ctrl Pts',(-107.658905866797,2.34856049574229,
126.480918027056));
#100466=CARTESIAN_POINT('Ctrl Pts',(-107.666678767062,2.22659904112551,
126.41899406817));
#100467=CARTESIAN_POINT('Ctrl Pts',(-107.674169102824,2.10907119258378,
126.359321201166));
#100468=CARTESIAN_POINT('Ctrl Pts',(-107.681659438587,1.98929305775323,
126.304452507247));
#100469=CARTESIAN_POINT('Ctrl Pts',(-107.689149774349,1.86769808071749,
126.254537880164));
#100470=CARTESIAN_POINT('Ctrl Pts',(-107.696924108468,1.7414927931721,126.202730724824));
#100471=CARTESIAN_POINT('Ctrl Pts',(-107.704698442587,1.61293039221567,
126.156096609493));
#100472=CARTESIAN_POINT('Ctrl Pts',(-107.712472776706,1.48247394698653,
126.114855946601));
#100473=CARTESIAN_POINT('Ctrl Pts',(-107.720237529653,1.35217827766691,
126.073666109139));
#100474=CARTESIAN_POINT('Ctrl Pts',(-107.7280022826,1.21999357771997,126.037856615385));
#100475=CARTESIAN_POINT('Ctrl Pts',(-107.735767035547,1.08640381868289,
126.007600272786));
#100476=CARTESIAN_POINT('Ctrl Pts',(-107.743524076432,0.952946742877412,
125.977373981214));
#100477=CARTESIAN_POINT('Ctrl Pts',(-107.751281117317,0.818087763978748,
125.952689950569));
#100478=CARTESIAN_POINT('Ctrl Pts',(-107.759038158202,0.682326639427653,
125.93367140354));
#100479=CARTESIAN_POINT('Ctrl Pts',(-107.766789349442,0.546667893396835,
125.914667198546));
#100480=CARTESIAN_POINT('Ctrl Pts',(-107.774540540683,0.410108741457273,
125.901320027264));
#100481=CARTESIAN_POINT('Ctrl Pts',(-107.782291731923,0.273159426780302,
125.893702108765));
#100482=CARTESIAN_POINT('Ctrl Pts',(-107.7900396287,0.136268319215125,125.886087428085));
#100483=CARTESIAN_POINT('Ctrl Pts',(-107.797787525477,-0.00101223172060871,
125.884197178658));
#100484=CARTESIAN_POINT('Ctrl Pts',(-107.805535422254,-0.138166779800137,
125.888051737577));
#100485=CARTESIAN_POINT('Ctrl Pts',(-107.813281698338,-0.275292638104918,
125.891905490206));
#100486=CARTESIAN_POINT('Ctrl Pts',(-107.821027974422,-0.41229215541587,
125.901501649977));
#100487=CARTESIAN_POINT('Ctrl Pts',(-107.828774250506,-0.548650200021222,
125.916808467408));
#100488=CARTESIAN_POINT('Ctrl Pts',(-107.836520583772,-0.685009251190497,
125.93211539783));
#100489=CARTESIAN_POINT('Ctrl Pts',(-107.844266917037,-0.820726431680461,
125.953133026416));
#100490=CARTESIAN_POINT('Ctrl Pts',(-107.852013250302,-0.95529244012774,
125.97977779453));
#100491=CARTESIAN_POINT('Ctrl Pts',(-107.859761318305,-1.08988858369941,
126.006428529555));
#100492=CARTESIAN_POINT('Ctrl Pts',(-107.867509386308,-1.22333265879628,
126.038708835755));
#100493=CARTESIAN_POINT('Ctrl Pts',(-107.875257454311,-1.35512664312525,
126.076484260935));
#100494=CARTESIAN_POINT('Ctrl Pts',(-107.883013757053,-1.4870606996693,
126.114299834286));
#100495=CARTESIAN_POINT('Ctrl Pts',(-107.890770059795,-1.61734078573751,
126.157622085306));
#100496=CARTESIAN_POINT('Ctrl Pts',(-107.898526362537,-1.74548458151935,
126.206266812718));
#100497=CARTESIAN_POINT('Ctrl Pts',(-107.906286805051,-1.87369677150367,
126.254937503287));
#100498=CARTESIAN_POINT('Ctrl Pts',(-107.914047247565,-1.99977004004005,
126.30893617686));
#100499=CARTESIAN_POINT('Ctrl Pts',(-107.921807690079,-2.12324400813961,
126.368031285291));
#100500=CARTESIAN_POINT('Ctrl Pts',(-107.929580590345,-2.24691618761394,
126.427221258437));
#100501=CARTESIAN_POINT('Ctrl Pts',(-107.93735349061,-2.36798038293016,
126.491523831684));
#100502=CARTESIAN_POINT('Ctrl Pts',(-107.945126390875,-2.48600190861309,
126.560662045227));
#100503=CARTESIAN_POINT('Ctrl Pts',(-107.952616726637,-2.59973305455787,
126.627286910558));
#100504=CARTESIAN_POINT('Ctrl Pts',(-107.960107062399,-2.71063864832953,
126.698401778377));
#100505=CARTESIAN_POINT('Ctrl Pts',(-107.967597398161,-2.8183582929577,
126.773723001132));
#100506=CARTESIAN_POINT('Ctrl Pts',(-107.975324751309,-2.9294865202445,
126.851427620291));
#100507=CARTESIAN_POINT('Ctrl Pts',(-107.983052104457,-3.03758561542063,
126.933862313187));
#100508=CARTESIAN_POINT('Ctrl Pts',(-107.990779457605,-3.1422226496235,
127.020761817126));
#100509=CARTESIAN_POINT('Ctrl Pts',(-107.998494604148,-3.24669439269638,
127.107524049234));
#100510=CARTESIAN_POINT('Ctrl Pts',(-108.006209750691,-3.34771466284118,
127.198736797226));
#100511=CARTESIAN_POINT('Ctrl Pts',(-108.013924897234,-3.44487945656981,
127.294091597647));
#100512=CARTESIAN_POINT('Ctrl Pts',(-108.021632994712,-3.54195547415997,
127.389359275658));
#100513=CARTESIAN_POINT('Ctrl Pts',(-108.02934109219,-3.63518274011879,
127.488761204126));
#100514=CARTESIAN_POINT('Ctrl Pts',(-108.037049189669,-3.72419014628851,
127.591948623941));
#100515=CARTESIAN_POINT('Ctrl Pts',(-108.044751967482,-3.8131361249043,
127.69506483001));
#100516=CARTESIAN_POINT('Ctrl Pts',(-108.052454745295,-3.89786777924379,
127.801961031591));
#100517=CARTESIAN_POINT('Ctrl Pts',(-108.060157523109,-3.97805106294793,
127.912251905384));
#100518=CARTESIAN_POINT('Ctrl Pts',(-108.067856706407,-4.05819692898108,
128.022491311746));
#100519=CARTESIAN_POINT('Ctrl Pts',(-108.075555889706,-4.13379841561625,
128.136121917994));
#100520=CARTESIAN_POINT('Ctrl Pts',(-108.083255073004,-4.20456226891132,
128.252726006312));
#100521=CARTESIAN_POINT('Ctrl Pts',(-108.090953828883,-4.27532219375253,
128.369323621357));
#100522=CARTESIAN_POINT('Ctrl Pts',(-108.098652584761,-4.34124480596481,
128.488894056327));
#100523=CARTESIAN_POINT('Ctrl Pts',(-108.10635134064,-4.4020807562358,128.610991501781));
#100524=CARTESIAN_POINT('Ctrl Pts',(-108.114049764063,-4.46291407942287,
128.733083674691));
#100525=CARTESIAN_POINT('Ctrl Pts',(-108.121748187485,-4.5186610060928,
128.857702283649));
#100526=CARTESIAN_POINT('Ctrl Pts',(-108.129446610908,-4.56911900262065,
128.984378584031));
#100527=CARTESIAN_POINT('Ctrl Pts',(-108.137148893038,-4.61960229038739,
129.11111837882));
#100528=CARTESIAN_POINT('Ctrl Pts',(-108.144851175168,-4.6647912115551,
129.23991755464));
#100529=CARTESIAN_POINT('Ctrl Pts',(-108.152553457298,-4.70453207169467,
129.370289123917));
#100530=CARTESIAN_POINT('Ctrl Pts',(-108.156706900654,-4.72596226714681,
129.440591784736));
#100531=CARTESIAN_POINT('Ctrl Pts',(-108.160860344009,-4.74580908471365,
129.511351411935));
#100532=CARTESIAN_POINT('Ctrl Pts',(-108.165013787364,-4.76405452823417,
129.582490119309));
#100533=CARTESIAN_POINT('Ctrl Pts',(-106.415236531453,-4.76405452823412,
129.582490119309));
#100534=CARTESIAN_POINT('Ctrl Pts',(-106.422964224241,-4.79807563422773,
129.715137895235));
#100535=CARTESIAN_POINT('Ctrl Pts',(-106.430691917029,-4.82656175502522,
129.849243845907));
#100536=CARTESIAN_POINT('Ctrl Pts',(-106.438419609817,-4.84940130922175,
129.984305738538));
#100537=CARTESIAN_POINT('Ctrl Pts',(-106.446206435515,-4.87241563347753,
130.120401135359));
#100538=CARTESIAN_POINT('Ctrl Pts',(-106.453993261214,-4.88969651031593,
130.257466773977));
#100539=CARTESIAN_POINT('Ctrl Pts',(-106.461780086913,-4.90118255664471,
130.394979854777));
#100540=CARTESIAN_POINT('Ctrl Pts',(-106.469566912612,-4.91266860297349,
130.532492935577));
#100541=CARTESIAN_POINT('Ctrl Pts',(-106.477353738311,-4.9183598004662,
130.670453051542));
#100542=CARTESIAN_POINT('Ctrl Pts',(-106.48514056401,-4.9182483945935,130.808334479476));
#100543=CARTESIAN_POINT('',(-106.139859435937,-4.91824889795569,130.801068162911));
#100544=CARTESIAN_POINT('Ctrl Pts',(-106.070096981463,-4.76405452823408,
129.582490119308));
#100545=CARTESIAN_POINT('Ctrl Pts',(-106.078931279564,-4.80265958447516,
129.733010647679));
#100546=CARTESIAN_POINT('Ctrl Pts',(-106.087765577665,-4.83417096701391,
129.885533426967));
#100547=CARTESIAN_POINT('Ctrl Pts',(-106.096599875766,-4.85840041307,130.039423699395));
#100548=CARTESIAN_POINT('Ctrl Pts',(-106.105377112359,-4.88247335900662,
130.192319981041));
#100549=CARTESIAN_POINT('Ctrl Pts',(-106.114154348953,-4.8993580463698,
130.346565977745));
#100550=CARTESIAN_POINT('Ctrl Pts',(-106.122931585546,-4.90891746033364,
130.501520015712));
#100551=CARTESIAN_POINT('Ctrl Pts',(-106.128574202343,-4.91506291502496,
130.601135224674));
#100552=CARTESIAN_POINT('Ctrl Pts',(-106.13421681914,-4.91818193725568,
130.70104267325));
#100553=CARTESIAN_POINT('Ctrl Pts',(-106.139859435937,-4.91824889795569,
130.801068162911));
#100554=CARTESIAN_POINT('Ctrl Pts',(-106.139859435992,-4.91824889795634,
130.801068163883));
#100555=CARTESIAN_POINT('Ctrl Pts',(-106.147648177268,-4.91834132659944,
130.939137554038));
#100556=CARTESIAN_POINT('Ctrl Pts',(-106.155436918545,-4.91261542175427,
131.077241192686));
#100557=CARTESIAN_POINT('Ctrl Pts',(-106.163225659822,-4.90108922495837,
131.214857233261));
#100558=CARTESIAN_POINT('Ctrl Pts',(-106.171014608845,-4.88956272072675,
131.352476944438));
#100559=CARTESIAN_POINT('Ctrl Pts',(-106.178803557869,-4.87223564783958,
131.48960864811));
#100560=CARTESIAN_POINT('Ctrl Pts',(-106.186592506893,-4.84917800910811,
131.625734891866));
#100561=CARTESIAN_POINT('Ctrl Pts',(-106.19438328114,-4.82611496716673,
131.761893034755));
#100562=CARTESIAN_POINT('Ctrl Pts',(-106.202174055386,-4.79731874994963,
131.89704486925));
#100563=CARTESIAN_POINT('Ctrl Pts',(-106.209964829633,-4.76291057467061,
132.030682728673));
#100564=CARTESIAN_POINT('Ctrl Pts',(-106.217759047408,-4.72848719095131,
132.164379656134));
#100565=CARTESIAN_POINT('Ctrl Pts',(-106.225553265183,-4.68844700662207,
132.296560903952));
#100566=CARTESIAN_POINT('Ctrl Pts',(-106.233347482957,-4.64296113357161,
132.426733871365));
#100567=CARTESIAN_POINT('Ctrl Pts',(-106.24115162473,-4.59741734557249,
132.557072581684));
#100568=CARTESIAN_POINT('Ctrl Pts',(-106.248955766503,-4.54641414880807,
132.68539754155));
#100569=CARTESIAN_POINT('Ctrl Pts',(-106.256759908277,-4.49017109703257,
132.811235447214));
#100570=CARTESIAN_POINT('Ctrl Pts',(-106.264569584085,-4.43388816245424,
132.937162586448));
#100571=CARTESIAN_POINT('Ctrl Pts',(-106.272379259894,-4.37235814057708,
133.060598813939));
#100572=CARTESIAN_POINT('Ctrl Pts',(-106.280188935702,-4.30584618069132,
133.181096137292));
#100573=CARTESIAN_POINT('Ctrl Pts',(-106.28801117471,-4.23922722494315,
133.301787301197));
#100574=CARTESIAN_POINT('Ctrl Pts',(-106.295833413718,-4.16761052345866,
133.419529790201));
#100575=CARTESIAN_POINT('Ctrl Pts',(-106.303655652726,-4.09130450084059,
133.533904635145));
#100576=CARTESIAN_POINT('Ctrl Pts',(-106.307937318965,-4.04953680228271,
133.59651010038));
#100577=CARTESIAN_POINT('Ctrl Pts',(-106.312218985205,-4.00636482728613,
133.658107142264));
#100578=CARTESIAN_POINT('Ctrl Pts',(-106.316500651445,-3.96184406440911,
133.718631482089));
#100579=CARTESIAN_POINT('Ctrl Pts',(-106.324274985564,-3.88100654310979,
133.828527119396));
#100580=CARTESIAN_POINT('Ctrl Pts',(-106.332049319683,-3.79546500442361,
133.935230806359));
#100581=CARTESIAN_POINT('Ctrl Pts',(-106.339823653802,-3.70550028188961,
134.038313419234));
#100582=CARTESIAN_POINT('Ctrl Pts',(-106.347588406749,-3.61564643283601,
134.141268992001));
#100583=CARTESIAN_POINT('Ctrl Pts',(-106.355353159696,-3.52138050076351,
134.24061207829));
#100584=CARTESIAN_POINT('Ctrl Pts',(-106.363117912643,-3.42302593417488,
134.335943338736));
#100585=CARTESIAN_POINT('Ctrl Pts',(-106.370874953528,-3.32476905472807,
134.43117991483));
#100586=CARTESIAN_POINT('Ctrl Pts',(-106.378631994413,-3.22243190103691,
134.522412324273));
#100587=CARTESIAN_POINT('Ctrl Pts',(-106.386389035298,-3.11637719662952,
134.60927536442));
#100588=CARTESIAN_POINT('Ctrl Pts',(-106.394140226538,-3.01040246889985,
134.696072900472));
#100589=CARTESIAN_POINT('Ctrl Pts',(-106.401891417778,-2.90071607175843,
134.77850737895));
#100590=CARTESIAN_POINT('Ctrl Pts',(-106.409642609019,-2.7877162151675,
134.85625170275));
#100591=CARTESIAN_POINT('Ctrl Pts',(-106.417390505796,-2.67476438653015,
134.933962983139));
#100592=CARTESIAN_POINT('Ctrl Pts',(-106.425138402573,-2.55850222088346,
135.006987852513));
#100593=CARTESIAN_POINT('Ctrl Pts',(-106.43288629935,-2.43935933901518,
135.075040783261));
#100594=CARTESIAN_POINT('Ctrl Pts',(-106.440632575434,-2.32024137926938,
135.143079478803));
#100595=CARTESIAN_POINT('Ctrl Pts',(-106.448378851518,-2.19824424114708,
135.206148110591));
#100596=CARTESIAN_POINT('Ctrl Pts',(-106.456125127602,-2.07382439198327,
135.264005833692));
#100597=CARTESIAN_POINT('Ctrl Pts',(-106.463871460867,-1.94940362438022,
135.321863983886));
#100598=CARTESIAN_POINT('Ctrl Pts',(-106.471617794133,-1.82256046455907,
135.374510983782));
#100599=CARTESIAN_POINT('Ctrl Pts',(-106.479364127398,-1.69377335044753,
135.421753269249));
#100600=CARTESIAN_POINT('Ctrl Pts',(-106.487112195401,-1.56495739535456,
135.469006134298));
#100601=CARTESIAN_POINT('Ctrl Pts',(-106.494860263404,-1.43419698668376,
135.510851741847));
#100602=CARTESIAN_POINT('Ctrl Pts',(-106.502608331407,-1.30198740316484,
135.547145860912));
#100603=CARTESIAN_POINT('Ctrl Pts',(-106.510364634149,-1.16963730572743,
135.583478553798));
#100604=CARTESIAN_POINT('Ctrl Pts',(-106.518120936891,-1.03583533434416,
135.614247868274));
#100605=CARTESIAN_POINT('Ctrl Pts',(-106.525877239633,-0.901089235364966,
135.639360230018));
#100606=CARTESIAN_POINT('Ctrl Pts',(-106.533637682147,-0.766271218335622,
135.664485994985));
#100607=CARTESIAN_POINT('Ctrl Pts',(-106.541398124661,-0.630508456447608,
135.683948735582));
#100608=CARTESIAN_POINT('Ctrl Pts',(-106.549158567175,-0.494314586192979,
135.697706727579));
#100609=CARTESIAN_POINT('Ctrl Pts',(-106.55693146744,-0.357902085447093,
135.711486805125));
#100610=CARTESIAN_POINT('Ctrl Pts',(-106.564704367706,-0.221057483905281,
135.719543810938));
#100611=CARTESIAN_POINT('Ctrl Pts',(-106.572477267971,-0.0842960965321487,
135.721888170169));
#100612=CARTESIAN_POINT('Ctrl Pts',(-106.579967603733,0.0474936699277105,
135.724147306037));
#100613=CARTESIAN_POINT('Ctrl Pts',(-106.587457939495,0.179205859333517,
135.721101929748));
#100614=CARTESIAN_POINT('Ctrl Pts',(-106.594948275257,0.310385124522492,
135.712806821506));
#100615=CARTESIAN_POINT('Ctrl Pts',(-106.602722609376,0.446538091423518,
135.704197201714));
#100616=CARTESIAN_POINT('Ctrl Pts',(-106.610496943495,0.582548216399707,
135.689904631742));
#100617=CARTESIAN_POINT('Ctrl Pts',(-106.618271277614,0.717902668102916,
135.669933432932));
#100618=CARTESIAN_POINT('Ctrl Pts',(-106.626036030561,0.853090307540641,
135.649986846841));
#100619=CARTESIAN_POINT('Ctrl Pts',(-106.633800783509,0.987623498436658,
135.624375613167));
#100620=CARTESIAN_POINT('Ctrl Pts',(-106.641565536456,1.12099143345606,
135.593156005617));
#100621=CARTESIAN_POINT('Ctrl Pts',(-106.649322577341,1.25422690556259,
135.561967405821));
#100622=CARTESIAN_POINT('Ctrl Pts',(-106.657079618226,1.3862990467572,135.525181605861));
#100623=CARTESIAN_POINT('Ctrl Pts',(-106.664836659111,1.5167045407839,135.482906374365));
#100624=CARTESIAN_POINT('Ctrl Pts',(-106.672587850351,1.64701169501333,
135.44066302295));
#100625=CARTESIAN_POINT('Ctrl Pts',(-106.680339041591,1.7756543333163,135.392938599746));
#100626=CARTESIAN_POINT('Ctrl Pts',(-106.688090232831,1.90214201742572,
135.339891326099));
#100627=CARTESIAN_POINT('Ctrl Pts',(-106.695838129608,2.0285759408947,135.286866598958));
#100628=CARTESIAN_POINT('Ctrl Pts',(-106.703586026385,2.15285637206435,
135.228523671913));
#100629=CARTESIAN_POINT('Ctrl Pts',(-106.711333923162,2.2745108679381,135.16506966245));
#100630=CARTESIAN_POINT('Ctrl Pts',(-106.719080199246,2.39613991631421,
135.101628926198));
#100631=CARTESIAN_POINT('Ctrl Pts',(-106.72682647533,2.51514377553532,135.033079414776));
#100632=CARTESIAN_POINT('Ctrl Pts',(-106.734572751414,2.631073084193,134.95967498451));
#100633=CARTESIAN_POINT('Ctrl Pts',(-106.74231908468,2.74700324861402,134.886270012391));
#100634=CARTESIAN_POINT('Ctrl Pts',(-106.750065417945,2.85985848686679,
134.808010259067));
#100635=CARTESIAN_POINT('Ctrl Pts',(-106.75781175121,2.96921734057817,134.725193621777));
#100636=CARTESIAN_POINT('Ctrl Pts',(-106.765559819213,3.07860068444704,
134.642358438275));
#100637=CARTESIAN_POINT('Ctrl Pts',(-106.773307887216,3.18448577409477,
134.554964576149));
#100638=CARTESIAN_POINT('Ctrl Pts',(-106.781055955219,3.28648355365717,
134.463350767053));
#100639=CARTESIAN_POINT('Ctrl Pts',(-106.788812257961,3.38858973767334,
134.37163958971));
#100640=CARTESIAN_POINT('Ctrl Pts',(-106.796568560703,3.48680006720204,
134.275699767773));
#100641=CARTESIAN_POINT('Ctrl Pts',(-106.804324863445,3.58076136621063,
134.175907903421));
#100642=CARTESIAN_POINT('Ctrl Pts',(-106.812085305959,3.67477281519387,
134.076062777145));
#100643=CARTESIAN_POINT('Ctrl Pts',(-106.819845748473,3.76453045906257,
133.972361807264));
#100644=CARTESIAN_POINT('Ctrl Pts',(-106.827606190987,3.84972156096882,
133.86521457774));
#100645=CARTESIAN_POINT('Ctrl Pts',(-106.835379091253,3.93504941919453,
133.757895345971));
#100646=CARTESIAN_POINT('Ctrl Pts',(-106.843151991518,4.01579585611967,
133.647119115499));
#100647=CARTESIAN_POINT('Ctrl Pts',(-106.850924891784,4.09169110239433,
133.533325070447));
#100648=CARTESIAN_POINT('Ctrl Pts',(-106.858415227546,4.16482736529955,
133.423667725561));
#100649=CARTESIAN_POINT('Ctrl Pts',(-106.865905563308,4.23345885960281,
133.311208430056));
#100650=CARTESIAN_POINT('Ctrl Pts',(-106.87339589907,4.2973855471772,133.196359890436));
#100651=CARTESIAN_POINT('Ctrl Pts',(-106.881170233189,4.36373603454005,
133.077156833531));
#100652=CARTESIAN_POINT('Ctrl Pts',(-106.888944567308,4.42522808541707,
132.955002180196));
#100653=CARTESIAN_POINT('Ctrl Pts',(-106.896718901427,4.48158813760678,
132.830329725761));
#100654=CARTESIAN_POINT('Ctrl Pts',(-106.904483654374,4.53787873106935,
132.705810918984));
#100655=CARTESIAN_POINT('Ctrl Pts',(-106.912248407321,4.58904975066781,
132.578780837915));
#100656=CARTESIAN_POINT('Ctrl Pts',(-106.920013160268,4.63487243722153,
132.449699656544));
#100657=CARTESIAN_POINT('Ctrl Pts',(-106.927770201154,4.68064961203698,
132.320746680422));
#100658=CARTESIAN_POINT('Ctrl Pts',(-106.935527242039,4.72108889506038,
132.189747024136));
#100659=CARTESIAN_POINT('Ctrl Pts',(-106.943284282924,4.75600890035877,
132.057182393482));
#100660=CARTESIAN_POINT('Ctrl Pts',(-106.951035474164,4.79090257220928,
131.924717730848));
#100661=CARTESIAN_POINT('Ctrl Pts',(-106.958786665404,4.82028515161546,
131.790690819419));
#100662=CARTESIAN_POINT('Ctrl Pts',(-106.966537856644,4.84402466081358,
131.655599801303));
#100663=CARTESIAN_POINT('Ctrl Pts',(-106.974285753421,4.86775408008712,
131.520566200473));
#100664=CARTESIAN_POINT('Ctrl Pts',(-106.982033650198,4.88584513197175,
131.384469776752));
#100665=CARTESIAN_POINT('Ctrl Pts',(-106.989781546975,4.89821670329584,
131.247819961873));
#100666=CARTESIAN_POINT('Ctrl Pts',(-106.997527823059,4.91058568675391,
131.111198731191));
#100667=CARTESIAN_POINT('Ctrl Pts',(-107.005274099143,4.91723753411131,
130.974024728725));
#100668=CARTESIAN_POINT('Ctrl Pts',(-107.013020375228,4.91814293106795,
130.836813230501));
#100669=CARTESIAN_POINT('Ctrl Pts',(-107.020766708493,4.91904833470803,
130.699600719413));
#100670=CARTESIAN_POINT('Ctrl Pts',(-107.028513041758,4.91420720072357,
130.562351102972));
#100671=CARTESIAN_POINT('Ctrl Pts',(-107.036259375023,4.90364234995155,
130.425579986776));
#100672=CARTESIAN_POINT('Ctrl Pts',(-107.044007443026,4.89307513325447,
130.288778241637));
#100673=CARTESIAN_POINT('Ctrl Pts',(-107.051755511029,4.87678167926728,
130.152455599702));
#100674=CARTESIAN_POINT('Ctrl Pts',(-107.059503579032,4.85483667832409,
130.017122477421));
#100675=CARTESIAN_POINT('Ctrl Pts',(-107.067259881774,4.83286835397271,
129.881645521486));
#100676=CARTESIAN_POINT('Ctrl Pts',(-107.075016184516,4.80523654665141,
129.747160572575));
#100677=CARTESIAN_POINT('Ctrl Pts',(-107.082772487258,4.77206720216523,
129.614168330362));
#100678=CARTESIAN_POINT('Ctrl Pts',(-107.090532929772,4.73888015420119,
129.481105106185));
#100679=CARTESIAN_POINT('Ctrl Pts',(-107.098293372286,4.70014979023972,
129.349536551073));
#100680=CARTESIAN_POINT('Ctrl Pts',(-107.1060538148,4.65605166296224,129.219947169527));
#100681=CARTESIAN_POINT('Ctrl Pts',(-107.113826715066,4.61188274545601,
129.090149759602));
#100682=CARTESIAN_POINT('Ctrl Pts',(-107.121599615331,4.56232898691303,
128.962338236928));
#100683=CARTESIAN_POINT('Ctrl Pts',(-107.129372515597,4.50761406845169,
128.836976955848));
#100684=CARTESIAN_POINT('Ctrl Pts',(-107.136862851359,4.45488817509484,
128.7161728731));
#100685=CARTESIAN_POINT('Ctrl Pts',(-107.144353187121,4.39736998386324,
128.597644257008));
#100686=CARTESIAN_POINT('Ctrl Pts',(-107.151843522883,4.33529859093212,
128.481782483259));
#100687=CARTESIAN_POINT('Ctrl Pts',(-107.159617857002,4.27087374227209,
128.361527775143));
#100688=CARTESIAN_POINT('Ctrl Pts',(-107.167392191121,4.20133952834792,
128.243765197274));
#100689=CARTESIAN_POINT('Ctrl Pts',(-107.17516652524,4.12691304640367,128.128959382251));
#100690=CARTESIAN_POINT('Ctrl Pts',(-107.182931278187,4.05257828844652,
128.014295055135));
#100691=CARTESIAN_POINT('Ctrl Pts',(-107.190696031134,3.9733634695789,127.902580565408));
#100692=CARTESIAN_POINT('Ctrl Pts',(-107.198460784081,3.88953209728597,
127.79425710993));
#100693=CARTESIAN_POINT('Ctrl Pts',(-107.206217824966,3.80578398749381,
127.686041242835));
#100694=CARTESIAN_POINT('Ctrl Pts',(-107.213974865851,3.71742868681588,
127.581210014661));
#100695=CARTESIAN_POINT('Ctrl Pts',(-107.221731906736,3.62477342445343,
127.480176404278));
#100696=CARTESIAN_POINT('Ctrl Pts',(-107.229483097976,3.53218803414521,
127.379218984126));
#100697=CARTESIAN_POINT('Ctrl Pts',(-107.237234289217,3.43530939959924,
127.282053768497));
#100698=CARTESIAN_POINT('Ctrl Pts',(-107.244985480457,3.33448528467254,
127.189061051997));
#100699=CARTESIAN_POINT('Ctrl Pts',(-107.252733377234,3.23370402268439,
127.096107859883));
#100700=CARTESIAN_POINT('Ctrl Pts',(-107.260481274011,3.12898090239863,
127.007323904205));
#100701=CARTESIAN_POINT('Ctrl Pts',(-107.268229170788,3.02070067951069,
126.92305278807));
#100702=CARTESIAN_POINT('Ctrl Pts',(-107.275975446872,2.91244310651083,
126.838799299636));
#100703=CARTESIAN_POINT('Ctrl Pts',(-107.283721722956,2.8006302192435,126.75905701307));
#100704=CARTESIAN_POINT('Ctrl Pts',(-107.29146799904,2.68567968892668,126.684129110601));
#100705=CARTESIAN_POINT('Ctrl Pts',(-107.299214332305,2.57072831007162,
126.609200655032));
#100706=CARTESIAN_POINT('Ctrl Pts',(-107.306960665571,2.45263956947877,
126.539086867966));
#100707=CARTESIAN_POINT('Ctrl Pts',(-107.314706998836,2.33185959596092,
126.474047247009));
#100708=CARTESIAN_POINT('Ctrl Pts',(-107.322455066839,2.21105257460493,
126.408993060879));
#100709=CARTESIAN_POINT('Ctrl Pts',(-107.330203134842,2.08755346521724,
126.349015487342));
#100710=CARTESIAN_POINT('Ctrl Pts',(-107.337951202845,1.96183206756199,
126.294327579862));
#100711=CARTESIAN_POINT('Ctrl Pts',(-107.345707505587,1.83597705170938,
126.239581549423));
#100712=CARTESIAN_POINT('Ctrl Pts',(-107.353463808329,1.70789538857726,
126.190136571632));
#100713=CARTESIAN_POINT('Ctrl Pts',(-107.361220111071,1.57807640776632,
126.14615732512));
#100714=CARTESIAN_POINT('Ctrl Pts',(-107.368980553585,1.44818813865619,
126.102154605561));
#100715=CARTESIAN_POINT('Ctrl Pts',(-107.376740996099,1.31656107926134,
126.063623539884));
#100716=CARTESIAN_POINT('Ctrl Pts',(-107.384501438613,1.18369774745451,
126.030678317164));
#100717=CARTESIAN_POINT('Ctrl Pts',(-107.392274338879,1.05062113163277,
125.997680207848));
#100718=CARTESIAN_POINT('Ctrl Pts',(-107.400047239144,0.916304660886786,
125.970285938371));
#100719=CARTESIAN_POINT('Ctrl Pts',(-107.407820139409,0.78125991478289,
125.948558314336));
#100720=CARTESIAN_POINT('Ctrl Pts',(-107.415310475171,0.651124385358525,
125.927620544164));
#100721=CARTESIAN_POINT('Ctrl Pts',(-107.422800810933,0.520312916416678,
125.911944615227));
#100722=CARTESIAN_POINT('Ctrl Pts',(-107.430291146695,0.389284020730129,
125.90154091726));
#100723=CARTESIAN_POINT('Ctrl Pts',(-107.438065480814,0.253287124636906,
125.890742759924));
#100724=CARTESIAN_POINT('Ctrl Pts',(-107.445839814933,0.116625191572592,
125.88559031356));
#100725=CARTESIAN_POINT('Ctrl Pts',(-107.453614149052,-0.0201935235346973,
125.88615207338));
#100726=CARTESIAN_POINT('Ctrl Pts',(-107.461378901999,-0.156843621803085,
125.88671314088));
#100727=CARTESIAN_POINT('Ctrl Pts',(-107.469143654947,-0.293649730455816,
125.892974400998));
#100728=CARTESIAN_POINT('Ctrl Pts',(-107.476908407894,-0.430098225847748,
125.904952635103));
#100729=CARTESIAN_POINT('Ctrl Pts',(-107.484665448779,-0.566411198670471,
125.916918972257));
#100730=CARTESIAN_POINT('Ctrl Pts',(-107.492422489664,-0.702366878122446,
125.934590949595));
#100731=CARTESIAN_POINT('Ctrl Pts',(-107.500179530549,-0.837451748495209,
125.957933311659));
#100732=CARTESIAN_POINT('Ctrl Pts',(-107.507930721789,-0.9724347503166,
125.981258071066));
#100733=CARTESIAN_POINT('Ctrl Pts',(-107.515681913029,-1.10654786645127,
126.010244637615));
#100734=CARTESIAN_POINT('Ctrl Pts',(-107.523433104269,-1.23928316941682,
126.044805986248));
#100735=CARTESIAN_POINT('Ctrl Pts',(-107.531181001046,-1.37196205633796,
126.079352645386));
#100736=CARTESIAN_POINT('Ctrl Pts',(-107.538928897823,-1.50326391726038,
126.119469275683));
#100737=CARTESIAN_POINT('Ctrl Pts',(-107.5466767946,-1.63269169930937,126.165017897147));
#100738=CARTESIAN_POINT('Ctrl Pts',(-107.554423070684,-1.76209240785649,
126.210556990821));
#100739=CARTESIAN_POINT('Ctrl Pts',(-107.562169346768,-1.88961944871283,
126.261525685881));
#100740=CARTESIAN_POINT('Ctrl Pts',(-107.569915622853,-2.01479198458728,
126.317736461105));
#100741=CARTESIAN_POINT('Ctrl Pts',(-107.577661956118,-2.13996544445746,
126.373947651263));
#100742=CARTESIAN_POINT('Ctrl Pts',(-107.585408289383,-2.26278400801027,
126.435400838638));
#100743=CARTESIAN_POINT('Ctrl Pts',(-107.593154622649,-2.38278820904152,
126.501860947217));
#100744=CARTESIAN_POINT('Ctrl Pts',(-107.600902690652,-2.50281928418105,
126.568335939076));
#100745=CARTESIAN_POINT('Ctrl Pts',(-107.608650758655,-2.62003440070854,
126.63981989395));
#100746=CARTESIAN_POINT('Ctrl Pts',(-107.616398826658,-2.73400037246204,
126.716032716593));
#100747=CARTESIAN_POINT('Ctrl Pts',(-107.624155129399,-2.84808746860638,
126.79232653913));
#100748=CARTESIAN_POINT('Ctrl Pts',(-107.631911432141,-2.95891819626775,
126.873359051527));
#100749=CARTESIAN_POINT('Ctrl Pts',(-107.639667734883,-3.06608951204773,
126.958807579756));
#100750=CARTESIAN_POINT('Ctrl Pts',(-107.647428177397,-3.17331802838582,
127.044301714437));
#100751=CARTESIAN_POINT('Ctrl Pts',(-107.655188619911,-3.27688294596889,
127.134216305205));
#100752=CARTESIAN_POINT('Ctrl Pts',(-107.662949062426,-3.37641657110857,
127.228190291527));
#100753=CARTESIAN_POINT('Ctrl Pts',(-107.670721962691,-3.47610997645951,
127.322315133234));
#100754=CARTESIAN_POINT('Ctrl Pts',(-107.678494862956,-3.5717588845171,
127.420512112318));
#100755=CARTESIAN_POINT('Ctrl Pts',(-107.686267763222,-3.66303393389649,
127.522384770363));
#100756=CARTESIAN_POINT('Ctrl Pts',(-107.693758098984,-3.75099090532443,
127.620554100688));
#100757=CARTESIAN_POINT('Ctrl Pts',(-107.701248434746,-3.83488630251744,
127.722136271789));
#100758=CARTESIAN_POINT('Ctrl Pts',(-107.708738770508,-3.91446354694372,
127.826751139789));
#100759=CARTESIAN_POINT('Ctrl Pts',(-107.716535406243,-3.99729491889724,
127.935643991076));
#100760=CARTESIAN_POINT('Ctrl Pts',(-107.724332041978,-4.0757128098723,
128.048171562633));
#100761=CARTESIAN_POINT('Ctrl Pts',(-107.732128677713,-4.1493821549345,
128.163941939627));
#100762=CARTESIAN_POINT('Ctrl Pts',(-107.739912552866,-4.22293092700115,
128.279522837793));
#100763=CARTESIAN_POINT('Ctrl Pts',(-107.747696428018,-4.29174642551336,
128.398335646724));
#100764=CARTESIAN_POINT('Ctrl Pts',(-107.755480303171,-4.35553438864326,
128.519956263725));
#100765=CARTESIAN_POINT('Ctrl Pts',(-107.763256838091,-4.4192621994103,
128.641462191887));
#100766=CARTESIAN_POINT('Ctrl Pts',(-107.771033373011,-4.47797172552326,
128.765770320832));
#100767=CARTESIAN_POINT('Ctrl Pts',(-107.778809907932,-4.5314123009601,
128.892428186436));
#100768=CARTESIAN_POINT('Ctrl Pts',(-107.786579663597,-4.58480628916007,
129.018975637061));
#100769=CARTESIAN_POINT('Ctrl Pts',(-107.794349419262,-4.63294032147407,
129.14786839028));
#100770=CARTESIAN_POINT('Ctrl Pts',(-107.802119174928,-4.67561020552408,
129.278630540357));
#100771=CARTESIAN_POINT('Ctrl Pts',(-107.808076652511,-4.70832743482112,
129.378892712207));
#100772=CARTESIAN_POINT('Ctrl Pts',(-107.814034130093,-4.73783315307493,
129.480253375528));
#100773=CARTESIAN_POINT('Ctrl Pts',(-107.819991607676,-4.76405452823401,
129.582490119308));
#100774=CARTESIAN_POINT('Origin',(213.235140564004,0.,130.804360617566));
#100775=CARTESIAN_POINT('',(-109.915204178194,-4.76405452823412,129.582490119309));
#100776=CARTESIAN_POINT('',(-109.569720587678,-4.76405452823413,129.582490119309));
#100777=CARTESIAN_POINT('',(213.235140564004,-4.76405452823405,129.582490119308));
#100778=CARTESIAN_POINT('',(-108.235140563964,-4.91824985693288,130.805546905785));
#100779=CARTESIAN_POINT('Ctrl Pts',(-108.23514056401,-4.91824985693268,
130.805546906598));
#100780=CARTESIAN_POINT('Ctrl Pts',(-108.238775383331,-4.91823446811159,
130.869347603656));
#100781=CARTESIAN_POINT('Ctrl Pts',(-108.242410202652,-4.9169776757414,
130.933131835064));
#100782=CARTESIAN_POINT('Ctrl Pts',(-108.246045021973,-4.91448107986788,
130.996867184001));
#100783=CARTESIAN_POINT('Ctrl Pts',(-108.253819356093,-4.90914123522478,
131.133187549347));
#100784=CARTESIAN_POINT('Ctrl Pts',(-108.261593690212,-4.89811664913808,
131.269501489038));
#100785=CARTESIAN_POINT('Ctrl Pts',(-108.269368024331,-4.88139933516864,
131.405296215709));
#100786=CARTESIAN_POINT('Ctrl Pts',(-108.277132777278,-4.8647026237946,
131.540923587515));
#100787=CARTESIAN_POINT('Ctrl Pts',(-108.284897530225,-4.84232719115706,
131.676032635167));
#100788=CARTESIAN_POINT('Ctrl Pts',(-108.292662283172,-4.81431703678716,
131.810111348016));
#100789=CARTESIAN_POINT('Ctrl Pts',(-108.300419324057,-4.78633470249745,
131.944056891998));
#100790=CARTESIAN_POINT('Ctrl Pts',(-108.308176364942,-4.75272886316572,
132.076973757449));
#100791=CARTESIAN_POINT('Ctrl Pts',(-108.315933405827,-4.71359517818133,
132.208356186906));
#100792=CARTESIAN_POINT('Ctrl Pts',(-108.323684597067,-4.67449100421316,
132.339639539851));
#100793=CARTESIAN_POINT('Ctrl Pts',(-108.331435788308,-4.62986739307658,
132.469390386819));
#100794=CARTESIAN_POINT('Ctrl Pts',(-108.339186979548,-4.57987075138741,
132.597114633901));
#100795=CARTESIAN_POINT('Ctrl Pts',(-108.346934876325,-4.52989535960474,
132.724784594771));
#100796=CARTESIAN_POINT('Ctrl Pts',(-108.354682773102,-4.4745516215501,
132.850429305628));
#100797=CARTESIAN_POINT('Ctrl Pts',(-108.362430669879,-4.41403525773697,
132.973571489278));
#100798=CARTESIAN_POINT('Ctrl Pts',(-108.370176945963,-4.35353155264258,
133.096687914239));
#100799=CARTESIAN_POINT('Ctrl Pts',(-108.377923222047,-4.28785754627787,
133.217302502551));
#100800=CARTESIAN_POINT('Ctrl Pts',(-108.385669498131,-4.21725623843067,
133.334959930361));
#100801=CARTESIAN_POINT('Ctrl Pts',(-108.393415831397,-4.14665440942056,
133.452618226691));
#100802=CARTESIAN_POINT('Ctrl Pts',(-108.401162164662,-4.07112540751411,
133.567318983718));
#100803=CARTESIAN_POINT('Ctrl Pts',(-108.408908497928,-3.99095693032238,
133.678633715727));
#100804=CARTESIAN_POINT('Ctrl Pts',(-108.416656565931,-3.91077049995615,
133.789973375898));
#100805=CARTESIAN_POINT('Ctrl Pts',(-108.424404633933,-3.82594275529821,
133.897925184976));
#100806=CARTESIAN_POINT('Ctrl Pts',(-108.432152701936,-3.73680299418588,
134.002092070509));
#100807=CARTESIAN_POINT('Ctrl Pts',(-108.439909004678,-3.64756849427478,
134.106369665848));
#100808=CARTESIAN_POINT('Ctrl Pts',(-108.44766530742,-3.55401307774977,
134.20685400442));
#100809=CARTESIAN_POINT('Ctrl Pts',(-108.455421610162,-3.45650476308482,
134.303182974484));
#100810=CARTESIAN_POINT('Ctrl Pts',(-108.463182052676,-3.35894440529616,
134.399563358221));
#100811=CARTESIAN_POINT('Ctrl Pts',(-108.47094249519,-3.25742723469645,
134.491783691448));
#100812=CARTESIAN_POINT('Ctrl Pts',(-108.478702937705,-3.152355212475,134.579521498493));
#100813=CARTESIAN_POINT('Ctrl Pts',(-108.48647583797,-3.04711451931563,
134.667400150055));
#100814=CARTESIAN_POINT('Ctrl Pts',(-108.494248738235,-2.93830788150435,
134.750781658089));
#100815=CARTESIAN_POINT('Ctrl Pts',(-108.502021638501,-2.82636788297,134.829385791725));
#100816=CARTESIAN_POINT('Ctrl Pts',(-108.509511974263,-2.71849718534192,
134.905132467112));
#100817=CARTESIAN_POINT('Ctrl Pts',(-108.517002310025,-2.60771724196288,
134.976442910247));
#100818=CARTESIAN_POINT('Ctrl Pts',(-108.524492645787,-2.49443584012262,
135.043107236793));
#100819=CARTESIAN_POINT('Ctrl Pts',(-108.532266979906,-2.37685933950062,
135.112299161542));
#100820=CARTESIAN_POINT('Ctrl Pts',(-108.540041314025,-2.25621550335653,
135.176704879091));
#100821=CARTESIAN_POINT('Ctrl Pts',(-108.547815648144,-2.13293143735857,
135.236040496125));
#100822=CARTESIAN_POINT('Ctrl Pts',(-108.555580401091,-2.00979930795374,
135.295302987315));
#100823=CARTESIAN_POINT('Ctrl Pts',(-108.563345154039,-1.88403377178589,
135.349507642609));
#100824=CARTESIAN_POINT('Ctrl Pts',(-108.571109906986,-1.75608938073606,
135.398414725798));
#100825=CARTESIAN_POINT('Ctrl Pts',(-108.578866947871,-1.62827206585947,
135.447273233783));
#100826=CARTESIAN_POINT('Ctrl Pts',(-108.586623988756,-1.49828056552746,
135.490844501837));
#100827=CARTESIAN_POINT('Ctrl Pts',(-108.594381029641,-1.36659209405418,
135.528935636652));
#100828=CARTESIAN_POINT('Ctrl Pts',(-108.602132220881,-1.2350029298811,
135.566998046645));
#100829=CARTESIAN_POINT('Ctrl Pts',(-108.609883412121,-1.10171971578006,
135.599588440916));
#100830=CARTESIAN_POINT('Ctrl Pts',(-108.617634603361,-0.967237283302234,
135.626562925671));
#100831=CARTESIAN_POINT('Ctrl Pts',(-108.625382500138,-0.832812009445832,
135.653525945549));
#100832=CARTESIAN_POINT('Ctrl Pts',(-108.633130396915,-0.697188913494261,
135.674877726568));
#100833=CARTESIAN_POINT('Ctrl Pts',(-108.640878293692,-0.560875333985677,
135.690524953958));
#100834=CARTESIAN_POINT('Ctrl Pts',(-108.648624569777,-0.424590268339345,
135.706168908285));
#100835=CARTESIAN_POINT('Ctrl Pts',(-108.656370845861,-0.287615394592241,
135.716110637903));
#100836=CARTESIAN_POINT('Ctrl Pts',(-108.664117121945,-0.150465136920227,
135.720308471752));
#100837=CARTESIAN_POINT('Ctrl Pts',(-108.67186345521,-0.0133138668359791,
135.724506336587));
#100838=CARTESIAN_POINT('Ctrl Pts',(-108.679609788475,0.124012398974345,
135.722960209086));
#100839=CARTESIAN_POINT('Ctrl Pts',(-108.687356121741,0.260997655756491,
135.715680530399));
#100840=CARTESIAN_POINT('Ctrl Pts',(-108.695104189744,0.398013589436917,
135.708399221479));
#100841=CARTESIAN_POINT('Ctrl Pts',(-108.702852257747,0.534687971788868,
135.695381827127));
#100842=CARTESIAN_POINT('Ctrl Pts',(-108.71060032575,0.670508740988721,
135.676690767582));
#100843=CARTESIAN_POINT('Ctrl Pts',(-108.718356628492,0.806473862118552,
135.657979842957));
#100844=CARTESIAN_POINT('Ctrl Pts',(-108.726112931234,0.941583169873703,
135.633583260871));
#100845=CARTESIAN_POINT('Ctrl Pts',(-108.733869233976,1.0753330864168,135.60361491545));
#100846=CARTESIAN_POINT('Ctrl Pts',(-108.74162967649,1.20915438931712,135.57363057502));
#100847=CARTESIAN_POINT('Ctrl Pts',(-108.749390119004,1.34161447788036,
135.538068646995));
#100848=CARTESIAN_POINT('Ctrl Pts',(-108.757150561518,1.47222477434846,
135.497093006728));
#100849=CARTESIAN_POINT('Ctrl Pts',(-108.764923461783,1.60304473805985,
135.456051588726));
#100850=CARTESIAN_POINT('Ctrl Pts',(-108.772696362049,1.73200860774313,
135.40957922457));
#100851=CARTESIAN_POINT('Ctrl Pts',(-108.780469262314,1.85864679505001,
135.357888387741));
#100852=CARTESIAN_POINT('Ctrl Pts',(-108.787959598076,1.98068136526252,
135.308076643032));
#100853=CARTESIAN_POINT('Ctrl Pts',(-108.795449933838,2.10055612603258,
135.253419375587));
#100854=CARTESIAN_POINT('Ctrl Pts',(-108.8029402696,2.21787407673078,135.194146220789));
#100855=CARTESIAN_POINT('Ctrl Pts',(-108.810714603719,2.33964017319065,
135.13262570631));
#100856=CARTESIAN_POINT('Ctrl Pts',(-108.818488937838,2.45903746775401,
135.065937493684));
#100857=CARTESIAN_POINT('Ctrl Pts',(-108.826263271957,2.57559625188908,
134.994287467734));
#100858=CARTESIAN_POINT('Ctrl Pts',(-108.834028024904,2.69201138773987,
134.922725744037));
#100859=CARTESIAN_POINT('Ctrl Pts',(-108.841792777851,2.80559464368708,
134.846214576803));
#100860=CARTESIAN_POINT('Ctrl Pts',(-108.849557530798,2.91589862647236,
134.765006810126));
#100861=CARTESIAN_POINT('Ctrl Pts',(-108.857314571683,3.02609305378692,
134.683879700147));
#100862=CARTESIAN_POINT('Ctrl Pts',(-108.865071612568,3.13301437675168,
134.598065504037));
#100863=CARTESIAN_POINT('Ctrl Pts',(-108.872828653453,3.23624236276918,
134.507861452171));
#100864=CARTESIAN_POINT('Ctrl Pts',(-108.880579844694,3.33939250375929,
134.417725423881));
#100865=CARTESIAN_POINT('Ctrl Pts',(-108.888331035934,3.43885455831209,
134.32320638525));
#100866=CARTESIAN_POINT('Ctrl Pts',(-108.896082227174,3.53423999596275,
134.224642873965));
#100867=CARTESIAN_POINT('Ctrl Pts',(-108.903830123951,3.62958489225804,
134.126121254801));
#100868=CARTESIAN_POINT('Ctrl Pts',(-108.911578020728,3.72085634648314,
134.023558862319));
#100869=CARTESIAN_POINT('Ctrl Pts',(-108.919325917505,3.80770162140692,
133.917332095886));
#100870=CARTESIAN_POINT('Ctrl Pts',(-108.927072193589,3.89452873017134,
133.811127549803));
#100871=CARTESIAN_POINT('Ctrl Pts',(-108.934818469673,3.97693125392143,
133.701260456889));
#100872=CARTESIAN_POINT('Ctrl Pts',(-108.942564745757,4.05459607477986,
133.588141092546));
#100873=CARTESIAN_POINT('Ctrl Pts',(-108.950311079023,4.13226146894226,
133.475020893181));
#100874=CARTESIAN_POINT('Ctrl Pts',(-108.958057412288,4.20518886913727,
133.358648696793));
#100875=CARTESIAN_POINT('Ctrl Pts',(-108.965803745553,4.27310814662839,
133.239464276493));
#100876=CARTESIAN_POINT('Ctrl Pts',(-108.973551813556,4.34104263417088,
133.120253165668));
#100877=CARTESIAN_POINT('Ctrl Pts',(-108.981299881559,4.40396657374991,
132.998228917361));
#100878=CARTESIAN_POINT('Ctrl Pts',(-108.989047949562,4.46165569935583,
132.873856083351));
#100879=CARTESIAN_POINT('Ctrl Pts',(-108.996804252304,4.51940613765103,
132.749351064413));
#100880=CARTESIAN_POINT('Ctrl Pts',(-109.004560555046,4.5719104832655,132.622492828768));
#100881=CARTESIAN_POINT('Ctrl Pts',(-109.012316857788,4.61899236242985,
132.493766613268));
#100882=CARTESIAN_POINT('Ctrl Pts',(-109.020077300302,4.66609937061072,
132.364971692712));
#100883=CARTESIAN_POINT('Ctrl Pts',(-109.027837742816,4.70777802678318,
132.234307177993));
#100884=CARTESIAN_POINT('Ctrl Pts',(-109.03559818533,4.74390211571169,132.102272702049));
#100885=CARTESIAN_POINT('Ctrl Pts',(-109.043371085596,4.7800841942347,131.970026272642));
#100886=CARTESIAN_POINT('Ctrl Pts',(-109.051143985861,4.81069379978623,
131.836405868655));
#100887=CARTESIAN_POINT('Ctrl Pts',(-109.058916886127,4.83565586834993,
131.701921415169));
#100888=CARTESIAN_POINT('Ctrl Pts',(-109.066407221889,4.85971050284589,
131.572325810311));
#100889=CARTESIAN_POINT('Ctrl Pts',(-109.073897557651,4.87852103207088,
131.441928190909));
#100890=CARTESIAN_POINT('Ctrl Pts',(-109.081387893413,4.89206606623963,
131.31118668837));
#100891=CARTESIAN_POINT('Ctrl Pts',(-109.089162227532,4.90612466449572,
131.175488082025));
#100892=CARTESIAN_POINT('Ctrl Pts',(-109.096936561651,4.91455513665716,
131.038989148726));
#100893=CARTESIAN_POINT('Ctrl Pts',(-109.10471089577,4.91727681052279,130.902196353342));
#100894=CARTESIAN_POINT('Ctrl Pts',(-109.112475648717,4.91999513016862,
130.765572142852));
#100895=CARTESIAN_POINT('Ctrl Pts',(-109.120240401664,4.91701864253065,
130.628655178));
#100896=CARTESIAN_POINT('Ctrl Pts',(-109.128005154612,4.90831824552124,
130.491958531812));
#100897=CARTESIAN_POINT('Ctrl Pts',(-109.135762195497,4.8996264898688,130.355397654661));
#100898=CARTESIAN_POINT('Ctrl Pts',(-109.143519236382,4.88522216305875,
130.219057048356));
#100899=CARTESIAN_POINT('Ctrl Pts',(-109.151276277267,4.86512818743791,
130.083450926761));
#100900=CARTESIAN_POINT('Ctrl Pts',(-109.159027468507,4.84504936484035,
129.947947066796));
#100901=CARTESIAN_POINT('Ctrl Pts',(-109.166778659747,4.81928949070307,
129.813176974253));
#100902=CARTESIAN_POINT('Ctrl Pts',(-109.174529850987,4.78792337616393,
129.679650518704));
#100903=CARTESIAN_POINT('Ctrl Pts',(-109.182277747764,4.75657059306024,
129.54618081546));
#100904=CARTESIAN_POINT('Ctrl Pts',(-109.190025644541,4.71961639798478,
129.413954077716));
#100905=CARTESIAN_POINT('Ctrl Pts',(-109.197773541318,4.67718680329669,
129.283470526347));
#100906=CARTESIAN_POINT('Ctrl Pts',(-109.205519817402,4.63476608396513,
129.153014269324));
#100907=CARTESIAN_POINT('Ctrl Pts',(-109.213266093487,4.58687236397928,
129.02430084496));
#100908=CARTESIAN_POINT('Ctrl Pts',(-109.221012369571,4.53368157179299,
128.897815452068));
#100909=CARTESIAN_POINT('Ctrl Pts',(-109.228758702836,4.48049038696428,
128.771329125489));
#100910=CARTESIAN_POINT('Ctrl Pts',(-109.236505036101,4.42200220346684,
128.647071223597));
#100911=CARTESIAN_POINT('Ctrl Pts',(-109.244251369367,4.35844100369424,
128.525506721456));
#100912=CARTESIAN_POINT('Ctrl Pts',(-109.25199943737,4.29486556983173,128.403914995787));
#100913=CARTESIAN_POINT('Ctrl Pts',(-109.259747505373,4.22621504017031,
128.285018216504));
#100914=CARTESIAN_POINT('Ctrl Pts',(-109.267495573375,4.15275903402116,
128.169256166533));
#100915=CARTESIAN_POINT('Ctrl Pts',(-109.275251876117,4.07922495795443,
128.053371083277));
#100916=CARTESIAN_POINT('Ctrl Pts',(-109.283008178859,4.00087541278862,
127.940627715261));
#100917=CARTESIAN_POINT('Ctrl Pts',(-109.290764481601,3.91802330770006,
127.831436733102));
#100918=CARTESIAN_POINT('Ctrl Pts',(-109.298524924115,3.83512698194838,
127.722187472428));
#100919=CARTESIAN_POINT('Ctrl Pts',(-109.306285366629,3.74772355682294,
127.616494676725));
#100920=CARTESIAN_POINT('Ctrl Pts',(-109.314045809144,3.65616516524623,
127.514734598253));
#100921=CARTESIAN_POINT('Ctrl Pts',(-109.321818709409,3.56445979601119,
127.412811165469));
#100922=CARTESIAN_POINT('Ctrl Pts',(-109.329591609675,3.46858640529162,
127.314833345195));
#100923=CARTESIAN_POINT('Ctrl Pts',(-109.33736450994,3.36893343356707,127.221139917875));
#100924=CARTESIAN_POINT('Ctrl Pts',(-109.344854845702,3.27290309837567,
127.130852482638));
#100925=CARTESIAN_POINT('Ctrl Pts',(-109.352345181464,3.17336343864022,
127.044543553235));
#100926=CARTESIAN_POINT('Ctrl Pts',(-109.359835517226,3.07068833158736,
126.962478756713));
#100927=CARTESIAN_POINT('Ctrl Pts',(-109.367609851345,2.96412026664301,
126.877302448488));
#100928=CARTESIAN_POINT('Ctrl Pts',(-109.375384185464,2.85383672433764,
126.796428645875));
#100929=CARTESIAN_POINT('Ctrl Pts',(-109.383158519583,2.74022020261252,
126.720198977315));
#100930=CARTESIAN_POINT('Ctrl Pts',(-109.39092327253,2.62674370309654,126.644063255009));
#100931=CARTESIAN_POINT('Ctrl Pts',(-109.398688025477,2.50994271860356,
126.572560494472));
#100932=CARTESIAN_POINT('Ctrl Pts',(-109.406452778424,2.39023318161349,
126.505992508619));
#100933=CARTESIAN_POINT('Ctrl Pts',(-109.414209819309,2.27064254182317,
126.439490639027));
#100934=CARTESIAN_POINT('Ctrl Pts',(-109.421966860194,2.14814943788668,
126.377913979112));
#100935=CARTESIAN_POINT('Ctrl Pts',(-109.429723901079,2.0231988825782,126.321521188807));
#100936=CARTESIAN_POINT('Ctrl Pts',(-109.437475092319,1.89834255345527,
126.265170924744));
#100937=CARTESIAN_POINT('Ctrl Pts',(-109.44522628356,1.77103281652043,126.213996909451));
#100938=CARTESIAN_POINT('Ctrl Pts',(-109.4529774748,1.6417390767333,126.168211799158));
#100939=CARTESIAN_POINT('Ctrl Pts',(-109.460725371577,1.51250029023479,
126.122446148758));
#100940=CARTESIAN_POINT('Ctrl Pts',(-109.468473268354,1.38127954582082,
126.082064978104));
#100941=CARTESIAN_POINT('Ctrl Pts',(-109.476221165131,1.24856580623878,
126.047232651031));
#100942=CARTESIAN_POINT('Ctrl Pts',(-109.483967441215,1.11587982751008,
126.012407610129));
#100943=CARTESIAN_POINT('Ctrl Pts',(-109.491713717299,0.981701852717511,
125.983129203305));
#100944=CARTESIAN_POINT('Ctrl Pts',(-109.499459993383,0.84653518699155,
125.959511678777));
#100945=CARTESIAN_POINT('Ctrl Pts',(-109.507206326648,0.711367523495783,
125.93589397991));
#100946=CARTESIAN_POINT('Ctrl Pts',(-109.514952659914,0.575211539633765,
125.917937314017));
#100947=CARTESIAN_POINT('Ctrl Pts',(-109.522698993179,0.438579500051587,
125.905704568747));
#100948=CARTESIAN_POINT('Ctrl Pts',(-109.530447061182,0.30191686267167,
125.893469084038));
#100949=CARTESIAN_POINT('Ctrl Pts',(-109.538195129185,0.164778346764372,
125.886960105508));
#100950=CARTESIAN_POINT('Ctrl Pts',(-109.545943197188,0.0276796899863722,
125.886188508208));
#100951=CARTESIAN_POINT('Ctrl Pts',(-109.55369949993,-0.109564676875734,
125.885416090846));
#100952=CARTESIAN_POINT('Ctrl Pts',(-109.561455802672,-0.24676870840196,
125.890393237846));
#100953=CARTESIAN_POINT('Ctrl Pts',(-109.569212105413,-0.383417760716848,
125.901078667355));
#100954=CARTESIAN_POINT('Ctrl Pts',(-109.576972547928,-0.520139746745752,
125.911769799999));
#100955=CARTESIAN_POINT('Ctrl Pts',(-109.584732990442,-0.656305775373332,
125.928175239184));
#100956=CARTESIAN_POINT('Ctrl Pts',(-109.592493432956,-0.791408958472185,
125.950202099043));
#100957=CARTESIAN_POINT('Ctrl Pts',(-109.600266333221,-0.926729021194078,
125.972264318373));
#100958=CARTESIAN_POINT('Ctrl Pts',(-109.608039233487,-1.06098244578844,
125.999965912161));
#100959=CARTESIAN_POINT('Ctrl Pts',(-109.615812133752,-1.19367424510417,
126.033163193536));
#100960=CARTESIAN_POINT('Ctrl Pts',(-109.623302469514,-1.32154236328789,
126.065153670114));
#100961=CARTESIAN_POINT('Ctrl Pts',(-109.630792805277,-1.44796012747283,
126.102247120405));
#100962=CARTESIAN_POINT('Ctrl Pts',(-109.638283141039,-1.57250196832677,
126.144272568815));
#100963=CARTESIAN_POINT('Ctrl Pts',(-109.646057503716,-1.70176632575835,
126.187891585102));
#100964=CARTESIAN_POINT('Ctrl Pts',(-109.653831866393,-1.82941915778745,
126.236962187181));
#100965=CARTESIAN_POINT('Ctrl Pts',(-109.661606229069,-1.9549662878274,
126.291347225612));
#100966=CARTESIAN_POINT('Ctrl Pts',(-109.669371003863,-2.08035858443769,
126.345665192641));
#100967=CARTESIAN_POINT('Ctrl Pts',(-109.677135778657,-2.20364999081397,
126.405284401296));
#100968=CARTESIAN_POINT('Ctrl Pts',(-109.68490055345,-2.32436175758185,
126.470018051226));
#100969=CARTESIAN_POINT('Ctrl Pts',(-109.692657609498,-2.44495352816216,
126.534687351246));
#100970=CARTESIAN_POINT('Ctrl Pts',(-109.700414665547,-2.56297041999857,
126.60446079129));
#100971=CARTESIAN_POINT('Ctrl Pts',(-109.708171721595,-2.67795427236633,
126.67910377979));
#100972=CARTESIAN_POINT('Ctrl Pts',(-109.715922921337,-2.79285131593833,
126.753690415439));
#100973=CARTESIAN_POINT('Ctrl Pts',(-109.723674121079,-2.90471955124832,
126.833139069955));
#100974=CARTESIAN_POINT('Ctrl Pts',(-109.73142532082,-3.01312633856167,
126.917169764216));
#100975=CARTESIAN_POINT('Ctrl Pts',(-109.739173191178,-3.12148656175295,
127.001164364653));
#100976=CARTESIAN_POINT('Ctrl Pts',(-109.746921061536,-3.22638798590924,
127.089736851114));
#100977=CARTESIAN_POINT('Ctrl Pts',(-109.754668931894,-3.32742803514063,
127.182564691032));
#100978=CARTESIAN_POINT('Ctrl Pts',(-109.762415172071,-3.42844682516336,
127.275372999621));
#100979=CARTESIAN_POINT('Ctrl Pts',(-109.770161412247,-3.52560556860359,
127.372434616387));
#100980=CARTESIAN_POINT('Ctrl Pts',(-109.777907652424,-3.6185361017395,
127.473387855308));
#100981=CARTESIAN_POINT('Ctrl Pts',(-109.785653940287,-3.71146720696074,
127.574341715702));
#100982=CARTESIAN_POINT('Ctrl Pts',(-109.793400228149,-3.8001697851892,
127.679186958386));
#100983=CARTESIAN_POINT('Ctrl Pts',(-109.801146516012,-3.88431404145138,
127.787526599944));
#100984=CARTESIAN_POINT('Ctrl Pts',(-109.808894529103,-3.96847703804494,
127.895890370549));
#100985=CARTESIAN_POINT('Ctrl Pts',(-109.816642542193,-4.04807945281788,
128.007749779919));
#100986=CARTESIAN_POINT('Ctrl Pts',(-109.824390555284,-4.1228333732546,
128.122676810911));
#100987=CARTESIAN_POINT('Ctrl Pts',(-109.832146669428,-4.19766545379882,
128.237724005622));
#100988=CARTESIAN_POINT('Ctrl Pts',(-109.839902783573,-4.26763870030987,
128.355844900542));
#100989=CARTESIAN_POINT('Ctrl Pts',(-109.847658897717,-4.3325096834453,
128.476584231108));
#100990=CARTESIAN_POINT('Ctrl Pts',(-109.855419147713,-4.39741525822069,
128.597387944411));
#100991=CARTESIAN_POINT('Ctrl Pts',(-109.863179397708,-4.45721297802206,
128.720812523861));
#100992=CARTESIAN_POINT('Ctrl Pts',(-109.870939647703,-4.51170701715605,
128.84638133937));
#100993=CARTESIAN_POINT('Ctrl Pts',(-109.878712038238,-4.56628630960457,
128.972146601277));
#100994=CARTESIAN_POINT('Ctrl Pts',(-109.886484428773,-4.61554520146936,
129.100062437227));
#100995=CARTESIAN_POINT('Ctrl Pts',(-109.894256819308,-4.65933705204792,
129.229634832576));
#100996=CARTESIAN_POINT('Ctrl Pts',(-109.90123927227,-4.69867817051366,
129.346038293219));
#100997=CARTESIAN_POINT('Ctrl Pts',(-109.908221725232,-4.73360767680117,
129.463778307667));
#100998=CARTESIAN_POINT('Ctrl Pts',(-109.915204178194,-4.76405452823412,
129.582490119309));
#100999=CARTESIAN_POINT('Ctrl Pts',(-108.165013787364,-4.76405452823417,
129.582490119309));
#101000=CARTESIAN_POINT('Ctrl Pts',(-108.172724877397,-4.79792817128851,
129.714562939473));
#101001=CARTESIAN_POINT('Ctrl Pts',(-108.180435967429,-4.82627913472933,
129.847942656428));
#101002=CARTESIAN_POINT('Ctrl Pts',(-108.188147057461,-4.84903199837822,
129.982124799078));
#101003=CARTESIAN_POINT('Ctrl Pts',(-108.195979308545,-4.87214236801854,
130.118415288206));
#101004=CARTESIAN_POINT('Ctrl Pts',(-108.203811559628,-4.88947718626042,
130.25553320641));
#101005=CARTESIAN_POINT('Ctrl Pts',(-108.211643810712,-4.90101233682553,
130.39294703395));
#101006=CARTESIAN_POINT('Ctrl Pts',(-108.219476061796,-4.91254748739063,
130.53036086149));
#101007=CARTESIAN_POINT('Ctrl Pts',(-108.22730831288,-4.91828301649803,
130.668070174626));
#101008=CARTESIAN_POINT('Ctrl Pts',(-108.235140563964,-4.91824985693288,
130.805546905785));
#101009=CARTESIAN_POINT('',(-107.889859436047,-4.918248694981,130.80794346806));
#101010=CARTESIAN_POINT('Ctrl Pts',(-107.819991607676,-4.76405452823401,
129.582490119308));
#101011=CARTESIAN_POINT('Ctrl Pts',(-107.827755149809,-4.7982251563202,
129.715720879604));
#101012=CARTESIAN_POINT('Ctrl Pts',(-107.835518691941,-4.82681644330726,
129.850439672405));
#101013=CARTESIAN_POINT('Ctrl Pts',(-107.843282234073,-4.84971133876424,
129.986141213517));
#101014=CARTESIAN_POINT('Ctrl Pts',(-107.851046301406,-4.87260778305285,
130.121851934792));
#101015=CARTESIAN_POINT('Ctrl Pts',(-107.858810368739,-4.88980699116055,
130.258545156335));
#101016=CARTESIAN_POINT('Ctrl Pts',(-107.866574436072,-4.90124315007472,
130.395705938961));
#101017=CARTESIAN_POINT('Ctrl Pts',(-107.874336102712,-4.91267577286425,
130.532824310702));
#101018=CARTESIAN_POINT('Ctrl Pts',(-107.882097769352,-4.91834888578083,
130.670409567373));
#101019=CARTESIAN_POINT('Ctrl Pts',(-107.889859435992,-4.91824869498171,
130.807943467089));
#101020=CARTESIAN_POINT('Ctrl Pts',(-107.889859436047,-4.918248694981,130.80794346806));
#101021=CARTESIAN_POINT('Ctrl Pts',(-107.89875976081,-4.91813380588136,
130.965653974093));
#101022=CARTESIAN_POINT('Ctrl Pts',(-107.907660085574,-4.91042916089496,
131.123058384268));
#101023=CARTESIAN_POINT('Ctrl Pts',(-107.916560410337,-4.89524667639518,
131.279484853679));
#101024=CARTESIAN_POINT('Ctrl Pts',(-107.925505275757,-4.87998821288942,
131.436694141453));
#101025=CARTESIAN_POINT('Ctrl Pts',(-107.934450141177,-4.85717698919893,
131.592915538265));
#101026=CARTESIAN_POINT('Ctrl Pts',(-107.943395006597,-4.82697604074685,
131.747485935091));
#101027=CARTESIAN_POINT('Ctrl Pts',(-107.952396337752,-4.79658444451355,
131.903032079524));
#101028=CARTESIAN_POINT('Ctrl Pts',(-107.961397668907,-4.75870961922783,
132.056906178003));
#101029=CARTESIAN_POINT('Ctrl Pts',(-107.970399000062,-4.71356615637689,
132.20845361732));
#101030=CARTESIAN_POINT('Ctrl Pts',(-107.975994798149,-4.68550211799258,
132.302665112971));
#101031=CARTESIAN_POINT('Ctrl Pts',(-107.981590596235,-4.6546299540778,
132.395977861219));
#101032=CARTESIAN_POINT('Ctrl Pts',(-107.987186394322,-4.62101034714682,
132.488239008087));
#101033=CARTESIAN_POINT('Ctrl Pts',(-107.994960728441,-4.57430207547727,
132.616418933607));
#101034=CARTESIAN_POINT('Ctrl Pts',(-108.00273506256,-4.52218249989022,
132.742856987582));
#101035=CARTESIAN_POINT('Ctrl Pts',(-108.010509396679,-4.46480058747047,
132.867062432328));
#101036=CARTESIAN_POINT('Ctrl Pts',(-108.018274149626,-4.4074893931294,
132.991114804965));
#101037=CARTESIAN_POINT('Ctrl Pts',(-108.026038902573,-4.34492892828445,
133.112939691508));
#101038=CARTESIAN_POINT('Ctrl Pts',(-108.03380365552,-4.27731742623493,
133.232062967058));
#101039=CARTESIAN_POINT('Ctrl Pts',(-108.041560696405,-4.2097730768824,
133.35106792769));
#101040=CARTESIAN_POINT('Ctrl Pts',(-108.04931773729,-4.13718786564272,
133.467376279358));
#101041=CARTESIAN_POINT('Ctrl Pts',(-108.057074778175,-4.05980730933153,
133.580535625306));
#101042=CARTESIAN_POINT('Ctrl Pts',(-108.064825969415,-3.98248510629969,
133.693609636911));
#101043=CARTESIAN_POINT('Ctrl Pts',(-108.072577160656,-3.90037497582993,
133.803539048052));
#101044=CARTESIAN_POINT('Ctrl Pts',(-108.080328351896,-3.81376719722825,
133.909898063459));
#101045=CARTESIAN_POINT('Ctrl Pts',(-108.088076248673,-3.7271962292427,
134.016211873448));
#101046=CARTESIAN_POINT('Ctrl Pts',(-108.09582414545,-3.63613166154339,
134.118958003389));
#101047=CARTESIAN_POINT('Ctrl Pts',(-108.103572042227,-3.54090559760411,
134.217741728921));
#101048=CARTESIAN_POINT('Ctrl Pts',(-108.111318318311,-3.44569945290483,
134.316504791027));
#101049=CARTESIAN_POINT('Ctrl Pts',(-108.119064594395,-3.3463338145956,
134.411306816053));
#101050=CARTESIAN_POINT('Ctrl Pts',(-108.126810870479,-3.24317910446583,
134.501788420628));
#101051=CARTESIAN_POINT('Ctrl Pts',(-108.134557203744,-3.14002363287128,
134.592270693118));
#101052=CARTESIAN_POINT('Ctrl Pts',(-108.14230353701,-3.03307932756264,
134.678432223707));
#101053=CARTESIAN_POINT('Ctrl Pts',(-108.150049870275,-2.92275097896852,
134.759952833333));
#101054=CARTESIAN_POINT('Ctrl Pts',(-108.157797938278,-2.81239792310586,
134.841491698935));
#101055=CARTESIAN_POINT('Ctrl Pts',(-108.165546006281,-2.69865963033845,
134.918387343188));
#101056=CARTESIAN_POINT('Ctrl Pts',(-108.173294074284,-2.58197091311574,
134.990362202172));
#101057=CARTESIAN_POINT('Ctrl Pts',(-108.181050377026,-2.46515817773561,
135.062413556893));
#101058=CARTESIAN_POINT('Ctrl Pts',(-108.188806679768,-2.34538908719667,
135.129533473541));
#101059=CARTESIAN_POINT('Ctrl Pts',(-108.19656298251,-2.22312465073385,
135.191489502133));
#101060=CARTESIAN_POINT('Ctrl Pts',(-108.204323425024,-2.10079495805999,
135.253478598523));
#101061=CARTESIAN_POINT('Ctrl Pts',(-108.212083867538,-1.9759676213175,
135.310298153157));
#101062=CARTESIAN_POINT('Ctrl Pts',(-108.219844310052,-1.84912386922385,
135.361763823205));
#101063=CARTESIAN_POINT('Ctrl Pts',(-108.227617210318,-1.72207649627869,
135.413312110516));
#101064=CARTESIAN_POINT('Ctrl Pts',(-108.235390110583,-1.59300660789415,
135.459489206854));
#101065=CARTESIAN_POINT('Ctrl Pts',(-108.243163010848,-1.4624116943013,
135.500160346991));
#101066=CARTESIAN_POINT('Ctrl Pts',(-108.25065334661,-1.33656423476664,
135.539352988741));
#101067=CARTESIAN_POINT('Ctrl Pts',(-108.258143682372,-1.20930099958607,
135.573432955384));
#101068=CARTESIAN_POINT('Ctrl Pts',(-108.265634018134,-1.08107438723236,
135.602324897526));
#101069=CARTESIAN_POINT('Ctrl Pts',(-108.273408352253,-0.94798602389743,
135.632312286436));
#101070=CARTESIAN_POINT('Ctrl Pts',(-108.281182686372,-0.813438204480298,
135.656805467986));
#101071=CARTESIAN_POINT('Ctrl Pts',(-108.288957020491,-0.677924320839947,
135.6756645167));
#101072=CARTESIAN_POINT('Ctrl Pts',(-108.296721773438,-0.542577445949959,
135.694500323321));
#101073=CARTESIAN_POINT('Ctrl Pts',(-108.304486526386,-0.406267259267573,
135.707715759358));
#101074=CARTESIAN_POINT('Ctrl Pts',(-108.312251279333,-0.269499805440736,
135.715221328008));
#101075=CARTESIAN_POINT('Ctrl Pts',(-108.320008320218,-0.132868190977123,
135.722719442023));
#101076=CARTESIAN_POINT('Ctrl Pts',(-108.327765361103,0.00421939897204796,
135.724518953153));
#101077=CARTESIAN_POINT('Ctrl Pts',(-108.335522401988,0.141249642368628,
135.720581890152));
#101078=CARTESIAN_POINT('Ctrl Pts',(-108.343273593228,0.278176550192536,
135.716647796122));
#101079=CARTESIAN_POINT('Ctrl Pts',(-108.351024784468,0.415045808318711,
135.706985749775));
#101080=CARTESIAN_POINT('Ctrl Pts',(-108.358775975708,0.551342280071368,
135.691609818569));
#101081=CARTESIAN_POINT('Ctrl Pts',(-108.366523872485,0.687580822187889,
135.676240422544));
#101082=CARTESIAN_POINT('Ctrl Pts',(-108.374271769262,0.823246674445855,
135.655162015603));
#101083=CARTESIAN_POINT('Ctrl Pts',(-108.382019666039,0.957828234021382,
135.628440647645));
#101084=CARTESIAN_POINT('Ctrl Pts',(-108.389765942123,1.09238164203589,
135.601724869222));
#101085=CARTESIAN_POINT('Ctrl Pts',(-108.397512218207,1.22585082527036,
135.569368553726));
#101086=CARTESIAN_POINT('Ctrl Pts',(-108.405258494291,1.35773320229044,
135.53148909201));
#101087=CARTESIAN_POINT('Ctrl Pts',(-108.413004827557,1.48961655283645,
135.493609350676));
#101088=CARTESIAN_POINT('Ctrl Pts',(-108.420751160822,1.6199126980223,135.450206489696));
#101089=CARTESIAN_POINT('Ctrl Pts',(-108.428497494087,1.74813346301937,
135.401448006117));
#101090=CARTESIAN_POINT('Ctrl Pts',(-108.43624556209,1.87638294216757,135.352678603414));
#101091=CARTESIAN_POINT('Ctrl Pts',(-108.443993630094,2.00255575092929,
135.298551330472));
#101092=CARTESIAN_POINT('Ctrl Pts',(-108.451741698097,2.12618334016567,
135.239281977241));
#101093=CARTESIAN_POINT('Ctrl Pts',(-108.459498000838,2.24994232227492,
135.179949631836));
#101094=CARTESIAN_POINT('Ctrl Pts',(-108.46725430358,2.37115032804475,135.115464458372));
#101095=CARTESIAN_POINT('Ctrl Pts',(-108.475010606322,2.48936260396792,
135.046088672082));
#101096=CARTESIAN_POINT('Ctrl Pts',(-108.482771048836,2.60763797334238,
134.976675857845));
#101097=CARTESIAN_POINT('Ctrl Pts',(-108.49053149135,2.72291409845608,134.902367441324));
#101098=CARTESIAN_POINT('Ctrl Pts',(-108.498291933864,2.83477577058887,
134.823468652066));
#101099=CARTESIAN_POINT('Ctrl Pts',(-108.50606483413,2.94681701300808,134.744443207467));
#101100=CARTESIAN_POINT('Ctrl Pts',(-108.513837734395,3.0554325393396,134.660812903429));
#101101=CARTESIAN_POINT('Ctrl Pts',(-108.521610634661,3.160240062159,134.572923448676));
#101102=CARTESIAN_POINT('Ctrl Pts',(-108.529100970423,3.26123756753083,
134.488228996982));
#101103=CARTESIAN_POINT('Ctrl Pts',(-108.536591306185,3.35869889585605,
134.399579887362));
#101104=CARTESIAN_POINT('Ctrl Pts',(-108.544081641947,3.45231612113009,
134.307316007274));
#101105=CARTESIAN_POINT('Ctrl Pts',(-108.551855976066,3.54948287195378,
134.211553914131));
#101106=CARTESIAN_POINT('Ctrl Pts',(-108.559630310185,3.64281606218321,
134.11159418597));
#101107=CARTESIAN_POINT('Ctrl Pts',(-108.567404644304,3.73193127820006,
134.007776294198));
#101108=CARTESIAN_POINT('Ctrl Pts',(-108.575169397251,3.82093666767763,
133.904086348699));
#101109=CARTESIAN_POINT('Ctrl Pts',(-108.582934150198,3.90573417375926,
133.796547994121));
#101110=CARTESIAN_POINT('Ctrl Pts',(-108.590698903146,3.9859749707582,133.685538604951));
#101111=CARTESIAN_POINT('Ctrl Pts',(-108.598455944031,4.06613607146636,
133.57463947187));
#101112=CARTESIAN_POINT('Ctrl Pts',(-108.606212984916,4.14174924206289,
133.460276479645));
#101113=CARTESIAN_POINT('Ctrl Pts',(-108.613970025801,4.212505073163,133.342860976257));
#101114=CARTESIAN_POINT('Ctrl Pts',(-108.621721217041,4.28320754674038,
133.225534016814));
#101115=CARTESIAN_POINT('Ctrl Pts',(-108.629472408281,4.34905977074026,
133.105159461555));
#101116=CARTESIAN_POINT('Ctrl Pts',(-108.637223599521,4.40979513655629,
132.982178313358));
#101117=CARTESIAN_POINT('Ctrl Pts',(-108.644971496298,4.47050468822176,
132.859249435429));
#101118=CARTESIAN_POINT('Ctrl Pts',(-108.652719393075,4.52610153445893,
132.733716517848));
#101119=CARTESIAN_POINT('Ctrl Pts',(-108.660467289852,4.57636471109577,
132.606045688142));
#101120=CARTESIAN_POINT('Ctrl Pts',(-108.668213565936,4.62661737375961,
132.478401564422));
#101121=CARTESIAN_POINT('Ctrl Pts',(-108.67595984202,4.67153844285894,132.348620781651));
#101122=CARTESIAN_POINT('Ctrl Pts',(-108.683706118104,4.71095502510017,
132.217189628446));
#101123=CARTESIAN_POINT('Ctrl Pts',(-108.69145245137,4.75037189830571,132.085757505046));
#101124=CARTESIAN_POINT('Ctrl Pts',(-108.699198784635,4.78428409126352,
131.952675361389));
#101125=CARTESIAN_POINT('Ctrl Pts',(-108.706945117901,4.81256865356381,
131.818444449029));
#101126=CARTESIAN_POINT('Ctrl Pts',(-108.714693185903,4.84085954999569,
131.684183476588));
#101127=CARTESIAN_POINT('Ctrl Pts',(-108.722441253906,4.86352022738405,
131.54877360602));
#101128=CARTESIAN_POINT('Ctrl Pts',(-108.730189321909,4.88047897366933,
131.412725680724));
#101129=CARTESIAN_POINT('Ctrl Pts',(-108.737945624651,4.897455743912,131.276533162074));
#101130=CARTESIAN_POINT('Ctrl Pts',(-108.745701927393,4.90871842895081,
131.139701622636));
#101131=CARTESIAN_POINT('Ctrl Pts',(-108.753458230135,4.91424723775195,
131.002746979868));
#101132=CARTESIAN_POINT('Ctrl Pts',(-108.761218672649,4.91977899744482,
130.865719240283));
#101133=CARTESIAN_POINT('Ctrl Pts',(-108.768979115163,4.91957078350195,
130.728568657222));
#101134=CARTESIAN_POINT('Ctrl Pts',(-108.776739557678,4.91365496373026,
130.591809541565));
#101135=CARTESIAN_POINT('Ctrl Pts',(-108.784512457943,4.90772964735949,
130.454830888035));
#101136=CARTESIAN_POINT('Ctrl Pts',(-108.792285358208,4.89607844910299,
130.318245347465));
#101137=CARTESIAN_POINT('Ctrl Pts',(-108.800058258474,4.87878558781025,
130.1825614131));
#101138=CARTESIAN_POINT('Ctrl Pts',(-108.807548594236,4.86212136558354,
130.051809931516));
#101139=CARTESIAN_POINT('Ctrl Pts',(-108.815038929998,4.84021858757171,
129.921895946623));
#101140=CARTESIAN_POINT('Ctrl Pts',(-108.82252926576,4.81319676919358,129.793262242765));
#101141=CARTESIAN_POINT('Ctrl Pts',(-108.830303599879,4.78515041035858,
129.659751352929));
#101142=CARTESIAN_POINT('Ctrl Pts',(-108.838077933998,4.7515003291591,129.527196821932));
#101143=CARTESIAN_POINT('Ctrl Pts',(-108.845852268117,4.7123243475531,129.396105560427));
#101144=CARTESIAN_POINT('Ctrl Pts',(-108.853617021064,4.67319664684327,
129.265175857186));
#101145=CARTESIAN_POINT('Ctrl Pts',(-108.861381774011,4.62855670682352,
129.135706206309));
#101146=CARTESIAN_POINT('Ctrl Pts',(-108.869146526959,4.57853347453332,
129.008194064855));
#101147=CARTESIAN_POINT('Ctrl Pts',(-108.876903567844,4.5285599260225,128.880808570257));
#101148=CARTESIAN_POINT('Ctrl Pts',(-108.884660608729,4.47321386739668,
128.755377077588));
#101149=CARTESIAN_POINT('Ctrl Pts',(-108.892417649614,4.41267413403358,
128.63238224536));
#101150=CARTESIAN_POINT('Ctrl Pts',(-108.900168840854,4.35218005415442,
128.509480164492));
#101151=CARTESIAN_POINT('Ctrl Pts',(-108.907920032094,4.28650026723182,
128.389011435979));
#101152=CARTESIAN_POINT('Ctrl Pts',(-108.915671223334,4.21586169301357,
128.27143873802));
#101153=CARTESIAN_POINT('Ctrl Pts',(-108.923419120111,4.14525314207361,
128.153916011595));
#101154=CARTESIAN_POINT('Ctrl Pts',(-108.931167016888,4.06969019665465,
128.039287202006));
#101155=CARTESIAN_POINT('Ctrl Pts',(-108.938914913665,3.98944558651591,
127.927990165985));
#101156=CARTESIAN_POINT('Ctrl Pts',(-108.946661189749,3.90921776181995,
127.816716410905));
#101157=CARTESIAN_POINT('Ctrl Pts',(-108.954407465834,3.82431044879798,
127.708773360081));
#101158=CARTESIAN_POINT('Ctrl Pts',(-108.962153741918,3.73503932278767,
127.604569324414));
#101159=CARTESIAN_POINT('Ctrl Pts',(-108.969900075183,3.64576753779807,
127.500364519537));
#101160=CARTESIAN_POINT('Ctrl Pts',(-108.977646408448,3.55213212990225,
127.3998990818));
#101161=CARTESIAN_POINT('Ctrl Pts',(-108.985392741714,3.4544883585294,127.303547391573));
#101162=CARTESIAN_POINT('Ctrl Pts',(-108.993140809717,3.35682272051084,
127.207174124054));
#101163=CARTESIAN_POINT('Ctrl Pts',(-109.00088887772,3.25514721104121,127.114916711772));
#101164=CARTESIAN_POINT('Ctrl Pts',(-109.008636945723,3.14985285501965,
127.027111611447));
#101165=CARTESIAN_POINT('Ctrl Pts',(-109.016393248464,3.04444659090363,
126.939213190818));
#101166=CARTESIAN_POINT('Ctrl Pts',(-109.024149551206,2.93541409787311,
126.855776785556));
#101167=CARTESIAN_POINT('Ctrl Pts',(-109.031905853948,2.8231787343609,126.777097912409));
#101168=CARTESIAN_POINT('Ctrl Pts',(-109.039666296463,2.71088346745585,
126.698377045977));
#101169=CARTESIAN_POINT('Ctrl Pts',(-109.047426738977,2.59538225289803,
126.624418982031));
#101170=CARTESIAN_POINT('Ctrl Pts',(-109.055187181491,2.47712529058811,
126.55547448621));
#101171=CARTESIAN_POINT('Ctrl Pts',(-109.062960081756,2.35867849170394,
126.486419314564));
#101172=CARTESIAN_POINT('Ctrl Pts',(-109.070732982022,2.23746745086413,
126.422393976671));
#101173=CARTESIAN_POINT('Ctrl Pts',(-109.078505882287,2.11396550018371,
126.363602469847));
#101174=CARTESIAN_POINT('Ctrl Pts',(-109.085996218049,1.99495315649417,
126.306948182384));
#101175=CARTESIAN_POINT('Ctrl Pts',(-109.093486553811,1.87381385512986,
126.255153927685));
#101176=CARTESIAN_POINT('Ctrl Pts',(-109.100976889573,1.75098472410171,
126.208358489796));
#101177=CARTESIAN_POINT('Ctrl Pts',(-109.108751223692,1.62349848923628,
126.159788788657));
#101178=CARTESIAN_POINT('Ctrl Pts',(-109.116525557811,1.49378791733207,
126.116450593162));
#101179=CARTESIAN_POINT('Ctrl Pts',(-109.12429989193,1.36232155134577,126.078552427083));
#101180=CARTESIAN_POINT('Ctrl Pts',(-109.132064644877,1.23101720590641,
126.040700967107));
#101181=CARTESIAN_POINT('Ctrl Pts',(-109.139829397824,1.09796174388108,
126.008276304143));
#101182=CARTESIAN_POINT('Ctrl Pts',(-109.147594150771,0.963643389005652,
125.981438839087));
#101183=CARTESIAN_POINT('Ctrl Pts',(-109.155351191656,0.829458441013838,
125.95462802938));
#101184=CARTESIAN_POINT('Ctrl Pts',(-109.163108232541,0.694013477237669,
125.933393450362));
#101185=CARTESIAN_POINT('Ctrl Pts',(-109.170865273426,0.557811236841828,
125.917845531479));
#101186=CARTESIAN_POINT('Ctrl Pts',(-109.178616464667,0.421711707614783,
125.902309337404));
#101187=CARTESIAN_POINT('Ctrl Pts',(-109.186367655907,0.28485642531544,
125.892451311916));
#101188=CARTESIAN_POINT('Ctrl Pts',(-109.194118847147,0.147757309883138,
125.888330629875));
#101189=CARTESIAN_POINT('Ctrl Pts',(-109.201866743924,0.0107164652323208,
125.884211699234));
#101190=CARTESIAN_POINT('Ctrl Pts',(-109.209614640701,-0.126567616457595,
125.885825273722));
#101191=CARTESIAN_POINT('Ctrl Pts',(-109.217362537478,-0.263579136821274,
125.893178570326));
#101192=CARTESIAN_POINT('Ctrl Pts',(-109.225108813562,-0.40056199732852,
125.900530328779));
#101193=CARTESIAN_POINT('Ctrl Pts',(-109.232855089646,-0.537272019757397,
125.913619400299));
#101194=CARTESIAN_POINT('Ctrl Pts',(-109.24060136573,-0.673195050352685,
125.932400900298));
#101195=CARTESIAN_POINT('Ctrl Pts',(-109.248347698996,-0.809119084301092,
125.951182538938));
#101196=CARTESIAN_POINT('Ctrl Pts',(-109.256094032261,-0.944255727538221,
125.975656636392));
#101197=CARTESIAN_POINT('Ctrl Pts',(-109.263840365526,-1.07809797685594,
126.005726664575));
#101198=CARTESIAN_POINT('Ctrl Pts',(-109.271588433529,-1.21197019921721,
126.035803426732));
#101199=CARTESIAN_POINT('Ctrl Pts',(-109.279336501532,-1.34454706946666,
126.071478527598));
#101200=CARTESIAN_POINT('Ctrl Pts',(-109.287084569535,-1.47533415852613,
126.112604849926));
#101201=CARTESIAN_POINT('Ctrl Pts',(-109.294840872277,-1.60626024966006,
126.153774881798));
#101202=CARTESIAN_POINT('Ctrl Pts',(-109.302597175019,-1.73539238619786,
126.200407591054));
#101203=CARTESIAN_POINT('Ctrl Pts',(-109.310353477761,-1.86225310595762,
126.252306528273));
#101204=CARTESIAN_POINT('Ctrl Pts',(-109.318113920275,-1.98918153510355,
126.304233165517));
#101205=CARTESIAN_POINT('Ctrl Pts',(-109.325874362789,-2.11383577664564,
126.3614314684));
#101206=CARTESIAN_POINT('Ctrl Pts',(-109.333634805303,-2.23576151030469,
126.423658215948));
#101207=CARTESIAN_POINT('Ctrl Pts',(-109.341407705569,-2.35788296997546,
126.485984855396));
#101208=CARTESIAN_POINT('Ctrl Pts',(-109.349180605834,-2.47726682835527,
126.553355877892));
#101209=CARTESIAN_POINT('Ctrl Pts',(-109.3569535061,-2.59348560915369,126.625483321256));
#101210=CARTESIAN_POINT('Ctrl Pts',(-109.364443841862,-2.70547954453265,
126.694988750376));
#101211=CARTESIAN_POINT('Ctrl Pts',(-109.371934177624,-2.81453426928065,
126.768910615648));
#101212=CARTESIAN_POINT('Ctrl Pts',(-109.379424513386,-2.92029674208176,
126.846956165063));
#101213=CARTESIAN_POINT('Ctrl Pts',(-109.387353516481,-3.03225313507579,
126.929572408523));
#101214=CARTESIAN_POINT('Ctrl Pts',(-109.395282519577,-3.14090019779782,
127.017090611809));
#101215=CARTESIAN_POINT('Ctrl Pts',(-109.403211522672,-3.24577532853165,
127.109211692395));
#101216=CARTESIAN_POINT('Ctrl Pts',(-109.410902197704,-3.34749814786704,
127.198563819747));
#101217=CARTESIAN_POINT('Ctrl Pts',(-109.418592872736,-3.44567216479411,
127.292245841371));
#101218=CARTESIAN_POINT('Ctrl Pts',(-109.426283547768,-3.53990365071903,
127.38994043163));
#101219=CARTESIAN_POINT('Ctrl Pts',(-109.43396725077,-3.63404971049636,
127.487546456243));
#101220=CARTESIAN_POINT('Ctrl Pts',(-109.441650953772,-3.72426007157515,
127.589157530773));
#101221=CARTESIAN_POINT('Ctrl Pts',(-109.449334656774,-3.81017496384986,
127.694416919144));
#101222=CARTESIAN_POINT('Ctrl Pts',(-109.457013135598,-3.89603144227701,
127.799604741276));
#101223=CARTESIAN_POINT('Ctrl Pts',(-109.464691614422,-3.97759800978754,
127.908435635457));
#101224=CARTESIAN_POINT('Ctrl Pts',(-109.472370093246,-4.05455294464068,
128.020517324274));
#101225=CARTESIAN_POINT('Ctrl Pts',(-109.480045091343,-4.1314729950906,
128.132548205396));
#101226=CARTESIAN_POINT('Ctrl Pts',(-109.48772008944,-4.20378534745559,
128.247826620486));
#101227=CARTESIAN_POINT('Ctrl Pts',(-109.495395087537,-4.27120996446139,
128.365929051582));
#101228=CARTESIAN_POINT('Ctrl Pts',(-109.503069587789,-4.33863020791451,
128.484023821868));
#101229=CARTESIAN_POINT('Ctrl Pts',(-109.510744088041,-4.40116314251367,
128.604941901142));
#101230=CARTESIAN_POINT('Ctrl Pts',(-109.518418588293,-4.45857344127018,
128.72823298871));
#101231=CARTESIAN_POINT('Ctrl Pts',(-109.526092904013,-4.51598235960552,
128.851521111764));
#101232=CARTESIAN_POINT('Ctrl Pts',(-109.533767219733,-4.56826872447677,
128.977181765286));
#101233=CARTESIAN_POINT('Ctrl Pts',(-109.541441535452,-4.6152446707871,
129.104743104338));
#101234=CARTESIAN_POINT('Ctrl Pts',(-109.549119155242,-4.66224084193589,
129.232359363146));
#101235=CARTESIAN_POINT('Ctrl Pts',(-109.556796775031,-4.70392189957251,
129.36187756421));
#101236=CARTESIAN_POINT('Ctrl Pts',(-109.564474394821,-4.7401493703113,
129.492809242424));
#101237=CARTESIAN_POINT('Ctrl Pts',(-109.566223125773,-4.74840089892985,
129.522631542127));
#101238=CARTESIAN_POINT('Ctrl Pts',(-109.567971856726,-4.75636970745135,
129.55252711971));
#101239=CARTESIAN_POINT('Ctrl Pts',(-109.569720587678,-4.76405452823413,
129.582490119309));
#101240=CARTESIAN_POINT('Origin',(213.235140564004,0.,130.804360617566));
#101241=CARTESIAN_POINT('',(-111.665402883959,-4.76405452823393,129.582490119308));
#101242=CARTESIAN_POINT('',(-111.319883193423,-4.764054528234,129.582490119308));
#101243=CARTESIAN_POINT('',(213.235140564004,-4.76405452823405,129.582490119308));
#101244=CARTESIAN_POINT('',(-109.985140563973,-4.91824789704149,130.799812458929));
#101245=CARTESIAN_POINT('Ctrl Pts',(-109.98514056401,-4.91824789704208,
130.799812459574));
#101246=CARTESIAN_POINT('Ctrl Pts',(-109.992803365887,-4.91837304686826,
130.935145900162));
#101247=CARTESIAN_POINT('Ctrl Pts',(-110.000466167764,-4.9129081225041,
131.070627357));
#101248=CARTESIAN_POINT('Ctrl Pts',(-110.008128969641,-4.90184331819967,
131.205752130084));
#101249=CARTESIAN_POINT('Ctrl Pts',(-110.015922695434,-4.89058946457277,
131.343185597122));
#101250=CARTESIAN_POINT('Ctrl Pts',(-110.023716421227,-4.87354257725691,
131.480249661262));
#101251=CARTESIAN_POINT('Ctrl Pts',(-110.031510147019,-4.85074769783324,
131.616413469581));
#101252=CARTESIAN_POINT('Ctrl Pts',(-110.039165636601,-4.82835712795713,
131.750162159719));
#101253=CARTESIAN_POINT('Ctrl Pts',(-110.046821126184,-4.80042086055033,
131.883041855564));
#101254=CARTESIAN_POINT('Ctrl Pts',(-110.054476615766,-4.76703376610004,
132.014555699097));
#101255=CARTESIAN_POINT('Ctrl Pts',(-110.062131371041,-4.73364987410669,
132.146056927953));
#101256=CARTESIAN_POINT('Ctrl Pts',(-110.069786126316,-4.69481629336717,
132.276192176238));
#101257=CARTESIAN_POINT('Ctrl Pts',(-110.077440881592,-4.65067855629213,
132.404476872263));
#101258=CARTESIAN_POINT('Ctrl Pts',(-110.085096654511,-4.60653495142652,
132.532778622803));
#101259=CARTESIAN_POINT('Ctrl Pts',(-110.09275242743,-4.55708591869811,
132.659228952612));
#101260=CARTESIAN_POINT('Ctrl Pts',(-110.100408200349,-4.50252601811771,
132.783361001263));
#101261=CARTESIAN_POINT('Ctrl Pts',(-110.108305716042,-4.44624330498246,
132.911412709767));
#101262=CARTESIAN_POINT('Ctrl Pts',(-110.116203231735,-4.38452180407454,
133.036996889814));
#101263=CARTESIAN_POINT('Ctrl Pts',(-110.124100747428,-4.3176269459999,
133.159627187973));
#101264=CARTESIAN_POINT('Ctrl Pts',(-110.131767916235,-4.25268321063482,
133.278680727521));
#101265=CARTESIAN_POINT('Ctrl Pts',(-110.139435085042,-4.1828639623609,
133.39494998521));
#101266=CARTESIAN_POINT('Ctrl Pts',(-110.14710225385,-4.10845633554988,
133.508019176145));
#101267=CARTESIAN_POINT('Ctrl Pts',(-110.155114942985,-4.03069553518883,
133.626183820822));
#101268=CARTESIAN_POINT('Ctrl Pts',(-110.163127632121,-3.94792346969235,
133.740852849937));
#101269=CARTESIAN_POINT('Ctrl Pts',(-110.171140321257,-3.86051427395563,
133.851590934277));
#101270=CARTESIAN_POINT('Ctrl Pts',(-110.179153010393,-3.77310507821891,
133.962329018618));
#101271=CARTESIAN_POINT('Ctrl Pts',(-110.187165699528,-3.68105913125749,
134.069135836365));
#101272=CARTESIAN_POINT('Ctrl Pts',(-110.195178388664,-3.58479269293473,
134.171621286297));
#101273=CARTESIAN_POINT('Ctrl Pts',(-110.202952722783,-3.49138991100893,
134.271058081689));
#101274=CARTESIAN_POINT('Ctrl Pts',(-110.210727056902,-3.39369870799688,
134.366763152123));
#101275=CARTESIAN_POINT('Ctrl Pts',(-110.218501391022,-3.29204923267864,
134.458344048306));
#101276=CARTESIAN_POINT('Ctrl Pts',(-110.226266143969,-3.19052503125433,
134.549812079218));
#101277=CARTESIAN_POINT('Ctrl Pts',(-110.234030896916,-3.08505255139815,
134.637165789708));
#101278=CARTESIAN_POINT('Ctrl Pts',(-110.241795649863,-2.97600068806793,
134.720047398594));
#101279=CARTESIAN_POINT('Ctrl Pts',(-110.249552690748,-2.86705713658573,
134.802846688298));
#101280=CARTESIAN_POINT('Ctrl Pts',(-110.257309731633,-2.75454158568171,
134.88118248065));
#101281=CARTESIAN_POINT('Ctrl Pts',(-110.265066772518,-2.63885783990856,
134.954735584151));
#101282=CARTESIAN_POINT('Ctrl Pts',(-110.272817963758,-2.52326133214814,
135.028233220684));
#101283=CARTESIAN_POINT('Ctrl Pts',(-110.280569154999,-2.40450171358722,
135.096955138288));
#101284=CARTESIAN_POINT('Ctrl Pts',(-110.288320346239,-2.28301346223526,
135.16062422228));
#101285=CARTESIAN_POINT('Ctrl Pts',(-110.296068243016,-2.16157684663075,
135.224266245213));
#101286=CARTESIAN_POINT('Ctrl Pts',(-110.303816139793,-2.03741425043942,
135.282859524822));
#101287=CARTESIAN_POINT('Ctrl Pts',(-110.31156403657,-1.9109863644262,135.336171974791));
#101288=CARTESIAN_POINT('Ctrl Pts',(-110.319310312654,-1.78458492440091,
135.389473272946));
#101289=CARTESIAN_POINT('Ctrl Pts',(-110.327056588738,-1.65591949708484,
135.437495786829));
#101290=CARTESIAN_POINT('Ctrl Pts',(-110.334802864823,-1.52547208209369,
135.48005500335));
#101291=CARTESIAN_POINT('Ctrl Pts',(-110.342549198088,-1.39502370416953,
135.522614534033));
#101292=CARTESIAN_POINT('Ctrl Pts',(-110.350295531353,-1.26279368400579,
135.559710565617));
#101293=CARTESIAN_POINT('Ctrl Pts',(-110.358041864619,-1.129280178338,135.591208154444));
#101294=CARTESIAN_POINT('Ctrl Pts',(-110.365789932622,-0.995736773246146,
135.622712796937));
#101295=CARTESIAN_POINT('Ctrl Pts',(-110.373538000625,-0.860909691149279,
135.648616412137));
#101296=CARTESIAN_POINT('Ctrl Pts',(-110.381286068628,-0.725307907443927,
135.668835049804));
#101297=CARTESIAN_POINT('Ctrl Pts',(-110.38904237137,-0.589562004549358,
135.68907517608));
#101298=CARTESIAN_POINT('Ctrl Pts',(-110.396798674112,-0.453040142598879,
135.703618197404));
#101299=CARTESIAN_POINT('Ctrl Pts',(-110.404554976854,-0.316257615550054,
135.712431947845));
#101300=CARTESIAN_POINT('Ctrl Pts',(-110.412315419368,-0.179402083547729,
135.72125040245));
#101301=CARTESIAN_POINT('Ctrl Pts',(-110.420075861882,-0.0422859999042523,
135.724333484295));
#101302=CARTESIAN_POINT('Ctrl Pts',(-110.427836304396,0.0945756958698464,
135.721701209822));
#101303=CARTESIAN_POINT('Ctrl Pts',(-110.435609204662,0.231657094187638,
135.719064709789));
#101304=CARTESIAN_POINT('Ctrl Pts',(-110.443382104927,0.368482898130376,
135.710694543155));
#101305=CARTESIAN_POINT('Ctrl Pts',(-110.451155005193,0.504542739864685,
135.696662702081));
#101306=CARTESIAN_POINT('Ctrl Pts',(-110.458645340954,0.635656463627944,
135.683140953775));
#101307=CARTESIAN_POINT('Ctrl Pts',(-110.466135676716,0.766058642772488,
135.664362060649));
#101308=CARTESIAN_POINT('Ctrl Pts',(-110.473626012477,0.895303752426226,
135.640434878099));
#101309=CARTESIAN_POINT('Ctrl Pts',(-110.481400346597,1.02944922970568,
135.615600489149));
#101310=CARTESIAN_POINT('Ctrl Pts',(-110.489174680716,1.16277309743821,
135.585141041592));
#101311=CARTESIAN_POINT('Ctrl Pts',(-110.496949014835,1.29476672343772,
135.549122170519));
#101312=CARTESIAN_POINT('Ctrl Pts',(-110.504713767782,1.4265976790898,135.513147689485));
#101313=CARTESIAN_POINT('Ctrl Pts',(-110.512478520729,1.55710128138099,
135.471627519299));
#101314=CARTESIAN_POINT('Ctrl Pts',(-110.520243273676,1.6857771221356,135.424678632268));
#101315=CARTESIAN_POINT('Ctrl Pts',(-110.528000314561,1.81432516023115,
135.377776375535));
#101316=CARTESIAN_POINT('Ctrl Pts',(-110.535757355446,1.9410486845304,135.325456265178));
#101317=CARTESIAN_POINT('Ctrl Pts',(-110.543514396331,2.06546088396031,
135.267885502601));
#101318=CARTESIAN_POINT('Ctrl Pts',(-110.551265587571,2.18977926318301,
135.210358154585));
#101319=CARTESIAN_POINT('Ctrl Pts',(-110.559016778812,2.31178943346622,
135.147588199133));
#101320=CARTESIAN_POINT('Ctrl Pts',(-110.566767970052,2.43102340440222,
135.079791387646));
#101321=CARTESIAN_POINT('Ctrl Pts',(-110.574515866829,2.55020669771975,
135.012023391613));
#101322=CARTESIAN_POINT('Ctrl Pts',(-110.582263763606,2.66661579938392,
134.939232981819));
#101323=CARTESIAN_POINT('Ctrl Pts',(-110.590011660383,2.77980643399327,
134.86168230213));
#101324=CARTESIAN_POINT('Ctrl Pts',(-110.597757936467,2.89297339156197,
134.784147844371));
#101325=CARTESIAN_POINT('Ctrl Pts',(-110.605504212551,3.00292289885171,
134.701855318145));
#101326=CARTESIAN_POINT('Ctrl Pts',(-110.613250488636,3.10923918720794,
134.615110509547));
#101327=CARTESIAN_POINT('Ctrl Pts',(-110.620996821901,3.215556260367,134.528365060618));
#101328=CARTESIAN_POINT('Ctrl Pts',(-110.628743155166,3.31823975814899,
134.437167510897));
#101329=CARTESIAN_POINT('Ctrl Pts',(-110.636489488432,3.41690688274867,
134.341864033412));
#101330=CARTESIAN_POINT('Ctrl Pts',(-110.644237556435,3.51559610316639,
134.246539213375));
#101331=CARTESIAN_POINT('Ctrl Pts',(-110.651985624438,3.61026687947045,
134.147106907453));
#101332=CARTESIAN_POINT('Ctrl Pts',(-110.659733692441,3.70057346831104,
134.043949953907));
#101333=CARTESIAN_POINT('Ctrl Pts',(-110.667489995183,3.79097603606927,
133.940683363922));
#101334=CARTESIAN_POINT('Ctrl Pts',(-110.675246297925,3.87700489290491,
133.833684513222));
#101335=CARTESIAN_POINT('Ctrl Pts',(-110.683002600667,3.95835444773843,
133.723369546735));
#101336=CARTESIAN_POINT('Ctrl Pts',(-110.690763043181,4.03974742127875,
133.612995701829));
#101337=CARTESIAN_POINT('Ctrl Pts',(-110.698523485695,4.11645589780784,
133.499302538377));
#101338=CARTESIAN_POINT('Ctrl Pts',(-110.706283928209,4.18821838034238,
133.382734108948));
#101339=CARTESIAN_POINT('Ctrl Pts',(-110.714056828475,4.26009606238465,
133.265978553528));
#101340=CARTESIAN_POINT('Ctrl Pts',(-110.72182972874,4.32701169332723,133.146338850045));
#101341=CARTESIAN_POINT('Ctrl Pts',(-110.729602629005,4.38874997593343,
133.024283298932));
#101342=CARTESIAN_POINT('Ctrl Pts',(-110.737092964767,4.44824391645371,
132.906664774549));
#101343=CARTESIAN_POINT('Ctrl Pts',(-110.744583300529,4.50293026489899,
132.786803277617));
#101344=CARTESIAN_POINT('Ctrl Pts',(-110.75207363629,4.55265978732259,132.665132479831));
#101345=CARTESIAN_POINT('Ctrl Pts',(-110.759847970409,4.60427481970683,
132.538848496758));
#101346=CARTESIAN_POINT('Ctrl Pts',(-110.767622304528,4.65071323094684,
132.410215275489));
#101347=CARTESIAN_POINT('Ctrl Pts',(-110.775396638647,4.69175531358146,
132.279696220058));
#101348=CARTESIAN_POINT('Ctrl Pts',(-110.783161391595,4.73274681551716,
132.149338017698));
#101349=CARTESIAN_POINT('Ctrl Pts',(-110.790926144542,4.76835510519319,
132.017098974865));
#101350=CARTESIAN_POINT('Ctrl Pts',(-110.798690897489,4.79840811188311,
131.88346332552));
#101351=CARTESIAN_POINT('Ctrl Pts',(-110.806447938374,4.82843126950303,
131.749960404987));
#101352=CARTESIAN_POINT('Ctrl Pts',(-110.814204979259,4.85291003915501,
131.615064017361));
#101353=CARTESIAN_POINT('Ctrl Pts',(-110.821962020144,4.87172195883974,
131.479274107029));
#101354=CARTESIAN_POINT('Ctrl Pts',(-110.829713211384,4.89051969230952,
131.343586596924));
#101355=CARTESIAN_POINT('Ctrl Pts',(-110.837464402624,4.90365902835306,
131.207007290996));
#101356=CARTESIAN_POINT('Ctrl Pts',(-110.845215593864,4.91106852448644,
131.070046541729));
#101357=CARTESIAN_POINT('Ctrl Pts',(-110.852963490641,4.91847487138633,
130.933144004435));
#101358=CARTESIAN_POINT('Ctrl Pts',(-110.860711387418,4.92015620099542,
130.79586073583));
#101359=CARTESIAN_POINT('Ctrl Pts',(-110.868459284195,4.91609292066558,
130.658712212557));
#101360=CARTESIAN_POINT('Ctrl Pts',(-110.876205560279,4.91203049028638,
130.521592377797));
#101361=CARTESIAN_POINT('Ctrl Pts',(-110.883951836363,4.90222585168377,
130.384607622852));
#101362=CARTESIAN_POINT('Ctrl Pts',(-110.891698112447,4.88671153824642,
130.248273030518));
#101363=CARTESIAN_POINT('Ctrl Pts',(-110.899444445713,4.87119711028592,
130.111937431792));
#101364=CARTESIAN_POINT('Ctrl Pts',(-110.907190778978,4.84997296759328,
129.976252393714));
#101365=CARTESIAN_POINT('Ctrl Pts',(-110.914937112243,4.82312344377584,
129.841727089893));
#101366=CARTESIAN_POINT('Ctrl Pts',(-110.922685180246,4.79626790719366,
129.707171660063));
#101367=CARTESIAN_POINT('Ctrl Pts',(-110.930433248249,4.76378455920772,
129.573776864623));
#101368=CARTESIAN_POINT('Ctrl Pts',(-110.938181316252,4.72580860976288,
129.442040520676));
#101369=CARTESIAN_POINT('Ctrl Pts',(-110.945937618994,4.6877922990271,129.310164165775));
#101370=CARTESIAN_POINT('Ctrl Pts',(-110.953693921736,4.64427183406049,
129.17995015966));
#101371=CARTESIAN_POINT('Ctrl Pts',(-110.961450224478,4.59543214993469,
129.051880541261));
#101372=CARTESIAN_POINT('Ctrl Pts',(-110.969210666992,4.54656639859894,
128.92374256825));
#101373=CARTESIAN_POINT('Ctrl Pts',(-110.976971109506,4.49237592550257,
128.797751622494));
#101374=CARTESIAN_POINT('Ctrl Pts',(-110.98473155202,4.43309297914226,128.674367730071));
#101375=CARTESIAN_POINT('Ctrl Pts',(-110.992504452286,4.37371486653356,
128.55078577087));
#101376=CARTESIAN_POINT('Ctrl Pts',(-111.000277352551,4.30922812865151,
128.429819573315));
#101377=CARTESIAN_POINT('Ctrl Pts',(-111.008050252817,4.23991038649881,
128.31190340089));
#101378=CARTESIAN_POINT('Ctrl Pts',(-111.015540588579,4.17311251887195,
128.198273778342));
#101379=CARTESIAN_POINT('Ctrl Pts',(-111.023030924341,4.10182895396599,
128.087476537716));
#101380=CARTESIAN_POINT('Ctrl Pts',(-111.030521260103,4.02634388746626,
127.9798716439));
#101381=CARTESIAN_POINT('Ctrl Pts',(-111.038295594222,3.94799678172954,
127.868186877832));
#101382=CARTESIAN_POINT('Ctrl Pts',(-111.046069928341,3.86487510519078,
127.759587529115));
#101383=CARTESIAN_POINT('Ctrl Pts',(-111.053844262461,3.77724997553727,
127.654508925057));
#101384=CARTESIAN_POINT('Ctrl Pts',(-111.061609015408,3.68973283602453,
127.549559820986));
#101385=CARTESIAN_POINT('Ctrl Pts',(-111.069373768355,3.59772353443533,
127.448123125633));
#101386=CARTESIAN_POINT('Ctrl Pts',(-111.077138521302,3.50153646208397,
127.350605347256));
#101387=CARTESIAN_POINT('Ctrl Pts',(-111.084895562187,3.40544492408886,
127.253184424911));
#101388=CARTESIAN_POINT('Ctrl Pts',(-111.092652603072,3.30518414563818,
127.159674950188));
#101389=CARTESIAN_POINT('Ctrl Pts',(-111.100409643957,3.20110855040108,
127.070450185988));
#101390=CARTESIAN_POINT('Ctrl Pts',(-111.108160835197,3.09711143938065,
126.981292706877));
#101391=CARTESIAN_POINT('Ctrl Pts',(-111.115912026437,2.98930553325379,
126.896413760349));
#101392=CARTESIAN_POINT('Ctrl Pts',(-111.123663217677,2.87808158961293,
126.816149310974));
#101393=CARTESIAN_POINT('Ctrl Pts',(-111.131411114454,2.76690491911467,
126.73591897613));
#101394=CARTESIAN_POINT('Ctrl Pts',(-111.139159011231,2.65231341689568,
126.660299465901));
#101395=CARTESIAN_POINT('Ctrl Pts',(-111.146906908009,2.53473017774764,
126.589585891852));
#101396=CARTESIAN_POINT('Ctrl Pts',(-111.154653184093,2.41717153447844,
126.518887109559));
#101397=CARTESIAN_POINT('Ctrl Pts',(-111.162399460177,2.2966227338761,126.45309242361));
#101398=CARTESIAN_POINT('Ctrl Pts',(-111.170145736261,2.17353471477774,
126.392452877579));
#101399=CARTESIAN_POINT('Ctrl Pts',(-111.177892069526,2.05044578707142,
126.331812883921));
#101400=CARTESIAN_POINT('Ctrl Pts',(-111.185638402792,1.92481795418158,
126.276328278894));
#101401=CARTESIAN_POINT('Ctrl Pts',(-111.193384736057,1.7971251826629,126.226203331022));
#101402=CARTESIAN_POINT('Ctrl Pts',(-111.20113280406,1.66940381523358,126.176067158015));
#101403=CARTESIAN_POINT('Ctrl Pts',(-111.208880872063,1.53961695285653,
126.131293173367));
#101404=CARTESIAN_POINT('Ctrl Pts',(-111.216628940066,1.40825650743737,
126.092036703428));
#101405=CARTESIAN_POINT('Ctrl Pts',(-111.224385242808,1.27675645057343,
126.052738511244));
#101406=CARTESIAN_POINT('Ctrl Pts',(-111.23214154555,1.1436798450156,126.018969660026));
#101407=CARTESIAN_POINT('Ctrl Pts',(-111.239897848291,1.00953220569041,
125.990835112474));
#101408=CARTESIAN_POINT('Ctrl Pts',(-111.247658290806,0.875312967731013,
125.962685548667));
#101409=CARTESIAN_POINT('Ctrl Pts',(-111.25541873332,0.740021942432409,
125.940176344755));
#101410=CARTESIAN_POINT('Ctrl Pts',(-111.263179175834,0.604171698748815,
125.923360758835));
#101411=CARTESIAN_POINT('Ctrl Pts',(-111.270952076099,0.468103376193841,
125.906518179043));
#101412=CARTESIAN_POINT('Ctrl Pts',(-111.278724976365,0.331474431247777,
125.895387513441));
#101413=CARTESIAN_POINT('Ctrl Pts',(-111.28649787663,0.194800283013736,
125.889969921637));
#101414=CARTESIAN_POINT('Ctrl Pts',(-111.293988212392,0.0630945843290355,
125.884749272941));
#101415=CARTESIAN_POINT('Ctrl Pts',(-111.301478548154,-0.0686527801770063,
125.88483354002));
#101416=CARTESIAN_POINT('Ctrl Pts',(-111.308968883916,-0.199985347138127,
125.890178190811));
#101417=CARTESIAN_POINT('Ctrl Pts',(-111.316743218035,-0.336297428291199,
125.895725485661));
#101418=CARTESIAN_POINT('Ctrl Pts',(-111.324517552154,-0.472594432587768,
125.906957505593));
#101419=CARTESIAN_POINT('Ctrl Pts',(-111.332291886273,-0.608363561101947,
125.923881456661));
#101420=CARTESIAN_POINT('Ctrl Pts',(-111.34005663922,-0.743965366299635,
125.940784550473));
#101421=CARTESIAN_POINT('Ctrl Pts',(-111.347821392167,-0.879040205896588,
125.963365570171));
#101422=CARTESIAN_POINT('Ctrl Pts',(-111.355586145114,-1.01307613679673,
125.991579737082));
#101423=CARTESIAN_POINT('Ctrl Pts',(-111.363343185999,-1.14697894132072,
126.019765881285));
#101424=CARTESIAN_POINT('Ctrl Pts',(-111.371100226884,-1.27984451048792,
126.053573958544));
#101425=CARTESIAN_POINT('Ctrl Pts',(-111.378857267769,-1.41116723299806,
126.092907539904));
#101426=CARTESIAN_POINT('Ctrl Pts',(-111.386608459009,-1.5423909240218,
126.132211459504));
#101427=CARTESIAN_POINT('Ctrl Pts',(-111.394359650249,-1.67207371119932,
126.177032477668));
#101428=CARTESIAN_POINT('Ctrl Pts',(-111.402110841489,-1.79972172399976,
126.227223436023));
#101429=CARTESIAN_POINT('Ctrl Pts',(-111.409858738266,-1.92731548298946,
126.277393061881));
#101430=CARTESIAN_POINT('Ctrl Pts',(-111.417606635044,-2.05287582460229,
126.332927945709));
#101431=CARTESIAN_POINT('Ctrl Pts',(-111.425354531821,-2.17592577005096,
126.393631640886));
#101432=CARTESIAN_POINT('Ctrl Pts',(-111.433100807905,-2.2989499761037,
126.454322638157));
#101433=CARTESIAN_POINT('Ctrl Pts',(-111.440847083989,-2.41946448008742,
126.520180123343));
#101434=CARTESIAN_POINT('Ctrl Pts',(-111.448593360073,-2.53701432847838,
126.59096040401));
#101435=CARTESIAN_POINT('Ctrl Pts',(-111.456339693338,-2.65456504459546,
126.661741207161));
#101436=CARTESIAN_POINT('Ctrl Pts',(-111.464086026603,-2.76915072651625,
126.737444676631));
#101437=CARTESIAN_POINT('Ctrl Pts',(-111.471832359868,-2.88034332684791,
126.81778246306));
#101438=CARTESIAN_POINT('Ctrl Pts',(-111.479580427871,-2.99156082799161,
126.89813824058));
#101439=CARTESIAN_POINT('Ctrl Pts',(-111.487328495874,-3.09938341867515,
126.983130171284));
#101440=CARTESIAN_POINT('Ctrl Pts',(-111.495076563877,-3.20341452804219,
127.07242835344));
#101441=CARTESIAN_POINT('Ctrl Pts',(-111.502832866619,-3.30755620291067,
127.161821442766));
#101442=CARTESIAN_POINT('Ctrl Pts',(-111.510589169361,-3.40789804970514,
127.255529671012));
#101443=CARTESIAN_POINT('Ctrl Pts',(-111.518345472102,-3.50407851716587,
127.353184469057));
#101444=CARTESIAN_POINT('Ctrl Pts',(-111.526105914617,-3.60031031903777,
127.450891388408));
#101445=CARTESIAN_POINT('Ctrl Pts',(-111.533866357131,-3.69237605362251,
127.552548785099));
#101446=CARTESIAN_POINT('Ctrl Pts',(-111.541626799645,-3.77995385733691,
127.657754207653));
#101447=CARTESIAN_POINT('Ctrl Pts',(-111.54939969991,-3.86767224871661,
127.763128515292));
#101448=CARTESIAN_POINT('Ctrl Pts',(-111.557172600175,-3.95088807501574,
127.872061919566));
#101449=CARTESIAN_POINT('Ctrl Pts',(-111.564945500441,-4.02932176400691,
127.984121410584));
#101450=CARTESIAN_POINT('Ctrl Pts',(-111.572435836203,-4.10490419084857,
128.092107256854));
#101451=CARTESIAN_POINT('Ctrl Pts',(-111.579926171966,-4.17604596319895,
128.202995594316));
#101452=CARTESIAN_POINT('Ctrl Pts',(-111.587416507729,-4.24253781754489,
128.316378316744));
#101453=CARTESIAN_POINT('Ctrl Pts',(-111.595487622467,-4.31418525800406,
128.438552407604));
#101454=CARTESIAN_POINT('Ctrl Pts',(-111.603558737205,-4.38064618870131,
128.563984957254));
#101455=CARTESIAN_POINT('Ctrl Pts',(-111.611629851943,-4.44162376095062,
128.692214451066));
#101456=CARTESIAN_POINT('Ctrl Pts',(-111.61968972964,-4.50251643693333,
128.820265416858));
#101457=CARTESIAN_POINT('Ctrl Pts',(-111.627749607336,-4.55794080676336,
128.951105260088));
#101458=CARTESIAN_POINT('Ctrl Pts',(-111.635809485033,-4.60764439350489,
129.084245445404));
#101459=CARTESIAN_POINT('Ctrl Pts',(-111.643856063879,-4.65726596900233,
129.217165948541));
#101460=CARTESIAN_POINT('Ctrl Pts',(-111.651902642724,-4.70118545278094,
129.35237890351));
#101461=CARTESIAN_POINT('Ctrl Pts',(-111.65994922157,-4.73919745996105,
129.489373736263));
#101462=CARTESIAN_POINT('Ctrl Pts',(-111.661767109033,-4.74778515326904,
129.520323683286));
#101463=CARTESIAN_POINT('Ctrl Pts',(-111.663584996496,-4.756071519496,129.551364489398));
#101464=CARTESIAN_POINT('Ctrl Pts',(-111.665402883959,-4.76405452823392,
129.582490119308));
#101465=CARTESIAN_POINT('Ctrl Pts',(-109.915204178194,-4.76405452823412,
129.582490119309));
#101466=CARTESIAN_POINT('Ctrl Pts',(-109.915713040413,-4.76627341212307,
129.591141513915));
#101467=CARTESIAN_POINT('Ctrl Pts',(-109.916221902632,-4.76846850299481,
129.599798068042));
#101468=CARTESIAN_POINT('Ctrl Pts',(-109.916730764851,-4.77063978033951,
129.60845963975));
#101469=CARTESIAN_POINT('Ctrl Pts',(-109.927005307824,-4.81448049310873,
129.783347236812));
#101470=CARTESIAN_POINT('Ctrl Pts',(-109.937279850797,-4.84872130166821,
129.960730603675));
#101471=CARTESIAN_POINT('Ctrl Pts',(-109.94755439377,-4.87313170538994,
130.139702476547));
#101472=CARTESIAN_POINT('Ctrl Pts',(-109.957592050043,-4.89697931035751,
130.314548029009));
#101473=CARTESIAN_POINT('Ctrl Pts',(-109.967629706315,-4.91144463375593,
130.490909983889));
#101474=CARTESIAN_POINT('Ctrl Pts',(-109.977667362588,-4.91635708443026,
130.667919857995));
#101475=CARTESIAN_POINT('Ctrl Pts',(-109.980158429716,-4.91757621806691,
130.711848785906));
#101476=CARTESIAN_POINT('Ctrl Pts',(-109.982649496845,-4.91820721261987,
130.755817495907));
#101477=CARTESIAN_POINT('Ctrl Pts',(-109.985140563974,-4.91824789704149,
130.799812458929));
#101478=CARTESIAN_POINT('',(-109.639859435959,-4.91824962741785,130.806275011501));
#101479=CARTESIAN_POINT('Ctrl Pts',(-109.569720587678,-4.76405452823413,
129.582490119309));
#101480=CARTESIAN_POINT('Ctrl Pts',(-109.577406436354,-4.79783008961758,
129.714180520527));
#101481=CARTESIAN_POINT('Ctrl Pts',(-109.585092285029,-4.8261157894635,
129.847173809154));
#101482=CARTESIAN_POINT('Ctrl Pts',(-109.592778133704,-4.84883573668985,
129.980968207412));
#101483=CARTESIAN_POINT('Ctrl Pts',(-109.600625017413,-4.87203171559869,
130.117565885619));
#101484=CARTESIAN_POINT('Ctrl Pts',(-109.608471901122,-4.88942606939395,
130.254998176776));
#101485=CARTESIAN_POINT('Ctrl Pts',(-109.616318784832,-4.90099394425744,
130.392727989059));
#101486=CARTESIAN_POINT('Ctrl Pts',(-109.624165668541,-4.91256181912092,
130.530457801341));
#101487=CARTESIAN_POINT('Ctrl Pts',(-109.63201255225,-4.91830326132474,
130.668484696905));
#101488=CARTESIAN_POINT('Ctrl Pts',(-109.63985943596,-4.91824962741785,
130.806275011501));
#101489=CARTESIAN_POINT('Ctrl Pts',(-109.639859435992,-4.91824962741763,
130.806275012075));
#101490=CARTESIAN_POINT('Ctrl Pts',(-109.645863669728,-4.91820858811826,
130.911708619347));
#101491=CARTESIAN_POINT('Ctrl Pts',(-109.651867903463,-4.91477752119081,
131.017072484126));
#101492=CARTESIAN_POINT('Ctrl Pts',(-109.657872137199,-4.90796816671738,
131.122215202225));
#101493=CARTESIAN_POINT('Ctrl Pts',(-109.665646471318,-4.89915135525686,
131.258354909087));
#101494=CARTESIAN_POINT('Ctrl Pts',(-109.673420805437,-4.88465181757774,
131.394343125707));
#101495=CARTESIAN_POINT('Ctrl Pts',(-109.681195139556,-4.86447465546066,
131.529667027906));
#101496=CARTESIAN_POINT('Ctrl Pts',(-109.688959892503,-4.8443223598926,
131.664824155491));
#101497=CARTESIAN_POINT('Ctrl Pts',(-109.69672464545,-4.81850641926187,
131.799318214662));
#101498=CARTESIAN_POINT('Ctrl Pts',(-109.704489398397,-4.78708388456926,
131.932638484316));
#101499=CARTESIAN_POINT('Ctrl Pts',(-109.712246439282,-4.7556925591811,
132.065826338398));
#101500=CARTESIAN_POINT('Ctrl Pts',(-109.720003480167,-4.7187058105029,
132.19784234493));
#101501=CARTESIAN_POINT('Ctrl Pts',(-109.727760521052,-4.67623217299796,
132.328183352243));
#101502=CARTESIAN_POINT('Ctrl Pts',(-109.735511712292,-4.63379056519351,
132.458426068389));
#101503=CARTESIAN_POINT('Ctrl Pts',(-109.743262903532,-4.58587042505701,
132.586995929277));
#101504=CARTESIAN_POINT('Ctrl Pts',(-109.751014094772,-4.53263072011456,
132.713402737995));
#101505=CARTESIAN_POINT('Ctrl Pts',(-109.75876199155,-4.47941364346685,
132.839755820448));
#101506=CARTESIAN_POINT('Ctrl Pts',(-109.766509888327,-4.42088165032147,
132.9639473197));
#101507=CARTESIAN_POINT('Ctrl Pts',(-109.774257785104,-4.35724257690382,
133.0855051085));
#101508=CARTESIAN_POINT('Ctrl Pts',(-109.782004061188,-4.29361681540843,
133.20703747003));
#101509=CARTESIAN_POINT('Ctrl Pts',(-109.789750337272,-4.22488627974989,
133.32593687076));
#101510=CARTESIAN_POINT('Ctrl Pts',(-109.797496613356,-4.15130550981274,
133.441754336126));
#101511=CARTESIAN_POINT('Ctrl Pts',(-109.805242946621,-4.07772419671917,
133.55757265643));
#101512=CARTESIAN_POINT('Ctrl Pts',(-109.812989279887,-3.99929278755774,
133.670308665976));
#101513=CARTESIAN_POINT('Ctrl Pts',(-109.820735613152,-3.91630982060835,
133.779541360228));
#101514=CARTESIAN_POINT('Ctrl Pts',(-109.828483681155,-3.83330827019899,
133.888798516384));
#101515=CARTESIAN_POINT('Ctrl Pts',(-109.836231749158,-3.74575337019301,
133.994550484837));
#101516=CARTESIAN_POINT('Ctrl Pts',(-109.843979817161,-3.65398444392659,
134.096408725666));
#101517=CARTESIAN_POINT('Ctrl Pts',(-109.851736119903,-3.56211798455314,
134.198375222645));
#101518=CARTESIAN_POINT('Ctrl Pts',(-109.859492422644,-3.46602881431032,
134.29643943437));
#101519=CARTESIAN_POINT('Ctrl Pts',(-109.867248725386,-3.36609407241288,
134.390248758343));
#101520=CARTESIAN_POINT('Ctrl Pts',(-109.8750091679,-3.26610599233444,134.484108151177));
#101521=CARTESIAN_POINT('Ctrl Pts',(-109.882769610414,-3.16226854668325,
134.573707875885));
#101522=CARTESIAN_POINT('Ctrl Pts',(-109.890530052929,-3.05499179487866,
134.658735819298));
#101523=CARTESIAN_POINT('Ctrl Pts',(-109.898302953194,-2.94754283290878,
134.743900257113));
#101524=CARTESIAN_POINT('Ctrl Pts',(-109.90607585346,-2.83664384838213,
134.82447801797));
#101525=CARTESIAN_POINT('Ctrl Pts',(-109.913848753725,-2.72273443545673,
134.900200001194));
#101526=CARTESIAN_POINT('Ctrl Pts',(-109.921339089487,-2.61296591660983,
134.973169299597));
#101527=CARTESIAN_POINT('Ctrl Pts',(-109.928829425249,-2.50040230588036,
135.041629570522));
#101528=CARTESIAN_POINT('Ctrl Pts',(-109.936319761011,-2.38545661371691,
135.105381404144));
#101529=CARTESIAN_POINT('Ctrl Pts',(-109.94409409513,-2.26615272069961,
135.171550407913));
#101530=CARTESIAN_POINT('Ctrl Pts',(-109.951868429249,-2.14390462838403,
135.232856488996));
#101531=CARTESIAN_POINT('Ctrl Pts',(-109.959642763369,-2.01914654791204,
135.289026745669));
#101532=CARTESIAN_POINT('Ctrl Pts',(-109.967407516316,-1.89454222062462,
135.345127777521));
#101533=CARTESIAN_POINT('Ctrl Pts',(-109.975172269263,-1.76743441307371,
135.396105419705));
#101534=CARTESIAN_POINT('Ctrl Pts',(-109.98293702221,-1.63828364684828,
135.441731613612));
#101535=CARTESIAN_POINT('Ctrl Pts',(-109.990694063095,-1.50926115498458,
135.48731249094));
#101536=CARTESIAN_POINT('Ctrl Pts',(-109.99845110398,-1.37820010868962,
135.527552367959));
#101537=CARTESIAN_POINT('Ctrl Pts',(-110.006208144865,-1.24558248923989,
135.562270592019));
#101538=CARTESIAN_POINT('Ctrl Pts',(-110.013959336105,-1.11306487776877,
135.596962634796));
#101539=CARTESIAN_POINT('Ctrl Pts',(-110.021710527345,-0.978993406257185,
135.626141214034));
#101540=CARTESIAN_POINT('Ctrl Pts',(-110.029461718585,-0.843866417082174,
135.649675110209));
#101541=CARTESIAN_POINT('Ctrl Pts',(-110.037209615362,-0.708796860482009,
135.673199003851));
#101542=CARTESIAN_POINT('Ctrl Pts',(-110.044957512139,-0.572673062856663,
135.691082919197));
#101543=CARTESIAN_POINT('Ctrl Pts',(-110.052705408916,-0.436004578791037,
135.703246518439));
#101544=CARTESIAN_POINT('Ctrl Pts',(-110.060451685001,-0.299364682826046,
135.715407573318));
#101545=CARTESIAN_POINT('Ctrl Pts',(-110.068197961085,-0.162180716226217,
135.721850657492));
#101546=CARTESIAN_POINT('Ctrl Pts',(-110.075944237169,-0.0249679990312448,
135.722547240858));
#101547=CARTESIAN_POINT('Ctrl Pts',(-110.083690570434,0.112245731037023,
135.723243829365));
#101548=CARTESIAN_POINT('Ctrl Pts',(-110.0914369037,0.249487821163756,135.718193830434));
#101549=CARTESIAN_POINT('Ctrl Pts',(-110.099183236965,0.386242701076687,
135.70742084954));
#101550=CARTESIAN_POINT('Ctrl Pts',(-110.106931304968,0.523028206296596,
135.696645456111));
#101551=CARTESIAN_POINT('Ctrl Pts',(-110.114679372971,0.659325894508578,
135.680144561137));
#101552=CARTESIAN_POINT('Ctrl Pts',(-110.122427440974,0.794625463520789,
135.657993631631));
#101553=CARTESIAN_POINT('Ctrl Pts',(-110.130183743716,0.930068830525216,
135.635819159854));
#101554=CARTESIAN_POINT('Ctrl Pts',(-110.137940046458,1.06451157279787,
135.607982721331));
#101555=CARTESIAN_POINT('Ctrl Pts',(-110.145696349199,1.19745318291215,
135.574611023701));
#101556=CARTESIAN_POINT('Ctrl Pts',(-110.153456791714,1.33046574796655,
135.541221514591));
#101557=CARTESIAN_POINT('Ctrl Pts',(-110.161217234228,1.46197520970428,
135.502290970535));
#101558=CARTESIAN_POINT('Ctrl Pts',(-110.168977676742,1.59149733134458,
135.457995681344));
#101559=CARTESIAN_POINT('Ctrl Pts',(-110.176750577007,1.72122737339297,
135.413629285422));
#101560=CARTESIAN_POINT('Ctrl Pts',(-110.184523477273,1.8489633356778,135.363881076881));
#101561=CARTESIAN_POINT('Ctrl Pts',(-110.192296377538,1.97424120480058,
135.308975443249));
#101562=CARTESIAN_POINT('Ctrl Pts',(-110.1997867133,2.09496490782483,135.256065767699));
#101563=CARTESIAN_POINT('Ctrl Pts',(-110.207277049062,2.21340585376656,
135.198367262696));
#101564=CARTESIAN_POINT('Ctrl Pts',(-110.214767384824,2.32917303125561,
135.136119619746));
#101565=CARTESIAN_POINT('Ctrl Pts',(-110.222541718943,2.44932955646568,
135.071511838495));
#101566=CARTESIAN_POINT('Ctrl Pts',(-110.230316053063,2.5669861787307,135.001798490493));
#101567=CARTESIAN_POINT('Ctrl Pts',(-110.238090387182,2.68167859637454,
134.927197379827));
#101568=CARTESIAN_POINT('Ctrl Pts',(-110.245855140129,2.79622966586399,
134.852688208361));
#101569=CARTESIAN_POINT('Ctrl Pts',(-110.253619893076,2.90782347475742,
134.773303470787));
#101570=CARTESIAN_POINT('Ctrl Pts',(-110.261384646023,3.01601922772018,
134.689307345711));
#101571=CARTESIAN_POINT('Ctrl Pts',(-110.269141686908,3.1241075191358,134.60539464677));
#101572=CARTESIAN_POINT('Ctrl Pts',(-110.276898727793,3.2288041641905,134.516879913122));
#101573=CARTESIAN_POINT('Ctrl Pts',(-110.284655768678,3.32969665204159,
134.424071002097));
#101574=CARTESIAN_POINT('Ctrl Pts',(-110.292406959918,3.43051305608263,
134.331332078994));
#101575=CARTESIAN_POINT('Ctrl Pts',(-110.300158151158,3.52753072640563,
134.234305687715));
#101576=CARTESIAN_POINT('Ctrl Pts',(-110.307909342398,3.62036989808175,
134.133340170457));
#101577=CARTESIAN_POINT('Ctrl Pts',(-110.315657239175,3.71316961063347,
134.032417566237));
#101578=CARTESIAN_POINT('Ctrl Pts',(-110.323405135953,3.80179409273827,
133.927559453152));
#101579=CARTESIAN_POINT('Ctrl Pts',(-110.33115303273,3.88590032722215,133.819151109357));
#101580=CARTESIAN_POINT('Ctrl Pts',(-110.338899308814,3.9699889684949,133.710765442251));
#101581=CARTESIAN_POINT('Ctrl Pts',(-110.346645584898,4.04956100254009,
133.598831330276));
#101582=CARTESIAN_POINT('Ctrl Pts',(-110.354391860982,4.12431388310457,
133.483766905558));
#101583=CARTESIAN_POINT('Ctrl Pts',(-110.362138194247,4.19906731547773,
133.36870163146));
#101584=CARTESIAN_POINT('Ctrl Pts',(-110.369884527512,4.26900131039169,
133.250506326364));
#101585=CARTESIAN_POINT('Ctrl Pts',(-110.377630860778,4.33385704947505,
133.129627513476));
#101586=CARTESIAN_POINT('Ctrl Pts',(-110.385378928781,4.3987273125514,133.008721630616));
#101587=CARTESIAN_POINT('Ctrl Pts',(-110.393126996784,4.45851687201439,
132.885131388582));
#101588=CARTESIAN_POINT('Ctrl Pts',(-110.400875064787,4.51301338960115,
132.759326910825));
#101589=CARTESIAN_POINT('Ctrl Pts',(-110.408631367528,4.5675678267354,132.633388726572));
#101590=CARTESIAN_POINT('Ctrl Pts',(-110.41638767027,4.616817828782,132.505231964918));
#101591=CARTESIAN_POINT('Ctrl Pts',(-110.424143973012,4.66059946197643,
132.375346205509));
#101592=CARTESIAN_POINT('Ctrl Pts',(-110.431904415526,4.70440446274684,
132.245391122159));
#101593=CARTESIAN_POINT('Ctrl Pts',(-110.439664858041,4.74273516982851,
132.113705577464));
#101594=CARTESIAN_POINT('Ctrl Pts',(-110.447425300555,4.77547815902452,
131.980792262491));
#101595=CARTESIAN_POINT('Ctrl Pts',(-110.45519820082,4.80827371017357,131.847665583264));
#101596=CARTESIAN_POINT('Ctrl Pts',(-110.462971101086,4.83546354112521,
131.71330757864));
#101597=CARTESIAN_POINT('Ctrl Pts',(-110.470744001351,4.85698562488538,
131.578229923171));
#101598=CARTESIAN_POINT('Ctrl Pts',(-110.478234337113,4.87772532669024,
131.448062680716));
#101599=CARTESIAN_POINT('Ctrl Pts',(-110.485724672875,4.89320216468743,
131.317227507154));
#101600=CARTESIAN_POINT('Ctrl Pts',(-110.493215008637,4.90340644693239,
131.186182930536));
#101601=CARTESIAN_POINT('Ctrl Pts',(-110.500989342756,4.91399762764009,
131.050169758967));
#101602=CARTESIAN_POINT('Ctrl Pts',(-110.508763676875,4.91894209183884,
130.913500143009));
#101603=CARTESIAN_POINT('Ctrl Pts',(-110.516538010995,4.91817211787623,
130.776682441238));
#101604=CARTESIAN_POINT('Ctrl Pts',(-110.524302763942,4.91740309283771,
130.640033355057));
#101605=CARTESIAN_POINT('Ctrl Pts',(-110.532067516889,4.91093364436117,
130.503236933395));
#101606=CARTESIAN_POINT('Ctrl Pts',(-110.539832269836,4.89874777274482,
130.366806824841));
#101607=CARTESIAN_POINT('Ctrl Pts',(-110.547589310721,4.88657400430795,
130.230512220595));
#101608=CARTESIAN_POINT('Ctrl Pts',(-110.555346351606,4.86869514603252,
130.094583592318));
#101609=CARTESIAN_POINT('Ctrl Pts',(-110.563103392491,4.8451472348218,129.959534401473));
#101610=CARTESIAN_POINT('Ctrl Pts',(-110.570854583731,4.82161708127407,
129.824587052272));
#101611=CARTESIAN_POINT('Ctrl Pts',(-110.578605774971,4.79242645095818,
129.690518204058));
#101612=CARTESIAN_POINT('Ctrl Pts',(-110.586356966211,4.75766314181056,
129.557835651287));
#101613=CARTESIAN_POINT('Ctrl Pts',(-110.594104862988,4.72291460799662,
129.42520949214));
#101614=CARTESIAN_POINT('Ctrl Pts',(-110.601852759766,4.68259820507299,
129.293968833945));
#101615=CARTESIAN_POINT('Ctrl Pts',(-110.609600656543,4.63685266930219,
129.164610519019));
#101616=CARTESIAN_POINT('Ctrl Pts',(-110.617346932627,4.59111670251143,
129.035279263064));
#101617=CARTESIAN_POINT('Ctrl Pts',(-110.625093208711,4.53995399202432,
128.90782993556));
#101618=CARTESIAN_POINT('Ctrl Pts',(-110.632839484795,4.48355279060068,
128.782743087864));
#101619=CARTESIAN_POINT('Ctrl Pts',(-110.64058581806,4.42715117283611,128.657655316806));
#101620=CARTESIAN_POINT('Ctrl Pts',(-110.648332151326,4.36551114767705,
128.534930416766));
#101621=CARTESIAN_POINT('Ctrl Pts',(-110.656078484591,4.2988684900923,128.41502749567));
#101622=CARTESIAN_POINT('Ctrl Pts',(-110.663826552594,4.23221090834635,
128.295097723145));
#101623=CARTESIAN_POINT('Ctrl Pts',(-110.671574620597,4.16054865479605,
128.177991528762));
#101624=CARTESIAN_POINT('Ctrl Pts',(-110.6793226886,4.08416248359781,128.064141671921));
#101625=CARTESIAN_POINT('Ctrl Pts',(-110.687078991342,4.00769512826792,
127.950170814098));
#101626=CARTESIAN_POINT('Ctrl Pts',(-110.694835294084,3.92649404420397,
127.839463532466));
#101627=CARTESIAN_POINT('Ctrl Pts',(-110.702591596826,3.84088251842448,
127.732422378903));
#101628=CARTESIAN_POINT('Ctrl Pts',(-110.71035203934,3.75522529919598,127.625324094253));
#101629=CARTESIAN_POINT('Ctrl Pts',(-110.718112481854,3.6651532043725,127.521896131297));
#101630=CARTESIAN_POINT('Ctrl Pts',(-110.725872924368,3.57102785363685,
127.422505633826));
#101631=CARTESIAN_POINT('Ctrl Pts',(-110.733645824634,3.47675140453215,
127.322955585904));
#101632=CARTESIAN_POINT('Ctrl Pts',(-110.741418724899,3.37840897780296,
127.227456227692));
#101633=CARTESIAN_POINT('Ctrl Pts',(-110.749191625164,3.27639753263701,
127.136336316852));
#101634=CARTESIAN_POINT('Ctrl Pts',(-110.756681960926,3.17809446045501,
127.048528844288));
#101635=CARTESIAN_POINT('Ctrl Pts',(-110.764172296688,3.07638473247442,
126.964788135019));
#101636=CARTESIAN_POINT('Ctrl Pts',(-110.77166263245,2.97164888259986,126.885370188764));
#101637=CARTESIAN_POINT('Ctrl Pts',(-110.779436966569,2.86294194114248,
126.802941086937));
#101638=CARTESIAN_POINT('Ctrl Pts',(-110.787211300689,2.75063052622654,
126.724907903406));
#101639=CARTESIAN_POINT('Ctrl Pts',(-110.794985634808,2.63510572911355,
126.651602394542));
#101640=CARTESIAN_POINT('Ctrl Pts',(-110.802750387755,2.51972330598856,
126.578387228167));
#101641=CARTESIAN_POINT('Ctrl Pts',(-110.810515140702,2.40113570724194,
126.509888351048));
#101642=CARTESIAN_POINT('Ctrl Pts',(-110.818279893649,2.27976643174905,
126.446396863796));
#101643=CARTESIAN_POINT('Ctrl Pts',(-110.826036934534,2.15851770193159,
126.382968437185));
#101644=CARTESIAN_POINT('Ctrl Pts',(-110.833793975419,2.03449313765044,
126.324537683183));
#101645=CARTESIAN_POINT('Ctrl Pts',(-110.841551016304,1.90814420740121,
126.271351821384));
#101646=CARTESIAN_POINT('Ctrl Pts',(-110.849302207544,1.78189055786297,
126.218206067458));
#101647=CARTESIAN_POINT('Ctrl Pts',(-110.857053398784,1.65331639012675,
126.17029748419));
#101648=CARTESIAN_POINT('Ctrl Pts',(-110.864804590024,1.52289638297982,
126.12782668));
#101649=CARTESIAN_POINT('Ctrl Pts',(-110.872552486801,1.39253180781518,
126.085373927034));
#101650=CARTESIAN_POINT('Ctrl Pts',(-110.880300383578,1.2603233245844,126.048354477148));
#101651=CARTESIAN_POINT('Ctrl Pts',(-110.888048280356,1.12676393113888,
126.016920163003));
#101652=CARTESIAN_POINT('Ctrl Pts',(-110.89579455644,0.993232475439257,
125.985492424239));
#101653=CARTESIAN_POINT('Ctrl Pts',(-110.903540832524,0.858351051920262,
125.959647586936));
#101654=CARTESIAN_POINT('Ctrl Pts',(-110.911287108608,0.722625717265087,
125.939487018463));
#101655=CARTESIAN_POINT('Ctrl Pts',(-110.919033441873,0.586899380716138,
125.91932630117));
#101656=CARTESIAN_POINT('Ctrl Pts',(-110.926779775139,0.450329507322539,
125.904849993878));
#101657=CARTESIAN_POINT('Ctrl Pts',(-110.934526108404,0.313429799715211,
125.896107891478));
#101658=CARTESIAN_POINT('Ctrl Pts',(-110.942274176407,0.176499434367747,
125.887363831345));
#101659=CARTESIAN_POINT('Ctrl Pts',(-110.95002224441,0.0392394779213967,
125.884356556295));
#101660=CARTESIAN_POINT('Ctrl Pts',(-110.957770312413,-0.0978342224023159,
125.887083776933));
#101661=CARTESIAN_POINT('Ctrl Pts',(-110.965526615155,-0.235053606286117,
125.889813896094));
#101662=CARTESIAN_POINT('Ctrl Pts',(-110.973282917897,-0.372085947099265,
125.898290677953));
#101663=CARTESIAN_POINT('Ctrl Pts',(-110.981039220638,-0.508417822016762,
125.912459721109));
#101664=CARTESIAN_POINT('Ctrl Pts',(-110.988799663153,-0.644822461360775,
125.92663632671));
#101665=CARTESIAN_POINT('Ctrl Pts',(-110.996560105667,-0.780525503212871,
125.946511190713));
#101666=CARTESIAN_POINT('Ctrl Pts',(-111.004320548181,-0.915022594832922,
125.971978522424));
#101667=CARTESIAN_POINT('Ctrl Pts',(-111.012093448446,-1.04973559312453,
125.997486736557));
#101668=CARTESIAN_POINT('Ctrl Pts',(-111.019866348712,-1.18323839166486,
126.028605269552));
#101669=CARTESIAN_POINT('Ctrl Pts',(-111.027639248977,-1.31503983118537,
126.065177849947));
#101670=CARTESIAN_POINT('Ctrl Pts',(-111.035129584739,-1.44204995639116,
126.100420924924));
#101671=CARTESIAN_POINT('Ctrl Pts',(-111.042619920501,-1.56747997913212,
126.140728300803));
#101672=CARTESIAN_POINT('Ctrl Pts',(-111.050110256263,-1.69090883172269,
126.185918197734));
#101673=CARTESIAN_POINT('Ctrl Pts',(-111.057884754316,-1.81902022814314,
126.23282247237));
#101674=CARTESIAN_POINT('Ctrl Pts',(-111.065659252369,-1.94538144609914,
126.285135622105));
#101675=CARTESIAN_POINT('Ctrl Pts',(-111.073433750422,-2.06950194428199,
126.342707923203));
#101676=CARTESIAN_POINT('Ctrl Pts',(-111.081198629165,-2.19346886939339,
126.40020899066));
#101677=CARTESIAN_POINT('Ctrl Pts',(-111.088963507908,-2.31520023982343,
126.462956099113));
#101678=CARTESIAN_POINT('Ctrl Pts',(-111.09672838665,-2.43422221038913,
126.530750282855));
#101679=CARTESIAN_POINT('Ctrl Pts',(-111.104485515354,-2.55312538644857,
126.598476801976));
#101680=CARTESIAN_POINT('Ctrl Pts',(-111.112242644058,-2.6693242067441,
126.671240179177));
#101681=CARTESIAN_POINT('Ctrl Pts',(-111.119999772762,-2.7823666343237,
126.748794199086));
#101682=CARTESIAN_POINT('Ctrl Pts',(-111.127751013966,-2.89532326504654,
126.826289357103));
#101683=CARTESIAN_POINT('Ctrl Pts',(-111.135502255169,-3.0051279504709,
126.908567700077));
#101684=CARTESIAN_POINT('Ctrl Pts',(-111.143253496373,-3.11135533081537,
126.995338293149));
#101685=CARTESIAN_POINT('Ctrl Pts',(-111.151001249663,-3.21753491081371,
127.082069841067));
#101686=CARTESIAN_POINT('Ctrl Pts',(-111.158749002952,-3.32014008624431,
127.173289370495));
#101687=CARTESIAN_POINT('Ctrl Pts',(-111.166496756242,-3.41877666201874,
127.268664194266));
#101688=CARTESIAN_POINT('Ctrl Pts',(-111.174242834922,-3.51739191834894,
127.364018403592));
#101689=CARTESIAN_POINT('Ctrl Pts',(-111.181988913601,-3.61204000067276,
127.463525848915));
#101690=CARTESIAN_POINT('Ctrl Pts',(-111.189734992281,-3.70236211807162,
127.566815589436));
#101691=CARTESIAN_POINT('Ctrl Pts',(-111.197481074189,-3.7926842731182,
127.67010537301));
#101692=CARTESIAN_POINT('Ctrl Pts',(-111.205227156097,-3.87868020250311,
127.777177160502));
#101693=CARTESIAN_POINT('Ctrl Pts',(-111.212973238005,-3.96003037444908,
127.887625714298));
#101694=CARTESIAN_POINT('Ctrl Pts',(-111.220721000616,-4.04139819731153,
127.998098232619));
#101695=CARTESIAN_POINT('Ctrl Pts',(-111.228468763227,-4.11811802552781,
128.111948660221));
#101696=CARTESIAN_POINT('Ctrl Pts',(-111.236216525838,-4.18991298812066,
128.228741815321));
#101697=CARTESIAN_POINT('Ctrl Pts',(-111.243971783412,-4.26177740309686,
128.345647952763));
#101698=CARTESIAN_POINT('Ctrl Pts',(-111.251727040985,-4.32870723333778,
128.465502169262));
#101699=CARTESIAN_POINT('Ctrl Pts',(-111.259482298559,-4.39047081830445,
128.587843291643));
#101700=CARTESIAN_POINT('Ctrl Pts',(-111.267241673625,-4.45226719535576,
128.710249368486));
#101701=CARTESIAN_POINT('Ctrl Pts',(-111.27500104869,-4.5088917005392,128.835144626436));
#101702=CARTESIAN_POINT('Ctrl Pts',(-111.282760423756,-4.56016078627259,
128.962047759813));
#101703=CARTESIAN_POINT('Ctrl Pts',(-111.290530533217,-4.61150079815912,
129.089126452222));
#101704=CARTESIAN_POINT('Ctrl Pts',(-111.298300642677,-4.6574704619042,
129.218218200255));
#101705=CARTESIAN_POINT('Ctrl Pts',(-111.306070752138,-4.69793588766045,
129.348825850571));
#101706=CARTESIAN_POINT('Ctrl Pts',(-111.310674899233,-4.72191351286471,
129.426216888217));
#101707=CARTESIAN_POINT('Ctrl Pts',(-111.315279046328,-4.74395950786869,
129.504139939888));
#101708=CARTESIAN_POINT('Ctrl Pts',(-111.319883193423,-4.764054528234,129.582490119308));
#101709=CARTESIAN_POINT('Origin',(213.235140564004,0.,130.804360617566));
#101710=CARTESIAN_POINT('',(-113.415051629673,-4.76405452823414,129.582490119309));
#101711=CARTESIAN_POINT('',(-113.070135781827,-4.76405452823415,129.582490119309));
#101712=CARTESIAN_POINT('',(213.235140564004,-4.76405452823405,129.582490119308));
#101713=CARTESIAN_POINT('',(-111.735140564046,-4.91824993013872,130.805189587063));
#101714=CARTESIAN_POINT('Ctrl Pts',(-111.735140564046,-4.91824993013872,
130.805189587062));
#101715=CARTESIAN_POINT('Ctrl Pts',(-111.743365975676,-4.91822531490536,
130.951230991851));
#101716=CARTESIAN_POINT('Ctrl Pts',(-111.751591387307,-4.91169166136951,
131.097112736765));
#101717=CARTESIAN_POINT('Ctrl Pts',(-111.759816798937,-4.89871700114936,
131.242258785123));
#101718=CARTESIAN_POINT('Ctrl Pts',(-111.768057245701,-4.88571862470098,
131.387670144231));
#101719=CARTESIAN_POINT('Ctrl Pts',(-111.776297692464,-4.86625575973969,
131.532342811153));
#101720=CARTESIAN_POINT('Ctrl Pts',(-111.784538139227,-4.84044768410444,
131.675709732415));
#101721=CARTESIAN_POINT('Ctrl Pts',(-111.792802012384,-4.81456623985632,
131.819484225023));
#101722=CARTESIAN_POINT('Ctrl Pts',(-111.801065885542,-4.78230356247516,
131.961945239414));
#101723=CARTESIAN_POINT('Ctrl Pts',(-111.809329758699,-4.74382963025624,
132.102537609198));
#101724=CARTESIAN_POINT('Ctrl Pts',(-111.817606503093,-4.70529577370621,
132.243348955916));
#101725=CARTESIAN_POINT('Ctrl Pts',(-111.825883247486,-4.66053144156212,
132.382285550338));
#101726=CARTESIAN_POINT('Ctrl Pts',(-111.83415999188,-4.60975528610488,
132.51881075237));
#101727=CARTESIAN_POINT('Ctrl Pts',(-111.842456281904,-4.55885922214883,
132.6556583603));
#101728=CARTESIAN_POINT('Ctrl Pts',(-111.850752571929,-4.5019230691995,
132.790082901989));
#101729=CARTESIAN_POINT('Ctrl Pts',(-111.859048861953,-4.43921281799391,
132.921569303326));
#101730=CARTESIAN_POINT('Ctrl Pts',(-111.861320618483,-4.42204099514086,
132.957573962022));
#101731=CARTESIAN_POINT('Ctrl Pts',(-111.863592375012,-4.40443647618341,
132.993358473109));
#101732=CARTESIAN_POINT('Ctrl Pts',(-111.865864131542,-4.38640529312948,
133.028912632446));
#101733=CARTESIAN_POINT('Ctrl Pts',(-111.873638465661,-4.32469954261759,
133.150584964156));
#101734=CARTESIAN_POINT('Ctrl Pts',(-111.881412799781,-4.25782970485521,
133.269880632356));
#101735=CARTESIAN_POINT('Ctrl Pts',(-111.8891871339,-4.18600237924457,133.386330242379));
#101736=CARTESIAN_POINT('Ctrl Pts',(-111.896951886847,-4.11426357439335,
133.502636338665));
#101737=CARTESIAN_POINT('Ctrl Pts',(-111.904716639795,-4.03757964137516,
133.616103026116));
#101738=CARTESIAN_POINT('Ctrl Pts',(-111.912481392742,-3.95620410484703,
133.726283296778));
#101739=CARTESIAN_POINT('Ctrl Pts',(-111.920238433627,-3.87490939164875,
133.836354134841));
#101740=CARTESIAN_POINT('Ctrl Pts',(-111.927995474512,-3.78893257885525,
133.943144739397));
#101741=CARTESIAN_POINT('Ctrl Pts',(-111.935752515398,-3.69857153601745,
134.04623533067));
#101742=CARTESIAN_POINT('Ctrl Pts',(-111.943503706638,-3.60827863514509,
134.149248180525));
#101743=CARTESIAN_POINT('Ctrl Pts',(-111.951254897879,-3.51360834164596,
134.248566278018));
#101744=CARTESIAN_POINT('Ctrl Pts',(-111.959006089119,-3.41489978409298,
134.34380160833));
#101745=CARTESIAN_POINT('Ctrl Pts',(-111.966753985896,-3.31623318030997,
134.438996461087));
#101746=CARTESIAN_POINT('Ctrl Pts',(-111.974501882674,-3.2135320069729,
134.53011172712));
#101747=CARTESIAN_POINT('Ctrl Pts',(-111.982249779451,-3.10717319982014,
134.616795242424));
#101748=CARTESIAN_POINT('Ctrl Pts',(-111.989996055535,-3.00083664063701,
134.703460625406));
#101749=CARTESIAN_POINT('Ctrl Pts',(-111.99774233162,-2.89084427232924,
134.785695854723));
#101750=CARTESIAN_POINT('Ctrl Pts',(-112.005488607704,-2.77760684633535,
134.863188437232));
#101751=CARTESIAN_POINT('Ctrl Pts',(-112.013234940969,-2.66436858444834,
134.940681591772));
#101752=CARTESIAN_POINT('Ctrl Pts',(-112.020981274235,-2.54788553972355,
135.013431808846));
#101753=CARTESIAN_POINT('Ctrl Pts',(-112.028727607501,-2.42859789585341,
135.081169629289));
#101754=CARTESIAN_POINT('Ctrl Pts',(-112.036475675504,-2.309283538343,135.148922619147));
#101755=CARTESIAN_POINT('Ctrl Pts',(-112.044223743507,-2.18716367180985,
135.211660785727));
#101756=CARTESIAN_POINT('Ctrl Pts',(-112.05197181151,-2.06270318878847,
135.269160570247));
#101757=CARTESIAN_POINT('Ctrl Pts',(-112.059728114252,-1.93811042768414,
135.326721466223));
#101758=CARTESIAN_POINT('Ctrl Pts',(-112.067484416994,-1.81117243625772,
135.379032694398));
#101759=CARTESIAN_POINT('Ctrl Pts',(-112.075240719736,-1.68237471921097,
135.425918619654));
#101760=CARTESIAN_POINT('Ctrl Pts',(-112.083001162251,-1.55350825894461,
135.472829569339));
#101761=CARTESIAN_POINT('Ctrl Pts',(-112.090761604765,-1.42278046770866,
135.514309328098));
#101762=CARTESIAN_POINT('Ctrl Pts',(-112.09852204728,-1.29069116993974,
135.550232441198));
#101763=CARTESIAN_POINT('Ctrl Pts',(-112.106294947545,-1.1583898307037,
135.586213221267));
#101764=CARTESIAN_POINT('Ctrl Pts',(-112.114067847811,-1.0247229988327,
135.616619443862));
#101765=CARTESIAN_POINT('Ctrl Pts',(-112.121840748076,-0.890200713053664,
135.641376821072));
#101766=CARTESIAN_POINT('Ctrl Pts',(-112.129331083836,-0.760568651250498,
135.665234205252));
#101767=CARTESIAN_POINT('Ctrl Pts',(-112.136821419595,-0.630142556467407,
135.683846269707));
#101768=CARTESIAN_POINT('Ctrl Pts',(-112.144311755355,-0.499380592132474,
135.697192321876));
#101769=CARTESIAN_POINT('Ctrl Pts',(-112.152086089474,-0.363660748130608,
135.711044393674));
#101770=CARTESIAN_POINT('Ctrl Pts',(-112.159860423593,-0.227149143152057,
135.719267127933));
#101771=CARTESIAN_POINT('Ctrl Pts',(-112.167634757712,-0.0903523642468036,
135.721780623298));
#101772=CARTESIAN_POINT('Ctrl Pts',(-112.175399510659,0.0462758248546998,
135.724291021005));
#101773=CARTESIAN_POINT('Ctrl Pts',(-112.183164263606,0.183188101452787,
135.721106172501));
#101774=CARTESIAN_POINT('Ctrl Pts',(-112.190929016553,0.319871348825531,
135.712197756541));
#101775=CARTESIAN_POINT('Ctrl Pts',(-112.198686057438,0.456418840470089,
135.703298188545));
#101776=CARTESIAN_POINT('Ctrl Pts',(-112.206443098323,0.592737367962033,
135.688686391221));
#101777=CARTESIAN_POINT('Ctrl Pts',(-112.214200139208,0.728312752918227,
135.668386069436));
#101778=CARTESIAN_POINT('Ctrl Pts',(-112.221951330449,0.863785899421818,
135.648101056281));
#101779=CARTESIAN_POINT('Ctrl Pts',(-112.229702521689,0.99851663376067,
135.622136114834));
#101780=CARTESIAN_POINT('Ctrl Pts',(-112.237453712929,1.13199520080176,
135.590566832081));
#101781=CARTESIAN_POINT('Ctrl Pts',(-112.245201609706,1.26541703589138,
135.559010967115));
#101782=CARTESIAN_POINT('Ctrl Pts',(-112.252949506483,1.39758738252528,
135.521855588246));
#101783=CARTESIAN_POINT('Ctrl Pts',(-112.26069740326,1.52800621217691,135.479227468937));
#101784=CARTESIAN_POINT('Ctrl Pts',(-112.268443679344,1.65839776102087,
135.436608266512));
#101785=CARTESIAN_POINT('Ctrl Pts',(-112.276189955428,1.78703815024909,
135.388518722065));
#101786=CARTESIAN_POINT('Ctrl Pts',(-112.283936231513,1.9134424493424,135.335135502236));
#101787=CARTESIAN_POINT('Ctrl Pts',(-112.291682564778,2.03984768152336,
135.281751888344));
#101788=CARTESIAN_POINT('Ctrl Pts',(-112.299428898043,2.16401643046852,
135.2230746732));
#101789=CARTESIAN_POINT('Ctrl Pts',(-112.307175231309,2.28548406251401,
135.159328546552));
#101790=CARTESIAN_POINT('Ctrl Pts',(-112.314923299312,2.40697889639366,
135.0955681444));
#101791=CARTESIAN_POINT('Ctrl Pts',(-112.322671367315,2.5257710635777,135.026736753576));
#101792=CARTESIAN_POINT('Ctrl Pts',(-112.330419435318,2.64142119196144,
134.953104662353));
#101793=CARTESIAN_POINT('Ctrl Pts',(-112.33817573806,2.75719423467773,134.879394314068));
#101794=CARTESIAN_POINT('Ctrl Pts',(-112.345932040801,2.86981823746912,
134.800873283415));
#101795=CARTESIAN_POINT('Ctrl Pts',(-112.353688343543,2.97888300638684,
134.71785510418));
#101796=CARTESIAN_POINT('Ctrl Pts',(-112.361448786057,3.0880059864559,134.634792615643));
#101797=CARTESIAN_POINT('Ctrl Pts',(-112.369209228572,3.1935656466337,134.547228445286));
#101798=CARTESIAN_POINT('Ctrl Pts',(-112.376969671086,3.29518627098337,
134.455515298215));
#101799=CARTESIAN_POINT('Ctrl Pts',(-112.384742571351,3.3969700257807,134.363654925058));
#101800=CARTESIAN_POINT('Ctrl Pts',(-112.392515471617,3.4948018296186,134.267632539794));
#101801=CARTESIAN_POINT('Ctrl Pts',(-112.400288371882,3.58834349358395,
134.167837098018));
#101802=CARTESIAN_POINT('Ctrl Pts',(-112.407778707644,3.67848468244187,
134.071669471926));
#101803=CARTESIAN_POINT('Ctrl Pts',(-112.415269043406,3.76464202947925,
133.971998579962));
#101804=CARTESIAN_POINT('Ctrl Pts',(-112.422759379167,3.84655047693288,
133.86919870316));
#101805=CARTESIAN_POINT('Ctrl Pts',(-112.430533713286,3.93156450807075,
133.762501137779));
#101806=CARTESIAN_POINT('Ctrl Pts',(-112.438308047405,4.01227038425401,
133.652094647021));
#101807=CARTESIAN_POINT('Ctrl Pts',(-112.446082381524,4.08832705953567,
133.538362248284));
#101808=CARTESIAN_POINT('Ctrl Pts',(-112.453847134471,4.16429000176242,
133.424770014564));
#101809=CARTESIAN_POINT('Ctrl Pts',(-112.461611887418,4.23561492828482,
133.307860350296));
#101810=CARTESIAN_POINT('Ctrl Pts',(-112.469376640365,4.30200065951633,
133.188049646785));
#101811=CARTESIAN_POINT('Ctrl Pts',(-112.47713368125,4.3683204555037,133.068357940955));
#101812=CARTESIAN_POINT('Ctrl Pts',(-112.484890722135,4.42971063046171,
132.94577126967));
#101813=CARTESIAN_POINT('Ctrl Pts',(-112.49264776302,4.48591320199007,132.820735038826));
#101814=CARTESIAN_POINT('Ctrl Pts',(-112.50039895426,4.54207339072213,132.695793098776));
#101815=CARTESIAN_POINT('Ctrl Pts',(-112.5081501455,4.59305360300879,132.568405631124));
#101816=CARTESIAN_POINT('Ctrl Pts',(-112.51590133674,4.6386418972212,132.439042363914));
#101817=CARTESIAN_POINT('Ctrl Pts',(-112.523649233517,4.6842108151924,132.309734079544));
#101818=CARTESIAN_POINT('Ctrl Pts',(-112.531397130294,4.72439224345059,
132.178452033814));
#101819=CARTESIAN_POINT('Ctrl Pts',(-112.539145027071,4.75902256246914,
132.045685439041));
#101820=CARTESIAN_POINT('Ctrl Pts',(-112.546891303156,4.7936456375715,131.912946616177));
#101821=CARTESIAN_POINT('Ctrl Pts',(-112.55463757924,4.82271981445595,131.77872424001));
#101822=CARTESIAN_POINT('Ctrl Pts',(-112.562383855324,4.84613161097958,
131.643521788954));
#101823=CARTESIAN_POINT('Ctrl Pts',(-112.570130188589,4.86954358032375,
131.508318339863));
#101824=CARTESIAN_POINT('Ctrl Pts',(-112.577876521854,4.88729301919419,
131.37213518668));
#101825=CARTESIAN_POINT('Ctrl Pts',(-112.585622855119,4.89931781959404,
131.235484689161));
#101826=CARTESIAN_POINT('Ctrl Pts',(-112.593370923122,4.91134531286457,
131.09880358971));
#101827=CARTESIAN_POINT('Ctrl Pts',(-112.601118991125,4.91764558238198,
130.96165532705));
#101828=CARTESIAN_POINT('Ctrl Pts',(-112.608867059128,4.91820853797107,
130.82455565479));
#101829=CARTESIAN_POINT('Ctrl Pts',(-112.61662336187,4.91877209187605,130.687310271368));
#101830=CARTESIAN_POINT('Ctrl Pts',(-112.624379664612,4.91358614946113,
130.550113973093));
#101831=CARTESIAN_POINT('Ctrl Pts',(-112.632135967354,4.9026927757303,130.41348134042));
#101832=CARTESIAN_POINT('Ctrl Pts',(-112.639896409868,4.89179358787791,
130.276775782798));
#101833=CARTESIAN_POINT('Ctrl Pts',(-112.647656852382,4.87518094617575,
130.140634878135));
#101834=CARTESIAN_POINT('Ctrl Pts',(-112.655417294896,4.85294850777792,
130.005565372615));
#101835=CARTESIAN_POINT('Ctrl Pts',(-112.663190195161,4.83068037989626,
129.870279041534));
#101836=CARTESIAN_POINT('Ctrl Pts',(-112.670963095427,4.80277450732906,
129.736067929514));
#101837=CARTESIAN_POINT('Ctrl Pts',(-112.678735995692,4.76937533006668,
129.603426804464));
#101838=CARTESIAN_POINT('Ctrl Pts',(-112.686226331455,4.73719029702189,
129.4756075184));
#101839=CARTESIAN_POINT('Ctrl Pts',(-112.693716667218,4.69990450336563,
129.349246350512));
#101840=CARTESIAN_POINT('Ctrl Pts',(-112.70120700298,4.65768957213563,129.224768609445));
#101841=CARTESIAN_POINT('Ctrl Pts',(-112.7089813371,4.61387404896124,129.095571257004));
#101842=CARTESIAN_POINT('Ctrl Pts',(-112.716755671219,4.56460943883901,
128.967993712577));
#101843=CARTESIAN_POINT('Ctrl Pts',(-112.724530005338,4.5100336414892,128.842529938038));
#101844=CARTESIAN_POINT('Ctrl Pts',(-112.732294758285,4.45552510393205,
128.717220786389));
#101845=CARTESIAN_POINT('Ctrl Pts',(-112.740059511232,4.39571855732209,
128.594020576463));
#101846=CARTESIAN_POINT('Ctrl Pts',(-112.747824264179,4.33080152853476,
128.473407768849));
#101847=CARTESIAN_POINT('Ctrl Pts',(-112.755581305064,4.26594897625558,
128.352914755576));
#101848=CARTESIAN_POINT('Ctrl Pts',(-112.763338345949,4.19599622697075,
128.235004372547));
#101849=CARTESIAN_POINT('Ctrl Pts',(-112.771095386834,4.12117856748556,
128.120134420429));
#101850=CARTESIAN_POINT('Ctrl Pts',(-112.778846578074,4.04641732857948,
128.005351092635));
#101851=CARTESIAN_POINT('Ctrl Pts',(-112.786597769314,3.96679869424462,
127.893603958326));
#101852=CARTESIAN_POINT('Ctrl Pts',(-112.794348960554,3.8826033003593,127.785325229476));
#101853=CARTESIAN_POINT('Ctrl Pts',(-112.802096857332,3.79844369176225,
127.677092521975));
#101854=CARTESIAN_POINT('Ctrl Pts',(-112.809844754109,3.7097114320475,127.572325595924));
#101855=CARTESIAN_POINT('Ctrl Pts',(-112.817592650886,3.61672966904007,
127.471426540272));
#101856=CARTESIAN_POINT('Ctrl Pts',(-112.82533892697,3.523767355813,127.370548590528));
#101857=CARTESIAN_POINT('Ctrl Pts',(-112.833085203054,3.42655757214922,
127.273537189209));
#101858=CARTESIAN_POINT('Ctrl Pts',(-112.840831479138,3.32546256882749,
127.180759954437));
#101859=CARTESIAN_POINT('Ctrl Pts',(-112.848577812404,3.22436681924528,
127.087982034805));
#101860=CARTESIAN_POINT('Ctrl Pts',(-112.856324145669,3.1193860808266,126.999438608439));
#101861=CARTESIAN_POINT('Ctrl Pts',(-112.864070478934,3.01091784545658,
126.915458871519));
#101862=CARTESIAN_POINT('Ctrl Pts',(-112.871818546937,2.90242531937718,
126.831460327919));
#101863=CARTESIAN_POINT('Ctrl Pts',(-112.87956661494,2.79044405132565,126.75202774674));
#101864=CARTESIAN_POINT('Ctrl Pts',(-112.887314682943,2.67540250543436,
126.677448394558));
#101865=CARTESIAN_POINT('Ctrl Pts',(-112.895070985685,2.56023869201925,
126.602789778552));
#101866=CARTESIAN_POINT('Ctrl Pts',(-112.902827288427,2.44200843212858,
126.532994908356));
#101867=CARTESIAN_POINT('Ctrl Pts',(-112.910583591169,2.32116739403544,
126.468306536795));
#101868=CARTESIAN_POINT('Ctrl Pts',(-112.918344033683,2.20026185944183,
126.403583639103));
#101869=CARTESIAN_POINT('Ctrl Pts',(-112.926104476197,2.07674312200999,
126.343972840666));
#101870=CARTESIAN_POINT('Ctrl Pts',(-112.933864918712,1.95108814563578,
126.289669253756));
#101871=CARTESIAN_POINT('Ctrl Pts',(-112.941637818977,1.82523145673838,
126.235278493908));
#101872=CARTESIAN_POINT('Ctrl Pts',(-112.949410719243,1.69723204137605,
126.186212110499));
#101873=CARTESIAN_POINT('Ctrl Pts',(-112.957183619508,1.5675842351478,126.142616016216));
#101874=CARTESIAN_POINT('Ctrl Pts',(-112.96467395527,1.44264945324328,126.100604749773));
#101875=CARTESIAN_POINT('Ctrl Pts',(-112.972164291032,1.31618434175386,
126.063673046184));
#101876=CARTESIAN_POINT('Ctrl Pts',(-112.979654626793,1.18863949133075,
126.031906403836));
#101877=CARTESIAN_POINT('Ctrl Pts',(-112.987428960912,1.05625873913458,
125.998935319588));
#101878=CARTESIAN_POINT('Ctrl Pts',(-112.995203295031,0.922295412699854,
125.971424252312));
#101879=CARTESIAN_POINT('Ctrl Pts',(-113.00297762915,0.787239634307942,
125.949524181529));
#101880=CARTESIAN_POINT('Ctrl Pts',(-113.010742382097,0.652350300092618,
125.927651100625));
#101881=CARTESIAN_POINT('Ctrl Pts',(-113.018507135045,0.516371574973577,
125.9113753193));
#101882=CARTESIAN_POINT('Ctrl Pts',(-113.026271887992,0.379807364250885,
125.900797685517));
#101883=CARTESIAN_POINT('Ctrl Pts',(-113.034028928876,0.243378791027502,
125.89023055759));
#101884=CARTESIAN_POINT('Ctrl Pts',(-113.041785969761,0.106366276712021,
125.885350344579));
#101885=CARTESIAN_POINT('Ctrl Pts',(-113.049543010646,-0.0307178397643694,
125.886206545476));
#101886=CARTESIAN_POINT('Ctrl Pts',(-113.057294201886,-0.167698580042352,
125.887062100704));
#101887=CARTESIAN_POINT('Ctrl Pts',(-113.065045393126,-0.304750425630313,
125.893645457017));
#101888=CARTESIAN_POINT('Ctrl Pts',(-113.072796584367,-0.441358053805133,
125.905954128631));
#101889=CARTESIAN_POINT('Ctrl Pts',(-113.080544481144,-0.577907620093665,
125.918257568732));
#101890=CARTESIAN_POINT('Ctrl Pts',(-113.08829237792,-0.714012955913745,
125.936281449252));
#101891=CARTESIAN_POINT('Ctrl Pts',(-113.096040274698,-0.849161103153265,
125.959971235674));
#101892=CARTESIAN_POINT('Ctrl Pts',(-113.103786550782,-0.984280980313839,
125.983656066702));
#101893=CARTESIAN_POINT('Ctrl Pts',(-113.111532826866,-1.11844368229896,
126.013004378774));
#101894=CARTESIAN_POINT('Ctrl Pts',(-113.11927910295,-1.25114411617696,
126.047910106622));
#101895=CARTESIAN_POINT('Ctrl Pts',(-113.127025436215,-1.3838455296196,
126.082816092137));
#101896=CARTESIAN_POINT('Ctrl Pts',(-113.13477176948,-1.51508427531289,
126.123279475832));
#101897=CARTESIAN_POINT('Ctrl Pts',(-113.142518102746,-1.64436853711358,
126.169143775103));
#101898=CARTESIAN_POINT('Ctrl Pts',(-113.150266170748,-1.77368175122813,
126.215018345366));
#101899=CARTESIAN_POINT('Ctrl Pts',(-113.158014238751,-1.90103924209585,
126.266296107275));
#101900=CARTESIAN_POINT('Ctrl Pts',(-113.165762306754,-2.02596772888285,
126.322771856421));
#101901=CARTESIAN_POINT('Ctrl Pts',(-113.173518609496,-2.15102899115244,
126.379307628665));
#101902=CARTESIAN_POINT('Ctrl Pts',(-113.181274912238,-2.2736557355464,
126.441052262588));
#101903=CARTESIAN_POINT('Ctrl Pts',(-113.18903121498,-2.39339742740489,
126.5077536054));
#101904=CARTESIAN_POINT('Ctrl Pts',(-113.196791657494,-2.51320302900968,
126.574490548727));
#101905=CARTESIAN_POINT('Ctrl Pts',(-113.204552100008,-2.63012017669485,
126.646189268129));
#101906=CARTESIAN_POINT('Ctrl Pts',(-113.212312542522,-2.7437269063421,
126.722553943321));
#101907=CARTESIAN_POINT('Ctrl Pts',(-113.220085442787,-2.85751600759731,
126.799041205868));
#101908=CARTESIAN_POINT('Ctrl Pts',(-113.227858343053,-2.96798375615356,
126.880209160397));
#101909=CARTESIAN_POINT('Ctrl Pts',(-113.235631243318,-3.07474019106907,
126.965720777737));
#101910=CARTESIAN_POINT('Ctrl Pts',(-113.243121579081,-3.17761576068258,
127.048123832404));
#101911=CARTESIAN_POINT('Ctrl Pts',(-113.250611914843,-3.27704493072714,
127.134560024491));
#101912=CARTESIAN_POINT('Ctrl Pts',(-113.258102250606,-3.37271221373376,
127.224696473288));
#101913=CARTESIAN_POINT('Ctrl Pts',(-113.265759968658,-3.47051731930888,
127.316847150235));
#101914=CARTESIAN_POINT('Ctrl Pts',(-113.27341768671,-3.56471992965631,
127.413176237924));
#101915=CARTESIAN_POINT('Ctrl Pts',(-113.281075404762,-3.6549337278169,
127.513366465677));
#101916=CARTESIAN_POINT('Ctrl Pts',(-113.288724239367,-3.74504287215535,
127.613440466307));
#101917=CARTESIAN_POINT('Ctrl Pts',(-113.296373073973,-3.83117213571676,
127.717366406469));
#101918=CARTESIAN_POINT('Ctrl Pts',(-113.304021908578,-3.912969308254,127.824787786578));
#101919=CARTESIAN_POINT('Ctrl Pts',(-113.311663643837,-3.99469055988334,
127.932109462401));
#101920=CARTESIAN_POINT('Ctrl Pts',(-113.319305379096,-4.07208747274599,
128.0429198084));
#101921=CARTESIAN_POINT('Ctrl Pts',(-113.326947114355,-4.14484606607501,
128.156827019849));
#101922=CARTESIAN_POINT('Ctrl Pts',(-113.334583466117,-4.21755340197961,
128.27065398524));
#101923=CARTESIAN_POINT('Ctrl Pts',(-113.342219817878,-4.28562870190555,
128.38757313751));
#101924=CARTESIAN_POINT('Ctrl Pts',(-113.34985616964,-4.34879987894162,
128.50716174167));
#101925=CARTESIAN_POINT('Ctrl Pts',(-113.357489249431,-4.41194398882871,
128.626699105333));
#101926=CARTESIAN_POINT('Ctrl Pts',(-113.365122329222,-4.47018796774985,
128.748903289383));
#101927=CARTESIAN_POINT('Ctrl Pts',(-113.372755409012,-4.52330473628331,
128.873325318765));
#101928=CARTESIAN_POINT('Ctrl Pts',(-113.38038866589,-4.57642273712397,
128.997750234733));
#101929=CARTESIAN_POINT('Ctrl Pts',(-113.388021922768,-4.62441312113937,
129.124392732159));
#101930=CARTESIAN_POINT('Ctrl Pts',(-113.395655179646,-4.66709630748311,
129.252782350389));
#101931=CARTESIAN_POINT('Ctrl Pts',(-113.402120662988,-4.70324960806195,
129.361530287379));
#101932=CARTESIAN_POINT('Ctrl Pts',(-113.40858614633,-4.73559611044108,
129.47153118025));
#101933=CARTESIAN_POINT('Ctrl Pts',(-113.415051629673,-4.76405452823414,
129.582490119309));
#101934=CARTESIAN_POINT('Ctrl Pts',(-111.665402883959,-4.76405452823392,
129.582490119308));
#101935=CARTESIAN_POINT('Ctrl Pts',(-111.673434994141,-4.7993264617604,
129.720014852801));
#101936=CARTESIAN_POINT('Ctrl Pts',(-111.681467104322,-4.82867233280825,
129.859196828031));
#101937=CARTESIAN_POINT('Ctrl Pts',(-111.689499214503,-4.8519470411507,
129.99950474701));
#101938=CARTESIAN_POINT('Ctrl Pts',(-111.697520736002,-4.87519106658524,
130.139627698904));
#101939=CARTESIAN_POINT('Ctrl Pts',(-111.705542257501,-4.89237982900867,
130.280873292029));
#101940=CARTESIAN_POINT('Ctrl Pts',(-111.713563779,-4.90341893425279,130.422698702108));
#101941=CARTESIAN_POINT('Ctrl Pts',(-111.72075604067,-4.91331682376556,
130.549862290824));
#101942=CARTESIAN_POINT('Ctrl Pts',(-111.72794830234,-4.91827145356775,
130.677491661371));
#101943=CARTESIAN_POINT('Ctrl Pts',(-111.73514056401,-4.91824993013883,
130.805189586421));
#101944=CARTESIAN_POINT('',(-111.389859436035,-4.91824793280489,130.799851298284));
#101945=CARTESIAN_POINT('Ctrl Pts',(-111.319883193423,-4.764054528234,129.582490119308));
#101946=CARTESIAN_POINT('Ctrl Pts',(-111.322774755641,-4.77667488993176,
129.631696718027));
#101947=CARTESIAN_POINT('Ctrl Pts',(-111.325666317859,-4.78852586105957,
129.681071769191));
#101948=CARTESIAN_POINT('Ctrl Pts',(-111.328557880076,-4.79960393518158,
129.730589167075));
#101949=CARTESIAN_POINT('Ctrl Pts',(-111.33921170086,-4.84042056212739,
129.913033618565));
#101950=CARTESIAN_POINT('Ctrl Pts',(-111.349865521643,-4.87084727414698,
130.097880784251));
#101951=CARTESIAN_POINT('Ctrl Pts',(-111.360519342427,-4.89065949885459,
130.284136888039));
#101952=CARTESIAN_POINT('Ctrl Pts',(-111.370299373615,-4.90884679329887,
130.455116909294));
#101953=CARTESIAN_POINT('Ctrl Pts',(-111.380079404804,-4.91808971405691,
130.627284475731));
#101954=CARTESIAN_POINT('Ctrl Pts',(-111.389859435992,-4.9182479328042,
130.799851297532));
#101955=CARTESIAN_POINT('Ctrl Pts',(-111.389859436035,-4.91824793280489,
130.799851298284));
#101956=CARTESIAN_POINT('Ctrl Pts',(-111.397511849573,-4.91837173149822,
130.934876704435));
#101957=CARTESIAN_POINT('Ctrl Pts',(-111.405164263111,-4.91293087685927,
131.070069265922));
#101958=CARTESIAN_POINT('Ctrl Pts',(-111.412816676649,-4.90191088279818,
131.204926167264));
#101959=CARTESIAN_POINT('Ctrl Pts',(-111.420463247981,-4.89089930190938,
131.33968011262));
#101960=CARTESIAN_POINT('Ctrl Pts',(-111.428109819313,-4.87431708776526,
131.47409850816));
#101961=CARTESIAN_POINT('Ctrl Pts',(-111.435756390646,-4.8522018223889,
131.6076790708));
#101962=CARTESIAN_POINT('Ctrl Pts',(-111.443399754411,-4.83009583387479,
131.741203599363));
#101963=CARTESIAN_POINT('Ctrl Pts',(-111.451043118177,-4.80246147333269,
131.87389059729));
#101964=CARTESIAN_POINT('Ctrl Pts',(-111.458686481942,-4.76938807451487,
132.005243816372));
#101965=CARTESIAN_POINT('Ctrl Pts',(-111.466328398073,-4.73632093972174,
132.136572157461));
#101966=CARTESIAN_POINT('Ctrl Pts',(-111.473970314203,-4.69781691292974,
132.266566831726));
#101967=CARTESIAN_POINT('Ctrl Pts',(-111.481612230333,-4.65401613678662,
132.394743232231));
#101968=CARTESIAN_POINT('Ctrl Pts',(-111.489254459609,-4.61021356580659,
132.522924885058));
#101969=CARTESIAN_POINT('Ctrl Pts',(-111.496896688884,-4.56111394432089,
132.64928773508));
#101970=CARTESIAN_POINT('Ctrl Pts',(-111.504538918159,-4.50690665855051,
132.773364282777));
#101971=CARTESIAN_POINT('Ctrl Pts',(-111.512183221394,-4.45268466192745,
132.897474502548));
#101972=CARTESIAN_POINT('Ctrl Pts',(-111.519827524629,-4.39335240615422,
133.019296817625));
#101973=CARTESIAN_POINT('Ctrl Pts',(-111.527471827863,-4.32914635320659,
133.138386091938));
#101974=CARTESIAN_POINT('Ctrl Pts',(-111.535124225635,-4.26487231259977,
133.257601469643));
#101975=CARTESIAN_POINT('Ctrl Pts',(-111.542776623407,-4.19571436395245,
133.374077675035));
#101976=CARTESIAN_POINT('Ctrl Pts',(-111.550429021179,-4.12195378371499,
133.487396224377));
#101977=CARTESIAN_POINT('Ctrl Pts',(-111.558086021216,-4.04814884277513,
133.600782925169));
#101978=CARTESIAN_POINT('Ctrl Pts',(-111.565743021253,-3.9697359927938,
133.711007862496));
#101979=CARTESIAN_POINT('Ctrl Pts',(-111.57340002129,-3.88703752267745,
133.817684755424));
#101980=CARTESIAN_POINT('Ctrl Pts',(-111.581068124949,-3.80421912927281,
133.924516343399));
#101981=CARTESIAN_POINT('Ctrl Pts',(-111.588736228609,-3.71710296951947,
134.027789310629));
#101982=CARTESIAN_POINT('Ctrl Pts',(-111.596404332269,-3.62604920045386,
134.12715315674));
#101983=CARTESIAN_POINT('Ctrl Pts',(-111.599938056142,-3.58408851606613,
134.172943408247));
#101984=CARTESIAN_POINT('Ctrl Pts',(-111.603471780016,-3.54129208983065,
134.217904034757));
#101985=CARTESIAN_POINT('Ctrl Pts',(-111.607005503889,-3.49769749589534,
134.262003642765));
#101986=CARTESIAN_POINT('Ctrl Pts',(-111.614779838008,-3.40178764238884,
134.359024547467));
#101987=CARTESIAN_POINT('Ctrl Pts',(-111.622554172128,-3.30168599275238,
134.452205507928));
#101988=CARTESIAN_POINT('Ctrl Pts',(-111.630328506247,-3.19773260301129,
134.541162627593));
#101989=CARTESIAN_POINT('Ctrl Pts',(-111.638093259194,-3.09390732653218,
134.630010115558));
#101990=CARTESIAN_POINT('Ctrl Pts',(-111.645858012141,-2.98624004911221,
134.714643868376));
#101991=CARTESIAN_POINT('Ctrl Pts',(-111.653622765088,-2.8751086756547,
134.794715635064));
#101992=CARTESIAN_POINT('Ctrl Pts',(-111.661379805973,-2.76408767944398,
134.874707873345));
#101993=CARTESIAN_POINT('Ctrl Pts',(-111.669136846858,-2.64960974927478,
134.950146915377));
#101994=CARTESIAN_POINT('Ctrl Pts',(-111.676893887743,-2.53208670352203,
135.020723978135));
#101995=CARTESIAN_POINT('Ctrl Pts',(-111.684645078983,-2.41465228281275,
135.09124781818));
#101996=CARTESIAN_POINT('Ctrl Pts',(-111.692396270223,-2.29417765107022,
135.156916776342));
#101997=CARTESIAN_POINT('Ctrl Pts',(-111.700147461463,-2.17110421639548,
135.217464915455));
#101998=CARTESIAN_POINT('Ctrl Pts',(-111.70789535824,-2.04808309121306,
135.277987319994));
#101999=CARTESIAN_POINT('Ctrl Pts',(-111.715643255017,-1.9224657100605,
135.33339306212));
#102000=CARTESIAN_POINT('Ctrl Pts',(-111.723391151794,-1.79471853619688,
135.383461887284));
#102001=CARTESIAN_POINT('Ctrl Pts',(-111.731137427878,-1.66699808428811,
135.433520239129));
#102002=CARTESIAN_POINT('Ctrl Pts',(-111.738883703962,-1.53714908958031,
135.478243751951));
#102003=CARTESIAN_POINT('Ctrl Pts',(-111.746629980046,-1.40565810324164,
135.517460272707));
#102004=CARTESIAN_POINT('Ctrl Pts',(-111.754376313312,-1.27416614626692,
135.55667708295));
#102005=CARTESIAN_POINT('Ctrl Pts',(-111.762122646577,-1.14103254813241,
135.59038670827));
#102006=CARTESIAN_POINT('Ctrl Pts',(-111.769868979842,-1.00675874692166,
135.618466961219));
#102007=CARTESIAN_POINT('Ctrl Pts',(-111.777617047845,-0.872454876023937,
135.646553502545));
#102008=CARTESIAN_POINT('Ctrl Pts',(-111.785365115848,-0.737010676565102,
135.669008082921));
#102009=CARTESIAN_POINT('Ctrl Pts',(-111.793113183851,-0.600937100485652,
135.685759767785));
#102010=CARTESIAN_POINT('Ctrl Pts',(-111.800869486593,-0.464718903790064,
135.70252925654));
#102011=CARTESIAN_POINT('Ctrl Pts',(-111.808625789335,-0.327870382910718,
135.713583694226));
#102012=CARTESIAN_POINT('Ctrl Pts',(-111.816382092077,-0.190907484828074,
135.718904074972));
#102013=CARTESIAN_POINT('Ctrl Pts',(-111.824142534591,-0.0538714855224776,
135.724227295366));
#102014=CARTESIAN_POINT('Ctrl Pts',(-111.831902977105,0.0832786218547538,
135.723810361824));
#102015=CARTESIAN_POINT('Ctrl Pts',(-111.839663419619,0.220028576276249,
135.717686424809));
#102016=CARTESIAN_POINT('Ctrl Pts',(-111.847436319885,0.356998053864299,
135.711552657107));
#102017=CARTESIAN_POINT('Ctrl Pts',(-111.85520922015,0.493565705130944,
135.6996936124));
#102018=CARTESIAN_POINT('Ctrl Pts',(-111.862982120415,0.629223165585064,
135.682194283282));
#102019=CARTESIAN_POINT('Ctrl Pts',(-111.870472456177,0.75994913565005,
135.665331098855));
#102020=CARTESIAN_POINT('Ctrl Pts',(-111.877962791939,0.889829637803004,
135.643230639237));
#102021=CARTESIAN_POINT('Ctrl Pts',(-111.885453127701,1.01842207009617,
135.61601309355));
#102022=CARTESIAN_POINT('Ctrl Pts',(-111.89322746182,1.15189012354551,135.587763586345));
#102023=CARTESIAN_POINT('Ctrl Pts',(-111.901001795939,1.28439329135057,
135.553911818681));
#102024=CARTESIAN_POINT('Ctrl Pts',(-111.908776130058,1.41542478187872,
135.514536383856));
#102025=CARTESIAN_POINT('Ctrl Pts',(-111.916540883005,1.54629478780541,
135.475209475735));
#102026=CARTESIAN_POINT('Ctrl Pts',(-111.924305635952,1.67569635436854,
135.430372556639));
#102027=CARTESIAN_POINT('Ctrl Pts',(-111.9320703889,1.803132221322,135.380155330502));
#102028=CARTESIAN_POINT('Ctrl Pts',(-111.939827429785,1.93044151717586,
135.329987980822));
#102029=CARTESIAN_POINT('Ctrl Pts',(-111.94758447067,2.05578863731693,135.274451100906));
#102030=CARTESIAN_POINT('Ctrl Pts',(-111.955341511555,2.17869119595031,
135.21372426045));
#102031=CARTESIAN_POINT('Ctrl Pts',(-111.963092702795,2.30150107280869,
135.153043214577));
#102032=CARTESIAN_POINT('Ctrl Pts',(-111.970843894035,2.42186970836619,
135.087180170813));
#102033=CARTESIAN_POINT('Ctrl Pts',(-111.978595085275,2.53933477029247,
135.016362752761));
#102034=CARTESIAN_POINT('Ctrl Pts',(-111.986342982052,2.65674990643348,
134.945575434001));
#102035=CARTESIAN_POINT('Ctrl Pts',(-111.994090878829,2.77126358934399,
134.869838130548));
#102036=CARTESIAN_POINT('Ctrl Pts',(-112.001838775606,2.88243837784815,
134.789424238188));
#102037=CARTESIAN_POINT('Ctrl Pts',(-112.00958505169,2.99358991098321,134.709027166682));
#102038=CARTESIAN_POINT('Ctrl Pts',(-112.017331327775,3.10140362233403,
134.623955681033));
#102039=CARTESIAN_POINT('Ctrl Pts',(-112.025077603859,3.20547168187723,
134.534526077594));
#102040=CARTESIAN_POINT('Ctrl Pts',(-112.032823937124,3.30954050962734,
134.445095814005));
#102041=CARTESIAN_POINT('Ctrl Pts',(-112.04057027039,3.40986333387604,134.351307623244));
#102042=CARTESIAN_POINT('Ctrl Pts',(-112.048316603655,3.50606631533044,
134.25351733407));
#102043=CARTESIAN_POINT('Ctrl Pts',(-112.056064671658,3.60229084077539,
134.155705145439));
#102044=CARTESIAN_POINT('Ctrl Pts',(-112.063812739661,3.69439341340803,
134.053889353632));
#102045=CARTESIAN_POINT('Ctrl Pts',(-112.071560807664,3.78203817196968,
133.948461495125));
#102046=CARTESIAN_POINT('Ctrl Pts',(-112.079317110406,3.86977608042383,
133.842921586634));
#102047=CARTESIAN_POINT('Ctrl Pts',(-112.087073413148,3.95304646017374,
133.733762243856));
#102048=CARTESIAN_POINT('Ctrl Pts',(-112.094829715889,4.0315544390951,133.621407274459));
#102049=CARTESIAN_POINT('Ctrl Pts',(-112.102590158404,4.11010432008863,
133.508992337832));
#102050=CARTESIAN_POINT('Ctrl Pts',(-112.110350600918,4.18388652520632,
133.393378705439));
#102051=CARTESIAN_POINT('Ctrl Pts',(-112.118111043432,4.25265097422479,
133.275016958283));
#102052=CARTESIAN_POINT('Ctrl Pts',(-112.125883943697,4.32152581004145,
133.156465206342));
#102053=CARTESIAN_POINT('Ctrl Pts',(-112.133656843963,4.38536661122429,
133.035156870198));
#102054=CARTESIAN_POINT('Ctrl Pts',(-112.141429744228,4.44397010102323,
132.911565591865));
#102055=CARTESIAN_POINT('Ctrl Pts',(-112.148920079991,4.50044320635454,
132.792467167808));
#102056=CARTESIAN_POINT('Ctrl Pts',(-112.156410415752,4.55205304768174,
132.671249184682));
#102057=CARTESIAN_POINT('Ctrl Pts',(-112.163900751514,4.59866150635386,
132.548348981197));
#102058=CARTESIAN_POINT('Ctrl Pts',(-112.171675085634,4.64703713890294,
132.420788979141));
#102059=CARTESIAN_POINT('Ctrl Pts',(-112.179449419753,4.69017788680332,
132.291012604084));
#102060=CARTESIAN_POINT('Ctrl Pts',(-112.187223753872,4.72787593956728,
132.159488715777));
#102061=CARTESIAN_POINT('Ctrl Pts',(-112.194988506819,4.76552753285039,
132.028126918907));
#102062=CARTESIAN_POINT('Ctrl Pts',(-112.202753259766,4.7977496705034,131.895022266141));
#102063=CARTESIAN_POINT('Ctrl Pts',(-112.210518012713,4.82438269481104,
131.76066322475));
#102064=CARTESIAN_POINT('Ctrl Pts',(-112.218275053598,4.85098926682348,
131.626437630654));
#102065=CARTESIAN_POINT('Ctrl Pts',(-112.226032094483,4.87201769707431,
131.490960508307));
#102066=CARTESIAN_POINT('Ctrl Pts',(-112.233789135368,4.88735832132833,
131.354734764345));
#102067=CARTESIAN_POINT('Ctrl Pts',(-112.241540326608,4.90268737709833,
131.218611749276));
#102068=CARTESIAN_POINT('Ctrl Pts',(-112.249291517848,4.91233712072752,
131.081741623216));
#102069=CARTESIAN_POINT('Ctrl Pts',(-112.257042709088,4.91624915648167,
130.944636395565));
#102070=CARTESIAN_POINT('Ctrl Pts',(-112.264790605866,4.92015952951625,
130.807589441294));
#102071=CARTESIAN_POINT('Ctrl Pts',(-112.272538502643,4.91833703389468,
130.670307974163));
#102072=CARTESIAN_POINT('Ctrl Pts',(-112.28028639942,4.91077523759472,130.533307802922));
#102073=CARTESIAN_POINT('Ctrl Pts',(-112.288032675504,4.90321502305955,
130.396336289164));
#102074=CARTESIAN_POINT('Ctrl Pts',(-112.295778951588,4.88991791731495,
130.259646344382));
#102075=CARTESIAN_POINT('Ctrl Pts',(-112.303525227672,4.87092958735024,
130.123752053429));
#102076=CARTESIAN_POINT('Ctrl Pts',(-112.311271560937,4.85194111721796,
129.987856759336));
#102077=CARTESIAN_POINT('Ctrl Pts',(-112.319017894203,4.82726139313845,
129.852757517995));
#102078=CARTESIAN_POINT('Ctrl Pts',(-112.326764227468,4.79698771465657,
129.718961185129));
#102079=CARTESIAN_POINT('Ctrl Pts',(-112.334512295471,4.76670725659434,
129.585134889502));
#102080=CARTESIAN_POINT('Ctrl Pts',(-112.342260363474,4.73083043761234,
129.452612464206));
#102081=CARTESIAN_POINT('Ctrl Pts',(-112.350008431477,4.6895051272227,129.321888113857));
#102082=CARTESIAN_POINT('Ctrl Pts',(-112.357764734218,4.64813589580133,
129.191024828114));
#102083=CARTESIAN_POINT('Ctrl Pts',(-112.36552103696,4.60130672341606,129.061963808154));
#102084=CARTESIAN_POINT('Ctrl Pts',(-112.373277339702,4.54921478587561,
128.935182216645));
#102085=CARTESIAN_POINT('Ctrl Pts',(-112.381037782216,4.49709504529965,
128.808332957983));
#102086=CARTESIAN_POINT('Ctrl Pts',(-112.38879822473,4.43970710611637,128.683765906868));
#102087=CARTESIAN_POINT('Ctrl Pts',(-112.396558667245,4.3772948804146,128.561935012915));
#102088=CARTESIAN_POINT('Ctrl Pts',(-112.40433156751,4.31478246506725,128.439908545194));
#102089=CARTESIAN_POINT('Ctrl Pts',(-112.412104467775,4.24722983867589,
128.320627352286));
#102090=CARTESIAN_POINT('Ctrl Pts',(-112.419877368041,4.17492561363418,
128.204518471758));
#102091=CARTESIAN_POINT('Ctrl Pts',(-112.427367703803,4.1052498292953,128.092630441496));
#102092=CARTESIAN_POINT('Ctrl Pts',(-112.434858039565,4.03116208689624,
127.983688339525));
#102093=CARTESIAN_POINT('Ctrl Pts',(-112.442348375327,3.9529556753756,127.878044761235));
#102094=CARTESIAN_POINT('Ctrl Pts',(-112.450122709446,3.87178404399286,
127.768395674565));
#102095=CARTESIAN_POINT('Ctrl Pts',(-112.457897043565,3.78591813221081,
127.661952840864));
#102096=CARTESIAN_POINT('Ctrl Pts',(-112.465671377684,3.69564007837278,
127.55914452713));
#102097=CARTESIAN_POINT('Ctrl Pts',(-112.473436130632,3.60547328416748,
127.456462915454));
#102098=CARTESIAN_POINT('Ctrl Pts',(-112.481200883579,3.51090542254593,
127.357407202385));
#102099=CARTESIAN_POINT('Ctrl Pts',(-112.488965636526,3.41226115596433,
127.262375740975));
#102100=CARTESIAN_POINT('Ctrl Pts',(-112.496722677411,3.31371486425921,
127.167438666153));
#102101=CARTESIAN_POINT('Ctrl Pts',(-112.504479718296,3.21110050451521,
127.076518158385));
#102102=CARTESIAN_POINT('Ctrl Pts',(-112.512236759181,3.10478191013158,
126.989978314621));
#102103=CARTESIAN_POINT('Ctrl Pts',(-112.519987950421,2.99854349142686,
126.903503731226));
#102104=CARTESIAN_POINT('Ctrl Pts',(-112.527739141661,2.88860670014902,
126.821403482242));
#102105=CARTESIAN_POINT('Ctrl Pts',(-112.535490332901,2.77537073998687,
126.744003451241));
#102106=CARTESIAN_POINT('Ctrl Pts',(-112.543238229678,2.66218290812861,
126.666636317318));
#102107=CARTESIAN_POINT('Ctrl Pts',(-112.550986126455,2.54569901841734,
126.59396564823));
#102108=CARTESIAN_POINT('Ctrl Pts',(-112.558734023232,2.42634955869867,
126.526275662647));
#102109=CARTESIAN_POINT('Ctrl Pts',(-112.566480299317,2.30702506431409,
126.45859983635));
#102110=CARTESIAN_POINT('Ctrl Pts',(-112.574226575401,2.18483653205361,
126.395902814015));
#102111=CARTESIAN_POINT('Ctrl Pts',(-112.581972851485,2.06024116018702,
126.338424050129));
#102112=CARTESIAN_POINT('Ctrl Pts',(-112.58971918475,1.93564486858553,126.280944861948));
#102113=CARTESIAN_POINT('Ctrl Pts',(-112.597465518016,1.80864205693524,
126.228684172855));
#102114=CARTESIAN_POINT('Ctrl Pts',(-112.605211851281,1.6797117500904,126.181834089886));
#102115=CARTESIAN_POINT('Ctrl Pts',(-112.612959919284,1.55075257019676,
126.134973515165));
#102116=CARTESIAN_POINT('Ctrl Pts',(-112.620707987287,1.41986540356366,
126.093526091145));
#102117=CARTESIAN_POINT('Ctrl Pts',(-112.62845605529,1.28754596561625,126.057634540687));
#102118=CARTESIAN_POINT('Ctrl Pts',(-112.636212358032,1.1550858969961,126.021704844261));
#102119=CARTESIAN_POINT('Ctrl Pts',(-112.643968660774,1.02119089416524,
125.991342919481));
#102120=CARTESIAN_POINT('Ctrl Pts',(-112.651724963516,0.886368985929803,
125.966640794831));
#102121=CARTESIAN_POINT('Ctrl Pts',(-112.65948540603,0.751475119182901,
125.941925485913));
#102122=CARTESIAN_POINT('Ctrl Pts',(-112.667245848544,0.615653748251519,
125.922876050613));
#102123=CARTESIAN_POINT('Ctrl Pts',(-112.675006291058,0.479418634242783,
125.909532649635));
#102124=CARTESIAN_POINT('Ctrl Pts',(-112.682779191323,0.342964823534284,
125.896167828645));
#102125=CARTESIAN_POINT('Ctrl Pts',(-112.690552091589,0.206096333093022,
125.888527368046));
#102126=CARTESIAN_POINT('Ctrl Pts',(-112.698324991854,0.0693284437661364,
125.886599274294));
#102127=CARTESIAN_POINT('Ctrl Pts',(-112.705815327616,-0.0624675882854512,
125.884741271605));
#102128=CARTESIAN_POINT('Ctrl Pts',(-112.713305663378,-0.194169898531983,
125.888187520386));
#102129=CARTESIAN_POINT('Ctrl Pts',(-112.72079599914,-0.325323308651908,
125.896881854765));
#102130=CARTESIAN_POINT('Ctrl Pts',(-112.728570333259,-0.461449440179959,
125.905905837474));
#102131=CARTESIAN_POINT('Ctrl Pts',(-112.736344667379,-0.597415433499299,
125.920612309279));
#102132=CARTESIAN_POINT('Ctrl Pts',(-112.744119001498,-0.732708472789882,
125.940995387974));
#102133=CARTESIAN_POINT('Ctrl Pts',(-112.751883754445,-0.867834775501393,
125.961353346347));
#102134=CARTESIAN_POINT('Ctrl Pts',(-112.759648507392,-1.00228939146386,
125.987373934146));
#102135=CARTESIAN_POINT('Ctrl Pts',(-112.767413260339,-1.1355616869862,
126.018999323207));
#102136=CARTESIAN_POINT('Ctrl Pts',(-112.775170301224,-1.26870161458509,
126.050593301486));
#102137=CARTESIAN_POINT('Ctrl Pts',(-112.782927342109,-1.40066118070857,
126.087780913222));
#102138=CARTESIAN_POINT('Ctrl Pts',(-112.790684382994,-1.53093739944265,
126.130452858368));
#102139=CARTESIAN_POINT('Ctrl Pts',(-112.798435574234,-1.66111537586696,
126.173092624269));
#102140=CARTESIAN_POINT('Ctrl Pts',(-112.806186765474,-1.78961216157762,
126.221208370356));
#102141=CARTESIAN_POINT('Ctrl Pts',(-112.813937956714,-1.91593780215059,
126.274640383292));
#102142=CARTESIAN_POINT('Ctrl Pts',(-112.821685853491,-2.04220975095664,
126.328049686197));
#102143=CARTESIAN_POINT('Ctrl Pts',(-112.829433750268,-2.16631203066705,
126.386770609884));
#102144=CARTESIAN_POINT('Ctrl Pts',(-112.837181647045,-2.28777283086798,
126.45059459987));
#102145=CARTESIAN_POINT('Ctrl Pts',(-112.844927923129,-2.40920822408822,
126.514405239254));
#102146=CARTESIAN_POINT('Ctrl Pts',(-112.852674199213,-2.52800289095891,
126.583316639971));
#102147=CARTESIAN_POINT('Ctrl Pts',(-112.860420475298,-2.64370824480431,
126.657073579169));
#102148=CARTESIAN_POINT('Ctrl Pts',(-112.868166808563,-2.7594144527605,
126.730831062825));
#102149=CARTESIAN_POINT('Ctrl Pts',(-112.875913141828,-2.87203097250722,
126.809433946179));
#102150=CARTESIAN_POINT('Ctrl Pts',(-112.883659475094,-2.98113725432025,
126.892583050602));
#102151=CARTESIAN_POINT('Ctrl Pts',(-112.891407543096,-3.09026796972756,
126.975750775689));
#102152=CARTESIAN_POINT('Ctrl Pts',(-112.899155611099,-3.19588657206786,
127.063466510801));
#102153=CARTESIAN_POINT('Ctrl Pts',(-112.906903679102,-3.29760503826166,
127.155390341703));
#102154=CARTESIAN_POINT('Ctrl Pts',(-112.914659981844,-3.39943161205249,
127.247411870347));
#102155=CARTESIAN_POINT('Ctrl Pts',(-112.922416284586,-3.49734947886164,
127.343650166357));
#102156=CARTESIAN_POINT('Ctrl Pts',(-112.930172587328,-3.59100661053982,
127.443727554353));
#102157=CARTESIAN_POINT('Ctrl Pts',(-112.937933029842,-3.68471372984914,
127.543858356665));
#102158=CARTESIAN_POINT('Ctrl Pts',(-112.945693472356,-3.77415532788571,
127.647832037602));
#102159=CARTESIAN_POINT('Ctrl Pts',(-112.95345391487,-3.85901991588287,
127.755238063237));
#102160=CARTESIAN_POINT('Ctrl Pts',(-112.961226815136,-3.94402073605061,
127.862816506559));
#102161=CARTESIAN_POINT('Ctrl Pts',(-112.968999715401,-4.02442963422371,
127.973837988302));
#102162=CARTESIAN_POINT('Ctrl Pts',(-112.976772615666,-4.09997817902724,
128.08786250529));
#102163=CARTESIAN_POINT('Ctrl Pts',(-112.984262951429,-4.17278034393452,
128.197741943879));
#102164=CARTESIAN_POINT('Ctrl Pts',(-112.991753287191,-4.2410692329316,
128.310409609142));
#102165=CARTESIAN_POINT('Ctrl Pts',(-112.999243622953,-4.30464606495475,
128.425452187641));
#102166=CARTESIAN_POINT('Ctrl Pts',(-113.007400604759,-4.37388128731284,
128.550733650235));
#102167=CARTESIAN_POINT('Ctrl Pts',(-113.015557586564,-4.43772995529178,
128.679196150845));
#102168=CARTESIAN_POINT('Ctrl Pts',(-113.023714568369,-4.4959031403072,
128.810360112181));
#102169=CARTESIAN_POINT('Ctrl Pts',(-113.031853641808,-4.55394860814338,
128.941236107659));
#102170=CARTESIAN_POINT('Ctrl Pts',(-113.039992715246,-4.60634329976436,
129.074801434836));
#102171=CARTESIAN_POINT('Ctrl Pts',(-113.048131788685,-4.65284395117964,
129.210551899912));
#102172=CARTESIAN_POINT('Ctrl Pts',(-113.055466453066,-4.69474880364021,
129.332885739058));
#102173=CARTESIAN_POINT('Ctrl Pts',(-113.062801117447,-4.7318675628499,
129.456993629781));
#102174=CARTESIAN_POINT('Ctrl Pts',(-113.070135781827,-4.76405452823415,
129.582490119309));
#102175=CARTESIAN_POINT('Origin',(213.235140564004,0.,130.804360617566));
#102176=CARTESIAN_POINT('',(-115.165057694931,-4.76405452823392,129.582490119308));
#102177=CARTESIAN_POINT('',(-114.819798430105,-4.76405452823404,129.582490119308));
#102178=CARTESIAN_POINT('',(213.235140564004,-4.76405452823405,129.582490119308));
#102179=CARTESIAN_POINT('',(-113.48514056397,-4.91824815323073,130.80862274644));
#102180=CARTESIAN_POINT('Ctrl Pts',(-113.48514056401,-4.91824815323012,
130.808622747144));
#102181=CARTESIAN_POINT('Ctrl Pts',(-113.496784765158,-4.91807033148742,
131.013818633735));
#102182=CARTESIAN_POINT('Ctrl Pts',(-113.508428966306,-4.90504783934739,
131.218479327865));
#102183=CARTESIAN_POINT('Ctrl Pts',(-113.520073167454,-4.87939893910603,
131.421328246823));
#102184=CARTESIAN_POINT('Ctrl Pts',(-113.525565403109,-4.86730108862862,
131.517006262955));
#102185=CARTESIAN_POINT('Ctrl Pts',(-113.531057638764,-4.85239479824405,
131.612281762984));
#102186=CARTESIAN_POINT('Ctrl Pts',(-113.536549874419,-4.83470616053732,
131.707023015012));
#102187=CARTESIAN_POINT('Ctrl Pts',(-113.544324208538,-4.80966765376402,
131.841130543242));
#102188=CARTESIAN_POINT('Ctrl Pts',(-113.552098542657,-4.77900534524811,
131.974407902494));
#102189=CARTESIAN_POINT('Ctrl Pts',(-113.559872876776,-4.74278564405443,
132.106346561058));
#102190=CARTESIAN_POINT('Ctrl Pts',(-113.567637629724,-4.70661058040543,
132.238122617017));
#102191=CARTESIAN_POINT('Ctrl Pts',(-113.575402382671,-4.66489185403184,
132.368562881557));
#102192=CARTESIAN_POINT('Ctrl Pts',(-113.583167135618,-4.61774719864245,
132.497167125094));
#102193=CARTESIAN_POINT('Ctrl Pts',(-113.590924176503,-4.57064936798941,
132.625643637084));
#102194=CARTESIAN_POINT('Ctrl Pts',(-113.598681217388,-4.51813646658613,
132.752287392338));
#102195=CARTESIAN_POINT('Ctrl Pts',(-113.606438258273,-4.4603764364867,
132.876611834802));
#102196=CARTESIAN_POINT('Ctrl Pts',(-113.614189449513,-4.40265996367536,
133.000842523235));
#102197=CARTESIAN_POINT('Ctrl Pts',(-113.621940640754,-4.33970440220091,
133.122757027046));
#102198=CARTESIAN_POINT('Ctrl Pts',(-113.629691831994,-4.27172621541472,
133.241887684706));
#102199=CARTESIAN_POINT('Ctrl Pts',(-113.637439728771,-4.2037769211712,
133.360967708658));
#102200=CARTESIAN_POINT('Ctrl Pts',(-113.645187625548,-4.13080944083047,
133.47726590091));
#102201=CARTESIAN_POINT('Ctrl Pts',(-113.652935522325,-4.05308659406606,
133.590338385514));
#102202=CARTESIAN_POINT('Ctrl Pts',(-113.66068179841,-3.97538000524546,
133.703387217792));
#102203=CARTESIAN_POINT('Ctrl Pts',(-113.668428074494,-3.89292024987878,
133.813211362547));
#102204=CARTESIAN_POINT('Ctrl Pts',(-113.676174350578,-3.80601374643623,
133.919395516959));
#102205=CARTESIAN_POINT('Ctrl Pts',(-113.683920683843,-3.71910660146973,
134.025580455199));
#102206=CARTESIAN_POINT('Ctrl Pts',(-113.691667017109,-3.62775289055038,
134.128125046929));
#102207=CARTESIAN_POINT('Ctrl Pts',(-113.699413350374,-3.53229936885708,
134.226647021605));
#102208=CARTESIAN_POINT('Ctrl Pts',(-113.707161418377,-3.43682447100954,
134.325191059594));
#102209=CARTESIAN_POINT('Ctrl Pts',(-113.71490948638,-3.33724820742209,
134.419710407228));
#102210=CARTESIAN_POINT('Ctrl Pts',(-113.722657554383,-3.23395394207395,
134.509859904173));
#102211=CARTESIAN_POINT('Ctrl Pts',(-113.730413857125,-3.13054989435124,
134.600105213076));
#102212=CARTESIAN_POINT('Ctrl Pts',(-113.738170159867,-3.023420246278,134.685971136255));
#102213=CARTESIAN_POINT('Ctrl Pts',(-113.745926462609,-2.91298160735896,
134.767152716287));
#102214=CARTESIAN_POINT('Ctrl Pts',(-113.753686905123,-2.80248402401307,
134.848377625373));
#102215=CARTESIAN_POINT('Ctrl Pts',(-113.761447347638,-2.6886742549717,
134.924912991434));
#102216=CARTESIAN_POINT('Ctrl Pts',(-113.769207790152,-2.57199675024481,
134.996497993563));
#102217=CARTESIAN_POINT('Ctrl Pts',(-113.776980690417,-2.45513194442919,
135.068197910292));
#102218=CARTESIAN_POINT('Ctrl Pts',(-113.784753590683,-2.33539054528691,
135.134931392485));
#102219=CARTESIAN_POINT('Ctrl Pts',(-113.792526490948,-2.21324118035538,
135.196483855828));
#102220=CARTESIAN_POINT('Ctrl Pts',(-113.80001682671,-2.09553225252669,
135.255798732081));
#102221=CARTESIAN_POINT('Ctrl Pts',(-113.807507162471,-1.97558767108321,
135.310302608404));
#102222=CARTESIAN_POINT('Ctrl Pts',(-113.814997498232,-1.85384133432574,
135.359846910998));
#102223=CARTESIAN_POINT('Ctrl Pts',(-113.822771832351,-1.7274789481942,
135.411269700888));
#102224=CARTESIAN_POINT('Ctrl Pts',(-113.83054616647,-1.5987752045239,135.457512300488));
#102225=CARTESIAN_POINT('Ctrl Pts',(-113.83832050059,-1.46819384116792,
135.498355707812));
#102226=CARTESIAN_POINT('Ctrl Pts',(-113.846085253537,-1.33777340767224,
135.539148779288));
#102227=CARTESIAN_POINT('Ctrl Pts',(-113.853850006484,-1.20548032821458,
135.574555782418));
#102228=CARTESIAN_POINT('Ctrl Pts',(-113.861614759431,-1.07179909805683,
135.604405383597));
#102229=CARTESIAN_POINT('Ctrl Pts',(-113.869371800316,-0.938250641981456,
135.634225337732));
#102230=CARTESIAN_POINT('Ctrl Pts',(-113.877128841201,-0.803317158042228,
135.6584987897));
#102231=CARTESIAN_POINT('Ctrl Pts',(-113.884885882086,-0.667498776412525,
135.677104038473));
#102232=CARTESIAN_POINT('Ctrl Pts',(-113.892637073326,-0.531782816481107,
135.695695256883));
#102233=CARTESIAN_POINT('Ctrl Pts',(-113.900388264566,-0.395183672876246,
135.708626727257));
#102234=CARTESIAN_POINT('Ctrl Pts',(-113.908139455806,-0.25821180621588,
135.715827783865));
#102235=CARTESIAN_POINT('Ctrl Pts',(-113.915887352583,-0.121298156252501,
135.723025779831));
#102236=CARTESIAN_POINT('Ctrl Pts',(-113.92363524936,0.0159875120779447,
135.724498185728));
#102237=CARTESIAN_POINT('Ctrl Pts',(-113.931383146137,0.153129692915351,
135.720226193398));
#102238=CARTESIAN_POINT('Ctrl Pts',(-113.939129422221,0.29024318656497,
135.715955094676));
#102239=CARTESIAN_POINT('Ctrl Pts',(-113.946875698306,0.427212861893932,
135.705941999949));
#102240=CARTESIAN_POINT('Ctrl Pts',(-113.95462197439,0.563523686211019,
135.690220226435));
#102241=CARTESIAN_POINT('Ctrl Pts',(-113.962368307655,0.699835516743832,
135.674498336867));
#102242=CARTESIAN_POINT('Ctrl Pts',(-113.97011464092,0.835488098169624,
135.653067729221));
#102243=CARTESIAN_POINT('Ctrl Pts',(-113.977860974186,0.969972385807809,
135.626013511882));
#102244=CARTESIAN_POINT('Ctrl Pts',(-113.985609042189,1.10448679026958,
135.59895323594));
#102245=CARTESIAN_POINT('Ctrl Pts',(-113.993357110192,1.23783199711468,
135.566266921398));
#102246=CARTESIAN_POINT('Ctrl Pts',(-114.001105178195,1.36951039558305,
135.528090535638));
#102247=CARTESIAN_POINT('Ctrl Pts',(-114.008861480937,1.50132874342048,
135.489873575561));
#102248=CARTESIAN_POINT('Ctrl Pts',(-114.016617783678,1.63147636801053,
135.44615499744));
#102249=CARTESIAN_POINT('Ctrl Pts',(-114.02437408642,1.75947151242207,135.397120469711));
#102250=CARTESIAN_POINT('Ctrl Pts',(-114.032134528935,1.88753497169604,
135.348059770779));
#102251=CARTESIAN_POINT('Ctrl Pts',(-114.039894971449,2.01344330288188,
135.293677623662));
#102252=CARTESIAN_POINT('Ctrl Pts',(-114.047655413963,2.13673683387609,
135.234206976669));
#102253=CARTESIAN_POINT('Ctrl Pts',(-114.055428314228,2.26022828659174,
135.174640862114));
#102254=CARTESIAN_POINT('Ctrl Pts',(-114.063201214494,2.38109620623323,
135.109970108946));
#102255=CARTESIAN_POINT('Ctrl Pts',(-114.070974114759,2.49890675230919,
135.04047299872));
#102256=CARTESIAN_POINT('Ctrl Pts',(-114.078464450521,2.61243458828842,
134.973502283503));
#102257=CARTESIAN_POINT('Ctrl Pts',(-114.085954786283,2.72312321915914,
134.902050186605));
#102258=CARTESIAN_POINT('Ctrl Pts',(-114.093445122045,2.83061311294589,
134.826401451188));
#102259=CARTESIAN_POINT('Ctrl Pts',(-114.101219456164,2.94217851872625,
134.747884470974));
#102260=CARTESIAN_POINT('Ctrl Pts',(-114.108993790284,3.05065124464519,
134.664597620967));
#102261=CARTESIAN_POINT('Ctrl Pts',(-114.116768124403,3.15559637649354,
134.576812681034));
#102262=CARTESIAN_POINT('Ctrl Pts',(-114.12453287735,3.2604121728461,134.489135928194));
#102263=CARTESIAN_POINT('Ctrl Pts',(-114.132297630297,3.36170872824294,
134.396972363767));
#102264=CARTESIAN_POINT('Ctrl Pts',(-114.140062383244,3.45908001334582,
134.300636997341));
#102265=CARTESIAN_POINT('Ctrl Pts',(-114.147819424129,3.55635458791564,
134.204397312559));
#102266=CARTESIAN_POINT('Ctrl Pts',(-114.155576465014,3.64971137451852,
134.103994344706));
#102267=CARTESIAN_POINT('Ctrl Pts',(-114.163333505899,3.7387776500584,133.999783085085));
#102268=CARTESIAN_POINT('Ctrl Pts',(-114.171084697139,3.82777676002694,
133.895650411985));
#102269=CARTESIAN_POINT('Ctrl Pts',(-114.178835888379,3.91249154602938,
133.787715459388));
#102270=CARTESIAN_POINT('Ctrl Pts',(-114.186587079619,3.9925866385517,133.676369495714));
#102271=CARTESIAN_POINT('Ctrl Pts',(-114.194334976396,4.0726476885232,133.565070857044));
#102272=CARTESIAN_POINT('Ctrl Pts',(-114.202082873173,4.14809272242647,
133.450364407498));
#102273=CARTESIAN_POINT('Ctrl Pts',(-114.209830769951,4.21862727291639,
133.332673690488));
#102274=CARTESIAN_POINT('Ctrl Pts',(-114.217577046035,4.28914706909891,
133.215007591838));
#102275=CARTESIAN_POINT('Ctrl Pts',(-114.225323322119,4.35475822410486,
133.094358802517));
#102276=CARTESIAN_POINT('Ctrl Pts',(-114.233069598203,4.41521038090453,
132.971178642886));
#102277=CARTESIAN_POINT('Ctrl Pts',(-114.240815931468,4.4756629839482,132.847997573968));
#102278=CARTESIAN_POINT('Ctrl Pts',(-114.248562264733,4.53095634054831,
132.722285448429));
#102279=CARTESIAN_POINT('Ctrl Pts',(-114.256308597999,4.58088690371579,
132.594516543139));
#102280=CARTESIAN_POINT('Ctrl Pts',(-114.264056666002,4.63082864848676,
132.466719024889));
#102281=CARTESIAN_POINT('Ctrl Pts',(-114.271804734005,4.67540506777575,
132.33686417442));
#102282=CARTESIAN_POINT('Ctrl Pts',(-114.279552802008,4.71446158402071,
132.205444139449));
#102283=CARTESIAN_POINT('Ctrl Pts',(-114.287309104749,4.75355960999586,
132.073884429702));
#102284=CARTESIAN_POINT('Ctrl Pts',(-114.295065407491,4.78712590217075,
131.940756587802));
#102285=CARTESIAN_POINT('Ctrl Pts',(-114.302821710233,4.8150562672724,131.806566287826));
#102286=CARTESIAN_POINT('Ctrl Pts',(-114.310582152747,4.84300153965094,
131.672304366446));
#102287=CARTESIAN_POINT('Ctrl Pts',(-114.318342595262,4.86530482758688,
131.536979242635));
#102288=CARTESIAN_POINT('Ctrl Pts',(-114.326103037776,4.88191365309006,
131.401103565805));
#102289=CARTESIAN_POINT('Ctrl Pts',(-114.333875938041,4.8985491405544,131.265009769275));
#102290=CARTESIAN_POINT('Ctrl Pts',(-114.341648838307,4.9094718672722,131.128364043565));
#102291=CARTESIAN_POINT('Ctrl Pts',(-114.349421738572,4.91468145801539,
130.991681808945));
#102292=CARTESIAN_POINT('Ctrl Pts',(-114.356912074334,4.91970166701294,
130.859968317834));
#102293=CARTESIAN_POINT('Ctrl Pts',(-114.364402410096,4.91941690296997,
130.728221234129));
#102294=CARTESIAN_POINT('Ctrl Pts',(-114.371892745858,4.91387239255782,
130.596896952897));
#102295=CARTESIAN_POINT('Ctrl Pts',(-114.379667079977,4.90811766034822,
130.460593471627));
#102296=CARTESIAN_POINT('Ctrl Pts',(-114.387441414096,4.89667823258385,
130.324313718381));
#102297=CARTESIAN_POINT('Ctrl Pts',(-114.395215748216,4.8795476836109,130.188570502456));
#102298=CARTESIAN_POINT('Ctrl Pts',(-114.402980501163,4.86243824650862,
130.052994577913));
#102299=CARTESIAN_POINT('Ctrl Pts',(-114.41074525411,4.83965169204675,129.917954259197));
#102300=CARTESIAN_POINT('Ctrl Pts',(-114.418510007057,4.8112335779369,129.783961420667));
#102301=CARTESIAN_POINT('Ctrl Pts',(-114.426267047942,4.78284368909862,
129.650101665712));
#102302=CARTESIAN_POINT('Ctrl Pts',(-114.434024088827,4.74883345220964,
129.517287700539));
#102303=CARTESIAN_POINT('Ctrl Pts',(-114.441781129712,4.70930006556798,
129.386024989112));
#102304=CARTESIAN_POINT('Ctrl Pts',(-114.449532320952,4.66979649136065,
129.254861263917));
#102305=CARTESIAN_POINT('Ctrl Pts',(-114.457283512192,4.62477816997164,
129.125246836869));
#102306=CARTESIAN_POINT('Ctrl Pts',(-114.465034703432,4.57439301119051,
128.997675353977));
#102307=CARTESIAN_POINT('Ctrl Pts',(-114.472782600209,4.524029267446,128.870158092368));
#102308=CARTESIAN_POINT('Ctrl Pts',(-114.480530496986,4.46830336645975,
128.74468241079));
#102309=CARTESIAN_POINT('Ctrl Pts',(-114.488278393764,4.40741248050626,
128.621724988521));
#102310=CARTESIAN_POINT('Ctrl Pts',(-114.496024669848,4.34653433161346,
128.498793286294));
#102311=CARTESIAN_POINT('Ctrl Pts',(-114.503770945932,4.28049352012902,
128.378379145744));
#102312=CARTESIAN_POINT('Ctrl Pts',(-114.511517222016,4.20953443056437,
128.260937149012));
#102313=CARTESIAN_POINT('Ctrl Pts',(-114.519263555281,4.13857481719575,
128.143494285349));
#102314=CARTESIAN_POINT('Ctrl Pts',(-114.527009888547,4.06269705548542,
128.029023943909));
#102315=CARTESIAN_POINT('Ctrl Pts',(-114.534756221812,3.98219014587498,
127.91795373277));
#102316=CARTESIAN_POINT('Ctrl Pts',(-114.542504289815,3.90166520730044,
127.806858648228));
#102317=CARTESIAN_POINT('Ctrl Pts',(-114.550252357818,3.81650928738582,
127.699165525651));
#102318=CARTESIAN_POINT('Ctrl Pts',(-114.558000425821,3.72705289099508,
127.595270433382));
#102319=CARTESIAN_POINT('Ctrl Pts',(-114.565756728563,3.6375014192816,127.491264920172));
#102320=CARTESIAN_POINT('Ctrl Pts',(-114.573513031304,3.54364059633716,
127.391065797543));
#102321=CARTESIAN_POINT('Ctrl Pts',(-114.581269334046,3.44583954107468,
127.295034055437));
#102322=CARTESIAN_POINT('Ctrl Pts',(-114.58902977656,3.34798628644428,127.198951058298));
#102323=CARTESIAN_POINT('Ctrl Pts',(-114.596790219075,3.24618889909328,
127.107040135576));
#102324=CARTESIAN_POINT('Ctrl Pts',(-114.604550661589,3.14085031985415,
127.019622538019));
#102325=CARTESIAN_POINT('Ctrl Pts',(-114.612323561854,3.03534264177611,
126.932064609974));
#102326=CARTESIAN_POINT('Ctrl Pts',(-114.62009646212,2.92628272332133,126.849014658135));
#102327=CARTESIAN_POINT('Ctrl Pts',(-114.627869362385,2.81410399934133,
126.770751595438));
#102328=CARTESIAN_POINT('Ctrl Pts',(-114.635359698147,2.70600325453947,
126.695333592203));
#102329=CARTESIAN_POINT('Ctrl Pts',(-114.642850033909,2.59500677982708,
126.624360655414));
#102330=CARTESIAN_POINT('Ctrl Pts',(-114.650340369671,2.4815229994208,126.558041427274));
#102331=CARTESIAN_POINT('Ctrl Pts',(-114.65811470379,2.36373644698727,126.48920768544));
#102332=CARTESIAN_POINT('Ctrl Pts',(-114.665889037909,2.24289714080766,
126.425169464552));
#102333=CARTESIAN_POINT('Ctrl Pts',(-114.673663372028,2.11943304864548,
126.366209356646));
#102334=CARTESIAN_POINT('Ctrl Pts',(-114.681428124975,1.99612111494292,
126.307321911803));
#102335=CARTESIAN_POINT('Ctrl Pts',(-114.689192877922,1.87019118098777,
126.253500294611));
#102336=CARTESIAN_POINT('Ctrl Pts',(-114.696957630869,1.74209852623014,
126.204982856672));
#102337=CARTESIAN_POINT('Ctrl Pts',(-114.704714671754,1.614133094903,126.156513606936));
#102338=CARTESIAN_POINT('Ctrl Pts',(-114.71247171264,1.48400958073074,126.113338190113));
#102339=CARTESIAN_POINT('Ctrl Pts',(-114.720228753525,1.35220578291796,
126.075648046142));
#102340=CARTESIAN_POINT('Ctrl Pts',(-114.727979944765,1.22050137937422,
126.037986324602));
#102341=CARTESIAN_POINT('Ctrl Pts',(-114.735731136005,1.08711958868282,
126.005801749544));
#102342=CARTESIAN_POINT('Ctrl Pts',(-114.743482327245,0.952555678066113,
125.979236707998));
#102343=CARTESIAN_POINT('Ctrl Pts',(-114.751230224022,0.818048960700843,
125.952682957304));
#102344=CARTESIAN_POINT('Ctrl Pts',(-114.758978120799,0.682361505469531,
125.931744065236));
#102345=CARTESIAN_POINT('Ctrl Pts',(-114.766726017576,0.54600093257844,
125.91651180197));
#102346=CARTESIAN_POINT('Ctrl Pts',(-114.77447229366,0.409668883379975,
125.901282724965));
#102347=CARTESIAN_POINT('Ctrl Pts',(-114.782218569744,0.272664384886409,
125.891757945794));
#102348=CARTESIAN_POINT('Ctrl Pts',(-114.789964845828,0.135501985723202,
125.887977569596));
#102349=CARTESIAN_POINT('Ctrl Pts',(-114.797711179094,-0.00166142594186416,
125.884197165493));
#102350=CARTESIAN_POINT('Ctrl Pts',(-114.805457512359,-0.138982349785618,
125.886161259748));
#102351=CARTESIAN_POINT('Ctrl Pts',(-114.813203845624,-0.275944815223184,
125.893857840716));
#102352=CARTESIAN_POINT('Ctrl Pts',(-114.820951913627,-0.41293795245544,
125.90155614528));
#102353=CARTESIAN_POINT('Ctrl Pts',(-114.82869998163,-0.549572081270348,
125.914989469142));
#102354=CARTESIAN_POINT('Ctrl Pts',(-114.836448049633,-0.685335332201852,
125.934093833812));
#102355=CARTESIAN_POINT('Ctrl Pts',(-114.844204352375,-0.821242873931864,
125.953218502828));
#102356=CARTESIAN_POINT('Ctrl Pts',(-114.851960655117,-0.956277301065753,
125.978026198168));
#102357=CARTESIAN_POINT('Ctrl Pts',(-114.859716957859,-1.08993538475321,
126.008401493516));
#102358=CARTESIAN_POINT('Ctrl Pts',(-114.867477400373,-1.22366480578431,
126.038793001073));
#102359=CARTESIAN_POINT('Ctrl Pts',(-114.875237842887,-1.35601604252535,
126.074757927323));
#102360=CARTESIAN_POINT('Ctrl Pts',(-114.882998285401,-1.48650101826154,
126.116130910608));
#102361=CARTESIAN_POINT('Ctrl Pts',(-114.890771185667,-1.6171954600647,
126.157570309478));
#102362=CARTESIAN_POINT('Ctrl Pts',(-114.898544085932,-1.74601728650515,
126.204434980034));
#102363=CARTESIAN_POINT('Ctrl Pts',(-114.906316986197,-1.87249755810587,
126.256511020516));
#102364=CARTESIAN_POINT('Ctrl Pts',(-114.913807321959,-1.99437995324829,
126.306693965754));
#102365=CARTESIAN_POINT('Ctrl Pts',(-114.921297657721,-2.11408780084788,
126.361715837568));
#102366=CARTESIAN_POINT('Ctrl Pts',(-114.928787993483,-2.23122480104518,
126.421345793304));
#102367=CARTESIAN_POINT('Ctrl Pts',(-114.936563162424,-2.3528161414993,
126.483243282884));
#102368=CARTESIAN_POINT('Ctrl Pts',(-114.944338331365,-2.47202244986505,
126.550302346067));
#102369=CARTESIAN_POINT('Ctrl Pts',(-114.952113500305,-2.58837449630025,
126.622315599946));
#102370=CARTESIAN_POINT('Ctrl Pts',(-114.959878902606,-2.70458038917816,
126.694238395654));
#102371=CARTESIAN_POINT('Ctrl Pts',(-114.967644304906,-2.81793882506746,
126.771102794938));
#102372=CARTESIAN_POINT('Ctrl Pts',(-114.975409707207,-2.92800307381476,
126.852654522443));
#102373=CARTESIAN_POINT('Ctrl Pts',(-114.983311706695,-3.04000340601512,
126.93564078434));
#102374=CARTESIAN_POINT('Ctrl Pts',(-114.991213706184,-3.14859219035022,
127.023480673468));
#102375=CARTESIAN_POINT('Ctrl Pts',(-114.999115705672,-3.25332644318739,
127.11585819564));
#102376=CARTESIAN_POINT('Ctrl Pts',(-115.006866536838,-3.3560570890443,
127.206468499893));
#102377=CARTESIAN_POINT('Ctrl Pts',(-115.014617368004,-3.45507904201751,
127.301444117669));
#102378=CARTESIAN_POINT('Ctrl Pts',(-115.02236819917,-3.55000548578644,
127.400444620749));
#102379=CARTESIAN_POINT('Ctrl Pts',(-115.03011549927,-3.6448886836772,127.499400021921));
#102380=CARTESIAN_POINT('Ctrl Pts',(-115.03786279937,-3.73567981501322,
127.602376378269));
#102381=CARTESIAN_POINT('Ctrl Pts',(-115.04561009947,-3.82202807819197,
127.708995625839));
#102382=CARTESIAN_POINT('Ctrl Pts',(-115.053355547864,-3.90835570299911,
127.815589390005));
#102383=CARTESIAN_POINT('Ctrl Pts',(-115.061100996257,-3.99024232785089,
127.925824008542));
#102384=CARTESIAN_POINT('Ctrl Pts',(-115.068846444651,-4.0673769604366,
128.039287793171));
#102385=CARTESIAN_POINT('Ctrl Pts',(-115.076864048841,-4.14722191220701,
128.156738413051));
#102386=CARTESIAN_POINT('Ctrl Pts',(-115.084881653031,-4.22197453572727,
128.27764893658));
#102387=CARTESIAN_POINT('Ctrl Pts',(-115.092899257221,-4.29133860411453,
128.401529777216));
#102388=CARTESIAN_POINT('Ctrl Pts',(-115.100648655071,-4.35838229318922,
128.521266533652));
#102389=CARTESIAN_POINT('Ctrl Pts',(-115.108398052922,-4.42039199947249,
128.643777695005));
#102390=CARTESIAN_POINT('Ctrl Pts',(-115.116147450772,-4.47714731123146,
128.768596629272));
#102391=CARTESIAN_POINT('Ctrl Pts',(-115.124299158132,-4.53684907148763,
128.899895530787));
#102392=CARTESIAN_POINT('Ctrl Pts',(-115.132450865492,-4.59073607669625,
129.033747784281));
#102393=CARTESIAN_POINT('Ctrl Pts',(-115.140602572852,-4.6386098775966,
129.169588013819));
#102394=CARTESIAN_POINT('Ctrl Pts',(-115.148754280212,-4.68648367849696,
129.305428243356));
#102395=CARTESIAN_POINT('Ctrl Pts',(-115.156905987572,-4.72834416606678,
129.443255959199));
#102396=CARTESIAN_POINT('Ctrl Pts',(-115.165057694931,-4.76405452823392,
129.582490119308));
#102397=CARTESIAN_POINT('Ctrl Pts',(-113.415051629673,-4.76405452823414,
129.582490119309));
#102398=CARTESIAN_POINT('Ctrl Pts',(-113.422688410304,-4.79766851844642,
129.713550556983));
#102399=CARTESIAN_POINT('Ctrl Pts',(-113.430325190934,-4.82585680892114,
129.845947543374));
#102400=CARTESIAN_POINT('Ctrl Pts',(-113.437961971565,-4.84853264300647,
129.979185319705));
#102401=CARTESIAN_POINT('Ctrl Pts',(-113.445825070299,-4.87188048169826,
130.116371634339));
#102402=CARTESIAN_POINT('Ctrl Pts',(-113.453688169033,-4.88938398938119,
130.254448891163));
#102403=CARTESIAN_POINT('Ctrl Pts',(-113.461551267768,-4.90100592036944,
130.392870604317));
#102404=CARTESIAN_POINT('Ctrl Pts',(-113.469414366502,-4.91262785135766,
130.53129231747));
#102405=CARTESIAN_POINT('Ctrl Pts',(-113.477277465236,-4.91836823271671,
130.670058022627));
#102406=CARTESIAN_POINT('Ctrl Pts',(-113.48514056397,-4.91824815323073,
130.808622746439));
#102407=CARTESIAN_POINT('',(-113.139859436022,-4.91824999810658,130.804497089607));
#102408=CARTESIAN_POINT('Ctrl Pts',(-113.070135781827,-4.76405452823415,
129.582490119309));
#102409=CARTESIAN_POINT('Ctrl Pts',(-113.078251155085,-4.79966750581325,
129.721344578387));
#102410=CARTESIAN_POINT('Ctrl Pts',(-113.086366528344,-4.82924206252691,
129.861899006423));
#102411=CARTESIAN_POINT('Ctrl Pts',(-113.094481901602,-4.85262675814392,
130.003613086414));
#102412=CARTESIAN_POINT('Ctrl Pts',(-113.102583039655,-4.87597043458281,
130.145078585231));
#102413=CARTESIAN_POINT('Ctrl Pts',(-113.110684177708,-4.89314584612007,
130.28769935033));
#102414=CARTESIAN_POINT('Ctrl Pts',(-113.118785315761,-4.90405217150556,
130.430923391715));
#102415=CARTESIAN_POINT('Ctrl Pts',(-113.125810022504,-4.91350932888095,
130.5551166696));
#102416=CARTESIAN_POINT('Ctrl Pts',(-113.132834729248,-4.91825345922004,
130.679763201676));
#102417=CARTESIAN_POINT('Ctrl Pts',(-113.139859435992,-4.9182499981066,
130.80449708907));
#102418=CARTESIAN_POINT('Ctrl Pts',(-113.139859436022,-4.91824999810658,
130.804497089606));
#102419=CARTESIAN_POINT('Ctrl Pts',(-113.147991076814,-4.91824599158461,
130.948886201333));
#102420=CARTESIAN_POINT('Ctrl Pts',(-113.156122717607,-4.91187926007567,
131.093146870426));
#102421=CARTESIAN_POINT('Ctrl Pts',(-113.164254358399,-4.89920940978586,
131.236714895405));
#102422=CARTESIAN_POINT('Ctrl Pts',(-113.172397316585,-4.88652192594669,
131.380482734414));
#102423=CARTESIAN_POINT('Ctrl Pts',(-113.180540274771,-4.86751384528746,
131.523555677082));
#102424=CARTESIAN_POINT('Ctrl Pts',(-113.188683232958,-4.8422961614743,
131.665378008256));
#102425=CARTESIAN_POINT('Ctrl Pts',(-113.196846014214,-4.8170170881869,
131.807545589154));
#102426=CARTESIAN_POINT('Ctrl Pts',(-113.205008795471,-4.78549824440557,
131.948456145151));
#102427=CARTESIAN_POINT('Ctrl Pts',(-113.213171576728,-4.74790143450914,
132.087565601458));
#102428=CARTESIAN_POINT('Ctrl Pts',(-113.221344900657,-4.71025606630158,
132.226854725144));
#102429=CARTESIAN_POINT('Ctrl Pts',(-113.229518224587,-4.66651716453983,
132.364337792287));
#102430=CARTESIAN_POINT('Ctrl Pts',(-113.237691548517,-4.61689536894023,
132.499488994639));
#102431=CARTESIAN_POINT('Ctrl Pts',(-113.24588368943,-4.56715933187323,
132.634951347998));
#102432=CARTESIAN_POINT('Ctrl Pts',(-113.254075830343,-4.51151344663191,
132.76807079685));
#102433=CARTESIAN_POINT('Ctrl Pts',(-113.262267971257,-4.45021591031225,
132.898342808059));
#102434=CARTESIAN_POINT('Ctrl Pts',(-113.267409063093,-4.41174778984284,
132.980096818447));
#102435=CARTESIAN_POINT('Ctrl Pts',(-113.272550154929,-4.37105475365047,
133.060729916846));
#102436=CARTESIAN_POINT('Ctrl Pts',(-113.277691246765,-4.3282093812174,
133.140123151481));
#102437=CARTESIAN_POINT('Ctrl Pts',(-113.285465580885,-4.263418817003,133.260181215507));
#102438=CARTESIAN_POINT('Ctrl Pts',(-113.293239915004,-4.19352649637786,
133.37773160968));
#102439=CARTESIAN_POINT('Ctrl Pts',(-113.301014249123,-4.11875092976229,
133.492310364321));
#102440=CARTESIAN_POINT('Ctrl Pts',(-113.30877900207,-4.04406751734969,
133.606747910888));
#102441=CARTESIAN_POINT('Ctrl Pts',(-113.316543755017,-3.96451304492104,
133.718220780501));
#102442=CARTESIAN_POINT('Ctrl Pts',(-113.324308507964,-3.88035236159243,
133.826288580371));
#102443=CARTESIAN_POINT('Ctrl Pts',(-113.332065548849,-3.79627526784095,
133.934249045779));
#102444=CARTESIAN_POINT('Ctrl Pts',(-113.339822589734,-3.70760130622051,
134.038810865241));
#102445=CARTESIAN_POINT('Ctrl Pts',(-113.347579630619,-3.61463896147492,
134.139561996896));
#102446=CARTESIAN_POINT('Ctrl Pts',(-113.355330821859,-3.52174672035651,
134.24023715134));
#102447=CARTESIAN_POINT('Ctrl Pts',(-113.363082013099,-3.42457279705244,
134.337107051668));
#102448=CARTESIAN_POINT('Ctrl Pts',(-113.37083320434,-3.32346611129491,
134.429792463509));
#102449=CARTESIAN_POINT('Ctrl Pts',(-113.378581101117,-3.22240239857606,
134.522438481576));
#102450=CARTESIAN_POINT('Ctrl Pts',(-113.386328997894,-3.11740953553958,
134.610903284857));
#102451=CARTESIAN_POINT('Ctrl Pts',(-113.394076894671,-3.00887332190837,
134.694844442903));
#102452=CARTESIAN_POINT('Ctrl Pts',(-113.401823170755,-2.90035981171328,
134.778768042268));
#102453=CARTESIAN_POINT('Ctrl Pts',(-113.409569446839,-2.78830473426541,
134.858169639506));
#102454=CARTESIAN_POINT('Ctrl Pts',(-113.417315722924,-2.67312668163051,
134.932747325041));
#102455=CARTESIAN_POINT('Ctrl Pts',(-113.425062056189,-2.55794777877723,
135.007325561091));
#102456=CARTESIAN_POINT('Ctrl Pts',(-113.432808389454,-2.43964618291295,
135.077079601889));
#102457=CARTESIAN_POINT('Ctrl Pts',(-113.44055472272,-2.31866881060544,
135.141751308895));
#102458=CARTESIAN_POINT('Ctrl Pts',(-113.448302790723,-2.19766434625469,
135.20643749868));
#102459=CARTESIAN_POINT('Ctrl Pts',(-113.456050858726,-2.07398325780427,
135.266038905598));
#102460=CARTESIAN_POINT('Ctrl Pts',(-113.463798926729,-1.94809599130373,
135.32034390708));
#102461=CARTESIAN_POINT('Ctrl Pts',(-113.471555229471,-1.82207493031777,
135.374706624563));
#102462=CARTESIAN_POINT('Ctrl Pts',(-113.479311532213,-1.69384336694674,
135.423761536804));
#102463=CARTESIAN_POINT('Ctrl Pts',(-113.487067834955,-1.56389112974991,
135.467345455284));
#102464=CARTESIAN_POINT('Ctrl Pts',(-113.494828277469,-1.4338695331313,
135.510952635814));
#102465=CARTESIAN_POINT('Ctrl Pts',(-113.502588719983,-1.30212580811419,
135.549082895527));
#102466=CARTESIAN_POINT('Ctrl Pts',(-113.510349162498,-1.16916281779595,
135.581623575368));
#102467=CARTESIAN_POINT('Ctrl Pts',(-113.518122062763,-1.03598638348176,
135.614216492396));
#102468=CARTESIAN_POINT('Ctrl Pts',(-113.525894963029,-0.901587156147086,
135.641201821851));
#102469=CARTESIAN_POINT('Ctrl Pts',(-113.533667863294,-0.766476904147307,
135.662518315491));
#102470=CARTESIAN_POINT('Ctrl Pts',(-113.541158199056,-0.636278250133563,
135.683059900894));
#102471=CARTESIAN_POINT('Ctrl Pts',(-113.548648534818,-0.505419674967997,
135.698337612106));
#102472=CARTESIAN_POINT('Ctrl Pts',(-113.55613887058,-0.374359720922348,
135.708342454997));
#102473=CARTESIAN_POINT('Ctrl Pts',(-113.563913204699,-0.238330588880613,
135.718726634547));
#102474=CARTESIAN_POINT('Ctrl Pts',(-113.571687538818,-0.101653606550363,
135.723463105129));
#102475=CARTESIAN_POINT('Ctrl Pts',(-113.579461872937,0.0351627650186293,
135.722484918807));
#102476=CARTESIAN_POINT('Ctrl Pts',(-113.587226625884,0.171810522637293,
135.721507938012));
#102477=CARTESIAN_POINT('Ctrl Pts',(-113.594991378831,0.308596940492108,
135.71483031616));
#102478=CARTESIAN_POINT('Ctrl Pts',(-113.602756131778,0.445008346240295,
135.702436835254));
#102479=CARTESIAN_POINT('Ctrl Pts',(-113.610513172663,0.581284266257229,
135.690055663727));
#102480=CARTESIAN_POINT('Ctrl Pts',(-113.618270213548,0.717185528552299,
135.671969965922));
#102481=CARTESIAN_POINT('Ctrl Pts',(-113.626027254433,0.852198727101079,
135.648216560101));
#102482=CARTESIAN_POINT('Ctrl Pts',(-113.633778445673,0.987110111146399,
135.624481066907));
#102483=CARTESIAN_POINT('Ctrl Pts',(-113.641529636914,1.12113438094086,
135.595086440429));
#102484=CARTESIAN_POINT('Ctrl Pts',(-113.649280828154,1.25376387622911,
135.560121251278));
#102485=CARTESIAN_POINT('Ctrl Pts',(-113.657028724931,1.38633700044403,
135.525170923265));
#102486=CARTESIAN_POINT('Ctrl Pts',(-113.664776621708,1.5175161519623,135.484654841086));
#102487=CARTESIAN_POINT('Ctrl Pts',(-113.672524518485,1.64680470017511,
135.438712496953));
#102488=CARTESIAN_POINT('Ctrl Pts',(-113.680270794569,1.77606620401078,
135.392779762968));
#102489=CARTESIAN_POINT('Ctrl Pts',(-113.688017070653,1.90343752299542,
135.341423155546));
#102490=CARTESIAN_POINT('Ctrl Pts',(-113.695763346737,2.02843839281524,
135.284831658545));
#102491=CARTESIAN_POINT('Ctrl Pts',(-113.703509680003,2.15344018536291,
135.228239743799));
#102492=CARTESIAN_POINT('Ctrl Pts',(-113.711256013268,2.2760711376646,135.166413023612));
#102493=CARTESIAN_POINT('Ctrl Pts',(-113.719002346533,2.39587250113482,
135.099587971363));
#102494=CARTESIAN_POINT('Ctrl Pts',(-113.726750414536,2.51570069328991,
135.032747954107));
#102495=CARTESIAN_POINT('Ctrl Pts',(-113.734498482539,2.63269769431587,
134.960907567848));
#102496=CARTESIAN_POINT('Ctrl Pts',(-113.742246550542,2.7464311725708,134.884348225002));
#102497=CARTESIAN_POINT('Ctrl Pts',(-113.750002853284,2.86028552811971,
134.807707513976));
#102498=CARTESIAN_POINT('Ctrl Pts',(-113.757759156026,2.97086910732701,
134.726338046304));
#102499=CARTESIAN_POINT('Ctrl Pts',(-113.765515458768,3.07777985076991,
134.640563721247));
#102500=CARTESIAN_POINT('Ctrl Pts',(-113.773275901282,3.1847476556956,134.554743615851));
#102501=CARTESIAN_POINT('Ctrl Pts',(-113.781036343796,3.28803842448805,
134.464514225576));
#102502=CARTESIAN_POINT('Ctrl Pts',(-113.78879678631,3.38728556410607,134.370237728418));
#102503=CARTESIAN_POINT('Ctrl Pts',(-113.796569686576,3.48669202404362,
134.275809890257));
#102504=CARTESIAN_POINT('Ctrl Pts',(-113.804342586841,3.58204161123619,
134.17732224364));
#102505=CARTESIAN_POINT('Ctrl Pts',(-113.812115487107,3.67300617250755,
134.075172247609));
#102506=CARTESIAN_POINT('Ctrl Pts',(-113.819605822868,3.76066394284882,
133.976735661235));
#102507=CARTESIAN_POINT('Ctrl Pts',(-113.82709615863,3.84424977025502,133.87489861193));
#102508=CARTESIAN_POINT('Ctrl Pts',(-113.834586494392,3.92350823441002,
133.770042022744));
#102509=CARTESIAN_POINT('Ctrl Pts',(-113.842360828511,4.00577180732484,
133.661209764107));
#102510=CARTESIAN_POINT('Ctrl Pts',(-113.85013516263,4.08363398164012,133.548779726024));
#102511=CARTESIAN_POINT('Ctrl Pts',(-113.857909496749,4.15676359654165,
133.433143504182));
#102512=CARTESIAN_POINT('Ctrl Pts',(-113.865674249696,4.22980308572859,
133.317649793649));
#102513=CARTESIAN_POINT('Ctrl Pts',(-113.873439002643,4.29812141338876,
133.198958088594));
#102514=CARTESIAN_POINT('Ctrl Pts',(-113.881203755591,4.36142812374139,
133.07749233041));
#102515=CARTESIAN_POINT('Ctrl Pts',(-113.888960796476,4.42467195697684,
132.956147213729));
#102516=CARTESIAN_POINT('Ctrl Pts',(-113.89671783736,4.482913899043,132.832033871406));
#102517=CARTESIAN_POINT('Ctrl Pts',(-113.904474878245,4.53590741769,132.705604147639));
#102518=CARTESIAN_POINT('Ctrl Pts',(-113.912226069486,4.58886097351228,
132.579269765511));
#102519=CARTESIAN_POINT('Ctrl Pts',(-113.919977260726,4.63657383330587,
132.450622837954));
#102520=CARTESIAN_POINT('Ctrl Pts',(-113.927728451966,4.67884611126632,
132.320138348498));
#102521=CARTESIAN_POINT('Ctrl Pts',(-113.935476348743,4.72110042238105,
132.18970931843));
#102522=CARTESIAN_POINT('Ctrl Pts',(-113.94322424552,4.75791863059376,132.057444650994));
#102523=CARTESIAN_POINT('Ctrl Pts',(-113.950972142297,4.7891496536775,131.923837574533));
#102524=CARTESIAN_POINT('Ctrl Pts',(-113.958718418381,4.82037414390447,
131.790258445793));
#102525=CARTESIAN_POINT('Ctrl Pts',(-113.966464694465,4.84601368471408,
131.655337847022));
#102526=CARTESIAN_POINT('Ctrl Pts',(-113.974210970549,4.86596767898667,
131.519581988581));
#102527=CARTESIAN_POINT('Ctrl Pts',(-113.981957303814,4.88592182055509,
131.383825128022));
#102528=CARTESIAN_POINT('Ctrl Pts',(-113.98970363708,4.90019027498468,131.2472333823));
#102529=CARTESIAN_POINT('Ctrl Pts',(-113.997449970345,4.90872402921118,
131.110320529229));
#102530=CARTESIAN_POINT('Ctrl Pts',(-114.005198038348,4.91725969451279,
130.973377015474));
#102531=CARTESIAN_POINT('Ctrl Pts',(-114.012946106351,4.9200580797928,130.836112641412));
#102532=CARTESIAN_POINT('Ctrl Pts',(-114.020694174354,4.9171222594753,130.699043250183));
#102533=CARTESIAN_POINT('Ctrl Pts',(-114.028450477096,4.91418331893304,
130.561828179974));
#102534=CARTESIAN_POINT('Ctrl Pts',(-114.036206779838,4.90549800699418,
130.424808898062));
#102535=CARTESIAN_POINT('Ctrl Pts',(-114.043963082579,4.89112150634027,
130.288498743887));
#102536=CARTESIAN_POINT('Ctrl Pts',(-114.051723525094,4.87673733251505,
130.152115836878));
#102537=CARTESIAN_POINT('Ctrl Pts',(-114.059483967608,4.8566559745981,130.016443198328));
#102538=CARTESIAN_POINT('Ctrl Pts',(-114.067244410122,4.83098399070024,
129.881985019397));
#102539=CARTESIAN_POINT('Ctrl Pts',(-114.075017310387,4.80527079585478,
129.747310996261));
#102540=CARTESIAN_POINT('Ctrl Pts',(-114.082790210653,4.77394913036231,
129.613855709424));
#102541=CARTESIAN_POINT('Ctrl Pts',(-114.090563110918,4.73717601296352,
129.48211007977));
#102542=CARTESIAN_POINT('Ctrl Pts',(-114.09805344668,4.70173969100659,129.355153735595));
#102543=CARTESIAN_POINT('Ctrl Pts',(-114.105543782443,4.66124147865892,
129.229785199059));
#102544=CARTESIAN_POINT('Ctrl Pts',(-114.113034118205,4.6158637963526,129.106425260722));
#102545=CARTESIAN_POINT('Ctrl Pts',(-114.120808452324,4.56876560543119,
128.978388092834));
#102546=CARTESIAN_POINT('Ctrl Pts',(-114.128582786443,4.51626143731483,
128.85210925857));
#102547=CARTESIAN_POINT('Ctrl Pts',(-114.136357120562,4.45850175203502,
128.728079039937));
#102548=CARTESIAN_POINT('Ctrl Pts',(-114.144121873509,4.40081325040534,
128.604201677464));
#102549=CARTESIAN_POINT('Ctrl Pts',(-114.151886626456,4.33788228228746,
128.48256776774));
#102550=CARTESIAN_POINT('Ctrl Pts',(-114.159651379404,4.26990852313562,
128.363650830116));
#102551=CARTESIAN_POINT('Ctrl Pts',(-114.167408420289,4.20200227647944,
128.244852002471));
#102552=CARTESIAN_POINT('Ctrl Pts',(-114.175165461174,4.12906339883511,
128.12876511395));
#102553=CARTESIAN_POINT('Ctrl Pts',(-114.182922502059,4.05133878282114,
128.015841811944));
#102554=CARTESIAN_POINT('Ctrl Pts',(-114.190673693299,3.97367277954483,
127.903003666278));
#102555=CARTESIAN_POINT('Ctrl Pts',(-114.198424884539,3.89122844209005,
127.793324679314));
#102556=CARTESIAN_POINT('Ctrl Pts',(-114.206176075779,3.80429734439262,
127.687229760841));
#102557=CARTESIAN_POINT('Ctrl Pts',(-114.213923972556,3.71740319473054,
127.581179935538));
#102558=CARTESIAN_POINT('Ctrl Pts',(-114.221671869333,3.62602632495959,
127.478711450729));
#102559=CARTESIAN_POINT('Ctrl Pts',(-114.22941976611,3.53050003842044,127.380218018139));
#102560=CARTESIAN_POINT('Ctrl Pts',(-114.237166042194,3.43499373392113,
127.281745188251));
#102561=CARTESIAN_POINT('Ctrl Pts',(-114.244912318278,3.33534001111267,
127.187246037164));
#102562=CARTESIAN_POINT('Ctrl Pts',(-114.252658594362,3.23191038390806,
127.097078819147));
#102563=CARTESIAN_POINT('Ctrl Pts',(-114.260404927628,3.12847999320959,
127.006910935537));
#102564=CARTESIAN_POINT('Ctrl Pts',(-114.268151260893,3.0212739371987,126.92107530572));
#102565=CARTESIAN_POINT('Ctrl Pts',(-114.275897594158,2.91069797894401,
126.839890875233));
#102566=CARTESIAN_POINT('Ctrl Pts',(-114.283645662161,2.80009725797,126.758688264057));
#102567=CARTESIAN_POINT('Ctrl Pts',(-114.291393730164,2.68612544814,126.682139156217));
#102568=CARTESIAN_POINT('Ctrl Pts',(-114.299141798167,2.56921820469855,
126.610519790932));
#102569=CARTESIAN_POINT('Ctrl Pts',(-114.306898100909,2.4521867108477,126.538824307733));
#102570=CARTESIAN_POINT('Ctrl Pts',(-114.314654403651,2.33221388513286,
126.472069237892));
#102571=CARTESIAN_POINT('Ctrl Pts',(-114.322410706393,2.20976144215135,
126.410485627164));
#102572=CARTESIAN_POINT('Ctrl Pts',(-114.330171148907,2.08724364261372,
126.348869147408));
#102573=CARTESIAN_POINT('Ctrl Pts',(-114.337931591421,1.96224394488322,
126.292429787433));
#102574=CARTESIAN_POINT('Ctrl Pts',(-114.345692033935,1.83524413652449,
126.241350424519));
#102575=CARTESIAN_POINT('Ctrl Pts',(-114.353464934201,1.70804045679922,
126.190189064477));
#102576=CARTESIAN_POINT('Ctrl Pts',(-114.361237834466,1.57883061906044,
126.144405026371));
#102577=CARTESIAN_POINT('Ctrl Pts',(-114.369010734731,1.44811252141387,
126.104131560613));
#102578=CARTESIAN_POINT('Ctrl Pts',(-114.376501070493,1.32214635587791,
126.065322136779));
#102579=CARTESIAN_POINT('Ctrl Pts',(-114.383991406255,1.19477998247819,
126.031629673504));
#102580=CARTESIAN_POINT('Ctrl Pts',(-114.391481742017,1.06646602692964,
126.003128142888));
#102581=CARTESIAN_POINT('Ctrl Pts',(-114.399256076136,0.9332870087542,125.973545968075));
#102582=CARTESIAN_POINT('Ctrl Pts',(-114.407030410255,0.798665263733949,
125.949462417255));
#102583=CARTESIAN_POINT('Ctrl Pts',(-114.414804744374,0.66309460732753,
125.931015913543));
#102584=CARTESIAN_POINT('Ctrl Pts',(-114.422569497321,0.527691029639202,
125.912592143497));
#102585=CARTESIAN_POINT('Ctrl Pts',(-114.430334250269,0.391341251095219,
125.899791649993));
#102586=CARTESIAN_POINT('Ctrl Pts',(-114.438099003216,0.25455158639704,
125.892702389191));
#102587=CARTESIAN_POINT('Ctrl Pts',(-114.445856044101,0.117897783122235,
125.885620169543));
#102588=CARTESIAN_POINT('Ctrl Pts',(-114.453613084986,-0.0191946489391239,
125.884237914216));
#102589=CARTESIAN_POINT('Ctrl Pts',(-114.461370125871,-0.156212274555154,
125.888592031904));
#102590=CARTESIAN_POINT('Ctrl Pts',(-114.469121317111,-0.293126574114052,
125.892942866119));
#102591=CARTESIAN_POINT('Ctrl Pts',(-114.476872508351,-0.429965790325719,
125.903021450652));
#102592=CARTESIAN_POINT('Ctrl Pts',(-114.484623699591,-0.566214831716947,
125.918812150214));
#102593=CARTESIAN_POINT('Ctrl Pts',(-114.492371596368,-0.702405963631207,
125.934596138308));
#102594=CARTESIAN_POINT('Ctrl Pts',(-114.500119493145,-0.83800703207415,
125.956087367802));
#102595=CARTESIAN_POINT('Ctrl Pts',(-114.507867389922,-0.97250663762478,
125.983218231961));
#102596=CARTESIAN_POINT('Ctrl Pts',(-114.515613666006,-1.1069781087574,
126.010343420928));
#102597=CARTESIAN_POINT('Ctrl Pts',(-114.52335994209,-1.24034819227746,
126.043105820834));
#102598=CARTESIAN_POINT('Ctrl Pts',(-114.531106218175,-1.37211466637587,
126.081386511686));
#102599=CARTESIAN_POINT('Ctrl Pts',(-114.53885255144,-1.50388211314428,
126.119667485117));
#102600=CARTESIAN_POINT('Ctrl Pts',(-114.546598884705,-1.63404555142804,
126.163466721703));
#102601=CARTESIAN_POINT('Ctrl Pts',(-114.554345217971,-1.7621173184631,
126.212615239339));
#102602=CARTESIAN_POINT('Ctrl Pts',(-114.562093285973,-1.89021776628258,
126.261774763444));
#102603=CARTESIAN_POINT('Ctrl Pts',(-114.569841353977,-2.01622524582059,
126.316285812299));
#102604=CARTESIAN_POINT('Ctrl Pts',(-114.57758942198,-2.13967186689895,
126.375931170855));
#102605=CARTESIAN_POINT('Ctrl Pts',(-114.585345724721,-2.26324968851539,
126.435639921207));
#102606=CARTESIAN_POINT('Ctrl Pts',(-114.593102027463,-2.38426086217223,
126.500493711455));
#102607=CARTESIAN_POINT('Ctrl Pts',(-114.600858330205,-2.50226143451527,
126.570228973907));
#102608=CARTESIAN_POINT('Ctrl Pts',(-114.608618772719,-2.62032498731669,
126.640001456167));
#102609=CARTESIAN_POINT('Ctrl Pts',(-114.616379215234,-2.73537440922031,
126.714660389368));
#102610=CARTESIAN_POINT('Ctrl Pts',(-114.624139657748,-2.84699542244294,
126.793899281624));
#102611=CARTESIAN_POINT('Ctrl Pts',(-114.631912558013,-2.95879561962494,
126.873265375183));
#102612=CARTESIAN_POINT('Ctrl Pts',(-114.639685458279,-3.0671561009788,
126.957225880151));
#102613=CARTESIAN_POINT('Ctrl Pts',(-114.647458358544,-3.17169563306927,
127.045433925853));
#102614=CARTESIAN_POINT('Ctrl Pts',(-114.654948694306,-3.27243488985076,
127.130435386913));
#102615=CARTESIAN_POINT('Ctrl Pts',(-114.662439030068,-3.36962594934654,
127.219380724676));
#102616=CARTESIAN_POINT('Ctrl Pts',(-114.66992936583,-3.46296192147884,
127.311929116035));
#102617=CARTESIAN_POINT('Ctrl Pts',(-114.677593179188,-3.55845957241312,
127.406620945676));
#102618=CARTESIAN_POINT('Ctrl Pts',(-114.685256992546,-3.65024229607719,
127.505403328312));
#102619=CARTESIAN_POINT('Ctrl Pts',(-114.692920805904,-3.7379316658509,
127.607948578431));
#102620=CARTESIAN_POINT('Ctrl Pts',(-114.700575663818,-3.82551856741475,
127.710374000704));
#102621=CARTESIAN_POINT('Ctrl Pts',(-114.708230521732,-3.90902136515567,
127.816553246285));
#102622=CARTESIAN_POINT('Ctrl Pts',(-114.715885379645,-3.98809676030264,
127.92612030568));
#102623=CARTESIAN_POINT('Ctrl Pts',(-114.723533062815,-4.06709803967039,
128.035584670072));
#102624=CARTESIAN_POINT('Ctrl Pts',(-114.731180745984,-4.141679934057,128.148430209594));
#102625=CARTESIAN_POINT('Ctrl Pts',(-114.738828429153,-4.21153828487946,
128.264256616251));
#102626=CARTESIAN_POINT('Ctrl Pts',(-114.746470431731,-4.28134474589961,
128.379996988679));
#102627=CARTESIAN_POINT('Ctrl Pts',(-114.754112434309,-4.34643443729279,
128.498713478947));
#102628=CARTESIAN_POINT('Ctrl Pts',(-114.761754436886,-4.4065459059208,
128.61997598076));
#102629=CARTESIAN_POINT('Ctrl Pts',(-114.769393119383,-4.46663125901525,
128.741185799866));
#102630=CARTESIAN_POINT('Ctrl Pts',(-114.777031801879,-4.52174251339146,
128.864939069701));
#102631=CARTESIAN_POINT('Ctrl Pts',(-114.784670484375,-4.57166387757908,
128.990780607492));
#102632=CARTESIAN_POINT('Ctrl Pts',(-114.792308603226,-4.6215815581549,
129.116612859653));
#102633=CARTESIAN_POINT('Ctrl Pts',(-114.799946722077,-4.66630995621222,
129.244532701114));
#102634=CARTESIAN_POINT('Ctrl Pts',(-114.807584840927,-4.70568134977687,
129.374064810097));
#102635=CARTESIAN_POINT('Ctrl Pts',(-114.81165603732,-4.72666670999266,
129.443106764685));
#102636=CARTESIAN_POINT('Ctrl Pts',(-114.815727233713,-4.74613097435518,
129.512606454762));
#102637=CARTESIAN_POINT('Ctrl Pts',(-114.819798430105,-4.76405452823403,
129.582490119308));
#102638=CARTESIAN_POINT('Origin',(213.235140564004,0.,130.804360617566));
#102639=CARTESIAN_POINT('',(-116.915395520338,-4.76405452823393,129.582490119308));
#102640=CARTESIAN_POINT('',(-116.569768711529,-4.764054528234,129.582490119308));
#102641=CARTESIAN_POINT('',(213.235140564004,-4.76405452823405,129.582490119308));
#102642=CARTESIAN_POINT('',(-115.235140564048,-4.91824919069818,130.8015391469));
#102643=CARTESIAN_POINT('Ctrl Pts',(-115.235140564048,-4.91824919069818,
130.801539146901));
#102644=CARTESIAN_POINT('Ctrl Pts',(-115.242812832889,-4.91832654221255,
130.936374510484));
#102645=CARTESIAN_POINT('Ctrl Pts',(-115.25048510173,-4.91285488430728,
131.07143367892));
#102646=CARTESIAN_POINT('Ctrl Pts',(-115.258157370572,-4.90180540092902,
131.20621491196));
#102647=CARTESIAN_POINT('Ctrl Pts',(-115.265821042731,-4.89076829835908,
131.34084512431));
#102648=CARTESIAN_POINT('Ctrl Pts',(-115.273484714891,-4.87416583295605,
131.47519762382));
#102649=CARTESIAN_POINT('Ctrl Pts',(-115.281148387051,-4.85202119112362,
131.608769359057));
#102650=CARTESIAN_POINT('Ctrl Pts',(-115.28880541639,-4.82989574411947,
131.742225315202));
#102651=CARTESIAN_POINT('Ctrl Pts',(-115.29646244573,-4.80223774232766,
131.874901459221));
#102652=CARTESIAN_POINT('Ctrl Pts',(-115.30411947507,-4.76912225105761,
132.006299058988));
#102653=CARTESIAN_POINT('Ctrl Pts',(-115.311772234452,-4.73602522670474,
132.137623384631));
#102654=CARTESIAN_POINT('Ctrl Pts',(-115.319424993835,-4.69747686328041,
132.267670195588));
#102655=CARTESIAN_POINT('Ctrl Pts',(-115.327077753217,-4.6536033832788,
132.395950581607));
#102656=CARTESIAN_POINT('Ctrl Pts',(-115.334728333214,-4.60974239775475,
132.524194435389));
#102657=CARTESIAN_POINT('Ctrl Pts',(-115.342378913211,-4.56055944039268,
132.650672484618));
#102658=CARTESIAN_POINT('Ctrl Pts',(-115.350029493208,-4.50623056509855,
132.774911088037));
#102659=CARTESIAN_POINT('Ctrl Pts',(-115.357679649845,-4.45190469620125,
132.899142816464));
#102660=CARTESIAN_POINT('Ctrl Pts',(-115.365329806482,-4.39243363660449,
133.021134977492));
#102661=CARTESIAN_POINT('Ctrl Pts',(-115.372979963118,-4.3280413287019,
133.140434528971));
#102662=CARTESIAN_POINT('Ctrl Pts',(-115.380631451853,-4.26363780836859,
133.259754853707));
#102663=CARTESIAN_POINT('Ctrl Pts',(-115.388282940587,-4.19431152675196,
133.376381283243));
#102664=CARTESIAN_POINT('Ctrl Pts',(-115.395934429322,-4.12033178794101,
133.489886454303));
#102665=CARTESIAN_POINT('Ctrl Pts',(-115.403593655997,-4.04627723351424,
133.603506412999));
#102666=CARTESIAN_POINT('Ctrl Pts',(-115.411252882673,-3.96756004269017,
133.713998471985));
#102667=CARTESIAN_POINT('Ctrl Pts',(-115.418912109348,-3.88449238319413,
133.820964997893));
#102668=CARTESIAN_POINT('Ctrl Pts',(-115.42657526174,-3.80138214758843,
133.927986349211));
#102669=CARTESIAN_POINT('Ctrl Pts',(-115.434238414132,-3.71391726219272,
134.031478262712));
#102670=CARTESIAN_POINT('Ctrl Pts',(-115.441901566524,-3.62244855016294,
134.131078153505));
#102671=CARTESIAN_POINT('Ctrl Pts',(-115.449576772241,-3.53083596755705,
134.230834704355));
#102672=CARTESIAN_POINT('Ctrl Pts',(-115.457251977958,-3.43520726163659,
134.326686719321));
#102673=CARTESIAN_POINT('Ctrl Pts',(-115.464927183675,-3.33594878756641,
134.41830980775));
#102674=CARTESIAN_POINT('Ctrl Pts',(-115.471845869486,-3.24647389640542,
134.500901908242));
#102675=CARTESIAN_POINT('Ctrl Pts',(-115.478764555298,-3.1540501305834,
134.58005806291));
#102676=CARTESIAN_POINT('Ctrl Pts',(-115.485683241109,-3.05898074154688,
134.655570802085));
#102677=CARTESIAN_POINT('Ctrl Pts',(-115.493457575228,-2.95215392283586,
134.740422359248));
#102678=CARTESIAN_POINT('Ctrl Pts',(-115.501231909347,-2.84162473932073,
134.820960122092));
#102679=CARTESIAN_POINT('Ctrl Pts',(-115.509006243466,-2.72777672697051,
134.896843627952));
#102680=CARTESIAN_POINT('Ctrl Pts',(-115.516770996413,-2.61406902212063,
134.972633614173));
#102681=CARTESIAN_POINT('Ctrl Pts',(-115.52453574936,-2.49705094883447,
135.043780541496));
#102682=CARTESIAN_POINT('Ctrl Pts',(-115.532300502307,-2.37713935628005,
135.109983864359));
#102683=CARTESIAN_POINT('Ctrl Pts',(-115.540057543192,-2.25734686160982,
135.176121433149));
#102684=CARTESIAN_POINT('Ctrl Pts',(-115.547814584077,-2.13466690688147,
135.237324980973));
#102685=CARTESIAN_POINT('Ctrl Pts',(-115.555571624962,-2.00954529007976,
135.293337203562));
#102686=CARTESIAN_POINT('Ctrl Pts',(-115.563322816202,-1.88451802846241,
135.349307186898));
#102687=CARTESIAN_POINT('Ctrl Pts',(-115.571074007442,-1.75705312511785,
135.40009347811));
#102688=CARTESIAN_POINT('Ctrl Pts',(-115.578825198683,-1.62762063008387,
135.445484850661));
#102689=CARTESIAN_POINT('Ctrl Pts',(-115.58657309546,-1.49824314731317,
135.490856930668));
#102690=CARTESIAN_POINT('Ctrl Pts',(-115.594320992237,-1.36690010431146,
135.530838523472));
#102691=CARTESIAN_POINT('Ctrl Pts',(-115.602068889014,-1.23408096182825,
135.565266754233));
#102692=CARTESIAN_POINT('Ctrl Pts',(-115.609815165098,-1.10128960224641,
135.59968778335));
#102693=CARTESIAN_POINT('Ctrl Pts',(-115.617561441182,-0.96702313555767,
135.62855766296));
#102694=CARTESIAN_POINT('Ctrl Pts',(-115.625307717266,-0.831785212293523,
135.651763677258));
#102695=CARTESIAN_POINT('Ctrl Pts',(-115.633054050531,-0.696546290733931,
135.674969862858));
#102696=CARTESIAN_POINT('Ctrl Pts',(-115.640800383796,-0.560336283622972,
135.692512033598));
#102697=CARTESIAN_POINT('Ctrl Pts',(-115.648546717062,-0.423667644642334,
135.704328861278));
#102698=CARTESIAN_POINT('Ctrl Pts',(-115.656294785065,-0.286968399667777,
135.716148335254));
#102699=CARTESIAN_POINT('Ctrl Pts',(-115.664042853068,-0.149810707885037,
135.722239881167));
#102700=CARTESIAN_POINT('Ctrl Pts',(-115.671790921071,-0.0127103376618529,
135.722594193741));
#102701=CARTESIAN_POINT('Ctrl Pts',(-115.679547223812,0.124535744466881,
135.722948882883));
#102702=CARTESIAN_POINT('Ctrl Pts',(-115.687303526554,0.261723991750434,
135.717554157062));
#102703=CARTESIAN_POINT('Ctrl Pts',(-115.695059829296,0.398339888344879,
135.706452864337));
#102704=CARTESIAN_POINT('Ctrl Pts',(-115.70282027181,0.535028700956762,
135.695345646518));
#102705=CARTESIAN_POINT('Ctrl Pts',(-115.710580714325,0.671144166359014,
135.678525840771));
#102706=CARTESIAN_POINT('Ctrl Pts',(-115.718341156839,0.806179681484734,
135.656087875323));
#102707=CARTESIAN_POINT('Ctrl Pts',(-115.726114057104,0.941431967607224,
135.633613890461));
#102708=CARTESIAN_POINT('Ctrl Pts',(-115.73388695737,1.0756004562268,135.605503803742));
#102709=CARTESIAN_POINT('Ctrl Pts',(-115.741659857635,1.20819059981851,
135.571902807941));
#102710=CARTESIAN_POINT('Ctrl Pts',(-115.749150193397,1.33596075772162,
135.539523292973));
#102711=CARTESIAN_POINT('Ctrl Pts',(-115.75664052916,1.46226503664722,135.502045242308));
#102712=CARTESIAN_POINT('Ctrl Pts',(-115.764130864922,1.58667838962518,
135.459640926033));
#102713=CARTESIAN_POINT('Ctrl Pts',(-115.771905199041,1.715808912691,135.415628837219));
#102714=CARTESIAN_POINT('Ctrl Pts',(-115.77967953316,1.84331133703511,135.366170132839));
#102715=CARTESIAN_POINT('Ctrl Pts',(-115.787453867279,1.96869191121559,
135.31140346418));
#102716=CARTESIAN_POINT('Ctrl Pts',(-115.795218620226,2.09391796504398,
135.256704290545));
#102717=CARTESIAN_POINT('Ctrl Pts',(-115.802983373173,2.21702701692301,
135.196710323443));
#102718=CARTESIAN_POINT('Ctrl Pts',(-115.810748126121,2.3375408922028,135.131609817668));
#102719=CARTESIAN_POINT('Ctrl Pts',(-115.818505167006,2.45793507140303,
135.066573970632));
#102720=CARTESIAN_POINT('Ctrl Pts',(-115.826262207891,2.57573886171761,
134.99644186282));
#102721=CARTESIAN_POINT('Ctrl Pts',(-115.834019248776,2.69049482107732,
134.921449477459));
#102722=CARTESIAN_POINT('Ctrl Pts',(-115.841770440016,2.80516424207525,
134.84651364444));
#102723=CARTESIAN_POINT('Ctrl Pts',(-115.849521631256,2.91679008097579,
134.766725042186));
#102724=CARTESIAN_POINT('Ctrl Pts',(-115.857272822496,3.02494055338384,
134.682364964004));
#102725=CARTESIAN_POINT('Ctrl Pts',(-115.865020719273,3.13304505895596,
134.598040741106));
#102726=CARTESIAN_POINT('Ctrl Pts',(-115.87276861605,3.23767682829374,134.509149146715));
#102727=CARTESIAN_POINT('Ctrl Pts',(-115.880516512828,3.33843426469115,
134.416013940192));
#102728=CARTESIAN_POINT('Ctrl Pts',(-115.888262788912,3.43917062480496,
134.322898215547));
#102729=CARTESIAN_POINT('Ctrl Pts',(-115.896009064996,3.53603397704364,
134.225540909612));
#102730=CARTESIAN_POINT('Ctrl Pts',(-115.90375534108,3.62865725499519,134.124304832198));
#102731=CARTESIAN_POINT('Ctrl Pts',(-115.911501674345,3.72128121667087,
134.023068007483));
#102732=CARTESIAN_POINT('Ctrl Pts',(-115.919248007611,3.80966477769252,
133.917952642608));
#102733=CARTESIAN_POINT('Ctrl Pts',(-115.926994340876,3.8934793471757,133.809356729979));
#102734=CARTESIAN_POINT('Ctrl Pts',(-115.934742408879,3.9773126863507,133.700736498048));
#102735=CARTESIAN_POINT('Ctrl Pts',(-115.942490476882,4.05657475911999,
133.588634476802));
#102736=CARTESIAN_POINT('Ctrl Pts',(-115.950238544885,4.13097895129165,
133.473479567048));
#102737=CARTESIAN_POINT('Ctrl Pts',(-115.957994847627,4.20546222112427,
133.358202269286));
#102738=CARTESIAN_POINT('Ctrl Pts',(-115.965751150369,4.2750770841701,133.239865930393));
#102739=CARTESIAN_POINT('Ctrl Pts',(-115.973507453111,4.33958148133343,
133.118926587541));
#102740=CARTESIAN_POINT('Ctrl Pts',(-115.981267895625,4.40412030643554,
132.997922695722));
#102741=CARTESIAN_POINT('Ctrl Pts',(-115.989028338139,4.46354306135324,
132.874313383835));
#102742=CARTESIAN_POINT('Ctrl Pts',(-115.996788780653,4.51765535989615,
132.748575912152));
#102743=CARTESIAN_POINT('Ctrl Pts',(-116.004561680919,4.57185452430455,
132.622636595517));
#102744=CARTESIAN_POINT('Ctrl Pts',(-116.012334581184,4.62072605757451,
132.494562657693));
#102745=CARTESIAN_POINT('Ctrl Pts',(-116.02010748145,4.66412479948301,132.36484865576));
#102746=CARTESIAN_POINT('Ctrl Pts',(-116.027597817212,4.70594588780654,
132.239850084533));
#102747=CARTESIAN_POINT('Ctrl Pts',(-116.035088152973,4.74268509025783,
132.113328915723));
#102748=CARTESIAN_POINT('Ctrl Pts',(-116.042578488735,4.77425759426975,
131.985735869574));
#102749=CARTESIAN_POINT('Ctrl Pts',(-116.050352822854,4.80702717936878,
131.853305094294));
#102750=CARTESIAN_POINT('Ctrl Pts',(-116.058127156973,4.83433434540856,
131.719300055825));
#102751=CARTESIAN_POINT('Ctrl Pts',(-116.065901491092,4.85602885892827,
131.584211105644));
#102752=CARTESIAN_POINT('Ctrl Pts',(-116.073666244039,4.87769663589896,
131.449288640522));
#102753=CARTESIAN_POINT('Ctrl Pts',(-116.081430996986,4.89376546190486,
131.313285303894));
#102754=CARTESIAN_POINT('Ctrl Pts',(-116.089195749933,4.90413525595736,
131.176705153951));
#102755=CARTESIAN_POINT('Ctrl Pts',(-116.096952790818,4.91449475058421,
131.040260657339));
#102756=CARTESIAN_POINT('Ctrl Pts',(-116.104709831703,4.9191664482201,130.903240874827));
#102757=CARTESIAN_POINT('Ctrl Pts',(-116.112466872588,4.91810162962566,
130.766158220083));
#102758=CARTESIAN_POINT('Ctrl Pts',(-116.120218063829,4.9170376140192,130.629178940435));
#102759=CARTESIAN_POINT('Ctrl Pts',(-116.127969255069,4.91024569575109,
130.492137272298));
#102760=CARTESIAN_POINT('Ctrl Pts',(-116.135720446309,4.89772914483416,
130.355548534014));
#102761=CARTESIAN_POINT('Ctrl Pts',(-116.143468343086,4.88521791378525,
130.219017849588));
#102762=CARTESIAN_POINT('Ctrl Pts',(-116.151216239863,4.86698692498344,
130.082940100653));
#102763=CARTESIAN_POINT('Ctrl Pts',(-116.15896413664,4.84309149351998,129.947828161734));
#102764=CARTESIAN_POINT('Ctrl Pts',(-116.166710412724,4.81920106046559,
129.812744485319));
#102765=CARTESIAN_POINT('Ctrl Pts',(-116.174456688808,4.78964860958437,
129.678626601826));
#102766=CARTESIAN_POINT('Ctrl Pts',(-116.182202964892,4.75454097468424,
129.545979442187));
#102767=CARTESIAN_POINT('Ctrl Pts',(-116.189949298158,4.71943308062757,
129.413331303377));
#102768=CARTESIAN_POINT('Ctrl Pts',(-116.197695631423,4.67877002075748,
129.282154288037));
#102769=CARTESIAN_POINT('Ctrl Pts',(-116.205441964689,4.63270902595703,
129.1529399736));
#102770=CARTESIAN_POINT('Ctrl Pts',(-116.213190032692,4.58663771611622,
129.023696722514));
#102771=CARTESIAN_POINT('Ctrl Pts',(-116.220938100695,4.53516619716396,
128.896417415148));
#102772=CARTESIAN_POINT('Ctrl Pts',(-116.228686168698,4.47850039352463,
128.771575019501));
#102773=CARTESIAN_POINT('Ctrl Pts',(-116.236442471439,4.42177436479494,
128.646599939871));
#102774=CARTESIAN_POINT('Ctrl Pts',(-116.244198774181,4.35984318533914,
128.524067302298));
#102775=CARTESIAN_POINT('Ctrl Pts',(-116.251955076923,4.29295969329342,
128.404427257187));
#102776=CARTESIAN_POINT('Ctrl Pts',(-116.259715519437,4.22604050351418,
128.284723356582));
#102777=CARTESIAN_POINT('Ctrl Pts',(-116.267475961951,4.15416393914136,
128.16791545753));
#102778=CARTESIAN_POINT('Ctrl Pts',(-116.275236404466,4.07762646227381,
128.054425073473));
#102779=CARTESIAN_POINT('Ctrl Pts',(-116.283009304731,4.00096612065349,
127.940752504576));
#102780=CARTESIAN_POINT('Ctrl Pts',(-116.290782204996,3.91963014700623,
127.830408407749));
#102781=CARTESIAN_POINT('Ctrl Pts',(-116.298555105262,3.83395616356444,
127.72378223058));
#102782=CARTESIAN_POINT('Ctrl Pts',(-116.306045441024,3.75139664522004,
127.621032183526));
#102783=CARTESIAN_POINT('Ctrl Pts',(-116.313535776786,3.66480923896074,
127.521734669797));
#102784=CARTESIAN_POINT('Ctrl Pts',(-116.321026112548,3.57452730522823,
127.426204669911));
#102785=CARTESIAN_POINT('Ctrl Pts',(-116.328800446667,3.48082230453882,
127.327052621044));
#102786=CARTESIAN_POINT('Ctrl Pts',(-116.336574780786,3.38284026071406,
127.231645332329));
#102787=CARTESIAN_POINT('Ctrl Pts',(-116.344349114905,3.28091251548542,
127.140374246381));
#102788=CARTESIAN_POINT('Ctrl Pts',(-116.352113867852,3.17911038709295,
127.049215643889));
#102789=CARTESIAN_POINT('Ctrl Pts',(-116.359878620799,3.07337252113294,
126.962183359964));
#102790=CARTESIAN_POINT('Ctrl Pts',(-116.367643373746,2.96406889981733,
126.879634051341));
#102791=CARTESIAN_POINT('Ctrl Pts',(-116.375400414631,2.85487384039962,
126.797166731854));
#102792=CARTESIAN_POINT('Ctrl Pts',(-116.383157455516,2.74212038345597,
126.719173760982));
#102793=CARTESIAN_POINT('Ctrl Pts',(-116.390914496401,2.62621330317779,
126.645973099704));
#102794=CARTESIAN_POINT('Ctrl Pts',(-116.398665687641,2.51039362933032,
126.572827639613));
#102795=CARTESIAN_POINT('Ctrl Pts',(-116.406416878881,2.39142539497933,
126.504467503753));
#102796=CARTESIAN_POINT('Ctrl Pts',(-116.414168070121,2.26974391956358,
126.441168483119));
#102797=CARTESIAN_POINT('Ctrl Pts',(-116.421915966899,2.14811416202067,
126.377896366257));
#102798=CARTESIAN_POINT('Ctrl Pts',(-116.429663863676,2.02377380315551,
126.319681266281));
#102799=CARTESIAN_POINT('Ctrl Pts',(-116.437411760453,1.89718423799002,
126.266753866246));
#102800=CARTESIAN_POINT('Ctrl Pts',(-116.445158036537,1.77062115263295,
126.213837537483));
#102801=CARTESIAN_POINT('Ctrl Pts',(-116.452904312621,1.64181015727526,
126.166206859339));
#102802=CARTESIAN_POINT('Ctrl Pts',(-116.460650588705,1.51123381089445,
126.124044877009));
#102803=CARTESIAN_POINT('Ctrl Pts',(-116.46839692197,1.38065650062817,126.081882583448));
#102804=CARTESIAN_POINT('Ctrl Pts',(-116.476143255236,1.24831418538666,
126.045189186386));
#102805=CARTESIAN_POINT('Ctrl Pts',(-116.483889588501,1.11470543032008,
126.014098112638));
#102806=CARTESIAN_POINT('Ctrl Pts',(-116.491637656504,0.981066754499727,
125.983000076261));
#102807=CARTESIAN_POINT('Ctrl Pts',(-116.499385724507,0.846161455220684,
125.957506948303));
#102808=CARTESIAN_POINT('Ctrl Pts',(-116.50713379251,0.710498761037574,
125.937701129471));
#102809=CARTESIAN_POINT('Ctrl Pts',(-116.514890095251,0.574691882928494,
125.91787426078));
#102810=CARTESIAN_POINT('Ctrl Pts',(-116.522646397993,0.438126389385423,
125.903746832403));
#102811=CARTESIAN_POINT('Ctrl Pts',(-116.530402700735,0.30131766988116,
125.895349441747));
#102812=CARTESIAN_POINT('Ctrl Pts',(-116.538163143249,0.164435931443695,
125.88694756915));
#102813=CARTESIAN_POINT('Ctrl Pts',(-116.545923585763,0.0273110990737119,
125.884281835777));
#102814=CARTESIAN_POINT('Ctrl Pts',(-116.553684028278,-0.109541951026601,
125.88733065798));
#102815=CARTESIAN_POINT('Ctrl Pts',(-116.561456928543,-0.246614689792179,
125.890384374423));
#102816=CARTESIAN_POINT('Ctrl Pts',(-116.569229828808,-0.383414384057801,
125.899170952967));
#102817=CARTESIAN_POINT('Ctrl Pts',(-116.577002729074,-0.519430887473454,
125.9136168484));
#102818=CARTESIAN_POINT('Ctrl Pts',(-116.584493064836,-0.650502848391687,
125.927537599148));
#102819=CARTESIAN_POINT('Ctrl Pts',(-116.591983400599,-0.780847267046429,
125.94671330467));
#102820=CARTESIAN_POINT('Ctrl Pts',(-116.599473736361,-0.91001895194746,
125.971033754049));
#102821=CARTESIAN_POINT('Ctrl Pts',(-116.60724807048,-1.04408822053579,
125.996276320657));
#102822=CARTESIAN_POINT('Ctrl Pts',(-116.615022404599,-1.17731876263939,
126.027141419119));
#102823=CARTESIAN_POINT('Ctrl Pts',(-116.622796738718,-1.30920214819879,
126.063561866548));
#102824=CARTESIAN_POINT('Ctrl Pts',(-116.630561491665,-1.4409229992726,
126.099937429032));
#102825=CARTESIAN_POINT('Ctrl Pts',(-116.638326244612,-1.57129962396362,
126.141854614973));
#102826=CARTESIAN_POINT('Ctrl Pts',(-116.646090997559,-1.69983197243749,
126.189194929535));
#102827=CARTESIAN_POINT('Ctrl Pts',(-116.653848038444,-1.82823666077086,
126.236488225029));
#102828=CARTESIAN_POINT('Ctrl Pts',(-116.66160507933,-1.95480035367621,
126.28919379586));
#102829=CARTESIAN_POINT('Ctrl Pts',(-116.669362120215,-2.07903675123895,
126.347142959711));
#102830=CARTESIAN_POINT('Ctrl Pts',(-116.677113311455,-2.20317946116737,
126.405048423646));
#102831=CARTESIAN_POINT('Ctrl Pts',(-116.684864502695,-2.32499801615418,
126.468189445339));
#102832=CARTESIAN_POINT('Ctrl Pts',(-116.692615693935,-2.44402508463241,
126.536348849988));
#102833=CARTESIAN_POINT('Ctrl Pts',(-116.700363590712,-2.56300156343187,
126.604479285071));
#102834=CARTESIAN_POINT('Ctrl Pts',(-116.708111487489,-2.67918857692805,
126.677623666967));
#102835=CARTESIAN_POINT('Ctrl Pts',(-116.715859384266,-2.79214264965307,
126.755518500801));
#102836=CARTESIAN_POINT('Ctrl Pts',(-116.72360566035,-2.90507309482109,
126.833397040716));
#102837=CARTESIAN_POINT('Ctrl Pts',(-116.731351936434,-3.01477162268949,
126.916023834247));
#102838=CARTESIAN_POINT('Ctrl Pts',(-116.739098212518,-3.12082339723724,
127.003091831258));
#102839=CARTESIAN_POINT('Ctrl Pts',(-116.746844545784,-3.22687595463467,
127.090160470986));
#102840=CARTESIAN_POINT('Ctrl Pts',(-116.754590879049,-3.32928140282224,
127.18167013153));
#102841=CARTESIAN_POINT('Ctrl Pts',(-116.762337212314,-3.42765799939943,
127.277273476361));
#102842=CARTESIAN_POINT('Ctrl Pts',(-116.770085280317,-3.52605662673347,
127.372898230899));
#102843=CARTESIAN_POINT('Ctrl Pts',(-116.77783334832,-3.62042432679295,
127.472618221534));
#102844=CARTESIAN_POINT('Ctrl Pts',(-116.785581416323,-3.71041652305749,
127.576049559455));
#102845=CARTESIAN_POINT('Ctrl Pts',(-116.793337719065,-3.80050436409951,
127.679590825433));
#102846=CARTESIAN_POINT('Ctrl Pts',(-116.801094021807,-3.88620715475995,
127.786851022769));
#102847=CARTESIAN_POINT('Ctrl Pts',(-116.808850324549,-3.96722057197679,
127.897413078345));
#102848=CARTESIAN_POINT('Ctrl Pts',(-116.816610767063,-4.04827722849366,
128.008034144219));
#102849=CARTESIAN_POINT('Ctrl Pts',(-116.824371209577,-4.12463930683379,
128.121960255267));
#102850=CARTESIAN_POINT('Ctrl Pts',(-116.832131652091,-4.19604666276836,
128.238746565069));
#102851=CARTESIAN_POINT('Ctrl Pts',(-116.839904552357,-4.26756864812992,
128.355720350623));
#102852=CARTESIAN_POINT('Ctrl Pts',(-116.847677452622,-4.33411982702114,
128.475563168104));
#102853=CARTESIAN_POINT('Ctrl Pts',(-116.855450352887,-4.39548632854803,
128.597806063958));
#102854=CARTESIAN_POINT('Ctrl Pts',(-116.862940688649,-4.45462200317053,
128.715605122634));
#102855=CARTESIAN_POINT('Ctrl Pts',(-116.870431024411,-4.5089432811492,
128.835632510814));
#102856=CARTESIAN_POINT('Ctrl Pts',(-116.877921360173,-4.55830224917604,
128.957454104594));
#102857=CARTESIAN_POINT('Ctrl Pts',(-116.886665625701,-4.61592422185459,
129.099669406678));
#102858=CARTESIAN_POINT('Ctrl Pts',(-116.895409891229,-4.66693782596252,
129.244709120248));
#102859=CARTESIAN_POINT('Ctrl Pts',(-116.904154156758,-4.71108977676246,
129.391981002241));
#102860=CARTESIAN_POINT('Ctrl Pts',(-116.907901277951,-4.73000991477147,
129.455090429609));
#102861=CARTESIAN_POINT('Ctrl Pts',(-116.911648399145,-4.7476706039676,
129.518609447254));
#102862=CARTESIAN_POINT('Ctrl Pts',(-116.915395520338,-4.76405452823392,
129.582490119308));
#102863=CARTESIAN_POINT('Ctrl Pts',(-115.165057694931,-4.76405452823392,
129.582490119308));
#102864=CARTESIAN_POINT('Ctrl Pts',(-115.17283102114,-4.79810730784155,
129.715261390175));
#102865=CARTESIAN_POINT('Ctrl Pts',(-115.180604347349,-4.82656804915046,
129.849311089595));
#102866=CARTESIAN_POINT('Ctrl Pts',(-115.188377673557,-4.8493713020677,
129.984128310727));
#102867=CARTESIAN_POINT('Ctrl Pts',(-115.194663654803,-4.8678113901763,
130.093149661552));
#102868=CARTESIAN_POINT('Ctrl Pts',(-115.200949636049,-4.88255285482992,
130.202672705539));
#102869=CARTESIAN_POINT('Ctrl Pts',(-115.207235617295,-4.89358601074035,
130.31242666063));
#102870=CARTESIAN_POINT('Ctrl Pts',(-115.2165372662,-4.9099122673069,130.474834519684));
#102871=CARTESIAN_POINT('Ctrl Pts',(-115.225838915105,-4.91815541181523,
130.638068439213));
#102872=CARTESIAN_POINT('Ctrl Pts',(-115.23514056401,-4.9182491906978,130.801539146235));
#102873=CARTESIAN_POINT('',(-114.889859435954,-4.91824797553828,130.808823084782));
#102874=CARTESIAN_POINT('Ctrl Pts',(-114.819798430105,-4.76405452823403,
129.582490119308));
#102875=CARTESIAN_POINT('Ctrl Pts',(-114.827439539859,-4.79769472368095,
129.713652730795));
#102876=CARTESIAN_POINT('Ctrl Pts',(-114.835080649612,-4.82590446010578,
129.846168403197));
#102877=CARTESIAN_POINT('Ctrl Pts',(-114.842721759365,-4.84859321787777,
129.979541322175));
#102878=CARTESIAN_POINT('Ctrl Pts',(-114.850578038796,-4.87192087927397,
130.116669953217));
#102879=CARTESIAN_POINT('Ctrl Pts',(-114.858434318228,-4.88941194984212,
130.254704374717));
#102880=CARTESIAN_POINT('Ctrl Pts',(-114.866290597659,-4.90102515160505,
130.393099720039));
#102881=CARTESIAN_POINT('Ctrl Pts',(-114.874146877091,-4.91263835336799,
130.531495065361));
#102882=CARTESIAN_POINT('Ctrl Pts',(-114.882003156522,-4.9183737060733,
130.670250873629));
#102883=CARTESIAN_POINT('Ctrl Pts',(-114.889859435954,-4.91824797553828,
130.808823084782));
#102884=CARTESIAN_POINT('Ctrl Pts',(-114.889859435992,-4.91824797553766,
130.808823085458));
#102885=CARTESIAN_POINT('Ctrl Pts',(-114.900749617536,-4.91807369093242,
131.000908480268));
#102886=CARTESIAN_POINT('Ctrl Pts',(-114.911639799079,-4.90664298984596,
131.19250429803));
#102887=CARTESIAN_POINT('Ctrl Pts',(-114.922529980623,-4.88414751305809,
131.382535446825));
#102888=CARTESIAN_POINT('Ctrl Pts',(-114.931145650296,-4.8663504179064,
131.532876889631));
#102889=CARTESIAN_POINT('Ctrl Pts',(-114.93976131997,-4.84162875804521,
131.682239922326));
#102890=CARTESIAN_POINT('Ctrl Pts',(-114.948376989643,-4.8100970391455,
131.830104024322));
#102891=CARTESIAN_POINT('Ctrl Pts',(-114.956151323762,-4.78164444899655,
131.963528932277));
#102892=CARTESIAN_POINT('Ctrl Pts',(-114.963925657881,-4.74759107326653,
132.095980430018));
#102893=CARTESIAN_POINT('Ctrl Pts',(-114.971699992,-4.7080162764146,132.226951846105));
#102894=CARTESIAN_POINT('Ctrl Pts',(-114.979464744948,-4.66849025196288,
132.357761851627));
#102895=CARTESIAN_POINT('Ctrl Pts',(-114.987229497895,-4.62345645763071,
132.487095034187));
#102896=CARTESIAN_POINT('Ctrl Pts',(-114.994994250842,-4.57304535394844,
132.614454331502));
#102897=CARTESIAN_POINT('Ctrl Pts',(-115.002751291727,-4.52268431928502,
132.741687133768));
#102898=CARTESIAN_POINT('Ctrl Pts',(-115.010508332612,-4.46695674670145,
132.866949591082));
#102899=CARTESIAN_POINT('Ctrl Pts',(-115.018265373497,-4.40604293979356,
132.989759591483));
#102900=CARTESIAN_POINT('Ctrl Pts',(-115.026016564737,-4.34517506846139,
133.112476979906));
#102901=CARTESIAN_POINT('Ctrl Pts',(-115.033767755977,-4.27912892039318,
133.232745243738));
#102902=CARTESIAN_POINT('Ctrl Pts',(-115.041518947217,-4.2081328225189,
133.350102397586));
#102903=CARTESIAN_POINT('Ctrl Pts',(-115.049266843994,-4.13716689988001,
133.467409671513));
#102904=CARTESIAN_POINT('Ctrl Pts',(-115.057014740772,-4.06125541379793,
133.581807962536));
#102905=CARTESIAN_POINT('Ctrl Pts',(-115.064762637549,-3.9806724254539,
133.692860246046));
#102906=CARTESIAN_POINT('Ctrl Pts',(-115.072508913633,-3.90010629333387,
133.803889299813));
#102907=CARTESIAN_POINT('Ctrl Pts',(-115.080255189717,-3.81487083208093,
133.911573421998));
#102908=CARTESIAN_POINT('Ctrl Pts',(-115.088001465801,-3.72528295832849,
134.015505264399));
#102909=CARTESIAN_POINT('Ctrl Pts',(-115.095747799066,-3.63569442325884,
134.119437874002));
#102910=CARTESIAN_POINT('Ctrl Pts',(-115.103494132331,-3.54175366684228,
134.219617852418));
#102911=CARTESIAN_POINT('Ctrl Pts',(-115.111240465597,-3.44381708634754,
134.315671902297));
#102912=CARTESIAN_POINT('Ctrl Pts',(-115.1189885336,-3.34585857363477,134.411747462815));
#102913=CARTESIAN_POINT('Ctrl Pts',(-115.126736601603,-3.24390273529196,
134.503694982491));
#102914=CARTESIAN_POINT('Ctrl Pts',(-115.134484669606,-3.13834161846558,
134.591179196308));
#102915=CARTESIAN_POINT('Ctrl Pts',(-115.142240972347,-3.0326683100279,
134.678756389389));
#102916=CARTESIAN_POINT('Ctrl Pts',(-115.149997275089,-2.92338237031208,
134.761860550775));
#102917=CARTESIAN_POINT('Ctrl Pts',(-115.157753577831,-2.8109080552413,
134.840197453648));
#102918=CARTESIAN_POINT('Ctrl Pts',(-115.165514020345,-2.69837370924173,
134.918576167286));
#102919=CARTESIAN_POINT('Ctrl Pts',(-115.173274462859,-2.58264792677154,
134.992182342697));
#102920=CARTESIAN_POINT('Ctrl Pts',(-115.181034905374,-2.46418166889047,
135.060766585657));
#102921=CARTESIAN_POINT('Ctrl Pts',(-115.188807805639,-2.34552523845531,
135.129460926133));
#102922=CARTESIAN_POINT('Ctrl Pts',(-115.196580705904,-2.22411988795204,
135.193117042752));
#102923=CARTESIAN_POINT('Ctrl Pts',(-115.20435360617,-2.10043956820091,
135.251532379803));
#102924=CARTESIAN_POINT('Ctrl Pts',(-115.211843941932,-1.98125533960332,
135.307824172213));
#102925=CARTESIAN_POINT('Ctrl Pts',(-115.219334277694,-1.85995895545075,
135.359249480642));
#102926=CARTESIAN_POINT('Ctrl Pts',(-115.226824613456,-1.73698796414032,
135.405670852155));
#102927=CARTESIAN_POINT('Ctrl Pts',(-115.234598947575,-1.60935449031939,
135.453852304077));
#102928=CARTESIAN_POINT('Ctrl Pts',(-115.242373281694,-1.47951261266629,
135.496795504471));
#102929=CARTESIAN_POINT('Ctrl Pts',(-115.250147615813,-1.34793150664207,
135.534293356612));
#102930=CARTESIAN_POINT('Ctrl Pts',(-115.257912368761,-1.21651256257163,
135.571744996002));
#102931=CARTESIAN_POINT('Ctrl Pts',(-115.265677121708,-1.08335902732966,
135.60376453372));
#102932=CARTESIAN_POINT('Ctrl Pts',(-115.273441874655,-0.948959610595738,
135.630193055598));
#102933=CARTESIAN_POINT('Ctrl Pts',(-115.28119891554,-0.814693681257212,
135.656595328295));
#102934=CARTESIAN_POINT('Ctrl Pts',(-115.288955956425,-0.679184714098721,
135.677417561077));
#102935=CARTESIAN_POINT('Ctrl Pts',(-115.29671299731,-0.54293578206554,
135.692550855175));
#102936=CARTESIAN_POINT('Ctrl Pts',(-115.30446418855,-0.406789596411682,
135.707672737137));
#102937=CARTESIAN_POINT('Ctrl Pts',(-115.31221537979,-0.269904943578103,
135.71711417656));
#102938=CARTESIAN_POINT('Ctrl Pts',(-115.31996657103,-0.132793921240878,
135.720817556967));
#102939=CARTESIAN_POINT('Ctrl Pts',(-115.327714467807,0.00425882525448443,
135.724519363338));
#102940=CARTESIAN_POINT('Ctrl Pts',(-115.335462364584,0.141537359888569,
135.722487950804));
#102941=CARTESIAN_POINT('Ctrl Pts',(-115.343210261361,0.278525864719153,
135.714717672321));
#102942=CARTESIAN_POINT('Ctrl Pts',(-115.350956537445,0.415485714507284,
135.706949019213));
#102943=CARTESIAN_POINT('Ctrl Pts',(-115.35870281353,0.552155265073385,
135.693443910039));
#102944=CARTESIAN_POINT('Ctrl Pts',(-115.366449089614,0.688020501657005,
135.674248794085));
#102945=CARTESIAN_POINT('Ctrl Pts',(-115.374195422879,0.823886741167122,
135.655053536437));
#102946=CARTESIAN_POINT('Ctrl Pts',(-115.381941756144,0.95894826772659,
135.630168242889));
#102947=CARTESIAN_POINT('Ctrl Pts',(-115.38968808941,1.09269837427396,135.599690984221));
#102948=CARTESIAN_POINT('Ctrl Pts',(-115.397436157413,1.22647843323052,
135.569206900382));
#102949=CARTESIAN_POINT('Ctrl Pts',(-115.405184225416,1.35894610665796,
135.533128446372));
#102950=CARTESIAN_POINT('Ctrl Pts',(-115.412932293419,1.48960741554254,
135.491604243628));
#102951=CARTESIAN_POINT('Ctrl Pts',(-115.420688596161,1.62040759282092,
135.450035908467));
#102952=CARTESIAN_POINT('Ctrl Pts',(-115.428444898902,1.74939719730176,
135.403010381407));
#102953=CARTESIAN_POINT('Ctrl Pts',(-115.436201201644,1.87609936693917,
135.350725564188));
#102954=CARTESIAN_POINT('Ctrl Pts',(-115.443961644158,2.00286916133944,
135.298412840987));
#102955=CARTESIAN_POINT('Ctrl Pts',(-115.451722086673,2.12734873353291,
135.240835398411));
#102956=CARTESIAN_POINT('Ctrl Pts',(-115.459482529187,2.24908450562575,
135.1782378391));
#102957=CARTESIAN_POINT('Ctrl Pts',(-115.467255429452,2.37101569878714,
135.11553979263));
#102958=CARTESIAN_POINT('Ctrl Pts',(-115.475028329718,2.49019394997115,
135.047805718793));
#102959=CARTESIAN_POINT('Ctrl Pts',(-115.482801229983,2.60619266132521,
134.975324879527));
#102960=CARTESIAN_POINT('Ctrl Pts',(-115.490291565745,2.71797452733748,
134.905478901337));
#102961=CARTESIAN_POINT('Ctrl Pts',(-115.497781901507,2.8268037542206,134.831225453398));
#102962=CARTESIAN_POINT('Ctrl Pts',(-115.505272237269,2.93232819333034,
134.752858360898));
#102963=CARTESIAN_POINT('Ctrl Pts',(-115.513046571388,3.04185362362315,
134.671519956267));
#102964=CARTESIAN_POINT('Ctrl Pts',(-115.520820905507,3.14816566076399,
134.585492156043));
#102965=CARTESIAN_POINT('Ctrl Pts',(-115.528595239626,3.25083646761813,
134.495057749993));
#102966=CARTESIAN_POINT('Ctrl Pts',(-115.536359992573,3.35338074187878,
134.404734796266));
#102967=CARTESIAN_POINT('Ctrl Pts',(-115.54412474552,3.4522924240549,134.31001629822));
#102968=CARTESIAN_POINT('Ctrl Pts',(-115.551889498467,3.54717365563843,
134.21122752416));
#102969=CARTESIAN_POINT('Ctrl Pts',(-115.559646539352,3.64196064984516,
134.112536868503));
#102970=CARTESIAN_POINT('Ctrl Pts',(-115.567403580237,3.73272489074091,
134.009784262049));
#102971=CARTESIAN_POINT('Ctrl Pts',(-115.575160621122,3.81910283549119,
133.903334091871));
#102972=CARTESIAN_POINT('Ctrl Pts',(-115.582911812363,3.90541564196153,
133.796964196593));
#102973=CARTESIAN_POINT('Ctrl Pts',(-115.590663003603,3.9873484907932,133.686902590017));
#102974=CARTESIAN_POINT('Ctrl Pts',(-115.598414194843,4.06457610631102,
133.573548971309));
#102975=CARTESIAN_POINT('Ctrl Pts',(-115.60616209162,4.14177089803202,133.460243530913));
#102976=CARTESIAN_POINT('Ctrl Pts',(-115.613909988397,4.21426421431816,
133.3436491837));
#102977=CARTESIAN_POINT('Ctrl Pts',(-115.621657885174,4.28177249195604,
133.224196849551));
#102978=CARTESIAN_POINT('Ctrl Pts',(-115.629404161258,4.34926664831774,
133.104769502255));
#102979=CARTESIAN_POINT('Ctrl Pts',(-115.637150437342,4.41177764790559,
132.982485697291));
#102980=CARTESIAN_POINT('Ctrl Pts',(-115.644896713427,4.46906673228595,
132.85780299681));
#102981=CARTESIAN_POINT('Ctrl Pts',(-115.652643046692,4.52635623956123,
132.733119375949));
#102982=CARTESIAN_POINT('Ctrl Pts',(-115.660389379957,4.57842359147752,
132.606037179494));
#102983=CARTESIAN_POINT('Ctrl Pts',(-115.668135713223,4.62507741021612,
132.477035724097));
#102984=CARTESIAN_POINT('Ctrl Pts',(-115.675883781226,4.67174167675389,
132.348005379719));
#102985=CARTESIAN_POINT('Ctrl Pts',(-115.683631849229,4.71298986479103,
132.217055288728));
#102986=CARTESIAN_POINT('Ctrl Pts',(-115.691379917232,4.74868000602797,
132.084681383175));
#102987=CARTESIAN_POINT('Ctrl Pts',(-115.699136219973,4.78440807917179,
131.95216678906));
#102988=CARTESIAN_POINT('Ctrl Pts',(-115.706892522715,4.81456620339192,
131.818225735596));
#102989=CARTESIAN_POINT('Ctrl Pts',(-115.714648825457,4.83906312344394,
131.683366391054));
#102990=CARTESIAN_POINT('Ctrl Pts',(-115.722409267971,4.86357311823978,
131.548435068019));
#102991=CARTESIAN_POINT('Ctrl Pts',(-115.730169710485,4.88241583447588,
131.412584864368));
#102992=CARTESIAN_POINT('Ctrl Pts',(-115.737930153,4.89555189335025,131.276329601732));
#102993=CARTESIAN_POINT('Ctrl Pts',(-115.745703053265,4.90870903939248,
131.139855610052));
#102994=CARTESIAN_POINT('Ctrl Pts',(-115.75347595353,4.91614120060038,131.002975650622));
#102995=CARTESIAN_POINT('Ctrl Pts',(-115.761248853796,4.9178611546751,130.86620498544));
#102996=CARTESIAN_POINT('Ctrl Pts',(-115.768739189558,4.9195185840869,130.734406278441));
#102997=CARTESIAN_POINT('Ctrl Pts',(-115.77622952532,4.91587191080067,130.602709365307));
#102998=CARTESIAN_POINT('Ctrl Pts',(-115.783719861082,4.90697799332566,
130.471569338357));
#102999=CARTESIAN_POINT('Ctrl Pts',(-115.791494195201,4.89774686026636,
130.335457097426));
#103000=CARTESIAN_POINT('Ctrl Pts',(-115.79926852932,4.88283348839464,130.199513642299));
#103001=CARTESIAN_POINT('Ctrl Pts',(-115.807042863439,4.86224454032789,
130.064251779251));
#103002=CARTESIAN_POINT('Ctrl Pts',(-115.814807616386,4.84168096629954,
129.929156614361));
#103003=CARTESIAN_POINT('Ctrl Pts',(-115.822572369333,4.81545579159429,
129.794741753));
#103004=CARTESIAN_POINT('Ctrl Pts',(-115.830337122281,4.78362762140805,
129.661517740263));
#103005=CARTESIAN_POINT('Ctrl Pts',(-115.838094163166,4.75183106340914,
129.528426047494));
#103006=CARTESIAN_POINT('Ctrl Pts',(-115.845851204051,4.71444267473866,
129.396523227391));
#103007=CARTESIAN_POINT('Ctrl Pts',(-115.853608244936,4.67157252077776,
129.266312098951));
#103008=CARTESIAN_POINT('Ctrl Pts',(-115.861359436176,4.62873469553339,
129.136199163735));
#103009=CARTESIAN_POINT('Ctrl Pts',(-115.869110627416,4.58042345492907,
129.007775750796));
#103010=CARTESIAN_POINT('Ctrl Pts',(-115.876861818656,4.5267992577454,128.881531570933));
#103011=CARTESIAN_POINT('Ctrl Pts',(-115.884609715433,4.47319785227607,
128.755341048215));
#103012=CARTESIAN_POINT('Ctrl Pts',(-115.89235761221,4.4142881340431,128.631328275462));
#103013=CARTESIAN_POINT('Ctrl Pts',(-115.900105508987,4.35027937530218,
128.509964745159));
#103014=CARTESIAN_POINT('Ctrl Pts',(-115.907851785071,4.28628400581372,
128.388626601489));
#103015=CARTESIAN_POINT('Ctrl Pts',(-115.915598061155,4.21719189963404,
128.269936943602));
#103016=CARTESIAN_POINT('Ctrl Pts',(-115.92334433724,4.14325896199284,128.154343969247));
#103017=CARTESIAN_POINT('Ctrl Pts',(-115.931090670505,4.06932547859537,
128.038750141612));
#103018=CARTESIAN_POINT('Ctrl Pts',(-115.93883700377,3.99055130308902,127.926253372481));
#103019=CARTESIAN_POINT('Ctrl Pts',(-115.946583337036,3.90723625376387,
127.817273755794));
#103020=CARTESIAN_POINT('Ctrl Pts',(-115.954331405039,3.8239025466112,127.708269733877));
#103021=CARTESIAN_POINT('Ctrl Pts',(-115.962079473041,3.73602617953833,
127.602784742258));
#103022=CARTESIAN_POINT('Ctrl Pts',(-115.969827541044,3.64394765689159,
127.501206286274));
#103023=CARTESIAN_POINT('Ctrl Pts',(-115.977583843786,3.55177127209536,
127.399519871498));
#103024=CARTESIAN_POINT('Ctrl Pts',(-115.985340146528,3.45538407320305,
127.301748576381));
#103025=CARTESIAN_POINT('Ctrl Pts',(-115.99309644927,3.35516427088326,127.208243853904));
#103026=CARTESIAN_POINT('Ctrl Pts',(-116.000856891784,3.25489097823714,
127.114689225142));
#103027=CARTESIAN_POINT('Ctrl Pts',(-116.008617334298,3.15078130281278,
127.02540596092));
#103028=CARTESIAN_POINT('Ctrl Pts',(-116.016377776813,3.04324625209531,
126.940704924882));
#103029=CARTESIAN_POINT('Ctrl Pts',(-116.024150677078,2.93553857656792,
126.855867919222));
#103030=CARTESIAN_POINT('Ctrl Pts',(-116.031923577343,2.82439485473092,
126.775628069957));
#103031=CARTESIAN_POINT('Ctrl Pts',(-116.039696477609,2.71025549775606,
126.700253138542));
#103032=CARTESIAN_POINT('Ctrl Pts',(-116.047186813371,2.60026539390663,
126.627618275741));
#103033=CARTESIAN_POINT('Ctrl Pts',(-116.054677149133,2.48749393504998,
126.559500926831));
#103034=CARTESIAN_POINT('Ctrl Pts',(-116.062167484895,2.37235473665656,
126.496099243652));
#103035=CARTESIAN_POINT('Ctrl Pts',(-116.069941819014,2.25285000056076,
126.430293666384));
#103036=CARTESIAN_POINT('Ctrl Pts',(-116.077716153133,2.1304158798679,126.369359950409));
#103037=CARTESIAN_POINT('Ctrl Pts',(-116.085490487252,2.0054874143276,126.313569674595));
#103038=CARTESIAN_POINT('Ctrl Pts',(-116.093255240199,1.8807129119559,126.257848155309));
#103039=CARTESIAN_POINT('Ctrl Pts',(-116.101019993146,1.75345053475243,
126.207257621693));
#103040=CARTESIAN_POINT('Ctrl Pts',(-116.108784746093,1.62416149630504,
126.16202472963));
#103041=CARTESIAN_POINT('Ctrl Pts',(-116.116541786978,1.49500086955328,
126.116836763513));
#103042=CARTESIAN_POINT('Ctrl Pts',(-116.124298827863,1.36381795398044,
126.076995977624));
#103043=CARTESIAN_POINT('Ctrl Pts',(-116.132055868748,1.23109527847499,
126.042681556792));
#103044=CARTESIAN_POINT('Ctrl Pts',(-116.139807059989,1.0984726901714,126.008393012731));
#103045=CARTESIAN_POINT('Ctrl Pts',(-116.147558251229,0.964313030111163,
125.979622636087));
#103046=CARTESIAN_POINT('Ctrl Pts',(-116.155309442469,0.829115037750144,
125.956500128992));
#103047=CARTESIAN_POINT('Ctrl Pts',(-116.163057339246,0.693974508142587,
125.93338744958));
#103048=CARTESIAN_POINT('Ctrl Pts',(-116.170805236023,0.557796908546889,
125.915917931086));
#103049=CARTESIAN_POINT('Ctrl Pts',(-116.1785531328,0.421092035708382,125.904170360039));
#103050=CARTESIAN_POINT('Ctrl Pts',(-116.186299408884,0.284415758582256,
125.89242524633));
#103051=CARTESIAN_POINT('Ctrl Pts',(-116.194045684968,0.147212816877323,
125.886399732805));
#103052=CARTESIAN_POINT('Ctrl Pts',(-116.201791961052,0.00999861508217229,
125.886120780978));
#103053=CARTESIAN_POINT('Ctrl Pts',(-116.209538294318,-0.127216599596859,
125.885841827092));
#103054=CARTESIAN_POINT('Ctrl Pts',(-116.217284627583,-0.264442683567566,
125.891309520345));
#103055=CARTESIAN_POINT('Ctrl Pts',(-116.225030960848,-0.40116414079272,
125.902498686152));
#103056=CARTESIAN_POINT('Ctrl Pts',(-116.232779028851,-0.537916215840074,
125.913690357696));
#103057=CARTESIAN_POINT('Ctrl Pts',(-116.240527096854,-0.67416304968182,
125.930606019518));
#103058=CARTESIAN_POINT('Ctrl Pts',(-116.248275164857,-0.809394572185431,
125.953168651769));
#103059=CARTESIAN_POINT('Ctrl Pts',(-116.256031467599,-0.944769820360988,
125.975755263854));
#103060=CARTESIAN_POINT('Ctrl Pts',(-116.263787770341,-1.07912721536045,
126.004000770901));
#103061=CARTESIAN_POINT('Ctrl Pts',(-116.271544073083,-1.21196663773001,
126.037776942487));
#103062=CARTESIAN_POINT('Ctrl Pts',(-116.279304515597,-1.34487696049901,
126.071571141433));
#103063=CARTESIAN_POINT('Ctrl Pts',(-116.287064958111,-1.47626732190926,
126.110901774729));
#103064=CARTESIAN_POINT('Ctrl Pts',(-116.294825400625,-1.60565402398851,
126.155591079532));
#103065=CARTESIAN_POINT('Ctrl Pts',(-116.302598300891,-1.73524842908835,
126.200352123575));
#103066=CARTESIAN_POINT('Ctrl Pts',(-116.310371201156,-1.86283238327472,
126.250488886015));
#103067=CARTESIAN_POINT('Ctrl Pts',(-116.318144101422,-1.98794255825685,
126.305775568068));
#103068=CARTESIAN_POINT('Ctrl Pts',(-116.325634437184,-2.10850466324555,
126.359052439969));
#103069=CARTESIAN_POINT('Ctrl Pts',(-116.333124772946,-2.22676944617571,
126.417111171214));
#103070=CARTESIAN_POINT('Ctrl Pts',(-116.340615108708,-2.3423466270268,
126.479710881303));
#103071=CARTESIAN_POINT('Ctrl Pts',(-116.348390427865,-2.46232115113111,
126.544692310784));
#103072=CARTESIAN_POINT('Ctrl Pts',(-116.356165747023,-2.57977960639145,
126.614772967477));
#103073=CARTESIAN_POINT('Ctrl Pts',(-116.36394106618,-2.69425818120466,
126.68973354874));
#103074=CARTESIAN_POINT('Ctrl Pts',(-116.371706587397,-2.80859249772535,
126.764599669661));
#103075=CARTESIAN_POINT('Ctrl Pts',(-116.379472108614,-2.91995408184397,
126.844333266275));
#103076=CARTESIAN_POINT('Ctrl Pts',(-116.387237629831,-3.02790281808886,
126.928668732662));
#103077=CARTESIAN_POINT('Ctrl Pts',(-116.394993822415,-3.13572187673097,
127.012902887802));
#103078=CARTESIAN_POINT('Ctrl Pts',(-116.402750014998,-3.24013594675893,
127.101727663325));
#103079=CARTESIAN_POINT('Ctrl Pts',(-116.410506207582,-3.3407335963119,
127.194834041826));
#103080=CARTESIAN_POINT('Ctrl Pts',(-116.418257110972,-3.44126264513647,
127.287876928134));
#103081=CARTESIAN_POINT('Ctrl Pts',(-116.426008014362,-3.53798016537562,
127.385195344403));
#103082=CARTESIAN_POINT('Ctrl Pts',(-116.433758917752,-3.63050749963723,
127.486439829244));
#103083=CARTESIAN_POINT('Ctrl Pts',(-116.441506214166,-3.72299177520397,
127.587637198761));
#103084=CARTESIAN_POINT('Ctrl Pts',(-116.449253510581,-3.81128948195976,
127.692756713233));
#103085=CARTESIAN_POINT('Ctrl Pts',(-116.457000806996,-3.89505885799039,
127.801412140604));
#103086=CARTESIAN_POINT('Ctrl Pts',(-116.464746175871,-3.97880739205941,
127.910040534321));
#103087=CARTESIAN_POINT('Ctrl Pts',(-116.472491544745,-4.0580296001001,
128.022202780125));
#103088=CARTESIAN_POINT('Ctrl Pts',(-116.48023691362,-4.13242431335157,
128.137479975895));
#103089=CARTESIAN_POINT('Ctrl Pts',(-116.487984623368,-4.20684151083047,
128.252792011757));
#103090=CARTESIAN_POINT('Ctrl Pts',(-116.495732333116,-4.27642808098253,
128.371220553363));
#103091=CARTESIAN_POINT('Ctrl Pts',(-116.503480042864,-4.34092642726801,
128.492318054042));
#103092=CARTESIAN_POINT('Ctrl Pts',(-116.511228755889,-4.405433125659,128.613431236039));
#103093=CARTESIAN_POINT('Ctrl Pts',(-116.518977468914,-4.46485011097761,
128.737213716634));
#103094=CARTESIAN_POINT('Ctrl Pts',(-116.526726181939,-4.51896642917555,
128.863194608569));
#103095=CARTESIAN_POINT('Ctrl Pts',(-116.534481725635,-4.57313045216502,
128.989286555587));
#103096=CARTESIAN_POINT('Ctrl Pts',(-116.54223726933,-4.62198432500997,
129.117580423228));
#103097=CARTESIAN_POINT('Ctrl Pts',(-116.549992813026,-4.66536565734462,
129.247586277538));
#103098=CARTESIAN_POINT('Ctrl Pts',(-116.556584779194,-4.70223841395482,
129.358087130461));
#103099=CARTESIAN_POINT('Ctrl Pts',(-116.563176745361,-4.73515835422674,
129.469824375414));
#103100=CARTESIAN_POINT('Ctrl Pts',(-116.569768711529,-4.764054528234,129.582490119308));
#103101=CARTESIAN_POINT('Origin',(213.235140564004,0.,130.804360617566));
#103102=CARTESIAN_POINT('',(-118.665245282749,-4.764054528234,129.582490119308));
#103103=CARTESIAN_POINT('',(-118.320090776197,-4.76405452823413,129.582490119309));
#103104=CARTESIAN_POINT('',(213.235140564004,-4.76405452823405,129.582490119308));
#103105=CARTESIAN_POINT('',(-116.985140563956,-4.91824914438459,130.801459538413));
#103106=CARTESIAN_POINT('Ctrl Pts',(-116.98514056401,-4.91824914438515,
130.801459539365));
#103107=CARTESIAN_POINT('Ctrl Pts',(-116.992962856645,-4.91833097250967,
130.940184204984));
#103108=CARTESIAN_POINT('Ctrl Pts',(-117.00078514928,-4.91253913636687,
131.07892180876));
#103109=CARTESIAN_POINT('Ctrl Pts',(-117.008607441915,-4.90089696268117,
131.217146304918));
#103110=CARTESIAN_POINT('Ctrl Pts',(-117.016430946283,-4.88925298553342,
131.355392213111));
#103111=CARTESIAN_POINT('Ctrl Pts',(-117.024254450651,-4.87175689745055,
131.493124476448));
#103112=CARTESIAN_POINT('Ctrl Pts',(-117.032077955019,-4.84848393605076,
131.629822054798));
#103113=CARTESIAN_POINT('Ctrl Pts',(-117.039904238686,-4.82520270693484,
131.766568194943));
#103114=CARTESIAN_POINT('Ctrl Pts',(-117.047730522353,-4.79614058131351,
131.90227854341));
#103115=CARTESIAN_POINT('Ctrl Pts',(-117.055556806019,-4.7614239018093,
132.036442388302));
#103116=CARTESIAN_POINT('Ctrl Pts',(-117.063387438058,-4.7266879333254,
132.170680776143));
#103117=CARTESIAN_POINT('Ctrl Pts',(-117.071218070097,-4.68629124943694,
132.303370581688));
#103118=CARTESIAN_POINT('Ctrl Pts',(-117.079048702135,-4.64040993340714,
132.434016628028));
#103119=CARTESIAN_POINT('Ctrl Pts',(-117.086889979928,-4.59446624166729,
132.564840287843));
#103120=CARTESIAN_POINT('Ctrl Pts',(-117.094731257722,-4.54302315428032,
132.693614281432));
#103121=CARTESIAN_POINT('Ctrl Pts',(-117.102572535515,-4.48630500709428,
132.819863146917));
#103122=CARTESIAN_POINT('Ctrl Pts',(-117.110420056086,-4.42954170415399,
132.94621252455));
#103123=CARTESIAN_POINT('Ctrl Pts',(-117.118267576657,-4.36749514211798,
133.070032429201));
#103124=CARTESIAN_POINT('Ctrl Pts',(-117.126115097229,-4.3004350362841,
133.190873043932));
#103125=CARTESIAN_POINT('Ctrl Pts',(-117.133974930124,-4.23326971686555,
133.311903250882));
#103126=CARTESIAN_POINT('Ctrl Pts',(-117.14183476302,-4.1610753444807,133.429944511274));
#103127=CARTESIAN_POINT('Ctrl Pts',(-117.149694595916,-4.0841645832594,
133.544576433765));
#103128=CARTESIAN_POINT('Ctrl Pts',(-117.151919391939,-4.06239430417253,
133.577024025042));
#103129=CARTESIAN_POINT('Ctrl Pts',(-117.154144187963,-4.0402463801263,
133.609198660703));
#103130=CARTESIAN_POINT('Ctrl Pts',(-117.156368983986,-4.01772846487362,
133.641091314168));
#103131=CARTESIAN_POINT('Ctrl Pts',(-117.164143318105,-3.9390417920256,
133.75253710128));
#103132=CARTESIAN_POINT('Ctrl Pts',(-117.171917652224,-3.85558996144009,
133.860882953182));
#103133=CARTESIAN_POINT('Ctrl Pts',(-117.179691986343,-3.76764541453514,
133.965694369771));
#103134=CARTESIAN_POINT('Ctrl Pts',(-117.18745673929,-3.67980925142443,
134.070376615657));
#103135=CARTESIAN_POINT('Ctrl Pts',(-117.195221492237,-3.58749163760855,
134.171532796498));
#103136=CARTESIAN_POINT('Ctrl Pts',(-117.202986245185,-3.4910082002169,
134.268757362819));
#103137=CARTESIAN_POINT('Ctrl Pts',(-117.21074328607,-3.39462059153519,
134.36588536433));
#103138=CARTESIAN_POINT('Ctrl Pts',(-117.218500326955,-3.29407566681059,
134.459089246602));
#103139=CARTESIAN_POINT('Ctrl Pts',(-117.22625736784,-3.1897289841545,134.547996827208));
#103140=CARTESIAN_POINT('Ctrl Pts',(-117.23400855908,-3.08546099014392,
134.636837361916));
#103141=CARTESIAN_POINT('Ctrl Pts',(-117.24175975032,-2.97739724105038,
134.721387791196));
#103142=CARTESIAN_POINT('Ctrl Pts',(-117.24951094156,-2.86592951521695,
134.801313341368));
#103143=CARTESIAN_POINT('Ctrl Pts',(-117.257258838337,-2.75450916614035,
134.881204921049));
#103144=CARTESIAN_POINT('Ctrl Pts',(-117.265006735114,-2.63968803492435,
134.956475303899));
#103145=CARTESIAN_POINT('Ctrl Pts',(-117.272754631891,-2.52189011261899,
135.026830667475));
#103146=CARTESIAN_POINT('Ctrl Pts',(-117.280500907975,-2.40411683109921,
135.097171314225));
#103147=CARTESIAN_POINT('Ctrl Pts',(-117.28824718406,-2.28336833247884,
135.162598786336));
#103148=CARTESIAN_POINT('Ctrl Pts',(-117.295993460144,-2.16009631759652,
135.222863413899));
#103149=CARTESIAN_POINT('Ctrl Pts',(-117.303739793409,-2.03682339274835,
135.283128486323));
#103150=CARTESIAN_POINT('Ctrl Pts',(-117.311486126674,-1.9110272657063,
135.33823046644));
#103151=CARTESIAN_POINT('Ctrl Pts',(-117.31923245994,-1.78318252255282,
135.387966529265));
#103152=CARTESIAN_POINT('Ctrl Pts',(-117.326980527943,-1.65530914945569,
135.437713730137));
#103153=CARTESIAN_POINT('Ctrl Pts',(-117.334728595946,-1.52538661163492,
135.48209248083));
#103154=CARTESIAN_POINT('Ctrl Pts',(-117.342476663949,-1.39390729147759,
135.520948952927));
#103155=CARTESIAN_POINT('Ctrl Pts',(-117.350232966691,-1.26228823353399,
135.559846722145));
#103156=CARTESIAN_POINT('Ctrl Pts',(-117.357989269432,-1.12910946361085,
135.593210377538));
#103157=CARTESIAN_POINT('Ctrl Pts',(-117.365745572174,-0.994876813763548,
135.620936495504));
#103158=CARTESIAN_POINT('Ctrl Pts',(-117.373506014688,-0.860572519909357,
135.648677411734));
#103159=CARTESIAN_POINT('Ctrl Pts',(-117.381266457203,-0.725213610995721,
135.670774732041));
#103160=CARTESIAN_POINT('Ctrl Pts',(-117.389026899717,-0.589312815702003,
135.687176758662));
#103161=CARTESIAN_POINT('Ctrl Pts',(-117.396799799982,-0.453193860386973,
135.703605115272));
#103162=CARTESIAN_POINT('Ctrl Pts',(-117.404572700248,-0.316531670379598,
135.714319877809));
#103163=CARTESIAN_POINT('Ctrl Pts',(-117.412345600513,-0.179841665925045,
135.719321455426));
#103164=CARTESIAN_POINT('Ctrl Pts',(-117.419835936275,-0.0481206874296885,
135.724141213099));
#103165=CARTESIAN_POINT('Ctrl Pts',(-117.427326272038,0.0836258103552183,
135.723655952752));
#103166=CARTESIAN_POINT('Ctrl Pts',(-117.4348166078,0.214941501717956,135.717911595559));
#103167=CARTESIAN_POINT('Ctrl Pts',(-117.442590941919,0.351236067427596,
135.711949439318));
#103168=CARTESIAN_POINT('Ctrl Pts',(-117.450365276038,0.487498254002862,
135.700302630215));
#103169=CARTESIAN_POINT('Ctrl Pts',(-117.458139610157,0.623215242960326,
135.682965523012));
#103170=CARTESIAN_POINT('Ctrl Pts',(-117.465904363104,0.758764972858276,
135.665649782244));
#103171=CARTESIAN_POINT('Ctrl Pts',(-117.473669116051,0.893770457943031,
135.642657745792));
#103172=CARTESIAN_POINT('Ctrl Pts',(-117.481433868999,1.02771989378069,
135.614035750299));
#103173=CARTESIAN_POINT('Ctrl Pts',(-117.489190909884,1.16153628915069,
135.585442182575));
#103174=CARTESIAN_POINT('Ctrl Pts',(-117.496947950769,1.29429834273785,
135.551229864823));
#103175=CARTESIAN_POINT('Ctrl Pts',(-117.504704991654,1.42550073908048,
135.511496764458));
#103176=CARTESIAN_POINT('Ctrl Pts',(-117.512456182894,1.55660419467524,
135.471793627134));
#103177=CARTESIAN_POINT('Ctrl Pts',(-117.520207374134,1.68614996141089,
135.426578106781));
#103178=CARTESIAN_POINT('Ctrl Pts',(-117.527958565374,1.81364461894353,
135.375998864265));
#103179=CARTESIAN_POINT('Ctrl Pts',(-117.535706462151,1.94108508784587,
135.325441119275));
#103180=CARTESIAN_POINT('Ctrl Pts',(-117.543454358928,2.06647581879019,
135.269524330191));
#103181=CARTESIAN_POINT('Ctrl Pts',(-117.551202255706,2.18934043311451,
135.208446394482));
#103182=CARTESIAN_POINT('Ctrl Pts',(-117.55894853179,2.31217934681017,135.14738123496));
#103183=CARTESIAN_POINT('Ctrl Pts',(-117.566694807874,2.43249284504949,
135.081157250125));
#103184=CARTESIAN_POINT('Ctrl Pts',(-117.574441083958,2.54982671813193,
135.010019516003));
#103185=CARTESIAN_POINT('Ctrl Pts',(-117.582187417223,2.6671614573462,134.938881256758));
#103186=CARTESIAN_POINT('Ctrl Pts',(-117.589933750489,2.78151619319496,
134.862829378539));
#103187=CARTESIAN_POINT('Ctrl Pts',(-117.597680083754,2.89246375790431,
134.7821535322));
#103188=CARTESIAN_POINT('Ctrl Pts',(-117.605428151757,3.00343616855138,
134.701459619064));
#103189=CARTESIAN_POINT('Ctrl Pts',(-117.61317621976,3.11099957360763,134.616139907158));
#103190=CARTESIAN_POINT('Ctrl Pts',(-117.620924287763,3.21475840816102,
134.526525503712));
#103191=CARTESIAN_POINT('Ctrl Pts',(-117.628680590505,3.31862751883867,
134.436815857011));
#103192=CARTESIAN_POINT('Ctrl Pts',(-117.636436893247,3.41868368524422,
134.342802656748));
#103193=CARTESIAN_POINT('Ctrl Pts',(-117.644193195989,3.51456647959025,
134.244855570773));
#103194=CARTESIAN_POINT('Ctrl Pts',(-117.651953638503,3.6105004494706,134.146856207489));
#103195=CARTESIAN_POINT('Ctrl Pts',(-117.659714081017,3.70225634746651,
134.044919065239));
#103196=CARTESIAN_POINT('Ctrl Pts',(-117.667474523531,3.78951353640945,
133.939447573277));
#103197=CARTESIAN_POINT('Ctrl Pts',(-117.675247423797,3.87691079833841,
133.833806769113));
#103198=CARTESIAN_POINT('Ctrl Pts',(-117.683020324062,3.95979468337634,
133.724620589058));
#103199=CARTESIAN_POINT('Ctrl Pts',(-117.690793224328,4.03788693852398,
133.61232289192));
#103200=CARTESIAN_POINT('Ctrl Pts',(-117.69828356009,4.11314034349131,133.504107498939));
#103201=CARTESIAN_POINT('Ctrl Pts',(-117.705773895851,4.18394428035254,
133.393003144034));
#103202=CARTESIAN_POINT('Ctrl Pts',(-117.713264231613,4.25009072869888,
133.279418568469));
#103203=CARTESIAN_POINT('Ctrl Pts',(-117.721038565732,4.3187451397413,133.161527399194));
#103204=CARTESIAN_POINT('Ctrl Pts',(-117.728812899851,4.38259938962026,
133.040590777674));
#103205=CARTESIAN_POINT('Ctrl Pts',(-117.73658723397,4.44137153792066,132.917037101235));
#103206=CARTESIAN_POINT('Ctrl Pts',(-117.744351986917,4.50007125480122,
132.793635693659));
#103207=CARTESIAN_POINT('Ctrl Pts',(-117.752116739864,4.55370116574578,
132.66762399819));
#103208=CARTESIAN_POINT('Ctrl Pts',(-117.759881492811,4.60202361228762,
132.53945765648));
#103209=CARTESIAN_POINT('Ctrl Pts',(-117.767638533696,4.6502980642942,132.411418611388));
#103210=CARTESIAN_POINT('Ctrl Pts',(-117.775395574581,4.69327540528332,
132.281229542262));
#103211=CARTESIAN_POINT('Ctrl Pts',(-117.783152615466,4.73076492266621,
132.149368539093));
#103212=CARTESIAN_POINT('Ctrl Pts',(-117.790903806706,4.76822616891236,
132.017606973333));
#103213=CARTESIAN_POINT('Ctrl Pts',(-117.798654997946,4.8002077223216,131.884176357652));
#103214=CARTESIAN_POINT('Ctrl Pts',(-117.806406189187,4.82656794974035,
131.749572175387));
#103215=CARTESIAN_POINT('Ctrl Pts',(-117.814154085964,4.8529169733593,131.615025203491));
#103216=CARTESIAN_POINT('Ctrl Pts',(-117.821901982741,4.87364934797108,
131.479306039955));
#103217=CARTESIAN_POINT('Ctrl Pts',(-117.829649879518,4.88867407601971,
131.342922444057));
#103218=CARTESIAN_POINT('Ctrl Pts',(-117.837396155602,4.90369566121912,
131.206567376666));
#103219=CARTESIAN_POINT('Ctrl Pts',(-117.845142431686,4.91301193183634,
131.069548541729));
#103220=CARTESIAN_POINT('Ctrl Pts',(-117.85288870777,4.91658356583436,130.932380548309));
#103221=CARTESIAN_POINT('Ctrl Pts',(-117.860635041035,4.92015522619736,
130.795211542347));
#103222=CARTESIAN_POINT('Ctrl Pts',(-117.868381374301,4.91798215514722,
130.657893766536));
#103223=CARTESIAN_POINT('Ctrl Pts',(-117.876127707566,4.9100771495345,130.520943172586));
#103224=CARTESIAN_POINT('Ctrl Pts',(-117.883875775569,4.90217037365058,
130.383961909499));
#103225=CARTESIAN_POINT('Ctrl Pts',(-117.891623843572,4.8885291314603,130.247348382138));
#103226=CARTESIAN_POINT('Ctrl Pts',(-117.899371911575,4.86921818035638,
130.11161436201));
#103227=CARTESIAN_POINT('Ctrl Pts',(-117.907128214316,4.84988670534375,
129.97573608215));
#103228=CARTESIAN_POINT('Ctrl Pts',(-117.914884517058,4.82487353932085,
129.840739564473));
#103229=CARTESIAN_POINT('Ctrl Pts',(-117.9226408198,4.79429487429698,129.707127861589));
#103230=CARTESIAN_POINT('Ctrl Pts',(-117.930401262314,4.76369988851896,
129.573444846116));
#103231=CARTESIAN_POINT('Ctrl Pts',(-117.938161704828,4.72753358786435,
129.441148495131));
#103232=CARTESIAN_POINT('Ctrl Pts',(-117.945922147342,4.68596207656938,
129.310726633133));
#103233=CARTESIAN_POINT('Ctrl Pts',(-117.953695047608,4.64432383099382,
129.180095406383));
#103234=CARTESIAN_POINT('Ctrl Pts',(-117.961467947873,4.59726316981607,
129.051345049167));
#103235=CARTESIAN_POINT('Ctrl Pts',(-117.969240848139,4.5449947081957,128.924944174897));
#103236=CARTESIAN_POINT('Ctrl Pts',(-117.976731183901,4.49462633680913,
128.803138290786));
#103237=CARTESIAN_POINT('Ctrl Pts',(-117.984221519663,4.43942235374094,
128.683514315722));
#103238=CARTESIAN_POINT('Ctrl Pts',(-117.991711855426,4.37961420447853,
128.566468197804));
#103239=CARTESIAN_POINT('Ctrl Pts',(-117.999486189545,4.31753841106076,
128.444984240753));
#103240=CARTESIAN_POINT('Ctrl Pts',(-118.007260523664,4.25030578805859,
128.325892653909));
#103241=CARTESIAN_POINT('Ctrl Pts',(-118.015034857783,4.17812436259317,
128.209662200947));
#103242=CARTESIAN_POINT('Ctrl Pts',(-118.02279961073,4.10603189428359,128.09357499163));
#103243=CARTESIAN_POINT('Ctrl Pts',(-118.030564363677,4.02900296289648,
127.980342229266));
#103244=CARTESIAN_POINT('Ctrl Pts',(-118.038329116625,3.94729245245299,
127.870410148095));
#103245=CARTESIAN_POINT('Ctrl Pts',(-118.04608615751,3.86566309804061,127.760587253018));
#103246=CARTESIAN_POINT('Ctrl Pts',(-118.053843198395,3.7793616496228,127.654058826954));
#103247=CARTESIAN_POINT('Ctrl Pts',(-118.06160023928,3.68868725303599,127.551243741124));
#103248=CARTESIAN_POINT('Ctrl Pts',(-118.06935143052,3.59808123471687,127.44850618895));
#103249=CARTESIAN_POINT('Ctrl Pts',(-118.07710262176,3.50310908960216,127.349476695302));
#103250=CARTESIAN_POINT('Ctrl Pts',(-118.084853813,3.40411112567754,127.254542241009));
#103251=CARTESIAN_POINT('Ctrl Pts',(-118.092601709777,3.30515523852858,
127.159648136393));
#103252=CARTESIAN_POINT('Ctrl Pts',(-118.100349606554,3.20217721737219,
127.068845879444));
#103253=CARTESIAN_POINT('Ctrl Pts',(-118.108097503331,3.09555506806689,
126.982486485276));
#103254=CARTESIAN_POINT('Ctrl Pts',(-118.115843779416,2.98895522181642,
126.896145155632));
#103255=CARTESIAN_POINT('Ctrl Pts',(-118.1235900555,2.8787130672387,126.814245086156));
#103256=CARTESIAN_POINT('Ctrl Pts',(-118.131336331584,2.76524030499126,
126.737097518361));
#103257=CARTESIAN_POINT('Ctrl Pts',(-118.139082664849,2.65176670511382,
126.659949381081));
#103258=CARTESIAN_POINT('Ctrl Pts',(-118.146828998115,2.5350627732984,126.587554035301));
#103259=CARTESIAN_POINT('Ctrl Pts',(-118.15457533138,2.41556951133955,126.52017959917));
#103260=CARTESIAN_POINT('Ctrl Pts',(-118.162323399383,2.29604948969368,
126.452790075001));
#103261=CARTESIAN_POINT('Ctrl Pts',(-118.170071467386,2.17373923541706,
126.390423889886));
#103262=CARTESIAN_POINT('Ctrl Pts',(-118.177819535389,2.04910431932686,
126.333303186598));
#103263=CARTESIAN_POINT('Ctrl Pts',(-118.185575838131,1.92433693976416,
126.276121774746));
#103264=CARTESIAN_POINT('Ctrl Pts',(-118.193332140873,1.7972403189253,126.224197144454));
#103265=CARTESIAN_POINT('Ctrl Pts',(-118.201088443615,1.66830049383609,
126.177703452315));
#103266=CARTESIAN_POINT('Ctrl Pts',(-118.208848886129,1.53929184967992,
126.131184945093));
#103267=CARTESIAN_POINT('Ctrl Pts',(-118.216609328643,1.40843841385262,
126.090103268892));
#103268=CARTESIAN_POINT('Ctrl Pts',(-118.224369771157,1.27624039031671,
126.054582356571));
#103269=CARTESIAN_POINT('Ctrl Pts',(-118.232142671423,1.14383015077744,
126.019004422927));
#103270=CARTESIAN_POINT('Ctrl Pts',(-118.239915571688,1.01007139196343,
125.989005177026));
#103271=CARTESIAN_POINT('Ctrl Pts',(-118.247688471954,0.875474376345938,
125.964657354053));
#103272=CARTESIAN_POINT('Ctrl Pts',(-118.255178807715,0.745770301289418,
125.941194635775));
#103273=CARTESIAN_POINT('Ctrl Pts',(-118.262669143476,0.615288161879356,
125.922979629691));
#103274=CARTESIAN_POINT('Ctrl Pts',(-118.270159479238,0.484486182403032,
125.910031633777));
#103275=CARTESIAN_POINT('Ctrl Pts',(-118.277933813357,0.348724806104517,
125.89659271066));
#103276=CARTESIAN_POINT('Ctrl Pts',(-118.285708147476,0.212188806263716,
125.888785508856));
#103277=CARTESIAN_POINT('Ctrl Pts',(-118.293482481595,0.0753850107763749,
125.886688387471));
#103278=CARTESIAN_POINT('Ctrl Pts',(-118.301247234542,-0.0612501862595348,
125.884593850601));
#103279=CARTESIAN_POINT('Ctrl Pts',(-118.309011987489,-0.198152135105806,
125.888195398227));
#103280=CARTESIAN_POINT('Ctrl Pts',(-118.316776740436,-0.334807635217108,
125.897519789711));
#103281=CARTESIAN_POINT('Ctrl Pts',(-118.324533781321,-0.471327407158824,
125.906834920079));
#103282=CARTESIAN_POINT('Ctrl Pts',(-118.332290822206,-0.607600829947365,
125.921861556428));
#103283=CARTESIAN_POINT('Ctrl Pts',(-118.340047863091,-0.74311379973069,
125.942574429019));
#103284=CARTESIAN_POINT('Ctrl Pts',(-118.347799054331,-0.878524578128811,
125.963271681871));
#103285=CARTESIAN_POINT('Ctrl Pts',(-118.355550245572,-1.01317566005314,
125.98964657706));
#103286=CARTESIAN_POINT('Ctrl Pts',(-118.363301436812,-1.14655752279258,
126.021621976429));
#103287=CARTESIAN_POINT('Ctrl Pts',(-118.371049333589,-1.27988269468283,
126.0535837854));
#103288=CARTESIAN_POINT('Ctrl Pts',(-118.378797230366,-1.41193934092004,
126.091141273238));
#103289=CARTESIAN_POINT('Ctrl Pts',(-118.386545127143,-1.54222782114858,
126.134166145151));
#103290=CARTESIAN_POINT('Ctrl Pts',(-118.394291403227,-1.67248904783576,
126.177182017188));
#103291=CARTESIAN_POINT('Ctrl Pts',(-118.402037679311,-1.80098247317908,
126.225662875982));
#103292=CARTESIAN_POINT('Ctrl Pts',(-118.409783955395,-1.92722370661806,
126.279430579748));
#103293=CARTESIAN_POINT('Ctrl Pts',(-118.417530288661,-2.05346587194097,
126.333198680415));
#103294=CARTESIAN_POINT('Ctrl Pts',(-118.425276621926,-2.17745545248608,
126.392253550729));
#103295=CARTESIAN_POINT('Ctrl Pts',(-118.433022955191,-2.29872850061997,
126.456369087798));
#103296=CARTESIAN_POINT('Ctrl Pts',(-118.440771023194,-2.42002870701197,
126.520498983097));
#103297=CARTESIAN_POINT('Ctrl Pts',(-118.448519091197,-2.53861082488183,
126.589691617592));
#103298=CARTESIAN_POINT('Ctrl Pts',(-118.4562671592,-2.65403630682452,126.663675366963));
#103299=CARTESIAN_POINT('Ctrl Pts',(-118.464023461942,-2.76958446434316,
126.737737747145));
#103300=CARTESIAN_POINT('Ctrl Pts',(-118.471779764684,-2.88196895446078,
126.816601202816));
#103301=CARTESIAN_POINT('Ctrl Pts',(-118.479536067426,-2.99078053941757,
126.899950953156));
#103302=CARTESIAN_POINT('Ctrl Pts',(-118.48729650994,-3.09965020039379,
126.983345189767));
#103303=CARTESIAN_POINT('Ctrl Pts',(-118.495056952454,-3.20494285641292,
127.071230241827));
#103304=CARTESIAN_POINT('Ctrl Pts',(-118.502817394969,-3.30628386679137,
127.163252262313));
#103305=CARTESIAN_POINT('Ctrl Pts',(-118.510590295234,-3.40778755875631,
127.255422004715));
#103306=CARTESIAN_POINT('Ctrl Pts',(-118.5183631955,-3.50532665033385,127.351741711568));
#103307=CARTESIAN_POINT('Ctrl Pts',(-118.526136095765,-3.59856413802438,
127.451821399745));
#103308=CARTESIAN_POINT('Ctrl Pts',(-118.533626431528,-3.68841220819517,
127.548262939182));
#103309=CARTESIAN_POINT('Ctrl Pts',(-118.54111676729,-3.77426579226086,
127.64819560282));
#103310=CARTESIAN_POINT('Ctrl Pts',(-118.548607103053,-3.85586097286858,
127.751244304615));
#103311=CARTESIAN_POINT('Ctrl Pts',(-118.55637431177,-3.94047223972398,
127.858102101139));
#103312=CARTESIAN_POINT('Ctrl Pts',(-118.564141520487,-4.02077788700481,
127.968656369638));
#103313=CARTESIAN_POINT('Ctrl Pts',(-118.571908729203,-4.09643675520393,
128.082525028645));
#103314=CARTESIAN_POINT('Ctrl Pts',(-118.579686775332,-4.17220118852415,
128.196552566037));
#103315=CARTESIAN_POINT('Ctrl Pts',(-118.587464821461,-4.24330557771578,
128.313903478333));
#103316=CARTESIAN_POINT('Ctrl Pts',(-118.59524286759,-4.30944618965557,
128.434158811609));
#103317=CARTESIAN_POINT('Ctrl Pts',(-118.602990553207,-4.37532863099839,
128.553944745067));
#103318=CARTESIAN_POINT('Ctrl Pts',(-118.610738238824,-4.43628575567785,
128.6766121405));
#103319=CARTESIAN_POINT('Ctrl Pts',(-118.618485924442,-4.49205961804044,
128.801716502784));
#103320=CARTESIAN_POINT('Ctrl Pts',(-118.626279150826,-4.54816131823912,
128.92755622643));
#103321=CARTESIAN_POINT('Ctrl Pts',(-118.634072377211,-4.59901839116217,
129.055861332303));
#103322=CARTESIAN_POINT('Ctrl Pts',(-118.641865603595,-4.64441475660832,
129.186153390077));
#103323=CARTESIAN_POINT('Ctrl Pts',(-118.64965882998,-4.68981112205447,
129.316445447851));
#103324=CARTESIAN_POINT('Ctrl Pts',(-118.657452056364,-4.72974661527674,
129.448724087383));
#103325=CARTESIAN_POINT('Ctrl Pts',(-118.665245282749,-4.764054528234,129.582490119308));
#103326=CARTESIAN_POINT('Ctrl Pts',(-116.915395520338,-4.76405452823392,
129.582490119308));
#103327=CARTESIAN_POINT('Ctrl Pts',(-116.924092892827,-4.80208294653435,
129.730762345099));
#103328=CARTESIAN_POINT('Ctrl Pts',(-116.932790265316,-4.83322964626429,
129.880984325762));
#103329=CARTESIAN_POINT('Ctrl Pts',(-116.941487637805,-4.85731183919284,
130.032541494107));
#103330=CARTESIAN_POINT('Ctrl Pts',(-116.950137985105,-4.88126382387196,
130.183279219071));
#103331=CARTESIAN_POINT('Ctrl Pts',(-116.958788332406,-4.89822739411557,
130.335337530523));
#103332=CARTESIAN_POINT('Ctrl Pts',(-116.967438679707,-4.90807070138259,
130.488093242186));
#103333=CARTESIAN_POINT('Ctrl Pts',(-116.97333930779,-4.91478507865219,
130.592291907367));
#103334=CARTESIAN_POINT('Ctrl Pts',(-116.979239935873,-4.91818741855684,
130.696814686071));
#103335=CARTESIAN_POINT('Ctrl Pts',(-116.985140563957,-4.91824914438459,
130.801459538414));
#103336=CARTESIAN_POINT('',(-116.639859436028,-4.91824951514326,130.802176746446));
#103337=CARTESIAN_POINT('Ctrl Pts',(-116.569768711529,-4.764054528234,129.582490119308));
#103338=CARTESIAN_POINT('Ctrl Pts',(-116.57753385721,-4.79809338630334,
129.715207110309));
#103339=CARTESIAN_POINT('Ctrl Pts',(-116.585299002891,-4.82654756773742,
129.849212355614));
#103340=CARTESIAN_POINT('Ctrl Pts',(-116.593064148572,-4.84934893978864,
129.983996111587));
#103341=CARTESIAN_POINT('Ctrl Pts',(-116.60083993049,-4.87218154381213,
130.118964486385));
#103342=CARTESIAN_POINT('Ctrl Pts',(-116.608615712409,-4.88934583784685,
130.254713114104));
#103343=CARTESIAN_POINT('Ctrl Pts',(-116.616391494328,-4.90082561797627,
130.39072874659));
#103344=CARTESIAN_POINT('Ctrl Pts',(-116.617281907059,-4.90214017932632,
130.406304035615));
#103345=CARTESIAN_POINT('Ctrl Pts',(-116.618172319789,-4.90338025709753,
130.421882828062));
#103346=CARTESIAN_POINT('Ctrl Pts',(-116.619062732521,-4.90454587046754,
130.437464355688));
#103347=CARTESIAN_POINT('Ctrl Pts',(-116.625994967011,-4.9136206567155,
130.558773047115));
#103348=CARTESIAN_POINT('Ctrl Pts',(-116.632927201502,-4.91819545210003,
130.680422555685));
#103349=CARTESIAN_POINT('Ctrl Pts',(-116.639859435993,-4.91824951514299,
130.802176745828));
#103350=CARTESIAN_POINT('Ctrl Pts',(-116.639859436028,-4.91824951514326,
130.802176746446));
#103351=CARTESIAN_POINT('Ctrl Pts',(-116.647550252922,-4.91830949419432,
130.937254286567));
#103352=CARTESIAN_POINT('Ctrl Pts',(-116.655241069817,-4.91280050443035,
131.072559157636));
#103353=CARTESIAN_POINT('Ctrl Pts',(-116.662931886711,-4.9016926349703,
131.207588065513));
#103354=CARTESIAN_POINT('Ctrl Pts',(-116.670613714433,-4.8905977485991,
131.342459149038));
#103355=CARTESIAN_POINT('Ctrl Pts',(-116.678295542154,-4.87391703091717,
131.477054516098));
#103356=CARTESIAN_POINT('Ctrl Pts',(-116.685977369876,-4.85167255973251,
131.610869412086));
#103357=CARTESIAN_POINT('Ctrl Pts',(-116.69365215102,-4.82944849350706,
131.744561559034));
#103358=CARTESIAN_POINT('Ctrl Pts',(-116.701326932164,-4.80167089195159,
131.877474267016));
#103359=CARTESIAN_POINT('Ctrl Pts',(-116.709001713309,-4.76841371866942,
132.009106927004));
#103360=CARTESIAN_POINT('Ctrl Pts',(-116.716856240102,-4.73437765253562,
132.14382246289));
#103361=CARTESIAN_POINT('Ctrl Pts',(-116.724710766894,-4.69460219268531,
132.277196824325));
#103362=CARTESIAN_POINT('Ctrl Pts',(-116.732565293687,-4.64922239386322,
132.408702911125));
#103363=CARTESIAN_POINT('Ctrl Pts',(-116.740232642522,-4.60492402213343,
132.537075131121));
#103364=CARTESIAN_POINT('Ctrl Pts',(-116.747899991357,-4.55528555475067,
132.663666720708));
#103365=CARTESIAN_POINT('Ctrl Pts',(-116.755567340191,-4.500483211658,132.788002199124));
#103366=CARTESIAN_POINT('Ctrl Pts',(-116.76323391152,-4.44568642578892,
132.912325069318));
#103367=CARTESIAN_POINT('Ctrl Pts',(-116.770900482848,-4.38572696672752,
133.034391917382));
#103368=CARTESIAN_POINT('Ctrl Pts',(-116.778567054177,-4.32082899001699,
133.153747750741));
#103369=CARTESIAN_POINT('Ctrl Pts',(-116.786234592332,-4.25592282905808,
133.273118636));
#103370=CARTESIAN_POINT('Ctrl Pts',(-116.793902130488,-4.1860771030835,
133.389777475395));
#103371=CARTESIAN_POINT('Ctrl Pts',(-116.801569668643,-4.11156140404656,
133.503294830039));
#103372=CARTESIAN_POINT('Ctrl Pts',(-116.809564725951,-4.03386276440252,
133.621661082328));
#103373=CARTESIAN_POINT('Ctrl Pts',(-116.817559783258,-3.95108662217911,
133.736611128411));
#103374=CARTESIAN_POINT('Ctrl Pts',(-116.825554840566,-3.8635872492604,
133.847693762303));
#103375=CARTESIAN_POINT('Ctrl Pts',(-116.833233736856,-3.77954800047656,
133.954383682399));
#103376=CARTESIAN_POINT('Ctrl Pts',(-116.840912633146,-3.69115225753485,
134.057505957197));
#103377=CARTESIAN_POINT('Ctrl Pts',(-116.848591529437,-3.59875294848772,
134.15669715769));
#103378=CARTESIAN_POINT('Ctrl Pts',(-116.856275636906,-3.50629093390068,
134.255955672948));
#103379=CARTESIAN_POINT('Ctrl Pts',(-116.863959744375,-3.40982022794286,
134.351277523349));
#103380=CARTESIAN_POINT('Ctrl Pts',(-116.871643851844,-3.30972829668614,
134.442338306422));
#103381=CARTESIAN_POINT('Ctrl Pts',(-116.879338453627,-3.20949966821425,
134.533523452721));
#103382=CARTESIAN_POINT('Ctrl Pts',(-116.88703305541,-3.10564025306591,
134.620435667313));
#103383=CARTESIAN_POINT('Ctrl Pts',(-116.894727657192,-2.99856814818128,
134.70279262585));
#103384=CARTESIAN_POINT('Ctrl Pts',(-116.895655223573,-2.98566085452607,
134.712720565994));
#103385=CARTESIAN_POINT('Ctrl Pts',(-116.896582789953,-2.97270690586817,
134.722582364275));
#103386=CARTESIAN_POINT('Ctrl Pts',(-116.897510356333,-2.9597070593381,
134.732377570865));
#103387=CARTESIAN_POINT('Ctrl Pts',(-116.905284690452,-2.85074973557279,
134.814475424349));
#103388=CARTESIAN_POINT('Ctrl Pts',(-116.913059024572,-2.7382013347078,
134.892166409122));
#103389=CARTESIAN_POINT('Ctrl Pts',(-116.920833358691,-2.62245395594538,
134.965119960696));
#103390=CARTESIAN_POINT('Ctrl Pts',(-116.928598111638,-2.50684922548233,
135.037983603538));
#103391=CARTESIAN_POINT('Ctrl Pts',(-116.936362864585,-2.38805368900595,
135.106121223517));
#103392=CARTESIAN_POINT('Ctrl Pts',(-116.944127617532,-2.26649172944012,
135.169243010355));
#103393=CARTESIAN_POINT('Ctrl Pts',(-116.951884658417,-2.14505050692625,
135.232302103744));
#103394=CARTESIAN_POINT('Ctrl Pts',(-116.959641699302,-2.02084867400246,
135.290355098988));
#103395=CARTESIAN_POINT('Ctrl Pts',(-116.967398740187,-1.8943384495246,
135.343156151753));
#103396=CARTESIAN_POINT('Ctrl Pts',(-116.975149931427,-1.76792362739129,
135.395917386832));
#103397=CARTESIAN_POINT('Ctrl Pts',(-116.982901122667,-1.63920423795447,
135.443434412651));
#103398=CARTESIAN_POINT('Ctrl Pts',(-116.990652313907,-1.50865556838574,
135.48550806648));
#103399=CARTESIAN_POINT('Ctrl Pts',(-116.998400210684,-1.3781623854839,
135.527563837885));
#103400=CARTESIAN_POINT('Ctrl Pts',(-117.006148107461,-1.24584184016237,
135.564180719154));
#103401=CARTESIAN_POINT('Ctrl Pts',(-117.013896004239,-1.11218739011541,
135.595208378847));
#103402=CARTESIAN_POINT('Ctrl Pts',(-117.021642280323,-0.978560897698143,
135.626229548222));
#103403=CARTESIAN_POINT('Ctrl Pts',(-117.029388556407,-0.843601436146065,
135.651663733157));
#103404=CARTESIAN_POINT('Ctrl Pts',(-117.037134832491,-0.707815368325756,
135.671411107017));
#103405=CARTESIAN_POINT('Ctrl Pts',(-117.044881165756,-0.572028298163726,
135.691158626647));
#103406=CARTESIAN_POINT('Ctrl Pts',(-117.052627499022,-0.435414996452943,
135.705219195169));
#103407=CARTESIAN_POINT('Ctrl Pts',(-117.060373832287,-0.298489315003407,
135.713544581457));
#103408=CARTESIAN_POINT('Ctrl Pts',(-117.06812190029,-0.161532969996699,
135.721871832159));
#103409=CARTESIAN_POINT('Ctrl Pts',(-117.075869968293,-0.0242644962181748,
135.724461321187));
#103410=CARTESIAN_POINT('Ctrl Pts',(-117.083618036296,0.112800268468153,
135.721316907989));
#103411=CARTESIAN_POINT('Ctrl Pts',(-117.091374339038,0.250010707217295,
135.718169152871));
#103412=CARTESIAN_POINT('Ctrl Pts',(-117.09913064178,0.387016612897677,
135.709275330968));
#103413=CARTESIAN_POINT('Ctrl Pts',(-117.106886944522,0.523304730641585,
135.694691406111));
#103414=CARTESIAN_POINT('Ctrl Pts',(-117.114647387036,0.659665589457489,
135.680099697374));
#103415=CARTESIAN_POINT('Ctrl Pts',(-117.12240782955,0.795307510492773,
135.65981189205));
#103416=CARTESIAN_POINT('Ctrl Pts',(-117.130168272064,0.929726465333926,
135.633935315421));
#103417=CARTESIAN_POINT('Ctrl Pts',(-117.137941172329,1.06436120141491,
135.608017199413));
#103418=CARTESIAN_POINT('Ctrl Pts',(-117.145714072595,1.19776866746943,
135.576492473962));
#103419=CARTESIAN_POINT('Ctrl Pts',(-117.15348697286,1.32945818214053,135.539518904724));
#103420=CARTESIAN_POINT('Ctrl Pts',(-117.160977308622,1.45636045124926,
135.503889417858));
#103421=CARTESIAN_POINT('Ctrl Pts',(-117.168467644385,1.58166721122214,
135.463200462837));
#103422=CARTESIAN_POINT('Ctrl Pts',(-117.175957980147,1.70495794959927,
135.417635100252));
#103423=CARTESIAN_POINT('Ctrl Pts',(-117.183732314266,1.8329232937934,135.370342113096));
#103424=CARTESIAN_POINT('Ctrl Pts',(-117.191506648385,1.95912207942153,
135.317645830889));
#103425=CARTESIAN_POINT('Ctrl Pts',(-117.199280982504,2.08306425402082,
135.259697459615));
#103426=CARTESIAN_POINT('Ctrl Pts',(-117.207045735451,2.20685368096696,
135.20182050453));
#103427=CARTESIAN_POINT('Ctrl Pts',(-117.214810488398,2.32839167962045,
135.13870450318));
#103428=CARTESIAN_POINT('Ctrl Pts',(-117.222575241345,2.44720503505027,
135.070549851405));
#103429=CARTESIAN_POINT('Ctrl Pts',(-117.23033228223,2.5659003833805,135.002462891791));
#103430=CARTESIAN_POINT('Ctrl Pts',(-117.238089323115,2.68187613691915,
134.929347434126));
#103431=CARTESIAN_POINT('Ctrl Pts',(-117.245846364,2.79468102452733,134.851451058073));
#103432=CARTESIAN_POINT('Ctrl Pts',(-117.25359755524,2.90740084509273,134.773613424284));
#103433=CARTESIAN_POINT('Ctrl Pts',(-117.26134874648,3.0169542388032,134.69100226955));
#103434=CARTESIAN_POINT('Ctrl Pts',(-117.269099937721,3.12291674008852,
134.603909814112));
#103435=CARTESIAN_POINT('Ctrl Pts',(-117.276847834498,3.22883420448401,
134.516854375291));
#103436=CARTESIAN_POINT('Ctrl Pts',(-117.284595731275,3.3311635105954,134.425321671742));
#103437=CARTESIAN_POINT('Ctrl Pts',(-117.292343628052,3.42951145438546,
134.329645605583));
#103438=CARTESIAN_POINT('Ctrl Pts',(-117.300089904136,3.52783882590582,
134.233989552794));
#103439=CARTESIAN_POINT('Ctrl Pts',(-117.30783618022,3.62218621156281,134.134192133762));
#103440=CARTESIAN_POINT('Ctrl Pts',(-117.315582456304,3.71219592288139,
134.030625407171));
#103441=CARTESIAN_POINT('Ctrl Pts',(-117.323328789569,3.80220629863084,
133.927057916074));
#103442=CARTESIAN_POINT('Ctrl Pts',(-117.331075122835,3.88787867968421,
133.819721356989));
#103443=CARTESIAN_POINT('Ctrl Pts',(-117.3388214561,3.96889473837512,133.709021977897));
#103444=CARTESIAN_POINT('Ctrl Pts',(-117.346569524103,4.04992894005076,
133.598297808446));
#103445=CARTESIAN_POINT('Ctrl Pts',(-117.354317592106,4.12630451355463,
133.484209635882));
#103446=CARTESIAN_POINT('Ctrl Pts',(-117.362065660109,4.19774588298238,
133.367193535336));
#103447=CARTESIAN_POINT('Ctrl Pts',(-117.369821962851,4.26926318114782,
133.250053068685));
#103448=CARTESIAN_POINT('Ctrl Pts',(-117.377578265593,4.33583559546947,
133.129978792044));
#103449=CARTESIAN_POINT('Ctrl Pts',(-117.385334568335,4.39723278311197,
133.007432771088));
#103450=CARTESIAN_POINT('Ctrl Pts',(-117.393095010849,4.45866274028231,
132.884821343631));
#103451=CARTESIAN_POINT('Ctrl Pts',(-117.400855453363,4.51491180664084,
132.75973589955));
#103452=CARTESIAN_POINT('Ctrl Pts',(-117.408615895877,4.56579783831658,
132.63265850416));
#103453=CARTESIAN_POINT('Ctrl Pts',(-117.416388796143,4.61676555676768,
132.505377112854));
#103454=CARTESIAN_POINT('Ctrl Pts',(-117.424161696408,4.66235290647963,
132.376097749226));
#103455=CARTESIAN_POINT('Ctrl Pts',(-117.431934596673,4.70242739490873,
132.245318513589));
#103456=CARTESIAN_POINT('Ctrl Pts',(-117.439424932435,4.74104507474156,
132.119293432582));
#103457=CARTESIAN_POINT('Ctrl Pts',(-117.446915268197,4.77454366906303,
131.991875932476));
#103458=CARTESIAN_POINT('Ctrl Pts',(-117.454405603959,4.80284989467795,
131.863518751034));
#103459=CARTESIAN_POINT('Ctrl Pts',(-117.462179938078,4.83222935944075,
131.730294868044));
#103460=CARTESIAN_POINT('Ctrl Pts',(-117.469954272197,4.85610801099285,
131.595636627849));
#103461=CARTESIAN_POINT('Ctrl Pts',(-117.477728606316,4.87434817788376,
131.460038055992));
#103462=CARTESIAN_POINT('Ctrl Pts',(-117.485493359264,4.8925658653992,131.324606597257));
#103463=CARTESIAN_POINT('Ctrl Pts',(-117.493258112211,4.90515884292857,
131.188237496431));
#103464=CARTESIAN_POINT('Ctrl Pts',(-117.501022865158,4.91203992493745,
131.051437201484));
#103465=CARTESIAN_POINT('Ctrl Pts',(-117.508779906043,4.91891417255864,
130.914772778519));
#103466=CARTESIAN_POINT('Ctrl Pts',(-117.516536946928,4.92008779494067,
130.777678401651));
#103467=CARTESIAN_POINT('Ctrl Pts',(-117.524293987813,4.91552516479242,
130.640667560925));
#103468=CARTESIAN_POINT('Ctrl Pts',(-117.532045179053,4.91096597535903,
130.503760041139));
#103469=CARTESIAN_POINT('Ctrl Pts',(-117.539796370293,4.90067915650337,
130.366936321274));
#103470=CARTESIAN_POINT('Ctrl Pts',(-117.547547561533,4.88468112737937,
130.230711468413));
#103471=CARTESIAN_POINT('Ctrl Pts',(-117.55529545831,4.86868989784457,130.094544514749));
#103472=CARTESIAN_POINT('Ctrl Pts',(-117.563043355088,4.84699233149375,
129.958976309323));
#103473=CARTESIAN_POINT('Ctrl Pts',(-117.570791251865,4.81965681324779,
129.824518148077));
#103474=CARTESIAN_POINT('Ctrl Pts',(-117.578537527949,4.79232701300297,
129.69008811258));
#103475=CARTESIAN_POINT('Ctrl Pts',(-117.586283804033,4.75936168447198,
129.556768042296));
#103476=CARTESIAN_POINT('Ctrl Pts',(-117.594030080117,4.72088051180578,
129.425059977476));
#103477=CARTESIAN_POINT('Ctrl Pts',(-117.601776413382,4.68239905508025,
129.293350940417));
#103478=CARTESIAN_POINT('Ctrl Pts',(-117.609522746648,4.63840178261667,
129.163254307842));
#103479=CARTESIAN_POINT('Ctrl Pts',(-117.617269079913,4.5890584184665,129.035257484789));
#103480=CARTESIAN_POINT('Ctrl Pts',(-117.625017147916,4.53970400421199,
128.907231997735));
#103481=CARTESIAN_POINT('Ctrl Pts',(-117.632765215919,4.48500125654532,
128.781307620648));
#103482=CARTESIAN_POINT('Ctrl Pts',(-117.640513283922,4.42516810231528,
128.657951912601));
#103483=CARTESIAN_POINT('Ctrl Pts',(-117.648269586664,4.36527135669697,
128.534465100639));
#103484=CARTESIAN_POINT('Ctrl Pts',(-117.656025889406,4.30023348314129,
128.41355276354));
#103485=CARTESIAN_POINT('Ctrl Pts',(-117.663782192148,4.23031872465806,
128.295658453038));
#103486=CARTESIAN_POINT('Ctrl Pts',(-117.671542634662,4.16036665056294,
128.177701218793));
#103487=CARTESIAN_POINT('Ctrl Pts',(-117.679303077176,4.0855327181803,128.062765548301));
#103488=CARTESIAN_POINT('Ctrl Pts',(-117.68706351969,4.00612404950091,127.951265252439));
#103489=CARTESIAN_POINT('Ctrl Pts',(-117.694836419956,3.9265879069772,127.839585966403));
#103490=CARTESIAN_POINT('Ctrl Pts',(-117.702609320221,3.84246259302732,
127.731353384125));
#103491=CARTESIAN_POINT('Ctrl Pts',(-117.710382220487,3.75409555809586,
127.626948210719));
#103492=CARTESIAN_POINT('Ctrl Pts',(-117.717872556249,3.66894088746801,
127.526338428348));
#103493=CARTESIAN_POINT('Ctrl Pts',(-117.725362892011,3.57984774445693,
127.429282841063));
#103494=CARTESIAN_POINT('Ctrl Pts',(-117.732853227773,3.48715741880841,
127.336087819912));
#103495=CARTESIAN_POINT('Ctrl Pts',(-117.740627561892,3.39095271128988,
127.239359281207));
#103496=CARTESIAN_POINT('Ctrl Pts',(-117.748401896011,3.29056791452693,
127.146483427342));
#103497=CARTESIAN_POINT('Ctrl Pts',(-117.75617623013,3.1863442514188,127.057843118081));
#103498=CARTESIAN_POINT('Ctrl Pts',(-117.763940983077,3.08224903466071,
126.969312050079));
#103499=CARTESIAN_POINT('Ctrl Pts',(-117.771705736024,2.974324659918,126.885006391435));
#103500=CARTESIAN_POINT('Ctrl Pts',(-117.779470488971,2.86295009029976,
126.805273241307));
#103501=CARTESIAN_POINT('Ctrl Pts',(-117.787227529856,2.75168613947388,
126.725619283268));
#103502=CARTESIAN_POINT('Ctrl Pts',(-117.794984570741,2.63697912906497,
126.650529022105));
#103503=CARTESIAN_POINT('Ctrl Pts',(-117.802741611626,2.51924181536975,
126.580309985981));
#103504=CARTESIAN_POINT('Ctrl Pts',(-117.810492802866,2.4015932882988,126.510143902578));
#103505=CARTESIAN_POINT('Ctrl Pts',(-117.818243994106,2.2809193408671,126.444841931928));
#103506=CARTESIAN_POINT('Ctrl Pts',(-117.825995185346,2.15766218855235,
126.384668666469));
#103507=CARTESIAN_POINT('Ctrl Pts',(-117.833743082123,2.03445742381516,
126.324520976253));
#103508=CARTESIAN_POINT('Ctrl Pts',(-117.8414909789,1.90867198849386,126.269497826861));
#103509=CARTESIAN_POINT('Ctrl Pts',(-117.849238875677,1.78077301406596,
126.219818052067));
#103510=CARTESIAN_POINT('Ctrl Pts',(-117.856985151762,1.65290079334634,
126.170148669211));
#103511=CARTESIAN_POINT('Ctrl Pts',(-117.864731427846,1.52291627710181,
126.125820579218));
#103512=CARTESIAN_POINT('Ctrl Pts',(-117.87247770393,1.39130653822156,126.087004453442));
#103513=CARTESIAN_POINT('Ctrl Pts',(-117.880224037195,1.2596958278283,126.048188041134));
#103514=CARTESIAN_POINT('Ctrl Pts',(-117.88797037046,1.12646024585573,126.014883784831));
#103515=CARTESIAN_POINT('Ctrl Pts',(-117.895716703726,0.992101599961341,
125.987212345211));
#103516=CARTESIAN_POINT('Ctrl Pts',(-117.903464771729,0.857712865380334,
125.959534708764));
#103517=CARTESIAN_POINT('Ctrl Pts',(-117.911212839732,0.722200949271972,
125.937492477949));
#103518=CARTESIAN_POINT('Ctrl Pts',(-117.918960907734,0.586077017110458,
125.921155031835));
#103519=CARTESIAN_POINT('Ctrl Pts',(-117.926717210476,0.44980841081339,
125.904800222089));
#103520=CARTESIAN_POINT('Ctrl Pts',(-117.934473513218,0.312926877901743,
125.894162355429));
#103521=CARTESIAN_POINT('Ctrl Pts',(-117.94222981596,0.175948420813479,
125.889258867275));
#103522=CARTESIAN_POINT('Ctrl Pts',(-117.949990258474,0.0388968541975787,
125.884352761981));
#103523=CARTESIAN_POINT('Ctrl Pts',(-117.957750700988,-0.0982513489073537,
125.885187131341));
#103524=CARTESIAN_POINT('Ctrl Pts',(-117.965511143502,-0.234982030754595,
125.891727259811));
#103525=CARTESIAN_POINT('Ctrl Pts',(-117.973284043768,-0.371932204829973,
125.898277887077));
#103526=CARTESIAN_POINT('Ctrl Pts',(-117.981056944033,-0.508463128671392,
125.910552541806));
#103527=CARTESIAN_POINT('Ctrl Pts',(-117.988829844299,-0.644066698830658,
125.928464684514));
#103528=CARTESIAN_POINT('Ctrl Pts',(-117.996320180061,-0.774740737653156,
125.945725675717));
#103529=CARTESIAN_POINT('Ctrl Pts',(-118.003810515823,-0.904553372015585,
125.968221344539));
#103530=CARTESIAN_POINT('Ctrl Pts',(-118.011300851585,-1.03306236783459,
125.995830155287));
#103531=CARTESIAN_POINT('Ctrl Pts',(-118.019075185704,-1.16644382128672,
126.024485762485));
#103532=CARTESIAN_POINT('Ctrl Pts',(-118.026849519823,-1.29884334221009,
126.058740667415));
#103533=CARTESIAN_POINT('Ctrl Pts',(-118.034623853942,-1.42975438053048,
126.09851473464));
#103534=CARTESIAN_POINT('Ctrl Pts',(-118.042388606889,-1.56050408269493,
126.138239783881));
#103535=CARTESIAN_POINT('Ctrl Pts',(-118.050153359837,-1.68976858171951,
126.183470349152));
#103536=CARTESIAN_POINT('Ctrl Pts',(-118.057918112784,-1.81705101443552,
126.234075213629));
#103537=CARTESIAN_POINT('Ctrl Pts',(-118.065675153668,-1.94420702844499,
126.284629816641));
#103538=CARTESIAN_POINT('Ctrl Pts',(-118.073432194553,-2.06938453282734,
126.340547952829));
#103539=CARTESIAN_POINT('Ctrl Pts',(-118.081189235438,-2.19210169057048,
126.401648585114));
#103540=CARTESIAN_POINT('Ctrl Pts',(-118.088940426678,-2.31472630635053,
126.462703140937));
#103541=CARTESIAN_POINT('Ctrl Pts',(-118.096691617918,-2.43489391991838,
126.528932240348));
#103542=CARTESIAN_POINT('Ctrl Pts',(-118.104442809159,-2.55214289389311,
126.60010685362));
#103543=CARTESIAN_POINT('Ctrl Pts',(-118.112190705936,-2.66934203392666,
126.671251215783));
#103544=CARTESIAN_POINT('Ctrl Pts',(-118.119938602713,-2.7836246681184,
126.747336708686));
#103545=CARTESIAN_POINT('Ctrl Pts',(-118.12768649949,-2.89455418944136,
126.828088606387));
#103546=CARTESIAN_POINT('Ctrl Pts',(-118.135432775574,-3.00546050670013,
126.908823612532));
#103547=CARTESIAN_POINT('Ctrl Pts',(-118.143179051658,-3.11301479032648,
126.994222851986));
#103548=CARTESIAN_POINT('Ctrl Pts',(-118.150925327742,-3.21681017488339,
127.083968788569));
#103549=CARTESIAN_POINT('Ctrl Pts',(-118.158671661007,-3.32060632563383,
127.173715387636));
#103550=CARTESIAN_POINT('Ctrl Pts',(-118.166417994273,-3.42064322620289,
127.267808492144));
#103551=CARTESIAN_POINT('Ctrl Pts',(-118.174164327538,-3.5165481220496,
127.365891137142));
#103552=CARTESIAN_POINT('Ctrl Pts',(-118.181912395541,-3.61247449513265,
127.463995747068));
#103553=CARTESIAN_POINT('Ctrl Pts',(-118.189660463544,-3.70426674890516,
127.56609139582));
#103554=CARTESIAN_POINT('Ctrl Pts',(-118.197408531547,-3.79159021536647,
127.671785526489));
#103555=CARTESIAN_POINT('Ctrl Pts',(-118.205164834289,-3.87900649024745,
127.777591990138));
#103556=CARTESIAN_POINT('Ctrl Pts',(-118.212921137031,-3.96194424080455,
127.887004273689));
#103557=CARTESIAN_POINT('Ctrl Pts',(-118.220677439772,-4.04010988620406,
127.999597673947));
#103558=CARTESIAN_POINT('Ctrl Pts',(-118.228437882287,-4.11831725096182,
128.112251168693));
#103559=CARTESIAN_POINT('Ctrl Pts',(-118.236198324801,-4.19174722619774,
128.228088833223));
#103560=CARTESIAN_POINT('Ctrl Pts',(-118.243958767315,-4.26015110426036,
128.346659327464));
#103561=CARTESIAN_POINT('Ctrl Pts',(-118.25173166758,-4.32866479030085,
128.465420161589));
#103562=CARTESIAN_POINT('Ctrl Pts',(-118.259504567846,-4.39213607493075,
128.58692224528));
#103563=CARTESIAN_POINT('Ctrl Pts',(-118.267277468111,-4.45036312394494,
128.710691320009));
#103564=CARTESIAN_POINT('Ctrl Pts',(-118.274767803873,-4.50647347306347,
128.82996107712));
#103565=CARTESIAN_POINT('Ctrl Pts',(-118.282258139635,-4.5577141294953,
128.951335581379));
#103566=CARTESIAN_POINT('Ctrl Pts',(-118.289748475398,-4.60394830633779,
129.074377075717));
#103567=CARTESIAN_POINT('Ctrl Pts',(-118.298680373519,-4.65908054211458,
129.221098681668));
#103568=CARTESIAN_POINT('Ctrl Pts',(-118.30761227164,-4.70723965118029,
129.37057606111));
#103569=CARTESIAN_POINT('Ctrl Pts',(-118.316544169762,-4.74817859164396,
129.522181564409));
#103570=CARTESIAN_POINT('Ctrl Pts',(-118.317726371907,-4.75359716030281,
129.542247663321));
#103571=CARTESIAN_POINT('Ctrl Pts',(-118.318908574052,-4.75888930957911,
129.562351010166));
#103572=CARTESIAN_POINT('Ctrl Pts',(-118.320090776197,-4.76405452823413,
129.582490119309));
#103573=CARTESIAN_POINT('Origin',(213.235140564004,0.,130.804360617566));
#103574=CARTESIAN_POINT('',(-120.415010068595,-4.76405452823409,129.582490119308));
#103575=CARTESIAN_POINT('',(-120.07000000496,-4.76405452823398,129.582490119308));
#103576=CARTESIAN_POINT('',(213.235140564004,-4.76405452823405,129.582490119308));
#103577=CARTESIAN_POINT('',(-118.735140564061,-4.91824846256215,130.808249448373));
#103578=CARTESIAN_POINT('Ctrl Pts',(-118.735140564061,-4.91824846256215,
130.808249448372));
#103579=CARTESIAN_POINT('Ctrl Pts',(-118.744195936264,-4.91812165730422,
130.968621497431));
#103580=CARTESIAN_POINT('Ctrl Pts',(-118.753251308467,-4.91014697441995,
131.128664503842));
#103581=CARTESIAN_POINT('Ctrl Pts',(-118.76230668067,-4.8944441109897,131.287682360195));
#103582=CARTESIAN_POINT('Ctrl Pts',(-118.771417983749,-4.87864425818275,
131.447682396827));
#103583=CARTESIAN_POINT('Ctrl Pts',(-118.780529286828,-4.85502057080147,
131.606644491328));
#103584=CARTESIAN_POINT('Ctrl Pts',(-118.789640589907,-4.82374402601055,
131.763879577268));
#103585=CARTESIAN_POINT('Ctrl Pts',(-118.798816522011,-4.79224562792691,
131.922229975714));
#103586=CARTESIAN_POINT('Ctrl Pts',(-118.807992454115,-4.75298549464554,
132.078828692096));
#103587=CARTESIAN_POINT('Ctrl Pts',(-118.817168386218,-4.70618648829651,
132.232993460488));
#103588=CARTESIAN_POINT('Ctrl Pts',(-118.820463833101,-4.68937907975926,
132.288360239541));
#103589=CARTESIAN_POINT('Ctrl Pts',(-118.823759279983,-4.67159973789066,
132.343413290778));
#103590=CARTESIAN_POINT('Ctrl Pts',(-118.827054726866,-4.65286026331153,
132.398121714028));
#103591=CARTESIAN_POINT('Ctrl Pts',(-118.834829060985,-4.60865171078849,
132.527185108655));
#103592=CARTESIAN_POINT('Ctrl Pts',(-118.842603395104,-4.55899902669587,
132.654612117623));
#103593=CARTESIAN_POINT('Ctrl Pts',(-118.850377729223,-4.50404161356523,
132.779909201067));
#103594=CARTESIAN_POINT('Ctrl Pts',(-118.85814248217,-4.44915193053458,
132.905051867054));
#103595=CARTESIAN_POINT('Ctrl Pts',(-118.865907235117,-4.38897068188437,
133.028069475768));
#103596=CARTESIAN_POINT('Ctrl Pts',(-118.873671988064,-4.32368684989084,
133.148484139606));
#103597=CARTESIAN_POINT('Ctrl Pts',(-118.881429028949,-4.25846785871959,
133.268779205902));
#103598=CARTESIAN_POINT('Ctrl Pts',(-118.889186069834,-4.18815655480457,
133.386476130671));
#103599=CARTESIAN_POINT('Ctrl Pts',(-118.896943110719,-4.11298961724899,
133.501117831499));
#103600=CARTESIAN_POINT('Ctrl Pts',(-118.904694301959,-4.03787936366583,
133.615673080129));
#103601=CARTESIAN_POINT('Ctrl Pts',(-118.912445493199,-3.95792097828162,
133.727177365098));
#103602=CARTESIAN_POINT('Ctrl Pts',(-118.920196684439,-3.87339641117935,
133.83519933059));
#103603=CARTESIAN_POINT('Ctrl Pts',(-118.927944581216,-3.78890776927276,
133.943175383865));
#103604=CARTESIAN_POINT('Ctrl Pts',(-118.935692477993,-3.69985704607525,
134.047671754166));
#103605=CARTESIAN_POINT('Ctrl Pts',(-118.94344037477,-3.60656861173551,
134.148287337957));
#103606=CARTESIAN_POINT('Ctrl Pts',(-118.951186650855,-3.51329969132516,
134.248881875137));
#103607=CARTESIAN_POINT('Ctrl Pts',(-118.958932926939,-3.41579508859549,
134.345596953963));
#103608=CARTESIAN_POINT('Ctrl Pts',(-118.966679203023,-3.31441817155045,
134.438066060581));
#103609=CARTESIAN_POINT('Ctrl Pts',(-118.974425536288,-3.21304050616417,
134.530535849785));
#103610=CARTESIAN_POINT('Ctrl Pts',(-118.982171869553,-3.10779075827736,
134.618759340768));
#103611=CARTESIAN_POINT('Ctrl Pts',(-118.989918202819,-2.99906741989393,
134.702408548702));
#103612=CARTESIAN_POINT('Ctrl Pts',(-118.997666270822,-2.89031973367286,
134.786076489296));
#103613=CARTESIAN_POINT('Ctrl Pts',(-119.005414338824,-2.77809721885831,
134.865167870087));
#103614=CARTESIAN_POINT('Ctrl Pts',(-119.013162406827,-2.66282921193867,
134.939396729929));
#103615=CARTESIAN_POINT('Ctrl Pts',(-119.020918709569,-2.54743869680942,
135.013704481087));
#103616=CARTESIAN_POINT('Ctrl Pts',(-119.028675012311,-2.42899655297738,
135.083139175756));
#103617=CARTESIAN_POINT('Ctrl Pts',(-119.036431315053,-2.30795918546113,
135.147459449132));
#103618=CARTESIAN_POINT('Ctrl Pts',(-119.044191757567,-2.18685721665748,
135.211814052174));
#103619=CARTESIAN_POINT('Ctrl Pts',(-119.051952200081,-2.06315761659144,
135.27104862595));
#103620=CARTESIAN_POINT('Ctrl Pts',(-119.059712642595,-1.93733794080425,
135.324969510804));
#103621=CARTESIAN_POINT('Ctrl Pts',(-119.067485542861,-1.81131628810374,
135.378976954249));
#103622=CARTESIAN_POINT('Ctrl Pts',(-119.075258443126,-1.68316812443365,
135.427653524195));
#103623=CARTESIAN_POINT('Ctrl Pts',(-119.083031343392,-1.55338822721128,
135.470854813219));
#103624=CARTESIAN_POINT('Ctrl Pts',(-119.090521679153,-1.42832615615053,
135.512485626568));
#103625=CARTESIAN_POINT('Ctrl Pts',(-119.098012014915,-1.30174922303526,
135.549032242796));
#103626=CARTESIAN_POINT('Ctrl Pts',(-119.105502350677,-1.17410827665724,
135.580410535352));
#103627=CARTESIAN_POINT('Ctrl Pts',(-119.113276684796,-1.04162778500035,
135.612978545408));
#103628=CARTESIAN_POINT('Ctrl Pts',(-119.121051018915,-0.90758134484875,
135.64008174697));
#103629=CARTESIAN_POINT('Ctrl Pts',(-119.128825353034,-0.772459535743308,
135.661570652981));
#103630=CARTESIAN_POINT('Ctrl Pts',(-119.136590105981,-0.637504252191772,
135.683033075837));
#103631=CARTESIAN_POINT('Ctrl Pts',(-119.144354858928,-0.501476619037,135.698894909309));
#103632=CARTESIAN_POINT('Ctrl Pts',(-119.152119611875,-0.36488084619152,
135.709056839615));
#103633=CARTESIAN_POINT('Ctrl Pts',(-119.15987665276,-0.228420742192922,
135.719208676949));
#103634=CARTESIAN_POINT('Ctrl Pts',(-119.167633693645,-0.0913940088197629,
135.723671848391));
#103635=CARTESIAN_POINT('Ctrl Pts',(-119.17539073453,0.0456868667119894,
135.722398414565));
#103636=CARTESIAN_POINT('Ctrl Pts',(-119.18314192577,0.182664368488983,
135.721125941045));
#103637=CARTESIAN_POINT('Ctrl Pts',(-119.19089311701,0.319695541790409,
135.714125476552));
#103638=CARTESIAN_POINT('Ctrl Pts',(-119.198644308251,0.456265073845951,
135.701401075321));
#103639=CARTESIAN_POINT('Ctrl Pts',(-119.206392205028,0.592776560207071,
135.6886820823));
#103640=CARTESIAN_POINT('Ctrl Pts',(-119.214140101805,0.728826407104518,
135.67024402744));
#103641=CARTESIAN_POINT('Ctrl Pts',(-119.221887998582,0.86390182478649,
135.646143006277));
#103642=CARTESIAN_POINT('Ctrl Pts',(-119.229634274666,0.998948987602972,
135.622047026527));
#103643=CARTESIAN_POINT('Ctrl Pts',(-119.23738055075,1.13302174198946,135.59229050528));
#103644=CARTESIAN_POINT('Ctrl Pts',(-119.245126826834,1.26561532018001,
135.556981044638));
#103645=CARTESIAN_POINT('Ctrl Pts',(-119.252873160099,1.39820987714642,
135.52167132335));
#103646=CARTESIAN_POINT('Ctrl Pts',(-119.260619493364,1.52932485833007,
135.480808681481));
#103647=CARTESIAN_POINT('Ctrl Pts',(-119.26836582663,1.658468926145,135.434551097828));
#103648=CARTESIAN_POINT('Ctrl Pts',(-119.276113894633,1.78764191487831,
135.388283155111));
#103649=CARTESIAN_POINT('Ctrl Pts',(-119.283861962636,1.91484274396684,
135.336617998323));
#103650=CARTESIAN_POINT('Ctrl Pts',(-119.291610030639,2.0395987593405,135.279762271429));
#103651=CARTESIAN_POINT('Ctrl Pts',(-119.29936633338,2.1644873668921,135.222846117591));
#103652=CARTESIAN_POINT('Ctrl Pts',(-119.307122636122,2.2869256138614,135.160728536035));
#103653=CARTESIAN_POINT('Ctrl Pts',(-119.314878938864,2.40646373514178,
135.093663049658));
#103654=CARTESIAN_POINT('Ctrl Pts',(-119.322639381378,2.5260656575167,135.026561768411));
#103655=CARTESIAN_POINT('Ctrl Pts',(-119.330399823892,2.64276403741153,
134.954507525532));
#103656=CARTESIAN_POINT('Ctrl Pts',(-119.338160266406,2.75613781303765,
134.87779742425));
#103657=CARTESIAN_POINT('Ctrl Pts',(-119.345933166672,2.86969358631325,
134.800964181102));
#103658=CARTESIAN_POINT('Ctrl Pts',(-119.353706066937,2.97991377585785,
134.71946037671));
#103659=CARTESIAN_POINT('Ctrl Pts',(-119.361478967203,3.0864094483368,134.633624225587));
#103660=CARTESIAN_POINT('Ctrl Pts',(-119.368969302965,3.18903373488107,
134.550908434761));
#103661=CARTESIAN_POINT('Ctrl Pts',(-119.376459638728,3.28819936233715,
134.464170014852));
#103662=CARTESIAN_POINT('Ctrl Pts',(-119.38394997449,3.38359185787179,134.373742805262));
#103663=CARTESIAN_POINT('Ctrl Pts',(-119.391724308609,3.4826011888631,134.279887020541));
#103664=CARTESIAN_POINT('Ctrl Pts',(-119.399498642728,3.57785925510838,
134.181759896525));
#103665=CARTESIAN_POINT('Ctrl Pts',(-119.407272976847,3.66897511868935,
134.07969337027));
#103666=CARTESIAN_POINT('Ctrl Pts',(-119.415037729794,3.75997869011147,
133.977752631888));
#103667=CARTESIAN_POINT('Ctrl Pts',(-119.422802482742,3.84684995822226,
133.87188244005));
#103668=CARTESIAN_POINT('Ctrl Pts',(-119.430567235689,3.9292328297505,133.76245331931));
#103669=CARTESIAN_POINT('Ctrl Pts',(-119.438324276574,4.01153387744935,
133.653132885116));
#103670=CARTESIAN_POINT('Ctrl Pts',(-119.446081317459,4.08935516643966,
133.540260866713));
#103671=CARTESIAN_POINT('Ctrl Pts',(-119.453838358344,4.16237935210778,
133.424242521707));
#103672=CARTESIAN_POINT('Ctrl Pts',(-119.461589549584,4.23534846966934,
133.308311667038));
#103673=CARTESIAN_POINT('Ctrl Pts',(-119.469340740824,4.30352747696971,
133.18923953796));
#103674=CARTESIAN_POINT('Ctrl Pts',(-119.477091932064,4.36664124581274,
133.067461873115));
#103675=CARTESIAN_POINT('Ctrl Pts',(-119.484839828841,4.42972818962049,
132.945735967026));
#103676=CARTESIAN_POINT('Ctrl Pts',(-119.492587725618,4.4877539973247,132.821307158672));
#103677=CARTESIAN_POINT('Ctrl Pts',(-119.500335622395,4.54048868830118,
132.694637193602));
#103678=CARTESIAN_POINT('Ctrl Pts',(-119.508081898479,4.59321234831713,
132.567993725157));
#103679=CARTESIAN_POINT('Ctrl Pts',(-119.515828174563,4.64064694289837,
132.439110393176));
#103680=CARTESIAN_POINT('Ctrl Pts',(-119.523574450647,4.68261016143461,
132.30847003464));
#103681=CARTESIAN_POINT('Ctrl Pts',(-119.531320783913,4.72457368973386,
132.177828711746));
#103682=CARTESIAN_POINT('Ctrl Pts',(-119.539067117178,4.76106564183005,
132.04543070865));
#103683=CARTESIAN_POINT('Ctrl Pts',(-119.546813450444,4.79195334979348,
131.911774792978));
#103684=CARTESIAN_POINT('Ctrl Pts',(-119.554561518446,4.8228479748449,131.77808894599));
#103685=CARTESIAN_POINT('Ctrl Pts',(-119.56230958645,4.84813577038141,131.643145006728));
#103686=CARTESIAN_POINT('Ctrl Pts',(-119.570057654452,4.8677351107512,131.507452328554));
#103687=CARTESIAN_POINT('Ctrl Pts',(-119.577813957194,4.8873552815332,131.371615434587));
#103688=CARTESIAN_POINT('Ctrl Pts',(-119.585570259936,4.90127486411613,
131.235028599643));
#103689=CARTESIAN_POINT('Ctrl Pts',(-119.593326562678,4.90946404546602,
131.098207259161));
#103690=CARTESIAN_POINT('Ctrl Pts',(-119.601087005192,4.91765759762857,
130.96131289301));
#103691=CARTESIAN_POINT('Ctrl Pts',(-119.608847447706,4.92011464726175,
130.824184162635));
#103692=CARTESIAN_POINT('Ctrl Pts',(-119.616607890221,4.91685756154329,
130.687335910796));
#103693=CARTESIAN_POINT('Ctrl Pts',(-119.624380790486,4.91359524726167,
130.550267977994));
#103694=CARTESIAN_POINT('Ctrl Pts',(-119.632153690751,4.90460049304488,
130.413481813817));
#103695=CARTESIAN_POINT('Ctrl Pts',(-119.639926591017,4.88994762037499,
130.277487452099));
#103696=CARTESIAN_POINT('Ctrl Pts',(-119.647416926779,4.87582741653501,
130.146436827979));
#103697=CARTESIAN_POINT('Ctrl Pts',(-119.654907262541,4.85645337120164,
130.016121742427));
#103698=CARTESIAN_POINT('Ctrl Pts',(-119.662397598303,4.83193637267114,
129.886987218694));
#103699=CARTESIAN_POINT('Ctrl Pts',(-119.670171932422,4.80648980468948,
129.752956520244));
#103700=CARTESIAN_POINT('Ctrl Pts',(-119.677946266541,4.77542198776316,
129.619773103844));
#103701=CARTESIAN_POINT('Ctrl Pts',(-119.68572060066,4.73880087844502,129.487945296724));
#103702=CARTESIAN_POINT('Ctrl Pts',(-119.693485353608,4.70222490137129,
129.356279955594));
#103703=CARTESIAN_POINT('Ctrl Pts',(-119.701250106555,4.66010935294053,
129.225967272698));
#103704=CARTESIAN_POINT('Ctrl Pts',(-119.709014859502,4.61257348884296,
129.097507116962));
#103705=CARTESIAN_POINT('Ctrl Pts',(-119.716771900387,4.56508483803575,
128.969174549664));
#103706=CARTESIAN_POINT('Ctrl Pts',(-119.724528941272,4.51218671984167,
128.842691212224));
#103707=CARTESIAN_POINT('Ctrl Pts',(-119.732285982157,4.45404855644619,
128.718543147287));
#103708=CARTESIAN_POINT('Ctrl Pts',(-119.740037173397,4.3959542354919,128.594488703372));
#103709=CARTESIAN_POINT('Ctrl Pts',(-119.747788364637,4.33262789981089,
128.472766379335));
#103710=CARTESIAN_POINT('Ctrl Pts',(-119.755539555877,4.26428743515272,
128.353843175698));
#103711=CARTESIAN_POINT('Ctrl Pts',(-119.763287452654,4.19597601701498,
128.234970517595));
#103712=CARTESIAN_POINT('Ctrl Pts',(-119.771035349432,4.12265490296274,
128.118894951939));
#103713=CARTESIAN_POINT('Ctrl Pts',(-119.778783246209,4.04458826245784,
128.00605955269));
#103714=CARTESIAN_POINT('Ctrl Pts',(-119.786529522293,3.96653795181122,
127.893247756173));
#103715=CARTESIAN_POINT('Ctrl Pts',(-119.794275798377,3.88374431147446,
127.783675099248));
#103716=CARTESIAN_POINT('Ctrl Pts',(-119.802022074461,3.7965150225374,127.677755950176));
#103717=CARTESIAN_POINT('Ctrl Pts',(-119.809768407726,3.70928508969366,
127.571836019232));
#103718=CARTESIAN_POINT('Ctrl Pts',(-119.817514740992,3.61761969145584,
127.469569951754));
#103719=CARTESIAN_POINT('Ctrl Pts',(-119.825261074257,3.5218667448967,127.371338961111));
#103720=CARTESIAN_POINT('Ctrl Pts',(-119.83300914226,3.42609235512896,127.273085972318));
#103721=CARTESIAN_POINT('Ctrl Pts',(-119.840757210263,3.32622886839154,
127.178870138385));
#103722=CARTESIAN_POINT('Ctrl Pts',(-119.848505278266,3.22266069743728,
127.089035451219));
#103723=CARTESIAN_POINT('Ctrl Pts',(-119.856261581008,3.11898245299859,
126.999105286678));
#103724=CARTESIAN_POINT('Ctrl Pts',(-119.86401788375,3.01159195480981,126.913565827022));
#103725=CARTESIAN_POINT('Ctrl Pts',(-119.871774186492,2.90090673863142,
126.832720760245));
#103726=CARTESIAN_POINT('Ctrl Pts',(-119.879534629006,2.79016244642049,
126.751832544022));
#103727=CARTESIAN_POINT('Ctrl Pts',(-119.88729507152,2.6761202572117,126.675643930255));
#103728=CARTESIAN_POINT('Ctrl Pts',(-119.895055514034,2.5592254128055,126.604414385892));
#103729=CARTESIAN_POINT('Ctrl Pts',(-119.9028284143,2.44214291841763,126.533070497541));
#103730=CARTESIAN_POINT('Ctrl Pts',(-119.910601314565,2.32219896014561,
126.466701776083));
#103731=CARTESIAN_POINT('Ctrl Pts',(-119.918374214831,2.19986281647702,
126.405521378496));
#103732=CARTESIAN_POINT('Ctrl Pts',(-119.925864550593,2.08197389978224,
126.346565042468));
#103733=CARTESIAN_POINT('Ctrl Pts',(-119.933354886354,1.96186398285667,
126.292426488647));
#103734=CARTESIAN_POINT('Ctrl Pts',(-119.940845222116,1.83996741419893,
126.243252969507));
#103735=CARTESIAN_POINT('Ctrl Pts',(-119.948619556235,1.71344910008603,
126.19221502144));
#103736=CARTESIAN_POINT('Ctrl Pts',(-119.956393890354,1.58460520599674,
126.146364365957));
#103737=CARTESIAN_POINT('Ctrl Pts',(-119.964168224473,1.45390013420282,
126.105918592568));
#103738=CARTESIAN_POINT('Ctrl Pts',(-119.97193297742,1.32335614472843,126.065522664981));
#103739=CARTESIAN_POINT('Ctrl Pts',(-119.979697730367,1.19095591130534,
126.03051848048));
#103740=CARTESIAN_POINT('Ctrl Pts',(-119.987462483314,1.05718444843186,
126.001075897242));
#103741=CARTESIAN_POINT('Ctrl Pts',(-119.995219524199,0.923545849260778,
125.971662556793));
#103742=CARTESIAN_POINT('Ctrl Pts',(-120.002976565084,0.788539110285869,
125.947799908369));
#103743=CARTESIAN_POINT('Ctrl Pts',(-120.010733605969,0.652664729780009,
125.929608130208));
#103744=CARTESIAN_POINT('Ctrl Pts',(-120.01848479721,0.516892813201622,
125.911430070609));
#103745=CARTESIAN_POINT('Ctrl Pts',(-120.02623598845,0.380254943366777,
125.898914420937));
#103746=CARTESIAN_POINT('Ctrl Pts',(-120.03398717969,0.243261793611174,
125.89213029293));
#103747=CARTESIAN_POINT('Ctrl Pts',(-120.041735076467,0.106326869598815,
125.885349048359));
#103748=CARTESIAN_POINT('Ctrl Pts',(-120.049482973244,-0.030962644330799,
125.884294499632));
#103749=CARTESIAN_POINT('Ctrl Pts',(-120.057230870021,-0.168091187459792,
125.888983885799));
#103750=CARTESIAN_POINT('Ctrl Pts',(-120.064977146105,-0.305191046253711,
125.893672291047));
#103751=CARTESIAN_POINT('Ctrl Pts',(-120.072723422189,-0.44212961073246,
125.90410222797));
#103752=CARTESIAN_POINT('Ctrl Pts',(-120.080469698273,-0.578391951996569,
125.920238811922));
#103753=CARTESIAN_POINT('Ctrl Pts',(-120.088216031538,-0.714655299118141,
125.936375514991));
#103754=CARTESIAN_POINT('Ctrl Pts',(-120.095962364804,-0.850242024812184,
125.958218903167));
#103755=CARTESIAN_POINT('Ctrl Pts',(-120.103708698069,-0.984643345796628,
125.985682319103));
#103756=CARTESIAN_POINT('Ctrl Pts',(-120.111456766072,-1.11907476502522,
126.013151885281));
#103757=CARTESIAN_POINT('Ctrl Pts',(-120.119204834075,-1.25231986832657,
126.046243905363));
#103758=CARTESIAN_POINT('Ctrl Pts',(-120.126952902078,-1.38388146108346,
126.084820898041));
#103759=CARTESIAN_POINT('Ctrl Pts',(-120.13470920482,-1.5155828790669,126.123438890807));
#103760=CARTESIAN_POINT('Ctrl Pts',(-120.142465507562,-1.6455968365088,
126.167553391028));
#103761=CARTESIAN_POINT('Ctrl Pts',(-120.150221810304,-1.77344214382034,
126.216977264823));
#103762=CARTESIAN_POINT('Ctrl Pts',(-120.157982252818,-1.90135568602173,
126.266427517628));
#103763=CARTESIAN_POINT('Ctrl Pts',(-120.165742695332,-2.02709791345964,
126.3211926345));
#103764=CARTESIAN_POINT('Ctrl Pts',(-120.173503137846,-2.15020986517425,
126.381038269126));
#103765=CARTESIAN_POINT('Ctrl Pts',(-120.181276038112,-2.27351944712311,
126.440979973278));
#103766=CARTESIAN_POINT('Ctrl Pts',(-120.189048938377,-2.39418997138583,
126.506018307266));
#103767=CARTESIAN_POINT('Ctrl Pts',(-120.196821838643,-2.51178844647387,
126.575873670364));
#103768=CARTESIAN_POINT('Ctrl Pts',(-120.204312174405,-2.62511192078391,
126.64318961506));
#103769=CARTESIAN_POINT('Ctrl Pts',(-120.211802510167,-2.73558256335194,
126.714978279117));
#103770=CARTESIAN_POINT('Ctrl Pts',(-120.219292845929,-2.842841710528,126.790953826399));
#103771=CARTESIAN_POINT('Ctrl Pts',(-120.22701389374,-2.95340457842834,
126.869269518991));
#103772=CARTESIAN_POINT('Ctrl Pts',(-120.23473494155,-3.06091610256276,
126.952290169606));
#103773=CARTESIAN_POINT('Ctrl Pts',(-120.24245598936,-3.1649453704542,127.03974857055));
#103774=CARTESIAN_POINT('Ctrl Pts',(-120.250164846145,-3.2688103829921,
127.127068880446));
#103775=CARTESIAN_POINT('Ctrl Pts',(-120.257873702929,-3.36920378652162,
127.218812735198));
#103776=CARTESIAN_POINT('Ctrl Pts',(-120.265582559714,-3.46572382234608,
127.314669879159));
#103777=CARTESIAN_POINT('Ctrl Pts',(-120.273284374497,-3.5621556876001,
127.410439458098));
#103778=CARTESIAN_POINT('Ctrl Pts',(-120.280986189279,-3.65472094208111,
127.510314576008));
#103779=CARTESIAN_POINT('Ctrl Pts',(-120.288688004062,-3.74305094511466,
127.613944863346));
#103780=CARTESIAN_POINT('Ctrl Pts',(-120.296384511242,-3.831320076708,127.717503735257));
#103781=CARTESIAN_POINT('Ctrl Pts',(-120.304081018422,-3.91535950621426,
127.824812327972));
#103782=CARTESIAN_POINT('Ctrl Pts',(-120.311777525602,-3.99483786329218,
127.935483919535));
#103783=CARTESIAN_POINT('Ctrl Pts',(-120.319470455286,-4.07427927717795,
128.046104068641));
#103784=CARTESIAN_POINT('Ctrl Pts',(-120.327163384969,-4.14916360644363,
128.160083784069));
#103785=CARTESIAN_POINT('Ctrl Pts',(-120.334856314653,-4.21920046350886,
128.277004190145));
#103786=CARTESIAN_POINT('Ctrl Pts',(-120.342548792745,-4.28923320925824,
128.393917732739));
#103787=CARTESIAN_POINT('Ctrl Pts',(-120.350241270836,-4.35441883727088,
128.513771286775));
#103788=CARTESIAN_POINT('Ctrl Pts',(-120.357933748928,-4.41451103866694,
128.636118160647));
#103789=CARTESIAN_POINT('Ctrl Pts',(-120.365625921623,-4.47460085435652,
128.758460177254));
#103790=CARTESIAN_POINT('Ctrl Pts',(-120.373318094317,-4.5295974759841,
128.883294957802));
#103791=CARTESIAN_POINT('Ctrl Pts',(-120.381010267012,-4.57930155123303,
129.010153169868));
#103792=CARTESIAN_POINT('Ctrl Pts',(-120.388706168035,-4.62902971760968,
129.137072868992));
#103793=CARTESIAN_POINT('Ctrl Pts',(-120.396402069058,-4.67346007517859,
129.266017586356));
#103794=CARTESIAN_POINT('Ctrl Pts',(-120.404097970081,-4.71244223394075,
129.396500093838));
#103795=CARTESIAN_POINT('Ctrl Pts',(-120.407735336252,-4.73086663741748,
129.458170930981));
#103796=CARTESIAN_POINT('Ctrl Pts',(-120.411372702423,-4.748074716149,129.520185074516));
#103797=CARTESIAN_POINT('Ctrl Pts',(-120.415010068595,-4.76405452823409,
129.582490119308));
#103798=CARTESIAN_POINT('Ctrl Pts',(-118.665245282749,-4.764054528234,129.582490119308));
#103799=CARTESIAN_POINT('Ctrl Pts',(-118.672980934985,-4.79810898405142,
129.715267925692));
#103800=CARTESIAN_POINT('Ctrl Pts',(-118.680716587222,-4.82661864926354,
129.849510832222));
#103801=CARTESIAN_POINT('Ctrl Pts',(-118.688452239458,-4.84947065823497,
129.984715940027));
#103802=CARTESIAN_POINT('Ctrl Pts',(-118.696233626883,-4.87245777422998,
130.120720415613));
#103803=CARTESIAN_POINT('Ctrl Pts',(-118.704015014309,-4.88972001690422,
130.257698118956));
#103804=CARTESIAN_POINT('Ctrl Pts',(-118.711796401734,-4.9011949353849,
130.395128082377));
#103805=CARTESIAN_POINT('Ctrl Pts',(-118.719577789159,-4.91266985386559,
130.532558045797));
#103806=CARTESIAN_POINT('Ctrl Pts',(-118.727359176585,-4.91835742778128,
130.670439866815));
#103807=CARTESIAN_POINT('Ctrl Pts',(-118.73514056401,-4.91824846256287,
130.808249447467));
#103808=CARTESIAN_POINT('',(-118.389859435938,-4.91824882054746,130.800954493157));
#103809=CARTESIAN_POINT('Ctrl Pts',(-118.320090776197,-4.76405452823413,
129.582490119309));
#103810=CARTESIAN_POINT('Ctrl Pts',(-118.328971454939,-4.8028555469181,
129.73377470227));
#103811=CARTESIAN_POINT('Ctrl Pts',(-118.337852133682,-4.83449000944879,
129.887079065182));
#103812=CARTESIAN_POINT('Ctrl Pts',(-118.346732812425,-4.85876789631629,
130.041761383219));
#103813=CARTESIAN_POINT('Ctrl Pts',(-118.355552800387,-4.88287986749901,
130.195386598435));
#103814=CARTESIAN_POINT('Ctrl Pts',(-118.36437278835,-4.89973538446453,
130.350370840933));
#103815=CARTESIAN_POINT('Ctrl Pts',(-118.373192776313,-4.90919580011069,
130.506066033848));
#103816=CARTESIAN_POINT('Ctrl Pts',(-118.378748329521,-4.91515474730177,
130.604135660721));
#103817=CARTESIAN_POINT('Ctrl Pts',(-118.38430388273,-4.91818062704774,
130.702486980166));
#103818=CARTESIAN_POINT('Ctrl Pts',(-118.389859435938,-4.91824882054746,
130.800954493156));
#103819=CARTESIAN_POINT('Ctrl Pts',(-118.389859435993,-4.91824882054814,
130.800954494129));
#103820=CARTESIAN_POINT('Ctrl Pts',(-118.3976384828,-4.91834430703793,130.938831563033));
#103821=CARTESIAN_POINT('Ctrl Pts',(-118.405417529606,-4.91263765077987,
131.076749423057));
#103822=CARTESIAN_POINT('Ctrl Pts',(-118.413196576413,-4.90114527712532,
131.214187452964));
#103823=CARTESIAN_POINT('Ctrl Pts',(-118.420975537861,-4.8896530295752,
131.351623974779));
#103824=CARTESIAN_POINT('Ctrl Pts',(-118.428754499309,-4.87237522228776,
131.488580292133));
#103825=CARTESIAN_POINT('Ctrl Pts',(-118.436533460757,-4.84938025557986,
131.62453998776));
#103826=CARTESIAN_POINT('Ctrl Pts',(-118.444313967514,-4.82638072086928,
131.760526692091));
#103827=CARTESIAN_POINT('Ctrl Pts',(-118.452094474271,-4.79766182998921,
131.895515999847));
#103828=CARTESIAN_POINT('Ctrl Pts',(-118.459874981027,-4.7633432302008,
132.029001109221));
#103829=CARTESIAN_POINT('Ctrl Pts',(-118.467658664403,-4.72901061884117,
132.162540717791));
#103830=CARTESIAN_POINT('Ctrl Pts',(-118.475442347779,-4.68907384333215,
132.294574531751));
#103831=CARTESIAN_POINT('Ctrl Pts',(-118.483226031155,-4.6437024928228,
132.424610666371));
#103832=CARTESIAN_POINT('Ctrl Pts',(-118.491019424938,-4.59827454002439,
132.554809025451));
#103833=CARTESIAN_POINT('Ctrl Pts',(-118.498812818721,-4.54739859933736,
132.683004363148));
#103834=CARTESIAN_POINT('Ctrl Pts',(-118.506606212504,-4.49129276080419,
132.808723957694));
#103835=CARTESIAN_POINT('Ctrl Pts',(-118.514404928122,-4.43514860956972,
132.934529401723));
#103836=CARTESIAN_POINT('Ctrl Pts',(-118.522203643739,-4.37376761644027,
133.057855389245));
#103837=CARTESIAN_POINT('Ctrl Pts',(-118.530002359356,-4.30741353561459,
133.178254401143));
#103838=CARTESIAN_POINT('Ctrl Pts',(-118.537813725445,-4.24095182035202,
133.298848714967));
#103839=CARTESIAN_POINT('Ctrl Pts',(-118.545625091533,-4.1695011036118,
133.416506239816));
#103840=CARTESIAN_POINT('Ctrl Pts',(-118.553436457621,-4.09336851931609,
133.530808348144));
#103841=CARTESIAN_POINT('Ctrl Pts',(-118.558356338151,-4.04541746761306,
133.602799944868));
#103842=CARTESIAN_POINT('Ctrl Pts',(-118.563276218681,-3.99560997945149,
133.673461107767));
#103843=CARTESIAN_POINT('Ctrl Pts',(-118.568196099211,-3.94403066670205,
133.742694356714));
#103844=CARTESIAN_POINT('Ctrl Pts',(-118.57597043333,-3.86252567719863,
133.852095876973));
#103845=CARTESIAN_POINT('Ctrl Pts',(-118.583744767449,-3.77633618777062,
133.958276871339));
#103846=CARTESIAN_POINT('Ctrl Pts',(-118.591519101568,-3.68574563895189,
134.060809933531));
#103847=CARTESIAN_POINT('Ctrl Pts',(-118.599283854515,-3.59526673488852,
134.163216632887));
#103848=CARTESIAN_POINT('Ctrl Pts',(-118.607048607462,-3.50039781978248,
134.261984055095));
#103849=CARTESIAN_POINT('Ctrl Pts',(-118.614813360409,-3.40146476703581,
134.35671483711));
#103850=CARTESIAN_POINT('Ctrl Pts',(-118.622570401294,-3.30262997599211,
134.451351531177));
#103851=CARTESIAN_POINT('Ctrl Pts',(-118.630327442179,-3.19973936080105,
134.541959294994));
#103852=CARTESIAN_POINT('Ctrl Pts',(-118.638084483064,-3.09315786136248,
134.628175140682));
#103853=CARTESIAN_POINT('Ctrl Pts',(-118.645835674304,-2.98665673586157,
134.71432597033));
#103854=CARTESIAN_POINT('Ctrl Pts',(-118.653586865544,-2.87647056888741,
134.796091229255));
#103855=CARTESIAN_POINT('Ctrl Pts',(-118.661338056784,-2.76299955415722,
134.873146250433));
#103856=CARTESIAN_POINT('Ctrl Pts',(-118.669085953561,-2.64957676763507,
134.950168521172));
#103857=CARTESIAN_POINT('Ctrl Pts',(-118.676833850338,-2.53287223295046,
135.022484316764));
#103858=CARTESIAN_POINT('Ctrl Pts',(-118.684581747116,-2.41331730101888,
135.08981073011));
#103859=CARTESIAN_POINT('Ctrl Pts',(-118.6923280232,-2.29378737740143,135.157123060222));
#103860=CARTESIAN_POINT('Ctrl Pts',(-118.700074299284,-2.17140858294072,
135.219447892289));
#103861=CARTESIAN_POINT('Ctrl Pts',(-118.707820575368,-2.0466388426059,
135.276547164484));
#103862=CARTESIAN_POINT('Ctrl Pts',(-118.715566908633,-1.92186818124938,
135.333646858173));
#103863=CARTESIAN_POINT('Ctrl Pts',(-118.723313241899,-1.79470689430702,
135.385520752327));
#103864=CARTESIAN_POINT('Ctrl Pts',(-118.731059575164,-1.66563458912202,
135.431978198786));
#103865=CARTESIAN_POINT('Ctrl Pts',(-118.738807643167,-1.53653337908936,
135.478446049069));
#103866=CARTESIAN_POINT('Ctrl Pts',(-118.74655571117,-1.40552066701626,
135.519494905595));
#103867=CARTESIAN_POINT('Ctrl Pts',(-118.754303779173,-1.27309260043101,
135.554983554953));
#103868=CARTESIAN_POINT('Ctrl Pts',(-118.762060081915,-1.14052378772014,
135.59050992207));
#103869=CARTESIAN_POINT('Ctrl Pts',(-118.769816384657,-1.00653699382671,
135.620464175886));
#103870=CARTESIAN_POINT('Ctrl Pts',(-118.777572687398,-0.871640525306763,
135.644755834606));
#103871=CARTESIAN_POINT('Ctrl Pts',(-118.785333129913,-0.736672058479913,
135.669060458516));
#103872=CARTESIAN_POINT('Ctrl Pts',(-118.793093572427,-0.600793336735016,
135.687696412048));
#103873=CARTESIAN_POINT('Ctrl Pts',(-118.800854014941,-0.464518241034863,
135.700625098397));
#103874=CARTESIAN_POINT('Ctrl Pts',(-118.808626915206,-0.328024384453529,
135.71357453902));
#103875=CARTESIAN_POINT('Ctrl Pts',(-118.816399815472,-0.191133273044126,
135.720798383625));
#103876=CARTESIAN_POINT('Ctrl Pts',(-118.824172715737,-0.0543601487628199,
135.722310194039));
#103877=CARTESIAN_POINT('Ctrl Pts',(-118.831663051499,0.0774409279438527,
135.723767046336));
#103878=CARTESIAN_POINT('Ctrl Pts',(-118.839153387262,0.209132138962692,
135.719919956989));
#103879=CARTESIAN_POINT('Ctrl Pts',(-118.846643723024,0.34025847903006,
135.710826477016));
#103880=CARTESIAN_POINT('Ctrl Pts',(-118.854418057143,0.476356514132803,
135.701388214986));
#103881=CARTESIAN_POINT('Ctrl Pts',(-118.862192391262,0.612277116226453,
135.686267977587));
#103882=CARTESIAN_POINT('Ctrl Pts',(-118.869966725381,0.7475074897697,135.665473207832));
#103883=CARTESIAN_POINT('Ctrl Pts',(-118.877731478328,0.882571203962706,
135.644704065772));
#103884=CARTESIAN_POINT('Ctrl Pts',(-118.885496231275,1.01694599942176,
135.618274364898));
#103885=CARTESIAN_POINT('Ctrl Pts',(-118.893260984222,1.15012142083002,
135.586243487299));
#103886=CARTESIAN_POINT('Ctrl Pts',(-118.901018025107,1.28316457053266,
135.55424442322));
#103887=CARTESIAN_POINT('Ctrl Pts',(-118.908775065992,1.41501033913111,
135.516655344206));
#103888=CARTESIAN_POINT('Ctrl Pts',(-118.916532106877,1.5451560757129,135.473587080717));
#103889=CARTESIAN_POINT('Ctrl Pts',(-118.924283298117,1.67520366838288,
135.43055129534));
#103890=CARTESIAN_POINT('Ctrl Pts',(-118.932034489357,1.80355341112631,
135.382044672106));
#103891=CARTESIAN_POINT('Ctrl Pts',(-118.939785680598,1.92971583790101,
135.328228414867));
#103892=CARTESIAN_POINT('Ctrl Pts',(-118.947533577375,2.05582464227867,
135.274435030973));
#103893=CARTESIAN_POINT('Ctrl Pts',(-118.955281474152,2.17974762086387,
135.215336654626));
#103894=CARTESIAN_POINT('Ctrl Pts',(-118.963029370929,2.30101360019626,
135.151143275373));
#103895=CARTESIAN_POINT('Ctrl Pts',(-118.970775647013,2.42225421329996,
135.086963323991));
#103896=CARTESIAN_POINT('Ctrl Pts',(-118.978521923097,2.5408385873228,135.017690672364));
#103897=CARTESIAN_POINT('Ctrl Pts',(-118.986268199181,2.65631891447749,
134.943581907506));
#103898=CARTESIAN_POINT('Ctrl Pts',(-118.994014532446,2.77180009408156,
134.869472595594));
#103899=CARTESIAN_POINT('Ctrl Pts',(-119.001760865712,2.88417685205744,
134.790527310374));
#103900=CARTESIAN_POINT('Ctrl Pts',(-119.009507198977,2.99302955122568,
134.707046509101));
#103901=CARTESIAN_POINT('Ctrl Pts',(-119.01725526698,3.10190662720103,134.623547012882));
#103902=CARTESIAN_POINT('Ctrl Pts',(-119.025003334983,3.2072577637991,134.535510217368));
#103903=CARTESIAN_POINT('Ctrl Pts',(-119.032751402986,3.30869597431968,
134.443277216228));
#103904=CARTESIAN_POINT('Ctrl Pts',(-119.040507705728,3.41024199457768,
134.350946188757));
#103905=CARTESIAN_POINT('Ctrl Pts',(-119.04826400847,3.50786649156947,134.254410310212));
#103906=CARTESIAN_POINT('Ctrl Pts',(-119.056020311212,3.60121858829027,
134.154048325674));
#103907=CARTESIAN_POINT('Ctrl Pts',(-119.063780753726,3.69462050983586,
134.053632774924));
#103908=CARTESIAN_POINT('Ctrl Pts',(-119.07154119624,3.78374523346562,133.949387346127));
#103909=CARTESIAN_POINT('Ctrl Pts',(-119.079301638754,3.86828252137975,
133.841723519375));
#103910=CARTESIAN_POINT('Ctrl Pts',(-119.08707453902,3.95295551605331,133.733886861091));
#103911=CARTESIAN_POINT('Ctrl Pts',(-119.094847439285,4.03302613057707,
133.622621156565));
#103912=CARTESIAN_POINT('Ctrl Pts',(-119.10262033955,4.10822727403774,133.508367223947));
#103913=CARTESIAN_POINT('Ctrl Pts',(-119.110110675312,4.18069466651276,
133.398266709569));
#103914=CARTESIAN_POINT('Ctrl Pts',(-119.117601011074,4.24864031758024,
133.285391718292));
#103915=CARTESIAN_POINT('Ctrl Pts',(-119.125091346836,4.31186670508116,
133.17015616666));
#103916=CARTESIAN_POINT('Ctrl Pts',(-119.132865680955,4.37749034028207,
133.050551424062));
#103917=CARTESIAN_POINT('Ctrl Pts',(-119.140640015075,4.43823766180747,
132.928024714402));
#103918=CARTESIAN_POINT('Ctrl Pts',(-119.148414349194,4.49383775315963,
132.803011490224));
#103919=CARTESIAN_POINT('Ctrl Pts',(-119.156179102141,4.54936932236817,
132.678152333672));
#103920=CARTESIAN_POINT('Ctrl Pts',(-119.163943855088,4.59976612572708,
132.550813113657));
#103921=CARTESIAN_POINT('Ctrl Pts',(-119.171708608035,4.64480220950378,
132.421455388162));
#103922=CARTESIAN_POINT('Ctrl Pts',(-119.17946564892,4.68979356280718,132.292226142584));
#103923=CARTESIAN_POINT('Ctrl Pts',(-119.187222689805,4.72943466449426,
132.160982748025));
#103924=CARTESIAN_POINT('Ctrl Pts',(-119.19497973069,4.76354706427261,132.028208005503));
#103925=CARTESIAN_POINT('Ctrl Pts',(-119.20273092193,4.79763373962507,131.895533389447));
#103926=CARTESIAN_POINT('Ctrl Pts',(-119.21048211317,4.82619991478906,131.761330101125));
#103927=CARTESIAN_POINT('Ctrl Pts',(-119.21823330441,4.84911664677847,131.626097076801));
#103928=CARTESIAN_POINT('Ctrl Pts',(-119.225981201188,4.87202363854537,
131.49092153012));
#103929=CARTESIAN_POINT('Ctrl Pts',(-119.233729097965,4.88928589768466,
131.354717502583));
#103930=CARTESIAN_POINT('Ctrl Pts',(-119.241476994742,4.90082541358308,
131.217994910243));
#103931=CARTESIAN_POINT('Ctrl Pts',(-119.249223270826,4.91236251566357,
131.081300917321));
#103932=CARTESIAN_POINT('Ctrl Pts',(-119.25696954691,4.91817922268991,130.944088964689));
#103933=CARTESIAN_POINT('Ctrl Pts',(-119.264715822994,4.91824935753657,
130.806874497268));
#103934=CARTESIAN_POINT('Ctrl Pts',(-119.27246215626,4.91831949290093,130.669659016961));
#103935=CARTESIAN_POINT('Ctrl Pts',(-119.280208489525,4.91264297123998,
130.532441412794));
#103936=CARTESIAN_POINT('Ctrl Pts',(-119.28795482279,4.90124575160549,130.395737141895));
#103937=CARTESIAN_POINT('Ctrl Pts',(-119.295702890793,4.8898459796427,130.259002257023));
#103938=CARTESIAN_POINT('Ctrl Pts',(-119.303450958796,4.87272299292091,
130.12278132371));
#103939=CARTESIAN_POINT('Ctrl Pts',(-119.311199026799,4.84995458744018,
129.987584294288));
#103940=CARTESIAN_POINT('Ctrl Pts',(-119.318955329541,4.82716198342713,
129.852243575853));
#103941=CARTESIAN_POINT('Ctrl Pts',(-119.326711632283,4.79871204000369,
129.717929321291));
#103942=CARTESIAN_POINT('Ctrl Pts',(-119.334467935025,4.76473374854247,
129.585141454331));
#103943=CARTESIAN_POINT('Ctrl Pts',(-119.342228377539,4.73073732184402,
129.452282714488));
#103944=CARTESIAN_POINT('Ctrl Pts',(-119.349988820053,4.69120678032778,
129.320952359754));
#103945=CARTESIAN_POINT('Ctrl Pts',(-119.357749262568,4.64632062273903,
129.191633817017));
#103946=CARTESIAN_POINT('Ctrl Pts',(-119.365522162833,4.60136240990531,
129.062107680674));
#103947=CARTESIAN_POINT('Ctrl Pts',(-119.373295063098,4.55103154446283,
128.934600173846));
#103948=CARTESIAN_POINT('Ctrl Pts',(-119.381067963364,4.49555453004237,
128.809574280658));
#103949=CARTESIAN_POINT('Ctrl Pts',(-119.388558299126,4.44209424483472,
128.689093393609));
#103950=CARTESIAN_POINT('Ctrl Pts',(-119.396048634888,4.38385560195401,
128.570917103135));
#103951=CARTESIAN_POINT('Ctrl Pts',(-119.40353897065,4.32108007556043,128.455435322225));
#103952=CARTESIAN_POINT('Ctrl Pts',(-119.411313304769,4.25592439600279,
128.33557501449));
#103953=CARTESIAN_POINT('Ctrl Pts',(-119.419087638888,4.18567461614985,
128.218237892985));
#103954=CARTESIAN_POINT('Ctrl Pts',(-119.426861973007,4.11055065757387,
128.103887260168));
#103955=CARTESIAN_POINT('Ctrl Pts',(-119.434626725954,4.03551928256342,
127.989677554287));
#103956=CARTESIAN_POINT('Ctrl Pts',(-119.442391478901,3.95562589355626,
127.878447337458));
#103957=CARTESIAN_POINT('Ctrl Pts',(-119.450156231848,3.87113667884586,
127.770636194321));
#103958=CARTESIAN_POINT('Ctrl Pts',(-119.457913272733,3.7867313800146,127.662932130731));
#103959=CARTESIAN_POINT('Ctrl Pts',(-119.465670313618,3.69773957891601,
127.558640688631));
#103960=CARTESIAN_POINT('Ctrl Pts',(-119.473427354503,3.60447101297868,
127.458172969048));
#103961=CARTESIAN_POINT('Ctrl Pts',(-119.481178545743,3.51127278159232,
127.357781012953));
#103962=CARTESIAN_POINT('Ctrl Pts',(-119.488929736983,3.4138044697374,127.261207325317));
#103963=CARTESIAN_POINT('Ctrl Pts',(-119.496680928223,3.31241614978891,
127.168830076762));
#103964=CARTESIAN_POINT('Ctrl Pts',(-119.504428825,3.21107092258088,127.076492091002));
#103965=CARTESIAN_POINT('Ctrl Pts',(-119.512176721777,3.10580928943434,
126.988347259643));
#103966=CARTESIAN_POINT('Ctrl Pts',(-119.519924618554,2.99701809052568,
126.904736837307));
#103967=CARTESIAN_POINT('Ctrl Pts',(-119.527670894638,2.88824964839057,
126.821143904469));
#103968=CARTESIAN_POINT('Ctrl Pts',(-119.535417170723,2.77595341882597,
126.742083732124));
#103969=CARTESIAN_POINT('Ctrl Pts',(-119.543163446807,2.66054891086765,
126.667856954401));
#103970=CARTESIAN_POINT('Ctrl Pts',(-119.550909780072,2.5451435510193,126.593629628752));
#103971=CARTESIAN_POINT('Ctrl Pts',(-119.558656113337,2.42663019581498,
126.524235980414));
#103972=CARTESIAN_POINT('Ctrl Pts',(-119.566402446603,2.30545654543727,
126.45993278647));
#103973=CARTESIAN_POINT('Ctrl Pts',(-119.574150514605,2.18425575906088,
126.395615192272));
#103974=CARTESIAN_POINT('Ctrl Pts',(-119.581898582608,2.06039383731272,
126.336390504112));
#103975=CARTESIAN_POINT('Ctrl Pts',(-119.589646650611,1.93434186816958,
126.282468911704));
#103976=CARTESIAN_POINT('Ctrl Pts',(-119.597402953353,1.80815592949342,
126.228490010785));
#103977=CARTESIAN_POINT('Ctrl Pts',(-119.605159256095,1.67977565380446,
126.179825618532));
#103978=CARTESIAN_POINT('Ctrl Pts',(-119.612915558837,1.54969136408282,
126.136637431838));
#103979=CARTESIAN_POINT('Ctrl Pts',(-119.620676001351,1.41953764445899,
126.093426194307));
#103980=CARTESIAN_POINT('Ctrl Pts',(-119.628436443865,1.28767847427642,
126.055697093792));
#103981=CARTESIAN_POINT('Ctrl Pts',(-119.636196886379,1.1546170571987,126.023561258282));
#103982=CARTESIAN_POINT('Ctrl Pts',(-119.643969786645,1.02134203812164,
125.991373835477));
#103983=CARTESIAN_POINT('Ctrl Pts',(-119.65174268691,0.886861299255647,
125.964797696033));
#103984=CARTESIAN_POINT('Ctrl Pts',(-119.659515587175,0.751686793004185,
125.94389253026));
#103985=CARTESIAN_POINT('Ctrl Pts',(-119.667005922938,0.621426220534238,
125.923747319919));
#103986=CARTESIAN_POINT('Ctrl Pts',(-119.6744962587,0.490521751391431,125.90886796796));
#103987=CARTESIAN_POINT('Ctrl Pts',(-119.681986594462,0.359431953098699,
125.899262072828));
#103988=CARTESIAN_POINT('Ctrl Pts',(-119.689760928581,0.223371845264233,
125.889291967263));
#103989=CARTESIAN_POINT('Ctrl Pts',(-119.6975352627,0.0866810798254277,
125.884971516338));
#103990=CARTESIAN_POINT('Ctrl Pts',(-119.70530959682,-0.0501316807566252,
125.886366120102));
#103991=CARTESIAN_POINT('Ctrl Pts',(-119.713074349767,-0.186775831837826,
125.887759005142));
#103992=CARTESIAN_POINT('Ctrl Pts',(-119.720839102714,-0.323541291722485,
125.894852926867));
#103993=CARTESIAN_POINT('Ctrl Pts',(-119.728603855661,-0.45991434412875,
125.907661539762));
#103994=CARTESIAN_POINT('Ctrl Pts',(-119.736360896546,-0.596151948897583,
125.920457430963));
#103995=CARTESIAN_POINT('Ctrl Pts',(-119.744117937431,-0.731997535064224,
125.938956681691));
#103996=CARTESIAN_POINT('Ctrl Pts',(-119.751874978316,-0.866937811044434,
125.963120911222));
#103997=CARTESIAN_POINT('Ctrl Pts',(-119.759626169556,-1.00177632751303,
125.98726691832));
#103998=CARTESIAN_POINT('Ctrl Pts',(-119.767377360796,-1.13571050938475,
126.017069332419));
#103999=CARTESIAN_POINT('Ctrl Pts',(-119.775128552036,-1.26823296833418,
126.052438038175));
#104000=CARTESIAN_POINT('Ctrl Pts',(-119.782876448813,-1.40069910170322,
126.087791711287));
#104001=CARTESIAN_POINT('Ctrl Pts',(-119.79062434559,-1.53175432859126,
126.128706870011));
#104002=CARTESIAN_POINT('Ctrl Pts',(-119.798372242368,-1.66090244525615,
126.175042511209));
#104003=CARTESIAN_POINT('Ctrl Pts',(-119.806118518452,-1.79002354691951,
126.22136845999));
#104004=CARTESIAN_POINT('Ctrl Pts',(-119.813864794536,-1.91723796408203,
126.273112504014));
#104005=CARTESIAN_POINT('Ctrl Pts',(-119.82161107062,-2.04206600985632,
126.330084198536));
#104006=CARTESIAN_POINT('Ctrl Pts',(-119.829357403885,-2.16689497708273,
126.38705631361));
#104007=CARTESIAN_POINT('Ctrl Pts',(-119.837103737151,-2.28933718209762,
126.449255993856));
#104008=CARTESIAN_POINT('Ctrl Pts',(-119.844850070416,-2.40893459818407,
126.516445370716));
#104009=CARTESIAN_POINT('Ctrl Pts',(-119.852598138419,-2.52855879728214,
126.58364979417));
#104010=CARTESIAN_POINT('Ctrl Pts',(-119.860346206422,-2.64533659896179,
126.655845946296));
#104011=CARTESIAN_POINT('Ctrl Pts',(-119.868094274425,-2.75883653010626,
126.732751100108));
#104012=CARTESIAN_POINT('Ctrl Pts',(-119.875850577167,-2.87245709032837,
126.809737989634));
#104013=CARTESIAN_POINT('Ctrl Pts',(-119.883606879909,-2.98279249665029,
126.891443658783));
#104014=CARTESIAN_POINT('Ctrl Pts',(-119.891363182651,-3.08944167734946,
126.977542986066));
#104015=CARTESIAN_POINT('Ctrl Pts',(-119.899123625165,-3.19614777992781,
127.063688267153));
#104016=CARTESIAN_POINT('Ctrl Pts',(-119.906884067679,-3.29916344305824,
127.154231621061));
#104017=CARTESIAN_POINT('Ctrl Pts',(-119.914644510193,-3.39812317774284,
127.24880975569));
#104018=CARTESIAN_POINT('Ctrl Pts',(-119.922417410459,-3.49724177137852,
127.343539715537));
#104019=CARTESIAN_POINT('Ctrl Pts',(-119.930190310724,-3.5922911544,127.44231711731));
#104020=CARTESIAN_POINT('Ctrl Pts',(-119.93796321099,-3.68294438487962,
127.544743505023));
#104021=CARTESIAN_POINT('Ctrl Pts',(-119.945453546751,-3.77030214208787,
127.643446435544));
#104022=CARTESIAN_POINT('Ctrl Pts',(-119.952943882513,-3.85357762538255,
127.745537419654));
#104023=CARTESIAN_POINT('Ctrl Pts',(-119.960434218275,-3.9325165750294,
127.850634758652));
#104024=CARTESIAN_POINT('Ctrl Pts',(-119.96824087687,-4.01478917926819,
127.960170441817));
#104025=CARTESIAN_POINT('Ctrl Pts',(-119.976047535465,-4.09261365977126,
128.073321594936));
#104026=CARTESIAN_POINT('Ctrl Pts',(-119.983854194061,-4.16565686347,128.189693151458));
#104027=CARTESIAN_POINT('Ctrl Pts',(-119.991647965675,-4.23857948980098,
128.305872605562));
#104028=CARTESIAN_POINT('Ctrl Pts',(-119.99944173729,-4.30673635587862,
128.42526155029));
#104029=CARTESIAN_POINT('Ctrl Pts',(-120.007235508904,-4.36983533622441,
128.547433016427));
#104030=CARTESIAN_POINT('Ctrl Pts',(-120.015021864543,-4.43287427625572,
128.669488233248));
#104031=CARTESIAN_POINT('Ctrl Pts',(-120.022808220182,-4.49086472713496,
128.794320364123));
#104032=CARTESIAN_POINT('Ctrl Pts',(-120.030594575821,-4.54355834120615,
128.921474359037));
#104033=CARTESIAN_POINT('Ctrl Pts',(-120.038373959203,-4.59620477101535,
129.048514494473));
#104034=CARTESIAN_POINT('Ctrl Pts',(-120.046153342584,-4.64356366066462,
129.17787199853));
#104035=CARTESIAN_POINT('Ctrl Pts',(-120.053932725966,-4.68543328799281,
129.309068684107));
#104036=CARTESIAN_POINT('Ctrl Pts',(-120.059288485631,-4.71425866530427,
129.399391770436));
#104037=CARTESIAN_POINT('Ctrl Pts',(-120.064644245295,-4.74048325069915,
129.490586065944));
#104038=CARTESIAN_POINT('Ctrl Pts',(-120.07000000496,-4.76405452823399,
129.582490119308));
#104039=CARTESIAN_POINT('Origin',(213.235140564004,0.,130.804360617566));
#104040=CARTESIAN_POINT('',(-122.165194063467,-4.76405452823402,129.582490119308));
#104041=CARTESIAN_POINT('',(-121.81971904495,-4.76405452823411,129.582490119308));
#104042=CARTESIAN_POINT('',(213.235140564004,-4.76405452823405,129.582490119308));
#104043=CARTESIAN_POINT('',(-120.485140563958,-4.91824981073044,130.805725077145));
#104044=CARTESIAN_POINT('Ctrl Pts',(-120.48514056401,-4.91824981073019,
130.805725078055));
#104045=CARTESIAN_POINT('Ctrl Pts',(-120.489340532587,-4.91822935689092,
130.879451720875));
#104046=CARTESIAN_POINT('Ctrl Pts',(-120.493540501165,-4.91655120048444,
130.953153330112));
#104047=CARTESIAN_POINT('Ctrl Pts',(-120.497740469743,-4.91321818380445,
131.026779458569));
#104048=CARTESIAN_POINT('Ctrl Pts',(-120.505514803862,-4.90704861733907,
131.163064793063));
#104049=CARTESIAN_POINT('Ctrl Pts',(-120.513289137981,-4.89519445387011,
131.299309097387));
#104050=CARTESIAN_POINT('Ctrl Pts',(-120.5210634721,-4.87765082858863,131.434999545058));
#104051=CARTESIAN_POINT('Ctrl Pts',(-120.528828225047,-4.86012882425739,
131.57052276638));
#104052=CARTESIAN_POINT('Ctrl Pts',(-120.536592977994,-4.83693135906257,
131.705493105164));
#104053=CARTESIAN_POINT('Ctrl Pts',(-120.544357730941,-4.80810554847421,
131.839398828084));
#104054=CARTESIAN_POINT('Ctrl Pts',(-120.552114771826,-4.77930836808731,
131.973171553952));
#104055=CARTESIAN_POINT('Ctrl Pts',(-120.559871812711,-4.74489404870721,
132.105881388477));
#104056=CARTESIAN_POINT('Ctrl Pts',(-120.567628853596,-4.70496132664014,
132.237023165873));
#104057=CARTESIAN_POINT('Ctrl Pts',(-120.575380044836,-4.66505871814947,
132.368066048234));
#104058=CARTESIAN_POINT('Ctrl Pts',(-120.583131236076,-4.61964610355175,
132.497542854631));
#104059=CARTESIAN_POINT('Ctrl Pts',(-120.590882427316,-4.5688728944401,
132.624960391528));
#104060=CARTESIAN_POINT('Ctrl Pts',(-120.598630324094,-4.51812126529666,
132.752323772573));
#104061=CARTESIAN_POINT('Ctrl Pts',(-120.606378220871,-4.46201371761603,
132.877629262481));
#104062=CARTESIAN_POINT('Ctrl Pts',(-120.614126117648,-4.40074887360715,
133.000400784308));
#104063=CARTESIAN_POINT('Ctrl Pts',(-120.621872393732,-4.33949684488292,
133.123146624979));
#104064=CARTESIAN_POINT('Ctrl Pts',(-120.629618669816,-4.27308984007193,
133.243359202265));
#104065=CARTESIAN_POINT('Ctrl Pts',(-120.6373649459,-4.20177362614531,133.360584679954));
#104066=CARTESIAN_POINT('Ctrl Pts',(-120.645111279165,-4.1304568857785,
133.477811022975));
#104067=CARTESIAN_POINT('Ctrl Pts',(-120.65285761243,-4.05423106718569,
133.592049888389));
#104068=CARTESIAN_POINT('Ctrl Pts',(-120.660603945695,-3.97338647096173,
133.702874549718));
#104069=CARTESIAN_POINT('Ctrl Pts',(-120.668352013698,-3.89252377015109,
133.813724029461));
#104070=CARTESIAN_POINT('Ctrl Pts',(-120.676100081701,-3.80704046385279,
133.921157467882));
#104071=CARTESIAN_POINT('Ctrl Pts',(-120.683848149704,-3.71726826089569,
134.024779804417));
#104072=CARTESIAN_POINT('Ctrl Pts',(-120.691604452446,-3.62740064697311,
134.128512272004));
#104073=CARTESIAN_POINT('Ctrl Pts',(-120.699360755188,-3.53323528712383,
134.228425250459));
#104074=CARTESIAN_POINT('Ctrl Pts',(-120.70711705793,-3.43514239728022,
134.324158874982));
#104075=CARTESIAN_POINT('Ctrl Pts',(-120.714877500444,-3.33699715230778,
134.419943595423));
#104076=CARTESIAN_POINT('Ctrl Pts',(-120.722637942958,-3.23492049124312,
134.511544256189));
#104077=CARTESIAN_POINT('Ctrl Pts',(-120.730398385472,-3.12931633082908,
134.598640834433));
#104078=CARTESIAN_POINT('Ctrl Pts',(-120.738171285737,-3.02354264524165,
134.685877227836));
#104079=CARTESIAN_POINT('Ctrl Pts',(-120.745944186003,-2.91423045646014,
134.768594854116));
#104080=CARTESIAN_POINT('Ctrl Pts',(-120.753717086268,-2.80181404624344,
134.846516120855));
#104081=CARTESIAN_POINT('Ctrl Pts',(-120.76120742203,-2.69348425569646,
134.921604753278));
#104082=CARTESIAN_POINT('Ctrl Pts',(-120.768697757792,-2.58227227790492,
134.992239526238));
#104083=CARTESIAN_POINT('Ctrl Pts',(-120.776188093554,-2.46858717022877,
135.058213041603));
#104084=CARTESIAN_POINT('Ctrl Pts',(-120.783962427673,-2.35059165714305,
135.126687962853));
#104085=CARTESIAN_POINT('Ctrl Pts',(-120.791736761792,-2.22955800036758,
135.190358093839));
#104086=CARTESIAN_POINT('Ctrl Pts',(-120.799511095911,-2.1059150257965,
135.248942146419));
#104087=CARTESIAN_POINT('Ctrl Pts',(-120.807275848858,-1.98242443014161,
135.30745399939));
#104088=CARTESIAN_POINT('Ctrl Pts',(-120.815040601805,-1.85633126499734,
135.360892079882));
#104089=CARTESIAN_POINT('Ctrl Pts',(-120.822805354752,-1.72809153316525,
135.409019423113));
#104090=CARTESIAN_POINT('Ctrl Pts',(-120.830562395637,-1.59997917084234,
135.457098965588));
#104091=CARTESIAN_POINT('Ctrl Pts',(-120.838319436522,-1.46972484827676,
135.499878131209));
#104092=CARTESIAN_POINT('Ctrl Pts',(-120.846076477407,-1.33780694513731,
135.53716693518));
#104093=CARTESIAN_POINT('Ctrl Pts',(-120.853827668647,-1.20598852231497,
135.574427619373));
#104094=CARTESIAN_POINT('Ctrl Pts',(-120.861578859888,-1.07250939066434,
135.606206077065));
#104095=CARTESIAN_POINT('Ctrl Pts',(-120.869330051128,-0.937865248490862,
135.632361429307));
#104096=CARTESIAN_POINT('Ctrl Pts',(-120.877077947905,-0.803278333669372,
135.658505664827));
#104097=CARTESIAN_POINT('Ctrl Pts',(-120.884825844682,-0.667527776149154,
135.679031473968));
#104098=CARTESIAN_POINT('Ctrl Pts',(-120.892573741459,-0.531121473102041,
135.693848632002));
#104099=CARTESIAN_POINT('Ctrl Pts',(-120.900320017543,-0.394743703313317,
135.708662690605));
#104100=CARTESIAN_POINT('Ctrl Pts',(-120.908066293627,-0.257710849264619,
135.717770431093));
#104101=CARTESIAN_POINT('Ctrl Pts',(-120.915812569711,-0.120537579264298,
135.721133314619));
#104102=CARTESIAN_POINT('Ctrl Pts',(-120.923558902976,0.0166367033181279,
135.724496222969));
#104103=CARTESIAN_POINT('Ctrl Pts',(-120.931305236242,0.153951013072703,
135.722114180156));
#104104=CARTESIAN_POINT('Ctrl Pts',(-120.939051569507,0.290889418363816,
135.714000768207));
#104105=CARTESIAN_POINT('Ctrl Pts',(-120.94679963751,0.427858490061144,
135.705885539315));
#104106=CARTESIAN_POINT('Ctrl Pts',(-120.954547705513,0.564451099578084,
135.692036410388));
#104107=CARTESIAN_POINT('Ctrl Pts',(-120.962295773516,0.700155574548042,
135.672518917573));
#104108=CARTESIAN_POINT('Ctrl Pts',(-120.970052076257,0.836004277849088,
135.652980681335));
#104109=CARTESIAN_POINT('Ctrl Pts',(-120.977808378999,0.970962573421003,
135.627762102557));
#104110=CARTESIAN_POINT('Ctrl Pts',(-120.985564681741,1.10452758606241,
135.596980138676));
#104111=CARTESIAN_POINT('Ctrl Pts',(-120.993325124255,1.23816388637263,
135.566181745534));
#104112=CARTESIAN_POINT('Ctrl Pts',(-121.001085566769,1.37040504520718,
135.529814154234));
#104113=CARTESIAN_POINT('Ctrl Pts',(-121.008846009284,1.50076349141599,
135.488044211206));
#104114=CARTESIAN_POINT('Ctrl Pts',(-121.016618909549,1.63133120057534,
135.446207215357));
#104115=CARTESIAN_POINT('Ctrl Pts',(-121.024391809814,1.76000979038505,
135.398950672549));
#104116=CARTESIAN_POINT('Ctrl Pts',(-121.03216471008,1.88633097458358,135.346489910841));
#104117=CARTESIAN_POINT('Ctrl Pts',(-121.039655045842,2.00806006555982,
135.295936229959));
#104118=CARTESIAN_POINT('Ctrl Pts',(-121.047145381605,2.12759989103735,
135.240550263489));
#104119=CARTESIAN_POINT('Ctrl Pts',(-121.054635717367,2.24455485559791,
135.180564059216));
#104120=CARTESIAN_POINT('Ctrl Pts',(-121.062410051486,2.3659442031808,135.118303459779));
#104121=CARTESIAN_POINT('Ctrl Pts',(-121.070184385605,2.48493333551021,
135.05088967751));
#104122=CARTESIAN_POINT('Ctrl Pts',(-121.077958719724,2.60105380603633,
134.978531452667));
#104123=CARTESIAN_POINT('Ctrl Pts',(-121.085723472671,2.71703116846052,
134.906262402868));
#104124=CARTESIAN_POINT('Ctrl Pts',(-121.093488225619,2.83014657478166,
134.829061239692));
#104125=CARTESIAN_POINT('Ctrl Pts',(-121.101252978566,2.93995417916434,
134.747183525955));
#104126=CARTESIAN_POINT('Ctrl Pts',(-121.109010019451,3.04965272108634,
134.665387134317));
#104127=CARTESIAN_POINT('Ctrl Pts',(-121.116767060336,3.15604968767794,
134.578923667706));
#104128=CARTESIAN_POINT('Ctrl Pts',(-121.124524101221,3.25872666345328,
134.48809290906));
#104129=CARTESIAN_POINT('Ctrl Pts',(-121.132275292461,3.36132620972233,
134.397330646597));
#104130=CARTESIAN_POINT('Ctrl Pts',(-121.140026483701,3.46021105725778,
134.302207905428));
#104131=CARTESIAN_POINT('Ctrl Pts',(-121.147777674941,3.55499474356835,
134.203065582064));
#104132=CARTESIAN_POINT('Ctrl Pts',(-121.155525571718,3.64973814428392,
134.103965396831));
#104133=CARTESIAN_POINT('Ctrl Pts',(-121.163273468495,3.74038358106666,
134.000849309345));
#104134=CARTESIAN_POINT('Ctrl Pts',(-121.171021365272,3.8265806144706,133.89409585921));
#104135=CARTESIAN_POINT('Ctrl Pts',(-121.178767641356,3.91275961731335,
133.787364739596));
#104136=CARTESIAN_POINT('Ctrl Pts',(-121.18651391744,3.99449182215695,133.676998074714));
#104137=CARTESIAN_POINT('Ctrl Pts',(-121.194260193524,4.07146661438827,
133.563408038402));
#104138=CARTESIAN_POINT('Ctrl Pts',(-121.20200652679,4.14844197483012,133.449817163594));
#104139=CARTESIAN_POINT('Ctrl Pts',(-121.209752860055,4.22065963325971,
133.333003193528));
#104140=CARTESIAN_POINT('Ctrl Pts',(-121.21749919332,4.28785214296914,133.213407537519));
#104141=CARTESIAN_POINT('Ctrl Pts',(-121.225247261323,4.35505969997514,
133.093785098892));
#104142=CARTESIAN_POINT('Ctrl Pts',(-121.232995329326,4.41723967748522,
132.971380075532));
#104143=CARTESIAN_POINT('Ctrl Pts',(-121.240743397329,4.47417064150337,
132.846658375781));
#104144=CARTESIAN_POINT('Ctrl Pts',(-121.248499700071,4.53116211242765,
132.721804120323));
#104145=CARTESIAN_POINT('Ctrl Pts',(-121.256256002813,4.58289326317113,
132.594628626213));
#104146=CARTESIAN_POINT('Ctrl Pts',(-121.264012305555,4.62919067700666,
132.46561819495));
#104147=CARTESIAN_POINT('Ctrl Pts',(-121.271772748069,4.67551280116594,
132.336538906935));
#104148=CARTESIAN_POINT('Ctrl Pts',(-121.279533190583,4.71639529314128,
132.205623103317));
#104149=CARTESIAN_POINT('Ctrl Pts',(-121.287293633098,4.75171498144312,
132.073371176084));
#104150=CARTESIAN_POINT('Ctrl Pts',(-121.295066533363,4.78709136804415,
131.940906946316));
#104151=CARTESIAN_POINT('Ctrl Pts',(-121.302839433628,4.81688702114547,
131.807102688647));
#104152=CARTESIAN_POINT('Ctrl Pts',(-121.310612333894,4.84102998218019,
131.67246877565));
#104153=CARTESIAN_POINT('Ctrl Pts',(-121.318102669656,4.86429528576891,
131.542729144513));
#104154=CARTESIAN_POINT('Ctrl Pts',(-121.325593005418,4.88231169915768,
131.412219436047));
#104155=CARTESIAN_POINT('Ctrl Pts',(-121.33308334118,4.89506062173344,131.281397903378));
#104156=CARTESIAN_POINT('Ctrl Pts',(-121.340857675299,4.90829292358355,
131.145616232536));
#104157=CARTESIAN_POINT('Ctrl Pts',(-121.348632009418,4.91589233179786,
131.00906850957));
#104158=CARTESIAN_POINT('Ctrl Pts',(-121.356406343537,4.91778125866527,
130.872261681038));
#104159=CARTESIAN_POINT('Ctrl Pts',(-121.364171096484,4.91966785759914,
130.735623454695));
#104160=CARTESIAN_POINT('Ctrl Pts',(-121.371935849431,4.91585797268189,
130.598727145322));
#104161=CARTESIAN_POINT('Ctrl Pts',(-121.379700602379,4.90632562558624,
130.462085993593));
#104162=CARTESIAN_POINT('Ctrl Pts',(-121.387457643264,4.8968027461521,130.325580555782));
#104163=CARTESIAN_POINT('Ctrl Pts',(-121.395214684149,4.88156874225225,
130.189330158779));
#104164=CARTESIAN_POINT('Ctrl Pts',(-121.402971725034,4.86064966597449,
130.053848867383));
#104165=CARTESIAN_POINT('Ctrl Pts',(-121.410722916274,4.83974636493486,
129.918469743484));
#104166=CARTESIAN_POINT('Ctrl Pts',(-121.418474107514,4.81316658426278,
129.783858955584));
#104167=CARTESIAN_POINT('Ctrl Pts',(-121.426225298754,4.78098823743087,
129.650525908412));
#104168=CARTESIAN_POINT('Ctrl Pts',(-121.433973195531,4.7488235672547,129.517249531343));
#104169=CARTESIAN_POINT('Ctrl Pts',(-121.441721092308,4.71106515517172,
129.385250194128));
#104170=CARTESIAN_POINT('Ctrl Pts',(-121.449468989085,4.66784205619279,
129.255027341302));
#104171=CARTESIAN_POINT('Ctrl Pts',(-121.457215265169,4.6246279985545,129.124831728291));
#104172=CARTESIAN_POINT('Ctrl Pts',(-121.464961541253,4.57595165078101,
128.996412231355));
#104173=CARTESIAN_POINT('Ctrl Pts',(-121.472707817338,4.52199189160953,
128.870252969394));
#104174=CARTESIAN_POINT('Ctrl Pts',(-121.480454150603,4.46803173411928,
128.744092776154));
#104175=CARTESIAN_POINT('Ctrl Pts',(-121.488200483868,4.408788241155,128.620193210646));
#104176=CARTESIAN_POINT('Ctrl Pts',(-121.495946817134,4.34448822139555,
128.499017875878));
#104177=CARTESIAN_POINT('Ctrl Pts',(-121.503694885137,4.28017380209259,
128.377815404733));
#104178=CARTESIAN_POINT('Ctrl Pts',(-121.51144295314,4.21080078592403,128.259338723591));
#104179=CARTESIAN_POINT('Ctrl Pts',(-121.519191021143,4.13664146428917,
128.144025965981));
#104180=CARTESIAN_POINT('Ctrl Pts',(-121.526947323884,4.06240332524467,
128.0285906526));
#104181=CARTESIAN_POINT('Ctrl Pts',(-121.534703626626,3.98336893083296,
127.916326309377));
#104182=CARTESIAN_POINT('Ctrl Pts',(-121.542459929368,3.89985368430151,
127.807641694554));
#104183=CARTESIAN_POINT('Ctrl Pts',(-121.550220371882,3.81629386316838,
127.698899071479));
#104184=CARTESIAN_POINT('Ctrl Pts',(-121.557980814396,3.72824867537933,
127.593740283476));
#104185=CARTESIAN_POINT('Ctrl Pts',(-121.565741256911,3.63607253768694,
127.4925394323));
#104186=CARTESIAN_POINT('Ctrl Pts',(-121.573514157176,3.54374843067531,
127.391176124533));
#104187=CARTESIAN_POINT('Ctrl Pts',(-121.581287057442,3.44728039746618,
127.293783728102));
#104188=CARTESIAN_POINT('Ctrl Pts',(-121.589059957707,3.34705893359493,
127.200698652628));
#104189=CARTESIAN_POINT('Ctrl Pts',(-121.596550293469,3.2504807723783,127.110997454115));
#104190=CARTESIAN_POINT('Ctrl Pts',(-121.604040629231,3.15041756993152,
127.025296049977));
#104191=CARTESIAN_POINT('Ctrl Pts',(-121.611530964993,3.0472448135014,126.943857786446));
#104192=CARTESIAN_POINT('Ctrl Pts',(-121.619305299112,2.9401602306518,126.859331766399));
#104193=CARTESIAN_POINT('Ctrl Pts',(-121.627079633231,2.8293864298532,126.779130789415));
#104194=CARTESIAN_POINT('Ctrl Pts',(-121.63485396735,2.71530798154935,126.703594149229));
#104195=CARTESIAN_POINT('Ctrl Pts',(-121.642618720297,2.60137012473755,
126.628150601202));
#104196=CARTESIAN_POINT('Ctrl Pts',(-121.650383473245,2.48413604669699,
126.55736016619));
#104197=CARTESIAN_POINT('Ctrl Pts',(-121.658148226192,2.36402350942219,
126.491522119616));
#104198=CARTESIAN_POINT('Ctrl Pts',(-121.665905267077,2.2440302696127,126.425749464318));
#104199=CARTESIAN_POINT('Ctrl Pts',(-121.673662307962,2.12116460058219,
126.364919595567));
#104200=CARTESIAN_POINT('Ctrl Pts',(-121.681419348847,1.99587308139619,
126.309288459585));
#104201=CARTESIAN_POINT('Ctrl Pts',(-121.689170540087,1.87067604551961,
126.253699275475));
#104202=CARTESIAN_POINT('Ctrl Pts',(-121.696921731327,1.74305715658251,
126.203301178822));
#104203=CARTESIAN_POINT('Ctrl Pts',(-121.704672922567,1.61348710534638,
126.158303964513));
#104204=CARTESIAN_POINT('Ctrl Pts',(-121.712420819345,1.48397212483824,
126.11332587522));
#104205=CARTESIAN_POINT('Ctrl Pts',(-121.720168716122,1.35250799999222,
126.073744230652));
#104206=CARTESIAN_POINT('Ctrl Pts',(-121.727916612899,1.21958468502567,
126.039720415142));
#104207=CARTESIAN_POINT('Ctrl Pts',(-121.735662888983,1.08668917475112,
126.005703716682));
#104208=CARTESIAN_POINT('Ctrl Pts',(-121.743409165067,0.952335459991848,
125.977242631735));
#104209=CARTESIAN_POINT('Ctrl Pts',(-121.751155441151,0.817027532014618,
125.954448342645));
#104210=CARTESIAN_POINT('Ctrl Pts',(-121.758901774417,0.681718605225186,
125.931653885292));
#104211=CARTESIAN_POINT('Ctrl Pts',(-121.766648107682,0.545455836695285,
125.914526372214));
#104212=CARTESIAN_POINT('Ctrl Pts',(-121.774394440947,0.408751864394905,
125.903125571595));
#104213=CARTESIAN_POINT('Ctrl Pts',(-121.78214250895,0.272017278187582,
125.891722217845));
#104214=CARTESIAN_POINT('Ctrl Pts',(-121.789890576953,0.134841681138283,
125.886048160983));
#104215=CARTESIAN_POINT('Ctrl Pts',(-121.797638644956,-0.00225913245219713,
125.886111136417));
#104216=CARTESIAN_POINT('Ctrl Pts',(-121.805394947698,-0.139505658418695,
125.886174178783));
#104217=CARTESIAN_POINT('Ctrl Pts',(-121.81315125044,-0.276676850566443,
125.891986433451));
#104218=CARTESIAN_POINT('Ctrl Pts',(-121.820907553182,-0.413258325849479,
125.903503486551));
#104219=CARTESIAN_POINT('Ctrl Pts',(-121.828667995696,-0.549912698778263,
125.91502668665));
#104220=CARTESIAN_POINT('Ctrl Pts',(-121.83642843821,-0.685976340000499,
125.932260703145));
#104221=CARTESIAN_POINT('Ctrl Pts',(-121.844188880725,-0.820942936202866,
125.955109566321));
#104222=CARTESIAN_POINT('Ctrl Pts',(-121.85196178099,-0.956126192767228,
125.977995108521));
#104223=CARTESIAN_POINT('Ctrl Pts',(-121.859734681256,-1.09020850249341,
126.006513427764));
#104224=CARTESIAN_POINT('Ctrl Pts',(-121.867507581521,-1.22269576206403,
126.040517826716));
#104225=CARTESIAN_POINT('Ctrl Pts',(-121.874997917283,-1.35036677602753,
126.073286080113));
#104226=CARTESIAN_POINT('Ctrl Pts',(-121.882488253044,-1.47655639961478,
126.111148383958));
#104227=CARTESIAN_POINT('Ctrl Pts',(-121.889978588806,-1.60084011215543,
126.153931175266));
#104228=CARTESIAN_POINT('Ctrl Pts',(-121.897752983536,-1.72983708512919,
126.198336435306));
#104229=CARTESIAN_POINT('Ctrl Pts',(-121.905527378266,-1.85718936363839,
126.248183415226));
#104230=CARTESIAN_POINT('Ctrl Pts',(-121.913301772997,-1.98240360904195,
126.303331958097));
#104231=CARTESIAN_POINT('Ctrl Pts',(-121.921066572345,-2.10746331142232,
126.358412435051));
#104232=CARTESIAN_POINT('Ctrl Pts',(-121.928831371694,-2.23038987682462,
126.418781299487));
#104233=CARTESIAN_POINT('Ctrl Pts',(-121.936596171042,-2.35070569741676,
126.484248838152));
#104234=CARTESIAN_POINT('Ctrl Pts',(-121.944353244179,-2.47090180010097,
126.549651234621));
#104235=CARTESIAN_POINT('Ctrl Pts',(-121.952110317315,-2.58849198649592,
126.620142023403));
#104236=CARTESIAN_POINT('Ctrl Pts',(-121.959867390452,-2.7030195295595,
126.695483826359));
#104237=CARTESIAN_POINT('Ctrl Pts',(-121.967618599839,-2.81746049862763,
126.770768676719));
#104238=CARTESIAN_POINT('Ctrl Pts',(-121.975369809226,-2.92884310721815,
126.850897028237));
#104239=CARTESIAN_POINT('Ctrl Pts',(-121.983121018613,-3.03673642659321,
126.935586271872));
#104240=CARTESIAN_POINT('Ctrl Pts',(-121.990868860044,-3.14458286555112,
127.020238717426));
#104241=CARTESIAN_POINT('Ctrl Pts',(-121.998616701476,-3.24894272423925,
127.10944787217));
#104242=CARTESIAN_POINT('Ctrl Pts',(-122.006364542907,-3.34941540234577,
127.202888762195));
#104243=CARTESIAN_POINT('Ctrl Pts',(-122.014110743557,-3.44986680307331,
127.296309863982));
#104244=CARTESIAN_POINT('Ctrl Pts',(-122.021856944206,-3.546432374632,127.393960652319));
#104245=CARTESIAN_POINT('Ctrl Pts',(-122.029603144855,-3.63874616757133,
127.495477212173));
#104246=CARTESIAN_POINT('Ctrl Pts',(-122.037349382583,-3.73106040238364,
127.59699425795));
#104247=CARTESIAN_POINT('Ctrl Pts',(-122.045095620311,-3.81912255501641,
127.702376822868));
#104248=CARTESIAN_POINT('Ctrl Pts',(-122.052841858038,-3.90260525945919,
127.811225931097));
#104249=CARTESIAN_POINT('Ctrl Pts',(-122.060589810369,-3.98610644251257,
127.920099132704));
#104250=CARTESIAN_POINT('Ctrl Pts',(-122.0683377627,-4.0650259226125,128.032440094219));
#104251=CARTESIAN_POINT('Ctrl Pts',(-122.076085715031,-4.13907840437813,
128.147819064172));
#104252=CARTESIAN_POINT('Ctrl Pts',(-122.083841620825,-4.21320690282966,
128.263316473462));
#104253=CARTESIAN_POINT('Ctrl Pts',(-122.091597526618,-4.28245821230543,
128.381857790778));
#104254=CARTESIAN_POINT('Ctrl Pts',(-122.099353432412,-4.34659169747729,
128.502986315563));
#104255=CARTESIAN_POINT('Ctrl Pts',(-122.107113469675,-4.41075934571951,
128.624179363931));
#104256=CARTESIAN_POINT('Ctrl Pts',(-122.114873506939,-4.46980356933109,
128.747962013255));
#104257=CARTESIAN_POINT('Ctrl Pts',(-122.122633544202,-4.52353146089156,
128.873856490447));
#104258=CARTESIAN_POINT('Ctrl Pts',(-122.130405374641,-4.57734100443896,
128.999942293483));
#104259=CARTESIAN_POINT('Ctrl Pts',(-122.13817720508,-4.62581793532609,
129.128145971041));
#104260=CARTESIAN_POINT('Ctrl Pts',(-122.145949035519,-4.66881864859992,
129.257972733177));
#104261=CARTESIAN_POINT('Ctrl Pts',(-122.152364044835,-4.70431221455001,
129.36513408919));
#104262=CARTESIAN_POINT('Ctrl Pts',(-122.158779054151,-4.73607565219564,
129.473400906273));
#104263=CARTESIAN_POINT('Ctrl Pts',(-122.165194063467,-4.76405452823402,
129.582490119308));
#104264=CARTESIAN_POINT('Ctrl Pts',(-120.415010068595,-4.76405452823409,
129.582490119308));
#104265=CARTESIAN_POINT('Ctrl Pts',(-120.422714657118,-4.79790261253537,
129.714463286283));
#104266=CARTESIAN_POINT('Ctrl Pts',(-120.430419245642,-4.82623649557487,
129.847741980942));
#104267=CARTESIAN_POINT('Ctrl Pts',(-120.438123834165,-4.8489807157756,
129.981822423598));
#104268=CARTESIAN_POINT('Ctrl Pts',(-120.445959955797,-4.87211322640586,
130.118191894069));
#104269=CARTESIAN_POINT('Ctrl Pts',(-120.453796077429,-4.88946342946171,
130.255390308165));
#104270=CARTESIAN_POINT('Ctrl Pts',(-120.461632199062,-4.90100710441625,
130.392884707018));
#104271=CARTESIAN_POINT('Ctrl Pts',(-120.469468320694,-4.91255077937079,
130.530379105871));
#104272=CARTESIAN_POINT('Ctrl Pts',(-120.477304442326,-4.918287972603,130.66816906213));
#104273=CARTESIAN_POINT('Ctrl Pts',(-120.485140563958,-4.91824981073044,
130.805725077146));
#104274=CARTESIAN_POINT('',(-120.139859436048,-4.91824877114872,130.807837339308));
#104275=CARTESIAN_POINT('Ctrl Pts',(-120.07000000496,-4.76405452823399,
129.582490119308));
#104276=CARTESIAN_POINT('Ctrl Pts',(-120.077773079977,-4.79826467207663,
129.715874950939));
#104277=CARTESIAN_POINT('Ctrl Pts',(-120.085546154993,-4.82688359845568,
129.850755253548));
#104278=CARTESIAN_POINT('Ctrl Pts',(-120.09331923001,-4.84979292098213,
129.986624910817));
#104279=CARTESIAN_POINT('Ctrl Pts',(-120.101092419275,-4.87270258022868,
130.122496565093));
#104280=CARTESIAN_POINT('Ctrl Pts',(-120.10886560854,-4.88990239253311,
130.25935722365));
#104281=CARTESIAN_POINT('Ctrl Pts',(-120.116638797805,-4.90132518231807,
130.396690996825));
#104282=CARTESIAN_POINT('Ctrl Pts',(-120.124379010535,-4.91269951270971,
130.533442153017));
#104283=CARTESIAN_POINT('Ctrl Pts',(-120.132119223264,-4.91834574066988,
130.670662035112));
#104284=CARTESIAN_POINT('Ctrl Pts',(-120.139859435993,-4.91824877114942,
130.807837338329));
#104285=CARTESIAN_POINT('Ctrl Pts',(-120.139859436048,-4.91824877114872,
130.807837339307));
#104286=CARTESIAN_POINT('Ctrl Pts',(-120.148714778364,-4.91813783123406,
130.964775437756));
#104287=CARTESIAN_POINT('Ctrl Pts',(-120.15757012068,-4.91051123559427,
131.121414678335));
#104288=CARTESIAN_POINT('Ctrl Pts',(-120.166425462996,-4.89547851881717,
131.277090069049));
#104289=CARTESIAN_POINT('Ctrl Pts',(-120.175322363441,-4.8803752534876,
131.433496044503));
#104290=CARTESIAN_POINT('Ctrl Pts',(-120.184219263886,-4.8577963009599,
131.58892895109));
#104291=CARTESIAN_POINT('Ctrl Pts',(-120.193116164331,-4.82790228850742,
131.742732907824));
#104292=CARTESIAN_POINT('Ctrl Pts',(-120.20206730258,-4.79782603443221,
131.897474493213));
#104293=CARTESIAN_POINT('Ctrl Pts',(-120.211018440828,-4.7603453501292,
132.050567057875));
#104294=CARTESIAN_POINT('Ctrl Pts',(-120.219969579077,-4.71567234460993,
132.201363624285));
#104295=CARTESIAN_POINT('Ctrl Pts',(-120.226273666747,-4.6842101399758,
132.307566293556));
#104296=CARTESIAN_POINT('Ctrl Pts',(-120.232577754417,-4.64918150738479,
132.412630567728));
#104297=CARTESIAN_POINT('Ctrl Pts',(-120.238881842088,-4.61067448482932,
132.516337211286));
#104298=CARTESIAN_POINT('Ctrl Pts',(-120.246656176207,-4.56318681096764,
132.644230435423));
#104299=CARTESIAN_POINT('Ctrl Pts',(-120.254430510326,-4.51029853671385,
132.770348880144));
#104300=CARTESIAN_POINT('Ctrl Pts',(-120.262204844445,-4.45216161365228,
132.894202723664));
#104301=CARTESIAN_POINT('Ctrl Pts',(-120.269969597392,-4.39409633915254,
133.017903928391));
#104302=CARTESIAN_POINT('Ctrl Pts',(-120.277734350339,-4.33079545074578,
133.139345734496));
#104303=CARTESIAN_POINT('Ctrl Pts',(-120.285499103286,-4.26246006419136,
133.258055232565));
#104304=CARTESIAN_POINT('Ctrl Pts',(-120.293256144171,-4.19419254930622,
133.376646826686));
#104305=CARTESIAN_POINT('Ctrl Pts',(-120.301013185056,-4.12090068095356,
133.492511176647));
#104306=CARTESIAN_POINT('Ctrl Pts',(-120.308770225941,-4.0428327252676,
133.605197388605));
#104307=CARTESIAN_POINT('Ctrl Pts',(-120.316521417181,-3.9648236412342,
133.717798623015));
#104308=CARTESIAN_POINT('Ctrl Pts',(-120.324272608422,-3.88204586054762,
133.82722616975));
#104309=CARTESIAN_POINT('Ctrl Pts',(-120.332023799662,-3.79479224907234,
133.933056008441));
#104310=CARTESIAN_POINT('Ctrl Pts',(-120.339771696439,-3.70757572270962,
134.038840866627));
#104311=CARTESIAN_POINT('Ctrl Pts',(-120.347519593216,-3.61588739737021,
134.14103075705));
#104312=CARTESIAN_POINT('Ctrl Pts',(-120.355267489993,-3.52006177317402,
134.239232984269));
#104313=CARTESIAN_POINT('Ctrl Pts',(-120.363013766077,-3.42425619363265,
134.337414669699));
#104314=CARTESIAN_POINT('Ctrl Pts',(-120.370760042161,-3.32431530950407,
134.43161007142));
#104315=CARTESIAN_POINT('Ctrl Pts',(-120.378506318245,-3.22061172338323,
134.521462067581));
#104316=CARTESIAN_POINT('Ctrl Pts',(-120.386252651511,-3.11690737174593,
134.61131472701));
#104317=CARTESIAN_POINT('Ctrl Pts',(-120.393998984776,-3.00944055817514,
134.696823660885));
#104318=CARTESIAN_POINT('Ctrl Pts',(-120.401745318041,-2.89861801462052,
134.777671160151));
#104319=CARTESIAN_POINT('Ctrl Pts',(-120.409493386044,-2.78777065312581,
134.858536764653));
#104320=CARTESIAN_POINT('Ctrl Pts',(-120.417241454047,-2.67356638205318,
134.934738626938));
#104321=CARTESIAN_POINT('Ctrl Pts',(-120.42498952205,-2.55644169540641,
135.006001835053));
#104322=CARTESIAN_POINT('Ctrl Pts',(-120.432745824792,-2.43919252724871,
135.077340782554));
#104323=CARTESIAN_POINT('Ctrl Pts',(-120.440502127534,-2.31901707776987,
135.143730387177));
#104324=CARTESIAN_POINT('Ctrl Pts',(-120.448258430276,-2.19637776265242,
135.20494100954));
#104325=CARTESIAN_POINT('Ctrl Pts',(-120.45601887279,-2.07367299123988,
135.266184301855));
#104326=CARTESIAN_POINT('Ctrl Pts',(-120.463779315304,-1.94850209050223,
135.322242944326));
#104327=CARTESIAN_POINT('Ctrl Pts',(-120.471539757819,-1.82134740238802,
135.372935526913));
#104328=CARTESIAN_POINT('Ctrl Pts',(-120.479312658084,-1.69398859428018,
135.423709485734));
#104329=CARTESIAN_POINT('Ctrl Pts',(-120.487085558349,-1.56464000416947,
135.469100041473));
#104330=CARTESIAN_POINT('Ctrl Pts',(-120.494858458615,-1.4337999334238,
135.508975459762));
#104331=CARTESIAN_POINT('Ctrl Pts',(-120.502348794377,-1.30771622881598,
135.547401306157));
#104332=CARTESIAN_POINT('Ctrl Pts',(-120.509839130139,-1.18024789709782,
135.580705953943));
#104333=CARTESIAN_POINT('Ctrl Pts',(-120.517329465901,-1.05184778703333,
135.608816809));
#104334=CARTESIAN_POINT('Ctrl Pts',(-120.52510380002,-0.918579347769554,
135.637993495671));
#104335=CARTESIAN_POINT('Ctrl Pts',(-120.532878134139,-0.783884924263575,
135.661667192654));
#104336=CARTESIAN_POINT('Ctrl Pts',(-120.540652468258,-0.648258750999061,
135.679700980479));
#104337=CARTESIAN_POINT('Ctrl Pts',(-120.548417221205,-0.512799724871836,
135.697712543273));
#104338=CARTESIAN_POINT('Ctrl Pts',(-120.556181974152,-0.376411617591162,
135.710097975663));
#104339=CARTESIAN_POINT('Ctrl Pts',(-120.563946727099,-0.239601009221587,
135.716770862942));
#104340=CARTESIAN_POINT('Ctrl Pts',(-120.571703767984,-0.102926283076566,
135.723437122616));
#104341=CARTESIAN_POINT('Ctrl Pts',(-120.579460808869,0.0341697210926163,
135.724402109335));
#104342=CARTESIAN_POINT('Ctrl Pts',(-120.587217849755,0.171173459616725,
135.719630977294));
#104343=CARTESIAN_POINT('Ctrl Pts',(-120.594969040995,0.308073882555693,
135.714863443201));
#104344=CARTESIAN_POINT('Ctrl Pts',(-120.602720232235,0.444881789193491,
135.704368413847));
#104345=CARTESIAN_POINT('Ctrl Pts',(-120.610471423475,0.581082138031221,
135.688163092212));
#104346=CARTESIAN_POINT('Ctrl Pts',(-120.618219320252,0.717224598087617,
135.671964658271));
#104347=CARTESIAN_POINT('Ctrl Pts',(-120.625967217029,0.8527596265262,135.650060805315));
#104348=CARTESIAN_POINT('Ctrl Pts',(-120.633715113806,0.987176032066382,
135.62252069629));
#104349=CARTESIAN_POINT('Ctrl Pts',(-120.64146138989,1.12156432059221,135.594986348063));
#104350=CARTESIAN_POINT('Ctrl Pts',(-120.649207665974,1.25483406887601,
135.561818167253));
#104351=CARTESIAN_POINT('Ctrl Pts',(-120.656953942059,1.38648341938654,
135.523136601894));
#104352=CARTESIAN_POINT('Ctrl Pts',(-120.664700275324,1.51813374170249,
135.484454750995));
#104353=CARTESIAN_POINT('Ctrl Pts',(-120.672446608589,1.64816326726858,
135.440259544551));
#104354=CARTESIAN_POINT('Ctrl Pts',(-120.680192941855,1.77608484990299,
135.390721448164));
#104355=CARTESIAN_POINT('Ctrl Pts',(-120.687941009858,1.90403507968906,
135.341172258064));
#104356=CARTESIAN_POINT('Ctrl Pts',(-120.695689077861,2.02987606268763,
135.286277938276));
#104357=CARTESIAN_POINT('Ctrl Pts',(-120.703437145864,2.15314057201565,
135.226257126943));
#104358=CARTESIAN_POINT('Ctrl Pts',(-120.711193448606,2.27653608833087,
135.166172524777));
#104359=CARTESIAN_POINT('Ctrl Pts',(-120.718949751347,2.3973493088434,135.10095071854));
#104360=CARTESIAN_POINT('Ctrl Pts',(-120.726706054089,2.51513708446478,
135.030856625946));
#104361=CARTESIAN_POINT('Ctrl Pts',(-120.734466496603,2.63298772696853,
134.960725122023));
#104362=CARTESIAN_POINT('Ctrl Pts',(-120.742226939118,2.74780937985991,
134.885716363772));
#104363=CARTESIAN_POINT('Ctrl Pts',(-120.749987381632,2.85918870013053,
134.806138102578));
#104364=CARTESIAN_POINT('Ctrl Pts',(-120.757760281897,2.97074681637384,
134.726432095293));
#104365=CARTESIAN_POINT('Ctrl Pts',(-120.765533182163,3.0788512489136,134.642142167193));
#104366=CARTESIAN_POINT('Ctrl Pts',(-120.773306082428,3.1831218218354,134.553616347688));
#104367=CARTESIAN_POINT('Ctrl Pts',(-120.78079641819,3.28360189678864,134.468308664706));
#104368=CARTESIAN_POINT('Ctrl Pts',(-120.788286753952,3.38052178708731,
134.379067922782));
#104369=CARTESIAN_POINT('Ctrl Pts',(-120.795777089714,3.47357564142344,
134.28623587751));
#104370=CARTESIAN_POINT('Ctrl Pts',(-120.803551423833,3.5701576609308,134.189884077025));
#104371=CARTESIAN_POINT('Ctrl Pts',(-120.811325757952,3.6628806386751,134.089358055266));
#104372=CARTESIAN_POINT('Ctrl Pts',(-120.819100092071,3.75136223461914,
133.984999617386));
#104373=CARTESIAN_POINT('Ctrl Pts',(-120.826864845018,3.83973478490401,
133.880769791953));
#104374=CARTESIAN_POINT('Ctrl Pts',(-120.834629597965,3.9238761033969,133.772717243323));
#104375=CARTESIAN_POINT('Ctrl Pts',(-120.842394350913,4.0034396680596,133.661221462393));
#104376=CARTESIAN_POINT('Ctrl Pts',(-120.850151391798,4.08292420906822,
133.549836420644));
#104377=CARTESIAN_POINT('Ctrl Pts',(-120.857908432682,4.15783981873404,
133.435015268469));
#104378=CARTESIAN_POINT('Ctrl Pts',(-120.865665473567,4.22787959739684,
133.317171229692));
#104379=CARTESIAN_POINT('Ctrl Pts',(-120.873416664808,4.29786655851782,
133.199416058022));
#104380=CARTESIAN_POINT('Ctrl Pts',(-120.881167856048,4.36298480834441,
133.078642871845));
#104381=CARTESIAN_POINT('Ctrl Pts',(-120.888919047288,4.42297042771961,
132.955294288793));
#104382=CARTESIAN_POINT('Ctrl Pts',(-120.896666944065,4.48293055160648,
132.831998132179));
#104383=CARTESIAN_POINT('Ctrl Pts',(-120.904414840842,4.53776221326313,
132.706129106648));
#104384=CARTESIAN_POINT('Ctrl Pts',(-120.912162737619,4.58724729006206,
132.578154676164));
#104385=CARTESIAN_POINT('Ctrl Pts',(-120.919909013703,4.63672201564956,
132.450207015173));
#104386=CARTESIAN_POINT('Ctrl Pts',(-120.927655289787,4.68085224000453,
132.320155189641));
#104387=CARTESIAN_POINT('Ctrl Pts',(-120.935401565872,4.71946803321353,
132.188486531627));
#104388=CARTESIAN_POINT('Ctrl Pts',(-120.943147899137,4.75808411147559,
132.056816901665));
#104389=CARTESIAN_POINT('Ctrl Pts',(-120.950894232402,4.79118556733727,
131.923530790568));
#104390=CARTESIAN_POINT('Ctrl Pts',(-120.958640565668,4.81865250392724,
131.789130189037));
#104391=CARTESIAN_POINT('Ctrl Pts',(-120.966388633671,4.84612559154718,
131.654699489424));
#104392=CARTESIAN_POINT('Ctrl Pts',(-120.974136701674,4.86796157076954,
131.519154185713));
#104393=CARTESIAN_POINT('Ctrl Pts',(-120.981884769677,4.88409184051216,
131.383005548368));
#104394=CARTESIAN_POINT('Ctrl Pts',(-120.989641072418,4.90023925369744,
131.246712210631));
#104395=CARTESIAN_POINT('Ctrl Pts',(-120.99739737516,4.91066879764671,131.109814647203));
#104396=CARTESIAN_POINT('Ctrl Pts',(-121.005153677902,4.91536382222885,
130.972828886459));
#104397=CARTESIAN_POINT('Ctrl Pts',(-121.012914120416,4.92006135268698,
130.83577001229));
#104398=CARTESIAN_POINT('Ctrl Pts',(-121.02067456293,4.91901826807467,130.698623237768));
#104399=CARTESIAN_POINT('Ctrl Pts',(-121.028435005445,4.91227006635546,
130.561902667216));
#104400=CARTESIAN_POINT('Ctrl Pts',(-121.03620790571,4.90551103182378,130.424962620665));
#104401=CARTESIAN_POINT('Ctrl Pts',(-121.043980805976,4.89302861448386,
130.288450534859));
#104402=CARTESIAN_POINT('Ctrl Pts',(-121.051753706241,4.87491012696753,
130.152874380958));
#104403=CARTESIAN_POINT('Ctrl Pts',(-121.059244042003,4.85745029211018,
130.022226761748));
#104404=CARTESIAN_POINT('Ctrl Pts',(-121.066734377765,4.83475709660615,
129.892448512288));
#104405=CARTESIAN_POINT('Ctrl Pts',(-121.074224713527,4.80695274901388,
129.763981681193));
#104406=CARTESIAN_POINT('Ctrl Pts',(-121.081999047646,4.77809419113173,
129.630643991151));
#104407=CARTESIAN_POINT('Ctrl Pts',(-121.089773381765,4.74363783633687,
129.498296753679));
#104408=CARTESIAN_POINT('Ctrl Pts',(-121.097547715884,4.7036645908544,129.367446396312));
#104409=CARTESIAN_POINT('Ctrl Pts',(-121.105312468831,4.66374060882447,
129.236757300315));
#104410=CARTESIAN_POINT('Ctrl Pts',(-121.113077221778,4.61831337736683,
129.107561784197));
#104411=CARTESIAN_POINT('Ctrl Pts',(-121.120841974725,4.56751486929416,
128.980356510861));
#104412=CARTESIAN_POINT('Ctrl Pts',(-121.12859901561,4.51676681501585,128.853277579595));
#104413=CARTESIAN_POINT('Ctrl Pts',(-121.136356056495,4.46065824472712,
128.72818531805));
#104414=CARTESIAN_POINT('Ctrl Pts',(-121.14411309738,4.39937092857163,128.605561287173));
#104415=CARTESIAN_POINT('Ctrl Pts',(-121.151864288621,4.33812982965792,
128.48302972803));
#104416=CARTESIAN_POINT('Ctrl Pts',(-121.159615479861,4.2717179322864,128.362963043029));
#104417=CARTESIAN_POINT('Ctrl Pts',(-121.167366671101,4.20036496845406,
128.245822520472));
#104418=CARTESIAN_POINT('Ctrl Pts',(-121.175114567878,4.12904233153485,
128.128731785761));
#104419=CARTESIAN_POINT('Ctrl Pts',(-121.182862464655,4.05278300802332,
128.014565073075));
#104420=CARTESIAN_POINT('Ctrl Pts',(-121.190610361432,3.97186238798385,
127.903758570849));
#104421=CARTESIAN_POINT('Ctrl Pts',(-121.198356637516,3.89095869479341,
127.792975246954));
#104422=CARTESIAN_POINT('Ctrl Pts',(-121.2061029136,3.80539587491923,127.685551050979));
#104423=CARTESIAN_POINT('Ctrl Pts',(-121.213849189684,3.71549208335456,
127.581892364653));
#104424=CARTESIAN_POINT('Ctrl Pts',(-121.22159552295,3.62558762814065,127.478232913143));
#104425=CARTESIAN_POINT('Ctrl Pts',(-121.229341856215,3.53134239345751,
127.378339322103));
#104426=CARTESIAN_POINT('Ctrl Pts',(-121.23708818948,3.43311391111179,127.282583802401));
#104427=CARTESIAN_POINT('Ctrl Pts',(-121.244836257483,3.33486343117865,
127.186806838915));
#104428=CARTESIAN_POINT('Ctrl Pts',(-121.252584325486,3.23262820846716,
127.095170063634));
#104429=CARTESIAN_POINT('Ctrl Pts',(-121.260332393489,3.12680130873923,
127.008007546767));
#104430=CARTESIAN_POINT('Ctrl Pts',(-121.268088696231,3.02086193492277,
126.920752392539));
#104431=CARTESIAN_POINT('Ctrl Pts',(-121.275844998973,2.91132356093146,
126.837981244893));
#104432=CARTESIAN_POINT('Ctrl Pts',(-121.283601301715,2.79861133624859,
126.759987037996));
#104433=CARTESIAN_POINT('Ctrl Pts',(-121.291361744229,2.68583895365771,
126.681951203243));
#104434=CARTESIAN_POINT('Ctrl Pts',(-121.299122186743,2.56988967534342,
126.608697598245));
#104435=CARTESIAN_POINT('Ctrl Pts',(-121.306882629257,2.4512152193469,126.5404742435));
#104436=CARTESIAN_POINT('Ctrl Pts',(-121.314655529523,2.33235025657818,
126.472141370571));
#104437=CARTESIAN_POINT('Ctrl Pts',(-121.322428429788,2.21075172109453,
126.408855064928));
#104438=CARTESIAN_POINT('Ctrl Pts',(-121.330201330053,2.08689417803081,
126.350816438802));
#104439=CARTESIAN_POINT('Ctrl Pts',(-121.337691665816,1.96753916863208,
126.294887662925));
#104440=CARTESIAN_POINT('Ctrl Pts',(-121.345182001578,1.84608682536492,
126.243831777163));
#104441=CARTESIAN_POINT('Ctrl Pts',(-121.35267233734,1.72297511295921,126.197784902067));
#104442=CARTESIAN_POINT('Ctrl Pts',(-121.360446671459,1.59519558256207,
126.149992145708));
#104443=CARTESIAN_POINT('Ctrl Pts',(-121.368221005578,1.46522360199772,
126.107444338237));
#104444=CARTESIAN_POINT('Ctrl Pts',(-121.375995339697,1.3335289748852,126.070347147408));
#104445=CARTESIAN_POINT('Ctrl Pts',(-121.383760092644,1.20199664963107,
126.033295675551));
#104446=CARTESIAN_POINT('Ctrl Pts',(-121.391524845591,1.06874627468884,
126.001681559704));
#104447=CARTESIAN_POINT('Ctrl Pts',(-121.399289598539,0.934267041154496,
125.975662225834));
#104448=CARTESIAN_POINT('Ctrl Pts',(-121.407046639424,0.799921374290355,
125.949668734734));
#104449=CARTESIAN_POINT('Ctrl Pts',(-121.414803680308,0.664349659085967,
125.929259041081));
#104450=CARTESIAN_POINT('Ctrl Pts',(-121.422560721193,0.528055297606805,
125.914540511962));
#104451=CARTESIAN_POINT('Ctrl Pts',(-121.430311912434,0.391863716766036,
125.8998330822));
#104452=CARTESIAN_POINT('Ctrl Pts',(-121.438063103674,0.254950961479189,
125.890808316306));
#104453=CARTESIAN_POINT('Ctrl Pts',(-121.445814294914,0.117829302415059,
125.887522271841));
#104454=CARTESIAN_POINT('Ctrl Pts',(-121.453562191691,-0.0192340762863155,
125.884237624032));
#104455=CARTESIAN_POINT('Ctrl Pts',(-121.461310088468,-0.156505792134369,
125.886686855795));
#104456=CARTESIAN_POINT('Ctrl Pts',(-121.469057985245,-0.293470012388454,
125.894874044173));
#104457=CARTESIAN_POINT('Ctrl Pts',(-121.476804261329,-0.430405582680269,
125.903059519967));
#104458=CARTESIAN_POINT('Ctrl Pts',(-121.484550537413,-0.567033395295687,
125.916980541686));
#104459=CARTESIAN_POINT('Ctrl Pts',(-121.492296813497,-0.702839579230788,
125.936589095774));
#104460=CARTESIAN_POINT('Ctrl Pts',(-121.500043146763,-0.838646765656474,
125.956197794608));
#104461=CARTESIAN_POINT('Ctrl Pts',(-121.507789480028,-0.973631924346888,
125.981494053717));
#104462=CARTESIAN_POINT('Ctrl Pts',(-121.515535813294,-1.10728864908134,
126.012378260533));
#104463=CARTESIAN_POINT('Ctrl Pts',(-121.523283881297,-1.24097530531204,
126.043269383653));
#104464=CARTESIAN_POINT('Ctrl Pts',(-121.531031949299,-1.37333255475409,
126.07975085658));
#104465=CARTESIAN_POINT('Ctrl Pts',(-121.538780017302,-1.50386687303437,
126.121672555065));
#104466=CARTESIAN_POINT('Ctrl Pts',(-121.546536320044,-1.63453992474168,
126.16363880843));
#104467=CARTESIAN_POINT('Ctrl Pts',(-121.554292622786,-1.76338580222295,
126.211056717657));
#104468=CARTESIAN_POINT('Ctrl Pts',(-121.562048925528,-1.88992824798591,
126.263726930517));
#104469=CARTESIAN_POINT('Ctrl Pts',(-121.569809368042,-2.0165382332623,
126.316425255056));
#104470=CARTESIAN_POINT('Ctrl Pts',(-121.577569810556,-2.14084198294527,
126.374381303935));
#104471=CARTESIAN_POINT('Ctrl Pts',(-121.58533025307,-2.2623866657282,126.437349095113));
#104472=CARTESIAN_POINT('Ctrl Pts',(-121.593103153336,-2.3841264628265,
126.50041796778));
#104473=CARTESIAN_POINT('Ctrl Pts',(-121.600876053601,-2.50309800276387,
126.568514465478));
#104474=CARTESIAN_POINT('Ctrl Pts',(-121.608648953867,-2.61887557007755,
126.641348029193));
#104475=CARTESIAN_POINT('Ctrl Pts',(-121.616139289629,-2.7304443311911,
126.711533909409));
#104476=CARTESIAN_POINT('Ctrl Pts',(-121.623629625391,-2.83904705203017,
126.786118252141));
#104477=CARTESIAN_POINT('Ctrl Pts',(-121.631119961152,-2.94433247988447,
126.864806161743));
#104478=CARTESIAN_POINT('Ctrl Pts',(-121.638978256311,-3.05479000732286,
126.947359579732));
#104479=CARTESIAN_POINT('Ctrl Pts',(-121.646836551469,-3.16196897788224,
127.034708896594));
#104480=CARTESIAN_POINT('Ctrl Pts',(-121.654694846627,-3.26542016347724,
127.126560430164));
#104481=CARTESIAN_POINT('Ctrl Pts',(-121.662380624164,-3.36660022638171,
127.216395494799));
#104482=CARTESIAN_POINT('Ctrl Pts',(-121.670066401701,-3.46421413479997,
127.310536894367));
#104483=CARTESIAN_POINT('Ctrl Pts',(-121.677752179238,-3.55787009888527,
127.408665781165));
#104484=CARTESIAN_POINT('Ctrl Pts',(-121.685430974352,-3.65144097781133,
127.506705519215));
#104485=CARTESIAN_POINT('Ctrl Pts',(-121.693109769465,-3.74106078866552,
127.608725254032));
#104486=CARTESIAN_POINT('Ctrl Pts',(-121.700788564579,-3.82637188746135,
127.714366889199));
#104487=CARTESIAN_POINT('Ctrl Pts',(-121.708462128761,-3.91162487082498,
127.819936559413));
#104488=CARTESIAN_POINT('Ctrl Pts',(-121.716135692944,-3.99257473035327,
127.929122912813));
#104489=CARTESIAN_POINT('Ctrl Pts',(-121.723809257126,-4.06890204433508,
128.041532498391));
#104490=CARTESIAN_POINT('Ctrl Pts',(-121.731801739445,-4.14840156931981,
128.158613896791));
#104491=CARTESIAN_POINT('Ctrl Pts',(-121.739794221763,-4.22288572883434,
128.279191893274));
#104492=CARTESIAN_POINT('Ctrl Pts',(-121.747786704082,-4.29204148410264,
128.402785517503));
#104493=CARTESIAN_POINT('Ctrl Pts',(-121.755456199217,-4.35840256035367,
128.521384553691));
#104494=CARTESIAN_POINT('Ctrl Pts',(-121.763125694352,-4.41985729000343,
128.642759856617));
#104495=CARTESIAN_POINT('Ctrl Pts',(-121.770795189487,-4.47617489732447,
128.766459405274));
#104496=CARTESIAN_POINT('Ctrl Pts',(-121.778464572672,-4.53249168258754,
128.890157148311));
#104497=CARTESIAN_POINT('Ctrl Pts',(-121.786133955856,-4.58367133513182,
129.016178703345));
#104498=CARTESIAN_POINT('Ctrl Pts',(-121.793803339041,-4.62953074956426,
129.144050977367));
#104499=CARTESIAN_POINT('Ctrl Pts',(-121.80147589271,-4.675409122048,129.271976113143));
#104500=CARTESIAN_POINT('Ctrl Pts',(-121.809148446379,-4.71596273961054,
129.401753116337));
#104501=CARTESIAN_POINT('Ctrl Pts',(-121.816821000049,-4.75105805935766,
129.532892812581));
#104502=CARTESIAN_POINT('Ctrl Pts',(-121.817787015016,-4.75547674518463,
129.549403991887));
#104503=CARTESIAN_POINT('Ctrl Pts',(-121.818753029983,-4.75980897126095,
129.565936757105));
#104504=CARTESIAN_POINT('Ctrl Pts',(-121.81971904495,-4.76405452823411,
129.582490119308));
#104505=CARTESIAN_POINT('Origin',(213.235140564004,0.,130.804360617566));
#104506=CARTESIAN_POINT('',(-123.915406765754,-4.76405452823402,129.582490119308));
#104507=CARTESIAN_POINT('',(-123.5698746576,-4.76405452823401,129.582490119308));
#104508=CARTESIAN_POINT('',(213.235140564004,-4.76405452823405,129.582490119308));
#104509=CARTESIAN_POINT('',(-122.235140563971,-4.91824789589999,130.799811224715));
#104510=CARTESIAN_POINT('Ctrl Pts',(-122.23514056401,-4.91824789590063,
130.799811225407));
#104511=CARTESIAN_POINT('Ctrl Pts',(-122.242800405751,-4.91837300399556,
130.935062837746));
#104512=CARTESIAN_POINT('Ctrl Pts',(-122.250460247491,-4.91291479637063,
131.070467222207));
#104513=CARTESIAN_POINT('Ctrl Pts',(-122.258120089232,-4.90186230610599,
131.205520179931));
#104514=CARTESIAN_POINT('Ctrl Pts',(-122.265984828699,-4.89051416611397,
131.344185750667));
#104515=CARTESIAN_POINT('Ctrl Pts',(-122.273849568165,-4.87326819136258,
131.482480401144));
#104516=CARTESIAN_POINT('Ctrl Pts',(-122.281714307632,-4.85016973800614,
131.619858364362));
#104517=CARTESIAN_POINT('Ctrl Pts',(-122.289366382498,-4.82769587283603,
131.753521591725));
#104518=CARTESIAN_POINT('Ctrl Pts',(-122.297018457364,-4.79968204027882,
131.886316648974));
#104519=CARTESIAN_POINT('Ctrl Pts',(-122.30467053223,-4.76622246247628,
132.017746994895));
#104520=CARTESIAN_POINT('Ctrl Pts',(-122.312321721774,-4.73276675584337,
132.149162134731));
#104521=CARTESIAN_POINT('Ctrl Pts',(-122.319972911319,-4.69386665576557,
132.279212488126));
#104522=CARTESIAN_POINT('Ctrl Pts',(-122.327624100864,-4.64966706477045,
132.40741372002));
#104523=CARTESIAN_POINT('Ctrl Pts',(-122.335276159506,-4.60546245315207,
132.535629514268));
#104524=CARTESIAN_POINT('Ctrl Pts',(-122.342928218147,-4.55595728469253,
132.661995389799));
#104525=CARTESIAN_POINT('Ctrl Pts',(-122.350580276789,-4.50134551602286,
132.786044650877));
#104526=CARTESIAN_POINT('Ctrl Pts',(-122.358604740093,-4.44407594267695,
132.916131048533));
#104527=CARTESIAN_POINT('Ctrl Pts',(-122.366629203397,-4.38119041985976,
133.043669224295));
#104528=CARTESIAN_POINT('Ctrl Pts',(-122.3746536667,-4.31296759164002,133.168148597898));
#104529=CARTESIAN_POINT('Ctrl Pts',(-122.382316960419,-4.24781537507506,
133.28702533342));
#104530=CARTESIAN_POINT('Ctrl Pts',(-122.389980254138,-4.17779608753363,
133.403112291733));
#104531=CARTESIAN_POINT('Ctrl Pts',(-122.397643547857,-4.10319706125064,
133.515994246773));
#104532=CARTESIAN_POINT('Ctrl Pts',(-122.405312002117,-4.0285477992074,
133.628952217695));
#104533=CARTESIAN_POINT('Ctrl Pts',(-122.412980456377,-3.94931289385773,
133.738700565194));
#104534=CARTESIAN_POINT('Ctrl Pts',(-122.420648910638,-3.86582016351056,
133.844856880661));
#104535=CARTESIAN_POINT('Ctrl Pts',(-122.428327883103,-3.78221291287369,
133.951158802242));
#104536=CARTESIAN_POINT('Ctrl Pts',(-122.436006855568,-3.69433644631845,
134.053858560136));
#104537=CARTESIAN_POINT('Ctrl Pts',(-122.443685828033,-3.60255570892061,
134.152610223946));
#104538=CARTESIAN_POINT('Ctrl Pts',(-122.444748497499,-3.58985445394045,
134.166276164069));
#104539=CARTESIAN_POINT('Ctrl Pts',(-122.445811166966,-3.57707848019253,
134.1798665576));
#104540=CARTESIAN_POINT('Ctrl Pts',(-122.446873836433,-3.56422880358217,
134.193380549377));
#104541=CARTESIAN_POINT('Ctrl Pts',(-122.454648170552,-3.47022245219701,
134.29224693319));
#104542=CARTESIAN_POINT('Ctrl Pts',(-122.462422504671,-3.37195047524916,
134.387355556349));
#104543=CARTESIAN_POINT('Ctrl Pts',(-122.47019683879,-3.26974540435205,
134.478315986541));
#104544=CARTESIAN_POINT('Ctrl Pts',(-122.477961591737,-3.16766629207076,
134.569164316131));
#104545=CARTESIAN_POINT('Ctrl Pts',(-122.485726344684,-3.06166401954631,
134.655874367237));
#104546=CARTESIAN_POINT('Ctrl Pts',(-122.493491097631,-2.95210965281732,
134.738090610873));
#104547=CARTESIAN_POINT('Ctrl Pts',(-122.501248138516,-2.84266409702982,
134.820225196177));
#104548=CARTESIAN_POINT('Ctrl Pts',(-122.509005179401,-2.72967377857668,
134.897874623053));
#104549=CARTESIAN_POINT('Ctrl Pts',(-122.516762220286,-2.61354443753827,
134.970722163989));
#104550=CARTESIAN_POINT('Ctrl Pts',(-122.524513411526,-2.49750267053945,
135.043514770027));
#104551=CARTESIAN_POINT('Ctrl Pts',(-122.532264602766,-2.3783269225019,
135.111512490866));
#104552=CARTESIAN_POINT('Ctrl Pts',(-122.540015794007,-2.25645335026092,
135.174440861749));
#104553=CARTESIAN_POINT('Ctrl Pts',(-122.547763690784,-2.13463157753873,
135.237342486395));
#104554=CARTESIAN_POINT('Ctrl Pts',(-122.555511587561,-2.01011460786944,
135.295178867441));
#104555=CARTESIAN_POINT('Ctrl Pts',(-122.563259484338,-1.88336453625771,
135.347720727228));
#104556=CARTESIAN_POINT('Ctrl Pts',(-122.571005760422,-1.75664097802889,
135.40025159639));
#104557=CARTESIAN_POINT('Ctrl Pts',(-122.578752036506,-1.6276856079139,
135.447489997551));
#104558=CARTESIAN_POINT('Ctrl Pts',(-122.58649831259,-1.49698153978166,
135.489254355107));
#104559=CARTESIAN_POINT('Ctrl Pts',(-122.594244645855,-1.36627650682186,
135.531019020959));
#104560=CARTESIAN_POINT('Ctrl Pts',(-122.601990979121,-1.23382312250193,
135.567309443575));
#104561=CARTESIAN_POINT('Ctrl Pts',(-122.609737312386,-1.10012035576805,
135.597993714219));
#104562=CARTESIAN_POINT('Ctrl Pts',(-122.617485380389,-0.966387647226413,
135.628684856393));
#104563=CARTESIAN_POINT('Ctrl Pts',(-122.625233448392,-0.831405380506198,
135.653767260942));
#104564=CARTESIAN_POINT('Ctrl Pts',(-122.632981516395,-0.695683032602759,
135.673160077458));
#104565=CARTESIAN_POINT('Ctrl Pts',(-122.640737819137,-0.559816437372668,
135.692573504891));
#104566=CARTESIAN_POINT('Ctrl Pts',(-122.648494121879,-0.423208577358247,
135.706285209443));
#104567=CARTESIAN_POINT('Ctrl Pts',(-122.656250424621,-0.286374932773004,
135.714266162521));
#104568=CARTESIAN_POINT('Ctrl Pts',(-122.664010867135,-0.149468255951664,
135.722251375273));
#104569=CARTESIAN_POINT('Ctrl Pts',(-122.671771309649,-0.0123359451584667,
135.724499735477));
#104570=CARTESIAN_POINT('Ctrl Pts',(-122.679531752163,0.124507191482485,
135.721034393786));
#104571=CARTESIAN_POINT('Ctrl Pts',(-122.687304652429,0.261570000874363,
135.717563489221));
#104572=CARTESIAN_POINT('Ctrl Pts',(-122.695077552694,0.398342318170785,
135.708360580163));
#104573=CARTESIAN_POINT('Ctrl Pts',(-122.70285045296,0.534314223231023,
135.693500764192));
#104574=CARTESIAN_POINT('Ctrl Pts',(-122.710340788721,0.665343207046069,
135.679181139962));
#104575=CARTESIAN_POINT('Ctrl Pts',(-122.717831124483,0.795628657692951,
135.659608799687));
#104576=CARTESIAN_POINT('Ctrl Pts',(-122.725321460245,0.924725721187771,
135.634895308785));
#104577=CARTESIAN_POINT('Ctrl Pts',(-122.733095794364,1.0587175390868,135.609244798364));
#104578=CARTESIAN_POINT('Ctrl Pts',(-122.740870128483,1.19185352133314,
135.577974334926));
#104579=CARTESIAN_POINT('Ctrl Pts',(-122.748644462602,1.32362544470394,
135.541152648533));
#104580=CARTESIAN_POINT('Ctrl Pts',(-122.756409215549,1.45523497095563,
135.504376341578));
#104581=CARTESIAN_POINT('Ctrl Pts',(-122.764173968496,1.58548341025536,
135.462062528197));
#104582=CARTESIAN_POINT('Ctrl Pts',(-122.771938721444,1.71387107574249,
135.414331224656));
#104583=CARTESIAN_POINT('Ctrl Pts',(-122.779695762329,1.8421312247903,135.366647328519));
#104584=CARTESIAN_POINT('Ctrl Pts',(-122.787452803213,1.96853391383312,
135.313556785472));
#104585=CARTESIAN_POINT('Ctrl Pts',(-122.795209844098,2.0925933586198,135.255229757179));
#104586=CARTESIAN_POINT('Ctrl Pts',(-122.802961035338,2.21655924921363,
135.196946713752));
#104587=CARTESIAN_POINT('Ctrl Pts',(-122.810712226579,2.33818506039435,
135.133435210747));
#104588=CARTESIAN_POINT('Ctrl Pts',(-122.818463417819,2.45700412376505,
135.064913844355));
#104589=CARTESIAN_POINT('Ctrl Pts',(-122.826211314596,2.57577268586469,
134.996421601372));
#104590=CARTESIAN_POINT('Ctrl Pts',(-122.833959211373,2.69173653485233,
134.922923924974));
#104591=CARTESIAN_POINT('Ctrl Pts',(-122.84170710815,2.80445299930199,134.8446856586));
#104592=CARTESIAN_POINT('Ctrl Pts',(-122.849453384234,2.91714588589718,
134.766463757985));
#104593=CARTESIAN_POINT('Ctrl Pts',(-122.857199660318,3.02659241811215,
134.683503462592));
#104594=CARTESIAN_POINT('Ctrl Pts',(-122.864945936402,3.13237869640231,
134.596113083752));
#104595=CARTESIAN_POINT('Ctrl Pts',(-122.872692269667,3.23816575558289,
134.508722059816));
#104596=CARTESIAN_POINT('Ctrl Pts',(-122.880438602933,3.34029220550706,
134.41690113618));
#104597=CARTESIAN_POINT('Ctrl Pts',(-122.888184936198,3.43837736271539,
134.320998809656));
#104598=CARTESIAN_POINT('Ctrl Pts',(-122.895933004201,3.53648448541448,
134.225075006471));
#104599=CARTESIAN_POINT('Ctrl Pts',(-122.903681072204,3.63054823502001,
134.125068254915));
#104600=CARTESIAN_POINT('Ctrl Pts',(-122.911429140207,3.72022520503315,
134.021363490791));
#104601=CARTESIAN_POINT('Ctrl Pts',(-122.919185442949,3.80999748479707,
133.917548508009));
#104602=CARTESIAN_POINT('Ctrl Pts',(-122.926941745691,3.89537341534292,
133.810027957682));
#104603=CARTESIAN_POINT('Ctrl Pts',(-122.934698048432,3.97604994444538,
133.699219837248));
#104604=CARTESIAN_POINT('Ctrl Pts',(-122.942458490946,4.05676953304054,
133.588352575183));
#104605=CARTESIAN_POINT('Ctrl Pts',(-122.950218933461,4.13278450578335,
133.474194571934));
#104606=CARTESIAN_POINT('Ctrl Pts',(-122.957979375975,4.20383607360944,
133.35719146365));
#104607=CARTESIAN_POINT('Ctrl Pts',(-122.96575227624,4.27500169972006,133.24000053159));
#104608=CARTESIAN_POINT('Ctrl Pts',(-122.973525176505,4.3411878100385,133.119955710316));
#104609=CARTESIAN_POINT('Ctrl Pts',(-122.981298076771,4.40218196199473,
132.997526602162));
#104610=CARTESIAN_POINT('Ctrl Pts',(-122.988788412533,4.46095882289482,
132.879548100464));
#104611=CARTESIAN_POINT('Ctrl Pts',(-122.996278748296,4.51491452718198,
132.759355932951));
#104612=CARTESIAN_POINT('Ctrl Pts',(-123.003769084058,4.56390248355713,
132.637384671713));
#104613=CARTESIAN_POINT('Ctrl Pts',(-123.011543418177,4.61474783318588,
132.510788833037));
#104614=CARTESIAN_POINT('Ctrl Pts',(-123.019317752296,4.66040235710147,
132.381875311254));
#104615=CARTESIAN_POINT('Ctrl Pts',(-123.027092086415,4.7006491727853,132.251108839232));
#104616=CARTESIAN_POINT('Ctrl Pts',(-123.034856839362,4.74084638786554,
132.1205035252));
#104617=CARTESIAN_POINT('Ctrl Pts',(-123.042621592309,4.77564904121475,
131.988050174685));
#104618=CARTESIAN_POINT('Ctrl Pts',(-123.050386345256,4.80488801296413,
131.854234060117));
#104619=CARTESIAN_POINT('Ctrl Pts',(-123.058143386141,4.83409794415466,
131.7205508536));
#104620=CARTESIAN_POINT('Ctrl Pts',(-123.065900427026,4.85775510767214,
131.585507956072));
#104621=CARTESIAN_POINT('Ctrl Pts',(-123.073657467911,4.87574008708958,
131.449606048118));
#104622=CARTESIAN_POINT('Ctrl Pts',(-123.081408659151,4.89371150389416,
131.313806624849));
#104623=CARTESIAN_POINT('Ctrl Pts',(-123.089159850391,4.90601919949514,
131.17714986655));
#104624=CARTESIAN_POINT('Ctrl Pts',(-123.096911041632,4.91259483939269,
131.040146551142));
#104625=CARTESIAN_POINT('Ctrl Pts',(-123.104658938409,4.91916768446787,
130.903201465798));
#104626=CARTESIAN_POINT('Ctrl Pts',(-123.112406835186,4.92001330070399,
130.765910506004));
#104627=CARTESIAN_POINT('Ctrl Pts',(-123.120154731963,4.91511523366853,
130.628789258115));
#104628=CARTESIAN_POINT('Ctrl Pts',(-123.127901008047,4.91021819120311,
130.491696693035));
#104629=CARTESIAN_POINT('Ctrl Pts',(-123.135647284131,4.89957986917322,
130.354774159717));
#104630=CARTESIAN_POINT('Ctrl Pts',(-123.143393560215,4.88323593581998,
130.218536533377));
#104631=CARTESIAN_POINT('Ctrl Pts',(-123.15113989348,4.86689188181951,130.08229790136));
#104632=CARTESIAN_POINT('Ctrl Pts',(-123.158886226746,4.84484217902196,
129.946744574592));
#104633=CARTESIAN_POINT('Ctrl Pts',(-123.166632560011,4.81717425895649,
129.812385203885));
#104634=CARTESIAN_POINT('Ctrl Pts',(-123.174380628014,4.78950014285218,
129.67799574433));
#104635=CARTESIAN_POINT('Ctrl Pts',(-123.182128696017,4.75620538472538,
129.544801155745));
#104636=CARTESIAN_POINT('Ctrl Pts',(-123.18987676402,4.71742822236983,129.41329842295));
#104637=CARTESIAN_POINT('Ctrl Pts',(-123.197633066762,4.67860984718462,
129.281655927486));
#104638=CARTESIAN_POINT('Ctrl Pts',(-123.205389369504,4.63429753893669,
129.151709255358));
#104639=CARTESIAN_POINT('Ctrl Pts',(-123.213145672245,4.58467916357902,
129.023939310812));
#104640=CARTESIAN_POINT('Ctrl Pts',(-123.22090611476,4.53503430540045,128.896101171599));
#104641=CARTESIAN_POINT('Ctrl Pts',(-123.228666557274,4.48007789368029,
128.770442432954));
#104642=CARTESIAN_POINT('Ctrl Pts',(-123.236426999788,4.42004497292152,
128.647421698669));
#104643=CARTESIAN_POINT('Ctrl Pts',(-123.244199900053,4.35991568198887,
128.524203480581));
#104644=CARTESIAN_POINT('Ctrl Pts',(-123.251972800319,4.29469378331742,
128.403632073326));
#104645=CARTESIAN_POINT('Ctrl Pts',(-123.259745700584,4.22465953625129,
128.286140042386));
#104646=CARTESIAN_POINT('Ctrl Pts',(-123.267236036346,4.15717121047164,
128.172919142715));
#104647=CARTESIAN_POINT('Ctrl Pts',(-123.274726372108,4.08521451203541,
128.062557878201));
#104648=CARTESIAN_POINT('Ctrl Pts',(-123.28221670787,4.0090758225709,127.955414477082));
#104649=CARTESIAN_POINT('Ctrl Pts',(-123.289991041989,3.93005031155317,
127.844208701344));
#104650=CARTESIAN_POINT('Ctrl Pts',(-123.297765376108,3.84626910000627,
127.736117349959));
#104651=CARTESIAN_POINT('Ctrl Pts',(-123.305539710228,3.75800595055514,
127.631574091798));
#104652=CARTESIAN_POINT('Ctrl Pts',(-123.313304463175,3.66985157754765,
127.52715967386));
#104653=CARTESIAN_POINT('Ctrl Pts',(-123.321069216122,3.57722650672185,
127.426284944628));
#104654=CARTESIAN_POINT('Ctrl Pts',(-123.328833969069,3.48044759809827,
127.32935449104));
#104655=CARTESIAN_POINT('Ctrl Pts',(-123.336591009954,3.38376481165134,
127.232520310145));
#104656=CARTESIAN_POINT('Ctrl Pts',(-123.344348050839,3.2829366720871,127.139622883753));
#104657=CARTESIAN_POINT('Ctrl Pts',(-123.352105091724,3.17831986866529,
127.051033310369));
#104658=CARTESIAN_POINT('Ctrl Pts',(-123.359856282964,3.07378195758859,
126.962510543073));
#104659=CARTESIAN_POINT('Ctrl Pts',(-123.367607474204,2.96546136661579,
126.878289414304));
#104660=CARTESIAN_POINT('Ctrl Pts',(-123.375358665444,2.85375089121121,
126.798703503757));
#104661=CARTESIAN_POINT('Ctrl Pts',(-123.383106562221,2.74208789573849,
126.719151419344));
#104662=CARTESIAN_POINT('Ctrl Pts',(-123.390854458998,2.6270381992121,126.644230861169));
#104663=CARTESIAN_POINT('Ctrl Pts',(-123.398602355775,2.50902668501259,
126.574234359829));
#104664=CARTESIAN_POINT('Ctrl Pts',(-123.40634863186,2.39103985627782,126.504252500249));
#104665=CARTESIAN_POINT('Ctrl Pts',(-123.414094907944,2.27009277823699,
126.439192848089));
#104666=CARTESIAN_POINT('Ctrl Pts',(-123.421841184028,2.14663790954584,
126.379303697277));
#104667=CARTESIAN_POINT('Ctrl Pts',(-123.429587517293,2.02318212953872,
126.319414104377));
#104668=CARTESIAN_POINT('Ctrl Pts',(-123.437333850559,1.89721887370198,
126.264695259628));
#104669=CARTESIAN_POINT('Ctrl Pts',(-123.445080183824,1.76922334324927,
126.215348542598));
#104670=CARTESIAN_POINT('Ctrl Pts',(-123.452828251827,1.6411991490855,126.165990774714));
#104671=CARTESIAN_POINT('Ctrl Pts',(-123.46057631983,1.51114213940536,126.122007669094));
#104672=CARTESIAN_POINT('Ctrl Pts',(-123.468324387833,1.37954516251603,
126.083551554802));
#104673=CARTESIAN_POINT('Ctrl Pts',(-123.476080690575,1.24780832279347,
126.045054568893));
#104674=CARTESIAN_POINT('Ctrl Pts',(-123.483836993317,1.11452862225466,
126.012096418403));
#104675=CARTESIAN_POINT('Ctrl Pts',(-123.491593296058,0.980212205397892,
125.984778986876));
#104676=CARTESIAN_POINT('Ctrl Pts',(-123.499353738573,0.845824099825262,
125.957446975212));
#104677=CARTESIAN_POINT('Ctrl Pts',(-123.507114181087,0.710398561242755,
125.935761743216));
#104678=CARTESIAN_POINT('Ctrl Pts',(-123.514874623601,0.574448473305037,
125.919773427842));
#104679=CARTESIAN_POINT('Ctrl Pts',(-123.522647523867,0.438280146216711,
125.903759446604));
#104680=CARTESIAN_POINT('Ctrl Pts',(-123.530420424132,0.301585977167221,
125.893460686395));
#104681=CARTESIAN_POINT('Ctrl Pts',(-123.538193324397,0.164881382769034,
125.8888751693));
#104682=CARTESIAN_POINT('Ctrl Pts',(-123.545683660159,0.033146344718272,
125.884456347301));
#104683=CARTESIAN_POINT('Ctrl Pts',(-123.553173995921,-0.0985980658538286,
125.885342596421));
#104684=CARTESIAN_POINT('Ctrl Pts',(-123.560664331683,-0.229895665117554,
125.8914866068));
#104685=CARTESIAN_POINT('Ctrl Pts',(-123.568438665802,-0.366171452767279,
125.8978635692));
#104686=CARTESIAN_POINT('Ctrl Pts',(-123.576212999921,-0.502397559304757,
125.90992505958));
#104687=CARTESIAN_POINT('Ctrl Pts',(-123.58398733404,-0.638061151439749,
125.927675162308));
#104688=CARTESIAN_POINT('Ctrl Pts',(-123.591752086988,-0.77355755032167,
125.945403389622));
#104689=CARTESIAN_POINT('Ctrl Pts',(-123.599516839935,-0.908492430219827,
125.968806229833));
#104690=CARTESIAN_POINT('Ctrl Pts',(-123.607281592882,-1.04235413010378,
125.997835788757));
#104691=CARTESIAN_POINT('Ctrl Pts',(-123.615038633767,-1.17608287666028,
126.026836515114));
#104692=CARTESIAN_POINT('Ctrl Pts',(-123.622795674652,-1.30874018477532,
126.06145275642));
#104693=CARTESIAN_POINT('Ctrl Pts',(-123.630552715537,-1.43982103950688,
126.101585007706));
#104694=CARTESIAN_POINT('Ctrl Pts',(-123.638303906777,-1.57080304514604,
126.14168699495));
#104695=CARTESIAN_POINT('Ctrl Pts',(-123.646055098017,-1.70021059134348,
126.187296598619));
#104696=CARTESIAN_POINT('Ctrl Pts',(-123.653806289257,-1.82755071251333,
126.238263656737));
#104697=CARTESIAN_POINT('Ctrl Pts',(-123.661554186035,-1.95483671073461,
126.289209052496));
#104698=CARTESIAN_POINT('Ctrl Pts',(-123.669302082812,-2.08005666940539,
126.34550722883));
#104699=CARTESIAN_POINT('Ctrl Pts',(-123.677049979589,-2.20273481440205,
126.406958839252));
#104700=CARTESIAN_POINT('Ctrl Pts',(-123.684796255673,-2.32538729777607,
126.468397595322));
#104701=CARTESIAN_POINT('Ctrl Pts',(-123.692542531757,-2.44549867570165,
126.534987466314));
#104702=CARTESIAN_POINT('Ctrl Pts',(-123.700288807841,-2.56261548650922,
126.60648199488));
#104703=CARTESIAN_POINT('Ctrl Pts',(-123.708035141107,-2.67973316184601,
126.677977051202));
#104704=CARTESIAN_POINT('Ctrl Pts',(-123.715781474372,-2.79385589225454,
126.754376633633));
#104705=CARTESIAN_POINT('Ctrl Pts',(-123.723527807637,-2.90455739353712,
126.83538979251));
#104706=CARTESIAN_POINT('Ctrl Pts',(-123.73127587564,-3.01528368565291,
126.916421093721));
#104707=CARTESIAN_POINT('Ctrl Pts',(-123.739023943643,-3.12258690862798,
127.002067796436));
#104708=CARTESIAN_POINT('Ctrl Pts',(-123.746772011646,-3.22607250715903,
127.091997590995));
#104709=CARTESIAN_POINT('Ctrl Pts',(-123.754528314388,-3.32966809141612,
127.18202296401));
#104710=CARTESIAN_POINT('Ctrl Pts',(-123.76228461713,-3.42943765052578,
127.276340265363));
#104711=CARTESIAN_POINT('Ctrl Pts',(-123.770040919872,-3.52502188351182,
127.374578731897));
#104712=CARTESIAN_POINT('Ctrl Pts',(-123.777801362386,-3.62065713268125,
127.472869631259));
#104713=CARTESIAN_POINT('Ctrl Pts',(-123.7855618049,-3.71210234407415,127.575085574734));
#104714=CARTESIAN_POINT('Ctrl Pts',(-123.793322247414,-3.79903810990706,
127.680822159027));
#104715=CARTESIAN_POINT('Ctrl Pts',(-123.80109514768,-3.88611343274884,
127.786728481071));
#104716=CARTESIAN_POINT('Ctrl Pts',(-123.808868047945,-3.96866460870062,
127.896166425418));
#104717=CARTESIAN_POINT('Ctrl Pts',(-123.816640948211,-4.04641470656897,
128.008701288363));
#104718=CARTESIAN_POINT('Ctrl Pts',(-123.824131283973,-4.12133839254038,
128.117145225583));
#104719=CARTESIAN_POINT('Ctrl Pts',(-123.831621619735,-4.19180383800849,
128.228464568694));
#104720=CARTESIAN_POINT('Ctrl Pts',(-123.839111955497,-4.25760426759582,
128.342249945186));
#104721=CARTESIAN_POINT('Ctrl Pts',(-123.847202547063,-4.32867777051783,
128.465153782429));
#104722=CARTESIAN_POINT('Ctrl Pts',(-123.85529313863,-4.39451845037392,
128.591297548042));
#104723=CARTESIAN_POINT('Ctrl Pts',(-123.863383730196,-4.45483135510529,
128.720215550621));
#104724=CARTESIAN_POINT('Ctrl Pts',(-123.871462872162,-4.51505890654167,
128.848951111708));
#104725=CARTESIAN_POINT('Ctrl Pts',(-123.879542014128,-4.56977411494359,
128.980452780504));
#104726=CARTESIAN_POINT('Ctrl Pts',(-123.887621156094,-4.61872659268647,
129.114228159884));
#104727=CARTESIAN_POINT('Ctrl Pts',(-123.895686767567,-4.66759708757046,
129.247779499776));
#104728=CARTESIAN_POINT('Ctrl Pts',(-123.903752379041,-4.71072396876428,
129.383596637296));
#104729=CARTESIAN_POINT('Ctrl Pts',(-123.911817990514,-4.74790408347292,
129.521165434969));
#104730=CARTESIAN_POINT('Ctrl Pts',(-123.913014248927,-4.75341848559683,
129.541569074818));
#104731=CARTESIAN_POINT('Ctrl Pts',(-123.914210507341,-4.75880215823508,
129.562011208398));
#104732=CARTESIAN_POINT('Ctrl Pts',(-123.915406765754,-4.76405452823402,
129.582490119308));
#104733=CARTESIAN_POINT('Ctrl Pts',(-122.165194063467,-4.76405452823402,
129.582490119308));
#104734=CARTESIAN_POINT('Ctrl Pts',(-122.166271446518,-4.76875350298938,
129.600811350562));
#104735=CARTESIAN_POINT('Ctrl Pts',(-122.167348829569,-4.77334578412048,
129.619155771924));
#104736=CARTESIAN_POINT('Ctrl Pts',(-122.16842621262,-4.77783118013098,
129.63752203547));
#104737=CARTESIAN_POINT('Ctrl Pts',(-122.178817676348,-4.82109325846368,
129.814666423688));
#104738=CARTESIAN_POINT('Ctrl Pts',(-122.189209140076,-4.854519516994,129.994300071186));
#104739=CARTESIAN_POINT('Ctrl Pts',(-122.199600603804,-4.87787888710515,
130.175488114404));
#104740=CARTESIAN_POINT('Ctrl Pts',(-122.209731485858,-4.90065248567181,
130.352132593329));
#104741=CARTESIAN_POINT('Ctrl Pts',(-122.219862367913,-4.91385781485816,
130.530254837794));
#104742=CARTESIAN_POINT('Ctrl Pts',(-122.229993249967,-4.91732476503059,
130.708965556285));
#104743=CARTESIAN_POINT('Ctrl Pts',(-122.231709021302,-4.91791192947415,
130.739232094412));
#104744=CARTESIAN_POINT('Ctrl Pts',(-122.233424792636,-4.91821987222497,
130.769515450041));
#104745=CARTESIAN_POINT('Ctrl Pts',(-122.235140563971,-4.91824789589999,
130.799811224715));
#104746=CARTESIAN_POINT('',(-121.889859435959,-4.91824956029332,130.806440322977));
#104747=CARTESIAN_POINT('Ctrl Pts',(-121.81971904495,-4.76405452823411,
129.582490119308));
#104748=CARTESIAN_POINT('Ctrl Pts',(-121.82739965095,-4.79781016501553,
129.714102834806));
#104749=CARTESIAN_POINT('Ctrl Pts',(-121.835080256949,-4.8260827257844,
129.847018133833));
#104750=CARTESIAN_POINT('Ctrl Pts',(-121.842760862948,-4.84879609593379,
129.980734802916));
#104751=CARTESIAN_POINT('Ctrl Pts',(-121.850610625117,-4.87200970091906,
130.11739642185));
#104752=CARTESIAN_POINT('Ctrl Pts',(-121.858460387285,-4.88941633854078,
130.254894678313));
#104753=CARTESIAN_POINT('Ctrl Pts',(-121.866310149453,-4.90099086532254,
130.392691332186));
#104754=CARTESIAN_POINT('Ctrl Pts',(-121.874159911622,-4.91256539210432,
130.53048798606));
#104755=CARTESIAN_POINT('Ctrl Pts',(-121.88200967379,-4.918307854094,130.668582596542));
#104756=CARTESIAN_POINT('Ctrl Pts',(-121.889859435959,-4.91824956029332,
130.806440322977));
#104757=CARTESIAN_POINT('Ctrl Pts',(-121.889859435993,-4.91824956029306,
130.80644032358));
#104758=CARTESIAN_POINT('Ctrl Pts',(-121.896428818984,-4.91820077481326,
130.921811997752));
#104759=CARTESIAN_POINT('Ctrl Pts',(-121.902998201974,-4.91409278695161,
131.037093702136));
#104760=CARTESIAN_POINT('Ctrl Pts',(-121.909567584965,-4.90594236236138,
131.152085508375));
#104761=CARTESIAN_POINT('Ctrl Pts',(-121.917341919084,-4.8962969932197,
131.28816902245));
#104762=CARTESIAN_POINT('Ctrl Pts',(-121.925116253203,-4.8809699253112,
131.424066456723));
#104763=CARTESIAN_POINT('Ctrl Pts',(-121.932890587322,-4.85996938202834,
131.559265027572));
#104764=CARTESIAN_POINT('Ctrl Pts',(-121.940655340269,-4.8389947200382,
131.694296978266));
#104765=CARTESIAN_POINT('Ctrl Pts',(-121.948420093217,-4.81236055420518,
131.828631396617));
#104766=CARTESIAN_POINT('Ctrl Pts',(-121.956184846164,-4.78012704337739,
131.961757918268));
#104767=CARTESIAN_POINT('Ctrl Pts',(-121.963941887049,-4.74792554732696,
132.094752216781));
#104768=CARTESIAN_POINT('Ctrl Pts',(-121.971698927934,-4.71013586502534,
132.226540628525));
#104769=CARTESIAN_POINT('Ctrl Pts',(-121.979455968819,-4.66686959175194,
132.356620671836));
#104770=CARTESIAN_POINT('Ctrl Pts',(-121.987207160059,-4.62363594591171,
132.486602620773));
#104771=CARTESIAN_POINT('Ctrl Pts',(-121.994958351299,-4.57493405238862,
132.614878396067));
#104772=CARTESIAN_POINT('Ctrl Pts',(-122.002709542539,-4.52092585973126,
132.740958777565));
#104773=CARTESIAN_POINT('Ctrl Pts',(-122.010457439316,-4.46694062199641,
132.866985571539));
#104774=CARTESIAN_POINT('Ctrl Pts',(-122.018205336093,-4.40765372440739,
132.990818468955));
#104775=CARTESIAN_POINT('Ctrl Pts',(-122.02595323287,-4.34327587331147,
133.111986616468));
#104776=CARTESIAN_POINT('Ctrl Pts',(-122.033699508955,-4.27891148867419,
133.233129418217));
#104777=CARTESIAN_POINT('Ctrl Pts',(-122.041445785039,-4.20945845203306,
133.351608233738));
#104778=CARTESIAN_POINT('Ctrl Pts',(-122.049192061123,-4.1351740315922,
133.466975646245));
#104779=CARTESIAN_POINT('Ctrl Pts',(-122.056938394388,-4.06088906280073,
133.582343910367));
#104780=CARTESIAN_POINT('Ctrl Pts',(-122.064684727654,-3.98177285070284,
133.694600396927));
#104781=CARTESIAN_POINT('Ctrl Pts',(-122.072431060919,-3.89812649082136,
133.803325926478));
#104782=CARTESIAN_POINT('Ctrl Pts',(-122.080179128922,-3.81446139891765,
133.912075804357));
#104783=CARTESIAN_POINT('Ctrl Pts',(-122.087927196925,-3.72626437885274,
134.017292841944));
#104784=CARTESIAN_POINT('Ctrl Pts',(-122.095675264928,-3.63387711282874,
134.118590572074));
#104785=CARTESIAN_POINT('Ctrl Pts',(-122.10343156767,-3.54139165651886,
134.219995962638));
#104786=CARTESIAN_POINT('Ctrl Pts',(-122.111187870412,-3.44470732189457,
134.317473435408));
#104787=CARTESIAN_POINT('Ctrl Pts',(-122.118944173154,-3.34420338757461,
134.410672690173));
#104788=CARTESIAN_POINT('Ctrl Pts',(-122.126704615668,-3.24364581127851,
134.503921688187));
#104789=CARTESIAN_POINT('Ctrl Pts',(-122.134465058182,-3.13926487053839,
134.592887664816));
#104790=CARTESIAN_POINT('Ctrl Pts',(-122.142225500696,-3.03147251709762,
134.677261008821));
#104791=CARTESIAN_POINT('Ctrl Pts',(-122.149998400962,-2.92350712580204,
134.761769796408));
#104792=CARTESIAN_POINT('Ctrl Pts',(-122.157771301227,-2.8121196962751,
134.84167099075));
#104793=CARTESIAN_POINT('Ctrl Pts',(-122.165544201493,-2.69775145262236,
134.916698172093));
#104794=CARTESIAN_POINT('Ctrl Pts',(-122.173034537255,-2.58754078270355,
134.988997926412));
#104795=CARTESIAN_POINT('Ctrl Pts',(-122.180524873017,-2.47456252041896,
135.056771722278));
#104796=CARTESIAN_POINT('Ctrl Pts',(-122.188015208779,-2.35923088242923,
135.119822667671));
#104797=CARTESIAN_POINT('Ctrl Pts',(-122.195789542898,-2.23952641032965,
135.185264208823));
#104798=CARTESIAN_POINT('Ctrl Pts',(-122.203563877017,-2.11690739547165,
135.245824995209));
#104799=CARTESIAN_POINT('Ctrl Pts',(-122.211338211136,-1.99180970218241,
135.301234773332));
#104800=CARTESIAN_POINT('Ctrl Pts',(-122.219102964083,-1.86686618061986,
135.356576263854));
#104801=CARTESIAN_POINT('Ctrl Pts',(-122.22686771703,-1.73945041270459,
135.406779220239));
#104802=CARTESIAN_POINT('Ctrl Pts',(-122.234632469977,-1.61002429975069,
135.451618391427));
#104803=CARTESIAN_POINT('Ctrl Pts',(-122.242389510862,-1.48072673463677,
135.496413027718));
#104804=CARTESIAN_POINT('Ctrl Pts',(-122.250146551747,-1.34942316504612,
135.535854353397));
#104805=CARTESIAN_POINT('Ctrl Pts',(-122.257903592633,-1.21659666300919,
135.569764653118));
#104806=CARTESIAN_POINT('Ctrl Pts',(-122.265654783873,-1.08387032647049,
135.603649380818));
#104807=CARTESIAN_POINT('Ctrl Pts',(-122.273405975113,-0.949623720698228,
135.632011288344));
#104808=CARTESIAN_POINT('Ctrl Pts',(-122.281157166353,-0.814355977606796,
135.654722192154));
#104809=CARTESIAN_POINT('Ctrl Pts',(-122.28890506313,-0.679145726914747,
135.677423443224));
#104810=CARTESIAN_POINT('Ctrl Pts',(-122.296652959907,-0.542915586878875,
135.69447840303));
#104811=CARTESIAN_POINT('Ctrl Pts',(-122.304400856684,-0.406175591682259,
135.705809837054));
#104812=CARTESIAN_POINT('Ctrl Pts',(-122.312147132769,-0.269464199544866,
135.717138900787));
#104813=CARTESIAN_POINT('Ctrl Pts',(-122.319893408853,-0.132243553763652,
135.722746787843));
#104814=CARTESIAN_POINT('Ctrl Pts',(-122.327639684937,0.00497086149853406,
135.722608105547));
#104815=CARTESIAN_POINT('Ctrl Pts',(-122.335386018202,0.14218628964655,
135.722469422228));
#104816=CARTESIAN_POINT('Ctrl Pts',(-122.343132351467,0.279395096218759,
135.716584085305));
#104817=CARTESIAN_POINT('Ctrl Pts',(-122.350878684733,0.416081864188433,
135.704978838239));
#104818=CARTESIAN_POINT('Ctrl Pts',(-122.358626752736,0.552799242211888,
135.693370992259));
#104819=CARTESIAN_POINT('Ctrl Pts',(-122.366374820739,0.688993959512517,
135.676040720293));
#104820=CARTESIAN_POINT('Ctrl Pts',(-122.374122888742,0.824156182742329,
135.653066594314));
#104821=CARTESIAN_POINT('Ctrl Pts',(-122.381879191484,0.959462057991624,
135.630068051159));
#104822=CARTESIAN_POINT('Ctrl Pts',(-122.389635494226,1.09373286104974,
135.601413737249));
#104823=CARTESIAN_POINT('Ctrl Pts',(-122.397391796968,1.22646886506869,
135.567233404605));
#104824=CARTESIAN_POINT('Ctrl Pts',(-122.405152239482,1.35927571428996,
135.533034828888));
#104825=CARTESIAN_POINT('Ctrl Pts',(-122.412912681996,1.49054575819109,
135.493304470704));
#104826=CARTESIAN_POINT('Ctrl Pts',(-122.42067312451,1.61979584208923,135.448221564284));
#104827=CARTESIAN_POINT('Ctrl Pts',(-122.428446024776,1.74925340969599,
135.40306628678));
#104828=CARTESIAN_POINT('Ctrl Pts',(-122.436218925041,1.87668417386388,
135.3525414349));
#104829=CARTESIAN_POINT('Ctrl Pts',(-122.443991825306,2.00162549570208,
135.296874216594));
#104830=CARTESIAN_POINT('Ctrl Pts',(-122.451482161068,2.1220248857792,135.243230641893));
#104831=CARTESIAN_POINT('Ctrl Pts',(-122.45897249683,2.24011241010403,135.184812222256));
#104832=CARTESIAN_POINT('Ctrl Pts',(-122.466462832592,2.35549852362121,
135.121861024945));
#104833=CARTESIAN_POINT('Ctrl Pts',(-122.474237166711,2.47525953670711,
135.056523013852));
#104834=CARTESIAN_POINT('Ctrl Pts',(-122.48201150083,2.59248961413143,134.986094748223));
#104835=CARTESIAN_POINT('Ctrl Pts',(-122.489785834949,2.70672578865574,
134.910796854442));
#104836=CARTESIAN_POINT('Ctrl Pts',(-122.497550587896,2.82082117730422,
134.835591758586));
#104837=CARTESIAN_POINT('Ctrl Pts',(-122.505315340843,2.9319296811931,134.755529188638));
#104838=CARTESIAN_POINT('Ctrl Pts',(-122.51308009379,3.03961212128482,134.670876001557));
#104839=CARTESIAN_POINT('Ctrl Pts',(-122.520837134675,3.14718760965899,
134.586306893215));
#104840=CARTESIAN_POINT('Ctrl Pts',(-122.52859417556,3.25134350062011,134.497156481345));
#104841=CARTESIAN_POINT('Ctrl Pts',(-122.536351216445,3.35166916498331,
134.403735128644));
#104842=CARTESIAN_POINT('Ctrl Pts',(-122.544102407686,3.45191917298246,
134.310384225712));
#104843=CARTESIAN_POINT('Ctrl Pts',(-122.551853598926,3.54834441860959,
134.212769058011));
#104844=CARTESIAN_POINT('Ctrl Pts',(-122.559604790166,3.64056726442985,
134.111240273021));
#104845=CARTESIAN_POINT('Ctrl Pts',(-122.567352686943,3.73275091308064,
134.009754640473));
#104846=CARTESIAN_POINT('Ctrl Pts',(-122.57510058372,3.82073545208235,133.904358987789));
#104847=CARTESIAN_POINT('Ctrl Pts',(-122.582848480497,3.90418021591382,
133.795440674028));
#104848=CARTESIAN_POINT('Ctrl Pts',(-122.590594756581,3.98760752489955,
133.686545143631));
#104849=CARTESIAN_POINT('Ctrl Pts',(-122.598341032665,4.0664967099489,133.574128727979));
#104850=CARTESIAN_POINT('Ctrl Pts',(-122.606087308749,4.14054777570314,
133.458611393137));
#104851=CARTESIAN_POINT('Ctrl Pts',(-122.613833642014,4.21459938808562,
133.343093205572));
#104852=CARTESIAN_POINT('Ctrl Pts',(-122.62157997528,4.28381259891479,133.224474382284));
#104853=CARTESIAN_POINT('Ctrl Pts',(-122.629326308545,4.34793131272805,
133.103203013708));
#104854=CARTESIAN_POINT('Ctrl Pts',(-122.637074376548,4.41206438548262,
132.98190448725));
#104855=CARTESIAN_POINT('Ctrl Pts',(-122.644822444551,4.47110050830124,
132.857952579038));
#104856=CARTESIAN_POINT('Ctrl Pts',(-122.652570512554,4.52483020863011,
132.731818696376));
#104857=CARTESIAN_POINT('Ctrl Pts',(-122.660326815296,4.57861701352396,
132.605550757122));
#104858=CARTESIAN_POINT('Ctrl Pts',(-122.668083118038,4.62708597649866,
132.477096571174));
#104859=CARTESIAN_POINT('Ctrl Pts',(-122.675839420779,4.6700761470373,132.346946707019));
#104860=CARTESIAN_POINT('Ctrl Pts',(-122.683599863294,4.71308926272436,
132.216727377963));
#104861=CARTESIAN_POINT('Ctrl Pts',(-122.691360305808,4.75061765233928,
132.084810943202));
#104862=CARTESIAN_POINT('Ctrl Pts',(-122.699120748322,4.78255095380984,
131.951700774935));
#104863=CARTESIAN_POINT('Ctrl Pts',(-122.706893648587,4.81453551745083,
131.81837692641));
#104864=CARTESIAN_POINT('Ctrl Pts',(-122.714666548853,4.84090696932823,
131.68385589891));
#104865=CARTESIAN_POINT('Ctrl Pts',(-122.722439449118,4.86160639830543,
131.548649735084));
#104866=CARTESIAN_POINT('Ctrl Pts',(-122.72992978488,4.8815533509006,131.418358655877));
#104867=CARTESIAN_POINT('Ctrl Pts',(-122.737420120642,4.89623347131066,
131.287431694483));
#104868=CARTESIAN_POINT('Ctrl Pts',(-122.744910456404,4.90563985896102,
131.156327429457));
#104869=CARTESIAN_POINT('Ctrl Pts',(-122.752684790523,4.91540289265817,
131.020252306375));
#104870=CARTESIAN_POINT('Ctrl Pts',(-122.760459124642,4.91951531850364,
130.88355512423));
#104871=CARTESIAN_POINT('Ctrl Pts',(-122.768233458761,4.91791251062267,
130.746744644425));
#104872=CARTESIAN_POINT('Ctrl Pts',(-122.775998211708,4.91631167805917,
130.610102771309));
#104873=CARTESIAN_POINT('Ctrl Pts',(-122.783762964656,4.90900963080041,
130.473348265537));
#104874=CARTESIAN_POINT('Ctrl Pts',(-122.791527717603,4.89599349616577,
130.336994863576));
#104875=CARTESIAN_POINT('Ctrl Pts',(-122.799284758488,4.88299028933954,
130.200776889737));
#104876=CARTESIAN_POINT('Ctrl Pts',(-122.807041799373,4.86428432617648,
130.064959613588));
#104877=CARTESIAN_POINT('Ctrl Pts',(-122.814798840258,4.83991476849779,
129.93005626771));
#104878=CARTESIAN_POINT('Ctrl Pts',(-122.822550031498,4.81556358809209,
129.795254653495));
#104879=CARTESIAN_POINT('Ctrl Pts',(-122.830301222738,4.78555738347861,
129.661365980918));
#104880=CARTESIAN_POINT('Ctrl Pts',(-122.838052413978,4.74998704205606,
129.528897500577));
#104881=CARTESIAN_POINT('Ctrl Pts',(-122.845800310755,4.71443181897753,
129.396485322874));
#104882=CARTESIAN_POINT('Ctrl Pts',(-122.853548207532,4.67331726388662,
129.265492513652));
#104883=CARTESIAN_POINT('Ctrl Pts',(-122.861296104309,4.62678513489556,
129.136415061497));
#104884=CARTESIAN_POINT('Ctrl Pts',(-122.869042380393,4.58026273942278,
129.007364609563));
#104885=CARTESIAN_POINT('Ctrl Pts',(-122.876788656478,4.52832515663125,
128.880229085339));
#104886=CARTESIAN_POINT('Ctrl Pts',(-122.884534932562,4.47116356104546,
128.755487885335));
#104887=CARTESIAN_POINT('Ctrl Pts',(-122.892281265827,4.41400154350568,
128.63074576452));
#104888=CARTESIAN_POINT('Ctrl Pts',(-122.900027599092,4.35161559909351,
128.508398358616));
#104889=CARTESIAN_POINT('Ctrl Pts',(-122.907773932358,4.28424429312964,
128.388903331815));
#104890=CARTESIAN_POINT('Ctrl Pts',(-122.915522000361,4.21685789982901,
128.269381544932));
#104891=CARTESIAN_POINT('Ctrl Pts',(-122.923270068364,4.1444841153706,128.152713748733));
#104892=CARTESIAN_POINT('Ctrl Pts',(-122.931018136367,4.06740632303842,
128.039330985572));
#104893=CARTESIAN_POINT('Ctrl Pts',(-122.938774439108,3.99024661151119,
127.92582771786));
#104894=CARTESIAN_POINT('Ctrl Pts',(-122.94653074185,3.90837312526953,127.815616781425));
#104895=CARTESIAN_POINT('Ctrl Pts',(-122.954287044592,3.82211159578972,
127.709098752743));
#104896=CARTESIAN_POINT('Ctrl Pts',(-122.962047487106,3.73580402593434,
127.602523872182));
#104897=CARTESIAN_POINT('Ctrl Pts',(-122.969807929621,3.64510400457132,
127.499646119913));
#104898=CARTESIAN_POINT('Ctrl Pts',(-122.977568372135,3.55037537959195,
127.400830431643));
#104899=CARTESIAN_POINT('Ctrl Pts',(-122.9853412724,3.45549468781415,127.301856115658));
#104900=CARTESIAN_POINT('Ctrl Pts',(-122.993114172666,3.356572751443,127.206957165093));
#104901=CARTESIAN_POINT('Ctrl Pts',(-123.000887072931,3.25400852355268,
127.116459915114));
#104902=CARTESIAN_POINT('Ctrl Pts',(-123.008377408693,3.15517276369015,
127.029252468121));
#104903=CARTESIAN_POINT('Ctrl Pts',(-123.015867744455,3.0529551666889,126.946132446355));
#104904=CARTESIAN_POINT('Ctrl Pts',(-123.023358080217,2.9477378177461,126.867353528376));
#104905=CARTESIAN_POINT('Ctrl Pts',(-123.031132414336,2.83853112103815,
126.785587683778));
#104906=CARTESIAN_POINT('Ctrl Pts',(-123.038906748455,2.7257467768566,126.708239617481));
#104907=CARTESIAN_POINT('Ctrl Pts',(-123.046681082574,2.60977788871213,
126.635638699029));
#104908=CARTESIAN_POINT('Ctrl Pts',(-123.054445835521,2.49395192185787,
126.56312725472));
#104909=CARTESIAN_POINT('Ctrl Pts',(-123.062210588468,2.37494954815781,
126.4953515231));
#104910=CARTESIAN_POINT('Ctrl Pts',(-123.069975341416,2.25319603065291,
126.432600021427));
#104911=CARTESIAN_POINT('Ctrl Pts',(-123.077732382301,2.13156344045803,
126.369910845431));
#104912=CARTESIAN_POINT('Ctrl Pts',(-123.085489423185,2.00718548948093,
126.312236146741));
#104913=CARTESIAN_POINT('Ctrl Pts',(-123.09324646407,1.88051514274842,126.259820392153));
#104914=CARTESIAN_POINT('Ctrl Pts',(-123.100997655311,1.75394031910989,
126.207444164694));
#104915=CARTESIAN_POINT('Ctrl Pts',(-123.108748846551,1.62507690041153,
126.160319136515));
#104916=CARTESIAN_POINT('Ctrl Pts',(-123.116500037791,1.49440077780628,
126.118643022811));
#104917=CARTESIAN_POINT('Ctrl Pts',(-123.124247934568,1.36378019603886,
126.076984622568));
#104918=CARTESIAN_POINT('Ctrl Pts',(-123.131995831345,1.23134881442666,
126.040770649129));
#104919=CARTESIAN_POINT('Ctrl Pts',(-123.139743728122,1.09760054593546,
126.010149931326));
#104920=CARTESIAN_POINT('Ctrl Pts',(-123.147490004206,0.963880254698756,
125.979535618716));
#104921=CARTESIAN_POINT('Ctrl Pts',(-123.15523628029,0.828844005360271,
125.954512321767));
#104922=CARTESIAN_POINT('Ctrl Pts',(-123.162982556374,0.692998462279085,
125.935178325458));
#104923=CARTESIAN_POINT('Ctrl Pts',(-123.170728889639,0.557151916416775,
125.91584418643));
#104924=CARTESIAN_POINT('Ctrl Pts',(-123.178475222905,0.420496451955711,
125.902199486933));
#104925=CARTESIAN_POINT('Ctrl Pts',(-123.18622155617,0.283546065124721,
125.894290893881));
#104926=CARTESIAN_POINT('Ctrl Pts',(-123.193969624173,0.146565009204334,
125.886380529754));
#104927=CARTESIAN_POINT('Ctrl Pts',(-123.201717692176,0.00928928973071805,
125.884208850735));
#104928=CARTESIAN_POINT('Ctrl Pts',(-123.209465760179,-0.127765269568259,
125.887770427364));
#104929=CARTESIAN_POINT('Ctrl Pts',(-123.217222062921,-0.264965492084016,
125.891335789279));
#104930=CARTESIAN_POINT('Ctrl Pts',(-123.224978365663,-0.401943693427651,
125.900646568836));
#104931=CARTESIAN_POINT('Ctrl Pts',(-123.232734668404,-0.538186791443481,
125.91564524029));
#104932=CARTESIAN_POINT('Ctrl Pts',(-123.240495110918,-0.674502606502924,
125.930651916987));
#104933=CARTESIAN_POINT('Ctrl Pts',(-123.248255553433,-0.810082150153177,
125.951352475687));
#104934=CARTESIAN_POINT('Ctrl Pts',(-123.256015995947,-0.944421722976589,
125.977638057519));
#104935=CARTESIAN_POINT('Ctrl Pts',(-123.263788896212,-1.0789769496084,
126.0039658353));
#104936=CARTESIAN_POINT('Ctrl Pts',(-123.271561796477,-1.21228784730783,
126.035896461167));
#104937=CARTESIAN_POINT('Ctrl Pts',(-123.279334696743,-1.34386421717513,
126.073270676728));
#104938=CARTESIAN_POINT('Ctrl Pts',(-123.286825032505,-1.47065745458151,
126.109286245416));
#104939=CARTESIAN_POINT('Ctrl Pts',(-123.294315368268,-1.59583979096157,
126.150356402643));
#104940=CARTESIAN_POINT('Ctrl Pts',(-123.30180570403,-1.71899127297666,
126.196296808771));
#104941=CARTESIAN_POINT('Ctrl Pts',(-123.309580234757,-1.846815313366,126.243980265212));
#104942=CARTESIAN_POINT('Ctrl Pts',(-123.317354765484,-1.972856267363,126.297061888114));
#104943=CARTESIAN_POINT('Ctrl Pts',(-123.325129296211,-2.09662450801239,
126.35538896842));
#104944=CARTESIAN_POINT('Ctrl Pts',(-123.332894200136,-2.22023949280895,
126.4136438253));
#104945=CARTESIAN_POINT('Ctrl Pts',(-123.340659104061,-2.34158701345982,
126.477131050741));
#104946=CARTESIAN_POINT('Ctrl Pts',(-123.348424007986,-2.4601944402295,
126.545648796045));
#104947=CARTESIAN_POINT('Ctrl Pts',(-123.356181154412,-2.57868337267675,
126.614098088942));
#104948=CARTESIAN_POINT('Ctrl Pts',(-123.363938300838,-2.69443732272807,
126.68756770569));
#104949=CARTESIAN_POINT('Ctrl Pts',(-123.371695447264,-2.80700575770333,
126.765808681696));
#104950=CARTESIAN_POINT('Ctrl Pts',(-123.379446698754,-2.91948864786013,
126.843990199558));
#104951=CARTESIAN_POINT('Ctrl Pts',(-123.387197950244,-3.02879052179509,
126.926935636976));
#104952=CARTESIAN_POINT('Ctrl Pts',(-123.394949201734,-3.13448779722124,
127.01435147357));
#104953=CARTESIAN_POINT('Ctrl Pts',(-123.402696928731,-3.24013701210768,
127.101727562193));
#104954=CARTESIAN_POINT('Ctrl Pts',(-123.410444655728,-3.34218458896928,
127.193569756934));
#104955=CARTESIAN_POINT('Ctrl Pts',(-123.418192382725,-3.44023836948567,
127.289542980246));
#104956=CARTESIAN_POINT('Ctrl Pts',(-123.425938424521,-3.53827082241121,
127.385495328506));
#104957=CARTESIAN_POINT('Ctrl Pts',(-123.433684466316,-3.63231092807136,
127.48557664442));
#104958=CARTESIAN_POINT('Ctrl Pts',(-123.441430508112,-3.72200216550812,
127.589413815136));
#104959=CARTESIAN_POINT('Ctrl Pts',(-123.449176542539,-3.8116933176219,
127.693250887072));
#104960=CARTESIAN_POINT('Ctrl Pts',(-123.456922576966,-3.89703535446943,
127.800843510671));
#104961=CARTESIAN_POINT('Ctrl Pts',(-123.464668611393,-3.97771122281371,
127.911784518238));
#104962=CARTESIAN_POINT('Ctrl Pts',(-123.472416315909,-4.05840448534014,
128.022749445326));
#104963=CARTESIAN_POINT('Ctrl Pts',(-123.480164020426,-4.13442934805928,
128.137063876537));
#104964=CARTESIAN_POINT('Ctrl Pts',(-123.487911724943,-4.20551160005577,
128.254290962773));
#104965=CARTESIAN_POINT('Ctrl Pts',(-123.495666784776,-4.27666133429309,
128.371629339046));
#104966=CARTESIAN_POINT('Ctrl Pts',(-123.503421844609,-4.34285888487681,
128.491885557472));
#104967=CARTESIAN_POINT('Ctrl Pts',(-123.511176904442,-4.40387541924184,
128.614597079122));
#104968=CARTESIAN_POINT('Ctrl Pts',(-123.518936077391,-4.46492431546065,
128.737373684317));
#104969=CARTESIAN_POINT('Ctrl Pts',(-123.526695250341,-4.5207865611397,
128.862607830896));
#104970=CARTESIAN_POINT('Ctrl Pts',(-123.53445442329,-4.57128155361596,
128.989817143281));
#104971=CARTESIAN_POINT('Ctrl Pts',(-123.542224014698,-4.62184434712703,
129.117197263158));
#104972=CARTESIAN_POINT('Ctrl Pts',(-123.549993606105,-4.66702536594817,
129.246557476954));
#104973=CARTESIAN_POINT('Ctrl Pts',(-123.557763197513,-4.70669377031537,
129.377399926105));
#104974=CARTESIAN_POINT('Ctrl Pts',(-123.561800350875,-4.72730584933898,
129.445386903262));
#104975=CARTESIAN_POINT('Ctrl Pts',(-123.565837504238,-4.74643039414011,
129.51377388796));
#104976=CARTESIAN_POINT('Ctrl Pts',(-123.5698746576,-4.76405452823401,129.582490119308));
#104977=CARTESIAN_POINT('Origin',(213.235140564004,0.,130.804360617566));
#104978=CARTESIAN_POINT('',(-125.665057882386,-4.76405452823409,129.582490119308));
#104979=CARTESIAN_POINT('',(-125.320138230236,-4.76405452823398,129.582490119308));
#104980=CARTESIAN_POINT('',(213.235140564004,-4.76405452823405,129.582490119308));
#104981=CARTESIAN_POINT('',(-123.985140564039,-4.9182499550531,130.805025538748));
#104982=CARTESIAN_POINT('Ctrl Pts',(-123.985140564039,-4.9182499550531,
130.805025538749));
#104983=CARTESIAN_POINT('Ctrl Pts',(-123.993342529297,-4.91823026668018,
130.950655339306));
#104984=CARTESIAN_POINT('Ctrl Pts',(-124.001544494556,-4.91173814329656,
131.09613293352));
#104985=CARTESIAN_POINT('Ctrl Pts',(-124.009746459814,-4.89883958656253,
131.240885264783));
#104986=CARTESIAN_POINT('Ctrl Pts',(-124.01796249326,-4.88591890594608,
131.385885878363));
#104987=CARTESIAN_POINT('Ctrl Pts',(-124.026178526706,-4.86656988110953,
131.530158430338));
#104988=CARTESIAN_POINT('Ctrl Pts',(-124.034394560152,-4.84090979353874,
131.673138744202));
#104989=CARTESIAN_POINT('Ctrl Pts',(-124.042633092738,-4.81517943728027,
131.816510601508));
#104990=CARTESIAN_POINT('Ctrl Pts',(-124.050871625323,-4.78310351118545,
131.958582830783));
#104991=CARTESIAN_POINT('Ctrl Pts',(-124.059110157909,-4.74485002077881,
132.09880310096));
#104992=CARTESIAN_POINT('Ctrl Pts',(-124.06736096834,-4.7065395213777,132.239232340738));
#104993=CARTESIAN_POINT('Ctrl Pts',(-124.075611778772,-4.66203317409171,
132.377803810291));
#104994=CARTESIAN_POINT('Ctrl Pts',(-124.083862589203,-4.61154769293278,
132.513983657393));
#104995=CARTESIAN_POINT('Ctrl Pts',(-124.092132757458,-4.56094376413327,
132.650483005888));
#104996=CARTESIAN_POINT('Ctrl Pts',(-124.100402925713,-4.50433277511573,
132.784579220322));
#104997=CARTESIAN_POINT('Ctrl Pts',(-124.108673093967,-4.44197882532874,
132.915759958721));
#104998=CARTESIAN_POINT('Ctrl Pts',(-124.111635255748,-4.41964524259493,
132.962745528748));
#104999=CARTESIAN_POINT('Ctrl Pts',(-124.114597417529,-4.39657531659368,
133.009357330806));
#105000=CARTESIAN_POINT('Ctrl Pts',(-124.11755957931,-4.37278254367277,
133.055572710695));
#105001=CARTESIAN_POINT('Ctrl Pts',(-124.125333913429,-4.31033728240945,
133.176867167677));
#105002=CARTESIAN_POINT('Ctrl Pts',(-124.133108247548,-4.24274249699988,
133.295753569918));
#105003=CARTESIAN_POINT('Ctrl Pts',(-124.140882581667,-4.17020764035701,
133.411763789077));
#105004=CARTESIAN_POINT('Ctrl Pts',(-124.148647334614,-4.09776217644232,
133.52763103601));
#105005=CARTESIAN_POINT('Ctrl Pts',(-124.156412087561,-4.02038896027019,
133.640628824317));
#105006=CARTESIAN_POINT('Ctrl Pts',(-124.164176840508,-3.93834423286467,
133.750311697601));
#105007=CARTESIAN_POINT('Ctrl Pts',(-124.171933881393,-3.85638099343926,
133.85988563231));
#105008=CARTESIAN_POINT('Ctrl Pts',(-124.179690922278,-3.76975570887975,
133.966150893017));
#105009=CARTESIAN_POINT('Ctrl Pts',(-124.187447963163,-3.67876879853684,
134.068689520941));
#105010=CARTESIAN_POINT('Ctrl Pts',(-124.195199154403,-3.58785050213043,
134.171150823689));
#105011=CARTESIAN_POINT('Ctrl Pts',(-124.202950345644,-3.4925773852067,
134.269890796098));
#105012=CARTESIAN_POINT('Ctrl Pts',(-124.210701536884,-3.39329093201159,
134.364523494911));
#105013=CARTESIAN_POINT('Ctrl Pts',(-124.218449433661,-3.29404667820778,
134.459115972303));
#105014=CARTESIAN_POINT('Ctrl Pts',(-124.226197330438,-3.1907927632036,
134.549604378988));
#105015=CARTESIAN_POINT('Ctrl Pts',(-124.233945227215,-3.0839082594759,
134.635638851999));
#105016=CARTESIAN_POINT('Ctrl Pts',(-124.241691503299,-2.97704611368223,
134.721655328452));
#105017=CARTESIAN_POINT('Ctrl Pts',(-124.249437779383,-2.86655519410049,
134.803219479374));
#105018=CARTESIAN_POINT('Ctrl Pts',(-124.257184055467,-2.75284814679336,
134.880021317771));
#105019=CARTESIAN_POINT('Ctrl Pts',(-124.264930388732,-2.6391402601268,
134.956823723101));
#105020=CARTESIAN_POINT('Ctrl Pts',(-124.272676721998,-2.52221652234742,
135.028863526926));
#105021=CARTESIAN_POINT('Ctrl Pts',(-124.280423055263,-2.40251874926647,
135.095873954598));
#105022=CARTESIAN_POINT('Ctrl Pts',(-124.288171123266,-2.28279417069933,
135.16289938879));
#105023=CARTESIAN_POINT('Ctrl Pts',(-124.295919191269,-2.16029466174176,
135.224893014688));
#105024=CARTESIAN_POINT('Ctrl Pts',(-124.303667259272,-2.0354864671806,
135.281634107585));
#105025=CARTESIAN_POINT('Ctrl Pts',(-124.311423562014,-1.91054562498486,
135.338435505591));
#105026=CARTESIAN_POINT('Ctrl Pts',(-124.319179864756,-1.7832915521367,
135.389973056977));
#105027=CARTESIAN_POINT('Ctrl Pts',(-124.326936167498,-1.65421081348336,
135.436074085286));
#105028=CARTESIAN_POINT('Ctrl Pts',(-124.334696610012,-1.52506118055326,
135.482199719101));
#105029=CARTESIAN_POINT('Ctrl Pts',(-124.342457052526,-1.39408331234045,
135.522882932168));
#105030=CARTESIAN_POINT('Ctrl Pts',(-124.35021749504,-1.26177778769949,
135.558001314649));
#105031=CARTESIAN_POINT('Ctrl Pts',(-124.357990395306,-1.12925987448485,
135.593176072277));
#105032=CARTESIAN_POINT('Ctrl Pts',(-124.365763295571,-0.995410427848216,
135.622768063572));
#105033=CARTESIAN_POINT('Ctrl Pts',(-124.373536195836,-0.860739929278256,
135.646706106753));
#105034=CARTESIAN_POINT('Ctrl Pts',(-124.381026531598,-0.730965042547292,
135.669773941767));
#105035=CARTESIAN_POINT('Ctrl Pts',(-124.38851686736,-0.600428067297373,
135.687591720733));
#105036=CARTESIAN_POINT('Ctrl Pts',(-124.396007203122,-0.469587284429826,
135.700141540443));
#105037=CARTESIAN_POINT('Ctrl Pts',(-124.403781537241,-0.333785633510681,
135.713167190381));
#105038=CARTESIAN_POINT('Ctrl Pts',(-124.41155587136,-0.197226503659713,
135.720558787405));
#105039=CARTESIAN_POINT('Ctrl Pts',(-124.419330205479,-0.0604169589232291,
135.722239515381));
#105040=CARTESIAN_POINT('Ctrl Pts',(-124.427094958426,0.0762239802763863,
135.72391817201));
#105041=CARTESIAN_POINT('Ctrl Pts',(-124.434859711373,0.213114333128947,
135.719899958625));
#105042=CARTESIAN_POINT('Ctrl Pts',(-124.442624464321,0.349740820019951,
135.710159677996));
#105043=CARTESIAN_POINT('Ctrl Pts',(-124.450381505205,0.486231607558078,
135.70042907155));
#105044=CARTESIAN_POINT('Ctrl Pts',(-124.45813854609,0.622458663224571,
135.684987735381));
#105045=CARTESIAN_POINT('Ctrl Pts',(-124.465895586975,0.757907962461091,
135.663862503864));
#105046=CARTESIAN_POINT('Ctrl Pts',(-124.473646778216,0.893255118327599,
135.64275320305));
#105047=CARTESIAN_POINT('Ctrl Pts',(-124.481397969456,1.02782530044893,
135.615968598452));
#105048=CARTESIAN_POINT('Ctrl Pts',(-124.489149160696,1.16110922325608,
135.583587378682));
#105049=CARTESIAN_POINT('Ctrl Pts',(-124.496897057473,1.29433649684039,
135.551219921794));
#105050=CARTESIAN_POINT('Ctrl Pts',(-124.50464495425,1.42627821932577,135.513260672914));
#105051=CARTESIAN_POINT('Ctrl Pts',(-124.512392851027,1.55643514315609,
135.469839446973));
#105052=CARTESIAN_POINT('Ctrl Pts',(-124.520139127111,1.6865648409638,135.426427303817));
#105053=CARTESIAN_POINT('Ctrl Pts',(-124.527885403195,1.8149101120762,135.377555579797));
#105054=CARTESIAN_POINT('Ctrl Pts',(-124.535631679279,1.94098711037878,
135.323403890189));
#105055=CARTESIAN_POINT('Ctrl Pts',(-124.543378012545,2.06706503935294,
135.269251800847));
#105056=CARTESIAN_POINT('Ctrl Pts',(-124.55112434581,2.19087430287492,135.209819822439));
#105057=CARTESIAN_POINT('Ctrl Pts',(-124.558870679075,2.31195164363967,
135.145335468907));
#105058=CARTESIAN_POINT('Ctrl Pts',(-124.566618747078,2.43305609883556,
135.08083667455));
#105059=CARTESIAN_POINT('Ctrl Pts',(-124.574366815081,2.55142706886271,
135.011283437375));
#105060=CARTESIAN_POINT('Ctrl Pts',(-124.582114883084,2.66662683507841,
134.936948715228));
#105061=CARTESIAN_POINT('Ctrl Pts',(-124.589871185826,2.78194903697639,
134.862534989255));
#105062=CARTESIAN_POINT('Ctrl Pts',(-124.597627488568,2.89409297330497,
134.783329839145));
#105063=CARTESIAN_POINT('Ctrl Pts',(-124.605383791309,3.00265036628445,
134.699649289841));
#105064=CARTESIAN_POINT('Ctrl Pts',(-124.613144233824,3.11126569961346,
134.615924077708));
#105065=CARTESIAN_POINT('Ctrl Pts',(-124.620904676338,3.21629037605639,
134.5277189581));
#105066=CARTESIAN_POINT('Ctrl Pts',(-124.628665118852,3.31735083365361,
134.435388916679));
#105067=CARTESIAN_POINT('Ctrl Pts',(-124.636438019117,3.41857352246909,
134.342910658878));
#105068=CARTESIAN_POINT('Ctrl Pts',(-124.644210919383,3.5158189981967,134.24629452273));
#105069=CARTESIAN_POINT('Ctrl Pts',(-124.651983819648,3.6087514458723,134.145931515275));
#105070=CARTESIAN_POINT('Ctrl Pts',(-124.65947415541,3.6983055649957,134.049216955936));
#105071=CARTESIAN_POINT('Ctrl Pts',(-124.666964491173,3.78385459073554,
133.949023446409));
#105072=CARTESIAN_POINT('Ctrl Pts',(-124.674454826935,3.86513574859431,
133.845726874273));
#105073=CARTESIAN_POINT('Ctrl Pts',(-124.682229161054,3.94949870625497,
133.738513781213));
#105074=CARTESIAN_POINT('Ctrl Pts',(-124.690003495173,4.02953101149955,
133.627618056455));
#105075=CARTESIAN_POINT('Ctrl Pts',(-124.697777829292,4.10489395623549,
133.513424786345));
#105076=CARTESIAN_POINT('Ctrl Pts',(-124.705542582239,4.18016402287743,
133.399372249235));
#105077=CARTESIAN_POINT('Ctrl Pts',(-124.713307335186,4.25077596560525,
133.282030575958));
#105078=CARTESIAN_POINT('Ctrl Pts',(-124.721072088134,4.31643114510465,
133.161817983473));
#105079=CARTESIAN_POINT('Ctrl Pts',(-124.728829129019,4.38202111495419,
133.04172478783));
#105080=CARTESIAN_POINT('Ctrl Pts',(-124.736586169904,4.44266393263232,
132.918766688371));
#105081=CARTESIAN_POINT('Ctrl Pts',(-124.744343210789,4.49810433183068,
132.793390653153));
#105082=CARTESIAN_POINT('Ctrl Pts',(-124.752094402029,4.55350292299267,
132.668109164978));
#105083=CARTESIAN_POINT('Ctrl Pts',(-124.759845593269,4.60370674706152,
132.540413726498));
#105084=CARTESIAN_POINT('Ctrl Pts',(-124.767596784509,4.6485067257031,132.410775347202));
#105085=CARTESIAN_POINT('Ctrl Pts',(-124.775344681286,4.69328766315874,
132.281192067676));
#105086=CARTESIAN_POINT('Ctrl Pts',(-124.783092578063,4.73266919587337,
132.149667858539));
#105087=CARTESIAN_POINT('Ctrl Pts',(-124.79084047484,4.76649068532607,132.016692919041));
#105088=CARTESIAN_POINT('Ctrl Pts',(-124.798586750924,4.80030510005229,
131.883745795034));
#105089=CARTESIAN_POINT('Ctrl Pts',(-124.806333027008,4.8285616885587,131.749348922928));
#105090=CARTESIAN_POINT('Ctrl Pts',(-124.814079303092,4.85115003562096,
131.614006462609));
#105091=CARTESIAN_POINT('Ctrl Pts',(-124.821825636358,4.87373854942531,
131.478663003221));
#105092=CARTESIAN_POINT('Ctrl Pts',(-124.829571969623,4.8906586739325,131.342374327323));
#105093=CARTESIAN_POINT('Ctrl Pts',(-124.837318302888,4.90185142117565,
131.205653163246));
#105094=CARTESIAN_POINT('Ctrl Pts',(-124.845066370891,4.91304667495692,
131.068901381413));
#105095=CARTESIAN_POINT('Ctrl Pts',(-124.852814438894,4.91851196734212,
130.931717308263));
#105096=CARTESIAN_POINT('Ctrl Pts',(-124.860562506897,4.91824034788161,
130.794616749271));
#105097=CARTESIAN_POINT('Ctrl Pts',(-124.868318809639,4.91796843974071,
130.657370478174));
#105098=CARTESIAN_POINT('Ctrl Pts',(-124.876075112381,4.91194744059989,
130.520208290131));
#105099=CARTESIAN_POINT('Ctrl Pts',(-124.883831415123,4.90022254708108,
130.383644500002));
#105100=CARTESIAN_POINT('Ctrl Pts',(-124.891591857637,4.88849139563357,
130.247007821666));
#105101=CARTESIAN_POINT('Ctrl Pts',(-124.899352300151,4.87105033339611,
130.110970565243));
#105102=CARTESIAN_POINT('Ctrl Pts',(-124.907112742666,4.8479961004954,129.97603889741));
#105103=CARTESIAN_POINT('Ctrl Pts',(-124.914885642931,4.82490485889337,
129.840890625286));
#105104=CARTESIAN_POINT('Ctrl Pts',(-124.922658543196,4.79618252222367,
129.706851870852));
#105105=CARTESIAN_POINT('Ctrl Pts',(-124.930431443462,4.76197653959325,
129.574416513607));
#105106=CARTESIAN_POINT('Ctrl Pts',(-124.937921779224,4.72901403059102,
129.446795515182));
#105107=CARTESIAN_POINT('Ctrl Pts',(-124.945412114986,4.69095973146277,
129.320663657695));
#105108=CARTESIAN_POINT('Ctrl Pts',(-124.952902450748,4.64798785104083,
129.196445197192));
#105109=CARTESIAN_POINT('Ctrl Pts',(-124.960676784867,4.60338667871175,
129.067516956004));
#105110=CARTESIAN_POINT('Ctrl Pts',(-124.968451118986,4.55334638062493,
128.940241662958));
#105111=CARTESIAN_POINT('Ctrl Pts',(-124.976225453105,4.49800786083179,
128.815112431342));
#105112=CARTESIAN_POINT('Ctrl Pts',(-124.983990206052,4.44273754081855,
128.690137410321));
#105113=CARTESIAN_POINT('Ctrl Pts',(-124.991754959,4.38218214763921,128.567303542434));
#105114=CARTESIAN_POINT('Ctrl Pts',(-124.999519711947,4.31653211722015,
128.447088137875));
#105115=CARTESIAN_POINT('Ctrl Pts',(-125.007276752832,4.2509472913368,128.326992132951));
#105116=CARTESIAN_POINT('Ctrl Pts',(-125.015033793717,4.18027808414597,
128.209509756769));
#105117=CARTESIAN_POINT('Ctrl Pts',(-125.022790834602,4.10476256485621,
128.095097369254));
#105118=CARTESIAN_POINT('Ctrl Pts',(-125.030542025842,4.02930399240708,
127.98077126101));
#105119=CARTESIAN_POINT('Ctrl Pts',(-125.038293217082,3.94900659669696,
127.869510858342));
#105120=CARTESIAN_POINT('Ctrl Pts',(-125.046044408322,3.86415363940161,
127.761746656907));
#105121=CARTESIAN_POINT('Ctrl Pts',(-125.053792305099,3.77933674687652,
127.654028258131));
#105122=CARTESIAN_POINT('Ctrl Pts',(-125.061540201876,3.68996838514976,
127.549803411619));
#105123=CARTESIAN_POINT('Ctrl Pts',(-125.069288098653,3.5963741436887,127.449472231776));
#105124=CARTESIAN_POINT('Ctrl Pts',(-125.077034374737,3.5027994801253,127.349162039053));
#105125=CARTESIAN_POINT('Ctrl Pts',(-125.084780650822,3.4050009615987,127.252744178675));
#105126=CARTESIAN_POINT('Ctrl Pts',(-125.092526926906,3.30334306997183,
127.16058405683));
#105127=CARTESIAN_POINT('Ctrl Pts',(-125.100273260171,3.20168442792936,
127.06842325468));
#105128=CARTESIAN_POINT('Ctrl Pts',(-125.108019593436,3.09616664559266,
126.98052051637));
#105129=CARTESIAN_POINT('Ctrl Pts',(-125.115765926702,2.98718921139284,
126.897202612335));
#105130=CARTESIAN_POINT('Ctrl Pts',(-125.123513994705,2.87818737245238,
126.813866049834));
#105131=CARTESIAN_POINT('Ctrl Pts',(-125.131262062708,2.76572465048735,
126.73511660212));
#105132=CARTESIAN_POINT('Ctrl Pts',(-125.139010130711,2.65023125036484,
126.661238922263));
#105133=CARTESIAN_POINT('Ctrl Pts',(-125.146766433453,2.53461510248213,
126.587282724328));
#105134=CARTESIAN_POINT('Ctrl Pts',(-125.154522736195,2.41596217193923,
126.518208848419));
#105135=CARTESIAN_POINT('Ctrl Pts',(-125.162279038937,2.29472959627212,
126.454257269082));
#105136=CARTESIAN_POINT('Ctrl Pts',(-125.170039481451,2.17343231512914,
126.390271556861));
#105137=CARTESIAN_POINT('Ctrl Pts',(-125.177799923965,2.04955299836367,
126.331413756487));
#105138=CARTESIAN_POINT('Ctrl Pts',(-125.185560366479,1.92356978873832,
126.277876073203));
#105139=CARTESIAN_POINT('Ctrl Pts',(-125.193333266745,1.79738433968062,
126.224252446478));
#105140=CARTESIAN_POINT('Ctrl Pts',(-125.20110616701,1.66908861484836,126.175966140927));
#105141=CARTESIAN_POINT('Ctrl Pts',(-125.208879067276,1.53917782889359,
126.133160057374));
#105142=CARTESIAN_POINT('Ctrl Pts',(-125.216369403037,1.41398962723766,
126.09191008278));
#105143=CARTESIAN_POINT('Ctrl Pts',(-125.223859738799,1.28730204509113,
126.055748892478));
#105144=CARTESIAN_POINT('Ctrl Pts',(-125.231350074561,1.15956618520974,
126.024759240399));
#105145=CARTESIAN_POINT('Ctrl Pts',(-125.23912440868,1.02698718137328,125.992594606241));
#105146=CARTESIAN_POINT('Ctrl Pts',(-125.246898742799,0.892858869292728,
125.965899521473));
#105147=CARTESIAN_POINT('Ctrl Pts',(-125.254673076918,0.757672281223806,
125.944821979304));
#105148=CARTESIAN_POINT('Ctrl Pts',(-125.262437829865,0.62265229854234,
125.923770413321));
#105149=CARTESIAN_POINT('Ctrl Pts',(-125.270202582812,0.486577017492259,
125.908322674644));
#105150=CARTESIAN_POINT('Ctrl Pts',(-125.27796733576,0.349950947927619,
125.898576541952));
#105151=CARTESIAN_POINT('Ctrl Pts',(-125.285724376645,0.213460577301733,
125.888840089257));
#105152=CARTESIAN_POINT('Ctrl Pts',(-125.29348141753,0.0764208942680485,
125.88479400073));
#105153=CARTESIAN_POINT('Ctrl Pts',(-125.301238458415,-0.0606554704202938,
125.886484655689));
#105154=CARTESIAN_POINT('Ctrl Pts',(-125.308989649655,-0.197628464755912,
125.888174035712));
#105155=CARTESIAN_POINT('Ctrl Pts',(-125.316740840895,-0.33463769633316,
125.895591543535));
#105156=CARTESIAN_POINT('Ctrl Pts',(-125.324492032135,-0.471167867108309,
125.908731556505));
#105157=CARTESIAN_POINT('Ctrl Pts',(-125.332239928912,-0.607640008919003,
125.921865984619));
#105158=CARTESIAN_POINT('Ctrl Pts',(-125.339987825689,-0.743633106547314,
125.94071804301));
#105159=CARTESIAN_POINT('Ctrl Pts',(-125.347735722466,-0.87863454335215,
125.965230075648));
#105160=CARTESIAN_POINT('Ctrl Pts',(-125.35548199855,-1.01360774076633,
125.989736980896));
#105161=CARTESIAN_POINT('Ctrl Pts',(-125.363228274634,-1.1475893055227,
126.019901435659));
#105162=CARTESIAN_POINT('Ctrl Pts',(-125.370974550718,-1.28007479969716,
126.055614301992));
#105163=CARTESIAN_POINT('Ctrl Pts',(-125.378720883984,-1.41256127184962,
126.091327431949));
#105164=CARTESIAN_POINT('Ctrl Pts',(-125.386467217249,-1.54355127389247,
126.132588953447));
#105165=CARTESIAN_POINT('Ctrl Pts',(-125.394213550514,-1.67255395134867,
126.179239392957));
#105166=CARTESIAN_POINT('Ctrl Pts',(-125.401961618517,-1.80158551805987,
126.225900279509));
#105167=CARTESIAN_POINT('Ctrl Pts',(-125.40970968652,-1.92862850699809,
126.277952352556));
#105168=CARTESIAN_POINT('Ctrl Pts',(-125.417457754523,-2.05321089523569,
126.335187530497));
#105169=CARTESIAN_POINT('Ctrl Pts',(-125.425214057265,-2.17792569111822,
126.392483538665));
#105170=CARTESIAN_POINT('Ctrl Pts',(-125.432970360007,-2.30017430641158,
126.454973492404));
#105171=CARTESIAN_POINT('Ctrl Pts',(-125.440726662749,-2.41950774972887,
126.522402501061));
#105172=CARTESIAN_POINT('Ctrl Pts',(-125.448487105263,-2.53890488489792,
126.589867498611));
#105173=CARTESIAN_POINT('Ctrl Pts',(-125.456247547777,-2.65538341592438,
126.662276597465));
#105174=CARTESIAN_POINT('Ctrl Pts',(-125.464007990292,-2.76852318724998,
126.739331414207));
#105175=CARTESIAN_POINT('Ctrl Pts',(-125.471780890557,-2.88184458058059,
126.816509926182));
#105176=CARTESIAN_POINT('Ctrl Pts',(-125.479553790822,-2.99181619004853,
126.898348825397));
#105177=CARTESIAN_POINT('Ctrl Pts',(-125.487326691088,-3.09805011352928,
126.984508715128));
#105178=CARTESIAN_POINT('Ctrl Pts',(-125.49481702685,-3.20042216630728,
127.067536475845));
#105179=CARTESIAN_POINT('Ctrl Pts',(-125.502307362612,-3.29932333251835,
127.154576320044));
#105180=CARTESIAN_POINT('Ctrl Pts',(-125.509797698375,-3.39444015687818,
127.245293452722));
#105181=CARTESIAN_POINT('Ctrl Pts',(-125.517456387707,-3.49169483693849,
127.338049553169));
#105182=CARTESIAN_POINT('Ctrl Pts',(-125.52511507704,-3.58532055949805,
127.434962945229));
#105183=CARTESIAN_POINT('Ctrl Pts',(-125.532773766373,-3.67493289018205,
127.53571390751));
#105184=CARTESIAN_POINT('Ctrl Pts',(-125.54042355721,-3.76444110187399,
127.636347809019));
#105185=CARTESIAN_POINT('Ctrl Pts',(-125.548073348046,-3.84994492627025,
127.740810119028));
#105186=CARTESIAN_POINT('Ctrl Pts',(-125.555723138882,-3.93109427974338,
127.848742099173));
#105187=CARTESIAN_POINT('Ctrl Pts',(-125.563365814823,-4.01216815805833,
127.956573694251));
#105188=CARTESIAN_POINT('Ctrl Pts',(-125.571008490764,-4.08889537772311,
128.067868222531));
#105189=CARTESIAN_POINT('Ctrl Pts',(-125.578651166705,-4.16096430315406,
128.182231877329));
#105190=CARTESIAN_POINT('Ctrl Pts',(-125.586288389527,-4.23298180675273,
128.296513932622));
#105191=CARTESIAN_POINT('Ctrl Pts',(-125.593925612349,-4.30034741386355,
128.413860418107));
#105192=CARTESIAN_POINT('Ctrl Pts',(-125.601562835171,-4.36279157873713,
128.533846864469));
#105193=CARTESIAN_POINT('Ctrl Pts',(-125.609196777083,-4.42520891793052,
128.653781765295));
#105194=CARTESIAN_POINT('Ctrl Pts',(-125.616830718995,-4.48270883483468,
128.776354013667));
#105195=CARTESIAN_POINT('Ctrl Pts',(-125.624464660907,-4.53506694985962,
128.901113176272));
#105196=CARTESIAN_POINT('Ctrl Pts',(-125.632098594968,-4.58742501104085,
129.025872210579));
#105197=CARTESIAN_POINT('Ctrl Pts',(-125.63973252903,-4.63464111484539,
129.152817786874));
#105198=CARTESIAN_POINT('Ctrl Pts',(-125.647366463091,-4.67653852076034,
129.281478308803));
#105199=CARTESIAN_POINT('Ctrl Pts',(-125.653263602856,-4.70890385906255,
129.380867309802));
#105200=CARTESIAN_POINT('Ctrl Pts',(-125.659160742621,-4.73809625624943,
129.481279210812));
#105201=CARTESIAN_POINT('Ctrl Pts',(-125.665057882386,-4.76405452823409,
129.582490119308));
#105202=CARTESIAN_POINT('Ctrl Pts',(-123.915406765754,-4.76405452823402,
129.582490119308));
#105203=CARTESIAN_POINT('Ctrl Pts',(-123.923457752182,-4.79940371290318,
129.720316053834));
#105204=CARTESIAN_POINT('Ctrl Pts',(-123.931508738609,-4.82880155768346,
129.859809178845));
#105205=CARTESIAN_POINT('Ctrl Pts',(-123.939559725037,-4.8521014597191,
130.000436188847));
#105206=CARTESIAN_POINT('Ctrl Pts',(-123.947599312199,-4.87536837178949,
130.140864087274));
#105207=CARTESIAN_POINT('Ctrl Pts',(-123.955638899361,-4.8925544991057,
130.282422329576));
#105208=CARTESIAN_POINT('Ctrl Pts',(-123.963678486524,-4.90356392212458,
130.424566036064));
#105209=CARTESIAN_POINT('Ctrl Pts',(-123.970832512353,-4.91336065609192,
130.551052599003));
#105210=CARTESIAN_POINT('Ctrl Pts',(-123.977986538181,-4.91826712789107,
130.678002401489));
#105211=CARTESIAN_POINT('Ctrl Pts',(-123.98514056401,-4.91824995505317,
130.805025538236));
#105212=CARTESIAN_POINT('',(-123.639859436025,-4.91824795694567,130.7998777056));
#105213=CARTESIAN_POINT('Ctrl Pts',(-123.5698746576,-4.76405452823401,129.582490119308));
#105214=CARTESIAN_POINT('Ctrl Pts',(-123.573334214347,-4.77915717273279,
129.641375100994));
#105215=CARTESIAN_POINT('Ctrl Pts',(-123.576793771095,-4.79315808372837,
129.700501843481));
#105216=CARTESIAN_POINT('Ctrl Pts',(-123.580253327842,-4.8060513612251,
129.759825612999));
#105217=CARTESIAN_POINT('Ctrl Pts',(-123.59104783843,-4.84628097172893,
129.944927666523));
#105218=CARTESIAN_POINT('Ctrl Pts',(-123.601842349019,-4.87582893446835,
130.13242751813));
#105219=CARTESIAN_POINT('Ctrl Pts',(-123.612636859607,-4.89446950845077,
130.321296136005));
#105220=CARTESIAN_POINT('Ctrl Pts',(-123.621711051736,-4.91013933880728,
130.480064809361));
#105221=CARTESIAN_POINT('Ctrl Pts',(-123.630785243864,-4.91810204906405,
130.639800716198));
#105222=CARTESIAN_POINT('Ctrl Pts',(-123.639859435993,-4.91824795694516,
130.799877705041));
#105223=CARTESIAN_POINT('Ctrl Pts',(-123.639859436025,-4.91824795694567,
130.7998777056));
#105224=CARTESIAN_POINT('Ctrl Pts',(-123.647510149338,-4.9183709760766,
130.934843235573));
#105225=CARTESIAN_POINT('Ctrl Pts',(-123.655160862651,-4.91293427663035,
131.069980165572));
#105226=CARTESIAN_POINT('Ctrl Pts',(-123.662811575964,-4.90192233098187,
131.204786045731));
#105227=CARTESIAN_POINT('Ctrl Pts',(-123.670456272973,-4.89091904481468,
131.339485918375));
#105228=CARTESIAN_POINT('Ctrl Pts',(-123.678100969983,-4.87434926666466,
131.47385485943));
#105229=CARTESIAN_POINT('Ctrl Pts',(-123.685745666992,-4.85224953570836,
131.607390819811));
#105230=CARTESIAN_POINT('Ctrl Pts',(-123.693386929821,-4.83015973248057,
131.74086679264));
#105231=CARTESIAN_POINT('Ctrl Pts',(-123.701028192649,-4.80254498058789,
131.873510132164));
#105232=CARTESIAN_POINT('Ctrl Pts',(-123.708669455477,-4.76949358225916,
132.004824707528));
#105233=CARTESIAN_POINT('Ctrl Pts',(-123.716309116396,-4.73644911280605,
132.136111754183));
#105234=CARTESIAN_POINT('Ctrl Pts',(-123.723948777315,-4.69797036103166,
132.266070200052));
#105235=CARTESIAN_POINT('Ctrl Pts',(-123.731588438233,-4.65419646501906,
132.394215430907));
#105236=CARTESIAN_POINT('Ctrl Pts',(-123.739228259569,-4.61042164984267,
132.522363352555));
#105237=CARTESIAN_POINT('Ctrl Pts',(-123.746868080906,-4.56135159979542,
132.648697602335));
#105238=CARTESIAN_POINT('Ctrl Pts',(-123.754507902242,-4.50717473717055,
132.772750556351));
#105239=CARTESIAN_POINT('Ctrl Pts',(-123.76214964624,-4.45298424022255,
132.896834729932));
#105240=CARTESIAN_POINT('Ctrl Pts',(-123.769791390238,-4.39368453665895,
133.018636097276));
#105241=CARTESIAN_POINT('Ctrl Pts',(-123.777433134236,-4.32951117748467,
133.137709289868));
#105242=CARTESIAN_POINT('Ctrl Pts',(-123.785082886883,-4.26527056377848,
133.256907272746));
#105243=CARTESIAN_POINT('Ctrl Pts',(-123.79273263953,-4.19614628908974,
133.373371018123));
#105244=CARTESIAN_POINT('Ctrl Pts',(-123.800382392177,-4.12241878867837,
133.486681700742));
#105245=CARTESIAN_POINT('Ctrl Pts',(-123.808036614016,-4.04864821467418,
133.600058582516));
#105246=CARTESIAN_POINT('Ctrl Pts',(-123.815690835855,-3.97026929430983,
133.71027840705));
#105247=CARTESIAN_POINT('Ctrl Pts',(-123.823345057694,-3.88760355211351,
133.816954464087));
#105248=CARTESIAN_POINT('Ctrl Pts',(-123.831010526621,-3.80481634114609,
133.923787270573));
#105249=CARTESIAN_POINT('Ctrl Pts',(-123.838675995549,-3.71772999235346,
134.027065607486));
#105250=CARTESIAN_POINT('Ctrl Pts',(-123.846341464476,-3.62670402139129,
134.126438431785));
#105251=CARTESIAN_POINT('Ctrl Pts',(-123.850461293536,-3.5777818427361,
134.179846651576));
#105252=CARTESIAN_POINT('Ctrl Pts',(-123.854581122595,-3.52772228186842,
134.232127407389));
#105253=CARTESIAN_POINT('Ctrl Pts',(-123.858700951655,-3.47658503718195,
134.28323105806));
#105254=CARTESIAN_POINT('Ctrl Pts',(-123.866475285774,-3.38008636687777,
134.37966633469));
#105255=CARTESIAN_POINT('Ctrl Pts',(-123.874249619893,-3.27941935293837,
134.47223622157));
#105256=CARTESIAN_POINT('Ctrl Pts',(-123.882023954012,-3.17492638197591,
134.560558899278));
#105257=CARTESIAN_POINT('Ctrl Pts',(-123.889788706959,-3.07056218926165,
134.648772727178));
#105258=CARTESIAN_POINT('Ctrl Pts',(-123.897553459906,-2.96238171699174,
134.732749510652));
#105259=CARTESIAN_POINT('Ctrl Pts',(-123.905318212853,-2.85076498297038,
134.812143305583));
#105260=CARTESIAN_POINT('Ctrl Pts',(-123.913075253739,-2.73925910826277,
134.891458245478));
#105261=CARTESIAN_POINT('Ctrl Pts',(-123.920832294624,-2.6243240802436,
134.966199030146));
#105262=CARTESIAN_POINT('Ctrl Pts',(-123.928589335509,-2.50637358930765,
135.036059389138));
#105263=CARTESIAN_POINT('Ctrl Pts',(-123.936340526749,-2.38851204575459,
135.105867065889));
#105264=CARTESIAN_POINT('Ctrl Pts',(-123.944091717989,-2.26763990054034,
135.17080144408));
#105265=CARTESIAN_POINT('Ctrl Pts',(-123.951842909229,-2.14420017242268,
135.230599278448));
#105266=CARTESIAN_POINT('Ctrl Pts',(-123.959590806006,-2.02081290948184,
135.29037169714));
#105267=CARTESIAN_POINT('Ctrl Pts',(-123.967338702783,-1.89486058524985,
135.345011744073));
#105268=CARTESIAN_POINT('Ctrl Pts',(-123.975086599561,-1.76681099509527,
135.394302008271));
#105269=CARTESIAN_POINT('Ctrl Pts',(-123.982832875645,-1.63878819015452,
135.443581962009));
#105270=CARTESIAN_POINT('Ctrl Pts',(-123.990579151729,-1.50866935653103,
135.487514218523));
#105271=CARTESIAN_POINT('Ctrl Pts',(-123.998325427813,-1.37694208432276,
135.525929589732));
#105272=CARTESIAN_POINT('Ctrl Pts',(-124.006071761078,-1.24521383973352,
135.564345244515));
#105273=CARTESIAN_POINT('Ctrl Pts',(-124.013818094344,-1.11187750819803,
135.597243823274));
#105274=CARTESIAN_POINT('Ctrl Pts',(-124.021564427609,-0.977435262299058,
135.624506193222));
#105275=CARTESIAN_POINT('Ctrl Pts',(-124.029312495612,-0.842962908991819,
135.651774668388));
#105276=CARTESIAN_POINT('Ctrl Pts',(-124.037060563615,-0.707384531595962,
135.673404345446));
#105277=CARTESIAN_POINT('Ctrl Pts',(-124.044808631618,-0.571211504384053,
135.689327401461));
#105278=CARTESIAN_POINT('Ctrl Pts',(-124.05256493436,-0.434893750858157,
135.705267380689));
#105279=CARTESIAN_POINT('Ctrl Pts',(-124.060321237102,-0.29798047396495,
135.715488577774));
#105280=CARTESIAN_POINT('Ctrl Pts',(-124.068077539844,-0.160987726819701,
135.719975127911));
#105281=CARTESIAN_POINT('Ctrl Pts',(-124.075837982358,-0.0239218625201553,
135.724464072655));
#105282=CARTESIAN_POINT('Ctrl Pts',(-124.083598424872,0.113223165790601,
135.723212275206));
#105283=CARTESIAN_POINT('Ctrl Pts',(-124.091358867386,0.249933308409536,
135.716256015867));
#105284=CARTESIAN_POINT('Ctrl Pts',(-124.099131767652,0.386862910285958,
135.709288589722));
#105285=CARTESIAN_POINT('Ctrl Pts',(-124.106904667917,0.523355841899727,
135.696598438681));
#105286=CARTESIAN_POINT('Ctrl Pts',(-124.114677568183,0.658904265552558,
135.678273648318));
#105287=CARTESIAN_POINT('Ctrl Pts',(-124.122167903944,0.789525162573133,
135.660615010244));
#105288=CARTESIAN_POINT('Ctrl Pts',(-124.129658239706,0.919268726565691,
135.637724340616));
#105289=CARTESIAN_POINT('Ctrl Pts',(-124.137148575468,1.04769309540822,
135.609724520574));
#105290=CARTESIAN_POINT('Ctrl Pts',(-124.144922909587,1.18098671323608,
135.580663078844));
#105291=CARTESIAN_POINT('Ctrl Pts',(-124.152697243706,1.3132813607472,135.546005353983));
#105292=CARTESIAN_POINT('Ctrl Pts',(-124.160471577825,1.44407073411834,
135.50583302282));
#105293=CARTESIAN_POINT('Ctrl Pts',(-124.168236330772,1.57469892127578,
135.465710200464));
#105294=CARTESIAN_POINT('Ctrl Pts',(-124.17600108372,1.7038251552757,135.420086408028));
#105295=CARTESIAN_POINT('Ctrl Pts',(-124.183765836667,1.83095297462968,
135.369094374007));
#105296=CARTESIAN_POINT('Ctrl Pts',(-124.191522877552,1.9579545288413,135.318152985994));
#105297=CARTESIAN_POINT('Ctrl Pts',(-124.199279918437,2.08296125784006,
135.26185411155));
#105298=CARTESIAN_POINT('Ctrl Pts',(-124.207036959322,2.20549187786027,
135.200380253463));
#105299=CARTESIAN_POINT('Ctrl Pts',(-124.214788150562,2.32793009658628,
135.138952753291));
#105300=CARTESIAN_POINT('Ctrl Pts',(-124.222539341802,2.44789557494999,
135.072358211768));
#105301=CARTESIAN_POINT('Ctrl Pts',(-124.230290533042,2.56492737479648,
135.000827062627));
#105302=CARTESIAN_POINT('Ctrl Pts',(-124.238038429819,2.68190943300691,
134.929326316131));
#105303=CARTESIAN_POINT('Ctrl Pts',(-124.245786326597,2.79595995978222,
134.852893338624));
#105304=CARTESIAN_POINT('Ctrl Pts',(-124.253534223374,2.90664318628904,
134.771804183655));
#105305=CARTESIAN_POINT('Ctrl Pts',(-124.261280499458,3.01730326025094,
134.690731990789));
#105306=CARTESIAN_POINT('Ctrl Pts',(-124.269026775542,3.124597119785,134.605005788655));
#105307=CARTESIAN_POINT('Ctrl Pts',(-124.276773051626,3.22811886780967,
134.514944350322));
#105308=CARTESIAN_POINT('Ctrl Pts',(-124.284519384892,3.33164138000795,
134.424882247176));
#105309=CARTESIAN_POINT('Ctrl Pts',(-124.292265718157,3.43139143016995,
134.330485100586));
#105310=CARTESIAN_POINT('Ctrl Pts',(-124.300012051422,3.52699735195981,
134.232111008386));
#105311=CARTESIAN_POINT('Ctrl Pts',(-124.307760119425,3.62262468403336,
134.13371488599));
#105312=CARTESIAN_POINT('Ctrl Pts',(-124.315508187428,3.71410576859588,
134.031340326092));
#105313=CARTESIAN_POINT('Ctrl Pts',(-124.323256255431,3.80110713400509,
133.925380902395));
#105314=CARTESIAN_POINT('Ctrl Pts',(-124.331012558173,3.88820096550067,
133.819308863763));
#105315=CARTESIAN_POINT('Ctrl Pts',(-124.338768860915,3.9708053185411,133.709644653017));
#105316=CARTESIAN_POINT('Ctrl Pts',(-124.346525163657,4.04862790630293,
133.596813864946));
#105317=CARTESIAN_POINT('Ctrl Pts',(-124.354285606171,4.12649203032326,
133.483922855686));
#105318=CARTESIAN_POINT('Ctrl Pts',(-124.362046048686,4.19956909543263,
133.367862232121));
#105319=CARTESIAN_POINT('Ctrl Pts',(-124.3698064912,4.26761176885554,133.249084089214));
#105320=CARTESIAN_POINT('Ctrl Pts',(-124.377579391465,4.33576367041838,
133.130115273087));
#105321=CARTESIAN_POINT('Ctrl Pts',(-124.385352291731,4.39886485050586,
133.008420567427));
#105322=CARTESIAN_POINT('Ctrl Pts',(-124.393125191996,4.45671491932755,
132.884474842877));
#105323=CARTESIAN_POINT('Ctrl Pts',(-124.400615527759,4.51246199243284,
132.765034857614));
#105324=CARTESIAN_POINT('Ctrl Pts',(-124.408105863521,4.56333298928115,
132.64350495662));
#105325=CARTESIAN_POINT('Ctrl Pts',(-124.415596199283,4.60919245598536,
132.520323311271));
#105326=CARTESIAN_POINT('Ctrl Pts',(-124.423370533402,4.65679069830721,
132.392471196401));
#105327=CARTESIAN_POINT('Ctrl Pts',(-124.431144867521,4.69914066127909,
132.262434615822));
#105328=CARTESIAN_POINT('Ctrl Pts',(-124.43891920164,4.73603739234594,132.130683685601));
#105329=CARTESIAN_POINT('Ctrl Pts',(-124.446683954587,4.7728886514894,131.999095126625));
#105330=CARTESIAN_POINT('Ctrl Pts',(-124.454448707534,4.80429994633945,
131.865796794682));
#105331=CARTESIAN_POINT('Ctrl Pts',(-124.462213460481,4.83011459557783,
131.731278119875));
#105332=CARTESIAN_POINT('Ctrl Pts',(-124.469970501366,4.8559036053426,131.596893050912));
#105333=CARTESIAN_POINT('Ctrl Pts',(-124.477727542251,4.87610695828812,
131.461290432618));
#105334=CARTESIAN_POINT('Ctrl Pts',(-124.485484583136,4.89061805354644,
131.32497382987));
#105335=CARTESIAN_POINT('Ctrl Pts',(-124.493235774377,4.90511820587501,
131.188760024532));
#105336=CARTESIAN_POINT('Ctrl Pts',(-124.500986965617,4.91393460341063,
131.05183369363));
#105337=CARTESIAN_POINT('Ctrl Pts',(-124.508738156857,4.91701196824753,
130.914707192549));
#105338=CARTESIAN_POINT('Ctrl Pts',(-124.516486053634,4.92008802512227,
130.77763897389));
#105339=CARTESIAN_POINT('Ctrl Pts',(-124.524233950411,4.91742989201127,
130.640371144314));
#105340=CARTESIAN_POINT('Ctrl Pts',(-124.531981847188,4.90903427688573,
130.503419542169));
#105341=CARTESIAN_POINT('Ctrl Pts',(-124.539728123272,4.90064041794189,
130.366496587347));
#105342=CARTESIAN_POINT('Ctrl Pts',(-124.547474399356,4.88651148807015,
130.22989011837));
#105343=CARTESIAN_POINT('Ctrl Pts',(-124.555220675441,4.86669628279414,
130.094113932577));
#105344=CARTESIAN_POINT('Ctrl Pts',(-124.562967008706,4.84688093124675,
129.958336744515));
#105345=CARTESIAN_POINT('Ctrl Pts',(-124.570713341971,4.82137927699687,
129.823390238736));
#105346=CARTESIAN_POINT('Ctrl Pts',(-124.578459675237,4.79029170316129,
129.689780669279));
#105347=CARTESIAN_POINT('Ctrl Pts',(-124.58620774324,4.75919716747914,129.556141178885));
#105348=CARTESIAN_POINT('Ctrl Pts',(-124.593955811243,4.72251431159356,
129.423839601302));
#105349=CARTESIAN_POINT('Ctrl Pts',(-124.601703879246,4.68039401064077,
129.293369231867));
#105350=CARTESIAN_POINT('Ctrl Pts',(-124.609460181988,4.63822894373095,
129.16276019697));
#105351=CARTESIAN_POINT('Ctrl Pts',(-124.617216484729,4.59061500792062,
129.033986630676));
#105352=CARTESIAN_POINT('Ctrl Pts',(-124.624972787471,4.53775227998991,
128.907524486545));
#105353=CARTESIAN_POINT('Ctrl Pts',(-124.632733229985,4.48486133762936,
128.780994845759));
#105354=CARTESIAN_POINT('Ctrl Pts',(-124.6404936725,4.42671618671405,128.656779439258));
#105355=CARTESIAN_POINT('Ctrl Pts',(-124.648254115014,4.36356349813381,
128.53533072348));
#105356=CARTESIAN_POINT('Ctrl Pts',(-124.656027015279,4.30030943125177,
128.413687047443));
#105357=CARTESIAN_POINT('Ctrl Pts',(-124.663799915545,4.23203195797615,
128.294819276551));
#105358=CARTESIAN_POINT('Ctrl Pts',(-124.67157281581,4.15902228485217,128.179152683591));
#105359=CARTESIAN_POINT('Ctrl Pts',(-124.679063151572,4.08866669725028,
128.067690862639));
#105360=CARTESIAN_POINT('Ctrl Pts',(-124.686553487333,4.01391716603381,
127.959201772237));
#105361=CARTESIAN_POINT('Ctrl Pts',(-124.694043823095,3.93506912105555,
127.854036215909));
#105362=CARTESIAN_POINT('Ctrl Pts',(-124.701818157214,3.85323152848279,
127.744883275543));
#105363=CARTESIAN_POINT('Ctrl Pts',(-124.709592491333,3.76671925985676,
127.638965104158));
#105364=CARTESIAN_POINT('Ctrl Pts',(-124.717366825452,3.67581705527618,
127.536708243362));
#105365=CARTESIAN_POINT('Ctrl Pts',(-124.725131578399,3.58502687953833,
127.434577405007));
#105366=CARTESIAN_POINT('Ctrl Pts',(-124.732896331346,3.48985778979982,
127.336099188628));
#105367=CARTESIAN_POINT('Ctrl Pts',(-124.740661084293,3.39063686738969,
127.24166996358));
#105368=CARTESIAN_POINT('Ctrl Pts',(-124.748418125178,3.29151449259873,
127.14733452697));
#105369=CARTESIAN_POINT('Ctrl Pts',(-124.756175166063,3.18834857512451,
127.057040346483));
#105370=CARTESIAN_POINT('Ctrl Pts',(-124.763932206948,3.0815051579867,126.971149297563));
#105371=CARTESIAN_POINT('Ctrl Pts',(-124.771683398188,2.97474231230074,
126.885323019751));
#105372=CARTESIAN_POINT('Ctrl Pts',(-124.779434589428,2.86430779037907,
126.803893508347));
#105373=CARTESIAN_POINT('Ctrl Pts',(-124.787185780668,2.75060277226001,
126.727184210819));
#105374=CARTESIAN_POINT('Ctrl Pts',(-124.794933677446,2.63694608180668,
126.650507516789));
#105375=CARTESIAN_POINT('Ctrl Pts',(-124.802681574222,2.5200219832831,126.578547264618));
#105376=CARTESIAN_POINT('Ctrl Pts',(-124.810429471,2.40026268667866,126.511585047211));
#105377=CARTESIAN_POINT('Ctrl Pts',(-124.818175747084,2.28052844113769,
126.444636836856));
#105378=CARTESIAN_POINT('Ctrl Pts',(-124.825922023168,2.15796051817767,
126.382684772428));
#105379=CARTESIAN_POINT('Ctrl Pts',(-124.833668299252,2.033017565225,126.325965520884));
#105380=CARTESIAN_POINT('Ctrl Pts',(-124.841414632517,1.90807368997165,
126.269245850651));
#105381=CARTESIAN_POINT('Ctrl Pts',(-124.849160965782,1.78075510574187,
126.21775923199));
#105382=CARTESIAN_POINT('Ctrl Pts',(-124.856907299048,1.65154199792476,
126.171694852416));
#105383=CARTESIAN_POINT('Ctrl Pts',(-124.864655367051,1.52229995372822,
126.125620157045));
#105384=CARTESIAN_POINT('Ctrl Pts',(-124.872403435054,1.39116290989811,
126.084970248283));
#105385=CARTESIAN_POINT('Ctrl Pts',(-124.880151503057,1.25862744146967,
126.049884828788));
#105386=CARTESIAN_POINT('Ctrl Pts',(-124.887907805798,1.12595111276801,
126.01476212009));
#105387=CARTESIAN_POINT('Ctrl Pts',(-124.89566410854,0.991873769047962,
125.985215814733));
#105388=CARTESIAN_POINT('Ctrl Pts',(-124.903420411282,0.856903989906555,
125.961334846978));
#105389=CARTESIAN_POINT('Ctrl Pts',(-124.911180853796,0.721862173330159,
125.937441133231));
#105390=CARTESIAN_POINT('Ctrl Pts',(-124.91894129631,0.585927359534623,
125.919218834108));
#105391=CARTESIAN_POINT('Ctrl Pts',(-124.926701738824,0.449613544577908,
125.906704982159));
#105392=CARTESIAN_POINT('Ctrl Pts',(-124.93447463909,0.313080906584052,
125.894171041864));
#105393=CARTESIAN_POINT('Ctrl Pts',(-124.942247539355,0.176168442346944,
125.887363880175));
#105394=CARTESIAN_POINT('Ctrl Pts',(-124.950020439621,0.0393913501586266,
125.886268367106));
#105395=CARTESIAN_POINT('Ctrl Pts',(-124.957510775383,-0.0924135502116431,
125.885212678697));
#105396=CARTESIAN_POINT('Ctrl Pts',(-124.965001111145,-0.224092442029103,
125.889460572971));
#105397=CARTESIAN_POINT('Ctrl Pts',(-124.972491446907,-0.355190497303149,
125.898953114297));
#105398=CARTESIAN_POINT('Ctrl Pts',(-124.980265781026,-0.491259175185668,
125.908805568213));
#105399=CARTESIAN_POINT('Ctrl Pts',(-124.988040115145,-0.627133126902452,
125.924339431135));
#105400=CARTESIAN_POINT('Ctrl Pts',(-124.995814449264,-0.762299581941407,
125.94554569931));
#105401=CARTESIAN_POINT('Ctrl Pts',(-125.003579202212,-0.897299456404333,
125.966725832654));
#105402=CARTESIAN_POINT('Ctrl Pts',(-125.011343955159,-1.03159318653046,
125.993564401762));
#105403=CARTESIAN_POINT('Ctrl Pts',(-125.019108708106,-1.164670500106,126.026000471168));
#105404=CARTESIAN_POINT('Ctrl Pts',(-125.026865748991,-1.29761563941764,
126.058404324613));
#105405=CARTESIAN_POINT('Ctrl Pts',(-125.034622789876,-1.4293463890887,
126.096394522683));
#105406=CARTESIAN_POINT('Ctrl Pts',(-125.042379830761,-1.55936043786478,
126.139858705537));
#105407=CARTESIAN_POINT('Ctrl Pts',(-125.050131022001,-1.68927644203549,
126.183290111713));
#105408=CARTESIAN_POINT('Ctrl Pts',(-125.057882213241,-1.81747795279544,
126.232187162733));
#105409=CARTESIAN_POINT('Ctrl Pts',(-125.065633404481,-1.94347599701874,
126.286387165728));
#105410=CARTESIAN_POINT('Ctrl Pts',(-125.073381301258,-2.0694204887123,
126.340564132276));
#105411=CARTESIAN_POINT('Ctrl Pts',(-125.081129198035,-2.19316301816585,
126.400039413801));
#105412=CARTESIAN_POINT('Ctrl Pts',(-125.088877094812,-2.31423305323739,
126.464601587642));
#105413=CARTESIAN_POINT('Ctrl Pts',(-125.096623370896,-2.43527776306756,
126.529150256469));
#105414=CARTESIAN_POINT('Ctrl Pts',(-125.104369646981,-2.5536507456927,
126.598783517273));
#105415=CARTESIAN_POINT('Ctrl Pts',(-125.112115923065,-2.6689049763623,
126.673243421256));
#105416=CARTESIAN_POINT('Ctrl Pts',(-125.11986225633,-2.78416005781261,
126.747703874885));
#105417=CARTESIAN_POINT('Ctrl Pts',(-125.127608589595,-2.89629601297496,
126.826990830631));
#105418=CARTESIAN_POINT('Ctrl Pts',(-125.135354922861,-3.00489412110217,
126.910802555399));
#105419=CARTESIAN_POINT('Ctrl Pts',(-125.143102990864,-3.11351654902287,
126.994633049222));
#105420=CARTESIAN_POINT('Ctrl Pts',(-125.150851058867,-3.21859924391988,
127.082990089576));
#105421=CARTESIAN_POINT('Ctrl Pts',(-125.15859912687,-3.31975625905732,
127.175531406519));
#105422=CARTESIAN_POINT('Ctrl Pts',(-125.166355429612,-3.42102078507409,
127.268171077474));
#105423=CARTESIAN_POINT('Ctrl Pts',(-125.174111732354,-3.51835100786864,
127.365003644259));
#105424=CARTESIAN_POINT('Ctrl Pts',(-125.181868035095,-3.61139720483113,
127.465649295598));
#105425=CARTESIAN_POINT('Ctrl Pts',(-125.18962847761,-3.70449306335076,
127.566348664551));
#105426=CARTESIAN_POINT('Ctrl Pts',(-125.197388920124,-3.79330008693485,
127.670864875492));
#105427=CARTESIAN_POINT('Ctrl Pts',(-125.205149362638,-3.87750929162449,
127.778785505977));
#105428=CARTESIAN_POINT('Ctrl Pts',(-125.212922262904,-3.96185367640501,
127.886879380239));
#105429=CARTESIAN_POINT('Ctrl Pts',(-125.220695163169,-4.0415852655164,
127.998388276798));
#105430=CARTESIAN_POINT('Ctrl Pts',(-125.228468063434,-4.11643831098136,
128.112870566612));
#105431=CARTESIAN_POINT('Ctrl Pts',(-125.235958399196,-4.18857025970044,
128.223191136828));
#105432=CARTESIAN_POINT('Ctrl Pts',(-125.243448734959,-4.25617204340296,
128.336272408467));
#105433=CARTESIAN_POINT('Ctrl Pts',(-125.250939070721,-4.31904740066438,
128.451699865712));
#105434=CARTESIAN_POINT('Ctrl Pts',(-125.259118235739,-4.38770492670435,
128.577742308995));
#105435=CARTESIAN_POINT('Ctrl Pts',(-125.267297400758,-4.45092577115809,
128.706947432853));
#105436=CARTESIAN_POINT('Ctrl Pts',(-125.275476565776,-4.50842288035711,
128.838831122907));
#105437=CARTESIAN_POINT('Ctrl Pts',(-125.283637476055,-4.56579166414356,
128.970420467226));
#105438=CARTESIAN_POINT('Ctrl Pts',(-125.291798386335,-4.61746205009728,
129.104676156598));
#105439=CARTESIAN_POINT('Ctrl Pts',(-125.299959296614,-4.66319283653817,
129.241089805531));
#105440=CARTESIAN_POINT('Ctrl Pts',(-125.306685607822,-4.70088464919518,
129.353523421911));
#105441=CARTESIAN_POINT('Ctrl Pts',(-125.313411919029,-4.73454230683632,
129.467422415989));
#105442=CARTESIAN_POINT('Ctrl Pts',(-125.320138230236,-4.76405452823398,
129.582490119308));
#105443=CARTESIAN_POINT('Origin',(213.235140564004,0.,130.804360617566));
#105444=CARTESIAN_POINT('',(-127.415055402248,-4.76405452823392,129.582490119308));
#105445=CARTESIAN_POINT('',(-127.069805705487,-4.76405452823416,129.582490119309));
#105446=CARTESIAN_POINT('',(213.235140564004,-4.76405452823405,129.582490119308));
#105447=CARTESIAN_POINT('',(-125.735140563975,-4.91824810239634,130.808681008151));
#105448=CARTESIAN_POINT('Ctrl Pts',(-125.73514056401,-4.91824810239579,
130.808681008773));
#105449=CARTESIAN_POINT('Ctrl Pts',(-125.74658130245,-4.91807096085325,
131.010335445559));
#105450=CARTESIAN_POINT('Ctrl Pts',(-125.75802204089,-4.90548850143151,
131.211466635464));
#105451=CARTESIAN_POINT('Ctrl Pts',(-125.76946277933,-4.88071177055635,
131.410855197305));
#105452=CARTESIAN_POINT('Ctrl Pts',(-125.775723626949,-4.86715291355413,
131.519968906111));
#105453=CARTESIAN_POINT('Ctrl Pts',(-125.781984474568,-4.84994295193747,
131.628561430318));
#105454=CARTESIAN_POINT('Ctrl Pts',(-125.788245322187,-4.82912182240563,
131.736436519446));
#105455=CARTESIAN_POINT('Ctrl Pts',(-125.796019656307,-4.80326742894898,
131.870389146474));
#105456=CARTESIAN_POINT('Ctrl Pts',(-125.803793990425,-4.77179439142009,
132.003477386229));
#105457=CARTESIAN_POINT('Ctrl Pts',(-125.811568324545,-4.73477221323026,
132.135193120672));
#105458=CARTESIAN_POINT('Ctrl Pts',(-125.819333077492,-4.69779566156628,
132.266746527243));
#105459=CARTESIAN_POINT('Ctrl Pts',(-125.827097830439,-4.65528368123059,
132.396930421297));
#105460=CARTESIAN_POINT('Ctrl Pts',(-125.834862583386,-4.6073570487901,
132.525245299195));
#105461=CARTESIAN_POINT('Ctrl Pts',(-125.842619624271,-4.55947801775672,
132.653432732947));
#105462=CARTESIAN_POINT('Ctrl Pts',(-125.850376665156,-4.5061951728124,
132.779754480848));
#105463=CARTESIAN_POINT('Ctrl Pts',(-125.858133706041,-4.44767941470448,
132.903725018168));
#105464=CARTESIAN_POINT('Ctrl Pts',(-125.865884897281,-4.38920778378469,
133.027602068341));
#105465=CARTESIAN_POINT('Ctrl Pts',(-125.873636088521,-4.32551126054325,
133.149131084986));
#105466=CARTESIAN_POINT('Ctrl Pts',(-125.881387279761,-4.25680915110943,
133.267845732912));
#105467=CARTESIAN_POINT('Ctrl Pts',(-125.889135176538,-4.18813624190508,
133.386509923945));
#105468=CARTESIAN_POINT('Ctrl Pts',(-125.896883073315,-4.11446217337812,
133.502361787696));
#105469=CARTESIAN_POINT('Ctrl Pts',(-125.904630970092,-4.03605246233152,
133.614959056299));
#105470=CARTESIAN_POINT('Ctrl Pts',(-125.912377246176,-3.95765915290595,
133.727532771981));
#105471=CARTESIAN_POINT('Ctrl Pts',(-125.92012352226,-3.87453239458777,
133.836852926011));
#105472=CARTESIAN_POINT('Ctrl Pts',(-125.927869798344,-3.7869811282361,
133.942506088522));
#105473=CARTESIAN_POINT('Ctrl Pts',(-125.93561613161,-3.69942921560099,
134.048160030941));
#105474=CARTESIAN_POINT('Ctrl Pts',(-125.943362464875,-3.60745297922013,
134.150146626789));
#105475=CARTESIAN_POINT('Ctrl Pts',(-125.95110879814,-3.51140149483713,
134.248085723401));
#105476=CARTESIAN_POINT('Ctrl Pts',(-125.958856866143,-3.4153285003903,
134.346046752794));
#105477=CARTESIAN_POINT('Ctrl Pts',(-125.966604934146,-3.31517871562495,
134.439958200223));
#105478=CARTESIAN_POINT('Ctrl Pts',(-125.974353002149,-3.21133759850637,
134.529477245394));
#105479=CARTESIAN_POINT('Ctrl Pts',(-125.982109304891,-3.10738611781265,
134.619091432471));
#105480=CARTESIAN_POINT('Ctrl Pts',(-125.989865607633,-2.9997357643591,
134.704303636179));
#105481=CARTESIAN_POINT('Ctrl Pts',(-125.997621910375,-2.88880499629402,
134.784811440763));
#105482=CARTESIAN_POINT('Ctrl Pts',(-126.005382352889,-2.77781502113796,
134.865362214786));
#105483=CARTESIAN_POINT('Ctrl Pts',(-126.013142795403,-2.66354146823299,
134.941203370456));
#105484=CARTESIAN_POINT('Ctrl Pts',(-126.020903237917,-2.54643036704537,
135.012076797192));
#105485=CARTESIAN_POINT('Ctrl Pts',(-126.028676138183,-2.42913126872149,
135.083063996245));
#105486=CARTESIAN_POINT('Ctrl Pts',(-126.036449038448,-2.30898586246423,
135.149067342137));
#105487=CARTESIAN_POINT('Ctrl Pts',(-126.044221938713,-2.18646407336403,
135.209875107201));
#105488=CARTESIAN_POINT('Ctrl Pts',(-126.051712274475,-2.06839625991271,
135.268472356839));
#105489=CARTESIAN_POINT('Ctrl Pts',(-126.059202610237,-1.94812212018979,
135.322245086625));
#105490=CARTESIAN_POINT('Ctrl Pts',(-126.066692945999,-1.82607644886793,
135.371047366774));
#105491=CARTESIAN_POINT('Ctrl Pts',(-126.074467280118,-1.699403378822,135.421700000208));
#105492=CARTESIAN_POINT('Ctrl Pts',(-126.082241614237,-1.5704205279059,
135.467158286821));
#105493=CARTESIAN_POINT('Ctrl Pts',(-126.090015948356,-1.43959295850791,
135.507206051589));
#105494=CARTESIAN_POINT('Ctrl Pts',(-126.097780701303,-1.3089266223968,
135.547204461067));
#105495=CARTESIAN_POINT('Ctrl Pts',(-126.10554545425,-1.17642046154627,
135.581805502663));
#105496=CARTESIAN_POINT('Ctrl Pts',(-126.113310207198,-1.04256000519791,
135.610840795208));
#105497=CARTESIAN_POINT('Ctrl Pts',(-126.121067248083,-0.908832500941903,
135.63984724949));
#105498=CARTESIAN_POINT('Ctrl Pts',(-126.128824288968,-0.773753757616368,
135.663298873311));
#105499=CARTESIAN_POINT('Ctrl Pts',(-126.136581329852,-0.637824636957127,
135.681077012333));
#105500=CARTESIAN_POINT('Ctrl Pts',(-126.144332521093,-0.501998021504966,
135.698841744722));
#105501=CARTESIAN_POINT('Ctrl Pts',(-126.152083712333,-0.365322691235412,
135.710941457748));
#105502=CARTESIAN_POINT('Ctrl Pts',(-126.159834903573,-0.228309527471113,
135.717308594307));
#105503=CARTESIAN_POINT('Ctrl Pts',(-126.16758280035,-0.0913545979565474,
135.723673024664));
#105504=CARTESIAN_POINT('Ctrl Pts',(-126.175330697127,0.0459374897405901,
135.724309706451));
#105505=CARTESIAN_POINT('Ctrl Pts',(-126.183078593904,0.183051124820735,
135.71920296989));
#105506=CARTESIAN_POINT('Ctrl Pts',(-126.190824869988,0.32013607868425,
135.714097301549));
#105507=CARTESIAN_POINT('Ctrl Pts',(-126.198571146072,0.457042263732288,
135.703250619051));
#105508=CARTESIAN_POINT('Ctrl Pts',(-126.206317422156,0.593254859627366,
135.686699374149));
#105509=CARTESIAN_POINT('Ctrl Pts',(-126.214063755422,0.729468461012698,
135.670148007069));
#105510=CARTESIAN_POINT('Ctrl Pts',(-126.221810088687,0.864988074918127,
135.647892040717));
#105511=CARTESIAN_POINT('Ctrl Pts',(-126.229556421952,0.999305184173385,
135.6200196806));
#105512=CARTESIAN_POINT('Ctrl Pts',(-126.237304489955,1.13365237281416,
135.592141078662));
#105513=CARTESIAN_POINT('Ctrl Pts',(-126.245052557958,1.266796138207,135.5586436596));
#105514=CARTESIAN_POINT('Ctrl Pts',(-126.252800625961,1.39823970648345,
135.519666417375));
#105515=CARTESIAN_POINT('Ctrl Pts',(-126.260556928703,1.52982297454865,
135.480647749673));
#105516=CARTESIAN_POINT('Ctrl Pts',(-126.268313231445,1.65970206041054,
135.436137736024));
#105517=CARTESIAN_POINT('Ctrl Pts',(-126.276069534186,1.78739634628032,
135.386324974019));
#105518=CARTESIAN_POINT('Ctrl Pts',(-126.2838299767,1.91515878643526,135.336485625443));
#105519=CARTESIAN_POINT('Ctrl Pts',(-126.291590419215,2.04073374526613,
135.281338046152));
#105520=CARTESIAN_POINT('Ctrl Pts',(-126.299350861729,2.16366297720856,
135.221117978295));
#105521=CARTESIAN_POINT('Ctrl Pts',(-126.307123761994,2.28678954606724,
135.160801239839));
#105522=CARTESIAN_POINT('Ctrl Pts',(-126.31489666226,2.40726155707568,135.095395927537));
#105523=CARTESIAN_POINT('Ctrl Pts',(-126.322669562525,2.52464687175936,
135.0251829587));
#105524=CARTESIAN_POINT('Ctrl Pts',(-126.330159898287,2.63776493458266,
134.957522408133));
#105525=CARTESIAN_POINT('Ctrl Pts',(-126.33765023405,2.74801656545889,134.885397841961));
#105526=CARTESIAN_POINT('Ctrl Pts',(-126.345140569812,2.85504397238631,
134.809096186644));
#105527=CARTESIAN_POINT('Ctrl Pts',(-126.352914903931,2.96612935597375,
134.729901530877));
#105528=CARTESIAN_POINT('Ctrl Pts',(-126.36068923805,3.07409308144867,134.645955919712));
#105529=CARTESIAN_POINT('Ctrl Pts',(-126.368463572169,3.17850189706106,
134.557533775426));
#105530=CARTESIAN_POINT('Ctrl Pts',(-126.376228325116,3.28278203813949,
134.46922060353));
#105531=CARTESIAN_POINT('Ctrl Pts',(-126.383993078063,3.38351569096996,
134.376442125797));
#105532=CARTESIAN_POINT('Ctrl Pts',(-126.391757831011,3.48029875128976,
134.279515817592));
#105533=CARTESIAN_POINT('Ctrl Pts',(-126.399514871896,3.57698568530965,
134.182685777963));
#105534=CARTESIAN_POINT('Ctrl Pts',(-126.40727191278,3.66972956086441,134.081716381088));
#105535=CARTESIAN_POINT('Ctrl Pts',(-126.415028953665,3.75815982269649,
133.97696488056));
#105536=CARTESIAN_POINT('Ctrl Pts',(-126.422780144906,3.84652339858035,
133.872292373954));
#105537=CARTESIAN_POINT('Ctrl Pts',(-126.430531336146,3.93057958432218,
133.763843738194));
#105538=CARTESIAN_POINT('Ctrl Pts',(-126.438282527386,4.00999539838349,
133.652012275941));
#105539=CARTESIAN_POINT('Ctrl Pts',(-126.446030424163,4.08937745860524,
133.540228345042));
#105540=CARTESIAN_POINT('Ctrl Pts',(-126.45377832094,4.16412284397078,133.425064765406));
#105541=CARTESIAN_POINT('Ctrl Pts',(-126.461526217717,4.23393967081978,
133.306946865102));
#105542=CARTESIAN_POINT('Ctrl Pts',(-126.469272493801,4.30374189349386,
133.188853672517));
#105543=CARTESIAN_POINT('Ctrl Pts',(-126.477018769885,4.36861740945242,
133.067807724816));
#105544=CARTESIAN_POINT('Ctrl Pts',(-126.484765045969,4.42831861361938,
132.944261857991));
#105545=CARTESIAN_POINT('Ctrl Pts',(-126.492511379235,4.48802025848699,
132.820715079179));
#105546=CARTESIAN_POINT('Ctrl Pts',(-126.5002577125,4.54254734523984,132.694668696439));
#105547=CARTESIAN_POINT('Ctrl Pts',(-126.508004045766,4.59169921771805,
132.5665982169));
#105548=CARTESIAN_POINT('Ctrl Pts',(-126.515752113769,4.64086209741724,
132.438499056866));
#105549=CARTESIAN_POINT('Ctrl Pts',(-126.523500181772,4.68464722747635,
132.30837526299));
#105550=CARTESIAN_POINT('Ctrl Pts',(-126.531248249775,4.72290302904014,
132.176719914829));
#105551=CARTESIAN_POINT('Ctrl Pts',(-126.539004552516,4.76119948932512,
132.044924641796));
#105552=CARTESIAN_POINT('Ctrl Pts',(-126.546760855258,4.79395477263454,
131.911594938899));
#105553=CARTESIAN_POINT('Ctrl Pts',(-126.554517158,4.82106776580748,131.777237105098));
#105554=CARTESIAN_POINT('Ctrl Pts',(-126.562277600514,4.84819523000124,
131.642807560475));
#105555=CARTESIAN_POINT('Ctrl Pts',(-126.570038043028,4.86967434227033,
131.507349177482));
#105556=CARTESIAN_POINT('Ctrl Pts',(-126.577798485543,4.88545574623936,
131.371374915478));
#105557=CARTESIAN_POINT('Ctrl Pts',(-126.585571385808,4.90126248391906,
131.235182375518));
#105558=CARTESIAN_POINT('Ctrl Pts',(-126.593344286073,4.91135320694685,
131.098472691798));
#105559=CARTESIAN_POINT('Ctrl Pts',(-126.601117186339,4.91573067761112,
130.961761277326));
#105560=CARTESIAN_POINT('Ctrl Pts',(-126.608607522101,4.91994901619056,
130.830019667125));
#105561=CARTESIAN_POINT('Ctrl Pts',(-126.616097857863,4.91886227553077,
130.698276757829));
#105562=CARTESIAN_POINT('Ctrl Pts',(-126.623588193625,4.91251845967148,
130.566988660741));
#105563=CARTESIAN_POINT('Ctrl Pts',(-126.631362527744,4.9059341161057,130.430722735548));
#105564=CARTESIAN_POINT('Ctrl Pts',(-126.639136861863,4.89366532674861,
130.294515142293));
#105565=CARTESIAN_POINT('Ctrl Pts',(-126.646911195982,4.87570878768121,
130.158878719889));
#105566=CARTESIAN_POINT('Ctrl Pts',(-126.654675948929,4.85777437844344,
130.023409457254));
#105567=CARTESIAN_POINT('Ctrl Pts',(-126.662440701877,4.8341662174146,129.888510348748));
#105568=CARTESIAN_POINT('Ctrl Pts',(-126.670205454824,4.80493297738675,
129.754692981921));
#105569=CARTESIAN_POINT('Ctrl Pts',(-126.677962495709,4.77572877222501,
129.621008524389));
#105570=CARTESIAN_POINT('Ctrl Pts',(-126.685719536594,4.74091068916384,
129.488404049916));
#105571=CARTESIAN_POINT('Ctrl Pts',(-126.693476577479,4.70057900160301,
129.357384421428));
#105572=CARTESIAN_POINT('Ctrl Pts',(-126.701227768719,4.66027772848145,
129.226463595862));
#105573=CARTESIAN_POINT('Ctrl Pts',(-126.708978959959,4.61447124137126,
129.097125609569));
#105574=CARTESIAN_POINT('Ctrl Pts',(-126.716730151199,4.56331045228496,
128.969863199043));
#105575=CARTESIAN_POINT('Ctrl Pts',(-126.724478047976,4.51217140789884,
128.842654878437));
#105576=CARTESIAN_POINT('Ctrl Pts',(-126.732225944753,4.45568273329646,
128.717520741009));
#105577=CARTESIAN_POINT('Ctrl Pts',(-126.73997384153,4.39404449878123,128.594936256962));
#105578=CARTESIAN_POINT('Ctrl Pts',(-126.747720117614,4.33241915765589,
128.472377414946));
#105579=CARTESIAN_POINT('Ctrl Pts',(-126.755466393698,4.26564657470359,
128.352367514556));
#105580=CARTESIAN_POINT('Ctrl Pts',(-126.763212669783,4.1939738970784,128.23535964187));
#105581=CARTESIAN_POINT('Ctrl Pts',(-126.770959003048,4.12230069038169,
128.118350905459));
#105582=CARTESIAN_POINT('Ctrl Pts',(-126.778705336313,4.04572752105165,
128.004344574361));
#105583=CARTESIAN_POINT('Ctrl Pts',(-126.786451669579,3.9645459871471,127.893766489506));
#105584=CARTESIAN_POINT('Ctrl Pts',(-126.794199737582,3.88334627320102,
127.783163641456));
#105585=CARTESIAN_POINT('Ctrl Pts',(-126.801947805585,3.79753637242429,
127.675990882438));
#105586=CARTESIAN_POINT('Ctrl Pts',(-126.809695873588,3.70744919453781,
127.572642261579));
#105587=CARTESIAN_POINT('Ctrl Pts',(-126.817452176329,3.6172662709265,127.469183800577));
#105588=CARTESIAN_POINT('Ctrl Pts',(-126.825208479071,3.52279724650639,
127.369557891876));
#105589=CARTESIAN_POINT('Ctrl Pts',(-126.832964781813,3.42441343079969,
127.274123271797));
#105590=CARTESIAN_POINT('Ctrl Pts',(-126.840725224327,3.32597710468828,
127.178637715389));
#105591=CARTESIAN_POINT('Ctrl Pts',(-126.848485666841,3.22362211553307,
127.087348165154));
#105592=CARTESIAN_POINT('Ctrl Pts',(-126.856246109356,3.11775335224545,
127.000573413073));
#105593=CARTESIAN_POINT('Ctrl Pts',(-126.864019009621,3.01171463902042,
126.913659362457));
#105594=CARTESIAN_POINT('Ctrl Pts',(-126.871791909887,2.90215119256412,
126.83127482802));
#105595=CARTESIAN_POINT('Ctrl Pts',(-126.879564810152,2.78949813751974,
126.753696079089));
#105596=CARTESIAN_POINT('Ctrl Pts',(-126.887055145914,2.68094030478244,
126.678937513092));
#105597=CARTESIAN_POINT('Ctrl Pts',(-126.894545481676,2.56951385416692,
126.608641558313));
#105598=CARTESIAN_POINT('Ctrl Pts',(-126.902035817438,2.45562847238693,
126.543014366896));
#105599=CARTESIAN_POINT('Ctrl Pts',(-126.909810151557,2.33742509174123,
126.474898900568));
#105600=CARTESIAN_POINT('Ctrl Pts',(-126.917584485676,2.21619820560702,
126.411597449315));
#105601=CARTESIAN_POINT('Ctrl Pts',(-126.925358819795,2.09237749403648,
126.353389994775));
#105602=CARTESIAN_POINT('Ctrl Pts',(-126.933123572742,1.96870938042711,
126.29525427572));
#105603=CARTESIAN_POINT('Ctrl Pts',(-126.940888325689,1.84245415220137,
126.24220022697));
#105604=CARTESIAN_POINT('Ctrl Pts',(-126.948653078637,1.71406853128797,
126.194463424293));
#105605=CARTESIAN_POINT('Ctrl Pts',(-126.956410119522,1.58581042478318,
126.146774034481));
#105606=CARTESIAN_POINT('Ctrl Pts',(-126.964167160407,1.45542650048104,
126.104391516362));
#105607=CARTESIAN_POINT('Ctrl Pts',(-126.971924201292,1.32339571408289,
126.06750439783));
#105608=CARTESIAN_POINT('Ctrl Pts',(-126.979675392532,1.19146449312764,
126.030645096161));
#105609=CARTESIAN_POINT('Ctrl Pts',(-126.987426583772,1.05788925704805,
125.999273050227));
#105610=CARTESIAN_POINT('Ctrl Pts',(-126.995177775012,0.923166130640588,
125.973527629588));
#105611=CARTESIAN_POINT('Ctrl Pts',(-127.002925671789,0.788500265155893,
125.947793151439));
#105612=CARTESIAN_POINT('Ctrl Pts',(-127.010673568566,0.652687862919644,
125.927680615374));
#105613=CARTESIAN_POINT('Ctrl Pts',(-127.018421465344,0.516237093364168,
125.913278699837));
#105614=CARTESIAN_POINT('Ctrl Pts',(-127.026167741428,0.379814866368144,
125.898879796871));
#105615=CARTESIAN_POINT('Ctrl Pts',(-127.033914017512,0.242754926215932,
125.890189179441));
#105616=CARTESIAN_POINT('Ctrl Pts',(-127.041660293596,0.105572056130962,
125.88724381974));
#105617=CARTESIAN_POINT('Ctrl Pts',(-127.049406626861,-0.0316118266066049,
125.884298438297));
#105618=CARTESIAN_POINT('Ctrl Pts',(-127.057152960127,-0.168918250212538,
125.887098407602));
#105619=CARTESIAN_POINT('Ctrl Pts',(-127.064899293392,-0.30583132677999,
125.895628575372));
#105620=CARTESIAN_POINT('Ctrl Pts',(-127.072647361395,-0.442775064082211,
125.904160653415));
#105621=CARTESIAN_POINT('Ctrl Pts',(-127.080395429398,-0.579324888928421,
125.918425459112));
#105622=CARTESIAN_POINT('Ctrl Pts',(-127.088143497401,-0.714969330791542,
125.938355899265));
#105623=CARTESIAN_POINT('Ctrl Pts',(-127.095899800143,-0.850757937181479,
125.958307521727));
#105624=CARTESIAN_POINT('Ctrl Pts',(-127.103656102885,-0.985638850957818,
125.983936750323));
#105625=CARTESIAN_POINT('Ctrl Pts',(-127.111412405627,-1.11910955522665,
126.015125097579));
#105626=CARTESIAN_POINT('Ctrl Pts',(-127.119172848141,-1.25265149682872,
126.046330090996));
#105627=CARTESIAN_POINT('Ctrl Pts',(-127.126933290655,-1.38478135269379,
126.083100010443));
#105628=CARTESIAN_POINT('Ctrl Pts',(-127.134693733169,-1.51501206175335,
126.125266526266));
#105629=CARTESIAN_POINT('Ctrl Pts',(-127.142466633435,-1.64545182870879,
126.167500731523));
#105630=CARTESIAN_POINT('Ctrl Pts',(-127.1502395337,-1.7739859898281,126.215148708808));
#105631=CARTESIAN_POINT('Ctrl Pts',(-127.158012433966,-1.90014691640336,
126.267993705754));
#105632=CARTESIAN_POINT('Ctrl Pts',(-127.165502769727,-2.02172157551332,
126.318917653951));
#105633=CARTESIAN_POINT('Ctrl Pts',(-127.172993105489,-2.14109227145035,
126.374667201982));
#105634=CARTESIAN_POINT('Ctrl Pts',(-127.180483441251,-2.25786411690229,
126.435009099079));
#105635=CARTESIAN_POINT('Ctrl Pts',(-127.188258645785,-2.37907697184334,
126.497645889578));
#105636=CARTESIAN_POINT('Ctrl Pts',(-127.196033850318,-2.49787339678363,
126.565429686841));
#105637=CARTESIAN_POINT('Ctrl Pts',(-127.203809054852,-2.61378542659004,
126.638150252469));
#105638=CARTESIAN_POINT('Ctrl Pts',(-127.211574485278,-2.72955174490323,
126.710779402027));
#105639=CARTESIAN_POINT('Ctrl Pts',(-127.219339915704,-2.84244055508795,
126.788332764952));
#105640=CARTESIAN_POINT('Ctrl Pts',(-127.22710534613,-2.95200667842948,
126.870553348138));
#105641=CARTESIAN_POINT('Ctrl Pts',(-127.234936598468,-3.06250151420178,
126.953470855476));
#105642=CARTESIAN_POINT('Ctrl Pts',(-127.242767850806,-3.1696167021075,
127.041134914113));
#105643=CARTESIAN_POINT('Ctrl Pts',(-127.250599103144,-3.27292279347026,
127.13323552429));
#105644=CARTESIAN_POINT('Ctrl Pts',(-127.25834997073,-3.37516848807113,
127.224390757601));
#105645=CARTESIAN_POINT('Ctrl Pts',(-127.266100838315,-3.47368261274716,
127.319891630404));
#105646=CARTESIAN_POINT('Ctrl Pts',(-127.273851705901,-3.56808011938389,
127.419395724963));
#105647=CARTESIAN_POINT('Ctrl Pts',(-127.281599016516,-3.66243430582419,
127.518854155847));
#105648=CARTESIAN_POINT('Ctrl Pts',(-127.289346327131,-3.75267536492801,
127.622311869915));
#105649=CARTESIAN_POINT('Ctrl Pts',(-127.297093637747,-3.83845445671201,
127.729389000421));
#105650=CARTESIAN_POINT('Ctrl Pts',(-127.304839070779,-3.92421275968017,
127.836440180469));
#105651=CARTESIAN_POINT('Ctrl Pts',(-127.31258450381,-4.00551100395607,
127.947108725872));
#105652=CARTESIAN_POINT('Ctrl Pts',(-127.320329936842,-4.08204033137633,
128.060981351858));
#105653=CARTESIAN_POINT('Ctrl Pts',(-127.328223725626,-4.16003549884399,
128.17703509012));
#105654=CARTESIAN_POINT('Ctrl Pts',(-127.33611751441,-4.23307693528564,
128.296416576218));
#105655=CARTESIAN_POINT('Ctrl Pts',(-127.344011303193,-4.3008839601664,
128.41865732007));
#105656=CARTESIAN_POINT('Ctrl Pts',(-127.351760510745,-4.3674490436303,
128.538659124183));
#105657=CARTESIAN_POINT('Ctrl Pts',(-127.359509718296,-4.4289696688949,
128.661415971348));
#105658=CARTESIAN_POINT('Ctrl Pts',(-127.367258925848,-4.48522708801597,
128.786460463587));
#105659=CARTESIAN_POINT('Ctrl Pts',(-127.375225005248,-4.54305894560785,
128.915004491749));
#105660=CARTESIAN_POINT('Ctrl Pts',(-127.383191084648,-4.59532849085163,
129.045965689352));
#105661=CARTESIAN_POINT('Ctrl Pts',(-127.391157164048,-4.64185173657047,
129.178815934022));
#105662=CARTESIAN_POINT('Ctrl Pts',(-127.399123243448,-4.68837498228919,
129.311666178692));
#105663=CARTESIAN_POINT('Ctrl Pts',(-127.407089322848,-4.72915183134664,
129.446405033867));
#105664=CARTESIAN_POINT('Ctrl Pts',(-127.415055402248,-4.76405452823392,
129.582490119308));
#105665=CARTESIAN_POINT('Ctrl Pts',(-125.665057882386,-4.76405452823409,
129.582490119308));
#105666=CARTESIAN_POINT('Ctrl Pts',(-125.672695217592,-4.79767286397123,
129.713567500118));
#105667=CARTESIAN_POINT('Ctrl Pts',(-125.680332552798,-4.82586495161931,
129.845985106168));
#105668=CARTESIAN_POINT('Ctrl Pts',(-125.687969888004,-4.84854317541177,
129.979247207986));
#105669=CARTESIAN_POINT('Ctrl Pts',(-125.695831667332,-4.87188786124959,
130.116425583573));
#105670=CARTESIAN_POINT('Ctrl Pts',(-125.703693446661,-4.88938953514324,
130.254498400782));
#105671=CARTESIAN_POINT('Ctrl Pts',(-125.711555225989,-4.90101002084738,
130.392919445521));
#105672=CARTESIAN_POINT('Ctrl Pts',(-125.719417005318,-4.91263050655152,
130.53134049026));
#105673=CARTESIAN_POINT('Ctrl Pts',(-125.727278784646,-4.9183698294618,
130.670109298731));
#105674=CARTESIAN_POINT('Ctrl Pts',(-125.735140563975,-4.91824810239634,
130.808681008151));
#105675=CARTESIAN_POINT('',(-125.389859435955,-4.91824999990999,130.804330862985));
#105676=CARTESIAN_POINT('Ctrl Pts',(-125.320138230236,-4.76405452823398,
129.582490119308));
#105677=CARTESIAN_POINT('Ctrl Pts',(-125.328275130921,-4.79975582231666,
129.721688923094));
#105678=CARTESIAN_POINT('Ctrl Pts',(-125.336412031606,-4.82938928728266,
129.862598298068));
#105679=CARTESIAN_POINT('Ctrl Pts',(-125.344548932291,-4.85280195543081,
130.004675527129));
#105680=CARTESIAN_POINT('Ctrl Pts',(-125.352670622673,-4.87617085829199,
130.146487171309));
#105681=CARTESIAN_POINT('Ctrl Pts',(-125.360792313054,-4.89334209898037,
130.289461990503));
#105682=CARTESIAN_POINT('Ctrl Pts',(-125.368914003435,-4.90421331179742,
130.433045583008));
#105683=CARTESIAN_POINT('Ctrl Pts',(-125.375895814266,-4.9135587494866,
130.556477212902));
#105684=CARTESIAN_POINT('Ctrl Pts',(-125.382877625097,-4.91824924988505,
130.680358369937));
#105685=CARTESIAN_POINT('Ctrl Pts',(-125.389859435927,-4.91824999990999,
130.804330862496));
#105686=CARTESIAN_POINT('Ctrl Pts',(-125.389859435993,-4.91824999991,130.804330863662));
#105687=CARTESIAN_POINT('Ctrl Pts',(-125.397970397523,-4.91825087120044,
130.948353115535));
#105688=CARTESIAN_POINT('Ctrl Pts',(-125.406081359054,-4.91192127880867,
131.092254350031));
#105689=CARTESIAN_POINT('Ctrl Pts',(-125.414192320584,-4.89931885277626,
131.235472947859));
#105690=CARTESIAN_POINT('Ctrl Pts',(-125.422313830718,-4.88670003682647,
131.378877806729));
#105691=CARTESIAN_POINT('Ctrl Pts',(-125.430435340851,-4.86779213784465,
131.521597925211));
#105692=CARTESIAN_POINT('Ctrl Pts',(-125.438556850985,-4.84270420667647,
131.663080029911));
#105693=CARTESIAN_POINT('Ctrl Pts',(-125.446697426043,-4.81755738258036,
131.804894258266));
#105694=CARTESIAN_POINT('Ctrl Pts',(-125.4548380011,-4.78620157904461,131.945464332473));
#105695=CARTESIAN_POINT('Ctrl Pts',(-125.462978576158,-4.74879668757742,
132.084248535531));
#105696=CARTESIAN_POINT('Ctrl Pts',(-125.471129195619,-4.71134564337744,
132.223203980103));
#105697=CARTESIAN_POINT('Ctrl Pts',(-125.479279815079,-4.66783071693721,
132.360368838192));
#105698=CARTESIAN_POINT('Ctrl Pts',(-125.48743043454,-4.61846067915778,
132.495219576076));
#105699=CARTESIAN_POINT('Ctrl Pts',(-125.49559972164,-4.56897756750725,
132.630379167176));
#105700=CARTESIAN_POINT('Ctrl Pts',(-125.50376900874,-4.51361265832525,
132.763213731274));
#105701=CARTESIAN_POINT('Ctrl Pts',(-125.511938295841,-4.4526223398104,
132.893220919626));
#105702=CARTESIAN_POINT('Ctrl Pts',(-125.517754428738,-4.40920021575162,
132.985779679748));
#105703=CARTESIAN_POINT('Ctrl Pts',(-125.523570561636,-4.36292768914718,
133.076905826833));
#105704=CARTESIAN_POINT('Ctrl Pts',(-125.529386694533,-4.31391074000627,
133.166426914214));
#105705=CARTESIAN_POINT('Ctrl Pts',(-125.537161028653,-4.24839054869866,
133.286088355288));
#105706=CARTESIAN_POINT('Ctrl Pts',(-125.544935362771,-4.17778396040222,
133.40321111713));
#105707=CARTESIAN_POINT('Ctrl Pts',(-125.552709696891,-4.10231230580387,
133.517332568794));
#105708=CARTESIAN_POINT('Ctrl Pts',(-125.560474449838,-4.02693366327493,
133.631313375968));
#105709=CARTESIAN_POINT('Ctrl Pts',(-125.568239202785,-3.94670209780952,
133.742299909592));
#105710=CARTESIAN_POINT('Ctrl Pts',(-125.576003955732,-3.8618851344126,
133.849853397249));
#105711=CARTESIAN_POINT('Ctrl Pts',(-125.583760996617,-3.77715241241943,
133.957300061266));
#105712=CARTESIAN_POINT('Ctrl Pts',(-125.591518037502,-3.68784359624918,
134.061320159865));
#105713=CARTESIAN_POINT('Ctrl Pts',(-125.599275078387,-3.59426967314588,
134.161503536657));
#105714=CARTESIAN_POINT('Ctrl Pts',(-125.607026269627,-3.50076631486576,
134.261611364385));
#105715=CARTESIAN_POINT('Ctrl Pts',(-125.614777460867,-3.40300451739153,
134.357887944686));
#105716=CARTESIAN_POINT('Ctrl Pts',(-125.622528652107,-3.30133550249796,
134.449956174186));
#105717=CARTESIAN_POINT('Ctrl Pts',(-125.630276548884,-3.19970969964768,
134.541985272233));
#105718=CARTESIAN_POINT('Ctrl Pts',(-125.638024445661,-3.094180271519,134.629809315108));
#105719=CARTESIAN_POINT('Ctrl Pts',(-125.645772342439,-2.98513509515818,
134.71308822718));
#105720=CARTESIAN_POINT('Ctrl Pts',(-125.653518618523,-2.87611272869752,
134.796349719098));
#105721=CARTESIAN_POINT('Ctrl Pts',(-125.661264894607,-2.76357638731155,
134.875067734147));
#105722=CARTESIAN_POINT('Ctrl Pts',(-125.669011170691,-2.64794649311978,
134.948942916432));
#105723=CARTESIAN_POINT('Ctrl Pts',(-125.676757503956,-2.53231574537487,
135.022818644047));
#105724=CARTESIAN_POINT('Ctrl Pts',(-125.684503837221,-2.41359172872102,
135.091851257071));
#105725=CARTESIAN_POINT('Ctrl Pts',(-125.692250170487,-2.29222292280824,
135.155785342257));
#105726=CARTESIAN_POINT('Ctrl Pts',(-125.69999823849,-2.17082693719273,
135.219733745038));
#105727=CARTESIAN_POINT('Ctrl Pts',(-125.707746306493,-2.04678532958573,
135.278581165789));
#105728=CARTESIAN_POINT('Ctrl Pts',(-125.715494374496,-1.92056982552717,
135.332118849603));
#105729=CARTESIAN_POINT('Ctrl Pts',(-125.723250677238,-1.79422017812874,
135.385713433903));
#105730=CARTESIAN_POINT('Ctrl Pts',(-125.731006979979,-1.66569237941779,
135.433986855347));
#105731=CARTESIAN_POINT('Ctrl Pts',(-125.738763282721,-1.53547724225302,
135.476778910166));
#105732=CARTESIAN_POINT('Ctrl Pts',(-125.746523725235,-1.40519260534884,
135.519593804393));
#105733=CARTESIAN_POINT('Ctrl Pts',(-125.75428416775,-1.27321921152475,
135.556921396193));
#105734=CARTESIAN_POINT('Ctrl Pts',(-125.762044610264,-1.14006060034891,
135.588652089668));
#105735=CARTESIAN_POINT('Ctrl Pts',(-125.769817510529,-1.00668823114914,
135.62043372007));
#105736=CARTESIAN_POINT('Ctrl Pts',(-125.777590410795,-0.872127226561587,
135.646600423305));
#105737=CARTESIAN_POINT('Ctrl Pts',(-125.78536331106,-0.736889718295181,
135.667094067548));
#105738=CARTESIAN_POINT('Ctrl Pts',(-125.792853646822,-0.60656843409772,
135.686842716201));
#105739=CARTESIAN_POINT('Ctrl Pts',(-125.800343982584,-0.475619283671478,
135.701323571064));
#105740=CARTESIAN_POINT('Ctrl Pts',(-125.807834318346,-0.344500855542329,
135.710530429449));
#105741=CARTESIAN_POINT('Ctrl Pts',(-125.815608652465,-0.208411032357867,
135.720086368667));
#105742=CARTESIAN_POINT('Ctrl Pts',(-125.823382986584,-0.071707750095534,
135.723990759909));
#105743=CARTESIAN_POINT('Ctrl Pts',(-125.831157320703,0.0651001320843933,
135.722179751624));
#105744=CARTESIAN_POINT('Ctrl Pts',(-125.83892207365,0.201739410776776,
135.720370975244));
#105745=CARTESIAN_POINT('Ctrl Pts',(-125.846686826597,0.338482645716124,
135.712860819362));
#105746=CARTESIAN_POINT('Ctrl Pts',(-125.854451579544,0.474816081440552,
135.699637193134));
#105747=CARTESIAN_POINT('Ctrl Pts',(-125.862208620429,0.611014108874283,
135.686426700798));
#105748=CARTESIAN_POINT('Ctrl Pts',(-125.869965661314,0.74680276045711,
135.667514068522));
#105749=CARTESIAN_POINT('Ctrl Pts',(-125.877722702199,0.881668863800053,
135.642939239135));
#105750=CARTESIAN_POINT('Ctrl Pts',(-125.88547389344,1.01643326356554,135.618382941818));
#105751=CARTESIAN_POINT('Ctrl Pts',(-125.89322508468,1.15027611676581,135.588173016184));
#105752=CARTESIAN_POINT('Ctrl Pts',(-125.90097627592,1.28269031170572,135.552401121475));
#105753=CARTESIAN_POINT('Ctrl Pts',(-125.908724172697,1.4150482270807,135.516644430775));
#105754=CARTESIAN_POINT('Ctrl Pts',(-125.916472069474,1.54597831526078,
135.475330574537));
#105755=CARTESIAN_POINT('Ctrl Pts',(-125.924219966251,1.67498480396725,
135.42860206552));
#105756=CARTESIAN_POINT('Ctrl Pts',(-125.931966242335,1.80396430729735,
135.3818833311));
#105757=CARTESIAN_POINT('Ctrl Pts',(-125.939712518419,1.9310206441401,135.329752329826));
#105758=CARTESIAN_POINT('Ctrl Pts',(-125.947458794503,2.05567470947828,
135.272400965561));
#105759=CARTESIAN_POINT('Ctrl Pts',(-125.955205127769,2.18032969498462,
135.215049177941));
#105760=CARTESIAN_POINT('Ctrl Pts',(-125.962951461034,2.30258201842463,
135.152477113846));
#105761=CARTESIAN_POINT('Ctrl Pts',(-125.970697794299,2.42197437919295,
135.084924034808));
#105762=CARTESIAN_POINT('Ctrl Pts',(-125.978445862302,2.5413934770525,135.017355827727));
#105763=CARTESIAN_POINT('Ctrl Pts',(-125.986193930305,2.65795099757296,
134.944804578551));
#105764=CARTESIAN_POINT('Ctrl Pts',(-125.993941998308,2.7712163301598,134.867554326209));
#105765=CARTESIAN_POINT('Ctrl Pts',(-126.00169830105,2.88460204248983,134.79022197138));
#105766=CARTESIAN_POINT('Ctrl Pts',(-126.009454603792,2.99468825379429,
134.708180857663));
#105767=CARTESIAN_POINT('Ctrl Pts',(-126.017210906534,3.10107488376638,
134.621757325766));
#105768=CARTESIAN_POINT('Ctrl Pts',(-126.024971349048,3.20751829548612,
134.535287667027));
#105769=CARTESIAN_POINT('Ctrl Pts',(-126.032731791562,3.31025789863104,
134.444431188268));
#105770=CARTESIAN_POINT('Ctrl Pts',(-126.040492234076,3.40892931163234,
134.349552292327));
#105771=CARTESIAN_POINT('Ctrl Pts',(-126.048265134342,3.50775912074542,
134.254521088359));
#105772=CARTESIAN_POINT('Ctrl Pts',(-126.056038034607,3.60250741907165,
134.15545484649));
#105773=CARTESIAN_POINT('Ctrl Pts',(-126.063810934873,3.69284847896071,
134.052753015959));
#105774=CARTESIAN_POINT('Ctrl Pts',(-126.071301270635,3.77990541376911,
133.953784655656));
#105775=CARTESIAN_POINT('Ctrl Pts',(-126.078791606397,3.86286978150277,
133.851440682495));
#105776=CARTESIAN_POINT('Ctrl Pts',(-126.086281942159,3.94148848536463,
133.746103567288));
#105777=CARTESIAN_POINT('Ctrl Pts',(-126.094056276278,4.02308804127756,
133.636772563343));
#105778=CARTESIAN_POINT('Ctrl Pts',(-126.101830610397,4.10026437943399,
133.523870639173));
#105779=CARTESIAN_POINT('Ctrl Pts',(-126.109604944516,4.17268872890944,
133.40779139908));
#105780=CARTESIAN_POINT('Ctrl Pts',(-126.117369697463,4.2450238218469,133.291855216275));
#105781=CARTESIAN_POINT('Ctrl Pts',(-126.12513445041,4.3126183736294,133.172749837251));
#105782=CARTESIAN_POINT('Ctrl Pts',(-126.132899203357,4.37518451450922,
133.050900963631));
#105783=CARTESIAN_POINT('Ctrl Pts',(-126.140656244242,4.4376885138159,132.92917311203));
#105784=CARTESIAN_POINT('Ctrl Pts',(-126.148413285128,4.49517386365152,
132.804707534007));
#105785=CARTESIAN_POINT('Ctrl Pts',(-126.156170326013,4.54739678683776,
132.6779575661));
#105786=CARTESIAN_POINT('Ctrl Pts',(-126.163921517253,4.5995803283116,132.55130318133));
#105787=CARTESIAN_POINT('Ctrl Pts',(-126.171672708493,4.64650919373422,
132.422368195582));
#105788=CARTESIAN_POINT('Ctrl Pts',(-126.179423899733,4.68798639236415,
132.291628800346));
#105789=CARTESIAN_POINT('Ctrl Pts',(-126.18717179651,4.72944596207806,132.160944972841));
#105790=CARTESIAN_POINT('Ctrl Pts',(-126.194919693287,4.76545835556264,
132.028458633078));
#105791=CARTESIAN_POINT('Ctrl Pts',(-126.202667590064,4.79587549581106,
131.894663919945));
#105792=CARTESIAN_POINT('Ctrl Pts',(-126.210413866148,4.82628627344947,
131.760897193782));
#105793=CARTESIAN_POINT('Ctrl Pts',(-126.218160142232,4.85110403923783,
131.625823019614));
#105794=CARTESIAN_POINT('Ctrl Pts',(-126.225906418317,4.87023127936647,
131.489948210788));
#105795=CARTESIAN_POINT('Ctrl Pts',(-126.233652751582,4.88935866068808,
131.354072398965));
#105796=CARTESIAN_POINT('Ctrl Pts',(-126.241399084847,4.90279537803046,
131.217396327839));
#105797=CARTESIAN_POINT('Ctrl Pts',(-126.249145418113,4.91049554674885,
131.080434064061));
#105798=CARTESIAN_POINT('Ctrl Pts',(-126.256893486116,4.91819743986666,
130.943441128534));
#105799=CARTESIAN_POINT('Ctrl Pts',(-126.264641554119,4.92016020609354,
130.806162263096));
#105800=CARTESIAN_POINT('Ctrl Pts',(-126.272389622122,4.91639005988022,
130.669113282616));
#105801=CARTESIAN_POINT('Ctrl Pts',(-126.280145924864,4.91261590671065,
130.53191864485));
#105802=CARTESIAN_POINT('Ctrl Pts',(-126.287902227605,4.90309668043032,
130.394954771546));
#105803=CARTESIAN_POINT('Ctrl Pts',(-126.295658530347,4.88789068754124,
130.258734656721));
#105804=CARTESIAN_POINT('Ctrl Pts',(-126.303418972862,4.87267657875587,
130.12244183712));
#105805=CARTESIAN_POINT('Ctrl Pts',(-126.311179415376,4.85176971504005,
129.986893953194));
#105806=CARTESIAN_POINT('Ctrl Pts',(-126.31893985789,4.82527972168502,129.852594538114));
#105807=CARTESIAN_POINT('Ctrl Pts',(-126.326712758155,4.79874720424106,
129.718079533691));
#105808=CARTESIAN_POINT('Ctrl Pts',(-126.334485658421,4.76661373885582,
129.58481738334));
#105809=CARTESIAN_POINT('Ctrl Pts',(-126.342258558686,4.72903932973555,
129.453298043029));
#105810=CARTESIAN_POINT('Ctrl Pts',(-126.349748894448,4.69283084503144,
129.326559762017));
#105811=CARTESIAN_POINT('Ctrl Pts',(-126.35723923021,4.65157022915798,129.20144007239));
#105812=CARTESIAN_POINT('Ctrl Pts',(-126.364729565972,4.60544246063901,
129.078358646465));
#105813=CARTESIAN_POINT('Ctrl Pts',(-126.372503900091,4.55756574375593,
128.950610550866));
#105814=CARTESIAN_POINT('Ctrl Pts',(-126.38027823421,4.50429385331401,128.824653664031));
#105815=CARTESIAN_POINT('Ctrl Pts',(-126.388052568329,4.4457802310428,128.700977342989));
#105816=CARTESIAN_POINT('Ctrl Pts',(-126.395817321276,4.38733872158137,
128.57745344196));
#105817=CARTESIAN_POINT('Ctrl Pts',(-126.403582074223,4.32366849929613,
128.456204864495));
#105818=CARTESIAN_POINT('Ctrl Pts',(-126.411346827171,4.25497211838848,
128.337703905691));
#105819=CARTESIAN_POINT('Ctrl Pts',(-126.419103868056,4.18634396769479,
128.219320643711));
#105820=CARTESIAN_POINT('Ctrl Pts',(-126.426860908941,4.11269978759912,
128.103679905662));
#105821=CARTESIAN_POINT('Ctrl Pts',(-126.434617949826,4.03428921545152,
127.991231827661));
#105822=CARTESIAN_POINT('Ctrl Pts',(-126.442369141066,3.95593777332664,
127.878868547632));
#105823=CARTESIAN_POINT('Ctrl Pts',(-126.450120332306,3.87282731625049,
127.769693454848));
#105824=CARTESIAN_POINT('Ctrl Pts',(-126.457871523546,3.78525199930314,
127.664129676334));
#105825=CARTESIAN_POINT('Ctrl Pts',(-126.465619420323,3.69771390420153,
127.558610765241));
#105826=CARTESIAN_POINT('Ctrl Pts',(-126.4733673171,3.60571497268157,127.456700415878));
#105827=CARTESIAN_POINT('Ctrl Pts',(-126.481115213877,3.50959089854363,
127.358790303763));
#105828=CARTESIAN_POINT('Ctrl Pts',(-126.488861489961,3.41348693148979,
127.260900672333));
#105829=CARTESIAN_POINT('Ctrl Pts',(-126.496607766045,3.3132598118796,127.167009892592));
#105830=CARTESIAN_POINT('Ctrl Pts',(-126.50435404213,3.2092832275382,127.077473950663));
#105831=CARTESIAN_POINT('Ctrl Pts',(-126.512100375395,3.10530587566542,
126.9879373478));
#105832=CARTESIAN_POINT('Ctrl Pts',(-126.51984670866,2.99757930009304,126.90275590201));
#105833=CARTESIAN_POINT('Ctrl Pts',(-126.527593041925,2.88651119788386,
126.822246082926));
#105834=CARTESIAN_POINT('Ctrl Pts',(-126.535341109928,2.77541822274283,
126.741718234226));
#105835=CARTESIAN_POINT('Ctrl Pts',(-126.543089177931,2.66098254839991,
126.66586432342));
#105836=CARTESIAN_POINT('Ctrl Pts',(-126.550837245934,2.54364150357446,
126.594957932648));
#105837=CARTESIAN_POINT('Ctrl Pts',(-126.558593548676,2.42617574729036,
126.523976181721));
#105838=CARTESIAN_POINT('Ctrl Pts',(-126.566349851418,2.30579878733667,
126.45795265734));
#105839=CARTESIAN_POINT('Ctrl Pts',(-126.57410615416,2.18297373619734,126.397115590389));
#105840=CARTESIAN_POINT('Ctrl Pts',(-126.581866596674,2.06008312963003,
126.336246052865));
#105841=CARTESIAN_POINT('Ctrl Pts',(-126.589627039188,1.93474218545123,
126.280568647219));
#105842=CARTESIAN_POINT('Ctrl Pts',(-126.597387481703,1.80743379552507,
126.230263314568));
#105843=CARTESIAN_POINT('Ctrl Pts',(-126.605160381968,1.6799210388695,126.179877227331));
#105844=CARTESIAN_POINT('Ctrl Pts',(-126.612933282233,1.55043489465477,
126.134880574453));
#105845=CARTESIAN_POINT('Ctrl Pts',(-126.620706182499,1.41947406289477,
126.095403573032));
#105846=CARTESIAN_POINT('Ctrl Pts',(-126.628196518261,1.29327398723969,
126.057361660049));
#105847=CARTESIAN_POINT('Ctrl Pts',(-126.635686854023,1.16570487805469,
126.024445136282));
#105848=CARTESIAN_POINT('Ctrl Pts',(-126.643177189785,1.03721980295778,
125.9967252172));
#105849=CARTESIAN_POINT('Ctrl Pts',(-126.650951523904,0.903863177186204,
125.96795428896));
#105850=CARTESIAN_POINT('Ctrl Pts',(-126.658725858023,0.769097322985132,
125.944690665125));
#105851=CARTESIAN_POINT('Ctrl Pts',(-126.666500192142,0.633416889284741,
125.927069760249));
#105852=CARTESIAN_POINT('Ctrl Pts',(-126.674264945089,0.497903669593145,
125.909470571563));
#105853=CARTESIAN_POINT('Ctrl Pts',(-126.682029698036,0.361478497057188,
125.897500315025));
#105854=CARTESIAN_POINT('Ctrl Pts',(-126.689794450983,0.224648212411595,
125.891243863085));
#105855=CARTESIAN_POINT('Ctrl Pts',(-126.697551491868,0.0879538295340525,
125.884993625142));
#105856=CARTESIAN_POINT('Ctrl Pts',(-126.705308532753,-0.0491444767026139,
125.88444591597));
#105857=CARTESIAN_POINT('Ctrl Pts',(-126.713065573638,-0.186133058949208,
125.889634018164));
#105858=CARTESIAN_POINT('Ctrl Pts',(-126.720816764879,-0.323018337041245,
125.89481820797));
#105859=CARTESIAN_POINT('Ctrl Pts',(-126.728567956119,-0.459793666735248,
125.90572958492));
#105860=CARTESIAN_POINT('Ctrl Pts',(-126.736319147359,-0.59594406127791,
125.922349378504));
#105861=CARTESIAN_POINT('Ctrl Pts',(-126.744067044136,-0.732036588270405,
125.938962108232));
#105862=CARTESIAN_POINT('Ctrl Pts',(-126.751814940913,-0.867504321125767,
125.961278381736));
#105863=CARTESIAN_POINT('Ctrl Pts',(-126.75956283769,-1.00183628143945,
125.989227480498));
#105864=CARTESIAN_POINT('Ctrl Pts',(-126.767309113774,-1.13614014240291,
126.017170732911));
#105865=CARTESIAN_POINT('Ctrl Pts',(-126.775055389858,-1.26930832085694,
126.050744387359));
#105866=CARTESIAN_POINT('Ctrl Pts',(-126.782801665942,-1.40083932819723,
126.089826468885));
#105867=CARTESIAN_POINT('Ctrl Pts',(-126.790547999208,-1.53237130647008,
126.128908838907));
#105868=CARTESIAN_POINT('Ctrl Pts',(-126.798294332473,-1.6622657147427,
126.17349960579));
#105869=CARTESIAN_POINT('Ctrl Pts',(-126.806040665739,-1.79003592792838,
126.223426822015));
#105870=CARTESIAN_POINT('Ctrl Pts',(-126.813788733742,-1.91783475436689,
126.273365219093));
#105871=CARTESIAN_POINT('Ctrl Pts',(-126.821536801744,-2.04350807505169,
126.328642301279));
#105872=CARTESIAN_POINT('Ctrl Pts',(-126.829284869747,-2.16658933072317,
126.389038009364));
#105873=CARTESIAN_POINT('Ctrl Pts',(-126.837041172489,-2.28980139861769,
126.449497906727));
#105874=CARTESIAN_POINT('Ctrl Pts',(-126.844797475231,-2.41041554678848,
126.515087124747));
#105875=CARTESIAN_POINT('Ctrl Pts',(-126.852553777973,-2.52798943451812,
126.585539398142));
#105876=CARTESIAN_POINT('Ctrl Pts',(-126.860314220487,-2.64562607497205,
126.656029274037));
#105877=CARTESIAN_POINT('Ctrl Pts',(-126.868074663001,-2.76021889515922,
126.731387162467));
#105878=CARTESIAN_POINT('Ctrl Pts',(-126.875835105515,-2.87135549067515,
126.811304055398));
#105879=CARTESIAN_POINT('Ctrl Pts',(-126.883608005781,-2.98267049252045,
126.891349238021));
#105880=CARTESIAN_POINT('Ctrl Pts',(-126.891380906046,-3.09051787478126,
126.975967808403));
#105881=CARTESIAN_POINT('Ctrl Pts',(-126.899153806312,-3.19451852258594,
127.064810581618));
#105882=CARTESIAN_POINT('Ctrl Pts',(-126.906644142074,-3.29473848488082,
127.150423696246));
#105883=CARTESIAN_POINT('Ctrl Pts',(-126.914134477836,-3.39138630813309,
127.239959015622));
#105884=CARTESIAN_POINT('Ctrl Pts',(-126.921624813598,-3.48415718263795,
127.333073854826));
#105885=CARTESIAN_POINT('Ctrl Pts',(-126.929290870202,-3.57910443169735,
127.428373137885));
#105886=CARTESIAN_POINT('Ctrl Pts',(-126.936956926805,-3.6703093423292,
127.527742271385));
#105887=CARTESIAN_POINT('Ctrl Pts',(-126.944622983409,-3.75739536974699,
127.630851030704));
#105888=CARTESIAN_POINT('Ctrl Pts',(-126.95228006372,-3.84437942691375,
127.733839058531));
#105889=CARTESIAN_POINT('Ctrl Pts',(-126.95993714403,-3.9272539318922,127.840557702724));
#105890=CARTESIAN_POINT('Ctrl Pts',(-126.967594224341,-4.005677710359,127.950638636848));
#105891=CARTESIAN_POINT('Ctrl Pts',(-126.975244107721,-4.08402777790123,
128.060616105319));
#105892=CARTESIAN_POINT('Ctrl Pts',(-126.982893991101,-4.15793520554822,
128.17394925367));
#105893=CARTESIAN_POINT('Ctrl Pts',(-126.990543874482,-4.22709817404826,
128.290235702321));
#105894=CARTESIAN_POINT('Ctrl Pts',(-126.998188004376,-4.29620912499887,
128.406434691797));
#105895=CARTESIAN_POINT('Ctrl Pts',(-127.005832134269,-4.36058251228523,
128.525582216926));
#105896=CARTESIAN_POINT('Ctrl Pts',(-127.013476264163,-4.41995941163802,
128.647246373495));
#105897=CARTESIAN_POINT('Ctrl Pts',(-127.021117058123,-4.47931039863054,
128.76885743525));
#105898=CARTESIAN_POINT('Ctrl Pts',(-127.028757852082,-4.53366905933335,
128.892982582333));
#105899=CARTESIAN_POINT('Ctrl Pts',(-127.036398646042,-4.58282228281413,
129.019165113807));
#105900=CARTESIAN_POINT('Ctrl Pts',(-127.044038713696,-4.63197083396903,
129.14533565083));
#105901=CARTESIAN_POINT('Ctrl Pts',(-127.051678781349,-4.67591478172896,
129.273562809888));
#105902=CARTESIAN_POINT('Ctrl Pts',(-127.059318849003,-4.71448921379823,
129.403370069604));
#105903=CARTESIAN_POINT('Ctrl Pts',(-127.062814467831,-4.7321384699489,
129.462761782042));
#105904=CARTESIAN_POINT('Ctrl Pts',(-127.066310086659,-4.74866434615969,
129.522484032979));
#105905=CARTESIAN_POINT('Ctrl Pts',(-127.069805705487,-4.76405452823416,
129.582490119309));
#105906=CARTESIAN_POINT('Origin',(213.235140564004,0.,130.804360617566));
#105907=CARTESIAN_POINT('',(-129.165390467031,-4.76405452823393,129.582490119308));
#105908=CARTESIAN_POINT('',(-128.819767501811,-4.76405452823396,129.582490119308));
#105909=CARTESIAN_POINT('',(213.235140564004,-4.76405452823405,129.582490119308));
#105910=CARTESIAN_POINT('',(-127.485140564048,-4.91824927169589,130.801684059538));
#105911=CARTESIAN_POINT('Ctrl Pts',(-127.485140564048,-4.91824927169589,
130.801684059538));
#105912=CARTESIAN_POINT('Ctrl Pts',(-127.492816800484,-4.91832267662926,
130.936567651182));
#105913=CARTESIAN_POINT('Ctrl Pts',(-127.500493036919,-4.91284309997266,
131.071676197592));
#105914=CARTESIAN_POINT('Ctrl Pts',(-127.508169273355,-4.90178139325122,
131.206507649479));
#105915=CARTESIAN_POINT('Ctrl Pts',(-127.515836812447,-4.89073221968645,
131.341186334369));
#105916=CARTESIAN_POINT('Ctrl Pts',(-127.523504351538,-4.87411352755219,
131.475588152765));
#105917=CARTESIAN_POINT('Ctrl Pts',(-127.531171890629,-4.85194816724617,
131.609209699603));
#105918=CARTESIAN_POINT('Ctrl Pts',(-127.538832684027,-4.82980230742348,
131.742713689826));
#105919=CARTESIAN_POINT('Ctrl Pts',(-127.546493477426,-4.80211955205956,
131.875438380367));
#105920=CARTESIAN_POINT('Ctrl Pts',(-127.554154270824,-4.76897463277987,
132.006884635789));
#105921=CARTESIAN_POINT('Ctrl Pts',(-127.561810653954,-4.73584879481185,
132.138255218467));
#105922=CARTESIAN_POINT('Ctrl Pts',(-127.569467037084,-4.69726714482858,
132.268348441846));
#105923=CARTESIAN_POINT('Ctrl Pts',(-127.577123420214,-4.65335557905117,
132.396674945019));
#105924=CARTESIAN_POINT('Ctrl Pts',(-127.58477752692,-4.60945706921822,
132.524963293696));
#105925=CARTESIAN_POINT('Ctrl Pts',(-127.592431633627,-4.56023192387332,
132.651485587176));
#105926=CARTESIAN_POINT('Ctrl Pts',(-127.600085740334,-4.50585588773273,
132.775767673829));
#105927=CARTESIAN_POINT('Ctrl Pts',(-127.607739324453,-4.45148356414024,
132.900041275068));
#105928=CARTESIAN_POINT('Ctrl Pts',(-127.615392908572,-4.39196120994408,
133.022074605982));
#105929=CARTESIAN_POINT('Ctrl Pts',(-127.623046492691,-4.32751248485484,
133.141414052112));
#105930=CARTESIAN_POINT('Ctrl Pts',(-127.63070130741,-4.26305339721827,
133.260772686531));
#105931=CARTESIAN_POINT('Ctrl Pts',(-127.63835612213,-4.19366655447161,
133.377436221861));
#105932=CARTESIAN_POINT('Ctrl Pts',(-127.646010936849,-4.11962101464151,
133.490976659769));
#105933=CARTESIAN_POINT('Ctrl Pts',(-127.653673447881,-4.04550102786041,
133.604631253635));
#105934=CARTESIAN_POINT('Ctrl Pts',(-127.661335958913,-3.96671320802992,
133.7151561416));
#105935=CARTESIAN_POINT('Ctrl Pts',(-127.668998469945,-3.88356953119964,
133.822152982663));
#105936=CARTESIAN_POINT('Ctrl Pts',(-127.676664811165,-3.80038429411459,
133.92920330724));
#105937=CARTESIAN_POINT('Ctrl Pts',(-127.684331152385,-3.71283912305295,
134.032721766762));
#105938=CARTESIAN_POINT('Ctrl Pts',(-127.691997493605,-3.62128471047743,
134.13234500878));
#105939=CARTESIAN_POINT('Ctrl Pts',(-127.6996760532,-3.52958438134226,134.232127027205));
#105940=CARTESIAN_POINT('Ctrl Pts',(-127.707354612795,-3.4338623282698,
134.328001141216));
#105941=CARTESIAN_POINT('Ctrl Pts',(-127.71503317239,-3.33450488740009,
134.419642102929));
#105942=CARTESIAN_POINT('Ctrl Pts',(-127.722481677886,-3.23812425308863,
134.508537448274));
#105943=CARTESIAN_POINT('Ctrl Pts',(-127.729930183381,-3.13832324827053,
134.593449509662));
#105944=CARTESIAN_POINT('Ctrl Pts',(-127.737378688877,-3.03548065620261,
134.674120332112));
#105945=CARTESIAN_POINT('Ctrl Pts',(-127.745153022996,-2.92813930123221,
134.758320032005));
#105946=CARTESIAN_POINT('Ctrl Pts',(-127.752927357115,-2.81712190934436,
134.838183480158));
#105947=CARTESIAN_POINT('Ctrl Pts',(-127.760701691234,-2.70281408189493,
134.913372554907));
#105948=CARTESIAN_POINT('Ctrl Pts',(-127.768466444181,-2.58864712862715,
134.988468965841));
#105949=CARTESIAN_POINT('Ctrl Pts',(-127.776231197129,-2.47119813187394,
135.058902252749));
#105950=CARTESIAN_POINT('Ctrl Pts',(-127.783995950076,-2.35088576258619,
135.124374413119));
#105951=CARTESIAN_POINT('Ctrl Pts',(-127.791752990961,-2.23069288924006,
135.189781545616));
#105952=CARTESIAN_POINT('Ctrl Pts',(-127.799510031846,-2.10764264411985,
135.250237171774));
#105953=CARTESIAN_POINT('Ctrl Pts',(-127.807267072731,-1.98218238323482,
135.30548670579));
#105954=CARTESIAN_POINT('Ctrl Pts',(-127.815018263971,-1.85681673290829,
135.360694575703));
#105955=CARTESIAN_POINT('Ctrl Pts',(-127.822769455211,-1.72904504062368,
135.410704010917));
#105956=CARTESIAN_POINT('Ctrl Pts',(-127.830520646451,-1.59933863350574,
135.455306650136));
#105957=CARTESIAN_POINT('Ctrl Pts',(-127.838268543228,-1.46968735507068,
135.499890332043));
#105958=CARTESIAN_POINT('Ctrl Pts',(-127.846016440005,-1.33810336624751,
135.539071661697));
#105959=CARTESIAN_POINT('Ctrl Pts',(-127.853764336782,-1.20507711018253,
135.572690746764));
#105960=CARTESIAN_POINT('Ctrl Pts',(-127.861510612866,-1.07207868034261,
135.606302799442));
#105961=CARTESIAN_POINT('Ctrl Pts',(-127.869256888951,-0.937638962148778,
135.634354826067));
#105962=CARTESIAN_POINT('Ctrl Pts',(-127.877003165035,-0.802262282934139,
135.656737178786));
#105963=CARTESIAN_POINT('Ctrl Pts',(-127.8847494983,-0.666884604399793,
135.679119696728));
#105964=CARTESIAN_POINT('Ctrl Pts',(-127.892495831565,-0.530570336772146,
135.695832393477));
#105965=CARTESIAN_POINT('Ctrl Pts',(-127.900242164831,-0.393832297560471,
135.706817061421));
#105966=CARTESIAN_POINT('Ctrl Pts',(-127.907990232834,-0.257063636812804,
135.717804189306));
#105967=CARTESIAN_POINT('Ctrl Pts',(-127.915738300837,-0.11987140527484,
135.723060704555));
#105968=CARTESIAN_POINT('Ctrl Pts',(-127.92348636884,0.0172285815978464,
135.722580441697));
#105969=CARTESIAN_POINT('Ctrl Pts',(-127.931242671582,0.154474279967905,
135.72209966841));
#105970=CARTESIAN_POINT('Ctrl Pts',(-127.938998974323,0.291627146243551,
135.71586993874));
#105971=CARTESIAN_POINT('Ctrl Pts',(-127.946755277065,0.428172934941949,
135.703937231957));
#105972=CARTESIAN_POINT('Ctrl Pts',(-127.95451571958,0.564791602239091,
135.691998156329));
#105973=CARTESIAN_POINT('Ctrl Pts',(-127.962276162094,0.70080215880525,
135.674350088741));
#105974=CARTESIAN_POINT('Ctrl Pts',(-127.970036604608,0.835698585771106,
135.651090539507));
#105975=CARTESIAN_POINT('Ctrl Pts',(-127.977809504873,0.97081156045707,
135.62779365198));
#105976=CARTESIAN_POINT('Ctrl Pts',(-127.985582405139,1.10480644916865,
135.598867364404));
#105977=CARTESIAN_POINT('Ctrl Pts',(-127.993355305404,1.23718959737333,
135.564459877314));
#105978=CARTESIAN_POINT('Ctrl Pts',(-128.000845641166,1.36476028468559,
135.531303189047));
#105979=CARTESIAN_POINT('Ctrl Pts',(-128.008335976928,1.49083408394592,
135.49305698277));
#105980=CARTESIAN_POINT('Ctrl Pts',(-128.01582631269,1.61498700471631,135.449896112759));
#105981=CARTESIAN_POINT('Ctrl Pts',(-128.023600646809,1.74384722121518,
135.405098785242));
#105982=CARTESIAN_POINT('Ctrl Pts',(-128.031374980928,1.87104621406241,
135.354864853771));
#105983=CARTESIAN_POINT('Ctrl Pts',(-128.039149315047,1.99609108497388,
135.299335972669));
#105984=CARTESIAN_POINT('Ctrl Pts',(-128.046914067994,2.12098184925719,
135.243875525951));
#105985=CARTESIAN_POINT('Ctrl Pts',(-128.054678820941,2.24372341990366,
135.183133270658));
#105986=CARTESIAN_POINT('Ctrl Pts',(-128.062443573888,2.36383877708325,
135.117300368879));
#105987=CARTESIAN_POINT('Ctrl Pts',(-128.070200614773,2.48383483399644,
135.051532853267));
#105988=CARTESIAN_POINT('Ctrl Pts',(-128.077957655658,2.60120952763215,
134.980684939733));
#105989=CARTESIAN_POINT('Ctrl Pts',(-128.085714696543,2.71550686089337,
134.904995391713));
#105990=CARTESIAN_POINT('Ctrl Pts',(-128.093465887783,2.82971800164694,
134.829362921769));
#105991=CARTESIAN_POINT('Ctrl Pts',(-128.101217079024,2.94085607651002,
134.748896299649));
#105992=CARTESIAN_POINT('Ctrl Pts',(-128.108968270264,3.04849102139965,
134.663879441843));
#105993=CARTESIAN_POINT('Ctrl Pts',(-128.116716167041,3.1560802185666,134.578898718469));
#105994=CARTESIAN_POINT('Ctrl Pts',(-128.124464063818,3.26016894095434,
134.489371847755));
#105995=CARTESIAN_POINT('Ctrl Pts',(-128.132211960595,3.36035757011268,
134.395625027699));
#105996=CARTESIAN_POINT('Ctrl Pts',(-128.139958236679,3.46052524196961,
134.301897817456));
#105997=CARTESIAN_POINT('Ctrl Pts',(-128.147704512763,3.55679415800012,
134.203952680609));
#105998=CARTESIAN_POINT('Ctrl Pts',(-128.155450788847,3.6487994671194,134.102154654684));
#105999=CARTESIAN_POINT('Ctrl Pts',(-128.163197122113,3.74080545540084,
134.000355877309));
#106000=CARTESIAN_POINT('Ctrl Pts',(-128.170943455378,3.8285475118183,133.894704444157));
#106001=CARTESIAN_POINT('Ctrl Pts',(-128.178689788643,3.91169947426812,
133.785600340485));
#106002=CARTESIAN_POINT('Ctrl Pts',(-128.186437856646,3.99487005802305,
133.676471803706));
#106003=CARTESIAN_POINT('Ctrl Pts',(-128.194185924649,4.07344826542758,
133.563889368719));
#106004=CARTESIAN_POINT('Ctrl Pts',(-128.201933992652,4.147150098441,133.448283673084));
#106005=CARTESIAN_POINT('Ctrl Pts',(-128.209690295394,4.22093026263992,
133.33255511034));
#106006=CARTESIAN_POINT('Ctrl Pts',(-128.217446598136,4.28982348900082,
133.213797198516));
#106007=CARTESIAN_POINT('Ctrl Pts',(-128.225202900878,4.3535904989405,133.092467439818));
#106008=CARTESIAN_POINT('Ctrl Pts',(-128.232963343392,4.41739154325355,
132.971072923774));
#106009=CARTESIAN_POINT('Ctrl Pts',(-128.240723785906,4.47606075223969,
132.847104178907));
#106010=CARTESIAN_POINT('Ctrl Pts',(-128.24848422842,4.52940664852883,132.721039639928));
#106011=CARTESIAN_POINT('Ctrl Pts',(-128.256257128686,4.58283818038637,
132.59477273096));
#106012=CARTESIAN_POINT('Ctrl Pts',(-128.264030028951,4.63092918576915,
132.466403671156));
#106013=CARTESIAN_POINT('Ctrl Pts',(-128.271802929216,4.67353751765295,
132.336427892065));
#106014=CARTESIAN_POINT('Ctrl Pts',(-128.279293264978,4.71459692935002,
132.211177059929));
#106015=CARTESIAN_POINT('Ctrl Pts',(-128.286783600741,4.75056528084611,
132.084434593302));
#106016=CARTESIAN_POINT('Ctrl Pts',(-128.294273936503,4.78136050480752,
131.956651720355));
#106017=CARTESIAN_POINT('Ctrl Pts',(-128.302048270622,4.81332333904467,
131.824023920945));
#106018=CARTESIAN_POINT('Ctrl Pts',(-128.309822604741,4.83981427244164,
131.689855138807));
#106019=CARTESIAN_POINT('Ctrl Pts',(-128.31759693886,4.86068605922972,131.55463663085));
#106020=CARTESIAN_POINT('Ctrl Pts',(-128.325361691807,4.88153212340584,
131.419584767621));
#106021=CARTESIAN_POINT('Ctrl Pts',(-128.333126444754,4.89677276078116,
131.283486135315));
#106022=CARTESIAN_POINT('Ctrl Pts',(-128.340891197702,4.9063109605666,131.146845392007));
#106023=CARTESIAN_POINT('Ctrl Pts',(-128.348648238587,4.9158396868776,131.010340362211));
#106024=CARTESIAN_POINT('Ctrl Pts',(-128.356405279472,4.91967721965075,
130.873294680408));
#106025=CARTESIAN_POINT('Ctrl Pts',(-128.364162320357,4.91777795975678,
130.736221047341));
#106026=CARTESIAN_POINT('Ctrl Pts',(-128.371913511597,4.91588013210946,
130.599250782566));
#106027=CARTESIAN_POINT('Ctrl Pts',(-128.379664702837,4.90825412814875,
130.462252997827));
#106028=CARTESIAN_POINT('Ctrl Pts',(-128.387415894077,4.89490635471592,
130.325742982014));
#106029=CARTESIAN_POINT('Ctrl Pts',(-128.395163790854,4.88156425444292,
130.189290986599));
#106030=CARTESIAN_POINT('Ctrl Pts',(-128.402911687631,4.86250525953779,
130.053326736073));
#106031=CARTESIAN_POINT('Ctrl Pts',(-128.410659584408,4.8377878060797,129.918362758739));
#106032=CARTESIAN_POINT('Ctrl Pts',(-128.418405860492,4.81307552298004,
129.783427012959));
#106033=CARTESIAN_POINT('Ctrl Pts',(-128.426152136577,4.78270720601328,
129.649491508516));
#106034=CARTESIAN_POINT('Ctrl Pts',(-128.433898412661,4.74679276066588,
129.517060516661));
#106035=CARTESIAN_POINT('Ctrl Pts',(-128.441644745926,4.71087805020616,
129.38462854723));
#106036=CARTESIAN_POINT('Ctrl Pts',(-128.449391079191,4.66941723200348,
129.253701489883));
#106037=CARTESIAN_POINT('Ctrl Pts',(-128.457137412457,4.62257052639916,
129.124769955837));
#106038=CARTESIAN_POINT('Ctrl Pts',(-128.46488548046,4.57571332979974,128.995809548468));
#106039=CARTESIAN_POINT('Ctrl Pts',(-128.472633548463,4.52346797922504,
128.868845921037));
#106040=CARTESIAN_POINT('Ctrl Pts',(-128.480381616466,4.46604327437459,
128.744350779261));
#106041=CARTESIAN_POINT('Ctrl Pts',(-128.488137919208,4.40855753786471,
128.619723322567));
#106042=CARTESIAN_POINT('Ctrl Pts',(-128.495894221949,4.34588161490612,
128.497569947907));
#106043=CARTESIAN_POINT('Ctrl Pts',(-128.503650524691,4.27827107914381,
128.378339258249));
#106044=CARTESIAN_POINT('Ctrl Pts',(-128.511410967205,4.21062445760285,
128.259044931582));
#106045=CARTESIAN_POINT('Ctrl Pts',(-128.51917140972,4.1380381821004,128.142676729758));
#106046=CARTESIAN_POINT('Ctrl Pts',(-128.526931852234,4.0608112751145,128.02965435376));
#106047=CARTESIAN_POINT('Ctrl Pts',(-128.534704752499,3.98346039664162,
127.916450544211));
#106048=CARTESIAN_POINT('Ctrl Pts',(-128.542477652765,3.90145423412465,
127.806603606962));
#106049=CARTESIAN_POINT('Ctrl Pts',(-128.55025055303,3.81513277421867,127.700500927183));
#106050=CARTESIAN_POINT('Ctrl Pts',(-128.557740888792,3.73194931681184,
127.598255347073));
#106051=CARTESIAN_POINT('Ctrl Pts',(-128.565231224554,3.64475906266799,
127.499486755217));
#106052=CARTESIAN_POINT('Ctrl Pts',(-128.572721560316,3.5538972834282,127.404508097038));
#106053=CARTESIAN_POINT('Ctrl Pts',(-128.580495894435,3.4595904522105,127.305928294164));
#106054=CARTESIAN_POINT('Ctrl Pts',(-128.588270228554,3.36102945251901,
127.211119217635));
#106055=CARTESIAN_POINT('Ctrl Pts',(-128.596044562673,3.25854800276854,
127.120470285844));
#106056=CARTESIAN_POINT('Ctrl Pts',(-128.60380931562,3.15619285224613,127.029933070761));
#106057=CARTESIAN_POINT('Ctrl Pts',(-128.611574068567,3.04992715514856,
126.943546055744));
#106058=CARTESIAN_POINT('Ctrl Pts',(-128.619338821514,2.94012305790365,
126.861663638735));
#106059=CARTESIAN_POINT('Ctrl Pts',(-128.627095862399,2.83042801963579,
126.779862548496));
#106060=CARTESIAN_POINT('Ctrl Pts',(-128.634852903284,2.71720188640079,
126.702557384949));
#106061=CARTESIAN_POINT('Ctrl Pts',(-128.642609944169,2.60085136040926,
126.630063639205));
#106062=CARTESIAN_POINT('Ctrl Pts',(-128.650361135409,2.48458857525494,
126.557624561558));
#106063=CARTESIAN_POINT('Ctrl Pts',(-128.65811232665,2.36520641755945,126.489989885662));
#106064=CARTESIAN_POINT('Ctrl Pts',(-128.66586351789,2.24314187751414,126.427432747491));
#106065=CARTESIAN_POINT('Ctrl Pts',(-128.673611414667,2.12112921815404,
126.364902197771));
#106066=CARTESIAN_POINT('Ctrl Pts',(-128.681359311444,1.99643679118995,
126.307445071443));
#106067=CARTESIAN_POINT('Ctrl Pts',(-128.689107208221,1.86952738732846,
126.255289238644));
#106068=CARTESIAN_POINT('Ctrl Pts',(-128.696853484305,1.74264453017841,
126.203144315721));
#106069=CARTESIAN_POINT('Ctrl Pts',(-128.704599760389,1.61354597993184,
126.156298629153));
#106070=CARTESIAN_POINT('Ctrl Pts',(-128.712346036473,1.48271540087359,
126.114932283269));
#106071=CARTESIAN_POINT('Ctrl Pts',(-128.720092369739,1.35188385605355,
126.073565632027));
#106072=CARTESIAN_POINT('Ctrl Pts',(-128.727838703004,1.21932062968495,
126.037678520046));
#106073=CARTESIAN_POINT('Ctrl Pts',(-128.735585036269,1.0855250898876,126.007401336759));
#106074=CARTESIAN_POINT('Ctrl Pts',(-128.743333104272,0.951699587506616,
125.977117373106));
#106075=CARTESIAN_POINT('Ctrl Pts',(-128.751081172275,0.816641603802916,
125.952445924325));
#106076=CARTESIAN_POINT('Ctrl Pts',(-128.758829240278,0.680860859492816,
125.933466289775));
#106077=CARTESIAN_POINT('Ctrl Pts',(-128.76658554302,0.544935805792407,
125.914466483443));
#106078=CARTESIAN_POINT('Ctrl Pts',(-128.774341845762,0.408286844824283,
125.901170629737));
#106079=CARTESIAN_POINT('Ctrl Pts',(-128.782098148504,0.271429542767353,
125.893606188172));
#106080=CARTESIAN_POINT('Ctrl Pts',(-128.789858591018,0.134499195847249,
125.886037709237));
#106081=CARTESIAN_POINT('Ctrl Pts',(-128.797619033532,-0.00263932299382713,
125.88420674303));
#106082=CARTESIAN_POINT('Ctrl Pts',(-128.805379476046,-0.139471278478966,
125.888088572105));
#106083=CARTESIAN_POINT('Ctrl Pts',(-128.813152376312,-0.276522888766048,
125.891976632637));
#106084=CARTESIAN_POINT('Ctrl Pts',(-128.820925276577,-0.413266562053272,
125.901595786954));
#106085=CARTESIAN_POINT('Ctrl Pts',(-128.828698176843,-0.549192609133013,
125.916869385802));
#106086=CARTESIAN_POINT('Ctrl Pts',(-128.836188512605,-0.680177402022141,
125.931587750859));
#106087=CARTESIAN_POINT('Ctrl Pts',(-128.843678848366,-0.810402677726295,
125.951556544572));
#106088=CARTESIAN_POINT('Ctrl Pts',(-128.851169184128,-0.939423923888862,
125.976662848057));
#106089=CARTESIAN_POINT('Ctrl Pts',(-128.858943518247,-1.07333704981692,
126.00272106467));
#106090=CARTESIAN_POINT('Ctrl Pts',(-128.866717852367,-1.20637723885266,
126.034396603398));
#106091=CARTESIAN_POINT('Ctrl Pts',(-128.874492186486,-1.33803647931793,
126.071619187642));
#106092=CARTESIAN_POINT('Ctrl Pts',(-128.882256939433,-1.46953346153604,
126.108795898378));
#106093=CARTESIAN_POINT('Ctrl Pts',(-128.89002169238,-1.5996525088419,126.151505947211));
#106094=CARTESIAN_POINT('Ctrl Pts',(-128.897786445327,-1.72789430197759,
126.199627797554));
#106095=CARTESIAN_POINT('Ctrl Pts',(-128.905543486212,-1.85600872355644,
126.247701852597));
#106096=CARTESIAN_POINT('Ctrl Pts',(-128.913300527097,-1.98224923776051,
126.301176876037));
#106097=CARTESIAN_POINT('Ctrl Pts',(-128.921057567982,-2.10613058050234,
126.359881228439));
#106098=CARTESIAN_POINT('Ctrl Pts',(-128.928808759222,-2.2299185033608,
126.418541311433));
#106099=CARTESIAN_POINT('Ctrl Pts',(-128.936559950462,-2.3513504440127,
126.48242270739));
#106100=CARTESIAN_POINT('Ctrl Pts',(-128.944311141702,-2.46996040155432,
126.551305400754));
#106101=CARTESIAN_POINT('Ctrl Pts',(-128.952059038479,-2.58851994669915,
126.620158817135));
#106102=CARTESIAN_POINT('Ctrl Pts',(-128.959806935257,-2.70425955690565,
126.694009107164));
#106103=CARTESIAN_POINT('Ctrl Pts',(-128.967554832034,-2.8167373688906,
126.772590081289));
#106104=CARTESIAN_POINT('Ctrl Pts',(-128.975301108118,-2.92919165294203,
126.851154617968));
#106105=CARTESIAN_POINT('Ctrl Pts',(-128.983047384202,-3.03838517560633,
126.934447646691));
#106106=CARTESIAN_POINT('Ctrl Pts',(-128.990793660286,-3.14390497764968,
127.022159597788));
#106107=CARTESIAN_POINT('Ctrl Pts',(-128.998539993551,-3.24942555861639,
127.109872196355));
#106108=CARTESIAN_POINT('Ctrl Pts',(-129.006286326817,-3.35127206419146,
127.202003532466));
#106109=CARTESIAN_POINT('Ctrl Pts',(-129.014032660082,-3.4490648733832,
127.298203952257));
#106110=CARTESIAN_POINT('Ctrl Pts',(-129.021780728085,-3.5468795825961,
127.394425915463));
#106111=CARTESIAN_POINT('Ctrl Pts',(-129.029528796088,-3.64063851035369,
127.494718501493));
#106112=CARTESIAN_POINT('Ctrl Pts',(-129.037276864091,-3.72999942335993,
127.598695731113));
#106113=CARTESIAN_POINT('Ctrl Pts',(-129.045033166833,-3.81945531020804,
127.702783468971));
#106114=CARTESIAN_POINT('Ctrl Pts',(-129.052789469575,-3.90450358972869,
127.810563376235));
#106115=CARTESIAN_POINT('Ctrl Pts',(-129.060545772316,-3.98484248334066,
127.921616535018));
#106116=CARTESIAN_POINT('Ctrl Pts',(-129.068306214831,-4.0652242562391,
128.032728966216));
#106117=CARTESIAN_POINT('Ctrl Pts',(-129.076066657345,-4.14089141919241,
128.147117804122));
#106118=CARTESIAN_POINT('Ctrl Pts',(-129.083827099859,-4.21158654069804,
128.264336626988));
#106119=CARTESIAN_POINT('Ctrl Pts',(-129.091600000125,-4.28239514828893,
128.381743619915));
#106120=CARTESIAN_POINT('Ctrl Pts',(-129.09937290039,-4.34821557689528,
128.501989332903));
#106121=CARTESIAN_POINT('Ctrl Pts',(-129.107145800655,-4.40883681423906,
128.624603519192));
#106122=CARTESIAN_POINT('Ctrl Pts',(-129.114636136417,-4.46725431690987,
128.742760370964));
#106123=CARTESIAN_POINT('Ctrl Pts',(-129.12212647218,-4.52084394766207,
128.863116204355));
#106124=CARTESIAN_POINT('Ctrl Pts',(-129.129616807942,-4.56946043856356,
128.985236003115));
#106125=CARTESIAN_POINT('Ctrl Pts',(-129.13840322465,-4.62648922359083,
129.128486649591));
#106126=CARTESIAN_POINT('Ctrl Pts',(-129.147189641358,-4.67682727565074,
129.274545048183));
#106127=CARTESIAN_POINT('Ctrl Pts',(-129.155976058067,-4.72022285708224,
129.422811037573));
#106128=CARTESIAN_POINT('Ctrl Pts',(-129.159114194388,-4.73572192283395,
129.475765376298));
#106129=CARTESIAN_POINT('Ctrl Pts',(-129.16225233071,-4.75033582251471,
129.529001093919));
#106130=CARTESIAN_POINT('Ctrl Pts',(-129.165390467031,-4.76405452823393,
129.582490119308));
#106131=CARTESIAN_POINT('Ctrl Pts',(-127.415055402248,-4.76405452823392,
129.582490119308));
#106132=CARTESIAN_POINT('Ctrl Pts',(-127.422828522679,-4.79811179187028,
129.715278873335));
#106133=CARTESIAN_POINT('Ctrl Pts',(-127.43060164311,-4.82657620982016,
129.849348992912));
#106134=CARTESIAN_POINT('Ctrl Pts',(-127.438374763542,-4.84938165098749,
129.984189497881));
#106135=CARTESIAN_POINT('Ctrl Pts',(-127.445226864049,-4.869484925649,130.103053048338));
#106136=CARTESIAN_POINT('Ctrl Pts',(-127.452078964557,-4.88519157307536,
130.222514965625));
#106137=CARTESIAN_POINT('Ctrl Pts',(-127.458931065065,-4.89648988555254,
130.342224422076));
#106138=CARTESIAN_POINT('Ctrl Pts',(-127.467667564714,-4.91089535185762,
130.494855228206));
#106139=CARTESIAN_POINT('Ctrl Pts',(-127.476404064362,-4.91816572784717,
130.648169968883));
#106140=CARTESIAN_POINT('Ctrl Pts',(-127.48514056401,-4.91824927169553,
130.801684058878));
#106141=CARTESIAN_POINT('',(-127.139859435937,-4.91824794762588,130.808853742736));
#106142=CARTESIAN_POINT('Ctrl Pts',(-127.069805705487,-4.76405452823416,
129.582490119309));
#106143=CARTESIAN_POINT('Ctrl Pts',(-127.077448630367,-4.79770407965101,
129.71368920958));
#106144=CARTESIAN_POINT('Ctrl Pts',(-127.085091555248,-4.82592107650535,
129.846245715456));
#106145=CARTESIAN_POINT('Ctrl Pts',(-127.092734480128,-4.84861404133926,
129.979663739539));
#106146=CARTESIAN_POINT('Ctrl Pts',(-127.10058863943,-4.87193419214756,
130.116769158109));
#106147=CARTESIAN_POINT('Ctrl Pts',(-127.108442798731,-4.88942045119155,
130.254783960365));
#106148=CARTESIAN_POINT('Ctrl Pts',(-127.116296958033,-4.90103053263342,
130.39316385117));
#106149=CARTESIAN_POINT('Ctrl Pts',(-127.124151117334,-4.91264061407527,
130.531543741973));
#106150=CARTESIAN_POINT('Ctrl Pts',(-127.132005276636,-4.91837453580464,
130.67028826175));
#106151=CARTESIAN_POINT('Ctrl Pts',(-127.139859435937,-4.91824794762588,
130.808853742736));
#106152=CARTESIAN_POINT('Ctrl Pts',(-127.139859435993,-4.91824794762498,
130.808853743724));
#106153=CARTESIAN_POINT('Ctrl Pts',(-127.150602464173,-4.9180747985178,
130.998385533179));
#106154=CARTESIAN_POINT('Ctrl Pts',(-127.161345492353,-4.90694239374391,
131.187437242374));
#106155=CARTESIAN_POINT('Ctrl Pts',(-127.172088520534,-4.88503717887384,
131.374969786367));
#106156=CARTESIAN_POINT('Ctrl Pts',(-127.181416492826,-4.86601728672331,
131.537800819189));
#106157=CARTESIAN_POINT('Ctrl Pts',(-127.190744465118,-4.83887641295327,
131.699487419958));
#106158=CARTESIAN_POINT('Ctrl Pts',(-127.200072437411,-4.80376392792892,
131.859365445626));
#106159=CARTESIAN_POINT('Ctrl Pts',(-127.20784677153,-4.77449966965511,
131.992614682534));
#106160=CARTESIAN_POINT('Ctrl Pts',(-127.215621105649,-4.73964065499407,
132.124856433692));
#106161=CARTESIAN_POINT('Ctrl Pts',(-127.223395439768,-4.69926933118736,
132.255584520161));
#106162=CARTESIAN_POINT('Ctrl Pts',(-127.231160192715,-4.65894776142927,
132.386151495946));
#106163=CARTESIAN_POINT('Ctrl Pts',(-127.238924945662,-4.6131275136775,
132.515208148773));
#106164=CARTESIAN_POINT('Ctrl Pts',(-127.246689698609,-4.56194207180448,
132.642258219719));
#106165=CARTESIAN_POINT('Ctrl Pts',(-127.254446739494,-4.51080746803392,
132.769182102743));
#106166=CARTESIAN_POINT('Ctrl Pts',(-127.262203780379,-4.45431841982171,
132.894103009682));
#106167=CARTESIAN_POINT('Ctrl Pts',(-127.269960821264,-4.39265816217544,
133.016539935066));
#106168=CARTESIAN_POINT('Ctrl Pts',(-127.277712012504,-4.33104440300919,
133.138884529811));
#106169=CARTESIAN_POINT('Ctrl Pts',(-127.285463203744,-4.26426737156493,
133.258748523701));
#106170=CARTESIAN_POINT('Ctrl Pts',(-127.293214394985,-4.19255820277847,
133.375671329793));
#106171=CARTESIAN_POINT('Ctrl Pts',(-127.300962291762,-4.12087951230154,
133.492544440575));
#106172=CARTESIAN_POINT('Ctrl Pts',(-127.308710188539,-4.04427305781589,
133.6064785173));
#106173=CARTESIAN_POINT('Ctrl Pts',(-127.316458085316,-3.96301555571786,
133.717038211746));
#106174=CARTESIAN_POINT('Ctrl Pts',(-127.3242043614,-3.88177505093734,133.827574779488));
#106175=CARTESIAN_POINT('Ctrl Pts',(-127.331950637484,-3.79588566508369,
133.93473805409));
#106176=CARTESIAN_POINT('Ctrl Pts',(-127.339696913568,-3.70566678856273,
134.03812262406));
#106177=CARTESIAN_POINT('Ctrl Pts',(-127.347443246834,-3.61544724606663,
134.141507957191));
#106178=CARTESIAN_POINT('Ctrl Pts',(-127.355189580099,-3.52089840619136,
134.241114235455));
#106179=CARTESIAN_POINT('Ctrl Pts',(-127.362935913364,-3.42237893196932,
134.336570337913));
#106180=CARTESIAN_POINT('Ctrl Pts',(-127.370683981367,-3.32383739499426,
134.432047817102));
#106181=CARTESIAN_POINT('Ctrl Pts',(-127.37843204937,-3.22132373500662,
134.523372999078));
#106182=CARTESIAN_POINT('Ctrl Pts',(-127.386180117373,-3.11523203274245,
134.610213011534));
#106183=CARTESIAN_POINT('Ctrl Pts',(-127.393936420115,-3.00902757495447,
134.69714531859));
#106184=CARTESIAN_POINT('Ctrl Pts',(-127.401692722857,-2.89923778143554,
134.779582685715));
#106185=CARTESIAN_POINT('Ctrl Pts',(-127.409449025599,-2.78628869129055,
134.857233474107));
#106186=CARTESIAN_POINT('Ctrl Pts',(-127.417209468113,-2.67327931681531,
134.934925707063));
#106187=CARTESIAN_POINT('Ctrl Pts',(-127.424969910627,-2.55710761679417,
135.007826063037));
#106188=CARTESIAN_POINT('Ctrl Pts',(-127.432730353141,-2.43822606206505,
135.075687897554));
#106189=CARTESIAN_POINT('Ctrl Pts',(-127.440503253407,-2.31915366811048,
135.143658669911));
#106190=CARTESIAN_POINT('Ctrl Pts',(-127.448276153672,-2.19736307411755,
135.206574578302));
#106191=CARTESIAN_POINT('Ctrl Pts',(-127.456049053938,-2.07332945513943,
135.264235955841));
#106192=CARTESIAN_POINT('Ctrl Pts',(-127.4635393897,-1.95380477063333,135.319801197065));
#106193=CARTESIAN_POINT('Ctrl Pts',(-127.471029725462,-1.83219759337493,
135.370487187184));
#106194=CARTESIAN_POINT('Ctrl Pts',(-127.478520061224,-1.7089463003696,
135.416159139288));
#106195=CARTESIAN_POINT('Ctrl Pts',(-127.486294395343,-1.58102189712837,
135.463562757337));
#106196=CARTESIAN_POINT('Ctrl Pts',(-127.494068729462,-1.45092101769544,
135.50571477773));
#106197=CARTESIAN_POINT('Ctrl Pts',(-127.501843063581,-1.31911408949564,
135.542410963583));
#106198=CARTESIAN_POINT('Ctrl Pts',(-127.509607816528,-1.18746960155492,
135.579061924667));
#106199=CARTESIAN_POINT('Ctrl Pts',(-127.517372569475,-1.05412362132532,
135.610270325774));
#106200=CARTESIAN_POINT('Ctrl Pts',(-127.525137322422,-0.919565816787381,
135.635880230596));
#106201=CARTESIAN_POINT('Ctrl Pts',(-127.532894363307,-0.785141656957844,
135.6614646993));
#106202=CARTESIAN_POINT('Ctrl Pts',(-127.540651404192,-0.649508449625715,
135.681461664749));
#106203=CARTESIAN_POINT('Ctrl Pts',(-127.548408445077,-0.513169921313215,
135.69576529254));
#106204=CARTESIAN_POINT('Ctrl Pts',(-127.556159636317,-0.376934206945661,
135.710058133854));
#106205=CARTESIAN_POINT('Ctrl Pts',(-127.563910827557,-0.239994617546514,
135.718666142614));
#106206=CARTESIAN_POINT('Ctrl Pts',(-127.571662018797,-0.102863592031699,
135.721534820697));
#106207=CARTESIAN_POINT('Ctrl Pts',(-127.579409915575,0.0342091491393702,
135.724402279514));
#106208=CARTESIAN_POINT('Ctrl Pts',(-127.587157812352,0.171472774535073,
135.721535251213));
#106209=CARTESIAN_POINT('Ctrl Pts',(-127.594905709129,0.308411441394956,
135.712931228784));
#106210=CARTESIAN_POINT('Ctrl Pts',(-127.602651985213,0.445321463637787,
135.704329006132));
#106211=CARTESIAN_POINT('Ctrl Pts',(-127.610398261297,0.581906272600894,
135.689992200831));
#106212=CARTESIAN_POINT('Ctrl Pts',(-127.618144537381,0.717652145797315,
135.66997039026));
#106213=CARTESIAN_POINT('Ctrl Pts',(-127.625890870646,0.853399021038751,
135.649948431892));
#106214=CARTESIAN_POINT('Ctrl Pts',(-127.633637203911,0.988306561375466,
135.624241441564));
#106215=CARTESIAN_POINT('Ctrl Pts',(-127.641383537177,1.12186866611881,
135.592950572707));
#106216=CARTESIAN_POINT('Ctrl Pts',(-127.64913160518,1.25546068116927,135.561652696478));
#106217=CARTESIAN_POINT('Ctrl Pts',(-127.656879673183,1.38770628048699,
135.524768542592));
#106218=CARTESIAN_POINT('Ctrl Pts',(-127.664627741186,1.51811239891141,
135.482449736723));
#106219=CARTESIAN_POINT('Ctrl Pts',(-127.672384043927,1.64865711451052,
135.440085953923));
#106220=CARTESIAN_POINT('Ctrl Pts',(-127.680140346669,1.77735807138181,
135.392276101802));
#106221=CARTESIAN_POINT('Ctrl Pts',(-127.687896649411,1.90373962099859,
135.339220981231));
#106222=CARTESIAN_POINT('Ctrl Pts',(-127.695657091925,2.03018862425402,
135.286137543544));
#106223=CARTESIAN_POINT('Ctrl Pts',(-127.70341753444,2.15431539989403,135.227803425258));
#106224=CARTESIAN_POINT('Ctrl Pts',(-127.711177976954,2.27566786739423,
135.164465985537));
#106225=CARTESIAN_POINT('Ctrl Pts',(-127.718950877219,2.39721514064843,
135.101026870935));
#106226=CARTESIAN_POINT('Ctrl Pts',(-127.726723777485,2.51597886720291,
135.032568580212));
#106227=CARTESIAN_POINT('Ctrl Pts',(-127.73449667775,2.6315342179285,134.959382966768));
#106228=CARTESIAN_POINT('Ctrl Pts',(-127.741987013512,2.74288884059012,
134.888857834716));
#106229=CARTESIAN_POINT('Ctrl Pts',(-127.749477349274,2.85126404930867,
134.813943288126));
#106230=CARTESIAN_POINT('Ctrl Pts',(-127.756967685036,2.95630949056174,
134.734935290373));
#106231=CARTESIAN_POINT('Ctrl Pts',(-127.764742019155,3.06533776164671,
134.652931680373));
#106232=CARTESIAN_POINT('Ctrl Pts',(-127.772516353274,3.17112415343445,
134.566258322499));
#106233=CARTESIAN_POINT('Ctrl Pts',(-127.780290687394,3.27324255813862,
134.475200605646));
#106234=CARTESIAN_POINT('Ctrl Pts',(-127.788055440341,3.37523511103529,
134.384255109292));
#106235=CARTESIAN_POINT('Ctrl Pts',(-127.795820193288,3.47356838222508,
134.288936262676));
#106236=CARTESIAN_POINT('Ctrl Pts',(-127.803584946235,3.56784650057182,
134.189571749956));
#106237=CARTESIAN_POINT('Ctrl Pts',(-127.81134198712,3.66203098056234,134.090305927471));
#106238=CARTESIAN_POINT('Ctrl Pts',(-127.819099028005,3.75216805552674,
133.987002717089));
#106239=CARTESIAN_POINT('Ctrl Pts',(-127.82685606889,3.8378964074937,133.880028712118));
#106240=CARTESIAN_POINT('Ctrl Pts',(-127.83460726013,3.92356011104369,133.773135377077));
#106241=CARTESIAN_POINT('Ctrl Pts',(-127.84235845137,4.00482146561099,133.662577061182));
#106242=CARTESIAN_POINT('Ctrl Pts',(-127.85010964261,4.08135763462926,133.548755436238));
#106243=CARTESIAN_POINT('Ctrl Pts',(-127.857857539388,4.15786127373392,
133.434982188521));
#106244=CARTESIAN_POINT('Ctrl Pts',(-127.865605436165,4.22964350400189,
133.31794871414));
#106245=CARTESIAN_POINT('Ctrl Pts',(-127.873353332942,4.29642339060513,
133.198087651119));
#106246=CARTESIAN_POINT('Ctrl Pts',(-127.881099609026,4.36318930829571,
133.078251660448));
#106247=CARTESIAN_POINT('Ctrl Pts',(-127.88884588511,4.42495477347024,132.955589598923));
#106248=CARTESIAN_POINT('Ctrl Pts',(-127.896592161194,4.48148381742939,
132.830560473606));
#106249=CARTESIAN_POINT('Ctrl Pts',(-127.904338494459,4.53801327867318,
132.705530425353));
#106250=CARTESIAN_POINT('Ctrl Pts',(-127.912084827725,4.58930608050198,
132.578133634687));
#106251=CARTESIAN_POINT('Ctrl Pts',(-127.91983116099,4.63517376637939,132.448850574351));
#106252=CARTESIAN_POINT('Ctrl Pts',(-127.927579228993,4.68105172400696,
132.319538561972));
#106253=CARTESIAN_POINT('Ctrl Pts',(-127.935327296996,4.72150201743878,
132.188339807754));
#106254=CARTESIAN_POINT('Ctrl Pts',(-127.943075364999,4.75638569988476,
132.055751098764));
#106255=CARTESIAN_POINT('Ctrl Pts',(-127.950831667741,4.79130645712362,
131.923021472915));
#106256=CARTESIAN_POINT('Ctrl Pts',(-127.958587970483,4.82064868537411,
131.788899320007));
#106257=CARTESIAN_POINT('Ctrl Pts',(-127.966344273225,4.84432422444705,
131.65389335439));
#106258=CARTESIAN_POINT('Ctrl Pts',(-127.974104715739,4.86801239986804,
131.518815332024));
#106259=CARTESIAN_POINT('Ctrl Pts',(-127.981865158253,4.88602780824374,
131.382852944402));
#106260=CARTESIAN_POINT('Ctrl Pts',(-127.989625600767,4.89833419927982,
131.246520243341));
#106261=CARTESIAN_POINT('Ctrl Pts',(-127.997398501033,4.91066034562731,
131.109968688926));
#106262=CARTESIAN_POINT('Ctrl Pts',(-128.005171401298,4.91725914197024,
130.97304602389));
#106263=CARTESIAN_POINT('Ctrl Pts',(-128.012944301564,4.91814650231906,
130.836267422902));
#106264=CARTESIAN_POINT('Ctrl Pts',(-128.020434637326,4.91900160488408,
130.704461068586));
#106265=CARTESIAN_POINT('Ctrl Pts',(-128.027924973088,4.91455332267198,
130.572788793826));
#106266=CARTESIAN_POINT('Ctrl Pts',(-128.03541530885,4.90486128341468,130.441705336397));
#106267=CARTESIAN_POINT('Ctrl Pts',(-128.043189642969,4.89480176754306,
130.305651809837));
#106268=CARTESIAN_POINT('Ctrl Pts',(-128.050963977088,4.87906114558482,
130.169801655355));
#106269=CARTESIAN_POINT('Ctrl Pts',(-128.058738311207,4.85764920163124,
130.034667629166));
#106270=CARTESIAN_POINT('Ctrl Pts',(-128.066503064154,4.83626364598499,
129.899700143588));
#106271=CARTESIAN_POINT('Ctrl Pts',(-128.074267817101,4.80922073575887,
129.765447412705));
#106272=CARTESIAN_POINT('Ctrl Pts',(-128.082032570048,4.77658218289587,
129.632419615407));
#106273=CARTESIAN_POINT('Ctrl Pts',(-128.089789610933,4.74397604710368,
129.499523943192));
#106274=CARTESIAN_POINT('Ctrl Pts',(-128.097546651818,4.70578542124897,
129.367851160677));
#106275=CARTESIAN_POINT('Ctrl Pts',(-128.105303692703,4.66212342947555,
129.237903407542));
#106276=CARTESIAN_POINT('Ctrl Pts',(-128.113054883943,4.61849436354972,
129.108053649019));
#106277=CARTESIAN_POINT('Ctrl Pts',(-128.120806075183,4.56940226827529,
128.979926699702));
#106278=CARTESIAN_POINT('Ctrl Pts',(-128.128557266424,4.51501058046856,
128.85401128456));
#106279=CARTESIAN_POINT('Ctrl Pts',(-128.136305163201,4.46064201058017,
128.728149386829));
#106280=CARTESIAN_POINT('Ctrl Pts',(-128.144053059978,4.40097848286103,
128.604497511921));
#106281=CARTESIAN_POINT('Ctrl Pts',(-128.151800956755,4.33623213579808,
128.483525869685));
#106282=CARTESIAN_POINT('Ctrl Pts',(-128.159547232839,4.27149933227517,
128.362579532109));
#106283=CARTESIAN_POINT('Ctrl Pts',(-128.167293508923,4.20168600857646,
128.244312656527));
#106284=CARTESIAN_POINT('Ctrl Pts',(-128.175039785007,4.12705079349721,
128.129171874618));
#106285=CARTESIAN_POINT('Ctrl Pts',(-128.182786118272,4.05241502747766,
128.014030242767));
#106286=CARTESIAN_POINT('Ctrl Pts',(-128.190532451538,3.9729575117102,127.902015078706));
#106287=CARTESIAN_POINT('Ctrl Pts',(-128.198278784803,3.88898061616103,
127.793544643511));
#106288=CARTESIAN_POINT('Ctrl Pts',(-128.206026852806,3.80498491456847,
127.685049917115));
#106289=CARTESIAN_POINT('Ctrl Pts',(-128.213774920809,3.7164680585569,127.580101808277));
#106290=CARTESIAN_POINT('Ctrl Pts',(-128.221522988812,3.62377290501891,
127.479085742409));
#106291=CARTESIAN_POINT('Ctrl Pts',(-128.229279291554,3.53097923396852,
127.377962315464));
#106292=CARTESIAN_POINT('Ctrl Pts',(-128.237035594296,3.43399865928326,
127.280779568059));
#106293=CARTESIAN_POINT('Ctrl Pts',(-128.244791897037,3.33321152401844,
127.187886644391));
#106294=CARTESIAN_POINT('Ctrl Pts',(-128.252552339552,3.23237059562488,
127.094944140973));
#106295=CARTESIAN_POINT('Ctrl Pts',(-128.260312782066,3.1277193565407,127.006296276107));
#106296=CARTESIAN_POINT('Ctrl Pts',(-128.26807322458,3.01967069895121,126.922251405759));
#106297=CARTESIAN_POINT('Ctrl Pts',(-128.275846124845,2.91144859206446,
126.838071619124));
#106298=CARTESIAN_POINT('Ctrl Pts',(-128.283619025111,2.79981848672589,
126.758509819899));
#106299=CARTESIAN_POINT('Ctrl Pts',(-128.291391925376,2.68522241588744,
126.683831083669));
#106300=CARTESIAN_POINT('Ctrl Pts',(-128.298882261138,2.57479220087435,
126.611867107606));
#106301=CARTESIAN_POINT('Ctrl Pts',(-128.3063725969,2.46160818177543,126.544437492631));
#106302=CARTESIAN_POINT('Ctrl Pts',(-128.313862932662,2.34608517260426,
126.48173786912));
#106303=CARTESIAN_POINT('Ctrl Pts',(-128.321637266781,2.22618207342741,
126.416660970325));
#106304=CARTESIAN_POINT('Ctrl Pts',(-128.3294116009,2.1033793003307,126.356473674554));
#106305=CARTESIAN_POINT('Ctrl Pts',(-128.337185935019,1.9781135381811,126.301444907433));
#106306=CARTESIAN_POINT('Ctrl Pts',(-128.344950687966,1.85300215488837,
126.246483958349));
#106307=CARTESIAN_POINT('Ctrl Pts',(-128.352715440914,1.72543417662455,
126.19666904427));
#106308=CARTESIAN_POINT('Ctrl Pts',(-128.360480193861,1.59587218815095,
126.152224009341));
#106309=CARTESIAN_POINT('Ctrl Pts',(-128.368237234746,1.46643888247081,
126.107823117847));
#106310=CARTESIAN_POINT('Ctrl Pts',(-128.375994275631,1.33501587524167,
126.068781617758));
#106311=CARTESIAN_POINT('Ctrl Pts',(-128.383751316516,1.20208677716079,
126.035275753289));
#106312=CARTESIAN_POINT('Ctrl Pts',(-128.391502507756,1.06925792194662,
126.001795155853));
#106313=CARTESIAN_POINT('Ctrl Pts',(-128.399253698996,0.934925614105497,
125.973841980187));
#106314=CARTESIAN_POINT('Ctrl Pts',(-128.407004890236,0.799589373386491,
125.951542890053));
#106315=CARTESIAN_POINT('Ctrl Pts',(-128.414752787013,0.664310654180187,
125.929253277626));
#106316=CARTESIAN_POINT('Ctrl Pts',(-128.42250068379,0.528029235722478,
125.912613034503));
#106317=CARTESIAN_POINT('Ctrl Pts',(-128.430248580567,0.3912553849093,125.901697842473));
#106318=CARTESIAN_POINT('Ctrl Pts',(-128.437994856651,0.254510144237209,
125.890784933667));
#106319=CARTESIAN_POINT('Ctrl Pts',(-128.445741132736,0.117273065573916,
125.88559472503));
#106320=CARTESIAN_POINT('Ctrl Pts',(-128.45348740882,-0.019940292018846,
125.886151040163));
#106321=CARTESIAN_POINT('Ctrl Pts',(-128.461233742085,-0.15715466248963,
125.886707359404));
#106322=CARTESIAN_POINT('Ctrl Pts',(-128.46898007535,-0.294344920578484,
125.893010285475));
#106323=CARTESIAN_POINT('Ctrl Pts',(-128.476726408616,-0.430995733043958,
125.90503150629));
#106324=CARTESIAN_POINT('Ctrl Pts',(-128.484474476619,-0.567677147511227,
125.917055419173));
#106325=CARTESIAN_POINT('Ctrl Pts',(-128.492222544622,-0.703818486580345,
125.934800140736));
#106326=CARTESIAN_POINT('Ctrl Pts',(-128.499970612625,-0.83891015841089,
125.958185547615));
#106327=CARTESIAN_POINT('Ctrl Pts',(-128.507726915366,-0.974145407278053,
125.981595808782));
#106328=CARTESIAN_POINT('Ctrl Pts',(-128.515483218108,-1.10832837452776,
126.010658664105));
#106329=CARTESIAN_POINT('Ctrl Pts',(-128.52323952085,-1.24095973054725,
126.045242841165));
#106330=CARTESIAN_POINT('Ctrl Pts',(-128.530999963364,-1.3736618759149,
126.079845476841));
#106331=CARTESIAN_POINT('Ctrl Pts',(-128.538760405879,-1.50481038623784,
126.119975191855));
#106332=CARTESIAN_POINT('Ctrl Pts',(-128.546520848393,-1.63392265459852,
126.165451282249));
#106333=CARTESIAN_POINT('Ctrl Pts',(-128.554293748658,-1.76324218543442,
126.2110003749));
#106334=CARTESIAN_POINT('Ctrl Pts',(-128.562066648924,-1.89051857908216,
126.261912848164));
#106335=CARTESIAN_POINT('Ctrl Pts',(-128.569839549189,-2.01528989033665,
126.317960087029));
#106336=CARTESIAN_POINT('Ctrl Pts',(-128.577329884951,-2.13552545014673,
126.371969867585));
#106337=CARTESIAN_POINT('Ctrl Pts',(-128.584820220713,-2.25343462192729,
126.430747434437));
#106338=CARTESIAN_POINT('Ctrl Pts',(-128.592310556475,-2.36862859919677,
126.494049535803));
#106339=CARTESIAN_POINT('Ctrl Pts',(-128.600085911847,-2.48820589699215,
126.559760386366));
#106340=CARTESIAN_POINT('Ctrl Pts',(-128.607861267219,-2.60523610837478,
126.630555101034));
#106341=CARTESIAN_POINT('Ctrl Pts',(-128.615636622592,-2.71925675887713,
126.70621155466));
#106342=CARTESIAN_POINT('Ctrl Pts',(-128.62340217256,-2.83313361935999,
126.781772598876));
#106343=CARTESIAN_POINT('Ctrl Pts',(-128.631167722529,-2.94400814846235,
126.86218296753));
#106344=CARTESIAN_POINT('Ctrl Pts',(-128.638933272497,-3.05144185097819,
126.947174377235));
#106345=CARTESIAN_POINT('Ctrl Pts',(-128.646689474804,-3.15874623181723,
127.032063479831));
#106346=CARTESIAN_POINT('Ctrl Pts',(-128.65444567711,-3.2626177305517,127.12152239966));
#106347=CARTESIAN_POINT('Ctrl Pts',(-128.662201879417,-3.36264680274936,
127.215239618984));
#106348=CARTESIAN_POINT('Ctrl Pts',(-128.669952781949,-3.46260752558305,
127.308892801803));
#106349=CARTESIAN_POINT('Ctrl Pts',(-128.677703684481,-3.55873076114183,
127.406798229367));
#106350=CARTESIAN_POINT('Ctrl Pts',(-128.685454587013,-3.6506399867753,
127.508604141511));
#106351=CARTESIAN_POINT('Ctrl Pts',(-128.693201872009,-3.74250631611235,
127.610362538332));
#106352=CARTESIAN_POINT('Ctrl Pts',(-128.700949157004,-3.83016228799984,
127.716017507579));
#106353=CARTESIAN_POINT('Ctrl Pts',(-128.708696442,-3.9132684998003,127.825180745358));
#106354=CARTESIAN_POINT('Ctrl Pts',(-128.716441788902,-3.99635392140223,
127.934316674403));
#106355=CARTESIAN_POINT('Ctrl Pts',(-128.724187135804,-4.07489161252377,
128.046958813855));
#106356=CARTESIAN_POINT('Ctrl Pts',(-128.731932482706,-4.14858296278212,
128.162686439433));
#106357=CARTESIAN_POINT('Ctrl Pts',(-128.739680062984,-4.22229556199313,
128.278447435153));
#106358=CARTESIAN_POINT('Ctrl Pts',(-128.747427643263,-4.29115881307777,
128.397295367957));
#106359=CARTESIAN_POINT('Ctrl Pts',(-128.755175223541,-4.35491786124421,
128.518781153991));
#106360=CARTESIAN_POINT('Ctrl Pts',(-128.76292380285,-4.41868513097717,
128.640282605307));
#106361=CARTESIAN_POINT('Ctrl Pts',(-128.770672382159,-4.47734671218335,
128.764422237434));
#106362=CARTESIAN_POINT('Ctrl Pts',(-128.778420961468,-4.5306945309502,
128.890727912547));
#106363=CARTESIAN_POINT('Ctrl Pts',(-128.786176106855,-4.58408755618451,
129.017140617966));
#106364=CARTESIAN_POINT('Ctrl Pts',(-128.793931252241,-4.63215767846045,
129.145722669742));
#106365=CARTESIAN_POINT('Ctrl Pts',(-128.801686397627,-4.6747455146166,
129.2759832309));
#106366=CARTESIAN_POINT('Ctrl Pts',(-128.807713432355,-4.70784332964267,
129.377217300238));
#106367=CARTESIAN_POINT('Ctrl Pts',(-128.813740467083,-4.7376308916783,
129.479464761412));
#106368=CARTESIAN_POINT('Ctrl Pts',(-128.819767501811,-4.76405452823396,
129.582490119308));
#106369=CARTESIAN_POINT('Origin',(213.235140564004,0.,130.804360617566));
#106370=CARTESIAN_POINT('',(-130.915253971501,-4.76405452823413,129.582490119309));
#106371=CARTESIAN_POINT('',(-130.570084224261,-4.7640545282341,129.582490119308));
#106372=CARTESIAN_POINT('',(213.235140564004,-4.76405452823405,129.582490119308));
#106373=CARTESIAN_POINT('',(-129.235140563955,-4.9182490677973,130.801332481017));
#106374=CARTESIAN_POINT('Ctrl Pts',(-129.23514056401,-4.9182490677979,130.801332481984));
#106375=CARTESIAN_POINT('Ctrl Pts',(-129.24295191385,-4.91833434911582,
130.939845025767));
#106376=CARTESIAN_POINT('Ctrl Pts',(-129.250763263691,-4.91256390560037,
131.078377249122));
#106377=CARTESIAN_POINT('Ctrl Pts',(-129.258574613531,-4.9009593883557,
131.216404469829));
#106378=CARTESIAN_POINT('Ctrl Pts',(-129.266386848761,-4.88935355577846,
131.354447335453));
#106379=CARTESIAN_POINT('Ctrl Pts',(-129.274199083992,-4.87191236406227,
131.491984703982));
#106380=CARTESIAN_POINT('Ctrl Pts',(-129.282011319222,-4.84870939208773,
131.628496706801));
#106381=CARTESIAN_POINT('Ctrl Pts',(-129.289826024435,-4.82549908406397,
131.765051870418));
#106382=CARTESIAN_POINT('Ctrl Pts',(-129.297640729648,-4.7965234321486,
131.900580646536));
#106383=CARTESIAN_POINT('Ctrl Pts',(-129.305455434861,-4.76190715537071,
132.034573325243));
#106384=CARTESIAN_POINT('Ctrl Pts',(-129.31327419593,-4.72727291264148,
132.168635546551));
#106385=CARTESIAN_POINT('Ctrl Pts',(-129.321092956999,-4.68699231094,132.301159713808));
#106386=CARTESIAN_POINT('Ctrl Pts',(-129.328911718067,-4.64123985866449,
132.431651506388));
#106387=CARTESIAN_POINT('Ctrl Pts',(-129.336740892029,-4.59542647404768,
132.562317085729));
#106388=CARTESIAN_POINT('Ctrl Pts',(-129.344570065991,-4.54412681293921,
132.690944525078));
#106389=CARTESIAN_POINT('Ctrl Pts',(-129.352399239954,-4.4875636956581,
132.817059089745));
#106390=CARTESIAN_POINT('Ctrl Pts',(-129.360234429384,-4.43095711866616,
132.943270553288));
#106391=CARTESIAN_POINT('Ctrl Pts',(-129.368069618814,-4.36907919709057,
133.066964954525));
#106392=CARTESIAN_POINT('Ctrl Pts',(-129.375904808245,-4.30219819776465,
133.187693101642));
#106393=CARTESIAN_POINT('Ctrl Pts',(-129.383752384201,-4.23521146733595,
133.308612105956));
#106394=CARTESIAN_POINT('Ctrl Pts',(-129.391599960157,-4.16320606284185,
133.426555167243));
#106395=CARTESIAN_POINT('Ctrl Pts',(-129.399447536114,-4.08649330094691,
133.541102396364));
#106396=CARTESIAN_POINT('Ctrl Pts',(-129.40231983466,-4.05841559188692,
133.583027933829));
#106397=CARTESIAN_POINT('Ctrl Pts',(-129.405192133207,-4.02970765191056,
133.624498877993));
#106398=CARTESIAN_POINT('Ctrl Pts',(-129.408064431754,-4.00038604074756,
133.665495809669));
#106399=CARTESIAN_POINT('Ctrl Pts',(-129.415838765873,-3.92102242364362,
133.776460543836));
#106400=CARTESIAN_POINT('Ctrl Pts',(-129.423613099992,-3.83691260727512,
133.884296393359));
#106401=CARTESIAN_POINT('Ctrl Pts',(-129.431387434111,-3.74833167293782,
133.988570524615));
#106402=CARTESIAN_POINT('Ctrl Pts',(-129.439152187058,-3.65985990668539,
134.092716147324));
#106403=CARTESIAN_POINT('Ctrl Pts',(-129.446916940005,-3.56692823691752,
134.193308490456));
#106404=CARTESIAN_POINT('Ctrl Pts',(-129.454681692952,-3.46985475361051,
134.289943933361));
#106405=CARTESIAN_POINT('Ctrl Pts',(-129.462438733837,-3.37287768505588,
134.386483396581));
#106406=CARTESIAN_POINT('Ctrl Pts',(-129.470195774722,-3.27176726471152,
134.479073506505));
#106407=CARTESIAN_POINT('Ctrl Pts',(-129.477952815607,-3.1668813096812,
134.567344251983));
#106408=CARTESIAN_POINT('Ctrl Pts',(-129.485704006847,-3.06207444996532,
134.655548431806));
#106409=CARTESIAN_POINT('Ctrl Pts',(-129.493455198087,-2.95349802058249,
134.739439479849));
#106410=CARTESIAN_POINT('Ctrl Pts',(-129.501206389327,-2.84154583047943,
134.818685013499));
#106411=CARTESIAN_POINT('Ctrl Pts',(-129.508954286104,-2.72964122304344,
134.897896865684));
#106412=CARTESIAN_POINT('Ctrl Pts',(-129.516702182881,-2.61436402701347,
134.972466905131));
#106413=CARTESIAN_POINT('Ctrl Pts',(-129.524450079658,-2.49614001416456,
135.042103895796));
#106414=CARTESIAN_POINT('Ctrl Pts',(-129.532196355742,-2.37794073123053,
135.111726319904));
#106415=CARTESIAN_POINT('Ctrl Pts',(-129.539942631826,-2.25679619420837,
135.176417549411));
#106416=CARTESIAN_POINT('Ctrl Pts',(-129.54768890791,-2.13315961537935,
135.235930668667));
#106417=CARTESIAN_POINT('Ctrl Pts',(-129.555435241176,-2.00952212389335,
135.295444227235));
#106418=CARTESIAN_POINT('Ctrl Pts',(-129.563181574441,-1.88339290617092,
135.349779429709));
#106419=CARTESIAN_POINT('Ctrl Pts',(-129.570927907706,-1.75524777415475,
135.398736343802));
#106420=CARTESIAN_POINT('Ctrl Pts',(-129.578675975709,-1.62707394492495,
135.447704221456));
#106421=CARTESIAN_POINT('Ctrl Pts',(-129.586424043712,-1.49688366821777,
135.49129127455));
#106422=CARTESIAN_POINT('Ctrl Pts',(-129.594172111715,-1.36517025369483,
135.529346674786));
#106423=CARTESIAN_POINT('Ctrl Pts',(-129.601928414457,-1.23331685258735,
135.567442520755));
#106424=CARTESIAN_POINT('Ctrl Pts',(-129.609684717199,-1.09993745611978,
135.599994861024));
#106425=CARTESIAN_POINT('Ctrl Pts',(-129.61744101994,-0.965538516544453,
135.62690335305));
#106426=CARTESIAN_POINT('Ctrl Pts',(-129.625201462454,-0.831067844208397,
135.653826206948));
#106427=CARTESIAN_POINT('Ctrl Pts',(-129.632961904969,-0.695576930522671,
135.675099149746));
#106428=CARTESIAN_POINT('Ctrl Pts',(-129.640722347483,-0.55957880936594,
135.690673605762));
#106429=CARTESIAN_POINT('Ctrl Pts',(-129.648495247748,-0.42336237195178,
135.706273063277));
#106430=CARTESIAN_POINT('Ctrl Pts',(-129.656268148013,-0.286637490178972,
135.716155725754));
#106431=CARTESIAN_POINT('Ctrl Pts',(-129.664041048279,-0.149919572252493,
135.72032513985));
#106432=CARTESIAN_POINT('Ctrl Pts',(-129.671531384042,-0.0181716949980125,
135.724342985242));
#106433=CARTESIAN_POINT('Ctrl Pts',(-129.679021719805,0.113569407922806,
135.72305575556));
#106434=CARTESIAN_POINT('Ctrl Pts',(-129.686512055567,0.244847698787995,
135.716512148911));
#106435=CARTESIAN_POINT('Ctrl Pts',(-129.694286389686,0.381103445936596,
135.709720439429));
#106436=CARTESIAN_POINT('Ctrl Pts',(-129.702060723806,0.517292210455308,
135.697244379508));
#106437=CARTESIAN_POINT('Ctrl Pts',(-129.709835057925,0.652901148997882,
135.679081445689));
#106438=CARTESIAN_POINT('Ctrl Pts',(-129.717599810872,0.788342961643788,
135.660940896062));
#106439=CARTESIAN_POINT('Ctrl Pts',(-129.725364563819,0.923205986337173,
135.637127468892));
#106440=CARTESIAN_POINT('Ctrl Pts',(-129.733129316766,1.05697871019101,
135.607690615464));
#106441=CARTESIAN_POINT('Ctrl Pts',(-129.740886357651,1.19061856908893,
135.578282999133));
#106442=CARTESIAN_POINT('Ctrl Pts',(-129.748643398536,1.32316990281239,
135.543263154954));
#106443=CARTESIAN_POINT('Ctrl Pts',(-129.756400439421,1.45412800161747,
135.502732124526));
#106444=CARTESIAN_POINT('Ctrl Pts',(-129.764151630661,1.58498734390241,
135.462231658863));
#106445=CARTESIAN_POINT('Ctrl Pts',(-129.771902821901,1.71425547074857,
135.416228394398));
#106446=CARTESIAN_POINT('Ctrl Pts',(-129.779654013141,1.84143987589486,
135.36487399283));
#106447=CARTESIAN_POINT('Ctrl Pts',(-129.787401909918,1.96857022427568,
135.313541418253));
#106448=CARTESIAN_POINT('Ctrl Pts',(-129.795149806695,2.09361825065299,
135.256862376209));
#106449=CARTESIAN_POINT('Ctrl Pts',(-129.802897703472,2.21610878984904,
135.195037660353));
#106450=CARTESIAN_POINT('Ctrl Pts',(-129.810643979556,2.33857370666522,
135.133225876894));
#106451=CARTESIAN_POINT('Ctrl Pts',(-129.81839025564,2.45848185158128,135.066270736625));
#106452=CARTESIAN_POINT('Ctrl Pts',(-129.826136531724,2.57538051515948,
134.994420075931));
#106453=CARTESIAN_POINT('Ctrl Pts',(-129.83388286499,2.6922800416569,134.922568884853));
#106454=CARTESIAN_POINT('Ctrl Pts',(-129.841629198255,2.80616970940809,
134.845822305965));
#106455=CARTESIAN_POINT('Ctrl Pts',(-129.84937553152,2.91662412174053,134.764472585046));
#106456=CARTESIAN_POINT('Ctrl Pts',(-129.857123599523,3.02710326957233,
134.683104646422));
#106457=CARTESIAN_POINT('Ctrl Pts',(-129.864871667527,3.13414531642431,
134.597131746317));
#106458=CARTESIAN_POINT('Ctrl Pts',(-129.872619735529,3.237356720257,134.506887393743));
#106459=CARTESIAN_POINT('Ctrl Pts',(-129.880376038271,3.34067781839835,
134.416547128396));
#106460=CARTESIAN_POINT('Ctrl Pts',(-129.888132341013,3.44015984596066,
134.321926599697));
#106461=CARTESIAN_POINT('Ctrl Pts',(-129.895888643755,3.53544463210754,
134.223397662671));
#106462=CARTESIAN_POINT('Ctrl Pts',(-129.903649086269,3.63078027461376,
134.124816137786));
#106463=CARTESIAN_POINT('Ctrl Pts',(-129.911409528783,3.72191395226734,
134.022322340001));
#106464=CARTESIAN_POINT('Ctrl Pts',(-129.919169971297,3.80852748962882,
133.916321642907));
#106465=CARTESIAN_POINT('Ctrl Pts',(-129.926942871563,3.89528006672966,
133.810150784084));
#106466=CARTESIAN_POINT('Ctrl Pts',(-129.934715771828,3.97749776885261,
133.700462089264));
#106467=CARTESIAN_POINT('Ctrl Pts',(-129.942488672093,4.05490498917549,
133.58769110302));
#106468=CARTESIAN_POINT('Ctrl Pts',(-129.949979007856,4.12949826206492,
133.479019626177));
#106469=CARTESIAN_POINT('Ctrl Pts',(-129.957469343618,4.19962456335478,
133.367486326111));
#106470=CARTESIAN_POINT('Ctrl Pts',(-129.96495967938,4.26507836461446,133.253501202791));
#106471=CARTESIAN_POINT('Ctrl Pts',(-129.972734013499,4.33301386664132,
133.135194298879));
#106472=CARTESIAN_POINT('Ctrl Pts',(-129.980508347618,4.3961307579083,133.013871219091));
#106473=CARTESIAN_POINT('Ctrl Pts',(-129.988282681737,4.45414971100009,
132.889962069066));
#106474=CARTESIAN_POINT('Ctrl Pts',(-129.996047434684,4.51209716091734,
132.766205625994));
#106475=CARTESIAN_POINT('Ctrl Pts',(-130.003812187631,4.56495900926703,
132.63986980474));
#106476=CARTESIAN_POINT('Ctrl Pts',(-130.011576940578,4.61250037560581,
132.511411685208));
#106477=CARTESIAN_POINT('Ctrl Pts',(-130.019333981463,4.65999452318945,
132.38308115209));
#106478=CARTESIAN_POINT('Ctrl Pts',(-130.027091022348,4.70217857009222,
132.252632879793));
#106479=CARTESIAN_POINT('Ctrl Pts',(-130.034848063233,4.73886471752829,
132.120546110369));
#106480=CARTESIAN_POINT('Ctrl Pts',(-130.042599254474,4.77552319965514,
131.988558948606));
#106481=CARTESIAN_POINT('Ctrl Pts',(-130.050350445714,4.80669193049044,
131.854936124291));
#106482=CARTESIAN_POINT('Ctrl Pts',(-130.058101636954,4.83223229565244,
131.720173973744));
#106483=CARTESIAN_POINT('Ctrl Pts',(-130.065849533731,4.85776180547798,
131.585469100705));
#106484=CARTESIAN_POINT('Ctrl Pts',(-130.073597430508,4.87766763489656,
131.449626247881));
#106485=CARTESIAN_POINT('Ctrl Pts',(-130.081345327285,4.89186187891301,
131.31315371907));
#106486=CARTESIAN_POINT('Ctrl Pts',(-130.089091603369,4.90605315379964,
131.176709737369));
#106487=CARTESIAN_POINT('Ctrl Pts',(-130.096837879453,4.91453517926879,
131.039636730289));
#106488=CARTESIAN_POINT('Ctrl Pts',(-130.104584155537,4.91727176658343,
130.902449536723));
#106489=CARTESIAN_POINT('Ctrl Pts',(-130.112330488803,4.92000837409894,
130.765261330473));
#106490=CARTESIAN_POINT('Ctrl Pts',(-130.120076822068,4.91699945103348,
130.627959326942));
#106491=CARTESIAN_POINT('Ctrl Pts',(-130.127823155333,4.90826093474502,
130.491059390381));
#106492=CARTESIAN_POINT('Ctrl Pts',(-130.135571223336,4.89952046152641,
130.354128796027));
#106493=CARTESIAN_POINT('Ctrl Pts',(-130.143319291339,4.88504786675941,
130.21760083791));
#106494=CARTESIAN_POINT('Ctrl Pts',(-130.151067359342,4.86491102193539,
130.081986883858));
#106495=CARTESIAN_POINT('Ctrl Pts',(-130.158823662084,4.8447527754331,129.946228797682));
#106496=CARTESIAN_POINT('Ctrl Pts',(-130.166579964826,4.81891831072572,
129.811387043419));
#106497=CARTESIAN_POINT('Ctrl Pts',(-130.174336267568,4.78752687989382,
129.677963957062));
#106498=CARTESIAN_POINT('Ctrl Pts',(-130.182096710082,4.75611869451001,
129.544469658787));
#106499=CARTESIAN_POINT('Ctrl Pts',(-130.189857152596,4.71914773849338,
129.412395913483));
#106500=CARTESIAN_POINT('Ctrl Pts',(-130.197617595111,4.6767830825288,129.282229525487));
#106501=CARTESIAN_POINT('Ctrl Pts',(-130.205390495376,4.63435041905762,
129.15185418285));
#106502=CARTESIAN_POINT('Ctrl Pts',(-130.213163395641,4.5865068898357,129.023392682682));
#106503=CARTESIAN_POINT('Ctrl Pts',(-130.220936295907,4.53346995862913,
128.897312323288));
#106504=CARTESIAN_POINT('Ctrl Pts',(-130.228426631669,4.48236105346576,
128.775815302541));
#106505=CARTESIAN_POINT('Ctrl Pts',(-130.23591696743,4.42642990811386,128.656529586155));
#106506=CARTESIAN_POINT('Ctrl Pts',(-130.243407303192,4.36591037402112,
128.539849706019));
#106507=CARTESIAN_POINT('Ctrl Pts',(-130.251181637311,4.30309622339669,
128.41874587276));
#106508=CARTESIAN_POINT('Ctrl Pts',(-130.25895597143,4.23513990176855,128.300065756467));
#106509=CARTESIAN_POINT('Ctrl Pts',(-130.266730305549,4.1622522859011,128.184276845812));
#106510=CARTESIAN_POINT('Ctrl Pts',(-130.274495058497,4.08945449750606,
128.06863063464));
#106511=CARTESIAN_POINT('Ctrl Pts',(-130.282259811444,4.01173771332357,
127.955868867186));
#106512=CARTESIAN_POINT('Ctrl Pts',(-130.290024564391,3.92935952900686,
127.846436217872));
#106513=CARTESIAN_POINT('Ctrl Pts',(-130.297781605276,3.84706316386393,
127.737112258609));
#106514=CARTESIAN_POINT('Ctrl Pts',(-130.305538646161,3.76011484564662,
127.631111147682));
#106515=CARTESIAN_POINT('Ctrl Pts',(-130.313295687046,3.66881626443692,
127.528849927566));
#106516=CARTESIAN_POINT('Ctrl Pts',(-130.321046878286,3.57758653219737,
127.426665823432));
#106517=CARTESIAN_POINT('Ctrl Pts',(-130.328798069526,3.4820133260612,127.328216286974));
#106518=CARTESIAN_POINT('Ctrl Pts',(-130.336549260766,3.38243930337109,
127.233886220303));
#106519=CARTESIAN_POINT('Ctrl Pts',(-130.344297157543,3.28290760229726,
127.139596246427));
#106520=CARTESIAN_POINT('Ctrl Pts',(-130.352045054321,3.17937874997502,
127.049422528277));
#106521=CARTESIAN_POINT('Ctrl Pts',(-130.359792951098,3.07223288198794,
126.963713773435));
#106522=CARTESIAN_POINT('Ctrl Pts',(-130.367539227182,2.96510942660635,
126.878022947017));
#106523=CARTESIAN_POINT('Ctrl Pts',(-130.375285503266,2.8543707655923,126.796795470245));
#106524=CARTESIAN_POINT('Ctrl Pts',(-130.38303177935,2.74043048659089,126.720340072727));
#106525=CARTESIAN_POINT('Ctrl Pts',(-130.390778112615,2.626489366509,126.643884110834));
#106526=CARTESIAN_POINT('Ctrl Pts',(-130.398524445881,2.50934690593064,
126.57220051633));
#106527=CARTESIAN_POINT('Ctrl Pts',(-130.406270779146,2.38944573059084,
126.505554717893));
#106528=CARTESIAN_POINT('Ctrl Pts',(-130.414018847149,2.26951770421335,
126.438893994592));
#106529=CARTESIAN_POINT('Ctrl Pts',(-130.421766915152,2.14683007539228,
126.377273502211));
#106530=CARTESIAN_POINT('Ctrl Pts',(-130.429514983155,2.02184975856494,
126.320912545346));
#106531=CARTESIAN_POINT('Ctrl Pts',(-130.437271285897,1.8967366111701,126.264491687386));
#106532=CARTESIAN_POINT('Ctrl Pts',(-130.445027588639,1.76932626517598,
126.213341692342));
#106533=CARTESIAN_POINT('Ctrl Pts',(-130.452783891381,1.64010580874387,
126.167633754937));
#106534=CARTESIAN_POINT('Ctrl Pts',(-130.460544333895,1.5108163834634,126.121901421829));
#106535=CARTESIAN_POINT('Ctrl Pts',(-130.468304776409,1.37971529622514,
126.081617048781));
#106536=CARTESIAN_POINT('Ctrl Pts',(-130.476065218923,1.24730349613843,
126.046901521471));
#106537=CARTESIAN_POINT('Ctrl Pts',(-130.483838119188,1.11467913687526,
126.012130265714));
#106538=CARTESIAN_POINT('Ctrl Pts',(-130.491611019454,0.980740242377996,
125.98294580316));
#106539=CARTESIAN_POINT('Ctrl Pts',(-130.499383919719,0.845997508423659,
125.959417761531));
#106540=CARTESIAN_POINT('Ctrl Pts',(-130.506874255481,0.716153012244307,
125.93674502348));
#106541=CARTESIAN_POINT('Ctrl Pts',(-130.514364591243,0.585562410440587,
125.919324636694));
#106542=CARTESIAN_POINT('Ctrl Pts',(-130.521854927005,0.454684036282337,
125.90717310945));
#106543=CARTESIAN_POINT('Ctrl Pts',(-130.529629261125,0.318843368788455,
125.894560853357));
#106544=CARTESIAN_POINT('Ctrl Pts',(-130.537403595244,0.182262373990399,
125.887584929587));
#106545=CARTESIAN_POINT('Ctrl Pts',(-130.545177929363,0.0454483473876703,
125.88632061059));
#106546=CARTESIAN_POINT('Ctrl Pts',(-130.55294268231,-0.0911970681546911,
125.885057849753));
#106547=CARTESIAN_POINT('Ctrl Pts',(-130.560707435257,-0.228074556882044,
125.889492691671));
#106548=CARTESIAN_POINT('Ctrl Pts',(-130.568472188204,-0.364670764865625,
125.899648771213));
#106549=CARTESIAN_POINT('Ctrl Pts',(-130.576229229089,-0.501131303569768,
125.909794763594));
#106550=CARTESIAN_POINT('Ctrl Pts',(-130.583986269974,-0.637310730126963,
125.925650656538));
#106551=CARTESIAN_POINT('Ctrl Pts',(-130.591743310859,-0.772695104034419,
125.947188051278));
#106552=CARTESIAN_POINT('Ctrl Pts',(-130.599494502099,-0.907977383532191,
125.968709204501));
#106553=CARTESIAN_POINT('Ctrl Pts',(-130.607245693339,-1.04246541921117,
125.995903270378));
#106554=CARTESIAN_POINT('Ctrl Pts',(-130.61499688458,-1.17565016736236,
126.028690010575));
#106555=CARTESIAN_POINT('Ctrl Pts',(-130.622744781357,-1.30877830844295,
126.061462815532));
#106556=CARTESIAN_POINT('Ctrl Pts',(-130.630492678134,-1.44060388488783,
126.099823473805));
#106557=CARTESIAN_POINT('Ctrl Pts',(-130.638240574911,-1.57062804656535,
126.143640651526));
#106558=CARTESIAN_POINT('Ctrl Pts',(-130.645986850995,-1.70062500999159,
126.187448663639));
#106559=CARTESIAN_POINT('Ctrl Pts',(-130.653733127079,-1.8288209379017,
126.236710800146));
#106560=CARTESIAN_POINT('Ctrl Pts',(-130.661479403163,-1.95473253310938,
126.291245973941));
#106561=CARTESIAN_POINT('Ctrl Pts',(-130.669225736429,-2.08064505776769,
126.345781550302));
#106562=CARTESIAN_POINT('Ctrl Pts',(-130.676972069694,-2.20427285731595,
126.405590086236));
#106563=CARTESIAN_POINT('Ctrl Pts',(-130.684718402959,-2.32515336906907,
126.470442658859));
#106564=CARTESIAN_POINT('Ctrl Pts',(-130.692466470962,-2.44606095117516,
126.535309754765));
#106565=CARTESIAN_POINT('Ctrl Pts',(-130.700214538966,-2.56421967678846,
126.605222950291));
#106566=CARTESIAN_POINT('Ctrl Pts',(-130.707962606969,-2.67919266008354,
126.679907956587));
#106567=CARTESIAN_POINT('Ctrl Pts',(-130.71571890971,-2.79428783803299,
126.754672338996));
#106568=CARTESIAN_POINT('Ctrl Pts',(-130.723475212452,-2.9061901816876,
126.834218449801));
#106569=CARTESIAN_POINT('Ctrl Pts',(-130.731231515194,-3.01449237702997,
126.918229022866));
#106570=CARTESIAN_POINT('Ctrl Pts',(-130.738991957708,-3.12285237651492,
127.002284434903));
#106571=CARTESIAN_POINT('Ctrl Pts',(-130.746752400223,-3.22760810044807,
127.09080880494));
#106572=CARTESIAN_POINT('Ctrl Pts',(-130.754512842737,-3.32838706905434,
127.183446011965));
#106573=CARTESIAN_POINT('Ctrl Pts',(-130.762285743002,-3.42932781700776,
127.27623192846));
#106574=CARTESIAN_POINT('Ctrl Pts',(-130.770058643268,-3.52627877601712,
127.373143598867));
#106575=CARTESIAN_POINT('Ctrl Pts',(-130.777831543533,-3.61890532276465,
127.473788995852));
#106576=CARTESIAN_POINT('Ctrl Pts',(-130.785321879295,-3.70816466122221,
127.570775679142));
#106577=CARTESIAN_POINT('Ctrl Pts',(-130.792812215057,-3.79340833612041,
127.67122910638));
#106578=CARTESIAN_POINT('Ctrl Pts',(-130.800302550818,-3.87437471825148,
127.774772591931));
#106579=CARTESIAN_POINT('Ctrl Pts',(-130.808078562731,-3.95842910139558,
127.88226515338));
#106580=CARTESIAN_POINT('Ctrl Pts',(-130.815854574644,-4.03814451413704,
127.993434794596));
#106581=CARTESIAN_POINT('Ctrl Pts',(-130.823630586557,-4.11318170437701,
128.107896390235));
#106582=CARTESIAN_POINT('Ctrl Pts',(-130.83139410495,-4.18809833427191,
128.222174083339));
#106583=CARTESIAN_POINT('Ctrl Pts',(-130.839157623342,-4.25835149809897,
128.3397328746));
#106584=CARTESIAN_POINT('Ctrl Pts',(-130.846921141734,-4.3236422494969,
128.460154832899));
#106585=CARTESIAN_POINT('Ctrl Pts',(-130.854677470153,-4.38887253362138,
128.58046526564));
#106586=CARTESIAN_POINT('Ctrl Pts',(-130.862433798571,-4.44914936042055,
128.703633251401));
#106587=CARTESIAN_POINT('Ctrl Pts',(-130.87019012699,-4.50421697454002,
128.82921188677));
#106588=CARTESIAN_POINT('Ctrl Pts',(-130.877940118031,-4.55923959517303,
128.954687916992));
#106589=CARTESIAN_POINT('Ctrl Pts',(-130.885690109072,-4.60906131881629,
129.082570320442));
#106590=CARTESIAN_POINT('Ctrl Pts',(-130.893440100113,-4.65347252061787,
129.212388079375));
#106591=CARTESIAN_POINT('Ctrl Pts',(-130.900711390576,-4.69514053628081,
129.334187269515));
#106592=CARTESIAN_POINT('Ctrl Pts',(-130.907982681038,-4.7320460761973,
129.457689650613));
#106593=CARTESIAN_POINT('Ctrl Pts',(-130.915253971501,-4.76405452823413,
129.582490119309));
#106594=CARTESIAN_POINT('Ctrl Pts',(-129.165390467031,-4.76405452823393,
129.582490119308));
#106595=CARTESIAN_POINT('Ctrl Pts',(-129.174129006297,-4.80225600717498,
129.731437105911));
#106596=CARTESIAN_POINT('Ctrl Pts',(-129.182867545563,-4.83351255353467,
129.882349764501));
#106597=CARTESIAN_POINT('Ctrl Pts',(-129.191606084828,-4.85763968390153,
130.034607563733));
#106598=CARTESIAN_POINT('Ctrl Pts',(-129.200294685767,-4.88162893441413,
130.185995251897));
#106599=CARTESIAN_POINT('Ctrl Pts',(-129.208983286706,-4.898569928941,130.338712557988));
#106600=CARTESIAN_POINT('Ctrl Pts',(-129.217671887645,-4.90832920715419,
130.492130803652));
#106601=CARTESIAN_POINT('Ctrl Pts',(-129.223494779748,-4.91486964150533,
130.594948034814));
#106602=CARTESIAN_POINT('Ctrl Pts',(-129.229317671852,-4.91818549567706,
130.698079699626));
#106603=CARTESIAN_POINT('Ctrl Pts',(-129.235140563955,-4.9182490677973,
130.801332481017));
#106604=CARTESIAN_POINT('',(-128.889859436027,-4.91824958478679,130.802339666168));
#106605=CARTESIAN_POINT('Ctrl Pts',(-128.819767501811,-4.76405452823396,
129.582490119308));
#106606=CARTESIAN_POINT('Ctrl Pts',(-128.827532201341,-4.79809640912882,
129.715218896259));
#106607=CARTESIAN_POINT('Ctrl Pts',(-128.835296900871,-4.82655328367222,
129.849238742757));
#106608=CARTESIAN_POINT('Ctrl Pts',(-128.843061600402,-4.84935634828604,
129.984039905992));
#106609=CARTESIAN_POINT('Ctrl Pts',(-128.850837082564,-4.8721910789097,
130.119028264019));
#106610=CARTESIAN_POINT('Ctrl Pts',(-128.858612564726,-4.88935628061214,
130.254799718294));
#106611=CARTESIAN_POINT('Ctrl Pts',(-128.866388046888,-4.90083508009763,
130.390840871744));
#106612=CARTESIAN_POINT('Ctrl Pts',(-128.867844758022,-4.90298559561034,
130.416327736571));
#106613=CARTESIAN_POINT('Ctrl Pts',(-128.869301469155,-4.90493667231859,
130.441824072901));
#106614=CARTESIAN_POINT('Ctrl Pts',(-128.870758180288,-4.90668840227637,
130.467326516225));
#106615=CARTESIAN_POINT('Ctrl Pts',(-128.877125265523,-4.91434497446415,
130.578794209867));
#106616=CARTESIAN_POINT('Ctrl Pts',(-128.883492350758,-4.91820363946887,
130.690525757813));
#106617=CARTESIAN_POINT('Ctrl Pts',(-128.889859435993,-4.91824958478655,
130.802339665574));
#106618=CARTESIAN_POINT('Ctrl Pts',(-128.889859436027,-4.91824958478679,
130.802339666168));
#106619=CARTESIAN_POINT('Ctrl Pts',(-128.897555421386,-4.91830511952132,
130.937490707074));
#106620=CARTESIAN_POINT('Ctrl Pts',(-128.905251406744,-4.91278562112983,
131.072869404203));
#106621=CARTESIAN_POINT('Ctrl Pts',(-128.912947392103,-4.90166103705458,
131.20797199045));
#106622=CARTESIAN_POINT('Ctrl Pts',(-128.920634306705,-4.89054956480244,
131.342915340072));
#106623=CARTESIAN_POINT('Ctrl Pts',(-128.928321221307,-4.87384617933464,
131.477582831837));
#106624=CARTESIAN_POINT('Ctrl Pts',(-128.936008135908,-4.85157281406662,
131.611469217638));
#106625=CARTESIAN_POINT('Ctrl Pts',(-128.943687918832,-4.82932011332853,
131.745231387847));
#106626=CARTESIAN_POINT('Ctrl Pts',(-128.951367701755,-4.80150777839274,
131.878213502192));
#106627=CARTESIAN_POINT('Ctrl Pts',(-128.959047484678,-4.76820962903876,
132.009914430567));
#106628=CARTESIAN_POINT('Ctrl Pts',(-128.966970747988,-4.73385579278136,
132.145790814575));
#106629=CARTESIAN_POINT('Ctrl Pts',(-128.974894011297,-4.69366255280835,
132.280302995556));
#106630=CARTESIAN_POINT('Ctrl Pts',(-128.982817274606,-4.64776835386384,
132.412910396504));
#106631=CARTESIAN_POINT('Ctrl Pts',(-128.990489405404,-4.60332879867177,
132.541314727527));
#106632=CARTESIAN_POINT('Ctrl Pts',(-128.998161536201,-4.55354433661832,
132.667932788518));
#106633=CARTESIAN_POINT('Ctrl Pts',(-129.005833666998,-4.49859146641576,
132.792288654692));
#106634=CARTESIAN_POINT('Ctrl Pts',(-129.013504948196,-4.4436446816015,
132.916630749907));
#106635=CARTESIAN_POINT('Ctrl Pts',(-129.021176229395,-4.38353078813123,
133.038710783194));
#106636=CARTESIAN_POINT('Ctrl Pts',(-129.028847510593,-4.31847422177379,
133.158073314217));
#106637=CARTESIAN_POINT('Ctrl Pts',(-129.036519683198,-4.253410095812,133.277449715223));
#106638=CARTESIAN_POINT('Ctrl Pts',(-129.044191855803,-4.18340234600604,
133.394107635336));
#106639=CARTESIAN_POINT('Ctrl Pts',(-129.051864028408,-4.10872085066102,
133.507617178428));
#106640=CARTESIAN_POINT('Ctrl Pts',(-129.059538833809,-4.03401372747844,
133.62116567366));
#106641=CARTESIAN_POINT('Ctrl Pts',(-129.067213639211,-3.95462988835823,
133.731563309756));
#106642=CARTESIAN_POINT('Ctrl Pts',(-129.074888444613,-3.87088161302354,
133.838410485392));
#106643=CARTESIAN_POINT('Ctrl Pts',(-129.082571689898,-3.78704124079564,
133.945375159483));
#106644=CARTESIAN_POINT('Ctrl Pts',(-129.090254935184,-3.69882709964671,
134.048781266191));
#106645=CARTESIAN_POINT('Ctrl Pts',(-129.097938180469,-3.60659088887542,
134.148263310944));
#106646=CARTESIAN_POINT('Ctrl Pts',(-129.105626493196,-3.51429384422726,
134.247810968523));
#106647=CARTESIAN_POINT('Ctrl Pts',(-129.113314805924,-3.4179697312889,
134.343429131395));
#106648=CARTESIAN_POINT('Ctrl Pts',(-129.121003118651,-3.31800499906879,
134.43479115521));
#106649=CARTESIAN_POINT('Ctrl Pts',(-129.128702134705,-3.21790110039125,
134.526280369173));
#106650=CARTESIAN_POINT('Ctrl Pts',(-129.13640115076,-3.11414677331246,
134.613501365509));
#106651=CARTESIAN_POINT('Ctrl Pts',(-129.144100166814,-3.00715939119916,
134.696169381935));
#106652=CARTESIAN_POINT('Ctrl Pts',(-129.14580204591,-2.98350966922823,
134.714443271489));
#106653=CARTESIAN_POINT('Ctrl Pts',(-129.147503925006,-2.9597020700224,
134.732494859633));
#106654=CARTESIAN_POINT('Ctrl Pts',(-129.149205804101,-2.93574126871814,
134.750321370747));
#106655=CARTESIAN_POINT('Ctrl Pts',(-129.15698013822,-2.82628621074341,
134.831754448992));
#106656=CARTESIAN_POINT('Ctrl Pts',(-129.164754472339,-2.713266968064,134.90875888027));
#106657=CARTESIAN_POINT('Ctrl Pts',(-129.172528806458,-2.59707764485735,
134.981006493036));
#106658=CARTESIAN_POINT('Ctrl Pts',(-129.180293559406,-2.4810315146071,
135.053165067076));
#106659=CARTESIAN_POINT('Ctrl Pts',(-129.188058312353,-2.36182340610435,
135.120578282474));
#106660=CARTESIAN_POINT('Ctrl Pts',(-129.1958230653,-2.23987945856755,135.18295891766));
#106661=CARTESIAN_POINT('Ctrl Pts',(-129.203580106185,-2.11805662747856,
135.24527759552));
#106662=CARTESIAN_POINT('Ctrl Pts',(-129.21133714707,-1.99350371066769,
135.302573463366));
#106663=CARTESIAN_POINT('Ctrl Pts',(-129.219094187955,-1.86667441513644,
135.354603434205));
#106664=CARTESIAN_POINT('Ctrl Pts',(-129.226845379195,-1.73994076256337,
135.406594168838));
#106665=CARTESIAN_POINT('Ctrl Pts',(-129.234596570435,-1.61093450837533,
135.453326762818));
#106666=CARTESIAN_POINT('Ctrl Pts',(-129.242347761675,-1.48013214329801,
135.494604950314));
#106667=CARTESIAN_POINT('Ctrl Pts',(-129.250095658452,-1.3493853727153,
135.53586559348));
#106668=CARTESIAN_POINT('Ctrl Pts',(-129.257843555229,-1.21684438163768,
135.571676323606));
#106669=CARTESIAN_POINT('Ctrl Pts',(-129.265591452006,-1.08300353372696,
135.601889815855));
#106670=CARTESIAN_POINT('Ctrl Pts',(-129.27333772809,-0.949190682436344,
135.632096988092));
#106671=CARTESIAN_POINT('Ctrl Pts',(-129.281084004174,-0.814078896267816,
135.656709165243));
#106672=CARTESIAN_POINT('Ctrl Pts',(-129.288830280258,-0.678175136379287,
135.675629604893));
#106673=CARTESIAN_POINT('Ctrl Pts',(-129.296576613524,-0.54227037327989,
135.69455018421));
#106674=CARTESIAN_POINT('Ctrl Pts',(-129.304322946789,-0.405574012025448,
135.707778888279));
#106675=CARTESIAN_POINT('Ctrl Pts',(-129.312069280054,-0.268600188502013,
135.715270614831));
#106676=CARTESIAN_POINT('Ctrl Pts',(-129.319817348057,-0.13159569064107,
135.722764019103));
#106677=CARTESIAN_POINT('Ctrl Pts',(-129.32756541606,0.00568600282480028,
135.724517867993));
#106678=CARTESIAN_POINT('Ctrl Pts',(-129.335313484063,0.14272908708239,
135.720539160927));
#106679=CARTESIAN_POINT('Ctrl Pts',(-129.343069786805,0.279917822361323,
135.716556225244));
#106680=CARTESIAN_POINT('Ctrl Pts',(-129.350826089547,0.416867050421558,
135.706828574287));
#106681=CARTESIAN_POINT('Ctrl Pts',(-129.358582392288,0.553063866572545,
135.69141529518));
#106682=CARTESIAN_POINT('Ctrl Pts',(-129.366342834802,0.689333375065119,
135.675993789543));
#106683=CARTESIAN_POINT('Ctrl Pts',(-129.374103277317,0.82484928534065,
135.654880669232));
#106684=CARTESIAN_POINT('Ctrl Pts',(-129.381863719831,0.959108231643547,
135.628186325704));
#106685=CARTESIAN_POINT('Ctrl Pts',(-129.389636620096,1.093582702326,135.601449130046));
#106686=CARTESIAN_POINT('Ctrl Pts',(-129.397409520362,1.22679579669742,
135.569112899564));
#106687=CARTESIAN_POINT('Ctrl Pts',(-129.405182420627,1.3582578028564,135.531338383907));
#106688=CARTESIAN_POINT('Ctrl Pts',(-129.412672756389,1.4849408339594,135.494937067042));
#106689=CARTESIAN_POINT('Ctrl Pts',(-129.420163092151,1.60999758706895,
135.453486088079));
#106690=CARTESIAN_POINT('Ctrl Pts',(-129.427653427913,1.73300867185807,
135.407171063996));
#106691=CARTESIAN_POINT('Ctrl Pts',(-129.435427762032,1.86068375931449,
135.359099991698));
#106692=CARTESIAN_POINT('Ctrl Pts',(-129.443202096151,1.98655942954455,
135.305636478004));
#106693=CARTESIAN_POINT('Ctrl Pts',(-129.45097643027,2.11014655959868,135.246934709184));
#106694=CARTESIAN_POINT('Ctrl Pts',(-129.458741183217,2.23358137956032,
135.188305285047));
#106695=CARTESIAN_POINT('Ctrl Pts',(-129.466505936165,2.35473292138145,
135.124450616796));
#106696=CARTESIAN_POINT('Ctrl Pts',(-129.474270689112,2.47312919876496,
135.055573977151));
#106697=CARTESIAN_POINT('Ctrl Pts',(-129.482027729997,2.591407883297,134.986765746756));
#106698=CARTESIAN_POINT('Ctrl Pts',(-129.489784770882,2.70693641353036,
134.912945666421));
#106699=CARTESIAN_POINT('Ctrl Pts',(-129.497541811767,2.81926503377483,
134.834364058239));
#106700=CARTESIAN_POINT('Ctrl Pts',(-129.505293003007,2.93150894613283,
134.755841709059));
#106701=CARTESIAN_POINT('Ctrl Pts',(-129.513044194247,3.04055743252559,
134.672565202317));
#106702=CARTESIAN_POINT('Ctrl Pts',(-129.520795385487,3.14598781407482,
134.584829336679));
#106703=CARTESIAN_POINT('Ctrl Pts',(-129.528543282264,3.2513733848993,134.497130761125));
#106704=CARTESIAN_POINT('Ctrl Pts',(-129.536291179041,3.35314360953878,
134.404976845935));
#106705=CARTESIAN_POINT('Ctrl Pts',(-129.544039075818,3.45090732379814,
134.308703880584));
#106706=CARTESIAN_POINT('Ctrl Pts',(-129.551785351902,3.54865058799602,
134.212451053461));
#106707=CARTESIAN_POINT('Ctrl Pts',(-129.559531627987,3.64238873039872,
134.112081164129));
#106708=CARTESIAN_POINT('Ctrl Pts',(-129.567277904071,3.7317663339851,134.007968441729));
#106709=CARTESIAN_POINT('Ctrl Pts',(-129.575024237336,3.82114459733677,
133.903854950792));
#106710=CARTESIAN_POINT('Ctrl Pts',(-129.582770570601,3.9061620029787,133.795998868305));
#106711=CARTESIAN_POINT('Ctrl Pts',(-129.590516903867,3.98650270208916,
133.684808372471));
#106712=CARTESIAN_POINT('Ctrl Pts',(-129.59826497187,4.06686139294246,133.573592976296));
#106713=CARTESIAN_POINT('Ctrl Pts',(-129.606013039873,4.14254106429578,
133.459041997728));
#106714=CARTESIAN_POINT('Ctrl Pts',(-129.613761107876,4.21326879986361,
133.341593181324));
#106715=CARTESIAN_POINT('Ctrl Pts',(-129.621517410618,4.28407170571019,
133.224019538922));
#106716=CARTESIAN_POINT('Ctrl Pts',(-129.62927371336,4.3499119603961,133.103542241798));
#106717=CARTESIAN_POINT('Ctrl Pts',(-129.637030016102,4.41056203807861,
132.980624749228));
#106718=CARTESIAN_POINT('Ctrl Pts',(-129.644790458616,4.47124448653372,
132.857641651892));
#106719=CARTESIAN_POINT('Ctrl Pts',(-129.65255090113,4.52673108012555,132.732216121322));
#106720=CARTESIAN_POINT('Ctrl Pts',(-129.660311343644,4.57684261282624,
132.604831322665));
#106721=CARTESIAN_POINT('Ctrl Pts',(-129.66808424391,4.62703458900791,132.477242034619));
#106722=CARTESIAN_POINT('Ctrl Pts',(-129.675857144175,4.67183413391158,
132.347687563101));
#106723=CARTESIAN_POINT('Ctrl Pts',(-129.683630044441,4.71111178952633,
132.216666805716));
#106724=CARTESIAN_POINT('Ctrl Pts',(-129.691120380203,4.74896160342472,
132.090408982884));
#106725=CARTESIAN_POINT('Ctrl Pts',(-129.698610715965,4.78168395060627,
131.962789928077));
#106726=CARTESIAN_POINT('Ctrl Pts',(-129.706101051727,4.80920830517683,
131.834262816767));
#106727=CARTESIAN_POINT('Ctrl Pts',(-129.713875385846,4.83777625401698,
131.700862560965));
#106728=CARTESIAN_POINT('Ctrl Pts',(-129.721649719965,4.86083476022433,
131.566061459546));
#106729=CARTESIAN_POINT('Ctrl Pts',(-129.729424054084,4.87824916217283,
131.430354366944));
#106730=CARTESIAN_POINT('Ctrl Pts',(-129.737188807031,4.89564210242735,
131.294814521205));
#106731=CARTESIAN_POINT('Ctrl Pts',(-129.744953559978,4.9074047292151,131.158371289954));
#106732=CARTESIAN_POINT('Ctrl Pts',(-129.752718312925,4.91345294150957,
131.0215316425));
#106733=CARTESIAN_POINT('Ctrl Pts',(-129.76047535381,4.91949514663432,130.884827906114));
#106734=CARTESIAN_POINT('Ctrl Pts',(-129.768232394695,4.91983421488778,
130.747728925114));
#106735=CARTESIAN_POINT('Ctrl Pts',(-129.77598943558,4.91443764539859,130.610748396905));
#106736=CARTESIAN_POINT('Ctrl Pts',(-129.78374062682,4.90904514550445,130.473871166779));
#106737=CARTESIAN_POINT('Ctrl Pts',(-129.79149181806,4.89792563242171,130.337112600728));
#106738=CARTESIAN_POINT('Ctrl Pts',(-129.799243009301,4.88109866035963,
130.200987656343));
#106739=CARTESIAN_POINT('Ctrl Pts',(-129.806990906078,4.86427884020948,
130.064920568689));
#106740=CARTESIAN_POINT('Ctrl Pts',(-129.814738802855,4.84175643371894,
129.929486954272));
#106741=CARTESIAN_POINT('Ctrl Pts',(-129.822486699632,4.81360293694544,
129.795197683283));
#106742=CARTESIAN_POINT('Ctrl Pts',(-129.830232975716,4.78545532927654,
129.660936502714));
#106743=CARTESIAN_POINT('Ctrl Pts',(-129.8379792518,4.75167905440802,129.527819571854));
#106744=CARTESIAN_POINT('Ctrl Pts',(-129.845725527884,4.71239685033488,
129.396348193099));
#106745=CARTESIAN_POINT('Ctrl Pts',(-129.853471861149,4.6731143562896,129.264875843853));
#106746=CARTESIAN_POINT('Ctrl Pts',(-129.861218194415,4.62832596386533,
129.135049445553));
#106747=CARTESIAN_POINT('Ctrl Pts',(-129.86896452768,4.57820436094176,129.007355361048));
#106748=CARTESIAN_POINT('Ctrl Pts',(-129.876712595683,4.52807153363267,
128.879632680338));
#106749=CARTESIAN_POINT('Ctrl Pts',(-129.884460663686,4.47260326205642,
128.75404362749));
#106750=CARTESIAN_POINT('Ctrl Pts',(-129.892208731689,4.41202031518889,
128.631054426331));
#106751=CARTESIAN_POINT('Ctrl Pts',(-129.899965034431,4.3513729800444,128.507934510785));
#106752=CARTESIAN_POINT('Ctrl Pts',(-129.907721337173,4.28560028377494,
128.387420317908));
#106753=CARTESIAN_POINT('Ctrl Pts',(-129.915477639915,4.21496916451982,
128.269953782694));
#106754=CARTESIAN_POINT('Ctrl Pts',(-129.923238082429,4.14430034730951,
128.152424552052));
#106755=CARTESIAN_POINT('Ctrl Pts',(-129.930998524943,4.06876815537738,
128.03794654644));
#106756=CARTESIAN_POINT('Ctrl Pts',(-129.938758967457,3.98868222400822,
127.926931699525));
#106757=CARTESIAN_POINT('Ctrl Pts',(-129.946531867723,3.90846773159255,
127.815738641722));
#106758=CARTESIAN_POINT('Ctrl Pts',(-129.954304767988,3.82368513384148,
127.708020159406));
#106759=CARTESIAN_POINT('Ctrl Pts',(-129.962077668253,3.73468419222225,
127.60415483561));
#106760=CARTESIAN_POINT('Ctrl Pts',(-129.969568004015,3.64891865901144,
127.504065277955));
#106761=CARTESIAN_POINT('Ctrl Pts',(-129.977058339777,3.55923636178248,
127.407553824135));
#106762=CARTESIAN_POINT('Ctrl Pts',(-129.984548675539,3.46598044892533,
127.314924761992));
#106763=CARTESIAN_POINT('Ctrl Pts',(-129.992323009658,3.36918870978726,
127.218783640803));
#106764=CARTESIAN_POINT('Ctrl Pts',(-130.000097343777,3.26824041123828,
127.126520578463));
#106765=CARTESIAN_POINT('Ctrl Pts',(-130.007871677896,3.16347910043161,
127.038516350521));
#106766=CARTESIAN_POINT('Ctrl Pts',(-130.015636430844,3.05884689857715,
126.950620579925));
#106767=CARTESIAN_POINT('Ctrl Pts',(-130.023401183791,2.95041133094954,
126.866973449571));
#106768=CARTESIAN_POINT('Ctrl Pts',(-130.031165936738,2.83855346652765,
126.787919745331));
#106769=CARTESIAN_POINT('Ctrl Pts',(-130.038922977623,2.72680670091393,
126.708944558344));
#106770=CARTESIAN_POINT('Ctrl Pts',(-130.046680018508,2.61164472002733,
126.63455394256));
#106771=CARTESIAN_POINT('Ctrl Pts',(-130.054437059393,2.49348214452833,
126.565052907878));
#106772=CARTESIAN_POINT('Ctrl Pts',(-130.062188250633,2.3754086763462,126.495604284467));
#106773=CARTESIAN_POINT('Ctrl Pts',(-130.069939441873,2.25433945309223,
126.43103810028));
#106774=CARTESIAN_POINT('Ctrl Pts',(-130.077690633113,2.1307182927002,126.371616250963));
#106775=CARTESIAN_POINT('Ctrl Pts',(-130.08543852989,2.00714967459955,126.312219657517));
#106776=CARTESIAN_POINT('Ctrl Pts',(-130.093186426667,1.88103162826315,
126.257963219223));
#106777=CARTESIAN_POINT('Ctrl Pts',(-130.100934323444,1.75283260861695,
126.20906292224));
#106778=CARTESIAN_POINT('Ctrl Pts',(-130.108680599528,1.62466040544201,
126.160172854144));
#106779=CARTESIAN_POINT('Ctrl Pts',(-130.116426875613,1.49440845984381,
126.116636838093));
#106780=CARTESIAN_POINT('Ctrl Pts',(-130.124173151697,1.36256487461217,
126.078622577326));
#106781=CARTESIAN_POINT('Ctrl Pts',(-130.131919484962,1.23072031614095,
126.040608035946));
#106782=CARTESIAN_POINT('Ctrl Pts',(-130.139665818228,1.09728447025367,
126.008115439498));
#106783=CARTESIAN_POINT('Ctrl Pts',(-130.147412151493,0.962759869806269,
125.981262391779));
#106784=CARTESIAN_POINT('Ctrl Pts',(-130.155160219496,0.82820514350751,
125.954403330506));
#106785=CARTESIAN_POINT('Ctrl Pts',(-130.162908287499,0.69256156080494,
125.933186407578));
#106786=CARTESIAN_POINT('Ctrl Pts',(-130.170656355502,0.556340700032145,
125.917677889172));
#106787=CARTESIAN_POINT('Ctrl Pts',(-130.178412658244,0.419975062107657,
125.902152888127));
#106788=CARTESIAN_POINT('Ctrl Pts',(-130.186168960985,0.283031309579939,
125.892348455305));
#106789=CARTESIAN_POINT('Ctrl Pts',(-130.193925263727,0.146025541460958,
125.888278884749));
#106790=CARTESIAN_POINT('Ctrl Pts',(-130.201685706242,0.00894664923799438,
125.88420714214));
#106791=CARTESIAN_POINT('Ctrl Pts',(-130.209446148756,-0.12819393378499,
125.885876356081));
#106792=CARTESIAN_POINT('Ctrl Pts',(-130.21720659127,-0.264882270710789,
125.893248681847));
#106793=CARTESIAN_POINT('Ctrl Pts',(-130.224979491535,-0.40179003188927,
125.900632842325));
#106794=CARTESIAN_POINT('Ctrl Pts',(-130.232752391801,-0.538243706821677,
125.913738372119));
#106795=CARTESIAN_POINT('Ctrl Pts',(-130.240525292066,-0.673735728264205,
125.932475640377));
#106796=CARTESIAN_POINT('Ctrl Pts',(-130.248015627828,-0.804302273444213,
125.950531761738));
#106797=CARTESIAN_POINT('Ctrl Pts',(-130.25550596359,-0.933975565155572,
125.973817220118));
#106798=CARTESIAN_POINT('Ctrl Pts',(-130.262996299352,-1.06231411733078,
126.002207790071));
#106799=CARTESIAN_POINT('Ctrl Pts',(-130.270770633471,-1.19551866471845,
126.031674797112));
#106800=CARTESIAN_POINT('Ctrl Pts',(-130.27854496759,-1.32770721325576,
126.066735020841));
#106801=CARTESIAN_POINT('Ctrl Pts',(-130.28631930171,-1.45837371006082,
126.107305243792));
#106802=CARTESIAN_POINT('Ctrl Pts',(-130.294084054657,-1.58887917208691,
126.147825467569));
#106803=CARTESIAN_POINT('Ctrl Pts',(-130.301848807604,-1.71786594485178,
126.193842064517));
#106804=CARTESIAN_POINT('Ctrl Pts',(-130.309613560551,-1.84483797314648,
126.245220795699));
#106805=CARTESIAN_POINT('Ctrl Pts',(-130.317370601436,-1.97168389103233,
126.2965484968));
#106806=CARTESIAN_POINT('Ctrl Pts',(-130.325127642321,-2.09651868659945,
126.353227587953));
#106807=CARTESIAN_POINT('Ctrl Pts',(-130.332884683206,-2.21886163378716,
126.415074102356));
#106808=CARTESIAN_POINT('Ctrl Pts',(-130.340635874446,-2.34111232120587,
126.47687397782));
#106809=CARTESIAN_POINT('Ctrl Pts',(-130.348387065686,-2.46087455301941,
126.543833344531));
#106810=CARTESIAN_POINT('Ctrl Pts',(-130.356138256926,-2.57768809456893,
126.615720366886));
#106811=CARTESIAN_POINT('Ctrl Pts',(-130.363886153703,-2.69445198724798,
126.687576835339));
#106812=CARTESIAN_POINT('Ctrl Pts',(-130.37163405048,-2.80826935005605,
126.764356589385));
#106813=CARTESIAN_POINT('Ctrl Pts',(-130.379381947257,-2.91870525639027,
126.845782250422));
#106814=CARTESIAN_POINT('Ctrl Pts',(-130.387128223341,-3.02911806191362,
126.927190878966));
#106815=CARTESIAN_POINT('Ctrl Pts',(-130.394874499425,-3.13615050339798,
127.013243249622));
#106816=CARTESIAN_POINT('Ctrl Pts',(-130.402620775509,-3.23939765587746,
127.103619355387));
#106817=CARTESIAN_POINT('Ctrl Pts',(-130.410367108774,-3.34264557050411,
127.193996128287));
#106818=CARTESIAN_POINT('Ctrl Pts',(-130.41811344204,-3.44210784618725,
127.288696442476));
#106819=CARTESIAN_POINT('Ctrl Pts',(-130.425859775305,-3.53741390823919,
127.387361070552));
#106820=CARTESIAN_POINT('Ctrl Pts',(-130.433607843308,-3.63274131342305,
127.486047793887));
#106821=CARTESIAN_POINT('Ctrl Pts',(-130.441355911311,-3.72391038130586,
127.588700316546));
#106822=CARTESIAN_POINT('Ctrl Pts',(-130.449103979314,-3.81058883969292,
127.694924051674));
#106823=CARTESIAN_POINT('Ctrl Pts',(-130.456860282056,-3.89735942097691,
127.801260682651));
#106824=CARTESIAN_POINT('Ctrl Pts',(-130.464616584798,-3.97962961126454,
127.911175804674));
#106825=CARTESIAN_POINT('Ctrl Pts',(-130.47237288754,-4.05710842045033,
128.024242935307));
#106826=CARTESIAN_POINT('Ctrl Pts',(-130.480133330054,-4.13462858240921,
128.137370413271));
#106827=CARTESIAN_POINT('Ctrl Pts',(-130.487893772568,-4.20735206041497,
128.253652920698));
#106828=CARTESIAN_POINT('Ctrl Pts',(-130.495654215082,-4.27503289885926,
128.372637611924));
#106829=CARTESIAN_POINT('Ctrl Pts',(-130.503427115348,-4.34282238459404,
128.491813307938));
#106830=CARTESIAN_POINT('Ctrl Pts',(-130.511200015613,-4.4055528755781,
128.613699508202));
#106831=CARTESIAN_POINT('Ctrl Pts',(-130.518972915878,-4.46302542829209,
128.737820734351));
#106832=CARTESIAN_POINT('Ctrl Pts',(-130.526463251641,-4.51840870895248,
128.857429841292));
#106833=CARTESIAN_POINT('Ctrl Pts',(-130.533953587403,-4.56890957495682,
128.979114013185));
#106834=CARTESIAN_POINT('Ctrl Pts',(-130.541443923165,-4.61439390668836,
129.102434668408));
#106835=CARTESIAN_POINT('Ctrl Pts',(-130.55042514124,-4.66893147553119,
129.250301163703));
#106836=CARTESIAN_POINT('Ctrl Pts',(-130.559406359316,-4.71640066332549,
129.400907585557));
#106837=CARTESIAN_POINT('Ctrl Pts',(-130.568387577391,-4.7565558117372,
129.553616889887));
#106838=CARTESIAN_POINT('Ctrl Pts',(-130.568953126347,-4.7590843888292,
129.563233022909));
#106839=CARTESIAN_POINT('Ctrl Pts',(-130.569518675304,-4.76158397936226,
129.572857486753));
#106840=CARTESIAN_POINT('Ctrl Pts',(-130.570084224261,-4.7640545282341,
129.582490119308));
#106841=CARTESIAN_POINT('Origin',(213.235140564004,0.,130.804360617566));
#106842=CARTESIAN_POINT('',(-132.66500688127,-4.76405452823412,129.582490119309));
#106843=CARTESIAN_POINT('',(-132.320008282756,-4.76405452823417,129.582490119309));
#106844=CARTESIAN_POINT('',(213.235140564004,-4.76405452823405,129.582490119308));
#106845=CARTESIAN_POINT('',(-130.985140564062,-4.91824853312603,130.808159157235));
#106846=CARTESIAN_POINT('Ctrl Pts',(-130.985140564062,-4.91824853312603,
130.808159157235));
#106847=CARTESIAN_POINT('Ctrl Pts',(-130.994145389984,-4.91812534212975,
130.967663595687));
#106848=CARTESIAN_POINT('Ctrl Pts',(-131.003150215905,-4.9102388911086,
131.126846153038));
#106849=CARTESIAN_POINT('Ctrl Pts',(-131.012155041827,-4.89470640897744,
131.285018741824));
#106850=CARTESIAN_POINT('Ctrl Pts',(-131.021211888168,-4.87908419648849,
131.444105085595));
#106851=CARTESIAN_POINT('Ctrl Pts',(-131.03026873451,-4.85572746516266,
131.602169652566));
#106852=CARTESIAN_POINT('Ctrl Pts',(-131.039325580852,-4.82480465905455,
131.758532019603));
#106853=CARTESIAN_POINT('Ctrl Pts',(-131.048444313205,-4.79367055543172,
131.915962820709));
#106854=CARTESIAN_POINT('Ctrl Pts',(-131.057563045558,-4.7548667042909,
132.071667976947));
#106855=CARTESIAN_POINT('Ctrl Pts',(-131.06668177791,-4.70861331502907,
132.224974467995));
#106856=CARTESIAN_POINT('Ctrl Pts',(-131.070704576817,-4.68820827663491,
132.292606805556));
#106857=CARTESIAN_POINT('Ctrl Pts',(-131.074727375724,-4.66635402911844,
132.359772602815));
#106858=CARTESIAN_POINT('Ctrl Pts',(-131.078750174631,-4.64307238043769,
132.426415466366));
#106859=CARTESIAN_POINT('Ctrl Pts',(-131.08652450875,-4.59807900148245,
132.555207359738));
#106860=CARTESIAN_POINT('Ctrl Pts',(-131.094298842869,-4.5476515529689,
132.682329757796));
#106861=CARTESIAN_POINT('Ctrl Pts',(-131.102073176988,-4.49193243916302,
132.807289978401));
#106862=CARTESIAN_POINT('Ctrl Pts',(-131.109837929935,-4.4362819941853,
132.932096196702));
#106863=CARTESIAN_POINT('Ctrl Pts',(-131.117602682882,-4.37535301745541,
133.054745185841));
#106864=CARTESIAN_POINT('Ctrl Pts',(-131.125367435829,-4.30933739678566,
133.174760217457));
#106865=CARTESIAN_POINT('Ctrl Pts',(-131.133124476713,-4.24338734376119,
133.294656048452));
#106866=CARTESIAN_POINT('Ctrl Pts',(-131.140881517598,-4.17236088796681,
133.411922787704));
#106867=CARTESIAN_POINT('Ctrl Pts',(-131.148638558483,-4.09649748651096,
133.526104802002));
#106868=CARTESIAN_POINT('Ctrl Pts',(-131.156389749723,-4.02069129423618,
133.640200710754));
#106869=CARTESIAN_POINT('Ctrl Pts',(-131.164140940963,-3.94005563206689,
133.751216200419));
#106870=CARTESIAN_POINT('Ctrl Pts',(-131.171892132203,-3.85487507064748,
133.858721639482));
#106871=CARTESIAN_POINT('Ctrl Pts',(-131.17964002898,-3.76973071323882,
133.966181385866));
#106872=CARTESIAN_POINT('Ctrl Pts',(-131.187387925757,-3.68004554088208,
134.070133743063));
#106873=CARTESIAN_POINT('Ctrl Pts',(-131.195135822534,-3.58614635934712,
134.170179589502));
#106874=CARTESIAN_POINT('Ctrl Pts',(-131.202882098618,-3.49226681949672,
134.270204508506));
#106875=CARTESIAN_POINT('Ctrl Pts',(-131.210628374702,-3.39417529116859,
134.366324257233));
#106876=CARTESIAN_POINT('Ctrl Pts',(-131.218374650786,-3.29223736670814,
134.458174540544));
#106877=CARTESIAN_POINT('Ctrl Pts',(-131.226120984051,-3.19029868976522,
134.550025501874));
#106878=CARTESIAN_POINT('Ctrl Pts',(-131.233867317316,-3.08451385048509,
134.637606673191));
#106879=CARTESIAN_POINT('Ctrl Pts',(-131.241613650581,-2.97528333002523,
134.720592501479));
#106880=CARTESIAN_POINT('Ctrl Pts',(-131.249361718584,-2.86602834814781,
134.803596913867));
#106881=CARTESIAN_POINT('Ctrl Pts',(-131.257109786587,-2.753326460876,134.882003698979));
#106882=CARTESIAN_POINT('Ctrl Pts',(-131.26485785459,-2.6376087374702,134.955529514458));
#106883=CARTESIAN_POINT('Ctrl Pts',(-131.272614157332,-2.52176802789076,
135.029133474049));
#106884=CARTESIAN_POINT('Ctrl Pts',(-131.280370460073,-2.40290540982616,
135.097845891307));
#106885=CARTESIAN_POINT('Ctrl Pts',(-131.288126762815,-2.28147874909492,
135.161428184167));
#106886=CARTESIAN_POINT('Ctrl Pts',(-131.295887205329,-2.15998727929876,
135.225044412812));
#106887=CARTESIAN_POINT('Ctrl Pts',(-131.303647647843,-2.0359293934397,
135.283524894534));
#106888=CARTESIAN_POINT('Ctrl Pts',(-131.311408090357,-1.90978381707225,
135.336678880282));
#106889=CARTESIAN_POINT('Ctrl Pts',(-131.319180990623,-1.78343574062694,
135.389918193527));
#106890=CARTESIAN_POINT('Ctrl Pts',(-131.326953890888,-1.65499364315145,
135.437813787365));
#106891=CARTESIAN_POINT('Ctrl Pts',(-131.334726791153,-1.52495317194495,
135.480224268901));
#106892=CARTESIAN_POINT('Ctrl Pts',(-131.342217126917,-1.39963999938695,
135.521093022618));
#106893=CARTESIAN_POINT('Ctrl Pts',(-131.349707462681,-1.27284294179143,
135.556868452013));
#106894=CARTESIAN_POINT('Ctrl Pts',(-131.357197798445,-1.14501335169955,
135.58746917654));
#106895=CARTESIAN_POINT('Ctrl Pts',(-131.364972132564,-1.01233706387723,
135.619230136831));
#106896=CARTESIAN_POINT('Ctrl Pts',(-131.372746466683,-0.878128122414002,
135.645516857505));
#106897=CARTESIAN_POINT('Ctrl Pts',(-131.380520800802,-0.742878007731576,
135.666182840573));
#106898=CARTESIAN_POINT('Ctrl Pts',(-131.388285553749,-0.607794576728214,
135.686823354664));
#106899=CARTESIAN_POINT('Ctrl Pts',(-131.396050306696,-0.471672908366999,
135.701856855441));
#106900=CARTESIAN_POINT('Ctrl Pts',(-131.403815059643,-0.335017807769798,
135.71118710023));
#106901=CARTESIAN_POINT('Ctrl Pts',(-131.411572100528,-0.198498434945009,
135.720508078089));
#106902=CARTESIAN_POINT('Ctrl Pts',(-131.419329141413,-0.0614470717679311,
135.72413704622));
#106903=CARTESIAN_POINT('Ctrl Pts',(-131.427086182298,0.0756235122200777,
135.72202918579));
#106904=CARTESIAN_POINT('Ctrl Pts',(-131.434837373538,0.212590730214261,
135.719922914914));
#106905=CARTESIAN_POINT('Ctrl Pts',(-131.442588564779,0.349576750831591,
135.712088432477));
#106906=CARTESIAN_POINT('Ctrl Pts',(-131.450339756019,0.486066295528583,
135.698532929495));
#106907=CARTESIAN_POINT('Ctrl Pts',(-131.458087652796,0.622497828528287,
135.684983187963));
#106908=CARTESIAN_POINT('Ctrl Pts',(-131.465835549573,0.758432917064726,
135.665717300684));
#106909=CARTESIAN_POINT('Ctrl Pts',(-131.47358344635,0.893359122356336,
135.64079448365));
#106910=CARTESIAN_POINT('Ctrl Pts',(-131.481329722434,1.02825710399447,
135.615876879932));
#106911=CARTESIAN_POINT('Ctrl Pts',(-131.489075998518,1.16214623793336,
135.585304771093));
#106912=CARTESIAN_POINT('Ctrl Pts',(-131.496822274602,1.29452242076377,
135.549188829908));
#106913=CARTESIAN_POINT('Ctrl Pts',(-131.504568607867,1.42689958076527,
135.513072622124));
#106914=CARTESIAN_POINT('Ctrl Pts',(-131.512314941133,1.55776339019342,
135.471412603239));
#106915=CARTESIAN_POINT('Ctrl Pts',(-131.520061274398,1.68662348222734,
135.424369740035));
#106916=CARTESIAN_POINT('Ctrl Pts',(-131.527809342401,1.81551243158525,
135.377316341909));
#106917=CARTESIAN_POINT('Ctrl Pts',(-131.535557410404,1.94239640346392,
135.324877834806));
#106918=CARTESIAN_POINT('Ctrl Pts',(-131.543305478407,2.06680401045092,
135.26726373604));
#106919=CARTESIAN_POINT('Ctrl Pts',(-131.551061781149,2.19134383932326,
135.209588404324));
#106920=CARTESIAN_POINT('Ctrl Pts',(-131.558818083891,2.31340169044591,
135.146726657301));
#106921=CARTESIAN_POINT('Ctrl Pts',(-131.566574386632,2.43252935031116,
135.078934751018));
#106922=CARTESIAN_POINT('Ctrl Pts',(-131.574334829147,2.55172059219534,
135.011106662153));
#106923=CARTESIAN_POINT('Ctrl Pts',(-131.582095271661,2.66797819531203,
134.93834337811));
#106924=CARTESIAN_POINT('Ctrl Pts',(-131.589855714175,2.78088291422556,
134.860944559736));
#106925=CARTESIAN_POINT('Ctrl Pts',(-131.59762861444,2.8939688778171,134.783421493906));
#106926=CARTESIAN_POINT('Ctrl Pts',(-131.605401514706,3.00369088844627,
134.701248258012));
#106927=CARTESIAN_POINT('Ctrl Pts',(-131.613174414971,3.10966207879219,
134.614765427848));
#106928=CARTESIAN_POINT('Ctrl Pts',(-131.620664750733,3.21178094944371,
134.531426466398));
#106929=CARTESIAN_POINT('Ctrl Pts',(-131.628155086495,3.31041673820338,
134.444086004235));
#106930=CARTESIAN_POINT('Ctrl Pts',(-131.635645422257,3.40525701023964,
134.353079788861));
#106931=CARTESIAN_POINT('Ctrl Pts',(-131.643419756376,3.50369318001663,
134.25862304517));
#106932=CARTESIAN_POINT('Ctrl Pts',(-131.651194090495,3.59835215369516,
134.159917876335));
#106933=CARTESIAN_POINT('Ctrl Pts',(-131.658968424614,3.68884502119521,
134.057298593013));
#106934=CARTESIAN_POINT('Ctrl Pts',(-131.666733177562,3.7792263643234,133.954805778786));
#106935=CARTESIAN_POINT('Ctrl Pts',(-131.674497930509,3.86545156100374,
133.848408738411));
#106936=CARTESIAN_POINT('Ctrl Pts',(-131.682262683456,3.94716678005073,
133.738480157217));
#106937=CARTESIAN_POINT('Ctrl Pts',(-131.690019724341,4.02880083839017,
133.62866075864));
#106938=CARTESIAN_POINT('Ctrl Pts',(-131.697776765226,4.10593360151946,
133.51531711122));
#106939=CARTESIAN_POINT('Ctrl Pts',(-131.705533806111,4.17825019762267,
133.39885639682));
#106940=CARTESIAN_POINT('Ctrl Pts',(-131.713284997351,4.25051225921813,
133.282483506351));
#106941=CARTESIAN_POINT('Ctrl Pts',(-131.721036188591,4.31796517747307,
133.162998558434));
#106942=CARTESIAN_POINT('Ctrl Pts',(-131.728787379831,4.38033648175365,
133.040838958422));
#106943=CARTESIAN_POINT('Ctrl Pts',(-131.736535276609,4.44268127656636,
132.918731279498));
#106944=CARTESIAN_POINT('Ctrl Pts',(-131.744283173386,4.49994857571334,
132.79395155696));
#106945=CARTESIAN_POINT('Ctrl Pts',(-131.752031070163,4.55191121360761,
132.666962927758));
#106946=CARTESIAN_POINT('Ctrl Pts',(-131.759777346247,4.60386298203822,
132.54000086184));
#106947=CARTESIAN_POINT('Ctrl Pts',(-131.767523622331,4.6505121483431,132.410831169927));
#106948=CARTESIAN_POINT('Ctrl Pts',(-131.775269898415,4.69167934445549,
132.279937789831));
#106949=CARTESIAN_POINT('Ctrl Pts',(-131.783016231681,4.73284684445472,
132.14904344351));
#106950=CARTESIAN_POINT('Ctrl Pts',(-131.790762564946,4.7685321762155,132.016425756573));
#106951=CARTESIAN_POINT('Ctrl Pts',(-131.798508898211,4.79860571040627,
131.882584294989));
#106952=CARTESIAN_POINT('Ctrl Pts',(-131.806256966214,4.82868597935646,
131.748712860539));
#106953=CARTESIAN_POINT('Ctrl Pts',(-131.814005034217,4.8531518643085,131.613617487485));
#106954=CARTESIAN_POINT('Ctrl Pts',(-131.82175310222,4.87192484170143,131.477808016635));
#106955=CARTESIAN_POINT('Ctrl Pts',(-131.829509404962,4.89071777123815,
131.341854205862));
#106956=CARTESIAN_POINT('Ctrl Pts',(-131.837265707704,4.90380565309088,
131.205185169105));
#106957=CARTESIAN_POINT('Ctrl Pts',(-131.845022010446,4.91116181237985,
131.068316513734));
#106958=CARTESIAN_POINT('Ctrl Pts',(-131.85278245296,4.91852189787253,130.93137480744));
#106959=CARTESIAN_POINT('Ctrl Pts',(-131.860542895475,4.92014416047835,
130.794233660985));
#106960=CARTESIAN_POINT('Ctrl Pts',(-131.868303337989,4.91605410095466,
130.657407771432));
#106961=CARTESIAN_POINT('Ctrl Pts',(-131.876076238254,4.91195747570431,
130.520362236814));
#106962=CARTESIAN_POINT('Ctrl Pts',(-131.88384913852,4.90213023193319,130.383633360589));
#106963=CARTESIAN_POINT('Ctrl Pts',(-131.891622038785,4.88664979446709,
130.247730714727));
#106964=CARTESIAN_POINT('Ctrl Pts',(-131.899112374547,4.87173210989633,
130.116768472365));
#106965=CARTESIAN_POINT('Ctrl Pts',(-131.906602710309,4.85156515860612,
129.986573736567));
#106966=CARTESIAN_POINT('Ctrl Pts',(-131.91409304607,4.82626253582105,129.857590847331));
#106967=CARTESIAN_POINT('Ctrl Pts',(-131.921867380189,4.80000055640159,
129.723717532642));
#106968=CARTESIAN_POINT('Ctrl Pts',(-131.929641714309,4.76812258983259,
129.590725702443));
#106969=CARTESIAN_POINT('Ctrl Pts',(-131.937416048428,4.73069968573992,
129.459123260874));
#106970=CARTESIAN_POINT('Ctrl Pts',(-131.945180801375,4.69332290203206,
129.327683007553));
#106971=CARTESIAN_POINT('Ctrl Pts',(-131.952945554322,4.65041488361725,
129.197629108347));
#106972=CARTESIAN_POINT('Ctrl Pts',(-131.960710307269,4.60209792682021,
129.069460696978));
#106973=CARTESIAN_POINT('Ctrl Pts',(-131.968467348154,4.55382895910582,
128.941419584282));
#106974=CARTESIAN_POINT('Ctrl Pts',(-131.976224389039,4.50016188101653,
128.815260596145));
#106975=CARTESIAN_POINT('Ctrl Pts',(-131.983981429924,4.44126907027835,
128.691468734887));
#106976=CARTESIAN_POINT('Ctrl Pts',(-131.991732621164,4.38242067106679,
128.567770226035));
#106977=CARTESIAN_POINT('Ctrl Pts',(-131.999483812404,4.31835455034131,
128.44643564261));
#106978=CARTESIAN_POINT('Ctrl Pts',(-132.007235003644,4.24929143257928,
128.327930650152));
#106979=CARTESIAN_POINT('Ctrl Pts',(-132.014982900421,4.1802576684847,128.209476025476));
#106980=CARTESIAN_POINT('Ctrl Pts',(-132.022730797198,4.10623132798939,
128.093848936864));
#106981=CARTESIAN_POINT('Ctrl Pts',(-132.030478693975,4.02747927277771,
127.981490841993));
#106982=CARTESIAN_POINT('Ctrl Pts',(-132.03822497006,3.94874369079828,127.869156250012));
#106983=CARTESIAN_POINT('Ctrl Pts',(-132.045971246144,3.86528458457376,
127.760089611603));
#106984=CARTESIAN_POINT('Ctrl Pts',(-132.053717522228,3.77741215187059,
127.654703414409));
#106985=CARTESIAN_POINT('Ctrl Pts',(-132.061463855493,3.68953907051297,
127.549316439277));
#106986=CARTESIAN_POINT('Ctrl Pts',(-132.069210188758,3.5972528480442,127.447610259849));
#106987=CARTESIAN_POINT('Ctrl Pts',(-132.076956522024,3.50090371564495,
127.349963964562));
#106988=CARTESIAN_POINT('Ctrl Pts',(-132.084704590027,3.40453300652541,
127.252295802065));
#106989=CARTESIAN_POINT('Ctrl Pts',(-132.092452658029,3.30409785150523,
127.158689611121));
#106990=CARTESIAN_POINT('Ctrl Pts',(-132.100200726032,3.19998475019136,
127.069487037237));
#106991=CARTESIAN_POINT('Ctrl Pts',(-132.107957028774,3.09576099623459,
126.980189657795));
#106992=CARTESIAN_POINT('Ctrl Pts',(-132.115713331516,2.98785178477408,
126.89530549943));
#106993=CARTESIAN_POINT('Ctrl Pts',(-132.123469634258,2.87667649246938,
126.815135702852));
#106994=CARTESIAN_POINT('Ctrl Pts',(-132.131230076772,2.76544186256376,
126.73492311724));
#106995=CARTESIAN_POINT('Ctrl Pts',(-132.138990519286,2.65093800457677,
126.659430122247));
#106996=CARTESIAN_POINT('Ctrl Pts',(-132.1467509618,2.5336117315085,126.588913469699));
#106997=CARTESIAN_POINT('Ctrl Pts',(-132.154523862066,2.41609711589096,
126.51828361756));
#106998=CARTESIAN_POINT('Ctrl Pts',(-132.162296762331,2.2957513746586,126.452646258678));
#106999=CARTESIAN_POINT('Ctrl Pts',(-132.170069662597,2.17304507515138,
126.392211689452));
#107000=CARTESIAN_POINT('Ctrl Pts',(-132.177559998359,2.05479945870645,
126.33397406904));
#107001=CARTESIAN_POINT('Ctrl Pts',(-132.185050334121,1.93436221038816,
126.280567661433));
#107002=CARTESIAN_POINT('Ctrl Pts',(-132.192540669883,1.81216856701536,
126.232137072373));
#107003=CARTESIAN_POINT('Ctrl Pts',(-132.200315004003,1.68534191451682,
126.181870222809));
#107004=CARTESIAN_POINT('Ctrl Pts',(-132.208089338122,1.55622130165177,
126.136804726185));
#107005=CARTESIAN_POINT('Ctrl Pts',(-132.215863672241,1.4252724466168,126.097155341034));
#107006=CARTESIAN_POINT('Ctrl Pts',(-132.223628425188,1.29448497434277,
126.057554820206));
#107007=CARTESIAN_POINT('Ctrl Pts',(-132.231393178135,1.16187411358247,
126.023357242052));
#107008=CARTESIAN_POINT('Ctrl Pts',(-132.239157931082,1.02792590382294,
125.99472950918));
#107009=CARTESIAN_POINT('Ctrl Pts',(-132.246914971967,0.894110733314049,
125.966130209777));
#107010=CARTESIAN_POINT('Ctrl Pts',(-132.254672012852,0.758961236987637,
125.943089827811));
#107011=CARTESIAN_POINT('Ctrl Pts',(-132.262429053737,0.622978635402561,
125.925725492623));
#107012=CARTESIAN_POINT('Ctrl Pts',(-132.270180244977,0.487098579354945,
125.908374252014));
#107013=CARTESIAN_POINT('Ctrl Pts',(-132.277931436217,0.3503870547914,125.896690587724));
#107014=CARTESIAN_POINT('Ctrl Pts',(-132.285682627457,0.213355146288797,
125.890740501597));
#107015=CARTESIAN_POINT('Ctrl Pts',(-132.293430524235,0.0763814800025666,
125.884792944416));
#107016=CARTESIAN_POINT('Ctrl Pts',(-132.301178421012,-0.0609119096081409,
125.884574135466));
#107017=CARTESIAN_POINT('Ctrl Pts',(-132.308926317789,-0.198009366438615,
125.890098175113));
#107018=CARTESIAN_POINT('Ctrl Pts',(-132.316672593873,-0.335078145436599,
125.89562105925));
#107019=CARTESIAN_POINT('Ctrl Pts',(-132.324418869957,-0.471950682774863,
125.906884386841));
#107020=CARTESIAN_POINT('Ctrl Pts',(-132.332165146041,-0.608112271447121,
125.923850139366));
#107021=CARTESIAN_POINT('Ctrl Pts',(-132.339911479307,-0.744274865233481,
125.940816017129));
#107022=CARTESIAN_POINT('Ctrl Pts',(-132.347657812572,-0.879726111916518,
125.963484355482));
#107023=CARTESIAN_POINT('Ctrl Pts',(-132.355404145837,-1.01395776514861,
125.991765401573));
#107024=CARTESIAN_POINT('Ctrl Pts',(-132.36315221384,-1.14821947862856,
126.020052781009));
#107025=CARTESIAN_POINT('Ctrl Pts',(-132.370900281843,-1.28126067268819,
126.053955288736));
#107026=CARTESIAN_POINT('Ctrl Pts',(-132.378648349846,-1.41258499880986,
126.09333241943));
#107027=CARTESIAN_POINT('Ctrl Pts',(-132.386404652588,-1.5440488979883,
126.132751400606));
#107028=CARTESIAN_POINT('Ctrl Pts',(-132.39416095533,-1.67379190908892,
126.177656515349));
#107029=CARTESIAN_POINT('Ctrl Pts',(-132.401917258072,-1.8013339905753,
126.227857704107));
#107030=CARTESIAN_POINT('Ctrl Pts',(-132.409677700586,-1.92894414511079,
126.278085686751));
#107031=CARTESIAN_POINT('Ctrl Pts',(-132.4174381431,-2.05435067202608,126.333615217581));
#107032=CARTESIAN_POINT('Ctrl Pts',(-132.425198585614,-2.17709604539738,
126.3942091608));
#107033=CARTESIAN_POINT('Ctrl Pts',(-132.43297148588,-2.30003846053883,
126.454900374796));
#107034=CARTESIAN_POINT('Ctrl Pts',(-132.440744386145,-2.42031084225733,
126.520672059507));
#107035=CARTESIAN_POINT('Ctrl Pts',(-132.448517286411,-2.53748190909566,
126.591241983643));
#107036=CARTESIAN_POINT('Ctrl Pts',(-132.456007622173,-2.65039351251482,
126.659246513279));
#107037=CARTESIAN_POINT('Ctrl Pts',(-132.463497957934,-2.76042511033644,
126.73170631341));
#107038=CARTESIAN_POINT('Ctrl Pts',(-132.470988293696,-2.86721978552152,
126.808333369909));
#107039=CARTESIAN_POINT('Ctrl Pts',(-132.479072401512,-2.98248026192425,
126.89103478758));
#107040=CARTESIAN_POINT('Ctrl Pts',(-132.487156509327,-3.09436571278089,
126.978875139808));
#107041=CARTESIAN_POINT('Ctrl Pts',(-132.495240617143,-3.20238339056155,
127.071543493415));
#107042=CARTESIAN_POINT('Ctrl Pts',(-132.502943127705,-3.30530226830804,
127.159837587047));
#107043=CARTESIAN_POINT('Ctrl Pts',(-132.510645638266,-3.40470975968766,
127.252514062167));
#107044=CARTESIAN_POINT('Ctrl Pts',(-132.518348148828,-3.50020783643636,
127.349258858681));
#107045=CARTESIAN_POINT('Ctrl Pts',(-132.526043707272,-3.59561971870363,
127.445916335452));
#107046=CARTESIAN_POINT('Ctrl Pts',(-132.533739265715,-3.68712892603642,
127.546634550249));
#107047=CARTESIAN_POINT('Ctrl Pts',(-132.541434824159,-3.77437097888463,
127.651059684218));
#107048=CARTESIAN_POINT('Ctrl Pts',(-132.549125169276,-3.86155392993868,
127.75541407578));
#107049=CARTESIAN_POINT('Ctrl Pts',(-132.556815514393,-3.94447522285435,
127.863470087221));
#107050=CARTESIAN_POINT('Ctrl Pts',(-132.564505859511,-4.02280804413306,
127.97483795419));
#107051=CARTESIAN_POINT('Ctrl Pts',(-132.572192725819,-4.10110543073162,
128.086155442726));
#107052=CARTESIAN_POINT('Ctrl Pts',(-132.579879592127,-4.17481824789527,
128.200781480837));
#107053=CARTESIAN_POINT('Ctrl Pts',(-132.587566458435,-4.24366101930423,
128.318294605623));
#107054=CARTESIAN_POINT('Ctrl Pts',(-132.595252924575,-4.31250020685146,
128.435801612835));
#107055=CARTESIAN_POINT('Ctrl Pts',(-132.602939390716,-4.37646964477829,
128.556195069042));
#107056=CARTESIAN_POINT('Ctrl Pts',(-132.610625856856,-4.43532825009467,
128.679026202371));
#107057=CARTESIAN_POINT('Ctrl Pts',(-132.618312117137,-4.49418527906035,
128.801854046037));
#107058=CARTESIAN_POINT('Ctrl Pts',(-132.625998377419,-4.54793158141725,
128.927119075682));
#107059=CARTESIAN_POINT('Ctrl Pts',(-132.6336846377,-4.59637328421861,129.054350419132));
#107060=CARTESIAN_POINT('Ctrl Pts',(-132.641374478885,-4.64483755521738,
129.181641037586));
#107061=CARTESIAN_POINT('Ctrl Pts',(-132.649064320069,-4.68799215692162,
129.310899424951));
#107062=CARTESIAN_POINT('Ctrl Pts',(-132.656754161253,-4.72569239232696,
129.441637433789));
#107063=CARTESIAN_POINT('Ctrl Pts',(-132.659505067925,-4.73917899453737,
129.488406678066));
#107064=CARTESIAN_POINT('Ctrl Pts',(-132.662255974597,-4.7519680557209,
129.535365146417));
#107065=CARTESIAN_POINT('Ctrl Pts',(-132.66500688127,-4.76405452823412,
129.582490119309));
#107066=CARTESIAN_POINT('Ctrl Pts',(-130.915253971501,-4.76405452823413,
129.582490119309));
#107067=CARTESIAN_POINT('Ctrl Pts',(-130.92299794964,-4.7981437664688,129.715403541809));
#107068=CARTESIAN_POINT('Ctrl Pts',(-130.93074192778,-4.82667793081882,
129.849789113317));
#107069=CARTESIAN_POINT('Ctrl Pts',(-130.938485905919,-4.84954285845313,
129.985143230955));
#107070=CARTESIAN_POINT('Ctrl Pts',(-130.946261682268,-4.87250167371655,
130.121053137677));
#107071=CARTESIAN_POINT('Ctrl Pts',(-130.954037458616,-4.8897444930153,
130.257939177433));
#107072=CARTESIAN_POINT('Ctrl Pts',(-130.961813234965,-4.90120780769012,
130.395282277468));
#107073=CARTESIAN_POINT('Ctrl Pts',(-130.969589011313,-4.91267112236497,
130.532625377503));
#107074=CARTESIAN_POINT('Ctrl Pts',(-130.977364787662,-4.91835491001948,
130.67042514003));
#107075=CARTESIAN_POINT('Ctrl Pts',(-130.98514056401,-4.91824853312675,
130.808159156306));
#107076=CARTESIAN_POINT('',(-130.639859435939,-4.91824874376019,130.800845364896));
#107077=CARTESIAN_POINT('Ctrl Pts',(-130.570084224261,-4.7640545282341,
129.582490119308));
#107078=CARTESIAN_POINT('Ctrl Pts',(-130.579013117024,-4.80305957932508,
129.734570221528));
#107079=CARTESIAN_POINT('Ctrl Pts',(-130.587942009788,-4.83482173916823,
129.888688219058));
#107080=CARTESIAN_POINT('Ctrl Pts',(-130.596870902552,-4.85914920758507,
130.044194819253));
#107081=CARTESIAN_POINT('Ctrl Pts',(-130.605735204511,-4.88330069329145,
130.19857649874));
#107082=CARTESIAN_POINT('Ctrl Pts',(-130.61459950647,-4.90012458017203,
130.354326617327));
#107083=CARTESIAN_POINT('Ctrl Pts',(-130.62346380843,-4.90948058058899,
130.510790368189));
#107084=CARTESIAN_POINT('Ctrl Pts',(-130.628929017599,-4.9152489422156,
130.607256748715));
#107085=CARTESIAN_POINT('Ctrl Pts',(-130.634394226769,-4.91817952055531,
130.703994022351));
#107086=CARTESIAN_POINT('Ctrl Pts',(-130.639859435938,-4.91824874376019,
130.800845364897));
#107087=CARTESIAN_POINT('Ctrl Pts',(-130.639859435993,-4.91824874376088,
130.800845365864));
#107088=CARTESIAN_POINT('Ctrl Pts',(-130.647629166547,-4.91834715637149,
130.938536131584));
#107089=CARTESIAN_POINT('Ctrl Pts',(-130.655398897101,-4.91265908930728,
131.076274163644));
#107090=CARTESIAN_POINT('Ctrl Pts',(-130.663168627655,-4.90119937108808,
131.213540024851));
#107091=CARTESIAN_POINT('Ctrl Pts',(-130.67093798899,-4.88974019743642,
131.350799363162));
#107092=CARTESIAN_POINT('Ctrl Pts',(-130.678707350325,-4.87250994982521,
131.487586189239));
#107093=CARTESIAN_POINT('Ctrl Pts',(-130.68647671166,-4.84957544445324,
131.623385080605));
#107094=CARTESIAN_POINT('Ctrl Pts',(-130.694247346629,-4.82663717942049,
131.759206233527));
#107095=CARTESIAN_POINT('Ctrl Pts',(-130.702017981599,-4.79799285950334,
131.894038747379));
#107096=CARTESIAN_POINT('Ctrl Pts',(-130.709788616568,-4.76376057953252,
132.027376645013));
#107097=CARTESIAN_POINT('Ctrl Pts',(-130.71756216849,-4.72951544939281,
132.160764595244));
#107098=CARTESIAN_POINT('Ctrl Pts',(-130.725335720413,-4.68967827999649,
132.292656437506));
#107099=CARTESIAN_POINT('Ctrl Pts',(-130.733109272335,-4.64441715469809,
132.422560962284));
#107100=CARTESIAN_POINT('Ctrl Pts',(-130.740892326663,-4.59910070210849,
132.552624282617));
#107101=CARTESIAN_POINT('Ctrl Pts',(-130.748675380992,-4.54834717913024,
132.680695067481));
#107102=CARTESIAN_POINT('Ctrl Pts',(-130.75645843532,-4.49237322879146,
132.806301135098));
#107103=CARTESIAN_POINT('Ctrl Pts',(-130.764246603688,-4.43636249944749,
132.931989735147));
#107104=CARTESIAN_POINT('Ctrl Pts',(-130.772034772055,-4.37512468040176,
133.055210045001));
#107105=CARTESIAN_POINT('Ctrl Pts',(-130.779822940423,-4.30892214772164,
133.175514975126));
#107106=CARTESIAN_POINT('Ctrl Pts',(-130.787623850887,-4.2426113021474,
133.296016734203));
#107107=CARTESIAN_POINT('Ctrl Pts',(-130.795424761352,-4.17131971689215,
133.413593254228));
#107108=CARTESIAN_POINT('Ctrl Pts',(-130.803225671816,-4.09535325298106,
133.527826203138));
#107109=CARTESIAN_POINT('Ctrl Pts',(-130.808780963536,-4.04125496920386,
133.60917534286));
#107110=CARTESIAN_POINT('Ctrl Pts',(-130.814336255257,-3.98478678623946,
133.688829483076));
#107111=CARTESIAN_POINT('Ctrl Pts',(-130.819891546978,-3.92607112147604,
133.766648350318));
#107112=CARTESIAN_POINT('Ctrl Pts',(-130.827665881097,-3.84390168396533,
133.875551699615));
#107113=CARTESIAN_POINT('Ctrl Pts',(-130.835440215216,-3.75706743757816,
133.981206066808));
#107114=CARTESIAN_POINT('Ctrl Pts',(-130.843214549335,-3.66585441934026,
134.083185778916));
#107115=CARTESIAN_POINT('Ctrl Pts',(-130.850979302282,-3.5747538129954,
134.185039810144));
#107116=CARTESIAN_POINT('Ctrl Pts',(-130.858744055229,-3.47928543025752,
134.283227908407));
#107117=CARTESIAN_POINT('Ctrl Pts',(-130.866508808176,-3.37977755735265,
134.377354701708));
#107118=CARTESIAN_POINT('Ctrl Pts',(-130.874265849061,-3.28036851706996,
134.471388006951));
#107119=CARTESIAN_POINT('Ctrl Pts',(-130.882022889946,-3.17692825302688,
134.561367767638));
#107120=CARTESIAN_POINT('Ctrl Pts',(-130.889779930831,-3.06982390797201,
134.646933224108));
#107121=CARTESIAN_POINT('Ctrl Pts',(-130.897531122071,-2.96280033113704,
134.732434155001));
#107122=CARTESIAN_POINT('Ctrl Pts',(-130.905282313312,-2.85211847731784,
134.813527164532));
#107123=CARTESIAN_POINT('Ctrl Pts',(-130.913033504552,-2.73818050915732,
134.889890027786));
#107124=CARTESIAN_POINT('Ctrl Pts',(-130.920781401329,-2.62429096767219,
134.966220434786));
#107125=CARTESIAN_POINT('Ctrl Pts',(-130.928529298106,-2.50714838847784,
135.037824476906));
#107126=CARTESIAN_POINT('Ctrl Pts',(-130.936277194883,-2.38718583663365,
135.104421878045));
#107127=CARTESIAN_POINT('Ctrl Pts',(-130.944023470967,-2.26724837836954,
135.171005348444));
#107128=CARTESIAN_POINT('Ctrl Pts',(-130.951769747052,-2.14449246236137,
135.232584071319));
#107129=CARTESIAN_POINT('Ctrl Pts',(-130.959516023136,-2.01937745424393,
135.288922776773));
#107130=CARTESIAN_POINT('Ctrl Pts',(-130.967262356401,-1.89426152255575,
135.345261898107));
#107131=CARTESIAN_POINT('Ctrl Pts',(-130.975008689667,-1.76678682049953,
135.396360764311));
#107132=CARTESIAN_POINT('Ctrl Pts',(-130.982755022932,-1.63743410706188,
135.442031650264));
#107133=CARTESIAN_POINT('Ctrl Pts',(-130.990503090935,-1.5080524259811,
135.487712763896));
#107134=CARTESIAN_POINT('Ctrl Pts',(-130.998251158938,-1.37679226522868,
135.527963348317));
#107135=CARTESIAN_POINT('Ctrl Pts',(-131.005999226941,-1.24415062274655,
135.562645212924));
#107136=CARTESIAN_POINT('Ctrl Pts',(-131.013755529683,-1.11136800714816,
135.597363937829));
#107137=CARTESIAN_POINT('Ctrl Pts',(-131.021511832425,-0.977201355674347,
135.626502021016));
#107138=CARTESIAN_POINT('Ctrl Pts',(-131.029268135167,-0.842159516251782,
135.649972076576));
#107139=CARTESIAN_POINT('Ctrl Pts',(-131.037028577681,-0.707045600933118,
135.67345465881));
#107140=CARTESIAN_POINT('Ctrl Pts',(-131.044789020195,-0.571055954366869,
135.691263134715));
#107141=CARTESIAN_POINT('Ctrl Pts',(-131.05254946271,-0.434704682944541,
135.703362036338));
#107142=CARTESIAN_POINT('Ctrl Pts',(-131.060322362975,-0.298134528357001,
135.715480360191));
#107143=CARTESIAN_POINT('Ctrl Pts',(-131.068095263241,-0.161201979629705,
135.721870775904));
#107144=CARTESIAN_POINT('Ctrl Pts',(-131.075868163506,-0.02442218661788,
135.722549981478));
#107145=CARTESIAN_POINT('Ctrl Pts',(-131.083358499268,0.107385316386014,
135.723204496219));
#107146=CARTESIAN_POINT('Ctrl Pts',(-131.09084883503,0.239050669139419,
135.71855583637));
#107147=CARTESIAN_POINT('Ctrl Pts',(-131.098339170792,0.370119225138331,
135.708664321629));
#107148=CARTESIAN_POINT('Ctrl Pts',(-131.106113504911,0.506157285279768,
135.698397767099));
#107149=CARTESIAN_POINT('Ctrl Pts',(-131.11388783903,0.641983327902732,
135.682450422559));
#107150=CARTESIAN_POINT('Ctrl Pts',(-131.121662173149,0.777084612274554,
135.660832852416));
#107151=CARTESIAN_POINT('Ctrl Pts',(-131.129426926096,0.912019396387003,
135.639241923996));
#107152=CARTESIAN_POINT('Ctrl Pts',(-131.137191679043,1.0462308171014,135.611994735283));
#107153=CARTESIAN_POINT('Ctrl Pts',(-131.14495643199,1.17920879003412,135.579153774553));
#107154=CARTESIAN_POINT('Ctrl Pts',(-131.152713472875,1.31205468736982,
135.546345431928));
#107155=CARTESIAN_POINT('Ctrl Pts',(-131.16047051376,1.44366919777849,135.507954466737));
#107156=CARTESIAN_POINT('Ctrl Pts',(-131.168227554645,1.57355035431707,
135.464094767164));
#107157=CARTESIAN_POINT('Ctrl Pts',(-131.175978745885,1.70333356646536,
135.420268142532));
#107158=CARTESIAN_POINT('Ctrl Pts',(-131.183729937125,1.83138565760149,
135.370981116699));
#107159=CARTESIAN_POINT('Ctrl Pts',(-131.191481128366,1.95721815204557,
135.31639787005));
#107160=CARTESIAN_POINT('Ctrl Pts',(-131.199229025143,2.08299716432264,
135.261837822737));
#107161=CARTESIAN_POINT('Ctrl Pts',(-131.20697692192,2.20655809831076,135.201986187003));
#107162=CARTESIAN_POINT('Ctrl Pts',(-131.214724818697,2.32743106754529,
135.137055816668));
#107163=CARTESIAN_POINT('Ctrl Pts',(-131.222471094781,2.44827875276039,
135.072139028368));
#107164=CARTESIAN_POINT('Ctrl Pts',(-131.230217370865,2.56643924739674,
135.00214580346));
#107165=CARTESIAN_POINT('Ctrl Pts',(-131.237963646949,2.68146631388185,
134.927335450137));
#107166=CARTESIAN_POINT('Ctrl Pts',(-131.245709980214,2.79649422947079,
134.852524544582));
#107167=CARTESIAN_POINT('Ctrl Pts',(-131.25345631348,2.90838834300716,134.772896652813));
#107168=CARTESIAN_POINT('Ctrl Pts',(-131.261202646745,3.01673085405499,
134.688754780971));
#107169=CARTESIAN_POINT('Ctrl Pts',(-131.268950714748,3.12509762765683,
134.604594066139));
#107170=CARTESIAN_POINT('Ctrl Pts',(-131.276698782751,3.22991090738022,
134.515917599473));
#107171=CARTESIAN_POINT('Ctrl Pts',(-131.284446850754,3.33078579002894,
134.423068824018));
#107172=CARTESIAN_POINT('Ctrl Pts',(-131.292203153496,3.4317678837035,134.330121367779));
#107173=CARTESIAN_POINT('Ctrl Pts',(-131.299959456238,3.52880293064662,
134.232993009798));
#107174=CARTESIAN_POINT('Ctrl Pts',(-131.307715758979,3.62154236588328,
134.132064624026));
#107175=CARTESIAN_POINT('Ctrl Pts',(-131.315476201494,3.71433129894887,
134.031082369736));
#107176=CARTESIAN_POINT('Ctrl Pts',(-131.323236644008,3.80281979979047,
133.926296344877));
#107177=CARTESIAN_POINT('Ctrl Pts',(-131.330997086522,3.8867001411524,133.81811991042));
#107178=CARTESIAN_POINT('Ctrl Pts',(-131.338769986787,3.97071513468482,
133.709769821548));
#107179=CARTESIAN_POINT('Ctrl Pts',(-131.346542887053,4.05010695976115,
133.59801876596));
#107180=CARTESIAN_POINT('Ctrl Pts',(-131.354315787318,4.12461121380186,
133.483309179498));
#107181=CARTESIAN_POINT('Ctrl Pts',(-131.36180612308,4.19640705054329,133.37276957544));
#107182=CARTESIAN_POINT('Ctrl Pts',(-131.369296458842,4.26366434062614,
133.259483071011));
#107183=CARTESIAN_POINT('Ctrl Pts',(-131.376786794604,4.32618808517848,
133.14386477746));
#107184=CARTESIAN_POINT('Ctrl Pts',(-131.384561128723,4.39108243650947,
133.023862781166));
#107185=CARTESIAN_POINT('Ctrl Pts',(-131.392335462842,4.45108277766888,
132.900968555455));
#107186=CARTESIAN_POINT('Ctrl Pts',(-131.400109796961,4.50592084790166,
132.775619193944));
#107187=CARTESIAN_POINT('Ctrl Pts',(-131.407874549909,4.56069133511359,
132.65042431432));
#107188=CARTESIAN_POINT('Ctrl Pts',(-131.415639302856,4.61031205476097,
132.522780673959));
#107189=CARTESIAN_POINT('Ctrl Pts',(-131.423404055803,4.65455986693211,
132.393151197739));
#107190=CARTESIAN_POINT('Ctrl Pts',(-131.431161096688,4.69876373155253,
132.263650471341));
#107191=CARTESIAN_POINT('Ctrl Pts',(-131.438918137573,4.73760518298785,
132.13216820178));
#107192=CARTESIAN_POINT('Ctrl Pts',(-131.446675178458,4.77090871319876,
131.999188267407));
#107193=CARTESIAN_POINT('Ctrl Pts',(-131.454426369698,4.80418712895843,
131.866308614236));
#107194=CARTESIAN_POINT('Ctrl Pts',(-131.462177560938,4.83193584134976,
131.731933921975));
#107195=CARTESIAN_POINT('Ctrl Pts',(-131.469928752178,4.85402894694235,
131.596563902554));
#107196=CARTESIAN_POINT('Ctrl Pts',(-131.477676648955,4.87611266237567,
131.461251419003));
#107197=CARTESIAN_POINT('Ctrl Pts',(-131.485424545732,4.8925454891103,131.324944834739));
#107198=CARTESIAN_POINT('Ctrl Pts',(-131.49317244251,4.90325252198212,131.188154531244));
#107199=CARTESIAN_POINT('Ctrl Pts',(-131.500918718594,4.9139573151735,131.05139284133));
#107200=CARTESIAN_POINT('Ctrl Pts',(-131.508664994678,4.91893866632863,
130.914148022971));
#107201=CARTESIAN_POINT('Ctrl Pts',(-131.516411270762,4.91817353646652,
130.776935670886));
#107202=CARTESIAN_POINT('Ctrl Pts',(-131.524157604027,4.91740840095639,
130.63972230593));
#107203=CARTESIAN_POINT('Ctrl Pts',(-131.531903937293,4.91089670196464,
130.502541798686));
#107204=CARTESIAN_POINT('Ctrl Pts',(-131.539650270558,4.89866753579594,
130.365909438711));
#107205=CARTESIAN_POINT('Ctrl Pts',(-131.547398338561,4.88643563099029,
130.229246480868));
#107206=CARTESIAN_POINT('Ctrl Pts',(-131.555146406564,4.86848374603258,
130.093132303893));
#107207=CARTESIAN_POINT('Ctrl Pts',(-131.562894474567,4.84489277970605,
129.958076377105));
#107208=CARTESIAN_POINT('Ctrl Pts',(-131.570650777309,4.82127674061974,
129.822876911271));
#107209=CARTESIAN_POINT('Ctrl Pts',(-131.578407080051,4.79200971531739,
129.688738328121));
#107210=CARTESIAN_POINT('Ctrl Pts',(-131.586163382793,4.7572237359593,129.556159756917));
#107211=CARTESIAN_POINT('Ctrl Pts',(-131.593923825307,4.72241919027664,
129.423510424537));
#107212=CARTESIAN_POINT('Ctrl Pts',(-131.601684267821,4.68208993602448,
129.292423136677));
#107213=CARTESIAN_POINT('Ctrl Pts',(-131.609444710335,4.63641741139761,
129.163380224694));
#107214=CARTESIAN_POINT('Ctrl Pts',(-131.617217610601,4.59067156917959,
129.034130161574));
#107215=CARTESIAN_POINT('Ctrl Pts',(-131.624990510866,4.53956546186643,
128.906931395427));
#107216=CARTESIAN_POINT('Ctrl Pts',(-131.632763411131,4.48332840720811,
128.782245523013));
#107217=CARTESIAN_POINT('Ctrl Pts',(-131.640253746893,4.42913571113982,
128.662092296126));
#107218=CARTESIAN_POINT('Ctrl Pts',(-131.647744082655,4.37017877466386,
128.544272710335));
#107219=CARTESIAN_POINT('Ctrl Pts',(-131.655234418417,4.30670144097751,
128.429175201481));
#107220=CARTESIAN_POINT('Ctrl Pts',(-131.663008752536,4.2408173448901,128.309713735595));
#107221=CARTESIAN_POINT('Ctrl Pts',(-131.670783086655,4.16985460224,128.192806418424));
#107222=CARTESIAN_POINT('Ctrl Pts',(-131.678557420775,4.09403595077842,
128.078915205118));
#107223=CARTESIAN_POINT('Ctrl Pts',(-131.686322173722,4.01831073902906,
127.965164352554));
#107224=CARTESIAN_POINT('Ctrl Pts',(-131.694086926669,3.93774174036037,
127.854422530299));
#107225=CARTESIAN_POINT('Ctrl Pts',(-131.701851679616,3.85259781401043,
127.747127694483));
#107226=CARTESIAN_POINT('Ctrl Pts',(-131.709608720501,3.767538453808,127.639939425411));
#107227=CARTESIAN_POINT('Ctrl Pts',(-131.717365761386,3.67791344991105,
127.53619163394));
#107228=CARTESIAN_POINT('Ctrl Pts',(-131.725122802271,3.58403503649811,
127.436293528024));
#107229=CARTESIAN_POINT('Ctrl Pts',(-131.732873993511,3.49022741752687,
127.336470756047));
#107230=CARTESIAN_POINT('Ctrl Pts',(-131.740625184751,3.39217304008557,
127.240492174976));
#107231=CARTESIAN_POINT('Ctrl Pts',(-131.748376375991,3.29022427209507,
127.148733817438));
#107232=CARTESIAN_POINT('Ctrl Pts',(-131.756124272768,3.18831883505097,
127.05701445965));
#107233=CARTESIAN_POINT('Ctrl Pts',(-131.763872169546,3.08252258955126,
126.969512018848));
#107234=CARTESIAN_POINT('Ctrl Pts',(-131.771620066323,2.97322444591885,
126.886565388526));
#107235=CARTESIAN_POINT('Ctrl Pts',(-131.779366342407,2.86394916510189,
126.80363610885));
#107236=CARTESIAN_POINT('Ctrl Pts',(-131.787112618491,2.75117375441684,
126.72526098033));
#107237=CARTESIAN_POINT('Ctrl Pts',(-131.794858894575,2.6353195451722,126.651738077853));
#107238=CARTESIAN_POINT('Ctrl Pts',(-131.80260522784,2.51946448071794,126.578214632646));
#107239=CARTESIAN_POINT('Ctrl Pts',(-131.810351561106,2.4005309024574,126.509543694443));
#107240=CARTESIAN_POINT('Ctrl Pts',(-131.818097894371,2.27896806535331,
126.445979310292));
#107241=CARTESIAN_POINT('Ctrl Pts',(-131.825845962374,2.15737800509455,
126.382400691337));
#107242=CARTESIAN_POINT('Ctrl Pts',(-131.833594030377,2.03315786073327,
126.323931083147));
#107243=CARTESIAN_POINT('Ctrl Pts',(-131.84134209838,1.90677999100253,126.270777803895));
#107244=CARTESIAN_POINT('Ctrl Pts',(-131.849098401122,1.7802678053681,126.217568032705));
#107245=CARTESIAN_POINT('Ctrl Pts',(-131.856854703864,1.65159367429952,
126.169686029268));
#107246=CARTESIAN_POINT('Ctrl Pts',(-131.864611006606,1.52124889598726,
126.127290502744));
#107247=CARTESIAN_POINT('Ctrl Pts',(-131.87237144912,1.39083454874222,126.084872348452));
#107248=CARTESIAN_POINT('Ctrl Pts',(-131.880131891634,1.25874815386053,
126.047946611165));
#107249=CARTESIAN_POINT('Ctrl Pts',(-131.887892334148,1.12549358215017,
126.016621353671));
#107250=CARTESIAN_POINT('Ctrl Pts',(-131.895665234413,0.992025098371515,
125.985245810094));
#107251=CARTESIAN_POINT('Ctrl Pts',(-131.903438134679,0.857385074617616,
125.959488785472));
#107252=CARTESIAN_POINT('Ctrl Pts',(-131.911211034944,0.722085817158509,
125.93940685261));
#107253=CARTESIAN_POINT('Ctrl Pts',(-131.918701370706,0.591705028507405,
125.920054948591));
#107254=CARTESIAN_POINT('Ctrl Pts',(-131.926191706468,0.460712409888022,
125.905972724972));
#107255=CARTESIAN_POINT('Ctrl Pts',(-131.93368204223,0.329566566580926,
125.897164988626));
#107256=CARTESIAN_POINT('Ctrl Pts',(-131.941456376349,0.193448288762958,
125.888023304278));
#107257=CARTESIAN_POINT('Ctrl Pts',(-131.949230710468,0.0567337560766165,
125.884535008888));
#107258=CARTESIAN_POINT('Ctrl Pts',(-131.957005044587,-0.0800679803326742,
125.886762404919));
#107259=CARTESIAN_POINT('Ctrl Pts',(-131.964769797534,-0.216701120827791,
125.888987055884));
#107260=CARTESIAN_POINT('Ctrl Pts',(-131.972534550481,-0.353420864050336,
125.896913376348));
#107261=CARTESIAN_POINT('Ctrl Pts',(-131.980299303428,-0.489713420117738,
125.910551893407));
#107262=CARTESIAN_POINT('Ctrl Pts',(-131.988056344313,-0.625870608496693,
125.924176864498));
#107263=CARTESIAN_POINT('Ctrl Pts',(-131.995813385198,-0.761601067568436,
125.943502703118));
#107264=CARTESIAN_POINT('Ctrl Pts',(-132.003570426083,-0.896391748893166,
125.968487904703));
#107265=CARTESIAN_POINT('Ctrl Pts',(-132.011321617323,-1.03108078351677,
125.993454264752));
#107266=CARTESIAN_POINT('Ctrl Pts',(-132.019072808563,-1.16483106814385,
126.024071422061));
#107267=CARTESIAN_POINT('Ctrl Pts',(-132.026823999803,-1.29713577240741,
126.060246174338));
#107268=CARTESIAN_POINT('Ctrl Pts',(-132.03457189658,-1.4293842436425,126.096405551381));
#107269=CARTESIAN_POINT('Ctrl Pts',(-132.042319793357,-1.56018798019597,
126.138117722406));
#107270=CARTESIAN_POINT('Ctrl Pts',(-132.050067690134,-1.68905164584534,
126.185238666354));
#107271=CARTESIAN_POINT('Ctrl Pts',(-132.057813966218,-1.81788835599383,
126.232349753617));
#107272=CARTESIAN_POINT('Ctrl Pts',(-132.065560242303,-1.94478543548438,
126.284867229208));
#107273=CARTESIAN_POINT('Ctrl Pts',(-132.073306518387,-2.06926436560832,
126.342597731921));
#107274=CARTESIAN_POINT('Ctrl Pts',(-132.081052851652,-2.19374421460728,
126.400328660787));
#107275=CARTESIAN_POINT('Ctrl Pts',(-132.088799184917,-2.31580552394301,
126.463272529071));
#107276=CARTESIAN_POINT('Ctrl Pts',(-132.096545518183,-2.43499172335814,
126.531188684484));
#107277=CARTESIAN_POINT('Ctrl Pts',(-132.104293586185,-2.55420461369674,
126.59912004925));
#107278=CARTESIAN_POINT('Ctrl Pts',(-132.112041654188,-2.67054077328484,
126.672025723372));
#107279=CARTESIAN_POINT('Ctrl Pts',(-132.119789722191,-2.78357045803926,
126.749620358606));
#107280=CARTESIAN_POINT('Ctrl Pts',(-132.127546024933,-2.89672027208725,
126.827297462342));
#107281=CARTESIAN_POINT('Ctrl Pts',(-132.135302327675,-3.00655626855044,
126.909673260609));
#107282=CARTESIAN_POINT('Ctrl Pts',(-132.143058630417,-3.11267936224403,
126.996420196504));
#107283=CARTESIAN_POINT('Ctrl Pts',(-132.150819072931,-3.21885909702832,
127.08321343185));
#107284=CARTESIAN_POINT('Ctrl Pts',(-132.158579515445,-3.32132168842245,
127.17438219378));
#107285=CARTESIAN_POINT('Ctrl Pts',(-132.166339957959,-3.41970386566228,
127.269560972088));
#107286=CARTESIAN_POINT('Ctrl Pts',(-132.174112858225,-3.51824397470698,
127.36489253982));
#107287=CARTESIAN_POINT('Ctrl Pts',(-132.18188575849,-3.61269031060273,
127.464246704048));
#107288=CARTESIAN_POINT('Ctrl Pts',(-132.189658658755,-3.70271836299404,
127.567223025982));
#107289=CARTESIAN_POINT('Ctrl Pts',(-132.197148994518,-3.78947366891736,
127.666455899235));
#107290=CARTESIAN_POINT('Ctrl Pts',(-132.20463933028,-3.87212615251791,
127.769051913344));
#107291=CARTESIAN_POINT('Ctrl Pts',(-132.212129666042,-3.95042388228051,
127.87462782893));
#107292=CARTESIAN_POINT('Ctrl Pts',(-132.21994674266,-4.0321370887297,127.98480914086));
#107293=CARTESIAN_POINT('Ctrl Pts',(-132.227763819277,-4.10936709823398,
128.098586714222));
#107294=CARTESIAN_POINT('Ctrl Pts',(-132.235580895894,-4.18178267079426,
128.215562294648));
#107295=CARTESIAN_POINT('Ctrl Pts',(-132.243384955992,-4.25407766135055,
128.332343094456));
#107296=CARTESIAN_POINT('Ctrl Pts',(-132.251189016089,-4.32157398171214,
128.452310969956));
#107297=CARTESIAN_POINT('Ctrl Pts',(-132.258993076186,-4.38398164243891,
128.575036051412));
#107298=CARTESIAN_POINT('Ctrl Pts',(-132.266789639672,-4.44632935411981,
128.697643242669));
#107299=CARTESIAN_POINT('Ctrl Pts',(-132.274586203158,-4.50359795612399,
128.82300203038));
#107300=CARTESIAN_POINT('Ctrl Pts',(-132.282382766644,-4.55554141719004,
128.950654745868));
#107301=CARTESIAN_POINT('Ctrl Pts',(-132.290172170143,-4.60743717589171,
129.078190231272));
#107302=CARTESIAN_POINT('Ctrl Pts',(-132.297961573642,-4.65401738723624,
129.2080150941));
#107303=CARTESIAN_POINT('Ctrl Pts',(-132.305750977141,-4.69508279439975,
129.339648831503));
#107304=CARTESIAN_POINT('Ctrl Pts',(-132.310503412346,-4.7201374326307,
129.41996060478));
#107305=CARTESIAN_POINT('Ctrl Pts',(-132.315255847551,-4.74314014747024,
129.50094526613));
#107306=CARTESIAN_POINT('Ctrl Pts',(-132.320008282756,-4.76405452823418,
129.582490119309));
#107307=CARTESIAN_POINT('Origin',(213.235140564004,0.,130.804360617566));
#107308=CARTESIAN_POINT('',(-134.415184333433,-4.76405452823396,129.582490119308));
#107309=CARTESIAN_POINT('',(-134.069717999649,-4.76405452823413,129.582490119309));
#107310=CARTESIAN_POINT('',(213.235140564004,-4.76405452823405,129.582490119308));
#107311=CARTESIAN_POINT('',(-132.735140563954,-4.9182497588907,130.805900640808));
#107312=CARTESIAN_POINT('Ctrl Pts',(-132.73514056401,-4.91824975889039,
130.805900641798));
#107313=CARTESIAN_POINT('Ctrl Pts',(-132.739905681843,-4.91822356444062,
130.88955571917));
#107314=CARTESIAN_POINT('Ctrl Pts',(-132.744670799676,-4.91606315597891,
130.973174771754));
#107315=CARTESIAN_POINT('Ctrl Pts',(-132.749435917509,-4.91177322663725,
131.056683491261));
#107316=CARTESIAN_POINT('Ctrl Pts',(-132.757210251628,-4.90477416696683,
131.192928744802));
#107317=CARTESIAN_POINT('Ctrl Pts',(-132.764984585747,-4.89209086537747,
131.329098365177));
#107318=CARTESIAN_POINT('Ctrl Pts',(-132.772758919866,-4.8737215788707,
131.464679505794));
#107319=CARTESIAN_POINT('Ctrl Pts',(-132.780523672813,-4.85537493086784,
131.600093554771));
#107320=CARTESIAN_POINT('Ctrl Pts',(-132.78828842576,-4.83135629270741,
131.734920183313));
#107321=CARTESIAN_POINT('Ctrl Pts',(-132.796053178707,-4.80171589405253,
131.86864795438));
#107322=CARTESIAN_POINT('Ctrl Pts',(-132.803810219592,-4.77210493465952,
132.00224290514));
#107323=CARTESIAN_POINT('Ctrl Pts',(-132.811567260477,-4.73688341046714,
132.13474079113));
#107324=CARTESIAN_POINT('Ctrl Pts',(-132.819324301362,-4.69615313103981,
132.265637056959));
#107325=CARTESIAN_POINT('Ctrl Pts',(-132.827075492602,-4.65545356663297,
132.396434612896));
#107326=CARTESIAN_POINT('Ctrl Pts',(-132.834826683842,-4.60925363135559,
132.525632580914));
#107327=CARTESIAN_POINT('Ctrl Pts',(-132.842577875082,-4.55770573624154,
132.652738686125));
#107328=CARTESIAN_POINT('Ctrl Pts',(-132.850325771859,-4.50617975035794,
132.779790767851));
#107329=CARTESIAN_POINT('Ctrl Pts',(-132.858073668637,-4.4493104721373,
132.904752393572));
#107330=CARTESIAN_POINT('Ctrl Pts',(-132.865821565414,-4.38729941812407,
133.027148704233));
#107331=CARTESIAN_POINT('Ctrl Pts',(-132.873567841498,-4.32530133548654,
133.149519412224));
#107332=CARTESIAN_POINT('Ctrl Pts',(-132.881314117582,-4.25816379296523,
133.269325523963));
#107333=CARTESIAN_POINT('Ctrl Pts',(-132.889060393666,-4.18613531560761,
133.3861147077));
#107334=CARTESIAN_POINT('Ctrl Pts',(-132.896806726931,-4.11410630655223,
133.502904753548));
#107335=CARTESIAN_POINT('Ctrl Pts',(-132.904553060197,-4.03718649584882,
133.616677494188));
#107336=CARTESIAN_POINT('Ctrl Pts',(-132.912299393462,-3.95566877631886,
133.727007978189));
#107337=CARTESIAN_POINT('Ctrl Pts',(-132.920047461465,-3.87413280146092,
133.837363169937));
#107338=CARTESIAN_POINT('Ctrl Pts',(-132.927795529468,-3.78799710113754,
133.944274256717));
#107339=CARTESIAN_POINT('Ctrl Pts',(-132.935543597471,-3.69759578287759,
134.04734820449));
#107340=CARTESIAN_POINT('Ctrl Pts',(-132.943299900212,-3.60709838502069,
134.150531700482));
#107341=CARTESIAN_POINT('Ctrl Pts',(-132.951056202954,-3.51232657117879,
134.249869616509));
#107342=CARTESIAN_POINT('Ctrl Pts',(-132.958812505696,-3.41365274102419,
134.345004348048));
#107343=CARTESIAN_POINT('Ctrl Pts',(-132.96657294821,-3.31492624567543,
134.440189855857));
#107344=CARTESIAN_POINT('Ctrl Pts',(-132.974333390724,-3.21229387663329,
134.531167449867));
#107345=CARTESIAN_POINT('Ctrl Pts',(-132.982093833239,-3.10616149122688,
134.617619571915));
#107346=CARTESIAN_POINT('Ctrl Pts',(-132.989866733504,-2.99985873269342,
134.704210474584));
#107347=CARTESIAN_POINT('Ctrl Pts',(-132.997639633769,-2.89004504354419,
134.786261153979));
#107348=CARTESIAN_POINT('Ctrl Pts',(-133.005412534035,-2.7771563872757,
134.863496666421));
#107349=CARTESIAN_POINT('Ctrl Pts',(-133.012902869797,-2.66837151800949,
134.937924473443));
#107350=CARTESIAN_POINT('Ctrl Pts',(-133.020393205559,-2.55673162680563,
135.007880958831));
#107351=CARTESIAN_POINT('Ctrl Pts',(-133.027883541321,-2.44264702593649,
135.073161218342));
#107352=CARTESIAN_POINT('Ctrl Pts',(-133.03565787544,-2.32423687275231,
135.140916598732));
#107353=CARTESIAN_POINT('Ctrl Pts',(-133.043432209559,-2.20281788029023,
135.203848783836));
#107354=CARTESIAN_POINT('Ctrl Pts',(-133.051206543678,-2.07882057878,135.26167910111));
#107355=CARTESIAN_POINT('Ctrl Pts',(-133.058971296626,-1.95497609286226,
135.319438147686));
#107356=CARTESIAN_POINT('Ctrl Pts',(-133.066736049573,-1.8285599711679,
135.372107673208));
#107357=CARTESIAN_POINT('Ctrl Pts',(-133.07450080252,-1.7000296505217,135.419453493105));
#107358=CARTESIAN_POINT('Ctrl Pts',(-133.082257843405,-1.57162698800194,
135.466752288465));
#107359=CARTESIAN_POINT('Ctrl Pts',(-133.09001488429,-1.44111466982342,
135.508737766455));
#107360=CARTESIAN_POINT('Ctrl Pts',(-133.097771925175,-1.30897222328307,
135.545222857831));
#107361=CARTESIAN_POINT('Ctrl Pts',(-133.105523116415,-1.17692942638939,
135.581680435516));
#107362=CARTESIAN_POINT('Ctrl Pts',(-133.113274307655,-1.04325932330527,
135.612645779067));
#107363=CARTESIAN_POINT('Ctrl Pts',(-133.121025498895,-0.908458460722157,
135.637981029601));
#107364=CARTESIAN_POINT('Ctrl Pts',(-133.128773395672,-0.773714892101393,
135.663305511978));
#107365=CARTESIAN_POINT('Ctrl Pts',(-133.136521292449,-0.637841903297591,
135.683004588649));
#107366=CARTESIAN_POINT('Ctrl Pts',(-133.144269189227,-0.501347931295957,
135.696991128271));
#107367=CARTESIAN_POINT('Ctrl Pts',(-133.152015465311,-0.364882510890796,
135.710974742212));
#107368=CARTESIAN_POINT('Ctrl Pts',(-133.159761741395,-0.227796754340897,
135.719248156076));
#107369=CARTESIAN_POINT('Ctrl Pts',(-133.167508017479,-0.0906055550158913,
135.721775964667));
#107370=CARTESIAN_POINT('Ctrl Pts',(-133.175254350744,0.046586657023196,
135.724303791917));
#107371=CARTESIAN_POINT('Ctrl Pts',(-133.18300068401,0.183883922491684,
135.721085922059));
#107372=CARTESIAN_POINT('Ctrl Pts',(-133.190747017275,0.32077040199062,
135.712139077491));
#107373=CARTESIAN_POINT('Ctrl Pts',(-133.198495085278,0.45768753626735,
135.703190229339));
#107374=CARTESIAN_POINT('Ctrl Pts',(-133.206243153281,0.594193311461642,
135.688509879021));
#107375=CARTESIAN_POINT('Ctrl Pts',(-133.213991221284,0.729776463624133,
135.668166676163));
#107376=CARTESIAN_POINT('Ctrl Pts',(-133.221747524026,0.865503715174387,
135.647801852306));
#107377=CARTESIAN_POINT('Ctrl Pts',(-133.229503826768,1.00030599763536,
135.621762211319));
#107378=CARTESIAN_POINT('Ctrl Pts',(-133.23726012951,1.13368115707588,135.590167769614));
#107379=CARTESIAN_POINT('Ctrl Pts',(-133.245020572024,1.26712750285521,
135.558556465003));
#107380=CARTESIAN_POINT('Ctrl Pts',(-133.252781014538,1.39914483171764,
135.521384558041));
#107381=CARTESIAN_POINT('Ctrl Pts',(-133.260541457052,1.52924659718825,
135.47882186005));
#107382=CARTESIAN_POINT('Ctrl Pts',(-133.268314357318,1.65955721356232,
135.436190836638));
#107383=CARTESIAN_POINT('Ctrl Pts',(-133.276087257583,1.78794575526713,
135.388151866283));
#107384=CARTESIAN_POINT('Ctrl Pts',(-133.283860157848,1.91394525548041,
135.334923123649));
#107385=CARTESIAN_POINT('Ctrl Pts',(-133.29135049361,2.03536435648632,135.283629379885));
#107386=CARTESIAN_POINT('Ctrl Pts',(-133.298840829372,2.15456481706185,
135.227516766744));
#107387=CARTESIAN_POINT('Ctrl Pts',(-133.306331165134,2.27115246165902,
135.166819735816));
#107388=CARTESIAN_POINT('Ctrl Pts',(-133.314105499253,2.392160562238,135.10382135851));
#107389=CARTESIAN_POINT('Ctrl Pts',(-133.321879833373,2.51073712314737,
135.035684504641));
#107390=CARTESIAN_POINT('Ctrl Pts',(-133.329654167492,2.62641497717776,
134.962620762165));
#107391=CARTESIAN_POINT('Ctrl Pts',(-133.337418920439,2.7419502685915,134.889647064221));
#107392=CARTESIAN_POINT('Ctrl Pts',(-133.345183673386,2.85459363375357,
134.811758765819));
#107393=CARTESIAN_POINT('Ctrl Pts',(-133.352948426333,2.96390079077247,
134.729214139031));
#107394=CARTESIAN_POINT('Ctrl Pts',(-133.360705467218,3.07309938238206,
134.646751496731));
#107395=CARTESIAN_POINT('Ctrl Pts',(-133.368462508103,3.17896805002177,
134.559641963552));
#107396=CARTESIAN_POINT('Ctrl Pts',(-133.376219548988,3.28109021082183,
134.468187863896));
#107397=CARTESIAN_POINT('Ctrl Pts',(-133.383970740228,3.38313536050617,
134.376802730487));
#107398=CARTESIAN_POINT('Ctrl Pts',(-133.391721931468,3.48143933681013,
134.281079811588));
#107399=CARTESIAN_POINT('Ctrl Pts',(-133.399473122708,3.57561775953648,
134.1813623499));
#107400=CARTESIAN_POINT('Ctrl Pts',(-133.407221019485,3.66975615392075,
134.081687270793));
#107401=CARTESIAN_POINT('Ctrl Pts',(-133.414968916262,3.75977221436109,
133.978021309307));
#107402=CARTESIAN_POINT('Ctrl Pts',(-133.42271681304,3.84531781218241,133.870745131258));
#107403=CARTESIAN_POINT('Ctrl Pts',(-133.430463089124,3.93084551570882,
133.763491393074));
#107404=CARTESIAN_POINT('Ctrl Pts',(-133.438209365208,4.01190437302902,
133.652629245901));
#107405=CARTESIAN_POINT('Ctrl Pts',(-133.445955641292,4.08818628430396,
133.538572746741));
#107406=CARTESIAN_POINT('Ctrl Pts',(-133.453701974557,4.16446875867476,
133.424515405642));
#107407=CARTESIAN_POINT('Ctrl Pts',(-133.461448307823,4.23597399928683,
133.307263990484));
#107408=CARTESIAN_POINT('Ctrl Pts',(-133.469194641088,4.30243725137123,
133.187261530427));
#107409=CARTESIAN_POINT('Ctrl Pts',(-133.476942709091,4.36891538744003,
133.067232196651));
#107410=CARTESIAN_POINT('Ctrl Pts',(-133.484690777094,4.43034909877924,
132.944450934001));
#107411=CARTESIAN_POINT('Ctrl Pts',(-133.492438845097,4.48651979161184,
132.819384990117));
#107412=CARTESIAN_POINT('Ctrl Pts',(-133.500195147839,4.54275018332516,
132.69418612466));
#107413=CARTESIAN_POINT('Ctrl Pts',(-133.50795145058,4.59370622228072,132.56669808462));
#107414=CARTESIAN_POINT('Ctrl Pts',(-133.515707753322,4.63921745521967,
132.437408218123));
#107415=CARTESIAN_POINT('Ctrl Pts',(-133.523468195836,4.68475297887408,
132.308049345731));
#107416=CARTESIAN_POINT('Ctrl Pts',(-133.531228638351,4.72483779173659,
132.176887104347));
#107417=CARTESIAN_POINT('Ctrl Pts',(-133.538989080865,4.75935177062778,
132.044422626468));
#107418=CARTESIAN_POINT('Ctrl Pts',(-133.54676198113,4.79392115442189,131.911745504849));
#107419=CARTESIAN_POINT('Ctrl Pts',(-133.554534881396,4.82290175098418,
131.777762351667));
#107420=CARTESIAN_POINT('Ctrl Pts',(-133.562307781661,4.84622470986369,
131.642983968068));
#107421=CARTESIAN_POINT('Ctrl Pts',(-133.569798117423,4.86869982044101,
131.513105118198));
#107422=CARTESIAN_POINT('Ctrl Pts',(-133.577288453185,4.88592145038888,
131.382488156753));
#107423=CARTESIAN_POINT('Ctrl Pts',(-133.584778788947,4.8978737889557,131.251591441594));
#107424=CARTESIAN_POINT('Ctrl Pts',(-133.592553123066,4.91027930407208,
131.115731737695));
#107425=CARTESIAN_POINT('Ctrl Pts',(-133.600327457186,4.91704736674041,
130.979140284887));
#107426=CARTESIAN_POINT('Ctrl Pts',(-133.608101791305,4.91810347661472,
130.842324492635));
#107427=CARTESIAN_POINT('Ctrl Pts',(-133.615866544252,4.91915828492799,
130.705677313619));
#107428=CARTESIAN_POINT('Ctrl Pts',(-133.623631297199,4.91451514390814,
130.568806732468));
#107429=CARTESIAN_POINT('Ctrl Pts',(-133.631396050146,4.90415119995085,
130.432226138485));
#107430=CARTESIAN_POINT('Ctrl Pts',(-133.639153091031,4.89379754960881,
130.295781198274));
#107431=CARTESIAN_POINT('Ctrl Pts',(-133.646910131916,4.87773443312074,
130.15962605938));
#107432=CARTESIAN_POINT('Ctrl Pts',(-133.654667172801,4.85599103135013,
130.024274618495));
#107433=CARTESIAN_POINT('Ctrl Pts',(-133.662418364041,4.8342640264479,129.889025247183));
#107434=CARTESIAN_POINT('Ctrl Pts',(-133.670169555281,4.80686532416455,
129.754578751978));
#107435=CARTESIAN_POINT('Ctrl Pts',(-133.677920746521,4.77387593742032,
129.62144405389));
#107436=CARTESIAN_POINT('Ctrl Pts',(-133.685668643298,4.74090057204552,
129.4883659416));
#107437=CARTESIAN_POINT('Ctrl Pts',(-133.693416540075,4.70233934210709,
129.356598896199));
#107438=CARTESIAN_POINT('Ctrl Pts',(-133.701164436853,4.65832434048542,
129.226641567373));
#107439=CARTESIAN_POINT('Ctrl Pts',(-133.708910712937,4.61431854585323,
129.096711422819));
#107440=CARTESIAN_POINT('Ctrl Pts',(-133.716656989021,4.56486137401212,
128.968590611944));
#107441=CARTESIAN_POINT('Ctrl Pts',(-133.724403265105,4.51013464735419,
128.842762155792));
#107442=CARTESIAN_POINT('Ctrl Pts',(-133.73214959837,4.45540751671593,128.716932770802));
#107443=CARTESIAN_POINT('Ctrl Pts',(-133.739895931636,4.39541090957425,
128.593396132823));
#107444=CARTESIAN_POINT('Ctrl Pts',(-133.747642264901,4.33037445248886,
128.472614455624));
#107445=CARTESIAN_POINT('Ctrl Pts',(-133.755390332904,4.26532343093993,
128.351805730205));
#107446=CARTESIAN_POINT('Ctrl Pts',(-133.763138400907,4.19523049890691,
128.233753537401));
#107447=CARTESIAN_POINT('Ctrl Pts',(-133.77088646891,4.12037060978731,128.11889434511));
#107448=CARTESIAN_POINT('Ctrl Pts',(-133.778642771652,4.0454311586868,128.003913079102));
#107449=CARTESIAN_POINT('Ctrl Pts',(-133.786399074394,3.96571484367799,
127.892131920668));
#107450=CARTESIAN_POINT('Ctrl Pts',(-133.794155377135,3.8815395503921,127.78395770053));
#107451=CARTESIAN_POINT('Ctrl Pts',(-133.80191581965,3.79731933021748,127.675725744552));
#107452=CARTESIAN_POINT('Ctrl Pts',(-133.809676262164,3.70863564231168,
127.571104860946));
#107453=CARTESIAN_POINT('Ctrl Pts',(-133.817436704678,3.61584517412433,
127.4704669871));
#107454=CARTESIAN_POINT('Ctrl Pts',(-133.825209604943,3.5229057504399,127.369667560404));
#107455=CARTESIAN_POINT('Ctrl Pts',(-133.832982505209,3.4258466493997,127.272864196728));
#107456=CARTESIAN_POINT('Ctrl Pts',(-133.840755405474,3.32506040712498,
127.180390922402));
#107457=CARTESIAN_POINT('Ctrl Pts',(-133.848245741236,3.2279379986219,127.091279284523));
#107458=CARTESIAN_POINT('Ctrl Pts',(-133.855736076998,3.12735496134202,
127.006188581348));
#107459=CARTESIAN_POINT('Ctrl Pts',(-133.86322641276,3.02368837863848,126.925379868531));
#107460=CARTESIAN_POINT('Ctrl Pts',(-133.871000746879,2.9160912459434,126.841507268806));
#107461=CARTESIAN_POINT('Ctrl Pts',(-133.878775080999,2.80483129141674,
126.761982089327));
#107462=CARTESIAN_POINT('Ctrl Pts',(-133.886549415118,2.69029514375431,
126.687141276555));
#107463=CARTESIAN_POINT('Ctrl Pts',(-133.894314168065,2.57590015165748,
126.612392698397));
#107464=CARTESIAN_POINT('Ctrl Pts',(-133.902078921012,2.45823732422291,
126.542317212076));
#107465=CARTESIAN_POINT('Ctrl Pts',(-133.909843673959,2.33772623747939,
126.477211544435));
#107466=CARTESIAN_POINT('Ctrl Pts',(-133.917600714844,2.21733484404613,
126.412170540661));
#107467=CARTESIAN_POINT('Ctrl Pts',(-133.925357755729,2.09410116275597,
126.352089717147));
#107468=CARTESIAN_POINT('Ctrl Pts',(-133.933114796614,1.96847332241768,
126.297222296921));
#107469=CARTESIAN_POINT('Ctrl Pts',(-133.940865987854,1.84294021901086,
126.242396252642));
#107470=CARTESIAN_POINT('Ctrl Pts',(-133.948617179094,1.71501690703762,
126.192775942148));
#107471=CARTESIAN_POINT('Ctrl Pts',(-133.956368370334,1.58517534561964,
126.148568291212));
#107472=CARTESIAN_POINT('Ctrl Pts',(-133.964116267111,1.45538897032874,
126.104379429706));
#107473=CARTESIAN_POINT('Ctrl Pts',(-133.971864163888,1.32368633650381,
126.065598777936));
#107474=CARTESIAN_POINT('Ctrl Pts',(-133.979612060666,1.19055837167676,
126.032384734755));
#107475=CARTESIAN_POINT('Ctrl Pts',(-133.98735833675,1.05745825435041,125.999177639236));
#107476=CARTESIAN_POINT('Ctrl Pts',(-133.995104612834,0.922933778152838,
125.971534930803));
#107477=CARTESIAN_POINT('Ctrl Pts',(-134.002850888918,0.787489601811479,
125.949564721801));
#107478=CARTESIAN_POINT('Ctrl Pts',(-134.010597222183,0.652044425651795,
125.927594350619));
#107479=CARTESIAN_POINT('Ctrl Pts',(-134.018343555449,0.515679921722393,
125.911296625022));
#107480=CARTESIAN_POINT('Ctrl Pts',(-134.026089888714,0.378909082321167,
125.900728191513));
#107481=CARTESIAN_POINT('Ctrl Pts',(-134.033837956717,0.242107614038945,
125.890157391277));
#107482=CARTESIAN_POINT('Ctrl Pts',(-134.04158602472,0.104900018941983,
125.885318466336));
#107483=CARTESIAN_POINT('Ctrl Pts',(-134.049334092723,-0.0321978711377765,
125.886216012169));
#107484=CARTESIAN_POINT('Ctrl Pts',(-134.057090395465,-0.169441470486786,
125.887114511925));
#107485=CARTESIAN_POINT('Ctrl Pts',(-134.064846698207,-0.306574740325703,
125.893761658885));
#107486=CARTESIAN_POINT('Ctrl Pts',(-134.072603000948,-0.443083577498728,
125.906109908808));
#107487=CARTESIAN_POINT('Ctrl Pts',(-134.080363443463,-0.579665273548354,
125.918464749363));
#107488=CARTESIAN_POINT('Ctrl Pts',(-134.088123885977,-0.715621485476006,
125.936526704555));
#107489=CARTESIAN_POINT('Ctrl Pts',(-134.095884328491,-0.850446493544069,
125.960196724373));
#107490=CARTESIAN_POINT('Ctrl Pts',(-134.103657228756,-0.985487934684285,
125.983904741408));
#107491=CARTESIAN_POINT('Ctrl Pts',(-134.111430129022,-1.11939416107169,
126.013238729349));
#107492=CARTESIAN_POINT('Ctrl Pts',(-134.119203029287,-1.25167197153181,
126.048048985831));
#107493=CARTESIAN_POINT('Ctrl Pts',(-134.126693365049,-1.37914115039364,
126.081593801808));
#107494=CARTESIAN_POINT('Ctrl Pts',(-134.134183700811,-1.50509795739489,
126.120223556209));
#107495=CARTESIAN_POINT('Ctrl Pts',(-134.141674036573,-1.62911893625768,
126.163762105087));
#107496=CARTESIAN_POINT('Ctrl Pts',(-134.149448463505,-1.75784374496744,
126.208951970763));
#107497=CARTESIAN_POINT('Ctrl Pts',(-134.157222890436,-1.88489075048452,
126.259573488805));
#107498=CARTESIAN_POINT('Ctrl Pts',(-134.164997317368,-2.0097674703886,
126.315483499904));
#107499=CARTESIAN_POINT('Ctrl Pts',(-134.172762141421,-2.13448994407502,
126.371324451632));
#107500=CARTESIAN_POINT('Ctrl Pts',(-134.180526965474,-2.25704711259141,
126.432440740749));
#107501=CARTESIAN_POINT('Ctrl Pts',(-134.188291789527,-2.37696252734415,
126.49863974806));
#107502=CARTESIAN_POINT('Ctrl Pts',(-134.196048879903,-2.49675850769784,
126.564772821907));
#107503=CARTESIAN_POINT('Ctrl Pts',(-134.203805970279,-2.61391763040504,
126.635978351813));
#107504=CARTESIAN_POINT('Ctrl Pts',(-134.211563060655,-2.7279846190288,
126.712016181813));
#107505=CARTESIAN_POINT('Ctrl Pts',(-134.219314279841,-2.84196527257224,
126.78799646026));
#107506=CARTESIAN_POINT('Ctrl Pts',(-134.227065499026,-2.9528581264867,
126.86880154271));
#107507=CARTESIAN_POINT('Ctrl Pts',(-134.234816718212,-3.0602339789941,
126.954146200639));
#107508=CARTESIAN_POINT('Ctrl Pts',(-134.242564531346,-3.16756264825349,
127.039453356299));
#107509=CARTESIAN_POINT('Ctrl Pts',(-134.25031234448,-3.27137708505586,
127.12929587644));
#107510=CARTESIAN_POINT('Ctrl Pts',(-134.258060157614,-3.37127867937868,
127.223346357825));
#107511=CARTESIAN_POINT('Ctrl Pts',(-134.265806319367,-3.47115898052738,
127.317376793151));
#107512=CARTESIAN_POINT('Ctrl Pts',(-134.273552481121,-3.56712781376811,
127.41561313775));
#107513=CARTESIAN_POINT('Ctrl Pts',(-134.281298642874,-3.6588214573347,
127.517689261034));
#107514=CARTESIAN_POINT('Ctrl Pts',(-134.2890448311,-3.75051541426831,127.619765733168));
#107515=CARTESIAN_POINT('Ctrl Pts',(-134.296791019327,-3.83793389123298,
127.725681719254));
#107516=CARTESIAN_POINT('Ctrl Pts',(-134.304537207553,-3.92075196314873,
127.835036265804));
#107517=CARTESIAN_POINT('Ctrl Pts',(-134.312285099761,-4.00358825311694,
127.944414867815));
#107518=CARTESIAN_POINT('Ctrl Pts',(-134.320032991969,-4.08182188855919,
128.057233223704));
#107519=CARTESIAN_POINT('Ctrl Pts',(-134.327780884177,-4.15517020162144,
128.173059863555));
#107520=CARTESIAN_POINT('Ctrl Pts',(-134.335536584154,-4.22859242984516,
128.289003225175));
#107521=CARTESIAN_POINT('Ctrl Pts',(-134.343292284131,-4.29711929348696,
128.40796059487));
#107522=CARTESIAN_POINT('Ctrl Pts',(-134.351047984108,-4.36051295948724,
128.52947385277));
#107523=CARTESIAN_POINT('Ctrl Pts',(-134.358807811175,-4.42394035956292,
128.651051772294));
#107524=CARTESIAN_POINT('Ctrl Pts',(-134.366567638243,-4.48222895318106,
128.775187936481));
#107525=CARTESIAN_POINT('Ctrl Pts',(-134.37432746531,-4.53518875771006,
128.901403446624));
#107526=CARTESIAN_POINT('Ctrl Pts',(-134.382098745693,-4.58822672962043,
129.027805247785));
#107527=CARTESIAN_POINT('Ctrl Pts',(-134.389870026076,-4.63592006366403,
129.156292159856));
#107528=CARTESIAN_POINT('Ctrl Pts',(-134.397641306458,-4.67812819418134,
129.286368634285));
#107529=CARTESIAN_POINT('Ctrl Pts',(-134.403488982117,-4.70988865645254,
129.384247618922));
#107530=CARTESIAN_POINT('Ctrl Pts',(-134.409336657775,-4.73854434489769,
129.483026301651));
#107531=CARTESIAN_POINT('Ctrl Pts',(-134.415184333433,-4.76405452823397,
129.582490119308));
#107532=CARTESIAN_POINT('Ctrl Pts',(-132.66500688127,-4.76405452823412,
129.582490119309));
#107533=CARTESIAN_POINT('Ctrl Pts',(-132.672705270541,-4.79787842028983,
129.714368961085));
#107534=CARTESIAN_POINT('Ctrl Pts',(-132.680403659813,-4.82619617847106,
129.847552223936));
#107535=CARTESIAN_POINT('Ctrl Pts',(-132.688102049085,-4.84893225451799,
129.981536788551));
#107536=CARTESIAN_POINT('Ctrl Pts',(-132.695941801563,-4.87208582628908,
130.117981671415));
#107537=CARTESIAN_POINT('Ctrl Pts',(-132.703781554041,-4.88945067006474,
130.255257139546));
#107538=CARTESIAN_POINT('Ctrl Pts',(-132.71162130652,-4.90100241562209,
130.392828863546));
#107539=CARTESIAN_POINT('Ctrl Pts',(-132.719461058998,-4.91255416117943,
130.530400587546));
#107540=CARTESIAN_POINT('Ctrl Pts',(-132.727300811476,-4.91829285496466,
130.668268136608));
#107541=CARTESIAN_POINT('Ctrl Pts',(-132.735140563954,-4.9182497588907,
130.805900640808));
#107542=CARTESIAN_POINT('',(-132.389859436048,-4.9182488482065,130.807726566983));
#107543=CARTESIAN_POINT('Ctrl Pts',(-132.320008282756,-4.76405452823418,
129.582490119309));
#107544=CARTESIAN_POINT('Ctrl Pts',(-132.327791281343,-4.79830572555041,
129.71603501781));
#107545=CARTESIAN_POINT('Ctrl Pts',(-132.33557427993,-4.826953306866,129.851082946797));
#107546=CARTESIAN_POINT('Ctrl Pts',(-132.343357278516,-4.84987753848702,
129.987126915263));
#107547=CARTESIAN_POINT('Ctrl Pts',(-132.351139968801,-4.87280086202732,
130.12316549472));
#107548=CARTESIAN_POINT('Ctrl Pts',(-132.358922659086,-4.89000121271092,
130.2601996569));
#107549=CARTESIAN_POINT('Ctrl Pts',(-132.366705349371,-4.90141004073329,
130.397712520191));
#107550=CARTESIAN_POINT('Ctrl Pts',(-132.374423378245,-4.91272408007915,
130.534082876794));
#107551=CARTESIAN_POINT('Ctrl Pts',(-132.382141407119,-4.91834247332233,
130.670923633975));
#107552=CARTESIAN_POINT('Ctrl Pts',(-132.389859435993,-4.91824884820717,
130.807726566));
#107553=CARTESIAN_POINT('Ctrl Pts',(-132.389859436049,-4.9182488482065,
130.807726566983));
#107554=CARTESIAN_POINT('Ctrl Pts',(-132.398671358528,-4.91814195336178,
130.963918886508));
#107555=CARTESIAN_POINT('Ctrl Pts',(-132.407483281008,-4.91059060283849,
131.119819610132));
#107556=CARTESIAN_POINT('Ctrl Pts',(-132.416295203488,-4.89570197311823,
131.274770282546));
#107557=CARTESIAN_POINT('Ctrl Pts',(-132.425145933195,-4.88074777468338,
131.430403349283));
#107558=CARTESIAN_POINT('Ctrl Pts',(-132.433996662901,-4.85839163980709,
131.585077814765));
#107559=CARTESIAN_POINT('Ctrl Pts',(-132.442847392608,-4.82879182031729,
131.73814464963));
#107560=CARTESIAN_POINT('Ctrl Pts',(-132.451750270414,-4.79901760002992,
131.892113347362));
#107561=CARTESIAN_POINT('Ctrl Pts',(-132.460653148219,-4.76191417788455,
132.044455252463));
#107562=CARTESIAN_POINT('Ctrl Pts',(-132.469556026025,-4.71769122469761,
132.194530596709));
#107563=CARTESIAN_POINT('Ctrl Pts',(-132.476563113968,-4.68288516211224,
132.312648710673));
#107564=CARTESIAN_POINT('Ctrl Pts',(-132.483570201912,-4.64366980231781,
132.429363166074));
#107565=CARTESIAN_POINT('Ctrl Pts',(-132.490577289855,-4.60016777226407,
132.544371976587));
#107566=CARTESIAN_POINT('Ctrl Pts',(-132.498351623974,-4.55190245588252,
132.671973760211));
#107567=CARTESIAN_POINT('Ctrl Pts',(-132.506125958093,-4.49824744275542,
132.797767922314));
#107568=CARTESIAN_POINT('Ctrl Pts',(-132.513900292213,-4.43935766333605,
132.921265575158));
#107569=CARTESIAN_POINT('Ctrl Pts',(-132.52166504516,-4.38054046030684,
133.044611028183));
#107570=CARTESIAN_POINT('Ctrl Pts',(-132.529429798107,-4.31650149397504,
133.165665253779));
#107571=CARTESIAN_POINT('Ctrl Pts',(-132.537194551054,-4.24744475510768,
133.283956575541));
#107572=CARTESIAN_POINT('Ctrl Pts',(-132.544951591939,-4.1784566043667,
133.402130408696));
#107573=CARTESIAN_POINT('Ctrl Pts',(-132.552708632824,-4.10446079475703,
133.517546463555));
#107574=CARTESIAN_POINT('Ctrl Pts',(-132.560465673709,-4.02570833253192,
133.629755365895));
#107575=CARTESIAN_POINT('Ctrl Pts',(-132.568216864949,-3.94701525815128,
133.741879650628));
#107576=CARTESIAN_POINT('Ctrl Pts',(-132.57596805619,-3.863572894608,133.850801278078));
#107577=CARTESIAN_POINT('Ctrl Pts',(-132.58371924743,-3.77567668347278,
133.95609801849));
#107578=CARTESIAN_POINT('Ctrl Pts',(-132.591467144207,-3.68781783057211,
134.061350004977));
#107579=CARTESIAN_POINT('Ctrl Pts',(-132.599215040984,-3.59550914513596,
134.162979869197));
#107580=CARTESIAN_POINT('Ctrl Pts',(-132.606962937761,-3.49908751153531,
134.260596959184));
#107581=CARTESIAN_POINT('Ctrl Pts',(-132.614709213846,-3.4026860472618,
134.358193629779));
#107582=CARTESIAN_POINT('Ctrl Pts',(-132.62245548993,-3.30217362065905,
134.451778917749));
#107583=CARTESIAN_POINT('Ctrl Pts',(-132.630201766014,-3.19792500132062,
134.540997975998));
#107584=CARTESIAN_POINT('Ctrl Pts',(-132.637948099279,-3.09367561244242,
134.630217692841));
#107585=CARTESIAN_POINT('Ctrl Pts',(-132.645694432545,-2.98569027283076,
134.715070861438));
#107586=CARTESIAN_POINT('Ctrl Pts',(-132.65344076581,-2.87437764088469,
134.795242254508));
#107587=CARTESIAN_POINT('Ctrl Pts',(-132.661188833813,-2.76304008124663,
134.875431601406));
#107588=CARTESIAN_POINT('Ctrl Pts',(-132.668936901816,-2.64837406374902,
134.950936858034));
#107589=CARTESIAN_POINT('Ctrl Pts',(-132.676684969819,-2.53081774777548,
135.021485774595));
#107590=CARTESIAN_POINT('Ctrl Pts',(-132.684441272561,-2.41313649155023,
135.092109671384));
#107591=CARTESIAN_POINT('Ctrl Pts',(-132.692197575303,-2.29255913627593,
135.15776650389));
#107592=CARTESIAN_POINT('Ctrl Pts',(-132.699953878045,-2.16954948694773,
135.218229451841));
#107593=CARTESIAN_POINT('Ctrl Pts',(-132.707714320559,-2.04647418366593,
135.278724670688));
#107594=CARTESIAN_POINT('Ctrl Pts',(-132.715474763074,-1.92096435718586,
135.334020323721));
#107595=CARTESIAN_POINT('Ctrl Pts',(-132.723235205588,-1.7935034448138,
135.383937940414));
#107596=CARTESIAN_POINT('Ctrl Pts',(-132.731008105853,-1.66583792086975,
135.433935689297));
#107597=CARTESIAN_POINT('Ctrl Pts',(-132.738781006119,-1.53621542209145,
135.478538022471));
#107598=CARTESIAN_POINT('Ctrl Pts',(-132.746553906385,-1.40513504251891,
135.517616241313));
#107599=CARTESIAN_POINT('Ctrl Pts',(-132.754044242146,-1.27881976492886,
135.555273868464));
#107600=CARTESIAN_POINT('Ctrl Pts',(-132.761534577907,-1.15115106007221,
135.587801963274));
#107601=CARTESIAN_POINT('Ctrl Pts',(-132.769024913668,-1.02258221022359,
135.615130689585));
#107602=CARTESIAN_POINT('Ctrl Pts',(-132.776799247787,-0.889138633341971,
135.643495592864));
#107603=CARTESIAN_POINT('Ctrl Pts',(-132.784573581907,-0.754302596898488,
135.66634892804));
#107604=CARTESIAN_POINT('Ctrl Pts',(-132.792347916026,-0.618569159687465,
135.68355678673));
#107605=CARTESIAN_POINT('Ctrl Pts',(-132.800112668973,-0.483003001806959,
135.700743438271));
#107606=CARTESIAN_POINT('Ctrl Pts',(-132.80787742192,-0.346542027839381,
135.712298408067));
#107607=CARTESIAN_POINT('Ctrl Pts',(-132.815642174867,-0.209693334494366,
135.718138366709));
#107608=CARTESIAN_POINT('Ctrl Pts',(-132.823399215752,-0.0729805612011811,
135.723972525021));
#107609=CARTESIAN_POINT('Ctrl Pts',(-132.831156256637,0.0641187770441665,
135.724102951571));
#107610=CARTESIAN_POINT('Ctrl Pts',(-132.838913297522,0.201090933970913,
135.718497927285));
#107611=CARTESIAN_POINT('Ctrl Pts',(-132.846664488762,0.33795979912882,
135.712897129792));
#107612=CARTESIAN_POINT('Ctrl Pts',(-132.854415680002,0.474701284810364,
135.701569506328));
#107613=CARTESIAN_POINT('Ctrl Pts',(-132.862166871242,0.610800463778589,
135.684535394759));
#107614=CARTESIAN_POINT('Ctrl Pts',(-132.86991476802,0.746841796965374,
135.667508523141));
#107615=CARTESIAN_POINT('Ctrl Pts',(-132.877662664797,0.882240979283709,
135.644780035825));
#107616=CARTESIAN_POINT('Ctrl Pts',(-132.885410561574,1.01648724993869,
135.616422206242));
#107617=CARTESIAN_POINT('Ctrl Pts',(-132.893156837658,1.15070543916787,
135.588070308506));
#107618=CARTESIAN_POINT('Ctrl Pts',(-132.900903113742,1.28377081414098,
135.554091491442));
#107619=CARTESIAN_POINT('Ctrl Pts',(-132.908649389826,1.4151822598264,135.514609255799));
#107620=CARTESIAN_POINT('Ctrl Pts',(-132.916395723091,1.54659467556108,
135.475126728707));
#107621=CARTESIAN_POINT('Ctrl Pts',(-132.924142056357,1.67635276321543,
135.430140814469));
#107622=CARTESIAN_POINT('Ctrl Pts',(-132.931888389622,1.80397042330583,
135.379824940926));
#107623=CARTESIAN_POINT('Ctrl Pts',(-132.939636457625,1.93161666248619,
135.329497799492));
#107624=CARTESIAN_POINT('Ctrl Pts',(-132.947384525628,2.05712115663699,
135.273838466987));
#107625=CARTESIAN_POINT('Ctrl Pts',(-132.955132593631,2.18001801844423,
135.213068421646));
#107626=CARTESIAN_POINT('Ctrl Pts',(-132.962888896373,2.30304549649886,
135.152233789178));
#107627=CARTESIAN_POINT('Ctrl Pts',(-132.970645199115,2.42345945497546,
135.086277766985));
#107628=CARTESIAN_POINT('Ctrl Pts',(-132.978401501857,2.54081836562543,
135.01546796545));
#107629=CARTESIAN_POINT('Ctrl Pts',(-132.986161944371,2.65823991425993,
134.944620370591));
#107630=CARTESIAN_POINT('Ctrl Pts',(-132.993922386885,2.7726028401708,134.868914050087));
#107631=CARTESIAN_POINT('Ctrl Pts',(-133.001682829399,2.88349568137793,
134.788659265757));
#107632=CARTESIAN_POINT('Ctrl Pts',(-133.009455729665,2.99456653761808,
134.708275649323));
#107633=CARTESIAN_POINT('Ctrl Pts',(-133.01722862993,3.10215587051635,134.623329220555));
#107634=CARTESIAN_POINT('Ctrl Pts',(-133.025001530196,3.20588562975594,
134.534170316656));
#107635=CARTESIAN_POINT('Ctrl Pts',(-133.032491865957,3.30584455096627,
134.448252563492));
#107636=CARTESIAN_POINT('Ctrl Pts',(-133.039982201719,3.40221941183791,
134.358423496111));
#107637=CARTESIAN_POINT('Ctrl Pts',(-133.047472537481,3.49470644709292,
134.265026725579));
#107638=CARTESIAN_POINT('Ctrl Pts',(-133.0552468716,3.59070015640142,134.168088788104));
#107639=CARTESIAN_POINT('Ctrl Pts',(-133.063021205719,3.68280948577632,
134.067000197776));
#107640=CARTESIAN_POINT('Ctrl Pts',(-133.070795539838,3.77065418292927,
133.962105080827));
#107641=CARTESIAN_POINT('Ctrl Pts',(-133.078560292785,3.85839061934412,
133.857339237735));
#107642=CARTESIAN_POINT('Ctrl Pts',(-133.086325045733,3.94187263236082,
133.748776498982));
#107643=CARTESIAN_POINT('Ctrl Pts',(-133.09408979868,4.02075601643018,133.636798457809));
#107644=CARTESIAN_POINT('Ctrl Pts',(-133.101846839565,4.09956105241042,
133.524931634806));
#107645=CARTESIAN_POINT('Ctrl Pts',(-133.10960388045,4.17377632512013,133.409656577421));
#107646=CARTESIAN_POINT('Ctrl Pts',(-133.117360921335,4.24309745599594,
133.291388370009));
#107647=CARTESIAN_POINT('Ctrl Pts',(-133.125112112575,4.31236631126763,
133.173209349572));
#107648=CARTESIAN_POINT('Ctrl Pts',(-133.132863303815,4.37674817393998,
133.052042007774));
#107649=CARTESIAN_POINT('Ctrl Pts',(-133.140614495055,4.43598182408496,
132.928330560594));
#107650=CARTESIAN_POINT('Ctrl Pts',(-133.148362391832,4.4951902983486,132.80467169408));
#107651=CARTESIAN_POINT('Ctrl Pts',(-133.156110288609,4.54925474361721,
132.678471224723));
#107652=CARTESIAN_POINT('Ctrl Pts',(-133.163858185386,4.59795988689043,
132.550197935602));
#107653=CARTESIAN_POINT('Ctrl Pts',(-133.17160446147,4.6466548420975,132.421951478488));
#107654=CARTESIAN_POINT('Ctrl Pts',(-133.179350737554,4.68999258644652,
132.291633429314));
#107655=CARTESIAN_POINT('Ctrl Pts',(-133.187097013639,4.727806159701,132.159732145522));
#107656=CARTESIAN_POINT('Ctrl Pts',(-133.194843346904,4.76562001208673,
132.027829888064));
#107657=CARTESIAN_POINT('Ctrl Pts',(-133.202589680169,4.79790950426581,
131.894344748493));
#107658=CARTESIAN_POINT('Ctrl Pts',(-133.210336013434,4.82455779734822,
131.759779438056));
#107659=CARTESIAN_POINT('Ctrl Pts',(-133.218084081437,4.85121205813113,
131.62518399265));
#107660=CARTESIAN_POINT('Ctrl Pts',(-133.225832149441,4.8722225300475,131.489508278476));
#107661=CARTESIAN_POINT('Ctrl Pts',(-133.233580217444,4.88752372553465,
131.35326397412));
#107662=CARTESIAN_POINT('Ctrl Pts',(-133.241336520185,4.90284118331442,
131.216874867696));
#107663=CARTESIAN_POINT('Ctrl Pts',(-133.249092822927,4.91243719970382,
131.079916353069));
#107664=CARTESIAN_POINT('Ctrl Pts',(-133.256849125669,4.91629826609137,
130.942904550407));
#107665=CARTESIAN_POINT('Ctrl Pts',(-133.264609568183,4.92016139324633,
130.80581962042));
#107666=CARTESIAN_POINT('Ctrl Pts',(-133.272370010697,4.91828347661674,
130.668681736463));
#107667=CARTESIAN_POINT('Ctrl Pts',(-133.280130453212,4.9107031430074,130.532004777245));
#107668=CARTESIAN_POINT('Ctrl Pts',(-133.287903353477,4.90311064077362,
130.395108412038));
#107669=CARTESIAN_POINT('Ctrl Pts',(-133.295676253742,4.88979746689118,
130.258674839502));
#107670=CARTESIAN_POINT('Ctrl Pts',(-133.303449154008,4.87085402453883,
130.12321148989));
#107671=CARTESIAN_POINT('Ctrl Pts',(-133.31093948977,4.85259922403123,129.992672574245));
#107672=CARTESIAN_POINT('Ctrl Pts',(-133.318429825532,4.8291164519392,129.863034869194));
#107673=CARTESIAN_POINT('Ctrl Pts',(-133.325920161294,4.80053060543232,
129.734739671245));
#107674=CARTESIAN_POINT('Ctrl Pts',(-133.333694495413,4.77086091786727,
129.601580121875));
#107675=CARTESIAN_POINT('Ctrl Pts',(-133.341468829533,4.73559956626961,
129.469445082101));
#107676=CARTESIAN_POINT('Ctrl Pts',(-133.349243163652,4.69483053813357,
129.338840477579));
#107677=CARTESIAN_POINT('Ctrl Pts',(-133.357007916599,4.65411175418109,
129.208396831559));
#107678=CARTESIAN_POINT('Ctrl Pts',(-133.364772669546,4.60789891460797,
129.079480237585));
#107679=CARTESIAN_POINT('Ctrl Pts',(-133.372537422493,4.55632701310982,
128.952586546005));
#107680=CARTESIAN_POINT('Ctrl Pts',(-133.380294463378,4.50480633355128,
128.825818887028));
#107681=CARTESIAN_POINT('Ctrl Pts',(-133.388051504263,4.44793733072271,
128.701070491945));
#107682=CARTESIAN_POINT('Ctrl Pts',(-133.395808545148,4.38590470279817,
128.578821806295));
#107683=CARTESIAN_POINT('Ctrl Pts',(-133.403559736388,4.3239188541608,128.45666530933));
#107684=CARTESIAN_POINT('Ctrl Pts',(-133.411310927628,4.25677730725702,
128.337005116955));
#107685=CARTESIAN_POINT('Ctrl Pts',(-133.419062118868,4.18471259782026,
128.220301110483));
#107686=CARTESIAN_POINT('Ctrl Pts',(-133.426810015645,4.11267851780731,
128.103646706327));
#107687=CARTESIAN_POINT('Ctrl Pts',(-133.434557912422,4.03572564201934,
127.989946321033));
#107688=CARTESIAN_POINT('Ctrl Pts',(-133.442305809199,3.95413201062122,
127.879634458576));
#107689=CARTESIAN_POINT('Ctrl Pts',(-133.450052085284,3.87255544685205,
127.769345670983));
#107690=CARTESIAN_POINT('Ctrl Pts',(-133.457798361368,3.78634029068704,
127.6624443105));
#107691=CARTESIAN_POINT('Ctrl Pts',(-133.465544637452,3.69580716498571,
127.559334814627));
#107692=CARTESIAN_POINT('Ctrl Pts',(-133.473290970717,3.6052733709893,127.456224557623));
#107693=CARTESIAN_POINT('Ctrl Pts',(-133.481037303983,3.51042180180978,
127.356906514873));
#107694=CARTESIAN_POINT('Ctrl Pts',(-133.488783637248,3.41161224838277,
127.261750713952));
#107695=CARTESIAN_POINT('Ctrl Pts',(-133.496531705251,3.31278056724151,
127.166573603549));
#107696=CARTESIAN_POINT('Ctrl Pts',(-133.504279773254,3.20998941965065,
127.075560860904));
#107697=CARTESIAN_POINT('Ctrl Pts',(-133.512027841257,3.1036338976697,126.989044157332));
#107698=CARTESIAN_POINT('Ctrl Pts',(-133.519784143999,2.9971653397742,126.902435502777));
#107699=CARTESIAN_POINT('Ctrl Pts',(-133.527540446741,2.88712514380574,
126.820332679862));
#107700=CARTESIAN_POINT('Ctrl Pts',(-133.535296749483,2.77394023454401,
126.743026029321));
#107701=CARTESIAN_POINT('Ctrl Pts',(-133.543057191997,2.66069491508827,
126.665678117892));
#107702=CARTESIAN_POINT('Ctrl Pts',(-133.550817634511,2.5443018695595,126.593131686281));
#107703=CARTESIAN_POINT('Ctrl Pts',(-133.558578077025,2.42521431740076,
126.525632000655));
#107704=CARTESIAN_POINT('Ctrl Pts',(-133.56635097729,2.3059355953312,126.458023958541));
#107705=CARTESIAN_POINT('Ctrl Pts',(-133.574123877556,2.18395407108092,
126.395479030246));
#107706=CARTESIAN_POINT('Ctrl Pts',(-133.581896777821,2.05974552521942,
126.338195435462));
#107707=CARTESIAN_POINT('Ctrl Pts',(-133.589387113583,1.94005227286277,
126.282994243637));
#107708=CARTESIAN_POINT('Ctrl Pts',(-133.596877449345,1.81829138816176,
126.232678618709));
#107709=CARTESIAN_POINT('Ctrl Pts',(-133.604367785107,1.69490165633622,
126.187382012694));
#107710=CARTESIAN_POINT('Ctrl Pts',(-133.612142119226,1.56683356532517,
126.140367972094));
#107711=CARTESIAN_POINT('Ctrl Pts',(-133.619916453345,1.43660499226052,
126.098612129271));
#107712=CARTESIAN_POINT('Ctrl Pts',(-133.627690787465,1.30468698401493,
126.062317288342));
#107713=CARTESIAN_POINT('Ctrl Pts',(-133.635455540412,1.17293155292466,
126.02606717756));
#107714=CARTESIAN_POINT('Ctrl Pts',(-133.643220293359,1.03949120270712,
125.995264780303));
#107715=CARTESIAN_POINT('Ctrl Pts',(-133.650985046306,0.904856073691232,
125.970064541775));
#107716=CARTESIAN_POINT('Ctrl Pts',(-133.658742087191,0.77035466618351,
125.94488933248));
#107717=CARTESIAN_POINT('Ctrl Pts',(-133.666499128076,0.634661223211319,
125.925305280483));
#107718=CARTESIAN_POINT('Ctrl Pts',(-133.674256168961,0.498279791087177,
125.911416686527));
#107719=CARTESIAN_POINT('Ctrl Pts',(-133.682007360201,0.362001205261707,
125.897538566068));
#107720=CARTESIAN_POINT('Ctrl Pts',(-133.689758551441,0.225036050339748,
125.889347394184));
#107721=CARTESIAN_POINT('Ctrl Pts',(-133.697509742681,0.0878969287371864,
125.88689610906));
#107722=CARTESIAN_POINT('Ctrl Pts',(-133.705257639458,-0.0491839050802019,
125.884445865797));
#107723=CARTESIAN_POINT('Ctrl Pts',(-133.713005536235,-0.186438168431842,
125.887730664078));
#107724=CARTESIAN_POINT('Ctrl Pts',(-133.720753433012,-0.323350013316159,
125.89675144085));
#107725=CARTESIAN_POINT('Ctrl Pts',(-133.728499709096,-0.460233219194004,
125.90577033067));
#107726=CARTESIAN_POINT('Ctrl Pts',(-133.73624598518,-0.596773759201507,
125.920522786739));
#107727=CARTESIAN_POINT('Ctrl Pts',(-133.743992261264,-0.732458064127735,
125.940957668314));
#107728=CARTESIAN_POINT('Ctrl Pts',(-133.75173859453,-0.868143370644494,
125.961392700734));
#107729=CARTESIAN_POINT('Ctrl Pts',(-133.759484927795,-1.00297204286255,
125.987510184136));
#107730=CARTESIAN_POINT('Ctrl Pts',(-133.76723126106,-1.13643829031373,
126.019207425158));
#107731=CARTESIAN_POINT('Ctrl Pts',(-133.774979329063,-1.26993442660582,
126.050911764558));
#107732=CARTESIAN_POINT('Ctrl Pts',(-133.782727397066,-1.40206715069408,
126.088198257713));
#107733=CARTESIAN_POINT('Ctrl Pts',(-133.790475465069,-1.53234386119818,
126.130913778931));
#107734=CARTESIAN_POINT('Ctrl Pts',(-133.798231767811,-1.6627590313407,
126.173674698713));
#107735=CARTESIAN_POINT('Ctrl Pts',(-133.805988070553,-1.7913138753339,
126.221876050823));
#107736=CARTESIAN_POINT('Ctrl Pts',(-133.813744373295,-1.91753335802306,
126.27531558761));
#107737=CARTESIAN_POINT('Ctrl Pts',(-133.821504815809,-2.04382020785053,
126.328783646687));
#107738=CARTESIAN_POINT('Ctrl Pts',(-133.829265258323,-2.1677688595534,
126.387495293981));
#107739=CARTESIAN_POINT('Ctrl Pts',(-133.837025700837,-2.2889279875775,
126.451201795494));
#107740=CARTESIAN_POINT('Ctrl Pts',(-133.844798601102,-2.4102816109899,
126.515010564339));
#107741=CARTESIAN_POINT('Ctrl Pts',(-133.852571501368,-2.52883642395021,
126.583830013898));
#107742=CARTESIAN_POINT('Ctrl Pts',(-133.860344401633,-2.64416848759839,
126.657366999089));
#107743=CARTESIAN_POINT('Ctrl Pts',(-133.867834737396,-2.75530794023309,
126.728230729642));
#107744=CARTESIAN_POINT('Ctrl Pts',(-133.875325073158,-2.86345463285709,
126.80347478609));
#107745=CARTESIAN_POINT('Ctrl Pts',(-133.88281540892,-2.96825911438144,
126.882802140074));
#107746=CARTESIAN_POINT('Ctrl Pts',(-133.890603016867,-3.07722301654917,
126.965277792956));
#107747=CARTESIAN_POINT('Ctrl Pts',(-133.898390624814,-3.18293962587666,
127.052444551435));
#107748=CARTESIAN_POINT('Ctrl Pts',(-133.906178232761,-3.28497285252097,
127.144014128407));
#107749=CARTESIAN_POINT('Ctrl Pts',(-133.913859423379,-3.38561179948952,
127.234332411028));
#107750=CARTESIAN_POINT('Ctrl Pts',(-133.921540613997,-3.48266705776343,
127.328933697929));
#107751=CARTESIAN_POINT('Ctrl Pts',(-133.929221804614,-3.57574876308413,
127.427497599053));
#107752=CARTESIAN_POINT('Ctrl Pts',(-133.936896001566,-3.66874571821173,
127.525971758486));
#107753=CARTESIAN_POINT('Ctrl Pts',(-133.944570198517,-3.7577760417264,
127.628401069164));
#107754=CARTESIAN_POINT('Ctrl Pts',(-133.952244395468,-3.84248420284421,
127.734426055822));
#107755=CARTESIAN_POINT('Ctrl Pts',(-133.959913353601,-3.92713453762649,
127.840378664134));
#107756=CARTESIAN_POINT('Ctrl Pts',(-133.967582311734,-4.0074683300128,
127.949921754922));
#107757=CARTESIAN_POINT('Ctrl Pts',(-133.975251269866,-4.08316844507548,
128.062660686567));
#107758=CARTESIAN_POINT('Ctrl Pts',(-133.983123497348,-4.1608750273593,
128.17838781672));
#107759=CARTESIAN_POINT('Ctrl Pts',(-133.99099572483,-4.23369857512685,
128.297482249238));
#107760=CARTESIAN_POINT('Ctrl Pts',(-133.998867952312,-4.30134172047524,
128.419482745179));
#107761=CARTESIAN_POINT('Ctrl Pts',(-134.006532799929,-4.36720292718514,
128.538269354533));
#107762=CARTESIAN_POINT('Ctrl Pts',(-134.014197647547,-4.42815306647365,
128.659810455679));
#107763=CARTESIAN_POINT('Ctrl Pts',(-134.021862495164,-4.48396325040901,
128.783653654278));
#107764=CARTESIAN_POINT('Ctrl Pts',(-134.029838412578,-4.54203843209047,
128.912522899127));
#107765=CARTESIAN_POINT('Ctrl Pts',(-134.037814329992,-4.59454745370409,
129.043884623148));
#107766=CARTESIAN_POINT('Ctrl Pts',(-134.045790247406,-4.64128732456252,
129.177205113825));
#107767=CARTESIAN_POINT('Ctrl Pts',(-134.05376616482,-4.68802719542096,
129.310525604502));
#107768=CARTESIAN_POINT('Ctrl Pts',(-134.061742082235,-4.72899778085758,
129.445804393348));
#107769=CARTESIAN_POINT('Ctrl Pts',(-134.069717999649,-4.76405452823413,
129.582490119309));
#107770=CARTESIAN_POINT('Origin',(213.235140564004,0.,130.804360617566));
#107771=CARTESIAN_POINT('',(-136.165410316754,-4.76405452823394,129.582490119308));
#107772=CARTESIAN_POINT('',(-135.819866485249,-4.76405452823408,129.582490119308));
#107773=CARTESIAN_POINT('',(213.235140564004,-4.76405452823405,129.582490119308));
#107774=CARTESIAN_POINT('',(-134.485140563972,-4.91824790082115,130.799816547985));
#107775=CARTESIAN_POINT('Ctrl Pts',(-134.48514056401,-4.91824790082178,
130.799816548665));
#107776=CARTESIAN_POINT('Ctrl Pts',(-134.492797749234,-4.9183727917618,
130.934991568447));
#107777=CARTESIAN_POINT('Ctrl Pts',(-134.500454934458,-4.91292068941301,
131.070323998656));
#107778=CARTESIAN_POINT('Ctrl Pts',(-134.508112119682,-4.90187949338597,
131.205310109176));
#107779=CARTESIAN_POINT('Ctrl Pts',(-134.51604783487,-4.89043667406738,
131.345206336851));
#107780=CARTESIAN_POINT('Ctrl Pts',(-134.523983550059,-4.87299040046864,
131.484730136805));
#107781=CARTESIAN_POINT('Ctrl Pts',(-134.531919265247,-4.84958633597631,
131.623320587535));
#107782=CARTESIAN_POINT('Ctrl Pts',(-134.539568234451,-4.82702794466393,
131.75690326591));
#107783=CARTESIAN_POINT('Ctrl Pts',(-134.547217203656,-4.79893490755988,
131.889618442244));
#107784=CARTESIAN_POINT('Ctrl Pts',(-134.55486617286,-4.76540082329047,
132.020969862921));
#107785=CARTESIAN_POINT('Ctrl Pts',(-134.562514109117,-4.73187126759849,
132.152303545374));
#107786=CARTESIAN_POINT('Ctrl Pts',(-134.570162045374,-4.69290222506853,
132.28227344903));
#107787=CARTESIAN_POINT('Ctrl Pts',(-134.577809981631,-4.64863799249533,
132.410395448206));
#107788=CARTESIAN_POINT('Ctrl Pts',(-134.585458641586,-4.60436957134925,
132.538529571129));
#107789=CARTESIAN_POINT('Ctrl Pts',(-134.593107301541,-4.55480509528288,
132.66481506206));
#107790=CARTESIAN_POINT('Ctrl Pts',(-134.600755961495,-4.50013794097112,
132.788785364119));
#107791=CARTESIAN_POINT('Ctrl Pts',(-134.608407102135,-4.44545305649669,
132.912795873386));
#107792=CARTESIAN_POINT('Ctrl Pts',(-134.616058242775,-4.38566236507843,
133.034489333225));
#107793=CARTESIAN_POINT('Ctrl Pts',(-134.623709383415,-4.32100610677341,
133.153421980691));
#107794=CARTESIAN_POINT('Ctrl Pts',(-134.631368842986,-4.25627954901759,
133.272483941236));
#107795=CARTESIAN_POINT('Ctrl Pts',(-134.639028302557,-4.18667705819371,
133.388778745395));
#107796=CARTESIAN_POINT('Ctrl Pts',(-134.646687762129,-4.11248341754616,
133.5018897097));
#107797=CARTESIAN_POINT('Ctrl Pts',(-134.654352181613,-4.03824173251984,
133.615073919446));
#107798=CARTESIAN_POINT('Ctrl Pts',(-134.662016601097,-3.95940321316816,
133.725069860044));
#107799=CARTESIAN_POINT('Ctrl Pts',(-134.669681020581,-3.87629334941419,
133.831493408143));
#107800=CARTESIAN_POINT('Ctrl Pts',(-134.677356166266,-3.79306717507348,
133.938065893862));
#107801=CARTESIAN_POINT('Ctrl Pts',(-134.685031311951,-3.70555798788263,
134.041055707016));
#107802=CARTESIAN_POINT('Ctrl Pts',(-134.692706457636,-3.61412870578418,
134.140114919149));
#107803=CARTESIAN_POINT('Ctrl Pts',(-134.694660733157,-3.59084862547951,
134.165337761989));
#107804=CARTESIAN_POINT('Ctrl Pts',(-134.696615008678,-3.56731456141368,
134.190305973104));
#107805=CARTESIAN_POINT('Ctrl Pts',(-134.698569284199,-3.54353284044415,
134.215014231053));
#107806=CARTESIAN_POINT('Ctrl Pts',(-134.706343618318,-3.44892640303954,
134.313306539758));
#107807=CARTESIAN_POINT('Ctrl Pts',(-134.714117952437,-3.35007729366011,
134.407815191358));
#107808=CARTESIAN_POINT('Ctrl Pts',(-134.721892286556,-3.24732041443052,
134.498151784988));
#107809=CARTESIAN_POINT('Ctrl Pts',(-134.729657039504,-3.14469017387093,
134.58837704684));
#107810=CARTESIAN_POINT('Ctrl Pts',(-134.737421792451,-3.03816203663097,
134.674440225489));
#107811=CARTESIAN_POINT('Ctrl Pts',(-134.745186545398,-2.9281092260801,
134.755988057324));
#107812=CARTESIAN_POINT('Ctrl Pts',(-134.752943586283,-2.81816572153215,
134.837454894702));
#107813=CARTESIAN_POINT('Ctrl Pts',(-134.760700627168,-2.70470482242719,
134.914415078776));
#107814=CARTESIAN_POINT('Ctrl Pts',(-134.768457668053,-2.58813418933842,
134.986554357755));
#107815=CARTESIAN_POINT('Ctrl Pts',(-134.776208859293,-2.4716514630707,
135.058639235943));
#107816=CARTESIAN_POINT('Ctrl Pts',(-134.783960050533,-2.35206400165679,
135.125910240338));
#107817=CARTESIAN_POINT('Ctrl Pts',(-134.791711241773,-2.22980962459591,
135.188095566278));
#107818=CARTESIAN_POINT('Ctrl Pts',(-134.79945913855,-2.10760720890669,
135.250254461795));
#107819=CARTESIAN_POINT('Ctrl Pts',(-134.807207035327,-1.98274047978162,
135.307331801131));
#107820=CARTESIAN_POINT('Ctrl Pts',(-134.814954932104,-1.85567291934199,
135.359101123777));
#107821=CARTESIAN_POINT('Ctrl Pts',(-134.822701208188,-1.72863193869674,
135.410859617397));
#107822=CARTESIAN_POINT('Ctrl Pts',(-134.830447484273,-1.59939140427053,
135.4573121554));
#107823=CARTESIAN_POINT('Ctrl Pts',(-134.838193760357,-1.46843552628352,
135.498280106399));
#107824=CARTESIAN_POINT('Ctrl Pts',(-134.845940093622,-1.33747868160979,
135.539248359814));
#107825=CARTESIAN_POINT('Ctrl Pts',(-134.853686426887,-1.20480684124116,
135.574731828708));
#107826=CARTESIAN_POINT('Ctrl Pts',(-134.861432760153,-1.07091976784501,
135.604601644154));
#107827=CARTESIAN_POINT('Ctrl Pts',(-134.869180828156,-0.937002711367266,
135.634478148738));
#107828=CARTESIAN_POINT('Ctrl Pts',(-134.876928896159,-0.801870261840225,
135.658738413198));
#107829=CARTESIAN_POINT('Ctrl Pts',(-134.884676964162,-0.666032378979198,
135.677304689957));
#107830=CARTESIAN_POINT('Ctrl Pts',(-134.892433266904,-0.53005012599959,
135.695890699176));
#107831=CARTESIAN_POINT('Ctrl Pts',(-134.900189569645,-0.393361329975081,
135.708770578864));
#107832=CARTESIAN_POINT('Ctrl Pts',(-134.907945872387,-0.256481638273815,
135.715918438841));
#107833=CARTESIAN_POINT('Ctrl Pts',(-134.915706314901,-0.11952888975972,
135.723070113846));
#107834=CARTESIAN_POINT('Ctrl Pts',(-134.923466757416,0.0176145666959897,
135.724483669094));
#107835=CARTESIAN_POINT('Ctrl Pts',(-134.93122719993,0.154434073432016,
135.720185388595));
#107836=CARTESIAN_POINT('Ctrl Pts',(-134.939000100195,0.291473214986519,
135.715880208115));
#107837=CARTESIAN_POINT('Ctrl Pts',(-134.946773000461,0.428186977489429,
135.705844897649));
#107838=CARTESIAN_POINT('Ctrl Pts',(-134.954545900726,0.564065907387949,
135.690157657418));
#107839=CARTESIAN_POINT('Ctrl Pts',(-134.962036236488,0.695005295926288,
135.675040687882));
#107840=CARTESIAN_POINT('Ctrl Pts',(-134.96952657225,0.825169190298912,
135.654675625719));
#107841=CARTESIAN_POINT('Ctrl Pts',(-134.977016908012,0.954113423894353,
135.629176742233));
#107842=CARTESIAN_POINT('Ctrl Pts',(-134.984791242131,1.08794661729813,
135.602711060829));
#107843=CARTESIAN_POINT('Ctrl Pts',(-134.99256557625,1.22088978065673,135.570630740247));
#107844=CARTESIAN_POINT('Ctrl Pts',(-135.000339910369,1.35243511854286,
135.533007602977));
#107845=CARTESIAN_POINT('Ctrl Pts',(-135.008104663316,1.48381833855659,
135.49543083286));
#107846=CARTESIAN_POINT('Ctrl Pts',(-135.015869416263,1.61380678846277,
135.452324944236));
#107847=CARTESIAN_POINT('Ctrl Pts',(-135.023634169211,1.74190152123189,
135.403812992885));
#107848=CARTESIAN_POINT('Ctrl Pts',(-135.031391210096,1.86986902850694,
135.355349224288));
#107849=CARTESIAN_POINT('Ctrl Pts',(-135.039148250981,1.99594619839706,
135.30149021584));
#107850=CARTESIAN_POINT('Ctrl Pts',(-135.046905291866,2.11964829147391,
135.242409083159));
#107851=CARTESIAN_POINT('Ctrl Pts',(-135.054656483106,2.24325709984027,
135.183372504019));
#107852=CARTESIAN_POINT('Ctrl Pts',(-135.062407674346,2.36449404503223,
135.1191218069));
#107853=CARTESIAN_POINT('Ctrl Pts',(-135.070158865586,2.48289379795623,
135.049878424686));
#107854=CARTESIAN_POINT('Ctrl Pts',(-135.077906762363,2.60124322782633,
134.980664472757));
#107855=CARTESIAN_POINT('Ctrl Pts',(-135.08565465914,2.71675752705532,134.906462253237));
#107856=CARTESIAN_POINT('Ctrl Pts',(-135.093402555917,2.82899564459609,
134.827539299325));
#107857=CARTESIAN_POINT('Ctrl Pts',(-135.101148832001,2.94121028434255,
134.748632854393));
#107858=CARTESIAN_POINT('Ctrl Pts',(-135.108895108086,3.05014978590222,
134.665007863955));
#107859=CARTESIAN_POINT('Ctrl Pts',(-135.11664138417,3.15540213417772,134.576975153154));
#107860=CARTESIAN_POINT('Ctrl Pts',(-135.124387717435,3.26065525940142,
134.488941792516));
#107861=CARTESIAN_POINT('Ctrl Pts',(-135.1321340507,3.3622208771345,134.396500897421));
#107862=CARTESIAN_POINT('Ctrl Pts',(-135.139880383966,3.45972043236972,
134.300003275554));
#107863=CARTESIAN_POINT('Ctrl Pts',(-135.147628451969,3.55724182195499,
134.203484043712));
#107864=CARTESIAN_POINT('Ctrl Pts',(-135.155376519972,3.65069505929536,
134.102906552306));
#107865=CARTESIAN_POINT('Ctrl Pts',(-135.163124587975,3.73973908746803,
133.99865782042));
#107866=CARTESIAN_POINT('Ctrl Pts',(-135.170880890716,3.82887775269336,
133.894298291742));
#107867=CARTESIAN_POINT('Ctrl Pts',(-135.178637193458,3.91359759331332,
133.786260025999));
#107868=CARTESIAN_POINT('Ctrl Pts',(-135.1863934962,3.99359810718647,133.67496285765));
#107869=CARTESIAN_POINT('Ctrl Pts',(-135.194153938714,4.07364131974264,
133.563606286651));
#107870=CARTESIAN_POINT('Ctrl Pts',(-135.201914381228,4.14895997193643,
133.44898767377));
#107871=CARTESIAN_POINT('Ctrl Pts',(-135.209674823743,4.21929799221194,
133.331554222222));
#107872=CARTESIAN_POINT('Ctrl Pts',(-135.217447724008,4.28974892532192,
133.213932256073));
#107873=CARTESIAN_POINT('Ctrl Pts',(-135.225220624274,4.3552030624649,133.093486765312));
#107874=CARTESIAN_POINT('Ctrl Pts',(-135.232993524539,4.41545082360962,
132.970688636769));
#107875=CARTESIAN_POINT('Ctrl Pts',(-135.240483860301,4.47350842688144,
132.85235452951));
#107876=CARTESIAN_POINT('Ctrl Pts',(-135.247974196063,4.52673148765348,
132.731836145199));
#107877=CARTESIAN_POINT('Ctrl Pts',(-135.255464531825,4.57497606270637,
132.609568940216));
#107878=CARTESIAN_POINT('Ctrl Pts',(-135.263238865944,4.62504984548622,
132.482665936993));
#107879=CARTESIAN_POINT('Ctrl Pts',(-135.271013200063,4.66991879033201,
132.353476891634));
#107880=CARTESIAN_POINT('Ctrl Pts',(-135.278787534182,4.70936884770434,
132.222467848622));
#107881=CARTESIAN_POINT('Ctrl Pts',(-135.286552287129,4.74877028640672,
132.091620262546));
#107882=CARTESIAN_POINT('Ctrl Pts',(-135.294317040076,4.78276601380415,
131.958957512455));
#107883=CARTESIAN_POINT('Ctrl Pts',(-135.302081793023,4.81118986715228,
131.824965891269));
#107884=CARTESIAN_POINT('Ctrl Pts',(-135.309838833908,4.83958548952856,
131.691107352451));
#107885=CARTESIAN_POINT('Ctrl Pts',(-135.317595874794,4.86242017028661,
131.555922949086));
#107886=CARTESIAN_POINT('Ctrl Pts',(-135.325352915679,4.87957754299677,
131.419914079405));
#107887=CARTESIAN_POINT('Ctrl Pts',(-135.333104106919,4.89672197719873,
131.284007775069));
#107888=CARTESIAN_POINT('Ctrl Pts',(-135.340855298159,4.90819757629105,
131.147278628267));
#107889=CARTESIAN_POINT('Ctrl Pts',(-135.348606489399,4.91393911629018,
131.010237823427));
#107890=CARTESIAN_POINT('Ctrl Pts',(-135.356354386176,4.91967821598163,
130.873255264585));
#107891=CARTESIAN_POINT('Ctrl Pts',(-135.364102282953,4.91968808751038,
130.735961700969));
#107892=CARTESIAN_POINT('Ctrl Pts',(-135.37185017973,4.91395541526928,130.598872809544));
#107893=CARTESIAN_POINT('Ctrl Pts',(-135.379596455814,4.90822394217959,
130.461812594159));
#107894=CARTESIAN_POINT('Ctrl Pts',(-135.387342731898,4.89675233092962,
130.324957356184));
#107895=CARTESIAN_POINT('Ctrl Pts',(-135.395089007983,4.87957938329119,
130.188821744172));
#107896=CARTESIAN_POINT('Ctrl Pts',(-135.402835341248,4.86240630888604,
130.052685127238));
#107897=CARTESIAN_POINT('Ctrl Pts',(-135.410581674513,4.83953186304386,
129.917268534758));
#107898=CARTESIAN_POINT('Ctrl Pts',(-135.418328007778,4.81104657197576,
129.783080075903));
#107899=CARTESIAN_POINT('Ctrl Pts',(-135.426076075781,4.78255490182426,
129.648861566472));
#107900=CARTESIAN_POINT('Ctrl Pts',(-135.433824143784,4.74844996730653,
129.515872120318));
#107901=CARTESIAN_POINT('Ctrl Pts',(-135.441572211787,4.70887302894273,
129.384607871559));
#107902=CARTESIAN_POINT('Ctrl Pts',(-135.449328514529,4.6692540277377,129.253204113592));
#107903=CARTESIAN_POINT('Ctrl Pts',(-135.457084817271,4.62415151821778,
129.123529590673));
#107904=CARTESIAN_POINT('Ctrl Pts',(-135.464841120013,4.57375629025588,
128.996064054542));
#107905=CARTESIAN_POINT('Ctrl Pts',(-135.472601562527,4.52333416484358,
128.868530486217));
#107906=CARTESIAN_POINT('Ctrl Pts',(-135.480362005041,4.46761385093035,
128.743208611014));
#107907=CARTESIAN_POINT('Ctrl Pts',(-135.488122447555,4.40683318031578,
128.620555593447));
#107908=CARTESIAN_POINT('Ctrl Pts',(-135.495895347821,4.34595493917273,
128.497705682367));
#107909=CARTESIAN_POINT('Ctrl Pts',(-135.503668248086,4.2800002965339,128.37753353323));
#107910=CARTESIAN_POINT('Ctrl Pts',(-135.511441148352,4.20925213969972,
128.260469997486));
#107911=CARTESIAN_POINT('Ctrl Pts',(-135.518931484114,4.14107585656954,
128.147662016129));
#107912=CARTESIAN_POINT('Ctrl Pts',(-135.526421819876,4.06844869098213,
128.037740817199));
#107913=CARTESIAN_POINT('Ctrl Pts',(-135.533912155638,3.99165919989679,
127.931062879012));
#107914=CARTESIAN_POINT('Ctrl Pts',(-135.541686489757,3.91195821191808,
127.820340214376));
#107915=CARTESIAN_POINT('Ctrl Pts',(-135.549460823876,3.82752056990735,
127.712760865688));
#107916=CARTESIAN_POINT('Ctrl Pts',(-135.557235157995,3.73862267128287,
127.608756827315));
#107917=CARTESIAN_POINT('Ctrl Pts',(-135.564999910942,3.6498343313739,127.504880964624));
#107918=CARTESIAN_POINT('Ctrl Pts',(-135.57276466389,3.55659692356819,127.404571939464));
#107919=CARTESIAN_POINT('Ctrl Pts',(-135.580529416837,3.45922976485109,
127.308232402459));
#107920=CARTESIAN_POINT('Ctrl Pts',(-135.588286457722,3.3619593125684,127.21198855124));
#107921=CARTESIAN_POINT('Ctrl Pts',(-135.596043498607,3.26056754811422,
127.119706615525));
#107922=CARTESIAN_POINT('Ctrl Pts',(-135.603800539492,3.15541341312163,
127.031755515678));
#107923=CARTESIAN_POINT('Ctrl Pts',(-135.611551730732,3.0503385756795,126.943870740438));
#107924=CARTESIAN_POINT('Ctrl Pts',(-135.619302921972,2.9415073137202,126.860310550274));
#107925=CARTESIAN_POINT('Ctrl Pts',(-135.627054113212,2.82931444602472,
126.78140612764));
#107926=CARTESIAN_POINT('Ctrl Pts',(-135.634802009989,2.71716926329162,
126.702535241491));
#107927=CARTESIAN_POINT('Ctrl Pts',(-135.642549906766,2.60166563566736,
126.628316411577));
#107928=CARTESIAN_POINT('Ctrl Pts',(-135.650297803543,2.48323021937723,
126.559039576694));
#107929=CARTESIAN_POINT('Ctrl Pts',(-135.658044079628,2.364819577223,126.489777233031));
#107930=CARTESIAN_POINT('Ctrl Pts',(-135.665790355711,2.24347870348298,
126.425455025468));
#107931=CARTESIAN_POINT('Ctrl Pts',(-135.673536631796,2.11966155986546,
126.36631848909));
#107932=CARTESIAN_POINT('Ctrl Pts',(-135.681282965061,1.99584350225775,
126.307181516179));
#107933=CARTESIAN_POINT('Ctrl Pts',(-135.689029298326,1.86954949108976,
126.253230459335));
#107934=CARTESIAN_POINT('Ctrl Pts',(-135.696775631592,1.74125594462539,
126.204663801709));
#107935=CARTESIAN_POINT('Ctrl Pts',(-135.704523699595,1.6129336677103,126.156086267917));
#107936=CARTESIAN_POINT('Ctrl Pts',(-135.712271767598,1.48261133003691,
126.112895671134));
#107937=CARTESIAN_POINT('Ctrl Pts',(-135.720019835601,1.3507826980513,126.075241337494));
#107938=CARTESIAN_POINT('Ctrl Pts',(-135.727776138343,1.21881395702702,
126.037546984381));
#107939=CARTESIAN_POINT('Ctrl Pts',(-135.735532441084,1.08533610023545,
126.005400755895));
#107940=CARTESIAN_POINT('Ctrl Pts',(-135.743288743826,0.950855882991227,
125.978901452649));
#107941=CARTESIAN_POINT('Ctrl Pts',(-135.75104918634,0.816303889606305,
125.952388005927));
#107942=CARTESIAN_POINT('Ctrl Pts',(-135.758809628855,0.680748855983335,
125.9315275494));
#107943=CARTESIAN_POINT('Ctrl Pts',(-135.766570071369,0.54470396147231,
125.916367097024));
#107944=CARTESIAN_POINT('Ctrl Pts',(-135.774342971634,0.408440675619118,
125.901182307745));
#107945=CARTESIAN_POINT('Ctrl Pts',(-135.7821158719,0.271686347719986,125.891715834554));
#107946=CARTESIAN_POINT('Ctrl Pts',(-135.789888772165,0.134956372797775,
125.887962562085));
#107947=CARTESIAN_POINT('Ctrl Pts',(-135.797379107927,0.00319687686786632,
125.884345730524));
#107948=CARTESIAN_POINT('Ctrl Pts',(-135.804869443689,-0.128539697936056,
125.886033928844));
#107949=CARTESIAN_POINT('Ctrl Pts',(-135.812359779451,-0.259797464224848,
125.892977071142));
#107950=CARTESIAN_POINT('Ctrl Pts',(-135.82013411357,-0.39603190861952,
125.900183464791));
#107951=CARTESIAN_POINT('Ctrl Pts',(-135.827908447689,-0.532182069487139,
125.913073978675));
#107952=CARTESIAN_POINT('Ctrl Pts',(-135.835682781808,-0.667735098176365,
125.931649575326));
#107953=CARTESIAN_POINT('Ctrl Pts',(-135.843447534755,-0.803121069871718,
125.950202279215));
#107954=CARTESIAN_POINT('Ctrl Pts',(-135.851212287702,-0.937910990007601,
125.974426072739));
#107955=CARTESIAN_POINT('Ctrl Pts',(-135.858977040649,-1.07159349857896,
126.004269947974));
#107956=CARTESIAN_POINT('Ctrl Pts',(-135.866734081534,-1.2051432317993,
126.034084181851));
#107957=CARTESIAN_POINT('Ctrl Pts',(-135.874491122419,-1.33758736319606,
126.069507304486));
#107958=CARTESIAN_POINT('Ctrl Pts',(-135.882248163304,-1.46842149289897,
126.110436738582));
#107959=CARTESIAN_POINT('Ctrl Pts',(-135.889999354544,-1.59915695956568,
126.151335307474));
#107960=CARTESIAN_POINT('Ctrl Pts',(-135.897750545784,-1.72828446953734,
126.197731806567));
#107961=CARTESIAN_POINT('Ctrl Pts',(-135.905501737025,-1.85531198044017,
126.249473075844));
#107962=CARTESIAN_POINT('Ctrl Pts',(-135.913249633802,-1.9822855012628,
126.301192353702));
#107963=CARTESIAN_POINT('Ctrl Pts',(-135.920997530579,-2.10716043691919,
126.358251736391));
#107964=CARTESIAN_POINT('Ctrl Pts',(-135.928745427356,-2.22946223557937,
126.420448984945));
#107965=CARTESIAN_POINT('Ctrl Pts',(-135.93649170344,-2.3517384513398,126.482633223177));
#107966=CARTESIAN_POINT('Ctrl Pts',(-135.944237979524,-2.47144225243399,
126.549953012461));
#107967=CARTESIAN_POINT('Ctrl Pts',(-135.951984255608,-2.58812168584984,
126.622159139668));
#107968=CARTESIAN_POINT('Ctrl Pts',(-135.959730588873,-2.70480198056661,
126.694365799883));
#107969=CARTESIAN_POINT('Ctrl Pts',(-135.967476922138,-2.81845753060206,
126.771458664259));
#107970=CARTESIAN_POINT('Ctrl Pts',(-135.975223255404,-2.92866383074969,
126.853144193608));
#107971=CARTESIAN_POINT('Ctrl Pts',(-135.982971323407,-3.03889481083367,
126.934848015864));
#107972=CARTESIAN_POINT('Ctrl Pts',(-135.99071939141,-3.14567468993953,
127.021146316918));
#107973=CARTESIAN_POINT('Ctrl Pts',(-135.998467459413,-3.24861094293739,
127.111704391497));
#107974=CARTESIAN_POINT('Ctrl Pts',(-136.006223762154,-3.35165659781059,
127.202358712275));
#107975=CARTESIAN_POINT('Ctrl Pts',(-136.013980064896,-3.45085017223776,
127.297281591771));
#107976=CARTESIAN_POINT('Ctrl Pts',(-136.021736367638,-3.5458346288403,
127.39610008653));
#107977=CARTESIAN_POINT('Ctrl Pts',(-136.029496810152,-3.64086978150725,
127.494971323695));
#107978=CARTESIAN_POINT('Ctrl Pts',(-136.037257252666,-3.73169108117181,
127.597742026302));
#107979=CARTESIAN_POINT('Ctrl Pts',(-136.045017695181,-3.81798158768606,
127.704005854222));
#107980=CARTESIAN_POINT('Ctrl Pts',(-136.052790595446,-3.90441061538187,
127.810440266272));
#107981=CARTESIAN_POINT('Ctrl Pts',(-136.060563495711,-3.98629408202232,
127.920378695426));
#107982=CARTESIAN_POINT('Ctrl Pts',(-136.068336395977,-4.06335770770966,
128.033384760274));
#107983=CARTESIAN_POINT('Ctrl Pts',(-136.075826731739,-4.13761987649234,
128.14228277002));
#107984=CARTESIAN_POINT('Ctrl Pts',(-136.083317067501,-4.20740638396089,
128.254028993808));
#107985=CARTESIAN_POINT('Ctrl Pts',(-136.090807403263,-4.27251295053554,
128.36821280801));
#107986=CARTESIAN_POINT('Ctrl Pts',(-136.098918087298,-4.34301163134893,
128.491853305351));
#107987=CARTESIAN_POINT('Ctrl Pts',(-136.107028771333,-4.40823032391749,
128.618715240005));
#107988=CARTESIAN_POINT('Ctrl Pts',(-136.115139455368,-4.46787596845634,
128.748328664266));
#107989=CARTESIAN_POINT('Ctrl Pts',(-136.123517932265,-4.52949095095091,
128.882221573441));
#107990=CARTESIAN_POINT('Ctrl Pts',(-136.131896409163,-4.58515829912374,
129.019050525924));
#107991=CARTESIAN_POINT('Ctrl Pts',(-136.140274886061,-4.6346039730973,
129.158265518536));
#107992=CARTESIAN_POINT('Ctrl Pts',(-136.148653362959,-4.68404964707086,
129.297480511148));
#107993=CARTESIAN_POINT('Ctrl Pts',(-136.157031839857,-4.72727343413117,
129.439081191632));
#107994=CARTESIAN_POINT('Ctrl Pts',(-136.165410316754,-4.76405452823394,
129.582490119308));
#107995=CARTESIAN_POINT('Ctrl Pts',(-134.415184333433,-4.76405452823397,
129.582490119308));
#107996=CARTESIAN_POINT('Ctrl Pts',(-134.416830109084,-4.77123413959544,
129.61048331504));
#107997=CARTESIAN_POINT('Ctrl Pts',(-134.418475884735,-4.77816469915982,
129.638530767353));
#107998=CARTESIAN_POINT('Ctrl Pts',(-134.420121660386,-4.7848455356183,
129.666627668771));
#107999=CARTESIAN_POINT('Ctrl Pts',(-134.430958144317,-4.82883499242778,
129.851629567725));
#108000=CARTESIAN_POINT('Ctrl Pts',(-134.441794628249,-4.86211074913044,
130.03926938264));
#108001=CARTESIAN_POINT('Ctrl Pts',(-134.452631112179,-4.88441983383602,
130.228490884615));
#108002=CARTESIAN_POINT('Ctrl Pts',(-134.462854396381,-4.90546652339598,
130.407004986053));
#108003=CARTESIAN_POINT('Ctrl Pts',(-134.473077680582,-4.91675286075667,
130.586927132526));
#108004=CARTESIAN_POINT('Ctrl Pts',(-134.483300964783,-4.91811071544171,
130.767346388444));
#108005=CARTESIAN_POINT('Ctrl Pts',(-134.483914164512,-4.91819216051448,
130.778168061478));
#108006=CARTESIAN_POINT('Ctrl Pts',(-134.484527364242,-4.91823789935196,
130.788991514613));
#108007=CARTESIAN_POINT('Ctrl Pts',(-134.485140563972,-4.91824790082115,
130.799816547985));
#108008=CARTESIAN_POINT('',(-134.139859435957,-4.91824948933185,130.806601864317));
#108009=CARTESIAN_POINT('Ctrl Pts',(-134.069717999649,-4.76405452823413,
129.582490119309));
#108010=CARTESIAN_POINT('Ctrl Pts',(-134.077393660297,-4.79779154961053,
129.714030253624));
#108011=CARTESIAN_POINT('Ctrl Pts',(-134.085069320945,-4.82605188755225,
129.846872908459));
#108012=CARTESIAN_POINT('Ctrl Pts',(-134.092744981594,-4.84875916336053,
129.980517405403));
#108013=CARTESIAN_POINT('Ctrl Pts',(-134.100597390654,-4.87198932249181,
130.117239351146));
#108014=CARTESIAN_POINT('Ctrl Pts',(-134.108449799715,-4.88940751121968,
130.254800071525));
#108015=CARTESIAN_POINT('Ctrl Pts',(-134.116302208776,-4.90098825429152,
130.392660248612));
#108016=CARTESIAN_POINT('Ctrl Pts',(-134.124154617836,-4.91256899736335,
130.5305204257));
#108017=CARTESIAN_POINT('Ctrl Pts',(-134.132007026897,-4.91831234051333,
130.668679615899));
#108018=CARTESIAN_POINT('Ctrl Pts',(-134.139859435957,-4.91824948933185,
130.806601864317));
#108019=CARTESIAN_POINT('Ctrl Pts',(-134.139859435993,-4.91824948933156,
130.806601864944));
#108020=CARTESIAN_POINT('Ctrl Pts',(-134.14699396824,-4.9181923840658,130.931915093187));
#108021=CARTESIAN_POINT('Ctrl Pts',(-134.154128500486,-4.91334639594518,
131.057114832502));
#108022=CARTESIAN_POINT('Ctrl Pts',(-134.161263032733,-4.90373476650503,
131.181942929479));
#108023=CARTESIAN_POINT('Ctrl Pts',(-134.169037366852,-4.89326119709418,
131.317965208143));
#108024=CARTESIAN_POINT('Ctrl Pts',(-134.176811700971,-4.87710716690586,
131.453766824337));
#108025=CARTESIAN_POINT('Ctrl Pts',(-134.18458603509,-4.85528402063956,
131.588835054002));
#108026=CARTESIAN_POINT('Ctrl Pts',(-134.192350788037,-4.83348776945065,
131.723736824146));
#108027=CARTESIAN_POINT('Ctrl Pts',(-134.200115540984,-4.80603636535375,
131.857906623863));
#108028=CARTESIAN_POINT('Ctrl Pts',(-134.207880293932,-4.77299307281504,
131.990834464458));
#108029=CARTESIAN_POINT('Ctrl Pts',(-134.215637334817,-4.7399825993404,
132.123630279248));
#108030=CARTESIAN_POINT('Ctrl Pts',(-134.223394375701,-4.7013913837258,
132.255186212736));
#108031=CARTESIAN_POINT('Ctrl Pts',(-134.231151416586,-4.65733407793156,
132.385000471877));
#108032=CARTESIAN_POINT('Ctrl Pts',(-134.238902607827,-4.61330999609415,
132.514716837077));
#108033=CARTESIAN_POINT('Ctrl Pts',(-134.246653799067,-4.56382815385111,
132.642693773468));
#108034=CARTESIAN_POINT('Ctrl Pts',(-134.254404990307,-4.5090534747724,
132.768443055791));
#108035=CARTESIAN_POINT('Ctrl Pts',(-134.262152887084,-4.45430207639353,
132.894138891314));
#108036=CARTESIAN_POINT('Ctrl Pts',(-134.269900783861,-4.39426247125905,
133.01760859822));
#108037=CARTESIAN_POINT('Ctrl Pts',(-134.277648680638,-4.3291482280303,
133.138382614515));
#108038=CARTESIAN_POINT('Ctrl Pts',(-134.285394956722,-4.26404760529753,
133.25913136749));
#108039=CARTESIAN_POINT('Ctrl Pts',(-134.293141232806,-4.19387464128219,
133.377185207525));
#108040=CARTESIAN_POINT('Ctrl Pts',(-134.30088750889,-4.11888932297478,
133.492098292188));
#108041=CARTESIAN_POINT('Ctrl Pts',(-134.308633842156,-4.04390345114269,
133.607012225114));
#108042=CARTESIAN_POINT('Ctrl Pts',(-134.316380175421,-3.96410536778918,
133.718785028983));
#108043=CARTESIAN_POINT('Ctrl Pts',(-134.324126508686,-3.87979871452275,
133.826999364967));
#108044=CARTESIAN_POINT('Ctrl Pts',(-134.331874576689,-3.79547318136574,
133.935237934801));
#108045=CARTESIAN_POINT('Ctrl Pts',(-134.339622644693,-3.70663730941524,
134.039916142666));
#108046=CARTESIAN_POINT('Ctrl Pts',(-134.347370712696,-3.61363512707809,
134.140649608473));
#108047=CARTESIAN_POINT('Ctrl Pts',(-134.355127015437,-3.5205341009152,
134.241490135006));
#108048=CARTESIAN_POINT('Ctrl Pts',(-134.362883318179,-3.42325818458389,
134.338377256757));
#108049=CARTESIAN_POINT('Ctrl Pts',(-134.370639620921,-3.32218878205257,
134.430962988781));
#108050=CARTESIAN_POINT('Ctrl Pts',(-134.378400063435,-3.2210654357377,
134.523598136598));
#108051=CARTESIAN_POINT('Ctrl Pts',(-134.386160505949,-3.11614486778376,
134.61192706848));
#108052=CARTESIAN_POINT('Ctrl Pts',(-134.393920948464,-3.00784090699308,
134.695642686591));
#108053=CARTESIAN_POINT('Ctrl Pts',(-134.401693848729,-2.89936308706975,
134.779492692445));
#108054=CARTESIAN_POINT('Ctrl Pts',(-134.409466748994,-2.78749134004539,
134.858714359504));
#108055=CARTESIAN_POINT('Ctrl Pts',(-134.41723964926,-2.67266850362333,
134.933043958807));
#108056=CARTESIAN_POINT('Ctrl Pts',(-134.424729985022,-2.56201976652617,
135.00467148995));
#108057=CARTESIAN_POINT('Ctrl Pts',(-134.432220320784,-2.44863103913397,
135.071756299375));
#108058=CARTESIAN_POINT('Ctrl Pts',(-134.439710656546,-2.33291772897051,
135.134104020166));
#108059=CARTESIAN_POINT('Ctrl Pts',(-134.447484990665,-2.2128171134824,
135.198815673739));
#108060=CARTESIAN_POINT('Ctrl Pts',(-134.455259324784,-2.08983171977518,
135.258628921328));
#108061=CARTESIAN_POINT('Ctrl Pts',(-134.463033658903,-1.96439904921026,
135.313276167669));
#108062=CARTESIAN_POINT('Ctrl Pts',(-134.47079841185,-1.83912096320156,
135.367856066163));
#108063=CARTESIAN_POINT('Ctrl Pts',(-134.478563164797,-1.71140195636095,
135.417282476459));
#108064=CARTESIAN_POINT('Ctrl Pts',(-134.486327917745,-1.58170529261166,
135.461332963396));
#108065=CARTESIAN_POINT('Ctrl Pts',(-134.49408495863,-1.45213744541721,
135.505339698768));
#108066=CARTESIAN_POINT('Ctrl Pts',(-134.501841999515,-1.32059621803381,
135.543981011594));
#108067=CARTESIAN_POINT('Ctrl Pts',(-134.5095990404,-1.18756575534543,135.577082130417));
#108068=CARTESIAN_POINT('Ctrl Pts',(-134.51735023164,-1.0546356119636,135.610158287429));
#108069=CARTESIAN_POINT('Ctrl Pts',(-134.52510142288,-0.920218846489242,
135.637702472281));
#108070=CARTESIAN_POINT('Ctrl Pts',(-134.53285261412,-0.78481536187858,
135.659589542165));
#108071=CARTESIAN_POINT('Ctrl Pts',(-134.540600510897,-0.649469427360699,
135.68146730946));
#108072=CARTESIAN_POINT('Ctrl Pts',(-134.548348407674,-0.513137992972702,
135.697692681748));
#108073=CARTESIAN_POINT('Ctrl Pts',(-134.556096304451,-0.376331553596354,
135.708191530665));
#108074=CARTESIAN_POINT('Ctrl Pts',(-134.563842580535,-0.239553731177918,
135.71868818345));
#108075=CARTESIAN_POINT('Ctrl Pts',(-134.57158885662,-0.102301490977237,
135.723460665586));
#108076=CARTESIAN_POINT('Ctrl Pts',(-134.579335132704,0.0349095378211423,
135.722486722768));
#108077=CARTESIAN_POINT('Ctrl Pts',(-134.587081465969,0.172121579479979,
135.72151277276));
#108078=CARTESIAN_POINT('Ctrl Pts',(-134.594827799234,0.309292018174121,
135.714792315929));
#108079=CARTESIAN_POINT('Ctrl Pts',(-134.6025741325,0.44590560922136,135.702355232729));
#108080=CARTESIAN_POINT('Ctrl Pts',(-134.610322200503,0.582549793934916,
135.68991536433));
#108081=CARTESIAN_POINT('Ctrl Pts',(-134.618070268506,0.718636493578164,
135.671756357554));
#108082=CARTESIAN_POINT('Ctrl Pts',(-134.625818336509,0.853656362539028,
135.647959886415));
#108083=CARTESIAN_POINT('Ctrl Pts',(-134.63357463925,0.988819732223933,
135.624138124104));
#108084=CARTESIAN_POINT('Ctrl Pts',(-134.641330941992,1.12291362061326,
135.594666996603));
#108085=CARTESIAN_POINT('Ctrl Pts',(-134.649087244734,1.25543909995521,
135.55967929551));
#108086=CARTESIAN_POINT('Ctrl Pts',(-134.656847687248,1.38803531213538,
135.524672920428));
#108087=CARTESIAN_POINT('Ctrl Pts',(-134.664608129763,1.5190610739389,135.484144220339));
#108088=CARTESIAN_POINT('Ctrl Pts',(-134.672368572277,1.6480343306843,135.438275367255));
#108089=CARTESIAN_POINT('Ctrl Pts',(-134.680141472542,1.77721462675114,
135.392332881416));
#108090=CARTESIAN_POINT('Ctrl Pts',(-134.687914372808,1.90433547080781,
135.341033258414));
#108091=CARTESIAN_POINT('Ctrl Pts',(-134.695687273073,2.0289356156144,135.284606518205));
#108092=CARTESIAN_POINT('Ctrl Pts',(-134.703177608835,2.14900623130743,
135.230231032133));
#108093=CARTESIAN_POINT('Ctrl Pts',(-134.710667944597,2.2667359582452,135.171094862575));
#108094=CARTESIAN_POINT('Ctrl Pts',(-134.718158280359,2.38173673212182,
135.107442443579));
#108095=CARTESIAN_POINT('Ctrl Pts',(-134.725932614478,2.50109779529455,
135.041376623769));
#108096=CARTESIAN_POINT('Ctrl Pts',(-134.733706948597,2.61789698387393,
134.970236050257));
#108097=CARTESIAN_POINT('Ctrl Pts',(-134.741481282716,2.73167268221469,
134.894244163554));
#108098=CARTESIAN_POINT('Ctrl Pts',(-134.749246035663,2.84530816217566,
134.818345930059));
#108099=CARTESIAN_POINT('Ctrl Pts',(-134.75701078861,2.95592724389358,134.737608494486));
#108100=CARTESIAN_POINT('Ctrl Pts',(-134.764775541557,3.06309238090191,
134.652301382256));
#108101=CARTESIAN_POINT('Ctrl Pts',(-134.772532582442,3.1701510799854,134.567078998252));
#108102=CARTESIAN_POINT('Ctrl Pts',(-134.780289623327,3.27376235731816,
134.477296211662));
#108103=CARTESIAN_POINT('Ctrl Pts',(-134.788046664212,3.37351748058916,
134.383265879047));
#108104=CARTESIAN_POINT('Ctrl Pts',(-134.795797855453,3.47319737774557,
134.289306455438));
#108105=CARTESIAN_POINT('Ctrl Pts',(-134.803549046693,3.56902662560396,
134.191106128481));
#108106=CARTESIAN_POINT('Ctrl Pts',(-134.811300237933,3.66062972821697,
134.089017837946));
#108107=CARTESIAN_POINT('Ctrl Pts',(-134.81904813471,3.7521938970679,133.986972937658));
#108108=CARTESIAN_POINT('Ctrl Pts',(-134.826796031487,3.83953523266718,
133.881043650849));
#108109=CARTESIAN_POINT('Ctrl Pts',(-134.834543928264,3.92231543376989,
133.771619403131));
#108110=CARTESIAN_POINT('Ctrl Pts',(-134.842290204348,4.00507831903908,
133.662218044606));
#108111=CARTESIAN_POINT('Ctrl Pts',(-134.850036480432,4.08328173182491,
133.549323490909));
#108112=CARTESIAN_POINT('Ctrl Pts',(-134.857782756516,4.15662823877952,
133.43335752648));
#108113=CARTESIAN_POINT('Ctrl Pts',(-134.865529089782,4.22997528716148,
133.317390706017));
#108114=CARTESIAN_POINT('Ctrl Pts',(-134.873275423047,4.2984651491848,133.198352760001));
#108115=CARTESIAN_POINT('Ctrl Pts',(-134.881021756312,4.36184446178538,
133.076693329493));
#108116=CARTESIAN_POINT('Ctrl Pts',(-134.888769824315,4.42523796774349,
132.955006654199));
#108117=CARTESIAN_POINT('Ctrl Pts',(-134.896517892318,4.48351846631249,
132.830697672892));
#108118=CARTESIAN_POINT('Ctrl Pts',(-134.904265960321,4.53647935840965,
132.704239059263));
#108119=CARTESIAN_POINT('Ctrl Pts',(-134.912022263063,4.58949653797325,
132.577646043913));
#108120=CARTESIAN_POINT('Ctrl Pts',(-134.919778565805,4.63718266584084,
132.448899193589));
#108121=CARTESIAN_POINT('Ctrl Pts',(-134.927534868547,4.67937978070716,
132.318490047439));
#108122=CARTESIAN_POINT('Ctrl Pts',(-134.935295311061,4.72159941744422,
132.188011298002));
#108123=CARTESIAN_POINT('Ctrl Pts',(-134.943055753575,4.75832409896428,
132.055868861388));
#108124=CARTESIAN_POINT('Ctrl Pts',(-134.95081619609,4.78944652940935,131.922566772275));
#108125=CARTESIAN_POINT('Ctrl Pts',(-134.958589096355,4.82061892034268,
131.789050694814));
#108126=CARTESIAN_POINT('Ctrl Pts',(-134.96636199662,4.84617101594217,131.654371629164));
#108127=CARTESIAN_POINT('Ctrl Pts',(-134.974134896886,4.86604702311163,
131.519041967096));
#108128=CARTESIAN_POINT('Ctrl Pts',(-134.981625232648,4.88520048735589,
131.388631879119));
#108129=CARTESIAN_POINT('Ctrl Pts',(-134.98911556841,4.89908334620185,131.257617981438));
#108130=CARTESIAN_POINT('Ctrl Pts',(-134.996605904172,4.90769149070061,
131.126458886119));
#108131=CARTESIAN_POINT('Ctrl Pts',(-135.004380238291,4.9166260156144,130.990326853836));
#108132=CARTESIAN_POINT('Ctrl Pts',(-135.01215457241,4.91990625071914,130.853607170871));
#108133=CARTESIAN_POINT('Ctrl Pts',(-135.019928906529,4.91747066831249,
130.716808982594));
#108134=CARTESIAN_POINT('Ctrl Pts',(-135.027693659476,4.91503808754349,
130.580179385857));
#108135=CARTESIAN_POINT('Ctrl Pts',(-135.035458412423,4.90690371208257,
130.443471863464));
#108136=CARTESIAN_POINT('Ctrl Pts',(-135.043223165371,4.89305779674734,
130.307200220722));
#108137=CARTESIAN_POINT('Ctrl Pts',(-135.050980206256,4.87922563337041,
130.171063924897));
#108138=CARTESIAN_POINT('Ctrl Pts',(-135.058737247141,4.85969325847608,
130.035363033634));
#108139=CARTESIAN_POINT('Ctrl Pts',(-135.066494288026,4.83450295735238,
129.900610531618));
#108140=CARTESIAN_POINT('Ctrl Pts',(-135.074245479266,4.80933165243068,
129.765959647511));
#108141=CARTESIAN_POINT('Ctrl Pts',(-135.081996670506,4.77851098541058,
129.632256111866));
#108142=CARTESIAN_POINT('Ctrl Pts',(-135.089747861746,4.74213492978522,
129.500006612623));
#108143=CARTESIAN_POINT('Ctrl Pts',(-135.097495758523,4.70577433495381,
129.367813322945));
#108144=CARTESIAN_POINT('Ctrl Pts',(-135.1052436553,4.66386315121035,129.237073216683));
#108145=CARTESIAN_POINT('Ctrl Pts',(-135.112991552077,4.61654615326392,
129.108281410311));
#108146=CARTESIAN_POINT('Ctrl Pts',(-135.120737828161,4.56923905301355,
128.979516544408));
#108147=CARTESIAN_POINT('Ctrl Pts',(-135.128484104246,4.51652852248383,
128.852699534519));
#108148=CARTESIAN_POINT('Ctrl Pts',(-135.13623038033,4.45860865087981,128.728308604537));
#108149=CARTESIAN_POINT('Ctrl Pts',(-135.143976713595,4.40068835172437,
128.60391675633));
#108150=CARTESIAN_POINT('Ctrl Pts',(-135.15172304686,4.33755879979319,128.481951378191));
#108151=CARTESIAN_POINT('Ctrl Pts',(-135.159469380126,4.26946134191871,
128.362868673618));
#108152=CARTESIAN_POINT('Ctrl Pts',(-135.167217448129,4.20134863409078,
128.2437593013));
#108153=CARTESIAN_POINT('Ctrl Pts',(-135.174965516132,4.12826600056123,
128.127534226452));
#108154=CARTESIAN_POINT('Ctrl Pts',(-135.182713584135,4.05049944324079,
128.01462275841));
#108155=CARTESIAN_POINT('Ctrl Pts',(-135.190469886876,3.97265023469769,
127.901591286716));
#108156=CARTESIAN_POINT('Ctrl Pts',(-135.198226189618,3.89010738013041,
127.791880779383));
#108157=CARTESIAN_POINT('Ctrl Pts',(-135.20598249236,3.80319904340295,127.685889822648));
#108158=CARTESIAN_POINT('Ctrl Pts',(-135.213742934874,3.71624432107941,
127.579842295347));
#108159=CARTESIAN_POINT('Ctrl Pts',(-135.221503377388,3.62491973409948,
127.477518565939));
#108160=CARTESIAN_POINT('Ctrl Pts',(-135.229263819903,3.5295913450804,127.379281348522));
#108161=CARTESIAN_POINT('Ctrl Pts',(-135.237036720168,3.43410992646841,
127.280886432003));
#108162=CARTESIAN_POINT('Ctrl Pts',(-135.244809620433,3.334612146044,127.1865914056));
#108163=CARTESIAN_POINT('Ctrl Pts',(-135.252582520699,3.23149893598448,
127.096720169892));
#108164=CARTESIAN_POINT('Ctrl Pts',(-135.260072856461,3.1321341508374,127.010115979974));
#108165=CARTESIAN_POINT('Ctrl Pts',(-135.267563192223,3.02941247252673,
126.927619725755));
#108166=CARTESIAN_POINT('Ctrl Pts',(-135.275053527985,2.92371752338386,
126.849482755235));
#108167=CARTESIAN_POINT('Ctrl Pts',(-135.282827862104,2.81401511811908,
126.768383197728));
#108168=CARTESIAN_POINT('Ctrl Pts',(-135.290602196223,2.70076202393668,
126.691723114827));
#108169=CARTESIAN_POINT('Ctrl Pts',(-135.298376530342,2.58435334202991,
126.619829477039));
#108170=CARTESIAN_POINT('Ctrl Pts',(-135.306141283289,2.46808812341954,
126.548024441735));
#108171=CARTESIAN_POINT('Ctrl Pts',(-135.313906036236,2.3486753844421,126.480974367067));
#108172=CARTESIAN_POINT('Ctrl Pts',(-135.321670789183,2.22654213654588,
126.418965176253));
#108173=CARTESIAN_POINT('Ctrl Pts',(-135.329427830068,2.10453019311325,
126.357017573842));
#108174=CARTESIAN_POINT('Ctrl Pts',(-135.337184870953,1.97980346431021,
126.30010106762));
#108175=CARTESIAN_POINT('Ctrl Pts',(-135.344941911838,1.85281639490994,
126.248457362529));
#108176=CARTESIAN_POINT('Ctrl Pts',(-135.352693103078,1.72592508744669,
126.196852602358));
#108177=CARTESIAN_POINT('Ctrl Pts',(-135.360444294318,1.59677719286645,
126.150512875502));
#108178=CARTESIAN_POINT('Ctrl Pts',(-135.368195485558,1.46584979705351,
126.109632996609));
#108179=CARTESIAN_POINT('Ctrl Pts',(-135.375943382336,1.33497804887622,
126.068770492755));
#108180=CARTESIAN_POINT('Ctrl Pts',(-135.383691279113,1.20232867617534,
126.033363337685));
#108181=CARTESIAN_POINT('Ctrl Pts',(-135.39143917589,1.06839648872893,126.003557350885));
#108182=CARTESIAN_POINT('Ctrl Pts',(-135.399185451974,0.934492317008893,
125.973757598855));
#108183=CARTESIAN_POINT('Ctrl Pts',(-135.406931728058,0.79930624566797,
125.949556769507));
#108184=CARTESIAN_POINT('Ctrl Pts',(-135.414678004142,0.663345527966497,
125.931050061791));
#108185=CARTESIAN_POINT('Ctrl Pts',(-135.422424337407,0.527383806634076,
125.912543217463));
#108186=CARTESIAN_POINT('Ctrl Pts',(-135.430170670673,0.390647814923571,
125.89973063137));
#108187=CARTESIAN_POINT('Ctrl Pts',(-135.437917003938,0.253651823615402,
125.892655840722));
#108188=CARTESIAN_POINT('Ctrl Pts',(-135.445665071941,0.116625153004655,
125.885579465723));
#108189=CARTESIAN_POINT('Ctrl Pts',(-135.453413139944,-0.0206612426947995,
125.884243463208));
#108190=CARTESIAN_POINT('Ctrl Pts',(-135.461161207947,-0.157691582362782,
125.888639263853));
#108191=CARTESIAN_POINT('Ctrl Pts',(-135.468917510688,-0.294867559506259,
125.893039736406));
#108192=CARTESIAN_POINT('Ctrl Pts',(-135.47667381343,-0.431786545603219,
125.903184168647));
#108193=CARTESIAN_POINT('Ctrl Pts',(-135.484430116172,-0.567935818179739,
125.919011912619));
#108194=CARTESIAN_POINT('Ctrl Pts',(-135.492190558686,-0.70415775772241,
125.934848104334));
#108195=CARTESIAN_POINT('Ctrl Pts',(-135.4999510012,-0.839608779221424,
125.956373590666));
#108196=CARTESIAN_POINT('Ctrl Pts',(-135.507711443714,-0.973785855246366,
125.983476448596));
#108197=CARTESIAN_POINT('Ctrl Pts',(-135.51548434398,-1.10817832422542,
126.010622814441));
#108198=CARTESIAN_POINT('Ctrl Pts',(-135.523257244245,-1.24129238120005,
126.04336434998));
#108199=CARTESIAN_POINT('Ctrl Pts',(-135.531030144511,-1.37263880580378,
126.081538815793));
#108200=CARTESIAN_POINT('Ctrl Pts',(-135.538520480273,-1.49921045703433,
126.118325543619));
#108201=CARTESIAN_POINT('Ctrl Pts',(-135.546010816035,-1.62414046836977,
126.160156960324));
#108202=CARTESIAN_POINT('Ctrl Pts',(-135.553501151797,-1.74701001637993,
126.206846173307));
#108203=CARTESIAN_POINT('Ctrl Pts',(-135.561275715347,-1.87454196416161,
126.25530705209));
#108204=CARTESIAN_POINT('Ctrl Pts',(-135.569050278896,-2.00025798307386,
126.309155188687));
#108205=CARTESIAN_POINT('Ctrl Pts',(-135.576824842445,-2.12366937865501,
126.368234894295));
#108206=CARTESIAN_POINT('Ctrl Pts',(-135.584589771702,-2.24692784198943,
126.427241387928));
#108207=CARTESIAN_POINT('Ctrl Pts',(-135.592354700959,-2.36788701523326,
126.491466383794));
#108208=CARTESIAN_POINT('Ctrl Pts',(-135.600119630216,-2.48607550161256,
126.560705157614));
#108209=CARTESIAN_POINT('Ctrl Pts',(-135.607876794515,-2.60414579906952,
126.629874692404));
#108210=CARTESIAN_POINT('Ctrl Pts',(-135.615633958814,-2.71945058845976,
126.70404783078));
#108211=CARTESIAN_POINT('Ctrl Pts',(-135.623391123114,-2.83154085807021,
126.782972868097));
#108212=CARTESIAN_POINT('Ctrl Pts',(-135.631142385043,-2.94354583900826,
126.861837851926));
#108213=CARTESIAN_POINT('Ctrl Pts',(-135.638893646972,-3.05234085040114,
126.945447313396));
#108214=CARTESIAN_POINT('Ctrl Pts',(-135.646644908901,-3.15750410314911,
127.033505157449));
#108215=CARTESIAN_POINT('Ctrl Pts',(-135.654392610232,-3.26261904840245,
127.121522551499));
#108216=CARTESIAN_POINT('Ctrl Pts',(-135.662140311563,-3.36410525542632,
127.21398401172));
#108217=CARTESIAN_POINT('Ctrl Pts',(-135.669888012895,-3.46157261707227,
127.310552082567));
#108218=CARTESIAN_POINT('Ctrl Pts',(-135.677634018436,-3.55901864539654,
127.407099016925));
#108219=CARTESIAN_POINT('Ctrl Pts',(-135.685380023977,-3.65244730093421,
127.507750498632));
#108220=CARTESIAN_POINT('Ctrl Pts',(-135.693126029518,-3.74150434575747,
127.612131256574));
#108221=CARTESIAN_POINT('Ctrl Pts',(-135.700872017095,-3.83056118404747,
127.716511772446));
#108222=CARTESIAN_POINT('Ctrl Pts',(-135.708618004672,-3.91524617840537,
127.824621249715));
#108223=CARTESIAN_POINT('Ctrl Pts',(-135.716363992249,-3.99524476572642,
127.936050605654));
#108224=CARTESIAN_POINT('Ctrl Pts',(-135.724111639306,-4.07526049172812,
128.047503833916));
#108225=CARTESIAN_POINT('Ctrl Pts',(-135.731859286362,-4.15058758548289,
128.1622780383));
#108226=CARTESIAN_POINT('Ctrl Pts',(-135.739606933419,-4.22095450612584,
128.279934718532));
#108227=CARTESIAN_POINT('Ctrl Pts',(-135.747361798037,-4.29138697925732,
128.397701005494));
#108228=CARTESIAN_POINT('Ctrl Pts',(-135.755116662654,-4.35684985172949,
128.518354794396));
#108229=CARTESIAN_POINT('Ctrl Pts',(-135.762871527272,-4.41711712679915,
128.641432197429));
#108230=CARTESIAN_POINT('Ctrl Pts',(-135.770630500632,-4.47741633314267,
128.764574810283));
#108231=CARTESIAN_POINT('Ctrl Pts',(-135.778389473992,-4.53251430027346,
128.890143238351));
#108232=CARTESIAN_POINT('Ctrl Pts',(-135.786148447351,-4.58223337654167,
129.017654053687));
#108233=CARTESIAN_POINT('Ctrl Pts',(-135.793917530715,-4.63201723716028,
129.145331016626));
#108234=CARTESIAN_POINT('Ctrl Pts',(-135.801686614079,-4.67640808468846,
129.274955051779));
#108235=CARTESIAN_POINT('Ctrl Pts',(-135.809455697443,-4.7152781326607,
129.406027612108));
#108236=CARTESIAN_POINT('Ctrl Pts',(-135.812925960045,-4.73264044781501,
129.464574570995));
#108237=CARTESIAN_POINT('Ctrl Pts',(-135.816396222647,-4.74890193738055,
129.523410397543));
#108238=CARTESIAN_POINT('Ctrl Pts',(-135.819866485249,-4.76405452823408,
129.582490119308));
#108239=CARTESIAN_POINT('Origin',(213.235140564004,0.,130.804360617566));
#108240=CARTESIAN_POINT('',(-137.915064401336,-4.76405452823416,129.582490119309));
#108241=CARTESIAN_POINT('',(-137.570140320276,-4.76405452823416,129.582490119309));
#108242=CARTESIAN_POINT('',(213.235140564004,-4.76405452823405,129.582490119308));
#108243=CARTESIAN_POINT('',(-136.235140564053,-4.91824997458325,130.804860629426));
#108244=CARTESIAN_POINT('Ctrl Pts',(-136.235140564053,-4.91824997458325,
130.804860629426));
#108245=CARTESIAN_POINT('Ctrl Pts',(-136.243319774442,-4.91823520989426,
130.950090047185));
#108246=CARTESIAN_POINT('Ctrl Pts',(-136.251498984831,-4.91178351684229,
131.095174708989));
#108247=CARTESIAN_POINT('Ctrl Pts',(-136.259678195219,-4.89895887980969,
131.239544436697));
#108248=CARTESIAN_POINT('Ctrl Pts',(-136.267870559774,-4.88611361763175,
131.384146346152));
#108249=CARTESIAN_POINT('Ctrl Pts',(-136.276062924329,-4.86687497963747,
131.528030706833));
#108250=CARTESIAN_POINT('Ctrl Pts',(-136.284255288883,-4.84135826379696,
131.670636107272));
#108251=CARTESIAN_POINT('Ctrl Pts',(-136.292469269702,-4.81577421989171,
131.81361778441));
#108252=CARTESIAN_POINT('Ctrl Pts',(-136.30068325052,-4.78387902838337,
131.955313435641));
#108253=CARTESIAN_POINT('Ctrl Pts',(-136.308897231338,-4.7458387367286,
132.0951734419));
#108254=CARTESIAN_POINT('Ctrl Pts',(-136.317122921387,-4.70774421770548,
132.235232822028));
#108255=CARTESIAN_POINT('Ctrl Pts',(-136.325348611436,-4.66348720906491,
132.373451028176));
#108256=CARTESIAN_POINT('Ctrl Pts',(-136.333574301485,-4.61328250394212,
132.509296863096));
#108257=CARTESIAN_POINT('Ctrl Pts',(-136.341819169943,-4.56296074525599,
132.645459426079));
#108258=CARTESIAN_POINT('Ctrl Pts',(-136.3500640384,-4.506663686799,132.779238261702));
#108259=CARTESIAN_POINT('Ctrl Pts',(-136.358308906858,-4.44465355757561,
132.910123618388));
#108260=CARTESIAN_POINT('Ctrl Pts',(-136.361957613597,-4.41721142461937,
132.968045983737));
#108261=CARTESIAN_POINT('Ctrl Pts',(-136.365606320337,-4.38865100754711,
133.025402033596));
#108262=CARTESIAN_POINT('Ctrl Pts',(-136.369255027076,-4.35899775916615,
133.082149369423));
#108263=CARTESIAN_POINT('Ctrl Pts',(-136.377029361195,-4.29581530108187,
133.203061457071));
#108264=CARTESIAN_POINT('Ctrl Pts',(-136.384803695314,-4.22749807277276,
133.321534187978));
#108265=CARTESIAN_POINT('Ctrl Pts',(-136.392578029434,-4.15425837290117,
133.437100717477));
#108266=CARTESIAN_POINT('Ctrl Pts',(-136.400342782381,-4.08110893441424,
133.552524821557));
#108267=CARTESIAN_POINT('Ctrl Pts',(-136.408107535328,-4.0030493021788,
133.665049523549));
#108268=CARTESIAN_POINT('Ctrl Pts',(-136.415872288275,-3.92033842409087,
133.774230935121));
#108269=CARTESIAN_POINT('Ctrl Pts',(-136.42362932916,-3.83770969561308,
133.883303906177));
#108270=CARTESIAN_POINT('Ctrl Pts',(-136.431386370045,-3.75043914921582,
133.989039885342));
#108271=CARTESIAN_POINT('Ctrl Pts',(-136.43914341093,-3.65882974291745,
134.091022750314));
#108272=CARTESIAN_POINT('Ctrl Pts',(-136.44689460217,-3.56728941998486,
134.192928709216));
#108273=CARTESIAN_POINT('Ctrl Pts',(-136.45464579341,-3.47141701001369,
134.291086897698));
#108274=CARTESIAN_POINT('Ctrl Pts',(-136.46239698465,-3.37155634026913,
134.385113458365));
#108275=CARTESIAN_POINT('Ctrl Pts',(-136.470144881427,-3.27173811397295,
134.479100055236));
#108276=CARTESIAN_POINT('Ctrl Pts',(-136.477892778205,-3.16793528340938,
134.568958249493));
#108277=CARTESIAN_POINT('Ctrl Pts',(-136.485640674982,-3.06052904374713,
134.654340492173));
#108278=CARTESIAN_POINT('Ctrl Pts',(-136.493386951066,-2.9531452711551,
134.739704874728));
#108279=CARTESIAN_POINT('Ctrl Pts',(-136.50113322715,-2.84215989457701,
134.820594924868));
#108280=CARTESIAN_POINT('Ctrl Pts',(-136.508879503234,-2.72798743940898,
134.896703173233));
#108281=CARTESIAN_POINT('Ctrl Pts',(-136.516625836499,-2.61381414144566,
134.972811983413));
#108282=CARTESIAN_POINT('Ctrl Pts',(-136.524372169765,-2.49645404325894,
135.044138704529));
#108283=CARTESIAN_POINT('Ctrl Pts',(-136.53211850303,-2.37635057640724,
135.110419256334));
#108284=CARTESIAN_POINT('Ctrl Pts',(-136.539866571033,-2.25622021321672,
135.176714651209));
#108285=CARTESIAN_POINT('Ctrl Pts',(-136.547614639036,-2.13334560109405,
135.237961439228));
#108286=CARTESIAN_POINT('Ctrl Pts',(-136.555362707039,-2.0081943198016,
135.29394173794));
#108287=CARTESIAN_POINT('Ctrl Pts',(-136.563119009781,-1.88291002623824,
135.349981533179));
#108288=CARTESIAN_POINT('Ctrl Pts',(-136.570875312523,-1.75534458740969,
135.400743498033));
#108289=CARTESIAN_POINT('Ctrl Pts',(-136.578631615265,-1.6259856102789,
135.446057921103));
#108290=CARTESIAN_POINT('Ctrl Pts',(-136.586392057779,-1.49655759036708,
135.491396529845));
#108291=CARTESIAN_POINT('Ctrl Pts',(-136.594152500293,-1.36533449860536,
135.531281689686));
#108292=CARTESIAN_POINT('Ctrl Pts',(-136.601912942807,-1.23281764971714,
135.565594040225));
#108293=CARTESIAN_POINT('Ctrl Pts',(-136.609685843072,-1.1000880730188,
135.599961471995));
#108294=CARTESIAN_POINT('Ctrl Pts',(-136.617458743338,-0.966060971451945,
135.628738135447));
#108295=CARTESIAN_POINT('Ctrl Pts',(-136.625231643603,-0.831247250350906,
135.651855957562));
#108296=CARTESIAN_POINT('Ctrl Pts',(-136.632721979365,-0.701334347588259,
135.674133388613));
#108297=CARTESIAN_POINT('Ctrl Pts',(-136.640212315127,-0.570691329007694,
135.691156221838));
#108298=CARTESIAN_POINT('Ctrl Pts',(-136.647702650889,-0.439776576001578,
135.702909344046));
#108299=CARTESIAN_POINT('Ctrl Pts',(-136.655476985008,-0.303898150343225,
135.715108089455));
#108300=CARTESIAN_POINT('Ctrl Pts',(-136.663251319127,-0.167296555866609,
135.721668275347));
#108301=CARTESIAN_POINT('Ctrl Pts',(-136.671025653246,-0.0304793148249454,
135.722516173653));
#108302=CARTESIAN_POINT('Ctrl Pts',(-136.678790406194,0.106169311194472,
135.723363027));
#108303=CARTESIAN_POINT('Ctrl Pts',(-136.686555159141,0.243032667781021,
135.718511597631));
#108304=CARTESIAN_POINT('Ctrl Pts',(-136.694319912088,0.379597331447376,
135.707939813262));
#108305=CARTESIAN_POINT('Ctrl Pts',(-136.702076952973,0.516026357164553,
135.697378528937));
#108306=CARTESIAN_POINT('Ctrl Pts',(-136.709833993858,0.652156893063687,
135.681108226106));
#108307=CARTESIAN_POINT('Ctrl Pts',(-136.717591034743,0.787475087458587,
135.659158867662));
#108308=CARTESIAN_POINT('Ctrl Pts',(-136.725342225983,0.922691237350655,
135.637226061399));
#108309=CARTESIAN_POINT('Ctrl Pts',(-136.733093417223,1.05709588070808,
135.609622786164));
#108310=CARTESIAN_POINT('Ctrl Pts',(-136.740844608463,1.19018022039763,
135.576430829274));
#108311=CARTESIAN_POINT('Ctrl Pts',(-136.74859250524,1.32320799569249,135.543252979851));
#108312=CARTESIAN_POINT('Ctrl Pts',(-136.756340402017,1.45491620488167,
135.504491267554));
#108313=CARTESIAN_POINT('Ctrl Pts',(-136.764088298794,1.58480639987929,
135.460278543969));
#108314=CARTESIAN_POINT('Ctrl Pts',(-136.771834574878,1.71466942464822,
135.416075068733));
#108315=CARTESIAN_POINT('Ctrl Pts',(-136.779580850963,1.84271482176478,
135.366422976098));
#108316=CARTESIAN_POINT('Ctrl Pts',(-136.787327127047,1.96845984744815,
135.311504823323));
#108317=CARTESIAN_POINT('Ctrl Pts',(-136.795073460312,2.09420580135291,
135.256586265153));
#108318=CARTESIAN_POINT('Ctrl Pts',(-136.802819793577,2.2176509916552,135.196401725753));
#108319=CARTESIAN_POINT('Ctrl Pts',(-136.810566126843,2.33833355457501,
135.131181534827));
#108320=CARTESIAN_POINT('Ctrl Pts',(-136.818314194846,2.45904314351786,
135.065946738291));
#108321=CARTESIAN_POINT('Ctrl Pts',(-136.826062262849,2.57698853010902,
134.995674232083));
#108322=CARTESIAN_POINT('Ctrl Pts',(-136.833810330851,2.6917336653876,134.920639633512));
#108323=CARTESIAN_POINT('Ctrl Pts',(-136.841566633593,2.8066007531616,134.845525287277));
#108324=CARTESIAN_POINT('Ctrl Pts',(-136.849322936335,2.91826046749335,
134.765638952683));
#108325=CARTESIAN_POINT('Ctrl Pts',(-136.857079239077,3.02630646190114,
134.681299134122));
#108326=CARTESIAN_POINT('Ctrl Pts',(-136.864839681591,3.13441012370934,
134.59691430086));
#108327=CARTESIAN_POINT('Ctrl Pts',(-136.872600124105,3.23889592468964,
134.508071500474));
#108328=CARTESIAN_POINT('Ctrl Pts',(-136.88036056662,3.33939247070211,134.415127986024));
#108329=CARTESIAN_POINT('Ctrl Pts',(-136.888133466885,3.4400503426919,134.322035270393));
#108330=CARTESIAN_POINT('Ctrl Pts',(-136.895906367151,3.53670588684236,
134.224828963505));
#108331=CARTESIAN_POINT('Ctrl Pts',(-136.903679267416,3.62902567458206,
134.123902109357));
#108332=CARTESIAN_POINT('Ctrl Pts',(-136.911169603178,3.71798940549767,
134.026644200578));
#108333=CARTESIAN_POINT('Ctrl Pts',(-136.91865993894,3.80292693987788,133.925931786206));
#108334=CARTESIAN_POINT('Ctrl Pts',(-136.926150274702,3.88357779622821,
133.822142346443));
#108335=CARTESIAN_POINT('Ctrl Pts',(-136.933924608821,3.96728655431049,
133.714417698524));
#108336=CARTESIAN_POINT('Ctrl Pts',(-136.94169894294,4.04664232298926,133.603036849049));
#108337=CARTESIAN_POINT('Ctrl Pts',(-136.949473277059,4.12130874457731,
133.488386939041));
#108338=CARTESIAN_POINT('Ctrl Pts',(-136.957238030006,4.19588314647388,
133.3738783248));
#108339=CARTESIAN_POINT('Ctrl Pts',(-136.965002782953,4.26577948885518,
133.256108990656));
#108340=CARTESIAN_POINT('Ctrl Pts',(-136.972767535901,4.33070168374531,
133.135498963719));
#108341=CARTESIAN_POINT('Ctrl Pts',(-136.980524576786,4.39555939699623,
133.015008728361));
#108342=CARTESIAN_POINT('Ctrl Pts',(-136.988281617671,4.45545261025234,
132.891683756988));
#108343=CARTESIAN_POINT('Ctrl Pts',(-136.996038658556,4.51012878275617,
132.765972563251));
#108344=CARTESIAN_POINT('Ctrl Pts',(-137.003789849796,4.56476372353308,
132.640356169303));
#108345=CARTESIAN_POINT('Ctrl Pts',(-137.011541041036,4.61418929906316,
132.512357491797));
#108346=CARTESIAN_POINT('Ctrl Pts',(-137.019292232276,4.65819930205446,
132.382448804214));
#108347=CARTESIAN_POINT('Ctrl Pts',(-137.027040129053,4.70219059962042,
132.252595331289));
#108348=CARTESIAN_POINT('Ctrl Pts',(-137.03478802583,4.7407707774944,132.120833832424));
#108349=CARTESIAN_POINT('Ctrl Pts',(-137.042535922607,4.7737821841137,131.987655475638));
#108350=CARTESIAN_POINT('Ctrl Pts',(-137.050282198691,4.80678668545838,
131.854504976892));
#108351=CARTESIAN_POINT('Ctrl Pts',(-137.058028474775,4.83422463852874,
131.719938588975));
#108352=CARTESIAN_POINT('Ctrl Pts',(-137.065774750859,4.85598869911049,
131.584461134558));
#108353=CARTESIAN_POINT('Ctrl Pts',(-137.073521084125,4.87775292034962,
131.448982680077));
#108354=CARTESIAN_POINT('Ctrl Pts',(-137.08126741739,4.89384310351253,131.312593531691));
#108355=CARTESIAN_POINT('Ctrl Pts',(-137.089013750656,4.90420338284815,
131.175806767312));
#108356=CARTESIAN_POINT('Ctrl Pts',(-137.096761818659,4.91456598229647,
131.038989370485));
#108357=CARTESIAN_POINT('Ctrl Pts',(-137.104509886662,4.91919609503168,
130.901774570252));
#108358=CARTESIAN_POINT('Ctrl Pts',(-137.112257954664,4.91808991058727,
130.764678204841));
#108359=CARTESIAN_POINT('Ctrl Pts',(-137.120014257406,4.91698255047687,
130.627436131782));
#108360=CARTESIAN_POINT('Ctrl Pts',(-137.127770560148,4.9101267177213,130.490313136567));
#108361=CARTESIAN_POINT('Ctrl Pts',(-137.13552686289,4.89757073888565,130.353823249403));
#108362=CARTESIAN_POINT('Ctrl Pts',(-137.143287305404,4.88500805854603,
130.217260513477));
#108363=CARTESIAN_POINT('Ctrl Pts',(-137.151047747918,4.86673922205921,
130.081331946206));
#108364=CARTESIAN_POINT('Ctrl Pts',(-137.158808190433,4.84286404893974,
129.946543116003));
#108365=CARTESIAN_POINT('Ctrl Pts',(-137.166581090698,4.81895054927284,
129.811537910805));
#108366=CARTESIAN_POINT('Ctrl Pts',(-137.174353990963,4.78941281281852,
129.677676480815));
#108367=CARTESIAN_POINT('Ctrl Pts',(-137.182126891229,4.75440129233651,
129.545451798815));
#108368=CARTESIAN_POINT('Ctrl Pts',(-137.189617226991,4.72066252881273,
129.41803381706));
#108369=CARTESIAN_POINT('Ctrl Pts',(-137.197107562753,4.68184113432559,
129.292135943824));
#108370=CARTESIAN_POINT('Ctrl Pts',(-137.204597898515,4.63811389704672,
129.168181366835));
#108371=CARTESIAN_POINT('Ctrl Pts',(-137.212372232634,4.59272872827575,
129.039527014384));
#108372=CARTESIAN_POINT('Ctrl Pts',(-137.220146566753,4.54191459648595,
128.912558688953));
#108373=CARTESIAN_POINT('Ctrl Pts',(-137.227920900872,4.48581540483866,
128.787768636968));
#108374=CARTESIAN_POINT('Ctrl Pts',(-137.235685653819,4.42978535043149,
128.66313237757));
#108375=CARTESIAN_POINT('Ctrl Pts',(-137.243450406766,4.36848335458528,
128.540669403377));
#108376=CARTESIAN_POINT('Ctrl Pts',(-137.251215159714,4.30210275522069,
128.4208558565));
#108377=CARTESIAN_POINT('Ctrl Pts',(-137.258972200599,4.23578808600318,
128.301161310128));
#108378=CARTESIAN_POINT('Ctrl Pts',(-137.266729241484,4.16440503958002,
128.184111294144));
#108379=CARTESIAN_POINT('Ctrl Pts',(-137.274486282369,4.08819445874128,
128.070160710826));
#108380=CARTESIAN_POINT('Ctrl Pts',(-137.282237473609,4.01204134889428,
127.956296058529));
#108381=CARTESIAN_POINT('Ctrl Pts',(-137.289988664849,3.93106816725847,
127.845526510297));
#108382=CARTESIAN_POINT('Ctrl Pts',(-137.297739856089,3.84556079081068,
127.738280829518));
#108383=CARTESIAN_POINT('Ctrl Pts',(-137.305487752866,3.76008975727898,
127.631080731014));
#108384=CARTESIAN_POINT('Ctrl Pts',(-137.313235649643,3.67008860511802,
127.527401826131));
#108385=CARTESIAN_POINT('Ctrl Pts',(-137.32098354642,3.57588535337274,127.427642239905));
#108386=CARTESIAN_POINT('Ctrl Pts',(-137.328729822504,3.48170180691693,
127.327903521234));
#108387=CARTESIAN_POINT('Ctrl Pts',(-137.336476098589,3.38331817748795,
127.232082774597));
#108388=CARTESIAN_POINT('Ctrl Pts',(-137.344222374673,3.28110116452691,
127.140543180706));
#108389=CARTESIAN_POINT('Ctrl Pts',(-137.351968707938,3.17888339702297,
127.04900291109));
#108390=CARTESIAN_POINT('Ctrl Pts',(-137.359715041203,3.07283248076893,
126.961744118105));
#108391=CARTESIAN_POINT('Ctrl Pts',(-137.367461374469,2.96334988593871,
126.879091134332));
#108392=CARTESIAN_POINT('Ctrl Pts',(-137.375209442472,2.85384277324062,
126.796419640997));
#108393=CARTESIAN_POINT('Ctrl Pts',(-137.382957510475,2.74090276470982,
126.718356244837));
#108394=CARTESIAN_POINT('Ctrl Pts',(-137.390705578478,2.62496179000672,
126.64518297487));
#108395=CARTESIAN_POINT('Ctrl Pts',(-137.398461881219,2.50889759185583,
126.57193193548));
#108396=CARTESIAN_POINT('Ctrl Pts',(-137.406218183961,2.38982638738926,
126.503581613416));
#108397=CARTESIAN_POINT('Ctrl Pts',(-137.413974486703,2.26820676646648,
126.440369196051));
#108398=CARTESIAN_POINT('Ctrl Pts',(-137.421734929217,2.14652223349011,
126.377123040316));
#108399=CARTESIAN_POINT('Ctrl Pts',(-137.429495371731,2.02228692778529,
126.319020419003));
#108400=CARTESIAN_POINT('Ctrl Pts',(-137.437255814246,1.89598015326364,
126.266250623204));
#108401=CARTESIAN_POINT('Ctrl Pts',(-137.445028714511,1.76947061989453,
126.213396116644));
#108402=CARTESIAN_POINT('Ctrl Pts',(-137.452801614777,1.64088333963832,
126.165891678218));
#108403=CARTESIAN_POINT('Ctrl Pts',(-137.460574515042,1.51071438784972,
126.123877191589));
#108404=CARTESIAN_POINT('Ctrl Pts',(-137.468064850804,1.3852774053348,126.083390037377));
#108405=CARTESIAN_POINT('Ctrl Pts',(-137.475555186566,1.25837204698359,
126.048000700328));
#108406=CARTESIAN_POINT('Ctrl Pts',(-137.483045522328,1.13044991094067,
126.017789186849));
#108407=CARTESIAN_POINT('Ctrl Pts',(-137.490819856447,0.997677568228408,
125.986432194654));
#108408=CARTESIAN_POINT('Ctrl Pts',(-137.498594190566,0.863389240676738,
125.96055408159));
#108409=CARTESIAN_POINT('Ctrl Pts',(-137.506368524685,0.728076852320345,
125.940299849071));
#108410=CARTESIAN_POINT('Ctrl Pts',(-137.514133277632,0.592931224389387,
125.920070578083));
#108411=CARTESIAN_POINT('Ctrl Pts',(-137.521898030579,0.456764429729424,
125.905451454475));
#108412=CARTESIAN_POINT('Ctrl Pts',(-137.529662783526,0.320081564053693,
125.896537184021));
#108413=CARTESIAN_POINT('Ctrl Pts',(-137.537419824411,0.183534453726671,
125.887631767347));
#108414=CARTESIAN_POINT('Ctrl Pts',(-137.545176865296,0.0464726800311459,
125.884419953231));
#108415=CARTESIAN_POINT('Ctrl Pts',(-137.552933906181,-0.0905908534535143,
125.886944999605));
#108416=CARTESIAN_POINT('Ctrl Pts',(-137.560685097422,-0.227551026261189,
125.889468141822));
#108417=CARTESIAN_POINT('Ctrl Pts',(-137.568436288662,-0.364512566899337,
125.897719526295));
#108418=CARTESIAN_POINT('Ctrl Pts',(-137.576187479902,-0.500960221098191,
125.911690393713));
#108419=CARTESIAN_POINT('Ctrl Pts',(-137.583935376679,-0.637349881404335,
125.925655323139));
#108420=CARTESIAN_POINT('Ctrl Pts',(-137.591683273456,-0.773225701565315,
125.94533486083));
#108421=CARTESIAN_POINT('Ctrl Pts',(-137.599431170233,-0.908075425406258,
125.97066823138));
#108422=CARTESIAN_POINT('Ctrl Pts',(-137.607177446317,-1.04289694159163,
125.995996302735));
#108423=CARTESIAN_POINT('Ctrl Pts',(-137.614923722401,-1.17669240438214,
126.026975782433));
#108424=CARTESIAN_POINT('Ctrl Pts',(-137.622669998485,-1.30895804955339,
126.063494463896));
#108425=CARTESIAN_POINT('Ctrl Pts',(-137.630416331751,-1.44122467107977,
126.100013414932));
#108426=CARTESIAN_POINT('Ctrl Pts',(-137.638162665016,-1.57196107558851,
126.142071545272));
#108427=CARTESIAN_POINT('Ctrl Pts',(-137.645908998281,-1.70067738845764,
126.18950639637));
#108428=CARTESIAN_POINT('Ctrl Pts',(-137.653657066284,-1.82942252645239,
126.236951870174));
#108429=CARTESIAN_POINT('Ctrl Pts',(-137.661405134287,-1.9561463058355,
126.28977632555));
#108430=CARTESIAN_POINT('Ctrl Pts',(-137.66915320229,-2.08037797907659,
126.347768811413));
#108431=CARTESIAN_POINT('Ctrl Pts',(-137.676909505032,-2.20474168721854,
126.40582293238));
#108432=CARTESIAN_POINT('Ctrl Pts',(-137.684665807774,-2.32660764344301,
126.469055890344));
#108433=CARTESIAN_POINT('Ctrl Pts',(-137.692422110516,-2.44552841627364,
126.537210066238));
#108434=CARTESIAN_POINT('Ctrl Pts',(-137.70018255303,-2.56451266070136,
126.605400618068));
#108435=CARTESIAN_POINT('Ctrl Pts',(-137.707942995544,-2.68054825891351,
126.678517413229));
#108436=CARTESIAN_POINT('Ctrl Pts',(-137.715703438058,-2.79321687948089,
126.756259516224));
#108437=CARTESIAN_POINT('Ctrl Pts',(-137.723476338324,-2.90606636572026,
126.834126417745));
#108438=CARTESIAN_POINT('Ctrl Pts',(-137.731249238589,-3.01553776106076,
126.916633229076));
#108439=CARTESIAN_POINT('Ctrl Pts',(-137.739022138855,-3.12124523656904,
127.003438198508));
#108440=CARTESIAN_POINT('Ctrl Pts',(-137.746512474617,-3.22310997908124,
127.087087588653));
#108441=CARTESIAN_POINT('Ctrl Pts',(-137.754002810378,-3.32147947664331,
127.174727859672));
#108442=CARTESIAN_POINT('Ctrl Pts',(-137.761493146141,-3.41604231777075,
127.266022314676));
#108443=CARTESIAN_POINT('Ctrl Pts',(-137.769153108236,-3.5127466313919,
127.359384226218));
#108444=CARTESIAN_POINT('Ctrl Pts',(-137.776813070331,-3.60579530623451,
127.456882415243));
#108445=CARTESIAN_POINT('Ctrl Pts',(-137.784473032426,-3.69480578996644,
127.558194688823));
#108446=CARTESIAN_POINT('Ctrl Pts',(-137.792124079689,-3.78371268133452,
127.659389052946));
#108447=CARTESIAN_POINT('Ctrl Pts',(-137.799775126951,-3.86859046105256,
127.764388377782));
#108448=CARTESIAN_POINT('Ctrl Pts',(-137.807426174214,-3.94909117130883,
127.872831667821));
#108449=CARTESIAN_POINT('Ctrl Pts',(-137.815070089553,-4.02951684283165,
127.981173872453));
#108450=CARTESIAN_POINT('Ctrl Pts',(-137.822714004892,-4.10557331916048,
128.092953337223));
#108451=CARTESIAN_POINT('Ctrl Pts',(-137.830357920231,-4.17695130828101,
128.207774237191));
#108452=CARTESIAN_POINT('Ctrl Pts',(-137.837996312052,-4.2482777194334,
128.322512167201));
#108453=CARTESIAN_POINT('Ctrl Pts',(-137.845634703873,-4.31493215704285,
128.440286818867));
#108454=CARTESIAN_POINT('Ctrl Pts',(-137.853273095694,-4.37664761343337,
128.560671973764));
#108455=CARTESIAN_POINT('Ctrl Pts',(-137.860908196125,-4.43833647657792,
128.681005254588));
#108456=CARTESIAN_POINT('Ctrl Pts',(-137.868543296556,-4.49509040858418,
128.803946442666));
#108457=CARTESIAN_POINT('Ctrl Pts',(-137.876178396987,-4.54668772496982,
128.929043632598));
#108458=CARTESIAN_POINT('Ctrl Pts',(-137.883813309681,-4.59828377264686,
129.054137746559));
#108459=CARTESIAN_POINT('Ctrl Pts',(-137.891448222375,-4.64472329467837,
129.181387387688));
#108460=CARTESIAN_POINT('Ctrl Pts',(-137.899083135069,-4.68583238345119,
129.310319809321));
#108461=CARTESIAN_POINT('Ctrl Pts',(-137.904410223825,-4.71451532631305,
129.400279509065));
#108462=CARTESIAN_POINT('Ctrl Pts',(-137.909737312581,-4.74060428684821,
129.491057984052));
#108463=CARTESIAN_POINT('Ctrl Pts',(-137.915064401336,-4.76405452823416,
129.582490119309));
#108464=CARTESIAN_POINT('Ctrl Pts',(-136.165410316754,-4.76405452823394,
129.582490119308));
#108465=CARTESIAN_POINT('Ctrl Pts',(-136.173480782487,-4.79948346874215,
129.72062702064));
#108466=CARTESIAN_POINT('Ctrl Pts',(-136.181551248219,-4.82893486395653,
129.860441210009));
#108467=CARTESIAN_POINT('Ctrl Pts',(-136.189621713952,-4.8522606023129,
130.001397287306));
#108468=CARTESIAN_POINT('Ctrl Pts',(-136.197679934484,-4.8755509488655,
130.142139493995));
#108469=CARTESIAN_POINT('Ctrl Pts',(-136.205738155016,-4.89273411466211,
130.284019797074));
#108470=CARTESIAN_POINT('Ctrl Pts',(-136.213796375548,-4.90371264983407,
130.42649118197));
#108471=CARTESIAN_POINT('Ctrl Pts',(-136.220911105036,-4.91340577098946,
130.552281405652));
#108472=CARTESIAN_POINT('Ctrl Pts',(-136.228025834523,-4.91826281770671,
130.678532050252));
#108473=CARTESIAN_POINT('Ctrl Pts',(-136.23514056401,-4.91824997458333,
130.804860628664));
#108474=CARTESIAN_POINT('',(-135.889859436035,-4.91824798693904,130.799910733292));
#108475=CARTESIAN_POINT('Ctrl Pts',(-135.819866485249,-4.76405452823408,
129.582490119308));
#108476=CARTESIAN_POINT('Ctrl Pts',(-135.823893915369,-4.78163994115519,
129.651055377392));
#108477=CARTESIAN_POINT('Ctrl Pts',(-135.827921345489,-4.79773171155441,
129.719949130419));
#108478=CARTESIAN_POINT('Ctrl Pts',(-135.83194877561,-4.81232069727367,
129.789100764577));
#108479=CARTESIAN_POINT('Ctrl Pts',(-135.842894248747,-4.85196964126975,
129.977036329305));
#108480=CARTESIAN_POINT('Ctrl Pts',(-135.853839721884,-4.88062061044695,
130.167366481324));
#108481=CARTESIAN_POINT('Ctrl Pts',(-135.86478519502,-4.8980463227066,130.359023348611));
#108482=CARTESIAN_POINT('Ctrl Pts',(-135.873143275345,-4.91135278291635,
130.505374581804));
#108483=CARTESIAN_POINT('Ctrl Pts',(-135.881501355669,-4.91811461337833,
130.652499228452));
#108484=CARTESIAN_POINT('Ctrl Pts',(-135.889859435993,-4.91824798693837,
130.799910732551));
#108485=CARTESIAN_POINT('Ctrl Pts',(-135.889859436035,-4.91824798693904,
130.799910733292));
#108486=CARTESIAN_POINT('Ctrl Pts',(-135.897508745035,-4.9183700503033,
130.934821634027));
#108487=CARTESIAN_POINT('Ctrl Pts',(-135.905158054034,-4.9129368955204,
131.069908050386));
#108488=CARTESIAN_POINT('Ctrl Pts',(-135.912807363034,-4.90193198336201,
131.204667865805));
#108489=CARTESIAN_POINT('Ctrl Pts',(-135.92045048546,-4.89093597170746,
131.33931869078));
#108490=CARTESIAN_POINT('Ctrl Pts',(-135.928093607885,-4.87437719946991,
131.473643040524));
#108491=CARTESIAN_POINT('Ctrl Pts',(-135.935736730311,-4.85229119251697,
131.60713907114));
#108492=CARTESIAN_POINT('Ctrl Pts',(-135.943376195721,-4.83021575308755,
131.740571227717));
#108493=CARTESIAN_POINT('Ctrl Pts',(-135.95101566113,-4.80261840252355,
131.873175456455));
#108494=CARTESIAN_POINT('Ctrl Pts',(-135.95865512654,-4.76958644040095,
132.004455717982));
#108495=CARTESIAN_POINT('Ctrl Pts',(-135.966292838885,-4.73656205828356,
132.135705853988));
#108496=CARTESIAN_POINT('Ctrl Pts',(-135.973930551229,-4.69810564212933,
132.265632236171));
#108497=CARTESIAN_POINT('Ctrl Pts',(-135.981568263573,-4.65435535336774,
132.393750219607));
#108498=CARTESIAN_POINT('Ctrl Pts',(-135.98920598653,-4.61060500381579,
132.521868381062));
#108499=CARTESIAN_POINT('Ctrl Pts',(-135.996843709487,-4.56156089749562,
132.648177757406));
#108500=CARTESIAN_POINT('Ctrl Pts',(-136.004481432444,-4.50741051960844,
132.772210578875));
#108501=CARTESIAN_POINT('Ctrl Pts',(-136.012120929491,-4.45324756367058,
132.89627221069));
#108502=CARTESIAN_POINT('Ctrl Pts',(-136.019760426539,-4.39397613931752,
133.018055867051));
#108503=CARTESIAN_POINT('Ctrl Pts',(-136.027399923586,-4.32983091234054,
133.13711592686));
#108504=CARTESIAN_POINT('Ctrl Pts',(-136.035047345095,-4.26561914742068,
133.256299487853));
#108505=CARTESIAN_POINT('Ctrl Pts',(-136.042694766605,-4.19652367769785,
133.372753456631));
#108506=CARTESIAN_POINT('Ctrl Pts',(-136.050342188114,-4.1228241219153,
133.486058647221));
#108507=CARTESIAN_POINT('Ctrl Pts',(-136.057993947771,-4.04908275863514,
133.59942811237));
#108508=CARTESIAN_POINT('Ctrl Pts',(-136.065645707428,-3.97073234307121,
133.7096449157));
#108509=CARTESIAN_POINT('Ctrl Pts',(-136.073297467085,-3.88809365920726,
133.816321898813));
#108510=CARTESIAN_POINT('Ctrl Pts',(-136.080960620258,-3.80533192585335,
133.923157724586));
#108511=CARTESIAN_POINT('Ctrl Pts',(-136.08862377343,-3.71826943466092,
134.026442899304));
#108512=CARTESIAN_POINT('Ctrl Pts',(-136.096286926603,-3.62726508325272,
134.125825818094));
#108513=CARTESIAN_POINT('Ctrl Pts',(-136.100990084209,-3.57141238163821,
134.186820753202));
#108514=CARTESIAN_POINT('Ctrl Pts',(-136.105693241816,-3.51407559081868,
134.246346564863));
#108515=CARTESIAN_POINT('Ctrl Pts',(-136.110396399423,-3.45534375231488,
134.304329562548));
#108516=CARTESIAN_POINT('Ctrl Pts',(-136.118170733542,-3.35825984100745,
134.400175637659));
#108517=CARTESIAN_POINT('Ctrl Pts',(-136.125945067661,-3.2570311930191,
134.492131020747));
#108518=CARTESIAN_POINT('Ctrl Pts',(-136.13371940178,-3.15200251286159,
134.579815983666));
#108519=CARTESIAN_POINT('Ctrl Pts',(-136.141484154727,-3.04710327116569,
134.667392882705));
#108520=CARTESIAN_POINT('Ctrl Pts',(-136.149248907674,-2.938413612713,134.750709585043));
#108521=CARTESIAN_POINT('Ctrl Pts',(-136.157013660621,-2.82631565412691,
134.829422466251));
#108522=CARTESIAN_POINT('Ctrl Pts',(-136.164770701506,-2.71432903281359,
134.908057168715));
#108523=CARTESIAN_POINT('Ctrl Pts',(-136.172527742391,-2.59894116590414,
134.982096926471));
#108524=CARTESIAN_POINT('Ctrl Pts',(-136.180284783276,-2.48056760048377,
135.051237992995));
#108525=CARTESIAN_POINT('Ctrl Pts',(-136.188035974517,-2.36228330148941,
135.120326919704));
#108526=CARTESIAN_POINT('Ctrl Pts',(-136.195787165757,-2.24101812176485,
135.184524311755));
#108527=CARTESIAN_POINT('Ctrl Pts',(-136.203538356997,-2.1172166743084,
135.243569625546));
#108528=CARTESIAN_POINT('Ctrl Pts',(-136.211286253774,-1.99346784577013,
135.302589843503));
#108529=CARTESIAN_POINT('Ctrl Pts',(-136.219034150551,-1.86718524566903,
135.356462170535));
#108530=CARTESIAN_POINT('Ctrl Pts',(-136.226782047328,-1.73883798414876,
135.404972047298));
#108531=CARTESIAN_POINT('Ctrl Pts',(-136.234528323412,-1.61051757010912,
135.453471776841));
#108532=CARTESIAN_POINT('Ctrl Pts',(-136.242274599496,-1.48013371917215,
135.496611149119));
#108533=CARTESIAN_POINT('Ctrl Pts',(-136.25002087558,-1.3481750422978,135.534223947286));
#108534=CARTESIAN_POINT('Ctrl Pts',(-136.257767208846,-1.2162153913343,
135.571837023101));
#108535=CARTESIAN_POINT('Ctrl Pts',(-136.265513542111,-1.08268126722637,
135.603923336231));
#108536=CARTESIAN_POINT('Ctrl Pts',(-136.273259875376,-0.948075558447773,
135.630366812959));
#108537=CARTESIAN_POINT('Ctrl Pts',(-136.281007943379,-0.813439705654168,
135.656816211521));
#108538=CARTESIAN_POINT('Ctrl Pts',(-136.288756011382,-0.677732174228575,
135.677620183767));
#108539=CARTESIAN_POINT('Ctrl Pts',(-136.296504079385,-0.541464741826425,
135.692714020897));
#108540=CARTESIAN_POINT('Ctrl Pts',(-136.304260382127,-0.405052482775329,
135.707823899937));
#108541=CARTESIAN_POINT('Ctrl Pts',(-136.312016684869,-0.268079523240667,
135.71721147767));
#108542=CARTESIAN_POINT('Ctrl Pts',(-136.319772987611,-0.131062003350017,
135.720864030946));
#108543=CARTESIAN_POINT('Ctrl Pts',(-136.327533430125,0.00602864691651589,
135.7245185337));
#108544=CARTESIAN_POINT('Ctrl Pts',(-136.335293872639,0.143163514200399,
135.722431918731));
#108545=CARTESIAN_POINT('Ctrl Pts',(-136.343054315153,0.279828779171258,
135.714643594834));
#108546=CARTESIAN_POINT('Ctrl Pts',(-136.350827215419,0.416713431358021,
135.706842768428));
#108547=CARTESIAN_POINT('Ctrl Pts',(-136.358600115684,0.553126585521877,
135.69332198129));
#108548=CARTESIAN_POINT('Ctrl Pts',(-136.36637301595,0.68856094957552,135.674172408716));
#108549=CARTESIAN_POINT('Ctrl Pts',(-136.373863351712,0.819071933359431,
135.655718971339));
#108550=CARTESIAN_POINT('Ctrl Pts',(-136.381353687474,0.948673751509082,
135.632038939921));
#108551=CARTESIAN_POINT('Ctrl Pts',(-136.388844023236,1.07692529810143,
135.603257883065));
#108552=CARTESIAN_POINT('Ctrl Pts',(-136.396618357355,1.21003954106235,
135.57338558369));
#108553=CARTESIAN_POINT('Ctrl Pts',(-136.404392691474,1.34212076605131,
135.537923185887));
#108554=CARTESIAN_POINT('Ctrl Pts',(-136.412167025593,1.47266317581575,
135.496955446986));
#108555=CARTESIAN_POINT('Ctrl Pts',(-136.41993177854,1.60304470372636,135.456038197161));
#108556=CARTESIAN_POINT('Ctrl Pts',(-136.427696531487,1.73189082034094,
135.409629221991));
#108557=CARTESIAN_POINT('Ctrl Pts',(-136.435461284435,1.8587058813254,135.357864269615));
#108558=CARTESIAN_POINT('Ctrl Pts',(-136.44321832532,1.98539498780385,135.30615073092));
#108559=CARTESIAN_POINT('Ctrl Pts',(-136.450975366204,2.11005669348842,
135.249091948123));
#108560=CARTESIAN_POINT('Ctrl Pts',(-136.458732407089,2.23221083447676,
135.186873350342));
#108561=CARTESIAN_POINT('Ctrl Pts',(-136.46648359833,2.35427285807766,135.124701672089));
#108562=CARTESIAN_POINT('Ctrl Pts',(-136.47423478957,2.47383073388311,135.057378100491));
#108563=CARTESIAN_POINT('Ctrl Pts',(-136.48198598081,2.59042493499383,134.985135870873));
#108564=CARTESIAN_POINT('Ctrl Pts',(-136.489733877587,2.70696958045836,
134.912924346129));
#108565=CARTESIAN_POINT('Ctrl Pts',(-136.497481774364,2.82055272491218,
134.83579852682));
#108566=CARTESIAN_POINT('Ctrl Pts',(-136.505229671141,2.93074028801205,
134.75403711403));
#108567=CARTESIAN_POINT('Ctrl Pts',(-136.512975947225,3.04090480224909,
134.672292803965));
#108568=CARTESIAN_POINT('Ctrl Pts',(-136.520722223309,3.14767483415114,
134.585915061963));
#108569=CARTESIAN_POINT('Ctrl Pts',(-136.528468499394,3.2506464346191,134.495225125997));
#108570=CARTESIAN_POINT('Ctrl Pts',(-136.536214832659,3.35361879520044,
134.404534520579));
#108571=CARTESIAN_POINT('Ctrl Pts',(-136.543961165924,3.45279237500059,
134.309531916081));
#108572=CARTESIAN_POINT('Ctrl Pts',(-136.55170749919,3.54779769441297,134.210577666143));
#108573=CARTESIAN_POINT('Ctrl Pts',(-136.559455567193,3.64282428960779,
134.111601256087));
#108574=CARTESIAN_POINT('Ctrl Pts',(-136.567203635196,3.7336804962337,134.008671721625));
#108575=CARTESIAN_POINT('Ctrl Pts',(-136.574951703199,3.8200352446217,133.902184659107));
#108576=CARTESIAN_POINT('Ctrl Pts',(-136.582708005941,3.9064817718638,133.795584420871));
#108577=CARTESIAN_POINT('Ctrl Pts',(-136.590464308682,3.9884170372592,133.685419405807));
#108578=CARTESIAN_POINT('Ctrl Pts',(-136.598220611424,4.06555135011611,
133.57211698005));
#108579=CARTESIAN_POINT('Ctrl Pts',(-136.605981053939,4.14272683187848,
133.458754081376));
#108580=CARTESIAN_POINT('Ctrl Pts',(-136.613741496453,4.21509604908112,
133.342250767308));
#108581=CARTESIAN_POINT('Ctrl Pts',(-136.621501938967,4.28241442556141,
133.22306063002));
#108582=CARTESIAN_POINT('Ctrl Pts',(-136.629274839232,4.34984086747569,
133.103679158142));
#108583=CARTESIAN_POINT('Ctrl Pts',(-136.637047739498,4.41220008822957,
132.98160259241));
#108584=CARTESIAN_POINT('Ctrl Pts',(-136.644820639763,4.46929459241776,
132.8573070145));
#108585=CARTESIAN_POINT('Ctrl Pts',(-136.652310975525,4.52431356756571,
132.73752989393));
#108586=CARTESIAN_POINT('Ctrl Pts',(-136.659801311287,4.57444383488916,
132.615692578412));
#108587=CARTESIAN_POINT('Ctrl Pts',(-136.667291647049,4.61955261028419,
132.492234055747));
#108588=CARTESIAN_POINT('Ctrl Pts',(-136.675065981168,4.66637169860943,
132.364094565669));
#108589=CARTESIAN_POINT('Ctrl Pts',(-136.682840315287,4.70792930736034,
132.233802598122));
#108590=CARTESIAN_POINT('Ctrl Pts',(-136.690614649406,4.74402334950908,
132.101829508065));
#108591=CARTESIAN_POINT('Ctrl Pts',(-136.698379402353,4.78007290897649,
131.970019063048));
#108592=CARTESIAN_POINT('Ctrl Pts',(-136.706144155301,4.81067219706714,
131.836531991347));
#108593=CARTESIAN_POINT('Ctrl Pts',(-136.713908908248,4.83566751466568,
131.701858667763));
#108594=CARTESIAN_POINT('Ctrl Pts',(-136.721665949133,4.86063800656254,
131.567319103622));
#108595=CARTESIAN_POINT('Ctrl Pts',(-136.729422990018,4.88001553356104,
131.431596014186));
#108596=CARTESIAN_POINT('Ctrl Pts',(-136.737180030903,4.89369656211065,
131.295193603913));
#108597=CARTESIAN_POINT('Ctrl Pts',(-136.744931222143,4.90736727369014,
131.158894055759));
#108598=CARTESIAN_POINT('Ctrl Pts',(-136.752682413383,4.91534999843821,
131.021916593871));
#108599=CARTESIAN_POINT('Ctrl Pts',(-136.760433604623,4.91759257832591,
130.884773900635));
#108600=CARTESIAN_POINT('Ctrl Pts',(-136.7681815014,4.91983420505734,130.747689496701));
#108601=CARTESIAN_POINT('Ctrl Pts',(-136.775929398177,4.916340532956,130.610440391191));
#108602=CARTESIAN_POINT('Ctrl Pts',(-136.783677294954,4.90711141010853,
130.473542432935));
#108603=CARTESIAN_POINT('Ctrl Pts',(-136.791423571038,4.89788421779461,
130.33667311078));
#108604=CARTESIAN_POINT('Ctrl Pts',(-136.799169847122,4.88292398734956,
130.200155179611));
#108605=CARTESIAN_POINT('Ctrl Pts',(-136.806916123206,4.86228264102318,
130.064502130215));
#108606=CARTESIAN_POINT('Ctrl Pts',(-136.814662456472,4.8416411423271,129.92884807946));
#108607=CARTESIAN_POINT('Ctrl Pts',(-136.822408789737,4.81531850288144,
129.794059309735));
#108608=CARTESIAN_POINT('Ctrl Pts',(-136.830155123002,4.78341818565514,
129.66064145464));
#108609=CARTESIAN_POINT('Ctrl Pts',(-136.837903191005,4.75151072457403,
129.527193721542));
#108610=CARTESIAN_POINT('Ctrl Pts',(-136.845651259008,4.71402319108318,
129.395117894156));
#108611=CARTESIAN_POINT('Ctrl Pts',(-136.853399327011,4.6711094603522,129.264906340262));
#108612=CARTESIAN_POINT('Ctrl Pts',(-136.861155629753,4.62815012039746,
129.134556395979));
#108613=CARTESIAN_POINT('Ctrl Pts',(-136.868911932495,4.57975318551552,
129.006075055103));
#108614=CARTESIAN_POINT('Ctrl Pts',(-136.876668235237,4.52612162604393,
128.879937044452));
#108615=CARTESIAN_POINT('Ctrl Pts',(-136.884428677751,4.4724614417941,128.753731710146));
#108616=CARTESIAN_POINT('Ctrl Pts',(-136.892189120265,4.41356123373883,
128.629872551106));
#108617=CARTESIAN_POINT('Ctrl Pts',(-136.899949562779,4.34967042242846,
128.508810513832));
#108618=CARTESIAN_POINT('Ctrl Pts',(-136.907722463045,4.28567704791581,
128.387554137029));
#108619=CARTESIAN_POINT('Ctrl Pts',(-136.91549536331,4.21667725780417,128.26910419284));
#108620=CARTESIAN_POINT('Ctrl Pts',(-136.923268263576,4.14296484199955,
128.153884173518));
#108621=CARTESIAN_POINT('Ctrl Pts',(-136.930758599338,4.07193205817919,
128.042852692118));
#108622=CARTESIAN_POINT('Ctrl Pts',(-136.9382489351,3.99652350800793,127.934820633374));
#108623=CARTESIAN_POINT('Ctrl Pts',(-136.945739270862,3.91703675130559,
127.830136995943));
#108624=CARTESIAN_POINT('Ctrl Pts',(-136.953513604981,3.83453623006422,
127.721484246582));
#108625=CARTESIAN_POINT('Ctrl Pts',(-136.9612879391,3.74738081033742,127.61609466235));
#108626=CARTESIAN_POINT('Ctrl Pts',(-136.969062273219,3.65585782342812,
127.514393043656));
#108627=CARTESIAN_POINT('Ctrl Pts',(-136.976827026166,3.5644476304208,127.412816763118));
#108628=CARTESIAN_POINT('Ctrl Pts',(-136.984591779113,3.46868083909066,
127.314919692574));
#108629=CARTESIAN_POINT('Ctrl Pts',(-136.99235653206,3.36888693751949,127.221096202998));
#108630=CARTESIAN_POINT('Ctrl Pts',(-137.000113572945,3.2691921526582,127.127365900235));
#108631=CARTESIAN_POINT('Ctrl Pts',(-137.00787061383,3.1654785003042,127.037701392911));
#108632=CARTESIAN_POINT('Ctrl Pts',(-137.015627654715,3.05811421953378,
126.952462321559));
#108633=CARTESIAN_POINT('Ctrl Pts',(-137.023378845955,2.95083090300311,
126.867287529654));
#108634=CARTESIAN_POINT('Ctrl Pts',(-137.031130037196,2.83990274262951,
126.78653177323));
#108635=CARTESIAN_POINT('Ctrl Pts',(-137.038881228436,2.72573287993491,
126.710516051667));
#108636=CARTESIAN_POINT('Ctrl Pts',(-137.046629125213,2.61161154247706,
126.634532638813));
#108637=CARTESIAN_POINT('Ctrl Pts',(-137.05437702199,2.49425156780679,126.563285470074));
#108638=CARTESIAN_POINT('Ctrl Pts',(-137.062124918767,2.37408687204156,
126.497053502152));
#108639=CARTESIAN_POINT('Ctrl Pts',(-137.069871194851,2.25394731214024,
126.430835388529));
#108640=CARTESIAN_POINT('Ctrl Pts',(-137.077617470935,2.13100454027969,
126.369630577666));
#108641=CARTESIAN_POINT('Ctrl Pts',(-137.085363747019,2.00571863604758,
126.313672940215));
#108642=CARTESIAN_POINT('Ctrl Pts',(-137.093110080284,1.88043180698355,
126.257714889698));
#108643=CARTESIAN_POINT('Ctrl Pts',(-137.10085641355,1.75280216801121,126.207004249324));
#108644=CARTESIAN_POINT('Ctrl Pts',(-137.108602746815,1.62331104726103,
126.16172728008));
#108645=CARTESIAN_POINT('Ctrl Pts',(-137.116350814818,1.49379092787166,
126.116440171371));
#108646=CARTESIAN_POINT('Ctrl Pts',(-137.124098882821,1.36240886617453,
126.076589284166));
#108647=CARTESIAN_POINT('Ctrl Pts',(-137.131846950824,1.22966227841419,
126.042311295736));
#108648=CARTESIAN_POINT('Ctrl Pts',(-137.139603253566,1.09677460600084,
126.007996876252));
#108649=CARTESIAN_POINT('Ctrl Pts',(-137.147359556308,0.962519889676573,
125.979267285165));
#108650=CARTESIAN_POINT('Ctrl Pts',(-137.155115859049,0.827407240983745,
125.956208359224));
#108651=CARTESIAN_POINT('Ctrl Pts',(-137.162876301564,0.692222478602147,
125.93313712604));
#108652=CARTESIAN_POINT('Ctrl Pts',(-137.170636744078,0.556179259057161,
125.915742638328));
#108653=CARTESIAN_POINT('Ctrl Pts',(-137.178397186592,0.419791794311216,
125.904058799113));
#108654=CARTESIAN_POINT('Ctrl Pts',(-137.186170086857,0.283185388298951,
125.892356203963));
#108655=CARTESIAN_POINT('Ctrl Pts',(-137.193942987123,0.146234023607563,
125.886382593425));
#108656=CARTESIAN_POINT('Ctrl Pts',(-137.201715887388,0.00945279688317982,
125.886119701636));
#108657=CARTESIAN_POINT('Ctrl Pts',(-137.20920622315,-0.12235608772347,
125.885866366625));
#108658=CARTESIAN_POINT('Ctrl Pts',(-137.216696558913,-0.254006681698812,
125.890915748984));
#108659=CARTESIAN_POINT('Ctrl Pts',(-137.224186894675,-0.385044524237053,
125.901206145509));
#108660=CARTESIAN_POINT('Ctrl Pts',(-137.231961228794,-0.521050706398806,
125.911886705545));
#108661=CARTESIAN_POINT('Ctrl Pts',(-137.239735562913,-0.656827581653451,
125.928247383969));
#108662=CARTESIAN_POINT('Ctrl Pts',(-137.247509897032,-0.79186244379773,
125.950276055818));
#108663=CARTESIAN_POINT('Ctrl Pts',(-137.255274649979,-0.926730887542094,
125.972277579297));
#108664=CARTESIAN_POINT('Ctrl Pts',(-137.263039402926,-1.06085875552832,
125.999933135201));
#108665=CARTESIAN_POINT('Ctrl Pts',(-137.270804155873,-1.19373615592827,
126.033178683021));
#108666=CARTESIAN_POINT('Ctrl Pts',(-137.278561196758,-1.32648158062163,
126.066391210894));
#108667=CARTESIAN_POINT('Ctrl Pts',(-137.286318237643,-1.45797863250889,
126.105182587557));
#108668=CARTESIAN_POINT('Ctrl Pts',(-137.294075278528,-1.58772569360855,
126.149437397538));
#108669=CARTESIAN_POINT('Ctrl Pts',(-137.301826469769,-1.71737491144033,
126.193658834623));
#108670=CARTESIAN_POINT('Ctrl Pts',(-137.309577661009,-1.84527639669542,
126.243335378678));
#108671=CARTESIAN_POINT('Ctrl Pts',(-137.317328852249,-1.97094217566513,
126.29830136333));
#108672=CARTESIAN_POINT('Ctrl Pts',(-137.325076749026,-2.09655454332602,
126.353243985972));
#108673=CARTESIAN_POINT('Ctrl Pts',(-137.332824645803,-2.21993273719704,
126.413471421457));
#108674=CARTESIAN_POINT('Ctrl Pts',(-137.34057254258,-2.34060752084383,
126.478769386778));
#108675=CARTESIAN_POINT('Ctrl Pts',(-137.348318818664,-2.46125706192766,
126.544053693172));
#108676=CARTESIAN_POINT('Ctrl Pts',(-137.356065094748,-2.57920397395281,
126.614406233777));
#108677=CARTESIAN_POINT('Ctrl Pts',(-137.363811370832,-2.69400281065868,
126.689566343406));
#108678=CARTESIAN_POINT('Ctrl Pts',(-137.371557704098,-2.80880249478363,
126.764727007849));
#108679=CARTESIAN_POINT('Ctrl Pts',(-137.379304037363,-2.9204537301225,
126.844695097978));
#108680=CARTESIAN_POINT('Ctrl Pts',(-137.387050370628,-3.028539640421,126.929166337417));
#108681=CARTESIAN_POINT('Ctrl Pts',(-137.394798438631,-3.13664975580955,
127.013656493604));
#108682=CARTESIAN_POINT('Ctrl Pts',(-137.402546506634,-3.24119264938395,
127.102651565097));
#108683=CARTESIAN_POINT('Ctrl Pts',(-137.410294574637,-3.34178446505332,
127.195806938926));
#108684=CARTESIAN_POINT('Ctrl Pts',(-137.418050877379,-3.44248319090131,
127.289061319394));
#108685=CARTESIAN_POINT('Ctrl Pts',(-137.425807180121,-3.53922216307358,
127.386484568788));
#108686=CARTESIAN_POINT('Ctrl Pts',(-137.433563482863,-3.63165397745896,
127.487694754006));
#108687=CARTESIAN_POINT('Ctrl Pts',(-137.441323925377,-3.724135125487,127.588958958147));
#108688=CARTESIAN_POINT('Ctrl Pts',(-137.449084367891,-3.81230428384118,
127.694013826203));
#108689=CARTESIAN_POINT('Ctrl Pts',(-137.456844810405,-3.8958549848198,
127.802445062499));
#108690=CARTESIAN_POINT('Ctrl Pts',(-137.464617710671,-3.97953980880069,
127.911050362241));
#108691=CARTESIAN_POINT('Ctrl Pts',(-137.472390610936,-4.0585911343669,
128.023042541611));
#108692=CARTESIAN_POINT('Ctrl Pts',(-137.480163511202,-4.13274590678611,
128.137978362066));
#108693=CARTESIAN_POINT('Ctrl Pts',(-137.487653846963,-4.20420496644208,
128.248735975941));
#108694=CARTESIAN_POINT('Ctrl Pts',(-137.495144182725,-4.27111713984203,
128.362226663688));
#108695=CARTESIAN_POINT('Ctrl Pts',(-137.502634518487,-4.33328869247314,
128.478034722472));
#108696=CARTESIAN_POINT('Ctrl Pts',(-137.510836564675,-4.40136760942104,
128.604846534019));
#108697=CARTESIAN_POINT('Ctrl Pts',(-137.519038610863,-4.46395870610563,
128.734802713715));
#108698=CARTESIAN_POINT('Ctrl Pts',(-137.527240657051,-4.52077679713304,
128.867414512739));
#108699=CARTESIAN_POINT('Ctrl Pts',(-137.535424098946,-4.57746601051898,
128.999725515035));
#108700=CARTESIAN_POINT('Ctrl Pts',(-137.543607540842,-4.62840819793778,
129.134679827183));
#108701=CARTESIAN_POINT('Ctrl Pts',(-137.551790982737,-4.67336421070967,
129.27176477503));
#108702=CARTESIAN_POINT('Ctrl Pts',(-137.557907428584,-4.70696511129607,
129.374224433271));
#108703=CARTESIAN_POINT('Ctrl Pts',(-137.56402387443,-4.73722283313247,
129.477873747335));
#108704=CARTESIAN_POINT('Ctrl Pts',(-137.570140320276,-4.76405452823416,
129.582490119309));
#108705=CARTESIAN_POINT('Origin',(213.235140564004,0.,130.804360617566));
#108706=CARTESIAN_POINT('',(-139.665053375618,-4.76405452823406,129.582490119308));
#108707=CARTESIAN_POINT('',(-139.319813188101,-4.76405452823411,129.582490119308));
#108708=CARTESIAN_POINT('',(213.235140564004,-4.76405452823405,129.582490119308));
#108709=CARTESIAN_POINT('',(-137.985140563981,-4.91824805669077,130.808732728893));
#108710=CARTESIAN_POINT('Ctrl Pts',(-137.985140564011,-4.9182480566903,
130.808732729428));
#108711=CARTESIAN_POINT('Ctrl Pts',(-137.996393910965,-4.91807169202414,
131.007127739449));
#108712=CARTESIAN_POINT('Ctrl Pts',(-138.007647257918,-4.90588761893176,
131.205010702));
#108713=CARTESIAN_POINT('Ctrl Pts',(-138.018900604872,-4.88190026809492,
131.401213057349));
#108714=CARTESIAN_POINT('Ctrl Pts',(-138.025913993233,-4.86695070616923,
131.523491639974));
#108715=CARTESIAN_POINT('Ctrl Pts',(-138.032927381593,-4.84741748905136,
131.645118254441));
#108716=CARTESIAN_POINT('Ctrl Pts',(-138.039940769954,-4.82335853939743,
131.765815485421));
#108717=CARTESIAN_POINT('Ctrl Pts',(-138.047715104073,-4.79668921730225,
131.899608247586));
#108718=CARTESIAN_POINT('Ctrl Pts',(-138.055489438192,-4.76440661700594,
132.032502436212));
#108719=CARTESIAN_POINT('Ctrl Pts',(-138.063263772311,-4.72658333369079,
132.163990365761));
#108720=CARTESIAN_POINT('Ctrl Pts',(-138.071028525258,-4.68880666419196,
132.295316248188));
#108721=CARTESIAN_POINT('Ctrl Pts',(-138.078793278205,-4.64550300519149,
132.425238947745));
#108722=CARTESIAN_POINT('Ctrl Pts',(-138.086558031152,-4.59679617163898,
132.553259705251));
#108723=CARTESIAN_POINT('Ctrl Pts',(-138.094315072037,-4.54813771440021,
132.681153310736));
#108724=CARTESIAN_POINT('Ctrl Pts',(-138.102072112922,-4.49408690032992,
132.807148370388));
#108725=CARTESIAN_POINT('Ctrl Pts',(-138.109829153807,-4.43481758253591,
132.930760408793));
#108726=CARTESIAN_POINT('Ctrl Pts',(-138.117580345047,-4.37559296019541,
133.054279230399));
#108727=CARTESIAN_POINT('Ctrl Pts',(-138.125331536288,-4.31115783548495,
133.175418256576));
#108728=CARTESIAN_POINT('Ctrl Pts',(-138.133082727528,-4.24173434918522,
133.293712495755));
#108729=CARTESIAN_POINT('Ctrl Pts',(-138.140830624305,-4.172340369719,133.411956456726));
#108730=CARTESIAN_POINT('Ctrl Pts',(-138.148578521082,-4.09796244302441,
133.527357699045));
#108731=CARTESIAN_POINT('Ctrl Pts',(-138.156326417859,-4.01886877319504,
133.639475579316));
#108732=CARTESIAN_POINT('Ctrl Pts',(-138.164072693943,-3.93979164805634,
133.751570006943));
#108733=CARTESIAN_POINT('Ctrl Pts',(-138.171818970027,-3.8560009670781,
133.860382119352));
#108734=CARTESIAN_POINT('Ctrl Pts',(-138.179565246112,-3.76780818206042,
133.965500374948));
#108735=CARTESIAN_POINT('Ctrl Pts',(-138.187311579377,-3.67961474602376,
134.070619406502));
#108736=CARTESIAN_POINT('Ctrl Pts',(-138.195057912642,-3.58701939239329,
134.172044227318));
#108737=CARTESIAN_POINT('Ctrl Pts',(-138.202804245908,-3.49037350454223,
134.269396816697));
#108738=CARTESIAN_POINT('Ctrl Pts',(-138.210552313911,-3.39370597351482,
134.366771207514));
#108739=CARTESIAN_POINT('Ctrl Pts',(-138.218300381914,-3.29298637865716,
134.460071274816));
#108740=CARTESIAN_POINT('Ctrl Pts',(-138.226048449916,-3.18860225763736,
134.548956551053));
#108741=CARTESIAN_POINT('Ctrl Pts',(-138.233804752658,-3.08410719593141,
134.63793629562));
#108742=CARTESIAN_POINT('Ctrl Pts',(-138.2415610554,-2.97594012611937,134.722491622287));
#108743=CARTESIAN_POINT('Ctrl Pts',(-138.249317358142,-2.86452133948699,
134.802322668177));
#108744=CARTESIAN_POINT('Ctrl Pts',(-138.257077800656,-2.75304308529314,
134.8821963223));
#108745=CARTESIAN_POINT('Ctrl Pts',(-138.264838243171,-2.6383099829711,
134.957340457259));
#108746=CARTESIAN_POINT('Ctrl Pts',(-138.272598685685,-2.52076962491561,
135.027499682362));
#108747=CARTESIAN_POINT('Ctrl Pts',(-138.28037158595,-2.40304058064295,
135.097771533281));
#108748=CARTESIAN_POINT('Ctrl Pts',(-138.288144486216,-2.28249561930117,
135.163042297096));
#108749=CARTESIAN_POINT('Ctrl Pts',(-138.295917386481,-2.1596059461205,
135.223103110627));
#108750=CARTESIAN_POINT('Ctrl Pts',(-138.303407722243,-2.04118362210135,
135.280980562302));
#108751=CARTESIAN_POINT('Ctrl Pts',(-138.310898058005,-1.9205843809104,
135.334020152977));
#108752=CARTESIAN_POINT('Ctrl Pts',(-138.318388393767,-1.79824389748059,
135.382078602291));
#108753=CARTESIAN_POINT('Ctrl Pts',(-138.326162727886,-1.67126483743606,
135.431959202318));
#108754=CARTESIAN_POINT('Ctrl Pts',(-138.333937062005,-1.54200765877966,
135.476631491471));
#108755=CARTESIAN_POINT('Ctrl Pts',(-138.341711396124,-1.41093873120191,
135.515882129699));
#108756=CARTESIAN_POINT('Ctrl Pts',(-138.349476149071,-1.28003133436342,
135.555084395024));
#108757=CARTESIAN_POINT('Ctrl Pts',(-138.357240902018,-1.14731700218345,
135.588878192932));
#108758=CARTESIAN_POINT('Ctrl Pts',(-138.365005654965,-1.01328227989185,
135.617098100928));
#108759=CARTESIAN_POINT('Ctrl Pts',(-138.37276269585,-0.879380682775994,
135.645289980513));
#108760=CARTESIAN_POINT('Ctrl Pts',(-138.380519736736,-0.744161685455616,
135.66791890718));
#108761=CARTESIAN_POINT('Ctrl Pts',(-138.388276777621,-0.60812686266937,
135.684869277675));
#108762=CARTESIAN_POINT('Ctrl Pts',(-138.396027968861,-0.472194624800999,
135.701806865764));
#108763=CARTESIAN_POINT('Ctrl Pts',(-138.403779160101,-0.335448172420758,
135.713074373082));
#108764=CARTESIAN_POINT('Ctrl Pts',(-138.411530351341,-0.198398788625114,
135.718607353656));
#108765=CARTESIAN_POINT('Ctrl Pts',(-138.419278248118,-0.0614076544733079,
135.724137982566));
#108766=CARTESIAN_POINT('Ctrl Pts',(-138.427026144895,0.0758857651830259,
135.723938916651));
#108767=CARTESIAN_POINT('Ctrl Pts',(-138.434774041672,0.212965773710997,
135.717997625092));
#108768=CARTESIAN_POINT('Ctrl Pts',(-138.442520317756,0.350017108055913,
135.712057576323));
#108769=CARTESIAN_POINT('Ctrl Pts',(-138.45026659384,0.486854729714837,
135.700377707982));
#108770=CARTESIAN_POINT('Ctrl Pts',(-138.458012869925,0.622964049780873,
135.682997605002));
#108771=CARTESIAN_POINT('Ctrl Pts',(-138.46575920319,0.759074374575175,
135.665617373727));
#108772=CARTESIAN_POINT('Ctrl Pts',(-138.473505536455,0.894455999232597,
135.642536873371));
#108773=CARTESIAN_POINT('Ctrl Pts',(-138.481251869721,1.02860095293648,
135.613847403297));
#108774=CARTESIAN_POINT('Ctrl Pts',(-138.488999937724,1.16277594747246,
135.585151508415));
#108775=CARTESIAN_POINT('Ctrl Pts',(-138.496748005726,1.29571333772249,
135.550844226091));
#108776=CARTESIAN_POINT('Ctrl Pts',(-138.504496073729,1.42691720511787,
135.511067571715));
#108777=CARTESIAN_POINT('Ctrl Pts',(-138.512252376471,1.55826051754504,
135.471248642238));
#108778=CARTESIAN_POINT('Ctrl Pts',(-138.520008679213,1.68786625196201,
135.425948842396));
#108779=CARTESIAN_POINT('Ctrl Pts',(-138.527764981955,1.81525494753177,
135.375359691944));
#108780=CARTESIAN_POINT('Ctrl Pts',(-138.535525424469,1.94271163428396,
135.324743540538));
#108781=CARTESIAN_POINT('Ctrl Pts',(-138.543285866983,2.067948567534,135.268832572587));
#108782=CARTESIAN_POINT('Ctrl Pts',(-138.551046309498,2.1905089452371,135.207865315342));
#108783=CARTESIAN_POINT('Ctrl Pts',(-138.558819209763,2.31326606773889,
135.146800188043));
#108784=CARTESIAN_POINT('Ctrl Pts',(-138.566592110028,2.43333770597991,
135.080662740224));
#108785=CARTESIAN_POINT('Ctrl Pts',(-138.574365010294,2.55029343951556,
135.009736514542));
#108786=CARTESIAN_POINT('Ctrl Pts',(-138.581855346056,2.66299753754316,
134.941388635815));
#108787=CARTESIAN_POINT('Ctrl Pts',(-138.589345681818,2.77280808300221,
134.868594272977));
#108788=CARTESIAN_POINT('Ctrl Pts',(-138.59683601758,2.87936903712286,134.791642525151));
#108789=CARTESIAN_POINT('Ctrl Pts',(-138.604610351699,2.98997028220766,
134.711773128418));
#108790=CARTESIAN_POINT('Ctrl Pts',(-138.612384685818,3.09742100660305,
134.62717186673));
#108791=CARTESIAN_POINT('Ctrl Pts',(-138.620159019937,3.20128963707245,
134.538115794606));
#108792=CARTESIAN_POINT('Ctrl Pts',(-138.627923772884,3.3050302587378,134.449169476132));
#108793=CARTESIAN_POINT('Ctrl Pts',(-138.635688525831,3.40519727627937,
134.355779523033));
#108794=CARTESIAN_POINT('Ctrl Pts',(-138.643453278778,3.50138852548422,
134.25826586469));
#108795=CARTESIAN_POINT('Ctrl Pts',(-138.651210319663,3.5974842361843,134.160849058286));
#108796=CARTESIAN_POINT('Ctrl Pts',(-138.658967360548,3.68961176403253,
134.059316973845));
#108797=CARTESIAN_POINT('Ctrl Pts',(-138.666724401433,3.77740273534095,
133.954029114017));
#108798=CARTESIAN_POINT('Ctrl Pts',(-138.674475592673,3.8651275027951,133.848820652584));
#108799=CARTESIAN_POINT('Ctrl Pts',(-138.682226783913,3.94852197354323,
133.739862352265));
#108800=CARTESIAN_POINT('Ctrl Pts',(-138.689977975154,4.02725556636115,
133.627549535388));
#108801=CARTESIAN_POINT('Ctrl Pts',(-138.697725871931,4.10595569530195,
133.515284454454));
#108802=CARTESIAN_POINT('Ctrl Pts',(-138.705473768708,4.17999866241224,
133.399668012156));
#108803=CARTESIAN_POINT('Ctrl Pts',(-138.713221665485,4.24909517853229,
133.281127305462));
#108804=CARTESIAN_POINT('Ctrl Pts',(-138.720967941569,4.31817724115053,
133.162611394929));
#108805=CARTESIAN_POINT('Ctrl Pts',(-138.728714217653,4.38231471407525,
133.04117277425));
#108806=CARTESIAN_POINT('Ctrl Pts',(-138.736460493737,4.44126275335914,
132.917265778269));
#108807=CARTESIAN_POINT('Ctrl Pts',(-138.744206827003,4.50021122778415,
132.793357867635));
#108808=CARTESIAN_POINT('Ctrl Pts',(-138.751953160268,4.5539700241684,132.666981898389));
#108809=CARTESIAN_POINT('Ctrl Pts',(-138.759699493533,4.60234138461656,
132.538614590301));
#108810=CARTESIAN_POINT('Ctrl Pts',(-138.767447561536,4.65072357749543,
132.410218535244));
#108811=CARTESIAN_POINT('Ctrl Pts',(-138.775195629539,4.69371579585063,
132.279830619747));
#108812=CARTESIAN_POINT('Ctrl Pts',(-138.782943697542,4.7311694651505,132.147944836931));
#108813=CARTESIAN_POINT('Ctrl Pts',(-138.790700000284,4.76866294065585,
132.015918884336));
#108814=CARTESIAN_POINT('Ctrl Pts',(-138.798456303026,4.80060600134069,
131.882392261023));
#108815=CARTESIAN_POINT('Ctrl Pts',(-138.806212605767,4.82690061790301,
131.747871872076));
#108816=CARTESIAN_POINT('Ctrl Pts',(-138.813973048282,4.85320926869389,
131.613279685548));
#108817=CARTESIAN_POINT('Ctrl Pts',(-138.821733490796,4.87386340937981,
131.477693062832));
#108818=CARTESIAN_POINT('Ctrl Pts',(-138.82949393331,4.88881680702904,131.341625254231));
#108819=CARTESIAN_POINT('Ctrl Pts',(-138.837266833575,4.90379420919969,
131.205339017504));
#108820=CARTESIAN_POINT('Ctrl Pts',(-138.845039733841,4.9130525546221,131.068570441603));
#108821=CARTESIAN_POINT('Ctrl Pts',(-138.852812634106,4.91659774299873,
130.93183491317));
#108822=CARTESIAN_POINT('Ctrl Pts',(-138.860302969868,4.92001405484807,
130.800070065612));
#108823=CARTESIAN_POINT('Ctrl Pts',(-138.86779330563,4.91812537784109,130.668336212506));
#108824=CARTESIAN_POINT('Ctrl Pts',(-138.875283641392,4.91098249160705,
130.537089164491));
#108825=CARTESIAN_POINT('Ctrl Pts',(-138.883057975511,4.9035687806704,130.400865844758));
#108826=CARTESIAN_POINT('Ctrl Pts',(-138.89083230963,4.89047108434516,130.264735458718));
#108827=CARTESIAN_POINT('Ctrl Pts',(-138.898606643749,4.87168922056954,
130.129210855893));
#108828=CARTESIAN_POINT('Ctrl Pts',(-138.906371396697,4.85293050376244,
129.993853275029));
#108829=CARTESIAN_POINT('Ctrl Pts',(-138.914136149644,4.82850161097577,
129.859100375468));
#108830=CARTESIAN_POINT('Ctrl Pts',(-138.921900902591,4.79845432827841,
129.725463438996));
#108831=CARTESIAN_POINT('Ctrl Pts',(-138.929657943476,4.76843688896581,
129.591959232614));
#108832=CARTESIAN_POINT('Ctrl Pts',(-138.937414984361,4.73281224992935,
129.459569162548));
#108833=CARTESIAN_POINT('Ctrl Pts',(-138.945172025246,4.6916837559549,129.328797471981));
#108834=CARTESIAN_POINT('Ctrl Pts',(-138.952923216486,4.65058627729763,
129.198124397363));
#108835=CARTESIAN_POINT('Ctrl Pts',(-138.960674407726,4.60399332184252,
129.069067644491));
#108836=CARTESIAN_POINT('Ctrl Pts',(-138.968425598966,4.55205879823291,
128.942119022087));
#108837=CARTESIAN_POINT('Ctrl Pts',(-138.976173495743,4.50014634818131,
128.815224356235));
#108838=CARTESIAN_POINT('Ctrl Pts',(-138.98392139252,4.44289699317143,128.690436399849));
#108839=CARTESIAN_POINT('Ctrl Pts',(-138.991669289297,4.38051369412193,
128.568229396436));
#108840=CARTESIAN_POINT('Ctrl Pts',(-138.999415565381,4.31814344431375,
128.446047956095));
#108841=CARTESIAN_POINT('Ctrl Pts',(-139.007161841465,4.25064156417624,
128.326446742875));
#108842=CARTESIAN_POINT('Ctrl Pts',(-139.01490811755,4.17825795434795,128.209877330006));
#108843=CARTESIAN_POINT('Ctrl Pts',(-139.022654450815,4.1058738102002,128.093307056648));
#108844=CARTESIAN_POINT('Ctrl Pts',(-139.03040078408,4.02860807069741,127.979768960439));
#108845=CARTESIAN_POINT('Ctrl Pts',(-139.038147117346,3.94675492071036,
127.869687099379));
#108846=CARTESIAN_POINT('Ctrl Pts',(-139.045895185349,3.86488344027801,
127.759580586249));
#108847=CARTESIAN_POINT('Ctrl Pts',(-139.053643253352,3.77842273835661,
127.652932162116));
#108848=CARTESIAN_POINT('Ctrl Pts',(-139.061391321355,3.6877081171879,127.55013384229));
#108849=CARTESIAN_POINT('Ctrl Pts',(-139.069147624096,3.59689708344042,
127.447226267186));
#108850=CARTESIAN_POINT('Ctrl Pts',(-139.076903926838,3.50182335812934,
127.348177264087));
#108851=CARTESIAN_POINT('Ctrl Pts',(-139.08466022958,3.4028604276272,127.253343302403));
#108852=CARTESIAN_POINT('Ctrl Pts',(-139.092420672094,3.30384467762906,
127.158458724977));
#108853=CARTESIAN_POINT('Ctrl Pts',(-139.100181114608,3.20093587947142,
127.067793929997));
#108854=CARTESIAN_POINT('Ctrl Pts',(-139.107941557123,3.09454085514129,
126.981665238862));
#108855=CARTESIAN_POINT('Ctrl Pts',(-139.115714457388,2.9879750360728,126.895398286307));
#108856=CARTESIAN_POINT('Ctrl Pts',(-139.123487357653,2.87791212152879,
126.813682222061));
#108857=CARTESIAN_POINT('Ctrl Pts',(-139.131260257919,2.76478890982042,
126.736790661605));
#108858=CARTESIAN_POINT('Ctrl Pts',(-139.138750593681,2.65577801179751,
126.662694303051));
#108859=CARTESIAN_POINT('Ctrl Pts',(-139.146240929443,2.54392571422631,
126.593077935124));
#108860=CARTESIAN_POINT('Ctrl Pts',(-139.153731265205,2.42964295113666,
126.52814521227));
#108861=CARTESIAN_POINT('Ctrl Pts',(-139.161505599324,2.31102712234946,
126.460750545493));
#108862=CARTESIAN_POINT('Ctrl Pts',(-139.169279933443,2.18941714836848,
126.398188209533));
#108863=CARTESIAN_POINT('Ctrl Pts',(-139.177054267562,2.0652444056126,126.340735565259));
#108864=CARTESIAN_POINT('Ctrl Pts',(-139.184819020509,1.94122469466454,
126.283353726233));
#108865=CARTESIAN_POINT('Ctrl Pts',(-139.192583773456,1.81464885060286,
126.231069211861));
#108866=CARTESIAN_POINT('Ctrl Pts',(-139.200348526404,1.68597502091083,
126.184114813351));
#108867=CARTESIAN_POINT('Ctrl Pts',(-139.208105567289,1.55742899188043,
126.137207050612));
#108868=CARTESIAN_POINT('Ctrl Pts',(-139.215862608174,1.42678948887343,
126.095619001698));
#108869=CARTESIAN_POINT('Ctrl Pts',(-139.223619649059,1.29453660634004,
126.05953627547));
#108870=CARTESIAN_POINT('Ctrl Pts',(-139.231370840299,1.16238345673433,
126.023480759507));
#108871=CARTESIAN_POINT('Ctrl Pts',(-139.239122031539,1.02861972494722,
125.992922405199));
#108872=CARTESIAN_POINT('Ctrl Pts',(-139.246873222779,0.893742374965194,
125.967997559472));
#108873=CARTESIAN_POINT('Ctrl Pts',(-139.254621119556,0.758922351454701,
125.94308330747));
#108874=CARTESIAN_POINT('Ctrl Pts',(-139.262369016333,0.622990034792487,
125.923797872684));
#108875=CARTESIAN_POINT('Ctrl Pts',(-139.27011691311,0.486454124806543,
125.910226838545));
#108876=CARTESIAN_POINT('Ctrl Pts',(-139.277863189194,0.349946775189595,
125.896658643173));
#108877=CARTESIAN_POINT('Ctrl Pts',(-139.285609465278,0.212836472186074,
125.888802509518));
#108878=CARTESIAN_POINT('Ctrl Pts',(-139.293355741362,0.075638214541899,
125.886692275455));
#108879=CARTESIAN_POINT('Ctrl Pts',(-139.301102074628,-0.0615610558684601,
125.884582025815));
#108880=CARTESIAN_POINT('Ctrl Pts',(-139.308848407893,-0.198847891296058,
125.888217766415));
#108881=CARTESIAN_POINT('Ctrl Pts',(-139.316594741158,-0.335706505628503,
125.897581204898));
#108882=CARTESIAN_POINT('Ctrl Pts',(-139.324342809161,-0.472595768498903,
125.906946740259));
#108883=CARTESIAN_POINT('Ctrl Pts',(-139.332090877164,-0.609056229471209,
125.922042499203));
#108884=CARTESIAN_POINT('Ctrl Pts',(-139.339838945167,-0.744576835910049,
125.942798276309));
#108885=CARTESIAN_POINT('Ctrl Pts',(-139.347595247909,-0.880241475262313,
125.963576112902));
#108886=CARTESIAN_POINT('Ctrl Pts',(-139.355351550651,-1.0149638776184,
125.990025925053));
#108887=CARTESIAN_POINT('Ctrl Pts',(-139.363107853393,-1.14824225666175,
126.022026168522));
#108888=CARTESIAN_POINT('Ctrl Pts',(-139.370868295907,-1.28159177038893,
126.054043491484));
#108889=CARTESIAN_POINT('Ctrl Pts',(-139.378628738421,-1.41349534925753,
126.091617041605));
#108890=CARTESIAN_POINT('Ctrl Pts',(-139.386389180935,-1.54346696589354,
126.134575527469));
#108891=CARTESIAN_POINT('Ctrl Pts',(-139.394162081201,-1.67364722450692,
126.177602974108));
#108892=CARTESIAN_POINT('Ctrl Pts',(-139.401934981466,-1.8018889574237,
126.226032492506));
#108893=CARTESIAN_POINT('Ctrl Pts',(-139.409707881732,-1.92772586403322,
126.279644487726));
#108894=CARTESIAN_POINT('Ctrl Pts',(-139.417198217494,-2.04898828212412,
126.331307551878));
#108895=CARTESIAN_POINT('Ctrl Pts',(-139.424688553256,-2.16801740308042,
126.387782710308));
#108896=CARTESIAN_POINT('Ctrl Pts',(-139.432178889018,-2.28441976676988,
126.448834312779));
#108897=CARTESIAN_POINT('Ctrl Pts',(-139.439954129292,-2.40524964342127,
126.512208091129));
#108898=CARTESIAN_POINT('Ctrl Pts',(-139.447729369567,-2.52363178103368,
126.580714118607));
#108899=CARTESIAN_POINT('Ctrl Pts',(-139.455504609842,-2.6390994965336,
126.654139309022));
#108900=CARTESIAN_POINT('Ctrl Pts',(-139.463270068542,-2.75442194887057,
126.727472127509));
#108901=CARTESIAN_POINT('Ctrl Pts',(-139.471035527243,-2.86683694802424,
126.80571158659));
#108902=CARTESIAN_POINT('Ctrl Pts',(-139.478800985943,-2.97590088322747,
126.888597984859));
#108903=CARTESIAN_POINT('Ctrl Pts',(-139.48656150218,-3.08489540275135,
126.971431628606));
#108904=CARTESIAN_POINT('Ctrl Pts',(-139.494322018416,-3.19054278141714,
127.058906106823));
#108905=CARTESIAN_POINT('Ctrl Pts',(-139.502082534653,-3.29242681219755,
127.150717401703));
#108906=CARTESIAN_POINT('Ctrl Pts',(-139.509833439601,-3.39418466107156,
127.242414989615));
#108907=CARTESIAN_POINT('Ctrl Pts',(-139.51758434455,-3.49218816612692,
127.338438423298));
#108908=CARTESIAN_POINT('Ctrl Pts',(-139.525335249499,-3.58605405763608,
127.438443304528));
#108909=CARTESIAN_POINT('Ctrl Pts',(-139.533082571577,-3.67987655945166,
127.538401958304));
#108910=CARTESIAN_POINT('Ctrl Pts',(-139.540829893654,-3.76956498665699,
127.642338113013));
#108911=CARTESIAN_POINT('Ctrl Pts',(-139.548577215732,-3.85477247012094,
127.749870109135));
#108912=CARTESIAN_POINT('Ctrl Pts',(-139.556322634353,-3.93995901877257,
127.857375685485));
#108913=CARTESIAN_POINT('Ctrl Pts',(-139.564068052974,-4.02066657293211,
127.968475038309));
#108914=CARTESIAN_POINT('Ctrl Pts',(-139.571813471595,-4.09658841676912,
128.082753297232));
#108915=CARTESIAN_POINT('Ctrl Pts',(-139.579583463597,-4.17275113285114,
128.197394119279));
#108916=CARTESIAN_POINT('Ctrl Pts',(-139.587353455599,-4.24409748231012,
128.315233736527));
#108917=CARTESIAN_POINT('Ctrl Pts',(-139.595123447601,-4.31036172877056,
128.435824185579));
#108918=CARTESIAN_POINT('Ctrl Pts',(-139.602872468509,-4.37644712900863,
128.55608916279));
#108919=CARTESIAN_POINT('Ctrl Pts',(-139.610621489417,-4.43747766755824,
128.679089780643));
#108920=CARTESIAN_POINT('Ctrl Pts',(-139.618370510325,-4.49323626298589,
128.804357880696));
#108921=CARTESIAN_POINT('Ctrl Pts',(-139.626150987874,-4.54922120676266,
128.930134498358));
#108922=CARTESIAN_POINT('Ctrl Pts',(-139.633931465423,-4.59989115241724,
129.058196684052));
#108923=CARTESIAN_POINT('Ctrl Pts',(-139.641711942971,-4.64507580615303,
129.188051916361));
#108924=CARTESIAN_POINT('Ctrl Pts',(-139.64949242052,-4.69026045988882,
129.317907148669));
#108925=CARTESIAN_POINT('Ctrl Pts',(-139.657272898069,-4.7299597353934,
129.449555039483));
#108926=CARTESIAN_POINT('Ctrl Pts',(-139.665053375618,-4.76405452823406,
129.582490119308));
#108927=CARTESIAN_POINT('Ctrl Pts',(-137.915064401336,-4.76405452823416,
129.582490119309));
#108928=CARTESIAN_POINT('Ctrl Pts',(-137.922702589614,-4.79767840181093,
129.713589092071));
#108929=CARTESIAN_POINT('Ctrl Pts',(-137.930340777891,-4.82587511235423,
129.84603213272));
#108930=CARTESIAN_POINT('Ctrl Pts',(-137.937978966169,-4.84855616045776,
129.979323514529));
#108931=CARTESIAN_POINT('Ctrl Pts',(-137.945839232471,-4.87189665320671,
130.116490303137));
#108932=CARTESIAN_POINT('Ctrl Pts',(-137.953699498773,-4.88939578415974,
130.2545550626));
#108933=CARTESIAN_POINT('Ctrl Pts',(-137.961559765075,-4.90101442601767,
130.392971922453));
#108934=CARTESIAN_POINT('Ctrl Pts',(-137.969420031377,-4.91263306787557,
130.531388782306));
#108935=CARTESIAN_POINT('Ctrl Pts',(-137.977280297679,-4.91837124431475,
130.67015727946));
#108936=CARTESIAN_POINT('Ctrl Pts',(-137.985140563981,-4.91824805669077,
130.808732728894));
#108937=CARTESIAN_POINT('',(-137.639859435963,-4.91824999609688,130.804164676221));
#108938=CARTESIAN_POINT('Ctrl Pts',(-137.570140320276,-4.76405452823416,
129.582490119309));
#108939=CARTESIAN_POINT('Ctrl Pts',(-137.578299432275,-4.79984701474554,
129.72204448099));
#108940=CARTESIAN_POINT('Ctrl Pts',(-137.586458544274,-4.82954117751263,
129.86332018502));
#108941=CARTESIAN_POINT('Ctrl Pts',(-137.594617656273,-4.85298251559954,
130.005772008966));
#108942=CARTESIAN_POINT('Ctrl Pts',(-137.602760536601,-4.87637721968048,
130.147940440421));
#108943=CARTESIAN_POINT('Ctrl Pts',(-137.610903416929,-4.89354385174692,
130.291280003989));
#108944=CARTESIAN_POINT('Ctrl Pts',(-137.619046297257,-4.90437849770947,
130.435233791523));
#108945=CARTESIAN_POINT('Ctrl Pts',(-137.625984010159,-4.91360958794428,
130.557882044816));
#108946=CARTESIAN_POINT('Ctrl Pts',(-137.632921723061,-4.91824508829574,
130.680975806247));
#108947=CARTESIAN_POINT('Ctrl Pts',(-137.639859435962,-4.91824999609688,
130.80416467622));
#108948=CARTESIAN_POINT('Ctrl Pts',(-137.639859435993,-4.9182499960969,
130.804164676763));
#108949=CARTESIAN_POINT('Ctrl Pts',(-137.647950330633,-4.91825571965343,
130.947829913684));
#108950=CARTESIAN_POINT('Ctrl Pts',(-137.656041225272,-4.91196229675644,
131.091381545826));
#108951=CARTESIAN_POINT('Ctrl Pts',(-137.664132119912,-4.89942539442703,
131.234260451183));
#108952=CARTESIAN_POINT('Ctrl Pts',(-137.672232833425,-4.88687327767845,
131.377312750213));
#108953=CARTESIAN_POINT('Ctrl Pts',(-137.680333546939,-4.86806259391348,
131.519690357764));
#108954=CARTESIAN_POINT('Ctrl Pts',(-137.688434260452,-4.84310046393196,
131.660842350449));
#108955=CARTESIAN_POINT('Ctrl Pts',(-137.69655331512,-4.81808181617694,
131.802313931099));
#108956=CARTESIAN_POINT('Ctrl Pts',(-137.704672369788,-4.78688393570534,
131.94255401557));
#108957=CARTESIAN_POINT('Ctrl Pts',(-137.712791424457,-4.7496648149431,
132.081023144701));
#108958=CARTESIAN_POINT('Ctrl Pts',(-137.720920044814,-4.71240184344443,
132.219655415067));
#108959=CARTESIAN_POINT('Ctrl Pts',(-137.729048665171,-4.66910357720709,
132.356512245095));
#108960=CARTESIAN_POINT('Ctrl Pts',(-137.737177285528,-4.61997693377902,
132.491072268634));
#108961=CARTESIAN_POINT('Ctrl Pts',(-137.745324434336,-4.57073831063017,
132.625939009523));
#108962=CARTESIAN_POINT('Ctrl Pts',(-137.753471583145,-4.51564487449885,
132.75849816283));
#108963=CARTESIAN_POINT('Ctrl Pts',(-137.761618731954,-4.45495122267971,
132.888249450024));
#108964=CARTESIAN_POINT('Ctrl Pts',(-137.768106535402,-4.40661916285855,
132.991574044715));
#108965=CARTESIAN_POINT('Ctrl Pts',(-137.774594338851,-4.3547367290656,
133.093118493441));
#108966=CARTESIAN_POINT('Ctrl Pts',(-137.7810821423,-4.29945224525747,133.19264314969));
#108967=CARTESIAN_POINT('Ctrl Pts',(-137.788856476419,-4.23320485473174,
133.311903533714));
#108968=CARTESIAN_POINT('Ctrl Pts',(-137.796630810538,-4.16188661511739,
133.4285943232));
#108969=CARTESIAN_POINT('Ctrl Pts',(-137.804405144657,-4.08572166916645,
133.542254243075));
#108970=CARTESIAN_POINT('Ctrl Pts',(-137.812169897604,-4.00965058970434,
133.655774087257));
#108971=CARTESIAN_POINT('Ctrl Pts',(-137.819934650552,-3.92874490421212,
133.766270172248));
#108972=CARTESIAN_POINT('Ctrl Pts',(-137.827699403499,-3.84327480367038,
133.873305362258));
#108973=CARTESIAN_POINT('Ctrl Pts',(-137.835456444384,-3.75788959323741,
133.980234243409));
#108974=CARTESIAN_POINT('Ctrl Pts',(-137.843213485269,-3.66794923188803,
134.083708766644));
#108975=CARTESIAN_POINT('Ctrl Pts',(-137.850970526154,-3.57376719784275,
134.183320676241));
#108976=CARTESIAN_POINT('Ctrl Pts',(-137.858721717394,-3.47965618720185,
134.282857467723));
#108977=CARTESIAN_POINT('Ctrl Pts',(-137.866472908634,-3.38131013815635,
134.378537160432));
#108978=CARTESIAN_POINT('Ctrl Pts',(-137.874224099874,-3.27908256150896,
134.469984795971));
#108979=CARTESIAN_POINT('Ctrl Pts',(-137.881971996651,-3.1768984343088,
134.561393563825));
#108980=CARTESIAN_POINT('Ctrl Pts',(-137.889719893428,-3.07083635151974,
134.648573591943));
#108981=CARTESIAN_POINT('Ctrl Pts',(-137.897467790205,-2.96128625313847,
134.73118717211));
#108982=CARTESIAN_POINT('Ctrl Pts',(-137.90521406629,-2.85175907027616,
134.813783471297));
#108983=CARTESIAN_POINT('Ctrl Pts',(-137.912960342374,-2.73874563502764,
134.891814987232));
#108984=CARTESIAN_POINT('Ctrl Pts',(-137.920706618458,-2.62266818398729,
134.964984928796));
#108985=CARTESIAN_POINT('Ctrl Pts',(-137.928452951723,-2.50658987608973,
135.038155410484));
#108986=CARTESIAN_POINT('Ctrl Pts',(-137.936199284989,-2.38744783800748,
135.106464037707));
#108987=CARTESIAN_POINT('Ctrl Pts',(-137.943945618254,-2.26569209585419,
135.169658131973));
#108988=CARTESIAN_POINT('Ctrl Pts',(-137.951693686257,-2.14390908734681,
135.232866378117));
#108989=CARTESIAN_POINT('Ctrl Pts',(-137.95944175426,-2.01951155699064,
135.29095763209));
#108990=CARTESIAN_POINT('Ctrl Pts',(-137.967189822263,-1.892972492336,135.343726014376));
#108991=CARTESIAN_POINT('Ctrl Pts',(-137.974946125005,-1.76629894045744,
135.396550479528));
#108992=CARTESIAN_POINT('Ctrl Pts',(-137.982702427747,-1.63747966905109,
135.444040621386));
#108993=CARTESIAN_POINT('Ctrl Pts',(-137.990458730488,-1.50700645708785,
135.486039226868));
#108994=CARTESIAN_POINT('Ctrl Pts',(-137.998219173003,-1.3764636076429,
135.52806024827));
#108995=CARTESIAN_POINT('Ctrl Pts',(-138.005979615517,-1.24426543533416,
135.56458378897));
#108996=CARTESIAN_POINT('Ctrl Pts',(-138.013740058031,-1.11091613754168,
135.595503320288));
#108997=CARTESIAN_POINT('Ctrl Pts',(-138.021512958296,-0.977352775617833,
135.626472486383));
#108998=CARTESIAN_POINT('Ctrl Pts',(-138.029285858562,-0.842634979984229,
135.651819593783));
#108999=CARTESIAN_POINT('Ctrl Pts',(-138.037058758827,-0.707275226726109,
135.671489629228));
#109000=CARTESIAN_POINT('Ctrl Pts',(-138.044549094589,-0.576836141448093,
135.690444609339));
#109001=CARTESIAN_POINT('Ctrl Pts',(-138.052039430351,-0.44580126813016,
135.704128071259));
#109002=CARTESIAN_POINT('Ctrl Pts',(-138.059529766114,-0.314629224559155,
135.712536603974));
#109003=CARTESIAN_POINT('Ctrl Pts',(-138.067304100233,-0.178483753088626,
135.721263948763));
#109004=CARTESIAN_POINT('Ctrl Pts',(-138.075078434352,-0.04175923648286,
135.724336115985));
#109005=CARTESIAN_POINT('Ctrl Pts',(-138.082852768471,0.0950350868433429,
135.721692352844));
#109006=CARTESIAN_POINT('Ctrl Pts',(-138.090617521418,0.231660823391335,
135.719051847904));
#109007=CARTESIAN_POINT('Ctrl Pts',(-138.098382274365,0.368355808344941,
135.710709436285));
#109008=CARTESIAN_POINT('Ctrl Pts',(-138.106147027312,0.504606222160545,
135.69665615474));
#109009=CARTESIAN_POINT('Ctrl Pts',(-138.113904068197,0.640721310144724,
135.682616831113));
#109010=CARTESIAN_POINT('Ctrl Pts',(-138.121661109082,0.776392319318485,
135.662877965181));
#109011=CARTESIAN_POINT('Ctrl Pts',(-138.129418149967,0.911106329944074,
135.637482622858));
#109012=CARTESIAN_POINT('Ctrl Pts',(-138.137169341207,1.04571875168615,
135.61210643136));
#109013=CARTESIAN_POINT('Ctrl Pts',(-138.144920532447,1.17937522869683,
135.581082326009));
#109014=CARTESIAN_POINT('Ctrl Pts',(-138.152671723688,1.31156921663241,
135.544505051281));
#109015=CARTESIAN_POINT('Ctrl Pts',(-138.160419620465,1.44370701859692,
135.507943322871));
#109016=CARTESIAN_POINT('Ctrl Pts',(-138.168167517242,1.57438319177689,
135.465833223474));
#109017=CARTESIAN_POINT('Ctrl Pts',(-138.175915414019,1.70310284059474,
135.418320281115));
#109018=CARTESIAN_POINT('Ctrl Pts',(-138.183661690103,1.83179556403693,
135.370817277439));
#109019=CARTESIAN_POINT('Ctrl Pts',(-138.191407966187,1.95853221061903,
135.317913814046));
#109020=CARTESIAN_POINT('Ctrl Pts',(-138.199154242271,2.08283485237382,
135.259804707692));
#109021=CARTESIAN_POINT('Ctrl Pts',(-138.206900575537,2.20713841170265,
135.201695172389));
#109022=CARTESIAN_POINT('Ctrl Pts',(-138.214646908802,2.32900757617628,
135.138380083017));
#109023=CARTESIAN_POINT('Ctrl Pts',(-138.222393242067,2.44798651011493,
135.070101480393));
#109024=CARTESIAN_POINT('Ctrl Pts',(-138.23014131007,2.56699208856074,135.00180758725));
#109025=CARTESIAN_POINT('Ctrl Pts',(-138.237889378073,2.68310580949424,
134.92854816357));
#109026=CARTESIAN_POINT('Ctrl Pts',(-138.245637446076,2.7958987993247,134.850609864268));
#109027=CARTESIAN_POINT('Ctrl Pts',(-138.253393748818,2.90881166688716,
134.772588731214));
#109028=CARTESIAN_POINT('Ctrl Pts',(-138.26115005156,3.01839643100426,134.689879011513));
#109029=CARTESIAN_POINT('Ctrl Pts',(-138.268906354302,3.12425500531025,
134.602809475231));
#109030=CARTESIAN_POINT('Ctrl Pts',(-138.276666796816,3.23017007952469,
134.515693467315));
#109031=CARTESIAN_POINT('Ctrl Pts',(-138.28442723933,3.33235470996866,134.424213266789));
#109032=CARTESIAN_POINT('Ctrl Pts',(-138.292187681844,3.430446740048,134.328735487836));
#109033=CARTESIAN_POINT('Ctrl Pts',(-138.29996058211,3.52869623616224,134.233104439477));
#109034=CARTESIAN_POINT('Ctrl Pts',(-138.307733482375,3.62283973468952,
134.13346327329));
#109035=CARTESIAN_POINT('Ctrl Pts',(-138.315506382641,3.71255394557539,
134.030213413912));
#109036=CARTESIAN_POINT('Ctrl Pts',(-138.322996718403,3.79900681891668,
133.930716946995));
#109037=CARTESIAN_POINT('Ctrl Pts',(-138.330487054164,3.88134665269578,
133.827869842381));
#109038=CARTESIAN_POINT('Ctrl Pts',(-138.337977389926,3.95932268301334,
133.722056104466));
#109039=CARTESIAN_POINT('Ctrl Pts',(-138.345751724045,4.04025519822242,
133.612230406514));
#109040=CARTESIAN_POINT('Ctrl Pts',(-138.353526058164,4.11674284042205,
133.49886077988));
#109041=CARTESIAN_POINT('Ctrl Pts',(-138.361300392283,4.1884592407602,133.382342822895));
#109042=CARTESIAN_POINT('Ctrl Pts',(-138.36906514523,4.2600872570448,133.265968463877));
#109043=CARTESIAN_POINT('Ctrl Pts',(-138.376829898178,4.32695552820875,
133.146453824377));
#109044=CARTESIAN_POINT('Ctrl Pts',(-138.384594651125,4.3887787812045,133.024226350476));
#109045=CARTESIAN_POINT('Ctrl Pts',(-138.39235169201,4.45054063047365,132.902120274626));
#109046=CARTESIAN_POINT('Ctrl Pts',(-138.400108732895,4.5072672579379,132.777307073021));
#109047=CARTESIAN_POINT('Ctrl Pts',(-138.40786577378,4.55871765052375,132.650241557742));
#109048=CARTESIAN_POINT('Ctrl Pts',(-138.41561696502,4.6101292439684,132.523271863556));
#109049=CARTESIAN_POINT('Ctrl Pts',(-138.42336815626,4.65627237605335,132.39405359735));
#109050=CARTESIAN_POINT('Ctrl Pts',(-138.4311193475,4.69695295839971,132.263064140932));
#109051=CARTESIAN_POINT('Ctrl Pts',(-138.438867244277,4.73761625041343,
132.132130358527));
#109052=CARTESIAN_POINT('Ctrl Pts',(-138.446615141054,4.77282149471763,
131.999427255769));
#109053=CARTESIAN_POINT('Ctrl Pts',(-138.454363037831,4.80242362501266,
131.865449863775));
#109054=CARTESIAN_POINT('Ctrl Pts',(-138.462109313915,4.83201956318009,
131.731500496964));
#109055=CARTESIAN_POINT('Ctrl Pts',(-138.46985559,4.85601463431594,131.596277752624));
#109056=CARTESIAN_POINT('Ctrl Pts',(-138.477601866084,4.87431441153392,
131.460289028304));
#109057=CARTESIAN_POINT('Ctrl Pts',(-138.485348199349,4.89261432383673,
131.324299300145));
#109058=CARTESIAN_POINT('Ctrl Pts',(-138.493094532614,4.90521880618959,
131.187543968198));
#109059=CARTESIAN_POINT('Ctrl Pts',(-138.50084086588,4.91208510406753,131.050537368901));
#109060=CARTESIAN_POINT('Ctrl Pts',(-138.508588933883,4.91895293960527,
130.913500087926));
#109061=CARTESIAN_POINT('Ctrl Pts',(-138.516337001886,4.92008001404833,
130.776211818033));
#109062=CARTESIAN_POINT('Ctrl Pts',(-138.524085069889,4.91547568164379,
130.639188326704));
#109063=CARTESIAN_POINT('Ctrl Pts',(-138.53184137263,4.91086645569998,130.502019205178));
#109064=CARTESIAN_POINT('Ctrl Pts',(-138.539597675372,4.90051366781708,
130.365115815729));
#109065=CARTESIAN_POINT('Ctrl Pts',(-138.547353978114,4.88447874615702,
130.228990787943));
#109066=CARTESIAN_POINT('Ctrl Pts',(-138.555114420628,4.86843526617642,
130.09279310613));
#109067=CARTESIAN_POINT('Ctrl Pts',(-138.562874863143,4.84670367137383,
129.957374999607));
#109068=CARTESIAN_POINT('Ctrl Pts',(-138.570635305657,4.81939665015872,
129.823239324892));
#109069=CARTESIAN_POINT('Ctrl Pts',(-138.578408205922,4.79204579328902,
129.688888323684));
#109070=CARTESIAN_POINT('Ctrl Pts',(-138.586181106188,4.75910171872897,
129.555824247897));
#109071=CARTESIAN_POINT('Ctrl Pts',(-138.593954006453,4.72072741022136,
129.424536070428));
#109072=CARTESIAN_POINT('Ctrl Pts',(-138.601444342215,4.68374810448736,
129.298020548906));
#109073=CARTESIAN_POINT('Ctrl Pts',(-138.608934677977,4.64172661401346,
129.173154342537));
#109074=CARTESIAN_POINT('Ctrl Pts',(-138.616425013739,4.59485046856075,
129.050355989845));
#109075=CARTESIAN_POINT('Ctrl Pts',(-138.624199347858,4.54619699980529,
128.922901700287));
#109076=CARTESIAN_POINT('Ctrl Pts',(-138.631973681977,4.49215936104726,
128.797271428259));
#109077=CARTESIAN_POINT('Ctrl Pts',(-138.639748016096,4.43289397002839,
128.67395358768));
#109078=CARTESIAN_POINT('Ctrl Pts',(-138.647512769043,4.3737016183071,128.550787725319));
#109079=CARTESIAN_POINT('Ctrl Pts',(-138.65527752199,4.30929450117831,128.429928973024));
#109080=CARTESIAN_POINT('Ctrl Pts',(-138.663042274938,4.23987804408487,
128.311848384138));
#109081=CARTESIAN_POINT('Ctrl Pts',(-138.670799315822,4.1705305323954,128.193885074558));
#109082=CARTESIAN_POINT('Ctrl Pts',(-138.678556356707,4.09618377876101,
128.078694772092));
#109083=CARTESIAN_POINT('Ctrl Pts',(-138.686313397592,4.01709015601284,
127.966726084902));
#109084=CARTESIAN_POINT('Ctrl Pts',(-138.694064588833,3.93805617838074,
127.854841834171));
#109085=CARTESIAN_POINT('Ctrl Pts',(-138.701815780073,3.85428268137157,
127.746174681091));
#109086=CARTESIAN_POINT('Ctrl Pts',(-138.709566971313,3.76606639030969,
127.64114595424));
#109087=CARTESIAN_POINT('Ctrl Pts',(-138.71731486809,3.67788759352464,127.5361618674));
#109088=CARTESIAN_POINT('Ctrl Pts',(-138.725062764867,3.5852700093097,127.434813429808));
#109089=CARTESIAN_POINT('Ctrl Pts',(-138.732810661644,3.48855170948563,
127.337490266263));
#109090=CARTESIAN_POINT('Ctrl Pts',(-138.740556937728,3.39185364104515,
127.240187460626));
#109091=CARTESIAN_POINT('Ctrl Pts',(-138.748303213812,3.29105683858605,
127.146908531388));
#109092=CARTESIAN_POINT('Ctrl Pts',(-138.756049489896,3.18653714999846,
127.058007183334));
#109093=CARTESIAN_POINT('Ctrl Pts',(-138.763795823162,3.08201668987014,
126.96910517903));
#109094=CARTESIAN_POINT('Ctrl Pts',(-138.771542156427,2.97377358658391,
126.884581073697));
#109095=CARTESIAN_POINT('Ctrl Pts',(-138.779288489692,2.86221745608935,
126.804748849337));
#109096=CARTESIAN_POINT('Ctrl Pts',(-138.787036557695,2.750636343373,126.724898747104));
#109097=CARTESIAN_POINT('Ctrl Pts',(-138.794784625698,2.63574104497385,
126.649742844125));
#109098=CARTESIAN_POINT('Ctrl Pts',(-138.802532693701,2.51797054688072,
126.57955205533));
#109099=CARTESIAN_POINT('Ctrl Pts',(-138.810288996443,2.40007488090058,
126.50928666693));
#109100=CARTESIAN_POINT('Ctrl Pts',(-138.818045299185,2.27929824732104,
126.443997134534));
#109101=CARTESIAN_POINT('Ctrl Pts',(-138.825801601927,2.15610513935181,
126.383908865702));
#109102=CARTESIAN_POINT('Ctrl Pts',(-138.833562044441,2.03284627951158,
126.323788525951));
#109103=CARTESIAN_POINT('Ctrl Pts',(-138.841322486955,1.90716873343941,
126.268875137782));
#109104=CARTESIAN_POINT('Ctrl Pts',(-138.849082929469,1.77955647940521,
126.219345699476));
#109105=CARTESIAN_POINT('Ctrl Pts',(-138.856855829735,1.65173937085196,
126.169736752119));
#109106=CARTESIAN_POINT('Ctrl Pts',(-138.86462873,1.5219817183185,126.125529151837));
#109107=CARTESIAN_POINT('Ctrl Pts',(-138.872401630265,1.39078300524743,
126.086850077587));
#109108=CARTESIAN_POINT('Ctrl Pts',(-138.879891966028,1.26435369586256,
126.049577085112));
#109109=CARTESIAN_POINT('Ctrl Pts',(-138.88738230179,1.13658657801167,126.017437720587));
#109110=CARTESIAN_POINT('Ctrl Pts',(-138.894872637552,1.00793514442725,
125.990500440211));
#109111=CARTESIAN_POINT('Ctrl Pts',(-138.902646971671,0.87440585263892,
125.962541824662));
#109112=CARTESIAN_POINT('Ctrl Pts',(-138.91042130579,0.739500883055925,
125.940098989853));
#109113=CARTESIAN_POINT('Ctrl Pts',(-138.918195639909,0.603715699750552,
125.923304336762));
#109114=CARTESIAN_POINT('Ctrl Pts',(-138.925960392856,0.468097859548501,
125.90653038158));
#109115=CARTESIAN_POINT('Ctrl Pts',(-138.933725145803,0.331602348306135,
125.89539080557));
#109116=CARTESIAN_POINT('Ctrl Pts',(-138.94148989875,0.194736514010293,
125.889967394328));
#109117=CARTESIAN_POINT('Ctrl Pts',(-138.949246939635,0.0580066167901712,
125.884549369693));
#109118=CARTESIAN_POINT('Ctrl Pts',(-138.957003980521,-0.0790924833940932,
125.884836226973));
#109119=CARTESIAN_POINT('Ctrl Pts',(-138.964761021406,-0.216046946109414,
125.890858121426));
#109120=CARTESIAN_POINT('Ctrl Pts',(-138.972512212646,-0.352898130398864,
125.896875474721));
#109121=CARTESIAN_POINT('Ctrl Pts',(-138.980263403886,-0.489604505313652,
125.908619239761));
#109122=CARTESIAN_POINT('Ctrl Pts',(-138.988014595126,-0.625651207903403,
125.926067511515));
#109123=CARTESIAN_POINT('Ctrl Pts',(-138.995762491903,-0.761640087015575,
125.943508367287));
#109124=CARTESIAN_POINT('Ctrl Pts',(-139.00351038868,-0.896969464476789,
125.966648857862));
#109125=CARTESIAN_POINT('Ctrl Pts',(-139.011258285457,-1.03112880183341,
125.995415155562));
#109126=CARTESIAN_POINT('Ctrl Pts',(-139.019004561541,-1.1652600759488,
126.024175435973));
#109127=CARTESIAN_POINT('Ctrl Pts',(-139.026750837625,-1.29822141474103,
126.058559100878));
#109128=CARTESIAN_POINT('Ctrl Pts',(-139.03449711371,-1.42951208139341,
126.098441124879));
#109129=CARTESIAN_POINT('Ctrl Pts',(-139.042243446975,-1.56080371720383,
126.13832344328));
#109130=CARTESIAN_POINT('Ctrl Pts',(-139.04998978024,-1.69042428217927,
126.18370408813));
#109131=CARTESIAN_POINT('Ctrl Pts',(-139.057736113506,-1.81788820694238,
126.234408152872));
#109132=CARTESIAN_POINT('Ctrl Pts',(-139.065484181509,-1.94538067636714,
126.285123572438));
#109133=CARTESIAN_POINT('Ctrl Pts',(-139.073232249512,-2.07071518132734,
126.34116463964));
#109134=CARTESIAN_POINT('Ctrl Pts',(-139.080980317515,-2.1934265107705,
126.402308459271));
#109135=CARTESIAN_POINT('Ctrl Pts',(-139.088736620256,-2.31626825927505,
126.463517263281));
#109136=CARTESIAN_POINT('Ctrl Pts',(-139.096492922998,-2.43648091255858,
126.529839478638));
#109137=CARTESIAN_POINT('Ctrl Pts',(-139.10424922574,-2.55362375893157,
126.601006152342));
#109138=CARTESIAN_POINT('Ctrl Pts',(-139.112009668254,-2.67082912796878,
126.672210809842));
#109139=CARTESIAN_POINT('Ctrl Pts',(-139.119770110768,-2.78496110016019,
126.748264861086));
#109140=CARTESIAN_POINT('Ctrl Pts',(-139.127530553283,-2.89560915976181,
126.828856793344));
#109141=CARTESIAN_POINT('Ctrl Pts',(-139.135303453548,-3.00643484145187,
126.909578098926));
#109142=CARTESIAN_POINT('Ctrl Pts',(-139.143076353813,-3.11376512829503,
126.994851599148));
#109143=CARTESIAN_POINT('Ctrl Pts',(-139.150849254079,-3.21722303803153,
127.084325807775));
#109144=CARTESIAN_POINT('Ctrl Pts',(-139.158339589841,-3.31691999215239,
127.170547403544));
#109145=CARTESIAN_POINT('Ctrl Pts',(-139.165829925603,-3.41302099784068,
127.260669386768));
#109146=CARTESIAN_POINT('Ctrl Pts',(-139.173320261364,-3.50522333705938,
127.354347223413));
#109147=CARTESIAN_POINT('Ctrl Pts',(-139.180988868259,-3.59962010600881,
127.450254606853));
#109148=CARTESIAN_POINT('Ctrl Pts',(-139.188657475154,-3.69024688647966,
127.550211228781));
#109149=CARTESIAN_POINT('Ctrl Pts',(-139.196326082049,-3.77672901587722,
127.653884303875));
#109150=CARTESIAN_POINT('Ctrl Pts',(-139.203985690251,-3.86310966319121,
127.757435724243));
#109151=CARTESIAN_POINT('Ctrl Pts',(-139.211645298452,-3.94535507353085,
127.864694621992));
#109152=CARTESIAN_POINT('Ctrl Pts',(-139.219304906653,-4.02312619691822,
127.975290334563));
#109153=CARTESIAN_POINT('Ctrl Pts',(-139.226957293971,-4.10082400374231,
128.085781786103));
#109154=CARTESIAN_POINT('Ctrl Pts',(-139.23460968129,-4.1740556816684,128.199603469983));
#109155=CARTESIAN_POINT('Ctrl Pts',(-139.242262068609,-4.24252174968882,
128.316350917843));
#109156=CARTESIAN_POINT('Ctrl Pts',(-139.249908628741,-4.31093568174997,
128.433009464143));
#109157=CARTESIAN_POINT('Ctrl Pts',(-139.257555188873,-4.3745910227568,
128.552588995038));
#109158=CARTESIAN_POINT('Ctrl Pts',(-139.265201749005,-4.43323137458916,
128.674655792512));
#109159=CARTESIAN_POINT('Ctrl Pts',(-139.272844955505,-4.49184600791408,
128.796669053885));
#109160=CARTESIAN_POINT('Ctrl Pts',(-139.280488162006,-4.54544985390176,
128.921167049584));
#109161=CARTESIAN_POINT('Ctrl Pts',(-139.288131368507,-4.59383247771545,
129.047691545377));
#109162=CARTESIAN_POINT('Ctrl Pts',(-139.29577369175,-4.64220951038032,
129.17420141986));
#109163=CARTESIAN_POINT('Ctrl Pts',(-139.303416014994,-4.6853663742553,
129.302736954155));
#109164=CARTESIAN_POINT('Ctrl Pts',(-139.311058338237,-4.72314095957784,
129.432820410916));
#109165=CARTESIAN_POINT('Ctrl Pts',(-139.313976621525,-4.73756549221534,
129.482493836888));
#109166=CARTESIAN_POINT('Ctrl Pts',(-139.316894904813,-4.75120571705062,
129.532392799512));
#109167=CARTESIAN_POINT('Ctrl Pts',(-139.319813188101,-4.76405452823411,
129.582490119308));
#109168=CARTESIAN_POINT('Origin',(213.235140564004,0.,130.804360617566));
#109169=CARTESIAN_POINT('',(-141.415385046285,-4.76405452823413,129.582490119309));
#109170=CARTESIAN_POINT('',(-141.069766537825,-4.76405452823392,129.582490119308));
#109171=CARTESIAN_POINT('',(213.235140564004,-4.76405452823405,129.582490119308));
#109172=CARTESIAN_POINT('',(-139.735140564048,-4.91824935081372,130.801833619268));
#109173=CARTESIAN_POINT('Ctrl Pts',(-139.735140564048,-4.91824935081372,
130.801833619268));
#109174=CARTESIAN_POINT('Ctrl Pts',(-139.742821053676,-4.91831868187791,
130.936771368003));
#109175=CARTESIAN_POINT('Ctrl Pts',(-139.750501543305,-4.9128305693135,
131.071935030579));
#109176=CARTESIAN_POINT('Ctrl Pts',(-139.758182032933,-4.90175557619006,
131.206822210503));
#109177=CARTESIAN_POINT('Ctrl Pts',(-139.765853728862,-4.89069326326819,
131.341554952713));
#109178=CARTESIAN_POINT('Ctrl Pts',(-139.773525424791,-4.87405682454765,
131.476011445941));
#109179=CARTESIAN_POINT('Ctrl Pts',(-139.78119712072,-4.85186881855777,
131.609687898866));
#109180=CARTESIAN_POINT('Ctrl Pts',(-139.788861972103,-4.82970060830019,
131.74324508811));
#109181=CARTESIAN_POINT('Ctrl Pts',(-139.796526823485,-4.8019907490666,
131.876023228245));
#109182=CARTESIAN_POINT('Ctrl Pts',(-139.804191674868,-4.76881368250428,
132.007522752966));
#109183=CARTESIAN_POINT('Ctrl Pts',(-139.811895110775,-4.73546960404813,
132.139684240511));
#109184=CARTESIAN_POINT('Ctrl Pts',(-139.819598546683,-4.69660315285988,
132.27055379557));
#109185=CARTESIAN_POINT('Ctrl Pts',(-139.82730198259,-4.65234222047004,
132.399633298374));
#109186=CARTESIAN_POINT('Ctrl Pts',(-139.834959909155,-4.60834276697728,
132.52795024232));
#109187=CARTESIAN_POINT('Ctrl Pts',(-139.84261783572,-4.55901254032337,
132.654497847047));
#109188=CARTESIAN_POINT('Ctrl Pts',(-139.850275762285,-4.5045272934658,
132.778801532084));
#109189=CARTESIAN_POINT('Ctrl Pts',(-139.85793307981,-4.45004637985369,
132.903095331171));
#109190=CARTESIAN_POINT('Ctrl Pts',(-139.865590397335,-4.3904114222263,
133.025145198277));
#109191=CARTESIAN_POINT('Ctrl Pts',(-139.873247714861,-4.32584610092109,
133.144497060948));
#109192=CARTESIAN_POINT('Ctrl Pts',(-139.880906174034,-4.26127115341642,
133.263866718077));
#109193=CARTESIAN_POINT('Ctrl Pts',(-139.888564633207,-4.19176457141299,
133.380537218349));
#109194=CARTESIAN_POINT('Ctrl Pts',(-139.89622309238,-4.11759545269744,
133.494080073276));
#109195=CARTESIAN_POINT('Ctrl Pts',(-139.903960679402,-4.04266001236714,
133.608796062594));
#109196=CARTESIAN_POINT('Ctrl Pts',(-139.911698266424,-3.96296536702992,
133.720319057401));
#109197=CARTESIAN_POINT('Ctrl Pts',(-139.919435853446,-3.87883256599563,
133.828239085275));
#109198=CARTESIAN_POINT('Ctrl Pts',(-139.927105762205,-3.79543564836133,
133.935215170285));
#109199=CARTESIAN_POINT('Ctrl Pts',(-139.934775670964,-3.707678215686,134.038650802036));
#109200=CARTESIAN_POINT('Ctrl Pts',(-139.942445579722,-3.61591141374249,
134.138182405015));
#109201=CARTESIAN_POINT('Ctrl Pts',(-139.950217005876,-3.5229300045667,
134.239031388596));
#109202=CARTESIAN_POINT('Ctrl Pts',(-139.957988432029,-3.42583264137427,
134.335871962731));
#109203=CARTESIAN_POINT('Ctrl Pts',(-139.965759858183,-3.32501996462775,
134.428367419067));
#109204=CARTESIAN_POINT('Ctrl Pts',(-139.973531284336,-3.22420728788096,
134.520862875403));
#109205=CARTESIAN_POINT('Ctrl Pts',(-139.981302710489,-3.11967966202699,
134.609012993809));
#109206=CARTESIAN_POINT('Ctrl Pts',(-139.989074136643,-3.01186809004675,
134.692526466737));
#109207=CARTESIAN_POINT('Ctrl Pts',(-139.996848470762,-2.90401617639166,
134.77607118931));
#109208=CARTESIAN_POINT('Ctrl Pts',(-140.004622804881,-2.79251468992268,
134.855257363404));
#109209=CARTESIAN_POINT('Ctrl Pts',(-140.012397139,-2.6777512830939,134.929749220884));
#109210=CARTESIAN_POINT('Ctrl Pts',(-140.020161891947,-2.56312931190734,
135.004149273808));
#109211=CARTESIAN_POINT('Ctrl Pts',(-140.027926644894,-2.44525374380347,
135.073866310372));
#109212=CARTESIAN_POINT('Ctrl Pts',(-140.035691397842,-2.32454505600209,
135.138604882154));
#109213=CARTESIAN_POINT('Ctrl Pts',(-140.043448438727,-2.20395625777112,
135.203279154674));
#109214=CARTESIAN_POINT('Ctrl Pts',(-140.051205479612,-2.08054028193099,
135.262984618963));
#109215=CARTESIAN_POINT('Ctrl Pts',(-140.058962520497,-1.95474602593855,
135.317469417116));
#109216=CARTESIAN_POINT('Ctrl Pts',(-140.066713711737,-1.82904663237326,
135.371913127859));
#109217=CARTESIAN_POINT('Ctrl Pts',(-140.074464902977,-1.70097288577576,
135.421143853958));
#109218=CARTESIAN_POINT('Ctrl Pts',(-140.082216094217,-1.57099737289253,
135.464956107079));
#109219=CARTESIAN_POINT('Ctrl Pts',(-140.089963990994,-1.44107710306931,
135.508749738823));
#109220=CARTESIAN_POINT('Ctrl Pts',(-140.097711887771,-1.30925704431813,
135.547129353451));
#109221=CARTESIAN_POINT('Ctrl Pts',(-140.105459784548,-1.17602860400855,
135.579938047056));
#109222=CARTESIAN_POINT('Ctrl Pts',(-140.113206060632,-1.04282803221661,
135.61273987779));
#109223=CARTESIAN_POINT('Ctrl Pts',(-140.120952336717,-0.908220044231184,
135.639973011953));
#109224=CARTESIAN_POINT('Ctrl Pts',(-140.128698612801,-0.772709625498943,
135.661530873709));
#109225=CARTESIAN_POINT('Ctrl Pts',(-140.136444946066,-0.63719820645939,
135.683088894601));
#109226=CARTESIAN_POINT('Ctrl Pts',(-140.144191279331,-0.500784729490214,
135.698971498066));
#109227=CARTESIAN_POINT('Ctrl Pts',(-140.151937612597,-0.363982356925633,
135.709123599235));
#109228=CARTESIAN_POINT('Ctrl Pts',(-140.1596856806,-0.227149348418796,
135.719277973896));
#109229=CARTESIAN_POINT('Ctrl Pts',(-140.167433748603,-0.089927660835064,
135.723699263702));
#109230=CARTESIAN_POINT('Ctrl Pts',(-140.175181816606,0.0471668623958541,
135.722384443209));
#109231=CARTESIAN_POINT('Ctrl Pts',(-140.182938119348,0.184407091317694,
135.721068225309));
#109232=CARTESIAN_POINT('Ctrl Pts',(-140.190694422089,0.321519494335863,
135.714003722636));
#109233=CARTESIAN_POINT('Ctrl Pts',(-140.198450724831,0.457990115384167,
135.701240043967));
#109234=CARTESIAN_POINT('Ctrl Pts',(-140.206211167346,0.594533574912346,
135.688469552938));
#109235=CARTESIAN_POINT('Ctrl Pts',(-140.21397160986,0.730434182721979,
135.669993877467));
#109236=CARTESIAN_POINT('Ctrl Pts',(-140.221732052374,0.865186522892068,
135.64591360634));
#109237=CARTESIAN_POINT('Ctrl Pts',(-140.229504952639,1.00015517948135,
135.621794679424));
#109238=CARTESIAN_POINT('Ctrl Pts',(-140.237277852905,1.13397150305589,
135.592053262865));
#109239=CARTESIAN_POINT('Ctrl Pts',(-140.24505075317,1.26614275036817,135.556840559469));
#109240=CARTESIAN_POINT('Ctrl Pts',(-140.252541088933,1.39350923992966,
135.522907926534));
#109241=CARTESIAN_POINT('Ctrl Pts',(-140.260031424695,1.51934788783213,
135.483894981868));
#109242=CARTESIAN_POINT('Ctrl Pts',(-140.267521760458,1.64323577588066,
135.439979157455));
#109243=CARTESIAN_POINT('Ctrl Pts',(-140.275296094577,1.77182091085091,
135.394398251216));
#109244=CARTESIAN_POINT('Ctrl Pts',(-140.283070428696,1.89871175879676,
135.34339095409));
#109245=CARTESIAN_POINT('Ctrl Pts',(-140.290844762815,2.02341629285639,
135.287101918188));
#109246=CARTESIAN_POINT('Ctrl Pts',(-140.298609515762,2.14796713972295,
135.230882253492));
#109247=CARTESIAN_POINT('Ctrl Pts',(-140.306374268709,2.27033668090424,
135.169393960832));
#109248=CARTESIAN_POINT('Ctrl Pts',(-140.314139021656,2.3900490690662,135.102831102512));
#109249=CARTESIAN_POINT('Ctrl Pts',(-140.321896062541,2.50964255719625,
135.036334355362));
#109250=CARTESIAN_POINT('Ctrl Pts',(-140.329653103427,2.62658380479242,
134.9647732614));
#109251=CARTESIAN_POINT('Ctrl Pts',(-140.337410144312,2.74041827662706,
134.888389355421));
#109252=CARTESIAN_POINT('Ctrl Pts',(-140.345161335552,2.85416690500176,
134.81206305114));
#109253=CARTESIAN_POINT('Ctrl Pts',(-140.352912526792,2.96481309756629,
134.730921390873));
#109254=CARTESIAN_POINT('Ctrl Pts',(-140.360663718032,3.07192852648603,
134.645250903771));
#109255=CARTESIAN_POINT('Ctrl Pts',(-140.368411614809,3.17899842849065,
134.559616828911));
#109256=CARTESIAN_POINT('Ctrl Pts',(-140.376159511586,3.28254024688251,
134.469457999325));
#109257=CARTESIAN_POINT('Ctrl Pts',(-140.383907408363,3.38215635627519,
134.375103039557));
#109258=CARTESIAN_POINT('Ctrl Pts',(-140.391653684448,3.48175162812526,
134.280767816812));
#109259=CARTESIAN_POINT('Ctrl Pts',(-140.399399960532,3.57742254066734,
134.182238478445));
#109260=CARTESIAN_POINT('Ctrl Pts',(-140.407146236616,3.66880647166351,
134.079882276169));
#109261=CARTESIAN_POINT('Ctrl Pts',(-140.414892569881,3.76019107723546,
133.977525318324));
#109262=CARTESIAN_POINT('Ctrl Pts',(-140.422638903146,3.8472883777349,133.871341731845));
#109263=CARTESIAN_POINT('Ctrl Pts',(-140.430385236412,3.92977465192497,
133.761733480021));
#109264=CARTESIAN_POINT('Ctrl Pts',(-140.438133304415,4.01227939834366,
133.652100682191));
#109265=CARTESIAN_POINT('Ctrl Pts',(-140.445881372418,4.09017082863923,
133.539042005242));
#109266=CARTESIAN_POINT('Ctrl Pts',(-140.453629440421,4.16316757144591,
133.422989807536));
#109267=CARTESIAN_POINT('Ctrl Pts',(-140.461385743163,4.23624189605981,
133.306814268172));
#109268=CARTESIAN_POINT('Ctrl Pts',(-140.469142045905,4.30441093287157,
133.187639184032));
#109269=CARTESIAN_POINT('Ctrl Pts',(-140.476898348647,4.36743819267706,
133.065923505404));
#109270=CARTESIAN_POINT('Ctrl Pts',(-140.484658791161,4.43049909202883,
132.944142863453));
#109271=CARTESIAN_POINT('Ctrl Pts',(-140.492419233675,4.48841258107316,
132.819819279311));
#109272=CARTESIAN_POINT('Ctrl Pts',(-140.500179676189,4.5409900983555,132.693432344404));
#109273=CARTESIAN_POINT('Ctrl Pts',(-140.507952576455,4.59365201773618,
132.566842521968));
#109274=CARTESIAN_POINT('Ctrl Pts',(-140.51572547672,4.64096071320081,132.438183096945));
#109275=CARTESIAN_POINT('Ctrl Pts',(-140.523498376985,4.68277705619129,
132.307950356992));
#109276=CARTESIAN_POINT('Ctrl Pts',(-140.530988712747,4.72307326978234,
132.182451905182));
#109277=CARTESIAN_POINT('Ctrl Pts',(-140.538479048509,4.75826943749636,
132.055492837246));
#109278=CARTESIAN_POINT('Ctrl Pts',(-140.54596938427,4.78828624027411,131.927524872562));
#109279=CARTESIAN_POINT('Ctrl Pts',(-140.553743718389,4.81944113925448,
131.794704963594));
#109280=CARTESIAN_POINT('Ctrl Pts',(-140.561518052508,4.84511485837714,
131.660377409464));
#109281=CARTESIAN_POINT('Ctrl Pts',(-140.569292386627,4.86516314502173,
131.525034354303));
#109282=CARTESIAN_POINT('Ctrl Pts',(-140.577057139574,4.88518672394474,
131.389858097362));
#109283=CARTESIAN_POINT('Ctrl Pts',(-140.584821892521,4.89959860794207,
131.253669212564));
#109284=CARTESIAN_POINT('Ctrl Pts',(-140.592586645469,4.90830486001895,
131.116972939163));
#109285=CARTESIAN_POINT('Ctrl Pts',(-140.600343686353,4.91700246492351,
130.980412434428));
#109286=CARTESIAN_POINT('Ctrl Pts',(-140.608100727239,4.92000569063275,
130.843345931615));
#109287=CARTESIAN_POINT('Ctrl Pts',(-140.615857768123,4.91727205981716,
130.70628639954));
#109288=CARTESIAN_POINT('Ctrl Pts',(-140.623608959364,4.91454049045383,
130.569330225123));
#109289=CARTESIAN_POINT('Ctrl Pts',(-140.631360150604,4.90608068338522,
130.432381400288));
#109290=CARTESIAN_POINT('Ctrl Pts',(-140.639111341844,4.89190218204362,
130.295955165376));
#109291=CARTESIAN_POINT('Ctrl Pts',(-140.646859238621,4.8777297069433,130.159586915253));
#109292=CARTESIAN_POINT('Ctrl Pts',(-140.654607135398,4.85784341217327,
130.023741201341));
#109293=CARTESIAN_POINT('Ctrl Pts',(-140.662355032175,4.83230485263528,
129.888930186732));
#109294=CARTESIAN_POINT('Ctrl Pts',(-140.670101308259,4.8067716352134,129.754147371681));
#109295=CARTESIAN_POINT('Ctrl Pts',(-140.677847584343,4.77558857747059,
129.620399209318));
#109296=CARTESIAN_POINT('Ctrl Pts',(-140.685593860427,4.73886865249923,
129.488189292525));
#109297=CARTESIAN_POINT('Ctrl Pts',(-140.693340193692,4.70214845646967,
129.355978399788));
#109298=CARTESIAN_POINT('Ctrl Pts',(-140.701086526958,4.65989141628072,
129.225306151985));
#109299=CARTESIAN_POINT('Ctrl Pts',(-140.708832860223,4.6122607357949,129.096662175936));
#109300=CARTESIAN_POINT('Ctrl Pts',(-140.716580928226,4.56461938874837,
128.967989390961));
#109301=CARTESIAN_POINT('Ctrl Pts',(-140.724328996229,4.51160214252286,
128.84134614815));
#109302=CARTESIAN_POINT('Ctrl Pts',(-140.732077064232,4.45342066435591,
128.717202873459));
#109303=CARTESIAN_POINT('Ctrl Pts',(-140.739833366974,4.39517735022184,
128.592927657818));
#109304=CARTESIAN_POINT('Ctrl Pts',(-140.747589669715,4.33175900624082,
128.47115807251));
#109305=CARTESIAN_POINT('Ctrl Pts',(-140.755345972457,4.26342393209622,
128.352341156442));
#109306=CARTESIAN_POINT('Ctrl Pts',(-140.763106414971,4.19505238546502,
128.233460824209));
#109307=CARTESIAN_POINT('Ctrl Pts',(-140.770866857486,4.12175908854517,
128.11753663168));
#109308=CARTESIAN_POINT('Ctrl Pts',(-140.7786273,4.04384561311353,128.004986451828));
#109309=CARTESIAN_POINT('Ctrl Pts',(-140.786400200265,3.96580706405408,
127.892255596435));
#109310=CARTESIAN_POINT('Ctrl Pts',(-140.794173100531,3.88313375143666,
127.782909889182));
#109311=CARTESIAN_POINT('Ctrl Pts',(-140.801946000796,3.79616801374068,
127.677334638468));
#109312=CARTESIAN_POINT('Ctrl Pts',(-140.809436336558,3.71236369966012,
127.575597314042));
#109313=CARTESIAN_POINT('Ctrl Pts',(-140.816926672321,3.6245738284932,127.477361303959));
#109314=CARTESIAN_POINT('Ctrl Pts',(-140.824417008083,3.53313557065684,
127.38293750695));
#109315=CARTESIAN_POINT('Ctrl Pts',(-140.832191342202,3.43823040348566,
127.28493360298));
#109316=CARTESIAN_POINT('Ctrl Pts',(-140.839965676321,3.33909410014207,
127.190726251824));
#109317=CARTESIAN_POINT('Ctrl Pts',(-140.84774001044,3.23606274335815,127.10070283322));
#109318=CARTESIAN_POINT('Ctrl Pts',(-140.855504763387,3.13315836351357,
127.010790360434));
#109319=CARTESIAN_POINT('Ctrl Pts',(-140.863269516334,3.02636877299296,
126.925051815429));
#109320=CARTESIAN_POINT('Ctrl Pts',(-140.871034269281,2.91606826864997,
126.843839324217));
#109321=CARTESIAN_POINT('Ctrl Pts',(-140.878791310166,2.80587731632346,
126.762707494396));
#109322=CARTESIAN_POINT('Ctrl Pts',(-140.886548351051,2.69218270243471,
126.686093002745));
#109323=CARTESIAN_POINT('Ctrl Pts',(-140.894305391936,2.57539304214305,
126.614308858819));
#109324=CARTESIAN_POINT('Ctrl Pts',(-140.902056583176,2.45869145384224,
126.542578847873));
#109325=CARTESIAN_POINT('Ctrl Pts',(-140.909807774417,2.3388997965521,126.475672138169));
#109326=CARTESIAN_POINT('Ctrl Pts',(-140.917558965657,2.21645671502376,
126.413859200538));
#109327=CARTESIAN_POINT('Ctrl Pts',(-140.925306862434,2.09406567507118,
126.352072535054));
#109328=CARTESIAN_POINT('Ctrl Pts',(-140.933054759211,1.96902580053268,
126.295375511467));
#109329=CARTESIAN_POINT('Ctrl Pts',(-140.940802655988,1.84180126065065,
126.243993178558));
#109330=CARTESIAN_POINT('Ctrl Pts',(-140.948548932072,1.71460333339936,
126.192621593725));
#109331=CARTESIAN_POINT('Ctrl Pts',(-140.956295208156,1.58522201205899,
126.146562634616));
#109332=CARTESIAN_POINT('Ctrl Pts',(-140.96404148424,1.45414204829938,126.105993458023));
#109333=CARTESIAN_POINT('Ctrl Pts',(-140.971787817506,1.32306111693744,
126.065423981958));
#109334=CARTESIAN_POINT('Ctrl Pts',(-140.979534150771,1.19028189162174,
126.030344484867));
#109335=CARTESIAN_POINT('Ctrl Pts',(-140.987280484036,1.05630452493746,
126.000882313972));
#109336=CARTESIAN_POINT('Ctrl Pts',(-140.995028552039,0.922297154951022,
125.971413545229));
#109337=CARTESIAN_POINT('Ctrl Pts',(-141.002776620042,0.787091491447936,
125.947564689833));
#109338=CARTESIAN_POINT('Ctrl Pts',(-141.010524688045,0.65119772841829,
125.929411942862));
#109339=CARTESIAN_POINT('Ctrl Pts',(-141.018280990787,0.515159535880326,
125.911239902935));
#109340=CARTESIAN_POINT('Ctrl Pts',(-141.026037293529,0.37843217106558,
125.898776116581));
#109341=CARTESIAN_POINT('Ctrl Pts',(-141.033793596271,0.241531357754565,
125.89204490441));
#109342=CARTESIAN_POINT('Ctrl Pts',(-141.041554038785,0.104557476357109,
125.885310099588));
#109343=CARTESIAN_POINT('Ctrl Pts',(-141.049314481299,-0.0325896472359078,
125.884313968394));
#109344=CARTESIAN_POINT('Ctrl Pts',(-141.057074923813,-0.16939543774653,
125.889028660498));
#109345=CARTESIAN_POINT('Ctrl Pts',(-141.064847824079,-0.306420841057127,
125.893750921045));
#109346=CARTESIAN_POINT('Ctrl Pts',(-141.072620724344,-0.443103426278679,
125.904202294694));
#109347=CARTESIAN_POINT('Ctrl Pts',(-141.08039362461,-0.578933980232691,
125.920303030986));
#109348=CARTESIAN_POINT('Ctrl Pts',(-141.087883960372,-0.709826751410281,
125.935818464958));
#109349=CARTESIAN_POINT('Ctrl Pts',(-141.095374296134,-0.839928058625539,
125.956579606911));
#109350=CARTESIAN_POINT('Ctrl Pts',(-141.102864631895,-0.968794085126929,
125.98247083418));
#109351=CARTESIAN_POINT('Ctrl Pts',(-141.110638966015,-1.10254610619467,
126.009343735201));
#109352=CARTESIAN_POINT('Ctrl Pts',(-141.118413300134,-1.23539101230949,
126.041828540447));
#109353=CARTESIAN_POINT('Ctrl Pts',(-141.126187634253,-1.36682122899911,
126.07985188221));
#109354=CARTESIAN_POINT('Ctrl Pts',(-141.1339523872,-1.49808946969184,126.117828363601));
#109355=CARTESIAN_POINT('Ctrl Pts',(-141.141717140147,-1.62794611800273,
126.161329692689));
#109356=CARTESIAN_POINT('Ctrl Pts',(-141.149481893094,-1.7558926037528,
126.210231295639));
#109357=CARTESIAN_POINT('Ctrl Pts',(-141.157238933979,-1.88371201125019,
126.259084328829));
#109358=CARTESIAN_POINT('Ctrl Pts',(-141.164995974864,-2.00962466886434,
126.313326823342));
#109359=CARTESIAN_POINT('Ctrl Pts',(-141.172753015749,-2.13314636631659,
126.372784188983));
#109360=CARTESIAN_POINT('Ctrl Pts',(-141.180504206989,-2.25657491509577,
126.432196717363));
#109361=CARTESIAN_POINT('Ctrl Pts',(-141.188255398229,-2.37761574170534,
126.496816120435));
#109362=CARTESIAN_POINT('Ctrl Pts',(-141.196006589469,-2.49580419317262,
126.566419550038));
#109363=CARTESIAN_POINT('Ctrl Pts',(-141.203754486246,-2.61394241139541,
126.635993396327));
#109364=CARTESIAN_POINT('Ctrl Pts',(-141.211502383024,-2.72923032953855,
126.710546857939));
#109365=CARTESIAN_POINT('Ctrl Pts',(-141.219250279801,-2.8412277128769,
126.789811060507));
#109366=CARTESIAN_POINT('Ctrl Pts',(-141.226996555885,-2.95320166877703,
126.869058682713));
#109367=CARTESIAN_POINT('Ctrl Pts',(-141.234742831969,-3.0618861400312,
126.953014860175));
#109368=CARTESIAN_POINT('Ctrl Pts',(-141.242489108053,-3.16687005949524,
127.041367515158));
#109369=CARTESIAN_POINT('Ctrl Pts',(-141.250235441318,-3.27185475392629,
127.129720822339));
#109370=CARTESIAN_POINT('Ctrl Pts',(-141.257981774584,-3.37313854292823,
127.222470420057));
#109371=CARTESIAN_POINT('Ctrl Pts',(-141.265728107849,-3.47034394098518,
127.319264350062));
#109372=CARTESIAN_POINT('Ctrl Pts',(-141.273476175852,-3.56757110751745,
127.416079956397));
#109373=CARTESIAN_POINT('Ctrl Pts',(-141.281224243855,-3.6607177887021,
127.516941421444));
#109374=CARTESIAN_POINT('Ctrl Pts',(-141.288972311858,-3.74944410714905,
127.621460689848));
#109375=CARTESIAN_POINT('Ctrl Pts',(-141.2967286146,-3.83826472498297,127.726091042575));
#109376=CARTESIAN_POINT('Ctrl Pts',(-141.304484917342,-3.92265534186903,
127.834386665945));
#109377=CARTESIAN_POINT('Ctrl Pts',(-141.312241220084,-4.00231673488935,
127.945926812818));
#109378=CARTESIAN_POINT('Ctrl Pts',(-141.320001662598,-4.08202064559369,
128.057526492027));
#109379=CARTESIAN_POINT('Ctrl Pts',(-141.327762105112,-4.15699008928609,
128.172373818071));
#109380=CARTESIAN_POINT('Ctrl Pts',(-141.335522547626,-4.22697035672952,
128.290020810414));
#109381=CARTESIAN_POINT('Ctrl Pts',(-141.343295447892,-4.29706296271081,
128.407856660153));
#109382=CARTESIAN_POINT('Ctrl Pts',(-141.351068348157,-4.36215020203226,
128.528500812897));
#109383=CARTESIAN_POINT('Ctrl Pts',(-141.358841248423,-4.42202392885086,
128.651481746108));
#109384=CARTESIAN_POINT('Ctrl Pts',(-141.366331584185,-4.47972109488809,
128.769992012629));
#109385=CARTESIAN_POINT('Ctrl Pts',(-141.373821919947,-4.53257709263054,
128.8906718314));
#109386=CARTESIAN_POINT('Ctrl Pts',(-141.381312255709,-4.580449304905,129.013085309944));
#109387=CARTESIAN_POINT('Ctrl Pts',(-141.390142391297,-4.63688444194875,
129.15739494406));
#109388=CARTESIAN_POINT('Ctrl Pts',(-141.398972526884,-4.68654370990747,
129.304495840899));
#109389=CARTESIAN_POINT('Ctrl Pts',(-141.407802662471,-4.7291768839033,
129.453779608054));
#109390=CARTESIAN_POINT('Ctrl Pts',(-141.410330123743,-4.74137983312049,
129.496509296201));
#109391=CARTESIAN_POINT('Ctrl Pts',(-141.412857585014,-4.75300743572739,
129.539417673288));
#109392=CARTESIAN_POINT('Ctrl Pts',(-141.415385046285,-4.76405452823413,
129.582490119309));
#109393=CARTESIAN_POINT('Ctrl Pts',(-139.665053375618,-4.76405452823406,
129.582490119308));
#109394=CARTESIAN_POINT('Ctrl Pts',(-139.672826300165,-4.79811622310555,
129.715296150654));
#109395=CARTESIAN_POINT('Ctrl Pts',(-139.680599224713,-4.82658428168376,
129.849386479152));
#109396=CARTESIAN_POINT('Ctrl Pts',(-139.68837214926,-4.84939189227845,
129.98425005331));
#109397=CARTESIAN_POINT('Ctrl Pts',(-139.69579027045,-4.8711584253778,130.112957637062));
#109398=CARTESIAN_POINT('Ctrl Pts',(-139.70320839164,-4.88776983181743,
130.242369144826));
#109399=CARTESIAN_POINT('Ctrl Pts',(-139.71062651283,-4.89921231912583,
130.372039308092));
#109400=CARTESIAN_POINT('Ctrl Pts',(-139.718797863224,-4.9118166660722,
130.514876060481));
#109401=CARTESIAN_POINT('Ctrl Pts',(-139.726969213617,-4.91817558877562,
130.658271986534));
#109402=CARTESIAN_POINT('Ctrl Pts',(-139.735140564011,-4.91824935081338,
130.80183361861));
#109403=CARTESIAN_POINT('',(-139.389859435958,-4.91824792560688,130.808877780788));
#109404=CARTESIAN_POINT('Ctrl Pts',(-139.319813188101,-4.76405452823411,
129.582490119308));
#109405=CARTESIAN_POINT('Ctrl Pts',(-139.327458232781,-4.79771463792605,
129.713730376134));
#109406=CARTESIAN_POINT('Ctrl Pts',(-139.33510327746,-4.8259397234975,129.846332558212));
#109407=CARTESIAN_POINT('Ctrl Pts',(-139.34274832214,-4.84863732766595,
129.979800657791));
#109408=CARTESIAN_POINT('Ctrl Pts',(-139.350600174443,-4.87194892923586,
130.116879229458));
#109409=CARTESIAN_POINT('Ctrl Pts',(-139.358452026746,-4.88942966397046,
130.254870788241));
#109410=CARTESIAN_POINT('Ctrl Pts',(-139.366303879049,-4.90103622311378,
130.39323168131));
#109411=CARTESIAN_POINT('Ctrl Pts',(-139.374155731352,-4.91264278225707,
130.53159257438));
#109412=CARTESIAN_POINT('Ctrl Pts',(-139.382007583655,-4.91837518180347,
130.670322343648));
#109413=CARTESIAN_POINT('Ctrl Pts',(-139.389859435958,-4.91824792560688,
130.808877780788));
#109414=CARTESIAN_POINT('Ctrl Pts',(-139.389859435993,-4.91824792560632,
130.808877781408));
#109415=CARTESIAN_POINT('Ctrl Pts',(-139.400465185153,-4.91807603654967,
130.996029061678));
#109416=CARTESIAN_POINT('Ctrl Pts',(-139.411070934312,-4.90721832858287,
131.182709389041));
#109417=CARTESIAN_POINT('Ctrl Pts',(-139.421676683472,-4.88585637864041,
131.367912309781));
#109418=CARTESIAN_POINT('Ctrl Pts',(-139.43170708404,-4.86565328769117,
131.543068204345));
#109419=CARTESIAN_POINT('Ctrl Pts',(-139.441737484609,-4.83605519733954,
131.716903404704));
#109420=CARTESIAN_POINT('Ctrl Pts',(-139.451767885177,-4.79725281147905,
131.888587773312));
#109421=CARTESIAN_POINT('Ctrl Pts',(-139.459542219296,-4.76717796947889,
132.021656401574));
#109422=CARTESIAN_POINT('Ctrl Pts',(-139.467316553416,-4.73151460760105,
132.153683505883));
#109423=CARTESIAN_POINT('Ctrl Pts',(-139.475090887535,-4.69034825281445,
132.284163418557));
#109424=CARTESIAN_POINT('Ctrl Pts',(-139.482855640482,-4.64923263188098,
132.4144825264));
#109425=CARTESIAN_POINT('Ctrl Pts',(-139.490620393429,-4.60262762859607,
132.543257867254));
#109426=CARTESIAN_POINT('Ctrl Pts',(-139.498385146376,-4.55066974522794,
132.669994003944));
#109427=CARTESIAN_POINT('Ctrl Pts',(-139.506142187261,-4.49876346716205,
132.796604264516));
#109428=CARTESIAN_POINT('Ctrl Pts',(-139.513899228146,-4.44151503654386,
132.921178992091));
#109429=CARTESIAN_POINT('Ctrl Pts',(-139.521656269031,-4.37911061300287,
133.043238305513));
#109430=CARTESIAN_POINT('Ctrl Pts',(-139.529407460271,-4.31675324912303,
133.165205573057));
#109431=CARTESIAN_POINT('Ctrl Pts',(-139.537158651511,-4.24924780875008,
133.284660855401));
#109432=CARTESIAN_POINT('Ctrl Pts',(-139.544909842751,-4.17682822626087,
133.401144981122));
#109433=CARTESIAN_POINT('Ctrl Pts',(-139.552657739529,-4.10443942402598,
133.517579597983));
#109434=CARTESIAN_POINT('Ctrl Pts',(-139.560405636305,-4.02714083981685,
133.631045238542));
#109435=CARTESIAN_POINT('Ctrl Pts',(-139.568153533083,-3.94521183499113,
133.741108247095));
#109436=CARTESIAN_POINT('Ctrl Pts',(-139.575899809167,-3.86329996794725,
133.85114823284));
#109437=CARTESIAN_POINT('Ctrl Pts',(-139.583646085251,-3.77675984015605,
133.957786688885));
#109438=CARTESIAN_POINT('Ctrl Pts',(-139.591392361335,-3.6859133039606,
134.060620155469));
#109439=CARTESIAN_POINT('Ctrl Pts',(-139.599138694601,-3.59506609715677,
134.163454381147));
#109440=CARTESIAN_POINT('Ctrl Pts',(-139.606885027866,-3.49991267736521,
134.262483268314));
#109441=CARTESIAN_POINT('Ctrl Pts',(-139.614631361131,-3.40081396009166,
134.357337886188));
#109442=CARTESIAN_POINT('Ctrl Pts',(-139.622379429134,-3.30169305034735,
134.452213746097));
#109443=CARTESIAN_POINT('Ctrl Pts',(-139.630127497137,-3.19862536739638,
134.542913206283));
#109444=CARTESIAN_POINT('Ctrl Pts',(-139.63787556514,-3.09200701096162,
134.629105799492));
#109445=CARTESIAN_POINT('Ctrl Pts',(-139.645631867882,-2.98527533926872,
134.715389999215));
#109446=CARTESIAN_POINT('Ctrl Pts',(-139.653388170624,-2.87498576024801,
134.797157517331));
#109447=CARTESIAN_POINT('Ctrl Pts',(-139.661144473366,-2.76156608039902,
134.874119313864));
#109448=CARTESIAN_POINT('Ctrl Pts',(-139.66890491588,-2.64808586505189,
134.951122187224));
#109449=CARTESIAN_POINT('Ctrl Pts',(-139.676665358394,-2.53147255226469,
135.023314022413));
#109450=CARTESIAN_POINT('Ctrl Pts',(-139.684425800908,-2.41218010588707,
135.090450933841));
#109451=CARTESIAN_POINT('Ctrl Pts',(-139.692198701174,-2.29269616068424,
135.157695619399));
#109452=CARTESIAN_POINT('Ctrl Pts',(-139.699971601439,-2.17052483619671,
135.21986898819));
#109453=CARTESIAN_POINT('Ctrl Pts',(-139.707744501705,-2.04614251410275,
135.276774269553));
#109454=CARTESIAN_POINT('Ctrl Pts',(-139.715234837467,-1.92628180271707,
135.331610900603));
#109455=CARTESIAN_POINT('Ctrl Pts',(-139.722725173229,-1.80436833854923,
135.381555694223));
#109456=CARTESIAN_POINT('Ctrl Pts',(-139.730215508991,-1.68084131096866,
135.426476534529));
#109457=CARTESIAN_POINT('Ctrl Pts',(-139.73798984311,-1.55263071859196,
135.473100562148));
#109458=CARTESIAN_POINT('Ctrl Pts',(-139.745764177229,-1.42227565831415,
135.514459840581));
#109459=CARTESIAN_POINT('Ctrl Pts',(-139.753538511348,-1.290247792092,135.550353000356));
#109460=CARTESIAN_POINT('Ctrl Pts',(-139.761303264295,-1.1583826384153,
135.58620192502));
#109461=CARTESIAN_POINT('Ctrl Pts',(-139.769068017242,-1.0248491543818,
135.616598033078));
#109462=CARTESIAN_POINT('Ctrl Pts',(-139.776832770189,-0.890137948128198,
135.641388371859));
#109463=CARTESIAN_POINT('Ctrl Pts',(-139.784589811075,-0.755560538943744,
135.666154088527));
#109464=CARTESIAN_POINT('Ctrl Pts',(-139.79234685196,-0.619808117375787,
135.685325045648));
#109465=CARTESIAN_POINT('Ctrl Pts',(-139.800103892845,-0.483385044857731,
135.698798477107));
#109466=CARTESIAN_POINT('Ctrl Pts',(-139.807855084085,-0.347064850039692,
135.712261748146));
#109467=CARTESIAN_POINT('Ctrl Pts',(-139.815606275325,-0.210075398420547,
135.720036007271));
#109468=CARTESIAN_POINT('Ctrl Pts',(-139.823357466565,-0.072929451167475,
135.722069876728));
#109469=CARTESIAN_POINT('Ctrl Pts',(-139.831105363342,0.0641582053993405,
135.724102881737));
#109470=CARTESIAN_POINT('Ctrl Pts',(-139.838853260119,0.201401835203392,
135.720400343907));
#109471=CARTESIAN_POINT('Ctrl Pts',(-139.846601156896,0.338285589780728,
135.710962896358));
#109472=CARTESIAN_POINT('Ctrl Pts',(-139.854347432981,0.475140711227478,
135.70152742292));
#109473=CARTESIAN_POINT('Ctrl Pts',(-139.862093709065,0.611635717387672,
135.686359452747));
#109474=CARTESIAN_POINT('Ctrl Pts',(-139.869839985149,0.747257197084021,
135.665511689473));
#109475=CARTESIAN_POINT('Ctrl Pts',(-139.877586318414,0.88287967790751,
135.644663772307));
#109476=CARTESIAN_POINT('Ctrl Pts',(-139.885332651679,1.01762823297403,
135.618136037779));
#109477=CARTESIAN_POINT('Ctrl Pts',(-139.893078984945,1.15099738672146,
135.586032718229));
#109478=CARTESIAN_POINT('Ctrl Pts',(-139.900827052948,1.28439640756597,
135.553922209363));
#109479=CARTESIAN_POINT('Ctrl Pts',(-139.908575120951,1.416415032366,135.516233722356));
#109480=CARTESIAN_POINT('Ctrl Pts',(-139.916323188954,1.54656112808484,
135.473121881499));
#109481=CARTESIAN_POINT('Ctrl Pts',(-139.924079491696,1.67684554462315,
135.429964220864));
#109482=CARTESIAN_POINT('Ctrl Pts',(-139.931835794438,1.80525308482444,
135.381371815295));
#109483=CARTESIAN_POINT('Ctrl Pts',(-139.93959209718,1.93130933130658,135.327548357347));
#109484=CARTESIAN_POINT('Ctrl Pts',(-139.947352539694,2.05743285780295,
135.2736961722));
#109485=CARTESIAN_POINT('Ctrl Pts',(-139.955112982208,2.18120223732624,
135.214607539794));
#109486=CARTESIAN_POINT('Ctrl Pts',(-139.962873424722,2.3021669034735,135.150532566655));
#109487=CARTESIAN_POINT('Ctrl Pts',(-139.970646324988,2.4233257528416,135.086354734681));
#109488=CARTESIAN_POINT('Ctrl Pts',(-139.978419225253,2.54167055393297,
135.017174763819));
#109489=CARTESIAN_POINT('Ctrl Pts',(-139.986192125519,2.65677826208401,
134.943287088116));
#109490=CARTESIAN_POINT('Ctrl Pts',(-139.99368246128,2.76770151510152,134.872085415539));
#109491=CARTESIAN_POINT('Ctrl Pts',(-140.001172797042,2.87561868976568,
134.796512546289));
#109492=CARTESIAN_POINT('Ctrl Pts',(-140.008663132804,2.98018124065842,
134.716866570958));
#109493=CARTESIAN_POINT('Ctrl Pts',(-140.016437466923,3.08870831245255,
134.634200794262));
#109494=CARTESIAN_POINT('Ctrl Pts',(-140.024211801042,3.19396513893323,
134.546885090453));
#109495=CARTESIAN_POINT('Ctrl Pts',(-140.031986135161,3.29552735745211,
134.455207436974));
#109496=CARTESIAN_POINT('Ctrl Pts',(-140.039750888109,3.39696440961326,
134.363642768011));
#109497=CARTESIAN_POINT('Ctrl Pts',(-140.047515641056,3.4947156260412,134.2677271049));
#109498=CARTESIAN_POINT('Ctrl Pts',(-140.055280394003,3.5883871376408,134.167790535509));
#109499=CARTESIAN_POINT('Ctrl Pts',(-140.063037434888,3.68196561337455,
134.067953224527));
#109500=CARTESIAN_POINT('Ctrl Pts',(-140.070794475773,3.77147218234516,
133.964103238155));
#109501=CARTESIAN_POINT('Ctrl Pts',(-140.078551516658,3.85654776483319,
133.856609362354));
#109502=CARTESIAN_POINT('Ctrl Pts',(-140.086302707898,3.94155919116279,
133.749196548521));
#109503=CARTESIAN_POINT('Ctrl Pts',(-140.094053899138,4.02214604029632,
133.638145620085));
#109504=CARTESIAN_POINT('Ctrl Pts',(-140.101805090378,4.09798792673915,
133.523860206608));
#109505=CARTESIAN_POINT('Ctrl Pts',(-140.109552987155,4.1737975783572,133.40962336748));
#109506=CARTESIAN_POINT('Ctrl Pts',(-140.117300883932,4.24486606269023,
133.292155102648));
#109507=CARTESIAN_POINT('Ctrl Pts',(-140.125048780709,4.31091508370574,
133.17188975225));
#109508=CARTESIAN_POINT('Ctrl Pts',(-140.132795056793,4.37695028868971,
133.051649558771));
#109509=CARTESIAN_POINT('Ctrl Pts',(-140.140541332877,4.43796793070903,
132.928613785973));
#109510=CARTESIAN_POINT('Ctrl Pts',(-140.148287608962,4.49373483954257,
132.803242868821));
#109511=CARTESIAN_POINT('Ctrl Pts',(-140.156033942227,4.54950216003483,
132.677871026209));
#109512=CARTESIAN_POINT('Ctrl Pts',(-140.163780275492,4.60001851110245,
132.550164362067));
#109513=CARTESIAN_POINT('Ctrl Pts',(-140.171526608758,4.64509836447465,
132.420604487424));
#109514=CARTESIAN_POINT('Ctrl Pts',(-140.179274676761,4.69018831316752,
132.291015598746));
#109515=CARTESIAN_POINT('Ctrl Pts',(-140.187022744764,4.72983921309355,
132.159573042921));
#109516=CARTESIAN_POINT('Ctrl Pts',(-140.194770812767,4.76391514412091,
132.026774443615));
#109517=CARTESIAN_POINT('Ctrl Pts',(-140.202527115508,4.79802729145323,
131.893834704378));
#109518=CARTESIAN_POINT('Ctrl Pts',(-140.21028341825,4.82655253644694,131.759536421971));
#109519=CARTESIAN_POINT('Ctrl Pts',(-140.218039720992,4.84940581723492,
131.624388837976));
#109520=CARTESIAN_POINT('Ctrl Pts',(-140.225800163506,4.87227129550696,
131.489169121646));
#109521=CARTESIAN_POINT('Ctrl Pts',(-140.233560606021,4.88945872845459,
131.353099588187));
#109522=CARTESIAN_POINT('Ctrl Pts',(-140.241321048535,4.90093499563448,
131.21669450056));
#109523=CARTESIAN_POINT('Ctrl Pts',(-140.2490939488,4.91242968553726,131.080070443378));
#109524=CARTESIAN_POINT('Ctrl Pts',(-140.256866849066,4.91819487249433,
130.943110146455));
#109525=CARTESIAN_POINT('Ctrl Pts',(-140.264639749331,4.91824960623573,
130.806328678044));
#109526=CARTESIAN_POINT('Ctrl Pts',(-140.272130085093,4.91830235026777,
130.674519560543));
#109527=CARTESIAN_POINT('Ctrl Pts',(-140.279620420855,4.91305262396251,
130.542876803322));
#109528=CARTESIAN_POINT('Ctrl Pts',(-140.287110756617,4.902562822065,130.411854772761));
#109529=CARTESIAN_POINT('Ctrl Pts',(-140.294885090736,4.89167529614016,
130.275865002087));
#109530=CARTESIAN_POINT('Ctrl Pts',(-140.302659424855,4.87510800737002,
130.140113182227));
#109531=CARTESIAN_POINT('Ctrl Pts',(-140.310433758974,4.85287386095722,
130.00511200034));
#109532=CARTESIAN_POINT('Ctrl Pts',(-140.318198511921,4.83066711614275,
129.870277195344));
#109533=CARTESIAN_POINT('Ctrl Pts',(-140.325963264868,4.80280747248079,
129.736191569723));
#109534=CARTESIAN_POINT('Ctrl Pts',(-140.333728017815,4.76935974637463,
129.603364917257));
#109535=CARTESIAN_POINT('Ctrl Pts',(-140.3414850587,4.73594524102158,129.470670190094));
#109536=CARTESIAN_POINT('Ctrl Pts',(-140.349242099585,4.69695379315036,
129.33923232435));
#109537=CARTESIAN_POINT('Ctrl Pts',(-140.35699914047,4.65250158147564,129.209552761783));
#109538=CARTESIAN_POINT('Ctrl Pts',(-140.36475033171,4.60808289155947,129.079970991583));
#109539=CARTESIAN_POINT('Ctrl Pts',(-140.372501522951,4.55821176074062,
128.952145253679));
#109540=CARTESIAN_POINT('Ctrl Pts',(-140.380252714191,4.50305459781487,
128.8265632691));
#109541=CARTESIAN_POINT('Ctrl Pts',(-140.388000610968,4.44792087815481,
128.701034660215));
#109542=CARTESIAN_POINT('Ctrl Pts',(-140.395748507745,4.38750575180352,
128.577748265118));
#109543=CARTESIAN_POINT('Ctrl Pts',(-140.403496404522,4.32202421561829,
128.457172993598));
#109544=CARTESIAN_POINT('Ctrl Pts',(-140.411242680606,4.25655637675882,
128.336622943825));
#109545=CARTESIAN_POINT('Ctrl Pts',(-140.41898895669,4.1860244224995,128.218783232972));
#109546=CARTESIAN_POINT('Ctrl Pts',(-140.426735232774,4.11068969561761,
128.104098910093));
#109547=CARTESIAN_POINT('Ctrl Pts',(-140.434481566039,4.03535441263177,
127.989413740641));
#109548=CARTESIAN_POINT('Ctrl Pts',(-140.442227899305,3.95521650093072,
127.877884332413));
#109549=CARTESIAN_POINT('Ctrl Pts',(-140.44997423257,3.87058087095232,127.769927098123));
#109550=CARTESIAN_POINT('Ctrl Pts',(-140.457722300573,3.78592628741152,
127.661945687559));
#109551=CARTESIAN_POINT('Ctrl Pts',(-140.465470368576,3.69677222248597,
127.557538350393));
#109552=CARTESIAN_POINT('Ctrl Pts',(-140.473218436579,3.60346387290977,
127.457088417829));
#109553=CARTESIAN_POINT('Ctrl Pts',(-140.480974739321,3.51005635410912,
127.35653172588));
#109554=CARTESIAN_POINT('Ctrl Pts',(-140.488731042063,3.4124859972821,127.259941127331));
#109555=CARTESIAN_POINT('Ctrl Pts',(-140.496487344805,3.31113526377693,
127.167663444653));
#109556=CARTESIAN_POINT('Ctrl Pts',(-140.504247787319,3.20973043633369,
127.075336510597));
#109557=CARTESIAN_POINT('Ctrl Pts',(-140.512008229833,3.10454151147988,
126.987327329967));
#109558=CARTESIAN_POINT('Ctrl Pts',(-140.519768672347,2.99598325080118,
126.903941739622));
#109559=CARTESIAN_POINT('Ctrl Pts',(-140.527541572612,2.88725072276509,
126.820422291325));
#109560=CARTESIAN_POINT('Ctrl Pts',(-140.535314472878,2.77513837041962,
126.741541490332));
#109561=CARTESIAN_POINT('Ctrl Pts',(-140.543087373143,2.66008983211715,
126.667561716536));
#109562=CARTESIAN_POINT('Ctrl Pts',(-140.550577708905,2.54922359797177,
126.596271293861));
#109563=CARTESIAN_POINT('Ctrl Pts',(-140.558068044667,2.43563121270508,
126.52953191145));
#109564=CARTESIAN_POINT('Ctrl Pts',(-140.565558380429,2.31972867350278,
126.467536670963));
#109565=CARTESIAN_POINT('Ctrl Pts',(-140.573332714548,2.1994316542993,126.40319086209));
#109566=CARTESIAN_POINT('Ctrl Pts',(-140.581107048667,2.07626477930166,
126.343752216786));
#109567=CARTESIAN_POINT('Ctrl Pts',(-140.588881382787,1.9506663623127,126.28948699747));
#109568=CARTESIAN_POINT('Ctrl Pts',(-140.596646135734,1.82522273414763,
126.235288655186));
#109569=CARTESIAN_POINT('Ctrl Pts',(-140.604410888681,1.69735388190218,
126.186251206554));
#109570=CARTESIAN_POINT('Ctrl Pts',(-140.612175641628,1.5675237443699,126.142595675687));
#109571=CARTESIAN_POINT('Ctrl Pts',(-140.619932682513,1.43782255596051,
126.098983504108));
#109572=CARTESIAN_POINT('Ctrl Pts',(-140.627689723398,1.30616432700333,
126.060742736514));
#109573=CARTESIAN_POINT('Ctrl Pts',(-140.635446764283,1.17303373208401,
126.028046669981));
#109574=CARTESIAN_POINT('Ctrl Pts',(-140.643197955523,1.04000353198211,
125.995375259806));
#109575=CARTESIAN_POINT('Ctrl Pts',(-140.650949146763,0.905503554093948,
125.968240320934));
#109576=CARTESIAN_POINT('Ctrl Pts',(-140.658700338003,0.770034079951911,
125.94676547406));
#109577=CARTESIAN_POINT('Ctrl Pts',(-140.66644823478,0.634622183949966,
125.925299754569));
#109578=CARTESIAN_POINT('Ctrl Pts',(-140.674196131557,0.498241996588744,
125.909489403426));
#109579=CARTESIAN_POINT('Ctrl Pts',(-140.681944028334,0.36140423600666,
125.89940699488));
#109580=CARTESIAN_POINT('Ctrl Pts',(-140.689690304418,0.224595098934209,
125.889326695358));
#109581=CARTESIAN_POINT('Ctrl Pts',(-140.697436580502,0.0873289686834048,
125.884971983933));
#109582=CARTESIAN_POINT('Ctrl Pts',(-140.705182856587,-0.0498784602151125,
125.886363545413));
#109583=CARTESIAN_POINT('Ctrl Pts',(-140.712929189852,-0.187086901947514,
125.887755117165));
#109584=CARTESIAN_POINT('Ctrl Pts',(-140.720675523117,-0.324236250517871,
125.894893042498));
#109585=CARTESIAN_POINT('Ctrl Pts',(-140.728421856382,-0.460811354576384,
125.907745872868));
#109586=CARTESIAN_POINT('Ctrl Pts',(-140.736169924385,-0.597417043682692,
125.920601581541));
#109587=CARTESIAN_POINT('Ctrl Pts',(-140.743917992388,-0.733447843211009,
125.939174705307));
#109588=CARTESIAN_POINT('Ctrl Pts',(-140.751666060391,-0.868394658496127,
125.963382020258));
#109589=CARTESIAN_POINT('Ctrl Pts',(-140.759422363133,-1.00348489686223,
125.987615063031));
#109590=CARTESIAN_POINT('Ctrl Pts',(-140.767178665875,-1.13748846416222,
126.017494189693));
#109591=CARTESIAN_POINT('Ctrl Pts',(-140.774934968617,-1.26990683912721,
126.052885090697));
#109592=CARTESIAN_POINT('Ctrl Pts',(-140.782695411131,-1.40239588976633,
126.08829488089));
#109593=CARTESIAN_POINT('Ctrl Pts',(-140.790455853645,-1.5332976892453,
126.1292221906));
#109594=CARTESIAN_POINT('Ctrl Pts',(-140.798216296159,-1.66213073958446,
126.17548338145));
#109595=CARTESIAN_POINT('Ctrl Pts',(-140.805989196425,-1.79117060417328,
126.221818834871));
#109596=CARTESIAN_POINT('Ctrl Pts',(-140.81376209669,-1.91813472100845,
126.273505132378));
#109597=CARTESIAN_POINT('Ctrl Pts',(-140.821534996955,-2.04256254508814,
126.330310851202));
#109598=CARTESIAN_POINT('Ctrl Pts',(-140.829025332718,-2.16246710435282,
126.385051539064));
#109599=CARTESIAN_POINT('Ctrl Pts',(-140.83651566848,-2.28001629582192,
126.444545763501));
#109600=CARTESIAN_POINT('Ctrl Pts',(-140.844006004242,-2.39482280096016,
126.508547910464));
#109601=CARTESIAN_POINT('Ctrl Pts',(-140.851781395978,-2.51399844001437,
126.574985755218));
#109602=CARTESIAN_POINT('Ctrl Pts',(-140.859556787713,-2.63059606879468,
126.646491912489));
#109603=CARTESIAN_POINT('Ctrl Pts',(-140.867332179448,-2.74415456711921,
126.722841442766));
#109604=CARTESIAN_POINT('Ctrl Pts',(-140.875097758318,-2.85756974992467,
126.79909461678));
#109605=CARTESIAN_POINT('Ctrl Pts',(-140.882863337187,-2.96795311307466,
126.880178784166));
#109606=CARTESIAN_POINT('Ctrl Pts',(-140.890628916056,-3.0748677978928,
126.965822993941));
#109607=CARTESIAN_POINT('Ctrl Pts',(-140.8983851287,-3.18165353069318,127.05136390646));
#109608=CARTESIAN_POINT('Ctrl Pts',(-140.906141341344,-3.28497861443026,
127.141453664288));
#109609=CARTESIAN_POINT('Ctrl Pts',(-140.913897553988,-3.38443540720065,
127.235778260805));
#109610=CARTESIAN_POINT('Ctrl Pts',(-140.921648456278,-3.4838241060778,
127.330038277228));
#109611=CARTESIAN_POINT('Ctrl Pts',(-140.929399358569,-3.57934950058017,
127.428527096211));
#109612=CARTESIAN_POINT('Ctrl Pts',(-140.937150260859,-3.67063721667059,
127.53089067176));
#109613=CARTESIAN_POINT('Ctrl Pts',(-140.944897535052,-3.76188220215985,
127.633206332242));
#109614=CARTESIAN_POINT('Ctrl Pts',(-140.952644809245,-3.84889319701488,
127.739392848883));
#109615=CARTESIAN_POINT('Ctrl Pts',(-140.960392083438,-3.93133317036314,
127.849059860265));
#109616=CARTESIAN_POINT('Ctrl Pts',(-140.968137408987,-4.01375240787563,
127.958699287491));
#109617=CARTESIAN_POINT('Ctrl Pts',(-140.975882734536,-4.09160267843705,
128.071817154245));
#109618=CARTESIAN_POINT('Ctrl Pts',(-140.983628060084,-4.16458794100919,
128.187990929601));
#109619=CARTESIAN_POINT('Ctrl Pts',(-140.991375513376,-4.23759325359433,
128.304196619424));
#109620=CARTESIAN_POINT('Ctrl Pts',(-140.999122966667,-4.30573067500899,
128.423459567046));
#109621=CARTESIAN_POINT('Ctrl Pts',(-141.006870419959,-4.36874810115888,
128.54532916778));
#109622=CARTESIAN_POINT('Ctrl Pts',(-141.014618868035,-4.43177361884299,
128.667214416759));
#109623=CARTESIAN_POINT('Ctrl Pts',(-141.022367316111,-4.48967765933981,
128.791706634542));
#109624=CARTESIAN_POINT('Ctrl Pts',(-141.030115764188,-4.54225503612316,
128.918332449878));
#109625=CARTESIAN_POINT('Ctrl Pts',(-141.037870521161,-4.59487522215801,
129.045061365762));
#109626=CARTESIAN_POINT('Ctrl Pts',(-141.045625278135,-4.64215993836921,
129.173926985059));
#109627=CARTESIAN_POINT('Ctrl Pts',(-141.053380035108,-4.6839528132572,
129.304437584314));
#109628=CARTESIAN_POINT('Ctrl Pts',(-141.058842202681,-4.71339018785739,
129.396364483573));
#109629=CARTESIAN_POINT('Ctrl Pts',(-141.064304370253,-4.74010393889211,
129.489107134965));
#109630=CARTESIAN_POINT('Ctrl Pts',(-141.069766537825,-4.76405452823392,
129.582490119308));
#109631=CARTESIAN_POINT('Origin',(213.235140564004,0.,130.804360617566));
#109632=CARTESIAN_POINT('',(-143.165347877338,-4.75725076560214,129.584194750691));
#109633=CARTESIAN_POINT('',(-142.820077333605,-4.76405452823405,129.582490119308));
#109634=CARTESIAN_POINT('',(213.235140564004,-4.76405452823405,129.582490119308));
#109635=CARTESIAN_POINT('',(-141.485140564011,-4.91265574211895,130.801213014533));
#109636=CARTESIAN_POINT('Ctrl Pts',(-141.485140564011,-4.91219653301638,
130.801213308754));
#109637=CARTESIAN_POINT('Ctrl Pts',(-141.543347002514,-4.9061844889293,
131.831936216524));
#109638=CARTESIAN_POINT('Ctrl Pts',(-141.694369315622,-4.08506870756113,
134.515011964414));
#109639=CARTESIAN_POINT('Ctrl Pts',(-141.938207503334,0.324971199359551,
136.612636915233));
#109640=CARTESIAN_POINT('Ctrl Pts',(-142.216655127147,5.06232221927725,
133.670468357807));
#109641=CARTESIAN_POINT('Ctrl Pts',(-142.49510275096,5.14764642786865,128.094486804246));
#109642=CARTESIAN_POINT('Ctrl Pts',(-142.773550374773,0.502535045756554,
125.00874690043));
#109643=CARTESIAN_POINT('Ctrl Pts',(-142.996965416899,-3.59504696289219,
126.806148866277));
#109644=CARTESIAN_POINT('Ctrl Pts',(-143.127564584421,-4.59411981166379,
128.934973156602));
#109645=CARTESIAN_POINT('Ctrl Pts',(-143.165347877338,-4.75725076560214,
129.584194750691));
#109646=CARTESIAN_POINT('Ctrl Pts',(-141.415385046285,-4.76405452823413,
129.582490119309));
#109647=CARTESIAN_POINT('Ctrl Pts',(-141.424166289759,-4.80243581228232,
129.732138163295));
#109648=CARTESIAN_POINT('Ctrl Pts',(-141.432947533233,-4.83380612295216,
129.88376826295));
#109649=CARTESIAN_POINT('Ctrl Pts',(-141.441728776707,-4.85797926450059,
130.036753603409));
#109650=CARTESIAN_POINT('Ctrl Pts',(-141.450456965926,-4.88200635748487,
130.188814641612));
#109651=CARTESIAN_POINT('Ctrl Pts',(-141.459185155146,-4.89892289552827,
130.342214411613));
#109652=CARTESIAN_POINT('Ctrl Pts',(-141.467913344365,-4.908593800916,130.496318477415));
#109653=CARTESIAN_POINT('Ctrl Pts',(-141.473655750914,-4.91495643456568,
130.597705852775));
#109654=CARTESIAN_POINT('Ctrl Pts',(-141.479398157462,-4.91818375838515,
130.699397701661));
#109655=CARTESIAN_POINT('Ctrl Pts',(-141.485140564011,-4.91824899049676,
130.801209430865));
#109656=CARTESIAN_POINT('',(-141.139859436025,-4.91824965042212,130.802506265195));
#109657=CARTESIAN_POINT('Ctrl Pts',(-141.069766537825,-4.76405452823392,
129.582490119308));
#109658=CARTESIAN_POINT('Ctrl Pts',(-141.077530799274,-4.79809937124775,
129.715230445516));
#109659=CARTESIAN_POINT('Ctrl Pts',(-141.085295060724,-4.82655889760429,
129.849264650235));
#109660=CARTESIAN_POINT('Ctrl Pts',(-141.093059322173,-4.84936363347628,
129.984082973827));
#109661=CARTESIAN_POINT('Ctrl Pts',(-141.100834514477,-4.87220047481901,
130.119091100351));
#109662=CARTESIAN_POINT('Ctrl Pts',(-141.108609706782,-4.88936658559759,
130.254885163094));
#109663=CARTESIAN_POINT('Ctrl Pts',(-141.116384899086,-4.90084442332398,
130.390951618058));
#109664=CARTESIAN_POINT('Ctrl Pts',(-141.118407808742,-4.90383066827534,
130.426352690444));
#109665=CARTESIAN_POINT('Ctrl Pts',(-141.120430718398,-4.90643214275736,
130.46177221019));
#109666=CARTESIAN_POINT('Ctrl Pts',(-141.122453628054,-4.90864911493995,
130.497201165653));
#109667=CARTESIAN_POINT('Ctrl Pts',(-141.128255564034,-4.91500764441522,
130.598815457145));
#109668=CARTESIAN_POINT('Ctrl Pts',(-141.134057500014,-4.91821123919876,
130.700629226373));
#109669=CARTESIAN_POINT('Ctrl Pts',(-141.139859435993,-4.91824965042191,
130.802506264632));
#109670=CARTESIAN_POINT('Ctrl Pts',(-141.139859436025,-4.91824965042212,
130.802506265195));
#109671=CARTESIAN_POINT('Ctrl Pts',(-141.147560877912,-4.91830063714692,
130.937737004134));
#109672=CARTESIAN_POINT('Ctrl Pts',(-141.155262319799,-4.91277001159415,
131.073195518115));
#109673=CARTESIAN_POINT('Ctrl Pts',(-141.162963761685,-4.9016276276267,
131.208377526354));
#109674=CARTESIAN_POINT('Ctrl Pts',(-141.170656056235,-4.89049847795258,
131.343398973051));
#109675=CARTESIAN_POINT('Ctrl Pts',(-141.178348350785,-4.87377085989654,
131.478144173562));
#109676=CARTESIAN_POINT('Ctrl Pts',(-141.186040645335,-4.85146661083934,
131.612107351642));
#109677=CARTESIAN_POINT('Ctrl Pts',(-141.193725727755,-4.82918327376654,
131.745944928727));
#109678=CARTESIAN_POINT('Ctrl Pts',(-141.201410810175,-4.80133377254601,
131.879001551044));
#109679=CARTESIAN_POINT('Ctrl Pts',(-141.209095892594,-4.76799183109079,
132.010775538375));
#109680=CARTESIAN_POINT('Ctrl Pts',(-141.217087782564,-4.73331879664153,
132.147810270093));
#109681=CARTESIAN_POINT('Ctrl Pts',(-141.225079672534,-4.69270571207718,
132.283457393));
#109682=CARTESIAN_POINT('Ctrl Pts',(-141.233071562504,-4.64629449388461,
132.417162694263));
#109683=CARTESIAN_POINT('Ctrl Pts',(-141.240748780933,-4.60171066440629,
132.545603501982));
#109684=CARTESIAN_POINT('Ctrl Pts',(-141.248425999362,-4.55177676325002,
132.67225208524));
#109685=CARTESIAN_POINT('Ctrl Pts',(-141.256103217791,-4.49666961042024,
132.796632054199));
#109686=CARTESIAN_POINT('Ctrl Pts',(-141.263779517625,-4.44156905127304,
132.920997140842));
#109687=CARTESIAN_POINT('Ctrl Pts',(-141.271455817459,-4.38129663284183,
133.043093788377));
#109688=CARTESIAN_POINT('Ctrl Pts',(-141.279132117293,-4.31607711216116,
133.162466091114));
#109689=CARTESIAN_POINT('Ctrl Pts',(-141.286809235918,-4.25085063485896,
133.281851126665));
#109690=CARTESIAN_POINT('Ctrl Pts',(-141.294486354542,-4.18067619718312,
133.398510889518));
#109691=CARTESIAN_POINT('Ctrl Pts',(-141.302163473167,-4.10582400319464,
133.512015011556));
#109692=CARTESIAN_POINT('Ctrl Pts',(-141.309843148281,-4.03094688333255,
133.625556930606));
#109693=CARTESIAN_POINT('Ctrl Pts',(-141.317522823396,-3.95138912850936,
133.735940786137));
#109694=CARTESIAN_POINT('Ctrl Pts',(-141.325202498511,-3.86746335458778,
133.842766492926));
#109695=CARTESIAN_POINT('Ctrl Pts',(-141.332890594324,-3.78344555676406,
133.9497093332));
#109696=CARTESIAN_POINT('Ctrl Pts',(-141.340578690138,-3.69505042649711,
134.053085923735));
#109697=CARTESIAN_POINT('Ctrl Pts',(-141.348266785951,-3.60263002539251,
134.152530261213));
#109698=CARTESIAN_POINT('Ctrl Pts',(-141.355959873652,-3.51014961563883,
134.252039167989));
#109699=CARTESIAN_POINT('Ctrl Pts',(-141.363652961353,-3.41363901397913,
134.347610458735));
#109700=CARTESIAN_POINT('Ctrl Pts',(-141.371346049054,-3.31348505945223,
134.438916962333));
#109701=CARTESIAN_POINT('Ctrl Pts',(-141.379049968107,-3.21319009486476,
134.530352019373));
#109702=CARTESIAN_POINT('Ctrl Pts',(-141.386753887161,-3.10924184473051,
134.617510051455));
#109703=CARTESIAN_POINT('Ctrl Pts',(-141.394457806214,-3.00205814321372,
134.70010572823));
#109704=CARTESIAN_POINT('Ctrl Pts',(-141.396605621432,-2.97217584776836,
134.723133001789));
#109705=CARTESIAN_POINT('Ctrl Pts',(-141.39875343665,-2.9420422295363,134.745805926892));
#109706=CARTESIAN_POINT('Ctrl Pts',(-141.400901251868,-2.91166669313975,
134.768118951592));
#109707=CARTESIAN_POINT('Ctrl Pts',(-141.408675585987,-2.80171795685258,
134.848884237067));
#109708=CARTESIAN_POINT('Ctrl Pts',(-141.416449920106,-2.68823206032786,
134.925199261423));
#109709=CARTESIAN_POINT('Ctrl Pts',(-141.424224254225,-2.57160509811455,
134.996738258219));
#109710=CARTESIAN_POINT('Ctrl Pts',(-141.431989007172,-2.45512186820923,
135.068189089596));
#109711=CARTESIAN_POINT('Ctrl Pts',(-141.439753760119,-2.3355056049805,
135.134875402391));
#109712=CARTESIAN_POINT('Ctrl Pts',(-141.447518513066,-2.21318418815064,
135.196512574389));
#109713=CARTESIAN_POINT('Ctrl Pts',(-141.455275553951,-2.09098426267641,
135.258088527477));
#109714=CARTESIAN_POINT('Ctrl Pts',(-141.463032594836,-1.96608487733265,
135.314625144808));
#109715=CARTESIAN_POINT('Ctrl Pts',(-141.470789635721,-1.83894121045427,
135.365882105731));
#109716=CARTESIAN_POINT('Ctrl Pts',(-141.478540826961,-1.7118934236036,
135.417100413382));
#109717=CARTESIAN_POINT('Ctrl Pts',(-141.486292018202,-1.58260508503859,
135.46304684383));
#109718=CARTESIAN_POINT('Ctrl Pts',(-141.494043209442,-1.45155387138247,
135.503528035415));
#109719=CARTESIAN_POINT('Ctrl Pts',(-141.501791106219,-1.3205583579886,
135.543992021414));
#109720=CARTESIAN_POINT('Ctrl Pts',(-141.509539002996,-1.18780183251011,
135.578995273419));
#109721=CARTESIAN_POINT('Ctrl Pts',(-141.517286899773,-1.0537795462575,
135.608393478651));
#109722=CARTESIAN_POINT('Ctrl Pts',(-141.525033175857,-0.91978529457762,
135.637785534414));
#109723=CARTESIAN_POINT('Ctrl Pts',(-141.532779451941,-0.784526190409212,
135.661574791766));
#109724=CARTESIAN_POINT('Ctrl Pts',(-141.540525728025,-0.64850977441591,
135.679667596105));
#109725=CARTESIAN_POINT('Ctrl Pts',(-141.548272061291,-0.512492354380508,
135.697760534));
#109726=CARTESIAN_POINT('Ctrl Pts',(-141.556018394556,-0.375717998916713,
135.710156883422));
#109727=CARTESIAN_POINT('Ctrl Pts',(-141.563764727821,-0.238701108935161,
135.716814672628));
#109728=CARTESIAN_POINT('Ctrl Pts',(-141.571512795824,-0.101653534971293,
135.723473952799));
#109729=CARTESIAN_POINT('Ctrl Pts',(-141.579260863827,0.0356362911590168,
135.724392096561));
#109730=CARTESIAN_POINT('Ctrl Pts',(-141.58700893183,0.172652616806735,
135.719579243061));
#109731=CARTESIAN_POINT('Ctrl Pts',(-141.594765234572,0.309814565036055,
135.714761274402));
#109732=CARTESIAN_POINT('Ctrl Pts',(-141.602521537314,0.446702040771774,
135.704200154854));
#109733=CARTESIAN_POINT('Ctrl Pts',(-141.610277840056,0.582802508506382,
135.687958092643));
#109734=CARTESIAN_POINT('Ctrl Pts',(-141.61803828257,0.718975617158156,
135.671707361554));
#109735=CARTESIAN_POINT('Ctrl Pts',(-141.625798725084,0.854360495081336,
135.649769708611));
#109736=CARTESIAN_POINT('Ctrl Pts',(-141.633559167598,0.988454457830667,
135.622258587355));
#109737=CARTESIAN_POINT('Ctrl Pts',(-141.641332067863,1.12276368011367,
135.594703302804));
#109738=CARTESIAN_POINT('Ctrl Pts',(-141.649104968129,1.25577746654187,
135.561556765521));
#109739=CARTESIAN_POINT('Ctrl Pts',(-141.656877868395,1.38700709281581,
135.522982703194));
#109740=CARTESIAN_POINT('Ctrl Pts',(-141.664368204157,1.51346619163076,
135.485810905194));
#109741=CARTESIAN_POINT('Ctrl Pts',(-141.671858539919,1.63826830385689,
135.443599438269));
#109742=CARTESIAN_POINT('Ctrl Pts',(-141.679348875681,1.76099517684078,
135.396536468907));
#109743=CARTESIAN_POINT('Ctrl Pts',(-141.6871232098,1.88837527651317,135.347689092759));
#109744=CARTESIAN_POINT('Ctrl Pts',(-141.694897543919,2.01392316697685,
135.293460328688));
#109745=CARTESIAN_POINT('Ctrl Pts',(-141.702671878038,2.13715067292015,
135.234007337536));
#109746=CARTESIAN_POINT('Ctrl Pts',(-141.710436630986,2.2602263119752,135.174627616882));
#109747=CARTESIAN_POINT('Ctrl Pts',(-141.718201383933,2.38098690764954,
135.110036647888));
#109748=CARTESIAN_POINT('Ctrl Pts',(-141.72596613688,2.4989617197696,135.040440572622));
#109749=CARTESIAN_POINT('Ctrl Pts',(-141.733723177765,2.61681935764311,
134.970913621159));
#109750=CARTESIAN_POINT('Ctrl Pts',(-141.74148021865,2.73189638361879,134.896391653585));
#109751=CARTESIAN_POINT('Ctrl Pts',(-141.749237259535,2.84374457412099,
134.817127725144));
#109752=CARTESIAN_POINT('Ctrl Pts',(-141.756988450775,2.95550841903283,
134.737923570248));
#109753=CARTESIAN_POINT('Ctrl Pts',(-141.764739642015,3.06404795727677,
134.653984797337));
#109754=CARTESIAN_POINT('Ctrl Pts',(-141.772490833255,3.16894231232893,
134.565608772585));
#109755=CARTESIAN_POINT('Ctrl Pts',(-141.780238730032,3.2737920844819,134.47727031));
#109756=CARTESIAN_POINT('Ctrl Pts',(-141.78798662681,3.37499945651688,134.384498597965));
#109757=CARTESIAN_POINT('Ctrl Pts',(-141.795734523587,3.4721753185756,134.287632300851));
#109758=CARTESIAN_POINT('Ctrl Pts',(-141.803480799671,3.56933085353912,
134.190786266078));
#109759=CARTESIAN_POINT('Ctrl Pts',(-141.811227075755,3.66245627918677,
134.089847625687));
#109760=CARTESIAN_POINT('Ctrl Pts',(-141.818973351839,3.75119846312152,
133.985192765413));
#109761=CARTESIAN_POINT('Ctrl Pts',(-141.826719685104,3.83994130213079,
133.8805371326));
#109762=CARTESIAN_POINT('Ctrl Pts',(-141.83446601837,3.92430058200984,133.772165523357));
#109763=CARTESIAN_POINT('Ctrl Pts',(-141.842212351635,4.00396294448545,
133.660488030986));
#109764=CARTESIAN_POINT('Ctrl Pts',(-141.849960419638,4.08364314679447,
133.548785529215));
#109765=CARTESIAN_POINT('Ctrl Pts',(-141.857708487641,4.15862411165816,
133.433775989372));
#109766=CARTESIAN_POINT('Ctrl Pts',(-141.865456555644,4.22863559252291,
133.315898809222));
#109767=CARTESIAN_POINT('Ctrl Pts',(-141.873212858386,4.29872148242296,
133.197896347803));
#109768=CARTESIAN_POINT('Ctrl Pts',(-141.880969161128,4.36382713773829,
133.077020494525));
#109769=CARTESIAN_POINT('Ctrl Pts',(-141.88872546387,4.42372785804987,132.953736085095));
#109770=CARTESIAN_POINT('Ctrl Pts',(-141.896485906384,4.48366054917929,
132.830385875063));
#109771=CARTESIAN_POINT('Ctrl Pts',(-141.904246348898,4.53838261392825,
132.704624905693));
#109772=CARTESIAN_POINT('Ctrl Pts',(-141.912006791412,4.58771779075253,
132.576937424058));
#109773=CARTESIAN_POINT('Ctrl Pts',(-141.919779691678,4.63713216478255,
132.449044967141));
#109774=CARTESIAN_POINT('Ctrl Pts',(-141.927552591943,4.68114224481423,
132.319220188421));
#109775=CARTESIAN_POINT('Ctrl Pts',(-141.935325492209,4.71962161216651,
132.187962764309));
#109776=CARTESIAN_POINT('Ctrl Pts',(-141.94281582797,4.75670215759062,132.061476878184));
#109777=CARTESIAN_POINT('Ctrl Pts',(-141.950306163732,4.7886470450928,131.933660997651));
#109778=CARTESIAN_POINT('Ctrl Pts',(-141.957796499494,4.81538850869332,
131.804968719094));
#109779=CARTESIAN_POINT('Ctrl Pts',(-141.965570833613,4.84314388301496,
131.671397033678));
#109780=CARTESIAN_POINT('Ctrl Pts',(-141.973345167732,4.86538138943614,
131.536458066138));
#109781=CARTESIAN_POINT('Ctrl Pts',(-141.981119501851,4.88196938114517,
131.400647481467));
#109782=CARTESIAN_POINT('Ctrl Pts',(-141.988884254798,4.89853692963693,
131.265004271204));
#109783=CARTESIAN_POINT('Ctrl Pts',(-141.996649007745,4.90946876981461,
131.128491965482));
#109784=CARTESIAN_POINT('Ctrl Pts',(-142.004413760693,4.91468388827595,
130.991618036166));
#109785=CARTESIAN_POINT('Ctrl Pts',(-142.012170801578,4.91989382700812,
130.854880051966));
#109786=CARTESIAN_POINT('Ctrl Pts',(-142.019927842462,4.91939832856881,
130.717781547088));
#109787=CARTESIAN_POINT('Ctrl Pts',(-142.027684883347,4.91316801971071,
130.580836407262));
#109788=CARTESIAN_POINT('Ctrl Pts',(-142.035436074588,4.90694240917697,
130.443994538831));
#109789=CARTESIAN_POINT('Ctrl Pts',(-142.043187265828,4.89499061390475,
130.307306194231));
#109790=CARTESIAN_POINT('Ctrl Pts',(-142.050938457068,4.87733532243406,
130.17128620248));
#109791=CARTESIAN_POINT('Ctrl Pts',(-142.058686353845,4.85968753493327,
130.035324022854));
#109792=CARTESIAN_POINT('Ctrl Pts',(-142.066434250622,4.83634112287924,
129.900030017989));
#109793=CARTESIAN_POINT('Ctrl Pts',(-142.074182147399,4.80737069081658,
129.765914613395));
#109794=CARTESIAN_POINT('Ctrl Pts',(-142.081928423483,4.77840631874378,
129.631827262853));
#109795=CARTESIAN_POINT('Ctrl Pts',(-142.089674699567,4.74382034913029,
129.498918404113));
#109796=CARTESIAN_POINT('Ctrl Pts',(-142.097420975652,4.70373856926707,
129.367688583144));
#109797=CARTESIAN_POINT('Ctrl Pts',(-142.105167308917,4.66365649352931,
129.236457793467));
#109798=CARTESIAN_POINT('Ctrl Pts',(-142.112913642182,4.61807864079469,
129.106906440207));
#109799=CARTESIAN_POINT('Ctrl Pts',(-142.120659975447,4.56718065637211,
128.979519826001));
#109800=CARTESIAN_POINT('Ctrl Pts',(-142.12840804345,4.51627127369888,128.852104684446));
#109801=CARTESIAN_POINT('Ctrl Pts',(-142.136156111453,4.46003953361033,
128.726855609585));
#109802=CARTESIAN_POINT('Ctrl Pts',(-142.143904179456,4.39870903902877,
128.604237472725));
#109803=CARTESIAN_POINT('Ctrl Pts',(-142.151660482198,4.33731336166748,
128.481489015849));
#109804=CARTESIAN_POINT('Ctrl Pts',(-142.15941678494,4.27080827991578,128.361377432891));
#109805=CARTESIAN_POINT('Ctrl Pts',(-142.167173087682,4.19946341715095,
128.24434302573));
#109806=CARTESIAN_POINT('Ctrl Pts',(-142.174933530196,4.12808047548452,
128.127246153781));
#109807=CARTESIAN_POINT('Ctrl Pts',(-142.18269397271,4.05185282287614,128.013230055072));
#109808=CARTESIAN_POINT('Ctrl Pts',(-142.190454415225,3.97109259643092,
127.9027047708));
#109809=CARTESIAN_POINT('Ctrl Pts',(-142.19822731549,3.89020272650088,127.79200206153));
#109810=CARTESIAN_POINT('Ctrl Pts',(-142.206000215755,3.80476598659904,
127.684801670725));
#109811=CARTESIAN_POINT('Ctrl Pts',(-142.213773116021,3.71513443625474,
127.581480045306));
#109812=CARTESIAN_POINT('Ctrl Pts',(-142.221263451783,3.62876121853347,
127.481914421221));
#109813=CARTESIAN_POINT('Ctrl Pts',(-142.228753787545,3.53849309029612,
127.385950677131));
#109814=CARTESIAN_POINT('Ctrl Pts',(-142.236244123307,3.44467504586145,
127.2938910064));
#109815=CARTESIAN_POINT('Ctrl Pts',(-142.244018457426,3.34729986175733,
127.198340865273));
#109816=CARTESIAN_POINT('Ctrl Pts',(-142.251792791545,3.24579180209864,
127.1066940133));
#109817=CARTESIAN_POINT('Ctrl Pts',(-142.259567125664,3.14049672556235,
127.019329127706));
#109818=CARTESIAN_POINT('Ctrl Pts',(-142.267331878611,3.03533141579711,
126.932071911526));
#109819=CARTESIAN_POINT('Ctrl Pts',(-142.275096631558,2.92638867340537,
126.849086409037));
#109820=CARTESIAN_POINT('Ctrl Pts',(-142.282861384505,2.81405165911513,
126.770715080049));
#109821=CARTESIAN_POINT('Ctrl Pts',(-142.29061842539,2.70182621953176,126.69242159057));
#109822=CARTESIAN_POINT('Ctrl Pts',(-142.298375466275,2.58621353553775,
126.618733376737));
#109823=CARTESIAN_POINT('Ctrl Pts',(-142.30613250716,2.46763007679345,126.549952918884));
#109824=CARTESIAN_POINT('Ctrl Pts',(-142.313883698401,2.34913604275702,
126.481224328909));
#109825=CARTESIAN_POINT('Ctrl Pts',(-142.321634889641,2.22767602994654,
126.417396323709));
#109826=CARTESIAN_POINT('Ctrl Pts',(-142.329386080881,2.10369544230599,
126.358728092433));
#109827=CARTESIAN_POINT('Ctrl Pts',(-142.337133977658,1.97976754972299,
126.30008479672));
#109828=CARTESIAN_POINT('Ctrl Pts',(-142.344881874435,1.85332156572261,
126.246597080017));
#109829=CARTESIAN_POINT('Ctrl Pts',(-142.352629771212,1.72482725132048,
126.198478072863));
#109830=CARTESIAN_POINT('Ctrl Pts',(-142.360376047296,1.5963598151589,126.150369131167));
#109831=CARTESIAN_POINT('Ctrl Pts',(-142.36812232338,1.46584526674136,126.1076268023));
#109832=CARTESIAN_POINT('Ctrl Pts',(-142.375868599464,1.33377272067146,
126.070415815174));
#109833=CARTESIAN_POINT('Ctrl Pts',(-142.383614932729,1.2016991996722,126.033204553365));
#109834=CARTESIAN_POINT('Ctrl Pts',(-142.391361265995,1.06806803438588,
126.001524820798));
#109835=CARTESIAN_POINT('Ctrl Pts',(-142.39910759926,0.933382464245367,
125.975491160028));
#109836=CARTESIAN_POINT('Ctrl Pts',(-142.406855667263,0.798666732205084,
125.949451669201));
#109837=CARTESIAN_POINT('Ctrl Pts',(-142.414603735266,0.662896509232523,
125.929060840363));
#109838=CARTESIAN_POINT('Ctrl Pts',(-142.422351803269,0.52658376756393,
125.914381824336));
#109839=CARTESIAN_POINT('Ctrl Pts',(-142.430108106011,0.390126151091534,
125.899687207277));
#109840=CARTESIAN_POINT('Ctrl Pts',(-142.437864408752,0.253125253449516,
125.890716571599));
#109841=CARTESIAN_POINT('Ctrl Pts',(-142.445620711494,0.116097251099588,
125.887481069439));
#109842=CARTESIAN_POINT('Ctrl Pts',(-142.453381154008,-0.0210038872214008,
125.884243840395));
#109843=CARTESIAN_POINT('Ctrl Pts',(-142.461141596523,-0.158131768367437,
125.886747837062));
#109844=CARTESIAN_POINT('Ctrl Pts',(-142.468902039037,-0.294772695334932,
125.89495208694));
#109845=CARTESIAN_POINT('Ctrl Pts',(-142.476674939302,-0.431632970448808,
125.903169507007));
#109846=CARTESIAN_POINT('Ctrl Pts',(-142.484447839568,-0.568004340130829,
125.917105426235));
#109847=CARTESIAN_POINT('Ctrl Pts',(-142.492220739833,-0.703379792149672,
125.936667125727));
#109848=CARTESIAN_POINT('Ctrl Pts',(-142.499711075595,-0.833834005502211,
125.955517708169));
#109849=CARTESIAN_POINT('Ctrl Pts',(-142.507201411357,-0.963363149477259,
125.979592093257));
#109850=CARTESIAN_POINT('Ctrl Pts',(-142.51469174712,-1.09152650238254,
126.008763370393));
#109851=CARTESIAN_POINT('Ctrl Pts',(-142.522466081239,-1.22454920776332,
126.039040685367));
#109852=CARTESIAN_POINT('Ctrl Pts',(-142.530240415358,-1.35652188562031,
126.074904928725));
#109853=CARTESIAN_POINT('Ctrl Pts',(-142.538014749477,-1.48693899901593,
126.116269804057));
#109854=CARTESIAN_POINT('Ctrl Pts',(-142.545779502424,-1.61719538497429,
126.157583700877));
#109855=CARTESIAN_POINT('Ctrl Pts',(-142.553544255371,-1.74589965182567,
126.204384624342));
#109856=CARTESIAN_POINT('Ctrl Pts',(-142.561309008318,-1.87255657070242,
126.256535318369));
#109857=CARTESIAN_POINT('Ctrl Pts',(-142.569066049203,-1.99908769214247,
126.308634215592));
#109858=CARTESIAN_POINT('Ctrl Pts',(-142.576823090088,-2.12357515309508,
126.366072161446));
#109859=CARTESIAN_POINT('Ctrl Pts',(-142.584580130973,-2.2455393562644,
126.428662266221));
#109860=CARTESIAN_POINT('Ctrl Pts',(-142.592331322213,-2.36741158527987,
126.49120517131));
#109861=CARTESIAN_POINT('Ctrl Pts',(-142.600082513453,-2.48676399750776,
126.558892324118));
#109862=CARTESIAN_POINT('Ctrl Pts',(-142.607833704693,-2.6031377780654,
126.631489091757));
#109863=CARTESIAN_POINT('Ctrl Pts',(-142.615581601471,-2.71946209666113,
126.704055003832));
#109864=CARTESIAN_POINT('Ctrl Pts',(-142.623329498248,-2.83280997054145,
126.78152617392));
#109865=CARTESIAN_POINT('Ctrl Pts',(-142.631077395025,-2.94274816964395,
126.863622581036));
#109866=CARTESIAN_POINT('Ctrl Pts',(-142.638823671109,-3.05266337204549,
126.945701815353));
#109867=CARTESIAN_POINT('Ctrl Pts',(-142.646569947193,-3.15917000526206,
127.032404128509));
#109868=CARTESIAN_POINT('Ctrl Pts',(-142.654316223277,-3.26186509980353,
127.123407054536));
#109869=CARTESIAN_POINT('Ctrl Pts',(-142.662062556542,-3.36456095241727,
127.214410652326));
#109870=CARTESIAN_POINT('Ctrl Pts',(-142.669808889807,-3.46344491760358,
127.309714667041));
#109871=CARTESIAN_POINT('Ctrl Pts',(-142.677555223073,-3.55814861425983,
127.408957622141));
#109872=CARTESIAN_POINT('Ctrl Pts',(-142.685303291076,-3.65287351915166,
127.508222802012));
#109873=CARTESIAN_POINT('Ctrl Pts',(-142.693051359079,-3.74341602284071,
127.611428394751));
#109874=CARTESIAN_POINT('Ctrl Pts',(-142.700799427082,-3.82944626125069,
127.718177798177));
#109875=CARTESIAN_POINT('Ctrl Pts',(-142.708555729824,-3.91556793362217,
127.82504065614));
#109876=CARTESIAN_POINT('Ctrl Pts',(-142.716312032565,-3.99716751508839,
127.93545454369));
#109877=CARTESIAN_POINT('Ctrl Pts',(-142.724068335307,-4.07395661705488,
128.048991214953));
#109878=CARTESIAN_POINT('Ctrl Pts',(-142.731828777821,-4.15078670367695,
128.162588484156));
#109879=CARTESIAN_POINT('Ctrl Pts',(-142.739589220335,-4.22280098965747,
128.27931152559));
#109880=CARTESIAN_POINT('Ctrl Pts',(-142.74734966285,-4.28975628054519,
128.398706004779));
#109881=CARTESIAN_POINT('Ctrl Pts',(-142.755122563115,-4.35681905401003,
128.518292146585));
#109882=CARTESIAN_POINT('Ctrl Pts',(-142.76289546338,-4.41880642684689,
128.640557946883));
#109883=CARTESIAN_POINT('Ctrl Pts',(-142.770668363646,-4.47552235359413,
128.765026725095));
#109884=CARTESIAN_POINT('Ctrl Pts',(-142.778158699408,-4.53017651354393,
128.884970749698));
#109885=CARTESIAN_POINT('Ctrl Pts',(-142.785649035169,-4.57993571778879,
129.006960080163));
#109886=CARTESIAN_POINT('Ctrl Pts',(-142.793139370931,-4.62466851896773,
129.130555326569));
#109887=CARTESIAN_POINT('Ctrl Pts',(-142.802118691822,-4.67829364191574,
129.278719763172));
#109888=CARTESIAN_POINT('Ctrl Pts',(-142.811098012714,-4.72483570086139,
129.429576506611));
#109889=CARTESIAN_POINT('Ctrl Pts',(-142.820077333605,-4.76405452823405,
129.582490119308));
#109890=CARTESIAN_POINT('Origin',(213.235140564004,0.,130.804360617566));
#109891=CARTESIAN_POINT('',(-144.915004217899,-4.7640545282341,129.582490119308));
#109892=CARTESIAN_POINT('',(-144.570016427913,-4.76405452823402,129.582490119308));
#109893=CARTESIAN_POINT('',(213.235140564004,-4.76405452823405,129.582490119308));
#109894=CARTESIAN_POINT('',(-143.235140564011,-4.91565778800209,130.808061793682));
#109895=CARTESIAN_POINT('Ctrl Pts',(-143.235140564011,-4.91824860589129,
130.808063744402));
#109896=CARTESIAN_POINT('Ctrl Pts',(-143.244096688567,-4.91812913868428,
130.966732202243));
#109897=CARTESIAN_POINT('Ctrl Pts',(-143.253052813123,-4.91032750956385,
131.125085964154));
#109898=CARTESIAN_POINT('Ctrl Pts',(-143.262008937679,-4.89495850831957,
131.282444568698));
#109899=CARTESIAN_POINT('Ctrl Pts',(-143.271013498197,-4.8795063893897,
131.440654190352));
#109900=CARTESIAN_POINT('Ctrl Pts',(-143.280018058714,-4.8564049360629,
131.597857740923));
#109901=CARTESIAN_POINT('Ctrl Pts',(-143.289022619231,-4.82582010225577,
131.753382958275));
#109902=CARTESIAN_POINT('Ctrl Pts',(-143.298086497441,-4.79503379034313,
131.909932700604));
#109903=CARTESIAN_POINT('Ctrl Pts',(-143.307150375652,-4.75666526286325,
132.064781806234));
#109904=CARTESIAN_POINT('Ctrl Pts',(-143.316214253862,-4.71093213517195,
132.217265950667));
#109905=CARTESIAN_POINT('Ctrl Pts',(-143.320958043375,-4.68699664900692,
132.297072041212));
#109906=CARTESIAN_POINT('Ctrl Pts',(-143.325701832887,-4.66104464757951,
132.376230686379));
#109907=CARTESIAN_POINT('Ctrl Pts',(-143.3304456224,-4.63311244679749,132.4546491129));
#109908=CARTESIAN_POINT('Ctrl Pts',(-143.338219956519,-4.58733590865378,
132.583164732589));
#109909=CARTESIAN_POINT('Ctrl Pts',(-143.345994290638,-4.53613556432417,
132.709977809174));
#109910=CARTESIAN_POINT('Ctrl Pts',(-143.353768624757,-4.47965681453224,
132.834596536496));
#109911=CARTESIAN_POINT('Ctrl Pts',(-143.361533377704,-4.42324766975178,
132.959061682375));
#109912=CARTESIAN_POINT('Ctrl Pts',(-143.369298130651,-4.36157322268416,
133.081337507139));
#109913=CARTESIAN_POINT('Ctrl Pts',(-143.377062883598,-4.29482825956732,
133.200948459336));
#109914=CARTESIAN_POINT('Ctrl Pts',(-143.384819924483,-4.22814958848879,
133.32044061225));
#109915=CARTESIAN_POINT('Ctrl Pts',(-143.392576965368,-4.15641061272182,
133.437272820626));
#109916=CARTESIAN_POINT('Ctrl Pts',(-143.400334006253,-4.07985355850699,
133.55099091734));
#109917=CARTESIAN_POINT('Ctrl Pts',(-143.408085197493,-4.00335423656216,
133.664623258353));
#109918=CARTESIAN_POINT('Ctrl Pts',(-143.415836388733,-3.92204428558689,
133.775145838996));
#109919=CARTESIAN_POINT('Ctrl Pts',(-143.423587579973,-3.83621088624211,
133.88213076798));
#109920=CARTESIAN_POINT('Ctrl Pts',(-143.43133547675,-3.75041396838162,
133.989070225515));
#109921=CARTESIAN_POINT('Ctrl Pts',(-143.439083373527,-3.6600976701772,
134.092474717616));
#109922=CARTESIAN_POINT('Ctrl Pts',(-143.446831270304,-3.56559122091009,
134.191947119468));
#109923=CARTESIAN_POINT('Ctrl Pts',(-143.454577546388,-3.47110454035511,
134.291398713838));
#109924=CARTESIAN_POINT('Ctrl Pts',(-143.462323822473,-3.37242972124061,
134.386919570714));
#109925=CARTESIAN_POINT('Ctrl Pts',(-143.470070098557,-3.26993456670635,
134.478147627173));
#109926=CARTESIAN_POINT('Ctrl Pts',(-143.477816431822,-3.167438655576,134.569376357057));
#109927=CARTESIAN_POINT('Ctrl Pts',(-143.485562765087,-3.06112264479254,
134.656311963356));
#109928=CARTESIAN_POINT('Ctrl Pts',(-143.493309098353,-2.95138898982712,
134.738631336928));
#109929=CARTESIAN_POINT('Ctrl Pts',(-143.501057166356,-2.84163076077066,
134.820969145352));
#109930=CARTESIAN_POINT('Ctrl Pts',(-143.508805234359,-2.72845367724512,
134.898688429391));
#109931=CARTESIAN_POINT('Ctrl Pts',(-143.516553302362,-2.61229052530956,
134.971508475979));
#109932=CARTESIAN_POINT('Ctrl Pts',(-143.524309605103,-2.4960039137936,
135.04440591658));
#109933=CARTESIAN_POINT('Ctrl Pts',(-143.532065907845,-2.37672522598798,
135.112393510263));
#109934=CARTESIAN_POINT('Ctrl Pts',(-143.539822210587,-2.25491377154477,
135.17523546654));
#109935=CARTESIAN_POINT('Ctrl Pts',(-143.547582653101,-2.13303730266066,
135.238110963463));
#109936=CARTESIAN_POINT('Ctrl Pts',(-143.555343095615,-2.00862572801258,
135.295835186113));
#109937=CARTESIAN_POINT('Ctrl Pts',(-143.56310353813,-1.88215892542903,
135.348220303112));
#109938=CARTESIAN_POINT('Ctrl Pts',(-143.570876438395,-1.75548910710677,
135.400689513351));
#109939=CARTESIAN_POINT('Ctrl Pts',(-143.57864933866,-1.62675783528844,
135.44780235629));
#109940=CARTESIAN_POINT('Ctrl Pts',(-143.586422238926,-1.49646160878872,
135.489420458798));
#109941=CARTESIAN_POINT('Ctrl Pts',(-143.593912574688,-1.37090197831902,
135.529525638449));
#109942=CARTESIAN_POINT('Ctrl Pts',(-143.60140291045,-1.24388949481631,
135.56452855532));
#109943=CARTESIAN_POINT('Ctrl Pts',(-143.608893246212,-1.1158759978454,
135.594350577882));
#109944=CARTESIAN_POINT('Ctrl Pts',(-143.616667580331,-0.983008830228136,
135.625303311494));
#109945=CARTESIAN_POINT('Ctrl Pts',(-143.62444191445,-0.848642360616826,
135.650772577217));
#109946=CARTESIAN_POINT('Ctrl Pts',(-143.632216248569,-0.713268952102007,
135.670614871555));
#109947=CARTESIAN_POINT('Ctrl Pts',(-143.639981001516,-0.578062379214514,
135.690432712039));
#109948=CARTESIAN_POINT('Ctrl Pts',(-143.647745754463,-0.441851719686798,
135.704637323049));
#109949=CARTESIAN_POINT('Ctrl Pts',(-143.65551050741,-0.305142355144324,
135.713135536586));
#109950=CARTESIAN_POINT('Ctrl Pts',(-143.663267548295,-0.168568772269607,
135.721625309577));
#109951=CARTESIAN_POINT('Ctrl Pts',(-143.67102458918,-0.0314978577779321,
135.724419939924));
#109952=CARTESIAN_POINT('Ctrl Pts',(-143.678781630065,0.105557355464807,
135.721477730998));
#109953=CARTESIAN_POINT('Ctrl Pts',(-143.686532821305,0.24250921430492,
135.718537740815));
#109954=CARTESIAN_POINT('Ctrl Pts',(-143.694284012545,0.379445006170189,
135.709869530744));
#109955=CARTESIAN_POINT('Ctrl Pts',(-143.702035203785,0.515849505837805,
135.695483428315));
#109956=CARTESIAN_POINT('Ctrl Pts',(-143.709783100562,0.652196029954167,
135.681103440363));
#109957=CARTESIAN_POINT('Ctrl Pts',(-143.717530997339,0.788011323003643,
135.66101043457));
#109958=CARTESIAN_POINT('Ctrl Pts',(-143.725278894116,0.92278331616353,
135.63526674519));
#109959=CARTESIAN_POINT('Ctrl Pts',(-143.733025170201,1.0575271179278,135.609528440834));
#109960=CARTESIAN_POINT('Ctrl Pts',(-143.740771446285,1.19122767010683,
135.578141877266));
#109961=CARTESIAN_POINT('Ctrl Pts',(-143.748517722369,1.32338155232788,
135.541220793828));
#109962=CARTESIAN_POINT('Ctrl Pts',(-143.756264055634,1.45553641007868,
135.504299437848));
#109963=CARTESIAN_POINT('Ctrl Pts',(-143.764010388899,1.58614419854334,
135.461843585675));
#109964=CARTESIAN_POINT('Ctrl Pts',(-143.771756722165,1.71471553983686,
135.414017186112));
#109965=CARTESIAN_POINT('Ctrl Pts',(-143.779504790168,1.84331567379099,
135.366180076159));
#109966=CARTESIAN_POINT('Ctrl Pts',(-143.78725285817,1.96987808672668,135.31297016187));
#109967=CARTESIAN_POINT('Ctrl Pts',(-143.795000926173,2.09393267535656,
135.254599826145));
#109968=CARTESIAN_POINT('Ctrl Pts',(-143.802757228915,2.21811911067933,
135.196167453733));
#109969=CARTESIAN_POINT('Ctrl Pts',(-143.810513531657,2.33979204305571,
135.132563870609));
#109970=CARTESIAN_POINT('Ctrl Pts',(-143.818269834399,2.45850482718562,
135.064048056476));
#109971=CARTESIAN_POINT('Ctrl Pts',(-143.826030276913,2.57728097190311,
134.995495673389));
#109972=CARTESIAN_POINT('Ctrl Pts',(-143.833790719427,2.69309349027285,
134.922026044454));
#109973=CARTESIAN_POINT('Ctrl Pts',(-143.841551161941,2.80552496874744,
134.84394137703));
#109974=CARTESIAN_POINT('Ctrl Pts',(-143.849324062206,2.91813693221248,
134.765731361167));
#109975=CARTESIAN_POINT('Ctrl Pts',(-143.857096962472,3.02735669813637,
134.682891738731));
#109976=CARTESIAN_POINT('Ctrl Pts',(-143.864869862737,3.13279947954752,
134.59576543418));
#109977=CARTESIAN_POINT('Ctrl Pts',(-143.8723601985,3.23440915026375,134.511806390255));
#109978=CARTESIAN_POINT('Ctrl Pts',(-143.879850534262,3.33251144535074,
134.423867122263));
#109979=CARTESIAN_POINT('Ctrl Pts',(-143.887340870024,3.42679597955594,
134.332285273366));
#109980=CARTESIAN_POINT('Ctrl Pts',(-143.895115204143,3.52465534052926,
134.237231070835));
#109981=CARTESIAN_POINT('Ctrl Pts',(-143.902889538262,3.61871171401717,
134.137951514739));
#109982=CARTESIAN_POINT('Ctrl Pts',(-143.910663872381,3.70857823218911,
134.034783276946));
#109983=CARTESIAN_POINT('Ctrl Pts',(-143.918428625328,3.79833399790901,
133.931742184785));
#109984=CARTESIAN_POINT('Ctrl Pts',(-143.926193378276,3.88390992805215,
133.824822238455));
#109985=CARTESIAN_POINT('Ctrl Pts',(-143.933958131223,3.96495446663007,
133.714398270252));
#109986=CARTESIAN_POINT('Ctrl Pts',(-143.941715172108,4.04591851062975,
133.604083976691));
#109987=CARTESIAN_POINT('Ctrl Pts',(-143.949472212993,4.12235988971488,
133.490272900244));
#109988=CARTESIAN_POINT('Ctrl Pts',(-143.957229253878,4.19396621653495,
133.373374131945));
#109989=CARTESIAN_POINT('Ctrl Pts',(-143.964980445118,4.26551854446704,
133.256563517917));
#109990=CARTESIAN_POINT('Ctrl Pts',(-143.972731636358,4.33224287418394,
133.136670178721));
#109991=CARTESIAN_POINT('Ctrl Pts',(-143.980482827598,4.39386940271056,
133.014133170211));
#109992=CARTESIAN_POINT('Ctrl Pts',(-143.988230724375,4.45546973831852,
132.891648243199));
#109993=CARTESIAN_POINT('Ctrl Pts',(-143.995978621152,4.51197640684717,
132.766522230237));
#109994=CARTESIAN_POINT('Ctrl Pts',(-144.003726517929,4.56316506616442,
132.639219642515));
#109995=CARTESIAN_POINT('Ctrl Pts',(-144.011472794013,4.61434301791764,
132.51194368375));
#109996=CARTESIAN_POINT('Ctrl Pts',(-144.019219070097,4.6602050273441,132.382492418337));
#109997=CARTESIAN_POINT('Ctrl Pts',(-144.026965346182,4.70057467556714,
132.251350866986));
#109998=CARTESIAN_POINT('Ctrl Pts',(-144.034711679447,4.7409446217897,132.120208347578));
#109999=CARTESIAN_POINT('Ctrl Pts',(-144.042458012712,4.77582201088228,
131.987375890996));
#110000=CARTESIAN_POINT('Ctrl Pts',(-144.050204345977,4.8050802569149,131.853353843048));
#110001=CARTESIAN_POINT('Ctrl Pts',(-144.05795241398,4.83434505512889,131.719301781791));
#110002=CARTESIAN_POINT('Ctrl Pts',(-144.065700481983,4.85798812290462,
131.584059980956));
#110003=CARTESIAN_POINT('Ctrl Pts',(-144.073448549986,4.87593404168169,
131.448138749899));
#110004=CARTESIAN_POINT('Ctrl Pts',(-144.081204852728,4.89389903359476,
131.31207306014));
#110005=CARTESIAN_POINT('Ctrl Pts',(-144.08896115547,4.90615472974164,131.175326885892));
#110006=CARTESIAN_POINT('Ctrl Pts',(-144.096717458212,4.91267759438521,
131.038415987352));
#110007=CARTESIAN_POINT('Ctrl Pts',(-144.104477900726,4.91920394047805,
130.901432015342));
#110008=CARTESIAN_POINT('Ctrl Pts',(-144.11223834324,4.91999135594377,130.764283534621));
#110009=CARTESIAN_POINT('Ctrl Pts',(-144.119998785755,4.91506847417433,
130.627485077489));
#110010=CARTESIAN_POINT('Ctrl Pts',(-144.12777168602,4.91013768975805,130.490467019329));
#110011=CARTESIAN_POINT('Ctrl Pts',(-144.135544586285,4.89947832058561,
130.353800497595));
#110012=CARTESIAN_POINT('Ctrl Pts',(-144.143317486551,4.88317089195754,
130.217994603511));
#110013=CARTESIAN_POINT('Ctrl Pts',(-144.150807822313,4.8674562794359,130.08712559575));
#110014=CARTESIAN_POINT('Ctrl Pts',(-144.158298158075,4.84649716948137,
129.95705603411));
#110015=CARTESIAN_POINT('Ctrl Pts',(-144.165788493837,4.82040986003761,
129.828229558869));
#110016=CARTESIAN_POINT('Ctrl Pts',(-144.173562827956,4.79333344232742,
129.694518588665));
#110017=CARTESIAN_POINT('Ctrl Pts',(-144.181337162075,4.76064650736517,
129.561723272727));
#110018=CARTESIAN_POINT('Ctrl Pts',(-144.189111496194,4.72242319521703,
129.430351073285));
#110019=CARTESIAN_POINT('Ctrl Pts',(-144.196876249141,4.68424698988499,
129.299140778337));
#110020=CARTESIAN_POINT('Ctrl Pts',(-144.204641002089,4.6405480914579,129.169350482015));
#110021=CARTESIAN_POINT('Ctrl Pts',(-144.212405755036,4.59145183236326,
129.04147856434));
#110022=CARTESIAN_POINT('Ctrl Pts',(-144.220162795921,4.54240433636529,
128.913733650855));
#110023=CARTESIAN_POINT('Ctrl Pts',(-144.227919836806,4.48797028703326,
128.787903686889));
#110024=CARTESIAN_POINT('Ctrl Pts',(-144.235676877691,4.4283250112462,128.664472616461));
#110025=CARTESIAN_POINT('Ctrl Pts',(-144.243428068931,4.36872471442565,
128.541134626365));
#110026=CARTESIAN_POINT('Ctrl Pts',(-144.251179260171,4.30392118264851,
128.42019227965));
#110027=CARTESIAN_POINT('Ctrl Pts',(-144.258930451411,4.23413797094092,
128.302109889614));
#110028=CARTESIAN_POINT('Ctrl Pts',(-144.266678348188,4.16438441895973,
128.184077687744));
#110029=CARTESIAN_POINT('Ctrl Pts',(-144.274426244965,4.08965559509321,
128.068903360779));
#110030=CARTESIAN_POINT('Ctrl Pts',(-144.282174141742,4.01022104335957,
127.957026733755));
#110031=CARTESIAN_POINT('Ctrl Pts',(-144.289920417827,3.93080310762173,
127.84517350891));
#110032=CARTESIAN_POINT('Ctrl Pts',(-144.297666693911,3.84668162811568,
127.736616930521));
#110033=CARTESIAN_POINT('Ctrl Pts',(-144.305412969995,3.75816930778995,
127.631767590327));
#110034=CARTESIAN_POINT('Ctrl Pts',(-144.31315930326,3.66965633408651,127.526917476159));
#110035=CARTESIAN_POINT('Ctrl Pts',(-144.320905636525,3.57675270708537,
127.425774953541));
#110036=CARTESIAN_POINT('Ctrl Pts',(-144.328651969791,3.47981095909716,
127.32871697193));
#110037=CARTESIAN_POINT('Ctrl Pts',(-144.336400037794,3.38284750167649,
127.231637254858));
#110038=CARTESIAN_POINT('Ctrl Pts',(-144.344148105797,3.28184440003372,
127.138644175515));
#110039=CARTESIAN_POINT('Ctrl Pts',(-144.3518961738,3.17719022630799,127.050077020346));
#110040=CARTESIAN_POINT('Ctrl Pts',(-144.359652476542,3.07242482488117,
126.961415734951));
#110041=CARTESIAN_POINT('Ctrl Pts',(-144.367408779284,2.96400089876291,
126.877190023291));
#110042=CARTESIAN_POINT('Ctrl Pts',(-144.375165082025,2.85233964997165,
126.797698467634));
#110043=CARTESIAN_POINT('Ctrl Pts',(-144.38292552454,2.74061880420985,126.718164484939));
#110044=CARTESIAN_POINT('Ctrl Pts',(-144.390685967054,2.62565752042557,
126.64336990614));
#110045=CARTESIAN_POINT('Ctrl Pts',(-144.398446409568,2.50790416626174,
126.573568758428));
#110046=CARTESIAN_POINT('Ctrl Pts',(-144.406219309834,2.38996178395983,
126.503655559717));
#110047=CARTESIAN_POINT('Ctrl Pts',(-144.413992210099,2.26921871922076,
126.438751995629));
#110048=CARTESIAN_POINT('Ctrl Pts',(-144.421765110364,2.14614681079986,
126.379065494188));
#110049=CARTESIAN_POINT('Ctrl Pts',(-144.429255446126,2.02754887625214,
126.321548747417));
#110050=CARTESIAN_POINT('Ctrl Pts',(-144.436745781888,1.90678875940073,
126.268876465024));
#110051=CARTESIAN_POINT('Ctrl Pts',(-144.44423611765,1.78430256925667,126.221190600662));
#110052=CARTESIAN_POINT('Ctrl Pts',(-144.452010451769,1.65717227798209,
126.171696712259));
#110053=CARTESIAN_POINT('Ctrl Pts',(-144.459784785888,1.52777973095445,
126.127418044414));
#110054=CARTESIAN_POINT('Ctrl Pts',(-144.467559120007,1.39659194503779,
126.088566516722));
#110055=CARTESIAN_POINT('Ctrl Pts',(-144.475323872955,1.26556583634267,
126.049762870066));
#110056=CARTESIAN_POINT('Ctrl Pts',(-144.483088625902,1.13274926219005,
126.016373165463));
#110057=CARTESIAN_POINT('Ctrl Pts',(-144.490853378849,0.998629269045308,
125.988561343769));
#110058=CARTESIAN_POINT('Ctrl Pts',(-144.498610419734,0.86464248576852,
125.960777145168));
#110059=CARTESIAN_POINT('Ctrl Pts',(-144.506367460619,0.729355240104424,
125.938559883432));
#110060=CARTESIAN_POINT('Ctrl Pts',(-144.514124501504,0.593269456324948,
125.922023634656));
#110061=CARTESIAN_POINT('Ctrl Pts',(-144.521875692744,0.457286295893428,
125.905499855994));
#110062=CARTESIAN_POINT('Ctrl Pts',(-144.529626883984,0.320506182496859,
125.894648610029));
#110063=CARTESIAN_POINT('Ctrl Pts',(-144.537378075224,0.183440593014859,
125.889532786265));
#110064=CARTESIAN_POINT('Ctrl Pts',(-144.545125972001,0.0464332600652932,
125.884419136862));
#110065=CARTESIAN_POINT('Ctrl Pts',(-144.552873868778,-0.0908589177685185,
125.885036075798));
#110066=CARTESIAN_POINT('Ctrl Pts',(-144.560621765556,-0.227920208102862,
125.891394564229));
#110067=CARTESIAN_POINT('Ctrl Pts',(-144.56836804164,-0.364952828170341,
125.897751722602));
#110068=CARTESIAN_POINT('Ctrl Pts',(-144.576114317724,-0.501754266505367,
125.909848023494));
#110069=CARTESIAN_POINT('Ctrl Pts',(-144.583860593808,-0.637810057067511,
125.927642315921));
#110070=CARTESIAN_POINT('Ctrl Pts',(-144.591606927073,-0.773866851962038,
125.945436739701));
#110071=CARTESIAN_POINT('Ctrl Pts',(-144.599353260339,-0.909177600436715,
125.968929188245));
#110072=CARTESIAN_POINT('Ctrl Pts',(-144.607099593604,-1.04323461191162,
125.998026816527));
#110073=CARTESIAN_POINT('Ctrl Pts',(-144.614847661607,-1.17732164452531,
126.027130961021));
#110074=CARTESIAN_POINT('Ctrl Pts',(-144.62259572961,-1.3101539994524,126.061842700123));
#110075=CARTESIAN_POINT('Ctrl Pts',(-144.630343797613,-1.44123619266726,
126.102018509696));
#110076=CARTESIAN_POINT('Ctrl Pts',(-144.638100100355,-1.57245770159679,
126.142237018598));
#110077=CARTESIAN_POINT('Ctrl Pts',(-144.645856403097,-1.70192495868042,
126.187931083887));
#110078=CARTESIAN_POINT('Ctrl Pts',(-144.653612705838,-1.82915908822223,
126.238907727384));
#110079=CARTESIAN_POINT('Ctrl Pts',(-144.661373148353,-1.95646112645026,
126.28991157865));
#110080=CARTESIAN_POINT('Ctrl Pts',(-144.669133590867,-2.08152730585766,
126.34620346577));
#110081=CARTESIAN_POINT('Ctrl Pts',(-144.676894033381,-2.20390155251043,
126.40754347225));
#110082=CARTESIAN_POINT('Ctrl Pts',(-144.684666933646,-2.32647224516746,
126.468981947154));
#110083=CARTESIAN_POINT('Ctrl Pts',(-144.692439833912,-2.44634202760384,
126.535484545392));
#110084=CARTESIAN_POINT('Ctrl Pts',(-144.700212734177,-2.56308134437499,
126.606766415572));
#110085=CARTESIAN_POINT('Ctrl Pts',(-144.70770306994,-2.6755768929348,126.675457010223));
#110086=CARTESIAN_POINT('Ctrl Pts',(-144.715193405702,-2.78516536876059,
126.748585261411));
#110087=CARTESIAN_POINT('Ctrl Pts',(-144.722683741464,-2.89149161464991,
126.825860987692));
#110088=CARTESIAN_POINT('Ctrl Pts',(-144.730697094649,-3.00524215777342,
126.908532540338));
#110089=CARTESIAN_POINT('Ctrl Pts',(-144.738710447833,-3.11564733037586,
126.996234191182));
#110090=CARTESIAN_POINT('Ctrl Pts',(-144.746723801018,-3.22222827438724,
127.088660412996));
#110091=CARTESIAN_POINT('Ctrl Pts',(-144.754420725515,-3.32460058470019,
127.177436938185));
#110092=CARTESIAN_POINT('Ctrl Pts',(-144.762117650012,-3.4234445500382,
127.270571761214));
#110093=CARTESIAN_POINT('Ctrl Pts',(-144.769814574509,-3.51836411176413,
127.36774934488));
#110094=CARTESIAN_POINT('Ctrl Pts',(-144.777504538288,-3.61319783293093,
127.464839045944));
#110095=CARTESIAN_POINT('Ctrl Pts',(-144.785194502067,-3.70411393179018,
127.565963954223));
#110096=CARTESIAN_POINT('Ctrl Pts',(-144.792884465846,-3.79075008511641,
127.670768931547));
#110097=CARTESIAN_POINT('Ctrl Pts',(-144.800569212024,-3.87732745624877,
127.775502799221));
#110098=CARTESIAN_POINT('Ctrl Pts',(-144.808253958201,-3.95963040542177,
127.883911463481));
#110099=CARTESIAN_POINT('Ctrl Pts',(-144.815938704378,-4.03733444998907,
127.995604024084));
#110100=CARTESIAN_POINT('Ctrl Pts',(-144.823619971739,-4.11500331862091,
128.107246022449));
#110101=CARTESIAN_POINT('Ctrl Pts',(-144.831301239099,-4.18807719852429,
128.22216863258));
#110102=CARTESIAN_POINT('Ctrl Pts',(-144.83898250646,-4.25627310309848,
128.339949463895));
#110103=CARTESIAN_POINT('Ctrl Pts',(-144.846663330622,-4.32446507286651,
128.457723499424));
#110104=CARTESIAN_POINT('Ctrl Pts',(-144.854344154785,-4.38777942079224,
128.578355087569));
#110105=CARTESIAN_POINT('Ctrl Pts',(-144.862024978947,-4.44597769891592,
128.701394768285));
#110106=CARTESIAN_POINT('Ctrl Pts',(-144.869705608028,-4.50417449889121,
128.824431323979));
#110107=CARTESIAN_POINT('Ctrl Pts',(-144.877386237109,-4.55725532290773,
128.949875487892));
#110108=CARTESIAN_POINT('Ctrl Pts',(-144.88506686619,-4.60502904888281,
129.077255953266));
#110109=CARTESIAN_POINT('Ctrl Pts',(-144.892750950078,-4.65282426384832,
129.204693715357));
#110110=CARTESIAN_POINT('Ctrl Pts',(-144.900435033965,-4.69530748152023,
129.334069142459));
#110111=CARTESIAN_POINT('Ctrl Pts',(-144.908119117852,-4.73233685550399,
129.46489395186));
#110112=CARTESIAN_POINT('Ctrl Pts',(-144.910414151201,-4.7433965536316,
129.503967874638));
#110113=CARTESIAN_POINT('Ctrl Pts',(-144.91270918455,-4.75397007818319,
129.543171001613));
#110114=CARTESIAN_POINT('Ctrl Pts',(-144.915004217899,-4.7640545282341,
129.582490119308));
#110115=CARTESIAN_POINT('Ctrl Pts',(-143.165347877338,-4.75725076560214,
129.584194750691));
#110116=CARTESIAN_POINT('Ctrl Pts',(-143.188612106229,-4.85769505085557,
129.983938621581));
#110117=CARTESIAN_POINT('Ctrl Pts',(-143.21187633512,-4.91040493875306,
130.396321313897));
#110118=CARTESIAN_POINT('Ctrl Pts',(-143.235140564011,-4.91326838458752,
130.808059994614));
#110119=CARTESIAN_POINT('',(-142.889859435939,-4.91824866801256,130.80074093627));
#110120=CARTESIAN_POINT('Ctrl Pts',(-142.820077333605,-4.76405452823405,
129.582490119308));
#110121=CARTESIAN_POINT('Ctrl Pts',(-142.829056384281,-4.80327217539394,
129.735399130374));
#110122=CARTESIAN_POINT('Ctrl Pts',(-142.838035434958,-4.83516690740692,
129.890364784401));
#110123=CARTESIAN_POINT('Ctrl Pts',(-142.847014485634,-4.85954511673974,
130.046729888998));
#110124=CARTESIAN_POINT('Ctrl Pts',(-142.855924747846,-4.88373656472607,
130.201897081267));
#110125=CARTESIAN_POINT('Ctrl Pts',(-142.864835010057,-4.90052613806173,
130.358442230497));
#110126=CARTESIAN_POINT('Ctrl Pts',(-142.873745272269,-4.90977189919264,
130.515703449981));
#110127=CARTESIAN_POINT('Ctrl Pts',(-142.879116660159,-4.91534553644312,
130.610505487213));
#110128=CARTESIAN_POINT('Ctrl Pts',(-142.884488048049,-4.91817862317039,
130.705567377168));
#110129=CARTESIAN_POINT('Ctrl Pts',(-142.889859435939,-4.91824866801256,
130.800740936271));
#110130=CARTESIAN_POINT('Ctrl Pts',(-142.889859435993,-4.91824866801326,
130.800740937229));
#110131=CARTESIAN_POINT('Ctrl Pts',(-142.89762022287,-4.91834987145624,
130.938251339318));
#110132=CARTESIAN_POINT('Ctrl Pts',(-142.905381009747,-4.91267973923835,
131.075815413098));
#110133=CARTESIAN_POINT('Ctrl Pts',(-142.913141796625,-4.90125152276576,
131.212914864988));
#110134=CARTESIAN_POINT('Ctrl Pts',(-142.920901939177,-4.88982425510002,
131.350002934445));
#110135=CARTESIAN_POINT('Ctrl Pts',(-142.928662081729,-4.87263988591247,
131.486626071592));
#110136=CARTESIAN_POINT('Ctrl Pts',(-142.936422224281,-4.84976366603659,
131.622269809403));
#110137=CARTESIAN_POINT('Ctrl Pts',(-142.944183376621,-4.82688446939635,
131.757931197833));
#110138=CARTESIAN_POINT('Ctrl Pts',(-142.95194452896,-4.79831201220062,
131.892612550079));
#110139=CARTESIAN_POINT('Ctrl Pts',(-142.959705681299,-4.76416285473462,
132.025808674614));
#110140=CARTESIAN_POINT('Ctrl Pts',(-142.967469497837,-4.73000197476788,
132.159050521849));
#110141=CARTESIAN_POINT('Ctrl Pts',(-142.975233314374,-4.69026068064949,
132.290805750421));
#110142=CARTESIAN_POINT('Ctrl Pts',(-142.982997130911,-4.64510556720512,
132.420583786568));
#110143=CARTESIAN_POINT('Ctrl Pts',(-142.990770247241,-4.599896365257,132.550517275758));
#110144=CARTESIAN_POINT('Ctrl Pts',(-142.998543363572,-4.54926051948765,
132.678468474795));
#110145=CARTESIAN_POINT('Ctrl Pts',(-143.006316479902,-4.4934132428636,
132.803965701416));
#110146=CARTESIAN_POINT('Ctrl Pts',(-143.014094506739,-4.43753068587032,
132.929542208331));
#110147=CARTESIAN_POINT('Ctrl Pts',(-143.021872533576,-4.37643031110508,
133.052661306647));
#110148=CARTESIAN_POINT('Ctrl Pts',(-143.029650560413,-4.31037313362153,
133.17287629441));
#110149=CARTESIAN_POINT('Ctrl Pts',(-143.037441425418,-4.24420692422634,
133.293289705272));
#110150=CARTESIAN_POINT('Ctrl Pts',(-143.045232290423,-4.17306776748978,
133.410789096853));
#110151=CARTESIAN_POINT('Ctrl Pts',(-143.053023155428,-4.09726026937177,
133.524956388262));
#110152=CARTESIAN_POINT('Ctrl Pts',(-143.059211101867,-4.03704965890129,
133.615634520137));
#110153=CARTESIAN_POINT('Ctrl Pts',(-143.065399048306,-3.97389493110227,
133.704211170842));
#110154=CARTESIAN_POINT('Ctrl Pts',(-143.071586994745,-3.90796609425353,
133.790492575244));
#110155=CARTESIAN_POINT('Ctrl Pts',(-143.079361328864,-3.82513525355506,
133.898893718126));
#110156=CARTESIAN_POINT('Ctrl Pts',(-143.087135662983,-3.73765946788447,
134.004017543083));
#110157=CARTESIAN_POINT('Ctrl Pts',(-143.094909997102,-3.64582736016016,
134.105440126213));
#110158=CARTESIAN_POINT('Ctrl Pts',(-143.102674750049,-3.55410842730135,
134.206737715073));
#110159=CARTESIAN_POINT('Ctrl Pts',(-143.110439502996,-3.45804411454878,
134.304342850995));
#110160=CARTESIAN_POINT('Ctrl Pts',(-143.118204255943,-3.35796510878766,
134.397862167679));
#110161=CARTESIAN_POINT('Ctrl Pts',(-143.125961296828,-3.25798550290592,
134.491288599659));
#110162=CARTESIAN_POINT('Ctrl Pts',(-143.133718337713,-3.1539994230293,
134.580637022982));
#110163=CARTESIAN_POINT('Ctrl Pts',(-143.141475378598,-3.04637620115051,
134.665548919574));
#110164=CARTESIAN_POINT('Ctrl Pts',(-143.149226569839,-2.9388341387798,
134.750396783445));
#110165=CARTESIAN_POINT('Ctrl Pts',(-143.156977761079,-2.82766069947265,
134.830814538652));
#110166=CARTESIAN_POINT('Ctrl Pts',(-143.164728952319,-2.71325999989535,
134.906482414328));
#110167=CARTESIAN_POINT('Ctrl Pts',(-143.172476849096,-2.5989079236679,
134.982118129137));
#110168=CARTESIAN_POINT('Ctrl Pts',(-143.180224745873,-2.48133164072702,
135.053007764472));
#110169=CARTESIAN_POINT('Ctrl Pts',(-143.18797264265,-2.36096591422859,
135.118873685613));
#110170=CARTESIAN_POINT('Ctrl Pts',(-143.195718918734,-2.24062536564535,
135.184725829024));
#110171=CARTESIAN_POINT('Ctrl Pts',(-143.203465194818,-2.11749687685625,
135.245556160885));
#110172=CARTESIAN_POINT('Ctrl Pts',(-143.211211470902,-1.99204123713972,
135.301132211947));
#110173=CARTESIAN_POINT('Ctrl Pts',(-143.218957804168,-1.86658467133833,
135.35670867326));
#110174=CARTESIAN_POINT('Ctrl Pts',(-143.226704137433,-1.73880127779179,
135.407030618027));
#110175=CARTESIAN_POINT('Ctrl Pts',(-143.234450470698,-1.60917294931547,
135.451913251124));
#110176=CARTESIAN_POINT('Ctrl Pts',(-143.242198538701,-1.4795155914736,
135.496805935375));
#110177=CARTESIAN_POINT('Ctrl Pts',(-143.249946606704,-1.34801284593662,
135.536256756192));
#110178=CARTESIAN_POINT('Ctrl Pts',(-143.257694674707,-1.2151625426437,
135.570130550898));
#110179=CARTESIAN_POINT('Ctrl Pts',(-143.265450977449,-1.08217104446732,
135.604040347077));
#110180=CARTESIAN_POINT('Ctrl Pts',(-143.273207280191,-0.947829507008607,
135.632361179915));
#110181=CARTESIAN_POINT('Ctrl Pts',(-143.280963582933,-0.812647300709287,
135.655008762624));
#110182=CARTESIAN_POINT('Ctrl Pts',(-143.288724025447,-0.677392943596207,
135.677668433028));
#110183=CARTESIAN_POINT('Ctrl Pts',(-143.296484467961,-0.541297411356543,
135.694648771407));
#110184=CARTESIAN_POINT('Ctrl Pts',(-143.304244910475,-0.404875016760093,
135.705917439975));
#110185=CARTESIAN_POINT('Ctrl Pts',(-143.312017810741,-0.268233624824826,
135.71720419801));
#110186=CARTESIAN_POINT('Ctrl Pts',(-143.319790711006,-0.131264712866735,
135.722760948034));
#110187=CARTESIAN_POINT('Ctrl Pts',(-143.327563611272,0.00551668044895405,
135.722607523602));
#110188=CARTESIAN_POINT('Ctrl Pts',(-143.335053947034,0.137325725590153,
135.722459676535));
#110189=CARTESIAN_POINT('Ctrl Pts',(-143.342544282796,0.268960341185616,
135.717009618442));
#110190=CARTESIAN_POINT('Ctrl Pts',(-143.350034618558,0.399966256337925,
135.706320435464));
#110191=CARTESIAN_POINT('Ctrl Pts',(-143.357808952677,0.535939300577972,
135.695225968866));
#110192=CARTESIAN_POINT('Ctrl Pts',(-143.365583286796,0.671665750646524,
135.67845210812));
#110193=CARTESIAN_POINT('Ctrl Pts',(-143.373357620916,0.806632939619369,
135.656012538636));
#110194=CARTESIAN_POINT('Ctrl Pts',(-143.381122373863,0.941433793593803,
135.633600623916));
#110195=CARTESIAN_POINT('Ctrl Pts',(-143.38888712681,1.07547686631057,135.605536957018));
#110196=CARTESIAN_POINT('Ctrl Pts',(-143.396651879757,1.20825246322059,
135.57188713009));
#110197=CARTESIAN_POINT('Ctrl Pts',(-143.404408920642,1.34089618553632,
135.538270724644));
#110198=CARTESIAN_POINT('Ctrl Pts',(-143.412165961527,1.47227456073164,
135.499079295868));
#110199=CARTESIAN_POINT('Ctrl Pts',(-143.419923002412,1.60188632443349,
135.454429785449));
#110200=CARTESIAN_POINT('Ctrl Pts',(-143.427674193652,1.73140034689592,
135.409813945573));
#110201=CARTESIAN_POINT('Ctrl Pts',(-143.435425384892,1.85915004140789,
135.359748343491));
#110202=CARTESIAN_POINT('Ctrl Pts',(-143.443176576132,1.98464794075242,
135.304400130033));
#110203=CARTESIAN_POINT('Ctrl Pts',(-143.450924472909,2.11009250014213,
135.249075441043));
#110204=CARTESIAN_POINT('Ctrl Pts',(-143.458672369687,2.23328681093808,
135.188472763745));
#110205=CARTESIAN_POINT('Ctrl Pts',(-143.466420266464,2.35376229108314,
135.122807808348));
#110206=CARTESIAN_POINT('Ctrl Pts',(-143.474166542548,2.47421257035523,
135.057156588645));
#110207=CARTESIAN_POINT('Ctrl Pts',(-143.481912818632,2.59194480712546,
134.986445384079));
#110208=CARTESIAN_POINT('Ctrl Pts',(-143.489659094716,2.70651435057165,
134.910936214417));
#110209=CARTESIAN_POINT('Ctrl Pts',(-143.497405427982,2.82108473974403,
134.835426487363));
#110210=CARTESIAN_POINT('Ctrl Pts',(-143.505151761247,2.93249206256358,
134.755118939686));
#110211=CARTESIAN_POINT('Ctrl Pts',(-143.512898094512,3.04032037081962,
134.670319115181));
#110212=CARTESIAN_POINT('Ctrl Pts',(-143.520646162515,3.1481728264778,134.585500300343));
#110213=CARTESIAN_POINT('Ctrl Pts',(-143.528394230519,3.25244436543236,
134.496187448462));
#110214=CARTESIAN_POINT('Ctrl Pts',(-143.536142298522,3.35275218225372,
134.402726339236));
#110215=CARTESIAN_POINT('Ctrl Pts',(-143.543898601263,3.45316660741635,
134.309165898432));
#110216=CARTESIAN_POINT('Ctrl Pts',(-143.551654904005,3.54960860864155,
134.211448660141));
#110217=CARTESIAN_POINT('Ctrl Pts',(-143.559411206747,3.64173194590026,
134.109957613074));
#110218=CARTESIAN_POINT('Ctrl Pts',(-143.567171649262,3.7339044521581,134.008412397178));
#110219=CARTESIAN_POINT('Ctrl Pts',(-143.574932091776,3.82175345123784,
133.903089659139));
#110220=CARTESIAN_POINT('Ctrl Pts',(-143.58269253429,3.90497373783085,133.794404625495));
#110221=CARTESIAN_POINT('Ctrl Pts',(-143.590465434555,3.98832761701562,
133.685545120986));
#110222=CARTESIAN_POINT('Ctrl Pts',(-143.598238334821,4.06703771075116,
133.573312855313));
#110223=CARTESIAN_POINT('Ctrl Pts',(-143.606011235086,4.14084231458924,
133.458151865612));
#110224=CARTESIAN_POINT('Ctrl Pts',(-143.613501570848,4.21196393517264,
133.347177267964));
#110225=CARTESIAN_POINT('Ctrl Pts',(-143.62099190661,4.27853037202427,133.233483448261));
#110226=CARTESIAN_POINT('Ctrl Pts',(-143.628482242372,4.34034915678514,
133.117486697073));
#110227=CARTESIAN_POINT('Ctrl Pts',(-143.636256576491,4.40451181956171,
132.997091893803));
#110228=CARTESIAN_POINT('Ctrl Pts',(-143.64403091061,4.46376295702004,132.873834705931));
#110229=CARTESIAN_POINT('Ctrl Pts',(-143.651805244729,4.51783697408825,
132.748153851956));
#110230=CARTESIAN_POINT('Ctrl Pts',(-143.659569997676,4.57184434976315,
132.622627888402));
#110231=CARTESIAN_POINT('Ctrl Pts',(-143.667334750623,4.62068714698513,
132.494684557577));
#110232=CARTESIAN_POINT('Ctrl Pts',(-143.67509950357,4.66414504793186,132.364788134099));
#110233=CARTESIAN_POINT('Ctrl Pts',(-143.682856544455,4.70755978587884,
132.23502072558));
#110234=CARTESIAN_POINT('Ctrl Pts',(-143.69061358534,4.74560014777814,132.103304453141));
#110235=CARTESIAN_POINT('Ctrl Pts',(-143.698370626225,4.77809357434708,
131.970124254537));
#110236=CARTESIAN_POINT('Ctrl Pts',(-143.706121817465,4.81056249737024,
131.837044488156));
#110237=CARTESIAN_POINT('Ctrl Pts',(-143.713873008705,4.83749271875037,
131.702503371258));
#110238=CARTESIAN_POINT('Ctrl Pts',(-143.721624199946,4.85876137927811,
131.567001372926));
#110239=CARTESIAN_POINT('Ctrl Pts',(-143.729372096723,4.88002100005774,
131.431556966557));
#110240=CARTESIAN_POINT('Ctrl Pts',(-143.7371199935,4.89562378546336,131.295152876458));
#110241=CARTESIAN_POINT('Ctrl Pts',(-143.744867890277,4.9054979385556,131.158299930622));
#110242=CARTESIAN_POINT('Ctrl Pts',(-143.752614166361,4.91537002618787,
131.021475611472));
#110243=CARTESIAN_POINT('Ctrl Pts',(-143.760360442445,4.91951583688607,
130.884203013044));
#110244=CARTESIAN_POINT('Ctrl Pts',(-143.768106718529,4.91791547066745,
130.746997860748));
#110245=CARTESIAN_POINT('Ctrl Pts',(-143.775853051794,4.91631509263529,
130.609791695636));
#110246=CARTESIAN_POINT('Ctrl Pts',(-143.78359938506,4.90896845760624,130.472653368588));
#110247=CARTESIAN_POINT('Ctrl Pts',(-143.791345718325,4.89590779805969,
130.336097982501));
#110248=CARTESIAN_POINT('Ctrl Pts',(-143.799093786328,4.882844213669,130.199512015781));
#110249=CARTESIAN_POINT('Ctrl Pts',(-143.806841854331,4.86406409568915,
130.063509638907));
#110250=CARTESIAN_POINT('Ctrl Pts',(-143.814589922334,4.83965144268885,
129.9285998193));
#110251=CARTESIAN_POINT('Ctrl Pts',(-143.822346225076,4.81521284363039,
129.793546615931));
#110252=CARTESIAN_POINT('Ctrl Pts',(-143.830102527817,4.7851298209496,129.659588674749));
#110253=CARTESIAN_POINT('Ctrl Pts',(-143.837858830559,4.749537442702,129.527224312048));
#110254=CARTESIAN_POINT('Ctrl Pts',(-143.845619273073,4.71392606773046,
129.394789302502));
#110255=CARTESIAN_POINT('Ctrl Pts',(-143.853379715588,4.67279959515783,
129.263949939003));
#110256=CARTESIAN_POINT('Ctrl Pts',(-143.861140158102,4.62634239590514,
129.135187439507));
#110257=CARTESIAN_POINT('Ctrl Pts',(-143.868913058367,4.57981061943194,
129.006218239017));
#110258=CARTESIAN_POINT('Ctrl Pts',(-143.876685958633,4.5279311640038,128.87933292695));
#110259=CARTESIAN_POINT('Ctrl Pts',(-143.884458858898,4.47093615299246,
128.754991695589));
#110260=CARTESIAN_POINT('Ctrl Pts',(-143.89194919466,4.41601305419331,128.635170581185));
#110261=CARTESIAN_POINT('Ctrl Pts',(-143.899439530422,4.35634000879247,
128.517712065923));
#110262=CARTESIAN_POINT('Ctrl Pts',(-143.906929866184,4.29216321998859,
128.403003094106));
#110263=CARTESIAN_POINT('Ctrl Pts',(-143.914704200303,4.22555314873118,
128.283944896758));
#110264=CARTESIAN_POINT('Ctrl Pts',(-143.922478534422,4.15388007283489,
128.167471715966));
#110265=CARTESIAN_POINT('Ctrl Pts',(-143.930252868541,4.0773695379762,128.054044142452));
#110266=CARTESIAN_POINT('Ctrl Pts',(-143.938017621488,4.00095329551399,
127.940756358286));
#110267=CARTESIAN_POINT('Ctrl Pts',(-143.945782374435,3.91971167269818,
127.830507034183));
#110268=CARTESIAN_POINT('Ctrl Pts',(-143.953547127382,3.83391618974878,
127.723732481539));
#110269=CARTESIAN_POINT('Ctrl Pts',(-143.961304168267,3.74820592008233,
127.617063978885));
#110270=CARTESIAN_POINT('Ctrl Pts',(-143.969061209152,3.65795103447589,
127.513863682459));
#110271=CARTESIAN_POINT('Ctrl Pts',(-143.976818250037,3.56346625228798,
127.414538891973));
#110272=CARTESIAN_POINT('Ctrl Pts',(-143.984569441277,3.46905272180943,
127.315289003083));
#110273=CARTESIAN_POINT('Ctrl Pts',(-143.992320632517,3.37041591222463,
127.2199090851));
#110274=CARTESIAN_POINT('Ctrl Pts',(-144.000071823758,3.26791047394323,
127.12877301872));
#110275=CARTESIAN_POINT('Ctrl Pts',(-144.007819720535,3.16544860320739,
127.037675687598));
#110276=CARTESIAN_POINT('Ctrl Pts',(-144.015567617312,3.05912166567425,
126.950818879789));
#110277=CARTESIAN_POINT('Ctrl Pts',(-144.023315514089,2.94932062740195,
126.868539115099));
#110278=CARTESIAN_POINT('Ctrl Pts',(-144.031061790173,2.83954255713982,
126.786276561562));
#110279=CARTESIAN_POINT('Ctrl Pts',(-144.038808066257,2.72629214426961,
126.708589381085));
#110280=CARTESIAN_POINT('Ctrl Pts',(-144.046554342341,2.60999252675999,
126.635773078272));
#110281=CARTESIAN_POINT('Ctrl Pts',(-144.054300675606,2.49369205075284,
126.562956237945));
#110282=CARTESIAN_POINT('Ctrl Pts',(-144.062047008872,2.37434265656461,
126.495010554504));
#110283=CARTESIAN_POINT('Ctrl Pts',(-144.069793342137,2.25239513729084,
126.432187335546));
#110284=CARTESIAN_POINT('Ctrl Pts',(-144.07754141014,2.13042030871615,126.369350047764));
#110285=CARTESIAN_POINT('Ctrl Pts',(-144.085289478143,2.00584654476699,
126.311637686158));
#110286=CARTESIAN_POINT('Ctrl Pts',(-144.093037546146,1.87914745742925,
126.259254689676));
#110287=CARTESIAN_POINT('Ctrl Pts',(-144.100793848887,1.75231371279358,
126.206816019923));
#110288=CARTESIAN_POINT('Ctrl Pts',(-144.108550151629,1.62335049441414,
126.159718179586));
#110289=CARTESIAN_POINT('Ctrl Pts',(-144.116306454371,1.49275005748649,
126.118116884215));
#110290=CARTESIAN_POINT('Ctrl Pts',(-144.124066896885,1.36207991517334,
126.07649338498));
#110291=CARTESIAN_POINT('Ctrl Pts',(-144.131827339399,1.22977119010396,
126.040372379217));
#110292=CARTESIAN_POINT('Ctrl Pts',(-144.139587781913,1.09632840155966,
126.009858860508));
#110293=CARTESIAN_POINT('Ctrl Pts',(-144.147360682179,0.962671398804334,
125.97929635879));
#110294=CARTESIAN_POINT('Ctrl Pts',(-144.155133582444,0.827877079299284,
125.954359403425));
#110295=CARTESIAN_POINT('Ctrl Pts',(-144.16290648271,0.692458084197433,
125.935101447617));
#110296=CARTESIAN_POINT('Ctrl Pts',(-144.170396818472,0.561961910660792,
125.91654356701));
#110297=CARTESIAN_POINT('Ctrl Pts',(-144.177887154234,0.430885996531902,
125.90325899355));
#110298=CARTESIAN_POINT('Ctrl Pts',(-144.185377489997,0.299688967855314,
125.895249742362));
#110299=CARTESIAN_POINT('Ctrl Pts',(-144.193151824116,0.163517563965948,
125.886936817981));
#110300=CARTESIAN_POINT('Ctrl Pts',(-144.200926158235,0.0267843300386512,
125.884280807386));
#110301=CARTESIAN_POINT('Ctrl Pts',(-144.208700492354,-0.110001312959909,
125.887340913147));
#110302=CARTESIAN_POINT('Ctrl Pts',(-144.216465245301,-0.246618379877987,
125.890397247601));
#110303=CARTESIAN_POINT('Ctrl Pts',(-144.224229998248,-0.383287340238361,
125.899155673091));
#110304=CARTESIAN_POINT('Ctrl Pts',(-144.231994751195,-0.519494349596362,
125.913623588933));
#110305=CARTESIAN_POINT('Ctrl Pts',(-144.23975179208,-0.655566076232488,
125.928077135038));
#110306=CARTESIAN_POINT('Ctrl Pts',(-144.247508832965,-0.791176378668927,
125.948228845424));
#110307=CARTESIAN_POINT('Ctrl Pts',(-144.25526587385,-0.92581247062156,
125.974034093226));
#110308=CARTESIAN_POINT('Ctrl Pts',(-144.263017065091,-1.06034703245085,
125.99981988109));
#110309=CARTESIAN_POINT('Ctrl Pts',(-144.270768256331,-1.19390846366965,
126.03125064708));
#110310=CARTESIAN_POINT('Ctrl Pts',(-144.278519447571,-1.32599051065011,
126.068230105411));
#110311=CARTESIAN_POINT('Ctrl Pts',(-144.286267344348,-1.4580164192363,
126.105193846485));
#110312=CARTESIAN_POINT('Ctrl Pts',(-144.294015241125,-1.58856381847538,
126.147701484151));
#110313=CARTESIAN_POINT('Ctrl Pts',(-144.301763137902,-1.71713825801937,
126.195605984767));
#110314=CARTESIAN_POINT('Ctrl Pts',(-144.309509413986,-1.84568580256271,
126.243500464794));
#110315=CARTESIAN_POINT('Ctrl Pts',(-144.31725569007,-1.97226084216465,
126.296789425898));
#110316=CARTESIAN_POINT('Ctrl Pts',(-144.325001966154,-2.09638604402693,
126.355276597578));
#110317=CARTESIAN_POINT('Ctrl Pts',(-144.33274829942,-2.22051216215275,
126.413764200997));
#110318=CARTESIAN_POINT('Ctrl Pts',(-144.340494632685,-2.3421880527834,
126.477449924913));
#110319=CARTESIAN_POINT('Ctrl Pts',(-144.34824096595,-2.46095861903949,
126.546090342222));
#110320=CARTESIAN_POINT('Ctrl Pts',(-144.355989033953,-2.57975578313991,
126.614746131077));
#110321=CARTESIAN_POINT('Ctrl Pts',(-144.363737101956,-2.69564598975608,
126.688358625649));
#110322=CARTESIAN_POINT('Ctrl Pts',(-144.371485169959,-2.80820123976273,
126.766639867007));
#110323=CARTESIAN_POINT('Ctrl Pts',(-144.379241472701,-2.92087611482929,
126.8450043066));
#110324=CARTESIAN_POINT('Ctrl Pts',(-144.386997775443,-3.03020863142111,
126.928047181521));
#110325=CARTESIAN_POINT('Ctrl Pts',(-144.394754078185,-3.13580170567935,
127.015438511589));
#110326=CARTESIAN_POINT('Ctrl Pts',(-144.402514520699,-3.24145113814037,
127.102876485042));
#110327=CARTESIAN_POINT('Ctrl Pts',(-144.410274963213,-3.34335686100905,
127.194667276701));
#110328=CARTESIAN_POINT('Ctrl Pts',(-144.418035405727,-3.44115783521619,
127.290443171804));
#110329=CARTESIAN_POINT('Ctrl Pts',(-144.425808305993,-3.53911580822975,
127.386372814876));
#110330=CARTESIAN_POINT('Ctrl Pts',(-144.433581206258,-3.63295559725585,
127.486300059957));
#110331=CARTESIAN_POINT('Ctrl Pts',(-144.441354106524,-3.72235513553601,
127.589822500286));
#110332=CARTESIAN_POINT('Ctrl Pts',(-144.448844442285,-3.80850477541293,
127.689581639148));
#110333=CARTESIAN_POINT('Ctrl Pts',(-144.456334778047,-3.89053119659048,
127.79267888151));
#110334=CARTESIAN_POINT('Ctrl Pts',(-144.463825113809,-3.96818480510813,
127.898729461516));
#110335=CARTESIAN_POINT('Ctrl Pts',(-144.471653010412,-4.04933796534868,
128.009559336355));
#110336=CARTESIAN_POINT('Ctrl Pts',(-144.479480907015,-4.12597241173223,
128.12396630478));
#110337=CARTESIAN_POINT('Ctrl Pts',(-144.487308803618,-4.19775881841822,
128.24154888728));
#110338=CARTESIAN_POINT('Ctrl Pts',(-144.495123550815,-4.26942463733033,
128.358933952973));
#110339=CARTESIAN_POINT('Ctrl Pts',(-144.502938298012,-4.33625843984316,
128.479483682202));
#110340=CARTESIAN_POINT('Ctrl Pts',(-144.510753045208,-4.39797237210572,
128.602765269484));
#110341=CARTESIAN_POINT('Ctrl Pts',(-144.518560209974,-4.45962642506256,
128.725927240084));
#110342=CARTESIAN_POINT('Ctrl Pts',(-144.52636737474,-4.51617031912051,
128.851815454922));
#110343=CARTESIAN_POINT('Ctrl Pts',(-144.534174539506,-4.56736033728549,
128.979969592623));
#110344=CARTESIAN_POINT('Ctrl Pts',(-144.541974361762,-4.61850221208431,
129.108003203476));
#110345=CARTESIAN_POINT('Ctrl Pts',(-144.549774184018,-4.66430009660497,
129.238298138185));
#110346=CARTESIAN_POINT('Ctrl Pts',(-144.557574006274,-4.70455719433246,
129.370371542379));
#110347=CARTESIAN_POINT('Ctrl Pts',(-144.561721480154,-4.72596348486209,
129.440600193251));
#110348=CARTESIAN_POINT('Ctrl Pts',(-144.565868954034,-4.74580393375321,
129.511331328419));
#110349=CARTESIAN_POINT('Ctrl Pts',(-144.570016427913,-4.76405452823402,
129.582490119308));
#110350=CARTESIAN_POINT('Origin',(213.235140564004,0.,130.804360617566));
#110351=CARTESIAN_POINT('',(-146.665174983012,-4.76405452823419,129.582490119309));
#110352=CARTESIAN_POINT('',(-146.319717442688,-4.76405452823404,129.582490119308));
#110353=CARTESIAN_POINT('',(213.235140564004,-4.76405452823405,129.582490119308));
#110354=CARTESIAN_POINT('',(-144.985140563981,-4.91824970179615,130.806073300273));
#110355=CARTESIAN_POINT('Ctrl Pts',(-144.985140564011,-4.91824970179597,
130.806073300807));
#110356=CARTESIAN_POINT('Ctrl Pts',(-144.990470831099,-4.91821711222921,
130.899659565425));
#110357=CARTESIAN_POINT('Ctrl Pts',(-144.995801098188,-4.91551352483608,
130.993196152259));
#110358=CARTESIAN_POINT('Ctrl Pts',(-145.001131365277,-4.91014626190504,
131.086578174072));
#110359=CARTESIAN_POINT('Ctrl Pts',(-145.008905699396,-4.90231796838136,
131.222778298041));
#110360=CARTESIAN_POINT('Ctrl Pts',(-145.016680033515,-4.88880599865511,
131.358868188652));
#110361=CARTESIAN_POINT('Ctrl Pts',(-145.024454367634,-4.86961173160291,
131.494334998203));
#110362=CARTESIAN_POINT('Ctrl Pts',(-145.032219120581,-4.85044111976941,
131.629634857018));
#110363=CARTESIAN_POINT('Ctrl Pts',(-145.039983873528,-4.82560219866211,
131.764312779267));
#110364=CARTESIAN_POINT('Ctrl Pts',(-145.047748626475,-4.79514831027588,
131.897857643149));
#110365=CARTESIAN_POINT('Ctrl Pts',(-145.05550566736,-4.76472466912101,
132.031269868389));
#110366=CARTESIAN_POINT('Ctrl Pts',(-145.063262708245,-4.72869724526217,
132.163550896085));
#110367=CARTESIAN_POINT('Ctrl Pts',(-145.07101974913,-4.68717091774936,
132.294196799938));
#110368=CARTESIAN_POINT('Ctrl Pts',(-145.07877094037,-4.6456759055631,132.424744182699));
#110369=CARTESIAN_POINT('Ctrl Pts',(-145.08652213161,-4.59869036156111,
132.553658524858));
#110370=CARTESIAN_POINT('Ctrl Pts',(-145.094273322851,-4.5463696905704,
132.680448488419));
#110371=CARTESIAN_POINT('Ctrl Pts',(-145.102021219628,-4.49407125726064,
132.807184562863));
#110372=CARTESIAN_POINT('Ctrl Pts',(-145.109769116405,-4.43644235581175,
132.931797693896));
#110373=CARTESIAN_POINT('Ctrl Pts',(-145.117517013182,-4.37368738963638,
133.05381425795));
#110374=CARTESIAN_POINT('Ctrl Pts',(-145.125263289266,-4.31094555044709,
133.175805298769));
#110375=CARTESIAN_POINT('Ctrl Pts',(-145.13300956535,-4.24307995802164,
133.2952005055));
#110376=CARTESIAN_POINT('Ctrl Pts',(-145.140755841434,-4.17034188627465,
133.411549067618));
#110377=CARTESIAN_POINT('Ctrl Pts',(-145.148502174699,-4.09760327759184,
133.527898488594));
#110378=CARTESIAN_POINT('Ctrl Pts',(-145.156248507965,-4.01999232506947,
133.641200888568));
#110379=CARTESIAN_POINT('Ctrl Pts',(-145.16399484123,-3.93780450290235,
133.751033106904));
#110380=CARTESIAN_POINT('Ctrl Pts',(-145.171742909233,-3.85559827534241,
133.860889921404));
#110381=CARTESIAN_POINT('Ctrl Pts',(-145.179490977236,-3.7688133727838,
133.967274694913));
#110382=CARTESIAN_POINT('Ctrl Pts',(-145.187239045239,-3.67778628907491,
134.069796434481));
#110383=CARTESIAN_POINT('Ctrl Pts',(-145.194995347981,-3.58666246069784,
134.172427135375));
#110384=CARTESIAN_POINT('Ctrl Pts',(-145.202751650723,-3.49128770466755,
134.271186307969));
#110385=CARTESIAN_POINT('Ctrl Pts',(-145.210507953464,-3.39203659059686,
134.365718621271));
#110386=CARTESIAN_POINT('Ctrl Pts',(-145.218268395979,-3.29273250321821,
134.460301389314));
#110387=CARTESIAN_POINT('Ctrl Pts',(-145.226028838493,-3.18954822927861,
134.550652545359));
#110388=CARTESIAN_POINT('Ctrl Pts',(-145.233789281007,-3.08289155165424,
134.636457007695));
#110389=CARTESIAN_POINT('Ctrl Pts',(-145.241562181272,-2.9760636592624,
134.722399210971));
#110390=CARTESIAN_POINT('Ctrl Pts',(-145.249335081538,-2.86575253893195,
134.803779903063));
#110391=CARTESIAN_POINT('Ctrl Pts',(-145.257107981803,-2.75239581974219,
134.880326799217));
#110392=CARTESIAN_POINT('Ctrl Pts',(-145.264598317565,-2.64315990282333,
134.954091022887));
#110393=CARTESIAN_POINT('Ctrl Pts',(-145.272088653327,-2.53109623506778,
135.023366628437));
#110394=CARTESIAN_POINT('Ctrl Pts',(-145.279578989089,-2.41661636845603,
135.087951213107));
#110395=CARTESIAN_POINT('Ctrl Pts',(-145.287353323208,-2.29779596290646,
135.154984541936));
#110396=CARTESIAN_POINT('Ctrl Pts',(-145.295127657327,-2.17599613398452,
135.217176449182));
#110397=CARTESIAN_POINT('Ctrl Pts',(-145.302901991446,-2.05164910030208,
135.274250888225));
#110398=CARTESIAN_POINT('Ctrl Pts',(-145.310666744393,-1.92745531322579,
135.331254988122));
#110399=CARTESIAN_POINT('Ctrl Pts',(-145.31843149734,-1.80072091937854,
135.383154006986));
#110400=CARTESIAN_POINT('Ctrl Pts',(-145.326196250287,-1.67190477265788,
135.429716549131));
#110401=CARTESIAN_POINT('Ctrl Pts',(-145.333953291172,-1.54321656795012,
135.476232844702));
#110402=CARTESIAN_POINT('Ctrl Pts',(-145.341710332057,-1.41245109034158,
135.517423079274));
#110403=CARTESIAN_POINT('Ctrl Pts',(-145.349467372942,-1.28008899698821,
135.553103106088));
#110404=CARTESIAN_POINT('Ctrl Pts',(-145.357218564183,-1.14782671891888,
135.588756226315));
#110405=CARTESIAN_POINT('Ctrl Pts',(-145.364969755423,-1.01397059759738,
135.618907308292));
#110406=CARTESIAN_POINT('Ctrl Pts',(-145.372720946663,-0.87901800970143,
135.643421518311));
#110407=CARTESIAN_POINT('Ctrl Pts',(-145.38046884344,-0.744122780255502,
135.667925309137));
#110408=CARTESIAN_POINT('Ctrl Pts',(-145.388216740217,-0.608132394993289,
135.686796923381));
#110409=CARTESIAN_POINT('Ctrl Pts',(-145.395964636994,-0.471555811873031,
135.699952326317));
#110410=CARTESIAN_POINT('Ctrl Pts',(-145.403710913078,-0.335007797629711,
135.713104977425));
#110411=CARTESIAN_POINT('Ctrl Pts',(-145.411457189162,-0.197874218343641,
135.720543758093));
#110412=CARTESIAN_POINT('Ctrl Pts',(-145.419203465246,-0.0606701733661577,
135.72223639808));
#110413=CARTESIAN_POINT('Ctrl Pts',(-145.426949798512,0.0765348844206047,
135.723929050561));
#110414=CARTESIAN_POINT('Ctrl Pts',(-145.434696131777,0.21381001800127,
135.719875472899));
#110415=CARTESIAN_POINT('Ctrl Pts',(-145.442442465042,0.350639499328176,
135.710095527242));
#110416=CARTESIAN_POINT('Ctrl Pts',(-145.450190533045,0.487499622668529,
135.700313391433));
#110417=CARTESIAN_POINT('Ctrl Pts',(-145.457938601048,0.623913505267511,
135.684802363709));
#110418=CARTESIAN_POINT('Ctrl Pts',(-145.465686669051,0.759370310538065,
135.663634204634));
#110419=CARTESIAN_POINT('Ctrl Pts',(-145.473442971793,0.894971080913033,
135.642443547787));
#110420=CARTESIAN_POINT('Ctrl Pts',(-145.481199274535,1.0296123551137,135.6155838095));
#110421=CARTESIAN_POINT('Ctrl Pts',(-145.488955577277,1.16279271908662,
135.583178060714));
#110422=CARTESIAN_POINT('Ctrl Pts',(-145.496716019791,1.29604416543013,
135.550755016005));
#110423=CARTESIAN_POINT('Ctrl Pts',(-145.504476462305,1.42783277236835,
135.512780170801));
#110424=CARTESIAN_POINT('Ctrl Pts',(-145.512236904819,1.55767303613065,
135.469426295026));
#110425=CARTESIAN_POINT('Ctrl Pts',(-145.520009805084,1.68772173101102,
135.42600282376));
#110426=CARTESIAN_POINT('Ctrl Pts',(-145.52778270535,1.81581546712574,135.377183205962));
#110427=CARTESIAN_POINT('Ctrl Pts',(-145.535555605615,1.94148861439546,
135.323188454812));
#110428=CARTESIAN_POINT('Ctrl Pts',(-145.543045941377,2.06259322621445,
135.27115654887));
#110429=CARTESIAN_POINT('Ctrl Pts',(-145.55053627714,2.18144990488352,135.214319368328));
#110430=CARTESIAN_POINT('Ctrl Pts',(-145.558026612902,2.29766590933114,
135.152913759888));
#110431=CARTESIAN_POINT('Ctrl Pts',(-145.565800947021,2.41828827890691,
135.089179939142));
#110432=CARTESIAN_POINT('Ctrl Pts',(-145.57357528114,2.53644787449853,135.020322538508));
#110433=CARTESIAN_POINT('Ctrl Pts',(-145.581349615259,2.65167882554812,
134.946555985802));
#110434=CARTESIAN_POINT('Ctrl Pts',(-145.589114368206,2.76676776474871,
134.872880343781));
#110435=CARTESIAN_POINT('Ctrl Pts',(-145.596879121153,2.87893491471041,
134.794307796333));
#110436=CARTESIAN_POINT('Ctrl Pts',(-145.604643874101,2.98773757394863,
134.711099315216));
#110437=CARTESIAN_POINT('Ctrl Pts',(-145.612400914986,3.09643216885185,
134.627973477936));
#110438=CARTESIAN_POINT('Ctrl Pts',(-145.620157955871,3.20176861453724,
134.540221106066));
#110439=CARTESIAN_POINT('Ctrl Pts',(-145.627914996756,3.30333217618779,
134.448147054264));
#110440=CARTESIAN_POINT('Ctrl Pts',(-145.635666187996,3.40481914796659,
134.35614243622));
#110441=CARTESIAN_POINT('Ctrl Pts',(-145.643417379236,3.50253861034877,
134.259822886639));
#110442=CARTESIAN_POINT('Ctrl Pts',(-145.651168570476,3.59610827967456,
134.159533981694));
#110443=CARTESIAN_POINT('Ctrl Pts',(-145.658916467253,3.6896381793947,134.059287702209));
#110444=CARTESIAN_POINT('Ctrl Pts',(-145.66666436403,3.77902152791442,133.955075708104));
#110445=CARTESIAN_POINT('Ctrl Pts',(-145.674412260807,3.86391252022951,
133.8472807773));
#110446=CARTESIAN_POINT('Ctrl Pts',(-145.682158536891,3.94878575517905,
133.739508394871));
#110447=CARTESIAN_POINT('Ctrl Pts',(-145.689904812975,4.02916826131005,
133.628154873446));
#110448=CARTESIAN_POINT('Ctrl Pts',(-145.69765108906,4.10475446497433,133.513636137843));
#110449=CARTESIAN_POINT('Ctrl Pts',(-145.705397422325,4.18034122659889,
133.399116556889));
#110450=CARTESIAN_POINT('Ctrl Pts',(-145.71314375559,4.25113139974043,133.281432041433));
#110451=CARTESIAN_POINT('Ctrl Pts',(-145.720890088856,4.31686293137953,
133.161027224064));
#110452=CARTESIAN_POINT('Ctrl Pts',(-145.728638156859,4.3826091831393,133.040595442871));
#110453=CARTESIAN_POINT('Ctrl Pts',(-145.736386224862,4.44329435185884,
132.917442490635));
#110454=CARTESIAN_POINT('Ctrl Pts',(-145.744134292865,4.49870269208018,
132.792036936983));
#110455=CARTESIAN_POINT('Ctrl Pts',(-145.751890595606,4.55416992094495,
132.666498100816));
#110456=CARTESIAN_POINT('Ctrl Pts',(-145.759646898348,4.60434895991805,
132.538702238961));
#110457=CARTESIAN_POINT('Ctrl Pts',(-145.76740320109,4.64907232552509,132.409137728113));
#110458=CARTESIAN_POINT('Ctrl Pts',(-145.775163643604,4.69381956133894,
132.279504064785));
#110459=CARTESIAN_POINT('Ctrl Pts',(-145.782924086118,4.73310520973102,
132.1481002459));
#110460=CARTESIAN_POINT('Ctrl Pts',(-145.790684528633,4.76681220028328,
132.015428125895));
#110461=CARTESIAN_POINT('Ctrl Pts',(-145.798457428898,4.80057330028914,
131.882543028825));
#110462=CARTESIAN_POINT('Ctrl Pts',(-145.806230329163,4.82873776642562,
131.748385944923));
#110463=CARTESIAN_POINT('Ctrl Pts',(-145.814003229429,4.851239858909,131.613468084985));
#110464=CARTESIAN_POINT('Ctrl Pts',(-145.821493565191,4.87292394365119,
131.483454829093));
#110465=CARTESIAN_POINT('Ctrl Pts',(-145.828983900953,4.88935015200417,
131.352735454729));
#110466=CARTESIAN_POINT('Ctrl Pts',(-145.836474236715,4.90050546366366,
131.221768407506));
#110467=CARTESIAN_POINT('Ctrl Pts',(-145.844248570834,4.91208373235536,
131.085835704881));
#110468=CARTESIAN_POINT('Ctrl Pts',(-145.852022904953,4.91802019868463,
130.949205583677));
#110469=CARTESIAN_POINT('Ctrl Pts',(-145.859797239072,4.91824345243122,
130.812385897464));
#110470=CARTESIAN_POINT('Ctrl Pts',(-145.867561992019,4.91846643103752,
130.675734829286));
#110471=CARTESIAN_POINT('Ctrl Pts',(-145.875326744966,4.9129902059683,130.538895048148));
#110472=CARTESIAN_POINT('Ctrl Pts',(-145.883091497913,4.90179504918907,
130.402380072955));
#110473=CARTESIAN_POINT('Ctrl Pts',(-145.890848538798,4.89061101159739,
130.266000686361));
#110474=CARTESIAN_POINT('Ctrl Pts',(-145.898605579683,4.87371937774573,
130.129945850856));
#110475=CARTESIAN_POINT('Ctrl Pts',(-145.906362620568,4.85115245619196,
129.994729275977));
#110476=CARTESIAN_POINT('Ctrl Pts',(-145.914113811808,4.82860255252925,
129.859614668969));
#110477=CARTESIAN_POINT('Ctrl Pts',(-145.921865003049,4.80038594390358,
129.725337448424));
#110478=CARTESIAN_POINT('Ctrl Pts',(-145.929616194289,4.76658673968084,
129.592406032774));
#110479=CARTESIAN_POINT('Ctrl Pts',(-145.937364091066,4.73280190102157,
129.459531116522));
#110480=CARTESIAN_POINT('Ctrl Pts',(-145.945111987843,4.69343928212807,
129.328001245611));
#110481=CARTESIAN_POINT('Ctrl Pts',(-145.95285988462,4.64863400885555,129.198314256401));
#110482=CARTESIAN_POINT('Ctrl Pts',(-145.960606160704,4.60383810788032,
129.068654394914));
#110483=CARTESIAN_POINT('Ctrl Pts',(-145.968352436788,4.5536019446252,128.940837017663));
#110484=CARTESIAN_POINT('Ctrl Pts',(-145.976098712872,4.49811027839977,
128.815344029939));
#110485=CARTESIAN_POINT('Ctrl Pts',(-145.983845046137,4.44261820254738,
128.689850115854));
#110486=CARTESIAN_POINT('Ctrl Pts',(-145.991591379403,4.38187070442459,
128.5666809831));
#110487=CARTESIAN_POINT('Ctrl Pts',(-145.999337712668,4.31610021996306,
128.446297439079));
#110488=CARTESIAN_POINT('Ctrl Pts',(-146.007085780671,4.25031500665764,
128.325886935999));
#110489=CARTESIAN_POINT('Ctrl Pts',(-146.014833848674,4.17950475607948,
128.208263606));
#110490=CARTESIAN_POINT('Ctrl Pts',(-146.022581916677,4.10394707343582,
128.093862235176));
#110491=CARTESIAN_POINT('Ctrl Pts',(-146.030338219419,4.02830908718779,
127.979339277214));
#110492=CARTESIAN_POINT('Ctrl Pts',(-146.038094522161,3.94791380549875,
127.868045445662));
#110493=CARTESIAN_POINT('Ctrl Pts',(-146.045850824902,3.86308158460433,
127.760385628643));
#110494=CARTESIAN_POINT('Ctrl Pts',(-146.053611267417,3.77820408619936,
127.652668350338));
#110495=CARTESIAN_POINT('Ctrl Pts',(-146.061371709931,3.6888851843834,127.548589247894));
#110496=CARTESIAN_POINT('Ctrl Pts',(-146.069132152445,3.59548382408594,
127.448518080551));
#110497=CARTESIAN_POINT('Ctrl Pts',(-146.07690505271,3.50193252763315,127.348286270087));
#110498=CARTESIAN_POINT('Ctrl Pts',(-146.084677952976,3.40428595532249,
127.252075526249));
#110499=CARTESIAN_POINT('Ctrl Pts',(-146.092450853241,3.30293866931551,
127.160217479702));
#110500=CARTESIAN_POINT('Ctrl Pts',(-146.099941189003,3.20527561243356,
127.071698704524));
#110501=CARTESIAN_POINT('Ctrl Pts',(-146.107431524765,3.10417646746311,
126.98722185538));
#110502=CARTESIAN_POINT('Ctrl Pts',(-146.114921860527,3.00001989989066,
126.907045687674));
#110503=CARTESIAN_POINT('Ctrl Pts',(-146.122696194646,2.89191420440055,
126.8238296162));
#110504=CARTESIAN_POINT('Ctrl Pts',(-146.130470528765,2.78017221892343,
126.744983181061));
#110505=CARTESIAN_POINT('Ctrl Pts',(-146.138244862885,2.66518261608051,
126.670840968956));
#110506=CARTESIAN_POINT('Ctrl Pts',(-146.146009615832,2.55033472764619,
126.596790130502));
#110507=CARTESIAN_POINT('Ctrl Pts',(-146.153774368779,2.43224751085592,
126.527432189544));
#110508=CARTESIAN_POINT('Ctrl Pts',(-146.161539121726,2.31134234022524,
126.46306131335));
#110509=CARTESIAN_POINT('Ctrl Pts',(-146.169296162611,2.1905572543145,126.398754371219));
#110510=CARTESIAN_POINT('Ctrl Pts',(-146.177053203496,2.06696012723298,
126.339424819259));
#110511=CARTESIAN_POINT('Ctrl Pts',(-146.184810244381,1.94100062092707,
126.28532314792));
#110512=CARTESIAN_POINT('Ctrl Pts',(-146.192561435621,1.81513610166486,
126.231262275073));
#110513=CARTESIAN_POINT('Ctrl Pts',(-146.200312626861,1.68691310690037,
126.182421589437));
#110514=CARTESIAN_POINT('Ctrl Pts',(-146.208063818101,1.5568048466269,126.139005140004));
#110515=CARTESIAN_POINT('Ctrl Pts',(-146.215811714879,1.42675188583462,
126.09560714372));
#110516=CARTESIAN_POINT('Ctrl Pts',(-146.223559611656,1.29481562331984,
126.057628921779));
#110517=CARTESIAN_POINT('Ctrl Pts',(-146.231307508433,1.1614879417375,126.025225881686));
#110518=CARTESIAN_POINT('Ctrl Pts',(-146.239053784517,1.02818814943193,
125.99282961961));
#110519=CARTESIAN_POINT('Ctrl Pts',(-146.246800060601,0.893497896648766,
125.966006312002));
#110520=CARTESIAN_POINT('Ctrl Pts',(-146.254546336685,0.757922490875799,
125.944860997201));
#110521=CARTESIAN_POINT('Ctrl Pts',(-146.262292669951,0.622346084316169,
125.923715526311));
#110522=CARTESIAN_POINT('Ctrl Pts',(-146.270039003216,0.485884898023598,
125.908248192114));
#110523=CARTESIAN_POINT('Ctrl Pts',(-146.277785336482,0.349052259614766,
125.898512517333));
#110524=CARTESIAN_POINT('Ctrl Pts',(-146.285533404485,0.212188978485107,
125.888774662316));
#110525=CARTESIAN_POINT('Ctrl Pts',(-146.293281472487,0.0749544696171083,
125.884771048604));
#110526=CARTESIAN_POINT('Ctrl Pts',(-146.30102954049,-0.0621354167404537,
125.886503131578));
#110527=CARTESIAN_POINT('Ctrl Pts',(-146.308785843232,-0.19937100386044,
125.888237055431));
#110528=CARTESIAN_POINT('Ctrl Pts',(-146.316542145974,-0.336461269867287,
125.895718848371));
#110529=CARTESIAN_POINT('Ctrl Pts',(-146.324298448716,-0.472892410545639,
125.908897837547));
#110530=CARTESIAN_POINT('Ctrl Pts',(-146.33205889123,-0.609396368632005,
125.922083860747));
#110531=CARTESIAN_POINT('Ctrl Pts',(-146.339819333744,-0.745240113358501,
125.940973085343));
#110532=CARTESIAN_POINT('Ctrl Pts',(-146.347579776259,-0.879918537302853,
125.965463384703));
#110533=CARTESIAN_POINT('Ctrl Pts',(-146.355352676524,-1.01481315900914,
125.989992998065));
#110534=CARTESIAN_POINT('Ctrl Pts',(-146.36312557679,-1.14853834011378,
126.020141567723));
#110535=CARTESIAN_POINT('Ctrl Pts',(-146.370898477055,-1.28060179986094,
126.055756391828));
#110536=CARTESIAN_POINT('Ctrl Pts',(-146.378388812817,-1.40786442019636,
126.090076527369));
#110537=CARTESIAN_POINT('Ctrl Pts',(-146.385879148579,-1.53358374322851,
126.129472300885));
#110538=CARTESIAN_POINT('Ctrl Pts',(-146.393369484341,-1.65733739276342,
126.173764993994));
#110539=CARTESIAN_POINT('Ctrl Pts',(-146.401143943622,-1.78578526743254,
126.219737798146));
#110540=CARTESIAN_POINT('Ctrl Pts',(-146.408918402903,-1.912522291739,126.271131985916));
#110541=CARTESIAN_POINT('Ctrl Pts',(-146.416692862184,-2.03705685772722,
126.327801400836));
#110542=CARTESIAN_POINT('Ctrl Pts',(-146.424457711091,-2.16143748070047,
126.384400764037));
#110543=CARTESIAN_POINT('Ctrl Pts',(-146.432222559998,-2.28362071005336,
126.446262219059));
#110544=CARTESIAN_POINT('Ctrl Pts',(-146.439987408906,-2.40313127408453,
126.51319024784));
#110545=CARTESIAN_POINT('Ctrl Pts',(-146.447744516672,-2.5225226924516,
126.580051552942));
#110546=CARTESIAN_POINT('Ctrl Pts',(-146.455501624439,-2.63924640914733,
126.651969189893));
#110547=CARTESIAN_POINT('Ctrl Pts',(-146.463258732206,-2.75284861520924,
126.728700233746));
#110548=CARTESIAN_POINT('Ctrl Pts',(-146.471009961343,-2.8663647292182,
126.805373127909));
#110549=CARTESIAN_POINT('Ctrl Pts',(-146.478761190479,-2.97676371859975,
126.88685195016));
#110550=CARTESIAN_POINT('Ctrl Pts',(-146.486512419616,-3.08361812443508,
126.972848863029));
#110551=CARTESIAN_POINT('Ctrl Pts',(-146.494260205081,-3.19042505760531,
127.05880756968));
#110552=CARTESIAN_POINT('Ctrl Pts',(-146.502007990546,-3.29369023618939,
127.149280129012));
#110553=CARTESIAN_POINT('Ctrl Pts',(-146.509755776011,-3.39301705509289,
127.243936720563));
#110554=CARTESIAN_POINT('Ctrl Pts',(-146.5175018995,-3.49232256741227,127.33857300734));
#110555=CARTESIAN_POINT('Ctrl Pts',(-146.525248022988,-3.58769111786824,
127.437391271333));
#110556=CARTESIAN_POINT('Ctrl Pts',(-146.532994146476,-3.67876122571081,
127.540023179937));
#110557=CARTESIAN_POINT('Ctrl Pts',(-146.540740285835,-3.76983152013388,
127.642655298809));
#110558=CARTESIAN_POINT('Ctrl Pts',(-146.548486425193,-3.85660309504985,
127.749100785359));
#110559=CARTESIAN_POINT('Ctrl Pts',(-146.556232564552,-3.93875347818782,
127.858956723265));
#110560=CARTESIAN_POINT('Ctrl Pts',(-146.563980397272,-4.02092181999879,
127.96883667648));
#110561=CARTESIAN_POINT('Ctrl Pts',(-146.571728229993,-4.09846672603568,
128.082128251392));
#110562=CARTESIAN_POINT('Ctrl Pts',(-146.579476062714,-4.17110816626757,
128.19839827559));
#110563=CARTESIAN_POINT('Ctrl Pts',(-146.587231559407,-4.24382146168303,
128.314783311329));
#110564=CARTESIAN_POINT('Ctrl Pts',(-146.5949870561,-4.31162139687108,128.434152348484));
#110565=CARTESIAN_POINT('Ctrl Pts',(-146.602742552792,-4.37427294919856,
128.556045864599));
#110566=CARTESIAN_POINT('Ctrl Pts',(-146.610502172197,-4.43695780619945,
128.678004177571));
#110567=CARTESIAN_POINT('Ctrl Pts',(-146.618261791601,-4.49448866327323,
128.802489288919));
#110568=CARTESIAN_POINT('Ctrl Pts',(-146.626021411005,-4.5466784689929,
128.92902119173));
#110569=CARTESIAN_POINT('Ctrl Pts',(-146.633792151364,-4.59894307225455,
129.055734437911));
#110570=CARTESIAN_POINT('Ctrl Pts',(-146.641562891723,-4.64585119962519,
129.184499968273));
#110571=CARTESIAN_POINT('Ctrl Pts',(-146.649333632082,-4.6872653282045,
129.314821492363));
#110572=CARTESIAN_POINT('Ctrl Pts',(-146.654614082392,-4.7154074662754,
129.403378862766));
#110573=CARTESIAN_POINT('Ctrl Pts',(-146.659894532702,-4.74101374047461,
129.492654437527));
#110574=CARTESIAN_POINT('Ctrl Pts',(-146.665174983012,-4.76405452823419,
129.582490119309));
#110575=CARTESIAN_POINT('Ctrl Pts',(-144.915004217899,-4.7640545282341,
129.582490119308));
#110576=CARTESIAN_POINT('Ctrl Pts',(-144.922696708858,-4.79785557992013,
129.71427990683));
#110577=CARTESIAN_POINT('Ctrl Pts',(-144.930389199817,-4.82615815883693,
129.84737326594));
#110578=CARTESIAN_POINT('Ctrl Pts',(-144.938081690777,-4.84888658593865,
129.981267707133));
#110579=CARTESIAN_POINT('Ctrl Pts',(-144.945924836311,-4.87206014083276,
130.117784421165));
#110580=CARTESIAN_POINT('Ctrl Pts',(-144.953767981845,-4.88943888408906,
130.255133485846));
#110581=CARTESIAN_POINT('Ctrl Pts',(-144.961611127379,-4.90099825108423,
130.392779270358));
#110582=CARTESIAN_POINT('Ctrl Pts',(-144.969454272913,-4.91255761807938,
130.53042505487));
#110583=CARTESIAN_POINT('Ctrl Pts',(-144.977297418447,-4.91829765523471,
130.668367125102));
#110584=CARTESIAN_POINT('Ctrl Pts',(-144.985140563981,-4.91824970179615,
130.806073300273));
#110585=CARTESIAN_POINT('',(-144.639859436048,-4.91824892573493,130.807611310912));
#110586=CARTESIAN_POINT('Ctrl Pts',(-144.570016427913,-4.76405452823402,
129.582490119308));
#110587=CARTESIAN_POINT('Ctrl Pts',(-144.577809747297,-4.79834834559403,
129.716201192713));
#110588=CARTESIAN_POINT('Ctrl Pts',(-144.585603066681,-4.82702561414829,
129.851422976877));
#110589=CARTESIAN_POINT('Ctrl Pts',(-144.593396386065,-4.84996524191635,
129.987647562262));
#110590=CARTESIAN_POINT('Ctrl Pts',(-144.601188962403,-4.87290268252795,
130.123859159448));
#110591=CARTESIAN_POINT('Ctrl Pts',(-144.60898153874,-4.89010349849468,
130.261072990475));
#110592=CARTESIAN_POINT('Ctrl Pts',(-144.616774115077,-4.90149775451951,
130.398771139226));
#110593=CARTESIAN_POINT('Ctrl Pts',(-144.624469222049,-4.91274949145216,
130.5347469627));
#110594=CARTESIAN_POINT('Ctrl Pts',(-144.632164329021,-4.91833908962852,
130.671194688538));
#110595=CARTESIAN_POINT('Ctrl Pts',(-144.639859435993,-4.91824892573558,
130.807611309931));
#110596=CARTESIAN_POINT('Ctrl Pts',(-144.639859436049,-4.91824892573493,
130.807611310912));
#110597=CARTESIAN_POINT('Ctrl Pts',(-144.648629426068,-4.91814616736096,
130.963083146767));
#110598=CARTESIAN_POINT('Ctrl Pts',(-144.657399416086,-4.91066741602864,
131.118270672276));
#110599=CARTESIAN_POINT('Ctrl Pts',(-144.666169406105,-4.89591751247246,
131.272521672723));
#110600=CARTESIAN_POINT('Ctrl Pts',(-144.674975661587,-4.88110661545087,
131.427410528395));
#110601=CARTESIAN_POINT('Ctrl Pts',(-144.683781917069,-4.85896441776539,
131.58135492203));
#110602=CARTESIAN_POINT('Ctrl Pts',(-144.692588172551,-4.8296468260347,
131.733712326163));
#110603=CARTESIAN_POINT('Ctrl Pts',(-144.70144461531,-4.80016215192807,
131.886938022526));
#110604=CARTESIAN_POINT('Ctrl Pts',(-144.710301058068,-4.76342016027957,
132.038558415203));
#110605=CARTESIAN_POINT('Ctrl Pts',(-144.719157500827,-4.71962812449032,
132.18794054985));
#110606=CARTESIAN_POINT('Ctrl Pts',(-144.726862579758,-4.68152918324244,
132.317902563921));
#110607=CARTESIAN_POINT('Ctrl Pts',(-144.73456765869,-4.63809490151152,
132.446170711984));
#110608=CARTESIAN_POINT('Ctrl Pts',(-144.742272737621,-4.58949059879999,
132.572342265103));
#110609=CARTESIAN_POINT('Ctrl Pts',(-144.75004707174,-4.54044942838947,
132.699647879879));
#110610=CARTESIAN_POINT('Ctrl Pts',(-144.757821405859,-4.48602966459737,
132.825113098012));
#110611=CARTESIAN_POINT('Ctrl Pts',(-144.765595739979,-4.42638921100489,
132.948249983928));
#110612=CARTESIAN_POINT('Ctrl Pts',(-144.773360492926,-4.36682225894124,
133.071235114637));
#110613=CARTESIAN_POINT('Ctrl Pts',(-144.781125245873,-4.30204758767397,
133.191897274012));
#110614=CARTESIAN_POINT('Ctrl Pts',(-144.78888999882,-4.23227205541874,
133.30976603614));
#110615=CARTESIAN_POINT('Ctrl Pts',(-144.796647039705,-4.16256582520581,
133.427517729352));
#110616=CARTESIAN_POINT('Ctrl Pts',(-144.80440408059,-4.08786881628386,
133.542481212322));
#110617=CARTESIAN_POINT('Ctrl Pts',(-144.812161121475,-4.008434765724,133.654208647099));
#110618=CARTESIAN_POINT('Ctrl Pts',(-144.819912312715,-3.92906061699948,
133.76585182735));
#110619=CARTESIAN_POINT('Ctrl Pts',(-144.827663503955,-3.84495676258961,
133.874263499383));
#110620=CARTESIAN_POINT('Ctrl Pts',(-144.835414695195,-3.75642120882361,
133.979023239704));
#110621=CARTESIAN_POINT('Ctrl Pts',(-144.843162591972,-3.66792328502985,
134.083738454341));
#110622=CARTESIAN_POINT('Ctrl Pts',(-144.85091048875,-3.57499766003207,
134.184804526426));
#110623=CARTESIAN_POINT('Ctrl Pts',(-144.858658385527,-3.47798358996898,
134.281832861942));
#110624=CARTESIAN_POINT('Ctrl Pts',(-144.866404661611,-3.3809898131577,
134.378840901223));
#110625=CARTESIAN_POINT('Ctrl Pts',(-144.874150937695,-3.27990956860844,
134.471812607605));
#110626=CARTESIAN_POINT('Ctrl Pts',(-144.881897213779,-3.17511977902612,
134.560395421896));
#110627=CARTESIAN_POINT('Ctrl Pts',(-144.889643547044,-3.07032921590952,
134.648978890085));
#110628=CARTESIAN_POINT('Ctrl Pts',(-144.89738988031,-2.96182935169657,
134.733173149137));
#110629=CARTESIAN_POINT('Ctrl Pts',(-144.905136213575,-2.85003075609275,
134.812665465232));
#110630=CARTESIAN_POINT('Ctrl Pts',(-144.912884281578,-2.73820712396876,
134.892175583081));
#110631=CARTESIAN_POINT('Ctrl Pts',(-144.920632349581,-2.62308360904085,
134.966981436177));
#110632=CARTESIAN_POINT('Ctrl Pts',(-144.928380417584,-2.50510001983634,
135.036813446968));
#110633=CARTESIAN_POINT('Ctrl Pts',(-144.936136720326,-2.38699103626904,
135.106719676052));
#110634=CARTESIAN_POINT('Ctrl Pts',(-144.943893023068,-2.26601624324084,
135.171641303504));
#110635=CARTESIAN_POINT('Ctrl Pts',(-144.951649325809,-2.14264081787303,
135.231354336568));
#110636=CARTESIAN_POINT('Ctrl Pts',(-144.959409768324,-2.0191995433256,
135.291099240276));
#110637=CARTESIAN_POINT('Ctrl Pts',(-144.967170210838,-1.89335544191891,
135.345629854871));
#110638=CARTESIAN_POINT('Ctrl Pts',(-144.974930653352,-1.765593028403,135.394770655956));
#110639=CARTESIAN_POINT('Ctrl Pts',(-144.982703553617,-1.63762551931871,
135.443990342218));
#110640=CARTESIAN_POINT('Ctrl Pts',(-144.990476453883,-1.50773391508519,
135.487802800074));
#110641=CARTESIAN_POINT('Ctrl Pts',(-144.998249354148,-1.37641808392046,
135.526082371414));
#110642=CARTESIAN_POINT('Ctrl Pts',(-145.005739689911,-1.24987591397607,
135.562970383916));
#110643=CARTESIAN_POINT('Ctrl Pts',(-145.013230025673,-1.1220115667598,
135.594720720418));
#110644=CARTESIAN_POINT('Ctrl Pts',(-145.020720361436,-0.993278741260765,
135.621266305314));
#110645=CARTESIAN_POINT('Ctrl Pts',(-145.028494695555,-0.859664971561687,
135.648818374129));
#110646=CARTESIAN_POINT('Ctrl Pts',(-145.036269029674,-0.724692318579218,
135.670850500661));
#110647=CARTESIAN_POINT('Ctrl Pts',(-145.044043363793,-0.588856647073741,
135.687231792571));
#110648=CARTESIAN_POINT('Ctrl Pts',(-145.05180811674,-0.453188380893411,
135.703592896003));
#110649=CARTESIAN_POINT('Ctrl Pts',(-145.059572869687,-0.316659596850146,
135.714316975031));
#110650=CARTESIAN_POINT('Ctrl Pts',(-145.067337622635,-0.179777889508018,
135.719323788633));
#110651=CARTESIAN_POINT('Ctrl Pts',(-145.07509466352,-0.0430321350073147,
135.724325629397));
#110652=CARTESIAN_POINT('Ctrl Pts',(-145.082851704405,0.0940654570492294,
135.723621490945));
#110653=CARTESIAN_POINT('Ctrl Pts',(-145.09060874529,0.231000956826365,
135.717182782111));
#110654=CARTESIAN_POINT('Ctrl Pts',(-145.09835993653,0.36783319247773,135.710748928757));
#110655=CARTESIAN_POINT('Ctrl Pts',(-145.10611112777,0.5045031901976,135.698589130933));
#110656=CARTESIAN_POINT('Ctrl Pts',(-145.11386231901,0.640496156091784,
135.680726860634));
#110657=CARTESIAN_POINT('Ctrl Pts',(-145.121610215787,0.776431321347918,
135.662872182276));
#110658=CARTESIAN_POINT('Ctrl Pts',(-145.129358112564,0.911689640280075,
135.639319902812));
#110659=CARTESIAN_POINT('Ctrl Pts',(-145.137106009342,1.04576080150545,
135.610145403481));
#110660=CARTESIAN_POINT('Ctrl Pts',(-145.144852285426,1.17980391793451,
135.580977006826));
#110661=CARTESIAN_POINT('Ctrl Pts',(-145.15259856151,1.31265998881138,135.546188812605));
#110662=CARTESIAN_POINT('Ctrl Pts',(-145.160344837594,1.44382866017305,
135.505907369707));
#110663=CARTESIAN_POINT('Ctrl Pts',(-145.16809117086,1.57499829979187,135.46562562946));
#110664=CARTESIAN_POINT('Ctrl Pts',(-145.175837504125,1.70448014130158,
135.419850674397));
#110665=CARTESIAN_POINT('Ctrl Pts',(-145.18358383739,1.83178914992934,135.368758888171));
#110666=CARTESIAN_POINT('Ctrl Pts',(-145.191331905393,1.95912666852671,
135.317655660294));
#110667=CARTESIAN_POINT('Ctrl Pts',(-145.199079973396,2.08429002321555,
135.261233377549));
#110668=CARTESIAN_POINT('Ctrl Pts',(-145.206828041399,2.20681468351453,
135.199716350055));
#110669=CARTESIAN_POINT('Ctrl Pts',(-145.214584344141,2.32946956448071,
135.138133941532));
#110670=CARTESIAN_POINT('Ctrl Pts',(-145.222340646883,2.44947979893839,
135.071446147409));
#110671=CARTESIAN_POINT('Ctrl Pts',(-145.230096949625,2.56640549583982,
134.999923260815));
#110672=CARTESIAN_POINT('Ctrl Pts',(-145.237857392139,2.68339359950625,
134.928362200302));
#110673=CARTESIAN_POINT('Ctrl Pts',(-145.245617834653,2.79729356067612,
134.85196112287));
#110674=CARTESIAN_POINT('Ctrl Pts',(-145.253378277168,2.90769581364454,
134.771032789275));
#110675=CARTESIAN_POINT('Ctrl Pts',(-145.261151177433,3.01827529411048,
134.689974542335));
#110676=CARTESIAN_POINT('Ctrl Pts',(-145.268924077699,3.1253455406053,134.604374760621));
#110677=CARTESIAN_POINT('Ctrl Pts',(-145.276696977964,3.22853064241857,
134.514586076142));
#110678=CARTESIAN_POINT('Ctrl Pts',(-145.284187313725,3.32796470586329,
134.428061436517));
#110679=CARTESIAN_POINT('Ctrl Pts',(-145.291677649487,3.42379096609442,
134.337647372335));
#110680=CARTESIAN_POINT('Ctrl Pts',(-145.299167985248,3.51570775512027,
134.243689337402));
#110681=CARTESIAN_POINT('Ctrl Pts',(-145.306942319367,3.61110959714906,
134.146168855007));
#110682=CARTESIAN_POINT('Ctrl Pts',(-145.314716653486,3.70260186501073,
134.044521441985));
#110683=CARTESIAN_POINT('Ctrl Pts',(-145.322490987605,3.78980640825618,
133.939093532894));
#110684=CARTESIAN_POINT('Ctrl Pts',(-145.330255740553,3.87690347969578,
133.833795554279));
#110685=CARTESIAN_POINT('Ctrl Pts',(-145.3380204935,3.95972309378019,133.724726648233));
#110686=CARTESIAN_POINT('Ctrl Pts',(-145.345785246447,4.03792337420397,
133.612270496205));
#110687=CARTESIAN_POINT('Ctrl Pts',(-145.353542287332,4.1160459850068,133.499926037213));
#110688=CARTESIAN_POINT('Ctrl Pts',(-145.361299328217,4.18955817068668,
133.384201346178));
#110689=CARTESIAN_POINT('Ctrl Pts',(-145.369056369102,4.25815808505595,
133.265513352601));
#110690=CARTESIAN_POINT('Ctrl Pts',(-145.376807560342,4.32670626769607,
133.146914862565));
#110691=CARTESIAN_POINT('Ctrl Pts',(-145.384558751582,4.39034935752116,
133.025357855044));
#110692=CARTESIAN_POINT('Ctrl Pts',(-145.392309942822,4.44882884351171,
132.90128812791));
#110693=CARTESIAN_POINT('Ctrl Pts',(-145.400057839599,4.50728347416081,
132.77727113372));
#110694=CARTESIAN_POINT('Ctrl Pts',(-145.407805736377,4.56057869966388,
132.650743896941));
#110695=CARTESIAN_POINT('Ctrl Pts',(-145.415553633154,4.60850210462471,
132.522176502395));
#110696=CARTESIAN_POINT('Ctrl Pts',(-145.423299909238,4.65641548504234,
132.393636001376));
#110697=CARTESIAN_POINT('Ctrl Pts',(-145.431046185322,4.69895914348969,
132.263056557542));
#110698=CARTESIAN_POINT('Ctrl Pts',(-145.438792461406,4.73596909559401,
132.130927535621));
#110699=CARTESIAN_POINT('Ctrl Pts',(-145.446538794672,4.77297932089734,
131.998797538354));
#110700=CARTESIAN_POINT('Ctrl Pts',(-145.454285127937,4.80445565289487,
131.865118316649));
#110701=CARTESIAN_POINT('Ctrl Pts',(-145.462031461202,4.83028431500737,
131.730393283671));
#110702=CARTESIAN_POINT('Ctrl Pts',(-145.469779529205,4.8561187612697,131.595638079956));
#110703=CARTESIAN_POINT('Ctrl Pts',(-145.477527597208,4.87630294732916,
131.459836982832));
#110704=CARTESIAN_POINT('Ctrl Pts',(-145.485275665211,4.8907745015692,131.323502060046));
#110705=CARTESIAN_POINT('Ctrl Pts',(-145.493031967953,4.90526143634928,
131.187022238883));
#110706=CARTESIAN_POINT('Ctrl Pts',(-145.500788270695,4.91402356959464,
131.050007848104));
#110707=CARTESIAN_POINT('Ctrl Pts',(-145.508544573437,4.91705053471405,
130.912975080545));
#110708=CARTESIAN_POINT('Ctrl Pts',(-145.516305015951,4.92007911541589,
130.775869174473));
#110709=CARTESIAN_POINT('Ctrl Pts',(-145.524065458466,4.91736643635554,
130.638745262774));
#110710=CARTESIAN_POINT('Ctrl Pts',(-145.53182590098,4.90895425174767,130.502116979505));
#110711=CARTESIAN_POINT('Ctrl Pts',(-145.539598801245,4.90052856315427,
130.365269368386));
#110712=CARTESIAN_POINT('Ctrl Pts',(-145.547371701511,4.88638512605326,
130.228919364716));
#110713=CARTESIAN_POINT('Ctrl Pts',(-145.555144601776,4.86661743082042,
130.093573839035));
#110714=CARTESIAN_POINT('Ctrl Pts',(-145.562634937539,4.84756834110051,
129.963148464123));
#110715=CARTESIAN_POINT('Ctrl Pts',(-145.570125273301,4.82329686258288,
129.833656107256));
#110716=CARTESIAN_POINT('Ctrl Pts',(-145.577615609063,4.79393057642016,
129.705537296479));
#110717=CARTESIAN_POINT('Ctrl Pts',(-145.585389943182,4.76345085859289,
129.572560822056));
#110718=CARTESIAN_POINT('Ctrl Pts',(-145.593164277301,4.72738581681424,
129.440642876293));
#110719=CARTESIAN_POINT('Ctrl Pts',(-145.60093861142,4.68582251673542,129.310288864217));
#110720=CARTESIAN_POINT('Ctrl Pts',(-145.608703364367,4.64431043970944,
129.180095501811));
#110721=CARTESIAN_POINT('Ctrl Pts',(-145.616468117315,4.59731370445418,
129.051462607035));
#110722=CARTESIAN_POINT('Ctrl Pts',(-145.624232870262,4.54497032054591,
128.924885199303));
#110723=CARTESIAN_POINT('Ctrl Pts',(-145.631989911147,4.49267892482445,
128.798433510036));
#110724=CARTESIAN_POINT('Ctrl Pts',(-145.639746952032,4.43505159675745,
128.674033604014));
#110725=CARTESIAN_POINT('Ctrl Pts',(-145.647503992917,4.3722759557053,128.552164793562));
#110726=CARTESIAN_POINT('Ctrl Pts',(-145.655255184157,4.3095476542523,128.430387885328));
#110727=CARTESIAN_POINT('Ctrl Pts',(-145.663006375397,4.2416789457706,128.311138619633));
#110728=CARTESIAN_POINT('Ctrl Pts',(-145.670757566637,4.16890516111337,
128.194875453756));
#110729=CARTESIAN_POINT('Ctrl Pts',(-145.678505463414,4.09616230725602,
128.078661702827));
#110730=CARTESIAN_POINT('Ctrl Pts',(-145.686253360191,4.01851873070883,
127.965431858135));
#110731=CARTESIAN_POINT('Ctrl Pts',(-145.694001256968,3.93625511143424,
127.855618723095));
#110732=CARTESIAN_POINT('Ctrl Pts',(-145.701747533053,3.85400869993541,
127.745828558596));
#110733=CARTESIAN_POINT('Ctrl Pts',(-145.709493809137,3.76714440221338,
127.639453994874));
#110734=CARTESIAN_POINT('Ctrl Pts',(-145.717240085221,3.67598529711315,
127.536897510214));
#110735=CARTESIAN_POINT('Ctrl Pts',(-145.724986418486,3.58482551909723,
127.434340268505));
#110736=CARTESIAN_POINT('Ctrl Pts',(-145.732732751752,3.48937113018113,
127.335601454312));
#110737=CARTESIAN_POINT('Ctrl Pts',(-145.740479085017,3.38998416709723,
127.241048898206));
#110738=CARTESIAN_POINT('Ctrl Pts',(-145.74822715302,3.29057494699219,127.14647516771));
#110739=CARTESIAN_POINT('Ctrl Pts',(-145.755975221023,3.18723168348585,
127.056089830211));
#110740=CARTESIAN_POINT('Ctrl Pts',(-145.763723289026,3.08035148029499,
126.970222145843));
#110741=CARTESIAN_POINT('Ctrl Pts',(-145.771479591768,2.97335768355186,
126.884263200278));
#110742=CARTESIAN_POINT('Ctrl Pts',(-145.77923589451,2.86281974318605,126.802831744444));
#110743=CARTESIAN_POINT('Ctrl Pts',(-145.786992197251,2.74916634345377,
126.726215514885));
#110744=CARTESIAN_POINT('Ctrl Pts',(-145.794752639766,2.63545228348002,
126.649558392937));
#110745=CARTESIAN_POINT('Ctrl Pts',(-145.80251308228,2.51861978372378,126.577721822948));
#110746=CARTESIAN_POINT('Ctrl Pts',(-145.810273524794,2.39912354823579,
126.510948307666));
#110747=CARTESIAN_POINT('Ctrl Pts',(-145.818046425059,2.27943548678222,
126.44406760161));
#110748=CARTESIAN_POINT('Ctrl Pts',(-145.825819325325,2.15707549383549,
126.382266368289));
#110749=CARTESIAN_POINT('Ctrl Pts',(-145.83359222559,2.03252054776953,126.32573992751));
#110750=CARTESIAN_POINT('Ctrl Pts',(-145.841082561352,1.91249348773579,
126.271268365239));
#110751=CARTESIAN_POINT('Ctrl Pts',(-145.848572897114,1.79042857349879,
126.221694865612));
#110752=CARTESIAN_POINT('Ctrl Pts',(-145.856063232875,1.66676539450888,
126.17715020716));
#110753=CARTESIAN_POINT('Ctrl Pts',(-145.863837566994,1.53841348849389,
126.130916624442));
#110754=CARTESIAN_POINT('Ctrl Pts',(-145.871611901113,1.40793314859634,
126.089954293546));
#110755=CARTESIAN_POINT('Ctrl Pts',(-145.879386235232,1.27579664748769,
126.054463147435));
#110756=CARTESIAN_POINT('Ctrl Pts',(-145.887150988179,1.14382299280727,
126.019015740989));
#110757=CARTESIAN_POINT('Ctrl Pts',(-145.894915741126,1.0101976119957,125.989026203716));
#110758=CARTESIAN_POINT('Ctrl Pts',(-145.902680494073,0.875411576452517,
125.964645994335));
#110759=CARTESIAN_POINT('Ctrl Pts',(-145.910437534958,0.740759412299987,
125.940289999722));
#110760=CARTESIAN_POINT('Ctrl Pts',(-145.918194575843,0.604949269730058,
125.921532315073));
#110761=CARTESIAN_POINT('Ctrl Pts',(-145.925951616728,0.468485820624661,
125.908474170928));
#110762=CARTESIAN_POINT('Ctrl Pts',(-145.933702807968,0.332125279667952,
125.895425874031));
#110763=CARTESIAN_POINT('Ctrl Pts',(-145.941453999208,0.195112800405398,
125.888068599684));
#110764=CARTESIAN_POINT('Ctrl Pts',(-145.949205190448,0.0579612980052955,
125.886452164734));
#110765=CARTESIAN_POINT('Ctrl Pts',(-145.956953087225,-0.0791319113478376,
125.884836416813));
#110766=CARTESIAN_POINT('Ctrl Pts',(-145.964700984002,-0.216363636196324,
125.888956659892));
#110767=CARTESIAN_POINT('Ctrl Pts',(-145.97244888078,-0.353218032392594,
125.89881069079));
#110768=CARTESIAN_POINT('Ctrl Pts',(-145.980195156864,-0.49004380159942,
125.908662660437));
#110769=CARTESIAN_POINT('Ctrl Pts',(-145.987941432948,-0.626492009439593,
125.924246004199));
#110770=CARTESIAN_POINT('Ctrl Pts',(-145.995687709032,-0.76204940752565,
125.945506456039));
#110771=CARTESIAN_POINT('Ctrl Pts',(-146.003434042297,-0.89760780626544,
125.966767064818));
#110772=CARTESIAN_POINT('Ctrl Pts',(-146.011180375562,-1.03227499588601,
125.99370480472));
#110773=CARTESIAN_POINT('Ctrl Pts',(-146.018926708828,-1.16554582041393,
126.026213905397));
#110774=CARTESIAN_POINT('Ctrl Pts',(-146.026674776831,-1.29884649001916,
126.058730286261));
#110775=CARTESIAN_POINT('Ctrl Pts',(-146.034422844833,-1.43074979252714,
126.096820417978));
#110776=CARTESIAN_POINT('Ctrl Pts',(-146.042170912836,-1.56076406780385,
126.14032817909));
#110777=CARTESIAN_POINT('Ctrl Pts',(-146.049927215578,-1.69091652379934,
126.183882180769));
#110778=CARTESIAN_POINT('Ctrl Pts',(-146.05768351832,-1.81917557065732,
126.232865189642));
#110779=CARTESIAN_POINT('Ctrl Pts',(-146.065439821062,-1.94506741316322,
126.287072070135));
#110780=CARTESIAN_POINT('Ctrl Pts',(-146.073200263576,-2.07102644793634,
126.341307882472));
#110781=CARTESIAN_POINT('Ctrl Pts',(-146.08096070609,-2.19461540869649,
126.400772952599));
#110782=CARTESIAN_POINT('Ctrl Pts',(-146.088721148604,-2.31538449236595,
126.465215803779));
#110783=CARTESIAN_POINT('Ctrl Pts',(-146.09649404887,-2.43634744528957,
126.529762104345));
#110784=CARTESIAN_POINT('Ctrl Pts',(-146.104266949135,-2.55448113818088,
126.599301955636));
#110785=CARTESIAN_POINT('Ctrl Pts',(-146.1120398494,-2.6693634244918,126.673539637363));
#110786=CARTESIAN_POINT('Ctrl Pts',(-146.119530185163,-2.78006945032958,
126.745078592369));
#110787=CARTESIAN_POINT('Ctrl Pts',(-146.127020520925,-2.88775610731852,
126.820979574334));
#110788=CARTESIAN_POINT('Ctrl Pts',(-146.134510856687,-2.99207575894011,
126.900943433192));
#110789=CARTESIAN_POINT('Ctrl Pts',(-146.142227797771,-3.09955139567316,
126.983326440736));
#110790=CARTESIAN_POINT('Ctrl Pts',(-146.149944738854,-3.20381148190246,
127.07029702923));
#110791=CARTESIAN_POINT('Ctrl Pts',(-146.157661679937,-3.30443283070756,
127.161572299554));
#110792=CARTESIAN_POINT('Ctrl Pts',(-146.165338592275,-3.40453224389806,
127.252374113551));
#110793=CARTESIAN_POINT('Ctrl Pts',(-146.173015504613,-3.5010302502149,
127.347435823624));
#110794=CARTESIAN_POINT('Ctrl Pts',(-146.18069241695,-3.59353889837519,
127.446435477191));
#110795=CARTESIAN_POINT('Ctrl Pts',(-146.18836232351,-3.68596312521306,
127.545344785889));
#110796=CARTESIAN_POINT('Ctrl Pts',(-146.196032230069,-3.77440496146833,
127.648184601815));
#110797=CARTESIAN_POINT('Ctrl Pts',(-146.203702136628,-3.85851097715001,
127.754594052448));
#110798=CARTESIAN_POINT('Ctrl Pts',(-146.211366795343,-3.9425594464631,
127.860930696428));
#110799=CARTESIAN_POINT('Ctrl Pts',(-146.219031454058,-4.02227774844276,
127.97083180432));
#110800=CARTESIAN_POINT('Ctrl Pts',(-146.226696112773,-4.09735102217618,
128.083901526976));
#110801=CARTESIAN_POINT('Ctrl Pts',(-146.234447890266,-4.17327760094385,
128.198256433543));
#110802=CARTESIAN_POINT('Ctrl Pts',(-146.242199667759,-4.24445262150303,
128.315852125728));
#110803=CARTESIAN_POINT('Ctrl Pts',(-146.249951445252,-4.31059385348899,
128.43624666491));
#110804=CARTESIAN_POINT('Ctrl Pts',(-146.257611948836,-4.37595630038468,
128.555223609209));
#110805=CARTESIAN_POINT('Ctrl Pts',(-146.265272452421,-4.43640268564307,
128.676933474641));
#110806=CARTESIAN_POINT('Ctrl Pts',(-146.272932956006,-4.49170598713918,
128.800923474155));
#110807=CARTESIAN_POINT('Ctrl Pts',(-146.280730370453,-4.54799768614846,
128.927129460851));
#110808=CARTESIAN_POINT('Ctrl Pts',(-146.2885277849,-4.5989605040081,129.055697485442));
#110809=CARTESIAN_POINT('Ctrl Pts',(-146.296325199347,-4.64440591072963,
129.186128001753));
#110810=CARTESIAN_POINT('Ctrl Pts',(-146.304122613794,-4.68985131745129,
129.316558518066));
#110811=CARTESIAN_POINT('Ctrl Pts',(-146.311920028241,-4.72977919261785,
129.448851105942));
#110812=CARTESIAN_POINT('Ctrl Pts',(-146.319717442688,-4.76405452823404,
129.582490119308));
#110813=CARTESIAN_POINT('Origin',(213.235140564004,0.,130.804360617566));
#110814=CARTESIAN_POINT('',(-148.415413529701,-4.76405452823396,129.582490119308));
#110815=CARTESIAN_POINT('',(-148.069858671336,-4.76405452823417,129.582490119309));
#110816=CARTESIAN_POINT('',(213.235140564004,-4.76405452823405,129.582490119308));
#110817=CARTESIAN_POINT('',(-146.735140564047,-4.91824791181105,130.799828458446));
#110818=CARTESIAN_POINT('Ctrl Pts',(-146.735140564047,-4.91824791181105,
130.799828458447));
#110819=CARTESIAN_POINT('Ctrl Pts',(-146.742795394334,-4.91837240966069,
130.934932119401));
#110820=CARTESIAN_POINT('Ctrl Pts',(-146.750450224622,-4.91292580148298,
131.070197708801));
#110821=CARTESIAN_POINT('Ctrl Pts',(-146.758105054909,-4.90189488163458,
131.205121932946));
#110822=CARTESIAN_POINT('Ctrl Pts',(-146.76611170812,-4.89035697073346,
131.346247396458));
#110823=CARTESIAN_POINT('Ctrl Pts',(-146.774118361331,-4.87270916905005,
131.486998925891));
#110824=CARTESIAN_POINT('Ctrl Pts',(-146.782125014542,-4.8489974415009,
131.626800204902));
#110825=CARTESIAN_POINT('Ctrl Pts',(-146.789771185002,-4.82635328470157,
131.760307224841));
#110826=CARTESIAN_POINT('Ctrl Pts',(-146.797417355461,-4.79817939812983,
131.892947251875));
#110827=CARTESIAN_POINT('Ctrl Pts',(-146.805063525921,-4.76456878221447,
132.024224291116));
#110828=CARTESIAN_POINT('Ctrl Pts',(-146.812708519105,-4.73096334130619,
132.155481117707));
#110829=CARTESIAN_POINT('Ctrl Pts',(-146.820353512288,-4.69192293508799,
132.285374984212));
#110830=CARTESIAN_POINT('Ctrl Pts',(-146.827998505472,-4.6475912792535,
132.413421947506));
#110831=CARTESIAN_POINT('Ctrl Pts',(-146.835644080023,-4.6032562521943,
132.541478648199));
#110832=CARTESIAN_POINT('Ctrl Pts',(-146.843289654574,-4.55362930726439,
132.667687786376));
#110833=CARTESIAN_POINT('Ctrl Pts',(-146.850935229125,-4.49890326506744,
132.791582918685));
#110834=CARTESIAN_POINT('Ctrl Pts',(-146.858583143927,-4.44416047165521,
132.915515974329));
#110835=CARTESIAN_POINT('Ctrl Pts',(-146.866231058729,-4.38431563998919,
133.037133248047));
#110836=CARTESIAN_POINT('Ctrl Pts',(-146.873878973531,-4.3196084856433,
133.155991029272));
#110837=CARTESIAN_POINT('Ctrl Pts',(-146.881535126221,-4.25483163252887,
133.274976837158));
#110838=CARTESIAN_POINT('Ctrl Pts',(-146.88919127891,-4.18518219572135,
133.391196866629));
#110839=CARTESIAN_POINT('Ctrl Pts',(-146.896847431599,-4.11094447671507,
133.504234424222));
#110840=CARTESIAN_POINT('Ctrl Pts',(-146.904508421899,-4.03665984992233,
133.617343405636));
#110841=CARTESIAN_POINT('Ctrl Pts',(-146.912169412199,-3.9577814038534,
133.727265586795));
#110842=CARTESIAN_POINT('Ctrl Pts',(-146.919830402499,-3.87463419044237,
133.833616789096));
#110843=CARTESIAN_POINT('Ctrl Pts',(-146.927502235942,-3.79136929288242,
133.940118517798));
#110844=CARTESIAN_POINT('Ctrl Pts',(-146.935174069385,-3.70382383045527,
134.043038876829));
#110845=CARTESIAN_POINT('Ctrl Pts',(-146.942845902827,-3.61236036328028,
134.142029814521));
#110846=CARTESIAN_POINT('Ctrl Pts',(-146.945318845874,-3.58287797855105,
134.173938608271));
#110847=CARTESIAN_POINT('Ctrl Pts',(-146.94779178892,-3.55298876082955,
134.205439431177));
#110848=CARTESIAN_POINT('Ctrl Pts',(-146.950264731966,-3.52270557038244,
134.236521529717));
#110849=CARTESIAN_POINT('Ctrl Pts',(-146.958039066085,-3.42750255263486,
134.334236121055));
#110850=CARTESIAN_POINT('Ctrl Pts',(-146.965813400204,-3.3280799737141,
134.428141299042));
#110851=CARTESIAN_POINT('Ctrl Pts',(-146.973587734323,-3.22477509384618,
134.517850708654));
#110852=CARTESIAN_POINT('Ctrl Pts',(-146.98135248727,-3.12159752801007,
134.607449559436));
#110853=CARTESIAN_POINT('Ctrl Pts',(-146.989117240217,-3.01454747349441,
134.692862676526));
#110854=CARTESIAN_POINT('Ctrl Pts',(-146.996881993164,-2.90400029716957,
134.773739074773));
#110855=CARTESIAN_POINT('Ctrl Pts',(-147.004639034049,-2.793562917859,134.854535145441));
#110856=CARTESIAN_POINT('Ctrl Pts',(-147.012396074934,-2.67963564243843,
134.930803234923));
#110857=CARTESIAN_POINT('Ctrl Pts',(-147.020153115819,-2.56262803686791,
135.002231578798));
#110858=CARTESIAN_POINT('Ctrl Pts',(-147.027904307059,-2.44570866764246,
135.073606058004));
#110859=CARTESIAN_POINT('Ctrl Pts',(-147.035655498299,-2.32571392421053,
135.140147853202));
#110860=CARTESIAN_POINT('Ctrl Pts',(-147.043406689539,-2.20308327251162,
135.201587829899));
#110861=CARTESIAN_POINT('Ctrl Pts',(-147.051154586316,-2.08050474211114,
135.263001692966));
#110862=CARTESIAN_POINT('Ctrl Pts',(-147.058902483094,-1.95529288051316,
135.319317875569));
#110863=CARTESIAN_POINT('Ctrl Pts',(-147.066650379871,-1.82791253978112,
135.370312742743));
#110864=CARTESIAN_POINT('Ctrl Pts',(-147.074396655955,-1.70055884427036,
135.42129694289));
#110865=CARTESIAN_POINT('Ctrl Pts',(-147.082142932039,-1.57103793458912,
135.46696189642));
#110866=CARTESIAN_POINT('Ctrl Pts',(-147.089889208123,-1.43983509936622,
135.507131922779));
#110867=CARTESIAN_POINT('Ctrl Pts',(-147.097635541388,-1.30863129563363,
135.547302245664));
#110868=CARTESIAN_POINT('Ctrl Pts',(-147.105381874654,-1.17574591542118,
135.581977445982));
#110869=CARTESIAN_POINT('Ctrl Pts',(-147.113128207919,-1.04167949659853,
135.611031699392));
#110870=CARTESIAN_POINT('Ctrl Pts',(-147.120876275922,-0.907583054531121,
135.640092459301));
#110871=CARTESIAN_POINT('Ctrl Pts',(-147.128624343925,-0.772305429580536,
135.6635296847));
#110872=CARTESIAN_POINT('Ctrl Pts',(-147.136372411928,-0.636357045285282,
135.681268733721));
#110873=CARTESIAN_POINT('Ctrl Pts',(-147.144128714669,-0.500264173429578,
135.699026636014));
#110874=CARTESIAN_POINT('Ctrl Pts',(-147.151885017411,-0.363499506449614,
135.71107421357));
#110875=CARTESIAN_POINT('Ctrl Pts',(-147.159641320153,-0.226578839760653,
135.71738871558));
#110876=CARTESIAN_POINT('Ctrl Pts',(-147.167401762667,-0.0895850943892772,
135.723706587829));
#110877=CARTESIAN_POINT('Ctrl Pts',(-147.175162205181,0.0475644258267302,
135.724285285743));
#110878=CARTESIAN_POINT('Ctrl Pts',(-147.182922647695,0.184355232759708,
135.71915422571));
#110879=CARTESIAN_POINT('Ctrl Pts',(-147.190695547961,0.321365628439695,
135.714014928844));
#110880=CARTESIAN_POINT('Ctrl Pts',(-147.198468448226,0.458015770169014,
135.703147588835));
#110881=CARTESIAN_POINT('Ctrl Pts',(-147.206241348492,0.593796689860795,
135.686633505639));
#110882=CARTESIAN_POINT('Ctrl Pts',(-147.213731684254,0.724641631120937,
135.670719750962));
#110883=CARTESIAN_POINT('Ctrl Pts',(-147.221222020017,0.854679145953966,
135.649562721546));
#110884=CARTESIAN_POINT('Ctrl Pts',(-147.228712355779,0.983465771579554,
135.623279390344));
#110885=CARTESIAN_POINT('Ctrl Pts',(-147.236486689898,1.11713538124924,
135.595999518653));
#110886=CARTESIAN_POINT('Ctrl Pts',(-147.244261024017,1.24988079946168,
135.563110529677));
#110887=CARTESIAN_POINT('Ctrl Pts',(-147.252035358137,1.3811946774017,135.524687335667));
#110888=CARTESIAN_POINT('Ctrl Pts',(-147.259800111084,1.51234672272302,
135.48631149481));
#110889=CARTESIAN_POINT('Ctrl Pts',(-147.267564864031,1.64207036646498,
135.442415128249));
#110890=CARTESIAN_POINT('Ctrl Pts',(-147.275329616978,1.76986741991784,
135.393124326716));
#110891=CARTESIAN_POINT('Ctrl Pts',(-147.283086657863,1.89753754353559,
135.343882481503));
#110892=CARTESIAN_POINT('Ctrl Pts',(-147.290843698748,2.0232845224357,135.28925700342));
#110893=CARTESIAN_POINT('Ctrl Pts',(-147.298600739633,2.14662467997481,
135.229423955624));
#110894=CARTESIAN_POINT('Ctrl Pts',(-147.306351930873,2.26987182574184,
135.169636028395));
#110895=CARTESIAN_POINT('Ctrl Pts',(-147.314103122113,2.39071541246357,
135.104648517996));
#110896=CARTESIAN_POINT('Ctrl Pts',(-147.321854313353,2.50869146759271,
135.0346856858));
#110897=CARTESIAN_POINT('Ctrl Pts',(-147.32960221013,2.62661737975114,134.964752589674));
#110898=CARTESIAN_POINT('Ctrl Pts',(-147.337350106907,2.74167784879623,
134.889848576623));
#110899=CARTESIAN_POINT('Ctrl Pts',(-147.345098003684,2.85343346040303,
134.810243859693));
#110900=CARTESIAN_POINT('Ctrl Pts',(-147.352844279768,2.96516569514506,
134.730655794353));
#110901=CARTESIAN_POINT('Ctrl Pts',(-147.360590555852,3.0735941292553,134.646369207626));
#110902=CARTESIAN_POINT('Ctrl Pts',(-147.368336831937,3.1783086473509,134.55769742695));
#110903=CARTESIAN_POINT('Ctrl Pts',(-147.376083165202,3.28302393842515,
134.469024991718));
#110904=CARTESIAN_POINT('Ctrl Pts',(-147.383829498467,3.38402496041651,
134.375967550597));
#110905=CARTESIAN_POINT('Ctrl Pts',(-147.391575831732,3.48093530079744,
134.278878209141));
#110906=CARTESIAN_POINT('Ctrl Pts',(-147.399323899735,3.57786734357729,
134.181767125199));
#110907=CARTESIAN_POINT('Ctrl Pts',(-147.407071967738,3.67070660570791,
134.080622620881));
#110908=CARTESIAN_POINT('Ctrl Pts',(-147.414820035741,3.75911439248049,
133.97583378421));
#110909=CARTESIAN_POINT('Ctrl Pts',(-147.422576338483,3.84761614010079,
133.870933576718));
#110910=CARTESIAN_POINT('Ctrl Pts',(-147.430332641225,3.9316767514697,133.762381598958));
#110911=CARTESIAN_POINT('Ctrl Pts',(-147.438088943967,4.0109982856649,133.650599506854));
#110912=CARTESIAN_POINT('Ctrl Pts',(-147.445849386481,4.09036215615144,
133.538757753281));
#110913=CARTESIAN_POINT('Ctrl Pts',(-147.453609828995,4.16498169683597,
133.423682778004));
#110914=CARTESIAN_POINT('Ctrl Pts',(-147.461370271509,4.23460356315992,
133.305823334732));
#110915=CARTESIAN_POINT('Ctrl Pts',(-147.469143171775,4.30433719268442,
133.18777469302));
#110916=CARTESIAN_POINT('Ctrl Pts',(-147.47691607204,4.3690569312253,133.066932995924));
#110917=CARTESIAN_POINT('Ctrl Pts',(-147.484688972305,4.42855606905609,
132.943770397325));
#110918=CARTESIAN_POINT('Ctrl Pts',(-147.492179308068,4.4858922633597,132.825085069407));
#110919=CARTESIAN_POINT('Ctrl Pts',(-147.49966964383,4.53838070842162,132.70424493414));
#110920=CARTESIAN_POINT('Ctrl Pts',(-147.507159979592,4.58588011443595,
132.581686316058));
#110921=CARTESIAN_POINT('Ctrl Pts',(-147.514934313711,4.6351804748647,132.454480850725));
#110922=CARTESIAN_POINT('Ctrl Pts',(-147.52270864783,4.67926217800561,132.325021068937));
#110923=CARTESIAN_POINT('Ctrl Pts',(-147.53048298195,4.71791401523017,132.193774309522));
#110924=CARTESIAN_POINT('Ctrl Pts',(-147.538247734897,4.75651821751966,
132.062689300008));
#110925=CARTESIAN_POINT('Ctrl Pts',(-147.546012487844,4.78970575924094,
131.929822066209));
#110926=CARTESIAN_POINT('Ctrl Pts',(-147.553777240791,4.81731344093131,
131.795659903515));
#110927=CARTESIAN_POINT('Ctrl Pts',(-147.561534281676,4.84489370228309,
131.661630992572));
#110928=CARTESIAN_POINT('Ctrl Pts',(-147.569291322561,4.86690505413417,
131.526310092678));
#110929=CARTESIAN_POINT('Ctrl Pts',(-147.577048363446,4.88323418436421,
131.390199301127));
#110930=CARTESIAN_POINT('Ctrl Pts',(-147.584799554686,4.89955100067006,
131.254191151784));
#110931=CARTESIAN_POINT('Ctrl Pts',(-147.592550745926,4.91019407802103,
131.117394683028));
#110932=CARTESIAN_POINT('Ctrl Pts',(-147.600301937166,4.91510130536675,
130.980321466854));
#110933=CARTESIAN_POINT('Ctrl Pts',(-147.608049833943,4.92000644700997,
130.843306510452));
#110934=CARTESIAN_POINT('Ctrl Pts',(-147.61579773072,4.91918057346542,130.706015430476));
#110935=CARTESIAN_POINT('Ctrl Pts',(-147.623545627498,4.91261350844471,
130.568963975393));
#110936=CARTESIAN_POINT('Ctrl Pts',(-147.631291903582,4.90604781711242,
130.431941188519));
#110937=CARTESIAN_POINT('Ctrl Pts',(-147.639038179666,4.89374334172696,
130.295158317108));
#110938=CARTESIAN_POINT('Ctrl Pts',(-147.64678445575,4.87574201615306,130.15912976398));
#110939=CARTESIAN_POINT('Ctrl Pts',(-147.654530789015,4.85774055769745,
130.023100206719));
#110940=CARTESIAN_POINT('Ctrl Pts',(-147.662277122281,4.83404221643115,
129.887825366439));
#110941=CARTESIAN_POINT('Ctrl Pts',(-147.670023455546,4.80474060989277,
129.753812791835));
#110942=CARTESIAN_POINT('Ctrl Pts',(-147.677771523549,4.7754324414628,129.619770206045));
#110943=CARTESIAN_POINT('Ctrl Pts',(-147.685519591552,4.74051859432432,
129.486990830293));
#110944=CARTESIAN_POINT('Ctrl Pts',(-147.693267659555,4.70014334648945,
129.355969929612));
#110945=CARTESIAN_POINT('Ctrl Pts',(-147.701023962297,4.65972518736077,
129.224809778359));
#110946=CARTESIAN_POINT('Ctrl Pts',(-147.708780265039,4.61383414785842,
129.095412209785));
#110947=CARTESIAN_POINT('Ctrl Pts',(-147.716536567781,4.56266393470546,
128.968255805351));
#110948=CARTESIAN_POINT('Ctrl Pts',(-147.724297010295,4.51146641046904,
128.841031533716));
#110949=CARTESIAN_POINT('Ctrl Pts',(-147.732057452809,4.45498425909858,
128.716051165803));
#110950=CARTESIAN_POINT('Ctrl Pts',(-147.739817895323,4.39345809087738,
128.593770409906));
#110951=CARTESIAN_POINT('Ctrl Pts',(-147.747590795589,4.33183315538891,
128.471293358083));
#110952=CARTESIAN_POINT('Ctrl Pts',(-147.755363695854,4.2651482127556,128.351524920088));
#110953=CARTESIAN_POINT('Ctrl Pts',(-147.76313659612,4.19368876775168,128.234894217371));
#110954=CARTESIAN_POINT('Ctrl Pts',(-147.770626931882,4.12482705357146,
128.122503334476));
#110955=CARTESIAN_POINT('Ctrl Pts',(-147.778117267643,4.05153211206293,
128.013026274307));
#110956=CARTESIAN_POINT('Ctrl Pts',(-147.785607603405,3.97409466482375,
127.906817752047));
#110957=CARTESIAN_POINT('Ctrl Pts',(-147.793381937524,3.89372115323352,
127.796582301381));
#110958=CARTESIAN_POINT('Ctrl Pts',(-147.801156271643,3.80863020962687,
127.689518941783));
#110959=CARTESIAN_POINT('Ctrl Pts',(-147.808930605762,3.71910085597341,
127.586057977105));
#110960=CARTESIAN_POINT('Ctrl Pts',(-147.816695358709,3.62968183924686,
127.48272451882));
#110961=CARTESIAN_POINT('Ctrl Pts',(-147.824460111656,3.53583554940689,
127.382984914718));
#110962=CARTESIAN_POINT('Ctrl Pts',(-147.832224864604,3.43788374857132,
127.287239864193));
#110963=CARTESIAN_POINT('Ctrl Pts',(-147.839981905489,3.34002923484521,
127.191589909001));
#110964=CARTESIAN_POINT('Ctrl Pts',(-147.847738946374,3.23807760261019,
127.099926883506));
#110965=CARTESIAN_POINT('Ctrl Pts',(-147.855495987258,3.13239003257192,
127.012617516254));
#110966=CARTESIAN_POINT('Ctrl Pts',(-147.863247178499,3.02678216235249,
126.925373989676));
#110967=CARTESIAN_POINT('Ctrl Pts',(-147.870998369739,2.9174442621906,126.842477834471));
#110968=CARTESIAN_POINT('Ctrl Pts',(-147.878749560979,2.80477315955378,
126.764257823583));
#110969=CARTESIAN_POINT('Ctrl Pts',(-147.886497457756,2.69214994514103,
126.686071058287));
#110970=CARTESIAN_POINT('Ctrl Pts',(-147.894245354533,2.57619666644804,
126.612556706841));
#110971=CARTESIAN_POINT('Ctrl Pts',(-147.90199325131,2.45734173673487,126.544002105492));
#110972=CARTESIAN_POINT('Ctrl Pts',(-147.909739527394,2.33851166891046,
126.475461844287));
#110973=CARTESIAN_POINT('Ctrl Pts',(-147.917485803478,2.21678149580125,
126.411879464805));
#110974=CARTESIAN_POINT('Ctrl Pts',(-147.925232079562,2.09260666534645,
126.353497734186));
#110975=CARTESIAN_POINT('Ctrl Pts',(-147.932978412827,1.96843091826176,
126.295115572607));
#110976=CARTESIAN_POINT('Ctrl Pts',(-147.940724746093,1.84181083163353,
126.241934302843));
#110977=CARTESIAN_POINT('Ctrl Pts',(-147.948471079358,1.71322402312201,
126.194149504277));
#110978=CARTESIAN_POINT('Ctrl Pts',(-147.956219147361,1.5846084184868,126.146354004636));
#110979=CARTESIAN_POINT('Ctrl Pts',(-147.963967215364,1.45402558196438,
126.103957517135));
#110980=CARTESIAN_POINT('Ctrl Pts',(-147.971715283367,1.32197017984307,
126.067106359443));
#110981=CARTESIAN_POINT('Ctrl Pts',(-147.979471586109,1.18977442766799,
126.030216035902));
#110982=CARTESIAN_POINT('Ctrl Pts',(-147.98722788885,1.0561033606954,125.998882920611));
#110983=CARTESIAN_POINT('Ctrl Pts',(-147.994984191592,0.921464326278293,
125.973202727588));
#110984=CARTESIAN_POINT('Ctrl Pts',(-148.002744634106,0.786753430954979,
125.947508828273));
#110985=CARTESIAN_POINT('Ctrl Pts',(-148.010505076621,0.65107392533345,
125.927473920206));
#110986=CARTESIAN_POINT('Ctrl Pts',(-148.018265519135,0.514939265442972,
125.913141892605));
#110987=CARTESIAN_POINT('Ctrl Pts',(-148.0260384194,0.378586070110599,125.898786857962));
#110988=CARTESIAN_POINT('Ctrl Pts',(-148.033811319665,0.241776650843219,
125.890153022571));
#110989=CARTESIAN_POINT('Ctrl Pts',(-148.041584219931,0.105026361975948,
125.887232133807));
#110990=CARTESIAN_POINT('Ctrl Pts',(-148.049074555693,-0.0267527094392925,
125.884417426707));
#110991=CARTESIAN_POINT('Ctrl Pts',(-148.056564891455,-0.158476566930597,
125.886907511672));
#110992=CARTESIAN_POINT('Ctrl Pts',(-148.064055227217,-0.289689636442435,
125.894649528608));
#110993=CARTESIAN_POINT('Ctrl Pts',(-148.071829561336,-0.425877689364814,
125.902685086469));
#110994=CARTESIAN_POINT('Ctrl Pts',(-148.079603895455,-0.561946859468491,
125.916404146196));
#110995=CARTESIAN_POINT('Ctrl Pts',(-148.087378229574,-0.697384301744843,
125.935804548444));
#110996=CARTESIAN_POINT('Ctrl Pts',(-148.095142982522,-0.832654829477982,
125.955181041431));
#110997=CARTESIAN_POINT('Ctrl Pts',(-148.102907735469,-0.967294795162843,
125.980224890647));
#110998=CARTESIAN_POINT('Ctrl Pts',(-148.110672488416,-1.1007931587684,
126.010881976317));
#110999=CARTESIAN_POINT('Ctrl Pts',(-148.118429529301,-1.23415892991759,
126.041508612938));
#111000=CARTESIAN_POINT('Ctrl Pts',(-148.126186570186,-1.36638497682959,
126.077737304284));
#111001=CARTESIAN_POINT('Ctrl Pts',(-148.133943611071,-1.49696753339659,
126.119462404535));
#111002=CARTESIAN_POINT('Ctrl Pts',(-148.141694802311,-1.62745161664102,
126.161156039564));
#111003=CARTESIAN_POINT('Ctrl Pts',(-148.149445993551,-1.75629430552048,
126.208337714841));
#111004=CARTESIAN_POINT('Ctrl Pts',(-148.157197184791,-1.88300449910607,
126.260851277986));
#111005=CARTESIAN_POINT('Ctrl Pts',(-148.164945081568,-2.00966083747979,
126.313342521467));
#111006=CARTESIAN_POINT('Ctrl Pts',(-148.172692978346,-2.13418612283538,
126.371160996155));
#111007=CARTESIAN_POINT('Ctrl Pts',(-148.180440875123,-2.25610704322118,
126.434101578101));
#111008=CARTESIAN_POINT('Ctrl Pts',(-148.188187151207,-2.37800246037876,
126.497028994234));
#111009=CARTESIAN_POINT('Ctrl Pts',(-148.195933427291,-2.49729424897409,
126.565076207252));
#111010=CARTESIAN_POINT('Ctrl Pts',(-148.203679703375,-2.61353198139975,
126.637991257476));
#111011=CARTESIAN_POINT('Ctrl Pts',(-148.211426036641,-2.7297705718661,
126.710906845941));
#111012=CARTESIAN_POINT('Ctrl Pts',(-148.219172369906,-2.84295472998101,
126.788690135557));
#111013=CARTESIAN_POINT('Ctrl Pts',(-148.226918703171,-2.95266174525944,
126.871045008492));
#111014=CARTESIAN_POINT('Ctrl Pts',(-148.234666771174,-3.06239332866343,
126.953418324231));
#111015=CARTESIAN_POINT('Ctrl Pts',(-148.242414839177,-3.16864590713363,
127.04036502581));
#111016=CARTESIAN_POINT('Ctrl Pts',(-148.25016290718,-3.27102900025871,
127.131548024747));
#111017=CARTESIAN_POINT('Ctrl Pts',(-148.257919209922,-3.3735209073534,
127.222827934061));
#111018=CARTESIAN_POINT('Ctrl Pts',(-148.265675512664,-3.47213482144369,
127.318352874299));
#111019=CARTESIAN_POINT('Ctrl Pts',(-148.273431815406,-3.56651598197871,
127.417747735527));
#111020=CARTESIAN_POINT('Ctrl Pts',(-148.28119225792,-3.66094751658086,
127.517195646786));
#111021=CARTESIAN_POINT('Ctrl Pts',(-148.288952700435,-3.75114153910059,
127.62051730032));
#111022=CARTESIAN_POINT('Ctrl Pts',(-148.296713142949,-3.83678358876981,
127.727304434223));
#111023=CARTESIAN_POINT('Ctrl Pts',(-148.304486043214,-3.92256311866011,
127.834262992315));
#111024=CARTESIAN_POINT('Ctrl Pts',(-148.31225894348,-4.00377584176706,
127.944697832467));
#111025=CARTESIAN_POINT('Ctrl Pts',(-148.320031843745,-4.08015013965218,
128.058170911738));
#111026=CARTESIAN_POINT('Ctrl Pts',(-148.327522179507,-4.15374803943145,
128.167518958752));
#111027=CARTESIAN_POINT('Ctrl Pts',(-148.335012515269,-4.22285302293328,
128.279687922415));
#111028=CARTESIAN_POINT('Ctrl Pts',(-148.342502851031,-4.28726331394532,
128.394265943202));
#111029=CARTESIAN_POINT('Ctrl Pts',(-148.350634261164,-4.35718627997413,
128.518650337826));
#111030=CARTESIAN_POINT('Ctrl Pts',(-148.358765671297,-4.42178120596168,
128.646237719128));
#111031=CARTESIAN_POINT('Ctrl Pts',(-148.36689708143,-4.4807569195496,128.776553799743));
#111032=CARTESIAN_POINT('Ctrl Pts',(-148.375010992932,-4.5396057185882,
128.906589442775));
#111033=CARTESIAN_POINT('Ctrl Pts',(-148.383124904435,-4.59285927356076,
129.039341771286));
#111034=CARTESIAN_POINT('Ctrl Pts',(-148.391238815937,-4.64027184970223,
129.174311470037));
#111035=CARTESIAN_POINT('Ctrl Pts',(-148.399297053858,-4.68735910458748,
129.308355074584));
#111036=CARTESIAN_POINT('Ctrl Pts',(-148.40735529178,-4.728685140066,129.444585411646));
#111037=CARTESIAN_POINT('Ctrl Pts',(-148.415413529701,-4.76405452823396,
129.582490119308));
#111038=CARTESIAN_POINT('Ctrl Pts',(-146.665174983012,-4.76405452823419,
129.582490119309));
#111039=CARTESIAN_POINT('Ctrl Pts',(-146.667389024726,-4.77371530756762,
129.620157351307));
#111040=CARTESIAN_POINT('Ctrl Pts',(-146.66960306644,-4.78292519609886,
129.657923035737));
#111041=CARTESIAN_POINT('Ctrl Pts',(-146.671817108154,-4.79168258690122,
129.695775461212));
#111042=CARTESIAN_POINT('Ctrl Pts',(-146.682371017463,-4.83342737776348,
129.876210663977));
#111043=CARTESIAN_POINT('Ctrl Pts',(-146.692924926773,-4.86499443715233,
130.059082143305));
#111044=CARTESIAN_POINT('Ctrl Pts',(-146.703478836082,-4.88615669536868,
130.243418721463));
#111045=CARTESIAN_POINT('Ctrl Pts',(-146.714032745392,-4.90731895358504,
130.427755299621));
#111046=CARTESIAN_POINT('Ctrl Pts',(-146.724586654701,-4.91807626343323,
130.613557602484));
#111047=CARTESIAN_POINT('Ctrl Pts',(-146.735140564011,-4.91824791181047,
130.799828457817));
#111048=CARTESIAN_POINT('',(-146.389859435956,-4.91824941502472,130.806759389969));
#111049=CARTESIAN_POINT('Ctrl Pts',(-146.319717442688,-4.76405452823404,
129.582490119308));
#111050=CARTESIAN_POINT('Ctrl Pts',(-146.327388454375,-4.79777423132902,
129.713962729908));
#111051=CARTESIAN_POINT('Ctrl Pts',(-146.335059466061,-4.82602325428672,
129.846738034062));
#111052=CARTESIAN_POINT('Ctrl Pts',(-146.342730477747,-4.84872491478903,
129.980315859556));
#111053=CARTESIAN_POINT('Ctrl Pts',(-146.350585304115,-4.87197055810291,
130.117094509988));
#111054=CARTESIAN_POINT('Ctrl Pts',(-146.358440130483,-4.88939956768438,
130.254714181017));
#111055=CARTESIAN_POINT('Ctrl Pts',(-146.366294956852,-4.90098609526096,
130.392634547759));
#111056=CARTESIAN_POINT('Ctrl Pts',(-146.37414978322,-4.9125726228375,130.530554914501));
#111057=CARTESIAN_POINT('Ctrl Pts',(-146.382004609588,-4.91831671374134,
130.668775530728));
#111058=CARTESIAN_POINT('Ctrl Pts',(-146.389859435956,-4.91824941502472,
130.80675938997));
#111059=CARTESIAN_POINT('Ctrl Pts',(-146.389859435993,-4.9182494150244,
130.806759390615));
#111060=CARTESIAN_POINT('Ctrl Pts',(-146.397559117496,-4.91818344554288,
130.942017857041));
#111061=CARTESIAN_POINT('Ctrl Pts',(-146.405258798998,-4.912538321635,131.077135866295));
#111062=CARTESIAN_POINT('Ctrl Pts',(-146.4129584805,-4.90134546095345,131.211786359132));
#111063=CARTESIAN_POINT('Ctrl Pts',(-146.420732814619,-4.89004407937541,
131.347742362028));
#111064=CARTESIAN_POINT('Ctrl Pts',(-146.428507148739,-4.87306368550077,
131.483443127966));
#111065=CARTESIAN_POINT('Ctrl Pts',(-146.436281482858,-4.85041874491575,
131.618376011444));
#111066=CARTESIAN_POINT('Ctrl Pts',(-146.444046235805,-4.82780171219616,
131.753142602202));
#111067=CARTESIAN_POINT('Ctrl Pts',(-146.451810988752,-4.79953408705723,
131.887142811575));
#111068=CARTESIAN_POINT('Ctrl Pts',(-146.459575741699,-4.76568223723894,
132.019867045424));
#111069=CARTESIAN_POINT('Ctrl Pts',(-146.467332782584,-4.73186400955512,
132.152459455694));
#111070=CARTESIAN_POINT('Ctrl Pts',(-146.475089823469,-4.69247269063897,
132.283778036072));
#111071=CARTESIAN_POINT('Ctrl Pts',(-146.482846864354,-4.64762598488324,
132.413321700731));
#111072=CARTESIAN_POINT('Ctrl Pts',(-146.490598055594,-4.60281309837712,
132.542767675504));
#111073=CARTESIAN_POINT('Ctrl Pts',(-146.498349246834,-4.55255314098193,
132.670441030761));
#111074=CARTESIAN_POINT('Ctrl Pts',(-146.506100438074,-4.49701400517767,
132.795854554222));
#111075=CARTESIAN_POINT('Ctrl Pts',(-146.513848334852,-4.44149847498761,
132.92121477359));
#111076=CARTESIAN_POINT('Ctrl Pts',(-146.521596231629,-4.38070838709689,
133.04431671477));
#111077=CARTESIAN_POINT('Ctrl Pts',(-146.529344128406,-4.31486016456706,
133.164692124523));
#111078=CARTESIAN_POINT('Ctrl Pts',(-146.53709040449,-4.24902571606586,
133.285042354334));
#111079=CARTESIAN_POINT('Ctrl Pts',(-146.544836680574,-4.17813542496078,
133.402666844356));
#111080=CARTESIAN_POINT('Ctrl Pts',(-146.552582956658,-4.10245198739481,
133.51712134303));
#111081=CARTESIAN_POINT('Ctrl Pts',(-146.560329289923,-4.02676799115099,
133.631576686581));
#111082=CARTESIAN_POINT('Ctrl Pts',(-146.568075623189,-3.94629099348904,
133.742861665976));
#111083=CARTESIAN_POINT('Ctrl Pts',(-146.575821956454,-3.86132717085156,
133.850560798471));
#111084=CARTESIAN_POINT('Ctrl Pts',(-146.583570024457,-3.77634432115522,
133.958284049439));
#111085=CARTESIAN_POINT('Ctrl Pts',(-146.59131809246,-3.6868728891654,134.062419548692));
#111086=CARTESIAN_POINT('Ctrl Pts',(-146.599066160463,-3.59325923674562,
134.16258501746));
#111087=CARTESIAN_POINT('Ctrl Pts',(-146.606822463205,-3.4995460906219,
134.26285694328));
#111088=CARTESIAN_POINT('Ctrl Pts',(-146.614578765947,-3.40168219717782,
134.359150123825));
#111089=CARTESIAN_POINT('Ctrl Pts',(-146.622335068689,-3.30005107159837,
134.451118902309));
#111090=CARTESIAN_POINT('Ctrl Pts',(-146.630095511203,-3.19836570242715,
134.5431367673));
#111091=CARTESIAN_POINT('Ctrl Pts',(-146.637855953717,-3.09290939512924,
134.630825381373));
#111092=CARTESIAN_POINT('Ctrl Pts',(-146.645616396231,-2.98409784023135,
134.713880171479));
#111093=CARTESIAN_POINT('Ctrl Pts',(-146.653389296496,-2.8751116113657,
134.797068288507));
#111094=CARTESIAN_POINT('Ctrl Pts',(-146.661162196762,-2.76275969229254,
134.875607492694));
#111095=CARTESIAN_POINT('Ctrl Pts',(-146.668935097027,-2.64748651790352,
134.949236755645));
#111096=CARTESIAN_POINT('Ctrl Pts',(-146.676425432789,-2.53640381375977,
135.020189409427));
#111097=CARTESIAN_POINT('Ctrl Pts',(-146.683915768551,-2.42260882292317,
135.086582746558));
#111098=CARTESIAN_POINT('Ctrl Pts',(-146.691406104313,-2.30651812838755,
135.148224932427));
#111099=CARTESIAN_POINT('Ctrl Pts',(-146.699180438432,-2.18602581988309,
135.212204300508));
#111100=CARTESIAN_POINT('Ctrl Pts',(-146.706954772551,-2.06267860459535,
135.271267792897));
#111101=CARTESIAN_POINT('Ctrl Pts',(-146.71472910667,-1.93691560470815,
135.325150482483));
#111102=CARTESIAN_POINT('Ctrl Pts',(-146.722493859618,-1.81130759647854,
135.37896676647));
#111103=CARTESIAN_POINT('Ctrl Pts',(-146.730258612565,-1.68329008338702,
135.427614799163));
#111104=CARTESIAN_POINT('Ctrl Pts',(-146.738023365512,-1.55332767479957,
135.470874969542));
#111105=CARTESIAN_POINT('Ctrl Pts',(-146.745780406397,-1.42349434670848,
135.51409217331));
#111106=CARTESIAN_POINT('Ctrl Pts',(-146.753537447282,-1.29172033584053,
135.551932041415));
#111107=CARTESIAN_POINT('Ctrl Pts',(-146.761294488167,-1.15849084199306,
135.584222752766));
#111108=CARTESIAN_POINT('Ctrl Pts',(-146.769045679407,-1.02536181754346,
135.61648911344));
#111109=CARTESIAN_POINT('Ctrl Pts',(-146.776796870647,-0.890779873229676,
135.643214554959));
#111110=CARTESIAN_POINT('Ctrl Pts',(-146.784548061887,-0.75524566452571,
135.664276979883));
#111111=CARTESIAN_POINT('Ctrl Pts',(-146.792295958664,-0.619769061475753,
135.685330452715));
#111112=CARTESIAN_POINT('Ctrl Pts',(-146.800043855441,-0.483341384547462,
135.700725636247));
#111113=CARTESIAN_POINT('Ctrl Pts',(-146.807791752218,-0.34647357040469,
135.710391511019));
#111114=CARTESIAN_POINT('Ctrl Pts',(-146.815538028302,-0.209634386058108,
135.720055363897));
#111115=CARTESIAN_POINT('Ctrl Pts',(-146.823284304386,-0.0723556373705812,
135.723992264268));
#111116=CARTESIAN_POINT('Ctrl Pts',(-146.831030580471,0.0648469205584715,
135.722183097017));
#111117=CARTESIAN_POINT('Ctrl Pts',(-146.838776913736,0.202050491285826,
135.720373916412));
#111118=CARTESIAN_POINT('Ctrl Pts',(-146.846523247001,0.339177479201213,
135.712818588701));
#111119=CARTESIAN_POINT('Ctrl Pts',(-146.854269580267,0.475712831059523,
135.699550130227));
#111120=CARTESIAN_POINT('Ctrl Pts',(-146.86201764827,0.612278759063397,
135.686278700373));
#111121=CARTESIAN_POINT('Ctrl Pts',(-146.869765716273,0.748252398307283,
135.667291631675));
#111122=CARTESIAN_POINT('Ctrl Pts',(-146.877513784276,0.883124909789015,
135.642673697164));
#111123=CARTESIAN_POINT('Ctrl Pts',(-146.885270087018,1.01814076538077,
135.61802959842));
#111124=CARTESIAN_POINT('Ctrl Pts',(-146.893026389759,1.15205277020258,
135.587742749392));
#111125=CARTESIAN_POINT('Ctrl Pts',(-146.900782692501,1.28436281408676,
135.551948976332));
#111126=CARTESIAN_POINT('Ctrl Pts',(-146.908543135016,1.41674347582515,
135.516136099058));
#111127=CARTESIAN_POINT('Ctrl Pts',(-146.91630357753,1.54752010032395,135.474810558871));
#111128=CARTESIAN_POINT('Ctrl Pts',(-146.924064020044,1.67621175076582,
135.42815745881));
#111129=CARTESIAN_POINT('Ctrl Pts',(-146.931836920309,1.80510998846968,
135.381429467051));
#111130=CARTESIAN_POINT('Ctrl Pts',(-146.939609820575,1.9319162019058,135.329356973853));
#111131=CARTESIAN_POINT('Ctrl Pts',(-146.94738272084,2.05617055257688,135.272172802653));
#111132=CARTESIAN_POINT('Ctrl Pts',(-146.954873056602,2.17590794462324,
135.217067420115));
#111133=CARTESIAN_POINT('Ctrl Pts',(-146.962363392364,2.29327551165393,
135.157215691949));
#111134=CARTESIAN_POINT('Ctrl Pts',(-146.969853728126,2.4078866844924,135.092864409933));
#111135=CARTESIAN_POINT('Ctrl Pts',(-146.977628062245,2.52684337478388,
135.0260732295));
#111136=CARTESIAN_POINT('Ctrl Pts',(-146.985402396365,2.64320734648145,
134.954222984246));
#111137=CARTESIAN_POINT('Ctrl Pts',(-146.993176730484,2.75651835263832,
134.877539920527));
#111138=CARTESIAN_POINT('Ctrl Pts',(-147.000941483431,2.869689713107,134.800951361831));
#111139=CARTESIAN_POINT('Ctrl Pts',(-147.008706236378,2.97981527362293,
134.719542052387));
#111140=CARTESIAN_POINT('Ctrl Pts',(-147.016470989325,3.08645913650406,
134.633584176095));
#111141=CARTESIAN_POINT('Ctrl Pts',(-147.02422803021,3.19299707919715,134.547711674376));
#111142=CARTESIAN_POINT('Ctrl Pts',(-147.031985071095,3.29605990354734,
134.45729984));
#111143=CARTESIAN_POINT('Ctrl Pts',(-147.03974211198,3.39524078926313,134.362664011801));
#111144=CARTESIAN_POINT('Ctrl Pts',(-147.04749330322,3.49434688190162,134.268099549216));
#111145=CARTESIAN_POINT('Ctrl Pts',(-147.05524449446,3.58957658100332,134.169317701852));
#111146=CARTESIAN_POINT('Ctrl Pts',(-147.0629956857,3.68055654602248,134.066673688691));
#111147=CARTESIAN_POINT('Ctrl Pts',(-147.070743582477,3.77149784212941,
133.964073301973));
#111148=CARTESIAN_POINT('Ctrl Pts',(-147.078491479254,3.85819273786076,
133.857614306289));
#111149=CARTESIAN_POINT('Ctrl Pts',(-147.086239376031,3.94030530878379,
133.747688179369));
#111150=CARTESIAN_POINT('Ctrl Pts',(-147.093985652115,4.02240070352712,
133.637785046625));
#111151=CARTESIAN_POINT('Ctrl Pts',(-147.101731928199,4.0999154461931,133.524416538233));
#111152=CARTESIAN_POINT('Ctrl Pts',(-147.109478204283,4.17255467646619,
133.408006241379));
#111153=CARTESIAN_POINT('Ctrl Pts',(-147.117224537549,4.24519444294548,
133.291595085211));
#111154=CARTESIAN_POINT('Ctrl Pts',(-147.124970870814,4.31295841824567,
133.172142427463));
#111155=CARTESIAN_POINT('Ctrl Pts',(-147.132717204079,4.37559598108965,
133.050099443158));
#111156=CARTESIAN_POINT('Ctrl Pts',(-147.140465272082,4.43824757118162,
132.928029128173));
#111157=CARTESIAN_POINT('Ctrl Pts',(-147.148213340085,4.49577028589568,
132.803367680087));
#111158=CARTESIAN_POINT('Ctrl Pts',(-147.155961408088,4.54796040727584,
132.676589021461));
#111159=CARTESIAN_POINT('Ctrl Pts',(-147.16371771083,4.60020599693814,132.549675620967));
#111160=CARTESIAN_POINT('Ctrl Pts',(-147.171474013572,4.64710752267168,
132.420640877029));
#111161=CARTESIAN_POINT('Ctrl Pts',(-147.179230316314,4.68851001823618,
132.289977281244));
#111162=CARTESIAN_POINT('Ctrl Pts',(-147.186990758828,4.72993461155915,
132.159243946364));
#111163=CARTESIAN_POINT('Ctrl Pts',(-147.194751201342,4.76585422413791,
132.026880404484));
#111164=CARTESIAN_POINT('Ctrl Pts',(-147.202511643856,4.79616463030452,
131.893391334082));
#111165=CARTESIAN_POINT('Ctrl Pts',(-147.210284544122,4.82652369342594,
131.759687975174));
#111166=CARTESIAN_POINT('Ctrl Pts',(-147.218057444387,4.85125548590539,
131.624855861958));
#111167=CARTESIAN_POINT('Ctrl Pts',(-147.225830344652,4.87030733475456,
131.489407716338));
#111168=CARTESIAN_POINT('Ctrl Pts',(-147.233320680415,4.88866660091003,
131.35888345198));
#111169=CARTESIAN_POINT('Ctrl Pts',(-147.240811016177,4.90175168375792,
131.227787472777));
#111170=CARTESIAN_POINT('Ctrl Pts',(-147.248301351939,4.9095612661273,131.096578407309));
#111171=CARTESIAN_POINT('Ctrl Pts',(-147.256075686058,4.91766695118562,
130.960394510249));
#111172=CARTESIAN_POINT('Ctrl Pts',(-147.263850020177,4.92011487399926,
130.82365739266));
#111173=CARTESIAN_POINT('Ctrl Pts',(-147.271624354297,4.91684660731822,
130.686876565017));
#111174=CARTESIAN_POINT('Ctrl Pts',(-147.279389107244,4.91358236848378,
130.55026430752));
#111175=CARTESIAN_POINT('Ctrl Pts',(-147.287153860191,4.90461596624286,
130.413608834252));
#111176=CARTESIAN_POINT('Ctrl Pts',(-147.294918613138,4.88994078327235,
130.277424000325));
#111177=CARTESIAN_POINT('Ctrl Pts',(-147.302675654023,4.87528017590045,
130.141374427094));
#111178=CARTESIAN_POINT('Ctrl Pts',(-147.310432694908,4.85492211305399,
130.005794949164));
#111179=CARTESIAN_POINT('Ctrl Pts',(-147.318189735793,4.82891200192094,
129.871198284312));
#111180=CARTESIAN_POINT('Ctrl Pts',(-147.325940927033,4.80292150521505,
129.736703119852));
#111181=CARTESIAN_POINT('Ctrl Pts',(-147.333692118273,4.77128751785934,
129.603189675571));
#111182=CARTESIAN_POINT('Ctrl Pts',(-147.341443309513,4.73410709595915,
129.471164057981));
#111183=CARTESIAN_POINT('Ctrl Pts',(-147.34919120629,4.69694247673003,129.3391945548));
#111184=CARTESIAN_POINT('Ctrl Pts',(-147.356939103068,4.65423621736833,
129.208711996121));
#111185=CARTESIAN_POINT('Ctrl Pts',(-147.364686999845,4.60613610381531,
129.080210607959));
#111186=CARTESIAN_POINT('Ctrl Pts',(-147.372433275929,4.55804605176913,
128.951736099517));
#111187=CARTESIAN_POINT('Ctrl Pts',(-147.380179552013,4.50456452670903,
128.825242303214));
#111188=CARTESIAN_POINT('Ctrl Pts',(-147.387925828097,4.44588852532864,
128.701206252606));
#111189=CARTESIAN_POINT('Ctrl Pts',(-147.395672161362,4.38721209081541,
128.577169286392));
#111190=CARTESIAN_POINT('Ctrl Pts',(-147.403418494628,4.32334127065386,
128.45559045549));
#111191=CARTESIAN_POINT('Ctrl Pts',(-147.411164827893,4.254520184245,128.336924485798));
#111192=CARTESIAN_POINT('Ctrl Pts',(-147.418912895896,4.18568368583092,
128.218231941686));
#111193=CARTESIAN_POINT('Ctrl Pts',(-147.426660963899,4.11189491133377,
128.102453894953));
#111194=CARTESIAN_POINT('Ctrl Pts',(-147.434409031902,4.0334424706931,127.990017906006));
#111195=CARTESIAN_POINT('Ctrl Pts',(-147.442165334644,3.95490664986482,
127.877462418752));
#111196=CARTESIAN_POINT('Ctrl Pts',(-147.449921637386,3.87169748562741,
127.768256405885));
#111197=CARTESIAN_POINT('Ctrl Pts',(-147.457677940128,3.78414556207228,
127.662796448629));
#111198=CARTESIAN_POINT('Ctrl Pts',(-147.465438382642,3.69654690941941,
127.557280204219));
#111199=CARTESIAN_POINT('Ctrl Pts',(-147.473198825156,3.60460114088831,
127.455514289314));
#111200=CARTESIAN_POINT('Ctrl Pts',(-147.48095926767,3.5086765202576,127.357859182967));
#111201=CARTESIAN_POINT('Ctrl Pts',(-147.488732167936,3.41259791291007,
127.260047311974));
#111202=CARTESIAN_POINT('Ctrl Pts',(-147.496505068201,3.31252797535881,
127.166359703869));
#111203=CARTESIAN_POINT('Ctrl Pts',(-147.504277968467,3.20886960402755,
127.077117812643));
#111204=CARTESIAN_POINT('Ctrl Pts',(-147.511768304229,3.10897947559666,
126.991120088953));
#111205=CARTESIAN_POINT('Ctrl Pts',(-147.51925863999,3.00575752236836,126.909250659213));
#111206=CARTESIAN_POINT('Ctrl Pts',(-147.526748975752,2.89958888959299,
126.831758531546));
#111207=CARTESIAN_POINT('Ctrl Pts',(-147.534523309871,2.78939484083403,
126.751328266304));
#111208=CARTESIAN_POINT('Ctrl Pts',(-147.54229764399,2.67567719328548,126.675359007466));
#111209=CARTESIAN_POINT('Ctrl Pts',(-147.550071978109,2.55883303118256,
126.604175314388));
#111210=CARTESIAN_POINT('Ctrl Pts',(-147.557836731056,2.44213286906676,
126.533079348851));
#111211=CARTESIAN_POINT('Ctrl Pts',(-147.565601484004,2.32231418969519,
126.466757415701));
#111212=CARTESIAN_POINT('Ctrl Pts',(-147.573366236951,2.19980573710036,
126.40549283352));
#111213=CARTESIAN_POINT('Ctrl Pts',(-147.581123277836,2.07741896162737,
126.344289100185));
#111214=CARTESIAN_POINT('Ctrl Pts',(-147.588880318721,1.95234807679316,
126.288132895494));
#111215=CARTESIAN_POINT('Ctrl Pts',(-147.596637359606,1.82504899027767,
126.237263153576));
#111216=CARTESIAN_POINT('Ctrl Pts',(-147.604388550846,1.69784590099373,
126.186431772926));
#111217=CARTESIAN_POINT('Ctrl Pts',(-147.612139742086,1.56841831615429,
126.140879064528));
#111218=CARTESIAN_POINT('Ctrl Pts',(-147.619890933326,1.43724449869644,
126.100796935264));
#111219=CARTESIAN_POINT('Ctrl Pts',(-147.627638830103,1.30612643361,126.060731841975));
#111220=CARTESIAN_POINT('Ctrl Pts',(-147.63538672688,1.1732639851917,126.0261328173));
#111221=CARTESIAN_POINT('Ctrl Pts',(-147.643134623657,1.03915284169651,
125.997142665975));
#111222=CARTESIAN_POINT('Ctrl Pts',(-147.650880899741,0.905069751361432,
125.968158578766));
#111223=CARTESIAN_POINT('Ctrl Pts',(-147.658627175825,0.769738867387632,
125.94478111379));
#111224=CARTESIAN_POINT('Ctrl Pts',(-147.666373451909,0.633668013140237,
125.927102380439));
#111225=CARTESIAN_POINT('Ctrl Pts',(-147.674119785175,0.497596154449264,
125.909423516588));
#111226=CARTESIAN_POINT('Ctrl Pts',(-147.68186611844,0.360784702291752,
125.897443518675));
#111227=CARTESIAN_POINT('Ctrl Pts',(-147.689612451705,0.223748182943215,
125.891202792589));
#111228=CARTESIAN_POINT('Ctrl Pts',(-147.697360519708,0.0866809752161283,
125.884960668936));
#111229=CARTESIAN_POINT('Ctrl Pts',(-147.705108587711,-0.0506110095109376,
125.884460392432));
#111230=CARTESIAN_POINT('Ctrl Pts',(-147.712856655714,-0.187612051837948,
125.889690254204));
#111231=CARTESIAN_POINT('Ctrl Pts',(-147.720612958456,-0.324758700503263,
125.894925674336));
#111232=CARTESIAN_POINT('Ctrl Pts',(-147.728369261198,-0.461613397770562,
125.905903383354));
#111233=CARTESIAN_POINT('Ctrl Pts',(-147.73612556394,-0.5976637998468,125.922559613341));
#111234=CARTESIAN_POINT('Ctrl Pts',(-147.743886006454,-0.733786816119395,
125.939224733259));
#111235=CARTESIAN_POINT('Ctrl Pts',(-147.751646448968,-0.869104296280502,
125.961574349587));
#111236=CARTESIAN_POINT('Ctrl Pts',(-147.759406891482,-1.00311390352681,
125.989493479311));
#111237=CARTESIAN_POINT('Ctrl Pts',(-147.767179791747,-1.13733863489112,
126.0174574273));
#111238=CARTESIAN_POINT('Ctrl Pts',(-147.774952692013,-1.27025091855097,
126.051008659262));
#111239=CARTESIAN_POINT('Ctrl Pts',(-147.782725592278,-1.40136253080141,
126.089981960758));
#111240=CARTESIAN_POINT('Ctrl Pts',(-147.79021592804,-1.52770790569526,
126.127538484577));
#111241=CARTESIAN_POINT('Ctrl Pts',(-147.797706263802,-1.65238096265682,
126.17012961068));
#111242=CARTESIAN_POINT('Ctrl Pts',(-147.805196599564,-1.77496402368408,
126.217565900432));
#111243=CARTESIAN_POINT('Ctrl Pts',(-147.812971196084,-1.90219915304758,
126.266802413312));
#111244=CARTESIAN_POINT('Ctrl Pts',(-147.820745792604,-2.02758557772969,
126.321415075754));
#111245=CARTESIAN_POINT('Ctrl Pts',(-147.828520389124,-2.15063555386864,
126.381245224889));
#111246=CARTESIAN_POINT('Ctrl Pts',(-147.836285343862,-2.27353292775047,
126.441001174776));
#111247=CARTESIAN_POINT('Ctrl Pts',(-147.8440502986,-2.39409927029319,126.505961567184));
#111248=CARTESIAN_POINT('Ctrl Pts',(-147.851815253339,-2.51186443515346,
126.575918809771));
#111249=CARTESIAN_POINT('Ctrl Pts',(-147.859572435662,-2.62951172170435,
126.645806027903));
#111250=CARTESIAN_POINT('Ctrl Pts',(-147.867329617985,-2.74436307660795,
126.720679943931));
#111251=CARTESIAN_POINT('Ctrl Pts',(-147.875086800309,-2.85597102575763,
126.800286122438));
#111252=CARTESIAN_POINT('Ctrl Pts',(-147.883202294935,-2.97273426191766,
126.883569392955));
#111253=CARTESIAN_POINT('Ctrl Pts',(-147.891317789561,-3.08594690877269,
126.972032362944));
#111254=CARTESIAN_POINT('Ctrl Pts',(-147.899433284187,-3.19512775469468,
127.065331105289));
#111255=CARTESIAN_POINT('Ctrl Pts',(-147.907180842681,-3.29935861542577,
127.154399917109));
#111256=CARTESIAN_POINT('Ctrl Pts',(-147.914928401174,-3.39991488835662,
127.247875374623));
#111257=CARTESIAN_POINT('Ctrl Pts',(-147.922675959667,-3.49641013770257,
127.345415805709));
#111258=CARTESIAN_POINT('Ctrl Pts',(-147.93042189067,-3.59288511677337,
127.442935746965));
#111259=CARTESIAN_POINT('Ctrl Pts',(-147.938167821672,-3.68530049487148,
127.544518685051));
#111260=CARTESIAN_POINT('Ctrl Pts',(-147.945913752675,-3.77330612332224,
127.649785533312));
#111261=CARTESIAN_POINT('Ctrl Pts',(-147.953659733964,-3.86131232310902,
127.755053064968));
#111262=CARTESIAN_POINT('Ctrl Pts',(-147.961405715253,-3.94490846597896,
127.864004254169));
#111263=CARTESIAN_POINT('Ctrl Pts',(-147.969151696543,-4.02378445040055,
127.976226646338));
#111264=CARTESIAN_POINT('Ctrl Pts',(-147.976899405556,-4.1026780279326,
128.088474069458));
#111265=CARTESIAN_POINT('Ctrl Pts',(-147.984647114569,-4.17684912795344,
128.203993827306));
#111266=CARTESIAN_POINT('Ctrl Pts',(-147.992394823582,-4.24603099350536,
128.322344528841));
#111267=CARTESIAN_POINT('Ctrl Pts',(-148.000149654562,-4.3152764534664,
128.440804022512));
#111268=CARTESIAN_POINT('Ctrl Pts',(-148.007904485542,-4.37952332477647,
128.562099317812));
#111269=CARTESIAN_POINT('Ctrl Pts',(-148.015659316523,-4.43855068430019,
128.685764175249));
#111270=CARTESIAN_POINT('Ctrl Pts',(-148.02341832273,-4.49760982435684,
128.80949561427));
#111271=CARTESIAN_POINT('Ctrl Pts',(-148.031177328938,-4.55144370020625,
128.9355987984));
#111272=CARTESIAN_POINT('Ctrl Pts',(-148.038936335146,-4.59987993991676,
129.063588489787));
#111273=CARTESIAN_POINT('Ctrl Pts',(-148.046705067216,-4.64837689413137,
129.1917386154));
#111274=CARTESIAN_POINT('Ctrl Pts',(-148.054473799287,-4.69146258125346,
129.321779599376));
#111275=CARTESIAN_POINT('Ctrl Pts',(-148.062242531358,-4.72901466968156,
129.453211729976));
#111276=CARTESIAN_POINT('Ctrl Pts',(-148.064781244684,-4.74128616861459,
129.49616191778));
#111277=CARTESIAN_POINT('Ctrl Pts',(-148.06731995801,-4.75296714721703,
129.539260588997));
#111278=CARTESIAN_POINT('Ctrl Pts',(-148.069858671336,-4.76405452823417,
129.582490119309));
#111279=CARTESIAN_POINT('Origin',(213.235140564004,0.,130.804360617566));
#111280=CARTESIAN_POINT('',(-150.165071172634,-4.76405452823414,129.582490119309));
#111281=CARTESIAN_POINT('',(-149.820142046519,-4.76405452823404,129.582490119308));
#111282=CARTESIAN_POINT('',(213.235140564004,-4.76405452823405,129.582490119308));
#111283=CARTESIAN_POINT('',(-148.485140564067,-4.91824998862805,130.804695072583));
#111284=CARTESIAN_POINT('Ctrl Pts',(-148.485140564067,-4.91824998862805,
130.804695072582));
#111285=CARTESIAN_POINT('Ctrl Pts',(-148.493297690597,-4.91824013910216,
130.949534971136));
#111286=CARTESIAN_POINT('Ctrl Pts',(-148.501454817127,-4.911827811054,131.094237558735));
#111287=CARTESIAN_POINT('Ctrl Pts',(-148.509611943658,-4.89907498434783,
131.238235438496));
#111288=CARTESIAN_POINT('Ctrl Pts',(-148.517781359492,-4.88630294458163,
131.382450261526));
#111289=CARTESIAN_POINT('Ctrl Pts',(-148.525950775326,-4.86717136828516,
131.525957933976));
#111290=CARTESIAN_POINT('Ctrl Pts',(-148.53412019116,-4.84179358268159,
131.668199702815));
#111291=CARTESIAN_POINT('Ctrl Pts',(-148.542310382095,-4.81635126051228,
131.810803197275));
#111292=CARTESIAN_POINT('Ctrl Pts',(-148.550500573029,-4.78463102363235,
131.952134029516));
#111293=CARTESIAN_POINT('Ctrl Pts',(-148.558690763964,-4.74679697583506,
132.091645175348));
#111294=CARTESIAN_POINT('Ctrl Pts',(-148.566892118927,-4.70891135654272,
132.23134648847));
#111295=CARTESIAN_POINT('Ctrl Pts',(-148.57509347389,-4.66489539047846,
132.369222854717));
#111296=CARTESIAN_POINT('Ctrl Pts',(-148.583294828853,-4.6149619667238,
132.504745605794));
#111297=CARTESIAN_POINT('Ctrl Pts',(-148.591515191756,-4.56491281434578,
132.640582452326));
#111298=CARTESIAN_POINT('Ctrl Pts',(-148.599735554659,-4.50891890724185,
132.774054476094));
#111299=CARTESIAN_POINT('Ctrl Pts',(-148.607955917562,-4.44724062400924,
132.904654381462));
#111300=CARTESIAN_POINT('Ctrl Pts',(-148.612287436656,-4.41474076181952,
132.973470806045));
#111301=CARTESIAN_POINT('Ctrl Pts',(-148.61661895575,-4.38066338322728,
133.04149023043));
#111302=CARTESIAN_POINT('Ctrl Pts',(-148.620950474844,-4.3450514503867,
133.108641623865));
#111303=CARTESIAN_POINT('Ctrl Pts',(-148.628724808963,-4.28113413673123,
133.229166861735));
#111304=CARTESIAN_POINT('Ctrl Pts',(-148.636499143082,-4.21209699704326,
133.347221531257));
#111305=CARTESIAN_POINT('Ctrl Pts',(-148.644273477201,-4.13815516786773,
133.462340088734));
#111306=CARTESIAN_POINT('Ctrl Pts',(-148.652038230148,-4.06430446538848,
133.577316772877));
#111307=CARTESIAN_POINT('Ctrl Pts',(-148.659802983095,-3.98556130961877,
133.689364218908));
#111308=CARTESIAN_POINT('Ctrl Pts',(-148.667567736042,-3.90218734573117,
133.79804012301));
#111309=CARTESIAN_POINT('Ctrl Pts',(-148.675324776927,-3.81889619003987,
133.906608088672));
#111310=CARTESIAN_POINT('Ctrl Pts',(-148.683081817812,-3.73098361564808,
134.011810868207));
#111311=CARTESIAN_POINT('Ctrl Pts',(-148.690838858697,-3.6387551080156,
134.113234191215));
#111312=CARTESIAN_POINT('Ctrl Pts',(-148.698590049937,-3.5465961506183,
134.214581030106));
#111313=CARTESIAN_POINT('Ctrl Pts',(-148.706341241177,-3.45012800018831,
134.312153797371));
#111314=CARTESIAN_POINT('Ctrl Pts',(-148.714092432417,-3.34969681426941,
134.405570735703));
#111315=CARTESIAN_POINT('Ctrl Pts',(-148.721840329194,-3.24930831428347,
134.498947969344));
#111316=CARTESIAN_POINT('Ctrl Pts',(-148.729588225971,-3.14496041461418,
134.588172621444));
#111317=CARTESIAN_POINT('Ctrl Pts',(-148.737336122748,-3.03703641899676,
134.672899469922));
#111318=CARTESIAN_POINT('Ctrl Pts',(-148.745082398832,-2.92913499875266,
134.757608595369));
#111319=CARTESIAN_POINT('Ctrl Pts',(-148.752828674916,-2.81765927778328,
134.837821547315));
#111320=CARTESIAN_POINT('Ctrl Pts',(-148.760574951,-2.70302564545779,134.91323338543));
#111321=CARTESIAN_POINT('Ctrl Pts',(-148.768321284265,-2.58839116693302,
134.988645780219));
#111322=CARTESIAN_POINT('Ctrl Pts',(-148.77606761753,-2.47059905716237,
135.059256775587));
#111323=CARTESIAN_POINT('Ctrl Pts',(-148.783813950796,-2.35009434701988,
135.124804995475));
#111324=CARTESIAN_POINT('Ctrl Pts',(-148.791562018799,-2.22956265068292,
135.190367894432));
#111325=CARTESIAN_POINT('Ctrl Pts',(-148.799310086801,-2.1063174885613,
135.25086557505));
#111326=CARTESIAN_POINT('Ctrl Pts',(-148.807058154804,-1.98082775806655,
135.306083005205));
#111327=CARTESIAN_POINT('Ctrl Pts',(-148.814814457546,-1.85520465559305,
135.361359121102));
#111328=CARTESIAN_POINT('Ctrl Pts',(-148.822570760288,-1.72733257777028,
135.411343618422));
#111329=CARTESIAN_POINT('Ctrl Pts',(-148.83032706303,-1.59770015560841,
135.455869757111));
#111330=CARTESIAN_POINT('Ctrl Pts',(-148.838087505544,-1.46799854471932,
135.500419660741));
#111331=CARTESIAN_POINT('Ctrl Pts',(-148.845847948058,-1.33653509193017,
135.539505289398));
#111332=CARTESIAN_POINT('Ctrl Pts',(-148.853608390572,-1.2038118292568,
135.573010336537));
#111333=CARTESIAN_POINT('Ctrl Pts',(-148.861381290837,-1.07087550741994,
135.606569168952));
#111334=CARTESIAN_POINT('Ctrl Pts',(-148.869154191103,-0.936675717348273,
135.634529438231));
#111335=CARTESIAN_POINT('Ctrl Pts',(-148.876927091368,-0.801723769290029,
135.656826182643));
#111336=CARTESIAN_POINT('Ctrl Pts',(-148.884417427131,-0.67167766445254,
135.678312384235));
#111337=CARTESIAN_POINT('Ctrl Pts',(-148.891907762893,-0.540933443552698,
135.694539640934));
#111338=CARTESIAN_POINT('Ctrl Pts',(-148.899398098656,-0.409949571488562,
135.705495630125));
#111339=CARTESIAN_POINT('Ctrl Pts',(-148.907172432775,-0.273999406117406,
135.716867018976));
#111340=CARTESIAN_POINT('Ctrl Pts',(-148.914946766894,-0.137360408838824,
135.722595550645));
#111341=CARTESIAN_POINT('Ctrl Pts',(-148.922721101013,-0.000540541306493031,
135.722610587862));
#111342=CARTESIAN_POINT('Ctrl Pts',(-148.93048585396,0.136110707967047,
135.722625606546));
#111343=CARTESIAN_POINT('Ctrl Pts',(-148.938250606908,0.272941996765018,
135.716941140966));
#111344=CARTESIAN_POINT('Ctrl Pts',(-148.946015359855,0.409439776752363,
135.705538244597));
#111345=CARTESIAN_POINT('Ctrl Pts',(-148.95377240074,0.545801985220342,
135.694146673746));
#111346=CARTESIAN_POINT('Ctrl Pts',(-148.961529441625,0.681830956984554,
135.677048007156));
#111347=CARTESIAN_POINT('Ctrl Pts',(-148.96928648251,0.817013032271916,
135.654275335125));
#111348=CARTESIAN_POINT('Ctrl Pts',(-148.97703767375,0.952093165704557,
135.631519836144));
#111349=CARTESIAN_POINT('Ctrl Pts',(-148.98478886499,1.08632728988379,135.603098913121));
#111350=CARTESIAN_POINT('Ctrl Pts',(-148.99254005623,1.21920711496585,135.569097449052));
#111351=CARTESIAN_POINT('Ctrl Pts',(-149.000287953007,1.35203046257774,
135.535110436512));
#111352=CARTESIAN_POINT('Ctrl Pts',(-149.008035849784,1.48350027797426,
135.495547697126));
#111353=CARTESIAN_POINT('Ctrl Pts',(-149.015783746561,1.61311893100992,
135.450545114217));
#111354=CARTESIAN_POINT('Ctrl Pts',(-149.023530022645,1.74271047061762,
135.405551944877));
#111355=CARTESIAN_POINT('Ctrl Pts',(-149.031276298729,1.87045124896878,
135.355121323505));
#111356=CARTESIAN_POINT('Ctrl Pts',(-149.039022574814,1.99585964250455,
135.299438742574));
#111357=CARTESIAN_POINT('Ctrl Pts',(-149.046768908079,2.12126896177642,
135.243755750606));
#111358=CARTESIAN_POINT('Ctrl Pts',(-149.054515241344,2.24434550455125,
135.182820880375));
#111359=CARTESIAN_POINT('Ctrl Pts',(-149.06226157461,2.36462881768856,135.116867268814));
#111360=CARTESIAN_POINT('Ctrl Pts',(-149.070009642613,2.4849390674397,135.050898887399));
#111361=CARTESIAN_POINT('Ctrl Pts',(-149.077757710616,2.60245450008479,
134.979909716133));
#111362=CARTESIAN_POINT('Ctrl Pts',(-149.085505778619,2.71674075250271,
134.904178021572));
#111363=CARTESIAN_POINT('Ctrl Pts',(-149.09326208136,2.83114846970988,134.828365838465));
#111364=CARTESIAN_POINT('Ctrl Pts',(-149.101018384102,2.94231982445245,
134.747801279607));
#111365=CARTESIAN_POINT('Ctrl Pts',(-149.108774686844,3.04985041660397,
134.662805317032));
#111366=CARTESIAN_POINT('Ctrl Pts',(-149.116535129358,3.1574384010705,134.577763989553));
#111367=CARTESIAN_POINT('Ctrl Pts',(-149.124295571873,3.26138145482849,
134.488286800491));
#111368=CARTESIAN_POINT('Ctrl Pts',(-149.132056014387,3.36131036531989,
134.394733257069));
#111369=CARTESIAN_POINT('Ctrl Pts',(-149.139828914652,3.4613996905694,134.301029533195));
#111370=CARTESIAN_POINT('Ctrl Pts',(-149.147601814918,3.55746172153592,
134.203236657583));
#111371=CARTESIAN_POINT('Ctrl Pts',(-149.155374715183,3.64916542839605,
134.101749696625));
#111372=CARTESIAN_POINT('Ctrl Pts',(-149.162865050945,3.73753547452559,
134.003952042327));
#111373=CARTESIAN_POINT('Ctrl Pts',(-149.170355386707,3.82185837015966,
133.902724455042));
#111374=CARTESIAN_POINT('Ctrl Pts',(-149.177845722469,3.901875936459,133.7984459936));
#111375=CARTESIAN_POINT('Ctrl Pts',(-149.185620056589,3.98492739310433,
133.6902137826));
#111376=CARTESIAN_POINT('Ctrl Pts',(-149.193394390708,4.0636036846603,133.578351935666));
#111377=CARTESIAN_POINT('Ctrl Pts',(-149.201168724827,4.13757081630893,
133.463249634153));
#111378=CARTESIAN_POINT('Ctrl Pts',(-149.208933477774,4.21144679007823,
133.348289185941));
#111379=CARTESIAN_POINT('Ctrl Pts',(-149.216698230721,4.28062494207831,
133.230096554915));
#111380=CARTESIAN_POINT('Ctrl Pts',(-149.224462983668,4.34481174664333,
133.109093562775));
#111381=CARTESIAN_POINT('Ctrl Pts',(-149.232220024553,4.40893479996935,
132.988210752512));
#111382=CARTESIAN_POINT('Ctrl Pts',(-149.239977065438,4.46807618943849,
132.864523479076));
#111383=CARTESIAN_POINT('Ctrl Pts',(-149.247734106323,4.5219861092022,132.738481785095));
#111384=CARTESIAN_POINT('Ctrl Pts',(-149.255485297563,4.57585537507598,
132.612535140136));
#111385=CARTESIAN_POINT('Ctrl Pts',(-149.263236488803,4.62450087058421,
132.484237966642));
#111386=CARTESIAN_POINT('Ctrl Pts',(-149.270987680043,4.66771926711822,
132.354063784587));
#111387=CARTESIAN_POINT('Ctrl Pts',(-149.278735576821,4.71091929468086,
132.223944930031));
#111388=CARTESIAN_POINT('Ctrl Pts',(-149.286483473598,4.74869668811154,
132.091951023907));
#111389=CARTESIAN_POINT('Ctrl Pts',(-149.294231370375,4.78089678864764,
131.958574184805));
#111390=CARTESIAN_POINT('Ctrl Pts',(-149.301977646459,4.81309015361685,
131.825225245262));
#111391=CARTESIAN_POINT('Ctrl Pts',(-149.309723922543,4.83970845452769,
131.69049432794));
#111392=CARTESIAN_POINT('Ctrl Pts',(-149.317470198627,4.8606474221536,131.554886899592));
#111393=CARTESIAN_POINT('Ctrl Pts',(-149.325216531893,4.88158654434618,
131.41927847022));
#111394=CARTESIAN_POINT('Ctrl Pts',(-149.332962865158,4.89684618993705,
131.282793903298));
#111395=CARTESIAN_POINT('Ctrl Pts',(-149.340709198423,4.90637361746105,
131.145946607299));
#111396=CARTESIAN_POINT('Ctrl Pts',(-149.348457266426,4.91590317858639,
131.009068665298));
#111397=CARTESIAN_POINT('Ctrl Pts',(-149.356205334429,4.91969794010098,
130.871828222526));
#111398=CARTESIAN_POINT('Ctrl Pts',(-149.363953402432,4.91775723166259,
130.734741130852));
#111399=CARTESIAN_POINT('Ctrl Pts',(-149.371709705174,4.91581446061618,
130.597508341386));
#111400=CARTESIAN_POINT('Ctrl Pts',(-149.379466007916,4.90812404829113,
130.460429620142));
#111401=CARTESIAN_POINT('Ctrl Pts',(-149.387222310658,4.8947374494049,130.324018693627));
#111402=CARTESIAN_POINT('Ctrl Pts',(-149.394982753172,4.88134370568778,
130.187534960493));
#111403=CARTESIAN_POINT('Ctrl Pts',(-149.402743195686,4.86224777190991,
130.051720119256));
#111404=CARTESIAN_POINT('Ctrl Pts',(-149.4105036382,4.83755254327486,129.917079121334));
#111405=CARTESIAN_POINT('Ctrl Pts',(-149.418276538466,4.81281767166647,
129.78222198573));
#111406=CARTESIAN_POINT('Ctrl Pts',(-149.426049438731,4.78246562995908,
129.648542840468));
#111407=CARTESIAN_POINT('Ctrl Pts',(-149.433822338997,4.74664986899012,
129.516533733347));
#111408=CARTESIAN_POINT('Ctrl Pts',(-149.441312674759,4.71213610114734,
129.389323489784));
#111409=CARTESIAN_POINT('Ctrl Pts',(-149.44880301052,4.67254904984274,129.263664265993));
#111410=CARTESIAN_POINT('Ctrl Pts',(-149.456293346282,4.62806807603627,
129.139978165702));
#111411=CARTESIAN_POINT('Ctrl Pts',(-149.464067680402,4.58190059258752,
129.011602469322));
#111412=CARTESIAN_POINT('Ctrl Pts',(-149.471842014521,4.53031451003106,
128.884945816362));
#111413=CARTESIAN_POINT('Ctrl Pts',(-149.47961634864,4.47345672530577,128.760499568151));
#111414=CARTESIAN_POINT('Ctrl Pts',(-149.487381101587,4.41666901271879,
128.636206688818));
#111415=CARTESIAN_POINT('Ctrl Pts',(-149.495145854534,4.3546226857735,128.514119146229));
#111416=CARTESIAN_POINT('Ctrl Pts',(-149.502910607481,4.28751397722068,
128.394711896769));
#111417=CARTESIAN_POINT('Ctrl Pts',(-149.510667648366,4.22047192198326,
128.275423244273));
#111418=CARTESIAN_POINT('Ctrl Pts',(-149.518424689251,4.14837768145254,
128.15880992582));
#111419=CARTESIAN_POINT('Ctrl Pts',(-149.526181730136,4.07147486307564,
128.045325369179));
#111420=CARTESIAN_POINT('Ctrl Pts',(-149.533932921376,3.99463003771219,
127.931926392124));
#111421=CARTESIAN_POINT('Ctrl Pts',(-149.541684112616,3.91298407064164,
127.821651802935));
#111422=CARTESIAN_POINT('Ctrl Pts',(-149.549435303856,3.82682544354861,
127.71492861684));
#111423=CARTESIAN_POINT('Ctrl Pts',(-149.557183200633,3.74070343617058,
127.608250790946));
#111424=CARTESIAN_POINT('Ctrl Pts',(-149.56493109741,3.65007282860089,127.505121669552));
#111425=CARTESIAN_POINT('Ctrl Pts',(-149.572678994188,3.55526405730715,
127.405937373572));
#111426=CARTESIAN_POINT('Ctrl Pts',(-149.580425270272,3.46047511796452,
127.306773824808));
#111427=CARTESIAN_POINT('Ctrl Pts',(-149.588171546356,3.36151002327435,
127.211553742584));
#111428=CARTESIAN_POINT('Ctrl Pts',(-149.59591782244,3.25873767666774,127.120638068681));
#111429=CARTESIAN_POINT('Ctrl Pts',(-149.603664155705,3.15596457141888,
127.029721723658));
#111430=CARTESIAN_POINT('Ctrl Pts',(-149.611410488971,3.04938445100277,
126.943110109404));
#111431=CARTESIAN_POINT('Ctrl Pts',(-149.619156822236,2.93940075245949,
126.861125108629));
#111432=CARTESIAN_POINT('Ctrl Pts',(-149.626904890239,2.82939242382964,
126.779121747882));
#111433=CARTESIAN_POINT('Ctrl Pts',(-149.634652958242,2.71597931376613,
126.701747295944));
#111434=CARTESIAN_POINT('Ctrl Pts',(-149.642401026245,2.59959506071738,
126.629281147329));
#111435=CARTESIAN_POINT('Ctrl Pts',(-149.650157328987,2.48308711309935,
126.556737980829));
#111436=CARTESIAN_POINT('Ctrl Pts',(-149.657913631729,2.36360204693584,
126.489113745355));
#111437=CARTESIAN_POINT('Ctrl Pts',(-149.66566993447,2.24159988741659,126.426642832323));
#111438=CARTESIAN_POINT('Ctrl Pts',(-149.673430376985,2.11953261167139,
126.364138576683));
#111439=CARTESIAN_POINT('Ctrl Pts',(-149.681190819499,1.99494592061158,
126.306793287445));
#111440=CARTESIAN_POINT('Ctrl Pts',(-149.688951262013,1.868320261537,126.254793334535));
#111441=CARTESIAN_POINT('Ctrl Pts',(-149.696724162278,1.74149133171317,
126.202709906684));
#111442=CARTESIAN_POINT('Ctrl Pts',(-149.704497062544,1.61261726088133,
126.155989095678));
#111443=CARTESIAN_POINT('Ctrl Pts',(-149.712269962809,1.48219496671664,
126.114767762835));
#111444=CARTESIAN_POINT('Ctrl Pts',(-149.719760298571,1.35651385145912,
126.075044929273));
#111445=CARTESIAN_POINT('Ctrl Pts',(-149.727250634333,1.22939541943093,
126.040428756842));
#111446=CARTESIAN_POINT('Ctrl Pts',(-149.734740970095,1.10129174743127,
126.010996501463));
#111447=CARTESIAN_POINT('Ctrl Pts',(-149.742515304215,0.968330985770924,
125.980448313176));
#111448=CARTESIAN_POINT('Ctrl Pts',(-149.750289638334,0.833887618851214,
125.955388130739));
#111449=CARTESIAN_POINT('Ctrl Pts',(-149.758063972453,0.69845444425737,
125.935957958398));
#111450=CARTESIAN_POINT('Ctrl Pts',(-149.7658287254,0.56318817894757,125.916551732007));
#111451=CARTESIAN_POINT('Ctrl Pts',(-149.773593478347,0.42693491638807,
125.902761765186));
#111452=CARTESIAN_POINT('Ctrl Pts',(-149.781358231294,0.290200319434784,
125.894679687292));
#111453=CARTESIAN_POINT('Ctrl Pts',(-149.789115272179,0.15360152921044,
125.886605636631));
#111454=CARTESIAN_POINT('Ctrl Pts',(-149.796872313064,0.0165227437279239,
125.884228215942));
#111455=CARTESIAN_POINT('Ctrl Pts',(-149.804629353949,-0.120522879613008,
125.887587560164));
#111456=CARTESIAN_POINT('Ctrl Pts',(-149.812380545189,-0.257465155783134,
125.890944371079));
#111457=CARTESIAN_POINT('Ctrl Pts',(-149.820131736429,-0.394373930321906,
125.900029326446));
#111458=CARTESIAN_POINT('Ctrl Pts',(-149.827882927669,-0.530734011826448,
125.914830530616));
#111459=CARTESIAN_POINT('Ctrl Pts',(-149.835630824446,-0.667036136659012,
125.929625443879));
#111460=CARTESIAN_POINT('Ctrl Pts',(-149.843378721224,-0.802789644424176,
125.950131731637));
#111461=CARTESIAN_POINT('Ctrl Pts',(-149.851126618001,-0.937482658395131,
125.976285501362));
#111462=CARTESIAN_POINT('Ctrl Pts',(-149.858872894085,-1.07214749749121,
126.002433800282));
#111463=CARTESIAN_POINT('Ctrl Pts',(-149.866619170169,-1.20575190047616,
126.034227156961));
#111464=CARTESIAN_POINT('Ctrl Pts',(-149.874365446253,-1.33779279549247,
126.071550300341));
#111465=CARTESIAN_POINT('Ctrl Pts',(-149.882111779518,-1.46983466520449,
126.108873719233));
#111466=CARTESIAN_POINT('Ctrl Pts',(-149.889858112784,-1.60031262769362,
126.151726899934));
#111467=CARTESIAN_POINT('Ctrl Pts',(-149.897604446049,-1.7287378063454,
126.199944404905));
#111468=CARTESIAN_POINT('Ctrl Pts',(-149.905352514052,-1.85719174492533,
126.248172707852));
#111469=CARTESIAN_POINT('Ctrl Pts',(-149.913100582055,-1.98359161895713,
126.301767588127));
#111470=CARTESIAN_POINT('Ctrl Pts',(-149.920848650058,-2.10746797375143,
126.360515232979));
#111471=CARTESIAN_POINT('Ctrl Pts',(-149.9286049528,-2.23147598580992,126.419325315528));
#111472=CARTESIAN_POINT('Ctrl Pts',(-149.936361255542,-2.35295476717775,
126.483298934598));
#111473=CARTESIAN_POINT('Ctrl Pts',(-149.944117558284,-2.47145846286881,
126.552175752251));
#111474=CARTESIAN_POINT('Ctrl Pts',(-149.951878000798,-2.59002540755066,
126.621089331536));
#111475=CARTESIAN_POINT('Ctrl Pts',(-149.959638443312,-2.70561377320711,
126.694911113634));
#111476=CARTESIAN_POINT('Ctrl Pts',(-149.967398885826,-2.81780706803946,
126.773337622121));
#111477=CARTESIAN_POINT('Ctrl Pts',(-149.975171786092,-2.93018046550842,
126.851890027802));
#111478=CARTESIAN_POINT('Ctrl Pts',(-149.982944686357,-3.03914759021873,
126.935061693928));
#111479=CARTESIAN_POINT('Ctrl Pts',(-149.990717586623,-3.1443247007252,
127.022508526472));
#111480=CARTESIAN_POINT('Ctrl Pts',(-149.998207922385,-3.24567835833818,
127.106776446387));
#111481=CARTESIAN_POINT('Ctrl Pts',(-150.005698258146,-3.34351254213525,
127.195013896687));
#111482=CARTESIAN_POINT('Ctrl Pts',(-150.013188593908,-3.43751789597122,
127.286882291069));
#111483=CARTESIAN_POINT('Ctrl Pts',(-150.02085013133,-3.53367186812148,
127.380850460693));
#111484=CARTESIAN_POINT('Ctrl Pts',(-150.028511668752,-3.62614329675247,
127.478933995053));
#111485=CARTESIAN_POINT('Ctrl Pts',(-150.036173206173,-3.71455151127092,
127.580808208714));
#111486=CARTESIAN_POINT('Ctrl Pts',(-150.043825811081,-3.80285665148715,
127.682563648192));
#111487=CARTESIAN_POINT('Ctrl Pts',(-150.051478415988,-3.88710773373148,
127.788100680055));
#111488=CARTESIAN_POINT('Ctrl Pts',(-150.059131020896,-3.96695892539313,
127.897056033119));
#111489=CARTESIAN_POINT('Ctrl Pts',(-150.066776475311,-4.04673550516101,
128.005909579748));
#111490=CARTESIAN_POINT('Ctrl Pts',(-150.074421929726,-4.12212013268671,
128.118174773394));
#111491=CARTESIAN_POINT('Ctrl Pts',(-150.082067384141,-4.19280585805743,
128.233453754387));
#111492=CARTESIAN_POINT('Ctrl Pts',(-150.089707243863,-4.26343985792733,
128.348648377994));
#111493=CARTESIAN_POINT('Ctrl Pts',(-150.097347103585,-4.32938158696644,
128.46685205875));
#111494=CARTESIAN_POINT('Ctrl Pts',(-150.104986963306,-4.39036657259015,
128.587636814116));
#111495=CARTESIAN_POINT('Ctrl Pts',(-150.112623519553,-4.45132518831032,
128.708369342161));
#111496=CARTESIAN_POINT('Ctrl Pts',(-150.1202600758,-4.50733114304092,128.83168036537));
#111497=CARTESIAN_POINT('Ctrl Pts',(-150.127896632047,-4.55816544276777,
128.957116492157));
#111498=CARTESIAN_POINT('Ctrl Pts',(-150.135532825893,-4.60899733009657,
129.082546666234));
#111499=CARTESIAN_POINT('Ctrl Pts',(-150.143169019738,-4.65465789211696,
129.210101372672));
#111500=CARTESIAN_POINT('Ctrl Pts',(-150.150805213584,-4.69497604676473,
129.339306699512));
#111501=CARTESIAN_POINT('Ctrl Pts',(-150.155560533267,-4.72008354380697,
129.419767285812));
#111502=CARTESIAN_POINT('Ctrl Pts',(-150.160315852951,-4.74312022574812,
129.500867591638));
#111503=CARTESIAN_POINT('Ctrl Pts',(-150.165071172634,-4.76405452823413,
129.582490119309));
#111504=CARTESIAN_POINT('Ctrl Pts',(-148.415413529701,-4.76405452823396,
129.582490119308));
#111505=CARTESIAN_POINT('Ctrl Pts',(-148.423504095412,-4.79956581021559,
129.720948068795));
#111506=CARTESIAN_POINT('Ctrl Pts',(-148.431594661122,-4.82907237912164,
129.861093556804));
#111507=CARTESIAN_POINT('Ctrl Pts',(-148.439685226832,-4.85242460871388,
130.002388997589));
#111508=CARTESIAN_POINT('Ctrl Pts',(-148.447762663752,-4.87573894397912,
130.143455154245));
#111509=CARTESIAN_POINT('Ctrl Pts',(-148.455840100671,-4.89291879809602,
130.285667209157));
#111510=CARTESIAN_POINT('Ctrl Pts',(-148.46391753759,-4.90386518617971,
130.428475930096));
#111511=CARTESIAN_POINT('Ctrl Pts',(-148.47099187973,-4.91345219939669,
130.55354998052));
#111512=CARTESIAN_POINT('Ctrl Pts',(-148.478066221871,-4.91825853069369,
130.679081352824));
#111513=CARTESIAN_POINT('Ctrl Pts',(-148.485140564011,-4.91824998862812,
130.804695071591));
#111514=CARTESIAN_POINT('',(-148.139859436045,-4.9182480226444,130.7999503733));
#111515=CARTESIAN_POINT('Ctrl Pts',(-148.069858671336,-4.76405452823417,
129.582490119309));
#111516=CARTESIAN_POINT('Ctrl Pts',(-148.074453855349,-4.78412318091859,
129.660737491541));
#111517=CARTESIAN_POINT('Ctrl Pts',(-148.079049039363,-4.80224668583714,
129.739413610789));
#111518=CARTESIAN_POINT('Ctrl Pts',(-148.083644223377,-4.81841171100897,
129.818413536982));
#111519=CARTESIAN_POINT('Ctrl Pts',(-148.094752159043,-4.85748741703195,
130.009380012998));
#111520=CARTESIAN_POINT('Ctrl Pts',(-148.105860094709,-4.88522080271822,
130.202739816459));
#111521=CARTESIAN_POINT('Ctrl Pts',(-148.116968030375,-4.90138261484219,
130.397382085672));
#111522=CARTESIAN_POINT('Ctrl Pts',(-148.124598498914,-4.91248478563783,
130.531089351929));
#111523=CARTESIAN_POINT('Ctrl Pts',(-148.132228967454,-4.91812737123165,
130.665401488351));
#111524=CARTESIAN_POINT('Ctrl Pts',(-148.139859435993,-4.91824802264357,
130.79995037238));
#111525=CARTESIAN_POINT('Ctrl Pts',(-148.139859436045,-4.9182480226444,
130.799950373301));
#111526=CARTESIAN_POINT('Ctrl Pts',(-148.147507635122,-4.91836895438269,
130.934811901826));
#111527=CARTESIAN_POINT('Ctrl Pts',(-148.155155834198,-4.91293873375263,
131.069852929669));
#111528=CARTESIAN_POINT('Ctrl Pts',(-148.162804033275,-4.90193984041586,
131.204571641207));
#111529=CARTESIAN_POINT('Ctrl Pts',(-148.170445879266,-4.89095008346705,
131.339178446721));
#111530=CARTESIAN_POINT('Ctrl Pts',(-148.178087725256,-4.87440088783354,
131.473463068676));
#111531=CARTESIAN_POINT('Ctrl Pts',(-148.185729571247,-4.85232679620336,
131.606923839591));
#111532=CARTESIAN_POINT('Ctrl Pts',(-148.193367541118,-4.83026390105813,
131.740316916145));
#111533=CARTESIAN_POINT('Ctrl Pts',(-148.20100551099,-4.80268174754368,
131.872886575743));
#111534=CARTESIAN_POINT('Ctrl Pts',(-148.208643480861,-4.76966666205955,
132.004136844759));
#111535=CARTESIAN_POINT('Ctrl Pts',(-148.216279549579,-4.73665979430195,
132.135354444503));
#111536=CARTESIAN_POINT('Ctrl Pts',(-148.223915618296,-4.69822278116591,
132.265252915777));
#111537=CARTESIAN_POINT('Ctrl Pts',(-148.231551687014,-4.65449283594518,
132.393347559814));
#111538=CARTESIAN_POINT('Ctrl Pts',(-148.239187619417,-4.61076367136765,
132.521439917175));
#111539=CARTESIAN_POINT('Ctrl Pts',(-148.24682355182,-4.56174189304386,
132.647728129766));
#111540=CARTESIAN_POINT('Ctrl Pts',(-148.254459484222,-4.50761407650963,
132.771744260822));
#111541=CARTESIAN_POINT('Ctrl Pts',(-148.262097044832,-4.45347471832187,
132.895786835791));
#111542=CARTESIAN_POINT('Ctrl Pts',(-148.269734605442,-4.39422731869069,
133.017555996583));
#111543=CARTESIAN_POINT('Ctrl Pts',(-148.277372166051,-4.33010568450893,
133.136605849844));
#111544=CARTESIAN_POINT('Ctrl Pts',(-148.285017568631,-4.26591821256074,
133.255777939173));
#111545=CARTESIAN_POINT('Ctrl Pts',(-148.292662971211,-4.19684670479271,
133.372224790697));
#111546=CARTESIAN_POINT('Ctrl Pts',(-148.300308373791,-4.12316998861898,
133.485526839092));
#111547=CARTESIAN_POINT('Ctrl Pts',(-148.307957985488,-4.04945271029629,
133.598891265058));
#111548=CARTESIAN_POINT('Ctrl Pts',(-148.315607597185,-3.97112540938517,
133.709107113066));
#111549=CARTESIAN_POINT('Ctrl Pts',(-148.323257208882,-3.88850815360802,
133.815786758421));
#111550=CARTESIAN_POINT('Ctrl Pts',(-148.330918363464,-3.80576623248856,
133.922627378071));
#111551=CARTESIAN_POINT('Ctrl Pts',(-148.338579518046,-3.71872168967319,
134.025920832434));
#111552=CARTESIAN_POINT('Ctrl Pts',(-148.346240672628,-3.62773282847055,
134.125314936393));
#111553=CARTESIAN_POINT('Ctrl Pts',(-148.351524397482,-3.56497987103348,
134.193864799451));
#111554=CARTESIAN_POINT('Ctrl Pts',(-148.356808122337,-3.50035154979511,
134.260560695635));
#111555=CARTESIAN_POINT('Ctrl Pts',(-148.362091847191,-3.43397442841546,
134.325298374398));
#111556=CARTESIAN_POINT('Ctrl Pts',(-148.36986618131,-3.3363088735842,134.42055169638));
#111557=CARTESIAN_POINT('Ctrl Pts',(-148.377640515429,-3.23452234261106,
134.511889168235));
#111558=CARTESIAN_POINT('Ctrl Pts',(-148.385414849548,-3.12896184513419,
134.598933167168));
#111559=CARTESIAN_POINT('Ctrl Pts',(-148.393179602495,-3.02353144153626,
134.685869892152));
#111560=CARTESIAN_POINT('Ctrl Pts',(-148.400944355442,-2.91433662443569,
134.768523426024));
#111561=CARTESIAN_POINT('Ctrl Pts',(-148.408709108389,-2.80176159511557,
134.846552476773));
#111562=CARTESIAN_POINT('Ctrl Pts',(-148.416466149274,-2.6892983769016,
134.924504027968));
#111563=CARTESIAN_POINT('Ctrl Pts',(-148.424223190159,-2.57346194684135,
134.997840015242));
#111564=CARTESIAN_POINT('Ctrl Pts',(-148.431980231044,-2.45466969331219,
135.066259227251));
#111565=CARTESIAN_POINT('Ctrl Pts',(-148.439731422285,-2.33596702194565,
135.1346268438));
#111566=CARTESIAN_POINT('Ctrl Pts',(-148.447482613525,-2.2143133012376,
135.198084870854));
#111567=CARTESIAN_POINT('Ctrl Pts',(-148.455233804765,-2.09015472195155,
135.256375476122));
#111568=CARTESIAN_POINT('Ctrl Pts',(-148.462981701542,-1.96604891337324,
135.314641306328));
#111569=CARTESIAN_POINT('Ctrl Pts',(-148.470729598319,-1.83944071685019,
135.3677439172));
#111570=CARTESIAN_POINT('Ctrl Pts',(-148.478477495096,-1.71080053991821,
135.415471608977));
#111571=CARTESIAN_POINT('Ctrl Pts',(-148.48622377118,-1.58218727173843,
135.463189317151));
#111572=CARTESIAN_POINT('Ctrl Pts',(-148.493970047264,-1.45154323490816,
135.505534206648));
#111573=CARTESIAN_POINT('Ctrl Pts',(-148.501716323348,-1.31935804314362,
135.542343038016));
#111574=CARTESIAN_POINT('Ctrl Pts',(-148.509462656614,-1.18717187561784,
135.579152141098));
#111575=CARTESIAN_POINT('Ctrl Pts',(-148.517208989879,-1.05344490709213,
135.610424999627));
#111576=CARTESIAN_POINT('Ctrl Pts',(-148.524955323144,-0.918680723296531,
135.636048603265));
#111577=CARTESIAN_POINT('Ctrl Pts',(-148.532703391147,-0.783886359996543,
135.66167794513));
#111578=CARTESIAN_POINT('Ctrl Pts',(-148.54045145915,-0.648054703232639,
135.681655441664));
#111579=CARTESIAN_POINT('Ctrl Pts',(-148.548199527153,-0.51169791507903,
135.695919500602));
#111580=CARTESIAN_POINT('Ctrl Pts',(-148.555955829895,-0.37519620530812,
135.710198719551));
#111581=CARTESIAN_POINT('Ctrl Pts',(-148.563712132637,-0.23816863871437,
135.718752330071));
#111582=CARTESIAN_POINT('Ctrl Pts',(-148.571468435379,-0.101131423311902,
135.72157075114));
#111583=CARTESIAN_POINT('Ctrl Pts',(-148.579228877893,0.035978932978537,
135.724390676485));
#111584=CARTESIAN_POINT('Ctrl Pts',(-148.586989320407,0.173098557653976,
135.721469321314));
#111585=CARTESIAN_POINT('Ctrl Pts',(-148.594749762921,0.309713880796437,
135.712849221458));
#111586=CARTESIAN_POINT('Ctrl Pts',(-148.602522663187,0.446548510983743,
135.704215283853));
#111587=CARTESIAN_POINT('Ctrl Pts',(-148.610295563452,0.582876832859398,
135.689864361635));
#111588=CARTESIAN_POINT('Ctrl Pts',(-148.618068463718,0.718192118744943,
135.669890716442));
#111589=CARTESIAN_POINT('Ctrl Pts',(-148.62555879948,0.848588353145884,
135.650643163564));
#111590=CARTESIAN_POINT('Ctrl Pts',(-148.633049135241,0.978043622995952,
135.62617464783));
#111591=CARTESIAN_POINT('Ctrl Pts',(-148.640539471003,1.10611759491657,
135.596613420655));
#111592=CARTESIAN_POINT('Ctrl Pts',(-148.648313805122,1.23904753041373,
135.565931370566));
#111593=CARTESIAN_POINT('Ctrl Pts',(-148.656088139241,1.37091043856259,
135.529665613894));
#111594=CARTESIAN_POINT('Ctrl Pts',(-148.663862473361,1.50120104742373,
135.487903985329));
#111595=CARTESIAN_POINT('Ctrl Pts',(-148.671627226308,1.63133108475315,
135.446193824239));
#111596=CARTESIAN_POINT('Ctrl Pts',(-148.679391979255,1.75989230954324,
135.399001386037));
#111597=CARTESIAN_POINT('Ctrl Pts',(-148.687156732202,1.88638991298052,
135.346465433475));
#111598=CARTESIAN_POINT('Ctrl Pts',(-148.694913773087,2.0127618772151,135.293981660362));
#111599=CARTESIAN_POINT('Ctrl Pts',(-148.702670813972,2.13707394020085,
135.236165083547));
#111600=CARTESIAN_POINT('Ctrl Pts',(-148.710427854857,2.2588470756914,135.173204051604));
#111601=CARTESIAN_POINT('Ctrl Pts',(-148.718179046097,2.38052838111338,
135.110290499066));
#111602=CARTESIAN_POINT('Ctrl Pts',(-148.725930237337,2.49967422409891,
135.042240392093));
#111603=CARTESIAN_POINT('Ctrl Pts',(-148.733681428577,2.61582650603231,
134.969289758961));
#111604=CARTESIAN_POINT('Ctrl Pts',(-148.741429325354,2.73192942014727,
134.896370131793));
#111605=CARTESIAN_POINT('Ctrl Pts',(-148.749177222131,2.84504097341543,
134.818554328608));
#111606=CARTESIAN_POINT('Ctrl Pts',(-148.756925118908,2.95472879006864,
134.736123687696));
#111607=CARTESIAN_POINT('Ctrl Pts',(-148.764671394993,3.0643936623952,134.653710289497));
#111608=CARTESIAN_POINT('Ctrl Pts',(-148.772417671077,3.17063591026333,
134.566684208386));
#111609=CARTESIAN_POINT('Ctrl Pts',(-148.780163947161,3.27305354752491,
134.475369135335));
#111610=CARTESIAN_POINT('Ctrl Pts',(-148.787910280426,3.37547194081008,
134.384053388218));
#111611=CARTESIAN_POINT('Ctrl Pts',(-148.795656613691,3.47406537533444,
134.28844884617));
#111612=CARTESIAN_POINT('Ctrl Pts',(-148.803402946957,3.56846657191188,
134.188918105281));
#111613=CARTESIAN_POINT('Ctrl Pts',(-148.81115101496,3.66288890898238,134.089365075173));
#111614=CARTESIAN_POINT('Ctrl Pts',(-148.818899082963,3.75311687096139,
133.98588438024));
#111615=CARTESIAN_POINT('Ctrl Pts',(-148.826647150966,3.83882180242114,
133.878873624817));
#111616=CARTESIAN_POINT('Ctrl Pts',(-148.834403453707,3.92461782210253,
133.771749137089));
#111617=CARTESIAN_POINT('Ctrl Pts',(-148.842159756449,4.0058809637121,133.661087399912));
#111618=CARTESIAN_POINT('Ctrl Pts',(-148.849916059191,4.08232414342432,
133.54731753493));
#111619=CARTESIAN_POINT('Ctrl Pts',(-148.857676501705,4.15880812316321,
133.433486947546));
#111620=CARTESIAN_POINT('Ctrl Pts',(-148.86543694422,4.23046681079151,133.31654526005));
#111621=CARTESIAN_POINT('Ctrl Pts',(-148.873197386734,4.2970583958223,133.196947545014));
#111622=CARTESIAN_POINT('Ctrl Pts',(-148.880970286999,4.36375687957711,
133.077157841108));
#111623=CARTESIAN_POINT('Ctrl Pts',(-148.888743187265,4.42537183025414,
132.954703938896));
#111624=CARTESIAN_POINT('Ctrl Pts',(-148.89651608753,4.48170865415154,132.830063113443));
#111625=CARTESIAN_POINT('Ctrl Pts',(-148.904006423292,4.53599749259683,
132.709953295946));
#111626=CARTESIAN_POINT('Ctrl Pts',(-148.911496759054,4.58538517280245,
132.587813080622));
#111627=CARTESIAN_POINT('Ctrl Pts',(-148.918987094816,4.62974158536802,
132.464082255436));
#111628=CARTESIAN_POINT('Ctrl Pts',(-148.926761428936,4.67577978479752,
132.335660138407));
#111629=CARTESIAN_POINT('Ctrl Pts',(-148.934535763055,4.71654349939442,
132.205117611908));
#111630=CARTESIAN_POINT('Ctrl Pts',(-148.942310097174,4.75183351514652,
132.072927252328));
#111631=CARTESIAN_POINT('Ctrl Pts',(-148.950074850121,4.78708003910796,
131.940899805552));
#111632=CARTESIAN_POINT('Ctrl Pts',(-148.957839603068,4.81686618657105,
131.807228940505));
#111633=CARTESIAN_POINT('Ctrl Pts',(-148.965604356015,4.84104124631871,
131.672405958514));
#111634=CARTESIAN_POINT('Ctrl Pts',(-148.9733613969,4.86519229505628,131.537716884608));
#111635=CARTESIAN_POINT('Ctrl Pts',(-148.981118437785,4.88374327806583,
131.4018783533));
#111636=CARTESIAN_POINT('Ctrl Pts',(-148.98887547867,4.89659373295067,131.265395189944));
#111637=CARTESIAN_POINT('Ctrl Pts',(-148.99662666991,4.90943449720761,131.129014949603));
#111638=CARTESIAN_POINT('Ctrl Pts',(-149.00437786115,4.91658325336494,130.991991432478));
#111639=CARTESIAN_POINT('Ctrl Pts',(-149.01212905239,4.91799096520328,130.854837628956));
#111640=CARTESIAN_POINT('Ctrl Pts',(-149.019876949168,4.91939807872653,
130.717742119461));
#111641=CARTESIAN_POINT('Ctrl Pts',(-149.027624845945,4.91506899709357,
130.580516823833));
#111642=CARTESIAN_POINT('Ctrl Pts',(-149.035372742722,4.90500670851211,
130.443677582269));
#111643=CARTESIAN_POINT('Ctrl Pts',(-149.043119018806,4.89494652474449,
130.306866964524));
#111644=CARTESIAN_POINT('Ctrl Pts',(-149.05086529489,4.87915554808234,130.170442629885));
#111645=CARTESIAN_POINT('Ctrl Pts',(-149.058611570974,4.85768882557762,
130.03491774356));
#111646=CARTESIAN_POINT('Ctrl Pts',(-149.066357904239,4.83622194461039,
129.899391856821));
#111647=CARTESIAN_POINT('Ctrl Pts',(-149.074104237505,4.80907929536316,
129.764765817797));
#111648=CARTESIAN_POINT('Ctrl Pts',(-149.08185057077,4.77636741682319,129.631544620911));
#111649=CARTESIAN_POINT('Ctrl Pts',(-149.089598638773,4.74364821268478,
129.498293590062));
#111650=CARTESIAN_POINT('Ctrl Pts',(-149.097346706776,4.70535739070186,
129.366448406991));
#111651=CARTESIAN_POINT('Ctrl Pts',(-149.105094774779,4.66165182037551,
129.236500493674));
#111652=CARTESIAN_POINT('Ctrl Pts',(-149.112851077521,4.61789979924897,
129.106414470169));
#111653=CARTESIAN_POINT('Ctrl Pts',(-149.120607380263,4.56872165866055,
128.978230115633));
#111654=CARTESIAN_POINT('Ctrl Pts',(-149.128363683005,4.51432325498414,
128.852420912552));
#111655=CARTESIAN_POINT('Ctrl Pts',(-149.136124125519,4.45989581724178,
128.726544561311));
#111656=CARTESIAN_POINT('Ctrl Pts',(-149.143884568033,4.40024273461425,
128.603046239379));
#111657=CARTESIAN_POINT('Ctrl Pts',(-149.151645010547,4.33561616807006,
128.482375366607));
#111658=CARTESIAN_POINT('Ctrl Pts',(-149.159417910813,4.27088585722397,
128.361510782238));
#111659=CARTESIAN_POINT('Ctrl Pts',(-149.167190811078,4.20116630708807,
128.243483053959));
#111660=CARTESIAN_POINT('Ctrl Pts',(-149.174963711343,4.12675388004265,
128.128713877794));
#111661=CARTESIAN_POINT('Ctrl Pts',(-149.182454047105,4.05504653215453,
128.018116850269));
#111662=CARTESIAN_POINT('Ctrl Pts',(-149.189944382867,3.97898175732552,
127.910545826359));
#111663=CARTESIAN_POINT('Ctrl Pts',(-149.197434718629,3.89885923431622,
127.806347986924));
#111664=CARTESIAN_POINT('Ctrl Pts',(-149.205209052748,3.81569884149349,
127.698199454736));
#111665=CARTESIAN_POINT('Ctrl Pts',(-149.212983386868,3.72790350024213,
127.593342362906));
#111666=CARTESIAN_POINT('Ctrl Pts',(-149.220757720987,3.63576312242217,
127.492199754906));
#111667=CARTESIAN_POINT('Ctrl Pts',(-149.228522473934,3.54373629938355,
127.391181796132));
#111668=CARTESIAN_POINT('Ctrl Pts',(-149.236287226881,3.4473753551353,127.293869499034));
#111669=CARTESIAN_POINT('Ctrl Pts',(-149.244051979828,3.34701217230263,
127.200655221594));
#111670=CARTESIAN_POINT('Ctrl Pts',(-149.251809020713,3.24674867159775,
127.107533525888));
#111671=CARTESIAN_POINT('Ctrl Pts',(-149.259566061598,3.14249112751129,
127.018502014279));
#111672=CARTESIAN_POINT('Ctrl Pts',(-149.267323102483,3.03460996153094,
126.93391807906));
#111673=CARTESIAN_POINT('Ctrl Pts',(-149.275074293723,2.92681014957661,
126.849397929244));
#111674=CARTESIAN_POINT('Ctrl Pts',(-149.282825484963,2.81539246123304,
126.769318920234));
#111675=CARTESIAN_POINT('Ctrl Pts',(-149.290576676203,2.70076198456721,
126.693999591425));
#111676=CARTESIAN_POINT('Ctrl Pts',(-149.29832457298,2.58618022891199,126.61871227534));
#111677=CARTESIAN_POINT('Ctrl Pts',(-149.306072469758,2.46838872691099,
126.548180830123));
#111678=CARTESIAN_POINT('Ctrl Pts',(-149.313820366535,2.34782308473086,
126.482681565935));
#111679=CARTESIAN_POINT('Ctrl Pts',(-149.321566642619,2.22728266228398,
126.417196002782));
#111680=CARTESIAN_POINT('Ctrl Pts',(-149.329312918703,2.10396959721172,
126.356740713449));
#111681=CARTESIAN_POINT('Ctrl Pts',(-149.337059194787,1.97834538421457,
126.301546763623));
#111682=CARTESIAN_POINT('Ctrl Pts',(-149.344805528052,1.8527202438882,126.246352406369));
#111683=CARTESIAN_POINT('Ctrl Pts',(-149.352551861318,1.72478427953526,
126.196419623384));
#111684=CARTESIAN_POINT('Ctrl Pts',(-149.360298194583,1.59501994419185,
126.151931742222));
#111685=CARTESIAN_POINT('Ctrl Pts',(-149.368046262586,1.46522654902508,
126.107433898309));
#111686=CARTESIAN_POINT('Ctrl Pts',(-149.375794330589,1.3336043378713,126.068383509348));
#111687=CARTESIAN_POINT('Ctrl Pts',(-149.383542398592,1.20065154975243,
126.034914222168));
#111688=CARTESIAN_POINT('Ctrl Pts',(-149.391298701334,1.06755745782838,
126.001409363431));
#111689=CARTESIAN_POINT('Ctrl Pts',(-149.399055004076,0.933130343757175,
125.973497551202));
#111690=CARTESIAN_POINT('Ctrl Pts',(-149.406811306818,0.797879832161182,
125.951261521532));
#111691=CARTESIAN_POINT('Ctrl Pts',(-149.414571749332,0.662557133294468,
125.929013623823));
#111692=CARTESIAN_POINT('Ctrl Pts',(-149.422332191846,0.526410549130532,
125.912447592082));
#111693=CARTESIAN_POINT('Ctrl Pts',(-149.43009263436,0.38995448848199,125.901594198552));
#111694=CARTESIAN_POINT('Ctrl Pts',(-149.437865534626,0.253279376451267,
125.890723382191));
#111695=CARTESIAN_POINT('Ctrl Pts',(-149.445638434891,0.116294186088119,
125.885583544159));
#111696=CARTESIAN_POINT('Ctrl Pts',(-149.453411335157,-0.0204861066943495,
125.886153283391));
#111697=CARTESIAN_POINT('Ctrl Pts',(-149.460901670918,-0.152294091303552,
125.886702311167));
#111698=CARTESIAN_POINT('Ctrl Pts',(-149.46839200668,-0.283911509068489,
125.892552994506));
#111699=CARTESIAN_POINT('Ctrl Pts',(-149.475882342442,-0.414884283208473,
125.903640864913));
#111700=CARTESIAN_POINT('Ctrl Pts',(-149.483656676561,-0.55082292988965,
125.915149135296));
#111701=CARTESIAN_POINT('Ctrl Pts',(-149.491431010681,-0.686497697419421,
125.932336022973));
#111702=CARTESIAN_POINT('Ctrl Pts',(-149.4992053448,-0.82139596290188,125.955186282215));
#111703=CARTESIAN_POINT('Ctrl Pts',(-149.506970097747,-0.956127978328336,
125.978008380554));
#111704=CARTESIAN_POINT('Ctrl Pts',(-149.514734850694,-1.09008501401763,
126.006479898467));
#111705=CARTESIAN_POINT('Ctrl Pts',(-149.522499603641,-1.2227575774215,
126.040533692776));
#111706=CARTESIAN_POINT('Ctrl Pts',(-149.530256644526,-1.35529836856504,
126.074553664375));
#111707=CARTESIAN_POINT('Ctrl Pts',(-149.538013685411,-1.48655684999594,
126.114144782202));
#111708=CARTESIAN_POINT('Ctrl Pts',(-149.545770726296,-1.6160321155932,
126.159188579431));
#111709=CARTESIAN_POINT('Ctrl Pts',(-149.553521917536,-1.74540974288462,
126.204198408782));
#111710=CARTESIAN_POINT('Ctrl Pts',(-149.561273108776,-1.87300646319637,
126.254652605089));
#111711=CARTESIAN_POINT('Ctrl Pts',(-149.569024300016,-1.99833532031902,
126.310382534613));
#111712=CARTESIAN_POINT('Ctrl Pts',(-149.576772196793,-2.123610909335,126.36608877743));
#111713=CARTESIAN_POINT('Ctrl Pts',(-149.58452009357,-2.24662019579938,
126.427066135125));
#111714=CARTESIAN_POINT('Ctrl Pts',(-149.592267990347,-2.36689525637319,
126.493097472285));
#111715=CARTESIAN_POINT('Ctrl Pts',(-149.600014266431,-2.48714515799717,
126.559114997113));
#111716=CARTESIAN_POINT('Ctrl Pts',(-149.607760542515,-2.60466162885577,
126.630184210578));
#111717=CARTESIAN_POINT('Ctrl Pts',(-149.615506818599,-2.71900081768446,
126.706041740766));
#111718=CARTESIAN_POINT('Ctrl Pts',(-149.623253151865,-2.83334085053892,
126.781899830918));
#111719=CARTESIAN_POINT('Ctrl Pts',(-149.63099948513,-2.94450322877614,
126.862546092183));
#111720=CARTESIAN_POINT('Ctrl Pts',(-149.638745818395,-3.05207293608227,
126.947673716178));
#111721=CARTESIAN_POINT('Ctrl Pts',(-149.646493886398,-3.15966673287837,
127.032820403915));
#111722=CARTESIAN_POINT('Ctrl Pts',(-149.654241954401,-3.26366595125462,
127.122450208801));
#111723=CARTESIAN_POINT('Ctrl Pts',(-149.661990022404,-3.36368883998906,
127.216216187609));
#111724=CARTESIAN_POINT('Ctrl Pts',(-149.669746325146,-3.46381803424008,
127.310081822015));
#111725=CARTESIAN_POINT('Ctrl Pts',(-149.677502627888,-3.55996217109209,
127.408092143962));
#111726=CARTESIAN_POINT('Ctrl Pts',(-149.685258930629,-3.65177617780567,
127.509863112678));
#111727=CARTESIAN_POINT('Ctrl Pts',(-149.693019373143,-3.74363918841935,
127.611688399625));
#111728=CARTESIAN_POINT('Ctrl Pts',(-149.700779815658,-3.83116721440323,
127.717278031949));
#111729=CARTESIAN_POINT('Ctrl Pts',(-149.708540258172,-3.91405631566911,
127.826215856096));
#111730=CARTESIAN_POINT('Ctrl Pts',(-149.716313158437,-3.99707847787888,
127.93532855691));
#111731=CARTESIAN_POINT('Ctrl Pts',(-149.724086058703,-4.07544661062439,
128.047799869179));
#111732=CARTESIAN_POINT('Ctrl Pts',(-149.731858958968,-4.14890036216591,
128.163184961287));
#111733=CARTESIAN_POINT('Ctrl Pts',(-149.73934929473,-4.21968388482365,
128.274375514665));
#111734=CARTESIAN_POINT('Ctrl Pts',(-149.746839630493,-4.28590396847165,
128.388271413092));
#111735=CARTESIAN_POINT('Ctrl Pts',(-149.754329966255,-4.34736941268764,
128.504455782116));
#111736=CARTESIAN_POINT('Ctrl Pts',(-149.762555614144,-4.41486880356576,
128.632045751385));
#111737=CARTESIAN_POINT('Ctrl Pts',(-149.770781262032,-4.47682817998231,
128.762761823252));
#111738=CARTESIAN_POINT('Ctrl Pts',(-149.779006909921,-4.53296421753863,
128.896110512099));
#111739=CARTESIAN_POINT('Ctrl Pts',(-149.787213600141,-4.58897087825169,
129.029151871944));
#111740=CARTESIAN_POINT('Ctrl Pts',(-149.795420290362,-4.63918083480873,
129.164813454452));
#111741=CARTESIAN_POINT('Ctrl Pts',(-149.803626980582,-4.68335698160947,
129.302578194806));
#111742=CARTESIAN_POINT('Ctrl Pts',(-149.809132002562,-4.71299020189066,
129.394990349183));
#111743=CARTESIAN_POINT('Ctrl Pts',(-149.81463702454,-4.73990931628902,
129.488348304389));
#111744=CARTESIAN_POINT('Ctrl Pts',(-149.820142046519,-4.76405452823404,
129.582490119308));
#111745=CARTESIAN_POINT('Origin',(213.235140564004,0.,130.804360617566));
#111746=CARTESIAN_POINT('',(-151.915051610183,-4.76405452823401,129.582490119308));
#111747=CARTESIAN_POINT('',(-151.569820863616,-4.76405452823393,129.582490119308));
#111748=CARTESIAN_POINT('',(213.235140564004,-4.76405452823405,129.582490119308));
#111749=CARTESIAN_POINT('',(-150.23514056396,-4.91824801635102,130.808777874548));
#111750=CARTESIAN_POINT('Ctrl Pts',(-150.235140564011,-4.91824801635022,
130.808777875439));
#111751=CARTESIAN_POINT('Ctrl Pts',(-150.246220776016,-4.91807253331176,
131.004163594484));
#111752=CARTESIAN_POINT('Ctrl Pts',(-150.257300988021,-4.90625068833561,
131.199047831327));
#111753=CARTESIAN_POINT('Ctrl Pts',(-150.268381200027,-4.88298081443509,
131.392307407981));
#111754=CARTESIAN_POINT('Ctrl Pts',(-150.276132872591,-4.86670130254354,
131.527511044654));
#111755=CARTESIAN_POINT('Ctrl Pts',(-150.283884545156,-4.84481967606861,
131.661920399415));
#111756=CARTESIAN_POINT('Ctrl Pts',(-150.291636217721,-4.81741652506013,
131.795158824356));
#111757=CARTESIAN_POINT('Ctrl Pts',(-150.29941055184,-4.78993326256789,
131.928786763915));
#111758=CARTESIAN_POINT('Ctrl Pts',(-150.307184885959,-4.75684229574795,
132.061481976966));
#111759=CARTESIAN_POINT('Ctrl Pts',(-150.314959220078,-4.71821930886351,
132.192737229285));
#111760=CARTESIAN_POINT('Ctrl Pts',(-150.322723973025,-4.67964392135857,
132.323830721235));
#111761=CARTESIAN_POINT('Ctrl Pts',(-150.330488725972,-4.63555018832687,
132.45348741196));
#111762=CARTESIAN_POINT('Ctrl Pts',(-150.338253478919,-4.58606495851269,
132.581209305216));
#111763=CARTESIAN_POINT('Ctrl Pts',(-150.346010519803,-4.53662887812639,
132.708804343286));
#111764=CARTESIAN_POINT('Ctrl Pts',(-150.353767560688,-4.48181209780396,
132.834468045893));
#111765=CARTESIAN_POINT('Ctrl Pts',(-150.361524601573,-4.42179141657143,
132.957717004891));
#111766=CARTESIAN_POINT('Ctrl Pts',(-150.369275792813,-4.36181599740159,
133.080873020891));
#111767=CARTESIAN_POINT('Ctrl Pts',(-150.377026984053,-4.29664465889072,
133.201617567748));
#111768=CARTESIAN_POINT('Ctrl Pts',(-150.384778175293,-4.22650236823941,
133.319487014741));
#111769=CARTESIAN_POINT('Ctrl Pts',(-150.39252607207,-4.15638988993283,
133.437306364074));
#111770=CARTESIAN_POINT('Ctrl Pts',(-150.400273968847,-4.08131086117433,
133.552252708723));
#111771=CARTESIAN_POINT('Ctrl Pts',(-150.408021865624,-4.00153616340971,
133.663887046089));
#111772=CARTESIAN_POINT('Ctrl Pts',(-150.415768141708,-3.92177815279212,
133.775498031959));
#111773=CARTESIAN_POINT('Ctrl Pts',(-150.423514417792,-3.83732665405074,
133.883798070673));
#111774=CARTESIAN_POINT('Ctrl Pts',(-150.431260693876,-3.74849561838572,
133.988377524155));
#111775=CARTESIAN_POINT('Ctrl Pts',(-150.439007027141,-3.6596639269903,
134.092957749618));
#111776=CARTESIAN_POINT('Ctrl Pts',(-150.446753360406,-3.56645288726782,
134.193817037067));
#111777=CARTESIAN_POINT('Ctrl Pts',(-150.454499693671,-3.46921617720046,
134.290579511777));
#111778=CARTESIAN_POINT('Ctrl Pts',(-150.462247761674,-3.3719576916462,
134.387363655771));
#111779=CARTESIAN_POINT('Ctrl Pts',(-150.469995829677,-3.27067201890082,
134.480048885677));
#111780=CARTESIAN_POINT('Ctrl Pts',(-150.47774389768,-3.16574876197482,
134.568297099304));
#111781=CARTESIAN_POINT('Ctrl Pts',(-150.485500200422,-3.06071399136262,
134.656639104181));
#111782=CARTESIAN_POINT('Ctrl Pts',(-150.493256503163,-2.95203421336577,
134.740534420578));
#111783=CARTESIAN_POINT('Ctrl Pts',(-150.501012805905,-2.84013153683342,
134.819685749605));
#111784=CARTESIAN_POINT('Ctrl Pts',(-150.508773248419,-2.72816913447328,
134.898879324079));
#111785=CARTESIAN_POINT('Ctrl Pts',(-150.516533690933,-2.61298073421539,
134.973323653833));
#111786=CARTESIAN_POINT('Ctrl Pts',(-150.524294133447,-2.49501547479722,
135.042766077526));
#111787=CARTESIAN_POINT('Ctrl Pts',(-150.532067033712,-2.37686084707217,
135.112319976364));
#111788=CARTESIAN_POINT('Ctrl Pts',(-150.539839933978,-2.25592079748713,
135.176855739468));
#111789=CARTESIAN_POINT('Ctrl Pts',(-150.547612834243,-2.13266779395145,
135.236167375892));
#111790=CARTESIAN_POINT('Ctrl Pts',(-150.555103170006,-2.01389534752485,
135.293322884946));
#111791=CARTESIAN_POINT('Ctrl Pts',(-150.56259350577,-1.89297547369181,
135.345627371121));
#111792=CARTESIAN_POINT('Ctrl Pts',(-150.570083841533,-1.77034471150173,
135.392940208786));
#111793=CARTESIAN_POINT('Ctrl Pts',(-150.577858175652,-1.64306436671462,
135.442046927061));
#111794=CARTESIAN_POINT('Ctrl Pts',(-150.585632509772,-1.51353764999049,
135.485931563407));
#111795=CARTESIAN_POINT('Ctrl Pts',(-150.593406843891,-1.38223222104053,
135.524383620647));
#111796=CARTESIAN_POINT('Ctrl Pts',(-150.601171596838,-1.25108861429664,
135.562788289164));
#111797=CARTESIAN_POINT('Ctrl Pts',(-150.608936349785,-1.11817102856585,
135.595773591143));
#111798=CARTESIAN_POINT('Ctrl Pts',(-150.616701102732,-0.983967007037161,
135.623177068891));
#111799=CARTESIAN_POINT('Ctrl Pts',(-150.624458143617,-0.849896278834962,
135.650553329119));
#111800=CARTESIAN_POINT('Ctrl Pts',(-150.632215184502,-0.714542038109991,
135.672358720107));
#111801=CARTESIAN_POINT('Ctrl Pts',(-150.639972225387,-0.578406554017688,
135.688480693974));
#111802=CARTESIAN_POINT('Ctrl Pts',(-150.647723416627,-0.442373730752734,
135.704590510135));
#111803=CARTESIAN_POINT('Ctrl Pts',(-150.655474607867,-0.305561223452434,
135.715025394223));
#111804=CARTESIAN_POINT('Ctrl Pts',(-150.663225799107,-0.16848069804129,
135.719724013785));
#111805=CARTESIAN_POINT('Ctrl Pts',(-150.670973695884,-0.0314584355100012,
135.724420636308));
#111806=CARTESIAN_POINT('Ctrl Pts',(-150.678721592662,0.105831228646485,
135.723385830068));
#111807=CARTESIAN_POINT('Ctrl Pts',(-150.686469489439,0.242872531071293,
135.716610203667));
#111808=CARTESIAN_POINT('Ctrl Pts',(-150.694215765523,0.379885167409903,
135.709835994582));
#111809=CARTESIAN_POINT('Ctrl Pts',(-150.701962041607,0.516649155111232,
135.697323373199));
#111810=CARTESIAN_POINT('Ctrl Pts',(-150.709708317691,0.652650155767247,
135.679115056169));
#111811=CARTESIAN_POINT('Ctrl Pts',(-150.717454650956,0.78865216035157,
135.660906604729));
#111812=CARTESIAN_POINT('Ctrl Pts',(-150.725200984222,0.92389077914432,
135.637002425626));
#111813=CARTESIAN_POINT('Ctrl Pts',(-150.732947317487,1.05785860650549,
135.607496908693));
#111814=CARTESIAN_POINT('Ctrl Pts',(-150.74069538549,1.19185643503291,135.577984784204));
#111815=CARTESIAN_POINT('Ctrl Pts',(-150.748443453493,1.32458252409625,
135.542868909889));
#111816=CARTESIAN_POINT('Ctrl Pts',(-150.756191521496,1.45554182880302,
135.502294317301));
#111817=CARTESIAN_POINT('Ctrl Pts',(-150.763947824238,1.58664031861709,
135.461676601553));
#111818=CARTESIAN_POINT('Ctrl Pts',(-150.77170412698,1.71596789900071,135.41558869412));
#111819=CARTESIAN_POINT('Ctrl Pts',(-150.779460429722,1.84304628383524,
135.36422502982));
#111820=CARTESIAN_POINT('Ctrl Pts',(-150.787220872236,1.97019249423002,
135.312833951186));
#111821=CARTESIAN_POINT('Ctrl Pts',(-150.79498131475,2.09508676119838,135.256161666376));
#111822=CARTESIAN_POINT('Ctrl Pts',(-150.802741757264,2.2172737431421,135.194449478907));
#111823=CARTESIAN_POINT('Ctrl Pts',(-150.81051465753,2.33965687047648,135.132638225556));
#111824=CARTESIAN_POINT('Ctrl Pts',(-150.818287557795,2.4593236866512,135.065771092969));
#111825=CARTESIAN_POINT('Ctrl Pts',(-150.82606045806,2.57584550520097,134.994134238639));
#111826=CARTESIAN_POINT('Ctrl Pts',(-150.833550793822,2.68813146214445,
134.925101564406));
#111827=CARTESIAN_POINT('Ctrl Pts',(-150.841041129584,2.79749685311942,
134.851640102322));
#111828=CARTESIAN_POINT('Ctrl Pts',(-150.848531465346,2.90358740578101,
134.774041113461));
#111829=CARTESIAN_POINT('Ctrl Pts',(-150.856305799465,3.01370041399339,
134.693499935351));
#111830=CARTESIAN_POINT('Ctrl Pts',(-150.864080133584,3.12063415568315,
134.608246158071));
#111831=CARTESIAN_POINT('Ctrl Pts',(-150.871854467704,3.22395875211928,
134.518559458115));
#111832=CARTESIAN_POINT('Ctrl Pts',(-150.879619220651,3.32715601022469,
134.428983289001));
#111833=CARTESIAN_POINT('Ctrl Pts',(-150.887383973598,3.42675268075169,
134.334985321135));
#111834=CARTESIAN_POINT('Ctrl Pts',(-150.895148726545,3.52234855443948,
134.236887926057));
#111835=CARTESIAN_POINT('Ctrl Pts',(-150.90290576743,3.61784948095785,134.138887962696));
#111836=CARTESIAN_POINT('Ctrl Pts',(-150.910662808315,3.70935724728015,
134.036796952998));
#111837=CARTESIAN_POINT('Ctrl Pts',(-150.9184198492,3.79650567493816,133.93097663535));
#111838=CARTESIAN_POINT('Ctrl Pts',(-150.92617104044,3.88358838328908,133.825236117626));
#111839=CARTESIAN_POINT('Ctrl Pts',(-150.93392223168,3.96631804883071,133.715772190239));
#111840=CARTESIAN_POINT('Ctrl Pts',(-150.94167342292,4.04436650290299,133.602982180532));
#111841=CARTESIAN_POINT('Ctrl Pts',(-150.949421319697,4.12238178430039,
133.490240109587));
#111842=CARTESIAN_POINT('Ctrl Pts',(-150.957169216474,4.19571958946585,
133.374175088837));
#111843=CARTESIAN_POINT('Ctrl Pts',(-150.964917113252,4.26409323445996,
133.255215968323));
#111844=CARTESIAN_POINT('Ctrl Pts',(-150.972663389336,4.33245257716132,
133.136281731492));
#111845=CARTESIAN_POINT('Ctrl Pts',(-150.98040966542,4.39584963041472,133.014454937787));
#111846=CARTESIAN_POINT('Ctrl Pts',(-150.988155941504,4.45404232047442,
132.890191404069));
#111847=CARTESIAN_POINT('Ctrl Pts',(-150.995902274769,4.51223544009941,
132.765926953066));
#111848=CARTESIAN_POINT('Ctrl Pts',(-151.003648608035,4.56522395406307,
132.639226080222));
#111849=CARTESIAN_POINT('Ctrl Pts',(-151.0113949413,4.6128130100626,132.510566700282));
#111850=CARTESIAN_POINT('Ctrl Pts',(-151.019143009303,4.66041272330121,
132.381878507967));
#111851=CARTESIAN_POINT('Ctrl Pts',(-151.026891077306,4.70261043686,132.251231302419));
#111852=CARTESIAN_POINT('Ctrl Pts',(-151.034639145309,4.73926058603645,
132.119119972027));
#111853=CARTESIAN_POINT('Ctrl Pts',(-151.042395448051,4.77594968742764,
131.986868232139));
#111854=CARTESIAN_POINT('Ctrl Pts',(-151.050151750793,4.80707934182604,
131.853149636288));
#111855=CARTESIAN_POINT('Ctrl Pts',(-151.057908053534,4.83255460742102,
131.718471676898));
#111856=CARTESIAN_POINT('Ctrl Pts',(-151.065668496049,4.8580434699323,131.583721835827));
#111857=CARTESIAN_POINT('Ctrl Pts',(-151.073428938563,4.87787187368826,
131.4480119976));
#111858=CARTESIAN_POINT('Ctrl Pts',(-151.081189381077,4.89199671091405,
131.311855684445));
#111859=CARTESIAN_POINT('Ctrl Pts',(-151.088962281342,4.90614422258249,
131.175480801088));
#111860=CARTESIAN_POINT('Ctrl Pts',(-151.096735181608,4.91456984732813,
131.038658401016));
#111861=CARTESIAN_POINT('Ctrl Pts',(-151.104508081873,4.91728262204888,
130.901903825408));
#111862=CARTESIAN_POINT('Ctrl Pts',(-151.111998417635,4.91989678057545,
130.770120623087));
#111863=CARTESIAN_POINT('Ctrl Pts',(-151.119488753397,4.91720623720689,
130.638400707617));
#111864=CARTESIAN_POINT('Ctrl Pts',(-151.126979089159,4.90926454528036,
130.507199572082));
#111865=CARTESIAN_POINT('Ctrl Pts',(-151.134753423278,4.9010217416906,130.371023905615));
#111866=CARTESIAN_POINT('Ctrl Pts',(-151.142527757397,4.8870956237371,130.234975771151));
#111867=CARTESIAN_POINT('Ctrl Pts',(-151.150302091517,4.86748913122206,
130.099568009819));
#111868=CARTESIAN_POINT('Ctrl Pts',(-151.158066844464,4.84790680195676,
129.964327126451));
#111869=CARTESIAN_POINT('Ctrl Pts',(-151.165831597411,4.82265808263384,
129.829725429153));
#111870=CARTESIAN_POINT('Ctrl Pts',(-151.173596350358,4.79179787068005,
129.696273875002));
#111871=CARTESIAN_POINT('Ctrl Pts',(-151.181353391243,4.76096830952383,
129.562954866816));
#111872=CARTESIAN_POINT('Ctrl Pts',(-151.189110432128,4.72453843459616,
129.430784106922));
#111873=CARTESIAN_POINT('Ctrl Pts',(-151.196867473013,4.68261465823956,
129.300265200067));
#111874=CARTESIAN_POINT('Ctrl Pts',(-151.204618664253,4.64072249692876,
129.169844718536));
#111875=CARTESIAN_POINT('Ctrl Pts',(-151.212369855493,4.59334479964782,
129.041073981332));
#111876=CARTESIAN_POINT('Ctrl Pts',(-151.220121046733,4.54063846596778,
128.914443851178));
#111877=CARTESIAN_POINT('Ctrl Pts',(-151.22786894351,4.48795453388548,128.787867542207));
#111878=CARTESIAN_POINT('Ctrl Pts',(-151.235616840287,4.42994661986385,
128.663430390926));
#111879=CARTESIAN_POINT('Ctrl Pts',(-151.243364737065,4.36682056791596,
128.541605396574));
#111880=CARTESIAN_POINT('Ctrl Pts',(-151.251111013149,4.30370772057747,
128.419805885385));
#111881=CARTESIAN_POINT('Ctrl Pts',(-151.258857289233,4.23547904456171,
128.300617791202));
#111882=CARTESIAN_POINT('Ctrl Pts',(-151.266603565317,4.16238718473159,
128.184491157673));
#111883=CARTESIAN_POINT('Ctrl Pts',(-151.274349898582,4.08929478535387,
128.068363666922));
#111884=CARTESIAN_POINT('Ctrl Pts',(-151.282096231848,4.0113393387887,127.955298012799));
#111885=CARTESIAN_POINT('Ctrl Pts',(-151.289842565113,3.9288176058177,127.845716454657));
#111886=CARTESIAN_POINT('Ctrl Pts',(-151.297590633116,3.84627739267689,
127.736110356485));
#111887=CARTESIAN_POINT('Ctrl Pts',(-151.305338701119,3.75916909344392,
127.629990219133));
#111888=CARTESIAN_POINT('Ctrl Pts',(-151.313086769122,3.66783039045661,
127.527746009568));
#111889=CARTESIAN_POINT('Ctrl Pts',(-151.320843071864,3.5763946116087,127.425393133641));
#111890=CARTESIAN_POINT('Ctrl Pts',(-151.328599374606,3.48071970839796,
127.326924706442));
#111891=CARTESIAN_POINT('Ctrl Pts',(-151.336355677347,3.38118133020755,
127.232694917258));
#111892=CARTESIAN_POINT('Ctrl Pts',(-151.344116119862,3.28158982538766,
127.138414834798));
#111893=CARTESIAN_POINT('Ctrl Pts',(-151.351876562376,3.17813103155089,
127.04837815469));
#111894=CARTESIAN_POINT('Ctrl Pts',(-151.35963700489,3.07121368868493,126.962898716032));
#111895=CARTESIAN_POINT('Ctrl Pts',(-151.367409905155,2.96412471260853,
126.877282058191));
#111896=CARTESIAN_POINT('Ctrl Pts',(-151.375182805421,2.85356640839853,
126.796237492155));
#111897=CARTESIAN_POINT('Ctrl Pts',(-151.382955705686,2.73997723184831,
126.72003596942));
#111898=CARTESIAN_POINT('Ctrl Pts',(-151.390446041448,2.63051730797986,
126.646604563977));
#111899=CARTESIAN_POINT('Ctrl Pts',(-151.39793637721,2.51824330818223,126.577670362564));
#111900=CARTESIAN_POINT('Ctrl Pts',(-151.405426712972,2.403567398574,126.513434514379));
#111901=CARTESIAN_POINT('Ctrl Pts',(-151.413201047091,2.2845435169978,126.446763144486));
#111902=CARTESIAN_POINT('Ctrl Pts',(-151.42097538121,2.16255496147165,126.38494224209));
#111903=CARTESIAN_POINT('Ctrl Pts',(-151.42874971533,2.03803478879638,126.32824653701));
#111904=CARTESIAN_POINT('Ctrl Pts',(-151.436514468277,1.91366807610524,
126.271620704318));
#111905=CARTESIAN_POINT('Ctrl Pts',(-151.444279221224,1.78677630652166,
126.220107661746));
#111906=CARTESIAN_POINT('Ctrl Pts',(-151.452043974171,1.65781903610666,
126.173937407316));
#111907=CARTESIAN_POINT('Ctrl Pts',(-151.459801015056,1.52898984787061,
126.127813009833));
#111908=CARTESIAN_POINT('Ctrl Pts',(-151.467558055941,1.39809960705316,
126.087020971184));
#111909=CARTESIAN_POINT('Ctrl Pts',(-151.475315096826,1.26562952906329,
126.05174397432));
#111910=CARTESIAN_POINT('Ctrl Pts',(-151.483066288066,1.13325934778988,
126.016493580113));
#111911=CARTESIAN_POINT('Ctrl Pts',(-151.490817479306,0.999312076958704,
125.986750049783));
#111912=CARTESIAN_POINT('Ctrl Pts',(-151.498568670546,0.86428550133109,
125.962646702568));
#111913=CARTESIAN_POINT('Ctrl Pts',(-151.506316567323,0.729316315599885,
125.938553599918));
#111914=CARTESIAN_POINT('Ctrl Pts',(-151.514064464101,0.593269121533218,
125.92009598104));
#111915=CARTESIAN_POINT('Ctrl Pts',(-151.521812360878,0.456653130504683,
125.907356331178));
#111916=CARTESIAN_POINT('Ctrl Pts',(-151.529558636962,0.32006571659637,
125.894619346177));
#111917=CARTESIAN_POINT('Ctrl Pts',(-151.537304913046,0.182910131413754,
125.887597987408));
#111918=CARTESIAN_POINT('Ctrl Pts',(-151.54505118913,0.0457015701417753,
125.886322957179));
#111919=CARTESIAN_POINT('Ctrl Pts',(-151.552797522395,-0.0915080039728203,
125.885047917537));
#111920=CARTESIAN_POINT('Ctrl Pts',(-151.56054385566,-0.228770164008777,
125.88951929471));
#111921=CARTESIAN_POINT('Ctrl Pts',(-151.568290188926,-0.365569244760797,
125.899715656941));
#111922=CARTESIAN_POINT('Ctrl Pts',(-151.576038256929,-0.502398960718268,
125.909914302577));
#111923=CARTESIAN_POINT('Ctrl Pts',(-151.583786324932,-0.63876500122497,
125.925840455389));
#111924=CARTESIAN_POINT('Ctrl Pts',(-151.591534392935,-0.774156750474476,
125.947420800336));
#111925=CARTESIAN_POINT('Ctrl Pts',(-151.599290695677,-0.909692395686082,
125.96902408113));
#111926=CARTESIAN_POINT('Ctrl Pts',(-151.607046998418,-1.04425129443386,
125.996293496729));
#111927=CARTESIAN_POINT('Ctrl Pts',(-151.61480330116,-1.1773324095725,126.029104450629));
#111928=CARTESIAN_POINT('Ctrl Pts',(-151.622563743675,-1.31048455410964,
126.061932916723));
#111929=CARTESIAN_POINT('Ctrl Pts',(-151.630324186189,-1.44215696824627,
126.100308705217));
#111930=CARTESIAN_POINT('Ctrl Pts',(-151.638084628703,-1.5718646763128,
126.14405756928));
#111931=CARTESIAN_POINT('Ctrl Pts',(-151.645857528968,-1.70178060270723,
126.187876662905));
#111932=CARTESIAN_POINT('Ctrl Pts',(-151.653630429234,-1.82972515537736,
126.237085927844));
#111933=CARTESIAN_POINT('Ctrl Pts',(-151.661403329499,-1.95523337908873,
126.291462934724));
#111934=CARTESIAN_POINT('Ctrl Pts',(-151.668893665261,-2.07617906273273,
126.343863200438));
#111935=CARTESIAN_POINT('Ctrl Pts',(-151.676384001023,-2.19486219803625,
126.401061876557));
#111936=CARTESIAN_POINT('Ctrl Pts',(-151.683874336785,-2.31089076662683,
126.46282092211));
#111937=CARTESIAN_POINT('Ctrl Pts',(-151.691649612949,-2.43133318634517,
126.526929347959));
#111938=CARTESIAN_POINT('Ctrl Pts',(-151.699424889113,-2.5492966480185,
126.596155075043));
#111939=CARTESIAN_POINT('Ctrl Pts',(-151.707200165277,-2.66431576793663,
126.670282177185));
#111940=CARTESIAN_POINT('Ctrl Pts',(-151.714965652402,-2.77919007927822,
126.744315953624));
#111941=CARTESIAN_POINT('Ctrl Pts',(-151.722731139526,-2.89112709957447,
126.823238615968));
#111942=CARTESIAN_POINT('Ctrl Pts',(-151.730496626651,-2.99968480245734,
126.906787764057));
#111943=CARTESIAN_POINT('Ctrl Pts',(-151.738252808443,-3.10811242135966,
126.990236795753));
#111944=CARTESIAN_POINT('Ctrl Pts',(-151.746008990236,-3.21316847992648,
127.078301034847));
#111945=CARTESIAN_POINT('Ctrl Pts',(-151.753765172028,-3.31443931528753,
127.170674460538));
#111946=CARTESIAN_POINT('Ctrl Pts',(-151.761516077246,-3.41564125552377,
127.262985044063));
#111947=CARTESIAN_POINT('Ctrl Pts',(-151.769266982464,-3.51306280789825,
127.359598719844));
#111948=CARTESIAN_POINT('Ctrl Pts',(-151.777017887682,-3.60632278748346,
127.460168784705));
#111949=CARTESIAN_POINT('Ctrl Pts',(-151.784765198523,-3.69953951901311,
127.560692211557));
#111950=CARTESIAN_POINT('Ctrl Pts',(-151.792512509363,-3.7885982528057,
127.665168090575));
#111951=CARTESIAN_POINT('Ctrl Pts',(-151.800259820204,-3.87315442984602,
127.773212679067));
#111952=CARTESIAN_POINT('Ctrl Pts',(-151.808005216091,-3.95768970658522,
127.881230561475));
#111953=CARTESIAN_POINT('Ctrl Pts',(-151.815750611978,-4.03772440161672,
127.992815089638));
#111954=CARTESIAN_POINT('Ctrl Pts',(-151.823496007865,-4.11295430966178,
128.107549554637));
#111955=CARTESIAN_POINT('Ctrl Pts',(-151.831243875261,-4.1882082231111,
128.222320630704));
#111956=CARTESIAN_POINT('Ctrl Pts',(-151.838991742656,-4.25865406613801,
128.340243328434));
#111957=CARTESIAN_POINT('Ctrl Pts',(-151.846739610052,-4.32403098437282,
128.460871955617));
#111958=CARTESIAN_POINT('Ctrl Pts',(-151.854488485788,-4.38941641103889,
128.581516281925));
#111959=CARTESIAN_POINT('Ctrl Pts',(-151.862237361525,-4.44973141953418,
128.704866891528));
#111960=CARTESIAN_POINT('Ctrl Pts',(-151.869986237261,-4.50476163073174,
128.830454410882));
#111961=CARTESIAN_POINT('Ctrl Pts',(-151.877742268904,-4.55984266105212,
128.956157907394));
#111962=CARTESIAN_POINT('Ctrl Pts',(-151.885498300547,-4.60962899216592,
129.08410207972));
#111963=CARTESIAN_POINT('Ctrl Pts',(-151.89325433219,-4.65395465341272,
129.213798092395));
#111964=CARTESIAN_POINT('Ctrl Pts',(-151.900520091521,-4.69547841216282,
129.335295793494));
#111965=CARTESIAN_POINT('Ctrl Pts',(-151.907785850852,-4.73221042479218,
129.45833044329));
#111966=CARTESIAN_POINT('Ctrl Pts',(-151.915051610183,-4.76405452823401,
129.582490119308));
#111967=CARTESIAN_POINT('Ctrl Pts',(-150.165071172634,-4.76405452823413,
129.582490119309));
#111968=CARTESIAN_POINT('Ctrl Pts',(-150.172710513743,-4.79768513315927,
129.713615337496));
#111969=CARTESIAN_POINT('Ctrl Pts',(-150.180349854851,-4.82588729218672,
129.84608862954));
#111970=CARTESIAN_POINT('Ctrl Pts',(-150.18798919596,-4.84857159836929,
129.979414244772));
#111971=CARTESIAN_POINT('Ctrl Pts',(-150.195847757293,-4.87190685842699,
130.116565801391));
#111972=CARTESIAN_POINT('Ctrl Pts',(-150.203706318627,-4.88940273674939,
130.254618883265));
#111973=CARTESIAN_POINT('Ctrl Pts',(-150.21156487996,-4.90101913576986,
130.393028035198));
#111974=CARTESIAN_POINT('Ctrl Pts',(-150.219423441294,-4.9126355347903,
130.531437187131));
#111975=CARTESIAN_POINT('Ctrl Pts',(-150.227282002627,-4.91837247641928,
130.670201946933));
#111976=CARTESIAN_POINT('Ctrl Pts',(-150.23514056396,-4.91824801635102,
130.808777874548));
#111977=CARTESIAN_POINT('',(-149.889859435963,-4.91824998668701,130.803998742957));
#111978=CARTESIAN_POINT('Ctrl Pts',(-149.820142046519,-4.76405452823404,
129.582490119308));
#111979=CARTESIAN_POINT('Ctrl Pts',(-149.828324075985,-4.79994118524423,
129.722411650335));
#111980=CARTESIAN_POINT('Ctrl Pts',(-149.836506105451,-4.82969789362151,
129.86406546982));
#111981=CARTESIAN_POINT('Ctrl Pts',(-149.844688134917,-4.8531686134343,
130.006903739687));
#111982=CARTESIAN_POINT('Ctrl Pts',(-149.85285286192,-4.87658969993171,
130.149439950779));
#111983=CARTESIAN_POINT('Ctrl Pts',(-149.861017588924,-4.89375125390065,
130.293155299377));
#111984=CARTESIAN_POINT('Ctrl Pts',(-149.869182315927,-4.90454780912303,
130.437490271904));
#111985=CARTESIAN_POINT('Ctrl Pts',(-149.876074689272,-4.91366187863253,
130.559332743429));
#111986=CARTESIAN_POINT('Ctrl Pts',(-149.882967062617,-4.9182409820493,
130.681616409001));
#111987=CARTESIAN_POINT('Ctrl Pts',(-149.889859435963,-4.91824998668701,
130.803998742957));
#111988=CARTESIAN_POINT('Ctrl Pts',(-149.889859435993,-4.91824998668705,
130.803998743496));
#111989=CARTESIAN_POINT('Ctrl Pts',(-149.897930859643,-4.91826053169582,
130.947316526095));
#111990=CARTESIAN_POINT('Ctrl Pts',(-149.906002283294,-4.91200233468265,
131.090528101548));
#111991=CARTESIAN_POINT('Ctrl Pts',(-149.914073706944,-4.89952911294758,
131.23307676361));
#111992=CARTESIAN_POINT('Ctrl Pts',(-149.922154256147,-4.88704178898657,
131.375786591207));
#111993=CARTESIAN_POINT('Ctrl Pts',(-149.93023480535,-4.86832545243638,
131.517831670927));
#111994=CARTESIAN_POINT('Ctrl Pts',(-149.938315354553,-4.84348530688792,
131.658663341699));
#111995=CARTESIAN_POINT('Ctrl Pts',(-149.946413553537,-4.81859090473859,
131.799802621287));
#111996=CARTESIAN_POINT('Ctrl Pts',(-149.954511752521,-4.78754601215525,
131.939722856525));
#111997=CARTESIAN_POINT('Ctrl Pts',(-149.962609951505,-4.75050673616793,
132.077886750837));
#111998=CARTESIAN_POINT('Ctrl Pts',(-149.970717255956,-4.71342581389545,
132.216205994107));
#111999=CARTESIAN_POINT('Ctrl Pts',(-149.978824560407,-4.67033716232297,
132.352764631252));
#112000=CARTESIAN_POINT('Ctrl Pts',(-149.986931864858,-4.62144586080497,
132.487043361921));
#112001=CARTESIAN_POINT('Ctrl Pts',(-149.995057568965,-4.57244359970468,
132.621626840293));
#112002=CARTESIAN_POINT('Ctrl Pts',(-150.003183273071,-4.51761248540803,
132.753919749579));
#112003=CARTESIAN_POINT('Ctrl Pts',(-150.011308977178,-4.45720534180436,
132.883423772809));
#112004=CARTESIAN_POINT('Ctrl Pts',(-150.018465181474,-4.4040055384498,
132.997476319552));
#112005=CARTESIAN_POINT('Ctrl Pts',(-150.025621385771,-4.3464816776517,
133.109366018076));
#112006=CARTESIAN_POINT('Ctrl Pts',(-150.032777590067,-4.28483443271258,
133.218770886501));
#112007=CARTESIAN_POINT('Ctrl Pts',(-150.040551924186,-4.21786229778898,
133.337625794238));
#112008=CARTESIAN_POINT('Ctrl Pts',(-150.048326258306,-4.14583504957903,
133.453880287348));
#112009=CARTESIAN_POINT('Ctrl Pts',(-150.056100592425,-4.06897963459425,
133.567074463725));
#112010=CARTESIAN_POINT('Ctrl Pts',(-150.063865345372,-3.99221893703967,
133.680129138396));
#112011=CARTESIAN_POINT('Ctrl Pts',(-150.071630098319,-3.91064212950941,
133.790130680279));
#112012=CARTESIAN_POINT('Ctrl Pts',(-150.079394851266,-3.82452205894767,
133.896643606415));
#112013=CARTESIAN_POINT('Ctrl Pts',(-150.087151892151,-3.73848752405432,
134.00305074241));
#112014=CARTESIAN_POINT('Ctrl Pts',(-150.094908933036,-3.647918950298,134.105975855995));
#112015=CARTESIAN_POINT('Ctrl Pts',(-150.102665973921,-3.55313229525969,
134.205012607241));
#112016=CARTESIAN_POINT('Ctrl Pts',(-150.110417165162,-3.4584171195754,
134.303974674103));
#112017=CARTESIAN_POINT('Ctrl Pts',(-150.118168356402,-3.35949046320697,
134.399053933775));
#112018=CARTESIAN_POINT('Ctrl Pts',(-150.125919547642,-3.25670811288556,
134.489877586726));
#112019=CARTESIAN_POINT('Ctrl Pts',(-150.133667444419,-3.1539694478047,
134.580662637202));
#112020=CARTESIAN_POINT('Ctrl Pts',(-150.141415341196,-3.04737864052349,
134.667195420074));
#112021=CARTESIAN_POINT('Ctrl Pts',(-150.149163237973,-2.9373276795397,
134.74914060706));
#112022=CARTESIAN_POINT('Ctrl Pts',(-150.156909514057,-2.82729973884452,
134.831068652879));
#112023=CARTESIAN_POINT('Ctrl Pts',(-150.164655790142,-2.7138133974866,
134.908410778214));
#112024=CARTESIAN_POINT('Ctrl Pts',(-150.172402066226,-2.59729269088903,
134.980872767716));
#112025=CARTESIAN_POINT('Ctrl Pts',(-150.180148399491,-2.48077112416191,
135.053335292117));
#112026=CARTESIAN_POINT('Ctrl Pts',(-150.187894732757,-2.361215479502,135.120917402338));
#112027=CARTESIAN_POINT('Ctrl Pts',(-150.195641066022,-2.2390773128107,
135.183369164002));
#112028=CARTESIAN_POINT('Ctrl Pts',(-150.203389134025,-2.11691179412432,
135.245834911304));
#112029=CARTESIAN_POINT('Ctrl Pts',(-150.211137202028,-1.99216295061391,
135.303167845905));
#112030=CARTESIAN_POINT('Ctrl Pts',(-150.218885270031,-1.86530501431347,
135.355164971312));
#112031=CARTESIAN_POINT('Ctrl Pts',(-150.226641572773,-1.73831225188818,
135.407217359884));
#112032=CARTESIAN_POINT('Ctrl Pts',(-150.234397875515,-1.60920628123026,
135.453922462391));
#112033=CARTESIAN_POINT('Ctrl Pts',(-150.242154178257,-1.47847982919974,
135.495126062262));
#112034=CARTESIAN_POINT('Ctrl Pts',(-150.249914620771,-1.34768360452567,
135.536351653734));
#112035=CARTESIAN_POINT('Ctrl Pts',(-150.257675063286,-1.21526555238251,
135.572069789939));
#112036=CARTESIAN_POINT('Ctrl Pts',(-150.2654355058,-1.08173050927903,135.602177013365));
#112037=CARTESIAN_POINT('Ctrl Pts',(-150.273208406065,-0.947981103869675,
135.632332567578));
#112038=CARTESIAN_POINT('Ctrl Pts',(-150.280981306331,-0.813111509206581,
135.656859139894));
#112039=CARTESIAN_POINT('Ctrl Pts',(-150.288754206596,-0.677634526761312,
135.67570483766));
#112040=CARTESIAN_POINT('Ctrl Pts',(-150.296244542358,-0.547082473887059,
135.693865446841));
#112041=CARTESIAN_POINT('Ctrl Pts',(-150.303734878119,-0.415966733239075,
135.70675100877));
#112042=CARTESIAN_POINT('Ctrl Pts',(-150.31122521388,-0.284745934870738,
135.714360904233));
#112043=CARTESIAN_POINT('Ctrl Pts',(-150.318999548,-0.148549860035717,135.722259331197));
#112044=CARTESIAN_POINT('Ctrl Pts',(-150.326773882119,-0.0118091754647882,
135.72449916056));
#112045=CARTESIAN_POINT('Ctrl Pts',(-150.334548216238,0.12496652004272,
135.721022740528));
#112046=CARTESIAN_POINT('Ctrl Pts',(-150.342312969185,0.261573651729139,
135.717550604873));
#112047=CARTESIAN_POINT('Ctrl Pts',(-150.350077722132,0.398215321413812,
135.708376246648));
#112048=CARTESIAN_POINT('Ctrl Pts',(-150.357842475079,0.534377664511189,
135.693493830537));
#112049=CARTESIAN_POINT('Ctrl Pts',(-150.365599515964,0.67040476925022,
135.678626195851));
#112050=CARTESIAN_POINT('Ctrl Pts',(-150.373356556849,0.805953108674859,
135.658061827693));
#112051=CARTESIAN_POINT('Ctrl Pts',(-150.381113597734,0.940510034705003,
135.631846913468));
#112052=CARTESIAN_POINT('Ctrl Pts',(-150.388864788974,1.07496549030998,
135.605651768113));
#112053=CARTESIAN_POINT('Ctrl Pts',(-150.396615980214,1.20843063844032,
135.573814632655));
#112054=CARTESIAN_POINT('Ctrl Pts',(-150.404367171454,1.34039952087395,
135.536433333294));
#112055=CARTESIAN_POINT('Ctrl Pts',(-150.412115068232,1.4723123130127,135.499067921983));
#112056=CARTESIAN_POINT('Ctrl Pts',(-150.419862965009,1.6027297289385,135.456163139832));
#112057=CARTESIAN_POINT('Ctrl Pts',(-150.427610861786,1.73115776811343,
135.40786752474));
#112058=CARTESIAN_POINT('Ctrl Pts',(-150.43535713787,1.85955894291115,135.35958201205));
#112059=CARTESIAN_POINT('Ctrl Pts',(-150.443103413954,1.98597120295921,
135.305908046896));
#112060=CARTESIAN_POINT('Ctrl Pts',(-150.450849690038,2.1099178150502,135.247043351707));
#112061=CARTESIAN_POINT('Ctrl Pts',(-150.458596023303,2.23386534208677,
135.188178221992));
#112062=CARTESIAN_POINT('Ctrl Pts',(-150.466342356569,2.35534683168672,
135.124122453508));
#112063=CARTESIAN_POINT('Ctrl Pts',(-150.474088689834,2.47390792998701,
135.055120857388));
#112064=CARTESIAN_POINT('Ctrl Pts',(-150.481836757837,2.59249557922307,
134.986103808838));
#112065=CARTESIAN_POINT('Ctrl Pts',(-150.48958482584,2.7081611979325,134.912138925309));
#112066=CARTESIAN_POINT('Ctrl Pts',(-150.497332893843,2.82047766542043,
134.83351546708));
#112067=CARTESIAN_POINT('Ctrl Pts',(-150.505089196585,2.93291350418674,
134.754808446904));
#112068=CARTESIAN_POINT('Ctrl Pts',(-150.512845499327,3.04199276041207,
134.671433186061));
#112069=CARTESIAN_POINT('Ctrl Pts',(-150.520601802069,3.14731935642298,
134.583720871787));
#112070=CARTESIAN_POINT('Ctrl Pts',(-150.528362244583,3.25270216840951,
134.49596174281));
#112071=CARTESIAN_POINT('Ctrl Pts',(-150.536122687097,3.35432803966295,
134.403861210352));
#112072=CARTESIAN_POINT('Ctrl Pts',(-150.543883129611,3.45183705198367,
134.307788086353));
#112073=CARTESIAN_POINT('Ctrl Pts',(-150.551656029877,3.54950259442742,
134.211560737246));
#112074=CARTESIAN_POINT('Ctrl Pts',(-150.559428930142,3.64303780463344,
134.111348338984));
#112075=CARTESIAN_POINT('Ctrl Pts',(-150.567201830407,3.7321218421228,134.007554276721));
#112076=CARTESIAN_POINT('Ctrl Pts',(-150.574692166169,3.81796745045954,
133.907533390064));
#112077=CARTESIAN_POINT('Ctrl Pts',(-150.582182501931,3.89967969915637,
133.804186965027));
#112078=CARTESIAN_POINT('Ctrl Pts',(-150.589672837693,3.97701016650376,
133.697900525365));
#112079=CARTESIAN_POINT('Ctrl Pts',(-150.597447171812,4.05727264202506,
133.587584203037));
#112080=CARTESIAN_POINT('Ctrl Pts',(-150.605221505931,4.13306875399035,
133.473751074893));
#112081=CARTESIAN_POINT('Ctrl Pts',(-150.612995840051,4.20407454771377,
133.35679871863));
#112082=CARTESIAN_POINT('Ctrl Pts',(-150.620760592998,4.2749928331424,133.239990495695));
#112083=CARTESIAN_POINT('Ctrl Pts',(-150.628525345945,4.34113234585888,
133.12007102438));
#112084=CARTESIAN_POINT('Ctrl Pts',(-150.636290098892,4.40221042008673,
132.997469479383));
#112085=CARTESIAN_POINT('Ctrl Pts',(-150.644047139777,4.46322783071036,
132.874989703969));
#112086=CARTESIAN_POINT('Ctrl Pts',(-150.651804180662,4.51919363377727,
132.749833503781));
#112087=CARTESIAN_POINT('Ctrl Pts',(-150.659561221547,4.56986958924957,
132.622457149588));
#112088=CARTESIAN_POINT('Ctrl Pts',(-150.667312412787,4.62050732958944,
132.495176850896));
#112089=CARTESIAN_POINT('Ctrl Pts',(-150.675063604027,4.66586301848597,
132.365680092465));
#112090=CARTESIAN_POINT('Ctrl Pts',(-150.682814795267,4.7057454771148,132.234445428727));
#112091=CARTESIAN_POINT('Ctrl Pts',(-150.690562692044,4.74561098463498,
132.103266543222));
#112092=CARTESIAN_POINT('Ctrl Pts',(-150.698310588821,4.78000777521548,
131.970351594831));
#112093=CARTESIAN_POINT('Ctrl Pts',(-150.706058485598,4.8087937986393,131.836196488559));
#112094=CARTESIAN_POINT('Ctrl Pts',(-150.713804761682,4.83757380064758,
131.702069444644));
#112095=CARTESIAN_POINT('Ctrl Pts',(-150.721551037766,4.86074528798491,
131.566703140859));
#112096=CARTESIAN_POINT('Ctrl Pts',(-150.72929731385,4.87821692418744,131.430605540157));
#112097=CARTESIAN_POINT('Ctrl Pts',(-150.737043647116,4.89568868936159,
131.294506934814));
#112098=CARTESIAN_POINT('Ctrl Pts',(-150.744789980381,4.9074604696614,131.157677409564));
#112099=CARTESIAN_POINT('Ctrl Pts',(-150.752536313647,4.9134926422659,131.020631551579));
#112100=CARTESIAN_POINT('Ctrl Pts',(-150.760284381649,4.91952616573362,
130.883555003124));
#112101=CARTESIAN_POINT('Ctrl Pts',(-150.768032449652,4.91981750662894,
130.746262416044));
#112102=CARTESIAN_POINT('Ctrl Pts',(-150.775780517655,4.91437915864869,
130.609269491321));
#112103=CARTESIAN_POINT('Ctrl Pts',(-150.783536820397,4.90893503072747,
130.472130968888));
#112104=CARTESIAN_POINT('Ctrl Pts',(-150.791293123139,4.89774906486869,
130.335293136301));
#112105=CARTESIAN_POINT('Ctrl Pts',(-150.799049425881,4.8808858086179,130.199268239716));
#112106=CARTESIAN_POINT('Ctrl Pts',(-150.806809868395,4.86401355193951,
130.063170742548));
#112107=CARTESIAN_POINT('Ctrl Pts',(-150.814570310909,4.84145803132284,
129.927887431394));
#112108=CARTESIAN_POINT('Ctrl Pts',(-150.822330753423,4.81333499411985,
129.793920467492));
#112109=CARTESIAN_POINT('Ctrl Pts',(-150.830103653689,4.78516681132089,
129.659738447927));
#112110=CARTESIAN_POINT('Ctrl Pts',(-150.837876553954,4.75141334834129,
129.526877377441));
#112111=CARTESIAN_POINT('Ctrl Pts',(-150.84564945422,4.71224056242093,129.395825227746));
#112112=CARTESIAN_POINT('Ctrl Pts',(-150.853139789982,4.6744918059379,129.269537153789));
#112113=CARTESIAN_POINT('Ctrl Pts',(-150.860630125744,4.63171099798405,
129.144929057636));
#112114=CARTESIAN_POINT('Ctrl Pts',(-150.868120461506,4.58408821260883,
129.022418328511));
#112115=CARTESIAN_POINT('Ctrl Pts',(-150.875894795626,4.53465979485293,
128.895262567859));
#112116=CARTESIAN_POINT('Ctrl Pts',(-150.883669129745,4.47985841016305,
128.769963565914));
#112117=CARTESIAN_POINT('Ctrl Pts',(-150.891443463864,4.41984344649703,
128.647008775386));
#112118=CARTESIAN_POINT('Ctrl Pts',(-150.899208216811,4.35990244591004,
128.524205515648));
#112119=CARTESIAN_POINT('Ctrl Pts',(-150.906972969758,4.29476082056689,
128.403741066989));
#112120=CARTESIAN_POINT('Ctrl Pts',(-150.914737722705,4.22462685953976,
128.28608522354));
#112121=CARTESIAN_POINT('Ctrl Pts',(-150.92249476359,4.15456255655145,128.168546237534));
#112122=CARTESIAN_POINT('Ctrl Pts',(-150.930251804475,4.07951598432393,
128.053810639068));
#112123=CARTESIAN_POINT('Ctrl Pts',(-150.93800884536,3.99974224181769,127.94232549173));
#112124=CARTESIAN_POINT('Ctrl Pts',(-150.9457600366,3.9200286573109,127.830924416208));
#112125=CARTESIAN_POINT('Ctrl Pts',(-150.95351122784,3.83559522462584,127.722769229533));
#112126=CARTESIAN_POINT('Ctrl Pts',(-150.96126241908,3.74674122833586,127.618279446223));
#112127=CARTESIAN_POINT('Ctrl Pts',(-150.969010315857,3.65792499736493,
127.513834073858));
#112128=CARTESIAN_POINT('Ctrl Pts',(-150.976758212634,3.56469219243346,
127.413051303542));
#112129=CARTESIAN_POINT('Ctrl Pts',(-150.984506109412,3.46738325085526,
127.316318694912));
#112130=CARTESIAN_POINT('Ctrl Pts',(-150.992252385496,3.3700946642099,127.21960632066));
#112131=CARTESIAN_POINT('Ctrl Pts',(-150.99999866158,3.2687319139637,127.126942698411));
#112132=CARTESIAN_POINT('Ctrl Pts',(-151.007744937664,3.16367299414463,
127.038679238503));
#112133=CARTESIAN_POINT('Ctrl Pts',(-151.015491270929,3.05861329880433,
126.950415127055));
#112134=CARTESIAN_POINT('Ctrl Pts',(-151.023237604195,2.9498576787917,126.86655149425));
#112135=CARTESIAN_POINT('Ctrl Pts',(-151.03098393746,2.83781765376463,126.787399822826));
#112136=CARTESIAN_POINT('Ctrl Pts',(-151.038732005463,2.72575253815063,
126.708230425933));
#112137=CARTESIAN_POINT('Ctrl Pts',(-151.046480073466,2.61040187318124,
126.633775315712));
#112138=CARTESIAN_POINT('Ctrl Pts',(-151.054228141469,2.49220628584793,
126.564302729839));
#112139=CARTESIAN_POINT('Ctrl Pts',(-151.061984444211,2.37388507883801,
126.494756307675));
#112140=CARTESIAN_POINT('Ctrl Pts',(-151.069740746953,2.25271324705414,
126.430203186592));
#112141=CARTESIAN_POINT('Ctrl Pts',(-151.077497049695,2.12915664721986,
126.370865942471));
#112142=CARTESIAN_POINT('Ctrl Pts',(-151.085257492209,2.00553410150769,
126.311497028276));
#112143=CARTESIAN_POINT('Ctrl Pts',(-151.093017934723,1.8795246105684,126.257349692419));
#112144=CARTESIAN_POINT('Ctrl Pts',(-151.100778377237,1.75161322114368,
126.20859798379));
#112145=CARTESIAN_POINT('Ctrl Pts',(-151.108551277503,1.62349649700157,
126.15976801459));
#112146=CARTESIAN_POINT('Ctrl Pts',(-151.116324177768,1.49347214436577,
126.116351105033));
#112147=CARTESIAN_POINT('Ctrl Pts',(-151.124097078034,1.362040411599,126.078471391222));
#112148=CARTESIAN_POINT('Ctrl Pts',(-151.131587413796,1.23538655337593,
126.041968700422));
#112149=CARTESIAN_POINT('Ctrl Pts',(-151.139077749557,1.10742616132385,
126.010607686078));
#112150=CARTESIAN_POINT('Ctrl Pts',(-151.146568085319,0.978613136485346,
125.984454042579));
#112151=CARTESIAN_POINT('Ctrl Pts',(-151.154342419439,0.844916126655815,
125.957308775738));
#112152=CARTESIAN_POINT('Ctrl Pts',(-151.162116753558,0.709877040642642,
125.935687561584));
#112153=CARTESIAN_POINT('Ctrl Pts',(-151.169891087677,0.573992139300663,
125.91971978261));
#112154=CARTESIAN_POINT('Ctrl Pts',(-151.177655840624,0.438274703954835,
125.903771682496));
#112155=CARTESIAN_POINT('Ctrl Pts',(-151.185420593571,0.301713911895122,
125.893463199796));
#112156=CARTESIAN_POINT('Ctrl Pts',(-151.193185346518,0.164817599560541,
125.888873030218));
#112157=CARTESIAN_POINT('Ctrl Pts',(-151.200942387404,0.0280572545732683,
125.88428741966));
#112158=CARTESIAN_POINT('Ctrl Pts',(-151.208699428289,-0.10903755930222,
125.885408832761));
#112159=CARTESIAN_POINT('Ctrl Pts',(-151.216456469174,-0.24595282758949,
125.89226429633));
#112160=CARTESIAN_POINT('Ctrl Pts',(-151.224207660414,-0.382764847007342,
125.89911459014));
#112161=CARTESIAN_POINT('Ctrl Pts',(-151.231958851654,-0.519397201439868,
125.911690308102));
#112162=CARTESIAN_POINT('Ctrl Pts',(-151.239710042894,-0.655335170818045,
125.929966411473));
#112163=CARTESIAN_POINT('Ctrl Pts',(-151.247457939671,-0.791215362933158,
125.948234747013));
#112164=CARTESIAN_POINT('Ctrl Pts',(-151.255205836449,-0.92640137032155,
125.972198597181));
#112165=CARTESIAN_POINT('Ctrl Pts',(-151.262953733226,-1.06038311339868,
126.001781027875));
#112166=CARTESIAN_POINT('Ctrl Pts',(-151.27070000931,-1.19433683038348,
126.031357270562));
#112167=CARTESIAN_POINT('Ctrl Pts',(-151.278446285394,-1.32708640258374,
126.066549671827));
#112168=CARTESIAN_POINT('Ctrl Pts',(-151.286192561478,-1.45813186352537,
126.10723016046));
#112169=CARTESIAN_POINT('Ctrl Pts',(-151.293938894744,-1.58917829181429,
126.147910949387));
#112170=CARTESIAN_POINT('Ctrl Pts',(-151.301685228009,-1.71852021035558,
126.19407979061));
#112171=CARTESIAN_POINT('Ctrl Pts',(-151.309431561275,-1.84567312347419,
126.245558825013));
#112172=CARTESIAN_POINT('Ctrl Pts',(-151.317179629278,-1.97285451160694,
126.297049387789));
#112173=CARTESIAN_POINT('Ctrl Pts',(-151.324927697281,-2.09784555652837,
126.353852363388));
#112174=CARTESIAN_POINT('Ctrl Pts',(-151.332675765284,-2.22018241263168,
126.415742028859));
#112175=CARTESIAN_POINT('Ctrl Pts',(-151.340432068026,-2.34264928980066,
126.477697471404));
#112176=CARTESIAN_POINT('Ctrl Pts',(-151.348188370768,-2.46245599367338,
126.544750226506));
#112177=CARTESIAN_POINT('Ctrl Pts',(-151.35594467351,-2.57916345791894,
126.616628663413));
#112178=CARTESIAN_POINT('Ctrl Pts',(-151.363705116024,-2.69593321245216,
126.688545464005));
#112179=CARTESIAN_POINT('Ctrl Pts',(-151.371465558538,-2.8096001074463,
126.765292859855));
#112180=CARTESIAN_POINT('Ctrl Pts',(-151.379226001052,-2.91975553102968,
126.846556845078));
#112181=CARTESIAN_POINT('Ctrl Pts',(-151.386998901318,-3.03008778587843,
126.927951282464));
#112182=CARTESIAN_POINT('Ctrl Pts',(-151.394771801583,-3.13689700014094,
127.013876552687));
#112183=CARTESIAN_POINT('Ctrl Pts',(-151.402544701849,-3.23980833813851,
127.103978881227));
#112184=CARTESIAN_POINT('Ctrl Pts',(-151.41003503761,-3.33897858977014,
127.190805763161));
#112185=CARTESIAN_POINT('Ctrl Pts',(-151.417525373371,-3.43452921682893,
127.281511070724));
#112186=CARTESIAN_POINT('Ctrl Pts',(-151.425015709133,-3.52615960416304,
127.375748433537));
#112187=CARTESIAN_POINT('Ctrl Pts',(-151.432687175097,-3.62000578411265,
127.472264630465));
#112188=CARTESIAN_POINT('Ctrl Pts',(-151.440358641061,-3.71005408140359,
127.572809541388));
#112189=CARTESIAN_POINT('Ctrl Pts',(-151.448030107026,-3.79593171616864,
127.677047798438));
#112190=CARTESIAN_POINT('Ctrl Pts',(-151.455692550273,-3.88170834681902,
127.781163456711));
#112191=CARTESIAN_POINT('Ctrl Pts',(-151.46335499352,-3.96332381434113,
127.888963517903));
#112192=CARTESIAN_POINT('Ctrl Pts',(-151.471017436767,-4.04044119313304,
128.000074963904));
#112193=CARTESIAN_POINT('Ctrl Pts',(-151.478672633333,-4.1174856389195,
128.111081327343));
#112194=CARTESIAN_POINT('Ctrl Pts',(-151.486327829899,-4.19004022802817,
128.225392519584));
#112195=CARTESIAN_POINT('Ctrl Pts',(-151.493983026465,-4.2578078167015,
128.342601966005));
#112196=CARTESIAN_POINT('Ctrl Pts',(-151.501632321317,-4.32552316047735,
128.459721050712));
#112197=CARTESIAN_POINT('Ctrl Pts',(-151.509281616169,-4.38845864790343,
128.579733596101));
#112198=CARTESIAN_POINT('Ctrl Pts',(-151.516930911021,-4.4463604043477,
128.702204054141));
#112199=CARTESIAN_POINT('Ctrl Pts',(-151.524576832615,-4.50423662673283,
128.824620504012));
#112200=CARTESIAN_POINT('Ctrl Pts',(-151.532222754209,-4.5570833629016,
128.949492347286));
#112201=CARTESIAN_POINT('Ctrl Pts',(-151.539868675803,-4.60469284971006,
129.07635980092));
#112202=CARTESIAN_POINT('Ctrl Pts',(-151.547513563034,-4.65229589576303,
129.203210091541));
#112203=CARTESIAN_POINT('Ctrl Pts',(-151.555158450265,-4.69466295854988,
129.332055080029));
#112204=CARTESIAN_POINT('Ctrl Pts',(-151.562803337496,-4.73163472374242,
129.462415796206));
#112205=CARTESIAN_POINT('Ctrl Pts',(-151.565142512869,-4.74294730953171,
129.502303445));
#112206=CARTESIAN_POINT('Ctrl Pts',(-151.567481688242,-4.75375512073537,
129.542332885786));
#112207=CARTESIAN_POINT('Ctrl Pts',(-151.569820863616,-4.76405452823393,
129.582490119308));
#112208=CARTESIAN_POINT('Origin',(213.235140564004,0.,130.804360617566));
#112209=CARTESIAN_POINT('',(-153.665379263862,-4.76405452823391,129.582490119308));
#112210=CARTESIAN_POINT('',(-153.319765814746,-4.76405452823394,129.582490119308));
#112211=CARTESIAN_POINT('',(213.235140564004,-4.76405452823405,129.582490119308));
#112212=CARTESIAN_POINT('',(-151.985140564048,-4.91824942752548,130.801987614138));
#112213=CARTESIAN_POINT('Ctrl Pts',(-151.985140564047,-4.91824942752548,
130.801987614138));
#112214=CARTESIAN_POINT('Ctrl Pts',(-151.992825592928,-4.91831456258477,
130.936985509313));
#112215=CARTESIAN_POINT('Ctrl Pts',(-152.000510621809,-4.91281729657113,
131.07221008295));
#112216=CARTESIAN_POINT('Ctrl Pts',(-152.00819565069,-4.90172794900123,
131.207158552616));
#112217=CARTESIAN_POINT('Ctrl Pts',(-152.015871793966,-4.89065142318675,
131.341950991797));
#112218=CARTESIAN_POINT('Ctrl Pts',(-152.023547937242,-4.87399570806901,
131.476467566512));
#112219=CARTESIAN_POINT('Ctrl Pts',(-152.031224080518,-4.85178311540639,
131.610204066108));
#112220=CARTESIAN_POINT('Ctrl Pts',(-152.038893284541,-4.82959060298433,
131.743819667566));
#112221=CARTESIAN_POINT('Ctrl Pts',(-152.046562488563,-4.80185127147943,
131.876656204003));
#112222=CARTESIAN_POINT('Ctrl Pts',(-152.054231692586,-4.76863931723582,
132.008213650379));
#112223=CARTESIAN_POINT('Ctrl Pts',(-152.062004104746,-4.73498041388242,
132.141541528061));
#112224=CARTESIAN_POINT('Ctrl Pts',(-152.069776516905,-4.69570054335466,
132.27355522112));
#112225=CARTESIAN_POINT('Ctrl Pts',(-152.077548929064,-4.65093081976605,
132.40374348988));
#112226=CARTESIAN_POINT('Ctrl Pts',(-152.085210972649,-4.60679682810612,
132.532083079833));
#112227=CARTESIAN_POINT('Ctrl Pts',(-152.092873016234,-4.55732801938075,
132.658648361305));
#112228=CARTESIAN_POINT('Ctrl Pts',(-152.100535059819,-4.50270033536339,
132.782964355665));
#112229=CARTESIAN_POINT('Ctrl Pts',(-152.108196415792,-4.4480775537778,
132.907269193581));
#112230=CARTESIAN_POINT('Ctrl Pts',(-152.115857771765,-4.38829697860385,
133.029324779174));
#112231=CARTESIAN_POINT('Ctrl Pts',(-152.123519127738,-4.32358248358636,
133.148676630847));
#112232=CARTESIAN_POINT('Ctrl Pts',(-152.131181544043,-4.25885903208279,
133.268045000816));
#112233=CARTESIAN_POINT('Ctrl Pts',(-152.138843960347,-4.18920049385073,
133.384708540768));
#112234=CARTESIAN_POINT('Ctrl Pts',(-152.146506376652,-4.11487616965667,
133.498238337674));
#112235=CARTESIAN_POINT('Ctrl Pts',(-152.154361643965,-4.03868121871575,
133.614625501625));
#112236=CARTESIAN_POINT('Ctrl Pts',(-152.162216911279,-3.95758274152315,
133.727718709357));
#112237=CARTESIAN_POINT('Ctrl Pts',(-152.170072178592,-3.87191670395517,
133.837089438304));
#112238=CARTESIAN_POINT('Ctrl Pts',(-152.177746001913,-3.78822941354097,
133.943933879998));
#112239=CARTESIAN_POINT('Ctrl Pts',(-152.185419825234,-3.70018357625764,
134.047225667719));
#112240=CARTESIAN_POINT('Ctrl Pts',(-152.193093648556,-3.60813113273665,
134.146601301819));
#112241=CARTESIAN_POINT('Ctrl Pts',(-152.201039637865,-3.51281388323865,
134.249501472061));
#112242=CARTESIAN_POINT('Ctrl Pts',(-152.208985627174,-3.41320092224242,
134.348202239315));
#112243=CARTESIAN_POINT('Ctrl Pts',(-152.216931616484,-3.30972107970913,
134.442344872209));
#112244=CARTESIAN_POINT('Ctrl Pts',(-152.224877605793,-3.2062412371761,
134.536487505102));
#112245=CARTESIAN_POINT('Ctrl Pts',(-152.232823595102,-3.09889491960027,
134.626071759748));
#112246=CARTESIAN_POINT('Ctrl Pts',(-152.240769584411,-2.98814391797463,
134.710788523975));
#112247=CARTESIAN_POINT('Ctrl Pts',(-152.24854391853,-2.87978544212651,
134.793675173447));
#112248=CARTESIAN_POINT('Ctrl Pts',(-152.256318252649,-2.76780399280436,
134.872181139208));
#112249=CARTESIAN_POINT('Ctrl Pts',(-152.264092586769,-2.65258925919592,
134.945973019095));
#112250=CARTESIAN_POINT('Ctrl Pts',(-152.271857339716,-2.53751651744961,
135.019673957085));
#112251=CARTESIAN_POINT('Ctrl Pts',(-152.279622092663,-2.41921874591742,
135.088672159913));
#112252=CARTESIAN_POINT('Ctrl Pts',(-152.28738684561,-2.29811821250707,
135.152674744195));
#112253=CARTESIAN_POINT('Ctrl Pts',(-152.295143886495,-2.17713795785372,
135.216613760208));
#112254=CARTESIAN_POINT('Ctrl Pts',(-152.30290092738,-2.05336082451832,
135.275566850218));
#112255=CARTESIAN_POINT('Ctrl Pts',(-152.310657968265,-1.92723723477123,
135.329284893552));
#112256=CARTESIAN_POINT('Ctrl Pts',(-152.318409159505,-1.80120875580408,
135.382962427693));
#112257=CARTESIAN_POINT('Ctrl Pts',(-152.326160350745,-1.67283770071316,
135.431412620412));
#112258=CARTESIAN_POINT('Ctrl Pts',(-152.333911541985,-1.54259789835482,
135.474432863955));
#112259=CARTESIAN_POINT('Ctrl Pts',(-152.341659438762,-1.41241345138656,
135.517434822746));
#112260=CARTESIAN_POINT('Ctrl Pts',(-152.349407335539,-1.28036220734792,
135.555011300176));
#112261=CARTESIAN_POINT('Ctrl Pts',(-152.357155232316,-1.14693651962243,
135.58700838658));
#112262=CARTESIAN_POINT('Ctrl Pts',(-152.364901508401,-1.01353874167486,
135.618998779884));
#112263=CARTESIAN_POINT('Ctrl Pts',(-152.372647784485,-0.878767471846586,
135.64541201245));
#112264=CARTESIAN_POINT('Ctrl Pts',(-152.380394060569,-0.743128334985456,
135.666144584408));
#112265=CARTESIAN_POINT('Ctrl Pts',(-152.388140393834,-0.607488196866845,
135.686877309409));
#112266=CARTESIAN_POINT('Ctrl Pts',(-152.395886727099,-0.47098056540843,
135.701929231052));
#112267=CARTESIAN_POINT('Ctrl Pts',(-152.403633060365,-0.334118928753958,
135.711248389255));
#112268=CARTESIAN_POINT('Ctrl Pts',(-152.411381128368,-0.197226642884703,
135.720569634418));
#112269=CARTESIAN_POINT('Ctrl Pts',(-152.419129196371,-0.059980584054659,
135.724155534947));
#112270=CARTESIAN_POINT('Ctrl Pts',(-152.426877264374,0.077103395447118,
135.722006205539));
#112271=CARTESIAN_POINT('Ctrl Pts',(-152.434633567116,0.214333069433443,
135.719854591798));
#112272=CARTESIAN_POINT('Ctrl Pts',(-152.442389869858,0.351399928443426,
135.7119555779));
#112273=CARTESIAN_POINT('Ctrl Pts',(-152.450146172599,0.48779032487234,
135.698361400306));
#112274=CARTESIAN_POINT('Ctrl Pts',(-152.457906615114,0.624253516962835,
135.684759967091));
#112275=CARTESIAN_POINT('Ctrl Pts',(-152.465667057628,0.760039140168273,
135.665457368357));
#112276=CARTESIAN_POINT('Ctrl Pts',(-152.473427500142,0.894642400244366,
135.64055726764));
#112277=CARTESIAN_POINT('Ctrl Pts',(-152.481200400407,1.02946173742268,
135.61561719507));
#112278=CARTESIAN_POINT('Ctrl Pts',(-152.488973300673,1.16309453724599,
135.585061751607));
#112279=CARTESIAN_POINT('Ctrl Pts',(-152.496746200938,1.29504898601056,
135.549045136724));
#112280=CARTESIAN_POINT('Ctrl Pts',(-152.5042365367,1.42220655818827,135.514337816511));
#112281=CARTESIAN_POINT('Ctrl Pts',(-152.511726872462,1.54780539171509,
135.4745595791));
#112282=CARTESIAN_POINT('Ctrl Pts',(-152.519217208224,1.6714236563107,135.429890427612));
#112283=CARTESIAN_POINT('Ctrl Pts',(-152.526991542343,1.79972894498233,
135.383527631668));
#112284=CARTESIAN_POINT('Ctrl Pts',(-152.534765876462,1.92630694603927,
135.331748858983));
#112285=CARTESIAN_POINT('Ctrl Pts',(-152.542540210581,2.05066652227431,
135.274701754093));
#112286=CARTESIAN_POINT('Ctrl Pts',(-152.550304963528,2.17487283644597,
135.217724954661));
#112287=CARTESIAN_POINT('Ctrl Pts',(-152.558069716475,2.2968658137131,135.155492903108));
#112288=CARTESIAN_POINT('Ctrl Pts',(-152.565834469423,2.41617079687032,
135.088202554759));
#112289=CARTESIAN_POINT('Ctrl Pts',(-152.573591510307,2.53535728463604,
135.020979040133));
#112290=CARTESIAN_POINT('Ctrl Pts',(-152.581348551192,2.65186075289129,
134.948707417466));
#112291=CARTESIAN_POINT('Ctrl Pts',(-152.589105592077,2.76522814512081,
134.871631983965));
#112292=CARTESIAN_POINT('Ctrl Pts',(-152.596856783317,2.87851004611781,
134.794614673648));
#112293=CARTESIAN_POINT('Ctrl Pts',(-152.604607974558,2.98866025634705,
134.71280098197));
#112294=CARTESIAN_POINT('Ctrl Pts',(-152.612359165798,3.09525220009408,
134.626480040126));
#112295=CARTESIAN_POINT('Ctrl Pts',(-152.620107062575,3.20179883942202,
134.540195786985));
#112296=CARTESIAN_POINT('Ctrl Pts',(-152.627854959352,3.30478991703817,
134.449408339397));
#112297=CARTESIAN_POINT('Ctrl Pts',(-152.635602856129,3.40382981535404,
134.354448736276));
#112298=CARTESIAN_POINT('Ctrl Pts',(-152.643349132213,3.50284899665824,
134.259508996657));
#112299=CARTESIAN_POINT('Ctrl Pts',(-152.651095408297,3.59791836059156,
134.160399107811));
#112300=CARTESIAN_POINT('Ctrl Pts',(-152.658841684381,3.68867752720004,
134.057488522034));
#112301=CARTESIAN_POINT('Ctrl Pts',(-152.666588017647,3.77943736377219,
133.954577176595));
#112302=CARTESIAN_POINT('Ctrl Pts',(-152.674334350912,3.8658866809311,133.847865371464));
#112303=CARTESIAN_POINT('Ctrl Pts',(-152.682080684177,3.94770421030237,
133.737757033065));
#112304=CARTESIAN_POINT('Ctrl Pts',(-152.68982875218,4.02954006214171,133.627624036667));
#112305=CARTESIAN_POINT('Ctrl Pts',(-152.697576820183,4.10674182903347,
133.51409330719));
#112306=CARTESIAN_POINT('Ctrl Pts',(-152.705324888186,4.17903077671307,
133.397598907771));
#112307=CARTESIAN_POINT('Ctrl Pts',(-152.713081190928,4.25139655394662,
133.280980696717));
#112308=CARTESIAN_POINT('Ctrl Pts',(-152.72083749367,4.31883887518129,133.161392856341));
#112309=CARTESIAN_POINT('Ctrl Pts',(-152.728593796412,4.38112404935522,
133.039295768004));
#112310=CARTESIAN_POINT('Ctrl Pts',(-152.736354238926,4.44344246700198,
132.917133512774));
#112311=CARTESIAN_POINT('Ctrl Pts',(-152.74411468144,4.50059809010008,132.792459696215));
#112312=CARTESIAN_POINT('Ctrl Pts',(-152.751875123954,4.55240528009769,
132.665755048695));
#112313=CARTESIAN_POINT('Ctrl Pts',(-152.75964802422,4.60429563559604,132.538847003626));
#112314=CARTESIAN_POINT('Ctrl Pts',(-152.767420924485,4.65082026810285,
132.409901980907));
#112315=CARTESIAN_POINT('Ctrl Pts',(-152.775193824751,4.69184307268158,
132.279417105918));
#112316=CARTESIAN_POINT('Ctrl Pts',(-152.782684160513,4.73137459498434,
132.153675684804));
#112317=CARTESIAN_POINT('Ctrl Pts',(-152.790174496275,4.76579727471635,
132.026504720053));
#112318=CARTESIAN_POINT('Ctrl Pts',(-152.797664832037,4.79503454403202,
131.89835640551));
#112319=CARTESIAN_POINT('Ctrl Pts',(-152.805439166156,4.82538035329972,
131.765349308674));
#112320=CARTESIAN_POINT('Ctrl Pts',(-152.813213500275,4.85023590679922,
131.630867960106));
#112321=CARTESIAN_POINT('Ctrl Pts',(-152.820987834394,4.86945995040386,
131.495405372928));
#112322=CARTESIAN_POINT('Ctrl Pts',(-152.828752587341,4.88866030209292,
131.360109731281));
#112323=CARTESIAN_POINT('Ctrl Pts',(-152.836517340288,4.90224289867473,
131.223835640518));
#112324=CARTESIAN_POINT('Ctrl Pts',(-152.844282093236,4.91011688042973,
131.087088902354));
#112325=CARTESIAN_POINT('Ctrl Pts',(-152.852039134121,4.91798304163505,
130.950477982978));
#112326=CARTESIAN_POINT('Ctrl Pts',(-152.859796175006,4.92015184899466,
130.813395738201));
#112327=CARTESIAN_POINT('Ctrl Pts',(-152.867553215891,4.91658394855288,
130.676355385906));
#112328=CARTESIAN_POINT('Ctrl Pts',(-152.875304407131,4.91301873869258,
130.539418376808));
#112329=CARTESIAN_POINT('Ctrl Pts',(-152.883055598371,4.90372544199692,
130.402523586564));
#112330=CARTESIAN_POINT('Ctrl Pts',(-152.890806789611,4.8887167381356,130.266186187875));
#112331=CARTESIAN_POINT('Ctrl Pts',(-152.898554686388,4.87371441337377,
130.129906736218));
#112332=CARTESIAN_POINT('Ctrl Pts',(-152.906302583165,4.85300155563226,
129.994184592733));
#112333=CARTESIAN_POINT('Ctrl Pts',(-152.914050479942,4.82664283635449,
129.85953153632));
#112334=CARTESIAN_POINT('Ctrl Pts',(-152.921796756026,4.80028963075256,
129.724906646424));
#112335=CARTESIAN_POINT('Ctrl Pts',(-152.92954303211,4.7682929877327,129.591350782228));
#112336=CARTESIAN_POINT('Ctrl Pts',(-152.937289308194,4.73076894380699,
129.459366839584));
#112337=CARTESIAN_POINT('Ctrl Pts',(-152.94503564146,4.69324462288736,129.327381922664));
#112338=CARTESIAN_POINT('Ctrl Pts',(-152.952781974725,4.65019292656167,
129.196969326513));
#112339=CARTESIAN_POINT('Ctrl Pts',(-152.960528307991,4.60178003616608,
129.06861767541));
#112340=CARTESIAN_POINT('Ctrl Pts',(-152.968276375994,4.55335630403916,
128.940237280845));
#112341=CARTESIAN_POINT('Ctrl Pts',(-152.976024443997,4.49956912673542,
128.813919115466));
#112342=CARTESIAN_POINT('Ctrl Pts',(-152.983772512,4.44063303118699,128.690132308033));
#112343=CARTESIAN_POINT('Ctrl Pts',(-152.991528814741,4.38163429765495,
128.566213938508));
#112344=CARTESIAN_POINT('Ctrl Pts',(-152.999285117483,4.31747588264024,
128.444832654769));
#112345=CARTESIAN_POINT('Ctrl Pts',(-153.007041420225,4.24841880229327,
128.326433915095));
#112346=CARTESIAN_POINT('Ctrl Pts',(-153.014801862739,4.17932486410306,
128.207971982448));
#112347=CARTESIAN_POINT('Ctrl Pts',(-153.022562305254,4.1053272616742,128.092496094826));
#112348=CARTESIAN_POINT('Ctrl Pts',(-153.030322747768,4.02673010490752,
127.980422281707));
#112349=CARTESIAN_POINT('Ctrl Pts',(-153.038095648033,3.94800677700748,
127.868168557755));
#112350=CARTESIAN_POINT('Ctrl Pts',(-153.045868548299,3.86466937777846,
127.759328132344));
#112351=CARTESIAN_POINT('Ctrl Pts',(-153.053641448564,3.77706258483867,
127.654284222824));
#112352=CARTESIAN_POINT('Ctrl Pts',(-153.061131784326,3.69264051949069,
127.553058924005));
#112353=CARTESIAN_POINT('Ctrl Pts',(-153.068622120088,3.60425428439401,
127.455359135876));
#112354=CARTESIAN_POINT('Ctrl Pts',(-153.07611245585,3.51224293624735,127.361493698953));
#112355=CARTESIAN_POINT('Ctrl Pts',(-153.083886789969,3.41674294986907,
127.264069325459));
#112356=CARTESIAN_POINT('Ctrl Pts',(-153.091661124088,3.31703501640613,
127.170467190563));
#112357=CARTESIAN_POINT('Ctrl Pts',(-153.099435458207,3.21345757045418,
127.081072620998));
#112358=CARTESIAN_POINT('Ctrl Pts',(-153.107200211154,3.11000777444794,
126.99178822225));
#112359=CARTESIAN_POINT('Ctrl Pts',(-153.114964964101,3.00269824763277,
126.90670132433));
#112360=CARTESIAN_POINT('Ctrl Pts',(-153.122729717049,2.89190542341845,
126.826161768275));
#112361=CARTESIAN_POINT('Ctrl Pts',(-153.130486757934,2.78122264019844,
126.745702205241));
#112362=CARTESIAN_POINT('Ctrl Pts',(-153.138243798819,2.66706375865052,
126.669781224464));
#112363=CARTESIAN_POINT('Ctrl Pts',(-153.146000839704,2.5498392917413,126.598709342342));
#112364=CARTESIAN_POINT('Ctrl Pts',(-153.153752030944,2.43270322471429,
126.527691056079));
#112365=CARTESIAN_POINT('Ctrl Pts',(-153.161503222184,2.31250650675344,
126.46151479182));
#112366=CARTESIAN_POINT('Ctrl Pts',(-153.169254413424,2.18968942091553,
126.40044834523));
#112367=CARTESIAN_POINT('Ctrl Pts',(-153.177002310201,2.06692453561584,
126.339407853509));
#112368=CARTESIAN_POINT('Ctrl Pts',(-153.184750206978,1.94154184690188,
126.283473033594));
#112369=CARTESIAN_POINT('Ctrl Pts',(-153.192498103755,1.81400688535183,
126.232866104565));
#112370=CARTESIAN_POINT('Ctrl Pts',(-153.20024437984,1.68649860136605,126.182269761415));
#112371=CARTESIAN_POINT('Ctrl Pts',(-153.207990655924,1.55683930320513,
126.136999236498));
#112372=CARTESIAN_POINT('Ctrl Pts',(-153.215736932008,1.42551481196126,
126.097228732503));
#112373=CARTESIAN_POINT('Ctrl Pts',(-153.223483265273,1.29418935131037,
126.057457934931));
#112374=CARTESIAN_POINT('Ctrl Pts',(-153.231229598538,1.16119904723143,
126.023187352613));
#112375=CARTESIAN_POINT('Ctrl Pts',(-153.238975931804,1.02704481824168,
125.994541285842));
#112376=CARTESIAN_POINT('Ctrl Pts',(-153.246723999807,0.8928605463416,125.965888803984));
#112377=CARTESIAN_POINT('Ctrl Pts',(-153.25447206781,0.757512213134137,
125.942863425702));
#112378=CARTESIAN_POINT('Ctrl Pts',(-153.262220135813,0.621510466977741,
125.925538238965));
#112379=CARTESIAN_POINT('Ctrl Pts',(-153.269976438555,0.485364176547275,
125.908194638814));
#112380=CARTESIAN_POINT('Ctrl Pts',(-153.277732741296,0.348563474368509,
125.896563381663));
#112381=CARTESIAN_POINT('Ctrl Pts',(-153.285489044038,0.211624222713222,
125.890665648313));
#112382=CARTESIAN_POINT('Ctrl Pts',(-153.293249486553,0.074611882456538,
125.884764767166));
#112383=CARTESIAN_POINT('Ctrl Pts',(-153.301009929067,-0.0625387638507193,
125.884603507895));
#112384=CARTESIAN_POINT('Ctrl Pts',(-153.308770371581,-0.199313319997331,
125.890150888325));
#112385=CARTESIAN_POINT('Ctrl Pts',(-153.316543271846,-0.336307438803744,
125.895707173901));
#112386=CARTESIAN_POINT('Ctrl Pts',(-153.324316172112,-0.47292387113516,
125.906990379601));
#112387=CARTESIAN_POINT('Ctrl Pts',(-153.332089072377,-0.608653898711304,
125.923917656719));
#112388=CARTESIAN_POINT('Ctrl Pts',(-153.339579408139,-0.739449797899905,
125.940229584676));
#112389=CARTESIAN_POINT('Ctrl Pts',(-153.347069743901,-0.869422315676756,
125.961782305557));
#112390=CARTESIAN_POINT('Ctrl Pts',(-153.354560079663,-0.998128347341169,
125.988457497202));
#112391=CARTESIAN_POINT('Ctrl Pts',(-153.362334413782,-1.13171430731719,
126.016144086846));
#112392=CARTESIAN_POINT('Ctrl Pts',(-153.370108747901,-1.26435900789317,
126.049436954873));
#112393=CARTESIAN_POINT('Ctrl Pts',(-153.37788308202,-1.39555533061107,
126.088259645184));
#112394=CARTESIAN_POINT('Ctrl Pts',(-153.385647834967,-1.52658996558657,
126.127034489999));
#112395=CARTESIAN_POINT('Ctrl Pts',(-153.393412587914,-1.65617940301768,
126.171325487383));
#112396=CARTESIAN_POINT('Ctrl Pts',(-153.401177340861,-1.78382584027905,
126.221005030875));
#112397=CARTESIAN_POINT('Ctrl Pts',(-153.408934381746,-1.91134549729944,
126.270635231944));
#112398=CARTESIAN_POINT('Ctrl Pts',(-153.416691422632,-2.03692563258346,
126.325643187554));
#112399=CARTESIAN_POINT('Ctrl Pts',(-153.424448463517,-2.16008310760382,
126.38585136322));
#112400=CARTESIAN_POINT('Ctrl Pts',(-153.432199654757,-2.28314770861475,
126.446014135432));
#112401=CARTESIAN_POINT('Ctrl Pts',(-153.439950845997,-2.40379293597087,
126.511369151123));
#112402=CARTESIAN_POINT('Ctrl Pts',(-153.447702037237,-2.52155550184845,
126.581690737786));
#112403=CARTESIAN_POINT('Ctrl Pts',(-153.455449934014,-2.63926801549364,
126.651982435899));
#112404=CARTESIAN_POINT('Ctrl Pts',(-153.463197830791,-2.75409996953678,
126.727236306488));
#112405=CARTESIAN_POINT('Ctrl Pts',(-153.470945727568,-2.86561277412387,
126.807180800335));
#112406=CARTESIAN_POINT('Ctrl Pts',(-153.478692003652,-2.97710225263617,
126.887108571517));
#112407=CARTESIAN_POINT('Ctrl Pts',(-153.486438279736,-3.08527364513676,
126.97172478669));
#112408=CARTESIAN_POINT('Ctrl Pts',(-153.494184555821,-3.18971779180335,
127.060714871618));
#112409=CARTESIAN_POINT('Ctrl Pts',(-153.501930889086,-3.29416270945276,
127.149705613451));
#112410=CARTESIAN_POINT('Ctrl Pts',(-153.509677222351,-3.39488002877393,
127.243070035905));
#112411=CARTESIAN_POINT('Ctrl Pts',(-153.517423555617,-3.49149441371472,
127.340453889391));
#112412=CARTESIAN_POINT('Ctrl Pts',(-153.52517162362,-3.58813043477726,
127.437859551315));
#112413=CARTESIAN_POINT('Ctrl Pts',(-153.532919691623,-3.68066141780383,
127.539286157918));
#112414=CARTESIAN_POINT('Ctrl Pts',(-153.540667759626,-3.76874985390454,
127.644343592106));
#112415=CARTESIAN_POINT('Ctrl Pts',(-153.548424062367,-3.85693191144352,
127.749512682586));
#112416=CARTESIAN_POINT('Ctrl Pts',(-153.556180365109,-3.94066173856956,
127.858320009126));
#112417=CARTESIAN_POINT('Ctrl Pts',(-153.563936667851,-4.01964267911597,
127.970343010929));
#112418=CARTESIAN_POINT('Ctrl Pts',(-153.571697110365,-4.09866577416863,
128.082425802781));
#112419=CARTESIAN_POINT('Ctrl Pts',(-153.579457552879,-4.17293472057995,
128.197727361253));
#112420=CARTESIAN_POINT('Ctrl Pts',(-153.587217995394,-4.24219754081677,
128.31579816362));
#112421=CARTESIAN_POINT('Ctrl Pts',(-153.594990895659,-4.31157154788131,
128.434058503721));
#112422=CARTESIAN_POINT('Ctrl Pts',(-153.602763795924,-4.37592318608638,
128.555096625708));
#112423=CARTESIAN_POINT('Ctrl Pts',(-153.61053669619,-4.43504718373698,
128.678439748736));
#112424=CARTESIAN_POINT('Ctrl Pts',(-153.618027031952,-4.49202187514845,
128.797299038559));
#112425=CARTESIAN_POINT('Ctrl Pts',(-153.625517367714,-4.5441422812807,
128.91829837087));
#112426=CARTESIAN_POINT('Ctrl Pts',(-153.633007703476,-4.59126844100411,
129.041000993116));
#112427=CARTESIAN_POINT('Ctrl Pts',(-153.641883209428,-4.64710953069987,
129.186394722947));
#112428=CARTESIAN_POINT('Ctrl Pts',(-153.650758715381,-4.69608666589014,
129.334563409874));
#112429=CARTESIAN_POINT('Ctrl Pts',(-153.659634221333,-4.73795109743712,
129.484890094669));
#112430=CARTESIAN_POINT('Ctrl Pts',(-153.661549235509,-4.74698393233495,
129.517325173191));
#112431=CARTESIAN_POINT('Ctrl Pts',(-153.663464249686,-4.75568581355614,
129.549860627792));
#112432=CARTESIAN_POINT('Ctrl Pts',(-153.665379263862,-4.76405452823391,
129.582490119308));
#112433=CARTESIAN_POINT('Ctrl Pts',(-151.915051610183,-4.76405452823401,
129.582490119308));
#112434=CARTESIAN_POINT('Ctrl Pts',(-151.922930001919,-4.79858365450474,
129.717118658585));
#112435=CARTESIAN_POINT('Ctrl Pts',(-151.930808393655,-4.82736512749261,
129.853069661433));
#112436=CARTESIAN_POINT('Ctrl Pts',(-151.938686785391,-4.85032903477576,
129.989810854254));
#112437=CARTESIAN_POINT('Ctrl Pts',(-151.946565177126,-4.87329294205884,
130.126552047075));
#112438=CARTESIAN_POINT('Ctrl Pts',(-151.954443568862,-4.89043929396322,
130.264083010487));
#112439=CARTESIAN_POINT('Ctrl Pts',(-151.962321960598,-4.90175321058763,
130.401870213961));
#112440=CARTESIAN_POINT('Ctrl Pts',(-151.969928161735,-4.91267624264595,
130.534897006605));
#112441=CARTESIAN_POINT('Ctrl Pts',(-151.977534362873,-4.91818496055907,
130.668374433924));
#112442=CARTESIAN_POINT('Ctrl Pts',(-151.985140564011,-4.91824942752517,
130.801987613495));
#112443=CARTESIAN_POINT('',(-151.639859435965,-4.91824790957522,130.808895202333));
#112444=CARTESIAN_POINT('Ctrl Pts',(-151.569820863616,-4.76405452823393,
129.582490119308));
#112445=CARTESIAN_POINT('Ctrl Pts',(-151.577468334592,-4.7977264028668,
129.713776247459));
#112446=CARTESIAN_POINT('Ctrl Pts',(-151.585115805568,-4.82596040729268,
129.846428963026));
#112447=CARTESIAN_POINT('Ctrl Pts',(-151.592763276544,-4.84866308297735,
129.979952120356));
#112448=CARTESIAN_POINT('Ctrl Pts',(-151.600612636447,-4.87196509651644,
130.117000213853));
#112449=CARTESIAN_POINT('Ctrl Pts',(-151.608461996351,-4.88943959269887,
130.254964903359));
#112450=CARTESIAN_POINT('Ctrl Pts',(-151.616311356255,-4.90104222611252,
130.393303248867));
#112451=CARTESIAN_POINT('Ctrl Pts',(-151.624160716158,-4.91264485952617,
130.531641594374));
#112452=CARTESIAN_POINT('Ctrl Pts',(-151.632010076062,-4.91837564423588,
130.670353139465));
#112453=CARTESIAN_POINT('Ctrl Pts',(-151.639859435965,-4.91824790957522,
130.808895202333));
#112454=CARTESIAN_POINT('Ctrl Pts',(-151.639859435994,-4.91824790957475,
130.80889520284));
#112455=CARTESIAN_POINT('Ctrl Pts',(-151.650460085486,-4.91807540244884,
130.995997828581));
#112456=CARTESIAN_POINT('Ctrl Pts',(-151.661060734978,-4.90722241257785,
131.182627316781));
#112457=CARTESIAN_POINT('Ctrl Pts',(-151.67166138447,-4.88587253895692,
131.367772186108));
#112458=CARTESIAN_POINT('Ctrl Pts',(-151.682262033962,-4.86452266533604,
131.552917055434));
#112459=CARTESIAN_POINT('Ctrl Pts',(-151.692862683455,-4.83267605973099,
131.736577937587));
#112460=CARTESIAN_POINT('Ctrl Pts',(-151.703463332947,-4.79056393105034,
131.917769924613));
#112461=CARTESIAN_POINT('Ctrl Pts',(-151.711237667066,-4.759679619757,132.050653013322));
#112462=CARTESIAN_POINT('Ctrl Pts',(-151.719012001185,-4.72321323218033,
132.182460578467));
#112463=CARTESIAN_POINT('Ctrl Pts',(-151.726786335304,-4.68125337184728,
132.312687482363));
#112464=CARTESIAN_POINT('Ctrl Pts',(-151.734551088251,-4.63934522329203,
132.442753893239));
#112465=CARTESIAN_POINT('Ctrl Pts',(-151.742315841198,-4.59195719143878,
132.5712431503));
#112466=CARTESIAN_POINT('Ctrl Pts',(-151.750080594145,-4.53922879189337,
132.697660656479));
#112467=CARTESIAN_POINT('Ctrl Pts',(-151.75783763503,-4.48655276293787,
132.823952603007));
#112468=CARTESIAN_POINT('Ctrl Pts',(-151.765594675915,-4.42854707127498,
132.948176535053));
#112469=CARTESIAN_POINT('Ctrl Pts',(-151.7733517168,-4.36540079425787,133.069853713559));
#112470=CARTESIAN_POINT('Ctrl Pts',(-151.78110290804,-4.30230213633922,
133.191439134359));
#112471=CARTESIAN_POINT('Ctrl Pts',(-151.78885409928,-4.23407078847632,
133.310481278696));
#112472=CARTESIAN_POINT('Ctrl Pts',(-151.79660529052,-4.16094347581855,
133.426522407682));
#112473=CARTESIAN_POINT('Ctrl Pts',(-151.804353187297,-4.0878472442195,
133.542514216092));
#112474=CARTESIAN_POINT('Ctrl Pts',(-151.812101084074,-4.00985939461461,
133.655507215972));
#112475=CARTESIAN_POINT('Ctrl Pts',(-151.819848980851,-3.92726192297093,
133.765069460205));
#112476=CARTESIAN_POINT('Ctrl Pts',(-151.827595256935,-3.84468172893774,
133.874608786379));
#112477=CARTESIAN_POINT('Ctrl Pts',(-151.83534153302,-3.75749406598494,
133.980718472339));
#112478=CARTESIAN_POINT('Ctrl Pts',(-151.843087809104,-3.6660232364665,
134.082997025005));
#112479=CARTESIAN_POINT('Ctrl Pts',(-151.850834142369,-3.57455173173131,
134.185276332669));
#112480=CARTESIAN_POINT('Ctrl Pts',(-151.858580475634,-3.47879725796815,
134.283724159185));
#112481=CARTESIAN_POINT('Ctrl Pts',(-151.8663268089,-3.37912296978222,134.377973777603));
#112482=CARTESIAN_POINT('Ctrl Pts',(-151.874074876903,-3.27942636023042,
134.472244502569));
#112483=CARTESIAN_POINT('Ctrl Pts',(-151.881822944905,-3.17580847352705,
134.562314880064));
#112484=CARTESIAN_POINT('Ctrl Pts',(-151.889571012908,-3.06866741370414,
134.647856860126));
#112485=CARTESIAN_POINT('Ctrl Pts',(-151.89732731565,-2.96141248308801,
134.733489755222));
#112486=CARTESIAN_POINT('Ctrl Pts',(-151.905083618392,-2.8506272053868,
134.814584394403));
#112487=CARTESIAN_POINT('Ctrl Pts',(-151.912839921134,-2.73674113864215,
134.890854347228));
#112488=CARTESIAN_POINT('Ctrl Pts',(-151.920600363648,-2.62279428747433,
134.967165007622));
#112489=CARTESIAN_POINT('Ctrl Pts',(-151.928360806162,-2.50574368307037,
135.038645646929));
#112490=CARTESIAN_POINT('Ctrl Pts',(-151.936121248676,-2.38604476546982,
135.105055147485));
#112491=CARTESIAN_POINT('Ctrl Pts',(-151.943894148942,-2.26615369654069,
135.171571254466));
#112492=CARTESIAN_POINT('Ctrl Pts',(-151.951667049207,-2.14360616866237,
135.2329997798));
#112493=CARTESIAN_POINT('Ctrl Pts',(-151.959439949473,-2.01887975248573,
135.289146856341));
#112494=CARTESIAN_POINT('Ctrl Pts',(-151.966930285235,-1.89868745570637,
135.343252845223));
#112495=CARTESIAN_POINT('Ctrl Pts',(-151.974420620996,-1.77647222218059,
135.392454591621));
#112496=CARTESIAN_POINT('Ctrl Pts',(-151.981910956758,-1.65267403736753,
135.436622655568));
#112497=CARTESIAN_POINT('Ctrl Pts',(-151.989685290877,-1.52418200674763,
135.482465365085));
#112498=CARTESIAN_POINT('Ctrl Pts',(-151.997459624996,-1.39357759598124,
135.523030368974));
#112499=CARTESIAN_POINT('Ctrl Pts',(-152.005233959115,-1.26133368407946,
135.558119172637));
#112500=CARTESIAN_POINT('Ctrl Pts',(-152.012998712062,-1.12925275098013,
135.593164732484));
#112501=CARTESIAN_POINT('Ctrl Pts',(-152.020763465009,-0.995536711276644,
135.622747421154));
#112502=CARTESIAN_POINT('Ctrl Pts',(-152.028528217957,-0.860677095082207,
135.646717275279));
#112503=CARTESIAN_POINT('Ctrl Pts',(-152.036285258841,-0.725951423359762,
135.670663322208));
#112504=CARTESIAN_POINT('Ctrl Pts',(-152.044042299727,-0.590084817913392,
135.689007560615));
#112505=CARTESIAN_POINT('Ctrl Pts',(-152.051799340611,-0.453582256398363,
135.701650296478));
#112506=CARTESIAN_POINT('Ctrl Pts',(-152.059550531852,-0.317182632526622,
135.714283498356));
#112507=CARTESIAN_POINT('Ctrl Pts',(-152.067301723092,-0.180148394883785,
135.721223719768));
#112508=CARTESIAN_POINT('Ctrl Pts',(-152.075052914332,-0.0429926078877076,
135.722422705235));
#112509=CARTESIAN_POINT('Ctrl Pts',(-152.082800811109,0.0941048842399591,
135.723621181101));
#112510=CARTESIAN_POINT('Ctrl Pts',(-152.090548707886,0.231323432837869,
135.719083270942));
#112511=CARTESIAN_POINT('Ctrl Pts',(-152.098296604663,0.368147202853541,
135.708812747981));
#112512=CARTESIAN_POINT('Ctrl Pts',(-152.106042880747,0.504942352286105,
135.698544373392));
#112513=CARTESIAN_POINT('Ctrl Pts',(-152.113789156831,0.641342497769553,
135.682545800402));
#112514=CARTESIAN_POINT('Ctrl Pts',(-152.121535432915,0.776834558460905,
135.660872856949));
#112515=CARTESIAN_POINT('Ctrl Pts',(-152.12928176618,0.912327619323686,
135.639199753512));
#112516=CARTESIAN_POINT('Ctrl Pts',(-152.137028099446,1.04691219596097,
135.611852257782));
#112517=CARTESIAN_POINT('Ctrl Pts',(-152.144774432711,1.18008345666775,
135.578937677139));
#112518=CARTESIAN_POINT('Ctrl Pts',(-152.152522500714,1.3132845401552,135.546015725504));
#112519=CARTESIAN_POINT('Ctrl Pts',(-152.160270568717,1.4450712984376,135.507524301937));
#112520=CARTESIAN_POINT('Ctrl Pts',(-152.16801863672,1.57495254883828,135.463621023618));
#112521=CARTESIAN_POINT('Ctrl Pts',(-152.175774939462,1.70497183857732,
135.419671084373));
#112522=CARTESIAN_POINT('Ctrl Pts',(-152.183531242204,1.83308120391858,
135.370297925966));
#112523=CARTESIAN_POINT('Ctrl Pts',(-152.191287544945,1.95880747620422,
135.315708125093));
#112524=CARTESIAN_POINT('Ctrl Pts',(-152.19904798746,2.08460085238727,135.261089187998));
#112525=CARTESIAN_POINT('Ctrl Pts',(-152.206808429974,2.20800824947343,
135.201248231026));
#112526=CARTESIAN_POINT('Ctrl Pts',(-152.214568872488,2.32858063187714,
135.136438098792));
#112527=CARTESIAN_POINT('Ctrl Pts',(-152.222341772753,2.44934656777267,
135.071523927581));
#112528=CARTESIAN_POINT('Ctrl Pts',(-152.230114673019,2.56726805809014,
135.001624840069));
#112529=CARTESIAN_POINT('Ctrl Pts',(-152.237887573284,2.68192385830763,
134.927037840044));
#112530=CARTESIAN_POINT('Ctrl Pts',(-152.245377909046,2.79241163139165,
134.85516226534));
#112531=CARTESIAN_POINT('Ctrl Pts',(-152.252868244809,2.89986677310276,
134.778933873803));
#112532=CARTESIAN_POINT('Ctrl Pts',(-152.260358580571,3.00394255904258,
134.698652872196));
#112533=CARTESIAN_POINT('Ctrl Pts',(-152.26813291469,3.11196441003506,134.615327992016));
#112534=CARTESIAN_POINT('Ctrl Pts',(-152.275907248809,3.21668777087802,
134.527373177787));
#112535=CARTESIAN_POINT('Ctrl Pts',(-152.283681582928,3.31769003978603,
134.435078984832));
#112536=CARTESIAN_POINT('Ctrl Pts',(-152.291446335875,3.41856783242444,
134.342898536222));
#112537=CARTESIAN_POINT('Ctrl Pts',(-152.299211088822,3.5157333718833,134.246389610807));
#112538=CARTESIAN_POINT('Ctrl Pts',(-152.306975841769,3.60879480570351,
134.145884687931));
#112539=CARTESIAN_POINT('Ctrl Pts',(-152.314732882654,3.70176380959571,
134.045479587961));
#112540=CARTESIAN_POINT('Ctrl Pts',(-152.322489923539,3.79063655587374,
133.941086673798));
#112541=CARTESIAN_POINT('Ctrl Pts',(-152.330246964424,3.8750562163759,133.833076910391));
#112542=CARTESIAN_POINT('Ctrl Pts',(-152.337998155665,3.9594122153555,133.725148597988));
#112543=CARTESIAN_POINT('Ctrl Pts',(-152.345749346905,4.03932157287999,
133.613609172044));
#112544=CARTESIAN_POINT('Ctrl Pts',(-152.353500538145,4.11446636639845,
133.498864204922));
#112545=CARTESIAN_POINT('Ctrl Pts',(-152.361248434922,4.18957922137501,
133.384168007472));
#112546=CARTESIAN_POINT('Ctrl Pts',(-152.368996331699,4.25993132630397,
133.266269305019));
#112547=CARTESIAN_POINT('Ctrl Pts',(-152.376744228476,4.32524703426072,
133.145604123722));
#112548=CARTESIAN_POINT('Ctrl Pts',(-152.38449050456,4.39054907957941,133.02496418298));
#112549=CARTESIAN_POINT('Ctrl Pts',(-152.392236780644,4.45081663741246,
132.901559258044));
#112550=CARTESIAN_POINT('Ctrl Pts',(-152.399983056729,4.50581934465717,
132.775851194722));
#112551=CARTESIAN_POINT('Ctrl Pts',(-152.407729389994,4.56082245791946,
132.650142203451));
#112552=CARTESIAN_POINT('Ctrl Pts',(-152.415475723259,4.61056048632403,
132.52213039805));
#112553=CARTESIAN_POINT('Ctrl Pts',(-152.423222056525,4.65485083674059,
132.39229850999));
#112554=CARTESIAN_POINT('Ctrl Pts',(-152.430970124527,4.69915110567397,
132.262437546978));
#112555=CARTESIAN_POINT('Ctrl Pts',(-152.438718192531,4.73800114281547,
132.130756060197));
#112556=CARTESIAN_POINT('Ctrl Pts',(-152.446466260534,4.77126805972803,
131.997752491478));
#112557=CARTESIAN_POINT('Ctrl Pts',(-152.454222563275,4.80457033311571,
131.864607564984));
#112558=CARTESIAN_POINT('Ctrl Pts',(-152.461978866017,4.83227753783932,
131.73013812955));
#112559=CARTESIAN_POINT('Ctrl Pts',(-152.469735168759,4.85430771350575,
131.594853935121));
#112560=CARTESIAN_POINT('Ctrl Pts',(-152.477495611273,4.8763496473403,131.459497535443));
#112561=CARTESIAN_POINT('Ctrl Pts',(-152.485256053787,4.89270846797341,
131.323325898254));
#112562=CARTESIAN_POINT('Ctrl Pts',(-152.493016496302,4.90335418604,131.186853478603));
#112563=CARTESIAN_POINT('Ctrl Pts',(-152.500789396567,4.9140169935583,131.050161981308));
#112564=CARTESIAN_POINT('Ctrl Pts',(-152.508562296832,4.91894835749858,
130.913169127612));
#112565=CARTESIAN_POINT('Ctrl Pts',(-152.516335197098,4.91817046260457,
130.776389860265));
#112566=CARTESIAN_POINT('Ctrl Pts',(-152.52382553286,4.91742084614935,130.644582863812));
#112567=CARTESIAN_POINT('Ctrl Pts',(-152.531315868622,4.91136987028146,
130.5129745022));
#112568=CARTESIAN_POINT('Ctrl Pts',(-152.538806204384,4.90008269444702,
130.382018753573));
#112569=CARTESIAN_POINT('Ctrl Pts',(-152.546580538503,4.88836756191021,
130.246097777935));
#112570=CARTESIAN_POINT('Ctrl Pts',(-152.554354872622,4.87097422023509,
130.110449323031));
#112571=CARTESIAN_POINT('Ctrl Pts',(-152.562129206741,4.84791869525746,
129.975585987963));
#112572=CARTESIAN_POINT('Ctrl Pts',(-152.569893959688,4.82489158415382,
129.840888859902));
#112573=CARTESIAN_POINT('Ctrl Pts',(-152.577658712635,4.79621623940532,
129.706975308136));
#112574=CARTESIAN_POINT('Ctrl Pts',(-152.585423465583,4.76196057947378,
129.574354722443));
#112575=CARTESIAN_POINT('Ctrl Pts',(-152.593180506468,4.72773894274661,
129.441865857385));
#112576=CARTESIAN_POINT('Ctrl Pts',(-152.600937547353,4.68794811770129,
129.31066777889));
#112577=CARTESIAN_POINT('Ctrl Pts',(-152.608694588238,4.64270733331829,
129.181261212214));
#112578=CARTESIAN_POINT('Ctrl Pts',(-152.616445779478,4.59750066536264,
129.051952232037));
#112579=CARTESIAN_POINT('Ctrl Pts',(-152.624196970718,4.54685234699244,
128.924432442177));
#112580=CARTESIAN_POINT('Ctrl Pts',(-152.631948161958,4.49093175281661,
128.799188541647));
#112581=CARTESIAN_POINT('Ctrl Pts',(-152.639696058735,4.43503492638511,
128.673997873117));
#112582=CARTESIAN_POINT('Ctrl Pts',(-152.647443955512,4.37387044010636,
128.551081526253));
#112583=CARTESIAN_POINT('Ctrl Pts',(-152.655191852289,4.30765614124125,
128.43090709341));
#112584=CARTESIAN_POINT('Ctrl Pts',(-152.662938128373,4.24145569298004,
128.310757798468));
#112585=CARTESIAN_POINT('Ctrl Pts',(-152.670684404457,4.1702077217476,128.193349618936));
#112586=CARTESIAN_POINT('Ctrl Pts',(-152.678430680542,4.09417627461906,
128.079126004758));
#112587=CARTESIAN_POINT('Ctrl Pts',(-152.686177013807,4.01814426624353,
127.964901547407));
#112588=CARTESIAN_POINT('Ctrl Pts',(-152.693923347072,3.93732892814867,
127.853862027775));
#112589=CARTESIAN_POINT('Ctrl Pts',(-152.701669680338,3.85203769994542,
127.746421994784));
#112590=CARTESIAN_POINT('Ctrl Pts',(-152.709417748341,3.76672737136311,
127.638957901344));
#112591=CARTESIAN_POINT('Ctrl Pts',(-152.717165816344,3.67693940116022,
127.535095204702));
#112592=CARTESIAN_POINT('Ctrl Pts',(-152.724913884347,3.58302131312101,
127.43521512765));
#112593=CARTESIAN_POINT('Ctrl Pts',(-152.732670187088,3.48900340782032,
127.335228896864));
#112594=CARTESIAN_POINT('Ctrl Pts',(-152.74042648983,3.39084688435725,127.239234026371));
#112595=CARTESIAN_POINT('Ctrl Pts',(-152.748182792572,3.28893630820075,
127.147575004066));
#112596=CARTESIAN_POINT('Ctrl Pts',(-152.755943235086,3.18697133930101,
127.055867060581));
#112597=CARTESIAN_POINT('Ctrl Pts',(-152.7637036776,3.0812486264919,126.968499825399));
#112598=CARTESIAN_POINT('Ctrl Pts',(-152.771464120114,2.97218478539028,
126.885776604942));
#112599=CARTESIAN_POINT('Ctrl Pts',(-152.77923702038,2.86294586532869,126.802920589827));
#112600=CARTESIAN_POINT('Ctrl Pts',(-152.787009920645,2.75035542034077,
126.724723710022));
#112601=CARTESIAN_POINT('Ctrl Pts',(-152.794782820911,2.63485867774022,
126.651445640007));
#112602=CARTESIAN_POINT('Ctrl Pts',(-152.802273156673,2.52356053265162,
126.580831412413));
#112603=CARTESIAN_POINT('Ctrl Pts',(-152.809763492435,2.4095639904248,126.514784735619));
#112604=CARTESIAN_POINT('Ctrl Pts',(-152.817253828197,2.29328621600259,
126.453496175413));
#112605=CARTESIAN_POINT('Ctrl Pts',(-152.825028162316,2.17259973442148,
126.389883840819));
#112606=CARTESIAN_POINT('Ctrl Pts',(-152.832802496435,2.04907332151543,
126.331196048502));
#112607=CARTESIAN_POINT('Ctrl Pts',(-152.840576830554,1.92314690378126,
126.277696387807));
#112608=CARTESIAN_POINT('Ctrl Pts',(-152.848341583501,1.79737567910258,
126.224262660663));
#112609=CARTESIAN_POINT('Ctrl Pts',(-152.856106336448,1.66921069110178,
126.176004494578));
#112610=CARTESIAN_POINT('Ctrl Pts',(-152.863871089395,1.5391172154132,126.133140085444));
#112611=CARTESIAN_POINT('Ctrl Pts',(-152.87162813028,1.40915295039868,126.090318249845));
#112612=CARTESIAN_POINT('Ctrl Pts',(-152.879385171165,1.27726437835644,
126.052879631773));
#112613=CARTESIAN_POINT('Ctrl Pts',(-152.88714221205,1.1439372198007,126.020994574741));
#112614=CARTESIAN_POINT('Ctrl Pts',(-152.89489340329,1.01071060429254,125.989133562478));
#112615=CARTESIAN_POINT('Ctrl Pts',(-152.902644594531,0.876047940301947,
125.962817865894));
#112616=CARTESIAN_POINT('Ctrl Pts',(-152.910395785771,0.740450252606506,
125.942168058039));
#112617=CARTESIAN_POINT('Ctrl Pts',(-152.918143682548,0.604910197545337,
125.921527026904));
#112618=CARTESIAN_POINT('Ctrl Pts',(-152.925891579325,0.468436294897397,
125.9065471536));
#112619=CARTESIAN_POINT('Ctrl Pts',(-152.933639476102,0.331539695118737,
125.897297902146));
#112620=CARTESIAN_POINT('Ctrl Pts',(-152.941385752186,0.194671731157229,
125.888050585437));
#112621=CARTESIAN_POINT('Ctrl Pts',(-152.94913202827,0.0573816357642553,
125.884531532591));
#112622=CARTESIAN_POINT('Ctrl Pts',(-152.956878304354,-0.0798147801698766,
125.886758288853));
#112623=CARTESIAN_POINT('Ctrl Pts',(-152.96462463762,-0.217012208856598,
125.888985061552));
#112624=CARTESIAN_POINT('Ctrl Pts',(-152.972370970885,-0.354115565790877,
125.896957721648));
#112625=CARTESIAN_POINT('Ctrl Pts',(-152.98011730415,-0.490609900603677,
125.910641685309));
#112626=CARTESIAN_POINT('Ctrl Pts',(-152.987865372153,-0.627134802376186,
125.924328713399));
#112627=CARTESIAN_POINT('Ctrl Pts',(-152.995613440156,-0.763050021693598,
125.943729551136));
#112628=CARTESIAN_POINT('Ctrl Pts',(-153.003361508159,-0.897846979930605,
125.968757877149));
#112629=CARTESIAN_POINT('Ctrl Pts',(-153.011117810901,-1.03278720197911,
125.993812803565));
#112630=CARTESIAN_POINT('Ctrl Pts',(-153.018874113643,-1.1666064037798,
126.024507094385));
#112631=CARTESIAN_POINT('Ctrl Pts',(-153.026630416385,-1.29880689088056,
126.060703407912));
#112632=CARTESIAN_POINT('Ctrl Pts',(-153.034390858899,-1.43107793736177,
126.096919040501));
#112633=CARTESIAN_POINT('Ctrl Pts',(-153.042151301413,-1.56172817538354,
126.138642428332));
#112634=CARTESIAN_POINT('Ctrl Pts',(-153.049911743928,-1.69027723374617,
126.185687005415));
#112635=CARTESIAN_POINT('Ctrl Pts',(-153.057684644193,-1.81903265046933,
126.23280710263));
#112636=CARTESIAN_POINT('Ctrl Pts',(-153.065457544459,-1.9456797857909,
126.285265309126));
#112637=CARTESIAN_POINT('Ctrl Pts',(-153.073230444724,-2.06975951197796,
126.342827402955));
#112638=CARTESIAN_POINT('Ctrl Pts',(-153.080720780486,-2.18932862757646,
126.398296969681));
#112639=CARTESIAN_POINT('Ctrl Pts',(-153.088211116248,-2.30651348289287,
126.458505647118));
#112640=CARTESIAN_POINT('Ctrl Pts',(-153.095701452009,-2.42092826169051,
126.523205468048));
#112641=CARTESIAN_POINT('Ctrl Pts',(-153.103476880256,-2.53969782439262,
126.590367853182));
#112642=CARTESIAN_POINT('Ctrl Pts',(-153.111252308503,-2.65585854781134,
126.66258281134));
#112643=CARTESIAN_POINT('Ctrl Pts',(-153.11902773675,-2.76895068315104,
126.739622596884));
#112644=CARTESIAN_POINT('Ctrl Pts',(-153.12679334467,-2.88189998368885,
126.816565081564));
#112645=CARTESIAN_POINT('Ctrl Pts',(-153.13455895259,-2.99178808809088,
126.898320049418));
#112646=CARTESIAN_POINT('Ctrl Pts',(-153.14232456051,-3.09817979041436,
126.98461389183));
#112647=CARTESIAN_POINT('Ctrl Pts',(-153.150080784105,-3.20444292402153,
127.070803452722));
#112648=CARTESIAN_POINT('Ctrl Pts',(-153.157837007701,-3.30721776915533,
127.16152071899));
#112649=CARTESIAN_POINT('Ctrl Pts',(-153.165593231296,-3.40609860147247,
127.256449206673));
#112650=CARTESIAN_POINT('Ctrl Pts',(-153.17334413396,-3.50491159947248,
127.351312571429));
#112651=CARTESIAN_POINT('Ctrl Pts',(-153.181095036625,-3.59983561853296,
127.450381140445));
#112652=CARTESIAN_POINT('Ctrl Pts',(-153.188845939289,-3.6904984470236,
127.553298594932));
#112653=CARTESIAN_POINT('Ctrl Pts',(-153.196593203296,-3.7811187139077,
127.656167734885));
#112654=CARTESIAN_POINT('Ctrl Pts',(-153.204340467304,-3.86748151329224,
127.762881871938));
#112655=CARTESIAN_POINT('Ctrl Pts',(-153.212087731312,-3.94925219847171,
127.873048601528));
#112656=CARTESIAN_POINT('Ctrl Pts',(-153.219833036126,-4.0310022047831,
127.983187471217));
#112657=CARTESIAN_POINT('Ctrl Pts',(-153.227578340939,-4.1081621764316,
128.096776881375));
#112658=CARTESIAN_POINT('Ctrl Pts',(-153.235323645753,-4.1804386525967,
128.213392510009));
#112659=CARTESIAN_POINT('Ctrl Pts',(-153.243070974539,-4.25273401576939,
128.330038612186));
#112660=CARTESIAN_POINT('Ctrl Pts',(-153.250818303326,-4.32014312312706,
128.449712183301));
#112661=CARTESIAN_POINT('Ctrl Pts',(-153.258565632113,-4.38241663012796,
128.571961114234));
#112662=CARTESIAN_POINT('Ctrl Pts',(-153.266313951439,-4.444698099145,128.694225675376));
#112663=CARTESIAN_POINT('Ctrl Pts',(-153.274062270765,-4.50184248965709,
128.819065900196));
#112664=CARTESIAN_POINT('Ctrl Pts',(-153.28181059009,-4.55364750967603,
128.946007201199));
#112665=CARTESIAN_POINT('Ctrl Pts',(-153.289564968543,-4.60549304082644,
129.073047769334));
#112666=CARTESIAN_POINT('Ctrl Pts',(-153.297319346996,-4.65199072157926,
129.202192330231));
#112667=CARTESIAN_POINT('Ctrl Pts',(-153.305073725448,-4.69298719647638,
129.332948290511));
#112668=CARTESIAN_POINT('Ctrl Pts',(-153.309971088547,-4.71887897163126,
129.415528657049));
#112669=CARTESIAN_POINT('Ctrl Pts',(-153.314868451647,-4.74257748189,129.498751441572));
#112670=CARTESIAN_POINT('Ctrl Pts',(-153.319765814746,-4.76405452823394,
129.582490119308));
#112671=CARTESIAN_POINT('Origin',(213.235140564004,0.,130.804360617566));
#112672=CARTESIAN_POINT('',(-155.415271106226,-4.76405452823407,129.582490119308));
#112673=CARTESIAN_POINT('',(-155.070070112882,-4.76405452823396,129.582490119308));
#112674=CARTESIAN_POINT('',(213.235140564004,-4.76405452823405,129.582490119308));
#112675=CARTESIAN_POINT('',(-153.735140563956,-4.91824891289641,130.801090557425));
#112676=CARTESIAN_POINT('Ctrl Pts',(-153.735140564011,-4.91824891289706,
130.801090558408));
#112677=CARTESIAN_POINT('Ctrl Pts',(-153.742931215836,-4.9183407379463,
130.939197677182));
#112678=CARTESIAN_POINT('Ctrl Pts',(-153.75072186766,-4.91261105069972,
131.077337777159));
#112679=CARTESIAN_POINT('Ctrl Pts',(-153.758512519485,-4.9010782060776,
131.214988771023));
#112680=CARTESIAN_POINT('Ctrl Pts',(-153.766303436599,-4.88954496873651,
131.352644452208));
#112681=CARTESIAN_POINT('Ctrl Pts',(-153.774094353712,-4.87220821190394,
131.489810610838));
#112682=CARTESIAN_POINT('Ctrl Pts',(-153.781885270826,-4.84913824902427,
131.625969590466));
#112683=CARTESIAN_POINT('Ctrl Pts',(-153.789678068041,-4.82606271890851,
131.762161427936));
#112684=CARTESIAN_POINT('Ctrl Pts',(-153.797470865256,-4.79725129229373,
131.897345223374));
#112685=CARTESIAN_POINT('Ctrl Pts',(-153.805263662471,-4.76282549066431,
132.031013138852));
#112686=CARTESIAN_POINT('Ctrl Pts',(-153.813059955468,-4.72838424591735,
132.164741016605));
#112687=CARTESIAN_POINT('Ctrl Pts',(-153.820856248465,-4.68832370769074,
132.296951288505));
#112688=CARTESIAN_POINT('Ctrl Pts',(-153.828652541462,-4.64281528299066,
132.42715121112));
#112689=CARTESIAN_POINT('Ctrl Pts',(-153.836458800242,-4.59724868614392,
132.557517564656));
#112690=CARTESIAN_POINT('Ctrl Pts',(-153.844265059022,-4.54622042260291,
132.685868073745));
#112691=CARTESIAN_POINT('Ctrl Pts',(-153.852071317802,-4.489950329851,132.811729317624));
#112692=CARTESIAN_POINT('Ctrl Pts',(-153.859883151995,-4.43364004768217,
132.937680454548));
#112693=CARTESIAN_POINT('Ctrl Pts',(-153.867694986188,-4.3720806477439,
133.061138440512));
#112694=CARTESIAN_POINT('Ctrl Pts',(-153.875506820381,-4.30553754988166,
133.181655186831));
#112695=CARTESIAN_POINT('Ctrl Pts',(-153.88333120146,-4.23888757459962,
133.302365499716));
#112696=CARTESIAN_POINT('Ctrl Pts',(-153.891155582539,-4.16723811338279,
133.42012481001));
#112697=CARTESIAN_POINT('Ctrl Pts',(-153.898979963618,-4.09089784138924,
133.534514077322));
#112698=CARTESIAN_POINT('Ctrl Pts',(-153.903138418175,-4.05032497706778,
133.595308990691));
#112699=CARTESIAN_POINT('Ctrl Pts',(-153.907296872732,-4.00842781287545,
133.655152541907));
#112700=CARTESIAN_POINT('Ctrl Pts',(-153.911455327288,-3.96525713331834,
133.713985838994));
#112701=CARTESIAN_POINT('Ctrl Pts',(-153.919229661407,-3.88454847522001,
133.823976149735));
#112702=CARTESIAN_POINT('Ctrl Pts',(-153.927003995526,-3.7991320617101,
133.930780025861));
#112703=CARTESIAN_POINT('Ctrl Pts',(-153.934778329645,-3.70928822316274,
134.033968014759));
#112704=CARTESIAN_POINT('Ctrl Pts',(-153.942543082592,-3.61955510911731,
134.137028833683));
#112705=CARTESIAN_POINT('Ctrl Pts',(-153.95030783554,-3.5254056809212,134.236482339973));
#112706=CARTESIAN_POINT('Ctrl Pts',(-153.958072588487,-3.42716291879298,
134.331928815426));
#112707=CARTESIAN_POINT('Ctrl Pts',(-153.965829629372,-3.32901773276055,
134.427280492094));
#112708=CARTESIAN_POINT('Ctrl Pts',(-153.973586670257,-3.22678758203929,
134.518632787314));
#112709=CARTESIAN_POINT('Ctrl Pts',(-153.981343711142,-3.12083476185748,
134.605620073547));
#112710=CARTESIAN_POINT('Ctrl Pts',(-153.989094902382,-3.01496184152142,
134.69254176199));
#112711=CARTESIAN_POINT('Ctrl Pts',(-153.996846093622,-2.90537214042314,
134.775104746269));
#112712=CARTESIAN_POINT('Ctrl Pts',(-154.004597284862,-2.79246348486383,
134.852981462768));
#112713=CARTESIAN_POINT('Ctrl Pts',(-154.012345181639,-2.67960281849553,
134.930825079585));
#112714=CARTESIAN_POINT('Ctrl Pts',(-154.020093078417,-2.56342632449215,
135.003986168622));
#112715=CARTESIAN_POINT('Ctrl Pts',(-154.027840975194,-2.44436328868205,
135.07217869891));
#112716=CARTESIAN_POINT('Ctrl Pts',(-154.035587251278,-2.32532515829235,
135.14035696479));
#112717=CARTESIAN_POINT('Ctrl Pts',(-154.043333527362,-2.20340202613747,
135.203568544989));
#112718=CARTESIAN_POINT('Ctrl Pts',(-154.051079803446,-2.0790500769467,
135.261572059718));
#112719=CARTESIAN_POINT('Ctrl Pts',(-154.058826136711,-1.95469720981792,
135.319576002615));
#112720=CARTESIAN_POINT('Ctrl Pts',(-154.066572469977,-1.82791584419325,
135.372371638059));
#112721=CARTESIAN_POINT('Ctrl Pts',(-154.074318803242,-1.69918419079703,
135.419764841277));
#112722=CARTESIAN_POINT('Ctrl Pts',(-154.082066871245,-1.57042370883941,
135.467168657874));
#112723=CARTESIAN_POINT('Ctrl Pts',(-154.089814939248,-1.43971243684242,
135.509167499762));
#112724=CARTESIAN_POINT('Ctrl Pts',(-154.097563007251,-1.30754548414376,
135.545616555542));
#112725=CARTESIAN_POINT('Ctrl Pts',(-154.105319309993,-1.17523806283514,
135.582104349813));
#112726=CARTESIAN_POINT('Ctrl Pts',(-154.113075612735,-1.04147224779288,
135.613030471224));
#112727=CARTESIAN_POINT('Ctrl Pts',(-154.120831915477,-0.906755675340532,
135.638300750391));
#112728=CARTESIAN_POINT('Ctrl Pts',(-154.128592357991,-0.771967200597233,
135.663584517067));
#112729=CARTESIAN_POINT('Ctrl Pts',(-154.136352800505,-0.636227344065018,
135.68320637059));
#112730=CARTESIAN_POINT('Ctrl Pts',(-154.144113243019,-0.500049692978532,
135.697123984729));
#112731=CARTESIAN_POINT('Ctrl Pts',(-154.151886143285,-0.363653437437238,
135.711063940657));
#112732=CARTESIAN_POINT('Ctrl Pts',(-154.15965904355,-0.226818373436666,
135.719281335245));
#112733=CARTESIAN_POINT('Ctrl Pts',(-154.167431943816,-0.0900598278066852,
135.72178598964));
#112734=CARTESIAN_POINT('Ctrl Pts',(-154.174922279578,0.0417272002145433,
135.724199593539));
#112735=CARTESIAN_POINT('Ctrl Pts',(-154.18241261534,0.173442868605299,
135.721308597997));
#112736=CARTESIAN_POINT('Ctrl Pts',(-154.189902951102,0.304631766308209,
135.713167249473));
#112737=CARTESIAN_POINT('Ctrl Pts',(-154.197677285221,0.440794730942865,
135.704717219245));
#112738=CARTESIAN_POINT('Ctrl Pts',(-154.20545161934,0.576821514684844,
135.690584075317));
#112739=CARTESIAN_POINT('Ctrl Pts',(-154.213225953459,0.712199281473261,
135.670771537943));
#112740=CARTESIAN_POINT('Ctrl Pts',(-154.220990706406,0.847410207262435,
135.650983417752));
#112741=CARTESIAN_POINT('Ctrl Pts',(-154.228755459353,0.981973324441182,
135.625529886797));
#112742=CARTESIAN_POINT('Ctrl Pts',(-154.2365202123,1.11537776006755,135.594466620031));
#112743=CARTESIAN_POINT('Ctrl Pts',(-154.244277253185,1.24864969652815,
135.563434205739));
#112744=CARTESIAN_POINT('Ctrl Pts',(-154.25203429407,1.38076486330313,135.526803231599));
#112745=CARTESIAN_POINT('Ctrl Pts',(-154.259791334955,1.51121981816764,
135.484680876232));
#112746=CARTESIAN_POINT('Ctrl Pts',(-154.267542526195,1.64157639593607,
135.44259028566));
#112747=CARTESIAN_POINT('Ctrl Pts',(-154.275293717435,1.77027488323562,
135.3950166761));
#112748=CARTESIAN_POINT('Ctrl Pts',(-154.283044908676,1.89682465668628,
135.342117693952));
#112749=CARTESIAN_POINT('Ctrl Pts',(-154.290792805453,2.02332064310723,
135.289241195281));
#112750=CARTESIAN_POINT('Ctrl Pts',(-154.29854070223,2.14766937212164,135.231043976271));
#112751=CARTESIAN_POINT('Ctrl Pts',(-154.306288599007,2.26939815829694,
135.167732600519));
#112752=CARTESIAN_POINT('Ctrl Pts',(-154.314034875091,2.39110148143435,
135.104434468142));
#112753=CARTESIAN_POINT('Ctrl Pts',(-154.321781151175,2.51018560516876,
135.036024487144));
#112754=CARTESIAN_POINT('Ctrl Pts',(-154.329527427259,2.6262008708577,134.962755986985));
#112755=CARTESIAN_POINT('Ctrl Pts',(-154.337273760524,2.74221699294514,
134.889486945975));
#112756=CARTESIAN_POINT('Ctrl Pts',(-154.34502009379,2.85516388122118,134.811359523002));
#112757=CARTESIAN_POINT('Ctrl Pts',(-154.352766427055,2.96461972843958,
134.728671121113));
#112758=CARTESIAN_POINT('Ctrl Pts',(-154.360514495058,3.0741000875359,134.645964201729));
#112759=CARTESIAN_POINT('Ctrl Pts',(-154.368262563061,3.18008753799965,
134.558694506582));
#112760=CARTESIAN_POINT('Ctrl Pts',(-154.376010631064,3.28219262720959,
134.467200311081));
#112761=CARTESIAN_POINT('Ctrl Pts',(-154.383766933806,3.38440623492354,
134.375608874461));
#112762=CARTESIAN_POINT('Ctrl Pts',(-154.391523236548,3.4827289471818,134.279784229856));
#112763=CARTESIAN_POINT('Ctrl Pts',(-154.399279539289,3.57680714678234,
134.180102565231));
#112764=CARTESIAN_POINT('Ctrl Pts',(-154.407039981804,3.67093555875065,
134.080367697501));
#112765=CARTESIAN_POINT('Ctrl Pts',(-154.414800424318,3.76081468792545,
133.976772002967));
#112766=CARTESIAN_POINT('Ctrl Pts',(-154.422560866832,3.84613131760403,
133.869724698755));
#112767=CARTESIAN_POINT('Ctrl Pts',(-154.430333767097,3.93158490511063,
133.762505552707));
#112768=CARTESIAN_POINT('Ctrl Pts',(-154.438106667363,4.01246112638024,
133.651824040489));
#112769=CARTESIAN_POINT('Ctrl Pts',(-154.445879567628,4.08848969748455,
133.538119029727));
#112770=CARTESIAN_POINT('Ctrl Pts',(-154.45336990339,4.16175443852481,133.428547482513));
#112771=CARTESIAN_POINT('Ctrl Pts',(-154.460860239152,4.2305176981983,133.316168706606));
#112772=CARTESIAN_POINT('Ctrl Pts',(-154.468350574914,4.29457895478601,
133.201395173764));
#112773=CARTESIAN_POINT('Ctrl Pts',(-154.476124909033,4.36106911338816,
133.08226996754));
#112774=CARTESIAN_POINT('Ctrl Pts',(-154.483899243152,4.42270429838098,
132.960187472385));
#112775=CARTESIAN_POINT('Ctrl Pts',(-154.491673577271,4.47921043930333,
132.835581162691));
#112776=CARTESIAN_POINT('Ctrl Pts',(-154.499438330219,4.53564694145726,
132.711128419136));
#112777=CARTESIAN_POINT('Ctrl Pts',(-154.507203083166,4.58696681670537,
132.584158402409));
#112778=CARTESIAN_POINT('Ctrl Pts',(-154.514967836113,4.63294076665846,
132.455131018056));
#112779=CARTESIAN_POINT('Ctrl Pts',(-154.522724876998,4.67886905463621,
132.326231785521));
#112780=CARTESIAN_POINT('Ctrl Pts',(-154.530481917883,4.71946185338369,
132.195279617733));
#112781=CARTESIAN_POINT('Ctrl Pts',(-154.538238958768,4.75453721248953,
132.062756007558));
#112782=CARTESIAN_POINT('Ctrl Pts',(-154.545990150008,4.78958612099428,
131.930332334467));
#112783=CARTESIAN_POINT('Ctrl Pts',(-154.553741341248,4.81912577193774,
131.796339954154));
#112784=CARTESIAN_POINT('Ctrl Pts',(-154.561492532488,4.84302360377905,
131.661276853694));
#112785=CARTESIAN_POINT('Ctrl Pts',(-154.569240429265,4.86691127840429,
131.526271158654));
#112786=CARTESIAN_POINT('Ctrl Pts',(-154.576988326042,4.88516183523863,
131.390196032773));
#112787=CARTESIAN_POINT('Ctrl Pts',(-154.584736222819,4.89769356406585,
131.253560812366));
#112788=CARTESIAN_POINT('Ctrl Pts',(-154.592482498903,4.91022267152555,
131.1169541731));
#112789=CARTESIAN_POINT('Ctrl Pts',(-154.600228774988,4.91703529471044,
130.979788061429));
#112790=CARTESIAN_POINT('Ctrl Pts',(-154.607975051072,4.91810151539024,
130.842577718663));
#112791=CARTESIAN_POINT('Ctrl Pts',(-154.615721384337,4.91916774394063,
130.705366363042));
#112792=CARTESIAN_POINT('Ctrl Pts',(-154.623467717602,4.91448748230462,
130.568111166628));
#112793=CARTESIAN_POINT('Ctrl Pts',(-154.631214050868,4.90408294696689,
130.431327761415));
#112794=CARTESIAN_POINT('Ctrl Pts',(-154.638962118871,4.8936760816056,130.294513724506));
#112795=CARTESIAN_POINT('Ctrl Pts',(-154.646710186874,4.87754242133503,
130.158172078802));
#112796=CARTESIAN_POINT('Ctrl Pts',(-154.654458254877,4.8557560581835,130.022813327945));
#112797=CARTESIAN_POINT('Ctrl Pts',(-154.662214557618,4.83394654022603,
129.887310716197));
#112798=CARTESIAN_POINT('Ctrl Pts',(-154.66997086036,4.80647238046654,129.752793472675));
#112799=CARTESIAN_POINT('Ctrl Pts',(-154.677727163102,4.77345893775802,
129.619762444328));
#112800=CARTESIAN_POINT('Ctrl Pts',(-154.685487605616,4.74042787478112,
129.486660413317));
#112801=CARTESIAN_POINT('Ctrl Pts',(-154.69324804813,4.70185174772653,129.355046553072));
#112802=CARTESIAN_POINT('Ctrl Pts',(-154.701008490645,4.6579055412718,129.225405573529));
#112803=CARTESIAN_POINT('Ctrl Pts',(-154.70878139091,4.61388878846499,129.095556482776));
#112804=CARTESIAN_POINT('Ctrl Pts',(-154.716554291175,4.56448487067994,
128.967686966388));
#112805=CARTESIAN_POINT('Ctrl Pts',(-154.724327191441,4.50991692461591,
128.842261640561));
#112806=CARTESIAN_POINT('Ctrl Pts',(-154.731817527203,4.45733266083968,
128.721395841255));
#112807=CARTESIAN_POINT('Ctrl Pts',(-154.739307862965,4.39995343542685,
128.602799890034));
#112808=CARTESIAN_POINT('Ctrl Pts',(-154.746798198727,4.33801788566053,
128.486865442557));
#112809=CARTESIAN_POINT('Ctrl Pts',(-154.754572532846,4.27373403069983,
128.366535305267));
#112810=CARTESIAN_POINT('Ctrl Pts',(-154.762346866965,4.20433789298146,
128.248691307871));
#112811=CARTESIAN_POINT('Ctrl Pts',(-154.770121201084,4.13004602500871,
128.133798337107));
#112812=CARTESIAN_POINT('Ctrl Pts',(-154.777885954031,4.05584571512399,
128.019046961662));
#112813=CARTESIAN_POINT('Ctrl Pts',(-154.785650706979,3.97676189020346,
127.907239701706));
#112814=CARTESIAN_POINT('Ctrl Pts',(-154.793415459926,3.89305754042848,
127.79881806265));
#112815=CARTESIAN_POINT('Ctrl Pts',(-154.801172500811,3.80943632699348,
127.690504109493));
#112816=CARTESIAN_POINT('Ctrl Pts',(-154.808929541696,3.72120395873303,
127.585569392886));
#112817=CARTESIAN_POINT('Ctrl Pts',(-154.816686582581,3.62866718058855,
127.484427251515));
#112818=CARTESIAN_POINT('Ctrl Pts',(-154.824437773821,3.53620018514767,
127.383361382219));
#112819=CARTESIAN_POINT('Ctrl Pts',(-154.832188965061,3.4394355036097,127.286082682769));
#112820=CARTESIAN_POINT('Ctrl Pts',(-154.839940156301,3.33872045385295,
127.19297185512));
#112821=CARTESIAN_POINT('Ctrl Pts',(-154.847688053078,3.23804821067969,
127.099900602057));
#112822=CARTESIAN_POINT('Ctrl Pts',(-154.855435949855,3.1334292251925,127.010993962352));
#112823=CARTESIAN_POINT('Ctrl Pts',(-154.863183846632,3.02524785008844,
126.926595989841));
#112824=CARTESIAN_POINT('Ctrl Pts',(-154.870930122716,2.91708910419564,
126.842215671567));
#112825=CARTESIAN_POINT('Ctrl Pts',(-154.8786763988,2.80536975893898,126.762342384911));
#112826=CARTESIAN_POINT('Ctrl Pts',(-154.886422674885,2.69050712989239,
126.687279801442));
#112827=CARTESIAN_POINT('Ctrl Pts',(-154.89416900815,2.57564365295612,126.612216663878));
#112828=CARTESIAN_POINT('Ctrl Pts',(-154.901915341415,2.45763717320808,
126.541964514238));
#112829=CARTESIAN_POINT('Ctrl Pts',(-154.909661674681,2.33693351499983,
126.476783372852));
#112830=CARTESIAN_POINT('Ctrl Pts',(-154.917409742684,2.21620282604407,
126.4115876346));
#112831=CARTESIAN_POINT('Ctrl Pts',(-154.925157810687,2.09277410065448,
126.351465350082));
#112832=CARTESIAN_POINT('Ctrl Pts',(-154.93290587869,1.96711688855453,126.296630123264));
#112833=CARTESIAN_POINT('Ctrl Pts',(-154.940662181432,1.84132612647439,
126.241736616914));
#112834=CARTESIAN_POINT('Ctrl Pts',(-154.948418484173,1.71330250532879,
126.192141549738));
#112835=CARTESIAN_POINT('Ctrl Pts',(-154.956174786915,1.58353516136397,
126.148010173793));
#112836=CARTESIAN_POINT('Ctrl Pts',(-154.963935229429,1.45369855666011,
126.103855243604));
#112837=CARTESIAN_POINT('Ctrl Pts',(-154.971695671944,1.32211674959033,
126.065169925518));
#112838=CARTESIAN_POINT('Ctrl Pts',(-154.979456114458,1.1892921238422,126.03206899753));
#112839=CARTESIAN_POINT('Ctrl Pts',(-154.987229014723,1.05625427621356,
125.998914932993));
#112840=CARTESIAN_POINT('Ctrl Pts',(-154.995001914989,0.921970006302803,
125.971363251223));
#112841=CARTESIAN_POINT('Ctrl Pts',(-155.002774815254,0.786950819710978,
125.949477357398));
#112842=CARTESIAN_POINT('Ctrl Pts',(-155.010265151016,0.656839920646407,
125.928387070941));
#112843=CARTESIAN_POINT('Ctrl Pts',(-155.017755486778,0.52604691517257,
125.912557829843));
#112844=CARTESIAN_POINT('Ctrl Pts',(-155.02524582254,0.395030303569576,
125.90200056125));
#112845=CARTESIAN_POINT('Ctrl Pts',(-155.033020156659,0.259046157314284,
125.891043010609));
#112846=CARTESIAN_POINT('Ctrl Pts',(-155.040794490778,0.122390357258395,
125.88573038758));
#112847=CARTESIAN_POINT('Ctrl Pts',(-155.048568824897,-0.0144289223016949,
125.886131783046));
#112848=CARTESIAN_POINT('Ctrl Pts',(-155.056333577844,-0.151079584327988,
125.886532683828));
#112849=CARTESIAN_POINT('Ctrl Pts',(-155.064098330791,-0.287892937775208,
125.892633590454));
#112850=CARTESIAN_POINT('Ctrl Pts',(-155.071863083738,-0.42435537902032,
125.904451886294));
#112851=CARTESIAN_POINT('Ctrl Pts',(-155.079620124623,-0.560682283845004,
125.916258444036));
#112852=CARTESIAN_POINT('Ctrl Pts',(-155.087377165508,-0.696658583073169,
125.933771056825));
#112853=CARTESIAN_POINT('Ctrl Pts',(-155.095134206393,-0.831770720026451,
125.956955071111));
#112854=CARTESIAN_POINT('Ctrl Pts',(-155.102885397633,-0.966780967865318,
125.980121602151));
#112855=CARTESIAN_POINT('Ctrl Pts',(-155.110636588873,-1.10092796676746,
126.008950956029));
#112856=CARTESIAN_POINT('Ctrl Pts',(-155.118387780114,-1.23370368759815,
126.043356703085));
#112857=CARTESIAN_POINT('Ctrl Pts',(-155.126135676891,-1.36642297520611,
126.07774782678));
#112858=CARTESIAN_POINT('Ctrl Pts',(-155.133883573668,-1.49777176627361,
126.117710531808));
#112859=CARTESIAN_POINT('Ctrl Pts',(-155.141631470445,-1.62725284654226,
126.163107420861));
#112860=CARTESIAN_POINT('Ctrl Pts',(-155.149377746529,-1.75670684216055,
126.208494813865));
#112861=CARTESIAN_POINT('Ctrl Pts',(-155.157124022613,-1.8842935353613,
126.259314000634));
#112862=CARTESIAN_POINT('Ctrl Pts',(-155.164870298697,-2.0095318693918,
126.315378023659));
#112863=CARTESIAN_POINT('Ctrl Pts',(-155.172616631963,-2.13477112790305,
126.371442460536));
#112864=CARTESIAN_POINT('Ctrl Pts',(-155.180362965228,-2.25766163581166,
126.432751651181));
#112865=CARTESIAN_POINT('Ctrl Pts',(-155.188109298493,-2.37774365169854,
126.499071058279));
#112866=CARTESIAN_POINT('Ctrl Pts',(-155.195857366496,-2.49785255912045,
126.565405317149));
#112867=CARTESIAN_POINT('Ctrl Pts',(-155.203605434499,-2.61515138082445,
126.636751836151));
#112868=CARTESIAN_POINT('Ctrl Pts',(-155.211353502502,-2.72920660264905,
126.712831027968));
#112869=CARTESIAN_POINT('Ctrl Pts',(-155.219109805244,-2.84338304372052,
126.788991077655));
#112870=CARTESIAN_POINT('Ctrl Pts',(-155.226866107986,-2.95430867272093,
126.869893630706));
#112871=CARTESIAN_POINT('Ctrl Pts',(-155.234622410728,-3.06158006832547,
126.955216485719));
#112872=CARTESIAN_POINT('Ctrl Pts',(-155.242382853242,-3.16890871790373,
127.040584880108));
#112873=CARTESIAN_POINT('Ctrl Pts',(-155.250143295756,-3.27257895241974,
127.130378021619));
#112874=CARTESIAN_POINT('Ctrl Pts',(-155.25790373827,-3.37222265524193,
127.224235280937));
#112875=CARTESIAN_POINT('Ctrl Pts',(-155.265676638536,-3.47202631498211,
127.31824320826));
#112876=CARTESIAN_POINT('Ctrl Pts',(-155.273449538801,-3.56779025312211,
127.41632801068));
#112877=CARTESIAN_POINT('Ctrl Pts',(-155.281222439066,-3.65918464381807,
127.518093616097));
#112878=CARTESIAN_POINT('Ctrl Pts',(-155.288712774828,-3.74725661820291,
127.616159785424));
#112879=CARTESIAN_POINT('Ctrl Pts',(-155.29620311059,-3.83127102130242,
127.717643553716));
#112880=CARTESIAN_POINT('Ctrl Pts',(-155.303693446352,-3.91097082919788,
127.822165078091));
#112881=CARTESIAN_POINT('Ctrl Pts',(-155.311488197042,-3.9939097190257,
127.930934464414));
#112882=CARTESIAN_POINT('Ctrl Pts',(-155.319282947731,-4.0724417498631,
128.043342282481));
#112883=CARTESIAN_POINT('Ctrl Pts',(-155.32707769842,-4.14623148879997,
128.158997220264));
#112884=CARTESIAN_POINT('Ctrl Pts',(-155.334859712521,-4.21990065562333,
128.274463178381));
#112885=CARTESIAN_POINT('Ctrl Pts',(-155.342641726622,-4.28884275654833,
128.393165364981));
#112886=CARTESIAN_POINT('Ctrl Pts',(-155.350423740722,-4.35276311837608,
128.514680225501));
#112887=CARTESIAN_POINT('Ctrl Pts',(-155.358198428636,-4.41662330394175,
128.636080688826));
#112888=CARTESIAN_POINT('Ctrl Pts',(-155.365973116549,-4.47547097388064,
128.760288218568));
#112889=CARTESIAN_POINT('Ctrl Pts',(-155.373747804463,-4.52905501556395,
128.886850844841));
#112890=CARTESIAN_POINT('Ctrl Pts',(-155.381515750894,-4.5825925941757,
129.013303727837));
#112891=CARTESIAN_POINT('Ctrl Pts',(-155.389283697325,-4.63087548063379,
129.142107285863));
#112892=CARTESIAN_POINT('Ctrl Pts',(-155.397051643756,-4.67369900638074,
129.272786048616));
#112893=CARTESIAN_POINT('Ctrl Pts',(-155.403124797913,-4.70717939604278,
129.374953626394));
#112894=CARTESIAN_POINT('Ctrl Pts',(-155.409197952069,-4.73732365996748,
129.478266869634));
#112895=CARTESIAN_POINT('Ctrl Pts',(-155.415271106226,-4.76405452823407,
129.582490119308));
#112896=CARTESIAN_POINT('Ctrl Pts',(-153.665379263862,-4.76405452823391,
129.582490119308));
#112897=CARTESIAN_POINT('Ctrl Pts',(-153.674204833383,-4.80262274046709,
129.732866993451));
#112898=CARTESIAN_POINT('Ctrl Pts',(-153.683030402904,-4.83411093424905,
129.885242807117));
#112899=CARTESIAN_POINT('Ctrl Pts',(-153.691855972424,-4.8583311825113,
130.038984119666));
#112900=CARTESIAN_POINT('Ctrl Pts',(-153.700625150211,-4.88239667341757,
130.191743088896));
#112901=CARTESIAN_POINT('Ctrl Pts',(-153.709394327997,-4.89928671230653,
130.345849991077));
#112902=CARTESIAN_POINT('Ctrl Pts',(-153.718163505784,-4.90886459777685,
130.500664349573));
#112903=CARTESIAN_POINT('Ctrl Pts',(-153.723822525174,-4.91504550104034,
130.600570803521));
#112904=CARTESIAN_POINT('Ctrl Pts',(-153.729481544565,-4.91818221245824,
130.700771498029));
#112905=CARTESIAN_POINT('Ctrl Pts',(-153.735140563956,-4.91824891289641,
130.801090557425));
#112906=CARTESIAN_POINT('',(-153.389859436024,-4.91824971158563,130.802676281535));
#112907=CARTESIAN_POINT('Ctrl Pts',(-153.319765814746,-4.76405452823394,
129.582490119308));
#112908=CARTESIAN_POINT('Ctrl Pts',(-153.32752964618,-4.79810227272907,
129.715241758348));
#112909=CARTESIAN_POINT('Ctrl Pts',(-153.335293477613,-4.82656440966018,
129.849290078614));
#112910=CARTESIAN_POINT('Ctrl Pts',(-153.343057309047,-4.84937079552965,
129.984125315982));
#112911=CARTESIAN_POINT('Ctrl Pts',(-153.350832221389,-4.87220973175494,
130.119152996598));
#112912=CARTESIAN_POINT('Ctrl Pts',(-153.358607133731,-4.88937675304912,
130.254969450077));
#112913=CARTESIAN_POINT('Ctrl Pts',(-153.366382046073,-4.90085364791497,
130.391060987493));
#112914=CARTESIAN_POINT('Ctrl Pts',(-153.36897105599,-4.90467540092215,
130.436378841185));
#112915=CARTESIAN_POINT('Ctrl Pts',(-153.371560065907,-4.90786662768838,
130.481727209334));
#112916=CARTESIAN_POINT('Ctrl Pts',(-153.374149075824,-4.91042793580915,
130.527087197049));
#112917=CARTESIAN_POINT('Ctrl Pts',(-153.379385862547,-4.91560869014808,
130.6188367805));
#112918=CARTESIAN_POINT('Ctrl Pts',(-153.38462264927,-4.91821822404875,
130.710732917615));
#112919=CARTESIAN_POINT('Ctrl Pts',(-153.389859435994,-4.91824971158545,
130.802676281007));
#112920=CARTESIAN_POINT('Ctrl Pts',(-153.389859436024,-4.91824971158563,
130.802676281536));
#112921=CARTESIAN_POINT('Ctrl Pts',(-153.397566623283,-4.91829605303094,
130.937992985503));
#112922=CARTESIAN_POINT('Ctrl Pts',(-153.405273810541,-4.9127536815725,
131.073537372969));
#112923=CARTESIAN_POINT('Ctrl Pts',(-153.412980997799,-4.90159240666056,
131.208804608086));
#112924=CARTESIAN_POINT('Ctrl Pts',(-153.420678966356,-4.89044448194448,
131.3439100477));
#112925=CARTESIAN_POINT('Ctrl Pts',(-153.428376934913,-4.87369105456227,
131.47873860129));
#112926=CARTESIAN_POINT('Ctrl Pts',(-153.43607490347,-4.85135391530499,
131.6127839293));
#112927=CARTESIAN_POINT('Ctrl Pts',(-153.443765584287,-4.82903792283001,
131.746702355323));
#112928=CARTESIAN_POINT('Ctrl Pts',(-153.451456265104,-4.80114880013807,
131.879838640546));
#112929=CARTESIAN_POINT('Ctrl Pts',(-153.459146945921,-4.76776022432417,
132.011690525194));
#112930=CARTESIAN_POINT('Ctrl Pts',(-153.467207352325,-4.73276650962672,
132.149881122463));
#112931=CARTESIAN_POINT('Ctrl Pts',(-153.47526775873,-4.69173146770541,
132.286660312855));
#112932=CARTESIAN_POINT('Ctrl Pts',(-153.483328165135,-4.64480057212113,
132.42146009123));
#112933=CARTESIAN_POINT('Ctrl Pts',(-153.491010778568,-4.6000693376497,
132.549941775163));
#112934=CARTESIAN_POINT('Ctrl Pts',(-153.498693392001,-4.54998251046827,
132.67662495948));
#112935=CARTESIAN_POINT('Ctrl Pts',(-153.506376005433,-4.49471727537261,
132.801032768162));
#112936=CARTESIAN_POINT('Ctrl Pts',(-153.514057634474,-4.43945912154896,
132.925424636162));
#112937=CARTESIAN_POINT('Ctrl Pts',(-153.521739263514,-4.37902404088357,
133.04754134441));
#112938=CARTESIAN_POINT('Ctrl Pts',(-153.529420892554,-4.31363715365821,
133.166926504283));
#112939=CARTESIAN_POINT('Ctrl Pts',(-153.537103270656,-4.2482438903378,
133.286323305805));
#112940=CARTESIAN_POINT('Ctrl Pts',(-153.544785648758,-4.1778980514845,
133.402987679917));
#112941=CARTESIAN_POINT('Ctrl Pts',(-153.55246802686,-4.10287020721939,
133.516488771841));
#112942=CARTESIAN_POINT('Ctrl Pts',(-153.560152887725,-4.02781811572429,
133.630026544641));
#112943=CARTESIAN_POINT('Ctrl Pts',(-153.567837748591,-3.9480812287841,
133.740398669932));
#112944=CARTESIAN_POINT('Ctrl Pts',(-153.575522609456,-3.86397253698667,
133.847204566229));
#112945=CARTESIAN_POINT('Ctrl Pts',(-153.583215873473,-3.77977187499904,
133.954127251389));
#112946=CARTESIAN_POINT('Ctrl Pts',(-153.590909137491,-3.69119011225881,
134.057475610537));
#112947=CARTESIAN_POINT('Ctrl Pts',(-153.598602401508,-3.59857970956993,
134.156883121051));
#112948=CARTESIAN_POINT('Ctrl Pts',(-153.606300583607,-3.50591010372204,
134.256354179918));
#112949=CARTESIAN_POINT('Ctrl Pts',(-153.613998765706,-3.40920701263355,
134.351879095128));
#112950=CARTESIAN_POINT('Ctrl Pts',(-153.621696947805,-3.30885770073661,
134.443130159427));
#112951=CARTESIAN_POINT('Ctrl Pts',(-153.629406090281,-3.2083655153262,
134.534511143503));
#112952=CARTESIAN_POINT('Ctrl Pts',(-153.637115232758,-3.10421705191336,
134.621605877482));
#112953=CARTESIAN_POINT('Ctrl Pts',(-153.644824375234,-2.99683063954928,
134.704128454291));
#112954=CARTESIAN_POINT('Ctrl Pts',(-153.647415150035,-2.96074179932616,
134.731861423703));
#112955=CARTESIAN_POINT('Ctrl Pts',(-153.650005924835,-2.92428748844057,
134.75907838895));
#112956=CARTESIAN_POINT('Ctrl Pts',(-153.652596699636,-2.887484224653,134.785769653935));
#112957=CARTESIAN_POINT('Ctrl Pts',(-153.660371033755,-2.77704588424454,
134.86586415385));
#112958=CARTESIAN_POINT('Ctrl Pts',(-153.668145367874,-2.66309753913652,
134.941486943402));
#112959=CARTESIAN_POINT('Ctrl Pts',(-153.675919701993,-2.54603725957195,
135.012314673324));
#112960=CARTESIAN_POINT('Ctrl Pts',(-153.68368445494,-2.42912124634028,
135.083055114399));
#112961=CARTESIAN_POINT('Ctrl Pts',(-153.691449207887,-2.30910126081001,
135.149012053506));
#112962=CARTESIAN_POINT('Ctrl Pts',(-153.699213960834,-2.18640690735201,
135.209903478325));
#112963=CARTESIAN_POINT('Ctrl Pts',(-153.706971001719,-2.06383441565523,
135.270734424923));
#112964=CARTESIAN_POINT('Ctrl Pts',(-153.714728042604,-1.93859318997076,
135.326509696751));
#112965=CARTESIAN_POINT('Ctrl Pts',(-153.722485083489,-1.81113986310011,
135.376991748413));
#112966=CARTESIAN_POINT('Ctrl Pts',(-153.730236274729,-1.68378264977487,
135.427435731167));
#112967=CARTESIAN_POINT('Ctrl Pts',(-153.737987465969,-1.55421701766041,
135.47259429552));
#112968=CARTESIAN_POINT('Ctrl Pts',(-153.74573865721,-1.42292181157704,
135.512276991148));
#112969=CARTESIAN_POINT('Ctrl Pts',(-153.753486553987,-1.2916824094585,
135.551942820571));
#112970=CARTESIAN_POINT('Ctrl Pts',(-153.761234450764,-1.15871526892059,
135.586137297395));
#112971=CARTESIAN_POINT('Ctrl Pts',(-153.768982347541,-1.02451651057077,
135.61471912625));
#112972=CARTESIAN_POINT('Ctrl Pts',(-153.776728623625,-0.890345823708212,
135.643294976403));
#112973=CARTESIAN_POINT('Ctrl Pts',(-153.784474899709,-0.754944413616102,
135.666260432437));
#112974=CARTESIAN_POINT('Ctrl Pts',(-153.792221175793,-0.618820381656688,
135.683524931026));
#112975=CARTESIAN_POINT('Ctrl Pts',(-153.799967509058,-0.482695344860406,
135.700789557059));
#112976=CARTESIAN_POINT('Ctrl Pts',(-153.807713842324,-0.345848063410923,
135.712353092482));
#112977=CARTESIAN_POINT('Ctrl Pts',(-153.815460175589,-0.208793184182127,
135.718176697634));
#112978=CARTESIAN_POINT('Ctrl Pts',(-153.823208243592,-0.0717076124639604,
135.724001606943));
#112979=CARTESIAN_POINT('Ctrl Pts',(-153.830956311595,0.0655852590054131,
135.724084011554));
#112980=CARTESIAN_POINT('Ctrl Pts',(-153.838704379598,0.202569748852529,
135.71843718996));
#112981=CARTESIAN_POINT('Ctrl Pts',(-153.84646068234,0.339699827445778,
135.712784366856));
#112982=CARTESIAN_POINT('Ctrl Pts',(-153.854216985082,0.476520478441192,
135.701390170063));
#112983=CARTESIAN_POINT('Ctrl Pts',(-153.861973287824,0.612519554506488,
135.684319926602));
#112984=CARTESIAN_POINT('Ctrl Pts',(-153.869733730338,0.748591217373533,
135.667240572238));
#112985=CARTESIAN_POINT('Ctrl Pts',(-153.877494172852,0.883840046208596,
135.64447919957));
#112986=CARTESIAN_POINT('Ctrl Pts',(-153.885254615366,1.0177640565039,135.616152320018));
#112987=CARTESIAN_POINT('Ctrl Pts',(-153.893027515632,1.15190305350974,
135.587779967645));
#112988=CARTESIAN_POINT('Ctrl Pts',(-153.900800415897,1.28471260311983,
135.553824351819));
#112989=CARTESIAN_POINT('Ctrl Pts',(-153.908573316162,1.41570498674655,
135.514452172196));
#112990=CARTESIAN_POINT('Ctrl Pts',(-153.916063651924,1.54193546727675,
135.476511270477));
#112991=CARTESIAN_POINT('Ctrl Pts',(-153.923553987686,1.66647831402322,
135.433540879754));
#112992=CARTESIAN_POINT('Ctrl Pts',(-153.931044323448,1.78891642750466,
135.385731709052));
#112993=CARTESIAN_POINT('Ctrl Pts',(-153.938818657567,1.91599681927462,
135.336109839112));
#112994=CARTESIAN_POINT('Ctrl Pts',(-153.946592991686,2.04121227774682,
135.28111783413));
#112995=CARTESIAN_POINT('Ctrl Pts',(-153.954367325805,2.164075593337,135.220915823699));
#112996=CARTESIAN_POINT('Ctrl Pts',(-153.962132078752,2.28678749087133,
135.160788006867));
#112997=CARTESIAN_POINT('Ctrl Pts',(-153.9698968317,2.40715266556961,135.095463130572));
#112998=CARTESIAN_POINT('Ctrl Pts',(-153.977661584647,2.52470164082529,
135.025150198594));
#112999=CARTESIAN_POINT('Ctrl Pts',(-153.985418625532,2.64213386478127,
134.954907102411));
#113000=CARTESIAN_POINT('Ctrl Pts',(-153.993175666416,2.75675512227696,
134.879686009037));
#113001=CARTESIAN_POINT('Ctrl Pts',(-154.000932707301,2.86811873846036,
134.799742697492));
#113002=CARTESIAN_POINT('Ctrl Pts',(-154.008683898542,2.97939837447466,
134.719859671819));
#113003=CARTESIAN_POINT('Ctrl Pts',(-154.016435089782,3.08742494259636,
134.635261743125));
#113004=CARTESIAN_POINT('Ctrl Pts',(-154.024186281022,3.19177938425175,
134.546248834064));
#113005=CARTESIAN_POINT('Ctrl Pts',(-154.031934177799,3.29608947248583,
134.457273757864));
#113006=CARTESIAN_POINT('Ctrl Pts',(-154.039682074576,3.3967302416395,134.363887686674));
#113007=CARTESIAN_POINT('Ctrl Pts',(-154.047429971353,3.49331465060994,
134.266431647215));
#113008=CARTESIAN_POINT('Ctrl Pts',(-154.055176247437,3.58987885620415,
134.168995993458));
#113009=CARTESIAN_POINT('Ctrl Pts',(-154.062922523521,3.68238811429914,
134.067492342329));
#113010=CARTESIAN_POINT('Ctrl Pts',(-154.070668799605,3.77049159020739,
133.962299222206));
#113011=CARTESIAN_POINT('Ctrl Pts',(-154.078415132871,3.85859571647536,
133.857105325571));
#113012=CARTESIAN_POINT('Ctrl Pts',(-154.086161466136,3.94229374462713,
133.748222205323));
#113013=CARTESIAN_POINT('Ctrl Pts',(-154.093907799401,4.02127481854961,
133.636061854667));
#113014=CARTESIAN_POINT('Ctrl Pts',(-154.101655867404,4.1002735797363,133.523876386477));
#113015=CARTESIAN_POINT('Ctrl Pts',(-154.109403935407,4.17455305966423,
133.408412547079));
#113016=CARTESIAN_POINT('Ctrl Pts',(-154.11715200341,4.24384569152576,133.290111371165));
#113017=CARTESIAN_POINT('Ctrl Pts',(-154.124908306152,4.31321196842056,
133.171684463354));
#113018=CARTESIAN_POINT('Ctrl Pts',(-154.132664608894,4.37758061185115,
133.050414533025));
#113019=CARTESIAN_POINT('Ctrl Pts',(-154.140420911636,4.43672975514852,
132.926767775083));
#113020=CARTESIAN_POINT('Ctrl Pts',(-154.14818135415,4.49591046812495,132.803055023143));
#113021=CARTESIAN_POINT('Ctrl Pts',(-154.155941796664,4.54986597628541,
132.676963275094));
#113022=CARTESIAN_POINT('Ctrl Pts',(-154.163702239178,4.59842296910078,
132.548977841987));
#113023=CARTESIAN_POINT('Ctrl Pts',(-154.171475139444,4.64705790991157,
132.420786955302));
#113024=CARTESIAN_POINT('Ctrl Pts',(-154.179248039709,4.69027689426186,
132.290696680087));
#113025=CARTESIAN_POINT('Ctrl Pts',(-154.187020939975,4.72795654748498,
132.15920745304));
#113026=CARTESIAN_POINT('Ctrl Pts',(-154.194511275737,4.76426645040473,
132.032498190596));
#113027=CARTESIAN_POINT('Ctrl Pts',(-154.202001611499,4.79543269450047,
131.904490220591));
#113028=CARTESIAN_POINT('Ctrl Pts',(-154.209491947261,4.82139027621796,
131.77563754352));
#113029=CARTESIAN_POINT('Ctrl Pts',(-154.21726628138,4.84833204753548,131.641899378036));
#113030=CARTESIAN_POINT('Ctrl Pts',(-154.225040615499,4.86974773015148,
131.50682754459));
#113031=CARTESIAN_POINT('Ctrl Pts',(-154.232814949618,4.88550869694688,
131.37091850036));
#113032=CARTESIAN_POINT('Ctrl Pts',(-154.240579702565,4.90125023975931,
131.235176951881));
#113033=CARTESIAN_POINT('Ctrl Pts',(-154.248344455512,4.91135088824354,
131.098600630203));
#113034=CARTESIAN_POINT('Ctrl Pts',(-154.256109208459,4.91573271962358,
130.961697490937));
#113035=CARTESIAN_POINT('Ctrl Pts',(-154.263866249344,4.92011019890692,
130.824930325799));
#113036=CARTESIAN_POINT('Ctrl Pts',(-154.27162329023,4.91878015213563,130.687837377279));
#113037=CARTESIAN_POINT('Ctrl Pts',(-154.279380331115,4.9117163347749,130.550932700388));
#113038=CARTESIAN_POINT('Ctrl Pts',(-154.287131522355,4.90465784429375,
130.414131264377));
#113039=CARTESIAN_POINT('Ctrl Pts',(-154.294882713595,4.89187420971017,
130.277518206265));
#113040=CARTESIAN_POINT('Ctrl Pts',(-154.302633904835,4.87339125305414,
130.141608207419));
#113041=CARTESIAN_POINT('Ctrl Pts',(-154.310381801612,4.85491615214787,
130.005755973949));
#113042=CARTESIAN_POINT('Ctrl Pts',(-154.318129698389,4.83074659964008,
129.870606592006));
#113043=CARTESIAN_POINT('Ctrl Pts',(-154.325877595166,4.8009603057981,129.736670023503));
#113044=CARTESIAN_POINT('Ctrl Pts',(-154.33362387125,4.77118024260667,129.602761471642));
#113045=CARTESIAN_POINT('Ctrl Pts',(-154.341370147335,4.73578585984384,
129.470065610009));
#113046=CARTESIAN_POINT('Ctrl Pts',(-154.349116423419,4.69490598943539,
129.339082209596));
#113047=CARTESIAN_POINT('Ctrl Pts',(-154.356862756684,4.65402581726097,
129.208097842293));
#113048=CARTESIAN_POINT('Ctrl Pts',(-154.364609089949,4.60766019311983,
129.078826334645));
#113049=CARTESIAN_POINT('Ctrl Pts',(-154.372355423215,4.55598771324147,
128.951751911095));
#113050=CARTESIAN_POINT('Ctrl Pts',(-154.380103491218,4.50430366166957,
128.824649030109));
#113051=CARTESIAN_POINT('Ctrl Pts',(-154.387851559221,4.44731053675606,
128.699744574386));
#113052=CARTESIAN_POINT('Ctrl Pts',(-154.395599627224,4.38523476708398,
128.577502045483));
#113053=CARTESIAN_POINT('Ctrl Pts',(-154.403355929965,4.32309302254526,
128.455129595767));
#113054=CARTESIAN_POINT('Ctrl Pts',(-154.411112232707,4.25585801968156,
128.335425073508));
#113055=CARTESIAN_POINT('Ctrl Pts',(-154.418868535449,4.18380205711718,
128.218827131153));
#113056=CARTESIAN_POINT('Ctrl Pts',(-154.426628977963,4.11170763611583,
128.102166956966));
#113057=CARTESIAN_POINT('Ctrl Pts',(-154.434389420477,4.03478734747495,
127.988616990068));
#113058=CARTESIAN_POINT('Ctrl Pts',(-154.442149862992,3.95335581855366,
127.878585363995));
#113059=CARTESIAN_POINT('Ctrl Pts',(-154.449922763257,3.87179356851299,
127.768377105388));
#113060=CARTESIAN_POINT('Ctrl Pts',(-154.457695663523,3.78570585235007,
127.661698778443));
#113061=CARTESIAN_POINT('Ctrl Pts',(-154.465468563788,3.69544701461065,
127.558924680022));
#113062=CARTESIAN_POINT('Ctrl Pts',(-154.47295889955,3.60846931297158,127.45988667895));
#113063=CARTESIAN_POINT('Ctrl Pts',(-154.480449235312,3.51761869864603,
127.364474200564));
#113064=CARTESIAN_POINT('Ctrl Pts',(-154.487939571074,3.42324199909756,
127.272987332551));
#113065=CARTESIAN_POINT('Ctrl Pts',(-154.495713905193,3.32528697829986,
127.17803171213));
#113066=CARTESIAN_POINT('Ctrl Pts',(-154.503488239312,3.22322291894911,
127.087004466531));
#113067=CARTESIAN_POINT('Ctrl Pts',(-154.511262573431,3.11739797843007,
127.000282160623));
#113068=CARTESIAN_POINT('Ctrl Pts',(-154.519027326378,3.01170345769294,
126.913666732206));
#113069=CARTESIAN_POINT('Ctrl Pts',(-154.526792079326,2.90225757745008,
126.831345932642));
#113070=CARTESIAN_POINT('Ctrl Pts',(-154.534556832273,2.78944557598048,
126.753659882984));
#113071=CARTESIAN_POINT('Ctrl Pts',(-154.542313873158,2.6767456209805,126.676050992205));
#113072=CARTESIAN_POINT('Ctrl Pts',(-154.550070914043,2.56068651794759,
126.603067910866));
#113073=CARTESIAN_POINT('Ctrl Pts',(-154.557827954928,2.44168657010954,
126.535010578526));
#113074=CARTESIAN_POINT('Ctrl Pts',(-154.565579146168,2.32277636105768,
126.467004568751));
#113075=CARTESIAN_POINT('Ctrl Pts',(-154.573330337408,2.20093005943492,
126.403917107708));
#113076=CARTESIAN_POINT('Ctrl Pts',(-154.581081528648,2.07659463869087,
126.346004668445));
#113077=CARTESIAN_POINT('Ctrl Pts',(-154.588829425425,1.95231206381791,
126.288116843514));
#113078=CARTESIAN_POINT('Ctrl Pts',(-154.596577322203,1.8255428276547,126.235399830409));
#113079=CARTESIAN_POINT('Ctrl Pts',(-154.60432521898,1.69675797989939,126.188063896151));
#113080=CARTESIAN_POINT('Ctrl Pts',(-154.612071495064,1.56800007115794,
126.14073786355));
#113081=CARTESIAN_POINT('Ctrl Pts',(-154.619817771148,1.43722775618427,
126.0987908057));
#113082=CARTESIAN_POINT('Ctrl Pts',(-154.627564047232,1.30493114327146,
126.062384471082));
#113083=CARTESIAN_POINT('Ctrl Pts',(-154.635310380497,1.17263355377529,
126.025977867721));
#113084=CARTESIAN_POINT('Ctrl Pts',(-154.643056713763,1.03881202084012,
125.995112172938));
#113085=CARTESIAN_POINT('Ctrl Pts',(-154.650803047028,0.903970471827993,
125.969898863807));
#113086=CARTESIAN_POINT('Ctrl Pts',(-154.658551115031,0.769098725986079,
125.944679908329));
#113087=CARTESIAN_POINT('Ctrl Pts',(-154.666299183034,0.63320689375795,
125.925115929169));
#113088=CARTESIAN_POINT('Ctrl Pts',(-154.674047251037,0.4968073223112,125.91126695946));
#113089=CARTESIAN_POINT('Ctrl Pts',(-154.681803553779,0.360262783776184,
125.897403270901));
#113090=CARTESIAN_POINT('Ctrl Pts',(-154.689559856521,0.22320981763661,
125.889266764778));
#113091=CARTESIAN_POINT('Ctrl Pts',(-154.697316159263,0.0861646586768549,
125.886865450909));
#113092=CARTESIAN_POINT('Ctrl Pts',(-154.705076601777,-0.0509536454105864,
125.884462855386));
#113093=CARTESIAN_POINT('Ctrl Pts',(-154.712837044291,-0.188063743357137,
125.887801541996));
#113094=CARTESIAN_POINT('Ctrl Pts',(-154.720597486805,-0.324652197088056,
125.896837411974));
#113095=CARTESIAN_POINT('Ctrl Pts',(-154.728370387071,-0.461459914730657,
125.905887787133));
#113096=CARTESIAN_POINT('Ctrl Pts',(-154.736143287336,-0.597743925872199,
125.920653579395));
#113097=CARTESIAN_POINT('Ctrl Pts',(-154.743916187602,-0.732997792081342,
125.941038985255));
#113098=CARTESIAN_POINT('Ctrl Pts',(-154.751406523364,-0.863334839565459,
125.960683330264));
#113099=CARTESIAN_POINT('Ctrl Pts',(-154.758896859125,-0.992715036042196,
125.985545749971));
#113100=CARTESIAN_POINT('Ctrl Pts',(-154.766387194887,-1.12069844052577,
126.015496653336));
#113101=CARTESIAN_POINT('Ctrl Pts',(-154.774161529006,-1.25353437469434,
126.046583154306));
#113102=CARTESIAN_POINT('Ctrl Pts',(-154.781935863125,-1.38528629157488,
126.083250088331));
#113103=CARTESIAN_POINT('Ctrl Pts',(-154.789710197244,-1.51544918890696,
126.125408083254));
#113104=CARTESIAN_POINT('Ctrl Pts',(-154.797474950192,-1.64545167210001,
126.167514122216));
#113105=CARTESIAN_POINT('Ctrl Pts',(-154.805239703139,-1.77386866385468,
126.215097637971));
#113106=CARTESIAN_POINT('Ctrl Pts',(-154.813004456086,-1.90020577999547,
126.268018362382));
#113107=CARTESIAN_POINT('Ctrl Pts',(-154.820761496971,-2.02641741633215,
126.320886525183));
#113108=CARTESIAN_POINT('Ctrl Pts',(-154.828518537856,-2.15055292974125,
126.379081197354));
#113109=CARTESIAN_POINT('Ctrl Pts',(-154.836275578741,-2.27213386946351,
126.442412573201));
#113110=CARTESIAN_POINT('Ctrl Pts',(-154.844026769981,-2.39362312405253,
126.505696190365));
#113111=CARTESIAN_POINT('Ctrl Pts',(-154.851777961221,-2.51256129404445,
126.574108621096));
#113112=CARTESIAN_POINT('Ctrl Pts',(-154.859529152461,-2.62849100133433,
126.647412443917));
#113113=CARTESIAN_POINT('Ctrl Pts',(-154.867277049238,-2.74437143540687,
126.720685110659));
#113114=CARTESIAN_POINT('Ctrl Pts',(-154.875024946015,-2.85724562021281,
126.798844826066));
#113115=CARTESIAN_POINT('Ctrl Pts',(-154.882772842792,-2.96668203828371,
126.881608937148));
#113116=CARTESIAN_POINT('Ctrl Pts',(-154.890519118876,-3.07609556461512,
126.964355735762));
#113117=CARTESIAN_POINT('Ctrl Pts',(-154.89826539496,-3.18207244292137,
127.051704778632));
#113118=CARTESIAN_POINT('Ctrl Pts',(-154.906011671044,-3.2842116741203,
127.143331152774));
#113119=CARTESIAN_POINT('Ctrl Pts',(-154.91375800431,-3.38635165928769,
127.234958203282));
#113120=CARTESIAN_POINT('Ctrl Pts',(-154.921504337575,-3.48465364979472,
127.330862386996));
#113121=CARTESIAN_POINT('Ctrl Pts',(-154.929250670841,-3.57875147177427,
127.430679991636));
#113122=CARTESIAN_POINT('Ctrl Pts',(-154.936998738843,-3.67287036630849,
127.530519949736));
#113123=CARTESIAN_POINT('Ctrl Pts',(-154.944746806846,-3.76278295071859,
127.634274788234));
#113124=CARTESIAN_POINT('Ctrl Pts',(-154.952494874849,-3.84816178126991,
127.74154590432));
#113125=CARTESIAN_POINT('Ctrl Pts',(-154.960251177591,-3.93363135345848,
127.848931029426));
#113126=CARTESIAN_POINT('Ctrl Pts',(-154.968007480333,-4.01455730240066,
127.959839591076));
#113127=CARTESIAN_POINT('Ctrl Pts',(-154.975763783075,-4.09065385169935,
128.073841595827));
#113128=CARTESIAN_POINT('Ctrl Pts',(-154.983524225589,-4.16679101601782,
128.187904446881));
#113129=CARTESIAN_POINT('Ctrl Pts',(-154.991284668103,-4.23809344145754,
128.305063697107));
#113130=CARTESIAN_POINT('Ctrl Pts',(-154.999045110617,-4.30432070373601,
128.424863540054));
#113131=CARTESIAN_POINT('Ctrl Pts',(-155.006818010883,-4.3706542798951,
128.544855696343));
#113132=CARTESIAN_POINT('Ctrl Pts',(-155.014590911148,-4.4318962376198,
128.667496566072));
#113133=CARTESIAN_POINT('Ctrl Pts',(-155.022363811414,-4.4878534367707,
128.79230828411));
#113134=CARTESIAN_POINT('Ctrl Pts',(-155.029854147176,-4.54177645078616,
128.912582781819));
#113135=CARTESIAN_POINT('Ctrl Pts',(-155.037344482938,-4.59079214943105,
129.03487275051));
#113136=CARTESIAN_POINT('Ctrl Pts',(-155.0448348187,-4.63477176247094,129.158738008247));
#113137=CARTESIAN_POINT('Ctrl Pts',(-155.053246583428,-4.68416155879476,
129.297840638497));
#113138=CARTESIAN_POINT('Ctrl Pts',(-155.061658348155,-4.72732056080959,
129.439264937836));
#113139=CARTESIAN_POINT('Ctrl Pts',(-155.070070112883,-4.76405452823396,
129.582490119308));
#113140=CARTESIAN_POINT('Origin',(213.235140564004,0.,130.804360617566));
#113141=CARTESIAN_POINT('',(-157.165002070592,-4.7640545282341,129.582490119308));
#113142=CARTESIAN_POINT('',(-156.820024427474,-4.76405452823416,129.582490119309));
#113143=CARTESIAN_POINT('',(213.235140564004,-4.76405452823405,129.582490119308));
#113144=CARTESIAN_POINT('',(-155.485140564065,-4.91824868045241,130.807963356535));
#113145=CARTESIAN_POINT('Ctrl Pts',(-155.485140564065,-4.91824868045242,
130.807963356535));
#113146=CARTESIAN_POINT('Ctrl Pts',(-155.494049736137,-4.91813304233005,
130.96582576278));
#113147=CARTESIAN_POINT('Ctrl Pts',(-155.502958908209,-4.91041303307629,
131.123380682287));
#113148=CARTESIAN_POINT('Ctrl Pts',(-155.511868080281,-4.89520103050853,
131.279954912536));
#113149=CARTESIAN_POINT('Ctrl Pts',(-155.52082239596,-4.8799119473028,131.437322519036));
#113150=CARTESIAN_POINT('Ctrl Pts',(-155.529776711638,-4.85705486365668,
131.59369933755));
#113151=CARTESIAN_POINT('Ctrl Pts',(-155.538731027317,-4.82679328265685,
131.748420821684));
#113152=CARTESIAN_POINT('Ctrl Pts',(-155.547742254425,-4.79633936648892,
131.904125677527));
#113153=CARTESIAN_POINT('Ctrl Pts',(-155.556753481532,-4.75838661846912,
132.058153957194));
#113154=CARTESIAN_POINT('Ctrl Pts',(-155.56576470864,-4.71315011348257,
132.209849525484));
#113155=CARTESIAN_POINT('Ctrl Pts',(-155.571223495815,-4.68574691408184,
132.301743094787));
#113156=CARTESIAN_POINT('Ctrl Pts',(-155.57668228299,-4.65567176233512,
132.392781059726));
#113157=CARTESIAN_POINT('Ctrl Pts',(-155.582141070166,-4.62298083148197,
132.482821607357));
#113158=CARTESIAN_POINT('Ctrl Pts',(-155.589915404285,-4.5764228304176,
132.61105619117));
#113159=CARTESIAN_POINT('Ctrl Pts',(-155.597689738404,-4.52445148752097,
132.737555247174));
#113160=CARTESIAN_POINT('Ctrl Pts',(-155.605464072523,-4.4672151945854,
132.861827863421));
#113161=CARTESIAN_POINT('Ctrl Pts',(-155.61322882547,-4.41004944026551,
132.985947324774));
#113162=CARTESIAN_POINT('Ctrl Pts',(-155.620993578417,-4.3476318082313,
133.107845454187));
#113163=CARTESIAN_POINT('Ctrl Pts',(-155.628758331364,-4.28015997592845,
133.227047894736));
#113164=CARTESIAN_POINT('Ctrl Pts',(-155.636515372249,-4.21275515760082,
133.34613194174));
#113165=CARTESIAN_POINT('Ctrl Pts',(-155.644272413134,-4.14030632017784,
133.462525289979));
#113166=CARTESIAN_POINT('Ctrl Pts',(-155.652029454019,-4.0630584500564,
133.575775255242));
#113167=CARTESIAN_POINT('Ctrl Pts',(-155.659780645259,-3.98586883315461,
133.688939817825));
#113168=CARTESIAN_POINT('Ctrl Pts',(-155.667531836499,-3.90388760634622,
133.798965393991));
#113169=CARTESIAN_POINT('Ctrl Pts',(-155.675283027739,-3.81740454966709,
133.905425848528));
#113170=CARTESIAN_POINT('Ctrl Pts',(-155.683030924516,-3.73095825059394,
134.011841054532));
#113171=CARTESIAN_POINT('Ctrl Pts',(-155.690778821293,-3.64001417324846,
134.114693849845));
#113172=CARTESIAN_POINT('Ctrl Pts',(-155.69852671807,-3.54490395822348,
134.213589121124));
#113173=CARTESIAN_POINT('Ctrl Pts',(-155.706272994155,-3.44981363820514,
134.312463705643));
#113174=CARTESIAN_POINT('Ctrl Pts',(-155.714019270239,-3.35055918473857,
134.407382131109));
#113175=CARTESIAN_POINT('Ctrl Pts',(-155.721765546323,-3.24751059812876,
134.497984580227));
#113176=CARTESIAN_POINT('Ctrl Pts',(-155.729511879588,-3.14446125083784,
134.588587698151));
#113177=CARTESIAN_POINT('Ctrl Pts',(-155.737258212854,-3.0376180081332,
134.674874518001));
#113178=CARTESIAN_POINT('Ctrl Pts',(-155.745004546119,-2.92738528488649,
134.756524386482));
#113179=CARTESIAN_POINT('Ctrl Pts',(-155.752752614122,-2.81712787578586,
134.838192539884));
#113180=CARTESIAN_POINT('Ctrl Pts',(-155.760500682125,-2.70347978982842,
134.915221442934));
#113181=CARTESIAN_POINT('Ctrl Pts',(-155.768248750128,-2.58687551383483,
134.987333022259));
#113182=CARTESIAN_POINT('Ctrl Pts',(-155.77600505287,-2.47014730942894,
135.059521242629));
#113183=CARTESIAN_POINT('Ctrl Pts',(-155.783761355611,-2.3504569718014,
135.126781493431));
#113184=CARTESIAN_POINT('Ctrl Pts',(-155.791517658353,-2.22826523741797,
135.188880784496));
#113185=CARTESIAN_POINT('Ctrl Pts',(-155.799278100868,-2.10600828562643,
135.251013219822));
#113186=CARTESIAN_POINT('Ctrl Pts',(-155.807038543382,-1.98124763230917,
135.30797904441));
#113187=CARTESIAN_POINT('Ctrl Pts',(-155.814798985896,-1.85446428978654,
135.359593351511));
#113188=CARTESIAN_POINT('Ctrl Pts',(-155.822571886161,-1.7274774233872,
135.41129051448));
#113189=CARTESIAN_POINT('Ctrl Pts',(-155.830344786427,-1.59846174741381,
135.457618860738));
#113190=CARTESIAN_POINT('Ctrl Pts',(-155.838117686692,-1.4679145937986,
135.498443042046));
#113191=CARTESIAN_POINT('Ctrl Pts',(-155.845608022454,-1.34211315804398,
135.537783161534));
#113192=CARTESIAN_POINT('Ctrl Pts',(-155.853098358217,-1.21488995509605,
135.572012268845));
#113193=CARTESIAN_POINT('Ctrl Pts',(-155.860588693979,-1.0866972948005,
135.601054484384));
#113194=CARTESIAN_POINT('Ctrl Pts',(-155.868363028098,-0.953644170828582,
135.631197844353));
#113195=CARTESIAN_POINT('Ctrl Pts',(-155.876137362217,-0.819125152066657,
135.65584871135));
#113196=CARTESIAN_POINT('Ctrl Pts',(-155.883911696336,-0.683633466029421,
135.674866581696));
#113197=CARTESIAN_POINT('Ctrl Pts',(-155.891676449283,-0.548308761385986,
135.693861014216));
#113198=CARTESIAN_POINT('Ctrl Pts',(-155.89944120223,-0.412014158026778,
135.707236209101));
#113199=CARTESIAN_POINT('Ctrl Pts',(-155.907205955177,-0.275255595353761,
135.714902076481));
#113200=CARTESIAN_POINT('Ctrl Pts',(-155.914962996062,-0.138632863213149,
135.722560330014));
#113201=CARTESIAN_POINT('Ctrl Pts',(-155.922720036947,-0.00154747661975313,
135.724520519021));
#113202=CARTESIAN_POINT('Ctrl Pts',(-155.930477077832,0.135487287246631,
135.720744070623));
#113203=CARTESIAN_POINT('Ctrl Pts',(-155.938228269072,0.272418712131794,
135.716970470074));
#113204=CARTESIAN_POINT('Ctrl Pts',(-155.945979460312,0.409299201039463,
135.707468853573));
#113205=CARTESIAN_POINT('Ctrl Pts',(-155.953730651553,0.545613601159354,
135.69225268478));
#113206=CARTESIAN_POINT('Ctrl Pts',(-155.96147854833,0.681870064023075,
135.677042983264));
#113207=CARTESIAN_POINT('Ctrl Pts',(-155.969226445107,0.817560528901214,
135.656123603509));
#113208=CARTESIAN_POINT('Ctrl Pts',(-155.976974341884,0.952173315904815,
135.629559995724));
#113209=CARTESIAN_POINT('Ctrl Pts',(-155.984720617968,1.08675794481492,
135.603001944474));
#113210=CARTESIAN_POINT('Ctrl Pts',(-155.992466894052,1.22026496091177,
135.570802089215));
#113211=CARTESIAN_POINT('Ctrl Pts',(-156.000213170136,1.35219164551349,
135.533077231649));
#113212=CARTESIAN_POINT('Ctrl Pts',(-156.007959503401,1.48411930396821,
135.495352095606));
#113213=CARTESIAN_POINT('Ctrl Pts',(-156.015705836667,1.61446623175116,
135.452101983362));
#113214=CARTESIAN_POINT('Ctrl Pts',(-156.023452169932,1.74274405804727,
135.403493819664));
#113215=CARTESIAN_POINT('Ctrl Pts',(-156.031200237935,1.87105061127299,
135.354874770505));
#113216=CARTESIAN_POINT('Ctrl Pts',(-156.038948305938,1.99728677544951,
135.300895420741));
#113217=CARTESIAN_POINT('Ctrl Pts',(-156.046696373941,2.12098374883439,
135.241771010991));
#113218=CARTESIAN_POINT('Ctrl Pts',(-156.054452676683,2.24481218883476,
135.182583763115));
#113219=CARTESIAN_POINT('Ctrl Pts',(-156.062208979425,2.36609569383071,
135.118240700744));
#113220=CARTESIAN_POINT('Ctrl Pts',(-156.069965282167,2.48438920328042,
135.049003517637));
#113221=CARTESIAN_POINT('Ctrl Pts',(-156.077725724681,2.60274584953787,
134.979729380561));
#113222=CARTESIAN_POINT('Ctrl Pts',(-156.085486167195,2.7181089916855,134.905556129177));
#113223=CARTESIAN_POINT('Ctrl Pts',(-156.093246609709,2.83006306353161,
134.826788506159));
#113224=CARTESIAN_POINT('Ctrl Pts',(-156.101019509974,2.94219685399266,
134.747894438361));
#113225=CARTESIAN_POINT('Ctrl Pts',(-156.10879241024,3.05091032803284,134.664391499036));
#113226=CARTESIAN_POINT('Ctrl Pts',(-156.116565310505,3.1558207932883,134.576624948594));
#113227=CARTESIAN_POINT('Ctrl Pts',(-156.124055646267,3.25691749887792,
134.492048933333));
#113228=CARTESIAN_POINT('Ctrl Pts',(-156.131545982029,3.35448266506848,
134.40351411814));
#113229=CARTESIAN_POINT('Ctrl Pts',(-156.139036317791,3.44820796768794,
134.311360029324));
#113230=CARTESIAN_POINT('Ctrl Pts',(-156.14681065191,3.54548689364354,134.215711890222));
#113231=CARTESIAN_POINT('Ctrl Pts',(-156.15458498603,3.63893718164784,134.115861625704));
#113232=CARTESIAN_POINT('Ctrl Pts',(-156.162359320149,3.72817402045526,
134.012148256376));
#113233=CARTESIAN_POINT('Ctrl Pts',(-156.170124073096,3.81730088283418,
133.908562704507));
#113234=CARTESIAN_POINT('Ctrl Pts',(-156.177888826043,3.90222437539272,
133.80112381418));
#113235=CARTESIAN_POINT('Ctrl Pts',(-156.18565357899,3.98259523036654,133.690208550767));
#113236=CARTESIAN_POINT('Ctrl Pts',(-156.193410619875,4.06288625987417,
133.579403449958));
#113237=CARTESIAN_POINT('Ctrl Pts',(-156.20116766076,4.13863342235182,133.465129161796));
#113238=CARTESIAN_POINT('Ctrl Pts',(-156.208924701645,4.20952682649004,
133.347796671325));
#113239=CARTESIAN_POINT('Ctrl Pts',(-156.216675892885,4.28036676936083,
133.230552662198));
#113240=CARTESIAN_POINT('Ctrl Pts',(-156.224427084125,4.34636003804496,
133.110255374414));
#113241=CARTESIAN_POINT('Ctrl Pts',(-156.232178275365,4.40723950722377,
132.98734549806));
#113242=CARTESIAN_POINT('Ctrl Pts',(-156.239926172142,4.46809310100409,
132.864487861683));
#113243=CARTESIAN_POINT('Ctrl Pts',(-156.24767406892,4.52383704503914,132.739020194886));
#113244=CARTESIAN_POINT('Ctrl Pts',(-156.255421965697,4.57424982896484,
132.611408365888));
#113245=CARTESIAN_POINT('Ctrl Pts',(-156.263168241781,4.62465206762291,
132.483823230534));
#113246=CARTESIAN_POINT('Ctrl Pts',(-156.270914517865,4.66972522073733,
132.354095188484));
#113247=CARTESIAN_POINT('Ctrl Pts',(-156.278660793949,4.70929582515879,
132.222710325375));
#113248=CARTESIAN_POINT('Ctrl Pts',(-156.286407127214,4.74886672168152,
132.091324492413));
#113249=CARTESIAN_POINT('Ctrl Pts',(-156.29415346048,4.78293487571136,131.958282188342));
#113250=CARTESIAN_POINT('Ctrl Pts',(-156.301899793745,4.81137674941061,
131.824084520263));
#113251=CARTESIAN_POINT('Ctrl Pts',(-156.309647861748,4.83982499247024,
131.689856799547));
#113252=CARTESIAN_POINT('Ctrl Pts',(-156.317395929751,4.86264436696675,
131.554473582365));
#113253=CARTESIAN_POINT('Ctrl Pts',(-156.325143997754,4.87976256213496,
131.418445627712));
#113254=CARTESIAN_POINT('Ctrl Pts',(-156.332900300496,4.89689895072467,
131.28227310093));
#113255=CARTESIAN_POINT('Ctrl Pts',(-156.340656603238,4.908322007026,131.145454856372));
#113256=CARTESIAN_POINT('Ctrl Pts',(-156.34841290598,4.91401133531657,131.008506787945));
#113257=CARTESIAN_POINT('Ctrl Pts',(-156.356173348494,4.91970370017297,
130.871485626209));
#113258=CARTESIAN_POINT('Ctrl Pts',(-156.363933791008,4.91965623932011,
130.734334893311));
#113259=CARTESIAN_POINT('Ctrl Pts',(-156.371694233522,4.91390071772362,
130.597568937716));
#113260=CARTESIAN_POINT('Ctrl Pts',(-156.379467133788,4.90813595685291,
130.460583433267));
#113261=CARTESIAN_POINT('Ctrl Pts',(-156.387240034053,4.89664485726546,
130.323984330253));
#113262=CARTESIAN_POINT('Ctrl Pts',(-156.395012934318,4.8795110417526,130.188280220285));
#113263=CARTESIAN_POINT('Ctrl Pts',(-156.402503270081,4.86300008359107,
130.057509296531));
#113264=CARTESIAN_POINT('Ctrl Pts',(-156.409993605843,4.84124959162055,
129.92756972883));
#113265=CARTESIAN_POINT('Ctrl Pts',(-156.417483941605,4.81437856219427,
129.798904441304));
#113266=CARTESIAN_POINT('Ctrl Pts',(-156.425258275724,4.78648870952013,
129.665360770294));
#113267=CARTESIAN_POINT('Ctrl Pts',(-156.433032609843,4.75299401739126,
129.532766889396));
#113268=CARTESIAN_POINT('Ctrl Pts',(-156.440806943962,4.71397171356682,
129.401629800127));
#113269=CARTESIAN_POINT('Ctrl Pts',(-156.448571696909,4.67499750124431,
129.270654325601));
#113270=CARTESIAN_POINT('Ctrl Pts',(-156.456336449856,4.63050934208417,
129.141132441591));
#113271=CARTESIAN_POINT('Ctrl Pts',(-156.464101202803,4.58063559997242,
129.01356175595));
#113272=CARTESIAN_POINT('Ctrl Pts',(-156.471858243688,4.53081139316444,
128.886117775313));
#113273=CARTESIAN_POINT('Ctrl Pts',(-156.479615284573,4.47561238966402,
128.760621498193));
#113274=CARTESIAN_POINT('Ctrl Pts',(-156.487372325458,4.41521685900641,
128.637555792381));
#113275=CARTESIAN_POINT('Ctrl Pts',(-156.495123516698,4.35486687308819,
128.514582891375));
#113276=CARTESIAN_POINT('Ctrl Pts',(-156.502874707938,4.2893283315785,128.394037262933));
#113277=CARTESIAN_POINT('Ctrl Pts',(-156.510625899179,4.21882761176835,
128.276381850907));
#113278=CARTESIAN_POINT('Ctrl Pts',(-156.518373795956,4.14835685664489,
128.158776445569));
#113279=CARTESIAN_POINT('Ctrl Pts',(-156.526121692733,4.07292831851209,
128.04405914808));
#113280=CARTESIAN_POINT('Ctrl Pts',(-156.53386958951,3.99281421373397,127.932668134534));
#113281=CARTESIAN_POINT('Ctrl Pts',(-156.541615865594,3.91271686709952,
127.821300421586));
#113282=CARTESIAN_POINT('Ctrl Pts',(-156.549362141678,3.82793613146532,
127.713257925821));
#113283=CARTESIAN_POINT('Ctrl Pts',(-156.557108417762,3.73878720337472,
127.60894932786));
#113284=CARTESIAN_POINT('Ctrl Pts',(-156.564854751027,3.64963761720686,
127.504639959916));
#113285=CARTESIAN_POINT('Ctrl Pts',(-156.572601084293,3.55612002825205,
127.404064841981));
#113286=CARTESIAN_POINT('Ctrl Pts',(-156.580347417558,3.45858925688764,
127.307598770565));
#113287=CARTESIAN_POINT('Ctrl Pts',(-156.588095485561,3.36103664418335,
127.211111096242));
#113288=CARTESIAN_POINT('Ctrl Pts',(-156.595843553564,3.25946933862601,
127.118734574394));
#113289=CARTESIAN_POINT('Ctrl Pts',(-156.603591621567,3.15427797048833,
127.030806119829));
#113290=CARTESIAN_POINT('Ctrl Pts',(-156.611347924309,3.04897480371294,
126.942784213856));
#113291=CARTESIAN_POINT('Ctrl Pts',(-156.61910422705,2.94004018062642,126.859220069917));
#113292=CARTESIAN_POINT('Ctrl Pts',(-156.626860529792,2.82789711299831,
126.780409700768));
#113293=CARTESIAN_POINT('Ctrl Pts',(-156.634620972306,2.71569419123814,
126.701557268153));
#113294=CARTESIAN_POINT('Ctrl Pts',(-156.642381414821,2.60027974159002,
126.627463877088));
#113295=CARTESIAN_POINT('Ctrl Pts',(-156.650141857335,2.48210366972528,
126.558380820719));
#113296=CARTESIAN_POINT('Ctrl Pts',(-156.6579147576,2.36373789113881,126.489186866094));
#113297=CARTESIAN_POINT('Ctrl Pts',(-156.665687657866,2.24260197707321,
126.425019501825));
#113298=CARTESIAN_POINT('Ctrl Pts',(-156.673460558131,2.11916902021499,
126.366083279875));
#113299=CARTESIAN_POINT('Ctrl Pts',(-156.680950893893,2.00022316224708,
126.309289538045));
#113300=CARTESIAN_POINT('Ctrl Pts',(-156.688441229655,1.87914465166531,
126.257353332653));
#113301=CARTESIAN_POINT('Ctrl Pts',(-156.695931565417,1.75637045351285,
126.210413960004));
#113302=CARTESIAN_POINT('Ctrl Pts',(-156.703705899536,1.62894123432155,
126.161694866774));
#113303=CARTESIAN_POINT('Ctrl Pts',(-156.711480233655,1.49928154781937,
126.11820466847));
#113304=CARTESIAN_POINT('Ctrl Pts',(-156.719254567774,1.36785969223231,
126.080152437895));
#113305=CARTESIAN_POINT('Ctrl Pts',(-156.727019320721,1.23659980233676,
126.042147103294));
#113306=CARTESIAN_POINT('Ctrl Pts',(-156.734784073668,1.10358243635882,
126.00956650951));
#113307=CARTESIAN_POINT('Ctrl Pts',(-156.742548826616,0.969295629694564,
125.98257162957));
#113308=CARTESIAN_POINT('Ctrl Pts',(-156.750305867501,0.835142198579437,
125.955603561326));
#113309=CARTESIAN_POINT('Ctrl Pts',(-156.758062908386,0.699722216696345,
125.934210243088));
#113310=CARTESIAN_POINT('Ctrl Pts',(-156.765819949271,0.563538293431292,
125.918502693482));
#113311=CARTESIAN_POINT('Ctrl Pts',(-156.773571140511,0.427457067522315,
125.902806989061));
#113312=CARTESIAN_POINT('Ctrl Pts',(-156.781322331751,0.290613433730575,
125.892788563518));
#113313=CARTESIAN_POINT('Ctrl Pts',(-156.789073522991,0.153519242285463,
125.888507191685));
#113314=CARTESIAN_POINT('Ctrl Pts',(-156.796821419768,0.0164833195286367,
125.884227639549));
#113315=CARTESIAN_POINT('Ctrl Pts',(-156.804569316545,-0.120802559117167,
125.885680303509));
#113316=CARTESIAN_POINT('Ctrl Pts',(-156.812317213322,-0.257822604099873,
125.892873005109));
#113317=CARTESIAN_POINT('Ctrl Pts',(-156.820063489406,-0.39481398744298,
125.900064202152));
#113318=CARTESIAN_POINT('Ctrl Pts',(-156.82780976549,-0.531539257547418,
125.912993028111));
#113319=CARTESIAN_POINT('Ctrl Pts',(-156.835556041575,-0.667484208402331,
125.931615201065));
#113320=CARTESIAN_POINT('Ctrl Pts',(-156.84330237484,-0.803430162771434,
125.950237511484));
#113321=CARTESIAN_POINT('Ctrl Pts',(-156.851048708105,-0.938595399049157,
125.974553199699));
#113322=CARTESIAN_POINT('Ctrl Pts',(-156.858795041371,-1.07247280123594,
126.004466331948));
#113323=CARTESIAN_POINT('Ctrl Pts',(-156.866543109374,-1.20638018433889,
126.034386163035));
#113324=CARTESIAN_POINT('Ctrl Pts',(-156.874291177376,-1.33899877798152,
126.069905847255));
#113325=CARTESIAN_POINT('Ctrl Pts',(-156.882039245379,-1.4698339809905,
126.11087884698));
#113326=CARTESIAN_POINT('Ctrl Pts',(-156.889795548121,-1.60080823721038,
126.151895393296));
#113327=CARTESIAN_POINT('Ctrl Pts',(-156.897551850863,-1.72999494282071,
126.198376715921));
#113328=CARTESIAN_POINT('Ctrl Pts',(-156.905308153605,-1.85691640571096,
126.250126925198));
#113329=CARTESIAN_POINT('Ctrl Pts',(-156.913068596119,-1.98390561040783,
126.30190475512));
#113330=CARTESIAN_POINT('Ctrl Pts',(-156.920829038633,-2.10862680793417,
126.358956912614));
#113331=CARTESIAN_POINT('Ctrl Pts',(-156.928589481148,-2.23062539324579,
126.421040709379));
#113332=CARTESIAN_POINT('Ctrl Pts',(-156.936362381413,-2.35281982151674,
126.483224168566));
#113333=CARTESIAN_POINT('Ctrl Pts',(-156.944135281679,-2.47228256285254,
126.550455216054));
#113334=CARTESIAN_POINT('Ctrl Pts',(-156.951908181944,-2.58858580373855,
126.622446390901));
#113335=CARTESIAN_POINT('Ctrl Pts',(-156.959398517706,-2.70066112886722,
126.691820505207));
#113336=CARTESIAN_POINT('Ctrl Pts',(-156.966888853468,-2.80980242184844,
126.765614497653));
#113337=CARTESIAN_POINT('Ctrl Pts',(-156.97437918923,-2.91565629847685,
126.843536030229));
#113338=CARTESIAN_POINT('Ctrl Pts',(-156.982321809287,-3.02790188403022,
126.926162650338));
#113339=CARTESIAN_POINT('Ctrl Pts',(-156.990264429343,-3.13683227136789,
127.013711797369));
#113340=CARTESIAN_POINT('Ctrl Pts',(-156.9982070494,-3.24198225670693,127.105883348514));
#113341=CARTESIAN_POINT('Ctrl Pts',(-157.005898703257,-3.34380977515242,
127.195142517634));
#113342=CARTESIAN_POINT('Ctrl Pts',(-157.013590357115,-3.44209181150377,
127.288736144081));
#113343=CARTESIAN_POINT('Ctrl Pts',(-157.021282010972,-3.53643426231045,
127.38634719295));
#113344=CARTESIAN_POINT('Ctrl Pts',(-157.028966694705,-3.63069122062843,
127.483869787348));
#113345=CARTESIAN_POINT('Ctrl Pts',(-157.036651378438,-3.72101541736759,
127.585402279919));
#113346=CARTESIAN_POINT('Ctrl Pts',(-157.044336062171,-3.80704667151909,
127.690588194383));
#113347=CARTESIAN_POINT('Ctrl Pts',(-157.052015522896,-3.89301945327776,
127.79570261771));
#113348=CARTESIAN_POINT('Ctrl Pts',(-157.059694983622,-3.97470484465933,
127.904465216283));
#113349=CARTESIAN_POINT('Ctrl Pts',(-157.067374444348,-4.05178067949858,
128.016483936695));
#113350=CARTESIAN_POINT('Ctrl Pts',(-157.075050424794,-4.12882158408524,
128.128451890973));
#113351=CARTESIAN_POINT('Ctrl Pts',(-157.082726405239,-4.2012568635084,
128.243672702675));
#113352=CARTESIAN_POINT('Ctrl Pts',(-157.090402385685,-4.26880600572468,
128.36172303741));
#113353=CARTESIAN_POINT('Ctrl Pts',(-157.098077877342,-4.33635084657299,
128.479765854982));
#113354=CARTESIAN_POINT('Ctrl Pts',(-157.105753369,-4.39900996460309,128.600637494883));
#113355=CARTESIAN_POINT('Ctrl Pts',(-157.113428860657,-4.4565475304664,
128.723887793616));
#113356=CARTESIAN_POINT('Ctrl Pts',(-157.121104166245,-4.51408370150439,
128.847135104516));
#113357=CARTESIAN_POINT('Ctrl Pts',(-157.128779471834,-4.5664984043857,
128.972760595479));
#113358=CARTESIAN_POINT('Ctrl Pts',(-157.136454777422,-4.61360324984863,
129.100292509923));
#113359=CARTESIAN_POINT('Ctrl Pts',(-157.144133411417,-4.66072852239329,
129.227879728759));
#113360=CARTESIAN_POINT('Ctrl Pts',(-157.151812045412,-4.70253920954631,
129.357374644865));
#113361=CARTESIAN_POINT('Ctrl Pts',(-157.159490679407,-4.73889629523923,
129.488288824134));
#113362=CARTESIAN_POINT('Ctrl Pts',(-157.161327809802,-4.74759480948431,
129.519610334963));
#113363=CARTESIAN_POINT('Ctrl Pts',(-157.163164940197,-4.75598137804317,
129.551013029241));
#113364=CARTESIAN_POINT('Ctrl Pts',(-157.165002070592,-4.7640545282341,
129.582490119308));
#113365=CARTESIAN_POINT('Ctrl Pts',(-155.415271106226,-4.76405452823407,
129.582490119308));
#113366=CARTESIAN_POINT('Ctrl Pts',(-155.423032857163,-4.79821772193378,
129.715691893045));
#113367=CARTESIAN_POINT('Ctrl Pts',(-155.4307946081,-4.82680380230719,129.850380280961));
#113368=CARTESIAN_POINT('Ctrl Pts',(-155.438556359037,-4.84969597482323,
129.986050154304));
#113369=CARTESIAN_POINT('Ctrl Pts',(-155.446320393199,-4.87259488138504,
130.121759936797));
#113370=CARTESIAN_POINT('Ctrl Pts',(-155.454084427362,-4.88979645416441,
130.258451400986));
#113371=CARTESIAN_POINT('Ctrl Pts',(-155.461848461524,-4.90123510417065,
130.395609451029));
#113372=CARTESIAN_POINT('Ctrl Pts',(-155.469612495686,-4.91267375417689,
130.532767501072));
#113373=CARTESIAN_POINT('Ctrl Pts',(-155.477376529849,-4.9183494550353,
130.670391749014));
#113374=CARTESIAN_POINT('Ctrl Pts',(-155.485140564011,-4.91824868045312,
130.807963355574));
#113375=CARTESIAN_POINT('',(-155.139859435941,-4.91824859371983,130.80064136053));
#113376=CARTESIAN_POINT('Ctrl Pts',(-155.070070112883,-4.76405452823396,
129.582490119308));
#113377=CARTESIAN_POINT('Ctrl Pts',(-155.079101386156,-4.80349387407437,
129.736263530164));
#113378=CARTESIAN_POINT('Ctrl Pts',(-155.088132659429,-4.83552633251772,
129.892113014839));
#113379=CARTESIAN_POINT('Ctrl Pts',(-155.097163932702,-4.85995645887181,
130.049373014774));
#113380=CARTESIAN_POINT('Ctrl Pts',(-155.106121891946,-4.88418826645835,
130.205356410203));
#113381=CARTESIAN_POINT('Ctrl Pts',(-155.11507985119,-4.90094059396684,
130.36272739353));
#113382=CARTESIAN_POINT('Ctrl Pts',(-155.124037810435,-4.91006984325492,
130.520816622993));
#113383=CARTESIAN_POINT('Ctrl Pts',(-155.129311685603,-4.91544456307824,
130.613889480205));
#113384=CARTESIAN_POINT('Ctrl Pts',(-155.134585560772,-4.91817794015085,
130.707210921886));
#113385=CARTESIAN_POINT('Ctrl Pts',(-155.139859435941,-4.91824859371983,
130.80064136053));
#113386=CARTESIAN_POINT('Ctrl Pts',(-155.139859435994,-4.91824859372054,
130.800641361475));
#113387=CARTESIAN_POINT('Ctrl Pts',(-155.147611646378,-4.91835244926784,
130.937977266002));
#113388=CARTESIAN_POINT('Ctrl Pts',(-155.155363856762,-4.91269960219612,
131.075373175227));
#113389=CARTESIAN_POINT('Ctrl Pts',(-155.163116067145,-4.90130174688514,
131.21231189956));
#113390=CARTESIAN_POINT('Ctrl Pts',(-155.170867366393,-4.88990523119227,
131.349234529147));
#113391=CARTESIAN_POINT('Ctrl Pts',(-155.17861866564,-4.87276508230385,
131.485699692495));
#113392=CARTESIAN_POINT('Ctrl Pts',(-155.186369964887,-4.84994500482501,
131.621193839633));
#113393=CARTESIAN_POINT('Ctrl Pts',(-155.194122017518,-4.82712270936145,
131.75670115605));
#113394=CARTESIAN_POINT('Ctrl Pts',(-155.201874070149,-4.79861945097126,
131.891236884105));
#113395=CARTESIAN_POINT('Ctrl Pts',(-155.209626122779,-4.76455027365204,
132.02429657996));
#113396=CARTESIAN_POINT('Ctrl Pts',(-155.217380593448,-4.73047046939316,
132.157397780116));
#113397=CARTESIAN_POINT('Ctrl Pts',(-155.225135064118,-4.69082138744712,
132.289021654418));
#113398=CARTESIAN_POINT('Ctrl Pts',(-155.232889534787,-4.64576815171044,
132.418678226667));
#113399=CARTESIAN_POINT('Ctrl Pts',(-155.240653107835,-4.60066203143611,
132.548486992821));
#113400=CARTESIAN_POINT('Ctrl Pts',(-155.248416680883,-4.55013921478554,
132.676323475793));
#113401=CARTESIAN_POINT('Ctrl Pts',(-155.256180253931,-4.49441350188924,
132.801716453799));
#113402=CARTESIAN_POINT('Ctrl Pts',(-155.263948538074,-4.43865397348732,
132.927185522837));
#113403=CARTESIAN_POINT('Ctrl Pts',(-155.271716822217,-4.37768543129941,
133.050207783983));
#113404=CARTESIAN_POINT('Ctrl Pts',(-155.27948510636,-4.31176754666298,
133.17033688246));
#113405=CARTESIAN_POINT('Ctrl Pts',(-155.287266329264,-4.24573986998919,
133.290666066522));
#113406=CARTESIAN_POINT('Ctrl Pts',(-155.295047552168,-4.17474658127562,
133.408092126304));
#113407=CARTESIAN_POINT('Ctrl Pts',(-155.302828775072,-4.09909104932332,
133.522197189521));
#113408=CARTESIAN_POINT('Ctrl Pts',(-155.309646664219,-4.03280185074966,
133.622175776661));
#113409=CARTESIAN_POINT('Ctrl Pts',(-155.316464553366,-3.96293409402055,
133.719605105171));
#113410=CARTESIAN_POINT('Ctrl Pts',(-155.323282442513,-3.88971625588467,
133.814226147985));
#113411=CARTESIAN_POINT('Ctrl Pts',(-155.331056776633,-3.80622708132492,
133.922121067607));
#113412=CARTESIAN_POINT('Ctrl Pts',(-155.338831110752,-3.71811299781759,
134.026710454927));
#113413=CARTESIAN_POINT('Ctrl Pts',(-155.346605444871,-3.62566520347868,
134.127572150825));
#113414=CARTESIAN_POINT('Ctrl Pts',(-155.354370197818,-3.53333134278399,
134.228309543697));
#113415=CARTESIAN_POINT('Ctrl Pts',(-155.362134950765,-3.43667465971446,
134.325328100484));
#113416=CARTESIAN_POINT('Ctrl Pts',(-155.369899703712,-3.33602822956078,
134.418236475156));
#113417=CARTESIAN_POINT('Ctrl Pts',(-155.377656744597,-3.23548176286012,
134.511052571922));
#113418=CARTESIAN_POINT('Ctrl Pts',(-155.385413785482,-3.13095372039143,
134.599766347042));
#113419=CARTESIAN_POINT('Ctrl Pts',(-155.393170826367,-3.02281560970584,
134.684021537314));
#113420=CARTESIAN_POINT('Ctrl Pts',(-155.400922017607,-2.91475904681087,
134.768213190091));
#113421=CARTESIAN_POINT('Ctrl Pts',(-155.408673208847,-2.80309814158936,
134.847952711063));
#113422=CARTESIAN_POINT('Ctrl Pts',(-155.416424400087,-2.68823894975632,
134.922922795258));
#113423=CARTESIAN_POINT('Ctrl Pts',(-155.424172296864,-2.57342857614361,
134.997861015167));
#113424=CARTESIAN_POINT('Ctrl Pts',(-155.431920193641,-2.45542294628743,
135.068033616874));
#113425=CARTESIAN_POINT('Ctrl Pts',(-155.439668090418,-2.3346585053298,
135.133165617331));
#113426=CARTESIAN_POINT('Ctrl Pts',(-155.447414366502,-2.21391932568985,
135.198283993578));
#113427=CARTESIAN_POINT('Ctrl Pts',(-155.455160642586,-2.09042282669038,
135.258363680333));
#113428=CARTESIAN_POINT('Ctrl Pts',(-155.46290691867,-1.96463120417875,
135.313175017613));
#113429=CARTESIAN_POINT('Ctrl Pts',(-155.470653251936,-1.83883865310245,
135.367986759496));
#113430=CARTESIAN_POINT('Ctrl Pts',(-155.478399585201,-1.71075130312537,
135.417529918128));
#113431=CARTESIAN_POINT('Ctrl Pts',(-155.486145918466,-1.58085216303489,
135.461622635225));
#113432=CARTESIAN_POINT('Ctrl Pts',(-155.493893986469,-1.45092393293247,
135.50572522658));
#113433=CARTESIAN_POINT('Ctrl Pts',(-155.501642054472,-1.31918347549303,
135.544374821926));
#113434=CARTESIAN_POINT('Ctrl Pts',(-155.509390122475,-1.18612943420565,
135.577439291526));
#113435=CARTESIAN_POINT('Ctrl Pts',(-155.517146425217,-1.05293398149965,
135.610538902437));
#113436=CARTESIAN_POINT('Ctrl Pts',(-155.524902727959,-0.918422536130609,
135.638041435486));
#113437=CARTESIAN_POINT('Ctrl Pts',(-155.532659030701,-0.783104972180423,
135.659865706127));
#113438=CARTESIAN_POINT('Ctrl Pts',(-155.540419473215,-0.647715185171655,
135.681701625039));
#113439=CARTESIAN_POINT('Ctrl Pts',(-155.548179915729,-0.511518810327363,
135.697853196678));
#113440=CARTESIAN_POINT('Ctrl Pts',(-155.555940358243,-0.375030347737595,
135.708291214625));
#113441=CARTESIAN_POINT('Ctrl Pts',(-155.563713258509,-0.238322781751173,
135.718745988606));
#113442=CARTESIAN_POINT('Ctrl Pts',(-155.571486158774,-0.101322581995252,
135.723468867033));
#113443=CARTESIAN_POINT('Ctrl Pts',(-155.57925905904,0.0354553431398876,
135.722482818279));
#113444=CARTESIAN_POINT('Ctrl Pts',(-155.586749394801,0.167261046172449,
135.72153261488));
#113445=CARTESIAN_POINT('Ctrl Pts',(-155.594239730563,0.298860046827601,
135.715281360497));
#113446=CARTESIAN_POINT('Ctrl Pts',(-155.601730066325,0.429798466647812,
135.703794905376));
#113447=CARTESIAN_POINT('Ctrl Pts',(-155.609504400444,0.565701456453974,
135.691872937818));
#113448=CARTESIAN_POINT('Ctrl Pts',(-155.617278734563,0.701323284573325,
135.674273182427));
#113449=CARTESIAN_POINT('Ctrl Pts',(-155.625053068683,0.836151376887149,
135.651012445109));
#113450=CARTESIAN_POINT('Ctrl Pts',(-155.63281782163,0.970813305627494,
135.627780374571));
#113451=CARTESIAN_POINT('Ctrl Pts',(-155.640582574577,1.10468306333046,
135.598901269399));
#113452=CARTESIAN_POINT('Ctrl Pts',(-155.648347327524,1.23725136416848,
135.564443823179));
#113453=CARTESIAN_POINT('Ctrl Pts',(-155.656104368409,1.36968799630085,
135.530020600582));
#113454=CARTESIAN_POINT('Ctrl Pts',(-155.663861409294,1.50082536800743,
135.490030160472));
#113455=CARTESIAN_POINT('Ctrl Pts',(-155.671618450179,1.63016293605966,
135.444592493712));
#113456=CARTESIAN_POINT('Ctrl Pts',(-155.679369641419,1.7594029696459,135.399189091849));
#113457=CARTESIAN_POINT('Ctrl Pts',(-155.687120832659,1.88684553372126,
135.348346768717));
#113458=CARTESIAN_POINT('Ctrl Pts',(-155.694872023899,2.01200418759494,
135.2922356394));
#113459=CARTESIAN_POINT('Ctrl Pts',(-155.702619920676,2.13710964570217,
135.23614835881));
#113460=CARTESIAN_POINT('Ctrl Pts',(-155.710367817453,2.25993276829467,
135.174796885603));
#113461=CARTESIAN_POINT('Ctrl Pts',(-155.71811571423,2.38000629508634,135.108399778383));
#113462=CARTESIAN_POINT('Ctrl Pts',(-155.725861990314,2.50005470508436,
135.042016560008));
#113463=CARTESIAN_POINT('Ctrl Pts',(-155.733608266399,2.61735432137557,
134.970589996017));
#113464=CARTESIAN_POINT('Ctrl Pts',(-155.741354542483,2.73146209636484,
134.894384808035));
#113465=CARTESIAN_POINT('Ctrl Pts',(-155.749100875748,2.84557071367193,
134.818179057524));
#113466=CARTESIAN_POINT('Ctrl Pts',(-155.756847209013,2.95648711753465,
134.737194829766));
#113467=CARTESIAN_POINT('Ctrl Pts',(-155.764593542279,3.06379722738064,
134.651740194888));
#113468=CARTESIAN_POINT('Ctrl Pts',(-155.772341610282,3.17113136858155,
134.566266423037));
#113469=CARTESIAN_POINT('Ctrl Pts',(-155.780089678285,3.27485730294596,
134.476320495464));
#113470=CARTESIAN_POINT('Ctrl Pts',(-155.787837746288,3.37459433699599,
134.382250515706));
#113471=CARTESIAN_POINT('Ctrl Pts',(-155.79559404903,3.47443737275283,134.288080557254));
#113472=CARTESIAN_POINT('Ctrl Pts',(-155.803350351771,3.57028275456598,
134.189778059603));
#113473=CARTESIAN_POINT('Ctrl Pts',(-155.811106654513,3.66178658018239,
134.087728112029));
#113474=CARTESIAN_POINT('Ctrl Pts',(-155.818867097028,3.75333924414566,
133.985623697325));
#113475=CARTESIAN_POINT('Ctrl Pts',(-155.826627539542,3.84054548618603,
133.879768148882));
#113476=CARTESIAN_POINT('Ctrl Pts',(-155.834387982056,3.92310263425139,
133.770578543415));
#113477=CARTESIAN_POINT('Ctrl Pts',(-155.842160882321,4.0057923103799,133.661213657101));
#113478=CARTESIAN_POINT('Ctrl Pts',(-155.849933782587,4.08381775614332,
133.548504340151));
#113479=CARTESIAN_POINT('Ctrl Pts',(-155.857706682852,4.1569199749223,133.432896214546));
#113480=CARTESIAN_POINT('Ctrl Pts',(-155.865197018614,4.22736474391726,
133.321490735503));
#113481=CARTESIAN_POINT('Ctrl Pts',(-155.872687354377,4.29323786090048,
133.207393813481));
#113482=CARTESIAN_POINT('Ctrl Pts',(-155.880177690139,4.35434939515777,
133.091022902948));
#113483=CARTESIAN_POINT('Ctrl Pts',(-155.887952024258,4.41777799180917,
132.970239753976));
#113484=CARTESIAN_POINT('Ctrl Pts',(-155.895726358377,4.476277729994,132.846624171282));
#113485=CARTESIAN_POINT('Ctrl Pts',(-155.903500692496,4.52958569016528,
132.720616481993));
#113486=CARTESIAN_POINT('Ctrl Pts',(-155.911265445443,4.58282795303991,
132.594764085919));
#113487=CARTESIAN_POINT('Ctrl Pts',(-155.91903019839,4.63089101794859,132.466525805617));
#113488=CARTESIAN_POINT('Ctrl Pts',(-155.926794951337,4.67355739732234,
132.336367248241));
#113489=CARTESIAN_POINT('Ctrl Pts',(-155.934551992222,4.71618139984661,
132.20633796618));
#113490=CARTESIAN_POINT('Ctrl Pts',(-155.942309033107,4.75341926261015,
132.074392571659));
#113491=CARTESIAN_POINT('Ctrl Pts',(-155.950066073992,4.78510138148113,
131.941017043865));
#113492=CARTESIAN_POINT('Ctrl Pts',(-155.957817265233,4.81675960861986,
131.807742095594));
#113493=CARTESIAN_POINT('Ctrl Pts',(-155.965568456473,4.84287034107949,
131.67303953953));
#113494=CARTESIAN_POINT('Ctrl Pts',(-155.973319647713,4.86331376842432,
131.537410583363));
#113495=CARTESIAN_POINT('Ctrl Pts',(-155.98106754449,4.88374850676721,131.401839273119));
#113496=CARTESIAN_POINT('Ctrl Pts',(-155.988815441267,4.89852067267687,
131.265342731688));
#113497=CARTESIAN_POINT('Ctrl Pts',(-155.996563338044,4.90756158009912,
131.128432214648));
#113498=CARTESIAN_POINT('Ctrl Pts',(-156.004309614128,4.91660059635842,
130.991550336336));
#113499=CARTESIAN_POINT('Ctrl Pts',(-156.012055890213,4.91991071297508,
130.854255044524));
#113500=CARTESIAN_POINT('Ctrl Pts',(-156.019802166297,4.91747516970204,
130.717062176206));
#113501=CARTESIAN_POINT('Ctrl Pts',(-156.027548499562,4.91503960845036,
130.579868295161));
#113502=CARTESIAN_POINT('Ctrl Pts',(-156.035294832827,4.90685830961618,
130.442777230022));
#113503=CARTESIAN_POINT('Ctrl Pts',(-156.043041166093,4.89296664065922,
130.306303877931));
#113504=CARTESIAN_POINT('Ctrl Pts',(-156.050789234096,4.87907186075926,
130.169799963578));
#113505=CARTESIAN_POINT('Ctrl Pts',(-156.058537302099,4.85946420566122,
130.033914426421));
#113506=CARTESIAN_POINT('Ctrl Pts',(-156.066285370102,4.8342307706067,129.899155713128));
#113507=CARTESIAN_POINT('Ctrl Pts',(-156.074041672843,4.80897051715722,
129.764253776671));
#113508=CARTESIAN_POINT('Ctrl Pts',(-156.081797975585,4.77807261183529,
129.630481441317));
#113509=CARTESIAN_POINT('Ctrl Pts',(-156.089554278327,4.74167515358669,
129.49833619193));
#113510=CARTESIAN_POINT('Ctrl Pts',(-156.097314720841,4.70525826891872,
129.366120412644));
#113511=CARTESIAN_POINT('Ctrl Pts',(-156.105075163356,4.66333610198203,
129.235533821808));
#113512=CARTESIAN_POINT('Ctrl Pts',(-156.11283560587,4.61609594959198,129.107056506141));
#113513=CARTESIAN_POINT('Ctrl Pts',(-156.120608506135,4.56877996311553,
128.978372947281));
#113514=CARTESIAN_POINT('Ctrl Pts',(-156.128381406401,4.51612908198456,
128.851805791076));
#113515=CARTESIAN_POINT('Ctrl Pts',(-156.136154306666,4.45837822659115,
128.72781380828));
#113516=CARTESIAN_POINT('Ctrl Pts',(-156.143644642428,4.40272676025738,
128.608329246376));
#113517=CARTESIAN_POINT('Ctrl Pts',(-156.15113497819,4.34233981713904,128.491236154113));
#113518=CARTESIAN_POINT('Ctrl Pts',(-156.158625313952,4.27746595131303,
128.376919969917));
#113519=CARTESIAN_POINT('Ctrl Pts',(-156.166399648071,4.21013237314557,
128.258269452851));
#113520=CARTESIAN_POINT('Ctrl Pts',(-156.17417398219,4.13775161987442,128.142234724393));
#113521=CARTESIAN_POINT('Ctrl Pts',(-156.181948316309,4.06055203674368,
128.02927499377));
#113522=CARTESIAN_POINT('Ctrl Pts',(-156.189713069256,3.98344759520005,
127.916454475921));
#113523=CARTESIAN_POINT('Ctrl Pts',(-156.197477822203,3.90153635867472,
127.8067017353));
#113524=CARTESIAN_POINT('Ctrl Pts',(-156.20524257515,3.81509249830841,127.700451422398));
#113525=CARTESIAN_POINT('Ctrl Pts',(-156.212999616035,3.72873449520216,
127.594306638803));
#113526=CARTESIAN_POINT('Ctrl Pts',(-156.22075665692,3.63785307231276,127.491657661544));
#113527=CARTESIAN_POINT('Ctrl Pts',(-156.228513697805,3.54276542251666,
127.392909867002));
#113528=CARTESIAN_POINT('Ctrl Pts',(-156.236264889045,3.44774947905759,
127.294236538941));
#113529=CARTESIAN_POINT('Ctrl Pts',(-156.244016080286,3.34853389235116,
127.199458818384));
#113530=CARTESIAN_POINT('Ctrl Pts',(-156.251767271526,3.2454755821541,127.108948420241));
#113531=CARTESIAN_POINT('Ctrl Pts',(-156.259515168303,3.14246107448762,
127.018476491431));
#113532=CARTESIAN_POINT('Ctrl Pts',(-156.26726306508,3.03560738490353,126.932268535125));
#113533=CARTESIAN_POINT('Ctrl Pts',(-156.275010961857,2.92530752070788,
126.850658684973));
#113534=CARTESIAN_POINT('Ctrl Pts',(-156.282757237941,2.81503072886603,
126.769065905842));
#113535=CARTESIAN_POINT('Ctrl Pts',(-156.290503514025,2.701309510345,126.692069552137));
#113536=CARTESIAN_POINT('Ctrl Pts',(-156.298249790109,2.58456879409407,
126.619962547222));
#113537=CARTESIAN_POINT('Ctrl Pts',(-156.305996123374,2.46782721609016,
126.547855010031));
#113538=CARTESIAN_POINT('Ctrl Pts',(-156.31374245664,2.34806642850909,126.480637099103));
#113539=CARTESIAN_POINT('Ctrl Pts',(-156.321488789905,2.22573874587498,
126.418557373278));
#113540=CARTESIAN_POINT('Ctrl Pts',(-156.329236857908,2.10338366880434,
126.356463745127));
#113541=CARTESIAN_POINT('Ctrl Pts',(-156.336984925911,1.9784609013917,126.299510768657));
#113542=CARTESIAN_POINT('Ctrl Pts',(-156.344732993914,1.85144529132593,
126.247899996017));
#113543=CARTESIAN_POINT('Ctrl Pts',(-156.352489296656,1.72429468755811,
126.196234370834));
#113544=CARTESIAN_POINT('Ctrl Pts',(-156.360245599398,1.59504716064527,
126.149922438825));
#113545=CARTESIAN_POINT('Ctrl Pts',(-156.36800190214,1.46419590454737,126.109116916159));
#113546=CARTESIAN_POINT('Ctrl Pts',(-156.375762344654,1.33327480919353,
126.068289614356));
#113547=CARTESIAN_POINT('Ctrl Pts',(-156.383522787168,1.20074865668212,
126.032974678594));
#113548=CARTESIAN_POINT('Ctrl Pts',(-156.391283229682,1.06712259607261,
126.00327402936));
#113549=CARTESIAN_POINT('Ctrl Pts',(-156.399056129948,0.933282027048574,
125.973525702007));
#113550=CARTESIAN_POINT('Ctrl Pts',(-156.406829030213,0.798338406644024,
125.949409739949));
#113551=CARTESIAN_POINT('Ctrl Pts',(-156.414601930479,0.66280469189865,
125.930976474807));
#113552=CARTESIAN_POINT('Ctrl Pts',(-156.42209226624,0.532197969074568,
125.913213305283));
#113553=CARTESIAN_POINT('Ctrl Pts',(-156.429582602002,0.401043616516894,
125.90072687425));
#113554=CARTESIAN_POINT('Ctrl Pts',(-156.437072937764,0.269800264039454,
125.893516405007));
#113555=CARTESIAN_POINT('Ctrl Pts',(-156.444847271883,0.133580779960928,
125.886032548631));
#113556=CARTESIAN_POINT('Ctrl Pts',(-156.452621606003,-0.00316608850629907,
125.88420892125));
#113557=CARTESIAN_POINT('Ctrl Pts',(-156.460395940122,-0.139930569451091,
125.888101623348));
#113558=CARTESIAN_POINT('Ctrl Pts',(-156.468160693069,-0.276526500396111,
125.891989528038));
#113559=CARTESIAN_POINT('Ctrl Pts',(-156.475925446016,-0.413139613575392,
125.901579734008));
#113560=CARTESIAN_POINT('Ctrl Pts',(-156.483690198963,-0.54925602902288,
125.91687651252));
#113561=CARTESIAN_POINT('Ctrl Pts',(-156.491447239848,-0.685237251727639,
125.932158098055));
#113562=CARTESIAN_POINT('Ctrl Pts',(-156.499204280733,-0.82072237243852,
125.953134933479));
#113563=CARTESIAN_POINT('Ctrl Pts',(-156.506961321618,-0.955198886028568,
125.979759271275));
#113564=CARTESIAN_POINT('Ctrl Pts',(-156.514712512858,-1.08957398983383,
126.006363531452));
#113565=CARTESIAN_POINT('Ctrl Pts',(-156.522463704098,-1.22294161847439,
126.038606741444));
#113566=CARTESIAN_POINT('Ctrl Pts',(-156.530214895338,-1.35479611382101,
126.07638953554));
#113567=CARTESIAN_POINT('Ctrl Pts',(-156.537962792116,-1.48659456748996,
126.114156270941));
#113568=CARTESIAN_POINT('Ctrl Pts',(-156.545710688892,-1.61688079193306,
126.157457800112));
#113569=CARTESIAN_POINT('Ctrl Pts',(-156.55345858567,-1.74516124099885,
126.206144082276));
#113570=CARTESIAN_POINT('Ctrl Pts',(-156.561204861754,-1.87341485655976,
126.254820180319));
#113571=CARTESIAN_POINT('Ctrl Pts',(-156.568951137838,-1.9996631659878,
126.308878652295));
#113572=CARTESIAN_POINT('Ctrl Pts',(-156.576697413922,-2.12343004008279,
126.368120325678));
#113573=CARTESIAN_POINT('Ctrl Pts',(-156.584443747187,-2.24719782779657,
126.427362436369));
#113574=CARTESIAN_POINT('Ctrl Pts',(-156.592190080453,-2.36848379097736,
126.491787656018));
#113575=CARTESIAN_POINT('Ctrl Pts',(-156.599936413718,-2.48683432298753,
126.561149791728));
#113576=CARTESIAN_POINT('Ctrl Pts',(-156.607684481721,-2.60521135877859,
126.630527460607));
#113577=CARTESIAN_POINT('Ctrl Pts',(-156.615432549724,-2.72065131807,126.704844047891));
#113578=CARTESIAN_POINT('Ctrl Pts',(-156.623180617727,-2.83272796255406,
126.783808994634));
#113579=CARTESIAN_POINT('Ctrl Pts',(-156.630936920469,-2.94492372342975,
126.862857866261));
#113580=CARTESIAN_POINT('Ctrl Pts',(-156.638693223211,-3.05374870879315,
126.94656474065));
#113581=CARTESIAN_POINT('Ctrl Pts',(-156.646449525952,-3.15880785082546,
127.034597226574));
#113582=CARTESIAN_POINT('Ctrl Pts',(-156.654209968467,-3.26392306608571,
127.122676698086));
#113583=CARTESIAN_POINT('Ctrl Pts',(-156.661970410981,-3.36526814427592,
127.215086118136));
#113584=CARTESIAN_POINT('Ctrl Pts',(-156.669730853495,-3.46248429140025,
127.311455581023));
#113585=CARTESIAN_POINT('Ctrl Pts',(-156.677503753761,-3.55985649851412,
127.407979744727));
#113586=CARTESIAN_POINT('Ctrl Pts',(-156.685276654026,-3.65308626340284,
127.508476367818));
#113587=CARTESIAN_POINT('Ctrl Pts',(-156.693049554291,-3.74185397483924,
127.612541090481));
#113588=CARTESIAN_POINT('Ctrl Pts',(-156.700539890054,-3.8273947563728,
127.712822798352));
#113589=CARTESIAN_POINT('Ctrl Pts',(-156.708030225816,-3.90879207561689,
127.816417448674));
#113590=CARTESIAN_POINT('Ctrl Pts',(-156.715520561578,-3.98579868541431,
127.922938763368));
#113591=CARTESIAN_POINT('Ctrl Pts',(-156.723359687267,-4.06639113311023,
128.03442027782));
#113592=CARTESIAN_POINT('Ctrl Pts',(-156.731198812957,-4.14242889248428,
128.149459757647));
#113593=CARTESIAN_POINT('Ctrl Pts',(-156.739037938646,-4.21358455281497,
128.267652459583));
#113594=CARTESIAN_POINT('Ctrl Pts',(-156.746863778478,-4.28461961755481,
128.385644846903));
#113595=CARTESIAN_POINT('Ctrl Pts',(-156.75468961831,-4.3507888698194,128.506779485963));
#113596=CARTESIAN_POINT('Ctrl Pts',(-156.762515458141,-4.41180659074676,
128.630620598994));
#113597=CARTESIAN_POINT('Ctrl Pts',(-156.770333624224,-4.47276447980175,
128.754340277701));
#113598=CARTESIAN_POINT('Ctrl Pts',(-156.778151790307,-4.52858071880324,
128.880760810003));
#113599=CARTESIAN_POINT('Ctrl Pts',(-156.78596995639,-4.57901390273034,
129.00941918646));
#113600=CARTESIAN_POINT('Ctrl Pts',(-156.793780602572,-4.62939857751095,
129.137953812886));
#113601=CARTESIAN_POINT('Ctrl Pts',(-156.801591248754,-4.67441037000992,
129.268721641938));
#113602=CARTESIAN_POINT('Ctrl Pts',(-156.809401894936,-4.71385493883423,
129.401237430484));
#113603=CARTESIAN_POINT('Ctrl Pts',(-156.812942739115,-4.73173656715076,
129.461311558493));
#113604=CARTESIAN_POINT('Ctrl Pts',(-156.816483583295,-4.74847470512542,
129.521744625465));
#113605=CARTESIAN_POINT('Ctrl Pts',(-156.820024427474,-4.76405452823416,
129.582490119309));
#113606=CARTESIAN_POINT('Origin',(213.235140564004,0.,130.804360617566));
#113607=CARTESIAN_POINT('',(-158.915166007136,-4.76405452823407,129.582490119308));
#113608=CARTESIAN_POINT('',(-158.569717364632,-4.76405452823396,129.582490119308));
#113609=CARTESIAN_POINT('',(213.235140564004,-4.76405452823405,129.582490119308));
#113610=CARTESIAN_POINT('',(-157.235140563979,-4.91824963986197,130.806242769961));
#113611=CARTESIAN_POINT('Ctrl Pts',(-157.235140564011,-4.91824963986175,
130.80624277053));
#113612=CARTESIAN_POINT('Ctrl Pts',(-157.241035980355,-4.91821002387229,
130.9097632227));
#113613=CARTESIAN_POINT('Ctrl Pts',(-157.246931396699,-4.91490228748288,
131.01321746358));
#113614=CARTESIAN_POINT('Ctrl Pts',(-157.252826813043,-4.90833734989934,
131.116462399174));
#113615=CARTESIAN_POINT('Ctrl Pts',(-157.260601147162,-4.89968011260356,
131.252612346627));
#113616=CARTESIAN_POINT('Ctrl Pts',(-157.268375481281,-4.88533997543229,
131.388617464613));
#113617=CARTESIAN_POINT('Ctrl Pts',(-157.2761498154,-4.8653214390861,131.523964923327));
#113618=CARTESIAN_POINT('Ctrl Pts',(-157.283914568347,-4.84532757379684,
131.659145578394));
#113619=CARTESIAN_POINT('Ctrl Pts',(-157.291679321294,-4.8196692901588,
131.79366980381));
#113620=CARTESIAN_POINT('Ctrl Pts',(-157.299444074241,-4.78840304052204,
131.927026811953));
#113621=CARTESIAN_POINT('Ctrl Pts',(-157.307201115126,-4.75716784496519,
132.060251368035));
#113622=CARTESIAN_POINT('Ctrl Pts',(-157.314958156011,-4.72033585644996,
132.192310635716));
#113623=CARTESIAN_POINT('Ctrl Pts',(-157.322715196896,-4.6780150196256,
132.322701336462));
#113624=CARTESIAN_POINT('Ctrl Pts',(-157.330466388137,-4.63572609727343,
132.452993708566));
#113625=CARTESIAN_POINT('Ctrl Pts',(-157.338217579377,-4.58795668561397,
132.5816196479));
#113626=CARTESIAN_POINT('Ctrl Pts',(-157.345968770617,-4.53486517750881,
132.708088771562));
#113627=CARTESIAN_POINT('Ctrl Pts',(-157.353716667394,-4.48179623471093,
132.834504142473));
#113628=CARTESIAN_POINT('Ctrl Pts',(-157.361464564171,-4.42340984549422,
132.958764161234));
#113629=CARTESIAN_POINT('Ctrl Pts',(-157.369212460948,-4.35991329256529,
133.080396457313));
#113630=CARTESIAN_POINT('Ctrl Pts',(-157.376958737032,-4.29643002174622,
133.202003310538));
#113631=CARTESIAN_POINT('Ctrl Pts',(-157.384705013117,-4.2278388942011,
133.32098318803));
#113632=CARTESIAN_POINT('Ctrl Pts',(-157.392451289201,-4.15439392340065,
133.436886817191));
#113633=CARTESIAN_POINT('Ctrl Pts',(-157.400197622466,-4.0809484104462,
133.552791301926));
#113634=CARTESIAN_POINT('Ctrl Pts',(-157.407943955731,-4.00264919200707,
133.665619162773));
#113635=CARTESIAN_POINT('Ctrl Pts',(-157.415690288997,-3.91979431270252,
133.774949045572));
#113636=CARTESIAN_POINT('Ctrl Pts',(-157.423438357,-3.83692087862234,133.88430341204));
#113637=CARTESIAN_POINT('Ctrl Pts',(-157.431186425003,-3.74948998967467,
133.990157930152));
#113638=CARTESIAN_POINT('Ctrl Pts',(-157.438934493006,-3.65784051355853,
134.092123662536));
#113639=CARTESIAN_POINT('Ctrl Pts',(-157.446690795747,-3.5660936312884,
134.194197765313));
#113640=CARTESIAN_POINT('Ctrl Pts',(-157.454447098489,-3.47011946721651,
134.292374534919));
#113641=CARTESIAN_POINT('Ctrl Pts',(-157.462203401231,-3.37029474701639,
134.386300927054));
#113642=CARTESIAN_POINT('Ctrl Pts',(-157.469963843745,-3.27041674735744,
134.480277450532));
#113643=CARTESIAN_POINT('Ctrl Pts',(-157.47772428626,-3.16668439205171,
134.569998820617));
#113644=CARTESIAN_POINT('Ctrl Pts',(-157.485484728774,-3.05950737441191,
134.655152443726));
#113645=CARTESIAN_POINT('Ctrl Pts',(-157.493257629039,-2.95215830670866,
134.74044276299));
#113646=CARTESIAN_POINT('Ctrl Pts',(-157.501030529305,-2.84135384281622,
134.821150452186));
#113647=CARTESIAN_POINT('Ctrl Pts',(-157.50880342957,-2.72753326118023,
134.897005895581));
#113648=CARTESIAN_POINT('Ctrl Pts',(-157.516293765332,-2.61785034438345,
134.970103802539));
#113649=CARTESIAN_POINT('Ctrl Pts',(-157.523784101094,-2.50536705263417,
135.038695961219));
#113650=CARTESIAN_POINT('Ctrl Pts',(-157.531274436856,-2.39049616237082,
135.102582477846));
#113651=CARTESIAN_POINT('Ctrl Pts',(-157.539048770975,-2.27126990738872,
135.168891271169));
#113652=CARTESIAN_POINT('Ctrl Pts',(-157.546823105094,-2.1490937553434,
135.230340596014));
#113653=CARTESIAN_POINT('Ctrl Pts',(-157.554597439213,-2.02440159721285,
135.286657041912));
#113654=CARTESIAN_POINT('Ctrl Pts',(-157.56236219216,-1.89986311102314,
135.342904082823));
#113655=CARTESIAN_POINT('Ctrl Pts',(-157.570126945108,-1.77281514121128,
135.394030671892));
#113656=CARTESIAN_POINT('Ctrl Pts',(-157.577891698055,-1.64371794174452,
135.439808210894));
#113657=CARTESIAN_POINT('Ctrl Pts',(-157.58564873894,-1.51474896343656,
135.485540282998));
#113658=CARTESIAN_POINT('Ctrl Pts',(-157.593405779825,-1.38373517195991,
135.525933747832));
#113659=CARTESIAN_POINT('Ctrl Pts',(-157.60116282071,-1.25115833651864,
135.560807387946));
#113660=CARTESIAN_POINT('Ctrl Pts',(-157.60891401195,-1.1186814783001,135.595654729577));
#113661=CARTESIAN_POINT('Ctrl Pts',(-157.61666520319,-0.984644298828111,
135.624990432721));
#113662=CARTESIAN_POINT('Ctrl Pts',(-157.62441639443,-0.849544986336227,
135.648682693842));
#113663=CARTESIAN_POINT('Ctrl Pts',(-157.632164291207,-0.714503094655859,
135.67236488512));
#113664=CARTESIAN_POINT('Ctrl Pts',(-157.639912187984,-0.578400352107374,
135.690408337643));
#113665=CARTESIAN_POINT('Ctrl Pts',(-157.647660084761,-0.441746218762442,
135.702732116412));
#113666=CARTESIAN_POINT('Ctrl Pts',(-157.655406360845,-0.305120670516284,
135.715053317313));
#113667=CARTESIAN_POINT('Ctrl Pts',(-157.66315263693,-0.167944350027724,
135.721657189137));
#113668=CARTESIAN_POINT('Ctrl Pts',(-157.670898913014,-0.0307325435426136,
135.722514597798));
#113669=CARTESIAN_POINT('Ctrl Pts',(-157.678645246279,0.106480275808695,
135.723372012787));
#113670=CARTESIAN_POINT('Ctrl Pts',(-157.686391579544,0.243728190721681,
135.718482877527));
#113671=CARTESIAN_POINT('Ctrl Pts',(-157.69413791281,0.380495603610463,
135.707870193179));
#113672=CARTESIAN_POINT('Ctrl Pts',(-157.701885980813,0.517293644612896,
135.697255132195));
#113673=CARTESIAN_POINT('Ctrl Pts',(-157.709634048816,0.653610579750593,
135.680914001831));
#113674=CARTESIAN_POINT('Ctrl Pts',(-157.717382116819,0.788936018728041,
135.658921670932));
#113675=CARTESIAN_POINT('Ctrl Pts',(-157.725138419561,0.924405283192612,
135.636905966321));
#113676=CARTESIAN_POINT('Ctrl Pts',(-157.732894722302,1.05888055995229,
135.60922712603));
#113677=CARTESIAN_POINT('Ctrl Pts',(-157.740651025044,1.19186119341141,
135.576011270971));
#113678=CARTESIAN_POINT('Ctrl Pts',(-157.748411467559,1.32491280263895,
135.54277768761));
#113679=CARTESIAN_POINT('Ctrl Pts',(-157.756171910073,1.45646780417877,
135.504001311335));
#113680=CARTESIAN_POINT('Ctrl Pts',(-157.763932352587,1.58604175495508,
135.459857864267));
#113681=CARTESIAN_POINT('Ctrl Pts',(-157.771705252852,1.71582370933987,
135.415643554219));
#113682=CARTESIAN_POINT('Ctrl Pts',(-157.779478153118,1.84361789330427,
135.366045098006));
#113683=CARTESIAN_POINT('Ctrl Pts',(-157.787251053383,1.96896003076597,
135.311286339136));
#113684=CARTESIAN_POINT('Ctrl Pts',(-157.794741389145,2.08974566581144,
135.25851819908));
#113685=CARTESIAN_POINT('Ctrl Pts',(-157.802231724907,2.20825415828578,
135.200958557263));
#113686=CARTESIAN_POINT('Ctrl Pts',(-157.809722060669,2.32409421614721,
135.138846646725));
#113687=CARTESIAN_POINT('Ctrl Pts',(-157.817496394788,2.44432638501281,
135.074379744219));
#113688=CARTESIAN_POINT('Ctrl Pts',(-157.825270728907,2.56206463683875,
135.004804348357));
#113689=CARTESIAN_POINT('Ctrl Pts',(-157.833045063026,2.67684441498163,
134.93033771887));
#113690=CARTESIAN_POINT('Ctrl Pts',(-157.840809815973,2.79148273730613,
134.855962862848));
#113691=CARTESIAN_POINT('Ctrl Pts',(-157.84857456892,2.90316951567248,134.776708977889));
#113692=CARTESIAN_POINT('Ctrl Pts',(-157.856339321867,3.0114636454075,134.692839725764));
#113693=CARTESIAN_POINT('Ctrl Pts',(-157.864096362752,3.11965021588619,
134.609053773762));
#113694=CARTESIAN_POINT('Ctrl Pts',(-157.871853403638,3.22445053633657,
134.520661814898));
#113695=CARTESIAN_POINT('Ctrl Pts',(-157.879610444523,3.32545173536253,
134.427971222788));
#113696=CARTESIAN_POINT('Ctrl Pts',(-157.887361635763,3.42637676859849,
134.335350529374));
#113697=CARTESIAN_POINT('Ctrl Pts',(-157.895112827003,3.52350809602809,
134.238437918268));
#113698=CARTESIAN_POINT('Ctrl Pts',(-157.902864018243,3.61646554469464,
134.137581286309));
#113699=CARTESIAN_POINT('Ctrl Pts',(-157.91061191502,3.70938348396591,134.036767521109));
#113700=CARTESIAN_POINT('Ctrl Pts',(-157.918359811797,3.79813080843224,
133.932013355998));
#113701=CARTESIAN_POINT('Ctrl Pts',(-157.926107708574,3.88236404957427,
133.823703666819));
#113702=CARTESIAN_POINT('Ctrl Pts',(-157.933853984658,3.9665796709381,133.715416633692));
#113703=CARTESIAN_POINT('Ctrl Pts',(-157.941600260742,4.04628284727668,
133.60357586426));
#113704=CARTESIAN_POINT('Ctrl Pts',(-157.949346536826,4.12117054245583,
133.488599135748));
#113705=CARTESIAN_POINT('Ctrl Pts',(-157.957092870092,4.19605879043883,
133.373621558505));
#113706=CARTESIAN_POINT('Ctrl Pts',(-157.964839203357,4.26613127295388,
133.255508303594));
#113707=CARTESIAN_POINT('Ctrl Pts',(-157.972585536622,4.33112864844156,
133.134705590558));
#113708=CARTESIAN_POINT('Ctrl Pts',(-157.980333604625,4.39614057964091,
133.013875824591));
#113709=CARTESIAN_POINT('Ctrl Pts',(-157.988081672628,4.45607495702969,
132.890355746248));
#113710=CARTESIAN_POINT('Ctrl Pts',(-157.995829740631,4.5107188914635,132.764615229777));
#113711=CARTESIAN_POINT('Ctrl Pts',(-158.003586043373,4.56542090212102,
132.638741074789));
#113712=CARTESIAN_POINT('Ctrl Pts',(-158.011342346115,4.61482108170882,
132.510642126643));
#113713=CARTESIAN_POINT('Ctrl Pts',(-158.019098648857,4.65875492274316,
132.380807772505));
#113714=CARTESIAN_POINT('Ctrl Pts',(-158.026859091371,4.70271221259141,
132.250904121863));
#113715=CARTESIAN_POINT('Ctrl Pts',(-158.034619533885,4.74119724076914,
132.119263594695));
#113716=CARTESIAN_POINT('Ctrl Pts',(-158.042379976399,4.77409599395775,
131.986388748778));
#113717=CARTESIAN_POINT('Ctrl Pts',(-158.050152876665,4.8070475591456,131.853300600363));
#113718=CARTESIAN_POINT('Ctrl Pts',(-158.05792577693,4.83439485121186,131.718974556981));
#113719=CARTESIAN_POINT('Ctrl Pts',(-158.065698677196,4.85607524347601,
131.583922220135));
#113720=CARTESIAN_POINT('Ctrl Pts',(-158.073189012958,4.87696749887192,
131.453779375908));
#113721=CARTESIAN_POINT('Ctrl Pts',(-158.08067934872,4.8925976769512,131.322962432477));
#113722=CARTESIAN_POINT('Ctrl Pts',(-158.088169684482,4.90295554833941,
131.19192990622));
#113723=CARTESIAN_POINT('Ctrl Pts',(-158.095944018601,4.91370614156943,
131.055929241905));
#113724=CARTESIAN_POINT('Ctrl Pts',(-158.10371835272,4.91881079158172,130.919265515186));
#113725=CARTESIAN_POINT('Ctrl Pts',(-158.111492686839,4.9182011809279,130.782447004915));
#113726=CARTESIAN_POINT('Ctrl Pts',(-158.119257439786,4.91759232156474,
130.645797111231));
#113727=CARTESIAN_POINT('Ctrl Pts',(-158.127022192733,4.91128321536974,
130.508993200753));
#113728=CARTESIAN_POINT('Ctrl Pts',(-158.134786945681,4.89925726060928,
130.372548902964));
#113729=CARTESIAN_POINT('Ctrl Pts',(-158.142543986566,4.88724325019662,
130.236240123575));
#113730=CARTESIAN_POINT('Ctrl Pts',(-158.150301027451,4.86952372490714,
130.100290633021));
#113731=CARTESIAN_POINT('Ctrl Pts',(-158.158058068336,4.84613411979584,
129.965213934649));
#113732=CARTESIAN_POINT('Ctrl Pts',(-158.165809259576,4.82276215296767,
129.830239098666));
#113733=CARTESIAN_POINT('Ctrl Pts',(-158.173560450816,4.79372868357652,
129.696136128472));
#113734=CARTESIAN_POINT('Ctrl Pts',(-158.181311642056,4.75912091431727,
129.563412921082));
#113735=CARTESIAN_POINT('Ctrl Pts',(-158.189059538833,4.72452785428319,
129.430746124597));
#113736=CARTESIAN_POINT('Ctrl Pts',(-158.19680743561,4.684365305031,129.299458302063));
#113737=CARTESIAN_POINT('Ctrl Pts',(-158.204555332387,4.63877142038355,
129.170046458069));
#113738=CARTESIAN_POINT('Ctrl Pts',(-158.212301608471,4.59318707299387,
129.040661684242));
#113739=CARTESIAN_POINT('Ctrl Pts',(-158.220047884555,4.54217377984429,
128.913152476936));
#113740=CARTESIAN_POINT('Ctrl Pts',(-158.22779416064,4.48591923031548,128.787999607829));
#113741=CARTESIAN_POINT('Ctrl Pts',(-158.235540493905,4.42966426552828,
128.662845814872));
#113742=CARTESIAN_POINT('Ctrl Pts',(-158.24328682717,4.36816812744529,128.54004875142));
#113743=CARTESIAN_POINT('Ctrl Pts',(-158.251033160436,4.30166605275713,
128.420067801434));
#113744=CARTESIAN_POINT('Ctrl Pts',(-158.258781228439,4.23514908539053,
128.300059982547));
#113745=CARTESIAN_POINT('Ctrl Pts',(-158.266529296442,4.16362414016712,
128.18286987393));
#113746=CARTESIAN_POINT('Ctrl Pts',(-158.274277364444,4.08737146381713,
128.068930563758));
#113747=CARTESIAN_POINT('Ctrl Pts',(-158.282033667186,4.01103774521519,
127.954870157532));
#113748=CARTESIAN_POINT('Ctrl Pts',(-158.289789969928,3.9299664759229,127.844067776896));
#113749=CARTESIAN_POINT('Ctrl Pts',(-158.29754627267,3.84448047090935,127.73692635237));
#113750=CARTESIAN_POINT('Ctrl Pts',(-158.305306715184,3.75894883944098,
127.629727743241));
#113751=CARTESIAN_POINT('Ctrl Pts',(-158.313067157698,3.66899803345964,
127.526194278649));
#113752=CARTESIAN_POINT('Ctrl Pts',(-158.320827600213,3.57498924207386,
127.426693525984));
#113753=CARTESIAN_POINT('Ctrl Pts',(-158.328600500478,3.48082953943043,
127.327033045877));
#113754=CARTESIAN_POINT('Ctrl Pts',(-158.336373400744,3.38259911417897,
127.231418487003));
#113755=CARTESIAN_POINT('Ctrl Pts',(-158.344146301009,3.2806945399007,127.140179072068));
#113756=CARTESIAN_POINT('Ctrl Pts',(-158.351636636771,3.18249445357985,
127.052256439685));
#113757=CARTESIAN_POINT('Ctrl Pts',(-158.359126972533,3.08088294718426,
126.968396574892));
#113758=CARTESIAN_POINT('Ctrl Pts',(-158.366617308295,2.97624025430221,
126.888855923255));
#113759=CARTESIAN_POINT('Ctrl Pts',(-158.374391642414,2.86763000191393,
126.806299463635));
#113760=CARTESIAN_POINT('Ctrl Pts',(-158.382165976533,2.7554101261273,126.72813469452));
#113761=CARTESIAN_POINT('Ctrl Pts',(-158.389940310652,2.63997132908655,
126.654693830449));
#113762=CARTESIAN_POINT('Ctrl Pts',(-158.397705063599,2.52467480004641,
126.58134347568));
#113763=CARTESIAN_POINT('Ctrl Pts',(-158.405469816546,2.40616756966668,
126.51270565017));
#113764=CARTESIAN_POINT('Ctrl Pts',(-158.413234569493,2.28487279533544,
126.449071950711));
#113765=CARTESIAN_POINT('Ctrl Pts',(-158.420991610378,2.16369849268403,
126.385501453139));
#113766=CARTESIAN_POINT('Ctrl Pts',(-158.428748651263,2.0397424997492,126.326925371213));
#113767=CARTESIAN_POINT('Ctrl Pts',(-158.436505692148,1.91345599495261,
126.273591453519));
#113768=CARTESIAN_POINT('Ctrl Pts',(-158.444256883389,1.78726472379148,
126.220297755347));
#113769=CARTESIAN_POINT('Ctrl Pts',(-158.452008074629,1.6587467975864,126.17223850438));
#113770=CARTESIAN_POINT('Ctrl Pts',(-158.459759265869,1.52837665966729,
126.129614865262));
#113771=CARTESIAN_POINT('Ctrl Pts',(-158.467507162646,1.39806193253436,
126.087009342328));
#113772=CARTESIAN_POINT('Ctrl Pts',(-158.475255059423,1.2658969302769,126.049834957513));
#113773=CARTESIAN_POINT('Ctrl Pts',(-158.4830029562,1.13237447244599,126.018244121214));
#113774=CARTESIAN_POINT('Ctrl Pts',(-158.490749232284,0.998879944634847,
125.986659893037));
#113775=CARTESIAN_POINT('Ctrl Pts',(-158.498495508368,0.864028906263758,
125.9606569802));
#113776=CARTESIAN_POINT('Ctrl Pts',(-158.506241784452,0.728327294856539,
125.940337343149));
#113777=CARTESIAN_POINT('Ctrl Pts',(-158.513988117718,0.592624681731036,
125.920017556103));
#113778=CARTESIAN_POINT('Ctrl Pts',(-158.521734450983,0.456071869695214,
125.905381186453));
#113779=CARTESIAN_POINT('Ctrl Pts',(-158.529480784248,0.319182502662992,
125.896478631159));
#113780=CARTESIAN_POINT('Ctrl Pts',(-158.537228852251,0.18226248020596,
125.887574082201));
#113781=CARTESIAN_POINT('Ctrl Pts',(-158.544976920254,0.0450061428429854,
125.884405928074));
#113782=CARTESIAN_POINT('Ctrl Pts',(-158.552724988257,-0.0920706598753649,
125.886972484005));
#113783=CARTESIAN_POINT('Ctrl Pts',(-158.560481290999,-0.229293149450692,
125.889541767702));
#113784=CARTESIAN_POINT('Ctrl Pts',(-158.568237593741,-0.366335331694764,
125.897857929382));
#113785=CARTESIAN_POINT('Ctrl Pts',(-158.575993896483,-0.502683720371866,
125.911867169459));
#113786=CARTESIAN_POINT('Ctrl Pts',(-158.583754338997,-0.639104882289376,
125.925883886688));
#113787=CARTESIAN_POINT('Ctrl Pts',(-158.591514781511,-0.77483112607358,
125.945599680742));
#113788=CARTESIAN_POINT('Ctrl Pts',(-158.599275224025,-0.90935797533449,
125.970909352145));
#113789=CARTESIAN_POINT('Ctrl Pts',(-158.60704812429,-1.04410077903657,
125.99625965288));
#113790=CARTESIAN_POINT('Ctrl Pts',(-158.614821024556,-1.1776399596222,
126.027221687087));
#113791=CARTESIAN_POINT('Ctrl Pts',(-158.622593924821,-1.30948417499589,
126.063639759096));
#113792=CARTESIAN_POINT('Ctrl Pts',(-158.630084260583,-1.43653552104805,
126.098733942456));
#113793=CARTESIAN_POINT('Ctrl Pts',(-158.637574596346,-1.56201270154158,
126.138894275263));
#113794=CARTESIAN_POINT('Ctrl Pts',(-158.645064932108,-1.68549443601759,
126.183939471323));
#113795=CARTESIAN_POINT('Ctrl Pts',(-158.652839423886,-1.8136606170759,
126.230693517809));
#113796=CARTESIAN_POINT('Ctrl Pts',(-158.660613915665,-1.94008296338148,
126.282858478307));
#113797=CARTESIAN_POINT('Ctrl Pts',(-158.668388407444,-2.06427075965575,
126.340285204524));
#113798=CARTESIAN_POINT('Ctrl Pts',(-158.676153281355,-2.18830492251237,
126.397640887816));
#113799=CARTESIAN_POINT('Ctrl Pts',(-158.683918155266,-2.31010968422649,
126.460245222378));
#113800=CARTESIAN_POINT('Ctrl Pts',(-158.691683029177,-2.42921096759975,
126.527899798455));
#113801=CARTESIAN_POINT('Ctrl Pts',(-158.699440154486,-2.54819339926752,
126.595486861726));
#113802=CARTESIAN_POINT('Ctrl Pts',(-158.707197279795,-2.66447738371206,
126.668113945272));
#113803=CARTESIAN_POINT('Ctrl Pts',(-158.714954405103,-2.77761059626085,
126.745535364116));
#113804=CARTESIAN_POINT('Ctrl Pts',(-158.722705644344,-2.89065796389446,
126.822898035976));
#113805=CARTESIAN_POINT('Ctrl Pts',(-158.730456883585,-3.00055899713958,
126.905047581949));
#113806=CARTESIAN_POINT('Ctrl Pts',(-158.738208122826,-3.10688799577204,
126.991693566245));
#113807=CARTESIAN_POINT('Ctrl Pts',(-158.74595588125,-3.21316924568295,
127.078300640789));
#113808=CARTESIAN_POINT('Ctrl Pts',(-158.753703639674,-3.31588134994253,
127.169399889908));
#113809=CARTESIAN_POINT('Ctrl Pts',(-158.761451398098,-3.41462972295018,
127.264659088108));
#113810=CARTESIAN_POINT('Ctrl Pts',(-158.769197483952,-3.51335677835895,
127.359897721946));
#113811=CARTESIAN_POINT('Ctrl Pts',(-158.776943569805,-3.60812152366368,
127.459294247038));
#113812=CARTESIAN_POINT('Ctrl Pts',(-158.784689655659,-3.69856473238077,
127.562478142384));
#113813=CARTESIAN_POINT('Ctrl Pts',(-158.792435746782,-3.78900800262413,
127.665662107924));
#113814=CARTESIAN_POINT('Ctrl Pts',(-158.800181837905,-3.87512947292165,
127.772633154739));
#113815=CARTESIAN_POINT('Ctrl Pts',(-158.807927929028,-3.95660913560079,
127.882986418566));
#113816=CARTESIAN_POINT('Ctrl Pts',(-158.815675702898,-4.03810649877011,
127.993363655332));
#113817=CARTESIAN_POINT('Ctrl Pts',(-158.823423476768,-4.11495981599913,
128.107124256495));
#113818=CARTESIAN_POINT('Ctrl Pts',(-158.831171250637,-4.18689170528051,
128.223833363156));
#113819=CARTESIAN_POINT('Ctrl Pts',(-158.838926546575,-4.2588934309567,
128.340655778995));
#113820=CARTESIAN_POINT('Ctrl Pts',(-158.846681842513,-4.32596398133885,
128.460432083946));
#113821=CARTESIAN_POINT('Ctrl Pts',(-158.854437138451,-4.38787115228131,
128.582701369734));
#113822=CARTESIAN_POINT('Ctrl Pts',(-158.862196552724,-4.44981119810611,
128.705035584808));
#113823=CARTESIAN_POINT('Ctrl Pts',(-158.869955966996,-4.50658223941287,
128.829865063082));
#113824=CARTESIAN_POINT('Ctrl Pts',(-158.877715381269,-4.55800016229432,
128.95670870689));
#113825=CARTESIAN_POINT('Ctrl Pts',(-158.885485591628,-4.60948962567612,
129.083728835029));
#113826=CARTESIAN_POINT('Ctrl Pts',(-158.893255801988,-4.65561096263242,
129.212768358475));
#113827=CARTESIAN_POINT('Ctrl Pts',(-158.901026012348,-4.69622969640936,
129.343330261597));
#113828=CARTESIAN_POINT('Ctrl Pts',(-158.905739343944,-4.72086861253178,
129.422527801271));
#113829=CARTESIAN_POINT('Ctrl Pts',(-158.91045267554,-4.74348382451808,
129.502285257724));
#113830=CARTESIAN_POINT('Ctrl Pts',(-158.915166007136,-4.76405452823407,
129.582490119308));
#113831=CARTESIAN_POINT('Ctrl Pts',(-157.165002070592,-4.7640545282341,
129.582490119308));
#113832=CARTESIAN_POINT('Ctrl Pts',(-157.172688962945,-4.79783407738971,
129.71419606879));
#113833=CARTESIAN_POINT('Ctrl Pts',(-157.180375855299,-4.82612241304179,
129.847204992258));
#113834=CARTESIAN_POINT('Ctrl Pts',(-157.188062747653,-4.84884368240038,
129.98101499989));
#113835=CARTESIAN_POINT('Ctrl Pts',(-157.195909050374,-4.87203614424156,
130.117599952386));
#113836=CARTESIAN_POINT('Ctrl Pts',(-157.203755353095,-4.88942804849412,
130.255019141227));
#113837=CARTESIAN_POINT('Ctrl Pts',(-157.211601655816,-4.90099459220552,
130.392735703752));
#113838=CARTESIAN_POINT('Ctrl Pts',(-157.219447958537,-4.91256113591689,
130.530452266277));
#113839=CARTESIAN_POINT('Ctrl Pts',(-157.227294261258,-4.91830236539209,
130.668465765227));
#113840=CARTESIAN_POINT('Ctrl Pts',(-157.235140563979,-4.91824963986197,
130.806242769962));
#113841=CARTESIAN_POINT('',(-156.889859436049,-4.91824900331411,130.807491735542));
#113842=CARTESIAN_POINT('Ctrl Pts',(-156.820024427474,-4.76405452823416,
129.582490119309));
#113843=CARTESIAN_POINT('Ctrl Pts',(-156.827828471748,-4.7983925626546,
129.716373594362));
#113844=CARTESIAN_POINT('Ctrl Pts',(-156.835632516021,-4.8271005684515,
129.851775581074));
#113845=CARTESIAN_POINT('Ctrl Pts',(-156.843436560295,-4.85005608473303,
129.988187206186));
#113846=CARTESIAN_POINT('Ctrl Pts',(-156.851239413947,-4.87300809881336,
130.1245780197));
#113847=CARTESIAN_POINT('Ctrl Pts',(-156.859042267599,-4.89020929928041,
130.261977789153));
#113848=CARTESIAN_POINT('Ctrl Pts',(-156.866845121251,-4.90158835447094,
130.399867520202));
#113849=CARTESIAN_POINT('Ctrl Pts',(-156.874516559498,-4.91277576398896,
130.535434916946));
#113850=CARTESIAN_POINT('Ctrl Pts',(-156.882187997746,-4.91833559564134,
130.671475538436));
#113851=CARTESIAN_POINT('Ctrl Pts',(-156.889859435994,-4.91824900331473,
130.807491734567));
#113852=CARTESIAN_POINT('Ctrl Pts',(-156.889859436049,-4.91824900331411,
130.807491735541));
#113853=CARTESIAN_POINT('Ctrl Pts',(-156.898588911057,-4.91815046823347,
130.962267143557));
#113854=CARTESIAN_POINT('Ctrl Pts',(-156.907318386066,-4.91074181595013,
131.116765549781));
#113855=CARTESIAN_POINT('Ctrl Pts',(-156.916047861075,-4.8961255726307,
131.270340702475));
#113856=CARTESIAN_POINT('Ctrl Pts',(-156.92481124902,-4.88145254700271,
131.424512475758));
#113857=CARTESIAN_POINT('Ctrl Pts',(-156.933574636966,-4.8595159309414,
131.577753621313));
#113858=CARTESIAN_POINT('Ctrl Pts',(-156.942338024912,-4.83046931390519,
131.729427788057));
#113859=CARTESIAN_POINT('Ctrl Pts',(-156.951149759663,-4.80126244935518,
131.881938727224));
#113860=CARTESIAN_POINT('Ctrl Pts',(-156.959961494414,-4.76486701429897,
132.032865164884));
#113861=CARTESIAN_POINT('Ctrl Pts',(-156.968773229165,-4.72148792238269,
132.181580593203));
#113862=CARTESIAN_POINT('Ctrl Pts',(-156.977171547907,-4.68014402689176,
132.323318809812));
#113863=CARTESIAN_POINT('Ctrl Pts',(-156.985569866649,-4.63245684193933,
132.463048641733));
#113864=CARTESIAN_POINT('Ctrl Pts',(-156.993968185391,-4.57864336005564,
132.600247040455));
#113865=CARTESIAN_POINT('Ctrl Pts',(-157.00174251951,-4.52882815285295,
132.727251769029));
#113866=CARTESIAN_POINT('Ctrl Pts',(-157.009516853629,-4.47364565493833,
132.852383394033));
#113867=CARTESIAN_POINT('Ctrl Pts',(-157.017291187748,-4.41325673716972,
132.975154950138));
#113868=CARTESIAN_POINT('Ctrl Pts',(-157.025055940695,-4.35294224334497,
133.097775201272));
#113869=CARTESIAN_POINT('Ctrl Pts',(-157.032820693642,-4.28743426738942,
133.218040823248));
#113870=CARTESIAN_POINT('Ctrl Pts',(-157.040585446589,-4.21694252730218,
133.335482658071));
#113871=CARTESIAN_POINT('Ctrl Pts',(-157.048342487474,-4.14652080060495,
133.452807848008));
#113872=CARTESIAN_POINT('Ctrl Pts',(-157.056099528359,-4.0711253602934,
133.567314499075));
#113873=CARTESIAN_POINT('Ctrl Pts',(-157.063856569244,-3.99101266485418,
133.67855632619));
#113874=CARTESIAN_POINT('Ctrl Pts',(-157.071607760484,-3.91096038302167,
133.789714264978));
#113875=CARTESIAN_POINT('Ctrl Pts',(-157.079358951724,-3.82619815424202,
133.897611964361));
#113876=CARTESIAN_POINT('Ctrl Pts',(-157.087110142965,-3.73702653856023,
134.001830822681));
#113877=CARTESIAN_POINT('Ctrl Pts',(-157.094858039742,-3.64789282319396,
134.106005385206));
#113878=CARTESIAN_POINT('Ctrl Pts',(-157.102605936519,-3.55435370202516,
134.206503920116));
#113879=CARTESIAN_POINT('Ctrl Pts',(-157.110353833296,-3.45675079038899,
134.302939905741));
#113880=CARTESIAN_POINT('Ctrl Pts',(-157.11810010938,-3.35916829517786,
134.399355719037));
#113881=CARTESIAN_POINT('Ctrl Pts',(-157.125846385464,-3.25752397824553,
134.491710398729));
#113882=CARTESIAN_POINT('Ctrl Pts',(-157.133592661548,-3.15219690144129,
134.579653686593));
#113883=CARTESIAN_POINT('Ctrl Pts',(-157.141338994814,-3.04686904713664,
134.667597623634));
#113884=CARTESIAN_POINT('Ctrl Pts',(-157.149085328079,-2.93785867882222,
134.751129853291));
#113885=CARTESIAN_POINT('Ctrl Pts',(-157.156831661344,-2.82557826229612,
134.829940146794));
#113886=CARTESIAN_POINT('Ctrl Pts',(-157.164579729347,-2.71327270134939,
134.908768089316));
#113887=CARTESIAN_POINT('Ctrl Pts',(-157.17232779735,-2.5976959549327,134.98287176692));
#113888=CARTESIAN_POINT('Ctrl Pts',(-157.180075865353,-2.47928946441981,
135.05198428429));
#113889=CARTESIAN_POINT('Ctrl Pts',(-157.187832168095,-2.36075713007959,
135.121170255266));
#113890=CARTESIAN_POINT('Ctrl Pts',(-157.195588470837,-2.23938938206019,
135.185354271969));
#113891=CARTESIAN_POINT('Ctrl Pts',(-157.203344773579,-2.11565275237175,
135.244315177455));
#113892=CARTESIAN_POINT('Ctrl Pts',(-157.211105216093,-1.99185008071841,
135.303307552152));
#113893=CARTESIAN_POINT('Ctrl Pts',(-157.218865658607,-1.86567636758244,
135.357071107657));
#113894=CARTESIAN_POINT('Ctrl Pts',(-157.226626101121,-1.73761718720378,
135.405433272201));
#113895=CARTESIAN_POINT('Ctrl Pts',(-157.234399001387,-1.60935243486022,
135.453873071986));
#113896=CARTESIAN_POINT('Ctrl Pts',(-157.242171901652,-1.47919653835052,
135.496894031036));
#113897=CARTESIAN_POINT('Ctrl Pts',(-157.249944801917,-1.34765012154788,
135.534373536406));
#113898=CARTESIAN_POINT('Ctrl Pts',(-157.257435137679,-1.22088574834322,
135.57049056735));
#113899=CARTESIAN_POINT('Ctrl Pts',(-157.264925473441,-1.09283049685582,
135.601461969015));
#113900=CARTESIAN_POINT('Ctrl Pts',(-157.272415809203,-0.963938465976928,
135.627223428834));
#113901=CARTESIAN_POINT('Ctrl Pts',(-157.280190143322,-0.830159454569675,
135.653961642232));
#113902=CARTESIAN_POINT('Ctrl Pts',(-157.287964477441,-0.695055186511383,
135.675171743711));
#113903=CARTESIAN_POINT('Ctrl Pts',(-157.29573881156,-0.559122314154034,
135.690725861826));
#113904=CARTESIAN_POINT('Ctrl Pts',(-157.303503564507,-0.423356966913566,
135.706260810881));
#113905=CARTESIAN_POINT('Ctrl Pts',(-157.311268317455,-0.286765431921058,
135.716153601756));
#113906=CARTESIAN_POINT('Ctrl Pts',(-157.319033070402,-0.149855782785903,
135.720327084789));
#113907=CARTESIAN_POINT('Ctrl Pts',(-157.326790111287,-0.0130821142439842,
135.72449642266));
#113908=CARTESIAN_POINT('Ctrl Pts',(-157.334547152171,0.124008651420045,
135.722957745299));
#113909=CARTESIAN_POINT('Ctrl Pts',(-157.342304193056,0.260902419850325,
135.715685590505));
#113910=CARTESIAN_POINT('Ctrl Pts',(-157.350055384297,0.397692955625139,
135.7084189197));
#113911=CARTESIAN_POINT('Ctrl Pts',(-157.357806575537,0.534286401025188,
135.695427398101));
#113912=CARTESIAN_POINT('Ctrl Pts',(-157.365557766777,0.670168114574924,
135.676737630966));
#113913=CARTESIAN_POINT('Ctrl Pts',(-157.373305663554,0.805992074771452,
135.65805580748));
#113914=CARTESIAN_POINT('Ctrl Pts',(-157.381053560331,0.941104518269342,
135.633680608608));
#113915=CARTESIAN_POINT('Ctrl Pts',(-157.388801457108,1.07499560200768,
135.603690520601));
#113916=CARTESIAN_POINT('Ctrl Pts',(-157.396547733192,1.20885867861767,
135.573706705874));
#113917=CARTESIAN_POINT('Ctrl Pts',(-157.404294009276,1.34150052236585,
135.538110423585));
#113918=CARTESIAN_POINT('Ctrl Pts',(-157.41204028536,1.47242155889865,135.497031266076));
#113919=CARTESIAN_POINT('Ctrl Pts',(-157.419786618626,1.60334356186061,
135.455951805331));
#113920=CARTESIAN_POINT('Ctrl Pts',(-157.427532951891,1.73254435922677,
135.409389505652));
#113921=CARTESIAN_POINT('Ctrl Pts',(-157.435279285156,1.85953999890823,
135.357523699969));
#113922=CARTESIAN_POINT('Ctrl Pts',(-157.443027353159,1.9865640783825,135.305646279299));
#113923=CARTESIAN_POINT('Ctrl Pts',(-157.450775421162,2.11138165563383,
135.248463137064));
#113924=CARTESIAN_POINT('Ctrl Pts',(-157.458523489165,2.23352957422692,
135.186201406955));
#113925=CARTESIAN_POINT('Ctrl Pts',(-157.466279791907,2.35580731308164,
135.123873504339));
#113926=CARTESIAN_POINT('Ctrl Pts',(-157.474036094649,2.47540937649589,
135.056456409427));
#113927=CARTESIAN_POINT('Ctrl Pts',(-157.481792397391,2.59189752692306,
134.984223088082));
#113928=CARTESIAN_POINT('Ctrl Pts',(-157.489552839905,2.70844785058351,
134.911951213639));
#113929=CARTESIAN_POINT('Ctrl Pts',(-157.497313282419,2.82188062640686,
134.834858210351));
#113930=CARTESIAN_POINT('Ctrl Pts',(-157.505073724933,2.93178820014002,
134.753259326323));
#113931=CARTESIAN_POINT('Ctrl Pts',(-157.512846625199,3.04187220726768,
134.671529452521));
#113932=CARTESIAN_POINT('Ctrl Pts',(-157.520619525464,3.14841939983107,
134.585279489793));
#113933=CARTESIAN_POINT('Ctrl Pts',(-157.528392425729,3.25105602065565,
134.49486435189));
#113934=CARTESIAN_POINT('Ctrl Pts',(-157.535882761492,3.34996154178944,
134.407736031989));
#113935=CARTESIAN_POINT('Ctrl Pts',(-157.543373097254,3.44523565052182,
134.316740321315));
#113936=CARTESIAN_POINT('Ctrl Pts',(-157.550863433016,3.53657878732559,
134.222224503612));
#113937=CARTESIAN_POINT('Ctrl Pts',(-157.558637767135,3.63138522692268,
134.124125089955));
#113938=CARTESIAN_POINT('Ctrl Pts',(-157.566412101254,3.72225704298993,
134.021922620821));
#113939=CARTESIAN_POINT('Ctrl Pts',(-157.574186435373,3.80881820092998,
133.915965826259));
#113940=CARTESIAN_POINT('Ctrl Pts',(-157.58195118832,3.89527267997883,133.810139613977));
#113941=CARTESIAN_POINT('Ctrl Pts',(-157.589715941267,3.97742682621833,
133.700568582227));
#113942=CARTESIAN_POINT('Ctrl Pts',(-157.597480694215,4.05494110525508,
133.587638486449));
#113943=CARTESIAN_POINT('Ctrl Pts',(-157.6052377351,4.13237839601712,133.474820554434));
#113944=CARTESIAN_POINT('Ctrl Pts',(-157.612994775985,4.2051847706449,133.35865051797));
#113945=CARTESIAN_POINT('Ctrl Pts',(-157.62075181687,4.27306092651146,133.239547136258));
#113946=CARTESIAN_POINT('Ctrl Pts',(-157.62850300811,4.3408858964408,133.120533571333));
#113947=CARTESIAN_POINT('Ctrl Pts',(-157.63625419935,4.40378785509949,132.998591402431));
#113948=CARTESIAN_POINT('Ctrl Pts',(-157.64400539059,4.46151100995585,132.874167992793));
#113949=CARTESIAN_POINT('Ctrl Pts',(-157.651753287367,4.51920963093165,
132.749797466422));
#113950=CARTESIAN_POINT('Ctrl Pts',(-157.659501184144,4.57173366179417,
132.622948150736));
#113951=CARTESIAN_POINT('Ctrl Pts',(-157.667249080921,4.6188735526225,132.494091414878));
#113952=CARTESIAN_POINT('Ctrl Pts',(-157.674995357005,4.66600358280189,
132.365261633071));
#113953=CARTESIAN_POINT('Ctrl Pts',(-157.682741633089,4.70775157887593,
132.234425633249));
#113954=CARTESIAN_POINT('Ctrl Pts',(-157.690487909174,4.74395653841211,
132.10207376929));
#113955=CARTESIAN_POINT('Ctrl Pts',(-157.698234242439,4.78016176520513,
131.969720928339));
#113956=CARTESIAN_POINT('Ctrl Pts',(-157.705980575704,4.81082377065371,
131.835852578034));
#113957=CARTESIAN_POINT('Ctrl Pts',(-157.71372690897,4.83583184470548,131.700972814802));
#113958=CARTESIAN_POINT('Ctrl Pts',(-157.721474976973,4.860845519142,131.566062846182));
#113959=CARTESIAN_POINT('Ctrl Pts',(-157.729223044976,4.8802026714119,131.430141398269));
#113960=CARTESIAN_POINT('Ctrl Pts',(-157.736971112979,4.89384404815594,
131.293720908996));
#113961=CARTESIAN_POINT('Ctrl Pts',(-157.74472741572,4.90749992311754,131.157155430404));
#113962=CARTESIAN_POINT('Ctrl Pts',(-157.752483718462,4.91542784853478,
131.020090240593));
#113963=CARTESIAN_POINT('Ctrl Pts',(-157.760240021204,4.9176206002208,130.883041585939));
#113964=CARTESIAN_POINT('Ctrl Pts',(-157.768000463718,4.91981452224442,
130.745919784291));
#113965=CARTESIAN_POINT('Ctrl Pts',(-157.775760906232,4.91626718127279,
130.608814926029));
#113966=CARTESIAN_POINT('Ctrl Pts',(-157.783521348747,4.90702345738327,
130.472240381521));
#113967=CARTESIAN_POINT('Ctrl Pts',(-157.791294249012,4.89776489464754,
130.335446595431));
#113968=CARTESIAN_POINT('Ctrl Pts',(-157.799067149277,4.88279171841866,
130.199185213126));
#113969=CARTESIAN_POINT('Ctrl Pts',(-157.806840049543,4.86220050280511,
130.063962526657));
#113970=CARTESIAN_POINT('Ctrl Pts',(-157.814330385305,4.84235782974526,
129.933655525446));
#113971=CARTESIAN_POINT('Ctrl Pts',(-157.821820721067,4.81729854419249,
129.804313315156));
#113972=CARTESIAN_POINT('Ctrl Pts',(-157.829311056829,4.7871529065549,129.676375639048));
#113973=CARTESIAN_POINT('Ctrl Pts',(-157.837085390948,4.75586428790367,
129.543587167064));
#113974=CARTESIAN_POINT('Ctrl Pts',(-157.844859725067,4.71899689234862,
129.411891203582));
#113975=CARTESIAN_POINT('Ctrl Pts',(-157.852634059186,4.67664086047165,
129.281792614268));
#113976=CARTESIAN_POINT('Ctrl Pts',(-157.860398812133,4.63433702861861,
129.151854359839));
#113977=CARTESIAN_POINT('Ctrl Pts',(-157.86816356508,4.58655813916371,129.023509930799));
#113978=CARTESIAN_POINT('Ctrl Pts',(-157.875928318028,4.53344521244988,
128.897253497288));
#113979=CARTESIAN_POINT('Ctrl Pts',(-157.883685358913,4.48038503824348,
128.771122463446));
#113980=CARTESIAN_POINT('Ctrl Pts',(-157.891442399798,4.42200152034097,
128.647075656168));
#113981=CARTESIAN_POINT('Ctrl Pts',(-157.899199440683,4.35848519233676,
128.525591236808));
#113982=CARTESIAN_POINT('Ctrl Pts',(-157.906950631923,4.29501676248966,
128.404198429793));
#113983=CARTESIAN_POINT('Ctrl Pts',(-157.914701823163,4.22642340733128,
128.285364509603));
#113984=CARTESIAN_POINT('Ctrl Pts',(-157.922453014403,4.15294324411424,
128.169546492496));
#113985=CARTESIAN_POINT('Ctrl Pts',(-157.93020091118,4.07949431192661,128.053777701137));
#113986=CARTESIAN_POINT('Ctrl Pts',(-157.937948807957,4.00116291173236,
127.941022592819));
#113987=CARTESIAN_POINT('Ctrl Pts',(-157.945696704734,3.91823235289083,
127.831712254362));
#113988=CARTESIAN_POINT('Ctrl Pts',(-157.953442980819,3.83531914133443,
127.722424781271));
#113989=CARTESIAN_POINT('Ctrl Pts',(-157.961189256903,3.74780892084494,
127.616580956058));
#113990=CARTESIAN_POINT('Ctrl Pts',(-157.968935532987,3.65602721428102,
127.514581282879));
#113991=CARTESIAN_POINT('Ctrl Pts',(-157.976681866252,3.56424483020552,
127.412580856761));
#113992=CARTESIAN_POINT('Ctrl Pts',(-157.984428199517,3.4681911586511,127.314424929928));
#113993=CARTESIAN_POINT('Ctrl Pts',(-157.992174532783,3.36823046873152,
127.220479122314));
#113994=CARTESIAN_POINT('Ctrl Pts',(-157.999922600786,3.26824739330839,
127.126512276188));
#113995=CARTESIAN_POINT('Ctrl Pts',(-158.007670668789,3.1643558433096,127.036757693097));
#113996=CARTESIAN_POINT('Ctrl Pts',(-158.015418736792,3.05695491939445,
126.951542209791));
#113997=CARTESIAN_POINT('Ctrl Pts',(-158.023175039534,2.94943984849941,
126.866236158455));
#113998=CARTESIAN_POINT('Ctrl Pts',(-158.030931342275,2.83840825976152,
126.785479087175));
#113999=CARTESIAN_POINT('Ctrl Pts',(-158.038687645017,2.72429058102847,
126.709556117639));
#114000=CARTESIAN_POINT('Ctrl Pts',(-158.046448087532,2.61011199425426,
126.633592625729));
#114001=CARTESIAN_POINT('Ctrl Pts',(-158.054208530046,2.49284436954304,
126.562468579292));
#114002=CARTESIAN_POINT('Ctrl Pts',(-158.06196897256,2.37294387870398,126.496423708671));
#114003=CARTESIAN_POINT('Ctrl Pts',(-158.069741872825,2.25285091295277,
126.430272816961));
#114004=CARTESIAN_POINT('Ctrl Pts',(-158.077514773091,2.13011698540537,
126.36921756868));
#114005=CARTESIAN_POINT('Ctrl Pts',(-158.085287673356,2.00522025456549,
126.313450376515));
#114006=CARTESIAN_POINT('Ctrl Pts',(-158.092778009118,1.88486383448922,
126.259710462255));
#114007=CARTESIAN_POINT('Ctrl Pts',(-158.10026834488,1.76249941386373,126.210880924886));
#114008=CARTESIAN_POINT('Ctrl Pts',(-158.107758680642,1.63856737008093,
126.167089864612));
#114009=CARTESIAN_POINT('Ctrl Pts',(-158.115533014761,1.50993640518813,
126.121638452977));
#114010=CARTESIAN_POINT('Ctrl Pts',(-158.12330734888,1.37920913345374,126.081471151881));
#114011=CARTESIAN_POINT('Ctrl Pts',(-158.131081682999,1.24685903584777,
126.046785015726));
#114012=CARTESIAN_POINT('Ctrl Pts',(-158.138846435946,1.11467204790863,
126.012141627133));
#114013=CARTESIAN_POINT('Ctrl Pts',(-158.146611188894,0.980866588039771,
125.982966061117));
#114014=CARTESIAN_POINT('Ctrl Pts',(-158.154375941841,0.845934640514557,
125.9594067843));
#114015=CARTESIAN_POINT('Ctrl Pts',(-158.162132982726,0.711136709301832,
125.935870906889));
#114016=CARTESIAN_POINT('Ctrl Pts',(-158.169890023611,0.57521489962812,
125.917940284662));
#114017=CARTESIAN_POINT('Ctrl Pts',(-158.177647064496,0.43867449024398,
125.905713074202));
#114018=CARTESIAN_POINT('Ctrl Pts',(-158.185398255736,0.302237047044501,
125.893495084376));
#114019=CARTESIAN_POINT('Ctrl Pts',(-158.193149446976,0.165182320487663,
125.886971980192));
#114020=CARTESIAN_POINT('Ctrl Pts',(-158.200900638216,0.0280235194879294,
125.886190455315));
#114021=CARTESIAN_POINT('Ctrl Pts',(-158.208648534993,-0.109076985362361,
125.885409262607));
#114022=CARTESIAN_POINT('Ctrl Pts',(-158.21639643177,-0.246281086536319,
125.890364797808));
#114023=CARTESIAN_POINT('Ctrl Pts',(-158.224144328547,-0.383072962855172,
125.901051717687));
#114024=CARTESIAN_POINT('Ctrl Pts',(-158.231890604631,-0.51983622526239,
125.911736402093));
#114025=CARTESIAN_POINT('Ctrl Pts',(-158.239636880715,-0.656187044797271,
125.928150056102));
#114026=CARTESIAN_POINT('Ctrl Pts',(-158.2473831568,-0.791612512914426,
125.950235290394));
#114027=CARTESIAN_POINT('Ctrl Pts',(-158.255129490065,-0.927038980711439,
125.972320687713));
#114028=CARTESIAN_POINT('Ctrl Pts',(-158.26287582333,-1.06153969759273,
126.000077685928));
#114029=CARTESIAN_POINT('Ctrl Pts',(-158.270622156596,-1.1946101607984,
126.033397441622));
#114030=CARTESIAN_POINT('Ctrl Pts',(-158.278370224598,-1.32771042421147,
126.066724659044));
#114031=CARTESIAN_POINT('Ctrl Pts',(-158.286118292601,-1.45937941741378,
126.105617017881));
#114032=CARTESIAN_POINT('Ctrl Pts',(-158.293866360604,-1.58912643973627,
126.149915406692));
#114033=CARTESIAN_POINT('Ctrl Pts',(-158.301622663346,-1.71901135873827,
126.194260876357));
#114034=CARTESIAN_POINT('Ctrl Pts',(-158.309378966088,-1.8469698557755,
126.244023726912));
#114035=CARTESIAN_POINT('Ctrl Pts',(-158.31713526883,-1.97252939313016,
126.298995942455));
#114036=CARTESIAN_POINT('Ctrl Pts',(-158.324895711344,-2.09815594539077,
126.353997498325));
#114037=CARTESIAN_POINT('Ctrl Pts',(-158.332656153858,-2.22138063557395,
126.414213787785));
#114038=CARTESIAN_POINT('Ctrl Pts',(-158.340416596372,-2.34175519974607,
126.47939060068));
#114039=CARTESIAN_POINT('Ctrl Pts',(-158.348189496638,-2.46232299985494,
126.544672041181));
#114040=CARTESIAN_POINT('Ctrl Pts',(-158.355962396903,-2.5800311951905,
126.614929717379));
#114041=CARTESIAN_POINT('Ctrl Pts',(-158.363735297169,-2.69445944715936,
126.689865344739));
#114042=CARTESIAN_POINT('Ctrl Pts',(-158.371225632931,-2.80472794394272,
126.762076873294));
#114043=CARTESIAN_POINT('Ctrl Pts',(-158.378715968693,-2.91195057492315,
126.838631968233));
#114044=CARTESIAN_POINT('Ctrl Pts',(-158.386206304455,-3.01578153103443,
126.919229368873));
#114045=CARTESIAN_POINT('Ctrl Pts',(-158.393887986589,-3.12226492854991,
127.001885691924));
#114046=CARTESIAN_POINT('Ctrl Pts',(-158.401569668722,-3.22553542916593,
127.089068988183));
#114047=CARTESIAN_POINT('Ctrl Pts',(-158.409251350856,-3.32517684946278,
127.180497763884));
#114048=CARTESIAN_POINT('Ctrl Pts',(-158.416924255383,-3.42470441277153,
127.271822066916));
#114049=CARTESIAN_POINT('Ctrl Pts',(-158.42459715991,-3.52061084737626,
127.367381937551));
#114050=CARTESIAN_POINT('Ctrl Pts',(-158.432270064437,-3.61251025297089,
127.466853653576));
#114051=CARTESIAN_POINT('Ctrl Pts',(-158.439935958313,-3.70432569105768,
127.566234483354));
#114052=CARTESIAN_POINT('Ctrl Pts',(-158.447601852189,-3.79214110987175,
127.669519759237));
#114053=CARTESIAN_POINT('Ctrl Pts',(-158.455267746065,-3.87560533796325,
127.776347023334));
#114054=CARTESIAN_POINT('Ctrl Pts',(-158.46292839003,-3.9590124064113,127.883101127846));
#114055=CARTESIAN_POINT('Ctrl Pts',(-158.470589033995,-4.03807396514902,
127.993392081312));
#114056=CARTESIAN_POINT('Ctrl Pts',(-158.47824967796,-4.11247760218458,
128.106822659718));
#114057=CARTESIAN_POINT('Ctrl Pts',(-158.485907859796,-4.18685732591744,
128.220216781576));
#114058=CARTESIAN_POINT('Ctrl Pts',(-158.493566041633,-4.25658188049758,
128.336748190372));
#114059=CARTESIAN_POINT('Ctrl Pts',(-158.50122422347,-4.32138107082593,
128.455989117312));
#114060=CARTESIAN_POINT('Ctrl Pts',(-158.508880677199,-4.38616563888634,
128.575203136928));
#114061=CARTESIAN_POINT('Ctrl Pts',(-158.516537130928,-4.44602686532444,
128.697125104533));
#114062=CARTESIAN_POINT('Ctrl Pts',(-158.524193584657,-4.50073995299582,
128.821301632562));
#114063=CARTESIAN_POINT('Ctrl Pts',(-158.531853047558,-4.55547454424035,
128.945526964984));
#114064=CARTESIAN_POINT('Ctrl Pts',(-158.539512510459,-4.60505678905809,
129.072008262286));
#114065=CARTESIAN_POINT('Ctrl Pts',(-158.547171973361,-4.64930959280485,
129.200271040032));
#114066=CARTESIAN_POINT('Ctrl Pts',(-158.554687103784,-4.69272851082307,
129.326116874877));
#114067=CARTESIAN_POINT('Ctrl Pts',(-158.562202234208,-4.73101699474162,
129.453677277636));
#114068=CARTESIAN_POINT('Ctrl Pts',(-158.569717364632,-4.76405452823396,
129.582490119308));
#114069=CARTESIAN_POINT('Origin',(213.235140564004,0.,130.804360617566));
#114070=CARTESIAN_POINT('',(-160.665416397755,-4.76405452823408,129.582490119308));
#114071=CARTESIAN_POINT('',(-160.319851210837,-4.76405452823417,129.582490119309));
#114072=CARTESIAN_POINT('',(213.235140564004,-4.76405452823405,129.582490119308));
#114073=CARTESIAN_POINT('',(-158.98514056405,-4.91824792883793,130.799846973648));
#114074=CARTESIAN_POINT('Ctrl Pts',(-158.985140564049,-4.91824792883793,
130.799846973648));
#114075=CARTESIAN_POINT('Ctrl Pts',(-158.992793339069,-4.9183718573925,
130.934884510481));
#114076=CARTESIAN_POINT('Ctrl Pts',(-159.000446114088,-4.91293013258963,
131.070088370763));
#114077=CARTESIAN_POINT('Ctrl Pts',(-159.008098889108,-4.90190847227337,
131.204955664908));
#114078=CARTESIAN_POINT('Ctrl Pts',(-159.015745855889,-4.890895177083,131.339720598622));
#114079=CARTESIAN_POINT('Ctrl Pts',(-159.023392822671,-4.87431040414284,
131.474149074946));
#114080=CARTESIAN_POINT('Ctrl Pts',(-159.031039789452,-4.85219193961457,
131.607738762426));
#114081=CARTESIAN_POINT('Ctrl Pts',(-159.03868359274,-4.83008262533319,
131.741273184831));
#114082=CARTESIAN_POINT('Ctrl Pts',(-159.046327396027,-4.80244423546131,
131.873969111832));
#114083=CARTESIAN_POINT('Ctrl Pts',(-159.053971199314,-4.76936630563182,
132.00533026964));
#114084=CARTESIAN_POINT('Ctrl Pts',(-159.061613585034,-4.73629451020871,
132.136667066108));
#114085=CARTESIAN_POINT('Ctrl Pts',(-159.069255970754,-4.69778527864374,
132.266669195356));
#114086=CARTESIAN_POINT('Ctrl Pts',(-159.076898356474,-4.65397895016428,
132.394852049145));
#114087=CARTESIAN_POINT('Ctrl Pts',(-159.084541085085,-4.61017065622125,
132.52304065413));
#114088=CARTESIAN_POINT('Ctrl Pts',(-159.092183813697,-4.56106492320184,
132.649409440511));
#114089=CARTESIAN_POINT('Ctrl Pts',(-159.099826542309,-4.50685132596009,
132.773490930215));
#114090=CARTESIAN_POINT('Ctrl Pts',(-159.107471374328,-4.4526228082238,
132.897606569233));
#114091=CARTESIAN_POINT('Ctrl Pts',(-159.115116206347,-4.3932837923077,
133.019433291276));
#114092=CARTESIAN_POINT('Ctrl Pts',(-159.122761038366,-4.329070918503,133.138526002682));
#114093=CARTESIAN_POINT('Ctrl Pts',(-159.130413981656,-4.26478991396683,
133.257745073071));
#114094=CARTESIAN_POINT('Ctrl Pts',(-159.138066924946,-4.19562492009736,
133.374223987828));
#114095=CARTESIAN_POINT('Ctrl Pts',(-159.145719868236,-4.12185737810384,
133.48754432672));
#114096=CARTESIAN_POINT('Ctrl Pts',(-159.153377439648,-4.04804522514282,
133.600933196159));
#114097=CARTESIAN_POINT('Ctrl Pts',(-159.16103501106,-3.96962521613434,
133.711159360329));
#114098=CARTESIAN_POINT('Ctrl Pts',(-159.168692582472,-3.88691978986297,
133.817836618743));
#114099=CARTESIAN_POINT('Ctrl Pts',(-159.176361230224,-3.80409473383051,
133.92466818112));
#114100=CARTESIAN_POINT('Ctrl Pts',(-159.184029877976,-3.71697214657841,
134.027940285255));
#114101=CARTESIAN_POINT('Ctrl Pts',(-159.191698525729,-3.62591231128936,
134.127302532999));
#114102=CARTESIAN_POINT('Ctrl Pts',(-159.195119077063,-3.58529565354169,
134.171622428778));
#114103=CARTESIAN_POINT('Ctrl Pts',(-159.198539628398,-3.54389611784006,
134.215164962064));
#114104=CARTESIAN_POINT('Ctrl Pts',(-159.201960179733,-3.50174776517832,
134.257901648388));
#114105=CARTESIAN_POINT('Ctrl Pts',(-159.209734513852,-3.4059516948696,
134.35503490151));
#114106=CARTESIAN_POINT('Ctrl Pts',(-159.217508847971,-3.30595933054666,
134.448333126196));
#114107=CARTESIAN_POINT('Ctrl Pts',(-159.22528318209,-3.20211027803959,
134.537412027575));
#114108=CARTESIAN_POINT('Ctrl Pts',(-159.233047935037,-3.09838921020848,
134.62638114717));
#114109=CARTESIAN_POINT('Ctrl Pts',(-159.240812687984,-2.99082120519507,
134.711141037687));
#114110=CARTESIAN_POINT('Ctrl Pts',(-159.248577440931,-2.8797837594613,
134.791343005443));
#114111=CARTESIAN_POINT('Ctrl Pts',(-159.256334481816,-2.76885659768368,
134.871465315474));
#114112=CARTESIAN_POINT('Ctrl Pts',(-159.264091522701,-2.65446716756238,
134.947038484225));
#114113=CARTESIAN_POINT('Ctrl Pts',(-159.271848563586,-2.53702692526766,
135.017753246193));
#114114=CARTESIAN_POINT('Ctrl Pts',(-159.279599754827,-2.41967524557337,
135.088414681609));
#114115=CARTESIAN_POINT('Ctrl Pts',(-159.287350946067,-2.29927766657136,
135.15422480188));
#114116=CARTESIAN_POINT('Ctrl Pts',(-159.295102137307,-2.17627528435696,
135.214917152653));
#114117=CARTESIAN_POINT('Ctrl Pts',(-159.302850034084,-2.05332518143635,
135.275583707557));
#114118=CARTESIAN_POINT('Ctrl Pts',(-159.310597930861,-1.92777282713566,
135.331136646611));
#114119=CARTESIAN_POINT('Ctrl Pts',(-159.318345827638,-1.80008442623519,
135.38135516868));
#114120=CARTESIAN_POINT('Ctrl Pts',(-159.326092103722,-1.6724227349952,
135.431563186116));
#114121=CARTESIAN_POINT('Ctrl Pts',(-159.333838379806,-1.5426262495021,
135.47643886304));
#114122=CARTESIAN_POINT('Ctrl Pts',(-159.34158465589,-1.41118131881087,
135.515809476244));
#114123=CARTESIAN_POINT('Ctrl Pts',(-159.349330989156,-1.27973541782321,
135.555180380073));
#114124=CARTESIAN_POINT('Ctrl Pts',(-159.357077322421,-1.14664142188218,
135.589046026913));
#114125=CARTESIAN_POINT('Ctrl Pts',(-159.364823655686,-1.01240062551212,
135.617283641671));
#114126=CARTESIAN_POINT('Ctrl Pts',(-159.372571723689,-0.878129766847015,
135.645527580047));
#114127=CARTESIAN_POINT('Ctrl Pts',(-159.380319791692,-0.742711979234038,
135.668140897909));
#114128=CARTESIAN_POINT('Ctrl Pts',(-159.388067859695,-0.606658131120976,
135.685052061864));
#114129=CARTESIAN_POINT('Ctrl Pts',(-159.395824162437,-0.470459683358521,
135.701981199205));
#114130=CARTESIAN_POINT('Ctrl Pts',(-159.403580465179,-0.333624213286068,
135.713196028202));
#114131=CARTESIAN_POINT('Ctrl Pts',(-159.411336767921,-0.196667645253042,
135.718676938257));
#114132=CARTESIAN_POINT('Ctrl Pts',(-159.419097210435,-0.0596379793756009,
135.724160773639));
#114133=CARTESIAN_POINT('Ctrl Pts',(-159.426857652949,0.0775125224771561,
135.723904592773));
#114134=CARTESIAN_POINT('Ctrl Pts',(-159.434618095463,0.214269560775753,
135.717940943339));
#114135=CARTESIAN_POINT('Ctrl Pts',(-159.442390995729,0.351246133612573,
135.711967720526));
#114136=CARTESIAN_POINT('Ctrl Pts',(-159.450163895994,0.487827590948962,
135.700268753663));
#114137=CARTESIAN_POINT('Ctrl Pts',(-159.457936796259,0.623505469023936,
135.682928439437));
#114138=CARTESIAN_POINT('Ctrl Pts',(-159.465427132022,0.754251114482975,
135.66621848931));
#114139=CARTESIAN_POINT('Ctrl Pts',(-159.472917467784,0.884157431173136,
135.644270276624));
#114140=CARTESIAN_POINT('Ctrl Pts',(-159.480407803546,1.01278167657808,
135.617203471648));
#114141=CARTESIAN_POINT('Ctrl Pts',(-159.488182137665,1.14628274933811,
135.589110420536));
#114142=CARTESIAN_POINT('Ctrl Pts',(-159.495956471784,1.27882550347499,
135.555413981878));
#114143=CARTESIAN_POINT('Ctrl Pts',(-159.503730805903,1.40990305558572,
135.516192154914));
#114144=CARTESIAN_POINT('Ctrl Pts',(-159.51149555885,1.54081906632821,135.477018665347));
#114145=CARTESIAN_POINT('Ctrl Pts',(-159.519260311798,1.67027309694941,
135.432333447445));
#114146=CARTESIAN_POINT('Ctrl Pts',(-159.527025064745,1.79776773551994,
135.382265622219));
#114147=CARTESIAN_POINT('Ctrl Pts',(-159.53478210563,1.92513574461842,135.332247525062));
#114148=CARTESIAN_POINT('Ctrl Pts',(-159.542539146515,2.0505478729293,135.276857601511));
#114149=CARTESIAN_POINT('Ctrl Pts',(-159.5502961874,2.17352152451703,135.216274855735));
#114150=CARTESIAN_POINT('Ctrl Pts',(-159.55804737864,2.29640244071768,135.15573779588));
#114151=CARTESIAN_POINT('Ctrl Pts',(-159.56579856988,2.41684819106677,135.090015880336));
#114152=CARTESIAN_POINT('Ctrl Pts',(-159.57354976112,2.534396176756,135.019336190656));
#114153=CARTESIAN_POINT('Ctrl Pts',(-159.581297657897,2.65189420141546,
134.948686541729));
#114154=CARTESIAN_POINT('Ctrl Pts',(-159.589045554674,2.76649657666931,
134.873083510743));
#114155=CARTESIAN_POINT('Ctrl Pts',(-159.596793451451,2.87776554119744,
134.792799980575));
#114156=CARTESIAN_POINT('Ctrl Pts',(-159.604539727536,2.98901123065688,
134.71253324399));
#114157=CARTESIAN_POINT('Ctrl Pts',(-159.61228600362,3.09692457946296,134.627588184244));
#114158=CARTESIAN_POINT('Ctrl Pts',(-159.620032279704,3.20109738714437,
134.538280619456));
#114159=CARTESIAN_POINT('Ctrl Pts',(-159.627778612969,3.30527096380593,
134.448972395421));
#114160=CARTESIAN_POINT('Ctrl Pts',(-159.635524946235,3.40570364742586,
134.355301856549));
#114161=CARTESIAN_POINT('Ctrl Pts',(-159.6432712795,3.50202118190441,134.257624393184));
#114162=CARTESIAN_POINT('Ctrl Pts',(-159.651019347503,3.59836028602659,
134.159925055628));
#114163=CARTESIAN_POINT('Ctrl Pts',(-159.658767415506,3.69058213275458,
134.058217286343));
#114164=CARTESIAN_POINT('Ctrl Pts',(-159.666515483509,3.77835040214406,
133.952892227875));
#114165=CARTESIAN_POINT('Ctrl Pts',(-159.674271786251,3.86621195269483,
133.847455228682));
#114166=CARTESIAN_POINT('Ctrl Pts',(-159.682028088993,3.94961021991599,
133.738393561338));
#114167=CARTESIAN_POINT('Ctrl Pts',(-159.689784391734,4.02824983514469,
133.626130687603));
#114168=CARTESIAN_POINT('Ctrl Pts',(-159.697544834249,4.10693142270382,
133.513807895792));
#114169=CARTESIAN_POINT('Ctrl Pts',(-159.705305276763,4.18084908682414,
133.398280822264));
#114170=CARTESIAN_POINT('Ctrl Pts',(-159.713065719277,4.24975221933218,
133.279999754593));
#114171=CARTESIAN_POINT('Ctrl Pts',(-159.720838619542,4.31876596126544,
133.161528811652));
#114172=CARTESIAN_POINT('Ctrl Pts',(-159.728611519808,4.38274890298996,
133.040295386055));
#114173=CARTESIAN_POINT('Ctrl Pts',(-159.736384420073,4.44149721274379,
132.916772881233));
#114174=CARTESIAN_POINT('Ctrl Pts',(-159.743874755835,4.4981098734592,132.797740730597));
#114175=CARTESIAN_POINT('Ctrl Pts',(-159.751365091597,4.54986175782703,
132.67658332216));
#114176=CARTESIAN_POINT('Ctrl Pts',(-159.758855427359,4.59661423469048,
132.553737832446));
#114177=CARTESIAN_POINT('Ctrl Pts',(-159.766629761478,4.64513934592479,
132.426234618649));
#114178=CARTESIAN_POINT('Ctrl Pts',(-159.774404095597,4.68843217389684,
132.296508897613));
#114179=CARTESIAN_POINT('Ctrl Pts',(-159.782178429716,4.72628435871543,
132.165029285193));
#114180=CARTESIAN_POINT('Ctrl Pts',(-159.789943182663,4.76408989409937,
132.033711709644));
#114181=CARTESIAN_POINT('Ctrl Pts',(-159.79770793561,4.79646802036818,131.90064491558));
#114182=CARTESIAN_POINT('Ctrl Pts',(-159.805472688558,4.8232585073882,131.766317182805));
#114183=CARTESIAN_POINT('Ctrl Pts',(-159.813229729443,4.85002238571876,
131.632122866229));
#114184=CARTESIAN_POINT('Ctrl Pts',(-159.820986770328,4.87120959302418,
131.496670484172));
#114185=CARTESIAN_POINT('Ctrl Pts',(-159.828743811213,4.88670987569229,
131.360462814389));
#114186=CARTESIAN_POINT('Ctrl Pts',(-159.836495002453,4.90219846947669,
131.22435785987));
#114187=CARTESIAN_POINT('Ctrl Pts',(-159.844246193693,4.91200863070341,
131.087499138202));
#114188=CARTESIAN_POINT('Ctrl Pts',(-159.851997384933,4.91608136355676,
130.950398589991));
#114189=CARTESIAN_POINT('Ctrl Pts',(-159.85974528171,4.92015236539,130.81335631317));
#114190=CARTESIAN_POINT('Ctrl Pts',(-159.867493178487,4.91849077737537,
130.676072804206));
#114191=CARTESIAN_POINT('Ctrl Pts',(-159.875241075264,4.91108956292033,
130.539063863958));
#114192=CARTESIAN_POINT('Ctrl Pts',(-159.882987351348,4.9036898966398,130.402083583027));
#114193=CARTESIAN_POINT('Ctrl Pts',(-159.890733627432,4.89055301306605,
130.26537814672));
#114194=CARTESIAN_POINT('Ctrl Pts',(-159.898479903516,4.87172397660285,
130.129461693065));
#114195=CARTESIAN_POINT('Ctrl Pts',(-159.906226236782,4.85289480114806,
129.993544236105));
#114196=CARTESIAN_POINT('Ctrl Pts',(-159.913972570047,4.8283734426092,129.858416160685));
#114197=CARTESIAN_POINT('Ctrl Pts',(-159.921718903312,4.79825660638337,
129.724584436222));
#114198=CARTESIAN_POINT('Ctrl Pts',(-159.929466971315,4.76813302570067,
129.590722741071));
#114199=CARTESIAN_POINT('Ctrl Pts',(-159.937215039318,4.73241155968775,
129.45815835591));
#114200=CARTESIAN_POINT('Ctrl Pts',(-159.944963107321,4.69123949850245,
129.327385658337));
#114201=CARTESIAN_POINT('Ctrl Pts',(-159.952719410063,4.65002367916073,
129.196473973984));
#114202=CARTESIAN_POINT('Ctrl Pts',(-159.960475712805,4.60334581018625,
129.067358154631));
#114203=CARTESIAN_POINT('Ctrl Pts',(-159.968232015547,4.5514025079743,128.940515593723));
#114204=CARTESIAN_POINT('Ctrl Pts',(-159.975992458061,4.49943148205784,
128.81360533312));
#114205=CARTESIAN_POINT('Ctrl Pts',(-159.983752900575,4.44218958619812,
128.688971103691));
#114206=CARTESIAN_POINT('Ctrl Pts',(-159.991513343089,4.37992020024621,
128.567067140622));
#114207=CARTESIAN_POINT('Ctrl Pts',(-159.999286243355,4.31755085394812,
128.44496748649));
#114208=CARTESIAN_POINT('Ctrl Pts',(-160.00705914362,4.25013808235659,128.3256071977));
#114209=CARTESIAN_POINT('Ctrl Pts',(-160.014832043886,4.17796999714021,
128.209413649804));
#114210=CARTESIAN_POINT('Ctrl Pts',(-160.022322379648,4.10842540360111,
128.097444030047));
#114211=CARTESIAN_POINT('Ctrl Pts',(-160.02981271541,4.03446540213675,127.988415165342));
#114212=CARTESIAN_POINT('Ctrl Pts',(-160.037303051172,3.95638286821043,
127.882679994597));
#114213=CARTESIAN_POINT('Ctrl Pts',(-160.045077385291,3.87533981127865,
127.772935842717));
#114214=CARTESIAN_POINT('Ctrl Pts',(-160.05285171941,3.78959871915223,127.66639243948));
#114215=CARTESIAN_POINT('Ctrl Pts',(-160.060626053529,3.69944122801285,
127.563478382282));
#114216=CARTESIAN_POINT('Ctrl Pts',(-160.068390806476,3.60939484792321,
127.460691157461));
#114217=CARTESIAN_POINT('Ctrl Pts',(-160.076155559423,3.51494315355772,
127.361524670306));
#114218=CARTESIAN_POINT('Ctrl Pts',(-160.083920312371,3.41641034024362,
127.266377654128));
#114219=CARTESIAN_POINT('Ctrl Pts',(-160.091677353256,3.31797539110931,
127.171325139309));
#114220=CARTESIAN_POINT('Ctrl Pts',(-160.09943439414,3.21546766894891,127.08028442064));
#114221=CARTESIAN_POINT('Ctrl Pts',(-160.107191435025,3.109250580157,126.993620021265));
#114222=CARTESIAN_POINT('Ctrl Pts',(-160.114942626265,3.00311359049814,
126.907020976189));
#114223=CARTESIAN_POINT('Ctrl Pts',(-160.122693817506,2.89327310368915,
126.82479192769));
#114224=CARTESIAN_POINT('Ctrl Pts',(-160.130445008746,2.78012794117947,
126.74725922702));
#114225=CARTESIAN_POINT('Ctrl Pts',(-160.138192905523,2.66703086838164,
126.669759479815));
#114226=CARTESIAN_POINT('Ctrl Pts',(-160.1459408023,2.55063223531128,126.596952330939));
#114227=CARTESIAN_POINT('Ctrl Pts',(-160.153688699077,2.43136219638818,
126.52912250344));
#114228=CARTESIAN_POINT('Ctrl Pts',(-160.161434975161,2.31211710618605,
126.461306864479));
#114229=CARTESIAN_POINT('Ctrl Pts',(-160.169181251245,2.19000214446463,
126.398466669145));
#114230=CARTESIAN_POINT('Ctrl Pts',(-160.176927527329,2.06547422851724,
126.340841907643));
#114231=CARTESIAN_POINT('Ctrl Pts',(-160.184673860595,1.94094539333288,
126.283216720768));
#114232=CARTESIAN_POINT('Ctrl Pts',(-160.19242019386,1.81400392319758,126.230807208736));
#114233=CARTESIAN_POINT('Ctrl Pts',(-160.200166527125,1.68512861746968,
126.183806039911));
#114234=CARTESIAN_POINT('Ctrl Pts',(-160.207914595128,1.55622445101008,
126.136794345501));
#114235=CARTESIAN_POINT('Ctrl Pts',(-160.215662663131,1.42538595443084,
126.095193538298));
#114236=CARTESIAN_POINT('Ctrl Pts',(-160.223410731134,1.29310867553237,
126.059146922087));
#114237=CARTESIAN_POINT('Ctrl Pts',(-160.231167033876,1.16069081076868,
126.023061995104));
#114238=CARTESIAN_POINT('Ctrl Pts',(-160.238923336618,1.02683148684558,
125.992543154068));
#114239=CARTESIAN_POINT('Ctrl Pts',(-160.24667963936,0.89203862435452,125.967683022857));
#114240=CARTESIAN_POINT('Ctrl Pts',(-160.254440081874,0.757173818853848,
125.942809623046));
#114241=CARTESIAN_POINT('Ctrl Pts',(-160.262200524388,0.621374868887031,
125.92360100584));
#114242=CARTESIAN_POINT('Ctrl Pts',(-160.269960966902,0.485155488136284,
125.910097934094));
#114243=CARTESIAN_POINT('Ctrl Pts',(-160.277733867168,0.348717435942938,
125.896573186017));
#114244=CARTESIAN_POINT('Ctrl Pts',(-160.285506767433,0.211857994831101,
125.888772308358));
#114245=CARTESIAN_POINT('Ctrl Pts',(-160.293279667699,0.0750924593514712,
125.886683911534));
#114246=CARTESIAN_POINT('Ctrl Pts',(-160.300770003461,-0.0567013044233523,
125.884671433195));
#114247=CARTESIAN_POINT('Ctrl Pts',(-160.308260339223,-0.18840756352225,
125.887963312532));
#114248=CARTESIAN_POINT('Ctrl Pts',(-160.315750674985,-0.319571074104795,
125.896503917224));
#114249=CARTESIAN_POINT('Ctrl Pts',(-160.323525009104,-0.455707689056029,
125.905368341538));
#114250=CARTESIAN_POINT('Ctrl Pts',(-160.331299343223,-0.591690826302174,
125.919915438741));
#114251=CARTESIAN_POINT('Ctrl Pts',(-160.339073677342,-0.727007663480937,
125.940139927698));
#114252=CARTESIAN_POINT('Ctrl Pts',(-160.346838430289,-0.862157734751858,
125.96033949178));
#114253=CARTESIAN_POINT('Ctrl Pts',(-160.354603183236,-0.996642756851381,
125.986202468677));
#114254=CARTESIAN_POINT('Ctrl Pts',(-160.362367936183,-1.12995202865933,
126.017671628773));
#114255=CARTESIAN_POINT('Ctrl Pts',(-160.370124977068,-1.26312889581919,
126.049109533256));
#114256=CARTESIAN_POINT('Ctrl Pts',(-160.377882017953,-1.39513195856115,
126.086142450845));
#114257=CARTESIAN_POINT('Ctrl Pts',(-160.385639058839,-1.52545810320711,
126.128661671113));
#114258=CARTESIAN_POINT('Ctrl Pts',(-160.393390250079,-1.65568596789307,
126.171148827306));
#114259=CARTESIAN_POINT('Ctrl Pts',(-160.401141441319,-1.78423906136659,
126.219113930433));
#114260=CARTESIAN_POINT('Ctrl Pts',(-160.408892632559,-1.91062724234163,
126.272397841536));
#114261=CARTESIAN_POINT('Ctrl Pts',(-160.416640529336,-2.03696170496875,
126.325659105556));
#114262=CARTESIAN_POINT('Ctrl Pts',(-160.424388426113,-2.16113272569281,
126.384234529758));
#114263=CARTESIAN_POINT('Ctrl Pts',(-160.43213632289,-2.28266824997923,
126.447916112808));
#114264=CARTESIAN_POINT('Ctrl Pts',(-160.439882598974,-2.40417835165429,
126.511584375044));
#114265=CARTESIAN_POINT('Ctrl Pts',(-160.447628875058,-2.52305370734948,
126.580356490281));
#114266=CARTESIAN_POINT('Ctrl Pts',(-160.455375151142,-2.63884543155285,
126.653977761627));
#114267=CARTESIAN_POINT('Ctrl Pts',(-160.463121484408,-2.75463801050396,
126.727599576428));
#114268=CARTESIAN_POINT('Ctrl Pts',(-160.470867817673,-2.86734658261668,
126.806070408995));
#114269=CARTESIAN_POINT('Ctrl Pts',(-160.478614150939,-2.97655024779111,
126.889091573825));
#114270=CARTESIAN_POINT('Ctrl Pts',(-160.486362218942,-3.08577836836934,
126.97213133067));
#114271=CARTESIAN_POINT('Ctrl Pts',(-160.494110286945,-3.19149970897399,
127.059723210931));
#114272=CARTESIAN_POINT('Ctrl Pts',(-160.501858354948,-3.29332584838174,
127.151527755405));
#114273=CARTESIAN_POINT('Ctrl Pts',(-160.509614657689,-3.39526020982207,
127.243429870842));
#114274=CARTESIAN_POINT('Ctrl Pts',(-160.517370960431,-3.49329080940013,
127.339553332108));
#114275=CARTESIAN_POINT('Ctrl Pts',(-160.525127263173,-3.58706517653859,
127.439520876692));
#114276=CARTESIAN_POINT('Ctrl Pts',(-160.532887705687,-3.68088959388028,
127.539541776965));
#114277=CARTESIAN_POINT('Ctrl Pts',(-160.540648148201,-3.77045299708215,
127.643410552802));
#114278=CARTESIAN_POINT('Ctrl Pts',(-160.548408590715,-3.85544341640844,
127.750717035651));
#114279=CARTESIAN_POINT('Ctrl Pts',(-160.556181490981,-3.94057026990094,
127.858195776392));
#114280=CARTESIAN_POINT('Ctrl Pts',(-160.563954391246,-4.02110924010688,
127.969122935338));
#114281=CARTESIAN_POINT('Ctrl Pts',(-160.571727291512,-4.096791380112,128.083058824244));
#114282=CARTESIAN_POINT('Ctrl Pts',(-160.579217627274,-4.16972228369511,
128.192852856598));
#114283=CARTESIAN_POINT('Ctrl Pts',(-160.586707963036,-4.23814318252366,
128.305440403681));
#114284=CARTESIAN_POINT('Ctrl Pts',(-160.594198298797,-4.3018548112296,
128.420408385326));
#114285=CARTESIAN_POINT('Ctrl Pts',(-160.602351087627,-4.37120116249653,
128.545544254579));
#114286=CARTESIAN_POINT('Ctrl Pts',(-160.610503876457,-4.43517049859319,
128.67386470153));
#114287=CARTESIAN_POINT('Ctrl Pts',(-160.618656665287,-4.49347352921566,
128.804891011711));
#114288=CARTESIAN_POINT('Ctrl Pts',(-160.626791612129,-4.55164896644803,
128.935630577088));
#114289=CARTESIAN_POINT('Ctrl Pts',(-160.634926558971,-4.60418268476158,
129.069063894864));
#114290=CARTESIAN_POINT('Ctrl Pts',(-160.643061505813,-4.65083102205554,
129.204687567601));
#114291=CARTESIAN_POINT('Ctrl Pts',(-160.650513136461,-4.6935610099174,
129.328919174256));
#114292=CARTESIAN_POINT('Ctrl Pts',(-160.657964767108,-4.73135320081311,
129.454988140006));
#114293=CARTESIAN_POINT('Ctrl Pts',(-160.665416397755,-4.76405452823407,
129.582490119308));
#114294=CARTESIAN_POINT('Ctrl Pts',(-158.915166007136,-4.76405452823407,
129.582490119308));
#114295=CARTESIAN_POINT('Ctrl Pts',(-158.917948190064,-4.77619699254554,
129.629833403371));
#114296=CARTESIAN_POINT('Ctrl Pts',(-158.920730372992,-4.78762722131158,
129.67733255829));
#114297=CARTESIAN_POINT('Ctrl Pts',(-158.92351255592,-4.79834208061758,
129.724964332657));
#114298=CARTESIAN_POINT('Ctrl Pts',(-158.934140375005,-4.839272382174,129.906915661448));
#114299=CARTESIAN_POINT('Ctrl Pts',(-158.944768194091,-4.86986636907114,
130.091270828495));
#114300=CARTESIAN_POINT('Ctrl Pts',(-158.955396013176,-4.88989965536501,
130.277042475491));
#114301=CARTESIAN_POINT('Ctrl Pts',(-158.965310863454,-4.90858900570155,
130.450351604227));
#114302=CARTESIAN_POINT('Ctrl Pts',(-158.975225713733,-4.91808736835487,
130.624893840766));
#114303=CARTESIAN_POINT('Ctrl Pts',(-158.985140564011,-4.9182479288373,
130.799846972967));
#114304=CARTESIAN_POINT('',(-158.639859435957,-4.91824933787898,130.806912666353));
#114305=CARTESIAN_POINT('Ctrl Pts',(-158.569717364632,-4.76405452823396,
129.582490119308));
#114306=CARTESIAN_POINT('Ctrl Pts',(-158.577384022907,-4.79775819872745,
129.713900219037));
#114307=CARTESIAN_POINT('Ctrl Pts',(-158.585050681181,-4.82599680652233,
129.846613416711));
#114308=CARTESIAN_POINT('Ctrl Pts',(-158.592717339456,-4.84869332716268,
129.980130017777));
#114309=CARTESIAN_POINT('Ctrl Pts',(-158.600574355539,-4.87195338667268,
130.116961743467));
#114310=CARTESIAN_POINT('Ctrl Pts',(-158.608431371623,-4.88939248921531,
130.25463684083));
#114311=CARTESIAN_POINT('Ctrl Pts',(-158.616288387706,-4.90098437315832,
130.392614049204));
#114312=CARTESIAN_POINT('Ctrl Pts',(-158.62414540379,-4.91257625710132,
130.530591257578));
#114313=CARTESIAN_POINT('Ctrl Pts',(-158.632002419873,-4.91832096728769,
130.66887012827));
#114314=CARTESIAN_POINT('Ctrl Pts',(-158.639859435957,-4.91824933787898,
130.806912666354));
#114315=CARTESIAN_POINT('Ctrl Pts',(-158.639859435994,-4.91824933787863,
130.806912667012));
#114316=CARTESIAN_POINT('Ctrl Pts',(-158.648124266752,-4.91817399056016,
130.952120237231));
#114317=CARTESIAN_POINT('Ctrl Pts',(-158.65638909751,-4.91166853530904,
131.09715679426));
#114318=CARTESIAN_POINT('Ctrl Pts',(-158.664653928268,-4.89877453424325,
131.241614691475));
#114319=CARTESIAN_POINT('Ctrl Pts',(-158.672428262387,-4.88664575927484,
131.377499380703));
#114320=CARTESIAN_POINT('Ctrl Pts',(-158.680202596506,-4.86883963092858,
131.513094267943));
#114321=CARTESIAN_POINT('Ctrl Pts',(-158.687976930625,-4.84537373514135,
131.647886805246));
#114322=CARTESIAN_POINT('Ctrl Pts',(-158.695741683572,-4.82193675897347,
131.782513222794));
#114323=CARTESIAN_POINT('Ctrl Pts',(-158.70350643652,-4.79285396025964,
131.916338876396));
#114324=CARTESIAN_POINT('Ctrl Pts',(-158.711271189467,-4.75819480755438,
132.048854585355));
#114325=CARTESIAN_POINT('Ctrl Pts',(-158.719028230352,-4.72357007880828,
132.181238677843));
#114326=CARTESIAN_POINT('Ctrl Pts',(-158.726785271237,-4.68338011625046,
132.312315039052));
#114327=CARTESIAN_POINT('Ctrl Pts',(-158.734542312122,-4.63774567234452,
132.44158330894));
#114328=CARTESIAN_POINT('Ctrl Pts',(-158.742293503362,-4.59214564172766,
132.57075409662));
#114329=CARTESIAN_POINT('Ctrl Pts',(-158.750044694602,-4.54110943158147,
132.698119139758));
#114330=CARTESIAN_POINT('Ctrl Pts',(-158.757795885842,-4.48480789707475,
132.823192257113));
#114331=CARTESIAN_POINT('Ctrl Pts',(-158.765543782619,-4.42853029222216,
132.948212215057));
#114332=CARTESIAN_POINT('Ctrl Pts',(-158.773291679396,-4.3669919741746,
133.070941828923));
#114333=CARTESIAN_POINT('Ctrl Pts',(-158.781039576173,-4.30041221237417,
133.190914171577));
#114334=CARTESIAN_POINT('Ctrl Pts',(-158.788785852257,-4.23384637762462,
133.310861418603));
#114335=CARTESIAN_POINT('Ctrl Pts',(-158.796532128341,-4.16224138629604,
133.428052199992));
#114336=CARTESIAN_POINT('Ctrl Pts',(-158.804278404425,-4.08586263394959,
133.542043871523));
#114337=CARTESIAN_POINT('Ctrl Pts',(-158.812024737691,-4.00948331779265,
133.656036384514));
#114338=CARTESIAN_POINT('Ctrl Pts',(-158.819771070956,-3.92833038792729,
133.766829415728));
#114339=CARTESIAN_POINT('Ctrl Pts',(-158.827517404221,-3.84271254428478,
133.874009353903));
#114340=CARTESIAN_POINT('Ctrl Pts',(-158.835265472224,-3.75707552711993,
133.981213294282));
#114341=CARTESIAN_POINT('Ctrl Pts',(-158.843013540227,-3.6669718504877,
134.084802226143));
#114342=CARTESIAN_POINT('Ctrl Pts',(-158.85076160823,-3.57275019687367,
134.184395986203));
#114343=CARTESIAN_POINT('Ctrl Pts',(-158.858517910972,-3.47842840336455,
134.284095595697));
#114344=CARTESIAN_POINT('Ctrl Pts',(-158.866274213714,-3.37998015919058,
134.379791266856));
#114345=CARTESIAN_POINT('Ctrl Pts',(-158.874030516456,-3.2777910765421,
134.471139683864));
#114346=CARTESIAN_POINT('Ctrl Pts',(-158.88179095897,-3.17554745250336,
134.562536856273));
#114347=CARTESIAN_POINT('Ctrl Pts',(-158.889551401484,-3.0695593135838,
134.649581903205));
#114348=CARTESIAN_POINT('Ctrl Pts',(-158.897311843998,-2.96024419663096,
134.731972787678));
#114349=CARTESIAN_POINT('Ctrl Pts',(-158.905084744263,-2.85075359734785,
134.814495933313));
#114350=CARTESIAN_POINT('Ctrl Pts',(-158.912857644529,-2.73792566946765,
134.892349764331));
#114351=CARTESIAN_POINT('Ctrl Pts',(-158.920630544794,-2.6222064286016,
134.965275962571));
#114352=CARTESIAN_POINT('Ctrl Pts',(-158.928120880556,-2.51069387362021,
135.035551109816));
#114353=CARTESIAN_POINT('Ctrl Pts',(-158.935611216318,-2.39649683605287,
135.101250514425));
#114354=CARTESIAN_POINT('Ctrl Pts',(-158.94310155208,-2.28003305892684,
135.162184881198));
#114355=CARTESIAN_POINT('Ctrl Pts',(-158.950875886199,-2.15915352229284,
135.225429593008));
#114356=CARTESIAN_POINT('Ctrl Pts',(-158.958650220318,-2.03544905610099,
135.283741141578));
#114357=CARTESIAN_POINT('Ctrl Pts',(-158.966424554437,-1.90936038708572,
135.336857277766));
#114358=CARTESIAN_POINT('Ctrl Pts',(-158.974189307384,-1.78342711108648,
135.389907953064));
#114359=CARTESIAN_POINT('Ctrl Pts',(-158.981954060332,-1.65511583548042,
135.437775805484));
#114360=CARTESIAN_POINT('Ctrl Pts',(-158.989718813279,-1.52489249786003,
135.480244056283));
#114361=CARTESIAN_POINT('Ctrl Pts',(-158.997475854164,-1.39479849989403,
135.522670127017));
#114362=CARTESIAN_POINT('Ctrl Pts',(-159.005232895049,-1.26279658847597,
135.559707148231));
#114363=CARTESIAN_POINT('Ctrl Pts',(-159.012989935934,-1.12937300033731,
135.591186255565));
#114364=CARTESIAN_POINT('Ctrl Pts',(-159.020741127174,-0.996050027964171,
135.622641624261));
#114365=CARTESIAN_POINT('Ctrl Pts',(-159.028492318414,-0.861307891793686,
135.648547332125));
#114366=CARTESIAN_POINT('Ctrl Pts',(-159.036243509654,-0.725647981265623,
135.668784331613));
#114367=CARTESIAN_POINT('Ctrl Pts',(-159.043991406431,-0.590045729818567,
135.689012729837));
#114368=CARTESIAN_POINT('Ctrl Pts',(-159.051739303208,-0.453526865727344,
135.703577154141));
#114369=CARTESIAN_POINT('Ctrl Pts',(-159.059487199985,-0.316602748504965,
135.712409696593));
#114370=CARTESIAN_POINT('Ctrl Pts',(-159.067233476069,-0.179707272856166,
135.721240391468));
#114371=CARTESIAN_POINT('Ctrl Pts',(-159.074979752153,-0.0424071025959459,
135.724341564189));
#114372=CARTESIAN_POINT('Ctrl Pts',(-159.082726028237,0.0947819003729015,
135.721697239546));
#114373=CARTESIAN_POINT('Ctrl Pts',(-159.090472361503,0.231971916039617,
135.719052895382));
#114374=CARTESIAN_POINT('Ctrl Pts',(-159.098218694768,0.369050371884892,
135.710662976758));
#114375=CARTESIAN_POINT('Ctrl Pts',(-159.105965028033,0.505502425186202,
135.696563634677));
#114376=CARTESIAN_POINT('Ctrl Pts',(-159.113713096036,0.641985035978571,
135.682461135147));
#114377=CARTESIAN_POINT('Ctrl Pts',(-159.121461164039,0.777840576268759,
135.662646708099));
#114378=CARTESIAN_POINT('Ctrl Pts',(-159.129209232042,0.912560732519729,
135.637208222443));
#114379=CARTESIAN_POINT('Ctrl Pts',(-159.136965534784,1.04742407095614,
135.611742700462));
#114380=CARTESIAN_POINT('Ctrl Pts',(-159.144721837526,1.18114923005184,
135.580641252197));
#114381=CARTESIAN_POINT('Ctrl Pts',(-159.152478140268,1.31323893568091,
135.544042733522));
#114382=CARTESIAN_POINT('Ctrl Pts',(-159.160238582782,1.44539914156338,
135.507424681115));
#114383=CARTESIAN_POINT('Ctrl Pts',(-159.167999025296,1.57592178278154,
135.465303832163));
#114384=CARTESIAN_POINT('Ctrl Pts',(-159.17575946781,1.70432705820341,135.417868213872));
#114385=CARTESIAN_POINT('Ctrl Pts',(-159.183532368076,1.83293846117232,
135.370356447717));
#114386=CARTESIAN_POINT('Ctrl Pts',(-159.191305268341,1.95942534513667,
135.317513013889));
#114387=CARTESIAN_POINT('Ctrl Pts',(-159.199078168607,2.08332929738123,
135.259573530679));
#114388=CARTESIAN_POINT('Ctrl Pts',(-159.206568504369,2.20272902886848,
135.203740293625));
#114389=CARTESIAN_POINT('Ctrl Pts',(-159.214058840131,2.31973008689436,
135.143175224679));
#114390=CARTESIAN_POINT('Ctrl Pts',(-159.221549175893,2.43394741173613,
135.078127464202));
#114391=CARTESIAN_POINT('Ctrl Pts',(-159.229323510012,2.55249532116304,
135.010613398117));
#114392=CARTESIAN_POINT('Ctrl Pts',(-159.237097844131,2.66841976406962,
134.938056143557));
#114393=CARTESIAN_POINT('Ctrl Pts',(-159.24487217825,2.78126187926213,134.860684744342));
#114394=CARTESIAN_POINT('Ctrl Pts',(-159.252636931197,2.89396492663266,
134.783408698461));
#114395=CARTESIAN_POINT('Ctrl Pts',(-159.260401684144,3.00359288520396,
134.701330531799));
#114396=CARTESIAN_POINT('Ctrl Pts',(-159.268166437092,3.10971152223076,
134.614725076644));
#114397=CARTESIAN_POINT('Ctrl Pts',(-159.275923477977,3.21572476073126,
134.528205639248));
#114398=CARTESIAN_POINT('Ctrl Pts',(-159.283680518862,3.31823531306843,
134.437168107329));
#114399=CARTESIAN_POINT('Ctrl Pts',(-159.291437559747,3.41683828604519,
134.34193029031));
#114400=CARTESIAN_POINT('Ctrl Pts',(-159.299188750987,3.51536690175314,
134.246764292869));
#114401=CARTESIAN_POINT('Ctrl Pts',(-159.306939942227,3.60999352332669,
134.147404585496));
#114402=CARTESIAN_POINT('Ctrl Pts',(-159.314691133467,3.70034697945598,
134.04420865322));
#114403=CARTESIAN_POINT('Ctrl Pts',(-159.322439030244,3.79066203295604,
133.941056581968));
#114404=CARTESIAN_POINT('Ctrl Pts',(-159.330186927021,3.87670727630846,
133.834071822285));
#114405=CARTESIAN_POINT('Ctrl Pts',(-159.337934823798,3.95814917434049,
133.723647889516));
#114406=CARTESIAN_POINT('Ctrl Pts',(-159.345681099882,4.03957403648313,
133.613247055053));
#114407=CARTESIAN_POINT('Ctrl Pts',(-159.353427375966,4.11639723669211,
133.499408792876));
#114408=CARTESIAN_POINT('Ctrl Pts',(-159.36117365205,4.18832649861039,133.382558477223));
#114409=CARTESIAN_POINT('Ctrl Pts',(-159.368919985316,4.26025629149425,
133.265707299007));
#114410=CARTESIAN_POINT('Ctrl Pts',(-159.376666318581,4.32729186905267,
133.145844355888));
#114411=CARTESIAN_POINT('Ctrl Pts',(-159.384412651847,4.3891853610824,133.023422340133));
#114412=CARTESIAN_POINT('Ctrl Pts',(-159.39216071985,4.45109271373045,132.900972908815));
#114413=CARTESIAN_POINT('Ctrl Pts',(-159.399908787853,4.50785551306411,
132.775963613326));
#114414=CARTESIAN_POINT('Ctrl Pts',(-159.407656855855,4.55927292980295,
132.648869607532));
#114415=CARTESIAN_POINT('Ctrl Pts',(-159.415413158597,4.61074499358424,
132.521640524716));
#114416=CARTESIAN_POINT('Ctrl Pts',(-159.423169461339,4.65686017923022,
132.392322668593));
#114417=CARTESIAN_POINT('Ctrl Pts',(-159.430925764081,4.69746652130789,
132.26140946496));
#114418=CARTESIAN_POINT('Ctrl Pts',(-159.438686206595,4.73809453621296,
132.130426389008));
#114419=CARTESIAN_POINT('Ctrl Pts',(-159.446446649109,4.77320774883561,
131.99784664664));
#114420=CARTESIAN_POINT('Ctrl Pts',(-159.454207091624,4.80270500756011,
131.864175541436));
#114421=CARTESIAN_POINT('Ctrl Pts',(-159.461979991889,4.83224961790295,
131.730289855507));
#114422=CARTESIAN_POINT('Ctrl Pts',(-159.469752892154,4.85616019081624,
131.595309690976));
#114423=CARTESIAN_POINT('Ctrl Pts',(-159.47752579242,4.87438717537133,131.459748080885));
#114424=CARTESIAN_POINT('Ctrl Pts',(-159.485016128182,4.89195156312684,
131.32911447678));
#114425=CARTESIAN_POINT('Ctrl Pts',(-159.492506463944,4.90423838510301,
131.197941273873));
#114426=CARTESIAN_POINT('Ctrl Pts',(-159.499996799706,4.91124911595562,
131.066687100265));
#114427=CARTESIAN_POINT('Ctrl Pts',(-159.507771133825,4.91852566079937,
130.930456384771));
#114428=CARTESIAN_POINT('Ctrl Pts',(-159.515545467944,4.92014118061332,
130.793706899404));
#114429=CARTESIAN_POINT('Ctrl Pts',(-159.523319802063,4.91604035076487,
130.65694850086));
#114430=CARTESIAN_POINT('Ctrl Pts',(-159.53108455501,4.9119445748227,130.52035864482));
#114431=CARTESIAN_POINT('Ctrl Pts',(-159.538849307957,4.90214647805531,
130.383760284498));
#114432=CARTESIAN_POINT('Ctrl Pts',(-159.546614060904,4.88664257124409,
130.247667305764));
#114433=CARTESIAN_POINT('Ctrl Pts',(-159.554371101789,4.87115406313168,
130.111709496495));
#114434=CARTESIAN_POINT('Ctrl Pts',(-159.562128142674,4.84997106670892,
129.976256455847));
#114435=CARTESIAN_POINT('Ctrl Pts',(-159.569885183559,4.82314210938111,
129.841820615688));
#114436=CARTESIAN_POINT('Ctrl Pts',(-159.5776363748,4.79633338397869,129.707486154643));
#114437=CARTESIAN_POINT('Ctrl Pts',(-159.58538756604,4.76388724849662,129.574167749116));
#114438=CARTESIAN_POINT('Ctrl Pts',(-159.59313875728,4.72590383805602,129.442370905436));
#114439=CARTESIAN_POINT('Ctrl Pts',(-159.600886654057,4.68793657157814,
129.31063007893));
#114440=CARTESIAN_POINT('Ctrl Pts',(-159.608634550834,4.64443681909469,
129.180409902913));
#114441=CARTESIAN_POINT('Ctrl Pts',(-159.616382447611,4.59555537230282,
129.052203694628));
#114442=CARTESIAN_POINT('Ctrl Pts',(-159.624128723695,4.54668415045573,
128.924024304318));
#114443=CARTESIAN_POINT('Ctrl Pts',(-159.631874999779,4.49243361264322,
128.797858408875));
#114444=CARTESIAN_POINT('Ctrl Pts',(-159.639621275863,4.43300365574765,
128.674181833842));
#114445=CARTESIAN_POINT('Ctrl Pts',(-159.647367609129,4.37357326015372,
128.550504345857));
#114446=CARTESIAN_POINT('Ctrl Pts',(-159.655113942394,4.30896353851874,
128.42931656734));
#114447=CARTESIAN_POINT('Ctrl Pts',(-159.66286027566,4.23942137376638,128.311071729741));
#114448=CARTESIAN_POINT('Ctrl Pts',(-159.670608343663,4.16986363552848,
128.19280041203));
#114449=CARTESIAN_POINT('Ctrl Pts',(-159.678356411666,4.09537145433454,
128.077473683611));
#114450=CARTESIAN_POINT('Ctrl Pts',(-159.686104479669,4.01623603745836,
127.965517340116));
#114451=CARTESIAN_POINT('Ctrl Pts',(-159.69386078241,3.93701651451929,127.853442008088));
#114452=CARTESIAN_POINT('Ctrl Pts',(-159.701617085152,3.85314412395863,
127.744744536355));
#114453=CARTESIAN_POINT('Ctrl Pts',(-159.709373387894,3.76495185784531,
127.639819486437));
#114454=CARTESIAN_POINT('Ctrl Pts',(-159.717133830408,3.67671252086414,
127.534838434861));
#114455=CARTESIAN_POINT('Ctrl Pts',(-159.724894272922,3.58414897786692,
127.433634105433));
#114456=CARTESIAN_POINT('Ctrl Pts',(-159.732654715437,3.48763168014751,
127.336564728802));
#114457=CARTESIAN_POINT('Ctrl Pts',(-159.740427615702,3.39095944429339,
127.239339527789));
#114458=CARTESIAN_POINT('Ctrl Pts',(-159.748200515967,3.29032105774447,
127.146262809612));
#114459=CARTESIAN_POINT('Ctrl Pts',(-159.755973416233,3.18612136624142,
127.05765356976));
#114460=CARTESIAN_POINT('Ctrl Pts',(-159.763463751995,3.08570959598768,
126.97226549897));
#114461=CARTESIAN_POINT('Ctrl Pts',(-159.770954087757,2.98199119276438,
126.891025927406));
#114462=CARTESIAN_POINT('Ctrl Pts',(-159.778444423519,2.87535281046917,
126.814181514089));
#114463=CARTESIAN_POINT('Ctrl Pts',(-159.786218757638,2.76467120149735,
126.734423521485));
#114464=CARTESIAN_POINT('Ctrl Pts',(-159.793993091757,2.65049321443222,
126.659147901778));
#114465=CARTESIAN_POINT('Ctrl Pts',(-159.801767425876,2.53321790183688,
126.588676791149));
#114466=CARTESIAN_POINT('Ctrl Pts',(-159.809532178823,2.41608712058281,
126.518292529865));
#114467=CARTESIAN_POINT('Ctrl Pts',(-159.81729693177,2.29586694074203,126.452701195817));
#114468=CARTESIAN_POINT('Ctrl Pts',(-159.825061684718,2.17298782304402,
126.392183492449));
#114469=CARTESIAN_POINT('Ctrl Pts',(-159.832818725603,2.050230750618,126.331725896118));
#114470=CARTESIAN_POINT('Ctrl Pts',(-159.840575766488,1.9248203443006,126.276332073847));
#114471=CARTESIAN_POINT('Ctrl Pts',(-159.848332807373,1.79721395778471,
126.226238180098));
#114472=CARTESIAN_POINT('Ctrl Pts',(-159.856083998613,1.6697038002377,126.176182062545));
#114473=CARTESIAN_POINT('Ctrl Pts',(-159.863835189853,1.54000132112621,
126.131418060579));
#114474=CARTESIAN_POINT('Ctrl Pts',(-159.871586381093,1.40858594271787,
126.092135166203));
#114475=CARTESIAN_POINT('Ctrl Pts',(-159.87933427787,1.27722641935079,126.052868968104));
#114476=CARTESIAN_POINT('Ctrl Pts',(-159.887082174647,1.14415581848234,
126.019079355904));
#114477=CARTESIAN_POINT('Ctrl Pts',(-159.894830071424,1.00987068847651,
125.990906114295));
#114478=CARTESIAN_POINT('Ctrl Pts',(-159.902576347508,0.875613648025022,
125.962738765922));
#114479=CARTESIAN_POINT('Ctrl Pts',(-159.910322623593,0.740142966154415,
125.940185531579));
#114480=CARTESIAN_POINT('Ctrl Pts',(-159.918068899677,0.603967017517046,
125.923335427685));
#114481=CARTESIAN_POINT('Ctrl Pts',(-159.925815232942,0.467790063659945,
125.906485199408));
#114482=CARTESIAN_POINT('Ctrl Pts',(-159.933561566207,0.330908220653752,
125.895338233598));
#114483=CARTESIAN_POINT('Ctrl Pts',(-159.941307899473,0.193836251203119,
125.889931803327));
#114484=CARTESIAN_POINT('Ctrl Pts',(-159.949055967476,0.056733585435131,
125.884524162324));
#114485=CARTESIAN_POINT('Ctrl Pts',(-159.956804035479,-0.0805589009149116,
125.884859630369));
#114486=CARTESIAN_POINT('Ctrl Pts',(-159.964552103482,-0.217525569277293,
125.890923359474));
#114487=CARTESIAN_POINT('Ctrl Pts',(-159.972308406224,-0.354637807444547,
125.896993533182));
#114488=CARTESIAN_POINT('Ctrl Pts',(-159.980064708966,-0.49142314468065,
125.908804112196));
#114489=CARTESIAN_POINT('Ctrl Pts',(-159.987821011707,-0.627369634858531,
125.926288210994));
#114490=CARTESIAN_POINT('Ctrl Pts',(-159.995581454222,-0.763388683771491,
125.943781641583));
#114491=CARTESIAN_POINT('Ctrl Pts',(-160.003341896736,-0.89856760835459,
125.966954559733));
#114492=CARTESIAN_POINT('Ctrl Pts',(-160.01110233925,-1.0324047810459,125.995688926696));
#114493=CARTESIAN_POINT('Ctrl Pts',(-160.018875239515,-1.16645680104831,
126.024469420615));
#114494=CARTESIAN_POINT('Ctrl Pts',(-160.026648139781,-1.29916238627948,
126.058829105746));
#114495=CARTESIAN_POINT('Ctrl Pts',(-160.034421040046,-1.43003432778728,
126.098599798756));
#114496=CARTESIAN_POINT('Ctrl Pts',(-160.041911375808,-1.55614874457298,
126.136924726897));
#114497=CARTESIAN_POINT('Ctrl Pts',(-160.04940171157,-1.68056022735749,
126.180273984169));
#114498=CARTESIAN_POINT('Ctrl Pts',(-160.056892047332,-1.80285225904415,
126.228455592922));
#114499=CARTESIAN_POINT('Ctrl Pts',(-160.06466667697,-1.92978585512154,
126.278465922945));
#114500=CARTESIAN_POINT('Ctrl Pts',(-160.072441306609,-2.05483803858265,
126.333841095074));
#114501=CARTESIAN_POINT('Ctrl Pts',(-160.080215936247,-2.17752203423722,
126.394419478173));
#114502=CARTESIAN_POINT('Ctrl Pts',(-160.087980916616,-2.3000537640038,
126.454922676067));
#114503=CARTESIAN_POINT('Ctrl Pts',(-160.095745896986,-2.42022280705301,
126.520616063905));
#114504=CARTESIAN_POINT('Ctrl Pts',(-160.103510877355,-2.53756028489532,
126.591289188902));
#114505=CARTESIAN_POINT('Ctrl Pts',(-160.111268077854,-2.65478020025133,
126.661891505251));
#114506=CARTESIAN_POINT('Ctrl Pts',(-160.119025278352,-2.76917386359483,
126.737463429008));
#114507=CARTESIAN_POINT('Ctrl Pts',(-160.126782478851,-2.88029535500852,
126.817747803357));
#114508=CARTESIAN_POINT('Ctrl Pts',(-160.13482700935,-2.99553283365445,
126.901005945026));
#114509=CARTESIAN_POINT('Ctrl Pts',(-160.14287153985,-3.10725067608075,
126.989332189158));
#114510=CARTESIAN_POINT('Ctrl Pts',(-160.150916070349,-3.21498207941223,
127.082388923483));
#114511=CARTESIAN_POINT('Ctrl Pts',(-160.158663626693,-3.31873643988849,
127.17201034917));
#114512=CARTESIAN_POINT('Ctrl Pts',(-160.166411183037,-3.4187931316515,
127.266018933222));
#114513=CARTESIAN_POINT('Ctrl Pts',(-160.17415873938,-3.51476749411372,
127.36407101859));
#114514=CARTESIAN_POINT('Ctrl Pts',(-160.181904642276,-3.61072137416904,
127.462102178133));
#114515=CARTESIAN_POINT('Ctrl Pts',(-160.189650545172,-3.70259438520297,
127.564174842764));
#114516=CARTESIAN_POINT('Ctrl Pts',(-160.197396448068,-3.79003834556156,
127.669908129224));
#114517=CARTESIAN_POINT('Ctrl Pts',(-160.205142375296,-3.87748258060947,
127.775641747827));
#114518=CARTESIAN_POINT('Ctrl Pts',(-160.212888302524,-3.96049748866926,
127.885035709547));
#114519=CARTESIAN_POINT('Ctrl Pts',(-160.220634229753,-4.03877510595296,
127.997675970864));
#114520=CARTESIAN_POINT('Ctrl Pts',(-160.228381858733,-4.11706992054616,
128.110340978839));
#114521=CARTESIAN_POINT('Ctrl Pts',(-160.236129487714,-4.19062515107944,
128.226253384234));
#114522=CARTESIAN_POINT('Ctrl Pts',(-160.243877116694,-4.259176325971,128.344970431608));
#114523=CARTESIAN_POINT('Ctrl Pts',(-160.251631726085,-4.32778926367754,
128.463794439934));
#114524=CARTESIAN_POINT('Ctrl Pts',(-160.259386335477,-4.39138894912225,
128.58542779636));
#114525=CARTESIAN_POINT('Ctrl Pts',(-160.267140944868,-4.44975688027795,
128.709403155249));
#114526=CARTESIAN_POINT('Ctrl Pts',(-160.274899711305,-4.50815610097031,
128.833444974118));
#114527=CARTESIAN_POINT('Ctrl Pts',(-160.282658477742,-4.56131782802171,
128.959830937214));
#114528=CARTESIAN_POINT('Ctrl Pts',(-160.290417244178,-4.60907220310745,
129.088074951063));
#114529=CARTESIAN_POINT('Ctrl Pts',(-160.298185461519,-4.65688474748967,
129.216475178119));
#114530=CARTESIAN_POINT('Ctrl Pts',(-160.305953678859,-4.69927667010316,
129.346737603508));
#114531=CARTESIAN_POINT('Ctrl Pts',(-160.313721896199,-4.7361282332075,
129.478361967071));
#114532=CARTESIAN_POINT('Ctrl Pts',(-160.315765001078,-4.74582049657902,
129.512980254337));
#114533=CARTESIAN_POINT('Ctrl Pts',(-160.317808105958,-4.75512979050262,
129.547692702345));
#114534=CARTESIAN_POINT('Ctrl Pts',(-160.319851210837,-4.76405452823417,
129.582490119309));
#114535=CARTESIAN_POINT('Origin',(213.235140564004,0.,130.804360617566));
#114536=CARTESIAN_POINT('',(-162.415078182266,-4.764054528234,129.582490119308));
#114537=CARTESIAN_POINT('',(-162.070143404005,-4.764054528234,129.582490119308));
#114538=CARTESIAN_POINT('',(213.235140564004,-4.76405452823405,129.582490119308));
#114539=CARTESIAN_POINT('',(-160.735140564062,-4.91824999711478,130.80452908244));
#114540=CARTESIAN_POINT('Ctrl Pts',(-160.735140564062,-4.91824999711478,
130.804529082441));
#114541=CARTESIAN_POINT('Ctrl Pts',(-160.743276258315,-4.91824504889373,
130.948989986876));
#114542=CARTESIAN_POINT('Ctrl Pts',(-160.751411952569,-4.91187105275536,
131.093321017711));
#114543=CARTESIAN_POINT('Ctrl Pts',(-160.759547646822,-4.89918799690607,
131.236957466227));
#114544=CARTESIAN_POINT('Ctrl Pts',(-160.767694811219,-4.88648705979481,
131.380796421221));
#114545=CARTESIAN_POINT('Ctrl Pts',(-160.775841975617,-4.86745934026142,
131.523938511925));
#114546=CARTESIAN_POINT('Ctrl Pts',(-160.783989140014,-4.84221620751817,
131.665827542148));
#114547=CARTESIAN_POINT('Ctrl Pts',(-160.792156277582,-4.81691119000347,
131.80806442025));
#114548=CARTESIAN_POINT('Ctrl Pts',(-160.800323415151,-4.78536034987918,
131.949041770207));
#114549=CARTESIAN_POINT('Ctrl Pts',(-160.808490552719,-4.74772586143461,
132.088215051357));
#114550=CARTESIAN_POINT('Ctrl Pts',(-160.816668331239,-4.71004233906773,
132.227569661181));
#114551=CARTESIAN_POINT('Ctrl Pts',(-160.82484610976,-4.66625944808496,
132.3651151975));
#114552=CARTESIAN_POINT('Ctrl Pts',(-160.83302388828,-4.6165881898404,132.500325401377));
#114553=CARTESIAN_POINT('Ctrl Pts',(-160.841220513682,-4.56680245694882,
132.635847216855));
#114554=CARTESIAN_POINT('Ctrl Pts',(-160.849417139084,-4.51110134880628,
132.769022633757));
#114555=CARTESIAN_POINT('Ctrl Pts',(-160.857613764485,-4.44974341291696,
132.899346684752));
#114556=CARTESIAN_POINT('Ctrl Pts',(-160.86262448386,-4.41223439144694,
132.979015721136));
#114557=CARTESIAN_POINT('Ctrl Pts',(-160.867635203235,-4.37261226985345,
133.057619691176));
#114558=CARTESIAN_POINT('Ctrl Pts',(-160.87264592261,-4.33094413413395,
133.135048492317));
#114559=CARTESIAN_POINT('Ctrl Pts',(-160.88042025673,-4.2662943333858,133.255182414305));
#114560=CARTESIAN_POINT('Ctrl Pts',(-160.888194590849,-4.19653984051435,
133.372814647883));
#114561=CARTESIAN_POINT('Ctrl Pts',(-160.895968924968,-4.12189862197519,
133.48748096758));
#114562=CARTESIAN_POINT('Ctrl Pts',(-160.903733677915,-4.047349392067,133.602005971286));
#114563=CARTESIAN_POINT('Ctrl Pts',(-160.911498430862,-3.96792563061788,
133.713572009399));
#114564=CARTESIAN_POINT('Ctrl Pts',(-160.919263183809,-3.88389167038163,
133.821738379007));
#114565=CARTESIAN_POINT('Ctrl Pts',(-160.927020224694,-3.79994117385935,
133.929797316252));
#114566=CARTESIAN_POINT('Ctrl Pts',(-160.934777265579,-3.71138982910379,
134.034462997831));
#114567=CARTESIAN_POINT('Ctrl Pts',(-160.942534306464,-3.61854563769635,
134.135323020597));
#114568=CARTESIAN_POINT('Ctrl Pts',(-160.950285497704,-3.525771460816,134.236106984036));
#114569=CARTESIAN_POINT('Ctrl Pts',(-160.958036688944,-3.42871114458747,
134.333090714492));
#114570=CARTESIAN_POINT('Ctrl Pts',(-160.965787880184,-3.32771316400612,
134.425894568891));
#114571=CARTESIAN_POINT('Ctrl Pts',(-160.973535776962,-3.22675811026059,
134.518658979176));
#114572=CARTESIAN_POINT('Ctrl Pts',(-160.981283673739,-3.12186900813265,
134.607246782868));
#114573=CARTESIAN_POINT('Ctrl Pts',(-160.989031570516,-3.01343125572059,
134.69131509756));
#114574=CARTESIAN_POINT('Ctrl Pts',(-160.9967778466,-2.90501618614869,134.775365826973));
#114575=CARTESIAN_POINT('Ctrl Pts',(-161.004524122684,-2.79305425155926,
134.854898708405));
#114576=CARTESIAN_POINT('Ctrl Pts',(-161.012270398768,-2.67796368986509,
134.929611341857));
#114577=CARTESIAN_POINT('Ctrl Pts',(-161.020016732033,-2.56287227859838,
135.004324526821));
#114578=CARTESIAN_POINT('Ctrl Pts',(-161.027763065299,-2.44465252207039,
135.074217179926));
#114579=CARTESIAN_POINT('Ctrl Pts',(-161.035509398564,-2.32375103398009,
135.139030638984));
#114580=CARTESIAN_POINT('Ctrl Pts',(-161.043257466567,-2.20282247083997,
135.203858612565));
#114581=CARTESIAN_POINT('Ctrl Pts',(-161.05100553457,-2.07921132561113,
135.263604944019));
#114582=CARTESIAN_POINT('Ctrl Pts',(-161.058753602573,-1.95338779597909,
135.318057459515));
#114583=CARTESIAN_POINT('Ctrl Pts',(-161.066509905315,-1.82743053960226,
135.372567847792));
#114584=CARTESIAN_POINT('Ctrl Pts',(-161.074266208057,-1.69925656112866,
135.421773025383));
#114585=CARTESIAN_POINT('Ctrl Pts',(-161.082022510799,-1.56935549750932,
135.465509229758));
#114586=CARTESIAN_POINT('Ctrl Pts',(-161.089782953313,-1.43938510178109,
135.509268777462));
#114587=CARTESIAN_POINT('Ctrl Pts',(-161.097543395827,-1.30768615938835,
135.547553426601));
#114588=CARTESIAN_POINT('Ctrl Pts',(-161.105303838341,-1.17476140103643,
135.580249928797));
#114589=CARTESIAN_POINT('Ctrl Pts',(-161.113076738607,-1.0416232600619,
135.612998918322));
#114590=CARTESIAN_POINT('Ctrl Pts',(-161.120849638872,-0.90725575430458,
135.640141757349));
#114591=CARTESIAN_POINT('Ctrl Pts',(-161.128622539138,-0.772170579979823,
135.661616597841));
#114592=CARTESIAN_POINT('Ctrl Pts',(-161.1361128749,-0.641996092000425,
135.682310773789));
#114593=CARTESIAN_POINT('Ctrl Pts',(-161.143603210662,-0.511155513583549,
135.69774185265));
#114594=CARTESIAN_POINT('Ctrl Pts',(-161.151093546424,-0.380107376144063,
135.707900302844));
#114595=CARTESIAN_POINT('Ctrl Pts',(-161.158867880543,-0.244090508743276,
135.718443913766));
#114596=CARTESIAN_POINT('Ctrl Pts',(-161.166642214662,-0.10741917187084,
135.723340578939));
#114597=CARTESIAN_POINT('Ctrl Pts',(-161.174416548781,0.0293982522418081,
135.72252275451));
#114598=CARTESIAN_POINT('Ctrl Pts',(-161.182181301728,0.166047061106961,
135.721705937975));
#114599=CARTESIAN_POINT('Ctrl Pts',(-161.189946054675,0.302841211782387,
135.715188646823));
#114600=CARTESIAN_POINT('Ctrl Pts',(-161.197710807622,0.439267050115026,
135.702955060994));
#114601=CARTESIAN_POINT('Ctrl Pts',(-161.205467848507,0.575557388381766,
135.690733625735));
#114602=CARTESIAN_POINT('Ctrl Pts',(-161.213224889392,0.711479755407197,
135.672807228983));
#114603=CARTESIAN_POINT('Ctrl Pts',(-161.220981930277,0.84652070236521,
135.649212087216));
#114604=CARTESIAN_POINT('Ctrl Pts',(-161.228733121517,0.98145981389484,
135.625634738729));
#114605=CARTESIAN_POINT('Ctrl Pts',(-161.236484312758,1.11551844480146,
135.596397221066));
#114606=CARTESIAN_POINT('Ctrl Pts',(-161.244235503998,1.24818883136562,
135.561587509754));
#114607=CARTESIAN_POINT('Ctrl Pts',(-161.251983400775,1.3808028294762,135.526792593498));
#114608=CARTESIAN_POINT('Ctrl Pts',(-161.259731297552,1.51202937941735,
135.486430293037));
#114609=CARTESIAN_POINT('Ctrl Pts',(-161.267479194329,1.64137168742383,
135.44063951839));
#114610=CARTESIAN_POINT('Ctrl Pts',(-161.275225470413,1.77068693980813,
135.394858322186));
#114611=CARTESIAN_POINT('Ctrl Pts',(-161.282971746497,1.89811836591234,
135.343651040801));
#114612=CARTESIAN_POINT('Ctrl Pts',(-161.290718022581,2.02318548024631,
135.287206095052));
#114613=CARTESIAN_POINT('Ctrl Pts',(-161.298464355846,2.14825351779714,
135.23076073264));
#114614=CARTESIAN_POINT('Ctrl Pts',(-161.306210689112,2.27095685239821,
135.169077789542));
#114615=CARTESIAN_POINT('Ctrl Pts',(-161.313957022377,2.39083645861087,
135.102393201281));
#114616=CARTESIAN_POINT('Ctrl Pts',(-161.32170509038,2.51074291102999,135.035693679469));
#114617=CARTESIAN_POINT('Ctrl Pts',(-161.329453158383,2.62782403515164,
134.963990473675));
#114618=CARTESIAN_POINT('Ctrl Pts',(-161.337201226386,2.74164716978996,
134.887564489391));
#114619=CARTESIAN_POINT('Ctrl Pts',(-161.344957529128,2.85559127701044,
134.811057278661));
#114620=CARTESIAN_POINT('Ctrl Pts',(-161.35271383187,2.96627015266854,134.729817480887));
#114621=CARTESIAN_POINT('Ctrl Pts',(-161.360470134612,3.07328135797828,
134.644168523855));
#114622=CARTESIAN_POINT('Ctrl Pts',(-161.368230577126,3.18034967839033,
134.558473853397));
#114623=CARTESIAN_POINT('Ctrl Pts',(-161.37599101964,3.28374613327749,134.468365591269));
#114624=CARTESIAN_POINT('Ctrl Pts',(-161.383751462154,3.38310370534486,
134.374205485537));
#114625=CARTESIAN_POINT('Ctrl Pts',(-161.391524362419,3.48262077500746,
134.279894225645));
#114626=CARTESIAN_POINT('Ctrl Pts',(-161.399297262685,3.57808573317624,
134.181518405061));
#114627=CARTESIAN_POINT('Ctrl Pts',(-161.40707016295,3.66916996104227,134.079475097929));
#114628=CARTESIAN_POINT('Ctrl Pts',(-161.414560498712,3.75694304780076,
133.98114132204));
#114629=CARTESIAN_POINT('Ctrl Pts',(-161.422050834474,3.84064818007237,
133.879402312868));
#114630=CARTESIAN_POINT('Ctrl Pts',(-161.429541170237,3.92002949123998,
133.774638693826));
#114631=CARTESIAN_POINT('Ctrl Pts',(-161.437315504356,4.00242056894595,
133.665902930328));
#114632=CARTESIAN_POINT('Ctrl Pts',(-161.445089838475,4.0804144680001,133.553564231017));
#114633=CARTESIAN_POINT('Ctrl Pts',(-161.452864172594,4.15367956882995,
133.438013803159));
#114634=CARTESIAN_POINT('Ctrl Pts',(-161.460628925541,4.22685437697091,
133.322605780876));
#114635=CARTESIAN_POINT('Ctrl Pts',(-161.468393678488,4.29531177516819,
133.203994232639));
#114636=CARTESIAN_POINT('Ctrl Pts',(-161.476158431435,4.3587608109427,133.082602759106));
#114637=CARTESIAN_POINT('Ctrl Pts',(-161.48391547232,4.42214682824041,132.961331853296));
#114638=CARTESIAN_POINT('Ctrl Pts',(-161.491672513205,4.48053420241659,
132.837286861075));
#114639=CARTESIAN_POINT('Ctrl Pts',(-161.49942955409,4.53367587178823,132.710919337371));
#114640=CARTESIAN_POINT('Ctrl Pts',(-161.50718074533,4.58677746661368,132.5846471084));
#114641=CARTESIAN_POINT('Ctrl Pts',(-161.51493193657,4.63464107952358,132.456056193017));
#114642=CARTESIAN_POINT('Ctrl Pts',(-161.522683127811,4.67706626812691,
132.325621340141));
#114643=CARTESIAN_POINT('Ctrl Pts',(-161.530431024588,4.7194734248933,132.195241925557));
#114644=CARTESIAN_POINT('Ctrl Pts',(-161.538178921365,4.75644663402547,
132.063020503258));
#114645=CARTESIAN_POINT('Ctrl Pts',(-161.545926818142,4.78783423529182,
131.929450124169));
#114646=CARTESIAN_POINT('Ctrl Pts',(-161.553673094226,4.81921527094861,
131.795907685123));
#114647=CARTESIAN_POINT('Ctrl Pts',(-161.56141937031,4.84501293334906,131.6610172309));
#114648=CARTESIAN_POINT('Ctrl Pts',(-161.569165646394,4.86512603211808,
131.525284853604));
#114649=CARTESIAN_POINT('Ctrl Pts',(-161.57691197966,4.88523927935745,131.389551474362));
#114650=CARTESIAN_POINT('Ctrl Pts',(-161.584658312925,4.89966782192467,
131.252976546389));
#114651=CARTESIAN_POINT('Ctrl Pts',(-161.59240464619,4.90836204459488,131.116073789698));
#114652=CARTESIAN_POINT('Ctrl Pts',(-161.600152714193,4.91705821427597,
130.979140374584));
#114653=CARTESIAN_POINT('Ctrl Pts',(-161.607900782196,4.92001748395377,
130.84187937477));
#114654=CARTESIAN_POINT('Ctrl Pts',(-161.615648850199,4.91724232343523,
130.704806636645));
#114655=CARTESIAN_POINT('Ctrl Pts',(-161.623405152941,4.91446421344307,
130.567588215983));
#114656=CARTESIAN_POINT('Ctrl Pts',(-161.631161455683,4.90593950651972,
130.430558848213));
#114657=CARTESIAN_POINT('Ctrl Pts',(-161.638917758425,4.89172278362837,
130.294231937103));
#114658=CARTESIAN_POINT('Ctrl Pts',(-161.646678200939,4.87749847284395,
130.157832264216));
#114659=CARTESIAN_POINT('Ctrl Pts',(-161.654438643453,4.85757614938197,
130.022136181682));
#114660=CARTESIAN_POINT('Ctrl Pts',(-161.662199085967,4.83206178032218,
129.887648005212));
#114661=CARTESIAN_POINT('Ctrl Pts',(-161.669971986233,4.80650645333211,
129.752943936381));
#114662=CARTESIAN_POINT('Ctrl Pts',(-161.677744886498,4.77534123107775,
129.619452029376));
#114663=CARTESIAN_POINT('Ctrl Pts',(-161.685517786764,4.73872255678805,
129.487663388782));
#114664=CARTESIAN_POINT('Ctrl Pts',(-161.693008122525,4.70343506354793,
129.360665597236));
#114665=CARTESIAN_POINT('Ctrl Pts',(-161.700498458287,4.66308382234028,
129.235249679244));
#114666=CARTESIAN_POINT('Ctrl Pts',(-161.707988794048,4.61785076026705,
129.111836638888));
#114667=CARTESIAN_POINT('Ctrl Pts',(-161.715763128167,4.5709026728938,128.983744355587));
#114668=CARTESIAN_POINT('Ctrl Pts',(-161.723537462287,4.5185465511121,128.857404068408));
#114669=CARTESIAN_POINT('Ctrl Pts',(-161.731311796406,4.46093228019504,
128.73330623537));
#114670=CARTESIAN_POINT('Ctrl Pts',(-161.739076549353,4.4033890137179,128.609361341821));
#114671=CARTESIAN_POINT('Ctrl Pts',(-161.7468413023,4.34060065482306,128.487653754832));
#114672=CARTESIAN_POINT('Ctrl Pts',(-161.754606055247,4.27276632381988,
128.368657227469));
#114673=CARTESIAN_POINT('Ctrl Pts',(-161.762363096132,4.20499936683054,
128.249778889134));
#114674=CARTESIAN_POINT('Ctrl Pts',(-161.770120137017,4.13219660367083,
128.133606589359));
#114675=CARTESIAN_POINT('Ctrl Pts',(-161.777877177902,4.05460439741788,
128.020592264606));
#114676=CARTESIAN_POINT('Ctrl Pts',(-161.785628369142,3.97707070405115,
127.907663164835));
#114677=CARTESIAN_POINT('Ctrl Pts',(-161.793379560382,3.89475497696704,
127.797887620953));
#114678=CARTESIAN_POINT('Ctrl Pts',(-161.801130751623,3.80794829186819,
127.691690884209));
#114679=CARTESIAN_POINT('Ctrl Pts',(-161.8088786484,3.72117850192603,127.58553928391));
#114680=CARTESIAN_POINT('Ctrl Pts',(-161.816626545177,3.62992179729761,
127.482963767491));
#114681=CARTESIAN_POINT('Ctrl Pts',(-161.824374441954,3.53451101962872,
127.384358437066));
#114682=CARTESIAN_POINT('Ctrl Pts',(-161.832120718038,3.43912019983797,
127.285773732751));
#114683=CARTESIAN_POINT('Ctrl Pts',(-161.839866994122,3.33957730707423,
127.191157843355));
#114684=CARTESIAN_POINT('Ctrl Pts',(-161.847613270206,3.23625343508876,
127.100869458352));
#114685=CARTESIAN_POINT('Ctrl Pts',(-161.855359603472,3.13292880038979,
127.01058040686));
#114686=CARTESIAN_POINT('Ctrl Pts',(-161.863105936737,3.02582342517673,
126.924619180763));
#114687=CARTESIAN_POINT('Ctrl Pts',(-161.870852270003,2.9153426984063,126.843305200969));
#114688=CARTESIAN_POINT('Ctrl Pts',(-161.878600338006,2.80483723024298,
126.761973011474));
#114689=CARTESIAN_POINT('Ctrl Pts',(-161.886348406009,2.69095522121042,
126.685290370897));
#114690=CARTESIAN_POINT('Ctrl Pts',(-161.894096474012,2.57413200247644,
126.613534028893));
#114691=CARTESIAN_POINT('Ctrl Pts',(-161.901852776754,2.45718462263553,
126.541701423395));
#114692=CARTESIAN_POINT('Ctrl Pts',(-161.909609079496,2.33729012233755,
126.474805780354));
#114693=CARTESIAN_POINT('Ctrl Pts',(-161.917365382237,2.21490994505608,
126.413078686536));
#114694=CARTESIAN_POINT('Ctrl Pts',(-161.925125824752,2.09246444978919,
126.351318647109));
#114695=CARTESIAN_POINT('Ctrl Pts',(-161.932886267266,1.96753098997938,
126.294732814897));
#114696=CARTESIAN_POINT('Ctrl Pts',(-161.94064670978,1.84059113851152,126.243504631752));
#114697=CARTESIAN_POINT('Ctrl Pts',(-161.948419610046,1.7134475119249,126.192194212581));
#114698=CARTESIAN_POINT('Ctrl Pts',(-161.956192510311,1.58429142599279,
126.146258760251));
#114699=CARTESIAN_POINT('Ctrl Pts',(-161.963965410577,1.45362062229731,
126.105832108667));
#114700=CARTESIAN_POINT('Ctrl Pts',(-161.971455746339,1.32770003145424,
126.066875067697));
#114701=CARTESIAN_POINT('Ctrl Pts',(-161.978946082101,1.20037323616632,
126.0330333426));
#114702=CARTESIAN_POINT('Ctrl Pts',(-161.986436417863,1.07209277513557,
126.004381435944));
#114703=CARTESIAN_POINT('Ctrl Pts',(-161.994210751982,0.938948521436942,
125.974643183539));
#114704=CARTESIAN_POINT('Ctrl Pts',(-162.001985086101,0.80435509699749,
125.950401860344));
#114705=CARTESIAN_POINT('Ctrl Pts',(-162.00975942022,0.668806154692202,
125.931796468173));
#114706=CARTESIAN_POINT('Ctrl Pts',(-162.017524173168,0.533424264343947,
125.913214005486));
#114707=CARTESIAN_POINT('Ctrl Pts',(-162.025288926115,0.397089582798854,
125.900253706443));
#114708=CARTESIAN_POINT('Ctrl Pts',(-162.033053679062,0.260308321317996,
125.893004120594));
#114709=CARTESIAN_POINT('Ctrl Pts',(-162.040810719947,0.123662912914318,
125.885761735135));
#114710=CARTESIAN_POINT('Ctrl Pts',(-162.048567760832,-0.0134278048507813,
125.884218795969));
#114711=CARTESIAN_POINT('Ctrl Pts',(-162.056324801717,-0.150450439772387,
125.888412313559));
#114712=CARTESIAN_POINT('Ctrl Pts',(-162.064075992957,-0.287369744858932,
125.892602668784));
#114713=CARTESIAN_POINT('Ctrl Pts',(-162.071827184198,-0.424220680093688,
125.902520858399));
#114714=CARTESIAN_POINT('Ctrl Pts',(-162.079578375438,-0.560488136031272,
125.918151850857));
#114715=CARTESIAN_POINT('Ctrl Pts',(-162.087326272215,-0.696697674664843,
125.933776199726));
#114716=CARTESIAN_POINT('Ctrl Pts',(-162.095074168992,-0.83232383963796,
125.955108477684));
#114717=CARTESIAN_POINT('Ctrl Pts',(-162.102822065769,-0.96685515263966,
125.982081677447));
#114718=CARTESIAN_POINT('Ctrl Pts',(-162.110568341853,-1.10135832459084,
126.009049234999));
#114719=CARTESIAN_POINT('Ctrl Pts',(-162.118314617937,-1.23476671700946,
126.041655290543));
#114720=CARTESIAN_POINT('Ctrl Pts',(-162.126060894021,-1.3665779690464,
126.079781512818));
#114721=CARTESIAN_POINT('Ctrl Pts',(-162.133807227287,-1.49839019408388,
126.117908016533));
#114722=CARTESIAN_POINT('Ctrl Pts',(-162.141553560552,-1.62860487964437,
126.161554659657));
#114723=CARTESIAN_POINT('Ctrl Pts',(-162.149299893818,-1.75673416523639,
126.210553031784));
#114724=CARTESIAN_POINT('Ctrl Pts',(-162.157047961821,-1.88489214449372,
126.259562376756));
#114725=CARTESIAN_POINT('Ctrl Pts',(-162.164796029824,-2.01096342938053,
126.313925695952));
#114726=CARTESIAN_POINT('Ctrl Pts',(-162.172544097827,-2.13447987544425,
126.37342632288));
#114727=CARTESIAN_POINT('Ctrl Pts',(-162.180300400569,-2.25812759625655,
126.432990187782));
#114728=CARTESIAN_POINT('Ctrl Pts',(-162.18805670331,-2.37921470132656,
126.497702097391));
#114729=CARTESIAN_POINT('Ctrl Pts',(-162.195813006052,-2.49729692867975,
126.567299004548));
#114730=CARTESIAN_POINT('Ctrl Pts',(-162.203573448567,-2.61544218007338,
126.636933057671));
#114731=CARTESIAN_POINT('Ctrl Pts',(-162.211333891081,-2.73057903000413,
126.711457091212));
#114732=CARTESIAN_POINT('Ctrl Pts',(-162.219094333595,-2.84229284173704,
126.790565099069));
#114733=CARTESIAN_POINT('Ctrl Pts',(-162.22686723386,-2.95418598639803,
126.869800098122));
#114734=CARTESIAN_POINT('Ctrl Pts',(-162.234640134126,-3.06264480266123,
126.953633537088));
#114735=CARTESIAN_POINT('Ctrl Pts',(-162.242413034391,-3.16728765078931,
127.04171899237));
#114736=CARTESIAN_POINT('Ctrl Pts',(-162.249903370153,-3.26812646780143,
127.126602319473));
#114737=CARTESIAN_POINT('Ctrl Pts',(-162.257393705915,-3.36542171254754,
127.215433679379));
#114738=CARTESIAN_POINT('Ctrl Pts',(-162.264884041676,-3.45886609568509,
127.307872608918));
#114739=CARTESIAN_POINT('Ctrl Pts',(-162.272547458222,-3.55446971809865,
127.402447544503));
#114740=CARTESIAN_POINT('Ctrl Pts',(-162.280210874769,-3.64636366415717,
127.501117029956));
#114741=CARTESIAN_POINT('Ctrl Pts',(-162.287874291315,-3.7341691449257,
127.603553866201));
#114742=CARTESIAN_POINT('Ctrl Pts',(-162.29552875626,-3.82187206051309,
127.705871046445));
#114743=CARTESIAN_POINT('Ctrl Pts',(-162.303183221204,-3.90549574552366,
127.811946526502));
#114744=CARTESIAN_POINT('Ctrl Pts',(-162.310837686149,-3.98469649210809,
127.921414740814));
#114745=CARTESIAN_POINT('Ctrl Pts',(-162.318484980424,-4.06382304378054,
128.030780405783));
#114746=CARTESIAN_POINT('Ctrl Pts',(-162.326132274699,-4.13853466162266,
128.143532160693));
#114747=CARTESIAN_POINT('Ctrl Pts',(-162.333779568974,-4.20852673648843,
128.259270094468));
#114748=CARTESIAN_POINT('Ctrl Pts',(-162.341421196602,-4.278466947207,128.374922266402));
#114749=CARTESIAN_POINT('Ctrl Pts',(-162.34906282423,-4.34369436568951,
128.493555870933));
#114750=CARTESIAN_POINT('Ctrl Pts',(-162.356704451859,-4.40394705155555,
128.614741146152));
#114751=CARTESIAN_POINT('Ctrl Pts',(-162.364342762253,-4.46417358170449,
128.73587381479));
#114752=CARTESIAN_POINT('Ctrl Pts',(-162.371981072647,-4.51942949633178,
128.859555590372));
#114753=CARTESIAN_POINT('Ctrl Pts',(-162.379619383041,-4.5694984873254,
128.985331580736));
#114754=CARTESIAN_POINT('Ctrl Pts',(-162.387257161753,-4.61956399315277,
129.111098816175));
#114755=CARTESIAN_POINT('Ctrl Pts',(-162.394894940465,-4.66444313873443,
129.238959604522));
#114756=CARTESIAN_POINT('Ctrl Pts',(-162.402532719178,-4.70396766027824,
129.368438853139));
#114757=CARTESIAN_POINT('Ctrl Pts',(-162.406714540207,-4.72560804573572,
129.439331067373));
#114758=CARTESIAN_POINT('Ctrl Pts',(-162.410896361237,-4.74564409874225,
129.510708134137));
#114759=CARTESIAN_POINT('Ctrl Pts',(-162.415078182266,-4.764054528234,129.582490119308));
#114760=CARTESIAN_POINT('Ctrl Pts',(-160.665416397755,-4.76405452823407,
129.582490119308));
#114761=CARTESIAN_POINT('Ctrl Pts',(-160.673527702719,-4.79965082279286,
129.721279531544));
#114762=CARTESIAN_POINT('Ctrl Pts',(-160.681639007684,-4.82921423771951,
129.861766890241));
#114763=CARTESIAN_POINT('Ctrl Pts',(-160.689750312649,-4.85259362622729,
130.003412328849));
#114764=CARTESIAN_POINT('Ctrl Pts',(-160.697847565096,-4.87593251086433,
130.144812372308));
#114765=CARTESIAN_POINT('Ctrl Pts',(-160.705944817544,-4.89310867773608,
130.287366164819));
#114766=CARTESIAN_POINT('Ctrl Pts',(-160.714042069992,-4.90402160249942,
130.430522170213));
#114767=CARTESIAN_POINT('Ctrl Pts',(-160.721074901332,-4.91349997306731,
130.554859659711));
#114768=CARTESIAN_POINT('Ctrl Pts',(-160.728107732671,-4.91825427453916,
130.679651087786));
#114769=CARTESIAN_POINT('Ctrl Pts',(-160.735140564011,-4.91824999711482,
130.804529081534));
#114770=CARTESIAN_POINT('',(-160.389859436025,-4.91824806388654,130.799996608369));
#114771=CARTESIAN_POINT('Ctrl Pts',(-160.319851210837,-4.76405452823417,
129.582490119309));
#114772=CARTESIAN_POINT('Ctrl Pts',(-160.32501403094,-4.78660687776802,
129.670421387862));
#114773=CARTESIAN_POINT('Ctrl Pts',(-160.330176851042,-4.80670294628824,
129.758895265214));
#114774=CARTESIAN_POINT('Ctrl Pts',(-160.335339671145,-4.82432417672621,
129.847762844019));
#114775=CARTESIAN_POINT('Ctrl Pts',(-160.346622984336,-4.86283527296383,
130.041982418629));
#114776=CARTESIAN_POINT('Ctrl Pts',(-160.357906297526,-4.88962764439993,
130.238596295259));
#114777=CARTESIAN_POINT('Ctrl Pts',(-160.369189610716,-4.90446956815478,
130.436445793804));
#114778=CARTESIAN_POINT('Ctrl Pts',(-160.376079552476,-4.91353250813849,
130.557258847472));
#114779=CARTESIAN_POINT('Ctrl Pts',(-160.382969494235,-4.91814028738697,
130.678532269095));
#114780=CARTESIAN_POINT('Ctrl Pts',(-160.389859435994,-4.91824806388606,
130.79999660782));
#114781=CARTESIAN_POINT('Ctrl Pts',(-160.389859436025,-4.91824806388654,
130.79999660837));
#114782=CARTESIAN_POINT('Ctrl Pts',(-160.397506818166,-4.91836768869606,
130.934814034577));
#114783=CARTESIAN_POINT('Ctrl Pts',(-160.405154200306,-4.91293979166222,
131.069814809062));
#114784=CARTESIAN_POINT('Ctrl Pts',(-160.412801582447,-4.90194590240347,
131.204497384697));
#114785=CARTESIAN_POINT('Ctrl Pts',(-160.420442448689,-4.89096138041009,
131.339065204998));
#114786=CARTESIAN_POINT('Ctrl Pts',(-160.428083314932,-4.87442033222005,
131.473314965856));
#114787=CARTESIAN_POINT('Ctrl Pts',(-160.435724181175,-4.85235634807507,
131.606745147449));
#114788=CARTESIAN_POINT('Ctrl Pts',(-160.443360955889,-4.83030417874477,
131.740103879894));
#114789=CARTESIAN_POINT('Ctrl Pts',(-160.450997730604,-4.80273501982829,
131.872643508878));
#114790=CARTESIAN_POINT('Ctrl Pts',(-160.458634505318,-4.76973425464364,
132.003868100902));
#114791=CARTESIAN_POINT('Ctrl Pts',(-160.466269233813,-4.73674233177829,
132.135057532234));
#114792=CARTESIAN_POINT('Ctrl Pts',(-160.473903962308,-4.69832179405056,
132.264932236198));
#114793=CARTESIAN_POINT('Ctrl Pts',(-160.481538690803,-4.65460893575638,
132.393007437245));
#114794=CARTESIAN_POINT('Ctrl Pts',(-160.489173138895,-4.61089768292314,
132.52107793442));
#114795=CARTESIAN_POINT('Ctrl Pts',(-160.496807586986,-4.56189462645772,
132.647348678373));
#114796=CARTESIAN_POINT('Ctrl Pts',(-160.504442035077,-4.50778546026211,
132.771351544528));
#114797=CARTESIAN_POINT('Ctrl Pts',(-160.512077968147,-4.45366576927798,
132.895378530513));
#114798=CARTESIAN_POINT('Ctrl Pts',(-160.519713901216,-4.39443815542719,
133.01713639209));
#114799=CARTESIAN_POINT('Ctrl Pts',(-160.527349834286,-4.33033559359262,
133.136178944401));
#114800=CARTESIAN_POINT('Ctrl Pts',(-160.534993528525,-4.26616787785568,
133.255342491671));
#114801=CARTESIAN_POINT('Ctrl Pts',(-160.542637222764,-4.19711551150681,
133.371784863109));
#114802=CARTESIAN_POINT('Ctrl Pts',(-160.550280917003,-4.1234565563492,
133.485086095939));
#114803=CARTESIAN_POINT('Ctrl Pts',(-160.55792869333,-4.04975826388435,
133.598447836896));
#114804=CARTESIAN_POINT('Ctrl Pts',(-160.565576469658,-3.97144871812164,
133.708664771202));
#114805=CARTESIAN_POINT('Ctrl Pts',(-160.573224245985,-3.88884729527296,
133.815348790334));
#114806=CARTESIAN_POINT('Ctrl Pts',(-160.580883717483,-3.80611955626038,
133.922195953339));
#114807=CARTESIAN_POINT('Ctrl Pts',(-160.588543188981,-3.71908709232117,
134.025499103716));
#114808=CARTESIAN_POINT('Ctrl Pts',(-160.59620266048,-3.62810763655974,
134.124905458407));
#114809=CARTESIAN_POINT('Ctrl Pts',(-160.602064205306,-3.55848401326856,
134.200977913819));
#114810=CARTESIAN_POINT('Ctrl Pts',(-160.607925750132,-3.48654968589756,
134.274768999458));
#114811=CARTESIAN_POINT('Ctrl Pts',(-160.613787294958,-3.41247785733266,
134.346136716604));
#114812=CARTESIAN_POINT('Ctrl Pts',(-160.621561629077,-3.31423427801122,
134.440793755808));
#114813=CARTESIAN_POINT('Ctrl Pts',(-160.629335963196,-3.21189363579122,
134.531509931887));
#114814=CARTESIAN_POINT('Ctrl Pts',(-160.637110297315,-3.1058052325787,
134.617909741386));
#114815=CARTESIAN_POINT('Ctrl Pts',(-160.644875050262,-2.99984757384174,
134.704203070841));
#114816=CARTESIAN_POINT('Ctrl Pts',(-160.652639803209,-2.89015164434804,
134.78619037349));
#114817=CARTESIAN_POINT('Ctrl Pts',(-160.660404556156,-2.77710371580365,
134.863532702384));
#114818=CARTESIAN_POINT('Ctrl Pts',(-160.668161597041,-2.6641680680556,
134.940798213788));
#114819=CARTESIAN_POINT('Ctrl Pts',(-160.675918637926,-2.54788736720672,
135.013427713087));
#114820=CARTESIAN_POINT('Ctrl Pts',(-160.683675678811,-2.4286808274601,
135.081122535282));
#114821=CARTESIAN_POINT('Ctrl Pts',(-160.691426870051,-2.30956418229223,
135.148766308285));
#114822=CARTESIAN_POINT('Ctrl Pts',(-160.699178061292,-2.18752642852371,
135.211482618882));
#114823=CARTESIAN_POINT('Ctrl Pts',(-160.706929252532,-2.06301531814953,
135.269016355647));
#114824=CARTESIAN_POINT('Ctrl Pts',(-160.714677149309,-1.93855712831887,
135.326525639039));
#114825=CARTESIAN_POINT('Ctrl Pts',(-160.722425046086,-1.81162802688853,
135.378856566015));
#114826=CARTESIAN_POINT('Ctrl Pts',(-160.730172942863,-1.68269970135527,
135.425800304239));
#114827=CARTESIAN_POINT('Ctrl Pts',(-160.737919218947,-1.55379834484835,
135.472734222846));
#114828=CARTESIAN_POINT('Ctrl Pts',(-160.745665495031,-1.42289896318864,
135.514283060457));
#114829=CARTESIAN_POINT('Ctrl Pts',(-160.753411771115,-1.29049215470584,
135.550286561061));
#114830=CARTESIAN_POINT('Ctrl Pts',(-160.761158104381,-1.15808436882588,
135.586290327436));
#114831=CARTESIAN_POINT('Ctrl Pts',(-160.768904437646,-1.02416951118544,
135.616748572538));
#114832=CARTESIAN_POINT('Ctrl Pts',(-160.776650770911,-0.889251846110277,
135.641551353591));
#114833=CARTESIAN_POINT('Ctrl Pts',(-160.784398838914,-0.754303967159656,
135.666359689056));
#114834=CARTESIAN_POINT('Ctrl Pts',(-160.792146906917,-0.618353218350478,
135.685509969605));
#114835=CARTESIAN_POINT('Ctrl Pts',(-160.79989497492,-0.481912127197375,
135.698943721791));
#114836=CARTESIAN_POINT('Ctrl Pts',(-160.807651277662,-0.345326024828738,
135.712391751528));
#114837=CARTESIAN_POINT('Ctrl Pts',(-160.815407580404,-0.208248928783801,
135.720111077879));
#114838=CARTESIAN_POINT('Ctrl Pts',(-160.823163883146,-0.0711970958349331,
135.722095262303));
#114839=CARTESIAN_POINT('Ctrl Pts',(-160.83092432566,0.0659278858037303,
135.724080505746));
#114840=CARTESIAN_POINT('Ctrl Pts',(-160.838684768174,0.203027186851613,
135.720324518627));
#114841=CARTESIAN_POINT('Ctrl Pts',(-160.846445210688,0.33958750583367,
135.710872962234));
#114842=CARTESIAN_POINT('Ctrl Pts',(-160.854218110954,0.476367043563012,
135.701406233364));
#114843=CARTESIAN_POINT('Ctrl Pts',(-160.861991011219,0.612605481453423,
135.686225707845));
#114844=CARTESIAN_POINT('Ctrl Pts',(-160.869763911485,0.747796675012283,
135.665428730166));
#114845=CARTESIAN_POINT('Ctrl Pts',(-160.877254247247,0.878073328159212,
135.64538777501));
#114846=CARTESIAN_POINT('Ctrl Pts',(-160.884744583009,1.00737725270633,
135.62013168165));
#114847=CARTESIAN_POINT('Ctrl Pts',(-160.892234918771,1.13526890413614,
135.589791379556));
#114848=CARTESIAN_POINT('Ctrl Pts',(-160.90000925289,1.26800960640155,135.558300715687));
#114849=CARTESIAN_POINT('Ctrl Pts',(-160.907783587009,1.3996493114814,135.521232943986));
#114850=CARTESIAN_POINT('Ctrl Pts',(-160.915557921128,1.5296832914725,135.478678973251));
#114851=CARTESIAN_POINT('Ctrl Pts',(-160.923322674075,1.65955701620473,
135.436177446481));
#114852=CARTESIAN_POINT('Ctrl Pts',(-160.931087427022,1.78782858528725,
135.38820329398));
#114853=CARTESIAN_POINT('Ctrl Pts',(-160.938852179969,1.91400404376249,
135.334898287971));
#114854=CARTESIAN_POINT('Ctrl Pts',(-160.946609220854,2.04005418299362,
135.281646225246));
#114855=CARTESIAN_POINT('Ctrl Pts',(-160.954366261739,2.16401199685134,
135.223073996826));
#114856=CARTESIAN_POINT('Ctrl Pts',(-160.962123302624,2.28539961449579,
135.159372863767));
#114857=CARTESIAN_POINT('Ctrl Pts',(-160.969874493865,2.40669569279335,
135.095719768228));
#114858=CARTESIAN_POINT('Ctrl Pts',(-160.977625685105,2.52542508796596,
135.026945647503));
#114859=CARTESIAN_POINT('Ctrl Pts',(-160.985376876345,2.64113114665654,
134.953289314068));
#114860=CARTESIAN_POINT('Ctrl Pts',(-160.993124773122,2.75678802718578,
134.879664286541));
#114861=CARTESIAN_POINT('Ctrl Pts',(-161.000872669899,2.86942379787809,
134.801161382973));
#114862=CARTESIAN_POINT('Ctrl Pts',(-161.008620566676,2.97860780356227,
134.718064568436));
#114863=CARTESIAN_POINT('Ctrl Pts',(-161.01636684276,3.08776897030619,134.634985135962));
#114864=CARTESIAN_POINT('Ctrl Pts',(-161.024113118844,3.19347949729487,
134.547313940524));
#114865=CARTESIAN_POINT('Ctrl Pts',(-161.031859394928,3.29533937622689,
134.455377114103));
#114866=CARTESIAN_POINT('Ctrl Pts',(-161.039605728194,3.39720000706553,
134.363439609026));
#114867=CARTESIAN_POINT('Ctrl Pts',(-161.047352061459,3.49520964289892,
134.267236672088));
#114868=CARTESIAN_POINT('Ctrl Pts',(-161.055098394724,3.5890032185711,134.167133128395));
#114869=CARTESIAN_POINT('Ctrl Pts',(-161.062846462727,3.68281779866359,
134.067007167208));
#114870=CARTESIAN_POINT('Ctrl Pts',(-161.07059453073,3.77241417256607,133.962979146318));
#114871=CARTESIAN_POINT('Ctrl Pts',(-161.078342598733,3.8574661112704,133.855448663313));
#114872=CARTESIAN_POINT('Ctrl Pts',(-161.086098901475,3.94260844418767,
133.747803895631));
#114873=CARTESIAN_POINT('Ctrl Pts',(-161.093855204217,4.02319645077549,
133.636649536951));
#114874=CARTESIAN_POINT('Ctrl Pts',(-161.101611506959,4.09894566471257,
133.522416448529));
#114875=CARTESIAN_POINT('Ctrl Pts',(-161.109371949473,4.1747353082859,133.408122390469));
#114876=CARTESIAN_POINT('Ctrl Pts',(-161.117132391987,4.24568081100074,
133.290746662861));
#114877=CARTESIAN_POINT('Ctrl Pts',(-161.124892834501,4.31154313700627,
133.170745801815));
#114878=CARTESIAN_POINT('Ctrl Pts',(-161.132665734767,4.37751119106466,
133.050552304734));
#114879=CARTESIAN_POINT('Ctrl Pts',(-161.140438635032,4.4383795885001,132.927725603616));
#114880=CARTESIAN_POINT('Ctrl Pts',(-161.148211535297,4.49395664452488,
132.802744149231));
#114881=CARTESIAN_POINT('Ctrl Pts',(-161.155701871059,4.54751333457375,
132.682306085521));
#114882=CARTESIAN_POINT('Ctrl Pts',(-161.163192206822,4.59615659758214,
132.559867496345));
#114883=CARTESIAN_POINT('Ctrl Pts',(-161.170682542584,4.63975900367446,
132.435868953531));
#114884=CARTESIAN_POINT('Ctrl Pts',(-161.178456876703,4.68501460824573,
132.307168968279));
#114885=CARTESIAN_POINT('Ctrl Pts',(-161.186231210822,4.72498291817413,
132.17638072013));
#114886=CARTESIAN_POINT('Ctrl Pts',(-161.194005544941,4.75946759984504,
132.043977989389));
#114887=CARTESIAN_POINT('Ctrl Pts',(-161.201770297888,4.79390978222777,
131.91173843318));
#114888=CARTESIAN_POINT('Ctrl Pts',(-161.209535050835,4.82288168532676,
131.777888728011));
#114889=CARTESIAN_POINT('Ctrl Pts',(-161.217299803782,4.84623559140791,
131.642921083526));
#114890=CARTESIAN_POINT('Ctrl Pts',(-161.225056844667,4.86956630206036,
131.508087490808));
#114891=CARTESIAN_POINT('Ctrl Pts',(-161.232813885552,4.88729005366754,
131.372138551175));
#114892=CARTESIAN_POINT('Ctrl Pts',(-161.240570926437,4.89930945870933,
131.235579692169));
#114893=CARTESIAN_POINT('Ctrl Pts',(-161.248322117677,4.91131979982429,
131.099123813261));
#114894=CARTESIAN_POINT('Ctrl Pts',(-161.256073308917,4.91763432249103,
130.962059318357));
#114895=CARTESIAN_POINT('Ctrl Pts',(-161.263824500158,4.9182071141168,130.824899486837));
#114896=CARTESIAN_POINT('Ctrl Pts',(-161.271572396935,4.91877966229084,
130.687797951904));
#114897=CARTESIAN_POINT('Ctrl Pts',(-161.279320293712,4.91361533154206,
130.550601551091));
#114898=CARTESIAN_POINT('Ctrl Pts',(-161.287068190489,4.90272025008849,
130.413826096848));
#114899=CARTESIAN_POINT('Ctrl Pts',(-161.294814466573,4.89182744765106,
130.277079253081));
#114900=CARTESIAN_POINT('Ctrl Pts',(-161.302560742657,4.87520630991227,
130.140753570225));
#114901=CARTESIAN_POINT('Ctrl Pts',(-161.310307018741,4.8529150066865,130.005361868896));
#114902=CARTESIAN_POINT('Ctrl Pts',(-161.318053352006,4.83062353891148,
129.869969168135));
#114903=CARTESIAN_POINT('Ctrl Pts',(-161.325799685272,4.80266188564376,
129.73551084843));
#114904=CARTESIAN_POINT('Ctrl Pts',(-161.333546018537,4.7691396579411,129.602491246314));
#114905=CARTESIAN_POINT('Ctrl Pts',(-161.34129408654,4.73560992316792,129.46944185538));
#114906=CARTESIAN_POINT('Ctrl Pts',(-161.349042154543,4.6965172315739,129.337832202198));
#114907=CARTESIAN_POINT('Ctrl Pts',(-161.356790222546,4.65202144117872,
129.208152744727));
#114908=CARTESIAN_POINT('Ctrl Pts',(-161.364546525288,4.60747836012794,
129.078335462385));
#114909=CARTESIAN_POINT('Ctrl Pts',(-161.37230282803,4.55752083614748,128.950452844109));
#114910=CARTESIAN_POINT('Ctrl Pts',(-161.380059130772,4.50235760401946,
128.824977110504));
#114911=CARTESIAN_POINT('Ctrl Pts',(-161.387819573286,4.44716492961338,
128.699434406722));
#114912=CARTESIAN_POINT('Ctrl Pts',(-161.3955800158,4.38676118288056,128.576301498173));
#114913=CARTESIAN_POINT('Ctrl Pts',(-161.403340458314,4.32140125586376,
128.456026261406));
#114914=CARTESIAN_POINT('Ctrl Pts',(-161.41111335858,4.2559364072899,128.335557948153));
#114915=CARTESIAN_POINT('Ctrl Pts',(-161.418886258845,4.18549968061349,
128.217956809345));
#114916=CARTESIAN_POINT('Ctrl Pts',(-161.42665915911,4.11038999970731,128.103642729151));
#114917=CARTESIAN_POINT('Ctrl Pts',(-161.434149494872,4.03801074489255,
127.993484253712));
#114918=CARTESIAN_POINT('Ctrl Pts',(-161.441639830634,3.96129256401282,
127.886378250718));
#114919=CARTESIAN_POINT('Ctrl Pts',(-161.449130166396,3.88053724366479,
127.782670070367));
#114920=CARTESIAN_POINT('Ctrl Pts',(-161.456904500515,3.79672006080012,
127.675029762836));
#114921=CARTESIAN_POINT('Ctrl Pts',(-161.464678834634,3.70828805131338,
127.570709048927));
#114922=CARTESIAN_POINT('Ctrl Pts',(-161.472453168754,3.61553369687891,
127.470129199498));
#114923=CARTESIAN_POINT('Ctrl Pts',(-161.480217921701,3.52289365389632,
127.369673305744));
#114924=CARTESIAN_POINT('Ctrl Pts',(-161.487982674648,3.42594212741971,
127.272949388035));
#114925=CARTESIAN_POINT('Ctrl Pts',(-161.495747427595,3.32501338231965,
127.18034777682));
#114926=CARTESIAN_POINT('Ctrl Pts',(-161.50350446848,3.22418488107207,127.08783813883));
#114927=CARTESIAN_POINT('Ctrl Pts',(-161.511261509365,3.11938730855479,
126.999442922031));
#114928=CARTESIAN_POINT('Ctrl Pts',(-161.51901855025,3.01099325494078,126.915517257234));
#114929=CARTESIAN_POINT('Ctrl Pts',(-161.52676974149,2.90268094212622,126.831654881434));
#114930=CARTESIAN_POINT('Ctrl Pts',(-161.53452093273,2.79077785443798,126.752255587196));
#114931=CARTESIAN_POINT('Ctrl Pts',(-161.54227212397,2.67569101147737,126.677635442127));
#114932=CARTESIAN_POINT('Ctrl Pts',(-161.550020020747,2.5606530834949,126.603047012611));
#114933=CARTESIAN_POINT('Ctrl Pts',(-161.557767917524,2.44243441897169,
126.533233904484));
#114934=CARTESIAN_POINT('Ctrl Pts',(-161.565515814302,2.32147229798197,
126.468469771131));
#114935=CARTESIAN_POINT('Ctrl Pts',(-161.573262090386,2.20053547966033,
126.403719185038));
#114936=CARTESIAN_POINT('Ctrl Pts',(-161.58100836647,2.07685669078846,126.344015657429));
#114937=CARTESIAN_POINT('Ctrl Pts',(-161.588754642554,1.95089882407887,
126.289587440461));
#114938=CARTESIAN_POINT('Ctrl Pts',(-161.596500975819,1.82494002757676,
126.235158821716));
#114939=CARTESIAN_POINT('Ctrl Pts',(-161.604247309085,1.69670247855829,
126.186005746397));
#114940=CARTESIAN_POINT('Ctrl Pts',(-161.61199364235,1.56666973708766,126.142308601834));
#114941=CARTESIAN_POINT('Ctrl Pts',(-161.619741710353,1.43660787568599,
126.098601671598));
#114942=CARTESIAN_POINT('Ctrl Pts',(-161.627489778356,1.3047503923855,126.060353227909));
#114943=CARTESIAN_POINT('Ctrl Pts',(-161.635237846359,1.17159633052308,
126.027693882194));
#114944=CARTESIAN_POINT('Ctrl Pts',(-161.642994149101,1.03830075093933,
125.994999825739));
#114945=CARTESIAN_POINT('Ctrl Pts',(-161.650750451843,0.903706220367848,
125.967906826649));
#114946=CARTESIAN_POINT('Ctrl Pts',(-161.658506754585,0.768322857626625,
125.946494517214));
#114947=CARTESIAN_POINT('Ctrl Pts',(-161.666267197099,0.632867236708392,
125.925070779384));
#114948=CARTESIAN_POINT('Ctrl Pts',(-161.674027639613,0.496622332888463,
125.909333817474));
#114949=CARTESIAN_POINT('Ctrl Pts',(-161.681788082127,0.360102732768053,
125.899311271805));
#114950=CARTESIAN_POINT('Ctrl Pts',(-161.689560982393,0.223363979265889,
125.889272637055));
#114951=CARTESIAN_POINT('Ctrl Pts',(-161.697333882658,0.0863500392680675,
125.884966761986));
#114952=CARTESIAN_POINT('Ctrl Pts',(-161.705106782924,-0.0504242511279812,
125.886369111128));
#114953=CARTESIAN_POINT('Ctrl Pts',(-161.712597118686,-0.182226451554115,
125.887720481346));
#114954=CARTESIAN_POINT('Ctrl Pts',(-161.720087454448,-0.313805815984554,
125.894372248864));
#114955=CARTESIAN_POINT('Ctrl Pts',(-161.72757779021,-0.444708668489591,
125.906257182289));
#114956=CARTESIAN_POINT('Ctrl Pts',(-161.735352124329,-0.580574742435354,
125.918592736578));
#114957=CARTESIAN_POINT('Ctrl Pts',(-161.743126458448,-0.716142374763522,
125.936605196641));
#114958=CARTESIAN_POINT('Ctrl Pts',(-161.750900792567,-0.850899044880972,
125.960276196551));
#114959=CARTESIAN_POINT('Ctrl Pts',(-161.758665545514,-0.985489639445686,
125.983918024069));
#114960=CARTESIAN_POINT('Ctrl Pts',(-161.766430298461,-1.11927087901136,
126.013204448969));
#114961=CARTESIAN_POINT('Ctrl Pts',(-161.774195051408,-1.25173368918903,
126.04806522789));
#114962=CARTESIAN_POINT('Ctrl Pts',(-161.781952092293,-1.38406493543623,
126.082891382595));
#114963=CARTESIAN_POINT('Ctrl Pts',(-161.789709133178,-1.51507998258062,
126.123280774522));
#114964=CARTESIAN_POINT('Ctrl Pts',(-161.797466174063,-1.64427865492304,
126.169111889885));
#114965=CARTESIAN_POINT('Ctrl Pts',(-161.805217365304,-1.7733798975418,
126.214908443648));
#114966=CARTESIAN_POINT('Ctrl Pts',(-161.812968556544,-1.90066712476996,
126.26613842261));
#114967=CARTESIAN_POINT('Ctrl Pts',(-161.820719747784,-2.02565441594169,
126.322630231914));
#114968=CARTESIAN_POINT('Ctrl Pts',(-161.828467644561,-2.15058858418035,
126.379098030692));
#114969=CARTESIAN_POINT('Ctrl Pts',(-161.836215541338,-2.27322440508434,
126.44082305106));
#114970=CARTESIAN_POINT('Ctrl Pts',(-161.843963438115,-2.3930952857491,
126.507585313245));
#114971=CARTESIAN_POINT('Ctrl Pts',(-161.851709714199,-2.51294109200942,
126.574333610204));
#114972=CARTESIAN_POINT('Ctrl Pts',(-161.859455990283,-2.6300227670859,
126.646116863035));
#114973=CARTESIAN_POINT('Ctrl Pts',(-161.867202266367,-2.74389807115714,
126.722669002855));
#114974=CARTESIAN_POINT('Ctrl Pts',(-161.874948599633,-2.85777421583017,
126.799221707766));
#114975=CARTESIAN_POINT('Ctrl Pts',(-161.882694932898,-2.96844361780387,
126.880543151792));
#114976=CARTESIAN_POINT('Ctrl Pts',(-161.890441266163,-3.07549313608341,
126.966324005911));
#114977=CARTESIAN_POINT('Ctrl Pts',(-161.898189334166,-3.18256662736019,
127.052124070058));
#114978=CARTESIAN_POINT('Ctrl Pts',(-161.905937402169,-3.28601831680974,
127.142385287072));
#114979=CARTESIAN_POINT('Ctrl Pts',(-161.913685470172,-3.38546857222495,
127.236758396329));
#114980=CARTESIAN_POINT('Ctrl Pts',(-161.921441772914,-3.48502452455496,
127.331231806448));
#114981=CARTESIAN_POINT('Ctrl Pts',(-161.929198075656,-3.58057026343033,
127.429825569142));
#114982=CARTESIAN_POINT('Ctrl Pts',(-161.936954378398,-3.67176306027024,
127.532153550198));
#114983=CARTESIAN_POINT('Ctrl Pts',(-161.944714820912,-3.76300452945184,
127.634536146778));
#114984=CARTESIAN_POINT('Ctrl Pts',(-161.952475263426,-3.84988817968207,
127.740656630709));
#114985=CARTESIAN_POINT('Ctrl Pts',(-161.96023570594,-3.93211260974882,
127.850097005978));
#114986=CARTESIAN_POINT('Ctrl Pts',(-161.968008606206,-4.01446903377025,
127.959713064653));
#114987=CARTESIAN_POINT('Ctrl Pts',(-161.975781506471,-4.09215106973453,
128.072659342158));
#114988=CARTESIAN_POINT('Ctrl Pts',(-161.983554406737,-4.16490107854198,
128.188489430283));
#114989=CARTESIAN_POINT('Ctrl Pts',(-161.991044742499,-4.23500644128207,
128.300108802944));
#114990=CARTESIAN_POINT('Ctrl Pts',(-161.99853507826,-4.30053198135975,
128.414405691581));
#114991=CARTESIAN_POINT('Ctrl Pts',(-162.006025414022,-4.36128903952838,
128.530962065576));
#114992=CARTESIAN_POINT('Ctrl Pts',(-162.014275408015,-4.42820798426658,
128.659339406174));
#114993=CARTESIAN_POINT('Ctrl Pts',(-162.022525402008,-4.48953361810604,
128.790824632779));
#114994=CARTESIAN_POINT('Ctrl Pts',(-162.030775396001,-4.5449844696847,
128.924919415287));
#114995=CARTESIAN_POINT('Ctrl Pts',(-162.039006074437,-4.60030549521436,
129.058700244171));
#114996=CARTESIAN_POINT('Ctrl Pts',(-162.047236752872,-4.64977904220322,
129.195078152985));
#114997=CARTESIAN_POINT('Ctrl Pts',(-162.055467431307,-4.69317003756102,
129.333531578881));
#114998=CARTESIAN_POINT('Ctrl Pts',(-162.060359422207,-4.71895993520688,
129.415822838925));
#114999=CARTESIAN_POINT('Ctrl Pts',(-162.065251413106,-4.74260194298077,
129.498846814994));
#115000=CARTESIAN_POINT('Ctrl Pts',(-162.070143404005,-4.764054528234,129.582490119308));
#115001=CARTESIAN_POINT('Origin',(213.235140564004,0.,130.804360617566));
#115002=CARTESIAN_POINT('',(-164.165050101093,-4.76405452823413,129.582490119309));
#115003=CARTESIAN_POINT('',(-163.819828717623,-4.76405452823398,129.582490119308));
#115004=CARTESIAN_POINT('',(213.235140564004,-4.76405452823405,129.582490119308));
#115005=CARTESIAN_POINT('',(-162.485140563971,-4.91824798157934,130.808816421734));
#115006=CARTESIAN_POINT('Ctrl Pts',(-162.485140564011,-4.91824798157869,
130.808816422445));
#115007=CARTESIAN_POINT('Ctrl Pts',(-162.496060307999,-4.918073492229,131.001415047217));
#115008=CARTESIAN_POINT('Ctrl Pts',(-162.506980051987,-4.90658238243364,
131.193522218363));
#115009=CARTESIAN_POINT('Ctrl Pts',(-162.517899795976,-4.88396733481339,
131.384055481245));
#115010=CARTESIAN_POINT('Ctrl Pts',(-162.526377085813,-4.86641066740618,
131.531971558301));
#115011=CARTESIAN_POINT('Ctrl Pts',(-162.534854375651,-4.8421507266267,
131.678939988927));
#115012=CARTESIAN_POINT('Ctrl Pts',(-162.543331665489,-4.8112959995807,
131.824465448904));
#115013=CARTESIAN_POINT('Ctrl Pts',(-162.551105999608,-4.78299981509265,
131.95792361423));
#115014=CARTESIAN_POINT('Ctrl Pts',(-162.558880333727,-4.74910170794549,
132.090414934641));
#115015=CARTESIAN_POINT('Ctrl Pts',(-162.566654667846,-4.70968044867888,
132.221432646022));
#115016=CARTESIAN_POINT('Ctrl Pts',(-162.574419420793,-4.67030777259114,
132.352288889783));
#115017=CARTESIAN_POINT('Ctrl Pts',(-162.58218417374,-4.62542559943551,
132.481674767203));
#115018=CARTESIAN_POINT('Ctrl Pts',(-162.589948926687,-4.57516380705058,
132.60909306343));
#115019=CARTESIAN_POINT('Ctrl Pts',(-162.597705967572,-4.52495193538641,
132.736384806009));
#115020=CARTESIAN_POINT('Ctrl Pts',(-162.605463008457,-4.46937122006502,
132.861712495059));
#115021=CARTESIAN_POINT('Ctrl Pts',(-162.613220049342,-4.40860139947938,
132.984593807619));
#115022=CARTESIAN_POINT('Ctrl Pts',(-162.620971240582,-4.34787740588808,
133.107382454425));
#115023=CARTESIAN_POINT('Ctrl Pts',(-162.628722431823,-4.28197226852108,
133.227728047732));
#115024=CARTESIAN_POINT('Ctrl Pts',(-162.636473623063,-4.21111377266266,
133.345168334846));
#115025=CARTESIAN_POINT('Ctrl Pts',(-162.64422151984,-4.14028539355529,
133.462558706706));
#115026=CARTESIAN_POINT('Ctrl Pts',(-162.651969416617,-4.06450804480952,
133.577045894308));
#115027=CARTESIAN_POINT('Ctrl Pts',(-162.659717313394,-3.98405527518577,
133.688192552122));
#115028=CARTESIAN_POINT('Ctrl Pts',(-162.667463589478,-3.90361933454707,
133.799315960451));
#115029=CARTESIAN_POINT('Ctrl Pts',(-162.675209865562,-3.81851014741903,
133.907099912374));
#115030=CARTESIAN_POINT('Ctrl Pts',(-162.682956141646,-3.72904415276827,
134.011136688514));
#115031=CARTESIAN_POINT('Ctrl Pts',(-162.690702474912,-3.63957749769998,
134.11517423263));
#115032=CARTESIAN_POINT('Ctrl Pts',(-162.698448808177,-3.54575422584954,
134.215464249335));
#115033=CARTESIAN_POINT('Ctrl Pts',(-162.706195141442,-3.44793029670246,
134.311633023807));
#115034=CARTESIAN_POINT('Ctrl Pts',(-162.713943209445,-3.35008446056483,
134.40782333461));
#115035=CARTESIAN_POINT('Ctrl Pts',(-162.721691277448,-3.24823646310393,
134.499890292635));
#115036=CARTESIAN_POINT('Ctrl Pts',(-162.729439345451,-3.14277795823583,
134.58749817358));
#115037=CARTESIAN_POINT('Ctrl Pts',(-162.737195648193,-3.03720737081365,
134.675199165225));
#115038=CARTESIAN_POINT('Ctrl Pts',(-162.744951950935,-2.9280189117952,
134.75843136258));
#115039=CARTESIAN_POINT('Ctrl Pts',(-162.752708253677,-2.81563649195168,
134.836900041761));
#115040=CARTESIAN_POINT('Ctrl Pts',(-162.760468696191,-2.70319409022693,
134.91541060204));
#115041=CARTESIAN_POINT('Ctrl Pts',(-162.768229138705,-2.58755466037525,
134.989152368025));
#115042=CARTESIAN_POINT('Ctrl Pts',(-162.775989581219,-2.46916887083393,
135.057875417094));
#115043=CARTESIAN_POINT('Ctrl Pts',(-162.783762481485,-2.35059303791345,
135.126708786503));
#115044=CARTESIAN_POINT('Ctrl Pts',(-162.79153538175,-2.22926238155688,
135.1905071575));
#115045=CARTESIAN_POINT('Ctrl Pts',(-162.799308282015,-2.10565061484523,
135.249067418999));
#115046=CARTESIAN_POINT('Ctrl Pts',(-162.806798617777,-1.98653244721482,
135.305498867487));
#115047=CARTESIAN_POINT('Ctrl Pts',(-162.814288953539,-1.86529642151892,
135.357066310976));
#115048=CARTESIAN_POINT('Ctrl Pts',(-162.821779289301,-1.74237992474672,
135.403631783777));
#115049=CARTESIAN_POINT('Ctrl Pts',(-162.82955362342,-1.61480301163777,
135.451962800634));
#115050=CARTESIAN_POINT('Ctrl Pts',(-162.837327957539,-1.48501155650677,
135.495058158009));
#115051=CARTESIAN_POINT('Ctrl Pts',(-162.845102291658,-1.35347449175632,
135.532710209407));
#115052=CARTESIAN_POINT('Ctrl Pts',(-162.852867044605,-1.22209953468272,
135.570315858017));
#115053=CARTESIAN_POINT('Ctrl Pts',(-162.860631797552,-1.08898362071227,
135.602491441784));
#115054=CARTESIAN_POINT('Ctrl Pts',(-162.8683965505,-0.954615272926989,
135.629077473838));
#115055=CARTESIAN_POINT('Ctrl Pts',(-162.876153591384,-0.820380381678994,
135.65563710027));
#115056=CARTESIAN_POINT('Ctrl Pts',(-162.883910632269,-0.684895913150993,
135.676618147574));
#115057=CARTESIAN_POINT('Ctrl Pts',(-162.891667673154,-0.548664812303447,
135.691911127406));
#115058=CARTESIAN_POINT('Ctrl Pts',(-162.899418864395,-0.412536444388588,
135.707192574684));
#115059=CARTESIAN_POINT('Ctrl Pts',(-162.907170055635,-0.275662951806377,
135.716794448873));
#115060=CARTESIAN_POINT('Ctrl Pts',(-162.914921246875,-0.138556364349379,
135.720658533315));
#115061=CARTESIAN_POINT('Ctrl Pts',(-162.922669143652,-0.00150805084967565,
135.724520975418));
#115062=CARTESIAN_POINT('Ctrl Pts',(-162.930417040429,0.13577277048724,
135.722650467196));
#115063=CARTESIAN_POINT('Ctrl Pts',(-162.938164937206,0.272770288692314,
135.715040757028));
#115064=CARTESIAN_POINT('Ctrl Pts',(-162.94591121329,0.409739149969904,
135.707432638647));
#115065=CARTESIAN_POINT('Ctrl Pts',(-162.953657489374,0.546424435872705,
135.694087727883));
#115066=CARTESIAN_POINT('Ctrl Pts',(-162.961403765458,0.682312077550561,
135.675051871518));
#115067=CARTESIAN_POINT('Ctrl Pts',(-162.969150098724,0.818200722320303,
135.656015874635));
#115068=CARTESIAN_POINT('Ctrl Pts',(-162.976896431989,0.953291323931337,
135.631288902564));
#115069=CARTESIAN_POINT('Ctrl Pts',(-162.984642765254,1.08707706072241,
135.600968432111));
#115070=CARTESIAN_POINT('Ctrl Pts',(-162.992390833257,1.22089275790145,
135.570641171598));
#115071=CARTESIAN_POINT('Ctrl Pts',(-163.00013890126,1.3534026275631,135.534718006523));
#115072=CARTESIAN_POINT('Ctrl Pts',(-163.007886969263,1.48411251683514,
135.49334697923));
#115073=CARTESIAN_POINT('Ctrl Pts',(-163.015643272005,1.61496132613314,
135.451931982318));
#115074=CARTESIAN_POINT('Ctrl Pts',(-163.023399574747,1.74400596020215,
135.405057675098));
#115075=CARTESIAN_POINT('Ctrl Pts',(-163.031155877489,1.87076932536499,
135.35292140025));
#115076=CARTESIAN_POINT('Ctrl Pts',(-163.038916320003,1.9976003479526,135.300757298703));
#115077=CARTESIAN_POINT('Ctrl Pts',(-163.046676762517,2.12214732063613,
135.243325797048));
#115078=CARTESIAN_POINT('Ctrl Pts',(-163.054437205031,2.24395637913678,
135.180870966124));
#115079=CARTESIAN_POINT('Ctrl Pts',(-163.062210105296,2.36596097635184,
135.11831587716));
#115080=CARTESIAN_POINT('Ctrl Pts',(-163.069983005562,2.48521853616227,
135.050721537591));
#115081=CARTESIAN_POINT('Ctrl Pts',(-163.077755905827,2.60130212196725,
134.978376709144));
#115082=CARTESIAN_POINT('Ctrl Pts',(-163.08524624159,2.71316577703477,134.908661797434));
#115083=CARTESIAN_POINT('Ctrl Pts',(-163.092736577352,2.82208196095618,
134.834535958241));
#115084=CARTESIAN_POINT('Ctrl Pts',(-163.100226913114,2.92769818093926,
134.756292603801));
#115085=CARTESIAN_POINT('Ctrl Pts',(-163.108001247233,3.03731887200142,
134.675082628798));
#115086=CARTESIAN_POINT('Ctrl Pts',(-163.115775581352,3.14373166851665,
134.589179495035));
#115087=CARTESIAN_POINT('Ctrl Pts',(-163.123549915471,3.2465084021888,134.49886549062));
#115088=CARTESIAN_POINT('Ctrl Pts',(-163.131314668418,3.34915847272184,
134.408662790144));
#115089=CARTESIAN_POINT('Ctrl Pts',(-163.139079421365,3.44818110564297,
134.31406029064));
#115090=CARTESIAN_POINT('Ctrl Pts',(-163.146844174313,3.5431780614734,134.215382793864));
#115091=CARTESIAN_POINT('Ctrl Pts',(-163.154601215198,3.63808066498807,
134.116803304968));
#115092=CARTESIAN_POINT('Ctrl Pts',(-163.162358256083,3.72896527893046,
134.014157153034));
#115093=CARTESIAN_POINT('Ctrl Pts',(-163.170115296968,3.81546793362102,
133.907808298776));
#115094=CARTESIAN_POINT('Ctrl Pts',(-163.177866488208,3.90190535598691,
133.801539643017));
#115095=CARTESIAN_POINT('Ctrl Pts',(-163.185617679448,3.98396715074385,
133.691574144787));
#115096=CARTESIAN_POINT('Ctrl Pts',(-163.193368870688,4.06132757395633,
133.578311121725));
#115097=CARTESIAN_POINT('Ctrl Pts',(-163.201116767465,4.13865511692518,
133.465096238469));
#115098=CARTESIAN_POINT('Ctrl Pts',(-163.208864664242,4.21128504258629,
133.348586940099));
#115099=CARTESIAN_POINT('Ctrl Pts',(-163.216612561019,4.27893328284376,
133.229213813838));
#115100=CARTESIAN_POINT('Ctrl Pts',(-163.224358837103,4.34656737254769,
133.109865657862));
#115101=CARTESIAN_POINT('Ctrl Pts',(-163.232105113188,4.40922165692871,
132.987655205467));
#115102=CARTESIAN_POINT('Ctrl Pts',(-163.239851389272,4.46665684141273,
132.863039738644));
#115103=CARTESIAN_POINT('Ctrl Pts',(-163.247597722537,4.52409244987031,
132.738423351937));
#115104=CARTESIAN_POINT('Ctrl Pts',(-163.255344055802,4.57630871790457,
132.611402270442));
#115105=CARTESIAN_POINT('Ctrl Pts',(-163.263090389068,4.62311370602557,
132.482455586171));
#115106=CARTESIAN_POINT('Ctrl Pts',(-163.270838457071,4.66992917579907,
132.353480025185));
#115107=CARTESIAN_POINT('Ctrl Pts',(-163.278586525074,4.71133082090973,
132.222578370769));
#115108=CARTESIAN_POINT('Ctrl Pts',(-163.286334593077,4.74717609187807,
132.090246388232));
#115109=CARTESIAN_POINT('Ctrl Pts',(-163.294090895818,4.783059459627,131.957773761689));
#115110=CARTESIAN_POINT('Ctrl Pts',(-163.30184719856,4.81337455421823,131.823868148292));
#115111=CARTESIAN_POINT('Ctrl Pts',(-163.309603501302,4.83802952485061,
131.689037609001));
#115112=CARTESIAN_POINT('Ctrl Pts',(-163.317363943816,4.86269765458316,
131.554135106591));
#115113=CARTESIAN_POINT('Ctrl Pts',(-163.325124386331,4.88169958666042,
131.418307081631));
#115114=CARTESIAN_POINT('Ctrl Pts',(-163.332884828845,4.89499534006176,
131.282067309244));
#115115=CARTESIAN_POINT('Ctrl Pts',(-163.34065772911,4.90831243698681,131.145608832679));
#115116=CARTESIAN_POINT('Ctrl Pts',(-163.348430629376,4.9159050288411,131.008737678439));
#115117=CARTESIAN_POINT('Ctrl Pts',(-163.356203529641,4.91778528938313,
130.871969123147));
#115118=CARTESIAN_POINT('Ctrl Pts',(-163.363693865403,4.91959719771836,
130.740172449339));
#115119=CARTESIAN_POINT('Ctrl Pts',(-163.371184201165,4.91610488768731,
130.608471352435));
#115120=CARTESIAN_POINT('Ctrl Pts',(-163.378674536927,4.90736468435062,
130.477320991086));
#115121=CARTESIAN_POINT('Ctrl Pts',(-163.386448871046,4.89829309354788,
130.341198023923));
#115122=CARTESIAN_POINT('Ctrl Pts',(-163.394223205165,4.88353907000355,
130.205237182349));
#115123=CARTESIAN_POINT('Ctrl Pts',(-163.401997539284,4.86310867527487,
130.069951280094));
#115124=CARTESIAN_POINT('Ctrl Pts',(-163.409762292231,4.84270345918178,
129.934832105623));
#115125=CARTESIAN_POINT('Ctrl Pts',(-163.417527045178,4.81663584892317,
129.800386598303));
#115126=CARTESIAN_POINT('Ctrl Pts',(-163.425291798126,4.78496385124945,
129.66712537157));
#115127=CARTESIAN_POINT('Ctrl Pts',(-163.433048839011,4.75332331065031,
129.533996501766));
#115128=CARTESIAN_POINT('Ctrl Pts',(-163.440805879896,4.71608954975383,
129.402049949678));
#115129=CARTESIAN_POINT('Ctrl Pts',(-163.448562920781,4.67337204451598,
129.271788662963));
#115130=CARTESIAN_POINT('Ctrl Pts',(-163.456314112021,4.63068675288106,
129.141625607297));
#115131=CARTESIAN_POINT('Ctrl Pts',(-163.464065303261,4.58252606937225,
129.013145657407));
#115132=CARTESIAN_POINT('Ctrl Pts',(-163.471816494501,4.52904987867432,
128.886838711829));
#115133=CARTESIAN_POINT('Ctrl Pts',(-163.479564391278,4.47559641678404,
128.760585450073));
#115134=CARTESIAN_POINT('Ctrl Pts',(-163.487312288055,4.41683209325552,
128.636503714961));
#115135=CARTESIAN_POINT('Ctrl Pts',(-163.495060184832,4.35296562756867,
128.51506524394));
#115136=CARTESIAN_POINT('Ctrl Pts',(-163.502806460916,4.28911252136964,
128.393652175229));
#115137=CARTESIAN_POINT('Ctrl Pts',(-163.510552737,4.22015957771432,128.274881616642));
#115138=CARTESIAN_POINT('Ctrl Pts',(-163.518299013084,4.14636217632811,
128.159202065567));
#115139=CARTESIAN_POINT('Ctrl Pts',(-163.52604534635,4.07256423018615,128.043521660571));
#115140=CARTESIAN_POINT('Ctrl Pts',(-163.533791679615,3.99392196522635,
127.930932638221));
#115141=CARTESIAN_POINT('Ctrl Pts',(-163.541538012881,3.91073470714457,
127.821855443583));
#115142=CARTESIAN_POINT('Ctrl Pts',(-163.549286080884,3.82752881985325,
127.712753821863));
#115143=CARTESIAN_POINT('Ctrl Pts',(-163.557034148887,3.73977615113876,
127.607165903613));
#115144=CARTESIAN_POINT('Ctrl Pts',(-163.564782216889,3.64781675092208,
127.505479593007));
#115145=CARTESIAN_POINT('Ctrl Pts',(-163.572538519631,3.5557596151604,127.40368520898));
#115146=CARTESIAN_POINT('Ctrl Pts',(-163.580294822373,3.459487079319,127.305801006465));
#115147=CARTESIAN_POINT('Ctrl Pts',(-163.588051125115,3.35937694187183,
127.212178881501));
#115148=CARTESIAN_POINT('Ctrl Pts',(-163.595811567629,3.25921337263006,
127.11850678759));
#115149=CARTESIAN_POINT('Ctrl Pts',(-163.603572010143,3.15520841681785,
127.029101558696));
#115150=CARTESIAN_POINT('Ctrl Pts',(-163.611332452658,3.04777271727758,
126.944274539987));
#115151=CARTESIAN_POINT('Ctrl Pts',(-163.619105352923,2.9401645524147,126.859311349417));
#115152=CARTESIAN_POINT('Ctrl Pts',(-163.626878253189,2.82911495531737,
126.778941284727));
#115153=CARTESIAN_POINT('Ctrl Pts',(-163.634651153454,2.71506402301407,
126.703432623388));
#115154=CARTESIAN_POINT('Ctrl Pts',(-163.642141489216,2.60515912937695,
126.630668892083));
#115155=CARTESIAN_POINT('Ctrl Pts',(-163.649631824978,2.49246758770634,
126.562419411565));
#115156=CARTESIAN_POINT('Ctrl Pts',(-163.65712216074,2.3774027809366,126.498882818332));
#115157=CARTESIAN_POINT('Ctrl Pts',(-163.664896494859,2.25797525704483,
126.432937215856));
#115158=CARTESIAN_POINT('Ctrl Pts',(-163.672670828978,2.13561264030401,
126.37186003782));
#115159=CARTESIAN_POINT('Ctrl Pts',(-163.680445163097,2.01074965184982,
126.315923372813));
#115160=CARTESIAN_POINT('Ctrl Pts',(-163.688209916044,1.88604054586957,
126.260055644747));
#115161=CARTESIAN_POINT('Ctrl Pts',(-163.695974668992,1.75883755278497,
126.20931598281));
#115162=CARTESIAN_POINT('Ctrl Pts',(-163.703739421939,1.62960162020577,
126.163931583315));
#115163=CARTESIAN_POINT('Ctrl Pts',(-163.711496462824,1.50049404657672,
126.118592260245));
#115164=CARTESIAN_POINT('Ctrl Pts',(-163.719253503709,1.36935791813451,
126.078597743425));
#115165=CARTESIAN_POINT('Ctrl Pts',(-163.727010544594,1.23667555341529,
126.044127783126));
#115166=CARTESIAN_POINT('Ctrl Pts',(-163.734761735834,1.10409324549961,
126.009683816892));
#115167=CARTESIAN_POINT('Ctrl Pts',(-163.742512927074,0.969967399089417,
125.980756212697));
#115168=CARTESIAN_POINT('Ctrl Pts',(-163.750264118314,0.834796601275304,
125.957475257152));
#115169=CARTESIAN_POINT('Ctrl Pts',(-163.758012015091,0.699683254655876,
125.934204196634));
#115170=CARTESIAN_POINT('Ctrl Pts',(-163.765759911868,0.56352622446324,
125.916575077618));
#115171=CARTESIAN_POINT('Ctrl Pts',(-163.773507808645,0.426835214747577,
125.904667284106));
#115172=CARTESIAN_POINT('Ctrl Pts',(-163.78125408473,0.290172797844429,
125.892761981448));
#115173=CARTESIAN_POINT('Ctrl Pts',(-163.789000360814,0.152977012833045,
125.886575657746));
#115174=CARTESIAN_POINT('Ctrl Pts',(-163.796746636898,0.0157632322466415,
125.886135878597));
#115175=CARTESIAN_POINT('Ctrl Pts',(-163.804492970163,-0.121451561220533,
125.885696096201));
#115176=CARTESIAN_POINT('Ctrl Pts',(-163.812239303428,-0.258683959564604,
125.891002944257));
#115177=CARTESIAN_POINT('Ctrl Pts',(-163.819985636694,-0.395418437595522,
125.902031852407));
#115178=CARTESIAN_POINT('Ctrl Pts',(-163.827733704697,-0.532183536364932,
125.913063230403));
#115179=CARTESIAN_POINT('Ctrl Pts',(-163.8354817727,-0.668450103312558,
125.929819186935));
#115180=CARTESIAN_POINT('Ctrl Pts',(-163.843229840703,-0.803707978381973,
125.952223300055));
#115181=CARTESIAN_POINT('Ctrl Pts',(-163.850986143445,-0.939109607130786,
125.974651224532));
#115182=CARTESIAN_POINT('Ctrl Pts',(-163.858742446186,-1.07350001614181,
126.002739233102));
#115183=CARTESIAN_POINT('Ctrl Pts',(-163.866498748928,-1.20637893600707,
126.036359681612));
#115184=CARTESIAN_POINT('Ctrl Pts',(-163.874259191443,-1.33932877735277,
126.069998074368));
#115185=CARTESIAN_POINT('Ctrl Pts',(-163.882019633957,-1.47076514758795,
126.109174679205));
#115186=CARTESIAN_POINT('Ctrl Pts',(-163.889780076471,-1.60020414071843,
126.153712300339));
#115187=CARTESIAN_POINT('Ctrl Pts',(-163.897552976736,-1.72985092081172,
126.198321417216));
#115188=CARTESIAN_POINT('Ctrl Pts',(-163.905325877002,-1.857493552203,126.248308605229));
#115189=CARTESIAN_POINT('Ctrl Pts',(-163.913098777267,-1.98266844226304,
126.303448608811));
#115190=CARTESIAN_POINT('Ctrl Pts',(-163.920589113029,-2.10329290976984,
126.356584134372));
#115191=CARTESIAN_POINT('Ctrl Pts',(-163.928079448791,-2.22162566156996,
126.414504208663));
#115192=CARTESIAN_POINT('Ctrl Pts',(-163.935569784553,-2.33727613557715,
126.476968408792));
#115193=CARTESIAN_POINT('Ctrl Pts',(-163.943345096754,-2.45732663401265,
126.541809114584));
#115194=CARTESIAN_POINT('Ctrl Pts',(-163.951120408956,-2.57486704658424,
126.611751984011));
#115195=CARTESIAN_POINT('Ctrl Pts',(-163.958895721157,-2.68943330620135,
126.686578258821));
#115196=CARTESIAN_POINT('Ctrl Pts',(-163.966661236855,-2.80385521807688,
126.761310256276));
#115197=CARTESIAN_POINT('Ctrl Pts',(-163.974426752554,-2.91531010934181,
126.840913203683));
#115198=CARTESIAN_POINT('Ctrl Pts',(-163.982192268252,-3.02335755442061,
126.925122011779));
#115199=CARTESIAN_POINT('Ctrl Pts',(-163.989948459034,-3.13127525494891,
127.00922970102));
#115200=CARTESIAN_POINT('Ctrl Pts',(-163.997704649816,-3.23579335209254,
127.097931996773));
#115201=CARTESIAN_POINT('Ctrl Pts',(-164.005460840598,-3.3365000523127,
127.19092036437));
#115202=CARTESIAN_POINT('Ctrl Pts',(-164.013211744224,-3.43713810387628,
127.28384534466));
#115203=CARTESIAN_POINT('Ctrl Pts',(-164.02096264785,-3.53396964127995,
127.381050320298));
#115204=CARTESIAN_POINT('Ctrl Pts',(-164.028713551475,-3.62661559769413,
127.482186273998));
#115205=CARTESIAN_POINT('Ctrl Pts',(-164.03646085016,-3.71921846452278,
127.583275189419));
#115206=CARTESIAN_POINT('Ctrl Pts',(-164.044208148844,-3.80763936072918,
127.688291157111));
#115207=CARTESIAN_POINT('Ctrl Pts',(-164.051955447529,-3.89153607157014,
127.796848345576));
#115208=CARTESIAN_POINT('Ctrl Pts',(-164.059700820705,-3.97541193078043,
127.905378553313));
#115209=CARTESIAN_POINT('Ctrl Pts',(-164.067446193881,-4.0547656045305,
128.017447920521));
#115210=CARTESIAN_POINT('Ctrl Pts',(-164.075191567058,-4.1292954327201,
128.132637897706));
#115211=CARTESIAN_POINT('Ctrl Pts',(-164.08293930202,-4.20384798718999,
128.247862999615));
#115212=CARTESIAN_POINT('Ctrl Pts',(-164.090687036983,-4.27357353930711,
128.366210287816));
#115213=CARTESIAN_POINT('Ctrl Pts',(-164.098434771945,-4.33821396565373,
128.487232513488));
#115214=CARTESIAN_POINT('Ctrl Pts',(-164.106183511002,-4.40286276929815,
128.608270423451));
#115215=CARTESIAN_POINT('Ctrl Pts',(-164.113932250058,-4.46242495728391,
128.731983612716));
#115216=CARTESIAN_POINT('Ctrl Pts',(-164.121680989115,-4.51668902184401,
128.857901436783));
#115217=CARTESIAN_POINT('Ctrl Pts',(-164.12943661064,-4.57100128401486,
128.983931101685));
#115218=CARTESIAN_POINT('Ctrl Pts',(-164.137192232166,-4.62000587286779,
129.112168951298));
#115219=CARTESIAN_POINT('Ctrl Pts',(-164.144947853691,-4.66353981952929,
129.242125227439));
#115220=CARTESIAN_POINT('Ctrl Pts',(-164.151648602825,-4.70115254398312,
129.354405642619));
#115221=CARTESIAN_POINT('Ctrl Pts',(-164.158349351959,-4.73468233602094,
129.467968387655));
#115222=CARTESIAN_POINT('Ctrl Pts',(-164.165050101093,-4.76405452823413,
129.582490119309));
#115223=CARTESIAN_POINT('Ctrl Pts',(-162.415078182266,-4.764054528234,129.582490119308));
#115224=CARTESIAN_POINT('Ctrl Pts',(-162.422718977359,-4.7976930599468,
129.71364624392));
#115225=CARTESIAN_POINT('Ctrl Pts',(-162.430359772452,-4.82590149337616,
129.846154608971));
#115226=CARTESIAN_POINT('Ctrl Pts',(-162.438000567544,-4.8485894907432,
129.979519412997));
#115227=CARTESIAN_POINT('Ctrl Pts',(-162.445857233615,-4.87191847901874,
130.116652095938));
#115228=CARTESIAN_POINT('Ctrl Pts',(-162.453713899686,-4.88941039429629,
130.254689879039));
#115229=CARTESIAN_POINT('Ctrl Pts',(-162.461570565758,-4.90102415081955,
130.393087793782));
#115230=CARTESIAN_POINT('Ctrl Pts',(-162.469427231829,-4.91263790734284,
130.531485708525));
#115231=CARTESIAN_POINT('Ctrl Pts',(-162.4772838979,-4.9183735252126,130.670243293803));
#115232=CARTESIAN_POINT('Ctrl Pts',(-162.485140563971,-4.91824798157934,
130.808816421733));
#115233=CARTESIAN_POINT('',(-162.139859435949,-4.91824997172906,130.803833277931));
#115234=CARTESIAN_POINT('Ctrl Pts',(-162.070143404005,-4.764054528234,129.582490119308));
#115235=CARTESIAN_POINT('Ctrl Pts',(-162.07834908068,-4.80003844195155,
129.722790852761));
#115236=CARTESIAN_POINT('Ctrl Pts',(-162.086554757355,-4.8298596052829,
129.864835002293));
#115237=CARTESIAN_POINT('Ctrl Pts',(-162.09476043403,-4.85336043351166,
130.008071998456));
#115238=CARTESIAN_POINT('Ctrl Pts',(-162.102947684613,-4.87680848993161,
130.150987351684));
#115239=CARTESIAN_POINT('Ctrl Pts',(-162.111134935197,-4.89396446228111,
130.295089896159));
#115240=CARTESIAN_POINT('Ctrl Pts',(-162.119322185781,-4.90472132866419,
130.439817409364));
#115241=CARTESIAN_POINT('Ctrl Pts',(-162.126167935837,-4.91371565684435,
130.560830974476));
#115242=CARTESIAN_POINT('Ctrl Pts',(-162.133013685893,-4.91823693878644,
130.682281121578));
#115243=CARTESIAN_POINT('Ctrl Pts',(-162.139859435949,-4.91824997172906,
130.803833277932));
#115244=CARTESIAN_POINT('Ctrl Pts',(-162.139859435994,-4.91824997172915,
130.803833278737));
#115245=CARTESIAN_POINT('Ctrl Pts',(-162.147911968904,-4.9182653021222,
130.946812898396));
#115246=CARTESIAN_POINT('Ctrl Pts',(-162.155964501813,-4.91204141168342,
131.089693691258));
#115247=CARTESIAN_POINT('Ctrl Pts',(-162.164017034723,-4.89963008146219,
131.231921288501));
#115248=CARTESIAN_POINT('Ctrl Pts',(-162.172078033823,-4.88720570234165,
131.374298419563));
#115249=CARTESIAN_POINT('Ctrl Pts',(-162.180139032924,-4.86858093756128,
131.516020642525));
#115250=CARTESIAN_POINT('Ctrl Pts',(-162.188200032025,-4.84385908642783,
131.656541474738));
#115251=CARTESIAN_POINT('Ctrl Pts',(-162.196278020079,-4.81908513277144,
131.797358461549));
#115252=CARTESIAN_POINT('Ctrl Pts',(-162.204356008134,-4.78818846408692,
131.936968655778));
#115253=CARTESIAN_POINT('Ctrl Pts',(-162.212433996188,-4.75132331563071,
132.074836832552));
#115254=CARTESIAN_POINT('Ctrl Pts',(-162.220520646977,-4.71441863344631,
132.212852857449));
#115255=CARTESIAN_POINT('Ctrl Pts',(-162.228607297766,-4.67153280467116,
132.349122809565));
#115256=CARTESIAN_POINT('Ctrl Pts',(-162.236693948555,-4.62286908537536,
132.483129357441));
#115257=CARTESIAN_POINT('Ctrl Pts',(-162.244798880779,-4.5740953523452,
132.617438852994));
#115258=CARTESIAN_POINT('Ctrl Pts',(-162.252903813003,-4.51951774017395,
132.749474392978));
#115259=CARTESIAN_POINT('Ctrl Pts',(-162.261008745228,-4.45938731641086,
132.878739518523));
#115260=CARTESIAN_POINT('Ctrl Pts',(-162.268830176097,-4.40136018681003,
133.00348309629));
#115261=CARTESIAN_POINT('Ctrl Pts',(-162.276651606966,-4.33816233291167,
133.125646591769));
#115262=CARTESIAN_POINT('Ctrl Pts',(-162.284473037835,-4.27005784405416,
133.244809156448));
#115263=CARTESIAN_POINT('Ctrl Pts',(-162.292247371954,-4.20236344641148,
133.363254183683));
#115264=CARTESIAN_POINT('Ctrl Pts',(-162.300021706073,-4.12962985860404,
133.479068072561));
#115265=CARTESIAN_POINT('Ctrl Pts',(-162.307796040192,-4.05208682249319,
133.591792310985));
#115266=CARTESIAN_POINT('Ctrl Pts',(-162.315560793139,-3.97463935124413,
133.70437762686));
#115267=CARTESIAN_POINT('Ctrl Pts',(-162.323325546086,-3.89239444453671,
133.813880549487));
#115268=CARTESIAN_POINT('Ctrl Pts',(-162.331090299033,-3.80562759516828,
133.91986726487));
#115269=CARTESIAN_POINT('Ctrl Pts',(-162.338847339918,-3.71894692385783,
134.025748712753));
#115270=CARTESIAN_POINT('Ctrl Pts',(-162.346604380804,-3.62775349374845,
134.128120602758));
#115271=CARTESIAN_POINT('Ctrl Pts',(-162.354361421689,-3.53236573007361,
134.226578525809));
#115272=CARTESIAN_POINT('Ctrl Pts',(-162.362112612929,-3.43704989905323,
134.324962200975));
#115273=CARTESIAN_POINT('Ctrl Pts',(-162.369863804169,-3.33754630112714,
134.419437504412));
#115274=CARTESIAN_POINT('Ctrl Pts',(-162.377614995409,-3.23421298577117,
134.509633809271));
#115275=CARTESIAN_POINT('Ctrl Pts',(-162.385362892186,-3.13092358983087,
134.599791778295));
#115276=CARTESIAN_POINT('Ctrl Pts',(-162.393110788963,-3.02380800782137,
134.685674109416));
#115277=CARTESIAN_POINT('Ctrl Pts',(-162.40085868574,-2.91326026221623,
134.766947866712));
#115278=CARTESIAN_POINT('Ctrl Pts',(-162.408604961824,-2.80273564081633,
134.848204623289));
#115279=CARTESIAN_POINT('Ctrl Pts',(-162.416351237908,-2.6887805986295,
134.924854492082));
#115280=CARTESIAN_POINT('Ctrl Pts',(-162.424097513992,-2.57182095419476,
134.996605844418));
#115281=CARTESIAN_POINT('Ctrl Pts',(-162.431843847258,-2.45486044639033,
135.068357726407));
#115282=CARTESIAN_POINT('Ctrl Pts',(-162.439590180523,-2.3348956253339,
135.135210815344));
#115283=CARTESIAN_POINT('Ctrl Pts',(-162.447336513788,-2.21237955998207,
135.196917930234));
#115284=CARTESIAN_POINT('Ctrl Pts',(-162.455084581791,-2.08983605800738,
135.258638864004));
#115285=CARTESIAN_POINT('Ctrl Pts',(-162.462832649794,-1.96474052395948,
135.31521135474));
#115286=CARTESIAN_POINT('Ctrl Pts',(-162.470580717797,-1.83756841678319,
135.366435296497));
#115287=CARTESIAN_POINT('Ctrl Pts',(-162.478337020539,-1.71026114957786,
135.417713679668));
#115288=CARTESIAN_POINT('Ctrl Pts',(-162.486093323281,-1.58087326374077,
135.46363201215));
#115289=CARTESIAN_POINT('Ctrl Pts',(-162.493849626023,-1.4498984157629,
135.504039079596));
#115290=CARTESIAN_POINT('Ctrl Pts',(-162.501610068537,-1.3188536625651,
135.54446771351));
#115291=CARTESIAN_POINT('Ctrl Pts',(-162.509370511051,-1.18622063739033,
135.579379121673));
#115292=CARTESIAN_POINT('Ctrl Pts',(-162.517130953565,-1.05250479716914,
135.608672921573));
#115293=CARTESIAN_POINT('Ctrl Pts',(-162.524903853831,-0.918574304410121,
135.638013746482));
#115294=CARTESIAN_POINT('Ctrl Pts',(-162.532676754096,-0.783557908362372,
135.661718874874));
#115295=CARTESIAN_POINT('Ctrl Pts',(-162.540449654362,-0.647968716881717,
135.679739536629));
#115296=CARTESIAN_POINT('Ctrl Pts',(-162.547939990124,-0.517308534038841,
135.697105101938));
#115297=CARTESIAN_POINT('Ctrl Pts',(-162.555430325886,-0.386116784575783,
135.709192286401));
#115298=CARTESIAN_POINT('Ctrl Pts',(-162.562920661648,-0.254852093818049,
135.716003262626));
#115299=CARTESIAN_POINT('Ctrl Pts',(-162.570694995767,-0.118610462414162,
135.723072479086));
#115300=CARTESIAN_POINT('Ctrl Pts',(-162.578469329886,0.0181413231455887,
135.724479887591));
#115301=CARTESIAN_POINT('Ctrl Pts',(-162.586243664005,0.154893322560722,
135.720170939489));
#115302=CARTESIAN_POINT('Ctrl Pts',(-162.594008416952,0.291476787357712,
135.715867301781));
#115303=CARTESIAN_POINT('Ctrl Pts',(-162.601773169899,0.428060078465787,
135.705861336908));
#115304=CARTESIAN_POINT('Ctrl Pts',(-162.609537922847,0.564129305298895,
135.690150337704));
#115305=CARTESIAN_POINT('Ctrl Pts',(-162.617294963732,0.700063386258412,
135.674454942885));
#115306=CARTESIAN_POINT('Ctrl Pts',(-162.625052004617,0.835484033140381,
135.653065834522));
#115307=CARTESIAN_POINT('Ctrl Pts',(-162.632809045502,0.96987888851874,
135.626032319798));
#115308=CARTESIAN_POINT('Ctrl Pts',(-162.640560236742,1.10417239569067,
135.599019191258));
#115309=CARTESIAN_POINT('Ctrl Pts',(-162.648311427982,1.23744126934094,
135.56637020543));
#115310=CARTESIAN_POINT('Ctrl Pts',(-162.656062619222,1.36918015611753,
135.528186266613));
#115311=CARTESIAN_POINT('Ctrl Pts',(-162.663810515999,1.50086305035318,
135.490018556989));
#115312=CARTESIAN_POINT('Ctrl Pts',(-162.671558412776,1.63101687635918,
135.446320681937));
#115313=CARTESIAN_POINT('Ctrl Pts',(-162.679306309553,1.75914854694267,
135.397244183725));
#115314=CARTESIAN_POINT('Ctrl Pts',(-162.687052585637,1.88725341514287,
135.348177951258));
#115315=CARTESIAN_POINT('Ctrl Pts',(-162.694798861721,2.01333660440385,
135.293735473251));
#115316=CARTESIAN_POINT('Ctrl Pts',(-162.702545137805,2.13692259394351,
135.234117370481));
#115317=CARTESIAN_POINT('Ctrl Pts',(-162.710291471071,2.26050949576669,
135.174498827623));
#115318=CARTESIAN_POINT('Ctrl Pts',(-162.718037804336,2.38159880895178,
135.109704753637));
#115319=CARTESIAN_POINT('Ctrl Pts',(-162.725784137601,2.4997376782887,135.039982720899));
#115320=CARTESIAN_POINT('Ctrl Pts',(-162.733532205604,2.61790300400614,
134.970245074396));
#115321=CARTESIAN_POINT('Ctrl Pts',(-162.741280273607,2.73311623445955,
134.895577471814));
#115322=CARTESIAN_POINT('Ctrl Pts',(-162.74902834161,2.84495201767705,134.81627176808));
#115323=CARTESIAN_POINT('Ctrl Pts',(-162.756784644352,2.95690666129596,
134.736881777299));
#115324=CARTESIAN_POINT('Ctrl Pts',(-162.764540947094,3.06547636765766,
134.652844064813));
#115325=CARTESIAN_POINT('Ctrl Pts',(-162.772297249836,3.17026708245786,
134.564492222761));
#115326=CARTESIAN_POINT('Ctrl Pts',(-162.78005769235,3.27511372721801,134.47609322467));
#115327=CARTESIAN_POINT('Ctrl Pts',(-162.787818134864,3.37617707349728,
134.383375773098));
#115328=CARTESIAN_POINT('Ctrl Pts',(-162.795578577378,3.47309945482742,
134.286710864077));
#115329=CARTESIAN_POINT('Ctrl Pts',(-162.803351477644,3.57017742456843,
134.189890779963));
#115330=CARTESIAN_POINT('Ctrl Pts',(-162.811124377909,3.6631008804719,134.089110863031));
#115331=CARTESIAN_POINT('Ctrl Pts',(-162.818897278174,3.75155144352328,
133.98477644401));
#115332=CARTESIAN_POINT('Ctrl Pts',(-162.826387613937,3.83678660581494,
133.884234843923));
#115333=CARTESIAN_POINT('Ctrl Pts',(-162.833877949699,3.91786824155212,
133.780392928005));
#115334=CARTESIAN_POINT('Ctrl Pts',(-162.841368285461,3.99455028042045,
133.673637725078));
#115335=CARTESIAN_POINT('Ctrl Pts',(-162.84914261958,4.07413974209891,133.562834866186));
#115336=CARTESIAN_POINT('Ctrl Pts',(-162.856916953699,4.14924151517748,
133.448542454658));
#115337=CARTESIAN_POINT('Ctrl Pts',(-162.864691287818,4.21953407114073,
133.331160032831));
#115338=CARTESIAN_POINT('Ctrl Pts',(-162.872456040765,4.2897399978106,133.213922274349));
#115339=CARTESIAN_POINT('Ctrl Pts',(-162.880220793712,4.35514830125592,
133.093602414877));
#115340=CARTESIAN_POINT('Ctrl Pts',(-162.887985546659,4.41547893344559,
132.970631341829));
#115341=CARTESIAN_POINT('Ctrl Pts',(-162.895742587544,4.47574964440102,
132.847782405384));
#115342=CARTESIAN_POINT('Ctrl Pts',(-162.903499628429,4.53095254923703,
132.722287844322));
#115343=CARTESIAN_POINT('Ctrl Pts',(-162.911256669314,4.58085218977948,
132.594605371194));
#115344=CARTESIAN_POINT('Ctrl Pts',(-162.919007860554,4.6307142006149,132.467019184412));
#115345=CARTESIAN_POINT('Ctrl Pts',(-162.926759051794,4.67528076565155,
132.337248732303));
#115346=CARTESIAN_POINT('Ctrl Pts',(-162.934510243035,4.71436362270386,
132.205773724193));
#115347=CARTESIAN_POINT('Ctrl Pts',(-162.942258139812,4.75342986849929,
132.074354596469));
#115348=CARTESIAN_POINT('Ctrl Pts',(-162.950006036589,4.78701693077016,
131.941232727657));
#115349=CARTESIAN_POINT('Ctrl Pts',(-162.957753933366,4.81498578064584,
131.806904878274));
#115350=CARTESIAN_POINT('Ctrl Pts',(-162.96550020945,4.84294878004108,131.672605127381));
#115351=CARTESIAN_POINT('Ctrl Pts',(-162.973246485534,4.86529582495158,
131.5371002802));
#115352=CARTESIAN_POINT('Ctrl Pts',(-162.980992761618,4.88193867272042,
131.400898846263));
#115353=CARTESIAN_POINT('Ctrl Pts',(-162.988739094883,4.89858164334296,
131.264696406918));
#115354=CARTESIAN_POINT('Ctrl Pts',(-162.996485428149,4.90952028538173,
131.127797758634));
#115355=CARTESIAN_POINT('Ctrl Pts',(-163.004231761414,4.91471810918807,
130.990717720245));
#115356=CARTESIAN_POINT('Ctrl Pts',(-163.011979829417,4.91991709701101,
130.853606983731));
#115357=CARTESIAN_POINT('Ctrl Pts',(-163.01972789742,4.91937269356245,130.716315166889));
#115358=CARTESIAN_POINT('Ctrl Pts',(-163.027475965423,4.91310053152602,
130.579357885096));
#115359=CARTESIAN_POINT('Ctrl Pts',(-163.035232268164,4.90682170336112,
130.442255043474));
#115360=CARTESIAN_POINT('Ctrl Pts',(-163.042988570906,4.89480297402604,
130.305487838324));
#115361=CARTESIAN_POINT('Ctrl Pts',(-163.050744873648,4.8771120080582,130.169568113393));
#115362=CARTESIAN_POINT('Ctrl Pts',(-163.058505316162,4.8594115998891,130.033575844011));
#115363=CARTESIAN_POINT('Ctrl Pts',(-163.066265758677,4.83603298926077,
129.8984323412));
#115364=CARTESIAN_POINT('Ctrl Pts',(-163.074026201191,4.80709497817862,
129.764639052304));
#115365=CARTESIAN_POINT('Ctrl Pts',(-163.081799101456,4.7781105132321,129.630630986545));
#115366=CARTESIAN_POINT('Ctrl Pts',(-163.089572001722,4.74354891257918,
129.497977844576));
#115367=CARTESIAN_POINT('Ctrl Pts',(-163.097344901987,4.70357910080727,
129.36716657884));
#115368=CARTESIAN_POINT('Ctrl Pts',(-163.104835237749,4.66506229237082,
129.241110632107));
#115369=CARTESIAN_POINT('Ctrl Pts',(-163.112325573511,4.62152375219774,
129.116765263576));
#115370=CARTESIAN_POINT('Ctrl Pts',(-163.119815909273,4.57315609158251,
128.994546697705));
#115371=CARTESIAN_POINT('Ctrl Pts',(-163.127590243392,4.52295455641437,
128.867694177763));
#115372=CARTESIAN_POINT('Ctrl Pts',(-163.135364577511,4.46739145647812,
128.742731088901));
#115373=CARTESIAN_POINT('Ctrl Pts',(-163.143138911631,4.4066291440415,128.620143904558));
#115374=CARTESIAN_POINT('Ctrl Pts',(-163.150903664578,4.3459417157248,128.497707797964));
#115375=CARTESIAN_POINT('Ctrl Pts',(-163.158668417525,4.28006799601437,
128.377642116796));
#115376=CARTESIAN_POINT('Ctrl Pts',(-163.166433170472,4.20921912989351,
128.260415378564));
#115377=CARTESIAN_POINT('Ctrl Pts',(-163.174190211357,4.13844063186508,
128.143305071582));
#115378=CARTESIAN_POINT('Ctrl Pts',(-163.181947252242,4.06269702192301,
128.029028428687));
#115379=CARTESIAN_POINT('Ctrl Pts',(-163.189704293127,3.98224611570434,
127.918030952324));
#115380=CARTESIAN_POINT('Ctrl Pts',(-163.197455484367,3.90185587813976,
127.807117180021));
#115381=CARTESIAN_POINT('Ctrl Pts',(-163.205206675607,3.81676563849148,
127.69947796748));
#115382=CARTESIAN_POINT('Ctrl Pts',(-163.212957866847,3.72727722949177,
127.595530999619));
#115383=CARTESIAN_POINT('Ctrl Pts',(-163.220705763624,3.63782685545318,
127.491628211993));
#115384=CARTESIAN_POINT('Ctrl Pts',(-163.228453660401,3.54398228458119,
127.391414843494));
#115385=CARTESIAN_POINT('Ctrl Pts',(-163.236201557179,3.44608630706758,
127.295276374243));
#115386=CARTESIAN_POINT('Ctrl Pts',(-163.243947833263,3.34821080728209,
127.199158015087));
#115387=CARTESIAN_POINT('Ctrl Pts',(-163.251694109347,3.24628586528319,
127.107113133511));
#115388=CARTESIAN_POINT('Ctrl Pts',(-163.259440385431,3.14069160722997,
127.019490832385));
#115389=CARTESIAN_POINT('Ctrl Pts',(-163.267186718696,3.03509656970406,
126.931867884451));
#115390=CARTESIAN_POINT('Ctrl Pts',(-163.274933051962,2.92583246294526,
126.848667831773));
#115391=CARTESIAN_POINT('Ctrl Pts',(-163.282679385227,2.8133126950708,126.770199646279));
#115392=CARTESIAN_POINT('Ctrl Pts',(-163.29042745323,2.70076772917464,126.691713888379));
#115393=CARTESIAN_POINT('Ctrl Pts',(-163.298175521233,2.58496597199776,
126.617962329877));
#115394=CARTESIAN_POINT('Ctrl Pts',(-163.305923589236,2.46634967520674,
126.549210521258));
#115395=CARTESIAN_POINT('Ctrl Pts',(-163.313679891978,2.34760731160378,
126.480385642399));
#115396=CARTESIAN_POINT('Ctrl Pts',(-163.32143619472,2.2260447716833,126.416571324669));
#115397=CARTESIAN_POINT('Ctrl Pts',(-163.329192497461,2.10212925842015,
126.357987304022));
#115398=CARTESIAN_POINT('Ctrl Pts',(-163.336952939976,1.97814760771621,
126.29937201532));
#115399=CARTESIAN_POINT('Ctrl Pts',(-163.34471338249,1.85181084123913,126.245992738225));
#115400=CARTESIAN_POINT('Ctrl Pts',(-163.352473825004,1.72360505622879,
126.198020565785));
#115401=CARTESIAN_POINT('Ctrl Pts',(-163.36024672527,1.59519346391078,126.149971384155));
#115402=CARTESIAN_POINT('Ctrl Pts',(-163.368019625535,1.46490722927346,
126.107346774152));
#115403=CARTESIAN_POINT('Ctrl Pts',(-163.3757925258,1.33324734706282,126.070267824427));
#115404=CARTESIAN_POINT('Ctrl Pts',(-163.383282861563,1.2063736332007,126.03453678792));
#115405=CARTESIAN_POINT('Ctrl Pts',(-163.390773197325,1.07822470856052,
126.003955285848));
#115406=CARTESIAN_POINT('Ctrl Pts',(-163.398263533087,0.949254865675583,
125.978586248359));
#115407=CARTESIAN_POINT('Ctrl Pts',(-163.406037867206,0.815395091999074,
125.952255336104));
#115408=CARTESIAN_POINT('Ctrl Pts',(-163.413812201325,0.680226893481132,
125.931456543786));
#115409=CARTESIAN_POINT('Ctrl Pts',(-163.421586535444,0.544247309369959,
125.916316230621));
#115410=CARTESIAN_POINT('Ctrl Pts',(-163.429351288391,0.408435307944097,
125.901194576539));
#115411=CARTESIAN_POINT('Ctrl Pts',(-163.437116041338,0.271814295381725,
125.891717569133));
#115412=CARTESIAN_POINT('Ctrl Pts',(-163.444880794285,0.134892577755928,
125.887960811309));
#115413=CARTESIAN_POINT('Ctrl Pts',(-163.45263783517,-0.00189314729040985,
125.884207784749));
#115414=CARTESIAN_POINT('Ctrl Pts',(-163.460394876055,-0.138978594755176,
125.886163712117));
#115415=CARTESIAN_POINT('Ctrl Pts',(-163.46815191694,-0.275849595165583,
125.893852490768));
#115416=CARTESIAN_POINT('Ctrl Pts',(-163.475903108181,-0.412617380089693,
125.901535471252));
#115417=CARTESIAN_POINT('Ctrl Pts',(-163.483654299421,-0.549170651075375,
125.914942676137));
#115418=CARTESIAN_POINT('Ctrl Pts',(-163.491405490661,-0.684994850008131,
125.934045933897));
#115419=CARTESIAN_POINT('Ctrl Pts',(-163.499153387438,-0.820761320032926,
125.953141072263));
#115420=CARTESIAN_POINT('Ctrl Pts',(-163.506901284215,-0.955798947978522,
125.977927394033));
#115421=CARTESIAN_POINT('Ctrl Pts',(-163.514649180992,-1.08959813203073,
126.00832486153));
#115422=CARTESIAN_POINT('Ctrl Pts',(-163.522395457076,-1.22336932817801,
126.038715970533));
#115423=CARTESIAN_POINT('Ctrl Pts',(-163.53014173316,-1.35590221469952,
126.074715804088));
#115424=CARTESIAN_POINT('Ctrl Pts',(-163.537888009244,-1.48669761399013,
126.116193249921));
#115425=CARTESIAN_POINT('Ctrl Pts',(-163.54563434251,-1.61749397878356,
126.157671001931));
#115426=CARTESIAN_POINT('Ctrl Pts',(-163.553380675775,-1.74655245807792,
126.204626328721));
#115427=CARTESIAN_POINT('Ctrl Pts',(-163.56112700904,-1.87338964785375,
126.256878425208));
#115428=CARTESIAN_POINT('Ctrl Pts',(-163.568875077043,-2.00025524193726,
126.309142223189));
#115429=CARTESIAN_POINT('Ctrl Pts',(-163.576623145046,-2.12489819522684,
126.366705002326));
#115430=CARTESIAN_POINT('Ctrl Pts',(-163.584371213049,-2.24685604474934,
126.429338220289));
#115431=CARTESIAN_POINT('Ctrl Pts',(-163.592127515791,-2.36894351252647,
126.492038005583));
#115432=CARTESIAN_POINT('Ctrl Pts',(-163.599883818533,-2.4883398275059,
126.559818815763));
#115433=CARTESIAN_POINT('Ctrl Pts',(-163.607640121275,-2.60460758498512,
126.632406352388));
#115434=CARTESIAN_POINT('Ctrl Pts',(-163.615400563789,-2.72093739806726,
126.705032631166));
#115435=CARTESIAN_POINT('Ctrl Pts',(-163.623161006303,-2.83413500389475,
126.782470527716));
#115436=CARTESIAN_POINT('Ctrl Pts',(-163.630921448817,-2.9437937096095,
126.864403554632));
#115437=CARTESIAN_POINT('Ctrl Pts',(-163.638694349083,-3.05362844921401,
126.946468107717));
#115438=CARTESIAN_POINT('Ctrl Pts',(-163.646467249348,-3.15991263304063,
127.033041963945));
#115439=CARTESIAN_POINT('Ctrl Pts',(-163.654240149614,-3.26227358588143,
127.123769073621));
#115440=CARTESIAN_POINT('Ctrl Pts',(-163.661730485376,-3.36091346025397,
127.211198024331));
#115441=CARTESIAN_POINT('Ctrl Pts',(-163.669220821137,-3.45591016803856,
127.302483295131));
#115442=CARTESIAN_POINT('Ctrl Pts',(-163.676711156899,-3.5469652081078,
127.397276692129));
#115443=CARTESIAN_POINT('Ctrl Pts',(-163.684385792604,-3.64026066025408,
127.494402483591));
#115444=CARTESIAN_POINT('Ctrl Pts',(-163.69206042831,-3.72973008599226,
127.595536548972));
#115445=CARTESIAN_POINT('Ctrl Pts',(-163.699735064015,-3.81500258888229,
127.70034091574));
#115446=CARTESIAN_POINT('Ctrl Pts',(-163.707400651281,-3.9001745550129,
127.805021717572));
#115447=CARTESIAN_POINT('Ctrl Pts',(-163.715066238548,-3.98115918533349,
127.913363909036));
#115448=CARTESIAN_POINT('Ctrl Pts',(-163.722731825814,-4.05762167876876,
128.024992096753));
#115449=CARTESIAN_POINT('Ctrl Pts',(-163.730390138672,-4.13401161163089,
128.136514352726));
#115450=CARTESIAN_POINT('Ctrl Pts',(-163.73804845153,-4.20588771635221,
128.251316074298));
#115451=CARTESIAN_POINT('Ctrl Pts',(-163.745706764389,-4.27295518551259,
128.368988562807));
#115452=CARTESIAN_POINT('Ctrl Pts',(-163.753359100149,-4.33997031039783,
128.486569211245));
#115453=CARTESIAN_POINT('Ctrl Pts',(-163.761011435909,-4.40218407095881,
128.607015819636));
#115454=CARTESIAN_POINT('Ctrl Pts',(-163.768663771669,-4.45934511343825,
128.72989099336));
#115455=CARTESIAN_POINT('Ctrl Pts',(-163.776312712522,-4.51648079681339,
128.852711654356));
#115456=CARTESIAN_POINT('Ctrl Pts',(-163.783961653376,-4.5685680526837,
128.977958373579));
#115457=CARTESIAN_POINT('Ctrl Pts',(-163.79161059423,-4.61540178522491,
129.105169803254));
#115458=CARTESIAN_POINT('Ctrl Pts',(-163.799258355588,-4.66222829582559,
129.23236161644));
#115459=CARTESIAN_POINT('Ctrl Pts',(-163.806906116946,-4.70380275481576,
129.361517161017));
#115460=CARTESIAN_POINT('Ctrl Pts',(-163.814553878304,-4.73996863624117,
129.492156216586));
#115461=CARTESIAN_POINT('Ctrl Pts',(-163.816312158077,-4.74828345345535,
129.522191150764));
#115462=CARTESIAN_POINT('Ctrl Pts',(-163.81807043785,-4.756312593584,129.552304433608));
#115463=CARTESIAN_POINT('Ctrl Pts',(-163.819828717624,-4.76405452823398,
129.582490119308));
#115464=CARTESIAN_POINT('Origin',(213.235140564004,0.,130.804360617566));
#115465=CARTESIAN_POINT('',(-165.915373126199,-4.76405452823409,129.582490119308));
#115466=CARTESIAN_POINT('',(-165.569765327751,-4.76405452823417,129.582490119309));
#115467=CARTESIAN_POINT('',(213.235140564004,-4.76405452823405,129.582490119308));
#115468=CARTESIAN_POINT('',(-164.235140564046,-4.91824950131384,130.802145820462));
#115469=CARTESIAN_POINT('Ctrl Pts',(-164.235140564046,-4.91824950131383,
130.802145820462));
#115470=CARTESIAN_POINT('Ctrl Pts',(-164.242830418784,-4.91831032367823,
130.937209914078));
#115471=CARTESIAN_POINT('Ctrl Pts',(-164.250520273522,-4.91280328631858,
131.072501252631));
#115472=CARTESIAN_POINT('Ctrl Pts',(-164.25821012826,-4.90169851106774,
131.207516628431));
#115473=CARTESIAN_POINT('Ctrl Pts',(-164.265891010091,-4.89060669342265,
131.342374461554));
#115474=CARTESIAN_POINT('Ctrl Pts',(-164.273571891923,-4.87393016165421,
131.476956577464));
#115475=CARTESIAN_POINT('Ctrl Pts',(-164.281252773754,-4.85169102683561,
131.610758312641));
#115476=CARTESIAN_POINT('Ctrl Pts',(-164.288926625913,-4.82947224564739,
131.744437590219));
#115477=CARTESIAN_POINT('Ctrl Pts',(-164.296600478073,-4.8017010543568,
131.877337515657));
#115478=CARTESIAN_POINT('Ctrl Pts',(-164.304274330232,-4.76845144967642,
132.008957576959));
#115479=CARTESIAN_POINT('Ctrl Pts',(-164.31211560948,-4.73447640953122,
132.143449307301));
#115480=CARTESIAN_POINT('Ctrl Pts',(-164.319956888727,-4.69478115867656,
132.276604255187));
#115481=CARTESIAN_POINT('Ctrl Pts',(-164.327798167975,-4.64950010821961,
132.407897896885));
#115482=CARTESIAN_POINT('Ctrl Pts',(-164.335464631022,-4.60522856921845,
132.536264432563));
#115483=CARTESIAN_POINT('Ctrl Pts',(-164.343131094069,-4.55561782055014,
132.662851388063));
#115484=CARTESIAN_POINT('Ctrl Pts',(-164.350797557115,-4.50084403328383,
132.787183365709));
#115485=CARTESIAN_POINT('Ctrl Pts',(-164.358463256884,-4.44607569932835,
132.911502964789));
#115486=CARTESIAN_POINT('Ctrl Pts',(-164.366128956653,-4.38614551016219,
133.033567666439));
#115487=CARTESIAN_POINT('Ctrl Pts',(-164.373794656422,-4.32127757200678,
133.152922562283));
#115488=CARTESIAN_POINT('Ctrl Pts',(-164.381461337856,-4.25640132690476,
133.272292742637));
#115489=CARTESIAN_POINT('Ctrl Pts',(-164.389128019289,-4.18658626648107,
133.388952075709));
#115490=CARTESIAN_POINT('Ctrl Pts',(-164.396794700723,-4.11210193200325,
133.502471208946));
#115491=CARTESIAN_POINT('Ctrl Pts',(-164.404767228344,-4.03464620110701,
133.620518950087));
#115492=CARTESIAN_POINT('Ctrl Pts',(-164.412739755965,-3.95214119226765,
133.7351703593));
#115493=CARTESIAN_POINT('Ctrl Pts',(-164.420712283587,-3.86493818351943,
133.845977934073));
#115494=CARTESIAN_POINT('Ctrl Pts',(-164.428390330897,-3.7809561820072,
133.952692622542));
#115495=CARTESIAN_POINT('Ctrl Pts',(-164.436068378207,-3.69261737648841,
134.055842119024));
#115496=CARTESIAN_POINT('Ctrl Pts',(-164.443746425517,-3.60027453263862,
134.155062984553));
#115497=CARTESIAN_POINT('Ctrl Pts',(-164.451429694675,-3.50786888632366,
134.254351330298));
#115498=CARTESIAN_POINT('Ctrl Pts',(-164.459112963834,-3.41145406407904,
134.34970544625));
#115499=CARTESIAN_POINT('Ctrl Pts',(-164.466796232992,-3.31141737594062,
134.440800913352));
#115500=CARTESIAN_POINT('Ctrl Pts',(-164.474489977799,-3.21124429413058,
134.532020583339));
#115501=CARTESIAN_POINT('Ctrl Pts',(-164.482183722607,-3.10743979991024,
134.618969766111));
#115502=CARTESIAN_POINT('Ctrl Pts',(-164.489877467415,-3.00042183492989,
134.701366118585));
#115503=CARTESIAN_POINT('Ctrl Pts',(-164.490739989003,-2.98842438668954,
134.710603315108));
#115504=CARTESIAN_POINT('Ctrl Pts',(-164.491602510591,-2.9763865785575,
134.719783338642));
#115505=CARTESIAN_POINT('Ctrl Pts',(-164.492465032179,-2.96430901914137,
134.728905827082));
#115506=CARTESIAN_POINT('Ctrl Pts',(-164.500239366298,-2.85544799636351,
134.811131332058));
#115507=CARTESIAN_POINT('Ctrl Pts',(-164.508013700417,-2.74299073370207,
134.888954180419));
#115508=CARTESIAN_POINT('Ctrl Pts',(-164.515788034536,-2.62732894263834,
134.962043348328));
#115509=CARTESIAN_POINT('Ctrl Pts',(-164.523552787484,-2.5118096943948,
135.035042440369));
#115510=CARTESIAN_POINT('Ctrl Pts',(-164.531317540431,-2.39309410300142,
135.103319252709));
#115511=CARTESIAN_POINT('Ctrl Pts',(-164.539082293378,-2.27160621140658,
135.166583477852));
#115512=CARTESIAN_POINT('Ctrl Pts',(-164.546839334263,-2.15023898329835,
135.229784868075));
#115513=CARTESIAN_POINT('Ctrl Pts',(-164.554596375148,-2.0261052790745,
135.287983399277));
#115514=CARTESIAN_POINT('Ctrl Pts',(-164.562353416033,-1.89965702912835,
135.340932697252));
#115515=CARTESIAN_POINT('Ctrl Pts',(-164.570104607273,-1.77330413479162,
135.393842065749));
#115516=CARTESIAN_POINT('Ctrl Pts',(-164.577855798513,-1.64464052804457,
135.44150992975));
#115517=CARTESIAN_POINT('Ctrl Pts',(-164.585606989753,-1.51414126229552,
135.483736569583));
#115518=CARTESIAN_POINT('Ctrl Pts',(-164.59335488653,-1.38369746221506,
135.525945261968));
#115519=CARTESIAN_POINT('Ctrl Pts',(-164.601102783307,-1.25141992609663,
135.562717209789));
#115520=CARTESIAN_POINT('Ctrl Pts',(-164.608850680084,-1.1178019350934,
135.59390150333));
#115521=CARTESIAN_POINT('Ctrl Pts',(-164.616596956168,-0.984211894093428,
135.625079273788));
#115522=CARTESIAN_POINT('Ctrl Pts',(-164.624343232252,-0.849282336420786,
135.650671626007));
#115523=CARTESIAN_POINT('Ctrl Pts',(-164.632089508336,-0.713519507588329,
135.670578139912));
#115524=CARTESIAN_POINT('Ctrl Pts',(-164.639835841602,-0.577755676586065,
135.690484800763));
#115525=CARTESIAN_POINT('Ctrl Pts',(-164.647582174867,-0.441158948979083,
135.704705482831));
#115526=CARTESIAN_POINT('Ctrl Pts',(-164.655328508132,-0.304243119693164,
135.713191352743));
#115527=CARTESIAN_POINT('Ctrl Pts',(-164.663076576135,-0.167296629056397,
135.721679123007));
#115528=CARTESIAN_POINT('Ctrl Pts',(-164.670824644138,-0.0300312846841078,
135.724429501382));
#115529=CARTESIAN_POINT('Ctrl Pts',(-164.678572712141,0.107037071390386,
135.721445742703));
#115530=CARTESIAN_POINT('Ctrl Pts',(-164.686329014883,0.244251105345036,
135.718458812851));
#115531=CARTESIAN_POINT('Ctrl Pts',(-164.694085317625,0.381267341283862,
135.709725580428));
#115532=CARTESIAN_POINT('Ctrl Pts',(-164.701841620367,0.517572459097017,
135.695301407648));
#115533=CARTESIAN_POINT('Ctrl Pts',(-164.709602062881,0.653950327055988,
135.680869536252));
#115534=CARTESIAN_POINT('Ctrl Pts',(-164.717362505395,0.789615934071009,
135.660740729522));
#115535=CARTESIAN_POINT('Ctrl Pts',(-164.725122947909,0.924065126279789,
135.635021721897));
#115536=CARTESIAN_POINT('Ctrl Pts',(-164.732895848174,1.05873014826737,
135.609261427837));
#115537=CARTESIAN_POINT('Ctrl Pts',(-164.74066874844,1.19217447252728,135.577893089714));
#115538=CARTESIAN_POINT('Ctrl Pts',(-164.748441648705,1.32390723312391,
135.541073897952));
#115539=CARTESIAN_POINT('Ctrl Pts',(-164.755931984467,1.45085117605698,
135.505593176552));
#115540=CARTESIAN_POINT('Ctrl Pts',(-164.763422320229,1.57620554110669,
135.465051120391));
#115541=CARTESIAN_POINT('Ctrl Pts',(-164.770912655991,1.69954960153836,
135.419630297055));
#115542=CARTESIAN_POINT('Ctrl Pts',(-164.77868699011,1.82757028951183,135.372487329397));
#115543=CARTESIAN_POINT('Ctrl Pts',(-164.786461324229,1.95383075328559,
135.319938999833));
#115544=CARTESIAN_POINT('Ctrl Pts',(-164.794235658348,2.07784076350627,
135.262135939855));
#115545=CARTESIAN_POINT('Ctrl Pts',(-164.802000411295,2.20169794247211,
135.204404116984));
#115546=CARTESIAN_POINT('Ctrl Pts',(-164.809765164243,2.32330983533017,
135.141430612568));
#115547=CARTESIAN_POINT('Ctrl Pts',(-164.81752991719,2.44220299259232,135.073415267658));
#115548=CARTESIAN_POINT('Ctrl Pts',(-164.825286958075,2.56097806349458,
135.005467476548));
#115549=CARTESIAN_POINT('Ctrl Pts',(-164.83304399896,2.67703943533007,134.932488003229));
#115550=CARTESIAN_POINT('Ctrl Pts',(-164.840801039845,2.789935547084,134.854723898263));
#115551=CARTESIAN_POINT('Ctrl Pts',(-164.848552231085,2.90274652300201,
134.777018435813));
#115552=CARTESIAN_POINT('Ctrl Pts',(-164.856303422325,3.01239666924048,
134.694535744359));
#115553=CARTESIAN_POINT('Ctrl Pts',(-164.864054613565,3.11846117801212,
134.607567546426));
#115554=CARTESIAN_POINT('Ctrl Pts',(-164.871802510342,3.2244806065383,134.520636312297));
#115555=CARTESIAN_POINT('Ctrl Pts',(-164.879550407119,3.32691712700626,
134.429223610869));
#115556=CARTESIAN_POINT('Ctrl Pts',(-164.887298303896,3.42537714428523,
134.333662883157));
#115557=CARTESIAN_POINT('Ctrl Pts',(-164.89504457998,3.52381656585087,134.23812214469));
#115558=CARTESIAN_POINT('Ctrl Pts',(-164.902790856064,3.61828085834464,
134.138435377919));
#115559=CARTESIAN_POINT('Ctrl Pts',(-164.910537132148,3.70841189745059,
134.03497422203));
#115560=CARTESIAN_POINT('Ctrl Pts',(-164.918283465414,3.79854360188352,
133.931512302413));
#115561=CARTESIAN_POINT('Ctrl Pts',(-164.926029798679,3.88434173229034,
133.824276232875));
#115562=CARTESIAN_POINT('Ctrl Pts',(-164.933776131944,3.96548748506379,
133.713671888005));
#115563=CARTESIAN_POINT('Ctrl Pts',(-164.941524199947,4.04665140986583,
133.603042774059));
#115564=CARTESIAN_POINT('Ctrl Pts',(-164.94927226795,4.1231606526135,133.489044198976));
#115565=CARTESIAN_POINT('Ctrl Pts',(-164.957020335953,4.19473912647206,
133.372111914585));
#115566=CARTESIAN_POINT('Ctrl Pts',(-164.964776638695,4.26639367478452,
133.255055353171));
#115567=CARTESIAN_POINT('Ctrl Pts',(-164.972532941437,4.33310678134179,
133.135059187929));
#115568=CARTESIAN_POINT('Ctrl Pts',(-164.980289244179,4.39464756188375,
133.012585214234));
#115569=CARTESIAN_POINT('Ctrl Pts',(-164.988049686693,4.45622118859342,
132.890045872491));
#115570=CARTESIAN_POINT('Ctrl Pts',(-164.995810129207,4.51261682782236,
132.765026443349));
#115571=CARTESIAN_POINT('Ctrl Pts',(-165.003570571721,4.56365177080036,
132.638008778302));
#115572=CARTESIAN_POINT('Ctrl Pts',(-165.011343471987,4.61476863959937,
132.510787213223));
#115573=CARTESIAN_POINT('Ctrl Pts',(-165.019116372252,4.66050748516016,
132.381561370914));
#115574=CARTESIAN_POINT('Ctrl Pts',(-165.026889272517,4.70073523121121,
132.250829196053));
#115575=CARTESIAN_POINT('Ctrl Pts',(-165.03437960828,4.7395005973667,132.124849465039));
#115576=CARTESIAN_POINT('Ctrl Pts',(-165.041869944042,4.77314851356853,
131.997471315848));
#115577=CARTESIAN_POINT('Ctrl Pts',(-165.049360279804,4.80160516602204,
131.86914740004));
#115578=CARTESIAN_POINT('Ctrl Pts',(-165.057134613923,4.83114076110182,
131.735958043963));
#115579=CARTESIAN_POINT('Ctrl Pts',(-165.064908948042,4.8551772279464,131.601327884214));
#115580=CARTESIAN_POINT('Ctrl Pts',(-165.072683282161,4.87357631615702,
131.465750784633));
#115581=CARTESIAN_POINT('Ctrl Pts',(-165.080448035108,4.89195272913579,
131.330340771711));
#115582=CARTESIAN_POINT('Ctrl Pts',(-165.088212788056,4.90470553499386,
131.193986524671));
#115583=CARTESIAN_POINT('Ctrl Pts',(-165.095977541003,4.91174695465368,
131.057194388946));
#115584=CARTESIAN_POINT('Ctrl Pts',(-165.103734581888,4.91878138067624,
130.920538117098));
#115585=CARTESIAN_POINT('Ctrl Pts',(-165.111491622773,4.92011568932038,
130.783445209992));
#115586=CARTESIAN_POINT('Ctrl Pts',(-165.119248663658,4.91571365146245,
130.64642911556));
#115587=CARTESIAN_POINT('Ctrl Pts',(-165.126999854898,4.91131493321552,
130.509516346032));
#115588=CARTESIAN_POINT('Ctrl Pts',(-165.134751046138,4.90118849125952,
130.372680663065));
#115589=CARTESIAN_POINT('Ctrl Pts',(-165.142502237378,4.8853501410317,130.236437152633));
#115590=CARTESIAN_POINT('Ctrl Pts',(-165.150250134155,4.86951852252524,
130.100251549327));
#115591=CARTESIAN_POINT('Ctrl Pts',(-165.157998030932,4.84797986933509,
129.964658005503));
#115592=CARTESIAN_POINT('Ctrl Pts',(-165.165745927709,4.82080196704985,
129.830167896905));
#115593=CARTESIAN_POINT('Ctrl Pts',(-165.173492203793,4.79362974979589,
129.695705920739));
#115594=CARTESIAN_POINT('Ctrl Pts',(-165.181238479878,4.76082070714668,
129.562347303671));
#115595=CARTESIAN_POINT('Ctrl Pts',(-165.188984755962,4.72249393473421,
129.43059422589));
#115596=CARTESIAN_POINT('Ctrl Pts',(-165.196731089227,4.68416687940215,
129.298840175537));
#115597=CARTESIAN_POINT('Ctrl Pts',(-165.204477422492,4.64032212223626,
129.168692063524));
#115598=CARTESIAN_POINT('Ctrl Pts',(-165.212223755758,4.59112881588843,
129.040637493485));
#115599=CARTESIAN_POINT('Ctrl Pts',(-165.219971823761,4.54192449304066,
128.912554246512));
#115600=CARTESIAN_POINT('Ctrl Pts',(-165.227719891764,4.48736937776267,
128.786565839331));
#115601=CARTESIAN_POINT('Ctrl Pts',(-165.235467959767,4.42768084873182,
128.663140086123));
#115602=CARTESIAN_POINT('Ctrl Pts',(-165.243224262508,4.36792888202211,
128.539583154555));
#115603=CARTESIAN_POINT('Ctrl Pts',(-165.25098056525,4.30303277338795,128.418594670212));
#115604=CARTESIAN_POINT('Ctrl Pts',(-165.258736867992,4.23325624577473,
128.300618494242));
#115605=CARTESIAN_POINT('Ctrl Pts',(-165.266497310506,4.1634424763278,128.182579350833));
#115606=CARTESIAN_POINT('Ctrl Pts',(-165.27425775302,4.08874331039939,128.067556047122));
#115607=CARTESIAN_POINT('Ctrl Pts',(-165.282018195535,4.00946538474539,
127.955962753673));
#115608=CARTESIAN_POINT('Ctrl Pts',(-165.2897910958,3.93006019512716,127.844190320763));
#115609=CARTESIAN_POINT('Ctrl Pts',(-165.297563996066,3.84606179738503,
127.735859210317));
#115610=CARTESIAN_POINT('Ctrl Pts',(-165.305336896331,3.75781719550393,
127.631350534431));
#115611=CARTESIAN_POINT('Ctrl Pts',(-165.312827232093,3.67278050717643,
127.530641012156));
#115612=CARTESIAN_POINT('Ctrl Pts',(-165.320317567855,3.58380118333138,
127.433481066278));
#115613=CARTESIAN_POINT('Ctrl Pts',(-165.327807903617,3.49122015438542,
127.340177467657));
#115614=CARTESIAN_POINT('Ctrl Pts',(-165.335582237736,3.39512888758716,
127.243336234735));
#115615=CARTESIAN_POINT('Ctrl Pts',(-165.343356571855,3.294853018719,127.150342784561));
#115616=CARTESIAN_POINT('Ctrl Pts',(-165.351130905974,3.19073332169938,
127.061580376582));
#115617=CARTESIAN_POINT('Ctrl Pts',(-165.358895658921,3.0867419429006,126.972927360338));
#115618=CARTESIAN_POINT('Ctrl Pts',(-165.366660411868,2.97891645618367,
126.888495262429));
#115619=CARTESIAN_POINT('Ctrl Pts',(-165.374425164816,2.86763541756558,
126.808631625952));
#115620=CARTESIAN_POINT('Ctrl Pts',(-165.382182205701,2.75646490484384,
126.728847311165));
#115621=CARTESIAN_POINT('Ctrl Pts',(-165.389939246586,2.64184598583662,
126.653622654542));
#115622=CARTESIAN_POINT('Ctrl Pts',(-165.397696287471,2.52419105610616,
126.58326566782));
#115623=CARTESIAN_POINT('Ctrl Pts',(-165.405447478711,2.40662485087423,
126.512961737849));
#115624=CARTESIAN_POINT('Ctrl Pts',(-165.413198669951,2.28602752617753,
126.447518371222));
#115625=CARTESIAN_POINT('Ctrl Pts',(-165.420949861191,2.16284098706366,
126.387200678513));
#115626=CARTESIAN_POINT('Ctrl Pts',(-165.428697757968,2.03970680551417,
126.326908622432));
#115627=CARTESIAN_POINT('Ctrl Pts',(-165.436445654745,1.91398594872568,
126.271738078873));
#115628=CARTESIAN_POINT('Ctrl Pts',(-165.444193551522,1.78614529136175,
126.221908428983));
#115629=CARTESIAN_POINT('Ctrl Pts',(-165.451939827606,1.65833137550742,
126.172089202382));
#115630=CARTESIAN_POINT('Ctrl Pts',(-165.459686103691,1.52839890509849,
126.127608789172));
#115631=CARTESIAN_POINT('Ctrl Pts',(-165.467432379775,1.39683475264722,
126.088638431485));
#115632=CARTESIAN_POINT('Ctrl Pts',(-165.47517871304,1.26526962901908,126.049667786127));
#115633=CARTESIAN_POINT('Ctrl Pts',(-165.482925046305,1.13207317417998,
126.016207388491));
#115634=CARTESIAN_POINT('Ctrl Pts',(-165.490671379571,0.997747054017446,
125.988378487336));
#115635=CARTESIAN_POINT('Ctrl Pts',(-165.498419447574,0.863390852452566,
125.960543354091));
#115636=CARTESIAN_POINT('Ctrl Pts',(-165.506167515577,0.72790486492431,
125.938342306136));
#115637=CARTESIAN_POINT('Ctrl Pts',(-165.51391558358,0.591800175237199,
125.921845321626));
#115638=CARTESIAN_POINT('Ctrl Pts',(-165.521671886321,0.455550831865665,
125.905330803924));
#115639=CARTESIAN_POINT('Ctrl Pts',(-165.529428189063,0.318681861523744,
125.894532506976));
#115640=CARTESIAN_POINT('Ctrl Pts',(-165.537184491805,0.181709245859055,
125.889468470991));
#115641=CARTESIAN_POINT('Ctrl Pts',(-165.544944934319,0.0446635237848468,
125.884401732176));
#115642=CARTESIAN_POINT('Ctrl Pts',(-165.552705376834,-0.0924855630699909,
125.885075350806));
#115643=CARTESIAN_POINT('Ctrl Pts',(-165.560465819348,-0.229223816622113,
125.891455213999));
#115644=CARTESIAN_POINT('Ctrl Pts',(-165.568238719613,-0.366181574557515,
125.897845318716));
#115645=CARTESIAN_POINT('Ctrl Pts',(-165.576011619879,-0.5027267916273,
125.909959938364));
#115646=CARTESIAN_POINT('Ctrl Pts',(-165.583784520144,-0.638351263300149,
125.927713129061));
#115647=CARTESIAN_POINT('Ctrl Pts',(-165.591274855906,-0.769045443809156,
125.944820946559));
#115648=CARTESIAN_POINT('Ctrl Pts',(-165.598765191668,-0.898884355967715,
125.967164447724));
#115649=CARTESIAN_POINT('Ctrl Pts',(-165.60625552743,-1.02742562354542,
125.994622615285));
#115650=CARTESIAN_POINT('Ctrl Pts',(-165.614029861549,-1.16084057235355,
126.023121867616));
#115651=CARTESIAN_POINT('Ctrl Pts',(-165.621804195668,-1.2932801521932,
126.057221564745));
#115652=CARTESIAN_POINT('Ctrl Pts',(-165.629578529787,-1.42423771941209,
126.096842165015));
#115653=CARTESIAN_POINT('Ctrl Pts',(-165.637343282734,-1.55503389313304,
126.136413936437));
#115654=CARTESIAN_POINT('Ctrl Pts',(-165.645108035681,-1.68435131769941,
126.1814929609));
#115655=CARTESIAN_POINT('Ctrl Pts',(-165.652872788628,-1.81169297648574,
126.231948604038));
#115656=CARTESIAN_POINT('Ctrl Pts',(-165.660629829513,-1.93890815774136,
126.282354133921));
#115657=CARTESIAN_POINT('Ctrl Pts',(-165.668386870398,-2.06415111727719,
126.338125512288));
#115658=CARTESIAN_POINT('Ctrl Pts',(-165.676143911283,-2.18693980622018,
126.399082266943));
#115659=CARTESIAN_POINT('Ctrl Pts',(-165.683895102523,-2.30963589925718,
126.459993053634));
#115660=CARTESIAN_POINT('Ctrl Pts',(-165.691646293764,-2.42988105680503,
126.52608126019));
#115661=CARTESIAN_POINT('Ctrl Pts',(-165.699397485004,-2.54721337335625,
126.597118398119));
#115662=CARTESIAN_POINT('Ctrl Pts',(-165.707145381781,-2.6644958205438,
126.668125343371));
#115663=CARTESIAN_POINT('Ctrl Pts',(-165.714893278558,-2.77886755534712,
126.744076834378));
#115664=CARTESIAN_POINT('Ctrl Pts',(-165.722641175335,-2.8898916490354,
126.824698657131));
#115665=CARTESIAN_POINT('Ctrl Pts',(-165.730387451419,-3.00089251887698,
126.905303615537));
#115666=CARTESIAN_POINT('Ctrl Pts',(-165.738133727503,-3.10854682429395,
126.990576732936));
#115667=CARTESIAN_POINT('Ctrl Pts',(-165.745880003587,-3.2124473279475,
127.08020095025));
#115668=CARTESIAN_POINT('Ctrl Pts',(-165.753626336853,-3.31634859857054,
127.169825829149));
#115669=CARTESIAN_POINT('Ctrl Pts',(-165.761372670118,-3.41649571609377,
127.263801616686));
#115670=CARTESIAN_POINT('Ctrl Pts',(-165.769119003383,-3.51251550783692,
127.361771785059));
#115671=CARTESIAN_POINT('Ctrl Pts',(-165.776867071386,-3.60855680254629,
127.45976389317));
#115672=CARTESIAN_POINT('Ctrl Pts',(-165.784615139389,-3.70046865864504,
127.56175188293));
#115673=CARTESIAN_POINT('Ctrl Pts',(-165.792363207392,-3.78791594825001,
127.667343589959));
#115674=CARTESIAN_POINT('Ctrl Pts',(-165.800119510134,-3.87545617787537,
127.773047521112));
#115675=CARTESIAN_POINT('Ctrl Pts',(-165.807875812876,-3.95852211260176,
127.882362518928));
#115676=CARTESIAN_POINT('Ctrl Pts',(-165.815632115618,-4.03681967400637,
127.994864224606));
#115677=CARTESIAN_POINT('Ctrl Pts',(-165.823392558132,-4.11515902517722,
128.107425975832));
#115678=CARTESIAN_POINT('Ctrl Pts',(-165.831153000646,-4.18872472224408,
128.22317749419));
#115679=CARTESIAN_POINT('Ctrl Pts',(-165.83891344316,-4.25726752871479,
128.341667731425));
#115680=CARTESIAN_POINT('Ctrl Pts',(-165.846686343426,-4.32592036618321,
128.460348179707));
#115681=CARTESIAN_POINT('Ctrl Pts',(-165.854459243691,-4.38953401869827,
128.581775785825));
#115682=CARTESIAN_POINT('Ctrl Pts',(-165.862232143956,-4.44790609631937,
128.705476528145));
#115683=CARTESIAN_POINT('Ctrl Pts',(-165.869722479719,-4.50415620189013,
128.824680436902));
#115684=CARTESIAN_POINT('Ctrl Pts',(-165.877212815481,-4.55553908507402,
128.945994799085));
#115685=CARTESIAN_POINT('Ctrl Pts',(-165.884703151243,-4.60191744597129,
129.06898201825));
#115686=CARTESIAN_POINT('Ctrl Pts',(-165.893625769841,-4.65716415835103,
129.215486538723));
#115687=CARTESIAN_POINT('Ctrl Pts',(-165.902548388439,-4.70545568793346,
129.364749909709));
#115688=CARTESIAN_POINT('Ctrl Pts',(-165.911471007037,-4.74654472126346,
129.516146244278));
#115689=CARTESIAN_POINT('Ctrl Pts',(-165.912771713424,-4.75253452879746,
129.538216242813));
#115690=CARTESIAN_POINT('Ctrl Pts',(-165.914072419812,-4.75837135876387,
129.560331527798));
#115691=CARTESIAN_POINT('Ctrl Pts',(-165.915373126199,-4.76405452823409,
129.582490119308));
#115692=CARTESIAN_POINT('Ctrl Pts',(-164.165050101093,-4.76405452823413,
129.582490119309));
#115693=CARTESIAN_POINT('Ctrl Pts',(-164.173211318972,-4.79982856714151,
129.721972554062));
#115694=CARTESIAN_POINT('Ctrl Pts',(-164.181372536851,-4.82943340149729,
129.862877416774));
#115695=CARTESIAN_POINT('Ctrl Pts',(-164.189533754729,-4.85279162353424,
130.004612831664));
#115696=CARTESIAN_POINT('Ctrl Pts',(-164.197694972608,-4.8761498455712,
130.146348246553));
#115697=CARTESIAN_POINT('Ctrl Pts',(-164.205856190487,-4.89326146842792,
130.288913713304));
#115698=CARTESIAN_POINT('Ctrl Pts',(-164.214017408366,-4.90411246578154,
130.431716034262));
#115699=CARTESIAN_POINT('Ctrl Pts',(-164.221058460247,-4.91347411210312,
130.554918057001));
#115700=CARTESIAN_POINT('Ctrl Pts',(-164.228099512129,-4.91819381059395,
130.678477256128));
#115701=CARTESIAN_POINT('Ctrl Pts',(-164.235140564011,-4.91824950131355,
130.802145819838));
#115702=CARTESIAN_POINT('',(-163.889859436036,-4.91824789958789,130.80890602176));
#115703=CARTESIAN_POINT('Ctrl Pts',(-163.819828717624,-4.76405452823398,
129.582490119308));
#115704=CARTESIAN_POINT('Ctrl Pts',(-163.827478923358,-4.79773937961931,
129.71382684362));
#115705=CARTESIAN_POINT('Ctrl Pts',(-163.835129129092,-4.82598313537643,
129.846534967663));
#115706=CARTESIAN_POINT('Ctrl Pts',(-163.842779334826,-4.84869131485123,
129.98011818006));
#115707=CARTESIAN_POINT('Ctrl Pts',(-163.850626018354,-4.87198270125662,
130.117132167493));
#115708=CARTESIAN_POINT('Ctrl Pts',(-163.858472701882,-4.88945024297251,
130.255066360533));
#115709=CARTESIAN_POINT('Ctrl Pts',(-163.86631938541,-4.90104854551911,
130.393378602187));
#115710=CARTESIAN_POINT('Ctrl Pts',(-163.874166068938,-4.9126468480657,
130.531690843841));
#115711=CARTESIAN_POINT('Ctrl Pts',(-163.882012752466,-4.91837592354709,
130.670380679545));
#115712=CARTESIAN_POINT('Ctrl Pts',(-163.889859435994,-4.91824789958858,
130.808906021016));
#115713=CARTESIAN_POINT('Ctrl Pts',(-163.889859436036,-4.91824789958789,
130.80890602176));
#115714=CARTESIAN_POINT('Ctrl Pts',(-163.900065351294,-4.91808138313789,
130.989081237333));
#115715=CARTESIAN_POINT('Ctrl Pts',(-163.910271266553,-4.90801070907263,
131.168816066842));
#115716=CARTESIAN_POINT('Ctrl Pts',(-163.920477181811,-4.88820076612934,
131.347201600279));
#115717=CARTESIAN_POINT('Ctrl Pts',(-163.930965019466,-4.86784360459338,
131.530514754195));
#115718=CARTESIAN_POINT('Ctrl Pts',(-163.94145285712,-4.83720162180321,
131.712403451349));
#115719=CARTESIAN_POINT('Ctrl Pts',(-163.951940694775,-4.79650129041414,
131.891907597496));
#115720=CARTESIAN_POINT('Ctrl Pts',(-163.953013390087,-4.79233846332531,
131.91026726919));
#115721=CARTESIAN_POINT('Ctrl Pts',(-163.9540860854,-4.78807045466479,131.928602014415));
#115722=CARTESIAN_POINT('Ctrl Pts',(-163.955158780712,-4.78369753452532,
131.946910818072));
#115723=CARTESIAN_POINT('Ctrl Pts',(-163.962933114831,-4.75200489836948,
132.079603443196));
#115724=CARTESIAN_POINT('Ctrl Pts',(-163.97070744895,-4.71473683637041,
132.211186585001));
#115725=CARTESIAN_POINT('Ctrl Pts',(-163.978481783069,-4.67198502532995,
132.341155654516));
#115726=CARTESIAN_POINT('Ctrl Pts',(-163.986246536016,-4.62928590207575,
132.470964548768));
#115727=CARTESIAN_POINT('Ctrl Pts',(-163.994011288963,-4.581116597636,132.59916296082));
#115728=CARTESIAN_POINT('Ctrl Pts',(-164.001776041911,-4.52761963578437,
132.725257152041));
#115729=CARTESIAN_POINT('Ctrl Pts',(-164.009533082796,-4.47417580786943,
132.851226104734));
#115730=CARTESIAN_POINT('Ctrl Pts',(-164.017290123681,-4.41541500458449,
132.97509463809));
#115731=CARTESIAN_POINT('Ctrl Pts',(-164.025047164566,-4.35152921400009,
133.096385172889));
#115732=CARTESIAN_POINT('Ctrl Pts',(-164.032798355806,-4.28769160018724,
133.217584241552));
#115733=CARTESIAN_POINT('Ctrl Pts',(-164.040549547046,-4.21873687317269,
133.336208836734));
#115734=CARTESIAN_POINT('Ctrl Pts',(-164.048300738286,-4.14490454010639,
133.451802669039));
#115735=CARTESIAN_POINT('Ctrl Pts',(-164.056048635063,-4.07110358775109,
133.567347370881));
#115736=CARTESIAN_POINT('Ctrl Pts',(-164.06379653184,-3.99242936261894,
133.679863543087));
#115737=CARTESIAN_POINT('Ctrl Pts',(-164.071544428617,-3.90916648483699,
133.788920963132));
#115738=CARTESIAN_POINT('Ctrl Pts',(-164.079290704701,-3.82592102385414,
133.897955570716));
#115739=CARTESIAN_POINT('Ctrl Pts',(-164.087036980786,-3.73808905651081,
134.003532554659));
#115740=CARTESIAN_POINT('Ctrl Pts',(-164.09478325687,-3.64599732315475,
134.10525240344));
#115741=CARTESIAN_POINT('Ctrl Pts',(-164.102529590135,-3.55390490999855,
134.206973003093));
#115742=CARTESIAN_POINT('Ctrl Pts',(-164.1102759234,-3.45755293048111,134.30483612094));
#115743=CARTESIAN_POINT('Ctrl Pts',(-164.118022256666,-3.35730676485025,
134.398477247448));
#115744=CARTESIAN_POINT('Ctrl Pts',(-164.125770324669,-3.25703814978579,
134.492139344236));
#115745=CARTESIAN_POINT('Ctrl Pts',(-164.133518392672,-3.15287389892922,
134.581577301449));
#115746=CARTESIAN_POINT('Ctrl Pts',(-164.141266460675,-3.04521410586984,
134.666465498575));
#115747=CARTESIAN_POINT('Ctrl Pts',(-164.149022763416,-2.93743989070108,
134.751443915887));
#115748=CARTESIAN_POINT('Ctrl Pts',(-164.156779066158,-2.82616301950824,
134.831862671143));
#115749=CARTESIAN_POINT('Ctrl Pts',(-164.1645353689,-2.71181478595766,134.907437954049));
#115750=CARTESIAN_POINT('Ctrl Pts',(-164.172295811414,-2.59740552131156,
134.98305357376));
#115751=CARTESIAN_POINT('Ctrl Pts',(-164.180056253929,-2.47992196264395,
135.053820368444));
#115752=CARTESIAN_POINT('Ctrl Pts',(-164.187816696443,-2.3598210093078,
135.1194999973));
#115753=CARTESIAN_POINT('Ctrl Pts',(-164.195589596708,-2.23952725925961,
135.185285060926));
#115754=CARTESIAN_POINT('Ctrl Pts',(-164.203362496974,-2.11660806903376,
135.245966466546));
#115755=CARTESIAN_POINT('Ctrl Pts',(-164.211135397239,-1.9915421805572,
135.301353257716));
#115756=CARTESIAN_POINT('Ctrl Pts',(-164.218625733001,-1.87102275214975,
135.354726599515));
#115757=CARTESIAN_POINT('Ctrl Pts',(-164.226116068763,-1.74851027799214,
135.403183475504));
#115758=CARTESIAN_POINT('Ctrl Pts',(-164.233606404525,-1.62444552332945,
135.446597126431));
#115759=CARTESIAN_POINT('Ctrl Pts',(-164.241380738644,-1.49567681578414,
135.491656819128));
#115760=CARTESIAN_POINT('Ctrl Pts',(-164.249155072763,-1.36482789412201,
135.531426045324));
#115761=CARTESIAN_POINT('Ctrl Pts',(-164.256929406882,-1.23237283688576,
135.565709192645));
#115762=CARTESIAN_POINT('Ctrl Pts',(-164.264694159829,-1.10008101866971,
135.599950089051));
#115763=CARTESIAN_POINT('Ctrl Pts',(-164.272458912777,-0.966187378191674,
135.628718262135));
#115764=CARTESIAN_POINT('Ctrl Pts',(-164.280223665724,-0.831184349327498,
135.651866743393));
#115765=CARTESIAN_POINT('Ctrl Pts',(-164.287980706609,-0.696315407374798,
135.674992233254));
#115766=CARTESIAN_POINT('Ctrl Pts',(-164.295737747494,-0.560339652635501,
135.692509073194));
#115767=CARTESIAN_POINT('Ctrl Pts',(-164.303494788379,-0.423762660274618,
135.70432064498));
#115768=CARTESIAN_POINT('Ctrl Pts',(-164.311245979619,-0.287288661686275,
135.716123309569));
#115769=CARTESIAN_POINT('Ctrl Pts',(-164.318997170859,-0.150214715872734,
135.722229236095));
#115770=CARTESIAN_POINT('Ctrl Pts',(-164.326748362099,-0.0130541714907547,
135.722593293142));
#115771=CARTESIAN_POINT('Ctrl Pts',(-164.334496258876,0.124048076001172,
135.722957195456));
#115772=CARTESIAN_POINT('Ctrl Pts',(-164.342244155653,0.261236458710503,
135.717584081121));
#115773=CARTESIAN_POINT('Ctrl Pts',(-164.34999205243,0.39799517411068,135.706480863325));
#115774=CARTESIAN_POINT('Ctrl Pts',(-164.357738328514,0.534725282535772,
135.695379968084));
#115775=CARTESIAN_POINT('Ctrl Pts',(-164.365484604598,0.671025512986141,
135.67855138511));
#115776=CARTESIAN_POINT('Ctrl Pts',(-164.373230880682,0.806383133965511,
135.656054064576));
#115777=CARTESIAN_POINT('Ctrl Pts',(-164.380977213948,0.941741754124274,
135.633556577971));
#115778=CARTESIAN_POINT('Ctrl Pts',(-164.388723547213,1.07615736525315,
135.605390334409));
#115779=CARTESIAN_POINT('Ctrl Pts',(-164.396469880478,1.20912579821097,
135.571665712334));
#115780=CARTESIAN_POINT('Ctrl Pts',(-164.404217948481,1.34212400852723,
135.537933537864));
#115781=CARTESIAN_POINT('Ctrl Pts',(-164.411966016484,1.47367401688612,
135.49864060405));
#115782=CARTESIAN_POINT('Ctrl Pts',(-164.419714084487,1.60328560917197,
135.453947515122));
#115783=CARTESIAN_POINT('Ctrl Pts',(-164.427470387229,1.73303495420068,
135.409206925846));
#115784=CARTESIAN_POINT('Ctrl Pts',(-164.435226689971,1.86084139754372,
135.35905484414));
#115785=CARTESIAN_POINT('Ctrl Pts',(-164.442982992713,1.98623303680093,
135.303700723184));
#115786=CARTESIAN_POINT('Ctrl Pts',(-164.450743435227,2.11169160135148,
135.248317058066));
#115787=CARTESIAN_POINT('Ctrl Pts',(-164.458503877741,2.2347324430946,135.187725993954));
#115788=CARTESIAN_POINT('Ctrl Pts',(-164.466264320256,2.35490807390126,
135.122183104188));
#115789=CARTESIAN_POINT('Ctrl Pts',(-164.474037220521,2.47527662129917,
135.056534999156));
#115790=CARTESIAN_POINT('Ctrl Pts',(-164.481810120786,2.59277043121956,
134.98591938513));
#115791=CARTESIAN_POINT('Ctrl Pts',(-164.489583021052,2.70697007489154,
134.910635824629));
#115792=CARTESIAN_POINT('Ctrl Pts',(-164.497073356814,2.81701827386481,
134.83808901118));
#115793=CARTESIAN_POINT('Ctrl Pts',(-164.504563692576,2.92400740082148,
134.761207922034));
#115794=CARTESIAN_POINT('Ctrl Pts',(-164.512054028338,3.02759256523099,
134.680294869002));
#115795=CARTESIAN_POINT('Ctrl Pts',(-164.519828362457,3.13510519263266,
134.596313972972));
#115796=CARTESIAN_POINT('Ctrl Pts',(-164.527602696576,3.23929120727552,
134.50772330752));
#115797=CARTESIAN_POINT('Ctrl Pts',(-164.535377030695,3.33972978389667,
134.414815995085));
#115798=CARTESIAN_POINT('Ctrl Pts',(-164.543141783642,3.44004457894859,
134.322023182608));
#115799=CARTESIAN_POINT('Ctrl Pts',(-164.550906536589,3.53662084093353,
134.224924571063));
#115800=CARTESIAN_POINT('Ctrl Pts',(-164.558671289536,3.62906874854865,
134.123855018948));
#115801=CARTESIAN_POINT('Ctrl Pts',(-164.566428330421,3.72142483559863,
134.022885850538));
#115802=CARTESIAN_POINT('Ctrl Pts',(-164.574185371307,3.80966046597174,
133.917953876902));
#115803=CARTESIAN_POINT('Ctrl Pts',(-164.581942412192,3.89342107628641,
133.809432228232));
#115804=CARTESIAN_POINT('Ctrl Pts',(-164.589693603432,3.9771185220734,133.700992416581));
#115805=CARTESIAN_POINT('Ctrl Pts',(-164.597444794672,4.05634742691817,
133.588968626264));
#115806=CARTESIAN_POINT('Ctrl Pts',(-164.605195985912,4.13079234299426,
133.473768357414));
#115807=CARTESIAN_POINT('Ctrl Pts',(-164.612943882689,4.20520561799523,
133.358617051751));
#115808=CARTESIAN_POINT('Ctrl Pts',(-164.620691779466,4.27483873659731,
133.240292280456));
#115809=CARTESIAN_POINT('Ctrl Pts',(-164.628439676243,4.33941871119797,
133.119231739552));
#115810=CARTESIAN_POINT('Ctrl Pts',(-164.636185952327,4.40398517705996,
132.998196521904));
#115811=CARTESIAN_POINT('Ctrl Pts',(-164.643932228411,4.46350041747012,
132.874427017644));
#115812=CARTESIAN_POINT('Ctrl Pts',(-164.651678504496,4.51773688498037,
132.748386466311));
#115813=CARTESIAN_POINT('Ctrl Pts',(-164.659424837761,4.57197375285197,
132.622344984575));
#115814=CARTESIAN_POINT('Ctrl Pts',(-164.667171171026,4.62093161553248,
132.49403278144));
#115815=CARTESIAN_POINT('Ctrl Pts',(-164.674917504292,4.66443082179806,
132.363933690929));
#115816=CARTESIAN_POINT('Ctrl Pts',(-164.682665572295,4.70793976940923,
132.23380546563));
#115817=CARTESIAN_POINT('Ctrl Pts',(-164.690413640298,4.74598750416377,
132.101889927398));
#115818=CARTESIAN_POINT('Ctrl Pts',(-164.6981617083,4.77844417424365,131.968686317762));
#115819=CARTESIAN_POINT('Ctrl Pts',(-164.705918011042,4.81093533965878,
131.835341137744));
#115820=CARTESIAN_POINT('Ctrl Pts',(-164.713674313784,4.8378234774116,131.700705532098));
#115821=CARTESIAN_POINT('Ctrl Pts',(-164.721430616526,4.85902973162015,
131.565289740239));
#115822=CARTESIAN_POINT('Ctrl Pts',(-164.72919105904,4.88024730424508,131.429801672894));
#115823=CARTESIAN_POINT('Ctrl Pts',(-164.736951501554,4.89577690638137,
131.293532977866));
#115824=CARTESIAN_POINT('Ctrl Pts',(-164.744711944069,4.90559168085346,
131.156998283225));
#115825=CARTESIAN_POINT('Ctrl Pts',(-164.752484844334,4.91542221087285,
131.020244410971));
#115826=CARTESIAN_POINT('Ctrl Pts',(-164.760257744599,4.91951956906265,
130.883224076824));
#115827=CARTESIAN_POINT('Ctrl Pts',(-164.768030644865,4.91790907435823,
130.746452078947));
#115828=CARTESIAN_POINT('Ctrl Pts',(-164.775520980627,4.91635712519291,
130.614652087701));
#115829=CARTESIAN_POINT('Ctrl Pts',(-164.783011316389,4.90950512398354,
130.483082998495));
#115830=CARTESIAN_POINT('Ctrl Pts',(-164.790501652151,4.89742099246282,
130.352198384419));
#115831=CARTESIAN_POINT('Ctrl Pts',(-164.79827598627,4.88487868742258,130.216351240418));
#115832=CARTESIAN_POINT('Ctrl Pts',(-164.806050320389,4.86665993735916,
130.080811176974));
#115833=CARTESIAN_POINT('Ctrl Pts',(-164.813824654508,4.84278388814765,
129.946090686136));
#115834=CARTESIAN_POINT('Ctrl Pts',(-164.821589407455,4.81893726403294,
129.811536226262));
#115835=CARTESIAN_POINT('Ctrl Pts',(-164.829354160402,4.78944728077334,
129.677799710566));
#115836=CARTESIAN_POINT('Ctrl Pts',(-164.83711891335,4.7543849563725,129.54539010595));
#115837=CARTESIAN_POINT('Ctrl Pts',(-164.844875954235,4.71935745636655,
129.413112012419));
#115838=CARTESIAN_POINT('Ctrl Pts',(-164.852632995119,4.67876872861081,
129.282158582768));
#115839=CARTESIAN_POINT('Ctrl Pts',(-164.860390036004,4.63274104793342,
129.153029807191));
#115840=CARTESIAN_POINT('Ctrl Pts',(-164.868141227245,4.58674807708801,
129.023998408629));
#115841=CARTESIAN_POINT('Ctrl Pts',(-164.875892418485,4.53532444795852,
128.896789292105));
#115842=CARTESIAN_POINT('Ctrl Pts',(-164.883643609725,4.47864249469079,
128.771888116584));
#115843=CARTESIAN_POINT('Ctrl Pts',(-164.891391506502,4.42198463276531,
128.647040027394));
#115844=CARTESIAN_POINT('Ctrl Pts',(-164.899139403279,4.36007305303164,
128.524498283474));
#115845=CARTESIAN_POINT('Ctrl Pts',(-164.906887300056,4.29312844508182,
128.404729142416));
#115846=CARTESIAN_POINT('Ctrl Pts',(-164.91463357614,4.22619784050083,128.284985054481));
#115847=CARTESIAN_POINT('Ctrl Pts',(-164.922379852224,4.15423649241504,
128.168012756874));
#115848=CARTESIAN_POINT('Ctrl Pts',(-164.930126128309,4.07751114241307,
128.054254083994));
#115849=CARTESIAN_POINT('Ctrl Pts',(-164.937872461574,4.00078522604189,
127.940494571373));
#115850=CARTESIAN_POINT('Ctrl Pts',(-164.945618794839,3.91929545619527,
127.829949054947));
#115851=CARTESIAN_POINT('Ctrl Pts',(-164.953365128105,3.83335179026499,
127.723030204486));
#115852=CARTESIAN_POINT('Ctrl Pts',(-164.961113196108,3.74738887784674,
127.61608741029));
#115853=CARTESIAN_POINT('Ctrl Pts',(-164.968861264111,3.65697032949276,
127.512773202843));
#115854=CARTESIAN_POINT('Ctrl Pts',(-164.976609332114,3.56244598315982,
127.413466682397));
#115855=CARTESIAN_POINT('Ctrl Pts',(-164.984365634855,3.46782117522687,
127.314054617799));
#115856=CARTESIAN_POINT('Ctrl Pts',(-164.992121937597,3.36908212235354,
127.218659032487));
#115857=CARTESIAN_POINT('Ctrl Pts',(-164.999878240339,3.26661547987926,
127.127622067014));
#115858=CARTESIAN_POINT('Ctrl Pts',(-165.007638682853,3.1640941478724,127.036536512372));
#115859=CARTESIAN_POINT('Ctrl Pts',(-165.015399125367,3.05784156470194,
126.949814460063));
#115860=CARTESIAN_POINT('Ctrl Pts',(-165.023159567882,2.9482761845781,126.867756674832));
#115861=CARTESIAN_POINT('Ctrl Pts',(-165.030932468147,2.83853492037933,
126.785567163159));
#115862=CARTESIAN_POINT('Ctrl Pts',(-165.038705368412,2.72547055482927,
126.708057102157));
#115863=CARTESIAN_POINT('Ctrl Pts',(-165.046478268678,2.60952988770485,
126.635483451269));
#115864=CARTESIAN_POINT('Ctrl Pts',(-165.05396860444,2.49780395586702,126.565548035392));
#115865=CARTESIAN_POINT('Ctrl Pts',(-165.061458940202,2.38340748086415,
126.500196511599));
#115866=CARTESIAN_POINT('Ctrl Pts',(-165.068949275964,2.26675877993803,
126.439616902745));
#115867=CARTESIAN_POINT('Ctrl Pts',(-165.076723610083,2.1456873080622,126.376740399608));
#115868=CARTESIAN_POINT('Ctrl Pts',(-165.084497944202,2.02180593456538,
126.318805634976));
#115869=CARTESIAN_POINT('Ctrl Pts',(-165.092272278321,1.89555618233674,
126.266073515354));
#115870=CARTESIAN_POINT('Ctrl Pts',(-165.100037031268,1.76946202164446,
126.213406383356));
#115871=CARTESIAN_POINT('Ctrl Pts',(-165.107801784216,1.64100564709012,
126.165929288042));
#115872=CARTESIAN_POINT('Ctrl Pts',(-165.115566537163,1.51065365390793,
126.123857588998));
#115873=CARTESIAN_POINT('Ctrl Pts',(-165.123323578048,1.38043112816301,
126.081827676158));
#115874=CARTESIAN_POINT('Ctrl Pts',(-165.131080618933,1.24831710021635,
126.045192594909));
#115875=CARTESIAN_POINT('Ctrl Pts',(-165.138837659818,1.11479831851221,
126.01411972889));
#115876=CARTESIAN_POINT('Ctrl Pts',(-165.146588851058,0.981380224359805,
125.983070295161));
#115877=CARTESIAN_POINT('Ctrl Pts',(-165.154340042298,0.846559864242099,
125.957574816004));
#115878=CARTESIAN_POINT('Ctrl Pts',(-165.162091233538,0.71083898761624,
125.937750812354));
#115879=CARTESIAN_POINT('Ctrl Pts',(-165.169839130315,0.575175795983603,
125.917935234435));
#115880=CARTESIAN_POINT('Ctrl Pts',(-165.177587027092,0.438613235140789,
125.903786394055));
#115881=CARTESIAN_POINT('Ctrl Pts',(-165.185334923869,0.301662868920606,
125.895370642427));
#115882=CARTESIAN_POINT('Ctrl Pts',(-165.193081199953,0.164741149764728,
125.886956651193));
#115883=CARTESIAN_POINT('Ctrl Pts',(-165.200827476037,0.0274321765665248,
125.884273387325));
#115884=CARTESIAN_POINT('Ctrl Pts',(-165.208573752121,-0.109748142537605,
125.887335255855));
#115885=CARTESIAN_POINT('Ctrl Pts',(-165.216320085387,-0.246929474275501,
125.890397146987));
#115886=CARTESIAN_POINT('Ctrl Pts',(-165.224066418652,-0.383981759156418,
125.899204246416));
#115887=CARTESIAN_POINT('Ctrl Pts',(-165.231812751917,-0.520390266873772,
125.913718836302));
#115888=CARTESIAN_POINT('Ctrl Pts',(-165.23956081992,-0.656829322330825,
125.92823667663));
#115889=CARTESIAN_POINT('Ctrl Pts',(-165.247308887923,-0.79262392504769,
125.948464509432));
#115890=CARTESIAN_POINT('Ctrl Pts',(-165.255056955926,-0.927266031284532,
125.974312919072));
#115891=CARTESIAN_POINT('Ctrl Pts',(-165.262813258668,-1.06205123675433,
126.00018880071));
#115892=CARTESIAN_POINT('Ctrl Pts',(-165.27056956141,-1.19568111433443,
126.0316971183));
#115893=CARTESIAN_POINT('Ctrl Pts',(-165.278325864152,-1.32765881483179,
126.06869750308));
#115894=CARTESIAN_POINT('Ctrl Pts',(-165.286086306666,-1.45970695580167,
126.10571763608));
#115895=CARTESIAN_POINT('Ctrl Pts',(-165.29384674918,-1.59010079107251,
126.148235555954));
#115896=CARTESIAN_POINT('Ctrl Pts',(-165.301607191694,-1.71836109402489,
126.196061776015));
#115897=CARTESIAN_POINT('Ctrl Pts',(-165.30938009196,-1.84682729180199,
126.24396477097));
#115898=CARTESIAN_POINT('Ctrl Pts',(-165.317152992225,-1.97315275265275,
126.297192942596));
#115899=CARTESIAN_POINT('Ctrl Pts',(-165.324925892491,-2.09687978312631,
126.355509278443));
#115900=CARTESIAN_POINT('Ctrl Pts',(-165.332416228253,-2.21610902439291,
126.411705668592));
#115901=CARTESIAN_POINT('Ctrl Pts',(-165.339906564015,-2.33292520124008,
126.472626567979));
#115902=CARTESIAN_POINT('Ctrl Pts',(-165.347396899777,-2.44694401402623,
126.538021665406));
#115903=CARTESIAN_POINT('Ctrl Pts',(-165.355172364684,-2.56530309774718,
126.605906110281));
#115904=CARTESIAN_POINT('Ctrl Pts',(-165.362947829591,-2.68102260916758,
126.678827201352));
#115905=CARTESIAN_POINT('Ctrl Pts',(-165.370723294498,-2.79364418792851,
126.756554395209));
#115906=CARTESIAN_POINT('Ctrl Pts',(-165.378488931618,-2.90612341881161,
126.834183345894));
#115907=CARTESIAN_POINT('Ctrl Pts',(-165.386254568737,-3.01551218996034,
126.916606091101));
#115908=CARTESIAN_POINT('Ctrl Pts',(-165.394020205857,-3.12137696430902,
127.003546374646));
#115909=CARTESIAN_POINT('Ctrl Pts',(-165.401776441018,-3.22711356679057,
127.090381398453));
#115910=CARTESIAN_POINT('Ctrl Pts',(-165.409532676179,-3.32933436994994,
127.181722820468));
#115911=CARTESIAN_POINT('Ctrl Pts',(-165.41728891134,-3.42763558196576,
127.277251691017));
#115912=CARTESIAN_POINT('Ctrl Pts',(-165.425039814993,-3.5258692233466,
127.372714896593));
#115913=CARTESIAN_POINT('Ctrl Pts',(-165.432790718646,-3.62018835469884,
127.472359552875));
#115914=CARTESIAN_POINT('Ctrl Pts',(-165.440541622299,-3.71022294051425,
127.575827081395));
#115915=CARTESIAN_POINT('Ctrl Pts',(-165.448288876738,-3.80021513701893,
127.679245896222));
#115916=CARTESIAN_POINT('Ctrl Pts',(-165.456036131177,-3.88592654633809,
127.786483707236));
#115917=CARTESIAN_POINT('Ctrl Pts',(-165.463783385616,-3.96702491824877,
127.897146081194));
#115918=CARTESIAN_POINT('Ctrl Pts',(-165.471528670312,-4.04810267087022,
128.007780319204));
#115919=CARTESIAN_POINT('Ctrl Pts',(-165.479273955009,-4.12456949064734,
128.121837071464));
#115920=CARTESIAN_POINT('Ctrl Pts',(-165.487019239706,-4.19613450775678,
128.238890240557));
#115921=CARTESIAN_POINT('Ctrl Pts',(-165.494766446468,-4.26771728439569,
128.355972457489));
#115922=CARTESIAN_POINT('Ctrl Pts',(-165.502513653229,-4.33439561961306,
128.476052245975));
#115923=CARTESIAN_POINT('Ctrl Pts',(-165.510260859991,-4.39592293717988,
128.598676008907));
#115924=CARTESIAN_POINT('Ctrl Pts',(-165.518009053047,-4.45745808776662,
128.721315383025));
#115925=CARTESIAN_POINT('Ctrl Pts',(-165.525757246103,-4.51384074641663,
128.846499023675));
#115926=CARTESIAN_POINT('Ctrl Pts',(-165.533505439158,-4.56487152273224,
128.973751144345));
#115927=CARTESIAN_POINT('Ctrl Pts',(-165.541259448977,-4.61594060913102,
129.101098796372));
#115928=CARTESIAN_POINT('Ctrl Pts',(-165.549013458795,-4.66164965118814,
129.230517663771));
#115929=CARTESIAN_POINT('Ctrl Pts',(-165.556767468614,-4.70184831378861,
129.361514299823));
#115930=CARTESIAN_POINT('Ctrl Pts',(-165.561100088326,-4.72430966244096,
129.434709797492));
#115931=CARTESIAN_POINT('Ctrl Pts',(-165.565432708038,-4.74505150669632,
129.508397626744));
#115932=CARTESIAN_POINT('Ctrl Pts',(-165.569765327751,-4.76405452823417,
129.582490119309));
#115933=CARTESIAN_POINT('Origin',(213.235140564004,0.,130.804360617566));
#115934=CARTESIAN_POINT('',(-167.665279524992,-4.76405452823393,129.582490119308));
#115935=CARTESIAN_POINT('',(-167.320062571459,-4.76405452823401,129.582490119308));
#115936=CARTESIAN_POINT('',(213.235140564004,-4.76405452823405,129.582490119308));
#115937=CARTESIAN_POINT('',(-165.985140563955,-4.91824883541683,130.800976031773));
#115938=CARTESIAN_POINT('Ctrl Pts',(-165.985140564011,-4.91824883541751,
130.800976032755));
#115939=CARTESIAN_POINT('Ctrl Pts',(-165.992921447872,-4.91834374325779,
130.938889662065));
#115940=CARTESIAN_POINT('Ctrl Pts',(-166.000702331733,-4.91263343217728,
131.076842827902));
#115941=CARTESIAN_POINT('Ctrl Pts',(-166.008483215594,-4.90113463722454,
131.214314676331));
#115942=CARTESIAN_POINT('Ctrl Pts',(-166.016264069799,-4.8896358860991,
131.35178600079));
#115943=CARTESIAN_POINT('Ctrl Pts',(-166.024044924003,-4.87234872630466,
131.48877562691));
#115944=CARTESIAN_POINT('Ctrl Pts',(-166.031825778208,-4.84934186529542,
131.624766941282));
#115945=CARTESIAN_POINT('Ctrl Pts',(-166.039608230963,-4.82633027760143,
131.760786194627));
#115946=CARTESIAN_POINT('Ctrl Pts',(-166.047390683719,-4.79759671352023,
131.895806347448));
#115947=CARTESIAN_POINT('Ctrl Pts',(-166.055173136475,-4.76326112125045,
132.029320434574));
#115948=CARTESIAN_POINT('Ctrl Pts',(-166.062958816668,-4.72891128976911,
132.162889890931));
#115949=CARTESIAN_POINT('Ctrl Pts',(-166.070744496861,-4.68895490117725,
132.29495166481));
#115950=CARTESIAN_POINT('Ctrl Pts',(-166.078530177055,-4.64356183651419,
132.425013736827));
#115951=CARTESIAN_POINT('Ctrl Pts',(-166.086325608341,-4.598111919788,132.555238703708));
#115952=CARTESIAN_POINT('Ctrl Pts',(-166.094121039627,-4.54721185565204,
132.683458602351));
#115953=CARTESIAN_POINT('Ctrl Pts',(-166.101916470914,-4.4910800146906,
132.80920060224));
#115954=CARTESIAN_POINT('Ctrl Pts',(-166.109717264546,-4.43490956158325,
132.935029097928));
#115955=CARTESIAN_POINT('Ctrl Pts',(-166.117518058177,-4.37350033261783,
133.058375954042));
#115956=CARTESIAN_POINT('Ctrl Pts',(-166.125318851809,-4.30711634929883,
133.178793563788));
#115957=CARTESIAN_POINT('Ctrl Pts',(-166.133132278773,-4.2406248575752,
133.299406189024));
#115958=CARTESIAN_POINT('Ctrl Pts',(-166.140945705736,-4.16914271861626,
133.417079763003));
#115959=CARTESIAN_POINT('Ctrl Pts',(-166.1487591327,-4.0929773134785,133.531395596045));
#115960=CARTESIAN_POINT('Ctrl Pts',(-166.153556346819,-4.04621399712678,
133.601582151935));
#115961=CARTESIAN_POINT('Ctrl Pts',(-166.158353560937,-3.99768608866018,
133.670503604081));
#115962=CARTESIAN_POINT('Ctrl Pts',(-166.163150775056,-3.94747195171253,
133.738069576025));
#115963=CARTESIAN_POINT('Ctrl Pts',(-166.170925109175,-3.86609524671875,
133.84756655239));
#115964=CARTESIAN_POINT('Ctrl Pts',(-166.178699443294,-3.78003027026917,
133.953848495734));
#115965=CARTESIAN_POINT('Ctrl Pts',(-166.186473777413,-3.68955996174399,
134.056487667851));
#115966=CARTESIAN_POINT('Ctrl Pts',(-166.19423853036,-3.5992011497885,134.159000346362));
#115967=CARTESIAN_POINT('Ctrl Pts',(-166.202003283307,-3.5044480642423,
134.257878895716));
#115968=CARTESIAN_POINT('Ctrl Pts',(-166.209768036254,-3.405626112538,134.352725571189));
#115969=CARTESIAN_POINT('Ctrl Pts',(-166.217525077139,-3.30690231218927,
134.447478043607));
#115970=CARTESIAN_POINT('Ctrl Pts',(-166.225282118024,-3.20411796820674,
134.538206342336));
#115971=CARTESIAN_POINT('Ctrl Pts',(-166.233039158909,-3.09763759478476,
134.624547052006));
#115972=CARTESIAN_POINT('Ctrl Pts',(-166.240790350149,-2.99123751904083,
134.710822651474));
#115973=CARTESIAN_POINT('Ctrl Pts',(-166.248541541389,-2.88114726406746,
134.792717002435));
#115974=CARTESIAN_POINT('Ctrl Pts',(-166.256292732629,-2.76776664276774,
134.869904969025));
#115975=CARTESIAN_POINT('Ctrl Pts',(-166.264040629406,-2.65443421125675,
134.94706012867));
#115976=CARTESIAN_POINT('Ctrl Pts',(-166.271788526183,-2.53781451742097,
135.019512662908));
#115977=CARTESIAN_POINT('Ctrl Pts',(-166.27953642296,-2.41833858028677,
135.086979159252));
#115978=CARTESIAN_POINT('Ctrl Pts',(-166.287282699044,-2.29888763494301,
135.15443154306));
#115979=CARTESIAN_POINT('Ctrl Pts',(-166.295028975128,-2.17658197491196,
135.216899771384));
#115980=CARTESIAN_POINT('Ctrl Pts',(-166.302775251212,-2.05187924581811,
135.274145245832));
#115981=CARTESIAN_POINT('Ctrl Pts',(-166.310521584478,-1.92717559619688,
135.331391142853));
#115982=CARTESIAN_POINT('Ctrl Pts',(-166.318267917743,-1.80007519751998,
135.383414045958));
#115983=CARTESIAN_POINT('Ctrl Pts',(-166.326014251008,-1.67105743334419,
135.430022744977));
#115984=CARTESIAN_POINT('Ctrl Pts',(-166.333762319011,-1.54201077653484,
135.476641881691));
#115985=CARTESIAN_POINT('Ctrl Pts',(-166.341510387014,-1.41104626744494,
135.517844268825));
#115986=CARTESIAN_POINT('Ctrl Pts',(-166.349258455017,-1.27865988774699,
135.553488111534));
#115987=CARTESIAN_POINT('Ctrl Pts',(-166.357014757759,-1.14613280622909,
135.589169836944));
#115988=CARTESIAN_POINT('Ctrl Pts',(-166.364771060501,-1.01218121347949,
135.619281114883));
#115989=CARTESIAN_POINT('Ctrl Pts',(-166.372527363242,-0.877313309652195,
135.643730867837));
#115990=CARTESIAN_POINT('Ctrl Pts',(-166.380287805757,-0.74237342276383,
135.66819367036));
#115991=CARTESIAN_POINT('Ctrl Pts',(-166.388048248271,-0.606516637385834,
135.686988873302));
#115992=CARTESIAN_POINT('Ctrl Pts',(-166.395808690785,-0.470256788889064,
135.700077277566));
#115993=CARTESIAN_POINT('Ctrl Pts',(-166.40358159105,-0.333778203986905,
135.713186692499));
#115994=CARTESIAN_POINT('Ctrl Pts',(-166.411354491316,-0.196895653610697,
135.720570980964));
#115995=CARTESIAN_POINT('Ctrl Pts',(-166.419127391581,-0.0601243952583667,
135.722243100871));
#115996=CARTESIAN_POINT('Ctrl Pts',(-166.426617727343,0.0716748833546202,
135.723854435007));
#115997=CARTESIAN_POINT('Ctrl Pts',(-166.434108063106,0.203370513056851,
135.72016170237));
#115998=CARTESIAN_POINT('Ctrl Pts',(-166.441598398868,0.334507421442165,
135.711221920629));
#115999=CARTESIAN_POINT('Ctrl Pts',(-166.449372732987,0.470616425560006,
135.701943184347));
#116000=CARTESIAN_POINT('Ctrl Pts',(-166.457147067106,0.606554656582134,
135.686982268632));
#116001=CARTESIAN_POINT('Ctrl Pts',(-166.464921401225,0.741809310595588,
135.666346015448));
#116002=CARTESIAN_POINT('Ctrl Pts',(-166.472686154172,0.876897275335291,
135.645735194601));
#116003=CARTESIAN_POINT('Ctrl Pts',(-166.48045090712,1.01130295650361,135.619463011353));
#116004=CARTESIAN_POINT('Ctrl Pts',(-166.488215660067,1.14451582953313,
135.587588249453));
#116005=CARTESIAN_POINT('Ctrl Pts',(-166.495972700952,1.27759639365991,
135.555745146016));
#116006=CARTESIAN_POINT('Ctrl Pts',(-166.503729741837,1.4094861295105,135.518310628044));
#116007=CARTESIAN_POINT('Ctrl Pts',(-166.511486782722,1.5396822566143,135.475394936768));
#116008=CARTESIAN_POINT('Ctrl Pts',(-166.519237973962,1.66978020180605,
135.432511608549));
#116009=CARTESIAN_POINT('Ctrl Pts',(-166.526989165202,1.79818671055663,
135.384155456197));
#116010=CARTESIAN_POINT('Ctrl Pts',(-166.534740356442,1.92441212821454,
135.330487109753));
#116011=CARTESIAN_POINT('Ctrl Pts',(-166.542488253219,2.05058389670226,
135.276841573789));
#116012=CARTESIAN_POINT('Ctrl Pts',(-166.550236149997,2.17457605883224,
135.21788848703));
#116013=CARTESIAN_POINT('Ctrl Pts',(-166.557984046774,2.29591719534093,
135.153837286619));
#116014=CARTESIAN_POINT('Ctrl Pts',(-166.565730322858,2.41723294989967,
135.089799484338));
#116015=CARTESIAN_POINT('Ctrl Pts',(-166.573476598942,2.53589843630963,
135.020665871958));
#116016=CARTESIAN_POINT('Ctrl Pts',(-166.581222875026,2.65146554634782,
134.946692511443));
#116017=CARTESIAN_POINT('Ctrl Pts',(-166.588969208291,2.767033509476,134.872718604874));
#116018=CARTESIAN_POINT('Ctrl Pts',(-166.596715541557,2.87950272130864,
134.793905089655));
#116019=CARTESIAN_POINT('Ctrl Pts',(-166.604461874822,2.98845319279131,
134.710551930981));
#116020=CARTESIAN_POINT('Ctrl Pts',(-166.612209942825,3.09742806297681,
134.627180105944));
#116021=CARTESIAN_POINT('Ctrl Pts',(-166.619958010828,3.2028823143341,134.539266852009));
#116022=CARTESIAN_POINT('Ctrl Pts',(-166.627706078831,3.30442856063603,
134.447152809025));
#116023=CARTESIAN_POINT('Ctrl Pts',(-166.635462381573,3.40608273149709,
134.35494086614));
#116024=CARTESIAN_POINT('Ctrl Pts',(-166.643218684315,3.5038203102532,134.258519478687));
#116025=CARTESIAN_POINT('Ctrl Pts',(-166.650974987057,3.59728997621696,
134.158266980229));
#116026=CARTESIAN_POINT('Ctrl Pts',(-166.658735429571,3.69080952975576,
134.057960973993));
#116027=CARTESIAN_POINT('Ctrl Pts',(-166.666495872085,3.78005637728183,
133.953820079078));
#116028=CARTESIAN_POINT('Ctrl Pts',(-166.674256314599,3.86471979891645,
133.846255411664));
#116029=CARTESIAN_POINT('Ctrl Pts',(-166.682029214865,3.9495191297913,133.738518071898));
#116030=CARTESIAN_POINT('Ctrl Pts',(-166.68980211513,4.02972010283157,133.627346293837));
#116031=CARTESIAN_POINT('Ctrl Pts',(-166.697575015395,4.10505511062848,
133.513180582274));
#116032=CARTESIAN_POINT('Ctrl Pts',(-166.705065351157,4.17765150113475,
133.403165081893));
#116033=CARTESIAN_POINT('Ctrl Pts',(-166.712555686919,4.24572940527844,
133.290369806626));
#116034=CARTESIAN_POINT('Ctrl Pts',(-166.720046022681,4.30909081588839,
133.17520844122));
#116035=CARTESIAN_POINT('Ctrl Pts',(-166.727820356801,4.37485459364,133.055680697643));
#116036=CARTESIAN_POINT('Ctrl Pts',(-166.73559469092,4.43574548587656,132.933225273528));
#116037=CARTESIAN_POINT('Ctrl Pts',(-166.743369025039,4.49149206589649,
132.808277303581));
#116038=CARTESIAN_POINT('Ctrl Pts',(-166.751133777986,4.54716994323846,
132.683483320841));
#116039=CARTESIAN_POINT('Ctrl Pts',(-166.758898530933,4.59771596511764,
132.556203257928));
#116040=CARTESIAN_POINT('Ctrl Pts',(-166.76666328388,4.64290363696878,132.426898407672));
#116041=CARTESIAN_POINT('Ctrl Pts',(-166.774420324765,4.68804642778731,
132.297721984816));
#116042=CARTESIAN_POINT('Ctrl Pts',(-166.78217736565,4.72784133143026,132.166525143382));
#116043=CARTESIAN_POINT('Ctrl Pts',(-166.789934406535,4.76210933184111,
132.033790474895));
#116044=CARTESIAN_POINT('Ctrl Pts',(-166.797685597775,4.79635149048652,
131.901155902653));
#116045=CARTESIAN_POINT('Ctrl Pts',(-166.805436789015,4.82507494447826,
131.766986188669));
#116046=CARTESIAN_POINT('Ctrl Pts',(-166.813187980256,4.84815016612017,
131.631780117728));
#116047=CARTESIAN_POINT('Ctrl Pts',(-166.820935877033,4.87121558017724,
131.496631512975));
#116048=CARTESIAN_POINT('Ctrl Pts',(-166.82868377381,4.88863747095705,131.360447811932));
#116049=CARTESIAN_POINT('Ctrl Pts',(-166.836431670587,4.90033723023199,
131.223738838868));
#116050=CARTESIAN_POINT('Ctrl Pts',(-166.844177946671,4.9120345421695,131.087058462374));
#116051=CARTESIAN_POINT('Ctrl Pts',(-166.851924222755,4.91801207007805,
130.949853421701));
#116052=CARTESIAN_POINT('Ctrl Pts',(-166.859670498839,4.91824303270179,
130.812639130737));
#116053=CARTESIAN_POINT('Ctrl Pts',(-166.867416832105,4.91847399703044,
130.675423826888));
#116054=CARTESIAN_POINT('Ctrl Pts',(-166.87516316537,4.91295831077049,130.538199663577));
#116055=CARTESIAN_POINT('Ctrl Pts',(-166.882909498635,4.90172132879331,
130.401482128003));
#116056=CARTESIAN_POINT('Ctrl Pts',(-166.890657566638,4.89048183037195,
130.264733975485));
#116057=CARTESIAN_POINT('Ctrl Pts',(-166.898405634641,4.87351851872493,
130.128493066046));
#116058=CARTESIAN_POINT('Ctrl Pts',(-166.906153702644,4.85090859208839,
129.993269442849));
#116059=CARTESIAN_POINT('Ctrl Pts',(-166.913910005386,4.82827463535267,
129.857902102377));
#116060=CARTESIAN_POINT('Ctrl Pts',(-166.921666308128,4.79998213998362,
129.723554594155));
#116061=CARTESIAN_POINT('Ctrl Pts',(-166.92942261087,4.76615951130919,129.590726992761));
#116062=CARTESIAN_POINT('Ctrl Pts',(-166.937183053384,4.73231883047954,
129.457828497277));
#116063=CARTESIAN_POINT('Ctrl Pts',(-166.944943495898,4.69294224722724,
129.326451899367));
#116064=CARTESIAN_POINT('Ctrl Pts',(-166.952703938412,4.64820769355471,
129.197080834803));
#116065=CARTESIAN_POINT('Ctrl Pts',(-166.960476838678,4.60340132800528,
129.067502092321));
#116066=CARTESIAN_POINT('Ctrl Pts',(-166.968249738943,4.55321994752032,
128.939935680729));
#116067=CARTESIAN_POINT('Ctrl Pts',(-166.976022639209,4.49788951291557,
128.814844849319));
#116068=CARTESIAN_POINT('Ctrl Pts',(-166.983512974971,4.44457047897841,
128.694301384717));
#116069=CARTESIAN_POINT('Ctrl Pts',(-166.991003310732,4.38647038945388,
128.576056914437));
#116070=CARTESIAN_POINT('Ctrl Pts',(-166.998493646494,4.32383026132284,
128.460501634229));
#116071=CARTESIAN_POINT('Ctrl Pts',(-167.006267980613,4.25881511369365,
128.340565040449));
#116072=CARTESIAN_POINT('Ctrl Pts',(-167.014042314732,4.18870291186473,
128.223145660416));
#116073=CARTESIAN_POINT('Ctrl Pts',(-167.021816648852,4.1137130342247,128.10870705404));
#116074=CARTESIAN_POINT('Ctrl Pts',(-167.029581401799,4.03881557490723,
127.994409483019));
#116075=CARTESIAN_POINT('Ctrl Pts',(-167.037346154746,3.95905261270079,
127.883085700282));
#116076=CARTESIAN_POINT('Ctrl Pts',(-167.045110907693,3.87468982048289,
127.775175602162));
#116077=CARTESIAN_POINT('Ctrl Pts',(-167.052867948578,3.79041081857929,
127.667372681873));
#116078=CARTESIAN_POINT('Ctrl Pts',(-167.060624989463,3.70154131765627,
127.562977004932));
#116079=CARTESIAN_POINT('Ctrl Pts',(-167.068382030348,3.6083905730819,127.462400035124));
#116080=CARTESIAN_POINT('Ctrl Pts',(-167.076133221588,3.51531007420823,
127.361898911192));
#116081=CARTESIAN_POINT('Ctrl Pts',(-167.083884412828,3.41795502244142,
127.265211048172));
#116082=CARTESIAN_POINT('Ctrl Pts',(-167.091635604068,3.31667504666567,
127.172715026746));
#116083=CARTESIAN_POINT('Ctrl Pts',(-167.099383500845,3.21543811758177,
127.080258318596));
#116084=CARTESIAN_POINT('Ctrl Pts',(-167.107131397622,3.11027987049151,
126.991990171584));
#116085=CARTESIAN_POINT('Ctrl Pts',(-167.1148792944,3.00158674532412,126.908252293508));
#116086=CARTESIAN_POINT('Ctrl Pts',(-167.122625570484,2.89291635641537,
126.824531931591));
#116087=CARTESIAN_POINT('Ctrl Pts',(-167.130371846568,2.78071286969311,
126.745340192166));
#116088=CARTESIAN_POINT('Ctrl Pts',(-167.138118122652,2.66539544153446,
126.670978200858));
#116089=CARTESIAN_POINT('Ctrl Pts',(-167.145864455917,2.55007716212859,
126.596615660627));
#116090=CARTESIAN_POINT('Ctrl Pts',(-167.153610789183,2.43164522399254,
126.527083151533));
#116091=CARTESIAN_POINT('Ctrl Pts',(-167.161357122448,2.31054702603529,
126.462637975229));
#116092=CARTESIAN_POINT('Ctrl Pts',(-167.169105190451,2.18942170897608,
126.398178366875));
#116093=CARTESIAN_POINT('Ctrl Pts',(-167.176853258454,2.06562928902431,
126.338808541968));
#116094=CARTESIAN_POINT('Ctrl Pts',(-167.184601326457,1.93964060747172,
126.284739242235));
#116095=CARTESIAN_POINT('Ctrl Pts',(-167.192357629199,1.81351802364926,
126.230612477007));
#116096=CARTESIAN_POINT('Ctrl Pts',(-167.200113931941,1.68519487523416,
126.181797644832));
#116097=CARTESIAN_POINT('Ctrl Pts',(-167.207870234683,1.5551612953463,126.138457017195));
#116098=CARTESIAN_POINT('Ctrl Pts',(-167.215630677197,1.42505831262161,
126.095093257359));
#116099=CARTESIAN_POINT('Ctrl Pts',(-167.223391119711,1.29324345494687,
126.05720963183));
#116100=CARTESIAN_POINT('Ctrl Pts',(-167.231151562225,1.16021979538792,
126.024917858322));
#116101=CARTESIAN_POINT('Ctrl Pts',(-167.23892446249,1.02698259444135,125.992574247193));
#116102=CARTESIAN_POINT('Ctrl Pts',(-167.246697362756,0.892533097600021,
125.965840502357));
#116103=CARTESIAN_POINT('Ctrl Pts',(-167.254470263021,0.757383186953273,
125.944776914138));
#116104=CARTESIAN_POINT('Ctrl Pts',(-167.261960598783,0.62714631598135,
125.924479040408));
#116105=CARTESIAN_POINT('Ctrl Pts',(-167.269450934545,0.496259376714351,
125.909446266736));
#116106=CARTESIAN_POINT('Ctrl Pts',(-167.276941270307,0.365180927454096,
125.899686729047));
#116107=CARTESIAN_POINT('Ctrl Pts',(-167.284715604427,0.229132598948755,
125.889557155519));
#116108=CARTESIAN_POINT('Ctrl Pts',(-167.292489938545,0.0924469913636022,
125.885076493563));
#116109=CARTESIAN_POINT('Ctrl Pts',(-167.300264272665,-0.0443673098444563,
125.886310739381));
#116110=CARTESIAN_POINT('Ctrl Pts',(-167.308029025612,-0.181012999652978,
125.887543464101));
#116111=CARTESIAN_POINT('Ctrl Pts',(-167.315793778559,-0.317786680314714,
125.894477079405));
#116112=CARTESIAN_POINT('Ctrl Pts',(-167.323558531506,-0.454174651904994,
125.907125841892));
#116113=CARTESIAN_POINT('Ctrl Pts',(-167.331315572391,-0.590427161039898,
125.91976204145));
#116114=CARTESIAN_POINT('Ctrl Pts',(-167.339072613276,-0.726294336697561,
125.938102056099));
#116115=CARTESIAN_POINT('Ctrl Pts',(-167.346829654161,-0.861262842660616,
125.962108106766));
#116116=CARTESIAN_POINT('Ctrl Pts',(-167.354580845401,-0.996129567823606,
125.986096054283));
#116117=CARTESIAN_POINT('Ctrl Pts',(-167.362332036641,-1.13009858883394,
126.015741464878));
#116118=CARTESIAN_POINT('Ctrl Pts',(-167.370083227881,-1.26266241209136,
126.050954817974));
#116119=CARTESIAN_POINT('Ctrl Pts',(-167.377831124658,-1.3951698921871,
126.086153204456));
#116120=CARTESIAN_POINT('Ctrl Pts',(-167.385579021436,-1.52627298533755,
126.12691472644));
#116121=CARTESIAN_POINT('Ctrl Pts',(-167.393326918213,-1.6554753228729,
126.173098962481));
#116122=CARTESIAN_POINT('Ctrl Pts',(-167.401073194297,-1.78465063406488,
126.219273537776));
#116123=CARTESIAN_POINT('Ctrl Pts',(-167.408819470381,-1.9119256125657,
126.270868439399));
#116124=CARTESIAN_POINT('Ctrl Pts',(-167.416565746465,-2.03682034859898,
126.327693784974));
#116125=CARTESIAN_POINT('Ctrl Pts',(-167.42431207973,-2.16171600657666,
126.38451955002));
#116126=CARTESIAN_POINT('Ctrl Pts',(-167.432058412996,-2.28423103116377,
126.44657567415));
#116127=CARTESIAN_POINT('Ctrl Pts',(-167.439804746261,-2.40390711715438,
126.513624825817));
#116128=CARTESIAN_POINT('Ctrl Pts',(-167.447552814264,-2.52361000377451,
126.580688992677));
#116129=CARTESIAN_POINT('Ctrl Pts',(-167.455300882267,-2.64047234569105,
126.652748221015));
#116130=CARTESIAN_POINT('Ctrl Pts',(-167.46304895027,-2.75406233870187,
126.729520289769));
#116131=CARTESIAN_POINT('Ctrl Pts',(-167.470805253012,-2.86777305650915,
126.80637395279));
#116132=CARTESIAN_POINT('Ctrl Pts',(-167.478561555754,-2.97820415351134,
126.887950242693));
#116133=CARTESIAN_POINT('Ctrl Pts',(-167.486317858496,-3.08495417718945,
126.973924508304));
#116134=CARTESIAN_POINT('Ctrl Pts',(-167.49407830101,-3.19176117656938,
127.059944660968));
#116135=CARTESIAN_POINT('Ctrl Pts',(-167.501838743524,-3.29488289397738,
127.150367208963));
#116136=CARTESIAN_POINT('Ctrl Pts',(-167.509599186038,-3.39395341485524,
127.244829288824));
#116137=CARTESIAN_POINT('Ctrl Pts',(-167.517372086303,-3.49318297252828,
127.339443007602));
#116138=CARTESIAN_POINT('Ctrl Pts',(-167.525144986569,-3.588348066352,127.438108935011));
#116139=CARTESIAN_POINT('Ctrl Pts',(-167.532917886834,-3.67912128759667,
127.540428998544));
#116140=CARTESIAN_POINT('Ctrl Pts',(-167.540408222596,-3.76659467360441,
127.639029470038));
#116141=CARTESIAN_POINT('Ctrl Pts',(-167.547898558358,-3.84998975960928,
127.741022777588));
#116142=CARTESIAN_POINT('Ctrl Pts',(-167.55538889412,-3.92905183866609,
127.846027520774));
#116143=CARTESIAN_POINT('Ctrl Pts',(-167.563193592337,-4.01143207996082,
127.955439215786));
#116144=CARTESIAN_POINT('Ctrl Pts',(-167.570998290554,-4.08937090091598,
128.068470084042));
#116145=CARTESIAN_POINT('Ctrl Pts',(-167.578802988771,-4.16253478024338,
128.184725668615));
#116146=CARTESIAN_POINT('Ctrl Pts',(-167.586594824583,-4.23557808303929,
128.300789660078));
#116147=CARTESIAN_POINT('Ctrl Pts',(-167.594386660396,-4.30386191328346,
128.4200674586));
#116148=CARTESIAN_POINT('Ctrl Pts',(-167.602178496208,-4.36709373417131,
128.542132649508));
#116149=CARTESIAN_POINT('Ctrl Pts',(-167.609962931,-4.430265494763,128.664081897662));
#116150=CARTESIAN_POINT('Ctrl Pts',(-167.617747365792,-4.48839461392436,
128.78881293102));
#116151=CARTESIAN_POINT('Ctrl Pts',(-167.625531800584,-4.54123229775526,
128.915871199983));
#116152=CARTESIAN_POINT('Ctrl Pts',(-167.633309299869,-4.59402290608838,
129.042816266949));
#116153=CARTESIAN_POINT('Ctrl Pts',(-167.641086799154,-4.64153131800097,
129.17208408541));
#116154=CARTESIAN_POINT('Ctrl Pts',(-167.648864298439,-4.68355533607567,
129.303196910165));
#116155=CARTESIAN_POINT('Ctrl Pts',(-167.654336040623,-4.7131206994435,
129.395439358262));
#116156=CARTESIAN_POINT('Ctrl Pts',(-167.659807782807,-4.73997245841085,
129.488594494564));
#116157=CARTESIAN_POINT('Ctrl Pts',(-167.665279524992,-4.76405452823393,
129.582490119308));
#116158=CARTESIAN_POINT('Ctrl Pts',(-165.915373126199,-4.76405452823409,
129.582490119308));
#116159=CARTESIAN_POINT('Ctrl Pts',(-165.924244735256,-4.80281720230029,
129.733625197187));
#116160=CARTESIAN_POINT('Ctrl Pts',(-165.933116344314,-4.83442761491979,
129.886776635631));
#116161=CARTESIAN_POINT('Ctrl Pts',(-165.941987953371,-4.85869608661611,
130.041304000793));
#116162=CARTESIAN_POINT('Ctrl Pts',(-165.95079959072,-4.88280050445183,
130.194786767385));
#116163=CARTESIAN_POINT('Ctrl Pts',(-165.959611228069,-4.89966182275025,
130.349626760674));
#116164=CARTESIAN_POINT('Ctrl Pts',(-165.968422865418,-4.90914170930784,
130.505177161416));
#116165=CARTESIAN_POINT('Ctrl Pts',(-165.973995431597,-4.91513688286347,
130.603548765699));
#116166=CARTESIAN_POINT('Ctrl Pts',(-165.979567997776,-4.91818086365629,
130.702204113299));
#116167=CARTESIAN_POINT('Ctrl Pts',(-165.985140563956,-4.91824883541683,
130.800976031772));
#116168=CARTESIAN_POINT('',(-165.63985943605,-4.91824976783883,130.802849441434));
#116169=CARTESIAN_POINT('Ctrl Pts',(-165.569765327751,-4.76405452823417,
129.582490119309));
#116170=CARTESIAN_POINT('Ctrl Pts',(-165.577528737229,-4.79810511363771,
129.715252835007));
#116171=CARTESIAN_POINT('Ctrl Pts',(-165.585292146708,-4.8265698199595,
129.849315028426));
#116172=CARTESIAN_POINT('Ctrl Pts',(-165.593055556187,-4.84937783460778,
129.984166933297));
#116173=CARTESIAN_POINT('Ctrl Pts',(-165.600830198457,-4.87221884992079,
130.119213953901));
#116174=CARTESIAN_POINT('Ctrl Pts',(-165.608604840728,-4.88938678319999,
130.255052580719));
#116175=CARTESIAN_POINT('Ctrl Pts',(-165.616379482998,-4.90086275411845,
130.391168981888));
#116176=CARTESIAN_POINT('Ctrl Pts',(-165.619534496529,-4.90551979713908,
130.446406132675));
#116177=CARTESIAN_POINT('Ctrl Pts',(-165.622689510059,-4.90924008483265,
130.50168903927));
#116178=CARTESIAN_POINT('Ctrl Pts',(-165.625844523589,-4.91202479896185,
130.556983502853));
#116179=CARTESIAN_POINT('Ctrl Pts',(-165.630516161058,-4.91614813305812,
130.638858171651));
#116180=CARTESIAN_POINT('Ctrl Pts',(-165.635187798526,-4.91822456870397,
130.720836791468));
#116181=CARTESIAN_POINT('Ctrl Pts',(-165.639859435994,-4.91824976783853,
130.802849440458));
#116182=CARTESIAN_POINT('Ctrl Pts',(-165.63985943605,-4.91824976783883,
130.802849441434));
#116183=CARTESIAN_POINT('Ctrl Pts',(-165.647572658369,-4.91829137346489,
130.9382584493));
#116184=CARTESIAN_POINT('Ctrl Pts',(-165.655285880688,-4.91273663719269,
131.073894834778));
#116185=CARTESIAN_POINT('Ctrl Pts',(-165.662999103007,-4.90155537433178,
131.209253164866));
#116186=CARTESIAN_POINT('Ctrl Pts',(-165.670703040709,-4.89038757066458,
131.344448560409));
#116187=CARTESIAN_POINT('Ctrl Pts',(-165.67840697841,-4.87360674481668,
131.479366173904));
#116188=CARTESIAN_POINT('Ctrl Pts',(-165.686110916112,-4.85123469155569,
131.613499066749));
#116189=CARTESIAN_POINT('Ctrl Pts',(-165.693807495515,-4.82888400661853,
131.747503844617));
#116190=CARTESIAN_POINT('Ctrl Pts',(-165.701504074918,-4.80095278398878,
131.880725003266));
#116191=CARTESIAN_POINT('Ctrl Pts',(-165.709200654322,-4.76751470411547,
132.012659673488));
#116192=CARTESIAN_POINT('Ctrl Pts',(-165.716891794583,-4.73410025479962,
132.144501106007));
#116193=CARTESIAN_POINT('Ctrl Pts',(-165.724582934844,-4.6951867898392,
132.275057475282));
#116194=CARTESIAN_POINT('Ctrl Pts',(-165.732274075106,-4.65089917305424,
132.403835514082));
#116195=CARTESIAN_POINT('Ctrl Pts',(-165.739962504378,-4.60662716685935,
132.532568160933));
#116196=CARTESIAN_POINT('Ctrl Pts',(-165.747650933651,-4.55698490298903,
132.659523347808));
#116197=CARTESIAN_POINT('Ctrl Pts',(-165.755339362923,-4.50214718436271,
132.784222681659));
#116198=CARTESIAN_POINT('Ctrl Pts',(-165.763026646874,-4.44731763474355,
132.908903439432));
#116199=CARTESIAN_POINT('Ctrl Pts',(-165.770713930825,-4.38729432942435,
133.031328648556));
#116200=CARTESIAN_POINT('Ctrl Pts',(-165.778401214776,-4.32230012797284,
133.151040115543));
#116201=CARTESIAN_POINT('Ctrl Pts',(-165.786089082622,-4.2573009898167,
133.270760675344));
#116202=CARTESIAN_POINT('Ctrl Pts',(-165.793776950469,-4.18733039434107,
133.387766733588));
#116203=CARTESIAN_POINT('Ctrl Pts',(-165.801464818316,-4.11265680816186,
133.501625350732));
#116204=CARTESIAN_POINT('Ctrl Pts',(-165.809154999391,-4.03796075319266,
133.615518227183));
#116205=CARTESIAN_POINT('Ctrl Pts',(-165.816845180466,-3.9585591108194,
133.726261446517));
#116206=CARTESIAN_POINT('Ctrl Pts',(-165.824535361542,-3.87476296104074,
133.833452075123));
#116207=CARTESIAN_POINT('Ctrl Pts',(-165.832233884725,-3.79087591139023,
133.94075898132));
#116208=CARTESIAN_POINT('Ctrl Pts',(-165.839932407907,-3.70258508251573,
134.04450528975));
#116209=CARTESIAN_POINT('Ctrl Pts',(-165.84763093109,-3.61024126495735,
134.14432185556));
#116210=CARTESIAN_POINT('Ctrl Pts',(-165.855334211813,-3.51784038068537,
134.244200106098));
#116211=CARTESIAN_POINT('Ctrl Pts',(-165.863037492536,-3.4213818015299,
134.340143498591));
#116212=CARTESIAN_POINT('Ctrl Pts',(-165.870740773259,-3.32125138849588,
134.431821475648));
#116213=CARTESIAN_POINT('Ctrl Pts',(-165.878455261322,-3.22097529783983,
134.523632833055));
#116214=CARTESIAN_POINT('Ctrl Pts',(-165.886169749385,-3.11701701183142,
134.611166131248));
#116215=CARTESIAN_POINT('Ctrl Pts',(-165.893884237449,-3.00979381929446,
134.694132362519));
#116216=CARTESIAN_POINT('Ctrl Pts',(-165.897353540766,-2.96157418701721,
134.731443331058));
#116217=CARTESIAN_POINT('Ctrl Pts',(-165.900822844084,-2.91269462428702,
134.767831246968));
#116218=CARTESIAN_POINT('Ctrl Pts',(-165.904292147402,-2.86319475940396,
134.803272823682));
#116219=CARTESIAN_POINT('Ctrl Pts',(-165.912066481521,-2.75227090720901,
134.882693570107));
#116220=CARTESIAN_POINT('Ctrl Pts',(-165.91984081564,-2.63786433591703,
134.957621322623));
#116221=CARTESIAN_POINT('Ctrl Pts',(-165.927615149759,-2.52037507671445,
135.027735161124));
#116222=CARTESIAN_POINT('Ctrl Pts',(-165.935379902706,-2.40303061252321,
135.097762590586));
#116223=CARTESIAN_POINT('Ctrl Pts',(-165.943144655653,-2.282611352077,135.162987711945));
#116224=CARTESIAN_POINT('Ctrl Pts',(-165.9509094086,-2.15954860847618,135.223131133233));
#116225=CARTESIAN_POINT('Ctrl Pts',(-165.958666449485,-2.03660809252719,
135.283214819227));
#116226=CARTESIAN_POINT('Ctrl Pts',(-165.96642349037,-1.91102966736331,
135.33822667878));
#116227=CARTESIAN_POINT('Ctrl Pts',(-165.974180531255,-1.78327140333194,
135.387931950551));
#116228=CARTESIAN_POINT('Ctrl Pts',(-165.981931722495,-1.65560948280146,
135.437599739189));
#116229=CARTESIAN_POINT('Ctrl Pts',(-165.989682913735,-1.52577135824068,
135.481968764081));
#116230=CARTESIAN_POINT('Ctrl Pts',(-165.997434104975,-1.39423702492319,
135.520851493295));
#116231=CARTESIAN_POINT('Ctrl Pts',(-166.005182001752,-1.26275859720598,
135.559717696311));
#116232=CARTESIAN_POINT('Ctrl Pts',(-166.012929898529,-1.12958576875664,
135.593102130866));
#116233=CARTESIAN_POINT('Ctrl Pts',(-166.020677795306,-0.99521551109569,
135.620866524235));
#116234=CARTESIAN_POINT('Ctrl Pts',(-166.02842407139,-0.860873360795957,
135.648625109891));
#116235=CARTESIAN_POINT('Ctrl Pts',(-166.036170347474,-0.725334662130575,
135.670765913614));
#116236=CARTESIAN_POINT('Ctrl Pts',(-166.043916623558,-0.589108058332495,
135.687201466714));
#116237=CARTESIAN_POINT('Ctrl Pts',(-166.051662956824,-0.452880448940758,
135.703637141138));
#116238=CARTESIAN_POINT('Ctrl Pts',(-166.059409290089,-0.315965312434059,
135.714367434072));
#116239=CARTESIAN_POINT('Ctrl Pts',(-166.067155623354,-0.178877522579107,
135.719356639377));
#116240=CARTESIAN_POINT('Ctrl Pts',(-166.074903691357,-0.0417590328643031,
135.72434696198));
#116241=CARTESIAN_POINT('Ctrl Pts',(-166.08265175936,0.0955317965049134,
135.723593624388));
#116242=CARTESIAN_POINT('Ctrl Pts',(-166.090399827363,0.232479374539408,
135.717113043947));
#116243=CARTESIAN_POINT('Ctrl Pts',(-166.098156130105,0.369572502089724,
135.710625575868));
#116244=CARTESIAN_POINT('Ctrl Pts',(-166.105912432846,0.506321258403937,
135.698398724047));
#116245=CARTESIAN_POINT('Ctrl Pts',(-166.113668735588,0.642213903302813,
135.680500931883));
#116246=CARTESIAN_POINT('Ctrl Pts',(-166.121429178102,0.77817907819792,
135.662593587128));
#116247=CARTESIAN_POINT('Ctrl Pts',(-166.129189620616,0.913286846248104,
135.639009338167));
#116248=CARTESIAN_POINT('Ctrl Pts',(-166.13695006313,1.0470359414843,135.609867749986));
#116249=CARTESIAN_POINT('Ctrl Pts',(-166.144722963396,1.18099974264222,
135.580679381141));
#116250=CARTESIAN_POINT('Ctrl Pts',(-166.152495863661,1.31360013412663,
135.545915945011));
#116251=CARTESIAN_POINT('Ctrl Pts',(-166.160268763926,1.44435042113434,
135.505747107046));
#116252=CARTESIAN_POINT('Ctrl Pts',(-166.167759099689,1.57034760588446,
135.467038507517));
#116253=CARTESIAN_POINT('Ctrl Pts',(-166.175249435452,1.69462657219126,
135.423310785273));
#116254=CARTESIAN_POINT('Ctrl Pts',(-166.182739771215,1.81677138920114,
135.37475718481));
#116255=CARTESIAN_POINT('Ctrl Pts',(-166.190514105334,1.94354736406204,
135.324362659833));
#116256=CARTESIAN_POINT('Ctrl Pts',(-166.198288439453,2.0684257506417,135.268609451688));
#116257=CARTESIAN_POINT('Ctrl Pts',(-166.206062773573,2.190920323137,135.207660652786));
#116258=CARTESIAN_POINT('Ctrl Pts',(-166.21382752652,2.31326393201936,135.146786967831));
#116259=CARTESIAN_POINT('Ctrl Pts',(-166.221592279467,2.4332292255688,135.080730604871));
#116260=CARTESIAN_POINT('Ctrl Pts',(-166.229357032414,2.5503480081424,135.00970342165));
#116261=CARTESIAN_POINT('Ctrl Pts',(-166.237114073299,2.66735046668975,
134.938746783629));
#116262=CARTESIAN_POINT('Ctrl Pts',(-166.244871114185,2.78151170837552,
134.862829351798));
#116263=CARTESIAN_POINT('Ctrl Pts',(-166.25262815507,2.89238662362302,134.782209619475));
#116264=CARTESIAN_POINT('Ctrl Pts',(-166.26037934631,3.00317792723491,134.701650683118));
#116265=CARTESIAN_POINT('Ctrl Pts',(-166.26813053755,3.11068752227287,134.616396733443));
#116266=CARTESIAN_POINT('Ctrl Pts',(-166.275881728791,3.21449818364169,
134.526750238477));
#116267=CARTESIAN_POINT('Ctrl Pts',(-166.283629625568,3.31826472271004,
134.437141845663));
#116268=CARTESIAN_POINT('Ctrl Pts',(-166.291377522345,3.41833515970329,
134.343144875771));
#116269=CARTESIAN_POINT('Ctrl Pts',(-166.299125419122,3.51432453661603,
134.245102705232));
#116270=CARTESIAN_POINT('Ctrl Pts',(-166.306871695207,3.6102938346204,134.147081043002));
#116271=CARTESIAN_POINT('Ctrl Pts',(-166.314617971291,3.70218349719951,
134.045016142387));
#116272=CARTESIAN_POINT('Ctrl Pts',(-166.322364247375,3.78964500037565,
133.939288660381));
#116273=CARTESIAN_POINT('Ctrl Pts',(-166.330110580641,3.87710714917261,
133.833560397919));
#116274=CARTESIAN_POINT('Ctrl Pts',(-166.337856913906,3.9601408241367,133.724169801366));
#116275=CARTESIAN_POINT('Ctrl Pts',(-166.345603247172,4.03843768283384,
133.611530748564));
#116276=CARTESIAN_POINT('Ctrl Pts',(-166.353351315175,4.11675207556993,
133.498866471027));
#116277=CARTESIAN_POINT('Ctrl Pts',(-166.361099383178,4.19032731810833,
133.382952610625));
#116278=CARTESIAN_POINT('Ctrl Pts',(-166.368847451181,4.25889853330216,
133.264231822637));
#116279=CARTESIAN_POINT('Ctrl Pts',(-166.376603753923,4.32754262679921,
133.145384856783));
#116280=CARTESIAN_POINT('Ctrl Pts',(-166.384360056665,4.39117187314136,
133.023725343098));
#116281=CARTESIAN_POINT('Ctrl Pts',(-166.392116359407,4.44956724763099,
132.899720818417));
#116282=CARTESIAN_POINT('Ctrl Pts',(-166.399876801921,4.50799378949023,
132.775650108787));
#116283=CARTESIAN_POINT('Ctrl Pts',(-166.407637244436,4.56118074171969,
132.64923225443));
#116284=CARTESIAN_POINT('Ctrl Pts',(-166.41539768695,4.6089577512274,132.520953612396));
#116285=CARTESIAN_POINT('Ctrl Pts',(-166.423170587216,4.65681145663234,
132.392469046098));
#116286=CARTESIAN_POINT('Ctrl Pts',(-166.430943487481,4.69923774380455,
132.262118094926));
#116287=CARTESIAN_POINT('Ctrl Pts',(-166.438716387747,4.7361162866634,132.130401937323));
#116288=CARTESIAN_POINT('Ctrl Pts',(-166.446206723507,4.77165420159061,
132.003473993847));
#116289=CARTESIAN_POINT('Ctrl Pts',(-166.453697059268,4.8020406473944,131.875278677785));
#116290=CARTESIAN_POINT('Ctrl Pts',(-166.461187395029,4.82721338535474,
131.746270376912));
#116291=CARTESIAN_POINT('Ctrl Pts',(-166.468961729148,4.85334055533075,
131.612370687077));
#116292=CARTESIAN_POINT('Ctrl Pts',(-166.476736063267,4.87393362057539,
131.47717099286));
#116293=CARTESIAN_POINT('Ctrl Pts',(-166.484510397386,4.88886697842848,
131.341168525231));
#116294=CARTESIAN_POINT('Ctrl Pts',(-166.492275150333,4.90378193225261,
131.205333668489));
#116295=CARTESIAN_POINT('Ctrl Pts',(-166.50003990328,4.91305101475983,131.068698391739));
#116296=CARTESIAN_POINT('Ctrl Pts',(-166.507804656227,4.91659939668784,
130.931771115519));
#116297=CARTESIAN_POINT('Ctrl Pts',(-166.515561697112,4.92014425431291,
130.794979837401));
#116298=CARTESIAN_POINT('Ctrl Pts',(-166.523318737997,4.91797970849462,
130.657897525268));
#116299=CARTESIAN_POINT('Ctrl Pts',(-166.531075778882,4.91008264438322,
130.521038384364));
#116300=CARTESIAN_POINT('Ctrl Pts',(-166.538826970123,4.90219153550928,
130.384282450003));
#116301=CARTESIAN_POINT('Ctrl Pts',(-166.546578161363,4.88857653531634,
130.247749740626));
#116302=CARTESIAN_POINT('Ctrl Pts',(-166.554329352603,4.86926659836753,
130.111954770882));
#116303=CARTESIAN_POINT('Ctrl Pts',(-166.56207724938,4.84996486865707,129.976217517622));
#116304=CARTESIAN_POINT('Ctrl Pts',(-166.569825146157,4.82497307130679,
129.84121776661));
#116305=CARTESIAN_POINT('Ctrl Pts',(-166.577573042934,4.79437201942716,
129.707464997266));
#116306=CARTESIAN_POINT('Ctrl Pts',(-166.585319319018,4.76377736862789,
129.573740206117));
#116307=CARTESIAN_POINT('Ctrl Pts',(-166.593065595103,4.72757588426715,
129.441262258685));
#116308=CARTESIAN_POINT('Ctrl Pts',(-166.600811871187,4.68589943813165,
129.310530132465));
#116309=CARTESIAN_POINT('Ctrl Pts',(-166.608558204452,4.64422268435015,
129.17979704121));
#116310=CARTESIAN_POINT('Ctrl Pts',(-166.616304537717,4.59707100689755,
129.050810169378));
#116311=CARTESIAN_POINT('Ctrl Pts',(-166.624050870983,4.54462594630597,
128.924052645275));
#116312=CARTESIAN_POINT('Ctrl Pts',(-166.631798938986,4.49216914100678,
128.797266734702));
#116313=CARTESIAN_POINT('Ctrl Pts',(-166.639547006989,4.43441674316936,
128.672711526498));
#116314=CARTESIAN_POINT('Ctrl Pts',(-166.647295074992,4.37159799864712,
128.550849135296));
#116315=CARTESIAN_POINT('Ctrl Pts',(-166.655051377734,4.3087124896154,128.428857227293));
#116316=CARTESIAN_POINT('Ctrl Pts',(-166.662807680476,4.2407500570566,128.309564201428));
#116317=CARTESIAN_POINT('Ctrl Pts',(-166.670563983218,4.16798566475193,
128.193407044459));
#116318=CARTESIAN_POINT('Ctrl Pts',(-166.678324425732,4.09518243590039,
128.077187890918));
#116319=CARTESIAN_POINT('Ctrl Pts',(-166.686084868246,4.01757236153604,
127.964108263468));
#116320=CARTESIAN_POINT('Ctrl Pts',(-166.69384531076,3.93547254761333,127.854574372856));
#116321=CARTESIAN_POINT('Ctrl Pts',(-166.701618211026,3.85324093978062,
127.744864648718));
#116322=CARTESIAN_POINT('Ctrl Pts',(-166.709391111291,3.76650543736798,
127.638712338639));
#116323=CARTESIAN_POINT('Ctrl Pts',(-166.717164011557,3.67562265680721,
127.536489575547));
#116324=CARTESIAN_POINT('Ctrl Pts',(-166.724654347318,3.58804369424514,
127.437982867383));
#116325=CARTESIAN_POINT('Ctrl Pts',(-166.73214468308,3.49661396033875,127.343125190251));
#116326=CARTESIAN_POINT('Ctrl Pts',(-166.739635018841,3.40168210284458,
127.252214515041));
#116327=CARTESIAN_POINT('Ctrl Pts',(-166.74740935296,3.30315087511524,127.157856933943));
#116328=CARTESIAN_POINT('Ctrl Pts',(-166.755183687079,3.20053459809648,
127.067452667768));
#116329=CARTESIAN_POINT('Ctrl Pts',(-166.762958021198,3.0941837149797,126.981376155074));
#116330=CARTESIAN_POINT('Ctrl Pts',(-166.770722774145,2.98796389982179,
126.89540572399));
#116331=CARTESIAN_POINT('Ctrl Pts',(-166.778487527092,2.878018937287,126.813752677777));
#116332=CARTESIAN_POINT('Ctrl Pts',(-166.786252280039,2.76473612893011,
126.736754786135));
#116333=CARTESIAN_POINT('Ctrl Pts',(-166.794009320924,2.65156583465549,
126.659833369885));
#116334=CARTESIAN_POINT('Ctrl Pts',(-166.801766361809,2.53506461320026,
126.587558125455));
#116335=CARTESIAN_POINT('Ctrl Pts',(-166.809523402694,2.41565258585925,
126.52022644052));
#116336=CARTESIAN_POINT('Ctrl Pts',(-166.817274593934,2.29633060805678,
126.452945530932));
#116337=CARTESIAN_POINT('Ctrl Pts',(-166.825025785174,2.17410253268466,
126.390600951777));
#116338=CARTESIAN_POINT('Ctrl Pts',(-166.832776976414,2.04941688613532,
126.333446450494));
#116339=CARTESIAN_POINT('Ctrl Pts',(-166.840524873191,1.92478423431202,
126.276316241399));
#116340=CARTESIAN_POINT('Ctrl Pts',(-166.848272769968,1.79769644346981,
126.22437188534));
#116341=CARTESIAN_POINT('Ctrl Pts',(-166.856020666745,1.66862583453439,
126.177820778029));
#116342=CARTESIAN_POINT('Ctrl Pts',(-166.863766942829,1.53958222438827,
126.131279408206));
#116343=CARTESIAN_POINT('Ctrl Pts',(-166.871513218913,1.40855698867826,
126.090129175737));
#116344=CARTESIAN_POINT('Ctrl Pts',(-166.879259494997,1.27604121122577,
126.054528842676));
#116345=CARTESIAN_POINT('Ctrl Pts',(-166.887005828262,1.1435244555721,126.018928246822));
#116346=CARTESIAN_POINT('Ctrl Pts',(-166.894752161527,1.00951751379776,
125.988877733562));
#116347=CARTESIAN_POINT('Ctrl Pts',(-166.902498494793,0.874524982520793,
125.964485710355));
#116348=CARTESIAN_POINT('Ctrl Pts',(-166.910246562795,0.739502220601866,
125.940088224724));
#116349=CARTESIAN_POINT('Ctrl Pts',(-166.917994630798,0.603493814642456,
125.921351820191));
#116350=CARTESIAN_POINT('Ctrl Pts',(-166.925742698801,0.46701246775624,
125.908333409976));
#116351=CARTESIAN_POINT('Ctrl Pts',(-166.933499001543,0.330386066870588,
125.89530116364));
#116352=CARTESIAN_POINT('Ctrl Pts',(-166.941255304285,0.193286110785362,
125.887999088571));
#116353=CARTESIAN_POINT('Ctrl Pts',(-166.949011607026,0.0562288734783581,
125.886432051972));
#116354=CARTESIAN_POINT('Ctrl Pts',(-166.95677204954,-0.0809015154032844,
125.884864178998));
#116355=CARTESIAN_POINT('Ctrl Pts',(-166.964532492055,-0.217988749482219,
125.88903743183));
#116356=CARTESIAN_POINT('Ctrl Pts',(-166.972292934569,-0.354519668638239,
125.898904587078));
#116357=CARTESIAN_POINT('Ctrl Pts',(-166.980065834834,-0.491269759345966,
125.90878758196));
#116358=CARTESIAN_POINT('Ctrl Pts',(-166.987838735099,-0.627461361889623,
125.924382700102));
#116359=CARTESIAN_POINT('Ctrl Pts',(-166.995611635364,-0.762588630404179,
125.945591056939));
#116360=CARTESIAN_POINT('Ctrl Pts',(-167.003101971128,-0.892803682366956,
125.966028436587));
#116361=CARTESIAN_POINT('Ctrl Pts',(-167.010592306891,-1.02203013714848,
125.991677969634));
#116362=CARTESIAN_POINT('Ctrl Pts',(-167.018082642654,-1.14982885077125,
126.022407389393));
#116363=CARTESIAN_POINT('Ctrl Pts',(-167.025856976774,-1.28247309144524,
126.054301924437));
#116364=CARTESIAN_POINT('Ctrl Pts',(-167.033631310893,-1.41399936523554,
126.091770190424));
#116365=CARTESIAN_POINT('Ctrl Pts',(-167.041405645012,-1.5439032232719,
126.134719742759));
#116366=CARTESIAN_POINT('Ctrl Pts',(-167.049170397959,-1.67364698641273,
126.177616363609));
#116367=CARTESIAN_POINT('Ctrl Pts',(-167.056935150907,-1.80177194453462,
126.22598070843));
#116368=CARTESIAN_POINT('Ctrl Pts',(-167.064699903854,-1.92778457647381,
126.279669502229));
#116369=CARTESIAN_POINT('Ctrl Pts',(-167.072456944739,-2.05367205089085,
126.333304971561));
#116370=CARTESIAN_POINT('Ctrl Pts',(-167.080213985624,-2.17745101687157,
126.392254213625));
#116371=CARTESIAN_POINT('Ctrl Pts',(-167.087971026509,-2.29864418792239,
126.45632451378));
#116372=CARTESIAN_POINT('Ctrl Pts',(-167.09572221775,-2.41974596626035,
126.520346498022));
#116373=CARTESIAN_POINT('Ctrl Pts',(-167.10347340899,-2.53826548672278,
126.589481671631));
#116374=CARTESIAN_POINT('Ctrl Pts',(-167.11122460023,-2.65374682493084,
126.663489833338));
#116375=CARTESIAN_POINT('Ctrl Pts',(-167.118972497007,-2.76917908048912,
126.737466539603));
#116376=CARTESIAN_POINT('Ctrl Pts',(-167.126720393785,-2.88157539362716,
126.816311904094));
#116377=CARTESIAN_POINT('Ctrl Pts',(-167.134468290562,-2.99050597546051,
126.89974065229));
#116378=CARTESIAN_POINT('Ctrl Pts',(-167.142214566646,-3.09941377136441,
126.98315194899));
#116379=CARTESIAN_POINT('Ctrl Pts',(-167.14996084273,-3.20485696774908,
127.071144484825));
#116380=CARTESIAN_POINT('Ctrl Pts',(-167.157707118815,-3.30643655079946,
127.163390911837));
#116381=CARTESIAN_POINT('Ctrl Pts',(-167.16545345208,-3.40801688368738,
127.255638019791));
#116382=CARTESIAN_POINT('Ctrl Pts',(-167.173199785346,-3.50573325690008,
127.352138818744));
#116383=CARTESIAN_POINT('Ctrl Pts',(-167.180946118611,-3.59922171737467,
127.452527374149));
#116384=CARTESIAN_POINT('Ctrl Pts',(-167.188694186614,-3.69273111394165,
127.552938410874));
#116385=CARTESIAN_POINT('Ctrl Pts',(-167.196442254618,-3.78201044732934,
127.657238650459));
#116386=CARTESIAN_POINT('Ctrl Pts',(-167.204190322621,-3.86673470627826,
127.765027504239));
#116387=CARTESIAN_POINT('Ctrl Pts',(-167.211946625363,-3.9515490111777,
127.872930917296));
#116388=CARTESIAN_POINT('Ctrl Pts',(-167.219702928105,-4.03179832885506,
127.984330043291));
#116389=CARTESIAN_POINT('Ctrl Pts',(-167.227459230847,-4.10719950570012,
128.098793157147));
#116390=CARTESIAN_POINT('Ctrl Pts',(-167.235219673361,-4.18264092642375,
128.213317363414));
#116391=CARTESIAN_POINT('Ctrl Pts',(-167.242980115875,-4.25322884918431,
128.330908481056));
#116392=CARTESIAN_POINT('Ctrl Pts',(-167.25074055839,-4.31872562877702,
128.451109248535));
#116393=CARTESIAN_POINT('Ctrl Pts',(-167.258513458655,-4.38432754961469,
128.571502972957));
#116394=CARTESIAN_POINT('Ctrl Pts',(-167.266286358921,-4.44482182288314,
128.694514367618));
#116395=CARTESIAN_POINT('Ctrl Pts',(-167.274059259186,-4.50001822092207,
128.819664400542));
#116396=CARTESIAN_POINT('Ctrl Pts',(-167.281549594947,-4.5532080908484,
128.940264914507));
#116397=CARTESIAN_POINT('Ctrl Pts',(-167.289039930707,-4.60147846758377,
129.062850989889));
#116398=CARTESIAN_POINT('Ctrl Pts',(-167.296530266468,-4.644703262792,129.186981669048));
#116399=CARTESIAN_POINT('Ctrl Pts',(-167.304374368132,-4.68996954975881,
129.316974996191));
#116400=CARTESIAN_POINT('Ctrl Pts',(-167.312218469795,-4.72980493418321,
129.448951471914));
#116401=CARTESIAN_POINT('Ctrl Pts',(-167.320062571459,-4.76405452823401,
129.582490119308));
#116402=CARTESIAN_POINT('Origin',(213.235140564004,0.,130.804360617566));
#116403=CARTESIAN_POINT('',(-169.415000431073,-4.76405452823411,129.582490119308));
#116404=CARTESIAN_POINT('',(-169.070032268681,-4.7640545282341,129.582490119308));
#116405=CARTESIAN_POINT('',(213.235140564004,-4.76405452823405,129.582490119308));
#116406=CARTESIAN_POINT('',(-167.735140564067,-4.91824875640079,130.807858139837));
#116407=CARTESIAN_POINT('Ctrl Pts',(-167.735140564067,-4.91824875640079,
130.807858139838));
#116408=CARTESIAN_POINT('Ctrl Pts',(-167.744004443693,-4.91813704849458,
130.964942849568));
#116409=CARTESIAN_POINT('Ctrl Pts',(-167.752868323319,-4.91049564785334,
131.121727305909));
#116410=CARTESIAN_POINT('Ctrl Pts',(-167.761732202945,-4.89543454578459,
131.277545222598));
#116411=CARTESIAN_POINT('Ctrl Pts',(-167.770638196226,-4.88030188610434,
131.434103454164));
#116412=CARTESIAN_POINT('Ctrl Pts',(-167.779544189507,-4.85767896409776,
131.589685791336));
#116413=CARTESIAN_POINT('Ctrl Pts',(-167.788450182788,-4.82772686809456,
131.743634991526));
#116414=CARTESIAN_POINT('Ctrl Pts',(-167.797410831803,-4.79759095724287,
131.898528971972));
#116415=CARTESIAN_POINT('Ctrl Pts',(-167.806371480818,-4.76003572865256,
132.051769562129));
#116416=CARTESIAN_POINT('Ctrl Pts',(-167.815332129834,-4.71527376576907,
132.202708348408));
#116417=CARTESIAN_POINT('Ctrl Pts',(-167.8215002592,-4.68446153584179,132.306608184075));
#116418=CARTESIAN_POINT('Ctrl Pts',(-167.827668388567,-4.65023550546441,
132.409417780665));
#116419=CARTESIAN_POINT('Ctrl Pts',(-167.833836517933,-4.61267790990394,
132.510931905847));
#116420=CARTESIAN_POINT('Ctrl Pts',(-167.841610852052,-4.56534017114263,
132.638880702002));
#116421=CARTESIAN_POINT('Ctrl Pts',(-167.849385186171,-4.51259975549616,
132.765061049956));
#116422=CARTESIAN_POINT('Ctrl Pts',(-167.85715952029,-4.45460804032886,
132.888982950157));
#116423=CARTESIAN_POINT('Ctrl Pts',(-167.864924273237,-4.3966877947678,
133.012752127691));
#116424=CARTESIAN_POINT('Ctrl Pts',(-167.872689026184,-4.33352929067561,
133.134268044771));
#116425=CARTESIAN_POINT('Ctrl Pts',(-167.880453779131,-4.26533308938072,
133.253057556579));
#116426=CARTESIAN_POINT('Ctrl Pts',(-167.888210820016,-4.19720462151417,
133.371729084971));
#116427=CARTESIAN_POINT('Ctrl Pts',(-167.895967860901,-4.12404860705336,
133.487679260074));
#116428=CARTESIAN_POINT('Ctrl Pts',(-167.903724901786,-4.04611278347342,
133.600456897366));
#116429=CARTESIAN_POINT('Ctrl Pts',(-167.911476093026,-3.96823573190462,
133.713149488164));
#116430=CARTESIAN_POINT('Ctrl Pts',(-167.919227284266,-3.88558626710797,
133.822673982814));
#116431=CARTESIAN_POINT('Ctrl Pts',(-167.926978475507,-3.79845675775636,
133.928606017972));
#116432=CARTESIAN_POINT('Ctrl Pts',(-167.934726372284,-3.71136428077037,
134.034493029188));
#116433=CARTESIAN_POINT('Ctrl Pts',(-167.942474269061,-3.6197957942505,
134.136790316466));
#116434=CARTESIAN_POINT('Ctrl Pts',(-167.950222165838,-3.52408533781213,
134.235104792569));
#116435=CARTESIAN_POINT('Ctrl Pts',(-167.957968441922,-3.42839490193797,
134.333398703403));
#116436=CARTESIAN_POINT('Ctrl Pts',(-167.965714718006,-3.32856449203041,
134.42771118022));
#116437=CARTESIAN_POINT('Ctrl Pts',(-167.97346099409,-3.2249662918492,134.517684664688));
#116438=CARTESIAN_POINT('Ctrl Pts',(-167.981207327355,-3.12136732692946,
134.607658813321));
#116439=CARTESIAN_POINT('Ctrl Pts',(-167.98895366062,-3.01400081141961,
134.693293649332));
#116440=CARTESIAN_POINT('Ctrl Pts',(-167.996699993886,-2.90327310460602,
134.774270987155));
#116441=CARTESIAN_POINT('Ctrl Pts',(-168.004448061889,-2.79252060109037,
134.855266459292));
#116442=CARTESIAN_POINT('Ctrl Pts',(-168.012196129892,-2.678405723973,134.931602127018));
#116443=CARTESIAN_POINT('Ctrl Pts',(-168.019944197895,-2.56136464473602,
135.003002566958));
#116444=CARTESIAN_POINT('Ctrl Pts',(-168.027700500637,-2.44419917284739,
135.074478892136));
#116445=CARTESIAN_POINT('Ctrl Pts',(-168.035456803378,-2.32410162056808,
135.141009307704));
#116446=CARTESIAN_POINT('Ctrl Pts',(-168.04321310612,-2.20153413410475,
135.202363632444));
#116447=CARTESIAN_POINT('Ctrl Pts',(-168.050973548634,-2.07890122968346,
135.263750703834));
#116448=CARTESIAN_POINT('Ctrl Pts',(-168.058733991148,-1.95379612075027,
135.319956019468));
#116449=CARTESIAN_POINT('Ctrl Pts',(-168.066494433663,-1.82670093629337,
135.370797604085));
#116450=CARTESIAN_POINT('Ctrl Pts',(-168.074267333928,-1.69940172736305,
135.421720804126));
#116451=CARTESIAN_POINT('Ctrl Pts',(-168.082040234193,-1.57010642795901,
135.467262936989));
#116452=CARTESIAN_POINT('Ctrl Pts',(-168.089813134459,-1.43931318470221,
135.507291684342));
#116453=CARTESIAN_POINT('Ctrl Pts',(-168.097303470221,-1.31327460527724,
135.545865285904));
#116454=CARTESIAN_POINT('Ctrl Pts',(-168.104793805984,-1.18584539718265,
135.579319315285));
#116455=CARTESIAN_POINT('Ctrl Pts',(-168.112284141746,-1.0574783237846,
135.607580647632));
#116456=CARTESIAN_POINT('Ctrl Pts',(-168.120058475865,-0.924244173791153,
135.636913516983));
#116457=CARTESIAN_POINT('Ctrl Pts',(-168.127832809984,-0.789577590530997,
135.660745071809));
#116458=CARTESIAN_POINT('Ctrl Pts',(-168.135607144103,-0.653972647666248,
135.678937813447));
#116459=CARTESIAN_POINT('Ctrl Pts',(-168.14337189705,-0.518534825774218,
135.697108134158));
#116460=CARTESIAN_POINT('Ctrl Pts',(-168.151136649998,-0.382161329030799,
135.709653417296));
#116461=CARTESIAN_POINT('Ctrl Pts',(-168.158901402945,-0.245358635866684,
135.716486654457));
#116462=CARTESIAN_POINT('Ctrl Pts',(-168.16665844383,-0.108691817066,135.723313104751));
#116463=CARTESIAN_POINT('Ctrl Pts',(-168.174415484715,0.0284029618794884,
135.724438779783));
#116464=CARTESIAN_POINT('Ctrl Pts',(-168.1821725256,0.165412198495755,135.719828231851));
#116465=CARTESIAN_POINT('Ctrl Pts',(-168.18992371684,0.302318115381099,
135.71522116077));
#116466=CARTESIAN_POINT('Ctrl Pts',(-168.19767490808,0.439138229173773,
135.704886489924));
#116467=CARTESIAN_POINT('Ctrl Pts',(-168.20542609932,0.575357478565201,
135.688840818607));
#116468=CARTESIAN_POINT('Ctrl Pts',(-168.213173996097,0.711518831141686,
135.672801967128));
#116469=CARTESIAN_POINT('Ctrl Pts',(-168.220921892874,0.847079439787187,
135.651056988588));
#116470=CARTESIAN_POINT('Ctrl Pts',(-168.228669789651,0.981528032506999,
135.623674446723));
#116471=CARTESIAN_POINT('Ctrl Pts',(-168.236416065735,1.11594850147996,
135.596297632696));
#116472=CARTESIAN_POINT('Ctrl Pts',(-168.244162341819,1.24925703434299,
135.563285678925));
#116473=CARTESIAN_POINT('Ctrl Pts',(-168.251908617903,1.38095163273355,
135.524758445138));
#116474=CARTESIAN_POINT('Ctrl Pts',(-168.259654951168,1.51264720326353,
135.486230926952));
#116475=CARTESIAN_POINT('Ctrl Pts',(-168.267401284434,1.64272844031071,
135.442188157287));
#116476=CARTESIAN_POINT('Ctrl Pts',(-168.275147617699,1.77070799822673,
135.392800030647));
#116477=CARTESIAN_POINT('Ctrl Pts',(-168.282895685702,1.89871621627722,
135.343400843879));
#116478=CARTESIAN_POINT('Ctrl Pts',(-168.290643753705,2.02462145396681,
135.288654058866));
#116479=CARTESIAN_POINT('Ctrl Pts',(-168.298391821708,2.14795622846961,
135.228777765969));
#116480=CARTESIAN_POINT('Ctrl Pts',(-168.30614812445,2.27142208463862,135.168837835834));
#116481=CARTESIAN_POINT('Ctrl Pts',(-168.313904427192,2.39231166804874,
135.103757678471));
#116482=CARTESIAN_POINT('Ctrl Pts',(-168.321660729933,2.51018151940827,
135.033801692001));
#116483=CARTESIAN_POINT('Ctrl Pts',(-168.329421172448,2.62811428145648,
134.963808367915));
#116484=CARTESIAN_POINT('Ctrl Pts',(-168.337181614962,2.74302377255823,
134.8889342426));
#116485=CARTESIAN_POINT('Ctrl Pts',(-168.344942057476,2.85449628927647,
134.809486582752));
#116486=CARTESIAN_POINT('Ctrl Pts',(-168.352714957741,2.96614775157461,
134.729911386468));
#116487=CARTESIAN_POINT('Ctrl Pts',(-168.360487858007,3.07435090531329,
134.645748224486));
#116488=CARTESIAN_POINT('Ctrl Pts',(-168.368260758272,3.17872516691717,
134.557344680376));
#116489=CARTESIAN_POINT('Ctrl Pts',(-168.375751094034,3.27930516120885,
134.47215482777));
#116490=CARTESIAN_POINT('Ctrl Pts',(-168.383241429796,3.37632958319387,
134.383027746063));
#116491=CARTESIAN_POINT('Ctrl Pts',(-168.390731765558,3.46949218120573,
134.29030483213));
#116492=CARTESIAN_POINT('Ctrl Pts',(-168.398506099677,3.56618706743725,
134.194066300733));
#116493=CARTESIAN_POINT('Ctrl Pts',(-168.406280433796,3.65902780712314,
134.093649027781));
#116494=CARTESIAN_POINT('Ctrl Pts',(-168.414054767915,3.74763165986214,
133.989394370056));
#116495=CARTESIAN_POINT('Ctrl Pts',(-168.421819520862,3.8361263162714,133.885268196878));
#116496=CARTESIAN_POINT('Ctrl Pts',(-168.42958427381,3.92039422437408,133.777314343742));
#116497=CARTESIAN_POINT('Ctrl Pts',(-168.437349026757,4.00008841757219,
133.665911895126));
#116498=CARTESIAN_POINT('Ctrl Pts',(-168.445106067642,4.07970345737412,
133.554620092993));
#116499=CARTESIAN_POINT('Ctrl Pts',(-168.452863108527,4.15475359640531,
133.439886827591));
#116500=CARTESIAN_POINT('Ctrl Pts',(-168.460620149412,4.2249314508805,133.322124962746));
#116501=CARTESIAN_POINT('Ctrl Pts',(-168.468371340652,4.29505638368982,
133.20445190304));
#116502=CARTESIAN_POINT('Ctrl Pts',(-168.476122531892,4.36031614593633,
133.083755124329));
#116503=CARTESIAN_POINT('Ctrl Pts',(-168.483873723132,4.42044629985622,
132.960476934602));
#116504=CARTESIAN_POINT('Ctrl Pts',(-168.491621619909,4.48055089685675,
132.837251141394));
#116505=CARTESIAN_POINT('Ctrl Pts',(-168.499369516686,4.53553005078597,
132.711446470012));
#116506=CARTESIAN_POINT('Ctrl Pts',(-168.507117413463,4.58516509125597,
132.583530128441));
#116507=CARTESIAN_POINT('Ctrl Pts',(-168.514863689547,4.63478974914537,
132.455640544211));
#116508=CARTESIAN_POINT('Ctrl Pts',(-168.522609965632,4.67907237574544,
132.325640532646));
#116509=CARTESIAN_POINT('Ctrl Pts',(-168.530356241716,4.71784247006198,
132.194017226293));
#116510=CARTESIAN_POINT('Ctrl Pts',(-168.538102574981,4.75661285057061,
132.062392948328));
#116511=CARTESIAN_POINT('Ctrl Pts',(-168.545848908246,4.78987050712963,
131.929145726699));
#116512=CARTESIAN_POINT('Ctrl Pts',(-168.553595241512,4.81749495457136,
131.794777411234));
#116513=CARTESIAN_POINT('Ctrl Pts',(-168.561343309515,4.84512558831652,
131.660379004917));
#116514=CARTESIAN_POINT('Ctrl Pts',(-168.569091377518,4.86712042395351,
131.524859388063));
#116515=CARTESIAN_POINT('Ctrl Pts',(-168.576839445521,4.88341026119186,
131.38872975038));
#116516=CARTESIAN_POINT('Ctrl Pts',(-168.584595748263,4.8997174114631,131.252455432499));
#116517=CARTESIAN_POINT('Ctrl Pts',(-168.592352051005,4.91030740463335,
131.115570187479));
#116518=CARTESIAN_POINT('Ctrl Pts',(-168.600108353747,4.91516298575077,
130.978590023826));
#116519=CARTESIAN_POINT('Ctrl Pts',(-168.607868796261,4.92002115843803,
130.841536749735));
#116520=CARTESIAN_POINT('Ctrl Pts',(-168.615629238775,4.91913882302528,
130.704388846829));
#116521=CARTESIAN_POINT('Ctrl Pts',(-168.623389681289,4.91255087487469,
130.567660460684));
#116522=CARTESIAN_POINT('Ctrl Pts',(-168.631162581554,4.90595235116488,
130.430712585995));
#116523=CARTESIAN_POINT('Ctrl Pts',(-168.63893548182,4.89362994696933,130.294185963431));
#116524=CARTESIAN_POINT('Ctrl Pts',(-168.646708382085,4.87567037947153,
130.158588666144));
#116525=CARTESIAN_POINT('Ctrl Pts',(-168.654198717847,4.85836368748974,
130.027920672162));
#116526=CARTESIAN_POINT('Ctrl Pts',(-168.66168905361,4.83582261947571,129.898115913359));
#116527=CARTESIAN_POINT('Ctrl Pts',(-168.669179389372,4.80816886578278,
129.769616581286));
#116528=CARTESIAN_POINT('Ctrl Pts',(-168.676953723491,4.77946661161336,
129.636245157981));
#116529=CARTESIAN_POINT('Ctrl Pts',(-168.68472805761,4.74516540347589,129.503857625438));
#116530=CARTESIAN_POINT('Ctrl Pts',(-168.692502391729,4.70534555396082,
129.372960505675));
#116531=CARTESIAN_POINT('Ctrl Pts',(-168.700267144676,4.66557477885148,
129.242224704914));
#116532=CARTESIAN_POINT('Ctrl Pts',(-168.708031897623,4.62029900748321,
129.112976032696));
#116533=CARTESIAN_POINT('Ctrl Pts',(-168.71579665057,4.56964963044401,128.985711306268));
#116534=CARTESIAN_POINT('Ctrl Pts',(-168.723553691455,4.51905055908011,
128.858572980962));
#116535=CARTESIAN_POINT('Ctrl Pts',(-168.73131073234,4.46308864683044,128.733415040999));
#116536=CARTESIAN_POINT('Ctrl Pts',(-168.739067773225,4.40194509928063,
128.610719260047));
#116537=CARTESIAN_POINT('Ctrl Pts',(-168.746818964465,4.34084766055557,
128.488116004937));
#116538=CARTESIAN_POINT('Ctrl Pts',(-168.754570155705,4.27457653786798,
128.367971561631));
#116539=CARTESIAN_POINT('Ctrl Pts',(-168.762321346945,4.20336092238527,
128.250747487379));
#116540=CARTESIAN_POINT('Ctrl Pts',(-168.770069243723,4.13217557543898,
128.133573236486));
#116541=CARTESIAN_POINT('Ctrl Pts',(-168.7778171405,4.0560501180718,128.019317219363));
#116542=CARTESIAN_POINT('Ctrl Pts',(-168.785565037277,3.97525942890647,
127.908415946929));
#116543=CARTESIAN_POINT('Ctrl Pts',(-168.793311313361,3.89448563941166,
127.79753787265));
#116544=CARTESIAN_POINT('Ctrl Pts',(-168.801057589445,3.80904878923027,
127.690013463064));
#116545=CARTESIAN_POINT('Ctrl Pts',(-168.808803865529,3.7192665568207,127.586249472528));
#116546=CARTESIAN_POINT('Ctrl Pts',(-168.816550198794,3.62948366165896,
127.48248471603));
#116547=CARTESIAN_POINT('Ctrl Pts',(-168.82429653206,3.53535557607895,127.382480729627));
#116548=CARTESIAN_POINT('Ctrl Pts',(-168.832042865325,3.43723939537676,
127.286610142991));
#116549=CARTESIAN_POINT('Ctrl Pts',(-168.839790933328,3.33910124223633,
127.190718086803));
#116550=CARTESIAN_POINT('Ctrl Pts',(-168.847539001331,3.23697349637781,
127.098961545496));
#116551=CARTESIAN_POINT('Ctrl Pts',(-168.855287069334,3.1312488317325,127.011675049756));
#116552=CARTESIAN_POINT('Ctrl Pts',(-168.863043372076,3.02541180165561,
126.92429578489));
#116553=CARTESIAN_POINT('Ctrl Pts',(-168.870799674817,2.91597051821281,
126.841396305171));
#116554=CARTESIAN_POINT('Ctrl Pts',(-168.878555977559,2.8033497872499,126.763270042879));
#116555=CARTESIAN_POINT('Ctrl Pts',(-168.886316420073,2.69066894721163,
126.685102082248));
#116556=CARTESIAN_POINT('Ctrl Pts',(-168.894076862588,2.57480560842427,
126.611712624476));
#116557=CARTESIAN_POINT('Ctrl Pts',(-168.901837305102,2.45621119791615,
126.543350219347));
#116558=CARTESIAN_POINT('Ctrl Pts',(-168.909610205367,2.33742640913197,
126.474878072817));
#116559=CARTESIAN_POINT('Ctrl Pts',(-168.917383105633,2.21590213447506,
126.411449286111));
#116560=CARTESIAN_POINT('Ctrl Pts',(-168.925156005898,2.09211270303249,
126.353265527556));
#116561=CARTESIAN_POINT('Ctrl Pts',(-168.93264634166,1.97282332922927,126.297196895181));
#116562=CARTESIAN_POINT('Ctrl Pts',(-168.940136677422,1.85143091152834,
126.245998691306));
#116563=CARTESIAN_POINT('Ctrl Pts',(-168.947627013184,1.72837325481305,
126.199807549727));
#116564=CARTESIAN_POINT('Ctrl Pts',(-168.955401347303,1.60064982964137,
126.151865056975));
#116565=CARTESIAN_POINT('Ctrl Pts',(-168.963175681422,1.47072780825174,
126.109164939757));
#116566=CARTESIAN_POINT('Ctrl Pts',(-168.970950015542,1.33907675287918,
126.071913416339));
#116567=CARTESIAN_POINT('Ctrl Pts',(-168.978714768489,1.20758794566637,
126.034707802095));
#116568=CARTESIAN_POINT('Ctrl Pts',(-168.986479521436,1.07437471687023,
126.002937526415));
#116569=CARTESIAN_POINT('Ctrl Pts',(-168.994244274383,0.93992607273314,
125.976760588535));
#116570=CARTESIAN_POINT('Ctrl Pts',(-169.002001315268,0.805610964884803,
125.950609649959));
#116571=CARTESIAN_POINT('Ctrl Pts',(-169.009758356153,0.670063264820346,
125.930041067956));
#116572=CARTESIAN_POINT('Ctrl Pts',(-169.017515397038,0.533786248415471,
125.915162799569));
#116573=CARTESIAN_POINT('Ctrl Pts',(-169.025266588278,0.397611999568561,
125.900295751001));
#116574=CARTESIAN_POINT('Ctrl Pts',(-169.033017779518,0.260709916172463,
125.891110517115));
#116575=CARTESIAN_POINT('Ctrl Pts',(-169.040768970758,0.12359220283955,
125.887663755861));
#116576=CARTESIAN_POINT('Ctrl Pts',(-169.048516867535,-0.0134672318076487,
125.884218459573));
#116577=CARTESIAN_POINT('Ctrl Pts',(-169.056264764312,-0.150741724086354,
125.886506794728));
#116578=CARTESIAN_POINT('Ctrl Pts',(-169.064012661089,-0.287715446388911,
125.894533442969));
#116579=CARTESIAN_POINT('Ctrl Pts',(-169.071758937174,-0.424660516741201,
125.902558412209));
#116580=CARTESIAN_POINT('Ctrl Pts',(-169.079505213258,-0.561304552209544,
125.916319284153));
#116581=CARTESIAN_POINT('Ctrl Pts',(-169.087251489342,-0.697133625866751,
125.935768647583));
#116582=CARTESIAN_POINT('Ctrl Pts',(-169.094997822607,-0.832963702183509,
125.955218154584));
#116583=CARTESIAN_POINT('Ctrl Pts',(-169.102744155873,-0.967978417667158,
125.980356181444));
#116584=CARTESIAN_POINT('Ctrl Pts',(-169.110490489138,-1.10167124968987,
126.011083709218));
#116585=CARTESIAN_POINT('Ctrl Pts',(-169.118238557141,-1.23539402129518,
126.041818118208));
#116586=CARTESIAN_POINT('Ctrl Pts',(-169.125986625144,-1.367793939423,126.078144431352));
#116587=CARTESIAN_POINT('Ctrl Pts',(-169.133734693147,-1.49837730407996,
126.119913102958));
#116588=CARTESIAN_POINT('Ctrl Pts',(-169.141490995889,-1.62909945429102,
126.161726166805));
#116589=CARTESIAN_POINT('Ctrl Pts',(-169.149247298631,-1.75800082136722,
126.208993024383));
#116590=CARTESIAN_POINT('Ctrl Pts',(-169.157003601373,-1.88460491448449,
126.261514881818));
#116591=CARTESIAN_POINT('Ctrl Pts',(-169.164764043887,-2.01127658001824,
126.31406477175));
#116592=CARTESIAN_POINT('Ctrl Pts',(-169.172524486401,-2.13564817407344,
126.371875085529));
#116593=CARTESIAN_POINT('Ctrl Pts',(-169.180284928915,-2.25726657734122,
126.434700372041));
#116594=CARTESIAN_POINT('Ctrl Pts',(-169.188057829181,-2.3790802132667,
126.497626511281));
#116595=CARTESIAN_POINT('Ctrl Pts',(-169.195830729446,-2.49813148676619,
126.565583516747));
#116596=CARTESIAN_POINT('Ctrl Pts',(-169.203603629711,-2.61399434210779,
126.638281328603));
#116597=CARTESIAN_POINT('Ctrl Pts',(-169.211093965474,-2.72564529081649,
126.708336391882));
#116598=CARTESIAN_POINT('Ctrl Pts',(-169.218584301236,-2.83433535668576,
126.782793391126));
#116599=CARTESIAN_POINT('Ctrl Pts',(-169.226074636998,-2.93971294160209,
126.861357842589));
#116600=CARTESIAN_POINT('Ctrl Pts',(-169.233946545084,-3.05045866638537,
126.943924520563));
#116601=CARTESIAN_POINT('Ctrl Pts',(-169.24181845317,-3.1579198704667,127.031307420539));
#116602=CARTESIAN_POINT('Ctrl Pts',(-169.249690361257,-3.2616447690163,
127.123211820893));
#116603=CARTESIAN_POINT('Ctrl Pts',(-169.257377057583,-3.36292920829519,
127.21295387692));
#116604=CARTESIAN_POINT('Ctrl Pts',(-169.265063753909,-3.46065084826931,
127.307006786171));
#116605=CARTESIAN_POINT('Ctrl Pts',(-169.272750450235,-3.55441752683353,
127.40505199559));
#116606=CARTESIAN_POINT('Ctrl Pts',(-169.280430166204,-3.64809905504815,
127.503008169288));
#116607=CARTESIAN_POINT('Ctrl Pts',(-169.288109882173,-3.73783248956393,
127.604949147311));
#116608=CARTESIAN_POINT('Ctrl Pts',(-169.295789598142,-3.82325977803816,
127.710517096614));
#116609=CARTESIAN_POINT('Ctrl Pts',(-169.303464084568,-3.90862889435205,
127.816013158868));
#116610=CARTESIAN_POINT('Ctrl Pts',(-169.311138570994,-3.9896974468948,
127.925130970572));
#116611=CARTESIAN_POINT('Ctrl Pts',(-169.318813057421,-4.06614557213797,
128.037477308013));
#116612=CARTESIAN_POINT('Ctrl Pts',(-169.326828671892,-4.14599178789105,
128.15481739804));
#116613=CARTESIAN_POINT('Ctrl Pts',(-169.334844286363,-4.22079706390486,
128.275679301211));
#116614=CARTESIAN_POINT('Ctrl Pts',(-169.342859900834,-4.29024528215741,
128.399578198837));
#116615=CARTESIAN_POINT('Ctrl Pts',(-169.350530325816,-4.35670273843905,
128.518141436017));
#116616=CARTESIAN_POINT('Ctrl Pts',(-169.358200750799,-4.41825472573536,
128.639485156536));
#116617=CARTESIAN_POINT('Ctrl Pts',(-169.365871175782,-4.47467010225927,
128.763157409052));
#116618=CARTESIAN_POINT('Ctrl Pts',(-169.373541492086,-4.5310846794608,
128.886827909315));
#116619=CARTESIAN_POINT('Ctrl Pts',(-169.381211808389,-4.58236263087159,
129.012826509912));
#116620=CARTESIAN_POINT('Ctrl Pts',(-169.388882124693,-4.62832047033365,
129.140680153537));
#116621=CARTESIAN_POINT('Ctrl Pts',(-169.396555634837,-4.67429744616276,
129.268587034092));
#116622=CARTESIAN_POINT('Ctrl Pts',(-169.404229144981,-4.71494976119077,
129.398350120979));
#116623=CARTESIAN_POINT('Ctrl Pts',(-169.411902655125,-4.75014347914318,
129.529480234921));
#116624=CARTESIAN_POINT('Ctrl Pts',(-169.412935247108,-4.75487934973022,
129.547125862772));
#116625=CARTESIAN_POINT('Ctrl Pts',(-169.41396783909,-4.75951645143451,
129.564796226742));
#116626=CARTESIAN_POINT('Ctrl Pts',(-169.415000431073,-4.76405452823411,
129.582490119308));
#116627=CARTESIAN_POINT('Ctrl Pts',(-167.665279524992,-4.76405452823393,
129.582490119308));
#116628=CARTESIAN_POINT('Ctrl Pts',(-167.673050734313,-4.79825694479428,
129.715844822382));
#116629=CARTESIAN_POINT('Ctrl Pts',(-167.680821943635,-4.8268704708693,
129.850693554765));
#116630=CARTESIAN_POINT('Ctrl Pts',(-167.688593152957,-4.84977697819716,
129.986530363633));
#116631=CARTESIAN_POINT('Ctrl Pts',(-167.696364556538,-4.87268405812648,
130.122370568057));
#116632=CARTESIAN_POINT('Ctrl Pts',(-167.70413596012,-4.88988375899316,
130.259198518599));
#116633=CARTESIAN_POINT('Ctrl Pts',(-167.711907363701,-4.90130916849556,
130.396498511798));
#116634=CARTESIAN_POINT('Ctrl Pts',(-167.719651763805,-4.91269487786053,
130.533321425502));
#116635=CARTESIAN_POINT('Ctrl Pts',(-167.727396163908,-4.91834635593093,
130.670612723358));
#116636=CARTESIAN_POINT('Ctrl Pts',(-167.735140564012,-4.91824875640148,
130.807858138868));
#116637=CARTESIAN_POINT('',(-167.389859435942,-4.91824852129168,130.800546785874));
#116638=CARTESIAN_POINT('Ctrl Pts',(-167.320062571459,-4.76405452823401,
129.582490119308));
#116639=CARTESIAN_POINT('Ctrl Pts',(-167.329148264296,-4.8037252648817,
129.73716571941));
#116640=CARTESIAN_POINT('Ctrl Pts',(-167.338233957133,-4.83590090763201,
129.893937563884));
#116641=CARTESIAN_POINT('Ctrl Pts',(-167.34731964997,-4.86038414129069,
130.052131223305));
#116642=CARTESIAN_POINT('Ctrl Pts',(-167.356327141138,-4.88465664476358,
130.208963290556));
#116643=CARTESIAN_POINT('Ctrl Pts',(-167.365334632306,-4.90136851684252,
130.367192697347));
#116644=CARTESIAN_POINT('Ctrl Pts',(-167.374342123475,-4.9103744866449,
130.526142243969));
#116645=CARTESIAN_POINT('Ctrl Pts',(-167.379514560964,-4.915546050509,130.617417003885));
#116646=CARTESIAN_POINT('Ctrl Pts',(-167.384686998453,-4.91817747662585,
130.708928866947));
#116647=CARTESIAN_POINT('Ctrl Pts',(-167.389859435942,-4.91824852129168,
130.800546785875));
#116648=CARTESIAN_POINT('Ctrl Pts',(-167.389859435994,-4.9182485212924,
130.800546786799));
#116649=CARTESIAN_POINT('Ctrl Pts',(-167.397603431916,-4.91835488690249,
130.937713991253));
#116650=CARTESIAN_POINT('Ctrl Pts',(-167.405347427839,-4.91271867954416,
131.074947458596));
#116651=CARTESIAN_POINT('Ctrl Pts',(-167.413091423761,-4.90135005703395,
131.21173106435));
#116652=CARTESIAN_POINT('Ctrl Pts',(-167.420834249603,-4.88998315226744,
131.348494002765));
#116653=CARTESIAN_POINT('Ctrl Pts',(-167.428577075445,-4.87288558719664,
131.484806825541));
#116654=CARTESIAN_POINT('Ctrl Pts',(-167.436319901287,-4.85011953972756,
131.620156862258));
#116655=CARTESIAN_POINT('Ctrl Pts',(-167.44406323119,-4.82735201017931,
131.755515710318));
#116656=CARTESIAN_POINT('Ctrl Pts',(-167.451806561093,-4.79891532830318,
131.88991126219));
#116657=CARTESIAN_POINT('Ctrl Pts',(-167.459549890996,-4.76492304045049,
132.022839784841));
#116658=CARTESIAN_POINT('Ctrl Pts',(-167.467295399081,-4.73092119064166,
132.155805699995));
#116659=CARTESIAN_POINT('Ctrl Pts',(-167.475040907166,-4.69136072150968,
132.287303386235));
#116660=CARTESIAN_POINT('Ctrl Pts',(-167.482786415251,-4.64640530396952,
132.416843427938));
#116661=CARTESIAN_POINT('Ctrl Pts',(-167.490540833312,-4.60139817236386,
132.546532484878));
#116662=CARTESIAN_POINT('Ctrl Pts',(-167.498295251373,-4.5509838239062,
132.674259029234));
#116663=CARTESIAN_POINT('Ctrl Pts',(-167.506049669435,-4.49537466340656,
132.799552262021));
#116664=CARTESIAN_POINT('Ctrl Pts',(-167.513808603169,-4.43973311971965,
132.924918457503));
#116665=CARTESIAN_POINT('Ctrl Pts',(-167.521567536903,-4.37889091000552,
133.047848168369));
#116666=CARTESIAN_POINT('Ctrl Pts',(-167.529326470637,-4.31310637938491,
133.167895348136));
#116667=CARTESIAN_POINT('Ctrl Pts',(-167.537098448307,-4.24721125506443,
133.288144345284));
#116668=CARTESIAN_POINT('Ctrl Pts',(-167.544870425977,-4.17635740882347,
133.405500793338));
#116669=CARTESIAN_POINT('Ctrl Pts',(-167.552642403647,-4.10084699031093,
133.519546987699));
#116670=CARTESIAN_POINT('Ctrl Pts',(-167.560087565858,-4.02851182179512,
133.628797483859));
#116671=CARTESIAN_POINT('Ctrl Pts',(-167.567532728069,-3.95190395140043,
133.735010250059));
#116672=CARTESIAN_POINT('Ctrl Pts',(-167.57497789028,-3.87132228266898,
133.837848189027));
#116673=CARTESIAN_POINT('Ctrl Pts',(-167.582752224399,-3.78717786797176,
133.945232887301));
#116674=CARTESIAN_POINT('Ctrl Pts',(-167.590526558518,-3.69842875172925,
134.049283961385));
#116675=CARTESIAN_POINT('Ctrl Pts',(-167.598300892637,-3.60536869646458,
134.149581032584));
#116676=CARTESIAN_POINT('Ctrl Pts',(-167.606065645584,-3.512423329401,134.249754496607));
#116677=CARTESIAN_POINT('Ctrl Pts',(-167.613830398531,-3.41517785766535,
134.346182879199));
#116678=CARTESIAN_POINT('Ctrl Pts',(-167.621595151478,-3.3139677326115,
134.438476869106));
#116679=CARTESIAN_POINT('Ctrl Pts',(-167.629352192362,-3.21285813088094,
134.530679191322));
#116680=CARTESIAN_POINT('Ctrl Pts',(-167.637109233247,-3.10779199914807,
134.618755030917));
#116681=CARTESIAN_POINT('Ctrl Pts',(-167.644866274132,-2.99914300675604,
134.702350392761));
#116682=CARTESIAN_POINT('Ctrl Pts',(-167.652617465372,-2.8905759474145,
134.785882714693));
#116683=CARTESIAN_POINT('Ctrl Pts',(-167.660368656612,-2.77843171391658,
134.864941046652));
#116684=CARTESIAN_POINT('Ctrl Pts',(-167.668119847852,-2.66311828597941,
134.939210561322));
#116685=CARTESIAN_POINT('Ctrl Pts',(-167.675867744629,-2.54785386932473,
135.013448509468));
#116686=CARTESIAN_POINT('Ctrl Pts',(-167.683615641406,-2.42942326529795,
135.082901477276));
#116687=CARTESIAN_POINT('Ctrl Pts',(-167.691363538183,-2.30826458485462,
135.147297143559));
#116688=CARTESIAN_POINT('Ctrl Pts',(-167.699109814267,-2.1871312481957,
135.211679339657));
#116689=CARTESIAN_POINT('Ctrl Pts',(-167.706856090351,-2.06327131519712,
135.271006155033));
#116690=CARTESIAN_POINT('Ctrl Pts',(-167.714602366435,-1.93714837114832,
135.325050747475));
#116691=CARTESIAN_POINT('Ctrl Pts',(-167.7223486997,-1.81102449608876,135.379095738862));
#116692=CARTESIAN_POINT('Ctrl Pts',(-167.730095032966,-1.68263793600738,
135.42785827552));
#116693=CARTESIAN_POINT('Ctrl Pts',(-167.737841366231,-1.55247279776552,
135.471159442746));
#116694=CARTESIAN_POINT('Ctrl Pts',(-167.745589434234,-1.42227850994327,
135.514470306968));
#116695=CARTESIAN_POINT('Ctrl Pts',(-167.753337502237,-1.2903052222948,
135.552317244671));
#116696=CARTESIAN_POINT('Ctrl Pts',(-167.76108557024,-1.15705237338171,
135.584571163949));
#116697=CARTESIAN_POINT('Ctrl Pts',(-167.768841872981,-1.02365790175525,
135.616859363076));
#116698=CARTESIAN_POINT('Ctrl Pts',(-167.776598175723,-0.888981532849623,
135.643542577221));
#116699=CARTESIAN_POINT('Ctrl Pts',(-167.784354478465,-0.753533625493269,
135.664542727091));
#116700=CARTESIAN_POINT('Ctrl Pts',(-167.792114920979,-0.618013425510501,
135.685554085374));
#116701=CARTESIAN_POINT('Ctrl Pts',(-167.799875363493,-0.481721254871638,
135.700876291772));
#116702=CARTESIAN_POINT('Ctrl Pts',(-167.807635806007,-0.345171781921969,
135.710483272317));
#116703=CARTESIAN_POINT('Ctrl Pts',(-167.815408706272,-0.208403107636025,
135.720105674841));
#116704=CARTESIAN_POINT('Ctrl Pts',(-167.823181606538,-0.071376696677498,
135.723994506665));
#116705=CARTESIAN_POINT('Ctrl Pts',(-167.830954506803,0.0653926919184216,
135.722175870129));
#116706=CARTESIAN_POINT('Ctrl Pts',(-167.838444842567,0.197190168765343,
135.720423345612));
#116707=CARTESIAN_POINT('Ctrl Pts',(-167.84593517833,0.328748678062574,
135.713371126581));
#116708=CARTESIAN_POINT('Ctrl Pts',(-167.853425514094,0.459614750610761,
135.701087824949));
#116709=CARTESIAN_POINT('Ctrl Pts',(-167.861199848213,0.595442650048543,
135.688338798204));
#116710=CARTESIAN_POINT('Ctrl Pts',(-167.868974182332,0.730954830702724,
135.669913800335));
#116711=CARTESIAN_POINT('Ctrl Pts',(-167.876748516451,0.865638830253724,
135.645832757118));
#116712=CARTESIAN_POINT('Ctrl Pts',(-167.884513269398,1.00015684381233,
135.621781391635));
#116713=CARTESIAN_POINT('Ctrl Pts',(-167.892278022345,1.13384832590805,
135.592087918313));
#116714=CARTESIAN_POINT('Ctrl Pts',(-167.900042775292,1.26620441830655,
135.556824129636));
#116715=CARTESIAN_POINT('Ctrl Pts',(-167.907799816177,1.39842905276819,
135.521595365452));
#116716=CARTESIAN_POINT('Ctrl Pts',(-167.915556857062,1.52932056164317,
135.48080739587));
#116717=CARTESIAN_POINT('Ctrl Pts',(-167.923313897947,1.6583791413953,135.434583256477));
#116718=CARTESIAN_POINT('Ctrl Pts',(-167.931065089187,1.78734039706799,
135.388393975068));
#116719=CARTESIAN_POINT('Ctrl Pts',(-167.938816280427,1.91447110827526,
135.336776814866));
#116720=CARTESIAN_POINT('Ctrl Pts',(-167.946567471667,2.03928587887777,
135.279904848909));
#116721=CARTESIAN_POINT('Ctrl Pts',(-167.954315368444,2.16404759987373,
135.223057055054));
#116722=CARTESIAN_POINT('Ctrl Pts',(-167.962063265221,2.28649498300679,
135.16095905934));
#116723=CARTESIAN_POINT('Ctrl Pts',(-167.969811161998,2.40616210707633,
135.093832260667));
#116724=CARTESIAN_POINT('Ctrl Pts',(-167.977557438082,2.52580419936324,
135.026719503474));
#116725=CARTESIAN_POINT('Ctrl Pts',(-167.985303714166,2.64266684859592,
134.954580226794));
#116726=CARTESIAN_POINT('Ctrl Pts',(-167.99304999025,2.75630862682354,134.877681844304));
#116727=CARTESIAN_POINT('Ctrl Pts',(-168.000796323516,2.86995124392879,
134.800782894169));
#116728=CARTESIAN_POINT('Ctrl Pts',(-168.008542656781,2.98037261878673,
134.719124987229));
#116729=CARTESIAN_POINT('Ctrl Pts',(-168.016288990046,3.08716055380728,
134.633018708532));
#116730=CARTESIAN_POINT('Ctrl Pts',(-168.024037058049,3.19397240324561,
134.54689314693));
#116731=CARTESIAN_POINT('Ctrl Pts',(-168.031785126052,3.29714888941794,
134.456317476643));
#116732=CARTESIAN_POINT('Ctrl Pts',(-168.039533194055,3.39631144490481,
134.36164211215));
#116733=CARTESIAN_POINT('Ctrl Pts',(-168.047289496796,3.49557939153557,
134.266866125552));
#116734=CARTESIAN_POINT('Ctrl Pts',(-168.055045799538,3.5908246023509,134.167982011176));
#116735=CARTESIAN_POINT('Ctrl Pts',(-168.06280210228,3.68170552561717,134.065376944594));
#116736=CARTESIAN_POINT('Ctrl Pts',(-168.070562544794,3.77263495476857,
133.962717114597));
#116737=CARTESIAN_POINT('Ctrl Pts',(-168.078322987308,3.85919520831048,
133.856332678266));
#116738=CARTESIAN_POINT('Ctrl Pts',(-168.086083429822,3.94108615866295,
133.746642547038));
#116739=CARTESIAN_POINT('Ctrl Pts',(-168.093856330088,4.02310856763886,
133.636776331473));
#116740=CARTESIAN_POINT('Ctrl Pts',(-168.101629230353,4.10044647416858,
133.523594139733));
#116741=CARTESIAN_POINT('Ctrl Pts',(-168.109402130618,4.17284359905884,
133.407543162124));
#116742=CARTESIAN_POINT('Ctrl Pts',(-168.116892466381,4.24260890610805,
133.295710929857));
#116743=CARTESIAN_POINT('Ctrl Pts',(-168.124382802143,4.30778626226982,
133.181215133421));
#116744=CARTESIAN_POINT('Ctrl Pts',(-168.131873137906,4.36818828151273,
133.064474375711));
#116745=CARTESIAN_POINT('Ctrl Pts',(-168.139647472025,4.43088046166951,
132.943307356698));
#116746=CARTESIAN_POINT('Ctrl Pts',(-168.147421806144,4.48862663285195,
132.819337959803));
#116747=CARTESIAN_POINT('Ctrl Pts',(-168.155196140263,4.54116656078055,
132.693008104459));
#116748=CARTESIAN_POINT('Ctrl Pts',(-168.16296089321,4.59364173794374,132.566833939371));
#116749=CARTESIAN_POINT('Ctrl Pts',(-168.170725646157,4.64092328954491,
132.438305461509));
#116750=CARTESIAN_POINT('Ctrl Pts',(-168.178490399105,4.68279656632752,
132.307889593306));
#116751=CARTESIAN_POINT('Ctrl Pts',(-168.18624743999,4.7246282539812,132.177603255983));
#116752=CARTESIAN_POINT('Ctrl Pts',(-168.194004480875,4.76106223774635,
132.045433628664));
#116753=CARTESIAN_POINT('Ctrl Pts',(-168.20176152176,4.79193187492677,131.911867713959));
#116754=CARTESIAN_POINT('Ctrl Pts',(-168.209512713,4.82277823307345,131.77840252235));
#116755=CARTESIAN_POINT('Ctrl Pts',(-168.21726390424,4.84806850906943,131.643543518573));
#116756=CARTESIAN_POINT('Ctrl Pts',(-168.22501509548,4.86768594569225,131.507792630351));
#116757=CARTESIAN_POINT('Ctrl Pts',(-168.232762992257,4.88729504438133,
131.372099439876));
#116758=CARTESIAN_POINT('Ctrl Pts',(-168.240510889034,4.90123604340663,
131.235515505043));
#116759=CARTESIAN_POINT('Ctrl Pts',(-168.248258785811,4.90944337014437,
131.098552490067));
#116760=CARTESIAN_POINT('Ctrl Pts',(-168.256005061896,4.91764898008629,
130.961618124801));
#116761=CARTESIAN_POINT('Ctrl Pts',(-168.26375133798,4.92012327996341,130.824305227132));
#116762=CARTESIAN_POINT('Ctrl Pts',(-168.271497614064,4.9168526498854,130.687129726522));
#116763=CARTESIAN_POINT('Ctrl Pts',(-168.279243947329,4.91358199566433,
130.549953213314));
#116764=CARTESIAN_POINT('Ctrl Pts',(-168.286990280595,4.90456633618552,
130.412914490042));
#116765=CARTESIAN_POINT('Ctrl Pts',(-168.29473661386,4.88984417257847,130.276528229018));
#116766=CARTESIAN_POINT('Ctrl Pts',(-168.302484681863,4.87511871204496,
130.140111425236));
#116767=CARTESIAN_POINT('Ctrl Pts',(-168.310232749866,4.85468424639725,
130.004347763085));
#116768=CARTESIAN_POINT('Ctrl Pts',(-168.317980817869,4.82863096432243,
129.86974514964));
#116769=CARTESIAN_POINT('Ctrl Pts',(-168.325737120611,4.80254999250934,
129.734999478936));
#116770=CARTESIAN_POINT('Ctrl Pts',(-168.333493423353,4.77083834947892,
129.601417706392));
#116771=CARTESIAN_POINT('Ctrl Pts',(-168.341249726095,4.73363715994987,
129.469496467009));
#116772=CARTESIAN_POINT('Ctrl Pts',(-168.349010168609,4.69641611502586,
129.337504817289));
#116773=CARTESIAN_POINT('Ctrl Pts',(-168.356770611123,4.65369980716572,
129.207175838048));
#116774=CARTESIAN_POINT('Ctrl Pts',(-168.364531053637,4.60567845213877,
129.078988466984));
#116775=CARTESIAN_POINT('Ctrl Pts',(-168.372303953903,4.55758000896946,
128.950595318172));
#116776=CARTESIAN_POINT('Ctrl Pts',(-168.380076854168,4.50415965313248,
128.824351007819));
#116777=CARTESIAN_POINT('Ctrl Pts',(-168.387849754434,4.44565509333515,
128.700712868155));
#116778=CARTESIAN_POINT('Ctrl Pts',(-168.395340090195,4.38927732165513,
128.581569286303));
#116779=CARTESIAN_POINT('Ctrl Pts',(-168.402830425957,4.32817871848307,
128.464845955974));
#116780=CARTESIAN_POINT('Ctrl Pts',(-168.410320761718,4.26261017956376,
128.350926795434));
#116781=CARTESIAN_POINT('Ctrl Pts',(-168.418095095837,4.1945555895575,128.23268835529));
#116782=CARTESIAN_POINT('Ctrl Pts',(-168.425869429956,4.12146984100777,
128.117096378876));
#116783=CARTESIAN_POINT('Ctrl Pts',(-168.433643764076,4.04358407026487,
128.004608676911));
#116784=CARTESIAN_POINT('Ctrl Pts',(-168.441408517023,3.96579428677336,
127.892259605985));
#116785=CARTESIAN_POINT('Ctrl Pts',(-168.449173269969,3.88321647178963,
127.783007515774));
#116786=CARTESIAN_POINT('Ctrl Pts',(-168.456938022917,3.79612743721554,
127.677285379757));
#116787=CARTESIAN_POINT('Ctrl Pts',(-168.464695063802,3.70912490069856,
127.571668248456));
#116788=CARTESIAN_POINT('Ctrl Pts',(-168.472452104687,3.6176203081724,127.469574394062));
#116789=CARTESIAN_POINT('Ctrl Pts',(-168.480209145572,3.52193331427772,
127.371407254603));
#116790=CARTESIAN_POINT('Ctrl Pts',(-168.487960336812,3.42631847868961,
127.273314143747));
#116791=CARTESIAN_POINT('Ctrl Pts',(-168.495711528052,3.32652779133241,
127.179142132638));
#116792=CARTESIAN_POINT('Ctrl Pts',(-168.503462719292,3.2229204280841,127.089260756628));
#116793=CARTESIAN_POINT('Ctrl Pts',(-168.511210616069,3.11935710072857,
126.999417582601));
#116794=CARTESIAN_POINT('Ctrl Pts',(-168.518958512846,3.01198061859749,
126.913861672267));
#116795=CARTESIAN_POINT('Ctrl Pts',(-168.526706409623,2.90118601568176,
126.832924760736));
#116796=CARTESIAN_POINT('Ctrl Pts',(-168.534452685707,2.79041458860849,
126.752004779463));
#116797=CARTESIAN_POINT('Ctrl Pts',(-168.542198961791,2.6762267784195,126.675702105657));
#116798=CARTESIAN_POINT('Ctrl Pts',(-168.549945237875,2.55904928929877,
126.604307070593));
#116799=CARTESIAN_POINT('Ctrl Pts',(-168.557691571141,2.44187093520091,
126.532911508508));
#116800=CARTESIAN_POINT('Ctrl Pts',(-168.565437904406,2.32170319200777,
126.466423860879));
#116801=CARTESIAN_POINT('Ctrl Pts',(-168.573184237671,2.19899987891132,
126.405089928571));
#116802=CARTESIAN_POINT('Ctrl Pts',(-168.580932305674,2.07626908725818,
126.343742260955));
#116803=CARTESIAN_POINT('Ctrl Pts',(-168.588680373677,1.95100194544226,
126.287550780033));
#116804=CARTESIAN_POINT('Ctrl Pts',(-168.59642844168,1.82367451925975,126.236714143691));
#116805=CARTESIAN_POINT('Ctrl Pts',(-168.604184744422,1.69621176797366,
126.185823477567));
#116806=CARTESIAN_POINT('Ctrl Pts',(-168.611941047164,1.56668472184361,
126.140299169992));
#116807=CARTESIAN_POINT('Ctrl Pts',(-168.619697349906,1.43558749531847,
126.100290932093));
#116808=CARTESIAN_POINT('Ctrl Pts',(-168.62745779242,1.30442029825626,126.060261340593));
#116809=CARTESIAN_POINT('Ctrl Pts',(-168.635218234934,1.17168162911119,
126.025753783441));
#116810=CARTESIAN_POINT('Ctrl Pts',(-168.642978677448,1.03787724800241,
125.99686710425));
#116811=CARTESIAN_POINT('Ctrl Pts',(-168.650751577714,0.903858072222484,
125.967934053596));
#116812=CARTESIAN_POINT('Ctrl Pts',(-168.658524477979,0.768770151305243,
125.94463997847));
#116813=CARTESIAN_POINT('Ctrl Pts',(-168.666297378245,0.633126739169326,
125.927032087044));
#116814=CARTESIAN_POINT('Ctrl Pts',(-168.673787714007,0.502414306726015,
125.910064286822));
#116815=CARTESIAN_POINT('Ctrl Pts',(-168.681278049769,0.37118637570029,
125.898376460903));
#116816=CARTESIAN_POINT('Ctrl Pts',(-168.688768385531,0.239901562680689,
125.891965040791));
#116817=CARTESIAN_POINT('Ctrl Pts',(-168.69654271965,0.103639046074826,
125.885310529736));
#116818=CARTESIAN_POINT('Ctrl Pts',(-168.70431705377,-0.033116389728072,
125.884319353145));
#116819=CARTESIAN_POINT('Ctrl Pts',(-168.712091387889,-0.169854640762195,
125.889044507333));
#116820=CARTESIAN_POINT('Ctrl Pts',(-168.719856140836,-0.306424374122569,
125.893763838192));
#116821=CARTESIAN_POINT('Ctrl Pts',(-168.727620893783,-0.442976577872466,
125.904185469273));
#116822=CARTESIAN_POINT('Ctrl Pts',(-168.73538564673,-0.578997355566437,
125.920310543627));
#116823=CARTESIAN_POINT('Ctrl Pts',(-168.743142687615,-0.714883035507554,
125.936419602329));
#116824=CARTESIAN_POINT('Ctrl Pts',(-168.7508997285,-0.850237954043831,
125.958220785486));
#116825=CARTESIAN_POINT('Ctrl Pts',(-168.758656769386,-0.984549906196488,
125.985663226703));
#116826=CARTESIAN_POINT('Ctrl Pts',(-168.766407960626,-1.11876057266032,
126.013084973362));
#116827=CARTESIAN_POINT('Ctrl Pts',(-168.774159151866,-1.25192945673756,
126.046139432572));
#116828=CARTESIAN_POINT('Ctrl Pts',(-168.781910343106,-1.38355151453494,
126.084724162379));
#116829=CARTESIAN_POINT('Ctrl Pts',(-168.789658239883,-1.51511762944608,
126.123292492647));
#116830=CARTESIAN_POINT('Ctrl Pts',(-168.797406136661,-1.64513785128884,
126.167386308769));
#116831=CARTESIAN_POINT('Ctrl Pts',(-168.805154033438,-1.77311955639681,
126.216852568393));
#116832=CARTESIAN_POINT('Ctrl Pts',(-168.812900309522,-1.90107449049138,
126.266308480742));
#116833=CARTESIAN_POINT('Ctrl Pts',(-168.820646585606,-2.02699139156891,
126.321134460434));
#116834=CARTESIAN_POINT('Ctrl Pts',(-168.82839286169,-2.15039535167048,
126.381128440299));
#116835=CARTESIAN_POINT('Ctrl Pts',(-168.836139194956,-2.27380022271188,
126.441122863025));
#116836=CARTESIAN_POINT('Ctrl Pts',(-168.843885528221,-2.39469176414734,
126.506285191108));
#116837=CARTESIAN_POINT('Ctrl Pts',(-168.851631861486,-2.51261787638955,
126.576366474979));
#116838=CARTESIAN_POINT('Ctrl Pts',(-168.859379929489,-2.63057039736744,
126.646463453069));
#116839=CARTESIAN_POINT('Ctrl Pts',(-168.867127997493,-2.74555583166465,
126.721481379239));
#116840=CARTESIAN_POINT('Ctrl Pts',(-168.874876065496,-2.85714971758546,
126.801127105291));
#116841=CARTESIAN_POINT('Ctrl Pts',(-168.882632368238,-2.96886220681607,
126.880857479769));
#116842=CARTESIAN_POINT('Ctrl Pts',(-168.89038867098,-3.07717562840205,
126.96522525184));
#116843=CARTESIAN_POINT('Ctrl Pts',(-168.898144973721,-3.18169694520404,
127.053895631544));
#116844=CARTESIAN_POINT('Ctrl Pts',(-168.905905416236,-3.28627404817961,
127.142613337299));
#116845=CARTESIAN_POINT('Ctrl Pts',(-168.91366585875,-3.38705472631127,
127.235637961473));
#116846=CARTESIAN_POINT('Ctrl Pts',(-168.921426301264,-3.48368244397181,
127.332597421139));
#116847=CARTESIAN_POINT('Ctrl Pts',(-168.92919920153,-3.58046527702294,
127.429712528738));
#116848=CARTESIAN_POINT('Ctrl Pts',(-168.936972101795,-3.67308156311091,
127.530774805901));
#116849=CARTESIAN_POINT('Ctrl Pts',(-168.944745002061,-3.76121415838317,
127.635377954742));
#116850=CARTESIAN_POINT('Ctrl Pts',(-168.952235337822,-3.84614291181632,
127.736178515633));
#116851=CARTESIAN_POINT('Ctrl Pts',(-168.959725673583,-3.92690811290851,
127.840266735162));
#116852=CARTESIAN_POINT('Ctrl Pts',(-168.967216009345,-4.00326487046784,
127.947254837344));
#116853=CARTESIAN_POINT('Ctrl Pts',(-168.975066780707,-4.08329592176035,
128.059391216194));
#116854=CARTESIAN_POINT('Ctrl Pts',(-168.982917552068,-4.15873583823605,
128.175066470889));
#116855=CARTESIAN_POINT('Ctrl Pts',(-168.99076832343,-4.22925912511095,
128.293872554427));
#116856=CARTESIAN_POINT('Ctrl Pts',(-168.998605668683,-4.29966180557835,
128.412475460041));
#116857=CARTESIAN_POINT('Ctrl Pts',(-169.006443013935,-4.36516441340019,
128.534198203532));
#116858=CARTESIAN_POINT('Ctrl Pts',(-169.014280359188,-4.42548336394001,
128.65860199694));
#116859=CARTESIAN_POINT('Ctrl Pts',(-169.022109933543,-4.48574250692737,
128.782882441279));
#116860=CARTESIAN_POINT('Ctrl Pts',(-169.029939507897,-4.54082805295072,
128.909838306252));
#116861=CARTESIAN_POINT('Ctrl Pts',(-169.037769082251,-4.59050090648996,
129.039003857584));
#116862=CARTESIAN_POINT('Ctrl Pts',(-169.045590964355,-4.64012495839209,
129.16804250881));
#116863=CARTESIAN_POINT('Ctrl Pts',(-169.053412846459,-4.68434677298601,
129.29928616832));
#116864=CARTESIAN_POINT('Ctrl Pts',(-169.061234728562,-4.72297445864585,
129.43224716545));
#116865=CARTESIAN_POINT('Ctrl Pts',(-169.064167241935,-4.73745642133288,
129.482095769278));
#116866=CARTESIAN_POINT('Ctrl Pts',(-169.067099755308,-4.75115256260494,
129.532185551135));
#116867=CARTESIAN_POINT('Ctrl Pts',(-169.070032268681,-4.76405452823411,
129.582490119308));
#116868=CARTESIAN_POINT('Origin',(213.235140564004,0.,130.804360617566));
#116869=CARTESIAN_POINT('',(-171.165157400749,-4.76405452823416,129.582490119309));
#116870=CARTESIAN_POINT('',(-170.819717755703,-4.76405452823413,129.582490119309));
#116871=CARTESIAN_POINT('',(213.235140564004,-4.76405452823405,129.582490119308));
#116872=CARTESIAN_POINT('',(-169.485140563978,-4.91824957353103,130.806408778158));
#116873=CARTESIAN_POINT('Ctrl Pts',(-169.485140564012,-4.91824957353078,
130.806408778756));
#116874=CARTESIAN_POINT('Ctrl Pts',(-169.491601129611,-4.91820232501163,
130.919866650305));
#116875=CARTESIAN_POINT('Ctrl Pts',(-169.498061695211,-4.91422942216106,
131.033238697484));
#116876=CARTESIAN_POINT('Ctrl Pts',(-169.504522260811,-4.9063465576463,
131.146335059261));
#116877=CARTESIAN_POINT('Ctrl Pts',(-169.51229659493,-4.89686069737473,
131.282429785109));
#116878=CARTESIAN_POINT('Ctrl Pts',(-169.520070929049,-4.8816929241367,
131.41834509075));
#116879=CARTESIAN_POINT('Ctrl Pts',(-169.527845263168,-4.86085086028999,
131.553568183277));
#116880=CARTESIAN_POINT('Ctrl Pts',(-169.535610016115,-4.84003448242426,
131.688624625427));
#116881=CARTESIAN_POINT('Ctrl Pts',(-169.543374769062,-4.81355778703188,
131.822990169166));
#116882=CARTESIAN_POINT('Ctrl Pts',(-169.551139522009,-4.78148033472624,
131.956154379976));
#116883=CARTESIAN_POINT('Ctrl Pts',(-169.558896562894,-4.74943474219844,
132.089186330215));
#116884=CARTESIAN_POINT('Ctrl Pts',(-169.566653603779,-4.7117995538491,
132.221018944375));
#116885=CARTESIAN_POINT('Ctrl Pts',(-169.574410644664,-4.66868577592679,
132.351149610337));
#116886=CARTESIAN_POINT('Ctrl Pts',(-169.582161835904,-4.62560451043985,
132.481182143752));
#116887=CARTESIAN_POINT('Ctrl Pts',(-169.589913027145,-4.57705300123568,
132.609514913977));
#116888=CARTESIAN_POINT('Ctrl Pts',(-169.597664218385,-4.52319262334111,
132.735658511381));
#116889=CARTESIAN_POINT('Ctrl Pts',(-169.605412115162,-4.46935513754385,
132.86174849439));
#116890=CARTESIAN_POINT('Ctrl Pts',(-169.613160011939,-4.41021342408801,
132.985650796377));
#116891=CARTESIAN_POINT('Ctrl Pts',(-169.620907908716,-4.34597763729324,
133.106894317351));
#116892=CARTESIAN_POINT('Ctrl Pts',(-169.6286541848,-4.2817552872403,133.228112476795));
#116893=CARTESIAN_POINT('Ctrl Pts',(-169.636400460884,-4.21244116624499,
133.346672616203));
#116894=CARTESIAN_POINT('Ctrl Pts',(-169.644146736968,-4.13829201792157,
133.462127017554));
#116895=CARTESIAN_POINT('Ctrl Pts',(-169.651893070234,-4.06414232224607,
133.577582271164));
#116896=CARTESIAN_POINT('Ctrl Pts',(-169.659639403499,-3.98515773929668,
133.689931412005));
#116897=CARTESIAN_POINT('Ctrl Pts',(-169.667385736764,-3.90163887307296,
133.798754908007));
#116898=CARTESIAN_POINT('Ctrl Pts',(-169.675133804767,-3.81810130337812,
133.907602774276));
#116899=CARTESIAN_POINT('Ctrl Pts',(-169.68288187277,-3.73002766782518,
134.012923114513));
#116900=CARTESIAN_POINT('Ctrl Pts',(-169.690629940773,-3.6377591954069,
134.114329061333));
#116901=CARTESIAN_POINT('Ctrl Pts',(-169.698386243515,-3.545392658958,134.2158427836));
#116902=CARTESIAN_POINT('Ctrl Pts',(-169.706142546257,-3.44882264320227,
134.31343351224));
#116903=CARTESIAN_POINT('Ctrl Pts',(-169.713898848999,-3.34842801591426,
134.406750502731));
#116904=CARTESIAN_POINT('Ctrl Pts',(-169.721659291513,-3.24797980499085,
134.50011729931));
#116905=CARTESIAN_POINT('Ctrl Pts',(-169.729419734027,-3.1437032121594,
134.589205558775));
#116906=CARTESIAN_POINT('Ctrl Pts',(-169.737180176541,-3.03600982598779,
134.673705187258));
#116907=CARTESIAN_POINT('Ctrl Pts',(-169.744953076807,-2.92814356083214,
134.758340462046));
#116908=CARTESIAN_POINT('Ctrl Pts',(-169.752725977072,-2.81684985927771,
134.838372157694));
#116909=CARTESIAN_POINT('Ctrl Pts',(-169.760498877338,-2.70256963285882,
134.913533337476));
#116910=CARTESIAN_POINT('Ctrl Pts',(-169.7679892131,-2.59244378052787,134.985962219051));
#116911=CARTESIAN_POINT('Ctrl Pts',(-169.775479548861,-2.47954503289768,
135.053868389152));
#116912=CARTESIAN_POINT('Ctrl Pts',(-169.782969884623,-2.36428737556901,
135.117054470395));
#116913=CARTESIAN_POINT('Ctrl Pts',(-169.790744218742,-2.24465968912837,
135.182636271114));
#116914=CARTESIAN_POINT('Ctrl Pts',(-169.798518552862,-2.1221117412432,
135.24334073653));
#116915=CARTESIAN_POINT('Ctrl Pts',(-169.806292886981,-1.99707907917962,
135.298897102456));
#116916=CARTESIAN_POINT('Ctrl Pts',(-169.814057639928,-1.87220050869754,
135.354385000126));
#116917=CARTESIAN_POINT('Ctrl Pts',(-169.821822392875,-1.74484367073196,
135.404737264885));
#116918=CARTESIAN_POINT('Ctrl Pts',(-169.829587145822,-1.61547020226498,
135.449728104439));
#116919=CARTESIAN_POINT('Ctrl Pts',(-169.837344186707,-1.48622522935037,
135.494674258457));
#116920=CARTESIAN_POINT('Ctrl Pts',(-169.845101227592,-1.35496797877043,
135.534269456759));
#116921=CARTESIAN_POINT('Ctrl Pts',(-169.852858268477,-1.22218131392522,
135.568335417918));
#116922=CARTESIAN_POINT('Ctrl Pts',(-169.860609459717,-1.08949478453673,
135.602375689671));
#116923=CARTESIAN_POINT('Ctrl Pts',(-169.868360650957,-0.955281513711783,
135.630894926937));
#116924=CARTESIAN_POINT('Ctrl Pts',(-169.876111842197,-0.820040482779182,
135.653764361234));
#116925=CARTESIAN_POINT('Ctrl Pts',(-169.883859738974,-0.684856932892583,
135.676624075412));
#116926=CARTESIAN_POINT('Ctrl Pts',(-169.891607635751,-0.548646876396235,
135.693838697607));
#116927=CARTESIAN_POINT('Ctrl Pts',(-169.899355532528,-0.411920256597,135.705330395549));
#116928=CARTESIAN_POINT('Ctrl Pts',(-169.907101808613,-0.275222237059142,
135.716819689676));
#116929=CARTESIAN_POINT('Ctrl Pts',(-169.914848084697,-0.138008258488271,
135.722588407947));
#116930=CARTESIAN_POINT('Ctrl Pts',(-169.922594360781,-0.000793774930625052,
135.722610553511));
#116931=CARTESIAN_POINT('Ctrl Pts',(-169.930340694046,0.136421721512981,
135.722632699238));
#116932=CARTESIAN_POINT('Ctrl Pts',(-169.938087027311,0.273637331985599,
135.716908187549));
#116933=CARTESIAN_POINT('Ctrl Pts',(-169.945833360577,0.410337608468786,
135.705463157768));
#116934=CARTESIAN_POINT('Ctrl Pts',(-169.95358142858,0.547068498030891,
135.694015564953));
#116935=CARTESIAN_POINT('Ctrl Pts',(-169.961329496583,0.683283434432496,
135.676844937477));
#116936=CARTESIAN_POINT('Ctrl Pts',(-169.969077564586,0.818472492582324,
135.654029249688));
#116937=CARTESIAN_POINT('Ctrl Pts',(-169.976833867327,0.953805231272109,
135.631189313114));
#116938=CARTESIAN_POINT('Ctrl Pts',(-169.984590170069,1.08810952755903,
135.60269239647));
#116939=CARTESIAN_POINT('Ctrl Pts',(-169.992346472811,1.22088550285722,
135.568667665964));
#116940=CARTESIAN_POINT('Ctrl Pts',(-170.000106915325,1.35373234469159,
135.534624775435));
#116941=CARTESIAN_POINT('Ctrl Pts',(-170.00786735784,1.48504886601324,135.495048304962));
#116942=CARTESIAN_POINT('Ctrl Pts',(-170.015627800354,1.61435170239241,
135.450116922355));
#116943=CARTESIAN_POINT('Ctrl Pts',(-170.023400700619,1.74386210716315,
135.405113411903));
#116944=CARTESIAN_POINT('Ctrl Pts',(-170.031173600884,1.87135200351641,
135.354737955165));
#116945=CARTESIAN_POINT('Ctrl Pts',(-170.03894650115,1.99635848657079,135.299217217681));
#116946=CARTESIAN_POINT('Ctrl Pts',(-170.046436836912,2.11682066909617,
135.245714798852));
#116947=CARTESIAN_POINT('Ctrl Pts',(-170.053927172674,2.23497658400925,
135.18743482865));
#116948=CARTESIAN_POINT('Ctrl Pts',(-170.061417508436,2.35043640279736,
135.124618917588));
#116949=CARTESIAN_POINT('Ctrl Pts',(-170.069191842555,2.47027391570589,
135.059421322166));
#116950=CARTESIAN_POINT('Ctrl Pts',(-170.076966176675,2.58758646093225,
134.989130509218));
#116951=CARTESIAN_POINT('Ctrl Pts',(-170.084740510794,2.70191081296185,
134.913966562337));
#116952=CARTESIAN_POINT('Ctrl Pts',(-170.092505263741,2.81609427044503,
134.838895248304));
#116953=CARTESIAN_POINT('Ctrl Pts',(-170.100270016688,2.92729653862137,
134.758962962614));
#116954=CARTESIAN_POINT('Ctrl Pts',(-170.108034769635,3.03507812597438,
134.674436047287));
#116955=CARTESIAN_POINT('Ctrl Pts',(-170.11579181052,3.14275266313536,134.589993085284));
#116956=CARTESIAN_POINT('Ctrl Pts',(-170.123548851405,3.24701297493629,
134.500964814821));
#116957=CARTESIAN_POINT('Ctrl Pts',(-170.13130589229,3.34744806870106,134.407661117087));
#116958=CARTESIAN_POINT('Ctrl Pts',(-170.13905708353,3.44780742358021,134.314427780397));
#116959=CARTESIAN_POINT('Ctrl Pts',(-170.14680827477,3.54434701682041,134.216925698898));
#116960=CARTESIAN_POINT('Ctrl Pts',(-170.15455946601,3.63668880025547,134.115505077205));
#116961=CARTESIAN_POINT('Ctrl Pts',(-170.162307362787,3.7289913359694,134.014127561981));
#116962=CARTESIAN_POINT('Ctrl Pts',(-170.170055259564,3.81709934781756,
133.908835107568));
#116963=CARTESIAN_POINT('Ctrl Pts',(-170.177803156342,3.90067171649274,
133.80001467347));
#116964=CARTESIAN_POINT('Ctrl Pts',(-170.185549432426,3.98422660363,133.691217002261));
#116965=CARTESIAN_POINT('Ctrl Pts',(-170.19329570851,4.0632474967456,133.578893129122));
#116966=CARTESIAN_POINT('Ctrl Pts',(-170.201041984594,4.13743390844848,
133.463462668207));
#116967=CARTESIAN_POINT('Ctrl Pts',(-170.208788317859,4.2116208677787,133.34803135521));
#116968=CARTESIAN_POINT('Ctrl Pts',(-170.216534651124,4.28097306310594,
133.229493737574));
#116969=CARTESIAN_POINT('Ctrl Pts',(-170.22428098439,4.3452338739408,133.108297605258));
#116970=CARTESIAN_POINT('Ctrl Pts',(-170.232029052393,4.40950907553861,
132.98707433191));
#116971=CARTESIAN_POINT('Ctrl Pts',(-170.239777120396,4.46869044070612,
132.863191704541));
#116972=CARTESIAN_POINT('Ctrl Pts',(-170.247525188399,4.5225679445012,132.737120884612));
#116973=CARTESIAN_POINT('Ctrl Pts',(-170.255281491141,4.57650270994852,
132.610916075114));
#116974=CARTESIAN_POINT('Ctrl Pts',(-170.263037793882,4.62512219960934,
132.482518787431));
#116975=CARTESIAN_POINT('Ctrl Pts',(-170.270794096624,4.66826488808641,
132.352419401062));
#116976=CARTESIAN_POINT('Ctrl Pts',(-170.278554539138,4.71143060311533,
132.222250576734));
#116977=CARTESIAN_POINT('Ctrl Pts',(-170.286314981653,4.74911358500167,
132.09037821927));
#116978=CARTESIAN_POINT('Ctrl Pts',(-170.294075424167,4.78120288175106,
131.957305571168));
#116979=CARTESIAN_POINT('Ctrl Pts',(-170.301848324432,4.81334369108835,
131.824019303037));
#116980=CARTESIAN_POINT('Ctrl Pts',(-170.309621224698,4.83987279572024,
131.689529277677));
#116981=CARTESIAN_POINT('Ctrl Pts',(-170.317394124963,4.86073068439009,
131.554347468337));
#116982=CARTESIAN_POINT('Ctrl Pts',(-170.324884460725,4.88083033626898,
131.424079858267));
#116983=CARTESIAN_POINT('Ctrl Pts',(-170.332374796487,4.89566390489223,
131.293170193242));
#116984=CARTESIAN_POINT('Ctrl Pts',(-170.339865132249,4.90522395219424,
131.162077043412));
#116985=CARTESIAN_POINT('Ctrl Pts',(-170.347639466368,4.91514647159538,
131.026013456962));
#116986=CARTESIAN_POINT('Ctrl Pts',(-170.355413800488,4.91941911613601,
130.889321188852));
#116987=CARTESIAN_POINT('Ctrl Pts',(-170.363188134607,4.91797666367118,
130.752508924385));
#116988=CARTESIAN_POINT('Ctrl Pts',(-170.370952887554,4.91653598890009,
130.615865268807));
#116989=CARTESIAN_POINT('Ctrl Pts',(-170.378717640501,4.90939423536557,
130.479102298308));
#116990=CARTESIAN_POINT('Ctrl Pts',(-170.386482393448,4.89653792825003,
130.342733733915));
#116991=CARTESIAN_POINT('Ctrl Pts',(-170.394239434333,4.88369439019996,
130.206500612703));
#116992=CARTESIAN_POINT('Ctrl Pts',(-170.401996475218,4.86514763007612,
130.070661504758));
#116993=CARTESIAN_POINT('Ctrl Pts',(-170.409753516103,4.84093620811762,
129.935729688209));
#116994=CARTESIAN_POINT('Ctrl Pts',(-170.417504707343,4.81674304418079,
129.800899624792));
#116995=CARTESIAN_POINT('Ctrl Pts',(-170.425255898583,4.78689378987004,
129.666975874185));
#116996=CARTESIAN_POINT('Ctrl Pts',(-170.433007089823,4.75147873797787,
129.534465793164));
#116997=CARTESIAN_POINT('Ctrl Pts',(-170.4407549866,4.71607873842743,129.402012032461));
#116998=CARTESIAN_POINT('Ctrl Pts',(-170.448502883378,4.67511774705443,
129.270971123223));
#116999=CARTESIAN_POINT('Ctrl Pts',(-170.456250780155,4.62873694053004,
129.141839219847));
#117000=CARTESIAN_POINT('Ctrl Pts',(-170.463997056239,4.58236583587065,
129.012734328082));
#117001=CARTESIAN_POINT('Ctrl Pts',(-170.471743332323,4.53057730314291,
128.885538015621));
#117002=CARTESIAN_POINT('Ctrl Pts',(-170.479489608407,4.4735619548437,128.760729902717));
#117003=CARTESIAN_POINT('Ctrl Pts',(-170.487235941672,4.41654618567006,
128.635920868507));
#117004=CARTESIAN_POINT('Ctrl Pts',(-170.494982274938,4.35430368638885,
128.513500424648));
#117005=CARTESIAN_POINT('Ctrl Pts',(-170.502728608203,4.28707248573286,
128.393926514635));
#117006=CARTESIAN_POINT('Ctrl Pts',(-170.510476676206,4.21982622911553,
128.274325826874));
#117007=CARTESIAN_POINT('Ctrl Pts',(-170.518224744209,4.1475892396298,128.157573282161));
#117008=CARTESIAN_POINT('Ctrl Pts',(-170.525972812212,4.07064439514418,
128.044100254705));
#117009=CARTESIAN_POINT('Ctrl Pts',(-170.533729114954,3.9936177727623,127.930506626765));
#117010=CARTESIAN_POINT('Ctrl Pts',(-170.541485417696,3.91187351999241,
127.820199802867));
#117011=CARTESIAN_POINT('Ctrl Pts',(-170.549241720438,3.82573689857504,
127.713580741001));
#117012=CARTESIAN_POINT('Ctrl Pts',(-170.557002162952,3.73955430344929,
127.606904773331));
#117013=CARTESIAN_POINT('Ctrl Pts',(-170.564762605466,3.64897492646274,
127.503920783061));
#117014=CARTESIAN_POINT('Ctrl Pts',(-170.57252304798,3.55436218751893,127.404994132111));
#117015=CARTESIAN_POINT('Ctrl Pts',(-170.580295948246,3.45959756780724,
127.305908675318));
#117016=CARTESIAN_POINT('Ctrl Pts',(-170.588068848511,3.3607869295795,127.21089384444));
#117017=CARTESIAN_POINT('Ctrl Pts',(-170.595841748776,3.25832884314138,
127.120276442028));
#117018=CARTESIAN_POINT('Ctrl Pts',(-170.603332084538,3.15959536622248,
127.032953210445));
#117019=CARTESIAN_POINT('Ctrl Pts',(-170.6108224203,3.05747526365405,126.949713437462));
#117020=CARTESIAN_POINT('Ctrl Pts',(-170.618312756062,2.95235032303649,
126.870811249302));
#117021=CARTESIAN_POINT('Ctrl Pts',(-170.626087090181,2.8432395383423,126.788917460696));
#117022=CARTESIAN_POINT('Ctrl Pts',(-170.633861424301,2.73054593059434,
126.711437254028));
#117023=CARTESIAN_POINT('Ctrl Pts',(-170.64163575842,2.6146622169822,126.63870045937));
#117024=CARTESIAN_POINT('Ctrl Pts',(-170.649400511367,2.49892131969058,
126.56605330631));
#117025=CARTESIAN_POINT('Ctrl Pts',(-170.657165264314,2.37999846704939,
126.498138139648));
#117026=CARTESIAN_POINT('Ctrl Pts',(-170.664930017261,2.25831858363902,
126.435243974892));
#117027=CARTESIAN_POINT('Ctrl Pts',(-170.672687058146,2.13675955440424,
126.372412277508));
#117028=CARTESIAN_POINT('Ctrl Pts',(-170.680444099031,2.01244928884994,
126.314591836172));
#117029=CARTESIAN_POINT('Ctrl Pts',(-170.688201139916,1.88584046515444,
126.262027648432));
#117030=CARTESIAN_POINT('Ctrl Pts',(-170.695952331156,1.75932711815759,
126.209503099754));
#117031=CARTESIAN_POINT('Ctrl Pts',(-170.703703522396,1.63051902279014,
126.162227064307));
#117032=CARTESIAN_POINT('Ctrl Pts',(-170.711454713636,1.499891838138,126.12039781494));
#117033=CARTESIAN_POINT('Ctrl Pts',(-170.719202610413,1.3693201735241,126.078586344119));
#117034=CARTESIAN_POINT('Ctrl Pts',(-170.72695050719,1.23693132894627,126.042217173942));
#117035=CARTESIAN_POINT('Ctrl Pts',(-170.734698403968,1.10321904259012,
126.011439712046));
#117036=CARTESIAN_POINT('Ctrl Pts',(-170.742444680052,0.96953472596176,
125.980668688133));
#117037=CARTESIAN_POINT('Ctrl Pts',(-170.750190956136,0.834527898957105,
125.955487133616));
#117038=CARTESIAN_POINT('Ctrl Pts',(-170.75793723222,0.698705110388279,
125.935993927267));
#117039=CARTESIAN_POINT('Ctrl Pts',(-170.765683565485,0.562881319206298,
125.916500577022));
#117040=CARTESIAN_POINT('Ctrl Pts',(-170.773429898751,0.426241941441041,
125.902695714275));
#117041=CARTESIAN_POINT('Ctrl Pts',(-170.781176232016,0.289300918270411,
125.894626608357));
#117042=CARTESIAN_POINT('Ctrl Pts',(-170.788924300019,0.152329228107311,
125.886555695418));
#117043=CARTESIAN_POINT('Ctrl Pts',(-170.796672368022,0.0150561483329293,
125.884223118273));
#117044=CARTESIAN_POINT('Ctrl Pts',(-170.804420436025,-0.12200249131536,
125.887624052057));
#117045=CARTESIAN_POINT('Ctrl Pts',(-170.812176738767,-0.259206798517073,
125.891028600394));
#117046=CARTESIAN_POINT('Ctrl Pts',(-170.819933041509,-0.396195818850764,
125.900178822656));
#117047=CARTESIAN_POINT('Ctrl Pts',(-170.82768934425,-0.532456403087785,
125.915017794516));
#117048=CARTESIAN_POINT('Ctrl Pts',(-170.835449786765,-0.66878971370134,
125.929864686382));
#117049=CARTESIAN_POINT('Ctrl Pts',(-170.843210229279,-0.804393427158591,
125.950406319318));
#117050=CARTESIAN_POINT('Ctrl Pts',(-170.850970671793,-0.93876371679538,
125.976534424907));
#117051=CARTESIAN_POINT('Ctrl Pts',(-170.858743572058,-1.07334970954993,
126.00270447365));
#117052=CARTESIAN_POINT('Ctrl Pts',(-170.866516472324,-1.20669794127393,
126.034478825098));
#117053=CARTESIAN_POINT('Ctrl Pts',(-170.874289372589,-1.33831802673905,
126.071698795525));
#117054=CARTESIAN_POINT('Ctrl Pts',(-170.881779708351,-1.46515339056616,
126.107565726276));
#117055=CARTESIAN_POINT('Ctrl Pts',(-170.889270044113,-1.59038377891071,
126.148489130217));
#117056=CARTESIAN_POINT('Ctrl Pts',(-170.896760379875,-1.71358902265974,
126.194285160058));
#117057=CARTESIAN_POINT('Ctrl Pts',(-170.904534904299,-1.84146876091866,
126.241818723818));
#117058=CARTESIAN_POINT('Ctrl Pts',(-170.912309428724,-1.96757174403429,
126.294752531509));
#117059=CARTESIAN_POINT('Ctrl Pts',(-170.920083953148,-2.09140816758484,
126.352934448454));
#117060=CARTESIAN_POINT('Ctrl Pts',(-170.927848852212,-2.21509127370658,
126.411044332457));
#117061=CARTESIAN_POINT('Ctrl Pts',(-170.935613751277,-2.33651305327552,
126.474389232686));
#117062=CARTESIAN_POINT('Ctrl Pts',(-170.943378650342,-2.45520064116338,
126.542767854979));
#117063=CARTESIAN_POINT('Ctrl Pts',(-170.951135793343,-2.57376967652441,
126.611078176462));
#117064=CARTESIAN_POINT('Ctrl Pts',(-170.958892936345,-2.68960961872044,
126.684412019881));
#117065=CARTESIAN_POINT('Ctrl Pts',(-170.966650079347,-2.80226964412983,
126.762520949285));
#117066=CARTESIAN_POINT('Ctrl Pts',(-170.974401328845,-2.91484407587179,
126.840570535282));
#117067=CARTESIAN_POINT('Ctrl Pts',(-170.982152578342,-3.02424307978171,
126.923387764059));
#117068=CARTESIAN_POINT('Ctrl Pts',(-170.98990382784,-3.13004273010074,
127.01067961223));
#117069=CARTESIAN_POINT('Ctrl Pts',(-170.997651559851,-3.23579436894872,
127.0979318477));
#117070=CARTESIAN_POINT('Ctrl Pts',(-171.005399291861,-3.3379496031451,
127.189654414129));
#117071=CARTESIAN_POINT('Ctrl Pts',(-171.013147023872,-3.43611588107539,
127.28551269327));
#117072=CARTESIAN_POINT('Ctrl Pts',(-171.02089307272,-3.53426083279562,
127.381350147604));
#117073=CARTESIAN_POINT('Ctrl Pts',(-171.028639121569,-3.62841827281185,
127.481321254211));
#117074=CARTESIAN_POINT('Ctrl Pts',(-171.036385170418,-3.71823124207505,
127.585053317391));
#117075=CARTESIAN_POINT('Ctrl Pts',(-171.044131213938,-3.80804414955658,
127.688785309215));
#117076=CARTESIAN_POINT('Ctrl Pts',(-171.051877257458,-3.89351233659524,
127.796277956744));
#117077=CARTESIAN_POINT('Ctrl Pts',(-171.059623300978,-3.97431827181639,
127.907124462744));
#117078=CARTESIAN_POINT('Ctrl Pts',(-171.067371016631,-4.05514165055738,
128.017994897101));
#117079=CARTESIAN_POINT('Ctrl Pts',(-171.075118732284,-4.13130054502534,
128.132220314472));
#117080=CARTESIAN_POINT('Ctrl Pts',(-171.082866447937,-4.20252023134042,
128.249364185538));
#117081=CARTESIAN_POINT('Ctrl Pts',(-171.090621545648,-4.27380777608902,
128.366619671806));
#117082=CARTESIAN_POINT('Ctrl Pts',(-171.098376643359,-4.34014651166784,
128.486798830294));
#117083=CARTESIAN_POINT('Ctrl Pts',(-171.10613174107,-4.40130706038281,
128.609439383734));
#117084=CARTESIAN_POINT('Ctrl Pts',(-171.11389095274,-4.4625000538186,128.732144996083));
#117085=CARTESIAN_POINT('Ctrl Pts',(-171.12165016441,-4.51850922753885,
128.857314248682));
#117086=CARTESIAN_POINT('Ctrl Pts',(-171.12940937608,-4.56915341137043,
128.984464970596));
#117087=CARTESIAN_POINT('Ctrl Pts',(-171.137179066458,-4.61986598947558,
129.11178740781));
#117088=CARTESIAN_POINT('Ctrl Pts',(-171.144948756837,-4.66519897841355,
129.241096290292));
#117089=CARTESIAN_POINT('Ctrl Pts',(-171.152718447215,-4.7050209508857,
129.371893893964));
#117090=CARTESIAN_POINT('Ctrl Pts',(-171.15686476506,-4.72627206219556,
129.441694415187));
#117091=CARTESIAN_POINT('Ctrl Pts',(-171.161011082905,-4.74595458264735,
129.511918706171));
#117092=CARTESIAN_POINT('Ctrl Pts',(-171.165157400749,-4.76405452823416,
129.582490119309));
#117093=CARTESIAN_POINT('Ctrl Pts',(-169.415000431073,-4.76405452823411,
129.582490119308));
#117094=CARTESIAN_POINT('Ctrl Pts',(-169.422682023387,-4.79781389926835,
129.714117394601));
#117095=CARTESIAN_POINT('Ctrl Pts',(-169.4303636157,-4.82608891842596,129.847047293059));
#117096=CARTESIAN_POINT('Ctrl Pts',(-169.438045208014,-4.84880351732504,
129.980778494838));
#117097=CARTESIAN_POINT('Ctrl Pts',(-169.445894434008,-4.87201381186302,
130.117428082886));
#117098=CARTESIAN_POINT('Ctrl Pts',(-169.453743660002,-4.8894181413164,
130.254913909779));
#117099=CARTESIAN_POINT('Ctrl Pts',(-169.461592885996,-4.90099142128198,
130.392697951029));
#117100=CARTESIAN_POINT('Ctrl Pts',(-169.46944211199,-4.91256470124756,
130.530481992279));
#117101=CARTESIAN_POINT('Ctrl Pts',(-169.477291337984,-4.91830697782338,
130.668563807642));
#117102=CARTESIAN_POINT('Ctrl Pts',(-169.485140563978,-4.91824957353103,
130.806408778157));
#117103=CARTESIAN_POINT('',(-169.139859436048,-4.91824908052575,130.80736800973));
#117104=CARTESIAN_POINT('Ctrl Pts',(-169.070032268681,-4.76405452823411,
129.582490119308));
#117105=CARTESIAN_POINT('Ctrl Pts',(-169.07784744914,-4.7984384088299,129.716552347903));
#117106=CARTESIAN_POINT('Ctrl Pts',(-169.085662629598,-4.82717822054996,
129.852141009683));
#117107=CARTESIAN_POINT('Ctrl Pts',(-169.093477810057,-4.85015012331475,
129.988746221046));
#117108=CARTESIAN_POINT('Ctrl Pts',(-169.101291338807,-4.87311717105495,
130.125322561416));
#117109=CARTESIAN_POINT('Ctrl Pts',(-169.109104867557,-4.89031866711784,
130.262914649134));
#117110=CARTESIAN_POINT('Ctrl Pts',(-169.116918396307,-4.90168187298647,
130.401002366707));
#117111=CARTESIAN_POINT('Ctrl Pts',(-169.124565409536,-4.91280291552475,
130.536147272018));
#117112=CARTESIAN_POINT('Ctrl Pts',(-169.132212422765,-4.91833199756882,
130.671766538623));
#117113=CARTESIAN_POINT('Ctrl Pts',(-169.139859435994,-4.91824908052634,
130.807368008766));
#117114=CARTESIAN_POINT('Ctrl Pts',(-169.139859436048,-4.91824908052575,
130.80736800973));
#117115=CARTESIAN_POINT('Ctrl Pts',(-169.148676452474,-4.91815347703479,
130.963716685191));
#117116=CARTESIAN_POINT('Ctrl Pts',(-169.1574934689,-4.91059820509904,131.119787728976));
#117117=CARTESIAN_POINT('Ctrl Pts',(-169.166310485326,-4.8956883266556,
131.274912283962));
#117118=CARTESIAN_POINT('Ctrl Pts',(-169.175032969929,-4.88093830477915,
131.428373667855));
#117119=CARTESIAN_POINT('Ctrl Pts',(-169.183755454533,-4.85899077049318,
131.58090858986));
#117120=CARTESIAN_POINT('Ctrl Pts',(-169.192477939136,-4.82999775806313,
131.731886746365));
#117121=CARTESIAN_POINT('Ctrl Pts',(-169.201342221473,-4.80053341852537,
131.885319290734));
#117122=CARTESIAN_POINT('Ctrl Pts',(-169.21020650381,-4.76379268072122,
132.037143802021));
#117123=CARTESIAN_POINT('Ctrl Pts',(-169.219070786147,-4.71998581934507,
132.186719806663));
#117124=CARTESIAN_POINT('Ctrl Pts',(-169.227935068484,-4.67617895796892,
132.336295811305));
#117125=CARTESIAN_POINT('Ctrl Pts',(-169.23679935082,-4.62530612193387,
132.483623132286));
#117126=CARTESIAN_POINT('Ctrl Pts',(-169.245663633157,-4.56762645801148,
132.628085268541));
#117127=CARTESIAN_POINT('Ctrl Pts',(-169.253437967276,-4.5170390599407,
132.7547844047));
#117128=CARTESIAN_POINT('Ctrl Pts',(-169.261212301395,-4.46109587271497,
132.879577799772));
#117129=CARTESIAN_POINT('Ctrl Pts',(-169.268986635513,-4.39996072850778,
133.001979476715));
#117130=CARTESIAN_POINT('Ctrl Pts',(-169.27675138846,-4.33890092790203,
133.124230304532));
#117131=CARTESIAN_POINT('Ctrl Pts',(-169.284516141407,-4.27266207468507,
133.244094932616));
#117132=CARTESIAN_POINT('Ctrl Pts',(-169.292280894354,-4.20145673886827,
133.361105488279));
#117133=CARTESIAN_POINT('Ctrl Pts',(-169.300037935238,-4.13032212519483,
133.477999827409));
#117134=CARTESIAN_POINT('Ctrl Pts',(-169.307794976123,-4.05423104730491,
133.592045403484));
#117135=CARTESIAN_POINT('Ctrl Pts',(-169.315552017007,-3.97344267559748,
133.702797500826));
#117136=CARTESIAN_POINT('Ctrl Pts',(-169.323303208247,-3.8927152270295,
133.81346607915));
#117137=CARTESIAN_POINT('Ctrl Pts',(-169.331054399487,-3.80729776478171,
133.92084580769));
#117138=CARTESIAN_POINT('Ctrl Pts',(-169.338805590727,-3.71749339147748,
134.024519922138));
#117139=CARTESIAN_POINT('Ctrl Pts',(-169.346553487504,-3.62772718742788,
134.128149972322));
#117140=CARTESIAN_POINT('Ctrl Pts',(-169.354301384281,-3.53357803622146,
134.228077246044));
#117141=CARTESIAN_POINT('Ctrl Pts',(-169.362049281057,-3.4353898997311,
134.323917308305));
#117142=CARTESIAN_POINT('Ctrl Pts',(-169.369795557141,-3.3372223020822,
134.419737322891));
#117143=CARTESIAN_POINT('Ctrl Pts',(-169.377541833225,-3.23501767924139,
134.511471553657));
#117144=CARTESIAN_POINT('Ctrl Pts',(-169.385288109309,-3.12915721815602,
134.598772056322));
#117145=CARTESIAN_POINT('Ctrl Pts',(-169.393034442574,-3.02329597563264,
134.68607320342));
#117146=CARTESIAN_POINT('Ctrl Pts',(-169.400780775839,-2.91377914264312,
134.768940308365));
#117147=CARTESIAN_POINT('Ctrl Pts',(-169.408527109104,-2.80102106579407,
134.847065658931));
#117148=CARTESIAN_POINT('Ctrl Pts',(-169.416275177106,-2.68823773755567,
134.925208505128));
#117149=CARTESIAN_POINT('Ctrl Pts',(-169.424023245109,-2.57221204239635,
134.998607261303));
#117150=CARTESIAN_POINT('Ctrl Pts',(-169.431771313112,-2.45338703817852,
135.066997724264));
#117151=CARTESIAN_POINT('Ctrl Pts',(-169.439527615853,-2.33443574533233,
135.135460873422));
#117152=CARTESIAN_POINT('Ctrl Pts',(-169.447283918595,-2.21267953965608,
135.198904901014));
#117153=CARTESIAN_POINT('Ctrl Pts',(-169.455040221336,-2.08858629076118,
135.257111494108));
#117154=CARTESIAN_POINT('Ctrl Pts',(-169.46280066385,-1.96442680956263,
135.315349153813));
#117155=CARTESIAN_POINT('Ctrl Pts',(-169.470561106364,-1.83792816011793,
135.368343658001));
#117156=CARTESIAN_POINT('Ctrl Pts',(-169.478321548878,-1.70957695816374,
135.415925393932));
#117157=CARTESIAN_POINT('Ctrl Pts',(-169.486094449143,-1.58101971546569,
135.463583512288));
#117158=CARTESIAN_POINT('Ctrl Pts',(-169.493867349408,-1.4506043496616,
135.505811378378));
#117159=CARTESIAN_POINT('Ctrl Pts',(-169.501640249673,-1.31883222172905,
135.542489428967));
#117160=CARTESIAN_POINT('Ctrl Pts',(-169.509130585439,-1.19185034249337,
135.57783414005));
#117161=CARTESIAN_POINT('Ctrl Pts',(-169.516620921205,-1.06360893179644,
135.608025459242));
#117162=CARTESIAN_POINT('Ctrl Pts',(-169.524111256971,-0.934562471605686,
135.633001839397));
#117163=CARTESIAN_POINT('Ctrl Pts',(-169.53188559109,-0.800623175719458,
135.658925206584));
#117164=CARTESIAN_POINT('Ctrl Pts',(-169.539659925209,-0.665392298922433,
135.679312497063));
#117165=CARTESIAN_POINT('Ctrl Pts',(-169.547434259328,-0.529367262754573,
135.69403886502));
#117166=CARTESIAN_POINT('Ctrl Pts',(-169.555199012275,-0.393509865286883,
135.708747084044));
#117167=CARTESIAN_POINT('Ctrl Pts',(-169.562963765222,-0.256860640792767,
135.717808220187));
#117168=CARTESIAN_POINT('Ctrl Pts',(-169.570728518169,-0.119928123100087,
135.721148218001));
#117169=CARTESIAN_POINT('Ctrl Pts',(-169.578485559054,0.0168683912856093,
135.724484898482));
#117170=CARTESIAN_POINT('Ctrl Pts',(-169.586242599939,0.153947250609493,
135.722111739227));
#117171=CARTESIAN_POINT('Ctrl Pts',(-169.593999640824,0.290794215045046,
135.714006407946));
#117172=CARTESIAN_POINT('Ctrl Pts',(-169.601750832064,0.427537982120017,
135.705907188958));
#117173=CARTESIAN_POINT('Ctrl Pts',(-169.609502023304,0.564049813680169,
135.69208442499));
#117174=CARTESIAN_POINT('Ctrl Pts',(-169.617253214545,0.699815239738818,
135.672567853575));
#117175=CARTESIAN_POINT('Ctrl Pts',(-169.625001111322,0.835522961869916,
135.653059577223));
#117176=CARTESIAN_POINT('Ctrl Pts',(-169.632749008099,0.970484523293181,
135.627862362174));
#117177=CARTESIAN_POINT('Ctrl Pts',(-169.640496904876,1.10419056816201,
135.597057796784));
#117178=CARTESIAN_POINT('Ctrl Pts',(-169.64824318096,1.23786864460862,135.566259675045));
#117179=CARTESIAN_POINT('Ctrl Pts',(-169.655989457044,1.370291346137,135.529856623721));
#117180=CARTESIAN_POINT('Ctrl Pts',(-169.663735733128,1.50095989651487,
135.487981273806));
#117181=CARTESIAN_POINT('Ctrl Pts',(-169.671482066393,1.63162941145847,
135.446105614775));
#117182=CARTESIAN_POINT('Ctrl Pts',(-169.679228399659,1.76054437709941,
135.398757695863));
#117183=CARTESIAN_POINT('Ctrl Pts',(-169.686974732924,1.88722194196574,
135.346119792628));
#117184=CARTESIAN_POINT('Ctrl Pts',(-169.694722800927,2.01392787539423,
135.293470101501));
#117185=CARTESIAN_POINT('Ctrl Pts',(-169.70247086893,2.13839505004803,135.235528218716));
#117186=CARTESIAN_POINT('Ctrl Pts',(-169.710218936933,2.26016170070031,
135.172524093123));
#117187=CARTESIAN_POINT('Ctrl Pts',(-169.717975239675,2.38205776639778,
135.109453005995));
#117188=CARTESIAN_POINT('Ctrl Pts',(-169.725731542417,2.50124722687086,
135.041309108458));
#117189=CARTESIAN_POINT('Ctrl Pts',(-169.733487845158,2.61729351431315,
134.968368028995));
#117190=CARTESIAN_POINT('Ctrl Pts',(-169.741248287673,2.73340173915345,
134.895388018681));
#117191=CARTESIAN_POINT('Ctrl Pts',(-169.749008730187,2.8463631263379,134.817605946245));
#117192=CARTESIAN_POINT('Ctrl Pts',(-169.756769172701,2.95577194817097,
134.735339535457));
#117193=CARTESIAN_POINT('Ctrl Pts',(-169.764542072966,3.06535640275742,
134.652941063324));
#117194=CARTESIAN_POINT('Ctrl Pts',(-169.772314973232,3.17137659324432,
134.566044115605));
#117195=CARTESIAN_POINT('Ctrl Pts',(-169.780087873497,3.27346092984274,
134.475005874642));
#117196=CARTESIAN_POINT('Ctrl Pts',(-169.787578209259,3.37183424367197,
134.387277103048));
#117197=CARTESIAN_POINT('Ctrl Pts',(-169.795068545021,3.46655267047621,
134.295703117773));
#117198=CARTESIAN_POINT('Ctrl Pts',(-169.802558880783,3.55731877029311,
134.20063301963));
#117199=CARTESIAN_POINT('Ctrl Pts',(-169.810333214902,3.65152629437217,
134.10195830982));
#117200=CARTESIAN_POINT('Ctrl Pts',(-169.818107549022,3.7417742913575,133.999204571723));
#117201=CARTESIAN_POINT('Ctrl Pts',(-169.825881883141,3.82768885643758,
133.892722817957));
#117202=CARTESIAN_POINT('Ctrl Pts',(-169.833646636088,3.91349753949483,
133.786372293435));
#117203=CARTESIAN_POINT('Ctrl Pts',(-169.841411389035,3.99498317363881,
133.676303196176));
#117204=CARTESIAN_POINT('Ctrl Pts',(-169.849176141982,4.07180857896975,
133.562903341311));
#117205=CARTESIAN_POINT('Ctrl Pts',(-169.856933182867,4.14855768022506,
133.449616116782));
#117206=CARTESIAN_POINT('Ctrl Pts',(-169.864690223752,4.22065554593491,
133.333005039611));
#117207=CARTESIAN_POINT('Ctrl Pts',(-169.872447264637,4.28780542812384,
133.213490683181));
#117208=CARTESIAN_POINT('Ctrl Pts',(-169.880198455878,4.35490467206418,
133.094066453458));
#117209=CARTESIAN_POINT('Ctrl Pts',(-169.887949647118,4.4170631687021,132.971743641784));
#117210=CARTESIAN_POINT('Ctrl Pts',(-169.895700838358,4.47402785347217,
132.846971160194));
#117211=CARTESIAN_POINT('Ctrl Pts',(-169.903448735135,4.53096832673171,
132.722251710237));
#117212=CARTESIAN_POINT('Ctrl Pts',(-169.911196631912,4.58271921665689,
132.59508501609));
#117213=CARTESIAN_POINT('Ctrl Pts',(-169.91894452869,4.62907384656703,132.465943713751));
#117214=CARTESIAN_POINT('Ctrl Pts',(-169.926690804774,4.67541878008789,
132.33682942499));
#117215=CARTESIAN_POINT('Ctrl Pts',(-169.934437080858,4.71636956680141,
132.205741717352));
#117216=CARTESIAN_POINT('Ctrl Pts',(-169.942183356942,4.75176819218133,
132.073171915701));
#117217=CARTESIAN_POINT('Ctrl Pts',(-169.949929690208,4.78716707886581,
131.940601135449));
#117218=CARTESIAN_POINT('Ctrl Pts',(-169.957676023473,4.81701362157322,
131.806548617083));
#117219=CARTESIAN_POINT('Ctrl Pts',(-169.965422356738,4.84120018088043,
131.671519121614));
#117220=CARTESIAN_POINT('Ctrl Pts',(-169.973170424742,4.86539215659986,
131.536459387227));
#117221=CARTESIAN_POINT('Ctrl Pts',(-169.980918492745,4.88392155779328,
131.400422625142));
#117222=CARTESIAN_POINT('Ctrl Pts',(-169.988666560748,4.89673225155445,
131.263921624492));
#117223=CARTESIAN_POINT('Ctrl Pts',(-169.99642286349,4.90955656067341,131.127275548954));
#117224=CARTESIAN_POINT('Ctrl Pts',(-170.004179166231,4.91664998448954,
130.990164639109));
#117225=CARTESIAN_POINT('Ctrl Pts',(-170.011935468973,4.91800844148806,
130.853105175747));
#117226=CARTESIAN_POINT('Ctrl Pts',(-170.019695911488,4.91936762353597,
130.715972559621));
#117227=CARTESIAN_POINT('Ctrl Pts',(-170.027456354002,4.91498575210007,
130.578891835265));
#117228=CARTESIAN_POINT('Ctrl Pts',(-170.035216796516,4.90491083145732,
130.442376090338));
#117229=CARTESIAN_POINT('Ctrl Pts',(-170.042989696782,4.89481973765754,
130.305641198217));
#117230=CARTESIAN_POINT('Ctrl Pts',(-170.050762597047,4.87901737713606,
130.169473486494));
#117231=CARTESIAN_POINT('Ctrl Pts',(-170.058535497313,4.85760340415545,
130.034378649961));
#117232=CARTESIAN_POINT('Ctrl Pts',(-170.066025833074,4.83696788303354,
129.904194851033));
#117233=CARTESIAN_POINT('Ctrl Pts',(-170.073516168835,4.81112171902776,
129.775007580153));
#117234=CARTESIAN_POINT('Ctrl Pts',(-170.081006504596,4.78019784697474,
129.647255779499));
#117235=CARTESIAN_POINT('Ctrl Pts',(-170.088780838715,4.74810148691061,
129.514660230481));
#117236=CARTESIAN_POINT('Ctrl Pts',(-170.096555172834,4.71043310371388,
129.383191129323));
#117237=CARTESIAN_POINT('Ctrl Pts',(-170.104329506954,4.66728590955701,
129.253352783624));
#117238=CARTESIAN_POINT('Ctrl Pts',(-170.112094259901,4.62419189046075,
129.123674452082));
#117239=CARTESIAN_POINT('Ctrl Pts',(-170.119859012848,4.57563261727034,
128.995623244629));
#117240=CARTESIAN_POINT('Ctrl Pts',(-170.127623765795,4.52175211586984,
128.869692463818));
#117241=CARTESIAN_POINT('Ctrl Pts',(-170.13538080668,4.46792512934291,128.743886759234));
#117242=CARTESIAN_POINT('Ctrl Pts',(-170.143137847565,4.40878758502785,
128.620197647302));
#117243=CARTESIAN_POINT('Ctrl Pts',(-170.15089488845,4.34453292369278,128.499102120683));
#117244=CARTESIAN_POINT('Ctrl Pts',(-170.15864607969,4.28032671729774,128.378097913144));
#117245=CARTESIAN_POINT('Ctrl Pts',(-170.16639727093,4.21101125721489,128.259683741894));
#117246=CARTESIAN_POINT('Ctrl Pts',(-170.17414846217,4.13682743827276,128.144315165237));
#117247=CARTESIAN_POINT('Ctrl Pts',(-170.181896358947,4.06267514943249,
128.028995623304));
#117248=CARTESIAN_POINT('Ctrl Pts',(-170.189644255724,3.98365882819056,
127.916719429544));
#117249=CARTESIAN_POINT('Ctrl Pts',(-170.197392152501,3.90006440280503,
127.807915938205));
#117250=CARTESIAN_POINT('Ctrl Pts',(-170.205138428585,3.81648746357121,
127.69913520621));
#117251=CARTESIAN_POINT('Ctrl Pts',(-170.212884704669,3.72833456303836,
127.593826041589));
#117252=CARTESIAN_POINT('Ctrl Pts',(-170.220630980753,3.63593365601639,
127.492386959527));
#117253=CARTESIAN_POINT('Ctrl Pts',(-170.228377314018,3.54353206691204,
127.390947128664));
#117254=CARTESIAN_POINT('Ctrl Pts',(-170.236123647284,3.44688267202423,
127.293377726395));
#117255=CARTESIAN_POINT('Ctrl Pts',(-170.243869980549,3.34635195934998,
127.200042148472));
#117256=CARTESIAN_POINT('Ctrl Pts',(-170.251618048552,3.24579873351952,
127.106685668693));
#117257=CARTESIAN_POINT('Ctrl Pts',(-170.259366116555,3.14136274676912,
127.017565165899));
#117258=CARTESIAN_POINT('Ctrl Pts',(-170.267114184558,3.03344508191169,
126.933005041347));
#117259=CARTESIAN_POINT('Ctrl Pts',(-170.2748704873,2.92541272087567,126.848355045287));
#117260=CARTESIAN_POINT('Ctrl Pts',(-170.282626790041,2.81389159808249,
126.768275351043));
#117261=CARTESIAN_POINT('Ctrl Pts',(-170.290383092783,2.69931386902168,
126.693048454885));
#117262=CARTESIAN_POINT('Ctrl Pts',(-170.298143535297,2.58467498637699,
126.617781407868));
#117263=CARTESIAN_POINT('Ctrl Pts',(-170.305903977811,2.46697658210621,
126.54737252051));
#117264=CARTESIAN_POINT('Ctrl Pts',(-170.313664420326,2.34667627887336,
126.482058741867));
#117265=CARTESIAN_POINT('Ctrl Pts',(-170.321437320591,2.22618285891401,
126.416640115748));
#117266=CARTESIAN_POINT('Ctrl Pts',(-170.329210220856,2.10307954471726,
126.356333114932));
#117267=CARTESIAN_POINT('Ctrl Pts',(-170.336983121122,1.97784565719827,
126.301327237854));
#117268=CARTESIAN_POINT('Ctrl Pts',(-170.344473456884,1.85716433692691,
126.248320962955));
#117269=CARTESIAN_POINT('Ctrl Pts',(-170.351963792647,1.73450494416747,
126.20023719724));
#117270=CARTESIAN_POINT('Ctrl Pts',(-170.359454128409,1.61030862793508,
126.157201357836));
#117271=CARTESIAN_POINT('Ctrl Pts',(-170.367228462528,1.48140337063193,
126.112533801503));
#117272=CARTESIAN_POINT('Ctrl Pts',(-170.375002796648,1.35043401120753,
126.073163018622));
#117273=CARTESIAN_POINT('Ctrl Pts',(-170.382777130767,1.21787522138547,
126.03928317773));
#117274=CARTESIAN_POINT('Ctrl Pts',(-170.390541883714,1.08547979842475,
126.005445090714));
#117275=CARTESIAN_POINT('Ctrl Pts',(-170.398306636661,0.951499217708815,
125.977084577066));
#117276=CARTESIAN_POINT('Ctrl Pts',(-170.406071389608,0.816426358154165,
125.95434710581));
#117277=CARTESIAN_POINT('Ctrl Pts',(-170.413828430493,0.681487654867818,
125.931632217732));
#117278=CARTESIAN_POINT('Ctrl Pts',(-170.421585471378,0.545459214722609,
125.914529322353));
#117279=CARTESIAN_POINT('Ctrl Pts',(-170.429342512263,0.408846904614433,
125.903133498661));
#117280=CARTESIAN_POINT('Ctrl Pts',(-170.437093703504,0.272337614911812,
125.891746268649));
#117281=CARTESIAN_POINT('Ctrl Pts',(-170.444844894744,0.13524571967397,
125.886057576345));
#117282=CARTESIAN_POINT('Ctrl Pts',(-170.452596085984,-0.00191529745561372,
125.8861109905));
#117283=CARTESIAN_POINT('Ctrl Pts',(-170.460343982761,-0.139018017493842,
125.886164381952));
#117284=CARTESIAN_POINT('Ctrl Pts',(-170.468091879538,-0.276189410845267,
125.891955025647));
#117285=CARTESIAN_POINT('Ctrl Pts',(-170.475839776315,-0.412913698413853,
125.9034744385));
#117286=CARTESIAN_POINT('Ctrl Pts',(-170.483586052399,-0.549609386208914,
125.91499144174));
#117287=CARTESIAN_POINT('Ctrl Pts',(-170.491332328484,-0.685857764909187,
125.932234797782));
#117288=CARTESIAN_POINT('Ctrl Pts',(-170.499078604568,-0.821146284817372,
125.955143996149));
#117289=CARTESIAN_POINT('Ctrl Pts',(-170.506824937833,-0.956435803394493,
125.978053363625));
#117290=CARTESIAN_POINT('Ctrl Pts',(-170.514571271099,-1.09076506356346,
126.006628591608));
#117291=CARTESIAN_POINT('Ctrl Pts',(-170.522317604364,-1.22363023447237,
126.040757767644));
#117292=CARTESIAN_POINT('Ctrl Pts',(-170.530065672367,-1.35652515961528,
126.074894586673));
#117293=CARTESIAN_POINT('Ctrl Pts',(-170.53781374037,-1.48795496447013,
126.114587731459));
#117294=CARTESIAN_POINT('Ctrl Pts',(-170.545561808373,-1.61742992601593,
126.159675106476));
#117295=CARTESIAN_POINT('Ctrl Pts',(-170.553318111115,-1.74704249509145,
126.204810400892));
#117296=CARTESIAN_POINT('Ctrl Pts',(-170.561074413857,-1.87469570075918,
126.255351249148));
#117297=CARTESIAN_POINT('Ctrl Pts',(-170.568830716599,-1.9999182803082,
126.311086762726));
#117298=CARTESIAN_POINT('Ctrl Pts',(-170.576591159113,-2.12520769491864,
126.366852024026));
#117299=CARTESIAN_POINT('Ctrl Pts',(-170.584351601627,-2.24806354838907,
126.427817301484));
#117300=CARTESIAN_POINT('Ctrl Pts',(-170.592112044142,-2.36803913254049,
126.493725660943));
#117301=CARTESIAN_POINT('Ctrl Pts',(-170.599884944407,-2.48820731215019,
126.559739822352));
#117302=CARTESIAN_POINT('Ctrl Pts',(-170.607657844673,-2.60548564820929,
126.630712720034));
#117303=CARTESIAN_POINT('Ctrl Pts',(-170.615430744938,-2.71945562565491,
126.70634351626));
#117304=CARTESIAN_POINT('Ctrl Pts',(-170.622921080699,-2.82928250733776,
126.779224942535));
#117305=CARTESIAN_POINT('Ctrl Pts',(-170.630411416461,-2.93603713912964,
126.856431313667));
#117306=CARTESIAN_POINT('Ctrl Pts',(-170.637901752222,-3.03937555223074,
126.937659269517));
#117307=CARTESIAN_POINT('Ctrl Pts',(-170.645579700367,-3.14530230938036,
127.020921763056));
#117308=CARTESIAN_POINT('Ctrl Pts',(-170.653257648512,-3.24799267487159,
127.108687882989));
#117309=CARTESIAN_POINT('Ctrl Pts',(-170.660935596657,-3.34703240044547,
127.200674008985));
#117310=CARTESIAN_POINT('Ctrl Pts',(-170.668604766083,-3.44595888717891,
127.292554960999));
#117311=CARTESIAN_POINT('Ctrl Pts',(-170.676273935508,-3.54124274087295,
127.388646057355));
#117312=CARTESIAN_POINT('Ctrl Pts',(-170.683943104934,-3.63250023729922,
127.488621621728));
#117313=CARTESIAN_POINT('Ctrl Pts',(-170.691605265208,-3.72367432995388,
127.588505814549));
#117314=CARTESIAN_POINT('Ctrl Pts',(-170.699267425482,-3.81082911358242,
127.6922671221));
#117315=CARTESIAN_POINT('Ctrl Pts',(-170.706929585756,-3.89361581775241,
127.799541334107));
#117316=CARTESIAN_POINT('Ctrl Pts',(-170.714586500158,-3.97634584228935,
127.906742101192));
#117317=CARTESIAN_POINT('Ctrl Pts',(-170.72224341456,-4.05471349128369,
128.017450672705));
#117318=CARTESIAN_POINT('Ctrl Pts',(-170.729900328962,-4.12840895911293,
128.131268301761));
#117319=CARTESIAN_POINT('Ctrl Pts',(-170.737554734118,-4.20208027622,128.245048631672));
#117320=CARTESIAN_POINT('Ctrl Pts',(-170.745209139275,-4.27108223460267,
128.361935659724));
#117321=CARTESIAN_POINT('Ctrl Pts',(-170.752863544432,-4.33514743436608,
128.481500358142));
#117322=CARTESIAN_POINT('Ctrl Pts',(-170.760516233525,-4.39919827116487,
128.601038251001));
#117323=CARTESIAN_POINT('Ctrl Pts',(-170.768168922618,-4.45831436466268,
128.723252264694));
#117324=CARTESIAN_POINT('Ctrl Pts',(-170.775821611711,-4.51227386738844,
128.847688031725));
#117325=CARTESIAN_POINT('Ctrl Pts',(-170.783477132258,-4.56625333483635,
128.972169839311));
#117326=CARTESIAN_POINT('Ctrl Pts',(-170.791132652804,-4.61507223721576,
129.098874675109));
#117327=CARTESIAN_POINT('Ctrl Pts',(-170.79878817335,-4.65855657066248,
129.227327409153));
#117328=CARTESIAN_POINT('Ctrl Pts',(-170.805764700801,-4.69818413669539,
129.3443872511));
#117329=CARTESIAN_POINT('Ctrl Pts',(-170.812741228252,-4.73338195825923,
129.462898234498));
#117330=CARTESIAN_POINT('Ctrl Pts',(-170.819717755703,-4.76405452823413,
129.582490119309));
#117331=CARTESIAN_POINT('Origin',(213.235140564004,0.,130.804360617566));
#117332=CARTESIAN_POINT('',(-172.915418914505,-4.76405452823406,129.582490119308));
#117333=CARTESIAN_POINT('',(-172.569844098739,-4.76405452823414,129.582490119309));
#117334=CARTESIAN_POINT('',(213.235140564004,-4.76405452823405,129.582490119308));
#117335=CARTESIAN_POINT('',(-171.235140564042,-4.91824795183872,130.799872106209));
#117336=CARTESIAN_POINT('Ctrl Pts',(-171.235140564042,-4.91824795183872,
130.799872106209));
#117337=CARTESIAN_POINT('Ctrl Pts',(-171.242791581675,-4.91837113477668,
130.934848757505));
#117338=CARTESIAN_POINT('Ctrl Pts',(-171.250442599308,-4.9129336827261,
131.069996001476));
#117339=CARTESIAN_POINT('Ctrl Pts',(-171.258093616941,-4.901920266296,131.20481132037));
#117340=CARTESIAN_POINT('Ctrl Pts',(-171.265738651492,-4.89091546233709,
131.339521213935));
#117341=CARTESIAN_POINT('Ctrl Pts',(-171.273383686044,-4.87434340088689,
131.473899299186));
#117342=CARTESIAN_POINT('Ctrl Pts',(-171.281028720596,-4.85224081964007,
131.607443484223));
#117343=CARTESIAN_POINT('Ctrl Pts',(-171.288670364304,-4.83014804166853,
131.740928437699));
#117344=CARTESIAN_POINT('Ctrl Pts',(-171.296312008013,-4.80252968590728,
131.873579829738));
#117345=CARTESIAN_POINT('Ctrl Pts',(-171.303953651722,-4.76947425097537,
132.004901508907));
#117346=CARTESIAN_POINT('Ctrl Pts',(-171.311593722981,-4.73642561798132,
132.136196165534));
#117347=CARTESIAN_POINT('Ctrl Pts',(-171.319233794241,-4.69794222833499,
132.266161262883));
#117348=CARTESIAN_POINT('Ctrl Pts',(-171.326873865501,-4.65416341139346,
132.394312189956));
#117349=CARTESIAN_POINT('Ctrl Pts',(-171.334514126357,-4.6103835080371,
132.522466297222));
#117350=CARTESIAN_POINT('Ctrl Pts',(-171.342154387212,-4.56130804653507,
132.648805763594));
#117351=CARTESIAN_POINT('Ctrl Pts',(-171.349794648068,-4.50712563271322,
132.772862990803));
#117352=CARTESIAN_POINT('Ctrl Pts',(-171.357436860504,-4.45292937887392,
132.896951906416));
#117353=CARTESIAN_POINT('Ctrl Pts',(-171.36507907294,-4.39362374029316,
133.018757054857));
#117354=CARTESIAN_POINT('Ctrl Pts',(-171.372721285377,-4.32944444139462,
133.137833113949));
#117355=CARTESIAN_POINT('Ctrl Pts',(-171.380371522867,-4.26519774809284,
133.257034214294));
#117356=CARTESIAN_POINT('Ctrl Pts',(-171.388021760357,-4.19606736896836,
133.373500149427));
#117357=CARTESIAN_POINT('Ctrl Pts',(-171.395671997848,-4.12233389934677,
133.486812161359));
#117358=CARTESIAN_POINT('Ctrl Pts',(-171.403326729994,-4.04855710994649,
133.600190746196));
#117359=CARTESIAN_POINT('Ctrl Pts',(-171.410981462141,-3.97017207940516,
133.710411391769));
#117360=CARTESIAN_POINT('Ctrl Pts',(-171.418636194287,-3.88750047758997,
133.817087471968));
#117361=CARTESIAN_POINT('Ctrl Pts',(-171.426302145668,-3.80470770732213,
133.923919903022));
#117362=CARTESIAN_POINT('Ctrl Pts',(-171.433968097048,-3.71761608277086,
134.027197091071));
#117363=CARTESIAN_POINT('Ctrl Pts',(-171.441634048429,-3.62658524128344,
134.126568099077));
#117364=CARTESIAN_POINT('Ctrl Pts',(-171.445641241453,-3.57900104268049,
134.178511920566));
#117365=CARTESIAN_POINT('Ctrl Pts',(-171.449648434477,-3.53034106028268,
134.229389052183));
#117366=CARTESIAN_POINT('Ctrl Pts',(-171.453655627501,-3.48066020141234,
134.279153794836));
#117367=CARTESIAN_POINT('Ctrl Pts',(-171.46142996162,-3.38427462830093,
134.375702110435));
#117368=CARTESIAN_POINT('Ctrl Pts',(-171.469204295739,-3.28371618382948,
134.468389924618));
#117369=CARTESIAN_POINT('Ctrl Pts',(-171.476978629858,-3.17932680684791,
134.556835016913));
#117370=CARTESIAN_POINT('Ctrl Pts',(-171.484743382805,-3.0750660804445,
134.645171108537));
#117371=CARTESIAN_POINT('Ctrl Pts',(-171.492508135752,-2.96698411090576,
134.729274631671));
#117372=CARTESIAN_POINT('Ctrl Pts',(-171.500272888699,-2.8554605102969,
134.808799197022));
#117373=CARTESIAN_POINT('Ctrl Pts',(-171.508029929584,-2.74404767650008,
134.888244777453));
#117374=CARTESIAN_POINT('Ctrl Pts',(-171.515786970469,-2.62920033042157,
134.963120225079));
#117375=CARTESIAN_POINT('Ctrl Pts',(-171.523544011354,-2.5113318031952,
135.033118784778));
#117376=CARTESIAN_POINT('Ctrl Pts',(-171.531295202594,-2.39355216154161,
135.103064558019));
#117377=CARTESIAN_POINT('Ctrl Pts',(-171.539046393834,-2.27275620834601,
135.168140564745));
#117378=CARTESIAN_POINT('Ctrl Pts',(-171.546797585075,-2.14938665351449,
135.228083040616));
#117379=CARTESIAN_POINT('Ctrl Pts',(-171.554545481852,-2.02606953403527,
135.288000039336));
#117380=CARTESIAN_POINT('Ctrl Pts',(-171.562293378629,-1.90018133942075,
135.342787676306));
#117381=CARTESIAN_POINT('Ctrl Pts',(-171.570041275406,-1.77218960989272,
135.392227992402));
#117382=CARTESIAN_POINT('Ctrl Pts',(-171.57778755149,-1.64422465347533,
135.441657966651));
#117383=CARTESIAN_POINT('Ctrl Pts',(-171.585533827574,-1.51415740182784,
135.485742704085));
#117384=CARTESIAN_POINT('Ctrl Pts',(-171.593280103658,-1.38247524640949,
135.52431244524));
#117385=CARTESIAN_POINT('Ctrl Pts',(-171.601026436923,-1.25079211894321,
135.562882471109));
#117386=CARTESIAN_POINT('Ctrl Pts',(-171.608772770189,-1.1174944391208,
135.595937309567));
#117387=CARTESIAN_POINT('Ctrl Pts',(-171.616519103454,-0.983084239545638,
135.623357239318));
#117388=CARTESIAN_POINT('Ctrl Pts',(-171.624267171457,-0.848643939738398,
135.650783309572));
#117389=CARTESIAN_POINT('Ctrl Pts',(-171.63201523946,-0.713091007418455,
135.672571881952));
#117390=CARTESIAN_POINT('Ctrl Pts',(-171.639763307463,-0.576936737012451,
135.688654534192));
#117391=CARTESIAN_POINT('Ctrl Pts',(-171.647519610205,-0.440637760227788,
135.704754279266));
#117392=CARTESIAN_POINT('Ctrl Pts',(-171.655275912947,-0.303736557552501,
135.715135944132));
#117393=CARTESIAN_POINT('Ctrl Pts',(-171.663032215688,-0.16674916315239,
135.719783059136));
#117394=CARTESIAN_POINT('Ctrl Pts',(-171.670792658203,-0.0296886544549024,
135.724432654445));
#117395=CARTESIAN_POINT('Ctrl Pts',(-171.678553100717,0.107457746870967,
135.723341604292));
#117396=CARTESIAN_POINT('Ctrl Pts',(-171.686313543231,0.244175948951485,
135.716545586442));
#117397=CARTESIAN_POINT('Ctrl Pts',(-171.694086443496,0.381113623227256,
135.709738659021));
#117398=CARTESIAN_POINT('Ctrl Pts',(-171.701859343762,0.517621335093968,
135.697208498816));
#117399=CARTESIAN_POINT('Ctrl Pts',(-171.709632244027,0.653191143957876,
135.679042596111));
#117400=CARTESIAN_POINT('Ctrl Pts',(-171.717122579789,0.78383264878984,
135.661537069727));
#117401=CARTESIAN_POINT('Ctrl Pts',(-171.724612915551,0.913602953612798,
135.638798487069));
#117402=CARTESIAN_POINT('Ctrl Pts',(-171.732103251313,1.04206005258033,
135.61094921129));
#117403=CARTESIAN_POINT('Ctrl Pts',(-171.739877585432,1.17538764149908,
135.582044021755));
#117404=CARTESIAN_POINT('Ctrl Pts',(-171.747651919551,1.3077228201397,135.547541382049));
#117405=CARTESIAN_POINT('Ctrl Pts',(-171.755426253671,1.43855918929407,
135.507522375511));
#117406=CARTESIAN_POINT('Ctrl Pts',(-171.763191006618,1.56923431431592,
135.467552688822));
#117407=CARTESIAN_POINT('Ctrl Pts',(-171.770955759565,1.69841393484881,
135.422080275406));
#117408=CARTESIAN_POINT('Ctrl Pts',(-171.778720512512,1.8256014341755,135.371237281768));
#117409=CARTESIAN_POINT('Ctrl Pts',(-171.786477553397,1.95266260908517,
135.320444786109));
#117410=CARTESIAN_POINT('Ctrl Pts',(-171.794234594282,2.07773523961322,
135.264292469583));
#117411=CARTESIAN_POINT('Ctrl Pts',(-171.801991635167,2.2003378284147,135.202962270745));
#117412=CARTESIAN_POINT('Ctrl Pts',(-171.809742826407,2.32284796165042,
135.141678321486));
#117413=CARTESIAN_POINT('Ctrl Pts',(-171.817494017647,2.4428914124644,135.075224436149));
#117414=CARTESIAN_POINT('Ctrl Pts',(-171.825245208887,2.56000697292905,
135.003830508047));
#117415=CARTESIAN_POINT('Ctrl Pts',(-171.832993105664,2.67707275615617,
134.932466924269));
#117416=CARTESIAN_POINT('Ctrl Pts',(-171.840741002442,2.79121279098485,
134.856167676845));
#117417=CARTESIAN_POINT('Ctrl Pts',(-171.848488899219,2.90199098532122,
134.775208308376));
#117418=CARTESIAN_POINT('Ctrl Pts',(-171.856235175303,3.01274600724743,
134.694265874862));
#117419=CARTESIAN_POINT('Ctrl Pts',(-171.863981451387,3.12014027197992,
134.608665489768));
#117420=CARTESIAN_POINT('Ctrl Pts',(-171.871727727471,3.22376750908492,
134.518725450195));
#117421=CARTESIAN_POINT('Ctrl Pts',(-171.879474060736,3.32739551114279,
134.428784746705));
#117422=CARTESIAN_POINT('Ctrl Pts',(-171.887220394002,3.42725613482055,
134.33450458108));
#117423=CARTESIAN_POINT('Ctrl Pts',(-171.894966727267,3.52297729431445,
134.236242615282));
#117424=CARTESIAN_POINT('Ctrl Pts',(-171.90271479527,3.61871988989795,134.137958644398));
#117425=CARTESIAN_POINT('Ctrl Pts',(-171.910462863273,3.71032090390886,
134.035691378966));
#117426=CARTESIAN_POINT('Ctrl Pts',(-171.918210931276,3.79744640362981,
133.929834001561));
#117427=CARTESIAN_POINT('Ctrl Pts',(-171.925967234018,3.88466450136878,
133.823864117675));
#117428=CARTESIAN_POINT('Ctrl Pts',(-171.93372353676,3.96739733408864,133.714296802067));
#117429=CARTESIAN_POINT('Ctrl Pts',(-171.941479839502,4.04535211633096,
133.601557306645));
#117430=CARTESIAN_POINT('Ctrl Pts',(-171.949240282016,4.12334850538773,
133.48875763876));
#117431=CARTESIAN_POINT('Ctrl Pts',(-171.95700072453,4.19656155389788,133.37278274788));
#117432=CARTESIAN_POINT('Ctrl Pts',(-171.964761167044,4.26474339935941,
133.254084438759));
#117433=CARTESIAN_POINT('Ctrl Pts',(-171.97253406731,4.33303469637237,133.135195584575));
#117434=CARTESIAN_POINT('Ctrl Pts',(-171.980306967575,4.39627847036963,
133.013574922825));
#117435=CARTESIAN_POINT('Ctrl Pts',(-171.98807986784,4.45427377510685,132.889697088953));
#117436=CARTESIAN_POINT('Ctrl Pts',(-171.995570203603,4.510160804436,132.77032252637));
#117437=CARTESIAN_POINT('Ctrl Pts',(-172.003060539365,4.56117421042881,
132.648852334288));
#117438=CARTESIAN_POINT('Ctrl Pts',(-172.010550875127,4.60717802571458,
132.525724525016));
#117439=CARTESIAN_POINT('Ctrl Pts',(-172.018325209246,4.65492608963912,
132.397928287433));
#117440=CARTESIAN_POINT('Ctrl Pts',(-172.026099543365,4.69742843821103,
132.267941434181));
#117441=CARTESIAN_POINT('Ctrl Pts',(-172.033873877484,4.73447956799728,
132.136233840781));
#117442=CARTESIAN_POINT('Ctrl Pts',(-172.041638630431,4.77148503557721,
132.004688565219));
#117443=CARTESIAN_POINT('Ctrl Pts',(-172.049403383378,4.80305254660979,
131.87142714173));
#117444=CARTESIAN_POINT('Ctrl Pts',(-172.057168136325,4.82902484622783,
131.73693881644));
#117445=CARTESIAN_POINT('Ctrl Pts',(-172.06492517721,4.85497134979189,131.602584066849));
#117446=CARTESIAN_POINT('Ctrl Pts',(-172.072682218095,4.8753336274519,131.467005221865));
#117447=CARTESIAN_POINT('Ctrl Pts',(-172.08043925898,4.89000448818936,131.330705721075));
#117448=CARTESIAN_POINT('Ctrl Pts',(-172.08819045022,4.9046642855166,131.194509004799));
#117449=CARTESIAN_POINT('Ctrl Pts',(-172.09594164146,4.91364116709979,131.05759310157));
#117450=CARTESIAN_POINT('Ctrl Pts',(-172.103692832701,4.91687925454406,
130.920470301634));
#117451=CARTESIAN_POINT('Ctrl Pts',(-172.111440729478,4.92011596571478,
130.783405782545));
#117452=CARTESIAN_POINT('Ctrl Pts',(-172.119188626255,4.91761872480073,
130.646134931685));
#117453=CARTESIAN_POINT('Ctrl Pts',(-172.126936523032,4.90938363516595,
130.509173583188));
#117454=CARTESIAN_POINT('Ctrl Pts',(-172.134682799116,4.90115026813439,
130.372240884053));
#117455=CARTESIAN_POINT('Ctrl Pts',(-172.1424290752,4.88718146316421,130.235617948521));
#117456=CARTESIAN_POINT('Ctrl Pts',(-172.150175351284,4.86752541352832,
130.099818630772));
#117457=CARTESIAN_POINT('Ctrl Pts',(-172.157921684549,4.84786921879592,
129.964018310583));
#117458=CARTESIAN_POINT('Ctrl Pts',(-172.165668017815,4.82252575163184,
129.829042007242));
#117459=CARTESIAN_POINT('Ctrl Pts',(-172.17341435108,4.79159480170818,129.6953960921));
#117460=CARTESIAN_POINT('Ctrl Pts',(-172.181162419083,4.76065692501263,
129.561720247881));
#117461=CARTESIAN_POINT('Ctrl Pts',(-172.188910487086,4.72412916379682,
129.429375765534));
#117462=CARTESIAN_POINT('Ctrl Pts',(-172.196658555089,4.68216181490638,
129.298856116898));
#117463=CARTESIAN_POINT('Ctrl Pts',(-172.204414857831,4.64014986261829,
129.168197750426));
#117464=CARTESIAN_POINT('Ctrl Pts',(-172.212171160573,4.59268689383651,
129.039368464727));
#117465=CARTESIAN_POINT('Ctrl Pts',(-172.219927463315,4.53997242734291,
128.912844447541));
#117466=CARTESIAN_POINT('Ctrl Pts',(-172.227687905829,4.48722982555134,
128.786252900678));
#117467=CARTESIAN_POINT('Ctrl Pts',(-172.235448348343,4.4292303063213,128.661969428099));
#117468=CARTESIAN_POINT('Ctrl Pts',(-172.243208790857,4.36622001005309,
128.540446775055));
#117469=CARTESIAN_POINT('Ctrl Pts',(-172.250981691122,4.30310856406351,
128.41872904306));
#117470=CARTESIAN_POINT('Ctrl Pts',(-172.258754591388,4.23497046151783,
128.299781326414));
#117471=CARTESIAN_POINT('Ctrl Pts',(-172.266527491653,4.16209641030288,
128.184029238934));
#117472=CARTESIAN_POINT('Ctrl Pts',(-172.274017827415,4.09187151440884,
128.072485031397));
#117473=CARTESIAN_POINT('Ctrl Pts',(-172.281508163177,4.01724919360767,
127.963908402267));
#117474=CARTESIAN_POINT('Ctrl Pts',(-172.288998498939,3.93852446637565,
127.858650501098));
#117475=CARTESIAN_POINT('Ctrl Pts',(-172.296772833058,3.85681486718197,
127.749401714613));
#117476=CARTESIAN_POINT('Ctrl Pts',(-172.304547167177,3.7704268037028,127.643382215742));
#117477=CARTESIAN_POINT('Ctrl Pts',(-172.312321501296,3.67964451589573,
127.541018879541));
#117478=CARTESIAN_POINT('Ctrl Pts',(-172.320086254243,3.58897410914518,
127.438781697003));
#117479=CARTESIAN_POINT('Ctrl Pts',(-172.32785100719,3.49392051019693,127.340192001446));
#117480=CARTESIAN_POINT('Ctrl Pts',(-172.335615760138,3.39481033557449,
127.245646545324));
#117481=CARTESIAN_POINT('Ctrl Pts',(-172.343372801023,3.29579859857468,
127.151194993081));
#117482=CARTESIAN_POINT('Ctrl Pts',(-172.351129841908,3.19273858494966,
127.060779954786));
#117483=CARTESIAN_POINT('Ctrl Pts',(-172.358886882793,3.08599591331679,
126.974763734669));
#117484=CARTESIAN_POINT('Ctrl Pts',(-172.366638074033,2.9793337371628,126.888812380054));
#117485=CARTESIAN_POINT('Ctrl Pts',(-172.374389265273,2.86899473388537,
126.807253485288));
#117486=CARTESIAN_POINT('Ctrl Pts',(-172.382140456513,2.75537970413742,
126.730410967837));
#117487=CARTESIAN_POINT('Ctrl Pts',(-172.38988835329,2.64181296380805,126.653601110506));
#117488=CARTESIAN_POINT('Ctrl Pts',(-172.397636250067,2.52497328955437,
126.581503862096));
#117489=CARTESIAN_POINT('Ctrl Pts',(-172.405384146844,2.40529256101639,
126.514401321906));
#117490=CARTESIAN_POINT('Ctrl Pts',(-172.413130422928,2.28563686710681,
126.447312818121));
#117491=CARTESIAN_POINT('Ctrl Pts',(-172.420876699012,2.16314164178756,
126.385217135504));
#117492=CARTESIAN_POINT('Ctrl Pts',(-172.428622975096,2.03826525477484,
126.328351478425));
#117493=CARTESIAN_POINT('Ctrl Pts',(-172.436369308362,1.91338794595283,
126.271485401576));
#117494=CARTESIAN_POINT('Ctrl Pts',(-172.444115641627,1.78612979617358,
126.21984958933));
#117495=CARTESIAN_POINT('Ctrl Pts',(-172.451861974893,1.65697076875139,
126.173633791893));
#117496=CARTESIAN_POINT('Ctrl Pts',(-172.459610042896,1.52778281706,126.127407644749));
#117497=CARTESIAN_POINT('Ctrl Pts',(-172.467358110899,1.39669350869382,
126.086604059378));
#117498=CARTESIAN_POINT('Ctrl Pts',(-172.475106178902,1.26419925460279,
126.051363320369));
#117499=CARTESIAN_POINT('Ctrl Pts',(-172.482862481644,1.13156418404234,
126.016085127083));
#117500=CARTESIAN_POINT('Ctrl Pts',(-172.490618784385,0.9975215633744,125.98638169119));
#117501=CARTESIAN_POINT('Ctrl Pts',(-172.498375087127,0.862579867607632,
125.962342542992));
#117502=CARTESIAN_POINT('Ctrl Pts',(-172.506135529641,0.727566149394817,
125.938290564378));
#117503=CARTESIAN_POINT('Ctrl Pts',(-172.513895972155,0.591652787162964,
125.919908949816));
#117504=CARTESIAN_POINT('Ctrl Pts',(-172.52165641467,0.455353733211432,
125.907235334285));
#117505=CARTESIAN_POINT('Ctrl Pts',(-172.529429314935,0.318835879918437,
125.894541373941));
#117506=CARTESIAN_POINT('Ctrl Pts',(-172.5372022152,0.181931488338155,125.887573743077));
#117507=CARTESIAN_POINT('Ctrl Pts',(-172.544975115466,0.0451557741424795,
125.88631791558));
#117508=CARTESIAN_POINT('Ctrl Pts',(-172.552465451228,-0.0866477983238361,
125.885107740575));
#117509=CARTESIAN_POINT('Ctrl Pts',(-172.55995578699,-0.218331578604747,
125.889201292303));
#117510=CARTESIAN_POINT('Ctrl Pts',(-172.567446122752,-0.349440669944215,
125.898540168274));
#117511=CARTESIAN_POINT('Ctrl Pts',(-172.575220456871,-0.485520802332531,
125.908233130567));
#117512=CARTESIAN_POINT('Ctrl Pts',(-172.58299479099,-0.621412867816529,
125.923607726199));
#117513=CARTESIAN_POINT('Ctrl Pts',(-172.590769125109,-0.756604085683117,
125.944655552438));
#117514=CARTESIAN_POINT('Ctrl Pts',(-172.598533878056,-0.891628692456069,
125.965677439113));
#117515=CARTESIAN_POINT('Ctrl Pts',(-172.606298631003,-1.0259537875782,
125.99235858533));
#117516=CARTESIAN_POINT('Ctrl Pts',(-172.61406338395,-1.15906902776432,
126.024638653751));
#117517=CARTESIAN_POINT('Ctrl Pts',(-172.621820424835,-1.29205205601728,
126.056886661152));
#117518=CARTESIAN_POINT('Ctrl Pts',(-172.62957746572,-1.4238272431674,126.094722432717));
#117519=CARTESIAN_POINT('Ctrl Pts',(-172.637334506605,-1.55389214660935,
126.138034197436));
#117520=CARTESIAN_POINT('Ctrl Pts',(-172.645085697846,-1.68385896709709,
126.181313300416));
#117521=CARTESIAN_POINT('Ctrl Pts',(-172.652836889086,-1.81211770158416,
126.230060054029));
#117522=CARTESIAN_POINT('Ctrl Pts',(-172.660588080326,-1.93817918658972,
126.284112338636));
#117523=CARTESIAN_POINT('Ctrl Pts',(-172.668335977103,-2.06418709210015,
126.33814164958));
#117524=CARTESIAN_POINT('Ctrl Pts',(-172.67608387388,-2.18799924698974,
126.397471852762));
#117525=CARTESIAN_POINT('Ctrl Pts',(-172.683831770657,-2.30914487163311,
126.461892077172));
#117526=CARTESIAN_POINT('Ctrl Pts',(-172.691578046741,-2.4302651552234,
126.52629882626));
#117527=CARTESIAN_POINT('Ctrl Pts',(-172.699324322825,-2.54871967304773,
126.59579329534));
#117528=CARTESIAN_POINT('Ctrl Pts',(-172.707070598909,-2.66406109832322,
126.670118059745));
#117529=CARTESIAN_POINT('Ctrl Pts',(-172.714816932175,-2.77940337502339,
126.744443372798));
#117530=CARTESIAN_POINT('Ctrl Pts',(-172.72256326544,-2.89163218467719,
126.823598840552));
#117531=CARTESIAN_POINT('Ctrl Pts',(-172.730309598705,-3.00032845316646,
126.907283220898));
#117532=CARTESIAN_POINT('Ctrl Pts',(-172.738057666708,-3.10904906343157,
126.990986341781));
#117533=CARTESIAN_POINT('Ctrl Pts',(-172.745805734712,-3.21423524862831,
127.079220154976));
#117534=CARTESIAN_POINT('Ctrl Pts',(-172.753553802715,-3.31550066111441,
127.171642843137));
#117535=CARTESIAN_POINT('Ctrl Pts',(-172.761310105456,-3.41687369968555,
127.264163759232));
#117536=CARTESIAN_POINT('Ctrl Pts',(-172.769066408198,-3.51431735219186,
127.360882179636));
#117537=CARTESIAN_POINT('Ctrl Pts',(-172.77682271094,-3.60748145109045,
127.461418703243));
#117538=CARTESIAN_POINT('Ctrl Pts',(-172.784583153454,-3.70069527447399,
127.562008886219));
#117539=CARTESIAN_POINT('Ctrl Pts',(-172.792343595968,-3.78962473955368,
127.666420935465));
#117540=CARTESIAN_POINT('Ctrl Pts',(-172.800104038482,-3.87396037918624,
127.77424279098));
#117541=CARTESIAN_POINT('Ctrl Pts',(-172.807876938748,-3.95843140187404,
127.882237731708));
#117542=CARTESIAN_POINT('Ctrl Pts',(-172.815649839013,-4.03829363477777,
127.993653099002));
#117543=CARTESIAN_POINT('Ctrl Pts',(-172.823422739279,-4.11328081247327,
128.108047575607));
#117544=CARTESIAN_POINT('Ctrl Pts',(-172.830913075041,-4.18554201737741,
128.218283524843));
#117545=CARTESIAN_POINT('Ctrl Pts',(-172.838403410803,-4.25327629616988,
128.331285483371));
#117546=CARTESIAN_POINT('Ctrl Pts',(-172.845893746565,-4.31628690171076,
128.446639165693));
#117547=CARTESIAN_POINT('Ctrl Pts',(-172.854068586708,-4.38505573183823,
128.572534445006));
#117548=CARTESIAN_POINT('Ctrl Pts',(-172.862243426851,-4.44839760949704,
128.701595936106));
#117549=CARTESIAN_POINT('Ctrl Pts',(-172.870418266993,-4.50602512050778,
128.833340405632));
#117550=CARTESIAN_POINT('Ctrl Pts',(-172.878574919318,-4.5635244187734,
128.96479176307));
#117551=CARTESIAN_POINT('Ctrl Pts',(-172.886731571643,-4.6153345655119,
129.098913895225));
#117552=CARTESIAN_POINT('Ctrl Pts',(-172.894888223968,-4.6612139626585,
129.235199231087));
#117553=CARTESIAN_POINT('Ctrl Pts',(-172.90173178748,-4.69970752052794,
129.349544836937));
#117554=CARTESIAN_POINT('Ctrl Pts',(-172.908575350993,-4.73402685051016,
129.465412659596));
#117555=CARTESIAN_POINT('Ctrl Pts',(-172.915418914505,-4.76405452823406,
129.582490119308));
#117556=CARTESIAN_POINT('Ctrl Pts',(-171.165157400749,-4.76405452823416,
129.582490119309));
#117557=CARTESIAN_POINT('Ctrl Pts',(-171.168507601729,-4.77867918020337,
129.639511415377));
#117558=CARTESIAN_POINT('Ctrl Pts',(-171.171857802708,-4.79227071959931,
129.696759316179));
#117559=CARTESIAN_POINT('Ctrl Pts',(-171.175208003688,-4.80482377000955,
129.754193201555));
#117560=CARTESIAN_POINT('Ctrl Pts',(-171.185974661452,-4.84516594604442,
129.938770482654));
#117561=CARTESIAN_POINT('Ctrl Pts',(-171.196741319217,-4.87488446168539,
130.125746382853));
#117562=CARTESIAN_POINT('Ctrl Pts',(-171.207507976981,-4.89375382829365,
130.31409892157));
#117563=CARTESIAN_POINT('Ctrl Pts',(-171.216718839325,-4.90989654798845,
130.47523428448));
#117564=CARTESIAN_POINT('Ctrl Pts',(-171.225929701668,-4.9180996550663,
130.637377204443));
#117565=CARTESIAN_POINT('Ctrl Pts',(-171.235140564012,-4.91824795183824,
130.799872105685));
#117566=CARTESIAN_POINT('',(-170.889859435956,-4.91824925841368,130.807061471733));
#117567=CARTESIAN_POINT('Ctrl Pts',(-170.819717755703,-4.76405452823413,
129.582490119309));
#117568=CARTESIAN_POINT('Ctrl Pts',(-170.827380355377,-4.79774344099872,
129.713842678877));
#117569=CARTESIAN_POINT('Ctrl Pts',(-170.835042955051,-4.82597252582046,
129.846498967558));
#117570=CARTESIAN_POINT('Ctrl Pts',(-170.842705554725,-4.84866437856723,
129.979959740254));
#117571=CARTESIAN_POINT('Ctrl Pts',(-170.85056453493,-4.87193778826417,
130.116840905317));
#117572=CARTESIAN_POINT('Ctrl Pts',(-170.858423515135,-4.88938625812206,
130.254567894436));
#117573=CARTESIAN_POINT('Ctrl Pts',(-170.866282495341,-4.90098307374099,
130.392598582643));
#117574=CARTESIAN_POINT('Ctrl Pts',(-170.874141475546,-4.91257988935995,
130.530629270849));
#117575=CARTESIAN_POINT('Ctrl Pts',(-170.882000455751,-4.91832509500793,
130.668963207153));
#117576=CARTESIAN_POINT('Ctrl Pts',(-170.889859435956,-4.91824925841368,
130.807061471733));
#117577=CARTESIAN_POINT('Ctrl Pts',(-170.889859435994,-4.91824925841332,
130.807061472394));
#117578=CARTESIAN_POINT('Ctrl Pts',(-170.898689416008,-4.91816405196695,
130.962222178274));
#117579=CARTESIAN_POINT('Ctrl Pts',(-170.907519396022,-4.91073700608355,
131.117177606773));
#117580=CARTESIAN_POINT('Ctrl Pts',(-170.916349376036,-4.8960220816411,
131.271426821206));
#117581=CARTESIAN_POINT('Ctrl Pts',(-170.924123710155,-4.88306636271859,
131.407235161509));
#117582=CARTESIAN_POINT('Ctrl Pts',(-170.931898044274,-4.86443515971341,
131.542719145533));
#117583=CARTESIAN_POINT('Ctrl Pts',(-170.939672378393,-4.84014917826146,
131.677366341874));
#117584=CARTESIAN_POINT('Ctrl Pts',(-170.94743713134,-4.81589312711116,
131.81184759758));
#117585=CARTESIAN_POINT('Ctrl Pts',(-170.955201884287,-4.78599623249637,
131.945493736452));
#117586=CARTESIAN_POINT('Ctrl Pts',(-170.962966637234,-4.75053106121194,
132.077796010101));
#117587=CARTESIAN_POINT('Ctrl Pts',(-170.970723678119,-4.71510111443569,
132.209966879267));
#117588=CARTESIAN_POINT('Ctrl Pts',(-170.978480719004,-4.6741139974901,
132.340796164225));
#117589=CARTESIAN_POINT('Ctrl Pts',(-170.986237759889,-4.62769350643511,
132.469784249258));
#117590=CARTESIAN_POINT('Ctrl Pts',(-170.993988951129,-4.58130802143347,
132.598675063373));
#117591=CARTESIAN_POINT('Ctrl Pts',(-171.001740142369,-4.52949744970189,
132.725727074835));
#117592=CARTESIAN_POINT('Ctrl Pts',(-171.009491333609,-4.47243560276683,
132.850455151453));
#117593=CARTESIAN_POINT('Ctrl Pts',(-171.017239230386,-4.41539800863882,
132.975130215313));
#117594=CARTESIAN_POINT('Ctrl Pts',(-171.024987127163,-4.35311374075912,
133.097482954075));
#117595=CARTESIAN_POINT('Ctrl Pts',(-171.03273502394,-4.2858049068253,133.217047784012));
#117596=CARTESIAN_POINT('Ctrl Pts',(-171.040481300024,-4.21851015244852,
133.336587603563));
#117597=CARTESIAN_POINT('Ctrl Pts',(-171.048227576109,-4.14619311424533,
133.453340333772));
#117598=CARTESIAN_POINT('Ctrl Pts',(-171.055973852193,-4.0691218773607,
133.566864954157));
#117599=CARTESIAN_POINT('Ctrl Pts',(-171.063720185458,-3.99205007155381,
133.680390412555));
#117600=CARTESIAN_POINT('Ctrl Pts',(-171.071466518723,-3.91022421663621,
133.790687390113));
#117601=CARTESIAN_POINT('Ctrl Pts',(-171.079212851989,-3.82395552458879,
133.897344162376));
#117602=CARTESIAN_POINT('Ctrl Pts',(-171.086960919992,-3.73766751326605,
134.004024819684));
#117603=CARTESIAN_POINT('Ctrl Pts',(-171.094708987995,-3.64693493081568,
134.107063345628));
#117604=CARTESIAN_POINT('Ctrl Pts',(-171.102457055998,-3.5521087674248,
134.206081706498));
#117605=CARTESIAN_POINT('Ctrl Pts',(-171.11021335874,-3.45718182165889,
134.30520530526));
#117606=CARTESIAN_POINT('Ctrl Pts',(-171.117969661481,-3.35815287479082,
134.400299920994));
#117607=CARTESIAN_POINT('Ctrl Pts',(-171.125725964223,-3.25540962172723,
134.491024591576));
#117608=CARTESIAN_POINT('Ctrl Pts',(-171.133486406737,-3.15261153149595,
134.581797684647));
#117609=CARTESIAN_POINT('Ctrl Pts',(-171.141246849251,-3.0460954883841,
134.668195938951));
#117610=CARTESIAN_POINT('Ctrl Pts',(-171.149007291766,-2.93628086008807,
134.749919864768));
#117611=CARTESIAN_POINT('Ctrl Pts',(-171.156780192031,-2.82628994760182,
134.831774981085));
#117612=CARTESIAN_POINT('Ctrl Pts',(-171.164553092297,-2.71299019179485,
134.90894055403));
#117613=CARTESIAN_POINT('Ctrl Pts',(-171.172325992562,-2.59682917247071,
134.981160985252));
#117614=CARTESIAN_POINT('Ctrl Pts',(-171.179816328324,-2.48489089879221,
135.050756021887));
#117615=CARTESIAN_POINT('Ctrl Pts',(-171.187306664086,-2.37029604610925,
135.115759059456));
#117616=CARTESIAN_POINT('Ctrl Pts',(-171.194796999848,-2.25346350200287,
135.175983349189));
#117617=CARTESIAN_POINT('Ctrl Pts',(-171.202571333967,-2.132201216475,135.238491061172));
#117618=CARTESIAN_POINT('Ctrl Pts',(-171.210345668086,-2.00814408329354,
135.296048505166));
#117619=CARTESIAN_POINT('Ctrl Pts',(-171.218120002205,-1.88173441741219,
135.348396119719));
#117620=CARTESIAN_POINT('Ctrl Pts',(-171.225884755152,-1.75548054014683,
135.400679220515));
#117621=CARTESIAN_POINT('Ctrl Pts',(-171.233649508099,-1.6268802566474,
135.447765118901));
#117622=CARTESIAN_POINT('Ctrl Pts',(-171.241414261046,-1.49640081546734,
135.489439876444));
#117623=CARTESIAN_POINT('Ctrl Pts',(-171.249171301931,-1.36605096830771,
135.53107324203));
#117624=CARTESIAN_POINT('Ctrl Pts',(-171.256928342816,-1.23382604771927,
135.567306043932));
#117625=CARTESIAN_POINT('Ctrl Pts',(-171.264685383701,-1.10021330934991,
135.597972380781));
#117626=CARTESIAN_POINT('Ctrl Pts',(-171.272436574942,-0.966701329385724,
135.628615591906));
#117627=CARTESIAN_POINT('Ctrl Pts',(-171.280187766182,-0.831803994278676,
135.65370060617));
#117628=CARTESIAN_POINT('Ctrl Pts',(-171.287938957422,-0.696023408855133,
135.673111430334));
#117629=CARTESIAN_POINT('Ctrl Pts',(-171.295686854199,-0.560300533802645,
135.692514004379));
#117630=CARTESIAN_POINT('Ctrl Pts',(-171.303434750976,-0.423695541305577,
135.706247129763));
#117631=CARTESIAN_POINT('Ctrl Pts',(-171.311182647753,-0.28672019477748,
135.714246012604));
#117632=CARTESIAN_POINT('Ctrl Pts',(-171.318928923837,-0.14977350053903,
135.722243222251));
#117633=CARTESIAN_POINT('Ctrl Pts',(-171.326675199921,-0.0124569964147891,
135.724508552408));
#117634=CARTESIAN_POINT('Ctrl Pts',(-171.334421476005,0.124713368004535,
135.721029168357));
#117635=CARTESIAN_POINT('Ctrl Pts',(-171.34216780927,0.261884744984515,
135.717549758623));
#117636=CARTESIAN_POINT('Ctrl Pts',(-171.349914142536,0.398909589267479,
135.708325559976));
#117637=CARTESIAN_POINT('Ctrl Pts',(-171.357660475801,0.535273287731169,
135.693395856746));
#117638=CARTESIAN_POINT('Ctrl Pts',(-171.365408543804,0.671667523899464,
135.678462810112));
#117639=CARTESIAN_POINT('Ctrl Pts',(-171.373156611807,0.807399931059714,
135.657821758945));
#117640=CARTESIAN_POINT('Ctrl Pts',(-171.38090467981,0.941962739975745,
135.631563664776));
#117641=CARTESIAN_POINT('Ctrl Pts',(-171.388660982552,1.07666856384623,
135.605277663193));
#117642=CARTESIAN_POINT('Ctrl Pts',(-171.396417285294,1.21020192198088,
135.573362768167));
#117643=CARTESIAN_POINT('Ctrl Pts',(-171.404173588035,1.34206639472225,
135.535960860048));
#117644=CARTESIAN_POINT('Ctrl Pts',(-171.41193403055,1.47400124750345,135.498538989405));
#117645=CARTESIAN_POINT('Ctrl Pts',(-171.419694473064,1.60426506887617,
135.45562439249));
#117646=CARTESIAN_POINT('Ctrl Pts',(-171.427454915578,1.73237921117304,
135.407408013715));
#117647=CARTESIAN_POINT('Ctrl Pts',(-171.435227815843,1.86069901366456,
135.359114233728));
#117648=CARTESIAN_POINT('Ctrl Pts',(-171.443000716109,1.98686188113952,
135.305501817403));
#117649=CARTESIAN_POINT('Ctrl Pts',(-171.450773616374,2.11041084365142,
135.246809169153));
#117650=CARTESIAN_POINT('Ctrl Pts',(-171.458263952136,2.22946849017897,
135.190250146503));
#117651=CARTESIAN_POINT('Ctrl Pts',(-171.465754287899,2.34609870368315,
135.128973981037));
#117652=CARTESIAN_POINT('Ctrl Pts',(-171.473244623661,2.45991794816356,
135.063232152469));
#117653=CARTESIAN_POINT('Ctrl Pts',(-171.48101895778,2.57805268388956,134.99499770249));
#117654=CARTESIAN_POINT('Ctrl Pts',(-171.488793291899,2.69353330238229,
134.921736127261));
#117655=CARTESIAN_POINT('Ctrl Pts',(-171.496567626018,2.8059023452044,134.843679259574));
#117656=CARTESIAN_POINT('Ctrl Pts',(-171.504332378965,2.91813290322363,
134.765718590001));
#117657=CARTESIAN_POINT('Ctrl Pts',(-171.512097131912,3.02725919754571,
134.682974607558));
#117658=CARTESIAN_POINT('Ctrl Pts',(-171.519861884859,3.13284867645284,
134.595724782738));
#117659=CARTESIAN_POINT('Ctrl Pts',(-171.527618925744,3.23833328240096,
134.508561615673));
#117660=CARTESIAN_POINT('Ctrl Pts',(-171.535375966629,3.34028776415866,
134.416901759641));
#117661=CARTESIAN_POINT('Ctrl Pts',(-171.543133007514,3.43830917062676,
134.321065482874));
#117662=CARTESIAN_POINT('Ctrl Pts',(-171.550884198754,3.53625665838989,
134.22530147699));
#117663=CARTESIAN_POINT('Ctrl Pts',(-171.558635389994,3.63027669601083,
134.125367591418));
#117664=CARTESIAN_POINT('Ctrl Pts',(-171.566386581235,3.72000029516956,
134.021623563991));
#117665=CARTESIAN_POINT('Ctrl Pts',(-171.574134478012,3.80968575940506,
133.917923630543));
#117666=CARTESIAN_POINT('Ctrl Pts',(-171.581882374789,3.89507816194029,
133.810417071221));
#117667=CARTESIAN_POINT('Ctrl Pts',(-171.589630271566,3.97584636922172,
133.699499424402));
#117668=CARTESIAN_POINT('Ctrl Pts',(-171.59737654765,4.05659768153535,133.588604979163));
#117669=CARTESIAN_POINT('Ctrl Pts',(-171.605122823734,4.1327264925753,133.474301181521));
#117670=CARTESIAN_POINT('Ctrl Pts',(-171.612869099818,4.20394312077346,
133.357015177));
#117671=CARTESIAN_POINT('Ctrl Pts',(-171.620615433083,4.27516027467669,
133.239728306701));
#117672=CARTESIAN_POINT('Ctrl Pts',(-171.628361766349,4.34146497046516,
133.119459519778));
#117673=CARTESIAN_POINT('Ctrl Pts',(-171.636108099614,4.40261209819438,
132.996663008965));
#117674=CARTESIAN_POINT('Ctrl Pts',(-171.643856167617,4.4637729193988,132.873838998725));
#117675=CARTESIAN_POINT('Ctrl Pts',(-171.65160423562,4.51977369998571,132.748486488098));
#117676=CARTESIAN_POINT('Ctrl Pts',(-171.659352303623,4.57041650679202,
132.621081844652));
#117677=CARTESIAN_POINT('Ctrl Pts',(-171.667108606365,4.62111313737612,
132.493541794034));
#117678=CARTESIAN_POINT('Ctrl Pts',(-171.674864909107,4.66644027411946,
132.363945617647));
#117679=CARTESIAN_POINT('Ctrl Pts',(-171.682621211849,4.70624895802751,
132.232787657203));
#117680=CARTESIAN_POINT('Ctrl Pts',(-171.690381654363,4.74607888902877,
132.101559693805));
#117681=CARTESIAN_POINT('Ctrl Pts',(-171.698142096877,4.78038440056246,
131.968768663741));
#117682=CARTESIAN_POINT('Ctrl Pts',(-171.705902539391,4.80906741881327,
131.834920476967));
#117683=CARTESIAN_POINT('Ctrl Pts',(-171.713675439656,4.83779648159133,
131.700857425201));
#117684=CARTESIAN_POINT('Ctrl Pts',(-171.721448339922,4.8608849489236,131.565734211096));
#117685=CARTESIAN_POINT('Ctrl Pts',(-171.729221240187,4.87828639377724,
131.430064159819));
#117686=CARTESIAN_POINT('Ctrl Pts',(-171.736711575949,4.89505525227881,
131.299326056639));
#117687=CARTESIAN_POINT('Ctrl Pts',(-171.744201911711,4.90654335809107,
131.168080490695));
#117688=CARTESIAN_POINT('Ctrl Pts',(-171.751692247473,4.91275497764192,
131.036786072615));
#117689=CARTESIAN_POINT('Ctrl Pts',(-171.759466581592,4.91920211263604,
130.900513586766));
#117690=CARTESIAN_POINT('Ctrl Pts',(-171.767240915711,4.91998516958657,
130.763756800922));
#117691=CARTESIAN_POINT('Ctrl Pts',(-171.775015249831,4.91505192852834,
130.62702589911));
#117692=CARTESIAN_POINT('Ctrl Pts',(-171.782780002778,4.91012476724883,
130.490463505914));
#117693=CARTESIAN_POINT('Ctrl Pts',(-171.790544755725,4.89949533902691,
130.353927320239));
#117694=CARTESIAN_POINT('Ctrl Pts',(-171.798309508672,4.88316328287778,
130.217931239674));
#117695=CARTESIAN_POINT('Ctrl Pts',(-171.806066549557,4.86684744795705,
130.082070232334));
#117696=CARTESIAN_POINT('Ctrl Pts',(-171.813823590442,4.84484030290152,
129.946748648228));
#117697=CARTESIAN_POINT('Ctrl Pts',(-171.821580631327,4.81719349353562,
129.812478614333));
#117698=CARTESIAN_POINT('Ctrl Pts',(-171.829331822567,4.78956753284368,
129.678309834514));
#117699=CARTESIAN_POINT('Ctrl Pts',(-171.837083013807,4.75631045153859,
129.545191407905));
#117700=CARTESIAN_POINT('Ctrl Pts',(-171.844834205047,4.71752546004666,
129.413628221916));
#117701=CARTESIAN_POINT('Ctrl Pts',(-171.852582101825,4.67875695321079,
129.28212095379));
#117702=CARTESIAN_POINT('Ctrl Pts',(-171.860329998602,4.63446531950464,
129.152167985791));
#117703=CARTESIAN_POINT('Ctrl Pts',(-171.868077895379,4.58480435079363,
129.024261708111));
#117704=CARTESIAN_POINT('Ctrl Pts',(-171.875824171463,4.5351537700867,128.896382185667));
#117705=CARTESIAN_POINT('Ctrl Pts',(-171.883570447547,4.4801362297954,128.770548866208));
#117706=CARTESIAN_POINT('Ctrl Pts',(-171.891316723631,4.4199545195836,128.647236349631));
#117707=CARTESIAN_POINT('Ctrl Pts',(-171.899063056896,4.359772365124,128.52392292279));
#117708=CARTESIAN_POINT('Ctrl Pts',(-171.906809390162,4.29442613615247,
128.403130687316));
#117709=CARTESIAN_POINT('Ctrl Pts',(-171.914555723427,4.22416546996696,
128.285311363415));
#117710=CARTESIAN_POINT('Ctrl Pts',(-171.92230379143,4.15388906939252,128.167465654693));
#117711=CARTESIAN_POINT('Ctrl Pts',(-171.930051859433,4.07869624183661,
128.052594518062));
#117712=CARTESIAN_POINT('Ctrl Pts',(-171.937799927436,3.99888078111654,
127.941121968603));
#117713=CARTESIAN_POINT('Ctrl Pts',(-171.945556230178,3.91898049157488,
127.829530944792));
#117714=CARTESIAN_POINT('Ctrl Pts',(-171.95331253292,3.83444798261287,127.721346042018));
#117715=CARTESIAN_POINT('Ctrl Pts',(-171.961068835662,3.74561864193781,
127.616959787475));
#117716=CARTESIAN_POINT('Ctrl Pts',(-171.968829278176,3.65674189036904,
127.512517818844));
#117717=CARTESIAN_POINT('Ctrl Pts',(-171.97658972069,3.56356400288141,127.411878825057));
#117718=CARTESIAN_POINT('Ctrl Pts',(-171.984350163204,3.46645760455681,
127.315398775082));
#117719=CARTESIAN_POINT('Ctrl Pts',(-171.99212306347,3.36919532242091,127.218763846766));
#117720=CARTESIAN_POINT('Ctrl Pts',(-171.999895963735,3.2679922160663,127.126301467508));
#117721=CARTESIAN_POINT('Ctrl Pts',(-172.007668864001,3.16325506554889,
127.038328162478));
#117722=CARTESIAN_POINT('Ctrl Pts',(-172.015159199763,3.06232537427002,
126.953552908677));
#117723=CARTESIAN_POINT('Ctrl Pts',(-172.022649535525,2.95811436437813,
126.872946205653));
#117724=CARTESIAN_POINT('Ctrl Pts',(-172.030139871287,2.85101018409053,
126.796752354186));
#117725=CARTESIAN_POINT('Ctrl Pts',(-172.037914205406,2.73984511625326,
126.717669589681));
#117726=CARTESIAN_POINT('Ctrl Pts',(-172.045688539525,2.62521102057852,
126.643090398473));
#117727=CARTESIAN_POINT('Ctrl Pts',(-172.053462873644,2.50750890317026,
126.573334481624));
#117728=CARTESIAN_POINT('Ctrl Pts',(-172.061227626591,2.38995184310237,
126.503664532709));
#117729=CARTESIAN_POINT('Ctrl Pts',(-172.068992379538,2.26933461759565,
126.438806228274));
#117730=CARTESIAN_POINT('Ctrl Pts',(-172.076757132485,2.14608938812568,
126.379037646225));
#117731=CARTESIAN_POINT('Ctrl Pts',(-172.08451417337,2.02296656755508,126.319328427175));
#117732=CARTESIAN_POINT('Ctrl Pts',(-172.092271214255,1.8972212868832,126.264699039963));
#117733=CARTESIAN_POINT('Ctrl Pts',(-172.10002825514,1.76931232886848,126.215382850632));
#117734=CARTESIAN_POINT('Ctrl Pts',(-172.10777944638,1.64149982799416,126.166103851024));
#117735=CARTESIAN_POINT('Ctrl Pts',(-172.115530637621,1.51152726078365,
126.122130214235));
#117736=CARTESIAN_POINT('Ctrl Pts',(-172.123281828861,1.37987519106998,
126.083648010388));
#117737=CARTESIAN_POINT('Ctrl Pts',(-172.131029725638,1.24827907699768,
126.045182162504));
#117738=CARTESIAN_POINT('Ctrl Pts',(-172.138777622415,1.11500525465913,
126.012203214865));
#117739=CARTESIAN_POINT('Ctrl Pts',(-172.146525519192,0.980551114127505,
125.984847926942));
#117740=CARTESIAN_POINT('Ctrl Pts',(-172.154271795276,0.846125098503584,
125.957498361156));
#117741=CARTESIAN_POINT('Ctrl Pts',(-172.16201807136,0.710519638652083,
125.935770193164));
#117742=CARTESIAN_POINT('Ctrl Pts',(-172.169764347444,0.57424364167457,
125.919749343115));
#117743=CARTESIAN_POINT('Ctrl Pts',(-172.17751068071,0.437966638738791,
125.903728374803));
#117744=CARTESIAN_POINT('Ctrl Pts',(-172.185257013975,0.301019477091297,
125.89341485415));
#117745=CARTESIAN_POINT('Ctrl Pts',(-172.19300334724,0.163917136791152,
125.888842920032));
#117746=CARTESIAN_POINT('Ctrl Pts',(-172.200751415243,0.0267840933723109,
125.884269962061));
#117747=CARTESIAN_POINT('Ctrl Pts',(-172.208499483246,-0.110503807176791,
125.885441162223));
#117748=CARTESIAN_POINT('Ctrl Pts',(-172.216247551249,-0.247431026223936,
125.892338533967));
#117749=CARTESIAN_POINT('Ctrl Pts',(-172.224003853991,-0.384503773148752,
125.89924323632));
#117750=CARTESIAN_POINT('Ctrl Pts',(-172.231760156733,-0.521214681722725,
125.911886247683));
#117751=CARTESIAN_POINT('Ctrl Pts',(-172.239516459475,-0.657052222455101,
125.930197567414));
#117752=CARTESIAN_POINT('Ctrl Pts',(-172.247276901989,-0.792962263772955,
125.948518660447));
#117753=CARTESIAN_POINT('Ctrl Pts',(-172.255037344503,-0.927997623673685,
125.97251402174));
#117754=CARTESIAN_POINT('Ctrl Pts',(-172.262797787017,-1.06165740242473,
126.002062561179));
#117755=CARTESIAN_POINT('Ctrl Pts',(-172.270570687283,-1.19553174371839,
126.031658534557));
#117756=CARTESIAN_POINT('Ctrl Pts',(-172.278343587548,-1.32802571306665,
126.066825399646));
#117757=CARTESIAN_POINT('Ctrl Pts',(-172.286116487814,-1.45865313432394,
126.107392010451));
#117758=CARTESIAN_POINT('Ctrl Pts',(-172.293606823576,-1.58453191978578,
126.146483922771));
#117759=CARTESIAN_POINT('Ctrl Pts',(-172.301097159337,-1.70867721828038,
126.190589704889));
#117760=CARTESIAN_POINT('Ctrl Pts',(-172.308587495099,-1.83067368905062,
126.239514847256));
#117761=CARTESIAN_POINT('Ctrl Pts',(-172.316362158004,-1.95730104808944,
126.290297148821));
#117762=CARTESIAN_POINT('Ctrl Pts',(-172.324136820909,-2.08201435566358,
126.346432786249));
#117763=CARTESIAN_POINT('Ctrl Pts',(-172.331911483814,-2.20432782329072,
126.40775716604));
#117764=CARTESIAN_POINT('Ctrl Pts',(-172.339676489964,-2.32648936777396,
126.46900537603));
#117765=CARTESIAN_POINT('Ctrl Pts',(-172.347441496114,-2.44625665720255,
126.53542933104));
#117766=CARTESIAN_POINT('Ctrl Pts',(-172.355206502264,-2.56316209831764,
126.606815725579));
#117767=CARTESIAN_POINT('Ctrl Pts',(-172.362963721089,-2.67995029797483,
126.67813052854));
#117768=CARTESIAN_POINT('Ctrl Pts',(-172.370720939913,-2.79388202959112,
126.75439766425));
#117769=CARTESIAN_POINT('Ctrl Pts',(-172.378478158738,-2.90451294396446,
126.835357263972));
#117770=CARTESIAN_POINT('Ctrl Pts',(-172.386451739572,-3.0182295424432,
126.918574964437));
#117771=CARTESIAN_POINT('Ctrl Pts',(-172.394425320405,-3.12845811514606,
127.006750549142));
#117772=CARTESIAN_POINT('Ctrl Pts',(-172.402398901239,-3.23474596164022,
127.099552710784));
#117773=CARTESIAN_POINT('Ctrl Pts',(-172.410146456388,-3.33802088537537,
127.189724225987));
#117774=CARTESIAN_POINT('Ctrl Pts',(-172.417894011538,-3.43757516142897,
127.284263291409));
#117775=CARTESIAN_POINT('Ctrl Pts',(-172.425641566688,-3.53302591456912,
127.382824274126));
#117776=CARTESIAN_POINT('Ctrl Pts',(-172.433387442438,-3.62845597731616,
127.48136389226));
#117777=CARTESIAN_POINT('Ctrl Pts',(-172.441133318188,-3.71978401533456,
127.583923412318));
#117778=CARTESIAN_POINT('Ctrl Pts',(-172.448879193938,-3.80666382319468,
127.690120164473));
#117779=CARTESIAN_POINT('Ctrl Pts',(-172.456625068071,-3.8935436129223,
127.796316894464));
#117780=CARTESIAN_POINT('Ctrl Pts',(-172.464370942205,-3.9759749273941,
127.90615055208));
#117781=CARTESIAN_POINT('Ctrl Pts',(-172.472116816338,-4.05365194871594,
128.01920551575));
#117782=CARTESIAN_POINT('Ctrl Pts',(-172.480260756539,-4.13532084826993,
128.138070455663));
#117783=CARTESIAN_POINT('Ctrl Pts',(-172.488404696739,-4.21173357218008,
128.260496177886));
#117784=CARTESIAN_POINT('Ctrl Pts',(-172.496548636939,-4.2825869625209,
128.385966114813));
#117785=CARTESIAN_POINT('Ctrl Pts',(-172.504303202507,-4.35005274046332,
128.505437136064));
#117786=CARTESIAN_POINT('Ctrl Pts',(-172.512057768075,-4.41247830169827,
128.627667653528));
#117787=CARTESIAN_POINT('Ctrl Pts',(-172.519812333643,-4.46965001415215,
128.752188155639));
#117788=CARTESIAN_POINT('Ctrl Pts',(-172.527571115191,-4.52685280956229,
128.876776356708));
#117789=CARTESIAN_POINT('Ctrl Pts',(-172.53532989674,-4.5787959173205,129.003656661905));
#117790=CARTESIAN_POINT('Ctrl Pts',(-172.543088678288,-4.62531453699467,
129.132341330487));
#117791=CARTESIAN_POINT('Ctrl Pts',(-172.55085655863,-4.67188770947539,
129.261176908744));
#117792=CARTESIAN_POINT('Ctrl Pts',(-172.558624438972,-4.71302357995576,
129.391820702198));
#117793=CARTESIAN_POINT('Ctrl Pts',(-172.566392319314,-4.748607623431,129.523771416771));
#117794=CARTESIAN_POINT('Ctrl Pts',(-172.567542912456,-4.75387839931574,
129.543316206413));
#117795=CARTESIAN_POINT('Ctrl Pts',(-172.568693505597,-4.75902745959226,
129.56288965497));
#117796=CARTESIAN_POINT('Ctrl Pts',(-172.569844098739,-4.76405452823414,
129.582490119309));
#117797=CARTESIAN_POINT('Origin',(213.235140564004,0.,130.804360617566));
#117798=CARTESIAN_POINT('',(-174.665085416107,-4.76405452823406,129.582490119308));
#117799=CARTESIAN_POINT('',(-174.32014438825,-4.76405452823397,129.582490119308));
#117800=CARTESIAN_POINT('',(213.235140564004,-4.76405452823405,129.582490119308));
#117801=CARTESIAN_POINT('',(-172.985140564014,-4.91824999999948,130.804362873451));
#117802=CARTESIAN_POINT('Ctrl Pts',(-172.985140564016,-4.91824999999948,
130.804362873489));
#117803=CARTESIAN_POINT('Ctrl Pts',(-172.993255459135,-4.91824993390674,
130.948454988518));
#117804=CARTESIAN_POINT('Ctrl Pts',(-173.001370354255,-4.91191326672245,
131.092424657378));
#117805=CARTESIAN_POINT('Ctrl Pts',(-173.009485249374,-4.89929800797417,
131.235709770295));
#117806=CARTESIAN_POINT('Ctrl Pts',(-173.017610838002,-4.88666612530449,
131.379183699035));
#117807=CARTESIAN_POINT('Ctrl Pts',(-173.02573642663,-4.86773917045749,
131.521970940276));
#117808=CARTESIAN_POINT('Ctrl Pts',(-173.033862015258,-4.84262656737017,
131.663517757733));
#117809=CARTESIAN_POINT('Ctrl Pts',(-173.042006812052,-4.81745460032891,
131.805399179243));
#117810=CARTESIAN_POINT('Ctrl Pts',(-173.050151608847,-4.78606780760041,
131.946033985146));
#117811=CARTESIAN_POINT('Ctrl Pts',(-173.058296405642,-4.74862644793337,
132.084880012377));
#117812=CARTESIAN_POINT('Ctrl Pts',(-173.066451341225,-4.71113848059374,
132.22389887762));
#117813=CARTESIAN_POINT('Ctrl Pts',(-173.074606276808,-4.66758100579246,
132.361124203243));
#117814=CARTESIAN_POINT('Ctrl Pts',(-173.082761212391,-4.61816315305185,
132.496032026054));
#117815=CARTESIAN_POINT('Ctrl Pts',(-173.090934843589,-4.56863200731042,
132.631249132073));
#117816=CARTESIAN_POINT('Ctrl Pts',(-173.099108474786,-4.51321374718174,
132.764137803449));
#117817=CARTESIAN_POINT('Ctrl Pts',(-173.107282105984,-4.45216510774585,
132.894195279895));
#117818=CARTESIAN_POINT('Ctrl Pts',(-173.112968527449,-4.40969337330281,
132.984676683788));
#117819=CARTESIAN_POINT('Ctrl Pts',(-173.118654948913,-4.36449748628318,
133.073788297874));
#117820=CARTESIAN_POINT('Ctrl Pts',(-173.124341370377,-4.3166763331456,
133.161368996287));
#117821=CARTESIAN_POINT('Ctrl Pts',(-173.132115704497,-4.25129644092726,
133.281107150784));
#117822=CARTESIAN_POINT('Ctrl Pts',(-173.139890038616,-4.18082717965119,
133.398312589513));
#117823=CARTESIAN_POINT('Ctrl Pts',(-173.147664372735,-4.10548933760674,
133.512522422425));
#117824=CARTESIAN_POINT('Ctrl Pts',(-173.155429125682,-4.03024434271947,
133.626591501925));
#117825=CARTESIAN_POINT('Ctrl Pts',(-173.163193878629,-3.95014291866849,
133.737671997999));
#117826=CARTESIAN_POINT('Ctrl Pts',(-173.170958631576,-3.86545207599381,
133.845324824967));
#117827=CARTESIAN_POINT('Ctrl Pts',(-173.178715672461,-3.78084534945801,
133.95287072963));
#117828=CARTESIAN_POINT('Ctrl Pts',(-173.186472713346,-3.69165851564237,
134.056995434827));
#117829=CARTESIAN_POINT('Ctrl Pts',(-173.194229754231,-3.59820208083672,
134.157288419944));
#117830=CARTESIAN_POINT('Ctrl Pts',(-173.201980945471,-3.50481612225568,
134.257505773342));
#117831=CARTESIAN_POINT('Ctrl Pts',(-173.209732136711,-3.40716723683549,
134.353896873221));
#117832=CARTESIAN_POINT('Ctrl Pts',(-173.217483327951,-3.30560620411024,
134.446084204804));
#117833=CARTESIAN_POINT('Ctrl Pts',(-173.225231224729,-3.204088337533,134.538232354313));
#117834=CARTESIAN_POINT('Ctrl Pts',(-173.232979121506,-3.09866191965195,
134.626180026942));
#117835=CARTESIAN_POINT('Ctrl Pts',(-173.240727018283,-2.98971442864739,
134.709586692666));
#117836=CARTESIAN_POINT('Ctrl Pts',(-173.248473294367,-2.88078972710931,
134.792975911513));
#117837=CARTESIAN_POINT('Ctrl Pts',(-173.256219570451,-2.76834572769189,
134.87182577531));
#117838=CARTESIAN_POINT('Ctrl Pts',(-173.263965846535,-2.65280250135353,
134.945836435594));
#117839=CARTESIAN_POINT('Ctrl Pts',(-173.2717121798,-2.53725842210117,135.019847642209));
#117840=CARTESIAN_POINT('Ctrl Pts',(-173.279458513066,-2.41861539949418,
135.089019363152));
#117841=CARTESIAN_POINT('Ctrl Pts',(-173.287204846331,-2.29732161350698,
135.153095659692));
#117842=CARTESIAN_POINT('Ctrl Pts',(-173.294952914334,-2.17600066461723,
135.217186305674));
#117843=CARTESIAN_POINT('Ctrl Pts',(-173.302700982337,-2.05202811673876,
135.276179074041));
#117844=CARTESIAN_POINT('Ctrl Pts',(-173.31044905034,-1.92587545040774,
135.32986465712));
#117845=CARTESIAN_POINT('Ctrl Pts',(-173.318205353082,-1.79958870752221,
135.383607297875));
#117846=CARTESIAN_POINT('Ctrl Pts',(-173.325961655824,-1.67111757793391,
135.432031332421));
#117847=CARTESIAN_POINT('Ctrl Pts',(-173.333717958566,-1.54095268639101,
135.47497598182));
#117848=CARTESIAN_POINT('Ctrl Pts',(-173.34147840108,-1.41071832192595,
135.517943552072));
#117849=CARTESIAN_POINT('Ctrl Pts',(-173.349238843594,-1.27878877008387,
135.555425803042));
#117850=CARTESIAN_POINT('Ctrl Pts',(-173.356999286108,-1.1456674416307,
135.587312548716));
#117851=CARTESIAN_POINT('Ctrl Pts',(-173.364772186374,-1.01233241500313,
135.619250481824));
#117852=CARTESIAN_POINT('Ctrl Pts',(-173.372545086639,-0.877802172599358,
135.645574884811));
#117853=CARTESIAN_POINT('Ctrl Pts',(-173.380317986905,-0.742588777640731,
135.666227025626));
#117854=CARTESIAN_POINT('Ctrl Pts',(-173.387808322667,-0.61229073017047,
135.686128409103));
#117855=CARTESIAN_POINT('Ctrl Pts',(-173.395298658429,-0.481358642569659,
135.700762738324));
#117856=CARTESIAN_POINT('Ctrl Pts',(-173.402788994191,-0.350251095779065,
135.710123273097));
#117857=CARTESIAN_POINT('Ctrl Pts',(-173.41056332831,-0.214172566503198,
135.719838715392));
#117858=CARTESIAN_POINT('Ctrl Pts',(-173.418337662429,-0.0774739544430357,
135.723903332622));
#117859=CARTESIAN_POINT('Ctrl Pts',(-173.426111996548,0.0593359564305044,
135.722252676851));
#117860=CARTESIAN_POINT('Ctrl Pts',(-173.433876749495,0.195977261315946,
135.720604055365));
#117861=CARTESIAN_POINT('Ctrl Pts',(-173.441641502442,0.332729204911828,
135.713254180141));
#117862=CARTESIAN_POINT('Ctrl Pts',(-173.449406255389,0.469078046280734,
135.700190358172));
#117863=CARTESIAN_POINT('Ctrl Pts',(-173.457163296274,0.60529146405821,
135.687139511375));
#117864=CARTESIAN_POINT('Ctrl Pts',(-173.464920337159,0.741102189692165,
135.668386048729));
#117865=CARTESIAN_POINT('Ctrl Pts',(-173.472677378044,0.87599700432949,
135.643969311552));
#117866=CARTESIAN_POINT('Ctrl Pts',(-173.480428569285,1.01079009373758,
135.619570987226));
#117867=CARTESIAN_POINT('Ctrl Pts',(-173.488179760525,1.14466826377962,
135.58951795833));
#117868=CARTESIAN_POINT('Ctrl Pts',(-173.495930951765,1.27712429567584,
135.553901289662));
#117869=CARTESIAN_POINT('Ctrl Pts',(-173.503678848542,1.4095240302253,135.518299759028));
#117870=CARTESIAN_POINT('Ctrl Pts',(-173.511426745319,1.54050245206364,
135.477139393131));
#117871=CARTESIAN_POINT('Ctrl Pts',(-173.519174642096,1.66956362221481,
135.43056212354));
#117872=CARTESIAN_POINT('Ctrl Pts',(-173.52692091818,1.79859779555143,135.38399459691));
#117873=CARTESIAN_POINT('Ctrl Pts',(-173.534667194264,1.92571514739029,
135.332012553018));
#117874=CARTESIAN_POINT('Ctrl Pts',(-173.542413470348,2.05043634811453,
135.27480733404));
#117875=CARTESIAN_POINT('Ctrl Pts',(-173.550159803614,2.17515846950252,
135.217601692786));
#117876=CARTESIAN_POINT('Ctrl Pts',(-173.557906136879,2.29748404911297,
135.155172962504));
#117877=CARTESIAN_POINT('Ctrl Pts',(-173.565652470144,2.41695550621841,
135.087759868565));
#117878=CARTESIAN_POINT('Ctrl Pts',(-173.573400538147,2.53645371812814,
135.020331677931));
#117879=CARTESIAN_POINT('Ctrl Pts',(-173.58114860615,2.65309619524257,134.947917094597));
#117880=CARTESIAN_POINT('Ctrl Pts',(-173.588896674153,2.7664519943435,134.870799652581));
#117881=CARTESIAN_POINT('Ctrl Pts',(-173.596652976895,2.87992826933682,
134.79360024923));
#117882=CARTESIAN_POINT('Ctrl Pts',(-173.604409279637,2.99011056466431,
134.71168822291));
#117883=CARTESIAN_POINT('Ctrl Pts',(-173.612165582379,3.09659841779299,
134.625389445175));
#117884=CARTESIAN_POINT('Ctrl Pts',(-173.619926024893,3.20314310669517,
134.539044607184));
#117885=CARTESIAN_POINT('Ctrl Pts',(-173.627686467407,3.30598913131837,
134.448308610985));
#117886=CARTESIAN_POINT('Ctrl Pts',(-173.635446909922,3.40477168323083,
134.353545432079));
#117887=CARTESIAN_POINT('Ctrl Pts',(-173.643219810187,3.50371280966513,
134.258630130905));
#117888=CARTESIAN_POINT('Ctrl Pts',(-173.650992710452,3.59857715754723,
134.159675010701));
#117889=CARTESIAN_POINT('Ctrl Pts',(-173.658765610718,3.68903853125977,
134.057079138647));
#117890=CARTESIAN_POINT('Ctrl Pts',(-173.66625594648,3.77621140617964,133.958212884965));
#117891=CARTESIAN_POINT('Ctrl Pts',(-173.673746282242,3.8592956733611,133.855966223884));
#117892=CARTESIAN_POINT('Ctrl Pts',(-173.681236618004,3.9380377878904,133.7507213293));
#117893=CARTESIAN_POINT('Ctrl Pts',(-173.689010952123,4.01976543362488,
133.641486042549));
#117894=CARTESIAN_POINT('Ctrl Pts',(-173.696785286242,4.09707405008418,
133.528674653613));
#117895=CARTESIAN_POINT('Ctrl Pts',(-173.704559620361,4.16963440522962,
133.412680381173));
#117896=CARTESIAN_POINT('Ctrl Pts',(-173.712324373308,4.24210533622226,
133.296829061308));
#117897=CARTESIAN_POINT('Ctrl Pts',(-173.720089126255,4.30983944390217,
133.177802991055));
#117898=CARTESIAN_POINT('Ctrl Pts',(-173.727853879203,4.3725483597584,133.056027534335));
#117899=CARTESIAN_POINT('Ctrl Pts',(-173.735610920088,4.43519499223536,
132.934373026716));
#117900=CARTESIAN_POINT('Ctrl Pts',(-173.743367960973,4.49282618755274,
132.809974912242));
#117901=CARTESIAN_POINT('Ctrl Pts',(-173.751125001858,4.54519763734802,
132.683286241412));
#117902=CARTESIAN_POINT('Ctrl Pts',(-173.758876193098,4.5975295934257,132.556693107494));
#117903=CARTESIAN_POINT('Ctrl Pts',(-173.766627384338,4.64460955013321,
132.427813215206));
#117904=CARTESIAN_POINT('Ctrl Pts',(-173.774378575578,4.68623995872471,
132.297122524821));
#117905=CARTESIAN_POINT('Ctrl Pts',(-173.782126472355,4.72785267328208,
132.166487381466));
#117906=CARTESIAN_POINT('Ctrl Pts',(-173.789874369132,4.76402032805993,
132.034043342506));
#117907=CARTESIAN_POINT('Ctrl Pts',(-173.797622265909,4.79459426697746,
131.900284372928));
#117908=CARTESIAN_POINT('Ctrl Pts',(-173.805368541993,4.82516181048598,
131.766553382844));
#117909=CARTESIAN_POINT('Ctrl Pts',(-173.813114818077,4.85013787843416,
131.631508390135));
#117910=CARTESIAN_POINT('Ctrl Pts',(-173.820861094162,4.86942436304803,
131.495656093505));
#117911=CARTESIAN_POINT('Ctrl Pts',(-173.828607427427,4.88871099003036,
131.359802794044));
#117912=CARTESIAN_POINT('Ctrl Pts',(-173.836353760692,4.90230789491901,
131.223142565854));
#117913=CARTESIAN_POINT('Ctrl Pts',(-173.844100093958,4.91016859056788,
131.086189421453));
#117914=CARTESIAN_POINT('Ctrl Pts',(-173.851848161961,4.91803104656503,
130.949205607346));
#117915=CARTESIAN_POINT('Ctrl Pts',(-173.859596229964,4.92015471474935,
130.811929136746));
#117916=CARTESIAN_POINT('Ctrl Pts',(-173.867344297966,4.9165452049854,130.674875831452));
#117917=CARTESIAN_POINT('Ctrl Pts',(-173.875100600708,4.91293185899151,
130.537676864273));
#117918=CARTESIAN_POINT('Ctrl Pts',(-173.88285690345,4.90357317335622,130.400701927651));
#117919=CARTESIAN_POINT('Ctrl Pts',(-173.890613206192,4.88852685326589,
130.264464083591));
#117920=CARTESIAN_POINT('Ctrl Pts',(-173.898373648706,4.87347250250149,
130.128153525291));
#117921=CARTESIAN_POINT('Ctrl Pts',(-173.90613409122,4.8527245275847,129.992581229729));
#117922=CARTESIAN_POINT('Ctrl Pts',(-173.913894533735,4.82639196354484,
129.85825085822));
#117923=CARTESIAN_POINT('Ctrl Pts',(-173.921667434,4.80001712813549,129.723704847673));
#117924=CARTESIAN_POINT('Ctrl Pts',(-173.929440334266,4.76803988017331,
129.590405125518));
#117925=CARTESIAN_POINT('Ctrl Pts',(-173.937213234531,4.73061964948173,
129.458841834926));
#117926=CARTESIAN_POINT('Ctrl Pts',(-173.944703570293,4.69455973843176,
129.332061201335));
#117927=CARTESIAN_POINT('Ctrl Pts',(-173.952193906055,4.65344580254648,
129.20689323646));
#117928=CARTESIAN_POINT('Ctrl Pts',(-173.959684241817,4.60746232832853,
129.083757829142));
#117929=CARTESIAN_POINT('Ctrl Pts',(-173.967458575936,4.55973537670931,
128.955953705429));
#117930=CARTESIAN_POINT('Ctrl Pts',(-173.975232910055,4.50661115577776,
128.829934465618));
#117931=CARTESIAN_POINT('Ctrl Pts',(-173.983007244174,4.44824253358713,
128.706189646247));
#117932=CARTESIAN_POINT('Ctrl Pts',(-173.990771997121,4.38994584550663,
128.582597331306));
#117933=CARTESIAN_POINT('Ctrl Pts',(-173.998536750068,4.32641778130796,
128.46127420984));
#117934=CARTESIAN_POINT('Ctrl Pts',(-174.006301503015,4.25786034148059,
128.342692814034));
#117935=CARTESIAN_POINT('Ctrl Pts',(-174.0140585439,4.18937099386895,128.224229194942));
#117936=CARTESIAN_POINT('Ctrl Pts',(-174.021815584785,4.11586240581359,
128.108502218655));
#117937=CARTESIAN_POINT('Ctrl Pts',(-174.02957262567,4.03758368689263,127.995962313579));
#117938=CARTESIAN_POINT('Ctrl Pts',(-174.03732381691,3.95936399856264,127.883507275721));
#117939=CARTESIAN_POINT('Ctrl Pts',(-174.04507500815,3.87638156170514,127.774234844921));
#117940=CARTESIAN_POINT('Ctrl Pts',(-174.05282619939,3.78893003525486,127.668568492689));
#117941=CARTESIAN_POINT('Ctrl Pts',(-174.060574096167,3.70151567803604,
127.562947051474));
#117942=CARTESIAN_POINT('Ctrl Pts',(-174.068321992945,3.60963625790074,
127.460928941005));
#117943=CARTESIAN_POINT('Ctrl Pts',(-174.076069889722,3.51362700933943,
127.362906229994));
#117944=CARTESIAN_POINT('Ctrl Pts',(-174.083816165806,3.41763784384346,
127.264904023221));
#117945=CARTESIAN_POINT('Ctrl Pts',(-174.09156244189,3.31752084160577,127.170895832681));
#117946=CARTESIAN_POINT('Ctrl Pts',(-174.099308717974,3.21364927294672,
127.081238082249));
#117947=CARTESIAN_POINT('Ctrl Pts',(-174.107055051239,3.1097769375312,126.991579669983));
#117948=CARTESIAN_POINT('Ctrl Pts',(-174.114801384505,3.00215027635157,
126.906272017367));
#117949=CARTESIAN_POINT('Ctrl Pts',(-174.12254771777,2.89117661525938,126.825632071676));
#117950=CARTESIAN_POINT('Ctrl Pts',(-174.130295785773,2.78017810238507,
126.744974067229));
#117951=CARTESIAN_POINT('Ctrl Pts',(-174.138043853776,2.66583141432503,
126.668986079516));
#117952=CARTESIAN_POINT('Ctrl Pts',(-174.145791921779,2.54857355883509,
126.597942203082));
#117953=CARTESIAN_POINT('Ctrl Pts',(-174.153548224521,2.4311910803011,126.526822820371));
#117954=CARTESIAN_POINT('Ctrl Pts',(-174.161304527262,2.31089158860516,
126.460658248605));
#117955=CARTESIAN_POINT('Ctrl Pts',(-174.169060830004,2.18813792840575,
126.399677261322));
#117956=CARTESIAN_POINT('Ctrl Pts',(-174.176821272518,2.06531875088184,
126.33866372665));
#117957=CARTESIAN_POINT('Ctrl Pts',(-174.184581715032,1.9400431517792,126.282839448272));
#117958=CARTESIAN_POINT('Ctrl Pts',(-174.192342157547,1.81279381172291,
126.232384933173));
#117959=CARTESIAN_POINT('Ctrl Pts',(-174.200115057812,1.6853401997293,126.181849424008));
#117960=CARTESIAN_POINT('Ctrl Pts',(-174.207887958077,1.55590688462521,
126.136701032509));
#117961=CARTESIAN_POINT('Ctrl Pts',(-174.215660858343,1.42499241345572,
126.097070560209));
#117962=CARTESIAN_POINT('Ctrl Pts',(-174.223151194105,1.29883701306407,
126.058880755399));
#117963=CARTESIAN_POINT('Ctrl Pts',(-174.230641529867,1.17130657266092,
126.025814731653));
#117964=CARTESIAN_POINT('Ctrl Pts',(-174.238131865629,1.04285407608206,
125.997944235427));
#117965=CARTESIAN_POINT('Ctrl Pts',(-174.245906199748,0.909531264055936,
125.969017020865));
#117966=CARTESIAN_POINT('Ctrl Pts',(-174.253680533868,0.774792769507084,
125.945595455182));
#117967=CARTESIAN_POINT('Ctrl Pts',(-174.261454867987,0.639133082307737,
125.927815532611));
#117968=CARTESIAN_POINT('Ctrl Pts',(-174.269219620934,0.50364058354861,
125.910057522205));
#117969=CARTESIAN_POINT('Ctrl Pts',(-174.276984373881,0.367229534951522,
125.89792737119));
#117970=CARTESIAN_POINT('Ctrl Pts',(-174.284749126828,0.230406677424843,
125.891510546019));
#117971=CARTESIAN_POINT('Ctrl Pts',(-174.292506167713,0.093719714288753,
125.88510009413));
#117972=CARTESIAN_POINT('Ctrl Pts',(-174.300263208598,-0.0433778558109409,
125.884391693661));
#117973=CARTESIAN_POINT('Ctrl Pts',(-174.308020249483,-0.180372424888108,
125.889419229224));
#117974=CARTESIAN_POINT('Ctrl Pts',(-174.315771440723,-0.317263685294886,
125.894442973483));
#117975=CARTESIAN_POINT('Ctrl Pts',(-174.323522631963,-0.454051710162949,
125.905194029822));
#117976=CARTESIAN_POINT('Ctrl Pts',(-174.331273823203,-0.59022149109199,
125.921654231354));
#117977=CARTESIAN_POINT('Ctrl Pts',(-174.339021719981,-0.726333396231504,
125.938107436862));
#117978=CARTESIAN_POINT('Ctrl Pts',(-174.346769616758,-0.861827192734683,
125.960264914543));
#117979=CARTESIAN_POINT('Ctrl Pts',(-174.354517513535,-0.996191819659431,
125.988056544841));
#117980=CARTESIAN_POINT('Ctrl Pts',(-174.362263789619,-1.13052834040079,
126.01584236173));
#117981=CARTESIAN_POINT('Ctrl Pts',(-174.370010065703,-1.26373577875568,
126.049259907909));
#117982=CARTESIAN_POINT('Ctrl Pts',(-174.377756341787,-1.39531250349853,
126.088187796297));
#117983=CARTESIAN_POINT('Ctrl Pts',(-174.385502675053,-1.52689019951104,
126.127115972041));
#117984=CARTESIAN_POINT('Ctrl Pts',(-174.393249008318,-1.65683678298991,
126.171554460243));
#117985=CARTESIAN_POINT('Ctrl Pts',(-174.400995341583,-1.78466542764453,
126.221331883871));
#117986=CARTESIAN_POINT('Ctrl Pts',(-174.408743409586,-1.91252269863765,
126.271120454809));
#117987=CARTESIAN_POINT('Ctrl Pts',(-174.416491477589,-2.03826072276117,
126.326250198472));
#117988=CARTESIAN_POINT('Ctrl Pts',(-174.424239545592,-2.16141268314659,
126.386501602655));
#117989=CARTESIAN_POINT('Ctrl Pts',(-174.431995848334,-2.2846955309012,
126.446817042747));
#117990=CARTESIAN_POINT('Ctrl Pts',(-174.439752151076,-2.40538647274651,
126.512264844971));
#117991=CARTESIAN_POINT('Ctrl Pts',(-174.447508453818,-2.52304285618185,
126.582579262691));
#117992=CARTESIAN_POINT('Ctrl Pts',(-174.455268896332,-2.6407620363716,
126.652931209333));
#117993=CARTESIAN_POINT('Ctrl Pts',(-174.463029338846,-2.75544310413847,
126.728154732801));
#117994=CARTESIAN_POINT('Ctrl Pts',(-174.47078978136,-2.86667329317578,
126.807941308648));
#117995=CARTESIAN_POINT('Ctrl Pts',(-174.478562681626,-2.97808203878708,
126.88785596499));
#117996=CARTESIAN_POINT('Ctrl Pts',(-174.486335581891,-3.08602852762187,
126.972348070314));
#117997=CARTESIAN_POINT('Ctrl Pts',(-174.494108482157,-3.19013323579247,
127.061068884293));
#117998=CARTESIAN_POINT('Ctrl Pts',(-174.501598817919,-3.29045347559684,
127.146564473209));
#117999=CARTESIAN_POINT('Ctrl Pts',(-174.509089153681,-3.38720617599272,
127.235986451051));
#118000=CARTESIAN_POINT('Ctrl Pts',(-174.516579489443,-3.4800861258268,
127.328992490399));
#118001=CARTESIAN_POINT('Ctrl Pts',(-174.5242450903,-3.57513935784502,127.424174762279));
#118002=CARTESIAN_POINT('Ctrl Pts',(-174.531910691157,-3.6664555477646,
127.523430863656));
#118003=CARTESIAN_POINT('Ctrl Pts',(-174.539576292015,-3.75365778843685,
127.626431060479));
#118004=CARTESIAN_POINT('Ctrl Pts',(-174.547232920712,-3.84075796372669,
127.729310701288));
#118005=CARTESIAN_POINT('Ctrl Pts',(-174.554889549409,-3.92375350504564,
127.835925421485));
#118006=CARTESIAN_POINT('Ctrl Pts',(-174.562546178106,-4.00230282902814,
127.945907342235));
#118007=CARTESIAN_POINT('Ctrl Pts',(-174.570195614279,-4.08077836493951,
128.055785947597));
#118008=CARTESIAN_POINT('Ctrl Pts',(-174.577845050453,-4.15481575665894,
128.169025138031));
#118009=CARTESIAN_POINT('Ctrl Pts',(-174.585494486626,-4.22411273459277,
128.285222934161));
#118010=CARTESIAN_POINT('Ctrl Pts',(-174.593138183411,-4.29335771885319,
128.401333546831));
#118011=CARTESIAN_POINT('Ctrl Pts',(-174.600781880196,-4.35786916126707,
128.520398003458));
#118012=CARTESIAN_POINT('Ctrl Pts',(-174.608425576981,-4.41738765085419,
128.641984747237));
#118013=CARTESIAN_POINT('Ctrl Pts',(-174.616065941024,-4.4768801896829,
128.763518477772));
#118014=CARTESIAN_POINT('Ctrl Pts',(-174.623706305068,-4.53138392989183,
128.887571946581));
#118015=CARTESIAN_POINT('Ctrl Pts',(-174.631346669112,-4.58068524476776,
129.01368874621));
#118016=CARTESIAN_POINT('Ctrl Pts',(-174.63898633773,-4.62998207223927,
129.13979406669));
#118017=CARTESIAN_POINT('Ctrl Pts',(-174.646626006347,-4.67407726516443,
129.267961971298));
#118018=CARTESIAN_POINT('Ctrl Pts',(-174.654265674965,-4.71280537081142,
129.397716170895));
#118019=CARTESIAN_POINT('Ctrl Pts',(-174.657872255346,-4.73108836618704,
129.458971308257));
#118020=CARTESIAN_POINT('Ctrl Pts',(-174.661478835727,-4.74817593400007,
129.520579721381));
#118021=CARTESIAN_POINT('Ctrl Pts',(-174.665085416107,-4.76405452823406,
129.582490119308));
#118022=CARTESIAN_POINT('Ctrl Pts',(-172.915418914505,-4.76405452823406,
129.582490119308));
#118023=CARTESIAN_POINT('Ctrl Pts',(-172.923551617668,-4.7997385967966,
129.721621761052));
#118024=CARTESIAN_POINT('Ctrl Pts',(-172.93168432083,-4.82936058183097,
129.86246191961));
#118025=CARTESIAN_POINT('Ctrl Pts',(-172.939817023993,-4.85276781019348,
130.004468348038));
#118026=CARTESIAN_POINT('Ctrl Pts',(-172.947934708106,-4.87613181131613,
130.146212526454));
#118027=CARTESIAN_POINT('Ctrl Pts',(-172.95605239222,-4.89330388817451,
130.289118353323));
#118028=CARTESIAN_POINT('Ctrl Pts',(-172.964170076333,-4.90418197276099,
130.432631898543));
#118029=CARTESIAN_POINT('Ctrl Pts',(-172.971160238893,-4.9135491245905,
130.556211850233));
#118030=CARTESIAN_POINT('Ctrl Pts',(-172.978150401452,-4.91825005692981,
130.680242069289));
#118031=CARTESIAN_POINT('Ctrl Pts',(-172.985140564012,-4.91824999999948,
130.804362873413));
#118032=CARTESIAN_POINT('',(-172.63985943603,-4.91824811045768,130.800049413617));
#118033=CARTESIAN_POINT('Ctrl Pts',(-172.569844098739,-4.76405452823414,
129.582490119309));
#118034=CARTESIAN_POINT('Ctrl Pts',(-172.575574438797,-4.78909101747142,
129.680107010863));
#118035=CARTESIAN_POINT('Ctrl Pts',(-172.581304778855,-4.81110043102754,
129.778394074122));
#118036=CARTESIAN_POINT('Ctrl Pts',(-172.587035118913,-4.83005787533671,
129.877147598137));
#118037=CARTESIAN_POINT('Ctrl Pts',(-172.598508350551,-4.86801428763181,
130.074870952193));
#118038=CARTESIAN_POINT('Ctrl Pts',(-172.609981582189,-4.89383874355218,
130.27499214093));
#118039=CARTESIAN_POINT('Ctrl Pts',(-172.621454813827,-4.90729647054678,
130.476299018687));
#118040=CARTESIAN_POINT('Ctrl Pts',(-172.627589687883,-4.91449247798305,
130.583940211727));
#118041=CARTESIAN_POINT('Ctrl Pts',(-172.633724561938,-4.91815332714998,
130.69192004631));
#118042=CARTESIAN_POINT('Ctrl Pts',(-172.639859435994,-4.91824811045712,
130.800049412982));
#118043=CARTESIAN_POINT('Ctrl Pts',(-172.63985943603,-4.91824811045768,
130.800049413617));
#118044=CARTESIAN_POINT('Ctrl Pts',(-172.647506292934,-4.91836625375992,
130.934828023003));
#118045=CARTESIAN_POINT('Ctrl Pts',(-172.655153149837,-4.91294006961445,
131.069793692025));
#118046=CARTESIAN_POINT('Ctrl Pts',(-172.66280000674,-4.90195016924981,
131.204445109507));
#118047=CARTESIAN_POINT('Ctrl Pts',(-172.670440188586,-4.8909698621364,
131.338978987718));
#118048=CARTESIAN_POINT('Ctrl Pts',(-172.678080370431,-4.87443553171941,
131.473198760116));
#118049=CARTESIAN_POINT('Ctrl Pts',(-172.685720552277,-4.85237984714444,
131.606603025773));
#118050=CARTESIAN_POINT('Ctrl Pts',(-172.693356430854,-4.83033658524968,
131.739932152592));
#118051=CARTESIAN_POINT('Ctrl Pts',(-172.700992309431,-4.80277821907229,
131.872446289167));
#118052=CARTESIAN_POINT('Ctrl Pts',(-172.708628188008,-4.76978921957538,
132.00364951659));
#118053=CARTESIAN_POINT('Ctrl Pts',(-172.716261878284,-4.73680967410985,
132.134815143618));
#118054=CARTESIAN_POINT('Ctrl Pts',(-172.723895568561,-4.69840268736267,
132.264670217367));
#118055=CARTESIAN_POINT('Ctrl Pts',(-172.731529258838,-4.65470366440352,
132.392729862763));
#118056=CARTESIAN_POINT('Ctrl Pts',(-172.739162527427,-4.61100705539324,
132.520782434102));
#118057=CARTESIAN_POINT('Ctrl Pts',(-172.746795796016,-4.56201912185757,
132.64703939245));
#118058=CARTESIAN_POINT('Ctrl Pts',(-172.754429064605,-4.50792470471584,
132.771032404904));
#118059=CARTESIAN_POINT('Ctrl Pts',(-172.762063677571,-4.45382076042516,
132.8950472551));
#118060=CARTESIAN_POINT('Ctrl Pts',(-172.769698290537,-4.39460870601867,
133.016796996958));
#118061=CARTESIAN_POINT('Ctrl Pts',(-172.777332903503,-4.33052071184678,
133.135835135284));
#118062=CARTESIAN_POINT('Ctrl Pts',(-172.784975198528,-4.26636823139755,
133.254993051525));
#118063=CARTESIAN_POINT('Ctrl Pts',(-172.792617493553,-4.19733020493732,
133.3714335597));
#118064=CARTESIAN_POINT('Ctrl Pts',(-172.800259788578,-4.1236839549241,
133.484736281984));
#118065=CARTESIAN_POINT('Ctrl Pts',(-172.807906040652,-4.04999957215319,
133.598097670461));
#118066=CARTESIAN_POINT('Ctrl Pts',(-172.815552292726,-3.9717024487071,
133.708317709803));
#118067=CARTESIAN_POINT('Ctrl Pts',(-172.8231985448,-3.88911129452465,133.815007790733));
#118068=CARTESIAN_POINT('Ctrl Pts',(-172.830856647217,-3.80639213860581,
133.921863222491));
#118069=CARTESIAN_POINT('Ctrl Pts',(-172.838514749634,-3.71936591941276,
134.025177460536));
#118070=CARTESIAN_POINT('Ctrl Pts',(-172.846172852051,-3.62838982436676,
134.124597106874));
#118071=CARTESIAN_POINT('Ctrl Pts',(-172.852609482276,-3.5519244741784,
134.208159256568));
#118072=CARTESIAN_POINT('Ctrl Pts',(-172.859046112501,-3.47266951968559,
134.288970687063));
#118073=CARTESIAN_POINT('Ctrl Pts',(-172.865482742726,-3.39085483562696,
134.366843816994));
#118074=CARTESIAN_POINT('Ctrl Pts',(-172.873257076845,-3.29203687226701,
134.46090106587));
#118075=CARTESIAN_POINT('Ctrl Pts',(-172.881031410964,-3.18914591107,134.550992584651));
#118076=CARTESIAN_POINT('Ctrl Pts',(-172.888805745083,-3.08253353326629,
134.63674500314));
#118077=CARTESIAN_POINT('Ctrl Pts',(-172.89657049803,-2.97605254569001,
134.722391739436));
#118078=CARTESIAN_POINT('Ctrl Pts',(-172.904335250977,-2.86585956862587,
134.803709772791));
#118079=CARTESIAN_POINT('Ctrl Pts',(-172.912100003924,-2.75234292988948,
134.880362513884));
#118080=CARTESIAN_POINT('Ctrl Pts',(-172.919857044809,-2.63893903747898,
134.956939122393));
#118081=CARTESIAN_POINT('Ctrl Pts',(-172.927614085694,-2.52221837466528,
135.028859442406));
#118082=CARTESIAN_POINT('Ctrl Pts',(-172.935371126579,-2.40260196594303,
135.09582736633));
#118083=CARTESIAN_POINT('Ctrl Pts',(-172.943122317819,-2.28307576088459,
135.162744789222));
#118084=CARTESIAN_POINT('Ctrl Pts',(-172.950873509059,-2.16065849620911,
135.224717059385));
#118085=CARTESIAN_POINT('Ctrl Pts',(-172.958624700299,-2.03579946855144,
135.281491795714));
#118086=CARTESIAN_POINT('Ctrl Pts',(-172.966372597076,-1.91099350931176,
135.338242401265));
#118087=CARTESIAN_POINT('Ctrl Pts',(-172.974120493853,-1.78374820637798,
135.389799705203));
#118088=CARTESIAN_POINT('Ctrl Pts',(-172.981868390631,-1.65453650972927,
135.435957750356));
#118089=CARTESIAN_POINT('Ctrl Pts',(-172.989614666715,-1.52535184138201,
135.482106140242));
#118090=CARTESIAN_POINT('Ctrl Pts',(-172.997360942799,-1.39420196541725,
135.52285738636));
#118091=CARTESIAN_POINT('Ctrl Pts',(-173.005107218883,-1.26157844659884,
135.558054222078));
#118092=CARTESIAN_POINT('Ctrl Pts',(-173.012853552148,-1.12895394878356,
135.593251317611));
#118093=CARTESIAN_POINT('Ctrl Pts',(-173.020599885413,-0.994856164292337,
135.622893820644));
#118094=CARTESIAN_POINT('Ctrl Pts',(-173.028346218679,-0.859790017360974,
135.646874860038));
#118095=CARTESIAN_POINT('Ctrl Pts',(-173.036094286682,-0.724693623302305,
135.67086126982));
#118096=CARTESIAN_POINT('Ctrl Pts',(-173.043842354685,-0.588628820152166,
135.689183624763));
#118097=CARTESIAN_POINT('Ctrl Pts',(-173.051590422688,-0.452108481873687,
135.701786572404));
#118098=CARTESIAN_POINT('Ctrl Pts',(-173.05934672543,-0.315443048155258,
135.714402914607));
#118099=CARTESIAN_POINT('Ctrl Pts',(-173.067103028172,-0.178321502101017,
135.721287670746));
#118100=CARTESIAN_POINT('Ctrl Pts',(-173.074859330913,-0.04126013011152,
135.722437545));
#118101=CARTESIAN_POINT('Ctrl Pts',(-173.082619773428,0.0958743956590458,
135.723588032978));
#118102=CARTESIAN_POINT('Ctrl Pts',(-173.090380215942,0.232948292814648,
135.71899755309));
#118103=CARTESIAN_POINT('Ctrl Pts',(-173.098140658456,0.36944854734374,
135.70871489039));
#118104=CARTESIAN_POINT('Ctrl Pts',(-173.105913558721,0.506167924199327,
135.698415721047));
#118105=CARTESIAN_POINT('Ctrl Pts',(-173.113686458987,0.642311429739336,
135.682406154748));
#118106=CARTESIAN_POINT('Ctrl Pts',(-173.121459359252,0.77737352141237,
135.660786615222));
#118107=CARTESIAN_POINT('Ctrl Pts',(-173.128949695014,0.907525765851477,
135.639953000414));
#118108=CARTESIAN_POINT('Ctrl Pts',(-173.136440030776,1.03667355368672,
135.6139102653));
#118109=CARTESIAN_POINT('Ctrl Pts',(-173.143930366538,1.16437814554918,
135.58279201256));
#118110=CARTESIAN_POINT('Ctrl Pts',(-173.151704700657,1.29692469582728,
135.550493901809));
#118111=CARTESIAN_POINT('Ctrl Pts',(-173.159479034776,1.42833631988041,
135.51262548864));
#118112=CARTESIAN_POINT('Ctrl Pts',(-173.167253368895,1.55810885254449,
135.469280752587));
#118113=CARTESIAN_POINT('Ctrl Pts',(-173.175018121842,1.68772145216052,
135.425989435047));
#118114=CARTESIAN_POINT('Ctrl Pts',(-173.182782874789,1.81569861238495,
135.377235345948));
#118115=CARTESIAN_POINT('Ctrl Pts',(-173.190547627736,1.94154725041979,
135.323163261728));
#118116=CARTESIAN_POINT('Ctrl Pts',(-173.198304668621,2.06727089381284,
135.269144882665));
#118117=CARTESIAN_POINT('Ctrl Pts',(-173.206061709506,2.19086986523984,
135.209819173058));
#118118=CARTESIAN_POINT('Ctrl Pts',(-173.213818750391,2.31186746697507,
135.145380299351));
#118119=CARTESIAN_POINT('Ctrl Pts',(-173.221569941631,2.43277382347777,
135.0809900195));
#118120=CARTESIAN_POINT('Ctrl Pts',(-173.229321132872,2.55108237127638,
135.011494433471));
#118121=CARTESIAN_POINT('Ctrl Pts',(-173.237072324112,2.66633791919391,
134.937135129098));
#118122=CARTESIAN_POINT('Ctrl Pts',(-173.244820220889,2.78154448042919,
134.862807429412));
#118123=CARTESIAN_POINT('Ctrl Pts',(-173.252568117666,2.89370029478576,
134.783620334415));
#118124=CARTESIAN_POINT('Ctrl Pts',(-173.260316014443,3.00237644364744,
134.699860425438));
#118125=CARTESIAN_POINT('Ctrl Pts',(-173.268062290527,3.11102985980157,
134.616118037228));
#118126=CARTESIAN_POINT('Ctrl Pts',(-173.275808566611,3.21620474876837,
134.527804976152));
#118127=CARTESIAN_POINT('Ctrl Pts',(-173.283554842695,3.31750309491557,
134.435249803113));
#118128=CARTESIAN_POINT('Ctrl Pts',(-173.291301175961,3.41880218882429,
134.342693946853));
#118129=CARTESIAN_POINT('Ctrl Pts',(-173.299047509226,3.51622439418338,
134.245896179862));
#118130=CARTESIAN_POINT('Ctrl Pts',(-173.306793842491,3.60940687339464,
134.145223542738));
#118131=CARTESIAN_POINT('Ctrl Pts',(-173.314541910494,3.70261022017591,
134.044528360676));
#118132=CARTESIAN_POINT('Ctrl Pts',(-173.322289978497,3.79157168597577,
133.939956868626));
#118133=CARTESIAN_POINT('Ctrl Pts',(-173.3300380465,3.87596748029428,133.831910642619));
#118134=CARTESIAN_POINT('Ctrl Pts',(-173.337794349242,3.96045297146721,
133.723749583799));
#118135=CARTESIAN_POINT('Ctrl Pts',(-173.345550651984,4.04036285681526,
133.612106722482));
#118136=CARTESIAN_POINT('Ctrl Pts',(-173.353306954726,4.11541529806242,
133.49741464357));
#118137=CARTESIAN_POINT('Ctrl Pts',(-173.36106739724,4.19050779705725,133.382661350041));
#118138=CARTESIAN_POINT('Ctrl Pts',(-173.368827839754,4.2607374859471,133.264855931722));
#118139=CARTESIAN_POINT('Ctrl Pts',(-173.376588282268,4.32586811237478,
133.144456371342));
#118140=CARTESIAN_POINT('Ctrl Pts',(-173.384361182534,4.39110329226603,
133.023863534898));
#118141=CARTESIAN_POINT('Ctrl Pts',(-173.392134082799,4.45122288095881,
132.900668586264));
#118142=CARTESIAN_POINT('Ctrl Pts',(-173.399906983064,4.50603810968254,
132.775351134182));
#118143=CARTESIAN_POINT('Ctrl Pts',(-173.407397318827,4.55886066677196,
132.654589287136));
#118144=CARTESIAN_POINT('Ctrl Pts',(-173.414887654589,4.60675771008897,
132.531856861114));
#118145=CARTESIAN_POINT('Ctrl Pts',(-173.422377990351,4.64960449400472,
132.407595195484));
#118146=CARTESIAN_POINT('Ctrl Pts',(-173.43015232447,4.69407582675482,132.278622111035));
#118147=CARTESIAN_POINT('Ctrl Pts',(-173.437926658589,4.7332472509744,132.147592987642));
#118148=CARTESIAN_POINT('Ctrl Pts',(-173.445700992708,4.76692532072162,
132.014982791972));
#118149=CARTESIAN_POINT('Ctrl Pts',(-173.453465745655,4.80056188525778,
131.882536026516));
#118150=CARTESIAN_POINT('Ctrl Pts',(-173.461230498602,4.82871847042807,
131.748512441074));
#118151=CARTESIAN_POINT('Ctrl Pts',(-173.46899525155,4.85125035745506,131.613405135372));
#118152=CARTESIAN_POINT('Ctrl Pts',(-173.476752292435,4.87375986549426,
131.47843202015));
#118153=CARTESIAN_POINT('Ctrl Pts',(-173.48450933332,4.89065572893891,131.342377709829));
#118154=CARTESIAN_POINT('Ctrl Pts',(-173.492266374205,4.90184363875416,
131.205748215413));
#118155=CARTESIAN_POINT('Ctrl Pts',(-173.500017565445,4.91302311167957,
131.069221754361));
#118156=CARTESIAN_POINT('Ctrl Pts',(-173.507768756685,4.91850316686881,
130.932121360653));
#118157=CARTESIAN_POINT('Ctrl Pts',(-173.515519947925,4.91824101705704,
130.794960583642));
#118158=CARTESIAN_POINT('Ctrl Pts',(-173.523267844702,4.91797897866593,
130.657858103621));
#118159=CARTESIAN_POINT('Ctrl Pts',(-173.531015741479,4.91197959016753,
130.520695681487));
#118160=CARTESIAN_POINT('Ctrl Pts',(-173.538763638256,4.90025211956312,
130.383989082829));
#118161=CARTESIAN_POINT('Ctrl Pts',(-173.54650991434,4.88852710209275,130.247311080245));
#118162=CARTESIAN_POINT('Ctrl Pts',(-173.554256190424,4.87107641917985,
130.111089100772));
#118163=CARTESIAN_POINT('Ctrl Pts',(-173.562002466509,4.84796136124566,
129.975835601426));
#118164=CARTESIAN_POINT('Ctrl Pts',(-173.569748799774,4.82484613268134,
129.840581103671));
#118165=CARTESIAN_POINT('Ctrl Pts',(-173.577495133039,4.79606651152239,
129.706295485686));
#118166=CARTESIAN_POINT('Ctrl Pts',(-173.585241466305,4.76173517683534,
129.573482407429));
#118167=CARTESIAN_POINT('Ctrl Pts',(-173.592989534308,4.72739615388388,
129.440639586605));
#118168=CARTESIAN_POINT('Ctrl Pts',(-173.60073760231,4.68750304127259,129.309270340154));
#118169=CARTESIAN_POINT('Ctrl Pts',(-173.608485670313,4.64221867961617,
129.179864143848));
#118170=CARTESIAN_POINT('Ctrl Pts',(-173.616241973055,4.59688618920134,
129.050320413097));
#118171=CARTESIAN_POINT('Ctrl Pts',(-173.623998275797,4.54615113302321,
128.922744269818));
#118172=CARTESIAN_POINT('Ctrl Pts',(-173.631754578539,4.49022511653739,
128.797606655239));
#118173=CARTESIAN_POINT('Ctrl Pts',(-173.639515021053,4.43426925065267,
128.672402250947));
#118174=CARTESIAN_POINT('Ctrl Pts',(-173.647275463567,4.37311707809791,
128.549639318517));
#118175=CARTESIAN_POINT('Ctrl Pts',(-173.655035906082,4.30702621254498,
128.429764174599));
#118176=CARTESIAN_POINT('Ctrl Pts',(-173.662808806347,4.24082925206739,
128.309696596459));
#118177=CARTESIAN_POINT('Ctrl Pts',(-173.670581706612,4.16967795890928,
128.192526404875));
#118178=CARTESIAN_POINT('Ctrl Pts',(-173.678354606878,4.09387380735918,
128.078671656602));
#118179=CARTESIAN_POINT('Ctrl Pts',(-173.68584494264,4.02082532765747,127.968955815213));
#118180=CARTESIAN_POINT('Ctrl Pts',(-173.693335278402,3.94345658354716,
127.862318801987));
#118181=CARTESIAN_POINT('Ctrl Pts',(-173.700825614164,3.86207145827823,
127.759104123664));
#118182=CARTESIAN_POINT('Ctrl Pts',(-173.708599948283,3.77760059124767,
127.65197602944));
#118183=CARTESIAN_POINT('Ctrl Pts',(-173.716374282402,3.68853519040565,
127.548195559094));
#118184=CARTESIAN_POINT('Ctrl Pts',(-173.724148616521,3.59517029640279,
127.448182195258));
#118185=CARTESIAN_POINT('Ctrl Pts',(-173.731913369468,3.50192046628777,
127.348292088956));
#118186=CARTESIAN_POINT('Ctrl Pts',(-173.739678122415,3.404381950158,127.252160134777));
#118187=CARTESIAN_POINT('Ctrl Pts',(-173.747442875362,3.30289138274313,
127.160174621174));
#118188=CARTESIAN_POINT('Ctrl Pts',(-173.755199916247,3.2015016171903,127.068280468879));
#118189=CARTESIAN_POINT('Ctrl Pts',(-173.762956957132,3.09616789955506,
126.980524822408));
#118190=CARTESIAN_POINT('Ctrl Pts',(-173.770713998017,2.98726497488921,
126.897260537929));
#118191=CARTESIAN_POINT('Ctrl Pts',(-173.778465189257,2.87844417476644,
126.814059043695));
#118192=CARTESIAN_POINT('Ctrl Pts',(-173.786216380497,2.76605983434295,
126.735342406399));
#118193=CARTESIAN_POINT('Ctrl Pts',(-173.793967571738,2.6505208896722,126.661424210148));
#118194=CARTESIAN_POINT('Ctrl Pts',(-173.801715468515,2.53503105213456,
126.587537431101));
#118195=CARTESIAN_POINT('Ctrl Pts',(-173.809463365292,2.41638960572452,
126.518445247014));
#118196=CARTESIAN_POINT('Ctrl Pts',(-173.817211262069,2.29503548822038,
126.454418644354));
#118197=CARTESIAN_POINT('Ctrl Pts',(-173.824957538153,2.17370675538154,
126.390405434679));
#118198=CARTESIAN_POINT('Ctrl Pts',(-173.832703814237,2.04966682567235,
126.331455881131));
#118199=CARTESIAN_POINT('Ctrl Pts',(-173.840450090321,1.92337997266463,
126.277795413877));
#118200=CARTESIAN_POINT('Ctrl Pts',(-173.848196423587,1.79709218743656,
126.224134550513));
#118201=CARTESIAN_POINT('Ctrl Pts',(-173.855942756852,1.66855780564238,
126.175763004246));
#118202=CARTESIAN_POINT('Ctrl Pts',(-173.863689090117,1.53826147645589,
126.132858215495));
#118203=CARTESIAN_POINT('Ctrl Pts',(-173.87143715812,1.40793596830971,126.089943818514));
#118204=CARTESIAN_POINT('Ctrl Pts',(-173.879185226123,1.27584809889036,
126.052498737407));
#118205=CARTESIAN_POINT('Ctrl Pts',(-173.886933294126,1.14249769735741,
126.020650543363));
#118206=CARTESIAN_POINT('Ctrl Pts',(-173.894689596868,1.00900556943065,
125.988768500679));
#118207=CARTESIAN_POINT('Ctrl Pts',(-173.90244589961,0.874248609808633,
125.96249531867));
#118208=CARTESIAN_POINT('Ctrl Pts',(-173.910202202352,0.738737412602422,
125.941907522911));
#118209=CARTESIAN_POINT('Ctrl Pts',(-173.917962644866,0.60315388898973,
125.921308738825));
#118210=CARTESIAN_POINT('Ctrl Pts',(-173.92572308738,0.46681571411805,125.906401429885));
#118211=CARTESIAN_POINT('Ctrl Pts',(-173.933483529894,0.330237633308961,
125.897210103465));
#118212=CARTESIAN_POINT('Ctrl Pts',(-173.94125643016,0.193440305240098,
125.888004022311));
#118213=CARTESIAN_POINT('Ctrl Pts',(-173.949029330425,0.0564026927094663,
125.884532269762));
#118214=CARTESIAN_POINT('Ctrl Pts',(-173.95680223069,-0.0803605270785853,
125.886767176849));
#118215=CARTESIAN_POINT('Ctrl Pts',(-173.964292566452,-0.212152059340465,
125.888920839433));
#118216=CARTESIAN_POINT('Ctrl Pts',(-173.971782902214,-0.343688494712483,
125.896373444647));
#118217=CARTESIAN_POINT('Ctrl Pts',(-173.979273237976,-0.47451657492709,
125.90905500069));
#118218=CARTESIAN_POINT('Ctrl Pts',(-173.987047572095,-0.610305041568332,
125.922217381785));
#118219=CARTESIAN_POINT('Ctrl Pts',(-173.994821906215,-0.745760515184663,
125.941054746775));
#118220=CARTESIAN_POINT('Ctrl Pts',(-174.002596240334,-0.880370596477415,
125.965545610216));
#118221=CARTESIAN_POINT('Ctrl Pts',(-174.010360993281,-1.01481478287542,
125.990006290856));
#118222=CARTESIAN_POINT('Ctrl Pts',(-174.018125746228,-1.14841526900349,
126.020106537523));
#118223=CARTESIAN_POINT('Ctrl Pts',(-174.025890499175,-1.28066341749588,
126.055773009278));
#118224=CARTESIAN_POINT('Ctrl Pts',(-174.03364754006,-1.41278021526318,
126.09140405659));
#118225=CARTESIAN_POINT('Ctrl Pts',(-174.041404580945,-1.54354697330977,
126.132590225974));
#118226=CARTESIAN_POINT('Ctrl Pts',(-174.04916162183,-1.67246426489251,
126.179206961183));
#118227=CARTESIAN_POINT('Ctrl Pts',(-174.05691281307,-1.80128433894267,
126.225788542348));
#118228=CARTESIAN_POINT('Ctrl Pts',(-174.06466400431,-1.92825735641036,
126.277792405618));
#118229=CARTESIAN_POINT('Ctrl Pts',(-174.072415195551,-2.05289845017935,
126.335044001376));
#118230=CARTESIAN_POINT('Ctrl Pts',(-174.080163092328,-2.1774865681584,
126.392271263679));
#118231=CARTESIAN_POINT('Ctrl Pts',(-174.087910989105,-2.29974437918586,
126.454741659475));
#118232=CARTESIAN_POINT('Ctrl Pts',(-174.095658885882,-2.41920663808135,
126.522232372784));
#118233=CARTESIAN_POINT('Ctrl Pts',(-174.103405161966,-2.5386439080476,
126.58970896849));
#118234=CARTESIAN_POINT('Ctrl Pts',(-174.11115143805,-2.65528644883749,
126.662203600732));
#118235=CARTESIAN_POINT('Ctrl Pts',(-174.118897714134,-2.76869364846007,
126.739447513516));
#118236=CARTESIAN_POINT('Ctrl Pts',(-174.1266440474,-2.882101685229,126.816691996497));
#118237=CARTESIAN_POINT('Ctrl Pts',(-174.134390380665,-2.99227401004361,
126.898685609886));
#118238=CARTESIAN_POINT('Ctrl Pts',(-174.14213671393,-3.09879937253713,
126.985116515487));
#118239=CARTESIAN_POINT('Ctrl Pts',(-174.149884781933,-3.20534859064743,
127.071566776691));
#118240=CARTESIAN_POINT('Ctrl Pts',(-174.157632849936,-3.30824891773031,
127.162456061171));
#118241=CARTESIAN_POINT('Ctrl Pts',(-174.165380917939,-3.40712285466095,
127.257432803845));
#118242=CARTESIAN_POINT('Ctrl Pts',(-174.173137220681,-3.50610187598796,
127.352510488931));
#118243=CARTESIAN_POINT('Ctrl Pts',(-174.180893523423,-3.60104567640467,
127.451684038943));
#118244=CARTESIAN_POINT('Ctrl Pts',(-174.188649826165,-3.69161388418876,
127.554565240536));
#118245=CARTESIAN_POINT('Ctrl Pts',(-174.196410268679,-3.78223043095229,
127.657501352925));
#118246=CARTESIAN_POINT('Ctrl Pts',(-174.204170711193,-3.86846648592348,
127.764148756128));
#118247=CARTESIAN_POINT('Ctrl Pts',(-174.211931153708,-3.95002319793488,
127.874087627165));
#118248=CARTESIAN_POINT('Ctrl Pts',(-174.219704053973,-4.03171083202067,
127.984202981836));
#118249=CARTESIAN_POINT('Ctrl Pts',(-174.227476954239,-4.10870389266763,
128.097620039311));
#118250=CARTESIAN_POINT('Ctrl Pts',(-174.235249854504,-4.18074746296302,
128.213890831325));
#118251=CARTESIAN_POINT('Ctrl Pts',(-174.242740190266,-4.25017206801078,
128.32593488718));
#118252=CARTESIAN_POINT('Ctrl Pts',(-174.250230526028,-4.31500063644984,
128.440628530722));
#118253=CARTESIAN_POINT('Ctrl Pts',(-174.25772086179,-4.37504705720004,
128.557552590656));
#118254=CARTESIAN_POINT('Ctrl Pts',(-174.265995971559,-4.44138463387784,
128.686726964323));
#118255=CARTESIAN_POINT('Ctrl Pts',(-174.274271081328,-4.50207445138269,
128.818991058705));
#118256=CARTESIAN_POINT('Ctrl Pts',(-174.282546191098,-4.55683688270711,
128.953841585808));
#118257=CARTESIAN_POINT('Ctrl Pts',(-174.290801622159,-4.61146908568318,
129.088371430263));
#118258=CARTESIAN_POINT('Ctrl Pts',(-174.29905705322,-4.66020189058618,
129.22547515269));
#118259=CARTESIAN_POINT('Ctrl Pts',(-174.307312484282,-4.70280224557678,
129.364626579107));
#118260=CARTESIAN_POINT('Ctrl Pts',(-174.311589785604,-4.72487432798964,
129.436723672016));
#118261=CARTESIAN_POINT('Ctrl Pts',(-174.315867086927,-4.74530091292852,
129.509370057858));
#118262=CARTESIAN_POINT('Ctrl Pts',(-174.32014438825,-4.76405452823397,
129.582490119308));
#118263=CARTESIAN_POINT('Origin',(213.235140564004,0.,130.804360617566));
#118264=CARTESIAN_POINT('',(-176.415048843504,-4.76405452823411,129.582490119309));
#118265=CARTESIAN_POINT('',(-176.069836735653,-4.76405452823418,129.582490119309));
#118266=CARTESIAN_POINT('',(213.235140564004,-4.76405452823405,129.582490119308));
#118267=CARTESIAN_POINT('',(-174.735140563982,-4.91824795254522,130.808848354713));
#118268=CARTESIAN_POINT('Ctrl Pts',(-174.735140564012,-4.91824795254474,
130.808848355242));
#118269=CARTESIAN_POINT('Ctrl Pts',(-174.745911124724,-4.91807457526139,
130.998857783261));
#118270=CARTESIAN_POINT('Ctrl Pts',(-174.756681685436,-4.90688666222565,
131.188385333141));
#118271=CARTESIAN_POINT('Ctrl Pts',(-174.767452246148,-4.88487163251762,
131.376385264172));
#118272=CARTESIAN_POINT('Ctrl Pts',(-174.776643868517,-4.86608395331184,
131.536824856658));
#118273=CARTESIAN_POINT('Ctrl Pts',(-174.785835490886,-4.83941174830359,
131.696152789862));
#118274=CARTESIAN_POINT('Ctrl Pts',(-174.795027113255,-4.80499718976505,
131.853734273062));
#118275=CARTESIAN_POINT('Ctrl Pts',(-174.802801447374,-4.77588913180794,
131.987017718812));
#118276=CARTESIAN_POINT('Ctrl Pts',(-174.810575781493,-4.74118514044176,
132.119300237066));
#118277=CARTESIAN_POINT('Ctrl Pts',(-174.818350115612,-4.70096706956376,
132.250075552599));
#118278=CARTESIAN_POINT('Ctrl Pts',(-174.826114868559,-4.66079856386371,
132.380689699243));
#118279=CARTESIAN_POINT('Ctrl Pts',(-174.833879621506,-4.61512961371124,
132.509799968916));
#118280=CARTESIAN_POINT('Ctrl Pts',(-174.841644374453,-4.56409312122651,
132.636909946581));
#118281=CARTESIAN_POINT('Ctrl Pts',(-174.849401415338,-4.51310731890562,
132.763893676824));
#118282=CARTESIAN_POINT('Ctrl Pts',(-174.857158456223,-4.45676472815101,
132.888880708253));
#118283=CARTESIAN_POINT('Ctrl Pts',(-174.864915497108,-4.3952480200623,
133.011389820961));
#118284=CARTESIAN_POINT('Ctrl Pts',(-174.872666688349,-4.33377770220161,
133.133806548594));
#118285=CARTESIAN_POINT('Ctrl Pts',(-174.880417879589,-4.26714120811986,
133.253748728899));
#118286=CARTESIAN_POINT('Ctrl Pts',(-174.888169070829,-4.19556913274437,
133.370755504341));
#118287=CARTESIAN_POINT('Ctrl Pts',(-174.895916967606,-4.12402747741026,
133.487712548781));
#118288=CARTESIAN_POINT('Ctrl Pts',(-174.903664864383,-4.04755461663727,
133.601736336972));
#118289=CARTESIAN_POINT('Ctrl Pts',(-174.91141276116,-3.96642675636401,
133.712391196652));
#118290=CARTESIAN_POINT('Ctrl Pts',(-174.919159037244,-3.88531586629019,
133.823022909721));
#118291=CARTESIAN_POINT('Ctrl Pts',(-174.926905313328,-3.79955214453047,
133.930286780879));
#118292=CARTESIAN_POINT('Ctrl Pts',(-174.934651589413,-3.70945450609213,
134.033777024555));
#118293=CARTESIAN_POINT('Ctrl Pts',(-174.942397922678,-3.61935620257362,
134.137268032174));
#118294=CARTESIAN_POINT('Ctrl Pts',(-174.950144255943,-3.52492417525399,
134.236985061852));
#118295=CARTESIAN_POINT('Ctrl Pts',(-174.957890589209,-3.42651665193184,
134.332556572517));
#118296=CARTESIAN_POINT('Ctrl Pts',(-174.965638657212,-3.32808709092703,
134.42814948576));
#118297=CARTESIAN_POINT('Ctrl Pts',(-174.973386725215,-3.22568054276838,
134.51959476033));
#118298=CARTESIAN_POINT('Ctrl Pts',(-174.981134793218,-3.11969069776469,
134.606559062253));
#118299=CARTESIAN_POINT('Ctrl Pts',(-174.98889109596,-3.01358820549229,
134.693615790871));
#118300=CARTESIAN_POINT('Ctrl Pts',(-174.996647398702,-2.90389511147362,
134.776181784986));
#118301=CARTESIAN_POINT('Ctrl Pts',(-175.004403701443,-2.79103711269373,
134.853964906637));
#118302=CARTESIAN_POINT('Ctrl Pts',(-175.012164143958,-2.67811887820181,
134.931789543483));
#118303=CARTESIAN_POINT('Ctrl Pts',(-175.019924586472,-2.56203270382088,
135.004826013173));
#118304=CARTESIAN_POINT('Ctrl Pts',(-175.027685028986,-2.44323077098833,
135.072827141061));
#118305=CARTESIAN_POINT('Ctrl Pts',(-175.035457929251,-2.32423812674647,
135.140937430396));
#118306=CARTESIAN_POINT('Ctrl Pts',(-175.043230829517,-2.20252135957344,
135.203996045214));
#118307=CARTESIAN_POINT('Ctrl Pts',(-175.051003729782,-2.07855541016828,
135.261802761819));
#118308=CARTESIAN_POINT('Ctrl Pts',(-175.058494065544,-1.9590959352747,
135.317508058668));
#118309=CARTESIAN_POINT('Ctrl Pts',(-175.065984401307,-1.83754825013354,
135.368336548634));
#118310=CARTESIAN_POINT('Ctrl Pts',(-175.073474737069,-1.71435057346656,
135.414152931082));
#118311=CARTESIAN_POINT('Ctrl Pts',(-175.081249071188,-1.58648181944417,
135.461706455597));
#118312=CARTESIAN_POINT('Ctrl Pts',(-175.089023405307,-1.4564304353754,
135.504010937089));
#118313=CARTESIAN_POINT('Ctrl Pts',(-175.096797739426,-1.32466660897776,
135.540861587434));
#118314=CARTESIAN_POINT('Ctrl Pts',(-175.104562492373,-1.19306516972009,
135.577666822646));
#118315=CARTESIAN_POINT('Ctrl Pts',(-175.11232724532,-1.05975586016739,
135.609031495923));
#118316=CARTESIAN_POINT('Ctrl Pts',(-175.120091998267,-0.925228165192352,
135.634799097128));
#118317=CARTESIAN_POINT('Ctrl Pts',(-175.127849039152,-0.790834085020836,
135.660541105589));
#118318=CARTESIAN_POINT('Ctrl Pts',(-175.135606080037,-0.655224409115649,
135.680697031747));
#118319=CARTESIAN_POINT('Ctrl Pts',(-175.143363120922,-0.518902739605467,
135.695160450858));
#118320=CARTESIAN_POINT('Ctrl Pts',(-175.151114312162,-0.382683871326505,
135.709612962992));
#118321=CARTESIAN_POINT('Ctrl Pts',(-175.158865503402,-0.245754465359081,
135.718381471483));
#118322=CARTESIAN_POINT('Ctrl Pts',(-175.166616694642,-0.108626896390376,
135.721410877618));
#118323=CARTESIAN_POINT('Ctrl Pts',(-175.17436459142,0.0284423897037063,
135.724438996175));
#118324=CARTESIAN_POINT('Ctrl Pts',(-175.182112488197,0.165709281231323,
135.721732855286));
#118325=CARTESIAN_POINT('Ctrl Pts',(-175.189860384974,0.302657938724789,
135.71328934333));
#118326=CARTESIAN_POINT('Ctrl Pts',(-175.197606661058,0.439577949511379,
135.704847597574));
#118327=CARTESIAN_POINT('Ctrl Pts',(-175.205352937142,0.576179468693615,
135.690670891929));
#118328=CARTESIAN_POINT('Ctrl Pts',(-175.213099213226,0.711948716028222,
135.67080820161));
#118329=CARTESIAN_POINT('Ctrl Pts',(-175.220845546492,0.847718965580385,
135.650945364669));
#118330=CARTESIAN_POINT('Ctrl Pts',(-175.228591879757,0.982656544178437,
135.625396515895));
#118331=CARTESIAN_POINT('Ctrl Pts',(-175.236338213022,1.11625523292035,
135.594262215457));
#118332=CARTESIAN_POINT('Ctrl Pts',(-175.244086281025,1.24988384016211,
135.563120942708));
#118333=CARTESIAN_POINT('Ctrl Pts',(-175.251834349028,1.38217258022104,
135.526391818018));
#118334=CARTESIAN_POINT('Ctrl Pts',(-175.259582417031,1.51262821055619,
135.484225889038));
#118335=CARTESIAN_POINT('Ctrl Pts',(-175.267338719773,1.64322249068787,
135.442015145607));
#118336=CARTESIAN_POINT('Ctrl Pts',(-175.275095022515,1.77197939664634,
135.394356175545));
#118337=CARTESIAN_POINT('Ctrl Pts',(-175.282851325257,1.89842304487477,
135.341449222078));
#118338=CARTESIAN_POINT('Ctrl Pts',(-175.290611767771,2.02493417988575,
135.288514030576));
#118339=CARTESIAN_POINT('Ctrl Pts',(-175.298372210285,2.14912924315125,
135.23032544022));
#118340=CARTESIAN_POINT('Ctrl Pts',(-175.306132652799,2.27055586452998,
135.167130280125));
#118341=CARTESIAN_POINT('Ctrl Pts',(-175.313905553065,2.39217741070076,
135.10383367355));
#118342=CARTESIAN_POINT('Ctrl Pts',(-175.32167845333,2.51102129501437,135.035514631731));
#118343=CARTESIAN_POINT('Ctrl Pts',(-175.329451353595,2.62666234655475,
134.96246450993));
#118344=CARTESIAN_POINT('Ctrl Pts',(-175.336941689357,2.73809955458783,
134.89206994406));
#118345=CARTESIAN_POINT('Ctrl Pts',(-175.344432025119,2.84656249551728,
134.817282474524));
#118346=CARTESIAN_POINT('Ctrl Pts',(-175.351922360881,2.95170046916539,
134.738397653847));
#118347=CARTESIAN_POINT('Ctrl Pts',(-175.359696695,3.06082478104204,134.656521891216));
#118348=CARTESIAN_POINT('Ctrl Pts',(-175.367471029119,3.16671268921718,
134.569972584143));
#118349=CARTESIAN_POINT('Ctrl Pts',(-175.375245363238,3.26893775169545,
134.479034621888));
#118350=CARTESIAN_POINT('Ctrl Pts',(-175.383010116185,3.37103683092005,
134.388208732544));
#118351=CARTESIAN_POINT('Ctrl Pts',(-175.390774869133,3.46948175691526,
134.293005206933));
#118352=CARTESIAN_POINT('Ctrl Pts',(-175.39853962208,3.56387627474123,134.193751264989));
#118353=CARTESIAN_POINT('Ctrl Pts',(-175.406296662965,3.65817703860136,
134.094595903459));
#118354=CARTESIAN_POINT('Ctrl Pts',(-175.41405370385,3.74843513240106,133.991398412879));
#118355=CARTESIAN_POINT('Ctrl Pts',(-175.421810744735,3.83428880873651,
133.884524962808));
#118356=CARTESIAN_POINT('Ctrl Pts',(-175.429561935975,3.92007774214691,
133.777732106836));
#118357=CARTESIAN_POINT('Ctrl Pts',(-175.437313127215,4.0014686252892,133.667269112576));
#118358=CARTESIAN_POINT('Ctrl Pts',(-175.445064318455,4.07813815102295,
133.553537273161));
#118359=CARTESIAN_POINT('Ctrl Pts',(-175.452812215232,4.15477509016293,
133.439853772813));
#118360=CARTESIAN_POINT('Ctrl Pts',(-175.460560112009,4.22669444499128,
133.322904514119));
#118361=CARTESIAN_POINT('Ctrl Pts',(-175.468308008786,4.29361477378184,
133.203121805526));
#118362=CARTESIAN_POINT('Ctrl Pts',(-175.47605428487,4.36052110428226,133.083364152893));
#118363=CARTESIAN_POINT('Ctrl Pts',(-175.483800560955,4.42243029811331,
132.960774570363));
#118364=CARTESIAN_POINT('Ctrl Pts',(-175.491546837039,4.47910584873974,
132.835811788105));
#118365=CARTESIAN_POINT('Ctrl Pts',(-175.499293170304,4.53578181773229,
132.7108480834));
#118366=CARTESIAN_POINT('Ctrl Pts',(-175.507039503569,4.58722390494409,
132.583511500068));
#118367=CARTESIAN_POINT('Ctrl Pts',(-175.514785836835,4.63324309081047,
132.454282289633));
#118368=CARTESIAN_POINT('Ctrl Pts',(-175.522533904838,4.67927258235439,
132.325024139213));
#118369=CARTESIAN_POINT('Ctrl Pts',(-175.530281972841,4.7198766248637,132.193872886536));
#118370=CARTESIAN_POINT('Ctrl Pts',(-175.538030040843,4.75491568936418,
132.061325155466));
#118371=CARTESIAN_POINT('Ctrl Pts',(-175.545786343585,4.78999199379943,
131.92863655109));
#118372=CARTESIAN_POINT('Ctrl Pts',(-175.553542646327,4.81949140524646,
131.794548882068));
#118373=CARTESIAN_POINT('Ctrl Pts',(-175.561298949069,4.84332516731719,
131.65957075907));
#118374=CARTESIAN_POINT('Ctrl Pts',(-175.569059391583,4.86717165018437,
131.524520594184));
#118375=CARTESIAN_POINT('Ctrl Pts',(-175.576819834097,4.8853464064593,131.388579415649));
#118376=CARTESIAN_POINT('Ctrl Pts',(-175.584580276612,4.89781258335714,
131.252261232444));
#118377=CARTESIAN_POINT('Ctrl Pts',(-175.592353176877,4.91029877206883,
131.11572421919));
#118378=CARTESIAN_POINT('Ctrl Pts',(-175.600126077143,4.91705804968544,
130.978809382595));
#118379=CARTESIAN_POINT('Ctrl Pts',(-175.607898977408,4.91810572637498,
130.842031915627));
#118380=CARTESIAN_POINT('Ctrl Pts',(-175.61538931317,4.91911531737791,130.710226654106));
#118381=CARTESIAN_POINT('Ctrl Pts',(-175.622879648932,4.91482137009318,
130.578549256001));
#118382=CARTESIAN_POINT('Ctrl Pts',(-175.630369984694,4.90528297921777,
130.447454528662));
#118383=CARTESIAN_POINT('Ctrl Pts',(-175.638144318813,4.89538293735313,
130.311389304891));
#118384=CARTESIAN_POINT('Ctrl Pts',(-175.645918652932,4.87980155493366,
130.175520794284));
#118385=CARTESIAN_POINT('Ctrl Pts',(-175.653692987051,4.85854801504704,
130.040361764175));
#118386=CARTESIAN_POINT('Ctrl Pts',(-175.661457739998,4.8373206682489,129.905369305491));
#118387=CARTESIAN_POINT('Ctrl Pts',(-175.669222492945,4.81043513299945,
129.771084970078));
#118388=CARTESIAN_POINT('Ctrl Pts',(-175.676987245893,4.77795252322328,
129.638019008806));
#118389=CARTESIAN_POINT('Ctrl Pts',(-175.684744286778,4.74550217563306,
129.505085210523));
#118390=CARTESIAN_POINT('Ctrl Pts',(-175.692501327663,4.70746590847843,
129.37336775557));
#118391=CARTESIAN_POINT('Ctrl Pts',(-175.700258368548,4.66395625727218,
129.243368915874));
#118392=CARTESIAN_POINT('Ctrl Pts',(-175.708009559788,4.6204794170323,129.113468109314));
#118393=CARTESIAN_POINT('Ctrl Pts',(-175.715760751028,4.57153753190743,
128.98528370761));
#118394=CARTESIAN_POINT('Ctrl Pts',(-175.723511942268,4.51729346577151,
128.859304626959));
#118395=CARTESIAN_POINT('Ctrl Pts',(-175.731259839045,4.46307245481078,
128.733379090777));
#118396=CARTESIAN_POINT('Ctrl Pts',(-175.739007735822,4.40355389930882,
128.609657369729));
#118397=CARTESIAN_POINT('Ctrl Pts',(-175.746755632599,4.33894938647817,
128.488609921986));
#118398=CARTESIAN_POINT('Ctrl Pts',(-175.754501908683,4.27435838751889,
128.367587794759));
#118399=CARTESIAN_POINT('Ctrl Pts',(-175.762248184767,4.20468373130066,
128.249239172855));
#118400=CARTESIAN_POINT('Ctrl Pts',(-175.769994460852,4.13018352294818,
128.134010990782));
#118401=CARTESIAN_POINT('Ctrl Pts',(-175.777740794117,4.05568276465198,
128.01878195812));
#118402=CARTESIAN_POINT('Ctrl Pts',(-175.785487127382,3.97635659541556,
127.906673739573));
#118403=CARTESIAN_POINT('Ctrl Pts',(-175.793233460648,3.89250689475741,
127.798104950334));
#118404=CARTESIAN_POINT('Ctrl Pts',(-175.800981528651,3.80863841654029,
127.689511847867));
#118405=CARTESIAN_POINT('Ctrl Pts',(-175.808729596654,3.72024463005167,
127.584460061318));
#118406=CARTESIAN_POINT('Ctrl Pts',(-175.816477664657,3.627667940195,127.483335417695));
#118407=CARTESIAN_POINT('Ctrl Pts',(-175.824233967398,3.53499285873054,
127.382103297596));
#118408=CARTESIAN_POINT('Ctrl Pts',(-175.83199027014,3.43812625767265,127.284806946899));
#118409=CARTESIAN_POINT('Ctrl Pts',(-175.839746572882,3.33744807058666,
127.191795955358));
#118410=CARTESIAN_POINT('Ctrl Pts',(-175.847507015396,3.23671614852086,
127.098735321049));
#118411=CARTESIAN_POINT('Ctrl Pts',(-175.855267457911,3.13216888467507,
127.009964856313));
#118412=CARTESIAN_POINT('Ctrl Pts',(-175.863027900425,3.02421880952979,
126.92579340085));
#118413=CARTESIAN_POINT('Ctrl Pts',(-175.87080080069,2.91609544334053,126.841486825893));
#118414=CARTESIAN_POINT('Ctrl Pts',(-175.878573700956,2.80455866833949,
126.761794240691));
#118415=CARTESIAN_POINT('Ctrl Pts',(-175.886346601221,2.6900502064823,126.686981238749));
#118416=CARTESIAN_POINT('Ctrl Pts',(-175.893836936983,2.57970441564334,
126.614887877871));
#118417=CARTESIAN_POINT('Ctrl Pts',(-175.901327272745,2.46659950792686,
126.547325647257));
#118418=CARTESIAN_POINT('Ctrl Pts',(-175.908817608507,2.35115006776496,
126.484490663349));
#118419=CARTESIAN_POINT('Ctrl Pts',(-175.916591942626,2.23132332698904,
126.419273271927));
#118420=CARTESIAN_POINT('Ctrl Pts',(-175.924366276745,2.10859118322595,
126.358942081489));
#118421=CARTESIAN_POINT('Ctrl Pts',(-175.932140610864,1.98339000583746,
126.30376652931));
#118422=CARTESIAN_POINT('Ctrl Pts',(-175.939905363811,1.8583431277109,126.248658976068));
#118423=CARTESIAN_POINT('Ctrl Pts',(-175.947670116758,1.73083362468,126.198694574944));
#118424=CARTESIAN_POINT('Ctrl Pts',(-175.955434869705,1.60132381882267,
126.15409771212));
#118425=CARTESIAN_POINT('Ctrl Pts',(-175.96319191059,1.47194264393028,126.109545143528));
#118426=CARTESIAN_POINT('Ctrl Pts',(-175.970948951475,1.34056548716186,
126.070349630549));
#118427=CARTESIAN_POINT('Ctrl Pts',(-175.97870599236,1.20767575230822,126.036687984112));
#118428=CARTESIAN_POINT('Ctrl Pts',(-175.986457183601,1.07488623063718,
126.003051722185));
#118429=CARTESIAN_POINT('Ctrl Pts',(-175.994208374841,0.940586778731302,
125.974941116047));
#118430=CARTESIAN_POINT('Ctrl Pts',(-176.001959566081,0.805276767535073,
125.952483414857));
#118431=CARTESIAN_POINT('Ctrl Pts',(-176.009707462858,0.670024266702931,
125.930035258788));
#118432=CARTESIAN_POINT('Ctrl Pts',(-176.017455359635,0.533762445733919,
125.913235292888));
#118433=CARTESIAN_POINT('Ctrl Pts',(-176.025203256412,0.397001482467536,
125.902159796973));
#118434=CARTESIAN_POINT('Ctrl Pts',(-176.032949532496,0.260269126646816,
125.891086617814));
#118435=CARTESIAN_POINT('Ctrl Pts',(-176.04069580858,0.123038225648086,
125.885735558414));
#118436=CARTESIAN_POINT('Ctrl Pts',(-176.048442084664,-0.0141756897444903,
125.886131046641));
#118437=CARTESIAN_POINT('Ctrl Pts',(-176.05618841793,-0.151390618019207,
125.886526537788));
#118438=CARTESIAN_POINT('Ctrl Pts',(-176.063934751195,-0.288588169473994,
125.89266866008));
#118439=CARTESIAN_POINT('Ctrl Pts',(-176.07168108446,-0.425252978037041,
125.904529705466));
#118440=CARTESIAN_POINT('Ctrl Pts',(-176.079429152463,-0.561948391736213,
125.916393407051));
#118441=CARTESIAN_POINT('Ctrl Pts',(-176.087177220466,-0.698110435715874,
125.933978546404));
#118442=CARTESIAN_POINT('Ctrl Pts',(-176.094925288469,-0.833229424573775,
125.957205597503));
#118443=CARTESIAN_POINT('Ctrl Pts',(-176.102681591211,-0.968492019501155,
125.980457334588));
#118444=CARTESIAN_POINT('Ctrl Pts',(-176.110437893953,-1.10270895888793,
126.009362895315));
#118445=CARTESIAN_POINT('Ctrl Pts',(-176.118194196695,-1.23538075960113,
126.043791592617));
#118446=CARTESIAN_POINT('Ctrl Pts',(-176.125954639209,-1.36812337124905,
126.07823866555));
#118447=CARTESIAN_POINT('Ctrl Pts',(-176.133715081723,-1.49931882715872,
126.118214635027));
#118448=CARTESIAN_POINT('Ctrl Pts',(-176.141475524237,-1.62848430894264,
126.163539362871));
#118449=CARTESIAN_POINT('Ctrl Pts',(-176.149248424503,-1.75785713862469,
126.208936849992));
#118450=CARTESIAN_POINT('Ctrl Pts',(-176.157021324768,-1.88519311889149,
126.259700108784));
#118451=CARTESIAN_POINT('Ctrl Pts',(-176.164794225033,-2.01003003689772,
126.315601065834));
#118452=CARTESIAN_POINT('Ctrl Pts',(-176.172284560796,-2.13032881849257,
126.36946988229));
#118453=CARTESIAN_POINT('Ctrl Pts',(-176.179774896558,-2.24830680193459,
126.428109208505));
#118454=CARTESIAN_POINT('Ctrl Pts',(-176.18726523232,-2.36357489589605,
126.49127624858));
#118455=CARTESIAN_POINT('Ctrl Pts',(-176.195040580708,-2.48322902315794,
126.556846839645));
#118456=CARTESIAN_POINT('Ctrl Pts',(-176.202815929095,-2.60034202907575,
126.627504267593));
#118457=CARTESIAN_POINT('Ctrl Pts',(-176.210591277483,-2.71445118038675,
126.703026950111));
#118458=CARTESIAN_POINT('Ctrl Pts',(-176.218356821904,-2.82841645102932,
126.778454405788));
#118459=CARTESIAN_POINT('Ctrl Pts',(-176.226122366324,-2.93938508089296,
126.858734694858));
#118460=CARTESIAN_POINT('Ctrl Pts',(-176.233887910745,-3.04691826152936,
126.943600048707));
#118461=CARTESIAN_POINT('Ctrl Pts',(-176.241644111132,-3.15432205088633,
127.028363286756));
#118462=CARTESIAN_POINT('Ctrl Pts',(-176.249400311519,-3.25829831912221,
127.117700360751));
#118463=CARTESIAN_POINT('Ctrl Pts',(-176.257156511905,-3.35843715721145,
127.211300233498));
#118464=CARTESIAN_POINT('Ctrl Pts',(-176.264907414555,-3.4585075972185,
127.304836174488));
#118465=CARTESIAN_POINT('Ctrl Pts',(-176.272658317204,-3.55474553722263,
127.402628855934));
#118466=CARTESIAN_POINT('Ctrl Pts',(-176.280409219854,-3.64677404245612,
127.504326959288));
#118467=CARTESIAN_POINT('Ctrl Pts',(-176.288156507,-3.73875961986784,127.605977624318));
#118468=CARTESIAN_POINT('Ctrl Pts',(-176.295903794146,-3.8265394081865,
127.711529796871));
#118469=CARTESIAN_POINT('Ctrl Pts',(-176.303651081292,-3.90977354953123,
127.82059557087));
#118470=CARTESIAN_POINT('Ctrl Pts',(-176.311396432377,-3.9929868905086,
127.929634089128));
#118471=CARTESIAN_POINT('Ctrl Pts',(-176.319141783462,-4.07165660931931,
128.042184150169));
#118472=CARTESIAN_POINT('Ctrl Pts',(-176.326887134546,-4.14548360211894,
128.157825379361));
#118473=CARTESIAN_POINT('Ctrl Pts',(-176.334634739561,-4.21933207888202,
128.273500260633));
#118474=CARTESIAN_POINT('Ctrl Pts',(-176.342382344575,-4.28833479834117,
128.392267780956));
#118475=CARTESIAN_POINT('Ctrl Pts',(-176.350129949589,-4.35223637709258,
128.513679151187));
#118476=CARTESIAN_POINT('Ctrl Pts',(-176.357878554451,-4.41614620250603,
128.635106189866));
#118477=CARTESIAN_POINT('Ctrl Pts',(-176.365627159314,-4.47495340090362,
128.759177408328));
#118478=CARTESIAN_POINT('Ctrl Pts',(-176.373375764176,-4.52844934324666,
128.885420908209));
#118479=CARTESIAN_POINT('Ctrl Pts',(-176.381130985486,-4.58199096517854,
129.011772206007));
#118480=CARTESIAN_POINT('Ctrl Pts',(-176.388886206796,-4.63021212521479,
129.140299127584));
#118481=CARTESIAN_POINT('Ctrl Pts',(-176.396641428105,-4.67295286081902,
129.270511008555));
#118482=CARTESIAN_POINT('Ctrl Pts',(-176.402777233238,-4.70676863659504,
129.373532533759));
#118483=CARTESIAN_POINT('Ctrl Pts',(-176.408913038371,-4.73715477371064,
129.477608384682));
#118484=CARTESIAN_POINT('Ctrl Pts',(-176.415048843504,-4.76405452823412,
129.582490119309));
#118485=CARTESIAN_POINT('Ctrl Pts',(-174.665085416107,-4.76405452823406,
129.582490119308));
#118486=CARTESIAN_POINT('Ctrl Pts',(-174.672727967862,-4.79770218485229,
129.713681821788));
#118487=CARTESIAN_POINT('Ctrl Pts',(-174.680370519616,-4.82591771939868,
129.846230089272));
#118488=CARTESIAN_POINT('Ctrl Pts',(-174.68801307137,-4.84860984056921,
129.979639042466));
#118489=CARTESIAN_POINT('Ctrl Pts',(-174.695867653472,-4.87193151826708,
130.116749213218));
#118490=CARTESIAN_POINT('Ctrl Pts',(-174.703722235574,-4.88941875912728,
130.254768074855));
#118491=CARTESIAN_POINT('Ctrl Pts',(-174.711576817676,-4.90102947258295,
130.393151216685));
#118492=CARTESIAN_POINT('Ctrl Pts',(-174.719431399778,-4.91264018603865,
130.531534358515));
#118493=CARTESIAN_POINT('Ctrl Pts',(-174.72728598188,-4.91837439034014,
130.670281320698));
#118494=CARTESIAN_POINT('Ctrl Pts',(-174.735140563982,-4.91824795254522,
130.808848354713));
#118495=CARTESIAN_POINT('',(-174.389859435964,-4.91824995130059,130.803668496368));
#118496=CARTESIAN_POINT('Ctrl Pts',(-174.32014438825,-4.76405452823397,
129.582490119308));
#118497=CARTESIAN_POINT('Ctrl Pts',(-174.328374466888,-4.80013889944959,
129.723182535021));
#118498=CARTESIAN_POINT('Ctrl Pts',(-174.336604545527,-4.83002649212231,
129.865629683102));
#118499=CARTESIAN_POINT('Ctrl Pts',(-174.344834624166,-4.85355817089815,
130.00927814121));
#118500=CARTESIAN_POINT('Ctrl Pts',(-174.353045096558,-4.8770337909267,
130.152584390304));
#118501=CARTESIAN_POINT('Ctrl Pts',(-174.36125556895,-4.89418364153536,
130.297085932918));
#118502=CARTESIAN_POINT('Ctrl Pts',(-174.369466041342,-4.90489914177198,
130.442217729268));
#118503=CARTESIAN_POINT('Ctrl Pts',(-174.376263839549,-4.91377095874204,
130.562378496879));
#118504=CARTESIAN_POINT('Ctrl Pts',(-174.383061637757,-4.91823296612448,
130.682970933855));
#118505=CARTESIAN_POINT('Ctrl Pts',(-174.389859435964,-4.91824995130059,
130.803668496368));
#118506=CARTESIAN_POINT('Ctrl Pts',(-174.389859435994,-4.91824995130066,
130.803668496902));
#118507=CARTESIAN_POINT('Ctrl Pts',(-174.397893643521,-4.91827002578954,
130.946318989852));
#118508=CARTESIAN_POINT('Ctrl Pts',(-174.405927851049,-4.91207954534012,
131.088878016736));
#118509=CARTESIAN_POINT('Ctrl Pts',(-174.413962058576,-4.8997283684063,
131.23079347082));
#118510=CARTESIAN_POINT('Ctrl Pts',(-174.422004104632,-4.88736514111757,
131.372847383903));
#118511=CARTESIAN_POINT('Ctrl Pts',(-174.430046150687,-4.86882925974451,
131.514256126069));
#118512=CARTESIAN_POINT('Ctrl Pts',(-174.438088196743,-4.84422213234544,
131.654475312766));
#118513=CARTESIAN_POINT('Ctrl Pts',(-174.446261554148,-4.81921321725763,
131.796984012661));
#118514=CARTESIAN_POINT('Ctrl Pts',(-174.454434911553,-4.78793315202345,
131.93826360489));
#118515=CARTESIAN_POINT('Ctrl Pts',(-174.462608268958,-4.75054129509018,
132.077757832163));
#118516=CARTESIAN_POINT('Ctrl Pts',(-174.470675033247,-4.71363708531844,
132.215432840773));
#118517=CARTESIAN_POINT('Ctrl Pts',(-174.478741797536,-4.67077971865268,
132.351368467718));
#118518=CARTESIAN_POINT('Ctrl Pts',(-174.486808561825,-4.62217132855038,
132.485049545365));
#118519=CARTESIAN_POINT('Ctrl Pts',(-174.495035215788,-4.57259948155753,
132.621380288124));
#118520=CARTESIAN_POINT('Ctrl Pts',(-174.503261869751,-4.51704640646669,
132.755365819133));
#118521=CARTESIAN_POINT('Ctrl Pts',(-174.511488523714,-4.45577587641786,
132.886485590192));
#118522=CARTESIAN_POINT('Ctrl Pts',(-174.519715177677,-4.39450534636902,
133.017605361251));
#118523=CARTESIAN_POINT('Ctrl Pts',(-174.52794183164,-4.32751759405783,
133.145859069558));
#118524=CARTESIAN_POINT('Ctrl Pts',(-174.536168485603,-4.25512302683112,
133.270756994678));
#118525=CARTESIAN_POINT('Ctrl Pts',(-174.543942819722,-4.1867088749093,
133.388787752388));
#118526=CARTESIAN_POINT('Ctrl Pts',(-174.551717153841,-4.11327164267325,
133.504156745509));
#118527=CARTESIAN_POINT('Ctrl Pts',(-174.55949148796,-4.03504385882099,
133.616406868944));
#118528=CARTESIAN_POINT('Ctrl Pts',(-174.567256240907,-3.95691248372091,
133.728518654134));
#118529=CARTESIAN_POINT('Ctrl Pts',(-174.575020993854,-3.87400252545046,
133.837518899834));
#118530=CARTESIAN_POINT('Ctrl Pts',(-174.582785746801,-3.78659211245163,
133.942975477089));
#118531=CARTESIAN_POINT('Ctrl Pts',(-174.590542787686,-3.69926851670726,
134.048327313385));
#118532=CARTESIAN_POINT('Ctrl Pts',(-174.598299828571,-3.60745360944987,
134.150142186383));
#118533=CARTESIAN_POINT('Ctrl Pts',(-174.606056869456,-3.51146827176608,
134.248017632845));
#118534=CARTESIAN_POINT('Ctrl Pts',(-174.613808060696,-3.4155553173717,
134.345819270672));
#118535=CARTESIAN_POINT('Ctrl Pts',(-174.621559251936,-3.31547846502927,
134.439687117057));
#118536=CARTESIAN_POINT('Ctrl Pts',(-174.629310443176,-3.21159801369159,
134.529252731568));
#118537=CARTESIAN_POINT('Ctrl Pts',(-174.637058339954,-3.10776171431726,
134.618780278303));
#118538=CARTESIAN_POINT('Ctrl Pts',(-174.64480623673,-3.0001253267856,134.704008975273));
#118539=CARTESIAN_POINT('Ctrl Pts',(-174.652554133508,-2.88908489294528,
134.784608291249));
#118540=CARTESIAN_POINT('Ctrl Pts',(-174.660300409592,-2.77806768636997,
134.865190747585));
#118541=CARTESIAN_POINT('Ctrl Pts',(-174.668046685676,-2.66364816599903,
134.941145519547));
#118542=CARTESIAN_POINT('Ctrl Pts',(-174.67579296176,-2.54625391770853,
135.012183575944));
#118543=CARTESIAN_POINT('Ctrl Pts',(-174.683539295025,-2.42885880284051,
135.083222156728));
#118544=CARTESIAN_POINT('Ctrl Pts',(-174.691285628291,-2.30848925072723,
135.149343747116));
#118545=CARTESIAN_POINT('Ctrl Pts',(-174.699031961556,-2.18559982659186,
135.210303928652));
#118546=CARTESIAN_POINT('Ctrl Pts',(-174.706780029559,-2.06268288222183,
135.271277761798));
#118547=CARTESIAN_POINT('Ctrl Pts',(-174.714528097562,-1.93724529309587,
135.327087712354));
#118548=CARTESIAN_POINT('Ctrl Pts',(-174.722276165565,-1.80976372745136,
135.377536572338));
#118549=CARTESIAN_POINT('Ctrl Pts',(-174.730032468307,-1.68214667288201,
135.42803904997));
#118550=CARTESIAN_POINT('Ctrl Pts',(-174.737788771048,-1.55248166637986,
135.473168910906));
#118551=CARTESIAN_POINT('Ctrl Pts',(-174.74554507379,-1.42126327577423,
135.512777948627));
#118552=CARTESIAN_POINT('Ctrl Pts',(-174.753305516304,-1.28997484996227,
135.552408126885));
#118553=CARTESIAN_POINT('Ctrl Pts',(-174.761065958818,-1.15713176651945,
135.58651151335));
#118554=CARTESIAN_POINT('Ctrl Pts',(-174.768826401333,-1.02324008406824,
135.614990804231));
#118555=CARTESIAN_POINT('Ctrl Pts',(-174.776599301598,-0.889133466802005,
135.643515812598));
#118556=CARTESIAN_POINT('Ctrl Pts',(-174.784372201863,-0.753975272450605,
135.666398618665));
#118557=CARTESIAN_POINT('Ctrl Pts',(-174.792145102129,-0.618278896240742,
135.683593576645));
#118558=CARTESIAN_POINT('Ctrl Pts',(-174.799635437891,-0.487515425104283,
135.700163454591));
#118559=CARTESIAN_POINT('Ctrl Pts',(-174.807125773653,-0.356252528198735,
135.711451813691));
#118560=CARTESIAN_POINT('Ctrl Pts',(-174.814616109415,-0.224948809127052,
135.717463618295));
#118561=CARTESIAN_POINT('Ctrl Pts',(-174.822390443534,-0.0886666696388036,
135.723703362298));
#118562=CARTESIAN_POINT('Ctrl Pts',(-174.830164777653,0.0480911495213038,
135.724278297794));
#118563=CARTESIAN_POINT('Ctrl Pts',(-174.837939111772,0.184814385447683,
135.719136981291));
#118564=CARTESIAN_POINT('Ctrl Pts',(-174.845703864719,0.321369122205461,
135.714002001002));
#118565=CARTESIAN_POINT('Ctrl Pts',(-174.853468617666,0.45788897359358,
135.703164800257));
#118566=CARTESIAN_POINT('Ctrl Pts',(-174.861233370613,0.593860042067909,
135.686625800136));
#118567=CARTESIAN_POINT('Ctrl Pts',(-174.868990411498,0.729696062159804,
135.670103226783));
#118568=CARTESIAN_POINT('Ctrl Pts',(-174.876747452383,0.864983998436506,
135.647890170797));
#118569=CARTESIAN_POINT('Ctrl Pts',(-174.884504493268,0.999211803111557,
135.620039057311));
#118570=CARTESIAN_POINT('Ctrl Pts',(-174.892255684508,1.13333838555514,
135.592208946566));
#118571=CARTESIAN_POINT('Ctrl Pts',(-174.900006875749,1.2664060463982,135.558749320188));
#118572=CARTESIAN_POINT('Ctrl Pts',(-174.907758066989,1.39791005588486,
135.519764156836));
#118573=CARTESIAN_POINT('Ctrl Pts',(-174.915505963766,1.52935817265969,
135.480795563218));
#118574=CARTESIAN_POINT('Ctrl Pts',(-174.923253860543,1.65924358584838,
135.436306214505));
#118575=CARTESIAN_POINT('Ctrl Pts',(-174.93100175732,1.7870741398746,135.38645065172));
#118576=CARTESIAN_POINT('Ctrl Pts',(-174.938748033404,1.91487795450462,
135.336605517643));
#118577=CARTESIAN_POINT('Ctrl Pts',(-174.946494309488,2.04062740091991,
135.28139654417));
#118578=CARTESIAN_POINT('Ctrl Pts',(-174.954240585572,2.16384818838424,
135.221027242989));
#118579=CARTESIAN_POINT('Ctrl Pts',(-174.961986918838,2.28706988543627,
135.160657496176));
#118580=CARTESIAN_POINT('Ctrl Pts',(-174.969733252103,2.40776253519777,
135.095127517655));
#118581=CARTESIAN_POINT('Ctrl Pts',(-174.977479585368,2.52547479789236,
135.024687631876));
#118582=CARTESIAN_POINT('Ctrl Pts',(-174.985227653371,2.64321342143187,
134.954231971573));
#118583=CARTESIAN_POINT('Ctrl Pts',(-174.992975721374,2.75796999436092,
134.878864416774));
#118584=CARTESIAN_POINT('Ctrl Pts',(-175.000723789377,2.86932094919215,
134.798879406235));
#118585=CARTESIAN_POINT('Ctrl Pts',(-175.008480092119,2.98079024914342,
134.718809386675));
#118586=CARTESIAN_POINT('Ctrl Pts',(-175.016236394861,3.08884638255133,
134.634112336595));
#118587=CARTESIAN_POINT('Ctrl Pts',(-175.023992697603,3.19309733308253,
134.545124240673));
#118588=CARTESIAN_POINT('Ctrl Pts',(-175.031753140117,3.29740392548496,
134.456088649125));
#118589=CARTESIAN_POINT('Ctrl Pts',(-175.039513582631,3.39790100185022,
134.36275771412));
#118590=CARTESIAN_POINT('Ctrl Pts',(-175.047274025145,3.49423316069496,
134.265504602031));
#118591=CARTESIAN_POINT('Ctrl Pts',(-175.055046925411,3.59071996047304,
134.168095370613));
#118592=CARTESIAN_POINT('Ctrl Pts',(-175.062819825676,3.68302821876085,
134.066751669449));
#118593=CARTESIAN_POINT('Ctrl Pts',(-175.070592725941,3.77084202980583,
133.961880759822));
#118594=CARTESIAN_POINT('Ctrl Pts',(-175.078083061704,3.85546358763205,
133.86082217191));
#118595=CARTESIAN_POINT('Ctrl Pts',(-175.085573397466,3.93591160589967,
133.75648861301));
#118596=CARTESIAN_POINT('Ctrl Pts',(-175.093063733228,4.01194237480773,
133.649268602672));
#118597=CARTESIAN_POINT('Ctrl Pts',(-175.100838067347,4.09085587342609,
133.537983313057));
#118598=CARTESIAN_POINT('Ctrl Pts',(-175.108612401466,4.16526052469369,
133.423235853293));
#118599=CARTESIAN_POINT('Ctrl Pts',(-175.116386735585,4.23483723817989,
133.305427715551));
#118600=CARTESIAN_POINT('Ctrl Pts',(-175.124151488532,4.30432820458459,
133.187764765811));
#118601=CARTESIAN_POINT('Ctrl Pts',(-175.13191624148,4.36900287503006,133.067048976679));
#118602=CARTESIAN_POINT('Ctrl Pts',(-175.139680994427,4.42858382960782,
132.943712932318));
#118603=CARTESIAN_POINT('Ctrl Pts',(-175.147438035312,4.4881056075417,132.820499387055));
#118604=CARTESIAN_POINT('Ctrl Pts',(-175.155195076197,4.54254356858293,
132.694671115367));
#118605=CARTESIAN_POINT('Ctrl Pts',(-175.162952117082,4.59166504514604,
132.566687254624));
#118606=CARTESIAN_POINT('Ctrl Pts',(-175.170703308322,4.64074947882176,
132.438799907505));
#118607=CARTESIAN_POINT('Ctrl Pts',(-175.178454499562,4.68452526856802,
132.308760570411));
#118608=CARTESIAN_POINT('Ctrl Pts',(-175.186205690802,4.72280707581413,
132.177050089785));
#118609=CARTESIAN_POINT('Ctrl Pts',(-175.193953587579,4.7610726122708,132.045395589626));
#118610=CARTESIAN_POINT('Ctrl Pts',(-175.201701484356,4.79384870165117,
131.912071733273));
#118611=CARTESIAN_POINT('Ctrl Pts',(-175.209449381133,4.8209993415828,131.777576118346));
#118612=CARTESIAN_POINT('Ctrl Pts',(-175.217195657217,4.84814430218586,
131.643108637002));
#118613=CARTESIAN_POINT('Ctrl Pts',(-175.224941933301,4.86966607659167,
131.507470267607));
#118614=CARTESIAN_POINT('Ctrl Pts',(-175.232688209386,4.88547951922007,
131.371170047429));
#118615=CARTESIAN_POINT('Ctrl Pts',(-175.240434542651,4.90129307857973,
131.234868821113));
#118616=CARTESIAN_POINT('Ctrl Pts',(-175.248180875916,4.91139817702218,
131.097906122625));
#118617=CARTESIAN_POINT('Ctrl Pts',(-175.255927209182,4.91576145942318,
130.960796983382));
#118618=CARTESIAN_POINT('Ctrl Pts',(-175.263675277185,4.92012571895103,
130.823657139497));
#118619=CARTESIAN_POINT('Ctrl Pts',(-175.271423345188,4.91874559133168,
130.686371180292));
#118620=CARTESIAN_POINT('Ctrl Pts',(-175.279171413191,4.91163984765625,
130.54945461643));
#118621=CARTESIAN_POINT('Ctrl Pts',(-175.286927715933,4.90452655191191,
130.412392536015));
#118622=CARTESIAN_POINT('Ctrl Pts',(-175.294684018674,4.89167550445891,
130.275701026261));
#118623=CARTESIAN_POINT('Ctrl Pts',(-175.302440321416,4.87315748431916,
130.139891509538));
#118624=CARTESIAN_POINT('Ctrl Pts',(-175.310200763931,4.85462958055448,
130.004009507186));
#118625=CARTESIAN_POINT('Ctrl Pts',(-175.317961206445,4.83042874621755,
129.869010820509));
#118626=CARTESIAN_POINT('Ctrl Pts',(-175.325721648959,4.80067683356496,
129.735396164381));
#118627=CARTESIAN_POINT('Ctrl Pts',(-175.333494549224,4.77087716050093,
129.601567018145));
#118628=CARTESIAN_POINT('Ctrl Pts',(-175.34126744949,4.73550870286761,129.469126720205));
#118629=CARTESIAN_POINT('Ctrl Pts',(-175.349040349755,4.69474334634035,
129.338561185688));
#118630=CARTESIAN_POINT('Ctrl Pts',(-175.356530685517,4.65545991320492,
129.212742037227));
#118631=CARTESIAN_POINT('Ctrl Pts',(-175.364021021279,4.61116525414913,
129.088664003982));
#118632=CARTESIAN_POINT('Ctrl Pts',(-175.371511357041,4.56205451057522,
128.966742130219));
#118633=CARTESIAN_POINT('Ctrl Pts',(-175.37928569116,4.51108171823132,128.840197551553));
#118634=CARTESIAN_POINT('Ctrl Pts',(-175.387060025279,4.45475896195995,
128.715575006328));
#118635=CARTESIAN_POINT('Ctrl Pts',(-175.394834359398,4.39325155232275,
128.593359970684));
#118636=CARTESIAN_POINT('Ctrl Pts',(-175.402599112345,4.33181994507102,
128.471295554149));
#118637=CARTESIAN_POINT('Ctrl Pts',(-175.410363865292,4.26521657196787,
128.351633089548));
#118638=CARTESIAN_POINT('Ctrl Pts',(-175.41812861824,4.19365542608364,128.234839800414));
#118639=CARTESIAN_POINT('Ctrl Pts',(-175.425885659125,4.12216535573814,
128.11816251202));
#118640=CARTESIAN_POINT('Ctrl Pts',(-175.43364270001,4.0457275147886,128.004349059259));
#118641=CARTESIAN_POINT('Ctrl Pts',(-175.441399740895,3.96460242599515,
127.893843366923));
#118642=CARTESIAN_POINT('Ctrl Pts',(-175.449150932135,3.88353851426233,
127.783421007788));
#118643=CARTESIAN_POINT('Ctrl Pts',(-175.456902123375,3.79779462070068,
127.676301757994));
#118644=CARTESIAN_POINT('Ctrl Pts',(-175.464653314615,3.70767511501683,
127.572901457375));
#118645=CARTESIAN_POINT('Ctrl Pts',(-175.472401211392,3.61759391252703,
127.469545104642));
#118646=CARTESIAN_POINT('Ctrl Pts',(-175.480149108169,3.52314105315951,
127.369904851404));
#118647=CARTESIAN_POINT('Ctrl Pts',(-175.487897004946,3.4246616672819,127.274364083977));
#118648=CARTESIAN_POINT('Ctrl Pts',(-175.495643281031,3.32620288116857,
127.178843301619));
#118649=CARTESIAN_POINT('Ctrl Pts',(-175.503389557114,3.22371952428284,
127.087420571474));
#118650=CARTESIAN_POINT('Ctrl Pts',(-175.511135833199,3.11759384082915,
127.000442676006));
#118651=CARTESIAN_POINT('Ctrl Pts',(-175.518882166464,3.01146737397992,
126.913464138487));
#118652=CARTESIAN_POINT('Ctrl Pts',(-175.526628499729,2.90169882929591,
126.830930748944));
#118653=CARTESIAN_POINT('Ctrl Pts',(-175.534374832995,2.78870348803471,
126.753148957047));
#118654=CARTESIAN_POINT('Ctrl Pts',(-175.542122900998,2.67568284225044,
126.675349746458));
#118655=CARTESIAN_POINT('Ctrl Pts',(-175.549870969001,2.5594342839417,126.602304472565));
#118656=CARTESIAN_POINT('Ctrl Pts',(-175.557619037004,2.44040167306233,
126.534275988824));
#118657=CARTESIAN_POINT('Ctrl Pts',(-175.565375339746,2.32124255290746,
126.466175203601));
#118658=CARTESIAN_POINT('Ctrl Pts',(-175.573131642488,2.19929380939415,
126.403102053886));
#118659=CARTESIAN_POINT('Ctrl Pts',(-175.580887945229,2.07502397443618,
126.345273427567));
#118660=CARTESIAN_POINT('Ctrl Pts',(-175.588648387744,1.95068781292527,
126.287413936368));
#118661=CARTESIAN_POINT('Ctrl Pts',(-175.596408830258,1.82402845236486,
126.234804696024));
#118662=CARTESIAN_POINT('Ctrl Pts',(-175.604169272772,1.69553302248052,
126.187613837399));
#118663=CARTESIAN_POINT('Ctrl Pts',(-175.611942173037,1.56683132032519,
126.14034722382));
#118664=CARTESIAN_POINT('Ctrl Pts',(-175.619715073303,1.43628803149051,
126.098516492843));
#118665=CARTESIAN_POINT('Ctrl Pts',(-175.627487973568,1.30440487854117,
126.062239681177));
#118666=CARTESIAN_POINT('Ctrl Pts',(-175.63497830933,1.17731601039659,126.027281622992));
#118667=CARTESIAN_POINT('Ctrl Pts',(-175.642468645092,1.04898330177843,
125.997480766402));
#118668=CARTESIAN_POINT('Ctrl Pts',(-175.649958980854,0.91986141987662,
125.972897274983));
#118669=CARTESIAN_POINT('Ctrl Pts',(-175.657733314973,0.785843842575069,
125.947381693015));
#118670=CARTESIAN_POINT('Ctrl Pts',(-175.665507649092,0.650551540258417,
125.92740609324));
#118671=CARTESIAN_POINT('Ctrl Pts',(-175.673281983211,0.514482312150306,
125.913093806914));
#118672=CARTESIAN_POINT('Ctrl Pts',(-175.681046736158,0.378580777205721,
125.898799159202));
#118673=CARTESIAN_POINT('Ctrl Pts',(-175.688811489106,0.241904606680187,
125.890153978265));
#118674=CARTESIAN_POINT('Ctrl Pts',(-175.696576242053,0.10496255744539,
125.887230771402));
#118675=CARTESIAN_POINT('Ctrl Pts',(-175.704333282938,-0.0318434790163065,
125.88431046791));
#118676=CARTESIAN_POINT('Ctrl Pts',(-175.712090323823,-0.168914480320329,
125.887100837067));
#118677=CARTESIAN_POINT('Ctrl Pts',(-175.719847364708,-0.305736141050252,
125.895622645892));
#118678=CARTESIAN_POINT('Ctrl Pts',(-175.727598555948,-0.442454623501687,
125.904138028354));
#118679=CARTESIAN_POINT('Ctrl Pts',(-175.735349747188,-0.578923751010477,
125.918376223353));
#118680=CARTESIAN_POINT('Ctrl Pts',(-175.743100938428,-0.71462914648377,
125.938305927625));
#118681=CARTESIAN_POINT('Ctrl Pts',(-175.750848835205,-0.850276863543373,
125.958227161241));
#118682=CARTESIAN_POINT('Ctrl Pts',(-175.758596731982,-0.985161108178815,
125.983835036147));
#118683=CARTESIAN_POINT('Ctrl Pts',(-175.766344628759,-1.11877277522967,
126.01504641406));
#118684=CARTESIAN_POINT('Ctrl Pts',(-175.774090904844,-1.25235649360048,
126.046251263226));
#118685=CARTESIAN_POINT('Ctrl Pts',(-175.781837180928,-1.38466778339019,
126.083057195085));
#118686=CARTESIAN_POINT('Ctrl Pts',(-175.789583457012,-1.51520827435996,
126.125330061157));
#118687=CARTESIAN_POINT('Ctrl Pts',(-175.797329790277,-1.6457497289498,
126.167603239277));
#118688=CARTESIAN_POINT('Ctrl Pts',(-175.805076123543,-1.7745199866872,
126.215343311688));
#118689=CARTESIAN_POINT('Ctrl Pts',(-175.812822456808,-1.90103675312087,
126.26836653404));
#118690=CARTESIAN_POINT('Ctrl Pts',(-175.820570524811,-2.02758185210666,
126.321401630574));
#118691=CARTESIAN_POINT('Ctrl Pts',(-175.828318592814,-2.15187209507656,
126.379722080241));
#118692=CARTESIAN_POINT('Ctrl Pts',(-175.836066660817,-2.27344641882782,
126.443096529802));
#118693=CARTESIAN_POINT('Ctrl Pts',(-175.843822963559,-2.39514995321728,
126.506538334483));
#118694=CARTESIAN_POINT('Ctrl Pts',(-175.8515792663,-2.51413145502923,126.5750446881));
#118695=CARTESIAN_POINT('Ctrl Pts',(-175.859335569042,-2.62995519739772,
126.648338634686));
#118696=CARTESIAN_POINT('Ctrl Pts',(-175.867096011556,-2.7458407583849,
126.721671700458));
#118697=CARTESIAN_POINT('Ctrl Pts',(-175.874856454071,-2.85856488046691,
126.799797228219));
#118698=CARTESIAN_POINT('Ctrl Pts',(-175.882616896585,-2.96772280486939,
126.882396260773));
#118699=CARTESIAN_POINT('Ctrl Pts',(-175.89038979685,-3.07705595926301,
126.965127888626));
#118700=CARTESIAN_POINT('Ctrl Pts',(-175.898162697116,-3.18281117425422,
127.052347122836));
#118701=CARTESIAN_POINT('Ctrl Pts',(-175.905935597381,-3.28461794891542,
127.143695651721));
#118702=CARTESIAN_POINT('Ctrl Pts',(-175.913425933143,-3.3827237908819,
127.231723431489));
#118703=CARTESIAN_POINT('Ctrl Pts',(-175.920916268905,-3.47716305924487,
127.323585282909));
#118704=CARTESIAN_POINT('Ctrl Pts',(-175.928406604667,-3.56763937796251,
127.418931201478));
#118705=CARTESIAN_POINT('Ctrl Pts',(-175.936084722842,-3.66038393431042,
127.516667438349));
#118706=CARTESIAN_POINT('Ctrl Pts',(-175.943762841017,-3.74927406527692,
127.618391590541));
#118707=CARTESIAN_POINT('Ctrl Pts',(-175.951440959192,-3.83394075869912,
127.723763058441));
#118708=CARTESIAN_POINT('Ctrl Pts',(-175.959110001431,-3.91850737167146,
127.829009971768));
#118709=CARTESIAN_POINT('Ctrl Pts',(-175.966779043669,-3.99886022424331,
127.937895319341));
#118710=CARTESIAN_POINT('Ctrl Pts',(-175.974448085908,-4.07466664012404,
128.050041312482));
#118711=CARTESIAN_POINT('Ctrl Pts',(-175.982397140053,-4.15324089824724,
128.166281977736));
#118712=CARTESIAN_POINT('Ctrl Pts',(-175.990346194199,-4.22693008600737,
128.286025634363));
#118713=CARTESIAN_POINT('Ctrl Pts',(-175.998295248344,-4.29540845154183,
128.408812810295));
#118714=CARTESIAN_POINT('Ctrl Pts',(-176.005950776368,-4.36135819056651,
128.527065957038));
#118715=CARTESIAN_POINT('Ctrl Pts',(-176.013606304392,-4.42247486355655,
128.648141468741));
#118716=CARTESIAN_POINT('Ctrl Pts',(-176.021261832416,-4.47851132733826,
128.771599108337));
#118717=CARTESIAN_POINT('Ctrl Pts',(-176.02891400081,-4.53452319950553,
128.89500256852));
#118718=CARTESIAN_POINT('Ctrl Pts',(-176.036566169204,-4.58545913263066,
129.020785711845));
#118719=CARTESIAN_POINT('Ctrl Pts',(-176.044218337598,-4.63111848361476,
129.14848482113));
#118720=CARTESIAN_POINT('Ctrl Pts',(-176.051869221783,-4.67677017191847,
129.276162499593));
#118721=CARTESIAN_POINT('Ctrl Pts',(-176.059520105969,-4.71714690477684,
129.405755126607));
#118722=CARTESIAN_POINT('Ctrl Pts',(-176.067170990154,-4.75209680438599,
129.53678063025));
#118723=CARTESIAN_POINT('Ctrl Pts',(-176.068059571987,-4.75615592292799,
129.551998071709));
#118724=CARTESIAN_POINT('Ctrl Pts',(-176.06894815382,-4.76014189558664,
129.567234823998));
#118725=CARTESIAN_POINT('Ctrl Pts',(-176.069836735653,-4.76405452823418,
129.582490119309));
#118726=CARTESIAN_POINT('Origin',(213.235140564004,0.,130.804360617566));
#118727=CARTESIAN_POINT('',(-178.165366640417,-4.76405452823403,129.582490119308));
#118728=CARTESIAN_POINT('',(-177.819765072025,-4.76405452823413,129.582490119309));
#118729=CARTESIAN_POINT('',(213.235140564004,-4.76405452823405,129.582490119308));
#118730=CARTESIAN_POINT('',(-176.485140564046,-4.91824957167407,130.802308002684));
#118731=CARTESIAN_POINT('Ctrl Pts',(-176.485140564046,-4.91824957167407,
130.802308002684));
#118732=CARTESIAN_POINT('Ctrl Pts',(-176.492835531866,-4.91830597039888,
130.937444411655));
#118733=CARTESIAN_POINT('Ctrl Pts',(-176.500530499686,-4.91278854347934,
131.072808430149));
#118734=CARTESIAN_POINT('Ctrl Pts',(-176.508225467506,-4.9016672619306,
131.207896385272));
#118735=CARTESIAN_POINT('Ctrl Pts',(-176.515911379896,-4.89055906789569,
131.342825369014));
#118736=CARTESIAN_POINT('Ctrl Pts',(-176.523597292285,-4.87386016830611,
131.477478541179));
#118737=CARTESIAN_POINT('Ctrl Pts',(-176.531283204674,-4.85159252065345,
131.611350751359));
#118738=CARTESIAN_POINT('Ctrl Pts',(-176.538962001415,-4.82934548847746,
131.745099022115));
#118739=CARTESIAN_POINT('Ctrl Pts',(-176.546640798155,-4.80154002977729,
131.878067377553));
#118740=CARTESIAN_POINT('Ctrl Pts',(-176.554319594896,-4.76824998833037,
132.009754790145));
#118741=CARTESIAN_POINT('Ctrl Pts',(-176.562229631773,-4.73395744688536,
132.145407852077));
#118742=CARTESIAN_POINT('Ctrl Pts',(-176.57013966865,-4.69384480792713,
132.279701173914));
#118743=CARTESIAN_POINT('Ctrl Pts',(-176.578049705527,-4.64804985722182,
132.412096785997));
#118744=CARTESIAN_POINT('Ctrl Pts',(-176.585720891864,-4.60363772544528,
132.540494595797));
#118745=CARTESIAN_POINT('Ctrl Pts',(-176.593392078201,-4.55388164059911,
132.667107245745));
#118746=CARTESIAN_POINT('Ctrl Pts',(-176.601063264538,-4.49895804444373,
132.791458898184));
#118747=CARTESIAN_POINT('Ctrl Pts',(-176.608733614919,-4.44404043350099,
132.915796999597));
#118748=CARTESIAN_POINT('Ctrl Pts',(-176.6164039653,-4.3839565923831,133.037874228065));
#118749=CARTESIAN_POINT('Ctrl Pts',(-176.624074315681,-4.31893089974082,
133.157235230835));
#118750=CARTESIAN_POINT('Ctrl Pts',(-176.631745571775,-4.25389752888149,
133.27661032772));
#118751=CARTESIAN_POINT('Ctrl Pts',(-176.63941682787,-4.1839213372524,133.393268210303));
#118752=CARTESIAN_POINT('Ctrl Pts',(-176.647088083964,-4.10927214498694,
133.506779071643));
#118753=CARTESIAN_POINT('Ctrl Pts',(-176.654761987838,-4.03459718710628,
133.620329111935));
#118754=CARTESIAN_POINT('Ctrl Pts',(-176.662435891712,-3.95524624017119,
133.730729637202));
#118755=CARTESIAN_POINT('Ctrl Pts',(-176.670109795586,-3.87153152354035,
133.83758113786));
#118756=CARTESIAN_POINT('Ctrl Pts',(-176.677792143222,-3.78772469380698,
133.944550209522));
#118757=CARTESIAN_POINT('Ctrl Pts',(-176.685474490857,-3.6995447577288,
134.047962148294));
#118758=CARTESIAN_POINT('Ctrl Pts',(-176.693156838493,-3.60734334901101,
134.14745155633));
#118759=CARTESIAN_POINT('Ctrl Pts',(-176.700844268316,-3.51508094528171,
134.247006780688));
#118760=CARTESIAN_POINT('Ctrl Pts',(-176.70853169814,-3.41879205509594,
134.342634027913));
#118761=CARTESIAN_POINT('Ctrl Pts',(-176.716219127963,-3.31886305635952,
134.434006753986));
#118762=CARTESIAN_POINT('Ctrl Pts',(-176.723917236586,-3.21879524377401,
134.525506408178));
#118763=CARTESIAN_POINT('Ctrl Pts',(-176.731615345209,-3.11507753719144,
134.612739493057));
#118764=CARTESIAN_POINT('Ctrl Pts',(-176.739313453832,-3.00812722510926,
134.695421354699));
#118765=CARTESIAN_POINT('Ctrl Pts',(-176.740929129203,-2.98568054454804,
134.71277458444));
#118766=CARTESIAN_POINT('Ctrl Pts',(-176.742544804574,-2.96309156194695,
134.729927493467));
#118767=CARTESIAN_POINT('Ctrl Pts',(-176.744160479945,-2.94036427676275,
134.746877704712));
#118768=CARTESIAN_POINT('Ctrl Pts',(-176.751934814064,-2.83100474094054,
134.828439018296));
#118769=CARTESIAN_POINT('Ctrl Pts',(-176.759709148183,-2.71807583208517,
134.905575865503));
#118770=CARTESIAN_POINT('Ctrl Pts',(-176.767483482302,-2.6019712694565,
134.977959613088));
#118771=CARTESIAN_POINT('Ctrl Pts',(-176.77524823525,-2.48600979532471,
135.050254154173));
#118772=CARTESIAN_POINT('Ctrl Pts',(-176.783012988197,-2.36688078312081,
135.117807046001));
#118773=CARTESIAN_POINT('Ctrl Pts',(-176.790777741144,-2.24501003512077,
135.180330567726));
#118774=CARTESIAN_POINT('Ctrl Pts',(-176.798534782029,-2.12326033086506,
135.242791990209));
#118775=CARTESIAN_POINT('Ctrl Pts',(-176.806291822914,-1.99877465557294,
135.300233806037));
#118776=CARTESIAN_POINT('Ctrl Pts',(-176.814048863799,-1.87200643101424,
135.352412396596));
#118777=CARTESIAN_POINT('Ctrl Pts',(-176.821800055039,-1.7453338033603,
135.404551638875));
#118778=CARTESIAN_POINT('Ctrl Pts',(-176.829551246279,-1.61638241263376,
135.451435407808));
#118779=CARTESIAN_POINT('Ctrl Pts',(-176.837302437519,-1.48562851919162,
135.492866879209));
#118780=CARTESIAN_POINT('Ctrl Pts',(-176.845050334296,-1.354930199642,135.534280741129));
#118781=CARTESIAN_POINT('Ctrl Pts',(-176.852798231074,-1.22243127303657,
135.570246796745));
#118782=CARTESIAN_POINT('Ctrl Pts',(-176.860546127851,-1.08862593001943,
135.600617141876));
#118783=CARTESIAN_POINT('Ctrl Pts',(-176.868292403935,-0.954848576195554,
135.630981134187));
#118784=CARTESIAN_POINT('Ctrl Pts',(-176.876038680019,-0.819765730543298,
135.655751657723));
#118785=CARTESIAN_POINT('Ctrl Pts',(-176.883784956103,-0.683884240481451,
135.674831375934));
#118786=CARTESIAN_POINT('Ctrl Pts',(-176.891531289368,-0.548001747373497,
135.693911234988));
#118787=CARTESIAN_POINT('Ctrl Pts',(-176.899277622634,-0.411320985259188,
135.707300150528));
#118788=CARTESIAN_POINT('Ctrl Pts',(-176.907023955899,-0.274356036807478,
135.714952417702));
#118789=CARTESIAN_POINT('Ctrl Pts',(-176.914772023902,-0.137360416005398,
135.722606398549));
#118790=CARTESIAN_POINT('Ctrl Pts',(-176.922520091905,-8.08725082983852E-5,
135.724521152855));
#118791=CARTESIAN_POINT('Ctrl Pts',(-176.930268159908,0.13696678102096,
135.720703075471));
#118792=CARTESIAN_POINT('Ctrl Pts',(-176.93802446265,0.274160090427464,
135.716880940189));
#118793=CARTESIAN_POINT('Ctrl Pts',(-176.945780765392,0.411120626108149,
135.707313812855));
#118794=CARTESIAN_POINT('Ctrl Pts',(-176.953537068133,0.547335414469305,
135.692060179381));
#118795=CARTESIAN_POINT('Ctrl Pts',(-176.961297510648,0.683622904764729,
135.676798404584));
#118796=CARTESIAN_POINT('Ctrl Pts',(-176.969057953162,0.819163468450381,
135.655844135738));
#118797=CARTESIAN_POINT('Ctrl Pts',(-176.976818395676,0.953453610727624,
135.629307174233));
#118798=CARTESIAN_POINT('Ctrl Pts',(-176.984591295941,1.0879593274626,135.602727613241));
#118799=CARTESIAN_POINT('Ctrl Pts',(-176.992364196207,1.22121023133064,
135.570547542823));
#118800=CARTESIAN_POINT('Ctrl Pts',(-177.000137096472,1.3527164223535,135.532927138531));
#118801=CARTESIAN_POINT('Ctrl Pts',(-177.007627432234,1.47944203209141,
135.496674330695));
#118802=CARTESIAN_POINT('Ctrl Pts',(-177.015117767997,1.60454728361578,
135.455369958083));
#118803=CARTESIAN_POINT('Ctrl Pts',(-177.022608103759,1.72761256932774,
135.409199145984));
#118804=CARTESIAN_POINT('Ctrl Pts',(-177.030382437878,1.85534391274966,
135.361277753511));
#118805=CARTESIAN_POINT('Ctrl Pts',(-177.038156771997,1.98128216061258,
135.307961814266));
#118806=CARTESIAN_POINT('Ctrl Pts',(-177.045931106116,2.1049380095826,135.249404941115));
#118807=CARTESIAN_POINT('Ctrl Pts',(-177.053695859063,2.22844146377053,
135.190920234077));
#118808=CARTESIAN_POINT('Ctrl Pts',(-177.06146061201,2.34966776584726,135.127207610304));
#118809=CARTESIAN_POINT('Ctrl Pts',(-177.069225364957,2.46814469158579,
135.058469789167));
#118810=CARTESIAN_POINT('Ctrl Pts',(-177.076982405842,2.58650394437144,
134.989800239402));
#118811=CARTESIAN_POINT('Ctrl Pts',(-177.084739446727,2.70211891909105,
134.916115619711));
#118812=CARTESIAN_POINT('Ctrl Pts',(-177.092496487612,2.81453956696313,
134.837665724857));
#118813=CARTESIAN_POINT('Ctrl Pts',(-177.100247678852,2.92687543754998,
134.759274989679));
#118814=CARTESIAN_POINT('Ctrl Pts',(-177.107998870092,3.03602145667123,
134.676126354876));
#118815=CARTESIAN_POINT('Ctrl Pts',(-177.115750061333,3.14155460020808,
134.588514123492));
#118816=CARTESIAN_POINT('Ctrl Pts',(-177.12349795811,3.24704288934388,134.500939129644));
#118817=CARTESIAN_POINT('Ctrl Pts',(-177.131245854887,3.34892105684096,
134.408904561705));
#118818=CARTESIAN_POINT('Ctrl Pts',(-177.138993751664,3.44679754461108,
134.312746250441));
#118819=CARTESIAN_POINT('Ctrl Pts',(-177.146740027748,3.54465355872992,
134.216608053422));
#118820=CARTESIAN_POINT('Ctrl Pts',(-177.154486303832,3.63850927937571,
134.116348102655));
#118821=CARTESIAN_POINT('Ctrl Pts',(-177.162232579916,3.7280088511409,134.012340210443));
#118822=CARTESIAN_POINT('Ctrl Pts',(-177.169978913182,3.81750908357147,
133.908331550469));
#118823=CARTESIAN_POINT('Ctrl Pts',(-177.177725246447,3.90265284794519,
133.800575190193));
#118824=CARTESIAN_POINT('Ctrl Pts',(-177.185471579712,3.9831238172353,133.689478937336));
#118825=CARTESIAN_POINT('Ctrl Pts',(-177.193219647715,4.06361280744114,
133.578357805243));
#118826=CARTESIAN_POINT('Ctrl Pts',(-177.200967715718,4.13942669096672,
133.463895608813));
#118827=CARTESIAN_POINT('Ctrl Pts',(-177.208715783721,4.2102920386376,133.346529772419));
#118828=CARTESIAN_POINT('Ctrl Pts',(-177.216472086463,4.2812327028432,133.229039198217));
#118829=CARTESIAN_POINT('Ctrl Pts',(-177.224228389205,4.34721412264418,
133.108639154611));
#118830=CARTESIAN_POINT('Ctrl Pts',(-177.231984691947,4.40800822913771,
132.985792833876));
#118831=CARTESIAN_POINT('Ctrl Pts',(-177.239745134461,4.46883478327634,
132.862880946361));
#118832=CARTESIAN_POINT('Ctrl Pts',(-177.247505576975,4.52446834887442,
132.737520537276));
#118833=CARTESIAN_POINT('Ctrl Pts',(-177.255266019489,4.57472915371374,
132.610194561389));
#118834=CARTESIAN_POINT('Ctrl Pts',(-177.263038919755,4.62507064165893,
132.482664190541));
#118835=CARTESIAN_POINT('Ctrl Pts',(-177.27081182002,4.6700220054038,132.353162317152));
#118836=CARTESIAN_POINT('Ctrl Pts',(-177.278584720286,4.70945320227301,
132.222187686746));
#118837=CARTESIAN_POINT('Ctrl Pts',(-177.286075056047,4.74745097581429,
132.095974314063));
#118838=CARTESIAN_POINT('Ctrl Pts',(-177.293565391809,4.78032288164842,
131.968393700483));
#118839=CARTESIAN_POINT('Ctrl Pts',(-177.301055727571,4.80799786276686,
131.839898938503));
#118840=CARTESIAN_POINT('Ctrl Pts',(-177.30883006169,4.83672214920632,131.706532258567));
#118841=CARTESIAN_POINT('Ctrl Pts',(-177.316604395809,4.8599386387158,131.571758276407));
#118842=CARTESIAN_POINT('Ctrl Pts',(-177.324378729928,4.8775120897474,131.436071688284));
#118843=CARTESIAN_POINT('Ctrl Pts',(-177.332143482875,4.89506388307123,
131.300552321754));
#118844=CARTESIAN_POINT('Ctrl Pts',(-177.339908235822,4.9069864256457,131.164122971094));
#118845=CARTESIAN_POINT('Ctrl Pts',(-177.34767298877,4.91319502228795,131.02729050669));
#118846=CARTESIAN_POINT('Ctrl Pts',(-177.355430029654,4.91939745246448,
130.890593946219));
#118847=CARTESIAN_POINT('Ctrl Pts',(-177.363187070539,4.91989721294986,
130.753495456812));
#118848=CARTESIAN_POINT('Ctrl Pts',(-177.370944111424,4.91466120079501,
130.616508697426));
#118849=CARTESIAN_POINT('Ctrl Pts',(-177.378695302665,4.90942913715766,
130.479625240822));
#118850=CARTESIAN_POINT('Ctrl Pts',(-177.386446493905,4.89846992518054,
130.34285373563));
#118851=CARTESIAN_POINT('Ctrl Pts',(-177.394197685145,4.88180251548238,
130.206709162009));
#118852=CARTESIAN_POINT('Ctrl Pts',(-177.401945581922,4.8651421898779,130.070622453462));
#118853=CARTESIAN_POINT('Ctrl Pts',(-177.409693478699,4.84277853936195,
129.935162533768));
#118854=CARTESIAN_POINT('Ctrl Pts',(-177.417441375476,4.81478246115655,
129.800840356565));
#118855=CARTESIAN_POINT('Ctrl Pts',(-177.42518765156,4.7867922391272,129.666546276666));
#118856=CARTESIAN_POINT('Ctrl Pts',(-177.432933927644,4.75317201259992,
129.53338984838));
#118857=CARTESIAN_POINT('Ctrl Pts',(-177.440680203728,4.71404393191347,
129.40187251762));
#118858=CARTESIAN_POINT('Ctrl Pts',(-177.448426536994,4.67491556239246,
129.270354216029));
#118859=CARTESIAN_POINT('Ctrl Pts',(-177.456172870259,4.63027936907037,
129.140475410841));
#118860=CARTESIAN_POINT('Ctrl Pts',(-177.463919203524,4.58030746964681,
129.012722666975));
#118861=CARTESIAN_POINT('Ctrl Pts',(-177.471667271527,4.53032437936306,
128.884941313769));
#118862=CARTESIAN_POINT('Ctrl Pts',(-177.47941533953,4.47500334767135,128.759287333333));
#118863=CARTESIAN_POINT('Ctrl Pts',(-177.487163407533,4.41456459693924,
128.636227207937));
#118864=CARTESIAN_POINT('Ctrl Pts',(-177.494919710275,4.35406161118338,
128.513036292774));
#118865=CARTESIAN_POINT('Ctrl Pts',(-177.502676013017,4.28843021367941,
128.392445091101));
#118866=CARTESIAN_POINT('Ctrl Pts',(-177.510432315759,4.2179368243953,128.274895850484));
#118867=CARTESIAN_POINT('Ctrl Pts',(-177.518192758273,4.14740581066662,
128.157283870298));
#118868=CARTESIAN_POINT('Ctrl Pts',(-177.525953200787,4.07200784924379,
128.042717412727));
#118869=CARTESIAN_POINT('Ctrl Pts',(-177.533713643301,3.99205209237518,
127.931608774078));
#118870=CARTESIAN_POINT('Ctrl Pts',(-177.541486543566,3.91196798342773,
127.820321773979));
#118871=CARTESIAN_POINT('Ctrl Pts',(-177.549259443832,3.82731169976449,
127.712503992746));
#118872=CARTESIAN_POINT('Ctrl Pts',(-177.557032344097,3.73843255887875,
127.608534423103));
#118873=CARTESIAN_POINT('Ctrl Pts',(-177.56452267986,3.65278439863484,127.508344409197));
#118874=CARTESIAN_POINT('Ctrl Pts',(-177.572013015622,3.56321528320005,
127.411727905865));
#118875=CARTESIAN_POINT('Ctrl Pts',(-177.579503351384,3.4700680040757,127.318989602941));
#118876=CARTESIAN_POINT('Ctrl Pts',(-177.587277685503,3.37338901755469,
127.222735099077));
#118877=CARTESIAN_POINT('Ctrl Pts',(-177.595052019622,3.27254892904052,
127.130353779533));
#118878=CARTESIAN_POINT('Ctrl Pts',(-177.602826353741,3.16789083914688,
127.042226822265));
#118879=CARTESIAN_POINT('Ctrl Pts',(-177.610591106688,3.06336173099519,
126.954208473595));
#118880=CARTESIAN_POINT('Ctrl Pts',(-177.618355859635,2.95502427989044,
126.870434304359));
#118881=CARTESIAN_POINT('Ctrl Pts',(-177.626120612582,2.84325915042936,
126.791249546838));
#118882=CARTESIAN_POINT('Ctrl Pts',(-177.633877653467,2.73160502767108,
126.712143436735));
#118883=CARTESIAN_POINT('Ctrl Pts',(-177.641634694352,2.61653031845178,
126.637617891744));
#118884=CARTESIAN_POINT('Ctrl Pts',(-177.649391735237,2.49844928564784,
126.567978407526));
#118885=CARTESIAN_POINT('Ctrl Pts',(-177.657142926478,2.38045729866815,
126.498391438984));
#118886=CARTESIAN_POINT('Ctrl Pts',(-177.664894117718,2.25946383601194,
126.433683395015));
#118887=CARTESIAN_POINT('Ctrl Pts',(-177.672645308958,2.13591240834263,
126.374116691281));
#118888=CARTESIAN_POINT('Ctrl Pts',(-177.680393205735,2.01241349332643,
126.314575304985));
#118889=CARTESIAN_POINT('Ctrl Pts',(-177.688141102512,1.88635912709672,
126.260171082148));
#118890=CARTESIAN_POINT('Ctrl Pts',(-177.695888999289,1.75821751110227,
126.211120557853));
#118891=CARTESIAN_POINT('Ctrl Pts',(-177.703635275373,1.63010269957183,
126.16208029387));
#118892=CARTESIAN_POINT('Ctrl Pts',(-177.711381551457,1.49990187161117,
126.118391640607));
#118893=CARTESIAN_POINT('Ctrl Pts',(-177.719127827541,1.36810293311139,
126.080222873288));
#118894=CARTESIAN_POINT('Ctrl Pts',(-177.726874160807,1.23630302170124,
126.042053824216));
#118895=CARTESIAN_POINT('Ctrl Pts',(-177.734620494072,1.10290535174681,
126.00940485115));
#118896=CARTESIAN_POINT('Ctrl Pts',(-177.742366827337,0.968412317916519,
125.982394146819));
#118897=CARTESIAN_POINT('Ctrl Pts',(-177.75011489534,0.833889165303631,
125.955377393628));
#118898=CARTESIAN_POINT('Ctrl Pts',(-177.757862963343,0.698270543936001,
125.934001498669));
#118899=CARTESIAN_POINT('Ctrl Pts',(-177.765611031346,0.562067954125812,
125.918333327687));
#118900=CARTESIAN_POINT('Ctrl Pts',(-177.773367334088,0.425720606582898,
125.902648504386));
#118901=CARTESIAN_POINT('Ctrl Pts',(-177.78112363683,0.288788439808046,
125.892683567776));
#118902=CARTESIAN_POINT('Ctrl Pts',(-177.788879939572,0.151787535704795,
125.888453416804));
#118903=CARTESIAN_POINT('Ctrl Pts',(-177.796640382086,0.0147135100936332,
125.884221008073));
#118904=CARTESIAN_POINT('Ctrl Pts',(-177.8044008246,-0.122428935197982,
125.885729479641));
#118905=CARTESIAN_POINT('Ctrl Pts',(-177.812161267115,-0.259125819268372,
125.892941589191));
#118906=CARTESIAN_POINT('Ctrl Pts',(-177.81993416738,-0.396042141312451,
125.900165276259));
#118907=CARTESIAN_POINT('Ctrl Pts',(-177.827707067645,-0.532511083387111,
125.913110860943));
#118908=CARTESIAN_POINT('Ctrl Pts',(-177.835479967911,-0.668024973541733,
125.931689307368));
#118909=CARTESIAN_POINT('Ctrl Pts',(-177.842970303673,-0.798612592451449,
125.94959238047));
#118910=CARTESIAN_POINT('Ctrl Pts',(-177.850460639435,-0.928313087764289,
125.972725833973));
#118911=CARTESIAN_POINT('Ctrl Pts',(-177.857950975197,-1.05668482811248,
126.000965959979));
#118912=CARTESIAN_POINT('Ctrl Pts',(-177.865725309316,-1.18992382201241,
126.030276818945));
#118913=CARTESIAN_POINT('Ctrl Pts',(-177.873499643435,-1.32215337351811,
126.065182081599));
#118914=CARTESIAN_POINT('Ctrl Pts',(-177.881273977554,-1.45286733255685,
126.105599123673));
#118915=CARTESIAN_POINT('Ctrl Pts',(-177.889038730501,-1.58342019832367,
126.145966355356));
#118916=CARTESIAN_POINT('Ctrl Pts',(-177.896803483448,-1.71246081812129,
126.191831736476));
#118917=CARTESIAN_POINT('Ctrl Pts',(-177.904568236396,-1.83949297974126,
126.24306160961));
#118918=CARTESIAN_POINT('Ctrl Pts',(-177.912325277281,-1.96639897122747,
126.294240600511));
#118919=CARTESIAN_POINT('Ctrl Pts',(-177.920082318166,-2.09130011409183,
126.350773335007));
#118920=CARTESIAN_POINT('Ctrl Pts',(-177.927839359051,-2.21371546697803,
126.412476409875));
#118921=CARTESIAN_POINT('Ctrl Pts',(-177.935590550291,-2.33603850549387,
126.474132953975));
#118922=CARTESIAN_POINT('Ctrl Pts',(-177.943341741531,-2.45587913750643,
126.540951902473));
#118923=CARTESIAN_POINT('Ctrl Pts',(-177.951092932771,-2.5727768569406,
126.612701959363));
#118924=CARTESIAN_POINT('Ctrl Pts',(-177.958840829548,-2.68962489172614,
126.684421520565));
#118925=CARTESIAN_POINT('Ctrl Pts',(-177.966588726325,-2.80353216920274,
126.761067817579));
#118926=CARTESIAN_POINT('Ctrl Pts',(-177.974336623102,-2.9140634379534,
126.842363981767));
#118927=CARTESIAN_POINT('Ctrl Pts',(-177.982082899186,-3.02457158594541,
126.92364314055));
#118928=CARTESIAN_POINT('Ctrl Pts',(-177.989829175271,-3.13170481510814,
127.009570000349));
#118929=CARTESIAN_POINT('Ctrl Pts',(-177.997575451355,-3.23505782567653,
127.09982502899));
#118930=CARTESIAN_POINT('Ctrl Pts',(-178.00532178462,-3.33841159917322,
127.190080723872));
#118931=CARTESIAN_POINT('Ctrl Pts',(-178.013068117885,-3.43798480391004,
127.284664394185));
#118932=CARTESIAN_POINT('Ctrl Pts',(-178.020814451151,-3.53340644440668,
127.383217247123));
#118933=CARTESIAN_POINT('Ctrl Pts',(-178.028562519154,-3.62884945391797,
127.481792170289));
#118934=CARTESIAN_POINT('Ctrl Pts',(-178.036310587157,-3.72013877726179,
127.584337764003));
#118935=CARTESIAN_POINT('Ctrl Pts',(-178.04405865516,-3.80694167998,127.690459831136));
#118936=CARTESIAN_POINT('Ctrl Pts',(-178.051814957901,-3.89383683785631,
127.796694686064));
#118937=CARTESIAN_POINT('Ctrl Pts',(-178.059571260643,-3.97623580214425,
127.906513304447));
#118938=CARTESIAN_POINT('Ctrl Pts',(-178.067327563385,-4.05384708306206,
128.019489545209));
#118939=CARTESIAN_POINT('Ctrl Pts',(-178.075088005899,-4.13149978745754,
128.132526084793));
#118940=CARTESIAN_POINT('Ctrl Pts',(-178.082848448413,-4.2043595091759,
128.248723273822));
#118941=CARTESIAN_POINT('Ctrl Pts',(-178.090608890927,-4.2721797620015,
128.367628555224));
#118942=CARTESIAN_POINT('Ctrl Pts',(-178.098381791193,-4.34010888591755,
128.48672471394));
#118943=CARTESIAN_POINT('Ctrl Pts',(-178.106154691458,-4.40298219551518,
128.608537304644));
#118944=CARTESIAN_POINT('Ctrl Pts',(-178.113927591724,-4.46060019010785,
128.73259108248));
#118945=CARTESIAN_POINT('Ctrl Pts',(-178.121417927486,-4.51612362546549,
128.852135193018));
#118946=CARTESIAN_POINT('Ctrl Pts',(-178.128908263248,-4.56676708168597,
128.973760089716));
#118947=CARTESIAN_POINT('Ctrl Pts',(-178.13639859901,-4.61239592518718,
129.097027348454));
#118948=CARTESIAN_POINT('Ctrl Pts',(-178.145370171086,-4.66704800905346,
129.244671076535));
#118949=CARTESIAN_POINT('Ctrl Pts',(-178.154341743163,-4.71465032755617,
129.395057764512));
#118950=CARTESIAN_POINT('Ctrl Pts',(-178.163313315239,-4.75495695955518,
129.547552209225));
#118951=CARTESIAN_POINT('Ctrl Pts',(-178.163997756965,-4.75803195472055,
129.559186018774));
#118952=CARTESIAN_POINT('Ctrl Pts',(-178.164682198691,-4.7610645102698,
129.570832084646));
#118953=CARTESIAN_POINT('Ctrl Pts',(-178.165366640417,-4.76405452823403,
129.582490119308));
#118954=CARTESIAN_POINT('Ctrl Pts',(-176.415048843504,-4.76405452823412,
129.582490119309));
#118955=CARTESIAN_POINT('Ctrl Pts',(-176.422813628312,-4.79809583181618,
129.715216645326));
#118956=CARTESIAN_POINT('Ctrl Pts',(-176.430578413119,-4.82655219102321,
129.849233699315));
#118957=CARTESIAN_POINT('Ctrl Pts',(-176.438343197927,-4.84935493139779,
129.984031530048));
#118958=CARTESIAN_POINT('Ctrl Pts',(-176.446118737036,-4.87218925378811,
130.119016057079));
#118959=CARTESIAN_POINT('Ctrl Pts',(-176.453894276145,-4.88935428061385,
130.254783133149));
#118960=CARTESIAN_POINT('Ctrl Pts',(-176.461669815255,-4.90083326745112,
130.390819389701));
#118961=CARTESIAN_POINT('Ctrl Pts',(-176.463017495547,-4.90282284066517,
130.41439761102));
#118962=CARTESIAN_POINT('Ctrl Pts',(-176.464365175839,-4.90464172672215,
130.437983923485));
#118963=CARTESIAN_POINT('Ctrl Pts',(-176.465712856132,-4.90628999728232,
130.461575663014));
#118964=CARTESIAN_POINT('Ctrl Pts',(-176.472188758758,-4.9142103027958,
130.574939202458));
#118965=CARTESIAN_POINT('Ctrl Pts',(-176.478664661385,-4.91820210782924,
130.688580401629));
#118966=CARTESIAN_POINT('Ctrl Pts',(-176.485140564012,-4.91824957167382,
130.802308002086));
#118967=CARTESIAN_POINT('',(-176.139859436039,-4.91824789567076,130.808910258228));
#118968=CARTESIAN_POINT('Ctrl Pts',(-176.069836735653,-4.76405452823418,
129.582490119309));
#118969=CARTESIAN_POINT('Ctrl Pts',(-176.077489986718,-4.79775357413248,
129.713882187812));
#118970=CARTESIAN_POINT('Ctrl Pts',(-176.085143237783,-4.82600791653814,
129.846650616237));
#118971=CARTESIAN_POINT('Ctrl Pts',(-176.092796488848,-4.84872203235654,
129.980298899343));
#118972=CARTESIAN_POINT('Ctrl Pts',(-176.100640313373,-4.87200175194107,
130.117275155806));
#118973=CARTESIAN_POINT('Ctrl Pts',(-176.108484137897,-4.88946162133592,
130.255175223402));
#118974=CARTESIAN_POINT('Ctrl Pts',(-176.116327962421,-4.90105518591459,
130.393457798009));
#118975=CARTESIAN_POINT('Ctrl Pts',(-176.124171786946,-4.91264875049327,
130.531740372616));
#118976=CARTESIAN_POINT('Ctrl Pts',(-176.13201561147,-4.91837602037099,
130.670405001707));
#118977=CARTESIAN_POINT('Ctrl Pts',(-176.139859435994,-4.91824789567149,
130.808910257436));
#118978=CARTESIAN_POINT('Ctrl Pts',(-176.139859436039,-4.91824789567076,
130.808910258228));
#118979=CARTESIAN_POINT('Ctrl Pts',(-176.149963599637,-4.91808284950663,
130.987328293797));
#118980=CARTESIAN_POINT('Ctrl Pts',(-176.160067763234,-4.9082057749942,
131.165313191804));
#118981=CARTESIAN_POINT('Ctrl Pts',(-176.170171926832,-4.88877810967605,
131.341977262446));
#118982=CARTESIAN_POINT('Ctrl Pts',(-176.180533275005,-4.8688559456477,
131.523138021375));
#118983=CARTESIAN_POINT('Ctrl Pts',(-176.190894623179,-4.8388907778309,
131.702910210726));
#118984=CARTESIAN_POINT('Ctrl Pts',(-176.201255971352,-4.7991043982783,
131.880362493459));
#118985=CARTESIAN_POINT('Ctrl Pts',(-176.203122057061,-4.79193884481255,
131.91232176781));
#118986=CARTESIAN_POINT('Ctrl Pts',(-176.204988142771,-4.78445485148977,
131.944205850854));
#118987=CARTESIAN_POINT('Ctrl Pts',(-176.20685422848,-4.77665387632276,
131.976009373939));
#118988=CARTESIAN_POINT('Ctrl Pts',(-176.214628562599,-4.74415408968602,
132.108506618505));
#118989=CARTESIAN_POINT('Ctrl Pts',(-176.222402896718,-4.70608573424566,
132.239860461107));
#118990=CARTESIAN_POINT('Ctrl Pts',(-176.230177230837,-4.66254355668122,
132.369566880188));
#118991=CARTESIAN_POINT('Ctrl Pts',(-176.237941983785,-4.61905504095927,
132.499113447699));
#118992=CARTESIAN_POINT('Ctrl Pts',(-176.245706736732,-4.57010624886383,
132.627016264303));
#118993=CARTESIAN_POINT('Ctrl Pts',(-176.253471489679,-4.51584270705513,
132.7527824681));
#118994=CARTESIAN_POINT('Ctrl Pts',(-176.261228530564,-4.46163306056114,
132.87842375913));
#118995=CARTESIAN_POINT('Ctrl Pts',(-176.268985571449,-4.40211932305708,
133.0019323038));
#118996=CARTESIAN_POINT('Ctrl Pts',(-176.276742612334,-4.33749638621665,
133.122831700426));
#118997=CARTESIAN_POINT('Ctrl Pts',(-176.284493803574,-4.27292218203551,
133.243639925876));
#118998=CARTESIAN_POINT('Ctrl Pts',(-176.292244994814,-4.20324663101173,
133.361842576224));
#118999=CARTESIAN_POINT('Ctrl Pts',(-176.299996186054,-4.12871201342084,
133.476984828475));
#119000=CARTESIAN_POINT('Ctrl Pts',(-176.307744082831,-4.05420907503059,
133.592078142196));
#119001=CARTESIAN_POINT('Ctrl Pts',(-176.315491979608,-3.97485138967346,
133.7041133174));
#119002=CARTESIAN_POINT('Ctrl Pts',(-176.323239876385,-3.89092619108978,
133.812661872093));
#119003=CARTESIAN_POINT('Ctrl Pts',(-176.330986152469,-3.80701854784865,
133.921187720769));
#119004=CARTESIAN_POINT('Ctrl Pts',(-176.338732428553,-3.71854553076091,
134.026228090499));
#119005=CARTESIAN_POINT('Ctrl Pts',(-176.346478704637,-3.62583630606058,
134.127385466127));
#119006=CARTESIAN_POINT('Ctrl Pts',(-176.354225037903,-3.53312639700193,
134.228543588475));
#119007=CARTESIAN_POINT('Ctrl Pts',(-176.361971371168,-3.43618048208862,
134.325818371297));
#119008=CARTESIAN_POINT('Ctrl Pts',(-176.369717704433,-3.33536615367179,
134.418847535988));
#119009=CARTESIAN_POINT('Ctrl Pts',(-176.377465772436,-3.23452924858498,
134.511897533915));
#119010=CARTESIAN_POINT('Ctrl Pts',(-176.385213840439,-3.12982249341971,
134.600699756689));
#119011=CARTESIAN_POINT('Ctrl Pts',(-176.392961908442,-3.02164795649696,
134.684931025315));
#119012=CARTESIAN_POINT('Ctrl Pts',(-176.400718211184,-2.91335845038894,
134.769251815936));
#119013=CARTESIAN_POINT('Ctrl Pts',(-176.408474513926,-2.80159410911006,
134.84899170732));
#119014=CARTESIAN_POINT('Ctrl Pts',(-176.416230816668,-2.68678794596961,
134.923869519837));
#119015=CARTESIAN_POINT('Ctrl Pts',(-176.423991259182,-2.57192050732314,
134.998787296898));
#119016=CARTESIAN_POINT('Ctrl Pts',(-176.431751701696,-2.45400834778893,
135.06883762467));
#119017=CARTESIAN_POINT('Ctrl Pts',(-176.43951214421,-2.33350980910276,
135.133784948042));
#119018=CARTESIAN_POINT('Ctrl Pts',(-176.447285044476,-2.21281783546493,
135.198836530624));
#119019=CARTESIAN_POINT('Ctrl Pts',(-176.455057944741,-2.08953153770764,
135.258768567959));
#119020=CARTESIAN_POINT('Ctrl Pts',(-176.462830845006,-1.96413081129394,
135.313393021378));
#119021=CARTESIAN_POINT('Ctrl Pts',(-176.470321180768,-1.84328871715109,
135.366031738325));
#119022=CARTESIAN_POINT('Ctrl Pts',(-176.47781151653,-1.72048354210743,
135.413741948317));
#119023=CARTESIAN_POINT('Ctrl Pts',(-176.485301852292,-1.59615681486123,
135.456399577514));
#119024=CARTESIAN_POINT('Ctrl Pts',(-176.493076186411,-1.46711620196301,
135.500674583687));
#119025=CARTESIAN_POINT('Ctrl Pts',(-176.50085052053,-1.33602761806071,
135.539646558526));
#119026=CARTESIAN_POINT('Ctrl Pts',(-176.508624854649,-1.20336632366152,
135.573122779131));
#119027=CARTESIAN_POINT('Ctrl Pts',(-176.516389607596,-1.0708685224514,
135.606557743286));
#119028=CARTESIAN_POINT('Ctrl Pts',(-176.524154360544,-0.936802242677544,
135.63451033477));
#119029=CARTESIAN_POINT('Ctrl Pts',(-176.531919113491,-0.801660803731147,
135.656836585385));
#119030=CARTESIAN_POINT('Ctrl Pts',(-176.539676154376,-0.666653589167438,
135.679140661254));
#119031=CARTESIAN_POINT('Ctrl Pts',(-176.547433195261,-0.5305737237678,
135.695829453633));
#119032=CARTESIAN_POINT('Ctrl Pts',(-176.555190236145,-0.393927361472714,
135.706809423661));
#119033=CARTESIAN_POINT('Ctrl Pts',(-176.562941427386,-0.257384045261832,
135.717781113608));
#119034=CARTESIAN_POINT('Ctrl Pts',(-176.570692618626,-0.12027547060289,
135.723052518991));
#119035=CARTESIAN_POINT('Ctrl Pts',(-176.578443809866,0.0168847486307748,
135.722581634129));
#119036=CARTESIAN_POINT('Ctrl Pts',(-176.586191706643,0.15398667111221,
135.722110949406));
#119037=CARTESIAN_POINT('Ctrl Pts',(-176.59393960342,0.291139804366465,
135.715902829998));
#119038=CARTESIAN_POINT('Ctrl Pts',(-176.601687500197,0.427828397506153,
135.703967328802));
#119039=CARTESIAN_POINT('Ctrl Pts',(-176.609433776281,0.564488398338821,
135.692034324256));
#119040=CARTESIAN_POINT('Ctrl Pts',(-176.617180052365,0.700683663100474,
135.674376354887));
#119041=CARTESIAN_POINT('Ctrl Pts',(-176.624926328449,0.835901828640993,
135.651055490918));
#119042=CARTESIAN_POINT('Ctrl Pts',(-176.632672661715,0.97112099233111,
135.627734454799));
#119043=CARTESIAN_POINT('Ctrl Pts',(-176.64041899498,1.10536265713054,135.598750507116));
#119044=CARTESIAN_POINT('Ctrl Pts',(-176.648165328245,1.23812333514411,
135.564217093288));
#119045=CARTESIAN_POINT('Ctrl Pts',(-176.655913396248,1.37091374399085,
135.529675945941));
#119046=CARTESIAN_POINT('Ctrl Pts',(-176.663661464251,1.5022221277916,135.489582957896));
#119047=CARTESIAN_POINT('Ctrl Pts',(-176.671409532254,1.63155925915677,
135.444101714476));
#119048=CARTESIAN_POINT('Ctrl Pts',(-176.679165834996,1.76103385156445,
135.39857213305));
#119049=CARTESIAN_POINT('Ctrl Pts',(-176.686922137738,1.88853263699357,
135.34764298645));
#119050=CARTESIAN_POINT('Ctrl Pts',(-176.69467844048,2.01358499678816,135.291526596579));
#119051=CARTESIAN_POINT('Ctrl Pts',(-176.702438882994,2.13870410079277,
135.2353802557));
#119052=CARTESIAN_POINT('Ctrl Pts',(-176.710199325508,2.26137382786905,
135.174041329674));
#119053=CARTESIAN_POINT('Ctrl Pts',(-176.717959768022,2.38114825392634,
135.107768111091));
#119054=CARTESIAN_POINT('Ctrl Pts',(-176.725732668288,2.50111495252507,
135.041388504854));
#119055=CARTESIAN_POINT('Ctrl Pts',(-176.733505568553,2.61817672827134,
134.970058981002));
#119056=CARTESIAN_POINT('Ctrl Pts',(-176.741278468819,2.73191598368738,
134.894081649687));
#119057=CARTESIAN_POINT('Ctrl Pts',(-176.748768804581,2.84152053067899,
134.820866285739));
#119058=CARTESIAN_POINT('Ctrl Pts',(-176.756259140343,2.94803967836508,
134.743335347838));
#119059=CARTESIAN_POINT('Ctrl Pts',(-176.763749476105,3.05113038286288,
134.66179324164));
#119060=CARTESIAN_POINT('Ctrl Pts',(-176.771523810224,3.15812980275411,
134.577159441702));
#119061=CARTESIAN_POINT('Ctrl Pts',(-176.779298144343,3.26177461054604,
134.487936207787));
#119062=CARTESIAN_POINT('Ctrl Pts',(-176.787072478462,3.3616457730922,134.394419218585));
#119063=CARTESIAN_POINT('Ctrl Pts',(-176.794837231409,3.461393853356,134.301017480714));
#119064=CARTESIAN_POINT('Ctrl Pts',(-176.802601984356,3.55737725919811,
134.203332781063));
#119065=CARTESIAN_POINT('Ctrl Pts',(-176.810366737304,3.64920821491691,
134.10170234488));
#119066=CARTESIAN_POINT('Ctrl Pts',(-176.818123778189,3.7409479628359,134.000172849478));
#119067=CARTESIAN_POINT('Ctrl Pts',(-176.825880819074,3.82854320770035,
133.894705704663));
#119068=CARTESIAN_POINT('Ctrl Pts',(-176.833637859959,3.91164166404732,
133.785676192038));
#119069=CARTESIAN_POINT('Ctrl Pts',(-176.841389051199,3.99467745520205,
133.676728899417));
#119070=CARTESIAN_POINT('Ctrl Pts',(-176.849140242439,4.0732229715109,133.56422489581));
#119071=CARTESIAN_POINT('Ctrl Pts',(-176.856891433679,4.14696525156086,
133.44857359402));
#119072=CARTESIAN_POINT('Ctrl Pts',(-176.864639330456,4.22067618917455,
133.332971447118));
#119073=CARTESIAN_POINT('Ctrl Pts',(-176.872387227233,4.28958774116858,
133.21422499155));
#119074=CARTESIAN_POINT('Ctrl Pts',(-176.88013512401,4.35342958937816,133.092773576983));
#119075=CARTESIAN_POINT('Ctrl Pts',(-176.887881400094,4.41725808324937,
132.971347567433));
#119076=CARTESIAN_POINT('Ctrl Pts',(-176.895627676178,4.47601880087756,
132.847218070175));
#119077=CARTESIAN_POINT('Ctrl Pts',(-176.903373952263,4.52948701890115,
132.720849701309));
#119078=CARTESIAN_POINT('Ctrl Pts',(-176.911120285528,4.58295563161505,
132.59448039962));
#119079=CARTESIAN_POINT('Ctrl Pts',(-176.918866618793,4.63113151441993,
132.465872553408));
#119080=CARTESIAN_POINT('Ctrl Pts',(-176.926612952059,4.67383796465551,
132.335511081317));
#119081=CARTESIAN_POINT('Ctrl Pts',(-176.934361020062,4.71655397870447,
132.205120415679));
#119082=CARTESIAN_POINT('Ctrl Pts',(-176.942109088065,4.75379800119929,
132.072975714176));
#119083=CARTESIAN_POINT('Ctrl Pts',(-176.949857156068,4.78544322175271,
131.939576999531));
#119084=CARTESIAN_POINT('Ctrl Pts',(-176.957613458809,4.81712207522315,
131.806036507144));
#119085=CARTESIAN_POINT('Ctrl Pts',(-176.965369761551,4.84319014965535,
131.671239720258));
#119086=CARTESIAN_POINT('Ctrl Pts',(-176.973126064293,4.86357169660049,
131.535697348851));
#119087=CARTESIAN_POINT('Ctrl Pts',(-176.980886506807,4.88396412179092,
131.400082634399));
#119088=CARTESIAN_POINT('Ctrl Pts',(-176.988646949322,4.89866392997535,
131.263721931019));
#119089=CARTESIAN_POINT('Ctrl Pts',(-176.996407391836,4.90764739716295,
131.127130020731));
#119090=CARTESIAN_POINT('Ctrl Pts',(-177.004180292101,4.9166452854096,130.990318840983));
#119091=CARTESIAN_POINT('Ctrl Pts',(-177.011953192367,4.91990848601988,
130.853276103724));
#119092=CARTESIAN_POINT('Ctrl Pts',(-177.019726092632,4.9174654511826,130.716516443453));
#119093=CARTESIAN_POINT('Ctrl Pts',(-177.027216428394,4.91511122681529,
130.584728341311));
#119094=CARTESIAN_POINT('Ctrl Pts',(-177.034706764156,4.90745845416787,
130.453203399852));
#119095=CARTESIAN_POINT('Ctrl Pts',(-177.042197099918,4.89457781474275,
130.322394770303));
#119096=CARTESIAN_POINT('Ctrl Pts',(-177.049971434037,4.88120880195881,
130.186626491806));
#119097=CARTESIAN_POINT('Ctrl Pts',(-177.057745768156,4.86216531860959,
130.051199842308));
#119098=CARTESIAN_POINT('Ctrl Pts',(-177.065520102275,4.83746962990001,
129.916627187816));
#119099=CARTESIAN_POINT('Ctrl Pts',(-177.073284855222,4.81280437641963,
129.782220382095));
#119100=CARTESIAN_POINT('Ctrl Pts',(-177.081049608169,4.78250084741113,
129.648665858125));
#119101=CARTESIAN_POINT('Ctrl Pts',(-177.088814361117,4.74663315778832,
129.516472141073));
#119102=CARTESIAN_POINT('Ctrl Pts',(-177.096571402002,4.71080109246049,
129.384409720683));
#119103=CARTESIAN_POINT('Ctrl Pts',(-177.104328442886,4.66941596602455,
129.253705792402));
#119104=CARTESIAN_POINT('Ctrl Pts',(-177.112085483771,4.62260309462542,
129.124859592839));
#119105=CARTESIAN_POINT('Ctrl Pts',(-177.119836675012,4.57582552517671,
128.996110557197));
#119106=CARTESIAN_POINT('Ctrl Pts',(-177.127587866252,4.52362849080941,
128.86921682779));
#119107=CARTESIAN_POINT('Ctrl Pts',(-177.135339057492,4.46618727882041,
128.744663005536));
#119108=CARTESIAN_POINT('Ctrl Pts',(-177.143086954269,4.40877048087887,
128.620162121979));
#119109=CARTESIAN_POINT('Ctrl Pts',(-177.150834851046,4.34611410184664,
128.497999521832));
#119110=CARTESIAN_POINT('Ctrl Pts',(-177.158582747823,4.27844166546919,
128.378640110649));
#119111=CARTESIAN_POINT('Ctrl Pts',(-177.166329023907,4.21078338470659,
128.259305666881));
#119112=CARTESIAN_POINT('Ctrl Pts',(-177.174075299991,4.13811132632168,
128.142773585651));
#119113=CARTESIAN_POINT('Ctrl Pts',(-177.181821576076,4.06069491653235,
128.029484069438));
#119114=CARTESIAN_POINT('Ctrl Pts',(-177.189567909341,3.98327793527256,
127.916193716948));
#119115=CARTESIAN_POINT('Ctrl Pts',(-177.197314242606,3.90111675330759,
127.806146300033));
#119116=CARTESIAN_POINT('Ctrl Pts',(-177.205060575872,3.81452383432444,
127.699752594019));
#119117=CARTESIAN_POINT('Ctrl Pts',(-177.212808643875,3.72791152345761,
127.593335061873));
#119118=CARTESIAN_POINT('Ctrl Pts',(-177.220556711878,3.6368657474451,127.490573171966));
#119119=CARTESIAN_POINT('Ctrl Pts',(-177.228304779881,3.54173864545286,
127.391843887965));
#119120=CARTESIAN_POINT('Ctrl Pts',(-177.236061082622,3.44651044124447,
127.293009673306));
#119121=CARTESIAN_POINT('Ctrl Pts',(-177.243817385364,3.34719251777253,
127.198216908093));
#119122=CARTESIAN_POINT('Ctrl Pts',(-177.251573688106,3.24417360591931,
127.107805372861));
#119123=CARTESIAN_POINT('Ctrl Pts',(-177.25933413062,3.14109970977099,127.01734558227));
#119124=CARTESIAN_POINT('Ctrl Pts',(-177.267094573134,3.03432119346774,
126.931271926352));
#119125=CARTESIAN_POINT('Ctrl Pts',(-177.274855015649,2.92425833430713,
126.849882617028));
#119126=CARTESIAN_POINT('Ctrl Pts',(-177.282627915914,2.81401879247408,
126.76836265436));
#119127=CARTESIAN_POINT('Ctrl Pts',(-177.29040081618,2.70048469600353,126.691542284325));
#119128=CARTESIAN_POINT('Ctrl Pts',(-177.298173716445,2.58410440057933,
126.619675741807));
#119129=CARTESIAN_POINT('Ctrl Pts',(-177.305664052207,2.47195482203776,
126.550421729131));
#119130=CARTESIAN_POINT('Ctrl Pts',(-177.313154387969,2.35716265326231,
126.485767779962));
#119131=CARTESIAN_POINT('Ctrl Pts',(-177.320644723731,2.24014734829281,
126.425899367259));
#119132=CARTESIAN_POINT('Ctrl Pts',(-177.32841905785,2.11869537246986,126.363761025492));
#119133=CARTESIAN_POINT('Ctrl Pts',(-177.336193391969,1.99446362885182,
126.30658143534));
#119134=CARTESIAN_POINT('Ctrl Pts',(-177.343967726088,1.86789522035938,
126.254618810797));
#119135=CARTESIAN_POINT('Ctrl Pts',(-177.351732479035,1.74148279611867,
126.202720225545));
#119136=CARTESIAN_POINT('Ctrl Pts',(-177.359497231982,1.61273979500866,
126.156025960285));
#119137=CARTESIAN_POINT('Ctrl Pts',(-177.36726198493,1.48213411457354,126.114748530312));
#119138=CARTESIAN_POINT('Ctrl Pts',(-177.375019025815,1.3516581535411,126.073512097665));
#119139=CARTESIAN_POINT('Ctrl Pts',(-177.3827760667,1.21932356522319,126.037681910766));
#119140=CARTESIAN_POINT('Ctrl Pts',(-177.390533107585,1.08561810795748,
126.007422387176));
#119141=CARTESIAN_POINT('Ctrl Pts',(-177.398284298825,0.952013479016992,
125.977185682529));
#119142=CARTESIAN_POINT('Ctrl Pts',(-177.406035490065,0.817040418589824,
125.952511365542));
#119143=CARTESIAN_POINT('Ctrl Pts',(-177.413786681305,0.681201382220152,
125.933513900684));
#119144=CARTESIAN_POINT('Ctrl Pts',(-177.421534578082,0.545420081064746,
125.914524510255));
#119145=CARTESIAN_POINT('Ctrl Pts',(-177.429282474859,0.408773922402197,
125.901207227089));
#119146=CARTESIAN_POINT('Ctrl Pts',(-177.437030371636,0.271774864485895,
125.893625287136));
#119147=CARTESIAN_POINT('Ctrl Pts',(-177.44477664772,0.134804463819151,
125.886044933161));
#119148=CARTESIAN_POINT('Ctrl Pts',(-177.452522923805,-0.00251829915094726,
125.884197557701));
#119149=CARTESIAN_POINT('Ctrl Pts',(-177.460269199889,-0.139677438159066,
125.88809442504));
#119150=CARTESIAN_POINT('Ctrl Pts',(-177.468015533154,-0.276837589644604,
125.891991321146));
#119151=CARTESIAN_POINT('Ctrl Pts',(-177.47576186642,-0.41383372395051,
125.901632533558));
#119152=CARTESIAN_POINT('Ctrl Pts',(-177.483508199685,-0.550151349906157,
125.916977211827));
#119153=CARTESIAN_POINT('Ctrl Pts',(-177.491256267688,-0.686499503249163,
125.932325326429));
#119154=CARTESIAN_POINT('Ctrl Pts',(-177.499004335691,-0.82216845744731,
125.953379404746));
#119155=CARTESIAN_POINT('Ctrl Pts',(-177.506752403694,-0.956650722471993,
125.980046940192));
#119156=CARTESIAN_POINT('Ctrl Pts',(-177.514508706436,-1.09127591684812,
126.006742818213));
#119157=CARTESIAN_POINT('Ctrl Pts',(-177.522265009177,-1.22471151850379,
126.03906399502));
#119158=CARTESIAN_POINT('Ctrl Pts',(-177.530021311919,-1.3564615419159,
126.076867079992));
#119159=CARTESIAN_POINT('Ctrl Pts',(-177.537781754434,-1.48828188428242,
126.114690341609));
#119160=CARTESIAN_POINT('Ctrl Pts',(-177.545542196948,-1.61841448501119,
126.15800121801));
#119161=CARTESIAN_POINT('Ctrl Pts',(-177.553302639462,-1.746381279821,126.20660730883));
#119162=CARTESIAN_POINT('Ctrl Pts',(-177.561075539727,-1.8745534982902,
126.255291426463));
#119163=CARTESIAN_POINT('Ctrl Pts',(-177.568848439993,-2.0005526036341,
126.30928759083));
#119164=CARTESIAN_POINT('Ctrl Pts',(-177.576621340258,-2.12392235364388,
126.368356007763));
#119165=CARTESIAN_POINT('Ctrl Pts',(-177.58411167602,-2.24280730248949,
126.425277138956));
#119166=CARTESIAN_POINT('Ctrl Pts',(-177.591602011782,-2.35925047219554,
126.486908002843));
#119167=CARTESIAN_POINT('Ctrl Pts',(-177.599092347544,-2.47286909395594,
126.552995953525));
#119168=CARTESIAN_POINT('Ctrl Pts',(-177.60686784926,-2.59081331121292,
126.621599950762));
#119169=CARTESIAN_POINT('Ctrl Pts',(-177.614643350975,-2.70608732028164,
126.695224480623));
#119170=CARTESIAN_POINT('Ctrl Pts',(-177.622418852691,-2.8182341662396,
126.773636210373));
#119171=CARTESIAN_POINT('Ctrl Pts',(-177.63018451916,-2.93023915743989,
126.851948756978));
#119172=CARTESIAN_POINT('Ctrl Pts',(-177.637950185629,-3.03912453927194,
126.935036231687));
#119173=CARTESIAN_POINT('Ctrl Pts',(-177.645715852098,-3.14445845962935,
127.022619740911));
#119174=CARTESIAN_POINT('Ctrl Pts',(-177.653472099438,-3.24966461842309,
127.110097018391));
#119175=CARTESIAN_POINT('Ctrl Pts',(-177.661228346779,-3.35132759661482,
127.202059220451));
#119176=CARTESIAN_POINT('Ctrl Pts',(-177.66898459412,-3.44904554979687,
127.298184943427));
#119177=CARTESIAN_POINT('Ctrl Pts',(-177.676735499376,-3.54669620013157,
127.394244460198));
#119178=CARTESIAN_POINT('Ctrl Pts',(-177.684486404633,-3.64040695375948,
127.494461519737));
#119179=CARTESIAN_POINT('Ctrl Pts',(-177.69223730989,-3.72980996493064,
127.598475297096));
#119180=CARTESIAN_POINT('Ctrl Pts',(-177.699984555376,-3.81917076239027,
127.70243996193));
#119181=CARTESIAN_POINT('Ctrl Pts',(-177.707731800862,-3.90422761101185,
127.810197481142));
#119182=CARTESIAN_POINT('Ctrl Pts',(-177.715479046349,-3.9846506692834,
127.921351407335));
#119183=CARTESIAN_POINT('Ctrl Pts',(-177.723224311547,-4.06505317046089,
128.032476921257));
#119184=CARTESIAN_POINT('Ctrl Pts',(-177.730969576744,-4.14082401090818,
128.146996797071));
#119185=CARTESIAN_POINT('Ctrl Pts',(-177.738714841942,-4.21167492248432,
128.264483177646));
#119186=CARTESIAN_POINT('Ctrl Pts',(-177.746461929158,-4.28254250122873,
128.381997196048));
#119187=CARTESIAN_POINT('Ctrl Pts',(-177.754209016374,-4.34848763261502,
128.502478781148));
#119188=CARTESIAN_POINT('Ctrl Pts',(-177.76195610359,-4.40926651739199,
128.625472864352));
#119189=CARTESIAN_POINT('Ctrl Pts',(-177.769704172855,-4.47005310672187,
128.748482538734));
#119190=CARTESIAN_POINT('Ctrl Pts',(-177.77745224212,-4.52567197910536,
128.874004991591));
#119191=CARTESIAN_POINT('Ctrl Pts',(-177.785200311385,-4.57592665268824,
129.001563254655));
#119192=CARTESIAN_POINT('Ctrl Pts',(-177.792953962452,-4.62621753033989,
129.12921341222));
#119193=CARTESIAN_POINT('Ctrl Pts',(-177.800707613519,-4.67113635666925,
129.258901942004));
#119194=CARTESIAN_POINT('Ctrl Pts',(-177.808461264585,-4.71053582112806,
129.390134560541));
#119195=CARTESIAN_POINT('Ctrl Pts',(-177.812229200399,-4.7296822402637,
129.453907882165));
#119196=CARTESIAN_POINT('Ctrl Pts',(-177.815997136212,-4.74752599936461,
129.518045636102));
#119197=CARTESIAN_POINT('Ctrl Pts',(-177.819765072025,-4.76405452823413,
129.582490119309));
#119198=CARTESIAN_POINT('Origin',(213.235140564004,0.,130.804360617566));
#119199=CARTESIAN_POINT('',(-179.915287826822,-4.76405452823417,129.582490119309));
#119200=CARTESIAN_POINT('',(-179.570054719422,-4.76405452823393,129.582490119308));
#119201=CARTESIAN_POINT('',(213.235140564004,-4.76405452823405,129.582490119308));
#119202=CARTESIAN_POINT('',(-178.235140563957,-4.91824875847738,130.800866016629));
#119203=CARTESIAN_POINT('Ctrl Pts',(-178.235140564012,-4.91824875847807,
130.800866017606));
#119204=CARTESIAN_POINT('Ctrl Pts',(-178.242912059243,-4.91834661808309,
130.938592191243));
#119205=CARTESIAN_POINT('Ctrl Pts',(-178.250683554473,-4.91265502275465,
131.076364389796));
#119206=CARTESIAN_POINT('Ctrl Pts',(-178.258455049704,-4.90118910695513,
131.213662951256));
#119207=CARTESIAN_POINT('Ctrl Pts',(-178.266226229677,-4.8897236562809,
131.350955943075));
#119208=CARTESIAN_POINT('Ctrl Pts',(-178.27399740965,-4.87248438266389,
131.487774950232));
#119209=CARTESIAN_POINT('Ctrl Pts',(-178.281768589622,-4.84953840587296,
131.623604361798));
#119210=CARTESIAN_POINT('Ctrl Pts',(-178.289541094918,-4.82658851579851,
131.759456938165));
#119211=CARTESIAN_POINT('Ctrl Pts',(-178.297313600214,-4.79793004946218,
131.894319201245));
#119212=CARTESIAN_POINT('Ctrl Pts',(-178.30508610551,-4.76368139923051,
132.027685018175));
#119213=CARTESIAN_POINT('Ctrl Pts',(-178.31286157721,-4.72941967788061,
132.161101734639));
#119214=CARTESIAN_POINT('Ctrl Pts',(-178.32063704891,-4.68956362187731,
132.293020493378));
#119215=CARTESIAN_POINT('Ctrl Pts',(-178.328412520609,-4.64428160317825,
132.422949957973));
#119216=CARTESIAN_POINT('Ctrl Pts',(-178.33619753434,-4.59894401455087,
132.553038871534));
#119217=CARTESIAN_POINT('Ctrl Pts',(-178.34398254807,-4.54816729194925,
132.68113324938));
#119218=CARTESIAN_POINT('Ctrl Pts',(-178.351767561801,-4.49216835570908,
132.806760808953));
#119219=CARTESIAN_POINT('Ctrl Pts',(-178.359557729245,-4.43613234792204,
132.932471534533));
#119220=CARTESIAN_POINT('Ctrl Pts',(-178.36734789669,-4.37486741040936,
133.055711842143));
#119221=CARTESIAN_POINT('Ctrl Pts',(-178.375138064134,-4.30863618326705,
133.176034562851));
#119222=CARTESIAN_POINT('Ctrl Pts',(-178.38294095569,-4.24229677699919,
133.296553813311));
#119223=CARTESIAN_POINT('Ctrl Pts',(-178.390743847245,-4.17097507715918,
133.414145626664));
#119224=CARTESIAN_POINT('Ctrl Pts',(-178.398546738801,-4.09497718847947,
133.528391617451));
#119225=CARTESIAN_POINT('Ctrl Pts',(-178.403979900142,-4.04205978115932,
133.607941217238));
#119226=CARTESIAN_POINT('Ctrl Pts',(-178.409413061482,-3.98687607958372,
133.685869291158));
#119227=CARTESIAN_POINT('Ctrl Pts',(-178.414846222822,-3.92954049509117,
133.76204460338));
#119228=CARTESIAN_POINT('Ctrl Pts',(-178.422620556941,-3.84749875864512,
133.871044187919));
#119229=CARTESIAN_POINT('Ctrl Pts',(-178.430394891061,-3.76078840842461,
133.976800260166));
#119230=CARTESIAN_POINT('Ctrl Pts',(-178.43816922518,-3.66969498233147,
134.078886812171));
#119231=CARTESIAN_POINT('Ctrl Pts',(-178.445933978127,-3.57871382074449,
134.180847551624));
#119232=CARTESIAN_POINT('Ctrl Pts',(-178.453698731074,-3.48336058895814,
134.279147480063));
#119233=CARTESIAN_POINT('Ctrl Pts',(-178.461463484021,-3.38396310956101,
134.373390840978));
#119234=CARTESIAN_POINT('Ctrl Pts',(-178.469220524906,-3.28466435314195,
134.467540598059));
#119235=CARTESIAN_POINT('Ctrl Pts',(-178.476977565791,-3.18132962460898,
134.557641538328));
#119236=CARTESIAN_POINT('Ctrl Pts',(-178.484734606676,-3.07432564361539,
134.643332472049));
#119237=CARTESIAN_POINT('Ctrl Pts',(-178.492485797916,-2.96740235515608,
134.728958785569));
#119238=CARTESIAN_POINT('Ctrl Pts',(-178.500236989156,-2.856815625741,134.81018146859));
#119239=CARTESIAN_POINT('Ctrl Pts',(-178.507988180396,-2.74296724005992,
134.886677825042));
#119240=CARTESIAN_POINT('Ctrl Pts',(-178.515736077173,-2.6291672429796,
134.963141668503));
#119241=CARTESIAN_POINT('Ctrl Pts',(-178.523483973951,-2.51210867069543,
135.034882963187));
#119242=CARTESIAN_POINT('Ctrl Pts',(-178.531231870728,-2.39222425946025,
135.101620925594));
#119243=CARTESIAN_POINT('Ctrl Pts',(-178.538978146812,-2.27236492545981,
135.168344927857));
#119244=CARTESIAN_POINT('Ctrl Pts',(-178.546724422896,-2.14968126963242,
135.230067489522));
#119245=CARTESIAN_POINT('Ctrl Pts',(-178.55447069898,-2.0246323815396,135.286552802437));
#119246=CARTESIAN_POINT('Ctrl Pts',(-178.562217032245,-1.89958257036413,
135.343038532314));
#119247=CARTESIAN_POINT('Ctrl Pts',(-178.569963365511,-1.77216784838562,
135.394286775354));
#119248=CARTESIAN_POINT('Ctrl Pts',(-178.577709698776,-1.64286875422958,
135.440109243072));
#119249=CARTESIAN_POINT('Ctrl Pts',(-178.585457766779,-1.51354070443772,
135.485941972413));
#119250=CARTESIAN_POINT('Ctrl Pts',(-178.593205834782,-1.38232781119079,
135.526346378023));
#119251=CARTESIAN_POINT('Ctrl Pts',(-178.600953902785,-1.24972691011741,
135.561183686866));
#119252=CARTESIAN_POINT('Ctrl Pts',(-178.608710205527,-1.11698507922857,
135.596058021216));
#119253=CARTESIAN_POINT('Ctrl Pts',(-178.616466508269,-0.982852672395769,
135.625353339897));
#119254=CARTESIAN_POINT('Ctrl Pts',(-178.62422281101,-0.847838434771901,
135.648981660643));
#119255=CARTESIAN_POINT('Ctrl Pts',(-178.631983253525,-0.712752135984214,
135.672622592535));
#119256=CARTESIAN_POINT('Ctrl Pts',(-178.639743696039,-0.576783455982213,
135.690590448432));
#119257=CARTESIAN_POINT('Ctrl Pts',(-178.647504138553,-0.440446459232609,
135.702849157825));
#119258=CARTESIAN_POINT('Ctrl Pts',(-178.655277038818,-0.303890602232393,
135.715127545987));
#119259=CARTESIAN_POINT('Ctrl Pts',(-178.663049939084,-0.166965637712462,
135.721678454702));
#119260=CARTESIAN_POINT('Ctrl Pts',(-178.670822839349,-0.03018673474577,
135.722517978158));
#119261=CARTESIAN_POINT('Ctrl Pts',(-178.678313175112,0.101619910576147,
135.723326982821));
#119262=CARTESIAN_POINT('Ctrl Pts',(-178.685803510874,0.233290621547758,
135.718832649925));
#119263=CARTESIAN_POINT('Ctrl Pts',(-178.693293846636,0.364370681277128,
135.709094766236));
#119264=CARTESIAN_POINT('Ctrl Pts',(-178.701068180755,0.500420681308806,
135.698987667727));
#119265=CARTESIAN_POINT('Ctrl Pts',(-178.708842514874,0.63626532236978,
135.683199534606));
#119266=CARTESIAN_POINT('Ctrl Pts',(-178.716616848993,0.77139185169714,
135.661740330295));
#119267=CARTESIAN_POINT('Ctrl Pts',(-178.72438160194,0.906351849653709,
135.640307572536));
#119268=CARTESIAN_POINT('Ctrl Pts',(-178.732146354887,1.04059511436018,
135.61321771052));
#119269=CARTESIAN_POINT('Ctrl Pts',(-178.739911107835,1.17361148854135,
135.580532634617));
#119270=CARTESIAN_POINT('Ctrl Pts',(-178.74766814872,1.30649574898521,135.547880021992));
#119271=CARTESIAN_POINT('Ctrl Pts',(-178.755425189605,1.43815516668883,
135.509643347339));
#119272=CARTESIAN_POINT('Ctrl Pts',(-178.76318223049,1.56808764156665,135.465935910411));
#119273=CARTESIAN_POINT('Ctrl Pts',(-178.77093342173,1.6979221333539,135.422261433602));
#119274=CARTESIAN_POINT('Ctrl Pts',(-178.77868461297,1.82603190540451,135.373124530313));
#119275=CARTESIAN_POINT('Ctrl Pts',(-178.78643580421,1.95192828993981,135.318688808275));
#119276=CARTESIAN_POINT('Ctrl Pts',(-178.794183700987,2.07777116515346,
135.264276222872));
#119277=CARTESIAN_POINT('Ctrl Pts',(-178.801931597764,2.20140216582424,
135.204569452893));
#119278=CARTESIAN_POINT('Ctrl Pts',(-178.809679494541,2.32235115632627,
135.139780801263));
#119279=CARTESIAN_POINT('Ctrl Pts',(-178.817425770625,2.44327484690683,
135.075005702023));
#119280=CARTESIAN_POINT('Ctrl Pts',(-178.82517204671,2.56151729879949,135.005151020031));
#119281=CARTESIAN_POINT('Ctrl Pts',(-178.832918322794,2.6766319708055,134.93047554027));
#119282=CARTESIAN_POINT('Ctrl Pts',(-178.840664656059,2.79174749256172,
134.855799509272));
#119283=CARTESIAN_POINT('Ctrl Pts',(-178.848410989325,2.90373486036354,
134.77630282227));
#119284=CARTESIAN_POINT('Ctrl Pts',(-178.85615732259,3.01217591891128,134.692287995493));
#119285=CARTESIAN_POINT('Ctrl Pts',(-178.863905390593,3.12064126208234,
134.608254354177));
#119286=CARTESIAN_POINT('Ctrl Pts',(-178.871653458596,3.22555840668735,
134.519700799111));
#119287=CARTESIAN_POINT('Ctrl Pts',(-178.879401526599,3.32654204724801,
134.426970321963));
#119288=CARTESIAN_POINT('Ctrl Pts',(-178.887157829341,3.42763301442343,
134.334141289761));
#119289=CARTESIAN_POINT('Ctrl Pts',(-178.894914132082,3.52478183797542,
134.23712673239));
#119290=CARTESIAN_POINT('Ctrl Pts',(-178.902670434824,3.61763950674951,
134.136307114991));
#119291=CARTESIAN_POINT('Ctrl Pts',(-178.910430877338,3.71054673645731,
134.035433687128));
#119292=CARTESIAN_POINT('Ctrl Pts',(-178.918191319852,3.79915799525986,
133.93075145081));
#119293=CARTESIAN_POINT('Ctrl Pts',(-178.925951762367,3.88316507161623,
133.822673406042));
#119294=CARTESIAN_POINT('Ctrl Pts',(-178.933724662632,3.96730700358959,
133.714421864802));
#119295=CARTESIAN_POINT('Ctrl Pts',(-178.941497562898,4.04682975652453,
133.60276394041));
#119296=CARTESIAN_POINT('Ctrl Pts',(-178.949270463163,4.12146840944813,
133.488141758498));
#119297=CARTESIAN_POINT('Ctrl Pts',(-178.956760798925,4.19339375933312,
133.377686381616));
#119298=CARTESIAN_POINT('Ctrl Pts',(-178.964251134687,4.26078378529405,
133.264478786661));
#119299=CARTESIAN_POINT('Ctrl Pts',(-178.971741470449,4.32344300204487,
133.14893385604));
#119300=CARTESIAN_POINT('Ctrl Pts',(-178.979515804568,4.38847796204466,
133.029008004254));
#119301=CARTESIAN_POINT('Ctrl Pts',(-178.987290138687,4.44862230519032,
132.906184188811));
#119302=CARTESIAN_POINT('Ctrl Pts',(-178.995064472806,4.50360725859762,
132.780899188606));
#119303=CARTESIAN_POINT('Ctrl Pts',(-179.002829225753,4.55852444796399,
132.655768590966));
#119304=CARTESIAN_POINT('Ctrl Pts',(-179.0105939787,4.60829474347329,132.528183198275));
#119305=CARTESIAN_POINT('Ctrl Pts',(-179.018358731647,4.65269446277708,
132.398605673554));
#119306=CARTESIAN_POINT('Ctrl Pts',(-179.026115772532,4.69705008365385,
132.269156847057));
#119307=CARTESIAN_POINT('Ctrl Pts',(-179.033872813417,4.73604561757761,
132.137720193522));
#119308=CARTESIAN_POINT('Ctrl Pts',(-179.041629854302,4.76950498948021,
132.004779385256));
#119309=CARTESIAN_POINT('Ctrl Pts',(-179.049381045542,4.80293912941014,
131.871938828688));
#119310=CARTESIAN_POINT('Ctrl Pts',(-179.057132236782,4.83084532209175,
131.737596752741));
#119311=CARTESIAN_POINT('Ctrl Pts',(-179.064883428023,4.85309707847332,
131.602252721433));
#119312=CARTESIAN_POINT('Ctrl Pts',(-179.0726313248,4.87533937726481,131.466966214949));
#119313=CARTESIAN_POINT('Ctrl Pts',(-179.080379221577,4.89193195641557,
131.330678985081));
#119314=CARTESIAN_POINT('Ctrl Pts',(-179.088127118354,4.90279931259945,
131.193901325162));
#119315=CARTESIAN_POINT('Ctrl Pts',(-179.095873394438,4.91366439556669,
131.057152276181));
#119316=CARTESIAN_POINT('Ctrl Pts',(-179.103619670522,4.91880660669958,
130.919913390691));
#119317=CARTESIAN_POINT('Ctrl Pts',(-179.111365946606,4.91820230270907,
130.782700236056));
#119318=CARTESIAN_POINT('Ctrl Pts',(-179.119112279871,4.91759799425773,
130.645486068543));
#119319=CARTESIAN_POINT('Ctrl Pts',(-179.126858613137,4.91124708775985,
130.508298023225));
#119320=CARTESIAN_POINT('Ctrl Pts',(-179.134604946402,4.89917807553393,
130.371651423409));
#119321=CARTESIAN_POINT('Ctrl Pts',(-179.142353014405,4.88710636053639,
130.234974222535));
#119322=CARTESIAN_POINT('Ctrl Pts',(-179.150101082408,4.86931402609475,
130.098839097816));
#119323=CARTESIAN_POINT('Ctrl Pts',(-179.157849150411,4.84588137379236,
129.963755613041));
#119324=CARTESIAN_POINT('Ctrl Pts',(-179.165605453153,4.82242381698827,
129.828528559931));
#119325=CARTESIAN_POINT('Ctrl Pts',(-179.173361755895,4.79331403439889,
129.694355765308));
#119326=CARTESIAN_POINT('Ctrl Pts',(-179.181118058636,4.75868347306896,
129.561736512842));
#119327=CARTESIAN_POINT('Ctrl Pts',(-179.188878501151,4.72403442836585,
129.429046477489));
#119328=CARTESIAN_POINT('Ctrl Pts',(-179.196638943665,4.68385884803004,
129.297912010122));
#119329=CARTESIAN_POINT('Ctrl Pts',(-179.204399386179,4.63833760479553,
129.16881565443));
#119330=CARTESIAN_POINT('Ctrl Pts',(-179.212172286444,4.59274328682007,
129.039512061807));
#119331=CARTESIAN_POINT('Ctrl Pts',(-179.21994518671,4.54178630312496,128.912253482031));
#119332=CARTESIAN_POINT('Ctrl Pts',(-179.227718086975,4.48569543026932,
128.787501780324));
#119333=CARTESIAN_POINT('Ctrl Pts',(-179.235208422737,4.43164360192636,
128.667285117205));
#119334=CARTESIAN_POINT('Ctrl Pts',(-179.242698758499,4.37282480120875,
128.549396509455));
#119335=CARTESIAN_POINT('Ctrl Pts',(-179.250189094261,4.30948241586416,
128.434224678457));
#119336=CARTESIAN_POINT('Ctrl Pts',(-179.25796342838,4.24373838472681,128.314686072481));
#119337=CARTESIAN_POINT('Ctrl Pts',(-179.265737762499,4.17291271682093,
128.197695660831));
#119338=CARTESIAN_POINT('Ctrl Pts',(-179.273512096618,4.09722760829128,
128.083715659407));
#119339=CARTESIAN_POINT('Ctrl Pts',(-179.281276849565,4.02163577489393,
127.969876128149));
#119340=CARTESIAN_POINT('Ctrl Pts',(-179.289041602512,3.94119663104747,
127.859039947773));
#119341=CARTESIAN_POINT('Ctrl Pts',(-179.29680635546,3.85617852248092,127.751645389239));
#119342=CARTESIAN_POINT('Ctrl Pts',(-179.304563396344,3.77124485509857,
127.644357496495));
#119343=CARTESIAN_POINT('Ctrl Pts',(-179.31232043723,3.6817415146055,127.540504727641));
#119344=CARTESIAN_POINT('Ctrl Pts',(-179.320077478115,3.58798025533687,
127.440496656314));
#119345=CARTESIAN_POINT('Ctrl Pts',(-179.327828669355,3.49428970216282,
127.340564001851));
#119346=CARTESIAN_POINT('Ctrl Pts',(-179.335579860595,3.39634788769476,
127.244470558066));
#119347=CARTESIAN_POINT('Ctrl Pts',(-179.343331051835,3.29450673886711,
127.152592770336));
#119348=CARTESIAN_POINT('Ctrl Pts',(-179.351078948612,3.19270887524427,
127.060754033117));
#119349=CARTESIAN_POINT('Ctrl Pts',(-179.358826845389,3.08701526322851,
126.973127649607));
#119350=CARTESIAN_POINT('Ctrl Pts',(-179.366574742166,2.97781441566159,
126.890052968903));
#119351=CARTESIAN_POINT('Ctrl Pts',(-179.37432101825,2.86863641055788,126.806995665632));
#119352=CARTESIAN_POINT('Ctrl Pts',(-179.382067294334,2.75595294011129,
126.728488407918));
#119353=CARTESIAN_POINT('Ctrl Pts',(-179.389813570418,2.64018498597006,
126.654829764282));
#119354=CARTESIAN_POINT('Ctrl Pts',(-179.397559903684,2.52441617725656,
126.581170576914));
#119355=CARTESIAN_POINT('Ctrl Pts',(-179.405306236949,2.40556316927225,
126.512360284919));
#119356=CARTESIAN_POINT('Ctrl Pts',(-179.413052570214,2.28407491890505,
126.448653461738));
#119357=CARTESIAN_POINT('Ctrl Pts',(-179.420800638217,2.16255946208602,
126.384932371855));
#119358=CARTESIAN_POINT('Ctrl Pts',(-179.42854870622,2.03840793474619,126.326317206531));
#119359=CARTESIAN_POINT('Ctrl Pts',(-179.436296774223,1.9120924522984,126.273015837441));
#119360=CARTESIAN_POINT('Ctrl Pts',(-179.444053076965,1.78564272025286,
126.219657819023));
#119361=CARTESIAN_POINT('Ctrl Pts',(-179.451809379707,1.65702479963027,
126.1716250307));
#119362=CARTESIAN_POINT('Ctrl Pts',(-179.459565682449,1.52672980226203,
126.129076757373));
#119363=CARTESIAN_POINT('Ctrl Pts',(-179.467326124963,1.39636526253059,
126.08650577475));
#119364=CARTESIAN_POINT('Ctrl Pts',(-179.475086567477,1.26432223869915,
126.049425245569));
#119365=CARTESIAN_POINT('Ctrl Pts',(-179.482847009991,1.13110447457022,
126.017943823125));
#119366=CARTESIAN_POINT('Ctrl Pts',(-179.490619910257,0.997672857459797,
125.986411863907));
#119367=CARTESIAN_POINT('Ctrl Pts',(-179.498392810522,0.863063115764055,
125.960497046634));
#119368=CARTESIAN_POINT('Ctrl Pts',(-179.506165710787,0.727787489092654,
125.940256544541));
#119369=CARTESIAN_POINT('Ctrl Pts',(-179.51365604655,0.597429472185839,
125.920751835681));
#119370=CARTESIAN_POINT('Ctrl Pts',(-179.521146382312,0.466453449186646,
125.906516086481));
#119371=CARTESIAN_POINT('Ctrl Pts',(-179.528636718074,0.335318019426584,
125.897554641338));
#119372=CARTESIAN_POINT('Ctrl Pts',(-179.536411052193,0.199210549992686,
125.888253420279));
#119373=CARTESIAN_POINT('Ctrl Pts',(-179.544185386312,0.0625001998143731,
125.884604885428));
#119374=CARTESIAN_POINT('Ctrl Pts',(-179.551959720431,-0.074304053336741,
125.886671935862));
#119375=CARTESIAN_POINT('Ctrl Pts',(-179.559724473378,-0.210939707472022,
125.888736438841));
#119376=CARTESIAN_POINT('Ctrl Pts',(-179.567489226326,-0.347668647150042,
125.896502505897));
#119377=CARTESIAN_POINT('Ctrl Pts',(-179.575253979273,-0.483977095179842,
125.909981266326));
#119378=CARTESIAN_POINT('Ctrl Pts',(-179.583011020158,-0.620150159737818,
125.923446639461));
#119379=CARTESIAN_POINT('Ctrl Pts',(-179.590768061043,-0.75590317721648,
125.942613376373));
#119380=CARTESIAN_POINT('Ctrl Pts',(-179.598525101928,-0.890723050881356,
125.967440573868));
#119381=CARTESIAN_POINT('Ctrl Pts',(-179.606276293168,-1.0254412558302,
125.99224904898));
#119382=CARTESIAN_POINT('Ctrl Pts',(-179.614027484408,-1.15922733467526,
126.02270941777));
#119383=CARTESIAN_POINT('Ctrl Pts',(-179.621778675648,-1.29157434815609,
126.058729072062));
#119384=CARTESIAN_POINT('Ctrl Pts',(-179.629526572425,-1.42386511062591,
126.09473341704));
#119385=CARTESIAN_POINT('Ctrl Pts',(-179.637274469202,-1.55471764778564,
126.136292245547));
#119386=CARTESIAN_POINT('Ctrl Pts',(-179.645022365979,-1.68363645494728,
126.183262117201));
#119387=CARTESIAN_POINT('Ctrl Pts',(-179.652768642063,-1.81252829507363,
126.230222163771));
#119388=CARTESIAN_POINT('Ctrl Pts',(-179.660514918148,-1.9394868426528,
126.282590868379));
#119389=CARTESIAN_POINT('Ctrl Pts',(-179.668261194232,-2.06403335266789,
126.340175430819));
#119390=CARTESIAN_POINT('Ctrl Pts',(-179.676007527497,-2.18858078205719,
126.397760418335));
#119391=CARTESIAN_POINT('Ctrl Pts',(-179.683753860762,-2.31071578348326,
126.460561176436));
#119392=CARTESIAN_POINT('Ctrl Pts',(-179.691500194028,-2.429981504936,126.528337588141));
#119393=CARTESIAN_POINT('Ctrl Pts',(-179.699248262031,-2.54927393512061,
126.596129177904));
#119394=CARTESIAN_POINT('Ctrl Pts',(-179.706996330034,-2.66569546687332,
126.668898445397));
#119395=CARTESIAN_POINT('Ctrl Pts',(-179.714744398037,-2.77881602195207,
126.746360546269));
#119396=CARTESIAN_POINT('Ctrl Pts',(-179.722500700779,-2.89205680290245,
126.823904974785));
#119397=CARTESIAN_POINT('Ctrl Pts',(-179.73025700352,-3.00198927584127,
126.906151978699));
#119398=CARTESIAN_POINT('Ctrl Pts',(-179.738013306262,-3.10821397193136,
126.992774469098));
#119399=CARTESIAN_POINT('Ctrl Pts',(-179.745773748776,-3.21449536334011,
127.079443192529));
#119400=CARTESIAN_POINT('Ctrl Pts',(-179.753534191291,-3.31706474242677,
127.170491796366));
#119401=CARTESIAN_POINT('Ctrl Pts',(-179.761294633805,-3.41555841026557,
127.265555196444));
#119402=CARTESIAN_POINT('Ctrl Pts',(-179.76906753407,-3.51421018888385,
127.36077120073));
#119403=CARTESIAN_POINT('Ctrl Pts',(-179.776840434336,-3.60877291201382,
127.460014597025));
#119404=CARTESIAN_POINT('Ctrl Pts',(-179.784613334601,-3.69892160017226,
127.562885327165));
#119405=CARTESIAN_POINT('Ctrl Pts',(-179.792103670363,-3.78579315644455,
127.662016447149));
#119406=CARTESIAN_POINT('Ctrl Pts',(-179.799594006125,-3.86856583511938,
127.764515514558));
#119407=CARTESIAN_POINT('Ctrl Pts',(-179.807084341887,-3.94698725566329,
127.869999585564));
#119408=CARTESIAN_POINT('Ctrl Pts',(-179.81489938152,-4.02880822192404,
127.980056360295));
#119409=CARTESIAN_POINT('Ctrl Pts',(-179.822714421154,-4.10615277853036,
128.093713091792));
#119410=CARTESIAN_POINT('Ctrl Pts',(-179.830529460787,-4.17868931704032,
128.210572142352));
#119411=CARTESIAN_POINT('Ctrl Pts',(-179.838331509096,-4.25110527449914,
128.327236932372));
#119412=CARTESIAN_POINT('Ctrl Pts',(-179.846133557405,-4.31872893195353,
128.447093113703));
#119413=CARTESIAN_POINT('Ctrl Pts',(-179.853935605714,-4.38126988870761,
128.569711377796));
#119414=CARTESIAN_POINT('Ctrl Pts',(-179.861730173332,-4.44375088049264,
128.692212074126));
#119415=CARTESIAN_POINT('Ctrl Pts',(-179.86952474095,-4.50115869139553,
128.817469244293));
#119416=CARTESIAN_POINT('Ctrl Pts',(-179.877319308568,-4.55324684430206,
128.945025726441));
#119417=CARTESIAN_POINT('Ctrl Pts',(-179.885106751938,-4.60528738855242,
129.072465621758));
#119418=CARTESIAN_POINT('Ctrl Pts',(-179.892894195309,-4.65201781159595,
129.202200288788));
#119419=CARTESIAN_POINT('Ctrl Pts',(-179.900681638679,-4.6932383823034,
129.333749673307));
#119420=CARTESIAN_POINT('Ctrl Pts',(-179.90555036806,-4.71900958783941,
129.415994682738));
#119421=CARTESIAN_POINT('Ctrl Pts',(-179.910419097441,-4.74262803915595,
129.498948563585));
#119422=CARTESIAN_POINT('Ctrl Pts',(-179.915287826822,-4.76405452823417,
129.582490119309));
#119423=CARTESIAN_POINT('Ctrl Pts',(-178.165366640417,-4.76405452823403,
129.582490119308));
#119424=CARTESIAN_POINT('Ctrl Pts',(-178.174286102188,-4.80301964378508,
129.734414513464));
#119425=CARTESIAN_POINT('Ctrl Pts',(-178.18320556396,-4.83475684527663,
129.888373267217));
#119426=CARTESIAN_POINT('Ctrl Pts',(-178.192125025732,-4.85907467737619,
130.043718558394));
#119427=CARTESIAN_POINT('Ctrl Pts',(-178.200980669897,-4.88321851850083,
130.197952373904));
#119428=CARTESIAN_POINT('Ctrl Pts',(-178.209836314062,-4.90004869699476,
130.353552808266));
#119429=CARTESIAN_POINT('Ctrl Pts',(-178.218691958226,-4.9094252417917,
130.509866376946));
#119430=CARTESIAN_POINT('Ctrl Pts',(-178.224174826803,-4.91523061990645,
130.606646095947));
#119431=CARTESIAN_POINT('Ctrl Pts',(-178.22965769538,-4.91817971751586,
130.70369880656));
#119432=CARTESIAN_POINT('Ctrl Pts',(-178.235140563957,-4.91824875847738,
130.80086601663));
#119433=CARTESIAN_POINT('',(-177.889859436045,-4.91824981877161,130.80302545727));
#119434=CARTESIAN_POINT('Ctrl Pts',(-177.819765072025,-4.76405452823413,
129.582490119309));
#119435=CARTESIAN_POINT('Ctrl Pts',(-177.827528067606,-4.79810789403879,
129.715263675749));
#119436=CARTESIAN_POINT('Ctrl Pts',(-177.835291063188,-4.8265751286225,
129.849339500209));
#119437=CARTESIAN_POINT('Ctrl Pts',(-177.843054058769,-4.84938475087311,
129.984207826618));
#119438=CARTESIAN_POINT('Ctrl Pts',(-177.850828440854,-4.87222782952149,
130.119273973418));
#119439=CARTESIAN_POINT('Ctrl Pts',(-177.85860282294,-4.88939667628533,
130.255134556517));
#119440=CARTESIAN_POINT('Ctrl Pts',(-177.866377205026,-4.90087174218351,
130.391275603111));
#119441=CARTESIAN_POINT('Ctrl Pts',(-177.870098127136,-4.90636386052159,
130.456434508968));
#119442=CARTESIAN_POINT('Ctrl Pts',(-177.873819049247,-4.91055247038315,
130.521657668791));
#119443=CARTESIAN_POINT('Ctrl Pts',(-177.877539971357,-4.91343964523087,
130.586888975338));
#119444=CARTESIAN_POINT('Ctrl Pts',(-177.88164645957,-4.91662599235856,
130.658879622671));
#119445=CARTESIAN_POINT('Ctrl Pts',(-177.885752947782,-4.91823024989552,
130.730940811616));
#119446=CARTESIAN_POINT('Ctrl Pts',(-177.889859435994,-4.91824981877137,
130.803025456376));
#119447=CARTESIAN_POINT('Ctrl Pts',(-177.889859436045,-4.91824981877161,
130.80302545727));
#119448=CARTESIAN_POINT('Ctrl Pts',(-177.897578984021,-4.91828660513675,
130.938533181825));
#119449=CARTESIAN_POINT('Ctrl Pts',(-177.905298531998,-4.91271888509105,
131.074267759702));
#119450=CARTESIAN_POINT('Ctrl Pts',(-177.913018079974,-4.90151653121722,
131.209723117934));
#119451=CARTESIAN_POINT('Ctrl Pts',(-177.920728283118,-4.89032773825667,
131.345014501845));
#119452=CARTESIAN_POINT('Ctrl Pts',(-177.928438486262,-4.87351791200395,
131.480026946718));
#119453=CARTESIAN_POINT('Ctrl Pts',(-177.936148689406,-4.85110890292581,
131.614252878582));
#119454=CARTESIAN_POINT('Ctrl Pts',(-177.943851468977,-4.82872146979285,
131.748349574418));
#119455=CARTESIAN_POINT('Ctrl Pts',(-177.951554248548,-4.80074564454809,
131.881660874833));
#119456=CARTESIAN_POINT('Ctrl Pts',(-177.959257028118,-4.76725516232351,
132.013683270872));
#119457=CARTESIAN_POINT('Ctrl Pts',(-177.966954298254,-4.73378863426308,
132.145611237511));
#119458=CARTESIAN_POINT('Ctrl Pts',(-177.974651568389,-4.69481539576988,
132.276251751023));
#119459=CARTESIAN_POINT('Ctrl Pts',(-177.982348838524,-4.65046036686952,
132.405110891243));
#119460=CARTESIAN_POINT('Ctrl Pts',(-177.990043303124,-4.60612150469107,
132.533923064299));
#119461=CARTESIAN_POINT('Ctrl Pts',(-177.997737767723,-4.55640488027498,
132.660954780006));
#119462=CARTESIAN_POINT('Ctrl Pts',(-178.005432232323,-4.5014853573474,
132.785726974424));
#119463=CARTESIAN_POINT('Ctrl Pts',(-178.013125478951,-4.44657452773564,
132.910479418413));
#119464=CARTESIAN_POINT('Ctrl Pts',(-178.020818725579,-4.38646259723445,
133.03297268916));
#119465=CARTESIAN_POINT('Ctrl Pts',(-178.028511972207,-4.32137249872143,
133.152747891802));
#119466=CARTESIAN_POINT('Ctrl Pts',(-178.036205725472,-4.25627811371228,
133.272530982217));
#119467=CARTESIAN_POINT('Ctrl Pts',(-178.043899478737,-4.18620509819149,
133.389595299688));
#119468=CARTESIAN_POINT('Ctrl Pts',(-178.051593232003,-4.11142201299136,
133.503507166679));
#119469=CARTESIAN_POINT('Ctrl Pts',(-178.059289216561,-4.03661723967682,
133.617452069665));
#119470=CARTESIAN_POINT('Ctrl Pts',(-178.06698520112,-3.95709989735997,
133.72824237193));
#119471=CARTESIAN_POINT('Ctrl Pts',(-178.074681185679,-3.87318119104158,
133.835474360708));
#119472=CARTESIAN_POINT('Ctrl Pts',(-178.082385491664,-3.78917174605771,
133.942822296072));
#119473=CARTESIAN_POINT('Ctrl Pts',(-178.09008979765,-3.70075168025727,
134.046603923423));
#119474=CARTESIAN_POINT('Ctrl Pts',(-178.097794103635,-3.60827196007457,
134.146449264601));
#119475=CARTESIAN_POINT('Ctrl Pts',(-178.105503084718,-3.5157361216954,
134.246355193554));
#119476=CARTESIAN_POINT('Ctrl Pts',(-178.113212065802,-3.41913600421425,
134.342319800581));
#119477=CARTESIAN_POINT('Ctrl Pts',(-178.120921046885,-3.31885770099228,
134.434011650801));
#119478=CARTESIAN_POINT('Ctrl Pts',(-178.128641384245,-3.21843167550299,
134.525838574388));
#119479=CARTESIAN_POINT('Ctrl Pts',(-178.136361721606,-3.11431694878514,
134.61337991927));
#119480=CARTESIAN_POINT('Ctrl Pts',(-178.144082058966,-3.00693114976664,
134.696345730983));
#119481=CARTESIAN_POINT('Ctrl Pts',(-178.148050571034,-2.9517312511805,
134.738992937919));
#119482=CARTESIAN_POINT('Ctrl Pts',(-178.152019083102,-2.89566748822361,
134.780431866513));
#119483=CARTESIAN_POINT('Ctrl Pts',(-178.15598759517,-2.83879919740751,
134.820627812275));
#119484=CARTESIAN_POINT('Ctrl Pts',(-178.163761929289,-2.72739394374767,
134.899371862246));
#119485=CARTESIAN_POINT('Ctrl Pts',(-178.171536263408,-2.61253338564665,
134.973601801254));
#119486=CARTESIAN_POINT('Ctrl Pts',(-178.179310597527,-2.49461950041102,
135.04299915024));
#119487=CARTESIAN_POINT('Ctrl Pts',(-178.187075350474,-2.37685093350067,
135.112310973196));
#119488=CARTESIAN_POINT('Ctrl Pts',(-178.194840103421,-2.25603686031665,
135.176801859868));
#119489=CARTESIAN_POINT('Ctrl Pts',(-178.202604856368,-2.13261028670629,
135.236195048988));
#119490=CARTESIAN_POINT('Ctrl Pts',(-178.210361897253,-2.00930630210852,
135.295529247955));
#119491=CARTESIAN_POINT('Ctrl Pts',(-178.218118938138,-1.88339533081727,
135.349775656748));
#119492=CARTESIAN_POINT('Ctrl Pts',(-178.225875979023,-1.75533686375186,
135.39870230678));
#119493=CARTESIAN_POINT('Ctrl Pts',(-178.233627170264,-1.6273749665728,
135.447592060845));
#119494=CARTESIAN_POINT('Ctrl Pts',(-178.241378361504,-1.49726916076229,
135.491169902165));
#119495=CARTESIAN_POINT('Ctrl Pts',(-178.249129552744,-1.36550057426087,
135.529251224151));
#119496=CARTESIAN_POINT('Ctrl Pts',(-178.256877449521,-1.23378799292357,
135.567316360559));
#119497=CARTESIAN_POINT('Ctrl Pts',(-178.264625346298,-1.10041441132796,
135.599889515772));
#119498=CARTESIAN_POINT('Ctrl Pts',(-178.272373243075,-0.965877633492174,
135.626835444833));
#119499=CARTESIAN_POINT('Ctrl Pts',(-178.280119519159,-0.831368997850033,
135.653775737386));
#119500=CARTESIAN_POINT('Ctrl Pts',(-178.287865795243,-0.695698033044637,
135.675091068361));
#119501=CARTESIAN_POINT('Ctrl Pts',(-178.295612071327,-0.559373905331694,
135.690697066945));
#119502=CARTESIAN_POINT('Ctrl Pts',(-178.303358404593,-0.423048771305566,
135.706303180729));
#119503=CARTESIAN_POINT('Ctrl Pts',(-178.311104737858,-0.286070853179251,
135.716199833558));
#119504=CARTESIAN_POINT('Ctrl Pts',(-178.318851071123,-0.148955232533464,
135.720354454137));
#119505=CARTESIAN_POINT('Ctrl Pts',(-178.326599139126,-0.01180890579494,
135.724510005114));
#119506=CARTESIAN_POINT('Ctrl Pts',(-178.334347207129,0.125474794115099,
135.722920953233));
#119507=CARTESIAN_POINT('Ctrl Pts',(-178.342095275132,0.262380385697254,
135.715606854083));
#119508=CARTESIAN_POINT('Ctrl Pts',(-178.349851577874,0.399431482171527,
135.708284981421));
#119509=CARTESIAN_POINT('Ctrl Pts',(-178.357607880616,0.536103276532238,
135.695225927641));
#119510=CARTESIAN_POINT('Ctrl Pts',(-178.365364183358,0.671884454715865,
135.676501249979));
#119511=CARTESIAN_POINT('Ctrl Pts',(-178.373124625872,0.807738103402582,
135.657766578393));
#119512=CARTESIAN_POINT('Ctrl Pts',(-178.380885068386,0.942699804202917,
135.63336032706));
#119513=CARTESIAN_POINT('Ctrl Pts',(-178.3886455109,1.0762690282611,135.603405110098));
#119514=CARTESIAN_POINT('Ctrl Pts',(-178.396418411166,1.21005266949546,
135.573401806363));
#119515=CARTESIAN_POINT('Ctrl Pts',(-178.404191311431,1.34243898930015,
135.537831838098));
#119516=CARTESIAN_POINT('Ctrl Pts',(-178.411964211697,1.47294233469106,
135.496867830259));
#119517=CARTESIAN_POINT('Ctrl Pts',(-178.419454547459,1.59870155475822,
135.457392967287));
#119518=CARTESIAN_POINT('Ctrl Pts',(-178.426944883221,1.72271203539251,
135.412909533879));
#119519=CARTESIAN_POINT('Ctrl Pts',(-178.434435218983,1.8445590297808,135.363613302837));
#119520=CARTESIAN_POINT('Ctrl Pts',(-178.442209553102,1.97102588999646,
135.312447990212));
#119521=CARTESIAN_POINT('Ctrl Pts',(-178.449983887221,2.09556257726352,
135.255935644863));
#119522=CARTESIAN_POINT('Ctrl Pts',(-178.45775822134,2.21768386757729,135.194242315971));
#119523=CARTESIAN_POINT('Ctrl Pts',(-178.465522974287,2.33965465431505,
135.132625018593));
#119524=CARTESIAN_POINT('Ctrl Pts',(-178.473287727234,2.45921562135268,
135.065839616714));
#119525=CARTESIAN_POINT('Ctrl Pts',(-178.481052480181,2.57589987136006,
134.994100814192));
#119526=CARTESIAN_POINT('Ctrl Pts',(-178.488809521066,2.69246822892538,
134.922433263661));
#119527=CARTESIAN_POINT('Ctrl Pts',(-178.496566561951,2.80616522451045,
134.845822306524));
#119528=CARTESIAN_POINT('Ctrl Pts',(-178.504323602836,2.91654733030766,
134.76452914082));
#119529=CARTESIAN_POINT('Ctrl Pts',(-178.512074794076,3.02684619610039,
134.683297278925));
#119530=CARTESIAN_POINT('Ctrl Pts',(-178.519825985316,3.13383483424316,
134.59739046739));
#119531=CARTESIAN_POINT('Ctrl Pts',(-178.527577176556,3.23709786857969,
134.507113708408));
#119532=CARTESIAN_POINT('Ctrl Pts',(-178.535325073334,3.34031701337215,
134.416875319456));
#119533=CARTESIAN_POINT('Ctrl Pts',(-178.543072970111,3.43981341005556,
134.322270933959));
#119534=CARTESIAN_POINT('Ctrl Pts',(-178.550820866888,3.53520419798672,
134.223646265335));
#119535=CARTESIAN_POINT('Ctrl Pts',(-178.558567142972,3.63057503222116,
134.125042226865));
#119536=CARTESIAN_POINT('Ctrl Pts',(-178.566313419056,3.72184169427708,
134.022419858821));
#119537=CARTESIAN_POINT('Ctrl Pts',(-178.57405969514,3.80865798380126,133.916161932709));
#119538=CARTESIAN_POINT('Ctrl Pts',(-178.581806028405,3.89547491418369,
133.809903222225));
#119539=CARTESIAN_POINT('Ctrl Pts',(-178.589552361671,3.97784115911567,
133.700009202882));
#119540=CARTESIAN_POINT('Ctrl Pts',(-178.597298694936,4.05545090126791,
133.586895621821));
#119541=CARTESIAN_POINT('Ctrl Pts',(-178.605046762939,4.1330780235839,133.473756709758));
#119542=CARTESIAN_POINT('Ctrl Pts',(-178.612794830942,4.20594630237465,
133.357397123591));
#119543=CARTESIAN_POINT('Ctrl Pts',(-178.620542898945,4.27379355996916,
133.238261122777));
#119544=CARTESIAN_POINT('Ctrl Pts',(-178.628299201687,4.34171292643635,
133.118998502804));
#119545=CARTESIAN_POINT('Ctrl Pts',(-178.636055504429,4.40460041788537,
132.996953913909));
#119546=CARTESIAN_POINT('Ctrl Pts',(-178.643811807171,4.46223985970607,
132.872596217528));
#119547=CARTESIAN_POINT('Ctrl Pts',(-178.651572249685,4.51991006543252,
132.7481721477));
#119548=CARTESIAN_POINT('Ctrl Pts',(-178.659332692199,4.57232649087066,
132.621432871501));
#119549=CARTESIAN_POINT('Ctrl Pts',(-178.667093134713,4.6193217466782,132.492865773959));
#119550=CARTESIAN_POINT('Ctrl Pts',(-178.674866034979,4.66639244344228,
132.364092289099));
#119551=CARTESIAN_POINT('Ctrl Pts',(-178.682638935244,4.70802446131689,
132.233485492179));
#119552=CARTESIAN_POINT('Ctrl Pts',(-178.69041183551,4.7441005272662,132.101547284817));
#119553=CARTESIAN_POINT('Ctrl Pts',(-178.697902171271,4.77886513734783,
131.974405363625));
#119554=CARTESIAN_POINT('Ctrl Pts',(-178.705392507033,4.80847065889238,
131.846027451783));
#119555=CARTESIAN_POINT('Ctrl Pts',(-178.712882842795,4.83285762032032,
131.716868307513));
#119556=CARTESIAN_POINT('Ctrl Pts',(-178.720657176914,4.85816922080323,
131.58281205503));
#119557=CARTESIAN_POINT('Ctrl Pts',(-178.728431511034,4.87793890559331,
131.447489509917));
#119558=CARTESIAN_POINT('Ctrl Pts',(-178.736205845153,4.89204410114357,
131.311398658512));
#119559=CARTESIAN_POINT('Ctrl Pts',(-178.7439705981,4.90613191330093,131.175475526918));
#119560=CARTESIAN_POINT('Ctrl Pts',(-178.751735351047,4.91456908636255,
131.038786358168));
#119561=CARTESIAN_POINT('Ctrl Pts',(-178.759500103994,4.91728388735268,
130.901840018886));
#119562=CARTESIAN_POINT('Ctrl Pts',(-178.767257144879,4.9199959919642,130.765029696639));
#119563=CARTESIAN_POINT('Ctrl Pts',(-178.775014185764,4.91699702730776,
130.627963100528));
#119564=CARTESIAN_POINT('Ctrl Pts',(-178.782771226649,4.90826700907514,
130.491154566979));
#119565=CARTESIAN_POINT('Ctrl Pts',(-178.790522417889,4.89954357421716,
130.354449201808));
#119566=CARTESIAN_POINT('Ctrl Pts',(-178.798273609129,4.88509771292451,
130.218001900438));
#119567=CARTESIAN_POINT('Ctrl Pts',(-178.806024800369,4.86496151122054,
130.082326991727));
#119568=CARTESIAN_POINT('Ctrl Pts',(-178.813772697147,4.84483386793941,
129.946709748471));
#119569=CARTESIAN_POINT('Ctrl Pts',(-178.821520593924,4.81902075182776,
129.811864630855));
#119570=CARTESIAN_POINT('Ctrl Pts',(-178.829268490701,4.78760607584458,
129.678300616928));
#119571=CARTESIAN_POINT('Ctrl Pts',(-178.837014766785,4.75619797113449,
129.544764541714));
#119572=CARTESIAN_POINT('Ctrl Pts',(-178.844761042869,4.71919072663617,
129.412509417502));
#119573=CARTESIAN_POINT('Ctrl Pts',(-178.852507318953,4.67671924911073,
129.282033409802));
#119574=CARTESIAN_POINT('Ctrl Pts',(-178.860253652219,4.63424745807043,
129.151556438958));
#119575=CARTESIAN_POINT('Ctrl Pts',(-178.867999985484,4.58631147452994,
129.022858982598));
#119576=CARTESIAN_POINT('Ctrl Pts',(-178.875746318749,4.53309577659699,
128.896423054987));
#119577=CARTESIAN_POINT('Ctrl Pts',(-178.883494386752,4.47986816137724,
128.769958812926));
#119578=CARTESIAN_POINT('Ctrl Pts',(-178.891242454755,4.42135863065274,
128.645757467678));
#119579=CARTESIAN_POINT('Ctrl Pts',(-178.898990522758,4.35779923905243,
128.524279729831));
#119580=CARTESIAN_POINT('Ctrl Pts',(-178.9067468255,4.29417229577462,128.402672883999));
#119581=CARTESIAN_POINT('Ctrl Pts',(-178.914503128242,4.22548495189499,
128.283795774974));
#119582=CARTESIAN_POINT('Ctrl Pts',(-178.922259430984,4.15201482616275,
128.168083707637));
#119583=CARTESIAN_POINT('Ctrl Pts',(-178.930019873498,4.07850548721226,
128.052309881286));
#119584=CARTESIAN_POINT('Ctrl Pts',(-178.937780316012,4.00020850299509,
127.93970478349));
#119585=CARTESIAN_POINT('Ctrl Pts',(-178.945540758526,3.91744344631057,
127.830672687157));
#119586=CARTESIAN_POINT('Ctrl Pts',(-178.953313658792,3.83454552780952,
127.721465562824));
#119587=CARTESIAN_POINT('Ctrl Pts',(-178.961086559057,3.74716545316439,
127.615843203123));
#119588=CARTESIAN_POINT('Ctrl Pts',(-178.968859459323,3.65566209747847,
127.514175563263));
#119589=CARTESIAN_POINT('Ctrl Pts',(-178.976349795085,3.56748511925551,
127.416203798198));
#119590=CARTESIAN_POINT('Ctrl Pts',(-178.983840130847,3.47547965372134,
127.321904437295));
#119591=CARTESIAN_POINT('Ctrl Pts',(-178.991330466609,3.37999615600626,
127.231573323606));
#119592=CARTESIAN_POINT('Ctrl Pts',(-178.999104800728,3.28089237245302,
127.137817278285));
#119593=CARTESIAN_POINT('Ctrl Pts',(-179.006879134847,3.17772768024682,
127.048039341494));
#119594=CARTESIAN_POINT('Ctrl Pts',(-179.014653468966,3.07085479539997,
126.962611811609));
#119595=CARTESIAN_POINT('Ctrl Pts',(-179.022418221913,2.9641136218319,126.87728956352));
#119596=CARTESIAN_POINT('Ctrl Pts',(-179.03018297486,2.85367365105237,126.796307296342));
#119597=CARTESIAN_POINT('Ctrl Pts',(-179.037947727807,2.73992423354038,
126.720000415899));
#119598=CARTESIAN_POINT('Ctrl Pts',(-179.045704768692,2.62628779355376,
126.643769324527));
#119599=CARTESIAN_POINT('Ctrl Pts',(-179.053461809577,2.50934877066748,
126.572204595192));
#119600=CARTESIAN_POINT('Ctrl Pts',(-179.061218850462,2.38952908867568,
126.50560105266));
#119601=CARTESIAN_POINT('Ctrl Pts',(-179.068970041702,2.26979976363732,
126.439047736377));
#119602=CARTESIAN_POINT('Ctrl Pts',(-179.076721232943,2.14719444371695,
126.377448349309));
#119603=CARTESIAN_POINT('Ctrl Pts',(-179.084472424183,2.02216319162956,
126.321053903887));
#119604=CARTESIAN_POINT('Ctrl Pts',(-179.09222032096,1.89718508116047,126.264683427609));
#119605=CARTESIAN_POINT('Ctrl Pts',(-179.099968217737,1.76978344491984,
126.213513653413));
#119606=CARTESIAN_POINT('Ctrl Pts',(-179.107716114514,1.64043185755897,
126.167749098018));
#119607=CARTESIAN_POINT('Ctrl Pts',(-179.115462390598,1.51110732776167,
126.121994115581));
#119608=CARTESIAN_POINT('Ctrl Pts',(-179.123208666682,1.37983402649866,
126.08164223333));
#119609=CARTESIAN_POINT('Ctrl Pts',(-179.130954942766,1.24710399492245,
126.046849221011));
#119610=CARTESIAN_POINT('Ctrl Pts',(-179.138701276032,1.11437298356347,
126.012055951859));
#119611=CARTESIAN_POINT('Ctrl Pts',(-179.146447609297,0.980185598621585,
125.982821733656));
#119612=CARTESIAN_POINT('Ctrl Pts',(-179.154193942562,0.845047087272823,
125.959251900231));
#119613=CARTESIAN_POINT('Ctrl Pts',(-179.161942010565,0.709878312591245,
125.935676788506));
#119614=CARTESIAN_POINT('Ctrl Pts',(-179.169690078568,0.573758372738378,
125.917768652887));
#119615=CARTESIAN_POINT('Ctrl Pts',(-179.177438146571,0.437200307775627,
125.905581284571));
#119616=CARTESIAN_POINT('Ctrl Pts',(-179.185194449313,0.300497107276185,
125.893380963375));
#119617=CARTESIAN_POINT('Ctrl Pts',(-179.192950752055,0.163355241530021,
125.886913589944));
#119618=CARTESIAN_POINT('Ctrl Pts',(-179.200707054797,0.0262910045776176,
125.886180888685));
#119619=CARTESIAN_POINT('Ctrl Pts',(-179.208467497311,-0.110846387685345,
125.885447796361));
#119620=CARTESIAN_POINT('Ctrl Pts',(-179.216227939825,-0.247905678082787,
125.890455460777));
#119621=CARTESIAN_POINT('Ctrl Pts',(-179.223988382339,-0.384374003464339,
125.901153535669));
#119622=CARTESIAN_POINT('Ctrl Pts',(-179.231761282605,-0.52106139991651,
125.911868784061));
#119623=CARTESIAN_POINT('Ctrl Pts',(-179.23953418287,-0.657155547236459,
125.928292650204));
#119624=CARTESIAN_POINT('Ctrl Pts',(-179.247307083135,-0.792151210869699,
125.950323172138));
#119625=CARTESIAN_POINT('Ctrl Pts',(-179.254797418897,-0.922239442095216,
125.971552829108));
#119626=CARTESIAN_POINT('Ctrl Pts',(-179.262287754659,-1.05130736659908,
125.997988525034));
#119627=CARTESIAN_POINT('Ctrl Pts',(-179.269778090421,-1.17891665368521,
126.029495322486));
#119628=CARTESIAN_POINT('Ctrl Pts',(-179.27755242454,-1.31136428567816,
126.062196709739));
#119629=CARTESIAN_POINT('Ctrl Pts',(-179.285326758659,-1.44266004261855,
126.100464919285));
#119630=CARTESIAN_POINT('Ctrl Pts',(-179.293101092779,-1.57230004771894,
126.144204437518));
#119631=CARTESIAN_POINT('Ctrl Pts',(-179.300865845726,-1.70178028309931,
126.187890050703));
#119632=CARTESIAN_POINT('Ctrl Pts',(-179.308630598673,-1.8296084598658,
126.237033432431));
#119633=CARTESIAN_POINT('Ctrl Pts',(-179.31639535162,-1.95529193815402,
126.291488306156));
#119634=CARTESIAN_POINT('Ctrl Pts',(-179.324152392505,-2.08085058584013,
126.345889094533));
#119635=CARTESIAN_POINT('Ctrl Pts',(-179.33190943339,-2.20426841771294,
126.405590722102));
#119636=CARTESIAN_POINT('Ctrl Pts',(-179.339666474275,-2.32506932923065,
126.470397572411));
#119637=CARTESIAN_POINT('Ctrl Pts',(-179.347417665515,-2.44577914384112,
126.53515555137));
#119638=CARTESIAN_POINT('Ctrl Pts',(-179.355168856755,-2.56387562298451,
126.605010906023));
#119639=CARTESIAN_POINT('Ctrl Pts',(-179.362920047995,-2.67890431290246,
126.679720664211));
#119640=CARTESIAN_POINT('Ctrl Pts',(-179.370667944772,-2.79388411255856,
126.754398668759));
#119641=CARTESIAN_POINT('Ctrl Pts',(-179.378415841549,-2.90579838913901,
126.833926760686));
#119642=CARTESIAN_POINT('Ctrl Pts',(-179.386163738326,-3.01421909826937,
126.918017054507));
#119643=CARTESIAN_POINT('Ctrl Pts',(-179.393910014411,-3.12261712812466,
127.002089758452));
#119644=CARTESIAN_POINT('Ctrl Pts',(-179.401656290495,-3.22752273534894,
127.090722526651));
#119645=CARTESIAN_POINT('Ctrl Pts',(-179.409402566579,-3.32853890617992,
127.183585588301));
#119646=CARTESIAN_POINT('Ctrl Pts',(-179.417148899844,-3.42955582268919,
127.276449335445));
#119647=CARTESIAN_POINT('Ctrl Pts',(-179.424895233109,-3.52668295768921,
127.373543173757));
#119648=CARTESIAN_POINT('Ctrl Pts',(-179.432641566375,-3.61955859240775,
127.474498959985));
#119649=CARTESIAN_POINT('Ctrl Pts',(-179.440389634378,-3.71245502598061,
127.575477354561));
#119650=CARTESIAN_POINT('Ctrl Pts',(-179.448137702381,-3.80109780006598,
127.680319130344));
#119651=CARTESIAN_POINT('Ctrl Pts',(-179.455885770384,-3.88516434792299,
127.788621727654));
#119652=CARTESIAN_POINT('Ctrl Pts',(-179.463642073126,-3.96932024270782,
127.897039430254));
#119653=CARTESIAN_POINT('Ctrl Pts',(-179.471398375867,-4.04888995545252,
128.008924992652));
#119654=CARTESIAN_POINT('Ctrl Pts',(-179.479154678609,-4.12359296582618,
128.123844974133));
#119655=CARTESIAN_POINT('Ctrl Pts',(-179.486915121123,-4.19833584744553,
128.238826291868));
#119656=CARTESIAN_POINT('Ctrl Pts',(-179.494675563638,-4.26820665186612,
128.356844919536));
#119657=CARTESIAN_POINT('Ctrl Pts',(-179.502436006152,-4.33297052176697,
128.477442157456));
#119658=CARTESIAN_POINT('Ctrl Pts',(-179.510208906417,-4.39783835638142,
128.59823298877));
#119659=CARTESIAN_POINT('Ctrl Pts',(-179.517981806683,-4.45758270355803,
128.721610350122));
#119660=CARTESIAN_POINT('Ctrl Pts',(-179.525754706948,-4.5120162551646,
128.847094060443));
#119661=CARTESIAN_POINT('Ctrl Pts',(-179.53324504271,-4.56447101006087,
128.968016121821));
#119662=CARTESIAN_POINT('Ctrl Pts',(-179.540735378472,-4.6119942762349,
129.090893761478));
#119663=CARTESIAN_POINT('Ctrl Pts',(-179.548225714234,-4.65446265192088,
129.215285262407));
#119664=CARTESIAN_POINT('Ctrl Pts',(-179.555502049297,-4.69571769586986,
129.336122868151));
#119665=CARTESIAN_POINT('Ctrl Pts',(-179.562778384359,-4.73228882758073,
129.458636134573));
#119666=CARTESIAN_POINT('Ctrl Pts',(-179.570054719422,-4.76405452823393,
129.582490119308));
#119667=CARTESIAN_POINT('Origin',(213.235140564004,0.,130.804360617566));
#119668=CARTESIAN_POINT('',(-181.664999290689,-4.76405452823418,129.582490119309));
#119669=CARTESIAN_POINT('',(-181.320039938991,-4.76405452823418,129.582490119309));
#119670=CARTESIAN_POINT('',(213.235140564004,-4.76405452823405,129.582490119308));
#119671=CARTESIAN_POINT('',(-179.985140564067,-4.91824883331974,130.807748249335));
#119672=CARTESIAN_POINT('Ctrl Pts',(-179.985140564067,-4.91824883331974,
130.807748249336));
#119673=CARTESIAN_POINT('Ctrl Pts',(-179.993960729007,-4.91814115236676,
130.964082159672));
#119674=CARTESIAN_POINT('Ctrl Pts',(-180.002780893947,-4.91057552406498,
131.120123073993));
#119675=CARTESIAN_POINT('Ctrl Pts',(-180.011601058887,-4.89565957716396,
131.27521130199));
#119676=CARTESIAN_POINT('Ctrl Pts',(-180.020460543816,-4.88067713548981,
131.43099090792));
#119677=CARTESIAN_POINT('Ctrl Pts',(-180.029320028745,-4.85827880522494,
131.585809153203));
#119678=CARTESIAN_POINT('Ctrl Pts',(-180.038179513674,-4.82862329315814,
131.739015717199));
#119679=CARTESIAN_POINT('Ctrl Pts',(-180.047091538771,-4.79879191244734,
131.893130855312));
#119680=CARTESIAN_POINT('Ctrl Pts',(-180.056003563869,-4.7616171115927,
132.045614980022));
#119681=CARTESIAN_POINT('Ctrl Pts',(-180.064915588966,-4.71730902760369,
132.195826966634));
#119682=CARTESIAN_POINT('Ctrl Pts',(-180.071787714544,-4.68314275069523,
132.311656491802));
#119683=CARTESIAN_POINT('Ctrl Pts',(-180.078659840122,-4.64473597477464,
132.426135393135));
#119684=CARTESIAN_POINT('Ctrl Pts',(-180.0855319657,-4.60220406385651,132.538978966691));
#119685=CARTESIAN_POINT('Ctrl Pts',(-180.093306299819,-4.55408834151546,
132.666637234001));
#119686=CARTESIAN_POINT('Ctrl Pts',(-180.101080633938,-4.50058080743443,
132.792494198247));
#119687=CARTESIAN_POINT('Ctrl Pts',(-180.108854968057,-4.44183581893942,
132.916060790433));
#119688=CARTESIAN_POINT('Ctrl Pts',(-180.116619721004,-4.3831632283927,
133.039475097838));
#119689=CARTESIAN_POINT('Ctrl Pts',(-180.124384473951,-4.31926619260353,
133.160604299769));
#119690=CARTESIAN_POINT('Ctrl Pts',(-180.132149226898,-4.25034814935119,
133.27897648105));
#119691=CARTESIAN_POINT('Ctrl Pts',(-180.139906267783,-4.1814985564708,
133.397231093413));
#119692=CARTESIAN_POINT('Ctrl Pts',(-180.147663308668,-4.10763807579476,
133.512733798804));
#119693=CARTESIAN_POINT('Ctrl Pts',(-180.155420349553,-4.02901718669648,
133.62503492911));
#119694=CARTESIAN_POINT('Ctrl Pts',(-180.163171540793,-3.95045558622215,
133.73725137226));
#119695=CARTESIAN_POINT('Ctrl Pts',(-180.170922732034,-3.8671409460421,
133.846270726925));
#119696=CARTESIAN_POINT('Ctrl Pts',(-180.178673923274,-3.77936821263246,
133.951670417354));
#119697=CARTESIAN_POINT('Ctrl Pts',(-180.186421820051,-3.69163278497605,
134.057025310104));
#119698=CARTESIAN_POINT('Ctrl Pts',(-180.194169716828,-3.5994432823843,
134.158763298683));
#119699=CARTESIAN_POINT('Ctrl Pts',(-180.201917613605,-3.50313613111719,
134.256493336533));
#119700=CARTESIAN_POINT('Ctrl Pts',(-180.209663889689,-3.40684912522998,
134.354202931366));
#119701=CARTESIAN_POINT('Ctrl Pts',(-180.217410165773,-3.30644645813239,
134.447905964751));
#119702=CARTESIAN_POINT('Ctrl Pts',(-180.225156441857,-3.20230248324751,
134.537247150571));
#119703=CARTESIAN_POINT('Ctrl Pts',(-180.232902775123,-3.0981577395956,
134.626588995887));
#119704=CARTESIAN_POINT('Ctrl Pts',(-180.240649108388,-2.99027192978512,
134.711568674828));
#119705=CARTESIAN_POINT('Ctrl Pts',(-180.248395441653,-2.8790533424594,
134.79187048135));
#119706=CARTESIAN_POINT('Ctrl Pts',(-180.256143509656,-2.76780984850203,
134.872190270904));
#119707=CARTESIAN_POINT('Ctrl Pts',(-180.263891577659,-2.65323240879196,
134.947829874661));
#119708=CARTESIAN_POINT('Ctrl Pts',(-180.271639645662,-2.53575886331033,
135.018516529447));
#119709=CARTESIAN_POINT('Ctrl Pts',(-180.279395948404,-2.41816046554677,
135.089278310851));
#119710=CARTESIAN_POINT('Ctrl Pts',(-180.287152251146,-2.29766014887279,
135.155076425877));
#119711=CARTESIAN_POINT('Ctrl Pts',(-180.294908553888,-2.17472145211095,
135.215683510784));
#119712=CARTESIAN_POINT('Ctrl Pts',(-180.302668996402,-2.05171713926471,
135.276322943517));
#119713=CARTESIAN_POINT('Ctrl Pts',(-180.310429438916,-1.92627221052881,
135.331765667491));
#119714=CARTESIAN_POINT('Ctrl Pts',(-180.31818988143,-1.79886989369378,
135.381832645669));
#119715=CARTESIAN_POINT('Ctrl Pts',(-180.325962781696,-1.67126305934953,
135.431979995805));
#119716=CARTESIAN_POINT('Ctrl Pts',(-180.333735681961,-1.54169292759772,
135.476734227691));
#119717=CARTESIAN_POINT('Ctrl Pts',(-180.341508582227,-1.41065844128908,
135.515966057808));
#119718=CARTESIAN_POINT('Ctrl Pts',(-180.348998917989,-1.28438738861264,
135.553771712082));
#119719=CARTESIAN_POINT('Ctrl Pts',(-180.356489253751,-1.15675689732088,
135.586449423876));
#119720=CARTESIAN_POINT('Ctrl Pts',(-180.363979589513,-1.02822016752291,
135.613928825794));
#119721=CARTESIAN_POINT('Ctrl Pts',(-180.371753923632,-0.894809928547707,
135.642450117588));
#119722=CARTESIAN_POINT('Ctrl Pts',(-180.379528257751,-0.760000770908441,
135.665461477155));
#119723=CARTESIAN_POINT('Ctrl Pts',(-180.38730259187,-0.624287596106585,
135.682828415948));
#119724=CARTESIAN_POINT('Ctrl Pts',(-180.395067344817,-0.488741675663636,
135.700173951541));
#119725=CARTESIAN_POINT('Ctrl Pts',(-180.402832097764,-0.352294338905479,
135.711888858062));
#119726=CARTESIAN_POINT('Ctrl Pts',(-180.410596850712,-0.215452584523784,
135.717889211797));
#119727=CARTESIAN_POINT('Ctrl Pts',(-180.418353891597,-0.0787467433016716,
135.723883605896));
#119728=CARTESIAN_POINT('Ctrl Pts',(-180.426110932482,0.0583523478990269,
135.72417472524));
#119729=CARTESIAN_POINT('Ctrl Pts',(-180.433867973367,0.195330980338071,
135.718730248619));
#119730=CARTESIAN_POINT('Ctrl Pts',(-180.441619164607,0.332206316124668,
135.713289877721));
#119731=CARTESIAN_POINT('Ctrl Pts',(-180.449370355847,0.468960984882857,
135.702122535486));
#119732=CARTESIAN_POINT('Ctrl Pts',(-180.457121547087,0.605080035891566,
135.685247956223));
#119733=CARTESIAN_POINT('Ctrl Pts',(-180.464869443864,0.741141232672686,
135.668380549107));
#119734=CARTESIAN_POINT('Ctrl Pts',(-180.472617340641,0.876566961838184,
135.645810777549));
#119735=CARTESIAN_POINT('Ctrl Pts',(-180.480365237418,1.01084637823296,
135.617610316274));
#119736=CARTESIAN_POINT('Ctrl Pts',(-180.488111513502,1.14509770626855,
135.589415753928));
#119737=CARTESIAN_POINT('Ctrl Pts',(-180.495857789587,1.27820281610075,
135.555592924915));
#119738=CARTESIAN_POINT('Ctrl Pts',(-180.503604065671,1.40966044828803,
135.516264742549));
#119739=CARTESIAN_POINT('Ctrl Pts',(-180.511350398936,1.54111905086551,
135.476936269871));
#119740=CARTESIAN_POINT('Ctrl Pts',(-180.519096732201,1.67092977696887,
135.432102474804));
#119741=CARTESIAN_POINT('Ctrl Pts',(-180.526843065467,1.7986063241752,135.381936215318));
#119742=CARTESIAN_POINT('Ctrl Pts',(-180.53459113347,1.9263114636592,135.331758721446));
#119743=CARTESIAN_POINT('Ctrl Pts',(-180.542339201473,2.05188110939729,
135.276246529846));
#119744=CARTESIAN_POINT('Ctrl Pts',(-180.550087269476,2.17484911480286,
135.215620572538));
#119745=CARTESIAN_POINT('Ctrl Pts',(-180.557843572218,2.29794781206775,
135.154930181241));
#119746=CARTESIAN_POINT('Ctrl Pts',(-180.56559987496,2.41843899428399,135.089115340456));
#119747=CARTESIAN_POINT('Ctrl Pts',(-180.573356177701,2.53588081984257,
135.018443142868));
#119748=CARTESIAN_POINT('Ctrl Pts',(-180.581116620216,2.65338532763989,
134.9477332254));
#119749=CARTESIAN_POINT('Ctrl Pts',(-180.58887706273,2.76783690968252,134.87216100064));
#119750=CARTESIAN_POINT('Ctrl Pts',(-180.596637505244,2.87882374061796,
134.792036247924));
#119751=CARTESIAN_POINT('Ctrl Pts',(-180.604410405509,2.98998873746736,
134.711782871843));
#119752=CARTESIAN_POINT('Ctrl Pts',(-180.612183305775,3.09767756139703,
134.6269626059));
#119753=CARTESIAN_POINT('Ctrl Pts',(-180.61995620604,3.2015117517228,134.537925343948));
#119754=CARTESIAN_POINT('Ctrl Pts',(-180.627446541802,3.30157130768515,
134.452124810741));
#119755=CARTESIAN_POINT('Ctrl Pts',(-180.634936877564,3.39805139018646,
134.362408765159));
#119756=CARTESIAN_POINT('Ctrl Pts',(-180.642427213326,3.49064783141407,
134.269120461992));
#119757=CARTESIAN_POINT('Ctrl Pts',(-180.650201547445,3.58675509485719,
134.172295104453));
#119758=CARTESIAN_POINT('Ctrl Pts',(-180.657975881564,3.67898284597718,
134.071314544067));
#119759=CARTESIAN_POINT('Ctrl Pts',(-180.665750215683,3.76695042939966,
133.966522461138));
#119760=CARTESIAN_POINT('Ctrl Pts',(-180.67351496863,3.85480960063723,133.861859525086));
#119761=CARTESIAN_POINT('Ctrl Pts',(-180.681279721577,3.93841880170574,
133.75339470941));
#119762=CARTESIAN_POINT('Ctrl Pts',(-180.689044474525,4.01743338003051,
133.64150920365));
#119763=CARTESIAN_POINT('Ctrl Pts',(-180.69680151541,4.09636947996217,133.529734824151));
#119764=CARTESIAN_POINT('Ctrl Pts',(-180.704558556295,4.17071981453642,
133.414546832993));
#119765=CARTESIAN_POINT('Ctrl Pts',(-180.71231559718,4.24017951888239,133.296359957484));
#119766=CARTESIAN_POINT('Ctrl Pts',(-180.72006678842,4.30958684312489,133.178262207617));
#119767=CARTESIAN_POINT('Ctrl Pts',(-180.72781797966,4.37411068070913,133.057170410442));
#119768=CARTESIAN_POINT('Ctrl Pts',(-180.7355691709,4.433489291225,132.933528475461));
#119769=CARTESIAN_POINT('Ctrl Pts',(-180.743317067677,4.4928426642475,132.8099390916));
#119770=CARTESIAN_POINT('Ctrl Pts',(-180.751064964454,4.5470549907979,132.683802077373));
#119771=CARTESIAN_POINT('Ctrl Pts',(-180.758812861231,4.59591044856734,
132.555585963217));
#119772=CARTESIAN_POINT('Ctrl Pts',(-180.766559137315,4.64475568682821,
132.427396669107));
#119773=CARTESIAN_POINT('Ctrl Pts',(-180.774305413399,4.68824614600501,
132.297129505223));
#119774=CARTESIAN_POINT('Ctrl Pts',(-180.782051689483,4.72621429357663,
132.165272632978));
#119775=CARTESIAN_POINT('Ctrl Pts',(-180.789798022749,4.76418272142055,
132.033414787394));
#119776=CARTESIAN_POINT('Ctrl Pts',(-180.797544356014,4.79662864813414,
131.899967585733));
#119777=CARTESIAN_POINT('Ctrl Pts',(-180.80529068928,4.82343464568437,131.765433601949));
#119778=CARTESIAN_POINT('Ctrl Pts',(-180.813038757283,4.85024664625185,
131.630869490213));
#119779=CARTESIAN_POINT('Ctrl Pts',(-180.820786825286,4.87141612800267,
131.495218495417));
#119780=CARTESIAN_POINT('Ctrl Pts',(-180.828534893288,4.88687700368533,
131.358992219038));
#119781=CARTESIAN_POINT('Ctrl Pts',(-180.83629119603,4.90235431137068,131.222621159752));
#119782=CARTESIAN_POINT('Ctrl Pts',(-180.844047498772,4.91211084899382,
131.085673986604));
#119783=CARTESIAN_POINT('Ctrl Pts',(-180.851803801514,4.91613250301284,
130.948666803576));
#119784=CARTESIAN_POINT('Ctrl Pts',(-180.859564244028,4.92015630350971,
130.811586495688));
#119785=CARTESIAN_POINT('Ctrl Pts',(-180.867324686542,4.91843912623242,
130.674446504842));
#119786=CARTESIAN_POINT('Ctrl Pts',(-180.875085129057,4.91101899564668,
130.537760754668));
#119787=CARTESIAN_POINT('Ctrl Pts',(-180.882858029322,4.90358695360859,
130.400855584392));
#119788=CARTESIAN_POINT('Ctrl Pts',(-180.890630929587,4.89043370141627,
130.264406501322));
#119789=CARTESIAN_POINT('Ctrl Pts',(-180.898403829853,4.871649047432,130.128921041323));
#119790=CARTESIAN_POINT('Ctrl Pts',(-180.905894165615,4.85354726293575,
129.998360819063));
#119791=CARTESIAN_POINT('Ctrl Pts',(-180.913384501377,4.83021645414565,
129.86869567912));
#119792=CARTESIAN_POINT('Ctrl Pts',(-180.920874837139,4.80178100090587,
129.74036706409));
#119793=CARTESIAN_POINT('Ctrl Pts',(-180.928649171258,4.77226740881377,
129.607172830616));
#119794=CARTESIAN_POINT('Ctrl Pts',(-180.936423505377,4.73716095571161,
129.474996552097));
#119795=CARTESIAN_POINT('Ctrl Pts',(-180.944197839496,4.69654503604511,
129.344344252281));
#119796=CARTESIAN_POINT('Ctrl Pts',(-180.951962592443,4.65597917186976,
129.213852969748));
#119797=CARTESIAN_POINT('Ctrl Pts',(-180.95972734539,4.60991746600389,129.08488229868));
#119798=CARTESIAN_POINT('Ctrl Pts',(-180.967492098337,4.55849433086872,
128.957928247308));
#119799=CARTESIAN_POINT('Ctrl Pts',(-180.975249139222,4.5071222699163,128.831100288489));
#119800=CARTESIAN_POINT('Ctrl Pts',(-180.983006180107,4.45039952260687,
128.706285323457));
#119801=CARTESIAN_POINT('Ctrl Pts',(-180.990763220992,4.38851022386175,
128.583964013902));
#119802=CARTESIAN_POINT('Ctrl Pts',(-180.998514412233,4.32666759631816,
128.461734947799));
#119803=CARTESIAN_POINT('Ctrl Pts',(-181.006265603473,4.2596663481538,128.341996141624));
#119804=CARTESIAN_POINT('Ctrl Pts',(-181.014016794713,4.18773847591968,
128.225207748928));
#119805=CARTESIAN_POINT('Ctrl Pts',(-181.02176469149,4.11584117494989,128.108468994414));
#119806=CARTESIAN_POINT('Ctrl Pts',(-181.029512588267,4.03902161920529,
127.994678491457));
#119807=CARTESIAN_POINT('Ctrl Pts',(-181.037260485044,3.95755733938158,
127.884271069623));
#119808=CARTESIAN_POINT('Ctrl Pts',(-181.045006761128,3.87611010012927,
127.773886742641));
#119809=CARTESIAN_POINT('Ctrl Pts',(-181.052753037212,3.79002030129498,
127.666884403591));
#119810=CARTESIAN_POINT('Ctrl Pts',(-181.060499313296,3.6996080914805,127.563668865493));
#119811=CARTESIAN_POINT('Ctrl Pts',(-181.068245646562,3.6091952142635,127.460452565482));
#119812=CARTESIAN_POINT('Ctrl Pts',(-181.075991979827,3.51446012000957,
127.361023416295));
#119813=CARTESIAN_POINT('Ctrl Pts',(-181.083738313092,3.41576216570124,
127.26575186696));
#119814=CARTESIAN_POINT('Ctrl Pts',(-181.091486381095,3.3170421086705,127.170458982223));
#119815=CARTESIAN_POINT('Ctrl Pts',(-181.099234449098,3.2143577068925,127.079325821528));
#119816=CARTESIAN_POINT('Ctrl Pts',(-181.106982517101,3.10810366340641,
126.992684519047));
#119817=CARTESIAN_POINT('Ctrl Pts',(-181.114738819843,3.00173669185833,
126.905951133159));
#119818=CARTESIAN_POINT('Ctrl Pts',(-181.122495122585,2.89179280344652,
126.82371938953));
#119819=CARTESIAN_POINT('Ctrl Pts',(-181.130251425327,2.77869858235167,
126.746280129092));
#119820=CARTESIAN_POINT('Ctrl Pts',(-181.138011867841,2.66554399946583,
126.668799536988));
#119821=CARTESIAN_POINT('Ctrl Pts',(-181.145772310355,2.54923606489846,
126.596116731981));
#119822=CARTESIAN_POINT('Ctrl Pts',(-181.153532752869,2.43022771030707,
126.528477511288));
#119823=CARTESIAN_POINT('Ctrl Pts',(-181.161305653134,2.31102831293982,
126.460729710112));
#119824=CARTESIAN_POINT('Ctrl Pts',(-181.1690785534,2.18912018081892,126.398041851348));
#119825=CARTESIAN_POINT('Ctrl Pts',(-181.176851453665,2.06497886185556,
126.340612712208));
#119826=CARTESIAN_POINT('Ctrl Pts',(-181.184341789427,1.94535039252626,
126.285271266929));
#119827=CARTESIAN_POINT('Ctrl Pts',(-181.19183212519,1.82364856594436,126.23481296174));
#119828=CARTESIAN_POINT('Ctrl Pts',(-181.199322460952,1.70031201061043,
126.189371762859));
#119829=CARTESIAN_POINT('Ctrl Pts',(-181.207096795071,1.57229911229676,
126.142207647111));
#119830=CARTESIAN_POINT('Ctrl Pts',(-181.21487112919,1.44211957032787,126.100299193248));
#119831=CARTESIAN_POINT('Ctrl Pts',(-181.222645463309,1.31024419354801,
126.063849757355));
#119832=CARTESIAN_POINT('Ctrl Pts',(-181.230410216256,1.17853134138399,
126.027445242135));
#119833=CARTESIAN_POINT('Ctrl Pts',(-181.238174969203,1.04512718603475,
125.996486461819));
#119834=CARTESIAN_POINT('Ctrl Pts',(-181.24593972215,0.910521686468727,
125.971128435995));
#119835=CARTESIAN_POINT('Ctrl Pts',(-181.253696763035,0.776049878982477,
125.94579559612));
#119836=CARTESIAN_POINT('Ctrl Pts',(-181.26145380392,0.640379483506111,
125.926052512528));
#119837=CARTESIAN_POINT('Ctrl Pts',(-181.269210844805,0.504014423755966,
125.91200407668));
#119838=CARTESIAN_POINT('Ctrl Pts',(-181.276962036045,0.36775219795833,
125.897966234867));
#119839=CARTESIAN_POINT('Ctrl Pts',(-181.284713227285,0.230796737915274,
125.889614533002));
#119840=CARTESIAN_POINT('Ctrl Pts',(-181.292464418526,0.0936605836422182,
125.887002510048));
#119841=CARTESIAN_POINT('Ctrl Pts',(-181.300212315303,-0.0434172841072315,
125.884391597274));
#119842=CARTESIAN_POINT('Ctrl Pts',(-181.30796021208,-0.180675303261666,
125.887515518829));
#119843=CARTESIAN_POINT('Ctrl Pts',(-181.315708108857,-0.317597627272033,
125.89637581628));
#119844=CARTESIAN_POINT('Ctrl Pts',(-181.323454384941,-0.454491310083921,
125.905234260348));
#119845=CARTESIAN_POINT('Ctrl Pts',(-181.331200661025,-0.591049047521525,
125.919826668363));
#119846=CARTESIAN_POINT('Ctrl Pts',(-181.338946937109,-0.726757210785079,
125.940102501566));
#119847=CARTESIAN_POINT('Ctrl Pts',(-181.346693270374,-0.862466375815651,
125.96037848444));
#119848=CARTESIAN_POINT('Ctrl Pts',(-181.35443960364,-0.997325567484876,
125.986337918446));
#119849=CARTESIAN_POINT('Ctrl Pts',(-181.362185936905,-1.13082887530605,
126.017878703125));
#119850=CARTESIAN_POINT('Ctrl Pts',(-181.369934004908,-1.26436208026681,
126.049426551144));
#119851=CARTESIAN_POINT('Ctrl Pts',(-181.377682072911,-1.39653841675175,
126.086558147126));
#119852=CARTESIAN_POINT('Ctrl Pts',(-181.385430140914,-1.52686510424168,
126.12912094286));
#119853=CARTESIAN_POINT('Ctrl Pts',(-181.393186443656,-1.65733030448651,
126.171728974839));
#119854=CARTESIAN_POINT('Ctrl Pts',(-181.400942746398,-1.78594155654096,
126.21977961588));
#119855=CARTESIAN_POINT('Ctrl Pts',(-181.408699049139,-1.91222358852397,
126.273071175256));
#119856=CARTESIAN_POINT('Ctrl Pts',(-181.416459491654,-2.03857302102973,
126.326391177942));
#119857=CARTESIAN_POINT('Ctrl Pts',(-181.424219934168,-2.16259040297888,
126.384957505823));
#119858=CARTESIAN_POINT('Ctrl Pts',(-181.431980376682,-2.28382411758841,
126.448521954068));
#119859=CARTESIAN_POINT('Ctrl Pts',(-181.439753276947,-2.40525244731925,
126.512188441609));
#119860=CARTESIAN_POINT('Ctrl Pts',(-181.447526177213,-2.52388784149363,
126.580868886882));
#119861=CARTESIAN_POINT('Ctrl Pts',(-181.455299077478,-2.63930601795003,
126.654270641901));
#119862=CARTESIAN_POINT('Ctrl Pts',(-181.46278941324,-2.75052845296859,
126.725004058236));
#119863=CARTESIAN_POINT('Ctrl Pts',(-181.470279749002,-2.85876326417252,
126.800121305243));
#119864=CARTESIAN_POINT('Ctrl Pts',(-181.477770084764,-2.96366065256876,
126.879325764356));
#119865=CARTESIAN_POINT('Ctrl Pts',(-181.485571301677,-3.07291173377017,
126.961817549197));
#119866=CARTESIAN_POINT('Ctrl Pts',(-181.493372518591,-3.17890946479242,
127.049020518601));
#119867=CARTESIAN_POINT('Ctrl Pts',(-181.501173735504,-3.28121524436916,
127.140645347158));
#119868=CARTESIAN_POINT('Ctrl Pts',(-181.508855785267,-3.38195825643629,
127.230870564611));
#119869=CARTESIAN_POINT('Ctrl Pts',(-181.516537835029,-3.47912097019819,
127.325383261093));
#119870=CARTESIAN_POINT('Ctrl Pts',(-181.524219884791,-3.57231315162841,
127.423863345092));
#119871=CARTESIAN_POINT('Ctrl Pts',(-181.531894943118,-3.66542051884068,
127.522253802353));
#119872=CARTESIAN_POINT('Ctrl Pts',(-181.539570001446,-3.75456426629303,
127.624604178921));
#119873=CARTESIAN_POINT('Ctrl Pts',(-181.547245059773,-3.83938845729224,
127.730555266456));
#119874=CARTESIAN_POINT('Ctrl Pts',(-181.554914880889,-3.92415476700669,
127.836434056396));
#119875=CARTESIAN_POINT('Ctrl Pts',(-181.562584702005,-4.00460713403721,
127.945908359317));
#119876=CARTESIAN_POINT('Ctrl Pts',(-181.570254523121,-4.08042798415152,
128.058583764169));
#119877=CARTESIAN_POINT('Ctrl Pts',(-181.578149920418,-4.15847879212069,
128.174573051728));
#119878=CARTESIAN_POINT('Ctrl Pts',(-181.586045317716,-4.2316211508202,
128.293954320808));
#119879=CARTESIAN_POINT('Ctrl Pts',(-181.593940715013,-4.29955471667743,
128.416262566648));
#119880=CARTESIAN_POINT('Ctrl Pts',(-181.60160643385,-4.36551208345984,
128.535012844653));
#119881=CARTESIAN_POINT('Ctrl Pts',(-181.609272152686,-4.42655931303819,
128.656521791086));
#119882=CARTESIAN_POINT('Ctrl Pts',(-181.616937871523,-4.48246715571917,
128.780337084996));
#119883=CARTESIAN_POINT('Ctrl Pts',(-181.624948108051,-4.54088764480406,
128.909716965876));
#119884=CARTESIAN_POINT('Ctrl Pts',(-181.632958344578,-4.59369582612956,
129.041614905708));
#119885=CARTESIAN_POINT('Ctrl Pts',(-181.640968581106,-4.6406858403334,
129.175490458889));
#119886=CARTESIAN_POINT('Ctrl Pts',(-181.648978817634,-4.68767585453736,
129.30936601207));
#119887=CARTESIAN_POINT('Ctrl Pts',(-181.656989054161,-4.72884756406629,
129.445218700358));
#119888=CARTESIAN_POINT('Ctrl Pts',(-181.664999290689,-4.76405452823418,
129.582490119309));
#119889=CARTESIAN_POINT('Ctrl Pts',(-179.915287826822,-4.76405452823417,
129.582490119309));
#119890=CARTESIAN_POINT('Ctrl Pts',(-179.92306888399,-4.79829769999019,
129.716003726273));
#119891=CARTESIAN_POINT('Ctrl Pts',(-179.930849941158,-4.82693968418732,
129.851018898772));
#119892=CARTESIAN_POINT('Ctrl Pts',(-179.938630998326,-4.84986100741504,
129.987028817588));
#119893=CARTESIAN_POINT('Ctrl Pts',(-179.946411829481,-4.87278166485761,
130.123034785786));
#119894=CARTESIAN_POINT('Ctrl Pts',(-179.954192660636,-4.88998191732996,
130.260035064349));
#119895=CARTESIAN_POINT('Ctrl Pts',(-179.961973491791,-4.90139348051783,
130.397512965935));
#119896=CARTESIAN_POINT('Ctrl Pts',(-179.969695849198,-4.91271928463228,
130.533957706923));
#119897=CARTESIAN_POINT('Ctrl Pts',(-179.977418206605,-4.91834311166686,
130.670872539273));
#119898=CARTESIAN_POINT('Ctrl Pts',(-179.985140564012,-4.91824883332041,
130.807748248363));
#119899=CARTESIAN_POINT('',(-179.639859435944,-4.91824845113006,130.800457355239));
#119900=CARTESIAN_POINT('Ctrl Pts',(-179.570054719422,-4.76405452823393,
129.582490119308));
#119901=CARTESIAN_POINT('Ctrl Pts',(-179.579197174056,-4.80396699441805,
129.738108219203));
#119902=CARTESIAN_POINT('Ctrl Pts',(-179.58833962869,-4.8362916101084,129.895843536568));
#119903=CARTESIAN_POINT('Ctrl Pts',(-179.597482083324,-4.86082915223956,
130.055012223801));
#119904=CARTESIAN_POINT('Ctrl Pts',(-179.606541047858,-4.88514261430456,
130.212727361621));
#119905=CARTESIAN_POINT('Ctrl Pts',(-179.615600012392,-4.90181051144224,
130.371849719594));
#119906=CARTESIAN_POINT('Ctrl Pts',(-179.624658976926,-4.91068588618086,
130.53169380667));
#119907=CARTESIAN_POINT('Ctrl Pts',(-179.629725796599,-4.91565002122716,
130.621097089119));
#119908=CARTESIAN_POINT('Ctrl Pts',(-179.634792616271,-4.91817723760474,
130.710725797053));
#119909=CARTESIAN_POINT('Ctrl Pts',(-179.639859435944,-4.91824845113006,
130.800457355239));
#119910=CARTESIAN_POINT('Ctrl Pts',(-179.639859435995,-4.91824845113077,
130.80045735614));
#119911=CARTESIAN_POINT('Ctrl Pts',(-179.647643348581,-4.91835785303648,
130.938307654795));
#119912=CARTESIAN_POINT('Ctrl Pts',(-179.655427261166,-4.91266728495612,
131.076231294055));
#119913=CARTESIAN_POINT('Ctrl Pts',(-179.663211173751,-4.90118571413701,
131.213703576513));
#119914=CARTESIAN_POINT('Ctrl Pts',(-179.670945887216,-4.88977671391655,
131.350306949481));
#119915=CARTESIAN_POINT('Ctrl Pts',(-179.67868060068,-4.87264975986795,
131.486464261715));
#119916=CARTESIAN_POINT('Ctrl Pts',(-179.686415314144,-4.84986584312386,
131.62166372303));
#119917=CARTESIAN_POINT('Ctrl Pts',(-179.694150299485,-4.82708112551935,
131.75686793664));
#119918=CARTESIAN_POINT('Ctrl Pts',(-179.701885284826,-4.79863911424742,
131.891113845955));
#119919=CARTESIAN_POINT('Ctrl Pts',(-179.709620270168,-4.76465219127589,
132.023898463912));
#119920=CARTESIAN_POINT('Ctrl Pts',(-179.717357210254,-4.73065667930619,
132.156716638506));
#119921=CARTESIAN_POINT('Ctrl Pts',(-179.725094150341,-4.69111356423603,
132.288072407442));
#119922=CARTESIAN_POINT('Ctrl Pts',(-179.732831090427,-4.64618538712646,
132.417476983782));
#119923=CARTESIAN_POINT('Ctrl Pts',(-179.740651277729,-4.6007737959558,
132.54827391556));
#119924=CARTESIAN_POINT('Ctrl Pts',(-179.748471465031,-4.54986071193366,
132.677077031875));
#119925=CARTESIAN_POINT('Ctrl Pts',(-179.756291652332,-4.4936638437746,
132.803402468467));
#119926=CARTESIAN_POINT('Ctrl Pts',(-179.764041702127,-4.43797099273028,
132.928594920532));
#119927=CARTESIAN_POINT('Ctrl Pts',(-179.771791751921,-4.37708898469712,
133.051353633612));
#119928=CARTESIAN_POINT('Ctrl Pts',(-179.779541801716,-4.31127556038019,
133.171233259887));
#119929=CARTESIAN_POINT('Ctrl Pts',(-179.787397057771,-4.24456872447766,
133.292740241798));
#119930=CARTESIAN_POINT('Ctrl Pts',(-179.795252313826,-4.17279583022991,
133.41128904481));
#119931=CARTESIAN_POINT('Ctrl Pts',(-179.803107569882,-4.09626958239033,
133.526447789367));
#119932=CARTESIAN_POINT('Ctrl Pts',(-179.810962825937,-4.01974333455076,
133.641606533924));
#119933=CARTESIAN_POINT('Ctrl Pts',(-179.818818081992,-3.93846402808792,
133.753374925537));
#119934=CARTESIAN_POINT('Ctrl Pts',(-179.826673338047,-3.85278485618213,
133.861357823072));
#119935=CARTESIAN_POINT('Ctrl Pts',(-179.834447672166,-3.76798831934649,
133.968228320824));
#119936=CARTESIAN_POINT('Ctrl Pts',(-179.842222006285,-3.67860745899652,
134.071737226023));
#119937=CARTESIAN_POINT('Ctrl Pts',(-179.849996340404,-3.58493859117706,
134.171465955982));
#119938=CARTESIAN_POINT('Ctrl Pts',(-179.857761093352,-3.491385161866,134.271071779194));
#119939=CARTESIAN_POINT('Ctrl Pts',(-179.865525846299,-3.39355450492741,
134.366906414405));
#119940=CARTESIAN_POINT('Ctrl Pts',(-179.873290599246,-3.29178443534814,
134.458582599562));
#119941=CARTESIAN_POINT('Ctrl Pts',(-179.881047640131,-3.19011544523642,
134.550167730639));
#119942=CARTESIAN_POINT('Ctrl Pts',(-179.888804681016,-3.08451511749853,
134.637602371029));
#119943=CARTESIAN_POINT('Ctrl Pts',(-179.896561721901,-2.97535926942331,
134.720534806792));
#119944=CARTESIAN_POINT('Ctrl Pts',(-179.904312913141,-2.86628573662238,
134.803404702559));
#119945=CARTESIAN_POINT('Ctrl Pts',(-179.912064104381,-2.75366233038859,
134.881778915971));
#119946=CARTESIAN_POINT('Ctrl Pts',(-179.919815295621,-2.63789893932337,
134.955345109035));
#119947=CARTESIAN_POINT('Ctrl Pts',(-179.927563192398,-2.52218475078761,
135.028880034504));
#119948=CARTESIAN_POINT('Ctrl Pts',(-179.935311089175,-2.40333356107528,
135.097610794808));
#119949=CARTESIAN_POINT('Ctrl Pts',(-179.943058985952,-2.28178513072117,
135.161267740712));
#119950=CARTESIAN_POINT('Ctrl Pts',(-179.950805262036,-2.16026212567808,
135.224911370955));
#119951=CARTESIAN_POINT('Ctrl Pts',(-179.958551538121,-2.03604334835015,
135.283483116575));
#119952=CARTESIAN_POINT('Ctrl Pts',(-179.966297814205,-1.9095937562906,
135.336758961538));
#119953=CARTESIAN_POINT('Ctrl Pts',(-179.97404414747,-1.78314323080907,
135.39003519977));
#119954=CARTESIAN_POINT('Ctrl Pts',(-179.981790480735,-1.65446221802928,
135.438015307539));
#119955=CARTESIAN_POINT('Ctrl Pts',(-179.989536814001,-1.5240359049478,
135.480523320352));
#119956=CARTESIAN_POINT('Ctrl Pts',(-179.997284882004,-1.393580383798,135.52304085254));
#119957=CARTESIAN_POINT('Ctrl Pts',(-180.005032950007,-1.26137915625431,
135.560083730166));
#119958=CARTESIAN_POINT('Ctrl Pts',(-180.01278101801,-1.12793243744398,
135.59152590394));
#119959=CARTESIAN_POINT('Ctrl Pts',(-180.020537320752,-0.994343889872685,
135.62300149483));
#119960=CARTESIAN_POINT('Ctrl Pts',(-180.028293623494,-0.859507587907298,
135.648864401312));
#119961=CARTESIAN_POINT('Ctrl Pts',(-180.036049926235,-0.723934356211346,
135.66903965224));
#119962=CARTESIAN_POINT('Ctrl Pts',(-180.04381036875,-0.588288764999606,
135.689225671307));
#119963=CARTESIAN_POINT('Ctrl Pts',(-180.051570811264,-0.45190584891694,
135.703717944691));
#119964=CARTESIAN_POINT('Ctrl Pts',(-180.059331253778,-0.315300425492684,
135.71249353184));
#119965=CARTESIAN_POINT('Ctrl Pts',(-180.067104154043,-0.178475710915488,
135.721283206341));
#119966=CARTESIAN_POINT('Ctrl Pts',(-180.074877054309,-0.0414281663132729,
135.724337847456));
#119967=CARTESIAN_POINT('Ctrl Pts',(-180.082649954574,0.0953276177084138,
135.721686690525));
#119968=CARTESIAN_POINT('Ctrl Pts',(-180.090140290336,0.227111984512766,
135.719131909827));
#119969=CARTESIAN_POINT('Ctrl Pts',(-180.097630626098,0.358625127450248,
135.71127898747));
#119970=CARTESIAN_POINT('Ctrl Pts',(-180.10512096186,0.489414003383709,
135.698199294494));
#119971=CARTESIAN_POINT('Ctrl Pts',(-180.112895295979,0.625161779301939,
135.684623680983));
#119972=CARTESIAN_POINT('Ctrl Pts',(-180.120669630098,0.76055929103879,
135.665374123379));
#119973=CARTESIAN_POINT('Ctrl Pts',(-180.128443964217,0.895094207063287,
135.640473666594));
#119974=CARTESIAN_POINT('Ctrl Pts',(-180.136208717164,1.02946332082715,
135.615603897398));
#119975=CARTESIAN_POINT('Ctrl Pts',(-180.143973470111,1.16297157332996,
135.58509715623));
#119976=CARTESIAN_POINT('Ctrl Pts',(-180.151738223059,1.29511055278657,
135.549028331807));
#119977=CARTESIAN_POINT('Ctrl Pts',(-180.159495263944,1.42711828994595,
135.512995331449));
#119978=CARTESIAN_POINT('Ctrl Pts',(-180.167252304829,1.55775908575723,
135.471411343807));
#119979=CARTESIAN_POINT('Ctrl Pts',(-180.175009345714,1.68653389489693,
135.424402444635));
#119980=CARTESIAN_POINT('Ctrl Pts',(-180.182760536954,1.81521159395151,
135.377428995238));
#119981=CARTESIAN_POINT('Ctrl Pts',(-180.190511728194,1.94202574141753,
135.325038910659));
#119982=CARTESIAN_POINT('Ctrl Pts',(-180.198262919434,2.06649200369359,
135.267408215472));
#119983=CARTESIAN_POINT('Ctrl Pts',(-180.206010816211,2.19090536448777,
135.209802014867));
#119984=CARTESIAN_POINT('Ctrl Pts',(-180.213758712988,2.31297247082939,
135.146959797708));
#119985=CARTESIAN_POINT('Ctrl Pts',(-180.221506609765,2.43222875786826,
135.079105794989));
#119986=CARTESIAN_POINT('Ctrl Pts',(-180.229252885849,2.55146009906276,
135.011265985864));
#119987=CARTESIAN_POINT('Ctrl Pts',(-180.236999161933,2.6678814508488,134.938416669642));
#119988=CARTESIAN_POINT('Ctrl Pts',(-180.244745438018,2.78105302127715,
134.860827942141));
#119989=CARTESIAN_POINT('Ctrl Pts',(-180.252491771283,2.89422542711247,
134.783238641898));
#119990=CARTESIAN_POINT('Ctrl Pts',(-180.260238104548,3.00414768126175,
134.700910081639));
#119991=CARTESIAN_POINT('Ctrl Pts',(-180.267984437814,3.11040948439129,
134.61415534982));
#119992=CARTESIAN_POINT('Ctrl Pts',(-180.275732505817,3.21669508411531,
134.52738118988));
#119993=CARTESIAN_POINT('Ctrl Pts',(-180.28348057382,3.31931829885344,134.436179133193));
#119994=CARTESIAN_POINT('Ctrl Pts',(-180.291228641823,3.41790270127258,
134.340901892192));
#119995=CARTESIAN_POINT('Ctrl Pts',(-180.298984944565,3.51659188036738,
134.245523389406));
#119996=CARTESIAN_POINT('Ctrl Pts',(-180.306741247306,3.61123339083883,
134.146061322491));
#119997=CARTESIAN_POINT('Ctrl Pts',(-180.314497550048,3.70148804412907,
134.042904938966));
#119998=CARTESIAN_POINT('Ctrl Pts',(-180.322257992563,3.79179086904529,
133.939693497773));
#119999=CARTESIAN_POINT('Ctrl Pts',(-180.330018435077,3.87770192656671,
133.832784115665));
#120000=CARTESIAN_POINT('Ctrl Pts',(-180.337778877591,3.95892364470687,
133.722597523282));
#120001=CARTESIAN_POINT('Ctrl Pts',(-180.345551777856,4.04027574715952,
133.612234049598));
#120002=CARTESIAN_POINT('Ctrl Pts',(-180.353324678122,4.1169232486707,133.498583177072));
#120003=CARTESIAN_POINT('Ctrl Pts',(-180.361097578387,4.18861259696973,
133.38209364777));
#120004=CARTESIAN_POINT('Ctrl Pts',(-180.368587914149,4.25769585688294,
133.269838806279));
#120005=CARTESIAN_POINT('Ctrl Pts',(-180.376078249911,4.32217503704249,
133.154948378128));
#120006=CARTESIAN_POINT('Ctrl Pts',(-180.383568585673,4.3818653030435,133.037842099129));
#120007=CARTESIAN_POINT('Ctrl Pts',(-180.391342919792,4.44381874362301,
132.916295699966));
#120008=CARTESIAN_POINT('Ctrl Pts',(-180.399117253911,4.50080920799675,
132.791977082604));
#120009=CARTESIAN_POINT('Ctrl Pts',(-180.40689158803,4.5525791567958,132.665329742406));
#120010=CARTESIAN_POINT('Ctrl Pts',(-180.414656340977,4.60428530375948,
132.538838483737));
#120011=CARTESIAN_POINT('Ctrl Pts',(-180.422421093925,4.65078359001705,
132.410024570987));
#120012=CARTESIAN_POINT('Ctrl Pts',(-180.430185846872,4.69186221257831,
132.27935622457));
#120013=CARTESIAN_POINT('Ctrl Pts',(-180.437942887757,4.73290003527265,
132.148817659796));
#120014=CARTESIAN_POINT('Ctrl Pts',(-180.445699928642,4.76852878996476,
132.016428697274));
#120015=CARTESIAN_POINT('Ctrl Pts',(-180.453456969527,4.79858480156904,
131.882677344994));
#120016=CARTESIAN_POINT('Ctrl Pts',(-180.461208160767,4.8286181477013,131.749026855648));
#120017=CARTESIAN_POINT('Ctrl Pts',(-180.468959352007,4.85308703009387,
131.614016401407));
#120018=CARTESIAN_POINT('Ctrl Pts',(-180.476710543247,4.87187774906408,
131.478148611429));
#120019=CARTESIAN_POINT('Ctrl Pts',(-180.484458440024,4.89066048147738,
131.342338568887));
#120020=CARTESIAN_POINT('Ctrl Pts',(-180.492206336801,4.90376979703001,
131.205672301821));
#120021=CARTESIAN_POINT('Ctrl Pts',(-180.499954233578,4.91114323895842,
131.068661864126));
#120022=CARTESIAN_POINT('Ctrl Pts',(-180.507700509662,4.91851513852172,
130.93168008606));
#120023=CARTESIAN_POINT('Ctrl Pts',(-180.515446785746,4.92015352997405,
130.794354670717));
#120024=CARTESIAN_POINT('Ctrl Pts',(-180.523193061831,4.91604793428645,
130.657201620906));
#120025=CARTESIAN_POINT('Ctrl Pts',(-180.530939395096,4.91194230829228,
130.520047558662));
#120026=CARTESIAN_POINT('Ctrl Pts',(-180.538685728361,4.9020926222485,130.38306625528));
#120027=CARTESIAN_POINT('Ctrl Pts',(-180.546432061627,4.88654050952772,
130.246772139166));
#120028=CARTESIAN_POINT('Ctrl Pts',(-180.55418012963,4.8709849140191,130.110447500929));
#120029=CARTESIAN_POINT('Ctrl Pts',(-180.561928197633,4.84972439502942,
129.974810744557));
#120030=CARTESIAN_POINT('Ctrl Pts',(-180.569676265636,4.82285223134933,
129.84036921871));
#120031=CARTESIAN_POINT('Ctrl Pts',(-180.577432568377,4.795951507614,129.70578480681));
#120032=CARTESIAN_POINT('Ctrl Pts',(-180.585188871119,4.76342730196317,
129.572398547));
#120033=CARTESIAN_POINT('Ctrl Pts',(-180.592945173861,4.72542375965904,
129.440706206012));
#120034=CARTESIAN_POINT('Ctrl Pts',(-180.600705616375,4.68739993372011,
129.308943576857));
#120035=CARTESIAN_POINT('Ctrl Pts',(-180.608466058889,4.64389106780674,
129.178877038601));
#120036=CARTESIAN_POINT('Ctrl Pts',(-180.616226501404,4.59509028959371,
129.050984362171));
#120037=CARTESIAN_POINT('Ctrl Pts',(-180.623999401669,4.54621117203903,
128.922886381063));
#120038=CARTESIAN_POINT('Ctrl Pts',(-180.631772301934,4.49202332100907,
128.796969594594));
#120039=CARTESIAN_POINT('Ctrl Pts',(-180.6395452022,4.43276722471806,128.67368987952));
#120040=CARTESIAN_POINT('Ctrl Pts',(-180.647035537962,4.37566523678433,
128.554891692612));
#120041=CARTESIAN_POINT('Ctrl Pts',(-180.654525873724,4.31385723758189,
128.438542449427));
#120042=CARTESIAN_POINT('Ctrl Pts',(-180.662016209486,4.24759645522655,
128.325024533844));
#120043=CARTESIAN_POINT('Ctrl Pts',(-180.669790543605,4.17882337516859,
128.207202551989));
#120044=CARTESIAN_POINT('Ctrl Pts',(-180.677564877724,4.10503533955871,
128.092057610922));
#120045=CARTESIAN_POINT('Ctrl Pts',(-180.685339211843,4.02646626728858,
127.980046105886));
#120046=CARTESIAN_POINT('Ctrl Pts',(-180.69310396479,3.94799402437853,127.86817264502));
#120047=CARTESIAN_POINT('Ctrl Pts',(-180.700868717737,3.86475269088806,
127.759425253595));
#120048=CARTESIAN_POINT('Ctrl Pts',(-180.708633470684,3.77702170922281,
127.654235212037));
#120049=CARTESIAN_POINT('Ctrl Pts',(-180.71639051157,3.68937786320486,127.54914964671));
#120050=CARTESIAN_POINT('Ctrl Pts',(-180.724147552455,3.59725349177691,
127.447614698306));
#120051=CARTESIAN_POINT('Ctrl Pts',(-180.73190459334,3.50097069949896,127.350031851547));
#120052=CARTESIAN_POINT('Ctrl Pts',(-180.73965578458,3.40476051482377,127.252522592771));
#120053=CARTESIAN_POINT('Ctrl Pts',(-180.74740697582,3.30439842459542,127.158959780689));
#120054=CARTESIAN_POINT('Ctrl Pts',(-180.75515816706,3.20024584750376,127.0697107574));
#120055=CARTESIAN_POINT('Ctrl Pts',(-180.762906063837,3.09613753803588,
126.980499667328));
#120056=CARTESIAN_POINT('Ctrl Pts',(-180.770653960614,2.98824224223235,
126.89559897327));
#120057=CARTESIAN_POINT('Ctrl Pts',(-180.778401857391,2.87695700613077,
126.815337999508));
#120058=CARTESIAN_POINT('Ctrl Pts',(-180.786148133475,2.76569504850156,
126.735093814613));
#120059=CARTESIAN_POINT('Ctrl Pts',(-180.793894409559,2.65104487791537,
126.659487648129));
#120060=CARTESIAN_POINT('Ctrl Pts',(-180.801640685643,2.53343495797927,
126.588807228485));
#120061=CARTESIAN_POINT('Ctrl Pts',(-180.809387018909,2.41582416987298,
126.518126287095));
#120062=CARTESIAN_POINT('Ctrl Pts',(-180.817133352174,2.29525392392618,
126.452371366488));
#120063=CARTESIAN_POINT('Ctrl Pts',(-180.82487968544,2.17217952718222,126.39178550045));
#120064=CARTESIAN_POINT('Ctrl Pts',(-180.832627753443,2.04907756878062,
126.331186066628));
#120065=CARTESIAN_POINT('Ctrl Pts',(-180.840375821446,1.92347069438084,
126.275758163452));
#120066=CARTESIAN_POINT('Ctrl Pts',(-180.848123889449,1.79583617024562,
126.225697547178));
#120067=CARTESIAN_POINT('Ctrl Pts',(-180.855880192191,1.66806599461945,
126.175583725885));
#120068=CARTESIAN_POINT('Ctrl Pts',(-180.863636494932,1.53826422894359,
126.130848729665));
#120069=CARTESIAN_POINT('Ctrl Pts',(-180.871392797674,1.40692588984619,
126.091639259053));
#120070=CARTESIAN_POINT('Ctrl Pts',(-180.879153240188,1.2755174515227,126.052408861167));
#120071=CARTESIAN_POINT('Ctrl Pts',(-180.886913682703,1.14257118442251,
126.018709961316));
#120072=CARTESIAN_POINT('Ctrl Pts',(-180.894674125217,1.00859344098332,
125.990638322574));
#120073=CARTESIAN_POINT('Ctrl Pts',(-180.902447025482,0.874400624576381,
125.962521620745));
#120074=CARTESIAN_POINT('Ctrl Pts',(-180.910219925748,0.739173408878079,
125.940050295721));
#120075=CARTESIAN_POINT('Ctrl Pts',(-180.917992826013,0.603425325667191,
125.923268430479));
#120076=CARTESIAN_POINT('Ctrl Pts',(-180.925483161775,0.472612027210911,
125.907096628309));
#120077=CARTESIAN_POINT('Ctrl Pts',(-180.932973497537,0.341315380425482,
125.896207840602));
#120078=CARTESIAN_POINT('Ctrl Pts',(-180.940463833299,0.20999397167983,
125.890595707199));
#120079=CARTESIAN_POINT('Ctrl Pts',(-180.948238167418,0.0736934718059715,
125.884770788052));
#120080=CARTESIAN_POINT('Ctrl Pts',(-180.956012501537,-0.0630654638079416,
125.884612098978));
#120081=CARTESIAN_POINT('Ctrl Pts',(-180.963786835656,-0.199772418043521,
125.890169530165));
#120082=CARTESIAN_POINT('Ctrl Pts',(-180.971551588603,-0.336310893175113,
125.895720112316));
#120083=CARTESIAN_POINT('Ctrl Pts',(-180.97931634155,-0.472797127501037,
125.90697278233));
#120084=CARTESIAN_POINT('Ctrl Pts',(-180.987081094497,-0.608717227139118,
125.923925555004));
#120085=CARTESIAN_POINT('Ctrl Pts',(-180.994838135382,-0.744502329018101,
125.940861489945));
#120086=CARTESIAN_POINT('Ctrl Pts',(-181.002595176267,-0.87972202974887,
125.963486212983));
#120087=CARTESIAN_POINT('Ctrl Pts',(-181.010352217152,-1.01386444348082,
125.99174574073));
#120088=CARTESIAN_POINT('Ctrl Pts',(-181.018103408392,-1.14790569937564,
126.019983957747));
#120089=CARTESIAN_POINT('Ctrl Pts',(-181.025854599632,-1.28087090426565,
126.053848441329));
#120090=CARTESIAN_POINT('Ctrl Pts',(-181.033605790873,-1.41225564720813,
126.093233677074));
#120091=CARTESIAN_POINT('Ctrl Pts',(-181.04135368765,-1.54358454812987,
126.132602173044));
#120092=CARTESIAN_POINT('Ctrl Pts',(-181.049101584427,-1.67333394942435,
126.177486642203));
#120093=CARTESIAN_POINT('Ctrl Pts',(-181.056849481204,-1.80101216816459,
126.227731046296));
#120094=CARTESIAN_POINT('Ctrl Pts',(-181.064595757288,-1.92866367937423,
126.277964940342));
#120095=CARTESIAN_POINT('Ctrl Pts',(-181.072342033372,-2.05424450620277,
126.333556396151));
#120096=CARTESIAN_POINT('Ctrl Pts',(-181.080088309456,-2.17728097953044,
126.394300459396));
#120097=CARTESIAN_POINT('Ctrl Pts',(-181.087834642722,-2.3003183610849,
126.455044971041));
#120098=CARTESIAN_POINT('Ctrl Pts',(-181.095580975987,-2.42081100109293,
126.520941992941));
#120099=CARTESIAN_POINT('Ctrl Pts',(-181.103327309252,-2.53830832377024,
126.591739828084));
#120100=CARTESIAN_POINT('Ctrl Pts',(-181.111075377255,-2.65583195915813,
126.662553517911));
#120101=CARTESIAN_POINT('Ctrl Pts',(-181.118823445258,-2.77035860763099,
126.738270003146));
#120102=CARTESIAN_POINT('Ctrl Pts',(-181.126571513261,-2.88146559983368,
126.818593557203));
#120103=CARTESIAN_POINT('Ctrl Pts',(-181.134327816003,-2.99269067787002,
126.89900248009));
#120104=CARTESIAN_POINT('Ctrl Pts',(-181.142084118745,-3.1004885220833,
126.984028023559));
#120105=CARTESIAN_POINT('Ctrl Pts',(-181.149840421487,-3.20446814057772,
127.073333011326));
#120106=CARTESIAN_POINT('Ctrl Pts',(-181.157600864001,-3.30850325612586,
127.162685663855));
#120107=CARTESIAN_POINT('Ctrl Pts',(-181.165361306515,-3.40871579973424,
127.25632204509));
#120108=CARTESIAN_POINT('Ctrl Pts',(-181.173121749029,-3.5047515073558,
127.353867908664));
#120109=CARTESIAN_POINT('Ctrl Pts',(-181.180894649295,-3.60094138002062,
127.451570361518));
#120110=CARTESIAN_POINT('Ctrl Pts',(-181.18866754956,-3.69294075537735,
127.55319454785));
#120111=CARTESIAN_POINT('Ctrl Pts',(-181.196440449825,-3.78043496869995,
127.658332246758));
#120112=CARTESIAN_POINT('Ctrl Pts',(-181.203930785587,-3.86474854698411,
127.759647925484));
#120113=CARTESIAN_POINT('Ctrl Pts',(-181.21142112135,-3.94487863715625,
127.864225857211));
#120114=CARTESIAN_POINT('Ctrl Pts',(-181.218911457112,-4.02058271306412,
127.971676782418));
#120115=CARTESIAN_POINT('Ctrl Pts',(-181.226774298583,-4.10005166699623,
128.084471404409));
#120116=CARTESIAN_POINT('Ctrl Pts',(-181.234637140055,-4.174892552443,128.200785850527));
#120117=CARTESIAN_POINT('Ctrl Pts',(-181.242499981526,-4.24478179121977,
128.320208728605));
#120118=CARTESIAN_POINT('Ctrl Pts',(-181.250349252588,-4.31455040877096,
128.439425495782));
#120119=CARTESIAN_POINT('Ctrl Pts',(-181.25819852365,-4.37938421453783,
128.56173968249));
#120120=CARTESIAN_POINT('Ctrl Pts',(-181.266047794713,-4.43900175716958,
128.686709451216));
#120121=CARTESIAN_POINT('Ctrl Pts',(-181.273889191536,-4.49855949261664,
128.811553852646));
#120122=CARTESIAN_POINT('Ctrl Pts',(-181.281730588359,-4.55291121398804,
128.939048195462));
#120123=CARTESIAN_POINT('Ctrl Pts',(-181.289571985181,-4.60182013260226,
129.0687239823));
#120124=CARTESIAN_POINT('Ctrl Pts',(-181.297405522347,-4.65068002839995,
129.198269791365));
#120125=CARTESIAN_POINT('Ctrl Pts',(-181.305239059512,-4.69410785428418,
129.329992335658));
#120126=CARTESIAN_POINT('Ctrl Pts',(-181.313072596677,-4.73191416286347,
129.463401476581));
#120127=CARTESIAN_POINT('Ctrl Pts',(-181.315395044115,-4.74312278581986,
129.502953943239));
#120128=CARTESIAN_POINT('Ctrl Pts',(-181.317717491553,-4.75383761304045,
129.542654522032));
#120129=CARTESIAN_POINT('Ctrl Pts',(-181.320039938991,-4.76405452823418,
129.582490119309));
#120130=CARTESIAN_POINT('Origin',(213.235140564004,0.,130.804360617566));
#120131=CARTESIAN_POINT('',(-183.415149158805,-4.76405452823414,129.582490119309));
#120132=CARTESIAN_POINT('',(-183.069718605797,-4.76405452823406,129.582490119308));
#120133=CARTESIAN_POINT('',(213.235140564004,-4.76405452823405,129.582490119308));
#120134=CARTESIAN_POINT('',(-181.735140563977,-4.91824950327072,130.806571064885));
#120135=CARTESIAN_POINT('Ctrl Pts',(-181.735140564012,-4.91824950327044,
130.806571065507));
#120136=CARTESIAN_POINT('Ctrl Pts',(-181.742166278867,-4.91819404319526,
130.929969803894));
#120137=CARTESIAN_POINT('Ctrl Pts',(-181.749191993722,-4.91349490493225,
131.053259845395));
#120138=CARTESIAN_POINT('Ctrl Pts',(-181.756217708576,-4.90417395891944,
131.176195047328));
#120139=CARTESIAN_POINT('Ctrl Pts',(-181.763992042696,-4.89385982717492,
131.312229508533));
#120140=CARTESIAN_POINT('Ctrl Pts',(-181.771766376815,-4.87786497991832,
131.448049965438));
#120141=CARTESIAN_POINT('Ctrl Pts',(-181.779540710934,-4.85620016088216,
131.583143681036));
#120142=CARTESIAN_POINT('Ctrl Pts',(-181.787305463881,-4.83456204179922,
131.718070905703));
#120143=CARTESIAN_POINT('Ctrl Pts',(-181.795070216828,-4.80726791575691,
131.852272788801));
#120144=CARTESIAN_POINT('Ctrl Pts',(-181.802834969775,-4.77438044942487,
131.98523926783));
#120145=CARTESIAN_POINT('Ctrl Pts',(-181.81059201066,-4.74152564738802,
132.118073682678));
#120146=CARTESIAN_POINT('Ctrl Pts',(-181.818349051545,-4.70308865379099,
132.249674758213));
#120147=CARTESIAN_POINT('Ctrl Pts',(-181.82610609243,-4.6591835323683,132.379540567352));
#120148=CARTESIAN_POINT('Ctrl Pts',(-181.833857283671,-4.61531152013915,
132.509308443675));
#120149=CARTESIAN_POINT('Ctrl Pts',(-181.841608474911,-4.56597971248463,
132.637343289375));
#120150=CARTESIAN_POINT('Ctrl Pts',(-181.849359666151,-4.51135246061705,
132.763156686223));
#120151=CARTESIAN_POINT('Ctrl Pts',(-181.857107562928,-4.45674842678867,
132.888916609021));
#120152=CARTESIAN_POINT('Ctrl Pts',(-181.864855459705,-4.39685358061205,
133.012456602989));
#120153=CARTESIAN_POINT('Ctrl Pts',(-181.872603356482,-4.33188094023251,
133.133306856136));
#120154=CARTESIAN_POINT('Ctrl Pts',(-181.880349632566,-4.26692189072869,
133.254131830015));
#120155=CARTESIAN_POINT('Ctrl Pts',(-181.888095908651,-4.19688734474357,
133.372267838051));
#120156=CARTESIAN_POINT('Ctrl Pts',(-181.895842184735,-4.12203676652123,
133.487268733389));
#120157=CARTESIAN_POINT('Ctrl Pts',(-181.903588518,-4.04718563576903,133.602270477636));
#120158=CARTESIAN_POINT('Ctrl Pts',(-181.911334851265,-3.9675186151122,
133.714136735334));
#120159=CARTESIAN_POINT('Ctrl Pts',(-181.919081184531,-3.88333885679162,
133.822449812045));
#120160=CARTESIAN_POINT('Ctrl Pts',(-181.926829252534,-3.79914024699795,
133.930787144718));
#120161=CARTESIAN_POINT('Ctrl Pts',(-181.934577320537,-3.71042712844116,
134.035569404395));
#120162=CARTESIAN_POINT('Ctrl Pts',(-181.94232538854,-3.61754307876341,
134.136411808018));
#120163=CARTESIAN_POINT('Ctrl Pts',(-181.950081691281,-3.52456031081195,
134.237361388148));
#120164=CARTESIAN_POINT('Ctrl Pts',(-181.957837994024,-3.42739802181008,
134.334362459562));
#120165=CARTESIAN_POINT('Ctrl Pts',(-181.965594296765,-3.32643720759424,
134.427066590514));
#120166=CARTESIAN_POINT('Ctrl Pts',(-181.97335473928,-3.22542250755198,
134.519820200452));
#120167=CARTESIAN_POINT('Ctrl Pts',(-181.981115181794,-3.12060554120253,
134.608272048101));
#120168=CARTESIAN_POINT('Ctrl Pts',(-181.988875624308,-3.01239977711739,
134.692114550793));
#120169=CARTESIAN_POINT('Ctrl Pts',(-181.996648524573,-2.90402031153368,
134.776091644914));
#120170=CARTESIAN_POINT('Ctrl Pts',(-182.004421424839,-2.79224149634652,
134.85544438141));
#120171=CARTESIAN_POINT('Ctrl Pts',(-182.012194325104,-2.67750585984077,
134.929908512454));
#120172=CARTESIAN_POINT('Ctrl Pts',(-182.019684660866,-2.5669411527255,
135.001665684771));
#120173=CARTESIAN_POINT('Ctrl Pts',(-182.027174996628,-2.4536311327147,
135.068883350007));
#120174=CARTESIAN_POINT('Ctrl Pts',(-182.03466533239,-2.33799097923109,
135.131366654485));
#120175=CARTESIAN_POINT('Ctrl Pts',(-182.042439666509,-2.21796629417824,
135.196219032444));
#120176=CARTESIAN_POINT('Ctrl Pts',(-182.050214000628,-2.09505109151086,
135.256176389005));
#120177=CARTESIAN_POINT('Ctrl Pts',(-182.057988334747,-1.96968255864387,
135.310970616298));
#120178=CARTESIAN_POINT('Ctrl Pts',(-182.065753087694,-1.84446853128913,
135.365697314603));
#120179=CARTESIAN_POINT('Ctrl Pts',(-182.073517840642,-1.71680754442264,
135.415273389231));
#120180=CARTESIAN_POINT('Ctrl Pts',(-182.081282593589,-1.5871626009352,
135.459475862186));
#120181=CARTESIAN_POINT('Ctrl Pts',(-182.089039634474,-1.45764642263331,
135.503634432622));
#120182=CARTESIAN_POINT('Ctrl Pts',(-182.096796675359,-1.32615057673516,
135.542429897177));
#120183=CARTESIAN_POINT('Ctrl Pts',(-182.104553716244,-1.19315900294414,
135.575686917055));
#120184=CARTESIAN_POINT('Ctrl Pts',(-182.112304907484,-1.06026771913327,
135.608918857555));
#120185=CARTESIAN_POINT('Ctrl Pts',(-182.120056098724,-0.925883330276927,
135.636620572151));
#120186=CARTESIAN_POINT('Ctrl Pts',(-182.127807289964,-0.790505592309228,
135.65866633219));
#120187=CARTESIAN_POINT('Ctrl Pts',(-182.135555186741,-0.655185393491669,
135.680702722192));
#120188=CARTESIAN_POINT('Ctrl Pts',(-182.143303083518,-0.518873070360332,
135.697087876165));
#120189=CARTESIAN_POINT('Ctrl Pts',(-182.151050980295,-0.382079030561141,
135.70774706745));
#120190=CARTESIAN_POINT('Ctrl Pts',(-182.15879725638,-0.245313605126137,
135.718404029062));
#120191=CARTESIAN_POINT('Ctrl Pts',(-182.166543532464,-0.108067052986587,
135.723337380018));
#120192=CARTESIAN_POINT('Ctrl Pts',(-182.174289808548,0.0291450231112156,
135.722524261664));
#120193=CARTESIAN_POINT('Ctrl Pts',(-182.182036141813,0.16635811207758,
135.721711137307));
#120194=CARTESIAN_POINT('Ctrl Pts',(-182.189782475079,0.303536333536031,
135.715151461312));
#120195=CARTESIAN_POINT('Ctrl Pts',(-182.197528808344,0.440164408135673,
135.702874510198));
#120196=CARTESIAN_POINT('Ctrl Pts',(-182.205276876347,0.576823079645122,
135.690594809746));
#120197=CARTESIAN_POINT('Ctrl Pts',(-182.21302494435,0.712930969817092,
135.672595321422));
#120198=CARTESIAN_POINT('Ctrl Pts',(-182.220773012353,0.847978637660013,
135.648957122186));
#120199=CARTESIAN_POINT('Ctrl Pts',(-182.228529315095,0.983169835771588,
135.62529379999));
#120200=CARTESIAN_POINT('Ctrl Pts',(-182.236285617837,1.1172981748916,135.595979862955));
#120201=CARTESIAN_POINT('Ctrl Pts',(-182.244041920579,1.24986457196712,
135.5611475178));
#120202=CARTESIAN_POINT('Ctrl Pts',(-182.251802363093,1.38250172372027,
135.526296581574));
#120203=CARTESIAN_POINT('Ctrl Pts',(-182.259562805607,1.51357489884223,
135.485921483424));
#120204=CARTESIAN_POINT('Ctrl Pts',(-182.267323248121,1.64260182946052,
135.440203830225));
#120205=CARTESIAN_POINT('Ctrl Pts',(-182.275096148387,1.77183588556232,
135.39441278699));
#120206=CARTESIAN_POINT('Ctrl Pts',(-182.282869048652,1.89901677012015,
135.343262196406));
#120207=CARTESIAN_POINT('Ctrl Pts',(-182.290641948918,2.02368296660664,
135.286981537649));
#120208=CARTESIAN_POINT('Ctrl Pts',(-182.298132284679,2.14381723283161,
135.232746822602));
#120209=CARTESIAN_POINT('Ctrl Pts',(-182.305622620441,2.26161619186303,
135.173748683604));
#120210=CARTESIAN_POINT('Ctrl Pts',(-182.313112956203,2.37669149316271,
135.11023109969));
#120211=CARTESIAN_POINT('Ctrl Pts',(-182.320887290322,2.49612990949109,
135.044305227274));
#120212=CARTESIAN_POINT('Ctrl Pts',(-182.328661624441,2.61301240105838,
134.973301601892));
#120213=CARTESIAN_POINT('Ctrl Pts',(-182.33643595856,2.72687709064381,134.897443122845));
#120214=CARTESIAN_POINT('Ctrl Pts',(-182.344200711507,2.84060145217569,
134.821678132594));
#120215=CARTESIAN_POINT('Ctrl Pts',(-182.351965464454,2.9513150895211,134.741070408096));
#120216=CARTESIAN_POINT('Ctrl Pts',(-182.359730217402,3.05858014060573,
134.655888961742));
#120217=CARTESIAN_POINT('Ctrl Pts',(-182.367487258287,3.16573865452946,
134.570792118802));
#120218=CARTESIAN_POINT('Ctrl Pts',(-182.375244299171,3.26945509427675,
134.481130835716));
#120219=CARTESIAN_POINT('Ctrl Pts',(-182.383001340056,3.369320361121,134.387217489761));
#120220=CARTESIAN_POINT('Ctrl Pts',(-182.390752531297,3.46911031879082,
134.29337496459));
#120221=CARTESIAN_POINT('Ctrl Pts',(-182.398503722537,3.56505460053173,
134.195287025673));
#120222=CARTESIAN_POINT('Ctrl Pts',(-182.406254913777,3.6567772969768,134.093306172423));
#120223=CARTESIAN_POINT('Ctrl Pts',(-182.414002810554,3.74846100882897,
133.991368663756));
#120224=CARTESIAN_POINT('Ctrl Pts',(-182.421750707331,3.83592644318413,
133.885541821693));
#120225=CARTESIAN_POINT('Ctrl Pts',(-182.429498604108,3.91883484258758,
133.776214675056));
#120226=CARTESIAN_POINT('Ctrl Pts',(-182.437244880192,4.00172589934117,
133.666910397302));
#120227=CARTESIAN_POINT('Ctrl Pts',(-182.444991156276,4.08006158108549,
133.554107582659));
#120228=CARTESIAN_POINT('Ctrl Pts',(-182.45273743236,4.15354396030729,133.438227666658));
#120229=CARTESIAN_POINT('Ctrl Pts',(-182.460483765626,4.22702688195942,
133.322346895258));
#120230=CARTESIAN_POINT('Ctrl Pts',(-182.468230098891,4.29565622022754,
133.203389307352));
#120231=CARTESIAN_POINT('Ctrl Pts',(-182.475976432157,4.35917808520141,
133.081804246726));
#120232=CARTESIAN_POINT('Ctrl Pts',(-182.48372450016,4.42271417545642,132.960191957968));
#120233=CARTESIAN_POINT('Ctrl Pts',(-182.491472568163,4.48114033541539,
132.83595137209));
#120234=CARTESIAN_POINT('Ctrl Pts',(-182.499220636166,4.53424941212098,
132.709554920303));
#120235=CARTESIAN_POINT('Ctrl Pts',(-182.506976938907,4.58741493378524,
132.583024132863));
#120236=CARTESIAN_POINT('Ctrl Pts',(-182.514733241649,4.63525193190573,
132.45433326345));
#120237=CARTESIAN_POINT('Ctrl Pts',(-182.522489544391,4.67760186915715,
132.323973665732));
#120238=CARTESIAN_POINT('Ctrl Pts',(-182.530249986905,4.71997440984532,
132.193544491172));
#120239=CARTESIAN_POINT('Ctrl Pts',(-182.53801042942,4.75685394908354,132.06144518999));
#120240=CARTESIAN_POINT('Ctrl Pts',(-182.545770871934,4.78813260031306,
131.928179670759));
#120241=CARTESIAN_POINT('Ctrl Pts',(-182.553543772199,4.81946146281031,
131.794700221885));
#120242=CARTESIAN_POINT('Ctrl Pts',(-182.561316672464,4.84517139696213,
131.660051198124));
#120243=CARTESIAN_POINT('Ctrl Pts',(-182.56908957273,4.86520600914096,131.524744925501));
#120244=CARTESIAN_POINT('Ctrl Pts',(-182.576579908492,4.88451231270299,
131.394357376703));
#120245=CARTESIAN_POINT('Ctrl Pts',(-182.584070244254,4.89854872220694,
131.263359840987));
#120246=CARTESIAN_POINT('Ctrl Pts',(-182.591560580016,4.90731059117172,
131.132210925289));
#120247=CARTESIAN_POINT('Ctrl Pts',(-182.599334914135,4.91640466906136,
130.99608945859));
#120248=CARTESIAN_POINT('Ctrl Pts',(-182.607109248254,4.91984514980589,
130.859373714271));
#120249=CARTESIAN_POINT('Ctrl Pts',(-182.614883582373,4.91756990898058,
130.722572765236));
#120250=CARTESIAN_POINT('Ctrl Pts',(-182.62264833532,4.91529747218625,130.585940411145));
#120251=CARTESIAN_POINT('Ctrl Pts',(-182.630413088267,4.90732333595251,
130.449223448429));
#120252=CARTESIAN_POINT('Ctrl Pts',(-182.638177841215,4.89363715287714,
130.31293567062));
#120253=CARTESIAN_POINT('Ctrl Pts',(-182.6459348821,4.87996456311174,130.176783255754));
#120254=CARTESIAN_POINT('Ctrl Pts',(-182.653691922985,4.86059125541069,
130.041059563987));
#120255=CARTESIAN_POINT('Ctrl Pts',(-182.66144896387,4.83555891376832,129.906277629209));
#120256=CARTESIAN_POINT('Ctrl Pts',(-182.66920015511,4.81054544920946,129.771597334537));
#120257=CARTESIAN_POINT('Ctrl Pts',(-182.67695134635,4.77988151605426,129.63785776611));
#120258=CARTESIAN_POINT('Ctrl Pts',(-182.68470253759,4.74366049384699,129.505565721666));
#120259=CARTESIAN_POINT('Ctrl Pts',(-182.692450434367,4.70745486654033,
129.37332990487));
#120260=CARTESIAN_POINT('Ctrl Pts',(-182.700198331144,4.66569695087129,
129.242540764698));
#120261=CARTESIAN_POINT('Ctrl Pts',(-182.707946227921,4.618530941128,129.11369358697));
#120262=CARTESIAN_POINT('Ctrl Pts',(-182.715692504005,4.57137479749729,
128.984873361295));
#120263=CARTESIAN_POINT('Ctrl Pts',(-182.72343878009,4.51881294423457,128.857994656986));
#120264=CARTESIAN_POINT('Ctrl Pts',(-182.731185056174,4.46103890988972,
128.733535925094));
#120265=CARTESIAN_POINT('Ctrl Pts',(-182.738931389439,4.40326444907,128.609076274477));
#120266=CARTESIAN_POINT('Ctrl Pts',(-182.746677722704,4.34027789500933,
128.487036986544));
#120267=CARTESIAN_POINT('Ctrl Pts',(-182.75442405597,4.27232005966242,128.36787454736));
#120268=CARTESIAN_POINT('Ctrl Pts',(-182.762172123973,4.20434700562956,
128.248685422574));
#120269=CARTESIAN_POINT('Ctrl Pts',(-182.769920191976,4.13140064865017,
128.132374768074));
#120270=CARTESIAN_POINT('Ctrl Pts',(-182.777668259979,4.05376648724896,
128.019372228119));
#120271=CARTESIAN_POINT('Ctrl Pts',(-182.78542456272,3.97604981533704,127.906249587719));
#120272=CARTESIAN_POINT('Ctrl Pts',(-182.793180865462,3.89363560815299,
127.796442408019));
#120273=CARTESIAN_POINT('Ctrl Pts',(-182.800937168204,3.80685156215607,
127.69034965962));
#120274=CARTESIAN_POINT('Ctrl Pts',(-182.808697610718,3.72002119690079,
127.584200286326));
#120275=CARTESIAN_POINT('Ctrl Pts',(-182.816458053233,3.62881660536122,
127.481769586489));
#120276=CARTESIAN_POINT('Ctrl Pts',(-182.824218495747,3.5336034247693,127.383420703016));
#120277=CARTESIAN_POINT('Ctrl Pts',(-182.831991396012,3.43823739952725,
127.284913941185));
#120278=CARTESIAN_POINT('Ctrl Pts',(-182.839764296278,3.33885020978783,
127.190502359112));
#120279=CARTESIAN_POINT('Ctrl Pts',(-182.847537196543,3.23584240781202,
127.100510327084));
#120280=CARTESIAN_POINT('Ctrl Pts',(-182.855027532305,3.1365791988993,127.013789732096));
#120281=CARTESIAN_POINT('Ctrl Pts',(-182.862517868067,3.03395428425488,
126.931173135403));
#120282=CARTESIAN_POINT('Ctrl Pts',(-182.870008203829,2.92835099134394,
126.852912334468));
#120283=CARTESIAN_POINT('Ctrl Pts',(-182.877782537948,2.818743717485,126.77168425148));
#120284=CARTESIAN_POINT('Ctrl Pts',(-182.885556872067,2.70558055367971,
126.694891478318));
#120285=CARTESIAN_POINT('Ctrl Pts',(-182.893331206186,2.58925621761079,
126.622861448361));
#120286=CARTESIAN_POINT('Ctrl Pts',(-182.901095959133,2.47307524088987,
126.550920188978));
#120287=CARTESIAN_POINT('Ctrl Pts',(-182.90886071208,2.35374117271796,126.483730197785));
#120288=CARTESIAN_POINT('Ctrl Pts',(-182.916625465027,2.23168068912202,
126.4215778983));
#120289=CARTESIAN_POINT('Ctrl Pts',(-182.924382505912,2.10974143771914,
126.359487329355));
#120290=CARTESIAN_POINT('Ctrl Pts',(-182.932139546797,1.98508150590871,
126.302424671168));
#120291=CARTESIAN_POINT('Ctrl Pts',(-182.939896587682,1.85815505485159,
126.250632161166));
#120292=CARTESIAN_POINT('Ctrl Pts',(-182.947647778922,1.73132432001839,
126.198878708298));
#120293=CARTESIAN_POINT('Ctrl Pts',(-182.955398970163,1.60223082852072,
126.152387640204));
#120294=CARTESIAN_POINT('Ctrl Pts',(-182.963150161403,1.47135143757472,
126.111354330585));
#120295=CARTESIAN_POINT('Ctrl Pts',(-182.97089805818,1.34052767386137,126.070338461217));
#120296=CARTESIAN_POINT('Ctrl Pts',(-182.978645954957,1.20791989268096,
126.034775853349));
#120297=CARTESIAN_POINT('Ctrl Pts',(-182.986393851734,1.07402273255796,
126.004812906328));
#120298=CARTESIAN_POINT('Ctrl Pts',(-182.994140127818,0.940153580834378,
125.97485622691));
#120299=CARTESIAN_POINT('Ctrl Pts',(-183.001886403902,0.804995967924261,
125.950496963824));
#120300=CARTESIAN_POINT('Ctrl Pts',(-183.009632679986,0.669057035157692,
125.931830910504));
#120301=CARTESIAN_POINT('Ctrl Pts',(-183.017379013251,0.533117098920988,
125.913164719394));
#120302=CARTESIAN_POINT('Ctrl Pts',(-183.025125346517,0.39639621864993,
125.900191875094));
#120303=CARTESIAN_POINT('Ctrl Pts',(-183.032871679782,0.259408613742112,
125.892956517554));
#120304=CARTESIAN_POINT('Ctrl Pts',(-183.040619747785,0.122390331409793,
125.885719539705));
#120305=CARTESIAN_POINT('Ctrl Pts',(-183.048367815788,-0.0148944040710403,
125.884222625977));
#120306=CARTESIAN_POINT('Ctrl Pts',(-183.056115883791,-0.151929801890471,
125.888457811591));
#120307=CARTESIAN_POINT('Ctrl Pts',(-183.063872186533,-0.289110842561633,
125.89269749841));
#120308=CARTESIAN_POINT('Ctrl Pts',(-183.071628489275,-0.426041624805545,
125.902681442188));
#120309=CARTESIAN_POINT('Ctrl Pts',(-183.079384792016,-0.562209355415556,
125.918349595967));
#120310=CARTESIAN_POINT('Ctrl Pts',(-183.08714523453,-0.698449762843326,
125.934026112312));
#120311=CARTESIAN_POINT('Ctrl Pts',(-183.094905677045,-0.833925921127289,
125.955392822951));
#120312=CARTESIAN_POINT('Ctrl Pts',(-183.102666119559,-0.968134671998613,
125.982338394538));
#120313=CARTESIAN_POINT('Ctrl Pts',(-183.110439019824,-1.10255886667133,
126.009327221549));
#120314=CARTESIAN_POINT('Ctrl Pts',(-183.11821192009,-1.2357112082651,126.041912712826));
#120315=CARTESIAN_POINT('Ctrl Pts',(-183.125984820355,-1.36710228659016,
126.079933202471));
#120316=CARTESIAN_POINT('Ctrl Pts',(-183.133475156117,-1.49371696826858,
126.116571551551));
#120317=CARTESIAN_POINT('Ctrl Pts',(-183.14096549188,-1.61869592401328,
126.158256510196));
#120318=CARTESIAN_POINT('Ctrl Pts',(-183.148455827642,-1.74162011162668,
126.204801676833));
#120319=CARTESIAN_POINT('Ctrl Pts',(-183.15623038486,-1.86920866845707,
126.253113003952));
#120320=CARTESIAN_POINT('Ctrl Pts',(-183.164004942078,-1.99498761497027,
126.306813704835));
#120321=CARTESIAN_POINT('Ctrl Pts',(-183.171779499296,-2.11846807574788,
126.365748663978));
#120322=CARTESIAN_POINT('Ctrl Pts',(-183.179544423664,-2.24179554147299,
126.424610601388));
#120323=CARTESIAN_POINT('Ctrl Pts',(-183.187309348032,-2.36282983852742,
126.488693725991));
#120324=CARTESIAN_POINT('Ctrl Pts',(-183.195074272399,-2.48109933137568,
126.557793866607));
#120325=CARTESIAN_POINT('Ctrl Pts',(-183.202831433245,-2.59925057609296,
126.626824919564));
#120326=CARTESIAN_POINT('Ctrl Pts',(-183.210588594091,-2.71464218244685,
126.700862809964));
#120327=CARTESIAN_POINT('Ctrl Pts',(-183.218345754937,-2.82682484457249,
126.779656360033));
#120328=CARTESIAN_POINT('Ctrl Pts',(-183.226097014844,-2.93892216838622,
126.858389971173));
#120329=CARTESIAN_POINT('Ctrl Pts',(-183.233848274751,-3.04781508831774,
126.941871817109));
#120330=CARTESIAN_POINT('Ctrl Pts',(-183.241599534659,-3.15308146877894,
127.029806297684));
#120331=CARTESIAN_POINT('Ctrl Pts',(-183.249347240883,-3.25829958826959,
127.11770046336));
#120332=CARTESIAN_POINT('Ctrl Pts',(-183.257094947108,-3.35989417716957,
127.210042951671));
#120333=CARTESIAN_POINT('Ctrl Pts',(-183.264842653332,-3.45747473226868,
127.30649676398));
#120334=CARTESIAN_POINT('Ctrl Pts',(-183.272588665805,-3.55503395496101,
127.402929490203));
#120335=CARTESIAN_POINT('Ctrl Pts',(-183.280334678278,-3.6485806119105,
127.503471477585));
#120336=CARTESIAN_POINT('Ctrl Pts',(-183.28808069075,-3.73776002458828,
127.607747869501));
#120337=CARTESIAN_POINT('Ctrl Pts',(-183.295826687299,-3.82693925393412,
127.71202404705));
#120338=CARTESIAN_POINT('Ctrl Pts',(-183.303572683848,-3.91175100311841,
127.820034316536));
#120339=CARTESIAN_POINT('Ctrl Pts',(-183.311318680397,-3.9918802286738,
127.931369962791));
#120340=CARTESIAN_POINT('Ctrl Pts',(-183.319066338468,-4.07202664200908,
128.042729490627));
#120341=CARTESIAN_POINT('Ctrl Pts',(-183.326813996539,-4.14748830531724,
128.157415497046));
#120342=CARTESIAN_POINT('Ctrl Pts',(-183.33456165461,-4.21799316285316,
128.274989798444));
#120343=CARTESIAN_POINT('Ctrl Pts',(-183.342316556619,-4.28856394132185,
128.392674029965));
#120344=CARTESIAN_POINT('Ctrl Pts',(-183.350071458629,-4.35416845854172,
128.5132516133));
#120345=CARTESIAN_POINT('Ctrl Pts',(-183.357826360638,-4.4145801711371,
128.636258919051));
#120346=CARTESIAN_POINT('Ctrl Pts',(-183.365585372232,-4.47502389793923,
128.759331410527));
#120347=CARTESIAN_POINT('Ctrl Pts',(-183.373344383826,-4.53026917973013,
128.884835832641));
#120348=CARTESIAN_POINT('Ctrl Pts',(-183.38110339542,-4.58013779618434,
129.012288958713));
#120349=CARTESIAN_POINT('Ctrl Pts',(-183.388872575828,-4.63007176950502,
129.139909122444));
#120350=CARTESIAN_POINT('Ctrl Pts',(-183.396641756236,-4.67461487900791,
129.269482721212));
#120351=CARTESIAN_POINT('Ctrl Pts',(-183.404410936644,-4.71363875007996,
129.400511339244));
#120352=CARTESIAN_POINT('Ctrl Pts',(-183.407990344031,-4.73161778069228,
129.460878685434));
#120353=CARTESIAN_POINT('Ctrl Pts',(-183.411569751418,-4.74842600050534,
129.52155472689));
#120354=CARTESIAN_POINT('Ctrl Pts',(-183.415149158805,-4.76405452823414,
129.582490119309));
#120355=CARTESIAN_POINT('Ctrl Pts',(-181.664999290689,-4.76405452823418,
129.582490119309));
#120356=CARTESIAN_POINT('Ctrl Pts',(-181.672675880478,-4.79779503273996,
129.714043834293));
#120357=CARTESIAN_POINT('Ctrl Pts',(-181.680352470268,-4.82605765331497,
129.846900063432));
#120358=CARTESIAN_POINT('Ctrl Pts',(-181.688029060058,-4.84876606521478,
129.980558027547));
#120359=CARTESIAN_POINT('Ctrl Pts',(-181.695880977377,-4.87199312014276,
130.117268638917));
#120360=CARTESIAN_POINT('Ctrl Pts',(-181.703732894697,-4.88940914158996,
130.254817604855));
#120361=CARTESIAN_POINT('Ctrl Pts',(-181.711584812017,-4.90098872141958,
130.392665809464));
#120362=CARTESIAN_POINT('Ctrl Pts',(-181.719436729337,-4.9125683012492,
130.530514014073));
#120363=CARTESIAN_POINT('Ctrl Pts',(-181.727288646657,-4.91831148526274,
130.668661014282));
#120364=CARTESIAN_POINT('Ctrl Pts',(-181.735140563977,-4.91824950327072,
130.806571064884));
#120365=CARTESIAN_POINT('',(-181.389859436049,-4.91824915695527,130.807240306567));
#120366=CARTESIAN_POINT('Ctrl Pts',(-181.320039938991,-4.76405452823418,
129.582490119309));
#120367=CARTESIAN_POINT('Ctrl Pts',(-181.327866674491,-4.79848591795568,
129.716737585264));
#120368=CARTESIAN_POINT('Ctrl Pts',(-181.33569340999,-4.82725862397902,
129.852519526693));
#120369=CARTESIAN_POINT('Ctrl Pts',(-181.34352014549,-4.8502474171004,129.989325001528));
#120370=CARTESIAN_POINT('Ctrl Pts',(-181.351344753954,-4.8732299626622,
130.126093297362));
#120371=CARTESIAN_POINT('Ctrl Pts',(-181.359169362417,-4.89043165683097,
130.263884199659));
#120372=CARTESIAN_POINT('Ctrl Pts',(-181.366993970881,-4.90177834412933,
130.40217642155));
#120373=CARTESIAN_POINT('Ctrl Pts',(-181.374615792586,-4.91283096458077,
130.536884587887));
#120374=CARTESIAN_POINT('Ctrl Pts',(-181.38223761429,-4.91832830176703,
130.672068059881));
#120375=CARTESIAN_POINT('Ctrl Pts',(-181.389859435995,-4.91824915695583,
130.807240305618));
#120376=CARTESIAN_POINT('Ctrl Pts',(-181.389859436049,-4.91824915695527,
130.807240306567));
#120377=CARTESIAN_POINT('Ctrl Pts',(-181.398817739788,-4.91815613411647,
130.966114927541));
#120378=CARTESIAN_POINT('Ctrl Pts',(-181.407776043528,-4.91036021059812,
131.124708256897));
#120379=CARTESIAN_POINT('Ctrl Pts',(-181.416734347267,-4.89497108865333,
131.282315744903));
#120380=CARTESIAN_POINT('Ctrl Pts',(-181.425417497863,-4.88005464160356,
131.43508233925));
#120381=CARTESIAN_POINT('Ctrl Pts',(-181.434100648459,-4.8580046953391,
131.58692260436));
#120382=CARTESIAN_POINT('Ctrl Pts',(-181.442783799056,-4.82897206538774,
131.737212081736));
#120383=CARTESIAN_POINT('Ctrl Pts',(-181.451879679367,-4.79855944910979,
131.89464515665));
#120384=CARTESIAN_POINT('Ctrl Pts',(-181.460975559678,-4.76048430540328,
132.050376121223));
#120385=CARTESIAN_POINT('Ctrl Pts',(-181.47007143999,-4.71497645596076,
132.203710495987));
#120386=CARTESIAN_POINT('Ctrl Pts',(-181.479167320301,-4.66946860651813,
132.35704487075));
#120387=CARTESIAN_POINT('Ctrl Pts',(-181.488263200613,-4.61652822818693,
132.507982437687));
#120388=CARTESIAN_POINT('Ctrl Pts',(-181.497359080924,-4.5564403008889,
132.65585591784));
#120389=CARTESIAN_POINT('Ctrl Pts',(-181.505133415044,-4.50508258647963,
132.782244766713));
#120390=CARTESIAN_POINT('Ctrl Pts',(-181.512907749162,-4.44838078293223,
132.906695307599));
#120391=CARTESIAN_POINT('Ctrl Pts',(-181.520682083282,-4.386501677665,133.028722569754));
#120392=CARTESIAN_POINT('Ctrl Pts',(-181.528446836229,-4.32469883286472,
133.150599444214));
#120393=CARTESIAN_POINT('Ctrl Pts',(-181.536211589176,-4.25773155688373,
133.27005863679));
#120394=CARTESIAN_POINT('Ctrl Pts',(-181.543976342123,-4.18581526386889,
133.386633577433));
#120395=CARTESIAN_POINT('Ctrl Pts',(-181.551733383008,-4.11397039913011,
133.503092734203));
#120396=CARTESIAN_POINT('Ctrl Pts',(-181.559490423893,-4.0371865032356,
133.616673009293));
#120397=CARTESIAN_POINT('Ctrl Pts',(-181.567247464778,-3.95572544889312,
133.72693127291));
#120398=CARTESIAN_POINT('Ctrl Pts',(-181.574998656018,-3.87432582496551,
133.837106389913));
#120399=CARTESIAN_POINT('Ctrl Pts',(-181.582749847258,-3.78825629441504,
133.943964168621));
#120400=CARTESIAN_POINT('Ctrl Pts',(-181.590501038498,-3.69782249121197,
134.047089697521));
#120401=CARTESIAN_POINT('Ctrl Pts',(-181.598248935275,-3.60742712478753,
134.150171395321));
#120402=CARTESIAN_POINT('Ctrl Pts',(-181.605996832053,-3.51267143226317,
134.249523705019));
#120403=CARTESIAN_POINT('Ctrl Pts',(-181.61374472883,-3.41390170930395,
134.344764292532));
#120404=CARTESIAN_POINT('Ctrl Pts',(-181.621491004914,-3.31515264684154,
134.439984957767));
#120405=CARTESIAN_POINT('Ctrl Pts',(-181.629237280998,-3.21239150530955,
134.531095340363));
#120406=CARTESIAN_POINT('Ctrl Pts',(-181.636983557082,-3.10600158262843,
134.617749822881));
#120407=CARTESIAN_POINT('Ctrl Pts',(-181.644729890347,-2.99961087460092,
134.704404945062));
#120408=CARTESIAN_POINT('Ctrl Pts',(-181.652476223613,-2.88959163510988,
134.786603854625));
#120409=CARTESIAN_POINT('Ctrl Pts',(-181.660222556878,-2.77636007621668,
134.864041367291));
#120410=CARTESIAN_POINT('Ctrl Pts',(-181.667970624881,-2.66310315990082,
134.941496221552));
#120411=CARTESIAN_POINT('Ctrl Pts',(-181.675718692884,-2.54663281535994,
135.01418733648));
#120412=CARTESIAN_POINT('Ctrl Pts',(-181.683466760887,-2.4273937005275,
135.081853210796));
#120413=CARTESIAN_POINT('Ctrl Pts',(-181.691223063629,-2.30802785694534,
135.149591001208));
#120414=CARTESIAN_POINT('Ctrl Pts',(-181.698979366371,-2.18588770531916,
135.212292688746));
#120415=CARTESIAN_POINT('Ctrl Pts',(-181.706735669113,-2.06144243552465,
135.269742812577));
#120416=CARTESIAN_POINT('Ctrl Pts',(-181.714496111627,-1.93693074554234,
135.327223599268));
#120417=CARTESIAN_POINT('Ctrl Pts',(-181.722256554141,-1.81011184722903,
135.379447088406));
#120418=CARTESIAN_POINT('Ctrl Pts',(-181.730016996655,-1.68147337978646,
135.426246632557));
#120419=CARTESIAN_POINT('Ctrl Pts',(-181.737789896921,-1.55262841045597,
135.473121303491));
#120420=CARTESIAN_POINT('Ctrl Pts',(-181.745562797186,-1.42195840793301,
135.514554511845));
#120421=CARTESIAN_POINT('Ctrl Pts',(-181.753335697452,-1.28996545172147,
135.550429748527));
#120422=CARTESIAN_POINT('Ctrl Pts',(-181.760826033214,-1.16277077193805,
135.585000829992));
#120423=CARTESIAN_POINT('Ctrl Pts',(-181.768316368976,-1.03434795419006,
135.614410947926));
#120424=CARTESIAN_POINT('Ctrl Pts',(-181.775806704738,-0.905151846678698,
135.638601322884));
#120425=CARTESIAN_POINT('Ctrl Pts',(-181.783581038857,-0.771057229483291,
135.663708883261));
#120426=CARTESIAN_POINT('Ctrl Pts',(-181.791355372976,-0.635704754977355,
135.68327260728));
#120427=CARTESIAN_POINT('Ctrl Pts',(-181.799129707095,-0.499592595456683,
135.697170679388));
#120428=CARTESIAN_POINT('Ctrl Pts',(-181.806894460042,-0.363648182007928,
135.711051623364));
#120429=CARTESIAN_POINT('Ctrl Pts',(-181.814659212989,-0.226946331599816,
135.719280769009));
#120430=CARTESIAN_POINT('Ctrl Pts',(-181.822423965936,-0.08999601943478,
135.721787157839));
#120431=CARTESIAN_POINT('Ctrl Pts',(-181.830181006821,0.0468182717495528,
135.724291057289));
#120432=CARTESIAN_POINT('Ctrl Pts',(-181.837938047706,0.18388014522574,
135.721083504079));
#120433=CARTESIAN_POINT('Ctrl Pts',(-181.845695088591,0.320675234751949,
135.712145296657));
#120434=CARTESIAN_POINT('Ctrl Pts',(-181.853446279831,0.457367166036849,
135.703213829606));
#120435=CARTESIAN_POINT('Ctrl Pts',(-181.861197471071,0.593792325261312,
135.688560335476));
#120436=CARTESIAN_POINT('Ctrl Pts',(-181.868948662312,0.7294364329914,135.668217682975));
#120437=CARTESIAN_POINT('Ctrl Pts',(-181.876696559089,0.865022888357463,
135.647883676643));
#120438=CARTESIAN_POINT('Ctrl Pts',(-181.884444455866,0.999828566655742,
135.621865379108));
#120439=CARTESIAN_POINT('Ctrl Pts',(-181.892192352643,1.13334461812831,
135.59024747781));
#120440=CARTESIAN_POINT('Ctrl Pts',(-181.899938628727,1.26683274092118,
135.558636190296));
#120441=CARTESIAN_POINT('Ctrl Pts',(-181.907684904811,1.39903139325775,
135.521427718866));
#120442=CARTESIAN_POINT('Ctrl Pts',(-181.915431180895,1.5294426155094,135.478757728249));
#120443=CARTESIAN_POINT('Ctrl Pts',(-181.92317751416,1.65985480042725,135.436087422652));
#120444=CARTESIAN_POINT('Ctrl Pts',(-181.930923847426,1.78847915735103,
135.387955639));
#120445=CARTESIAN_POINT('Ctrl Pts',(-181.938670180691,1.91483395331802,
135.334547588732));
#120446=CARTESIAN_POINT('Ctrl Pts',(-181.946418248694,2.0412170455653,135.281127578101));
#120447=CARTESIAN_POINT('Ctrl Pts',(-181.954166316697,2.16532920544419,
135.222429101825));
#120448=CARTESIAN_POINT('Ctrl Pts',(-181.9619143847,2.2867100760472,135.158684915388));
#120449=CARTESIAN_POINT('Ctrl Pts',(-181.969670687442,2.40821995168409,
135.094872980871));
#120450=CARTESIAN_POINT('Ctrl Pts',(-181.977426990184,2.52699239260691,
135.026004805807));
#120451=CARTESIAN_POINT('Ctrl Pts',(-181.985183292925,2.64259251692664,
134.952358671083));
#120452=CARTESIAN_POINT('Ctrl Pts',(-181.99294373544,2.75825434051338,134.8786732292));
#120453=CARTESIAN_POINT('Ctrl Pts',(-182.000704177954,2.87074015323274,
134.80020496986));
#120454=CARTESIAN_POINT('Ctrl Pts',(-182.008464620468,2.97964616898119,
134.717274080726));
#120455=CARTESIAN_POINT('Ctrl Pts',(-182.016237520733,3.08872701033434,
134.634210063566));
#120456=CARTESIAN_POINT('Ctrl Pts',(-182.024010420999,3.19421627012777,
134.546669350855));
#120457=CARTESIAN_POINT('Ctrl Pts',(-182.031783321264,3.29574453972754,
134.455011380287));
#120458=CARTESIAN_POINT('Ctrl Pts',(-182.039273657026,3.39358200099335,
134.366685407822));
#120459=CARTESIAN_POINT('Ctrl Pts',(-182.046763992788,3.48774123604373,
134.274536541253));
#120460=CARTESIAN_POINT('Ctrl Pts',(-182.05425432855,3.57792693550293,134.178915685527));
#120461=CARTESIAN_POINT('Ctrl Pts',(-182.062028662669,3.67153205316809,
134.079669335994));
#120462=CARTESIAN_POINT('Ctrl Pts',(-182.069802996788,3.76115288689754,
133.976368136514));
#120463=CARTESIAN_POINT('Ctrl Pts',(-182.077577330907,3.84641767552078,
133.869365369266));
#120464=CARTESIAN_POINT('Ctrl Pts',(-182.085342083855,3.93157738291237,
133.762494473365));
#120465=CARTESIAN_POINT('Ctrl Pts',(-182.093106836802,4.01239148547918,
133.651931389249));
#120466=CARTESIAN_POINT('Ctrl Pts',(-182.100871589749,4.0885251703094,133.538065977375));
#120467=CARTESIAN_POINT('Ctrl Pts',(-182.108628630634,4.16458323809056,
133.424313658233));
#120468=CARTESIAN_POINT('Ctrl Pts',(-182.116385671519,4.23596992326855,
133.307265861425));
#120469=CARTESIAN_POINT('Ctrl Pts',(-182.124142712404,4.30239104351552,
133.187344958928));
#120470=CARTESIAN_POINT('Ctrl Pts',(-182.131893903644,4.36876207507913,
133.067514489717));
#120471=CARTESIAN_POINT('Ctrl Pts',(-182.139645094884,4.43017480638999,
132.944815567991));
#120472=CARTESIAN_POINT('Ctrl Pts',(-182.147396286124,4.48637891022631,
132.819698637943));
#120473=CARTESIAN_POINT('Ctrl Pts',(-182.155144182901,4.54255912581914,
132.694634885927));
#120474=CARTESIAN_POINT('Ctrl Pts',(-182.162892079678,4.59353495715868,
132.56715552553));
#120475=CARTESIAN_POINT('Ctrl Pts',(-182.170639976455,4.639102608463,132.437734442094));
#120476=CARTESIAN_POINT('Ctrl Pts',(-182.178386252539,4.68466072799699,
132.308340430758));
#120477=CARTESIAN_POINT('Ctrl Pts',(-182.186132528623,4.724812787904,132.177005872811));
#120478=CARTESIAN_POINT('Ctrl Pts',(-182.193878804708,4.75940376741928,
132.044223045892));
#120479=CARTESIAN_POINT('Ctrl Pts',(-182.201625137973,4.79399500227735,
131.911439238801));
#120480=CARTESIAN_POINT('Ctrl Pts',(-182.209371471238,4.82302497627006,
131.777207519742));
#120481=CARTESIAN_POINT('Ctrl Pts',(-182.217117804504,4.8463891245921,131.642033295606));
#120482=CARTESIAN_POINT('Ctrl Pts',(-182.224865872507,4.86975850515314,
131.506828800141));
#120483=CARTESIAN_POINT('Ctrl Pts',(-182.23261394051,4.88745946865773,131.370681764779));
#120484=CARTESIAN_POINT('Ctrl Pts',(-182.240362008513,4.89943900473265,
131.234105310848));
#120485=CARTESIAN_POINT('Ctrl Pts',(-182.248118311254,4.91143127280104,
131.097383701837));
#120486=CARTESIAN_POINT('Ctrl Pts',(-182.255874613996,4.91768993216839,
130.960232152658));
#120487=CARTESIAN_POINT('Ctrl Pts',(-182.263630916738,4.91821404414322,
130.823166959378));
#120488=CARTESIAN_POINT('Ctrl Pts',(-182.271391359252,4.9187384358524,130.686028610276));
#120489=CARTESIAN_POINT('Ctrl Pts',(-182.279151801766,4.91352219632619,
130.548977099404));
#120490=CARTESIAN_POINT('Ctrl Pts',(-182.28691224428,4.90261645226236,130.4125252127));
#120491=CARTESIAN_POINT('Ctrl Pts',(-182.294685144546,4.89169320132999,
130.275854281314));
#120492=CARTESIAN_POINT('Ctrl Pts',(-182.302458044811,4.8750622420806,130.139785285917));
#120493=CARTESIAN_POINT('Ctrl Pts',(-182.310230945077,4.85282630523814,
130.004823305311));
#120494=CARTESIAN_POINT('Ctrl Pts',(-182.317721280839,4.83139870070879,
129.874767532648));
#120495=CARTESIAN_POINT('Ctrl Pts',(-182.325211616601,4.80476661598463,
129.74573998823));
#120496=CARTESIAN_POINT('Ctrl Pts',(-182.332701952363,4.77306565540504,
129.618178796894));
#120497=CARTESIAN_POINT('Ctrl Pts',(-182.340476286482,4.74016274326992,
129.485781084218));
#120498=CARTESIAN_POINT('Ctrl Pts',(-182.348250620601,4.70169476824667,
129.354543717016));
#120499=CARTESIAN_POINT('Ctrl Pts',(-182.35602495472,4.65775801064424,129.224970426138));
#120500=CARTESIAN_POINT('Ctrl Pts',(-182.363789707667,4.61387540116881,
129.09555682276));
#120501=CARTESIAN_POINT('Ctrl Pts',(-182.371554460614,4.56453754362383,
128.967803581878));
#120502=CARTESIAN_POINT('Ctrl Pts',(-182.379319213561,4.50989146409757,
128.842203120177));
#120503=CARTESIAN_POINT('Ctrl Pts',(-182.387076254446,4.45529965982786,
128.716727406625));
#120504=CARTESIAN_POINT('Ctrl Pts',(-182.394833295331,4.39541028046255,
128.593400573383));
#120505=CARTESIAN_POINT('Ctrl Pts',(-182.402590336216,4.33041966677546,
128.472698426745));
#120506=CARTESIAN_POINT('Ctrl Pts',(-182.410341527457,4.26547806301561,
128.352087302535));
#120507=CARTESIAN_POINT('Ctrl Pts',(-182.418092718697,4.19544306651655,
128.234097268103));
#120508=CARTESIAN_POINT('Ctrl Pts',(-182.425843909937,4.1205583407563,128.119182406921));
#120509=CARTESIAN_POINT('Ctrl Pts',(-182.433591806714,4.04570544300221,
128.00431638762));
#120510=CARTESIAN_POINT('Ctrl Pts',(-182.441339703491,3.96600712868981,
127.892523268852));
#120511=CARTESIAN_POINT('Ctrl Pts',(-182.449087600268,3.88175193438076,
127.784230656384));
#120512=CARTESIAN_POINT('Ctrl Pts',(-182.456833876352,3.79751436444203,
127.675960696395));
#120513=CARTESIAN_POINT('Ctrl Pts',(-182.464580152436,3.70872205040214,
127.571190094635));
#120514=CARTESIAN_POINT('Ctrl Pts',(-182.47232642852,3.61570536686982,127.470315362551));
#120515=CARTESIAN_POINT('Ctrl Pts',(-182.480072761786,3.52268799670936,
127.369439885832));
#120516=CARTESIAN_POINT('Ctrl Pts',(-182.487819095051,3.42544645986479,
127.272460623597));
#120517=CARTESIAN_POINT('Ctrl Pts',(-182.495565428317,3.32434944963606,
127.179738733948));
#120518=CARTESIAN_POINT('Ctrl Pts',(-182.50331349632,3.22322979943299,127.086996079874));
#120519=CARTESIAN_POINT('Ctrl Pts',(-182.511061564323,3.11825324584275,
126.998512959771));
#120520=CARTESIAN_POINT('Ctrl Pts',(-182.518809632326,3.00982283896963,
126.914611327378));
#120521=CARTESIAN_POINT('Ctrl Pts',(-182.526565935067,2.9012771909699,126.830620523332));
#120522=CARTESIAN_POINT('Ctrl Pts',(-182.534322237809,2.78927066657606,
126.751221173508));
#120523=CARTESIAN_POINT('Ctrl Pts',(-182.542078540551,2.67423713290575,
126.676693138288));
#120524=CARTESIAN_POINT('Ctrl Pts',(-182.549838983065,2.55914220237462,
126.602125325212));
#120525=CARTESIAN_POINT('Ctrl Pts',(-182.557599425579,2.44101737989998,
126.532434205961));
#120526=CARTESIAN_POINT('Ctrl Pts',(-182.565359868094,2.32032172204335,
126.467853939523));
#120527=CARTESIAN_POINT('Ctrl Pts',(-182.573132768359,2.19943231280187,
126.403170003107));
#120528=CARTESIAN_POINT('Ctrl Pts',(-182.580905668624,2.07596417359235,
126.343613484455));
#120529=CARTESIAN_POINT('Ctrl Pts',(-182.58867856889,1.95039776998001,126.289370960728));
#120530=CARTESIAN_POINT('Ctrl Pts',(-182.596168904652,1.82939602142133,
126.237100289366));
#120531=CARTESIAN_POINT('Ctrl Pts',(-182.603659240414,1.70644620173451,
126.189764077074));
#120532=CARTESIAN_POINT('Ctrl Pts',(-182.611149576176,1.5819902152108,126.147485053255));
#120533=CARTESIAN_POINT('Ctrl Pts',(-182.618923910295,1.45281544213099,
126.103603007398));
#120534=CARTESIAN_POINT('Ctrl Pts',(-182.626698244414,1.3216088481364,126.065030201631));
#120535=CARTESIAN_POINT('Ctrl Pts',(-182.634472578533,1.18884627811505,
126.031957911432));
#120536=CARTESIAN_POINT('Ctrl Pts',(-182.64223733148,1.05624732609592,125.998926379875));
#120537=CARTESIAN_POINT('Ctrl Pts',(-182.650002084427,0.922096589234707,
125.971381969506));
#120538=CARTESIAN_POINT('Ctrl Pts',(-182.657766837375,0.786887822827249,
125.949467146357));
#120539=CARTESIAN_POINT('Ctrl Pts',(-182.66552387826,0.651813347672695,
125.92757408932));
#120540=CARTESIAN_POINT('Ctrl Pts',(-182.673280919145,0.515683317642029,
125.911299554543));
#120541=CARTESIAN_POINT('Ctrl Pts',(-182.68103796003,0.379004169031384,
125.900735539896));
#120542=CARTESIAN_POINT('Ctrl Pts',(-182.68878915127,0.242428091229729,
125.890179491655));
#120543=CARTESIAN_POINT('Ctrl Pts',(-182.69654034251,0.105304107303662,
125.885325422026));
#120544=CARTESIAN_POINT('Ctrl Pts',(-182.70429153375,-0.0318540434016616,
125.886213773233));
#120545=CARTESIAN_POINT('Ctrl Pts',(-182.712039430527,-0.168953898234309,
125.887101746867));
#120546=CARTESIAN_POINT('Ctrl Pts',(-182.719787327304,-0.306087500824971,
125.893727284479));
#120547=CARTESIAN_POINT('Ctrl Pts',(-182.727535224081,-0.442739133272749,
125.906078763449));
#120548=CARTESIAN_POINT('Ctrl Pts',(-182.735281500165,-0.579362181144514,
125.918427658756));
#120549=CARTESIAN_POINT('Ctrl Pts',(-182.743027776249,-0.715503070274265,
125.936500077871));
#120550=CARTESIAN_POINT('Ctrl Pts',(-182.750774052334,-0.85064962880552,
125.960232391403));
#120551=CARTESIAN_POINT('Ctrl Pts',(-182.758520385599,-0.985797184958153,
125.98396488012));
#120552=CARTESIAN_POINT('Ctrl Pts',(-182.766266718864,-1.11995001079294,
126.013357279003));
#120553=CARTESIAN_POINT('Ctrl Pts',(-182.77401305213,-1.25260496603569,
126.048294610711));
#120554=CARTESIAN_POINT('Ctrl Pts',(-182.781761120133,-1.38528962843572,
126.083239766392));
#120555=CARTESIAN_POINT('Ctrl Pts',(-182.789509188136,-1.51647537476105,
126.123732226282));
#120556=CARTESIAN_POINT('Ctrl Pts',(-182.797257256139,-1.6456734777856,
126.169606916773));
#120557=CARTESIAN_POINT('Ctrl Pts',(-182.80501355888,-1.7750088940917,126.215530363432));
#120558=CARTESIAN_POINT('Ctrl Pts',(-182.812769861622,-1.902352078152,126.266847336577));
#120559=CARTESIAN_POINT('Ctrl Pts',(-182.820526164364,-2.02723305972525,
126.323344082888));
#120560=CARTESIAN_POINT('Ctrl Pts',(-182.828286606878,-2.15218069403846,
126.379870983214));
#120561=CARTESIAN_POINT('Ctrl Pts',(-182.836047049393,-2.27466315832567,
126.441582989575));
#120562=CARTESIAN_POINT('Ctrl Pts',(-182.843807491907,-2.39423531671549,
126.508220453338));
#120563=CARTESIAN_POINT('Ctrl Pts',(-182.851580392172,-2.51399942294907,
126.574964889473));
#120564=CARTESIAN_POINT('Ctrl Pts',(-182.859353292438,-2.63084355393906,
126.646650378709));
#120565=CARTESIAN_POINT('Ctrl Pts',(-182.867126192703,-2.74435103366134,
126.722973541272));
#120566=CARTESIAN_POINT('Ctrl Pts',(-182.874616528465,-2.85373223058731,
126.796522164628));
#120567=CARTESIAN_POINT('Ctrl Pts',(-182.882106864227,-2.9600149073766,
126.874376951055));
#120568=CARTESIAN_POINT('Ctrl Pts',(-182.889597199989,-3.06285694824154,
126.956232452197));
#120569=CARTESIAN_POINT('Ctrl Pts',(-182.897271718051,-3.16822780545898,
127.040100724848));
#120570=CARTESIAN_POINT('Ctrl Pts',(-182.904946236112,-3.27033860869109,
127.128449457481));
#120571=CARTESIAN_POINT('Ctrl Pts',(-182.912620754173,-3.36877703830128,
127.220992881942));
#120572=CARTESIAN_POINT('Ctrl Pts',(-182.920286491824,-3.46710284456976,
127.313430427532));
#120573=CARTESIAN_POINT('Ctrl Pts',(-182.927952229474,-3.56176434009002,
127.410052852803));
#120574=CARTESIAN_POINT('Ctrl Pts',(-182.935617967125,-3.65237997082311,
127.510532508628));
#120575=CARTESIAN_POINT('Ctrl Pts',(-182.943276696308,-3.74291275542632,
127.610920300052));
#120576=CARTESIAN_POINT('Ctrl Pts',(-182.95093542549,-3.82940676294885,
127.715158013987));
#120577=CARTESIAN_POINT('Ctrl Pts',(-182.958594154673,-3.9115156180739,
127.822879671448));
#120578=CARTESIAN_POINT('Ctrl Pts',(-182.966247640976,-3.99356826453599,
127.930527586676));
#120579=CARTESIAN_POINT('Ctrl Pts',(-182.973901127278,-4.07124148666013,
128.041654383705));
#120580=CARTESIAN_POINT('Ctrl Pts',(-182.98155461358,-4.14422807866773,
128.15585977851));
#120581=CARTESIAN_POINT('Ctrl Pts',(-182.989205542012,-4.2171902778377,
128.270027004747));
#120582=CARTESIAN_POINT('Ctrl Pts',(-182.996856470444,-4.28546874152419,
128.387270447522));
#120583=CARTESIAN_POINT('Ctrl Pts',(-183.004507398876,-4.34879885726115,
128.50715980754));
#120584=CARTESIAN_POINT('Ctrl Pts',(-183.012156622058,-4.41211485788887,
128.627022446441));
#120585=CARTESIAN_POINT('Ctrl Pts',(-183.019805845239,-4.47048452011149,
128.749529472692));
#120586=CARTESIAN_POINT('Ctrl Pts',(-183.027455068421,-4.52368893671273,
128.874225527381));
#120587=CARTESIAN_POINT('Ctrl Pts',(-183.035106947243,-4.57691182470863,
128.998964873778));
#120588=CARTESIAN_POINT('Ctrl Pts',(-183.042758826066,-4.62496572459593,
129.125894397969));
#120589=CARTESIAN_POINT('Ctrl Pts',(-183.050410704888,-4.66767971122647,
129.254538312944));
#120590=CARTESIAN_POINT('Ctrl Pts',(-183.056846671858,-4.7036062873606,
129.362740233909));
#120591=CARTESIAN_POINT('Ctrl Pts',(-183.063282638827,-4.73575598385233,
129.472154524254));
#120592=CARTESIAN_POINT('Ctrl Pts',(-183.069718605797,-4.76405452823406,
129.582490119308));
#120593=CARTESIAN_POINT('Origin',(213.235140564004,0.,130.804360617566));
#120594=CARTESIAN_POINT('',(-185.165421073984,-4.76405452823401,129.582490119308));
#120595=CARTESIAN_POINT('',(-184.819837330039,-4.76405452823405,129.582490119308));
#120596=CARTESIAN_POINT('',(213.235140564004,-4.76405452823405,129.582490119308));
#120597=CARTESIAN_POINT('',(-183.485140564052,-4.91824798071509,130.799903859564));
#120598=CARTESIAN_POINT('Ctrl Pts',(-183.485140564052,-4.91824798071509,
130.799903859564));
#120599=CARTESIAN_POINT('Ctrl Pts',(-183.492790120517,-4.91837024179223,
130.934824870645));
#120600=CARTESIAN_POINT('Ctrl Pts',(-183.500439676982,-4.91293645195532,
131.069920615074));
#120601=CARTESIAN_POINT('Ctrl Pts',(-183.508089233447,-4.90193026440357,
131.204688914623));
#120602=CARTESIAN_POINT('Ctrl Pts',(-183.515732635828,-4.89093293135145,
131.339348792808));
#120603=CARTESIAN_POINT('Ctrl Pts',(-183.52337603821,-4.8743721510898,131.473681350422));
#120604=CARTESIAN_POINT('Ctrl Pts',(-183.531019440591,-4.85228364227142,
131.607184706296));
#120605=CARTESIAN_POINT('Ctrl Pts',(-183.538659228572,-4.83020557863537,
131.740624931294));
#120606=CARTESIAN_POINT('Ctrl Pts',(-183.546299016552,-4.80260504893871,
131.873236337474));
#120607=CARTESIAN_POINT('Ctrl Pts',(-183.553938804532,-4.76956954354201,
132.004522869854));
#120608=CARTESIAN_POINT('Ctrl Pts',(-183.561576868312,-4.73654149382951,
132.135779772569));
#120609=CARTESIAN_POINT('Ctrl Pts',(-183.569214932091,-4.69808100518792,
132.265712005344));
#120610=CARTESIAN_POINT('Ctrl Pts',(-183.576852995871,-4.65432642489983,
132.393834930973));
#120611=CARTESIAN_POINT('Ctrl Pts',(-183.584491098882,-4.6105716198721,
132.521958514688));
#120612=CARTESIAN_POINT('Ctrl Pts',(-183.592129201894,-4.56152279959267,
132.648272391449));
#120613=CARTESIAN_POINT('Ctrl Pts',(-183.599767304905,-4.50736762758277,
132.772308821234));
#120614=CARTESIAN_POINT('Ctrl Pts',(-183.607407210404,-4.45319967569707,
132.89637452191));
#120615=CARTESIAN_POINT('Ctrl Pts',(-183.615047115903,-4.39392313754426,
133.018161337874));
#120616=CARTESIAN_POINT('Ctrl Pts',(-183.622687021401,-4.32977284733201,
133.137223698205));
#120617=CARTESIAN_POINT('Ctrl Pts',(-183.63033486744,-4.26555588247997,
133.256409806066));
#120618=CARTESIAN_POINT('Ctrl Pts',(-183.637982713479,-4.19645524369809,
133.372865449847));
#120619=CARTESIAN_POINT('Ctrl Pts',(-183.645630559517,-4.12275070500498,
133.486171514494));
#120620=CARTESIAN_POINT('Ctrl Pts',(-183.653282768779,-4.04900411665295,
133.599542222126));
#120621=CARTESIAN_POINT('Ctrl Pts',(-183.66093497804,-3.97064863261913,
133.709759445809));
#120622=CARTESIAN_POINT('Ctrl Pts',(-183.668587187302,-3.8880051776028,
133.816436114866));
#120623=CARTESIAN_POINT('Ctrl Pts',(-183.676250761655,-3.80523898019318,
133.923271220542));
#120624=CARTESIAN_POINT('Ctrl Pts',(-183.683914336009,-3.71817235596996,
134.026554965782));
#120625=CARTESIAN_POINT('Ctrl Pts',(-183.691577910362,-3.62716431972376,
134.125935855344));
#120626=CARTESIAN_POINT('Ctrl Pts',(-183.696168965331,-3.5726436903536,
134.1854724509));
#120627=CARTESIAN_POINT('Ctrl Pts',(-183.700760020299,-3.51670920889025,
134.243609084722));
#120628=CARTESIAN_POINT('Ctrl Pts',(-183.705351075268,-3.45944366050394,
134.300277181544));
#120629=CARTESIAN_POINT('Ctrl Pts',(-183.713125409387,-3.36247215619332,
134.396236981985));
#120630=CARTESIAN_POINT('Ctrl Pts',(-183.720899743506,-3.26135135780418,
134.488310951084));
#120631=CARTESIAN_POINT('Ctrl Pts',(-183.728674077625,-3.15642552453558,
134.57611895693));
#120632=CARTESIAN_POINT('Ctrl Pts',(-183.736438830572,-3.05162900297956,
134.663818747256));
#120633=CARTESIAN_POINT('Ctrl Pts',(-183.744203583519,-2.94303707393275,
134.74726278652));
#120634=CARTESIAN_POINT('Ctrl Pts',(-183.751968336466,-2.83103145099696,
134.826107002654));
#120635=CARTESIAN_POINT('Ctrl Pts',(-183.759725377351,-2.71913707362488,
134.9048729096));
#120636=CARTESIAN_POINT('Ctrl Pts',(-183.767482418236,-2.60383606730024,
134.979047861564));
#120637=CARTESIAN_POINT('Ctrl Pts',(-183.775239459121,-2.48554362280428,
135.048327625171));
#120638=CARTESIAN_POINT('Ctrl Pts',(-183.782990650361,-2.36734038356073,
135.117555144369));
#120639=CARTESIAN_POINT('Ctrl Pts',(-183.790741841601,-2.24615053231144,
135.181894626134));
#120640=CARTESIAN_POINT('Ctrl Pts',(-183.798493032841,-2.12241837636851,
135.241085005913));
#120641=CARTESIAN_POINT('Ctrl Pts',(-183.806240929618,-1.99873880989235,
135.300250228202));
#120642=CARTESIAN_POINT('Ctrl Pts',(-183.813988826396,-1.87251943979781,
135.354270532912));
#120643=CARTESIAN_POINT('Ctrl Pts',(-183.821736723173,-1.7442291244233,
135.402930811008));
#120644=CARTESIAN_POINT('Ctrl Pts',(-183.829482999257,-1.61596564461714,
135.451580910423));
#120645=CARTESIAN_POINT('Ctrl Pts',(-183.837229275341,-1.48563244650519,
135.494873074791));
#120646=CARTESIAN_POINT('Ctrl Pts',(-183.844975551425,-1.35371794589048,
135.532640514682));
#120647=CARTESIAN_POINT('Ctrl Pts',(-183.85272188469,-1.22180247151308,
135.570408233365));
#120648=CARTESIAN_POINT('Ctrl Pts',(-183.860468217956,-1.08830604720463,
135.602651038582));
#120649=CARTESIAN_POINT('Ctrl Pts',(-183.868214551221,-0.953731425044513,
135.62925226727));
#120650=CARTESIAN_POINT('Ctrl Pts',(-183.875962619224,-0.81912666583066,
135.655859453118));
#120651=CARTESIAN_POINT('Ctrl Pts',(-183.883710687227,-0.683443611768262,
135.676822472633));
#120652=CARTESIAN_POINT('Ctrl Pts',(-183.89145875523,-0.547193964316623,
135.69207601721));
#120653=CARTESIAN_POINT('Ctrl Pts',(-183.899215057972,-0.410799509118467,
135.707345773435));
#120654=CARTESIAN_POINT('Ctrl Pts',(-183.906971360713,-0.273837646764738,
135.716893889475));
#120655=CARTESIAN_POINT('Ctrl Pts',(-183.914727663455,-0.136824502115776,
135.720707037228));
#120656=CARTESIAN_POINT('Ctrl Pts',(-183.922488105969,0.000261770573871722,
135.724522220172));
#120657=CARTESIAN_POINT('Ctrl Pts',(-183.930248548483,0.137398989362215,
135.722596341163));
#120658=CARTESIAN_POINT('Ctrl Pts',(-183.938008990998,0.274073289081115,
135.714968206726));
#120659=CARTESIAN_POINT('Ctrl Pts',(-183.945781891263,0.410966990519299,
135.70732782693));
#120660=CARTESIAN_POINT('Ctrl Pts',(-183.953554791528,0.547395898572235,
135.693966937693));
#120661=CARTESIAN_POINT('Ctrl Pts',(-183.961327691794,0.682852614635353,
135.674976119655));
#120662=CARTESIAN_POINT('Ctrl Pts',(-183.968818027556,0.813385137877262,
135.656675665687));
#120663=CARTESIAN_POINT('Ctrl Pts',(-183.976308363318,0.943014622152609,
135.633147555643));
#120664=CARTESIAN_POINT('Ctrl Pts',(-183.98379869908,1.07129981466353,135.604516841024));
#120665=CARTESIAN_POINT('Ctrl Pts',(-183.991573033199,1.20444897923751,
135.574800584158));
#120666=CARTESIAN_POINT('Ctrl Pts',(-183.999347367318,1.3365716786525,135.539493021914));
#120667=CARTESIAN_POINT('Ctrl Pts',(-184.007121701437,1.46716201666007,
135.49867831872));
#120668=CARTESIAN_POINT('Ctrl Pts',(-184.014886454385,1.5975914137469,135.457913916001));
#120669=CARTESIAN_POINT('Ctrl Pts',(-184.022651207332,1.72649183739355,
135.411655992067));
#120670=CARTESIAN_POINT('Ctrl Pts',(-184.030415960279,1.85336748449725,
135.360039714024));
#120671=CARTESIAN_POINT('Ctrl Pts',(-184.038173001164,1.98011711691926,
135.308474701997));
#120672=CARTESIAN_POINT('Ctrl Pts',(-184.045930042049,2.10484561505189,
135.251562073242));
#120673=CARTESIAN_POINT('Ctrl Pts',(-184.053687082934,2.22707259798284,
135.189486693954));
#120674=CARTESIAN_POINT('Ctrl Pts',(-184.061438274174,2.34920740859568,
135.127458126191));
#120675=CARTESIAN_POINT('Ctrl Pts',(-184.069189465414,2.46884411162038,
135.060274733533));
#120676=CARTESIAN_POINT('Ctrl Pts',(-184.076940656654,2.58552290710035,
134.988169212538));
#120677=CARTESIAN_POINT('Ctrl Pts',(-184.084688553431,2.70215211097956,
134.916094338312));
#120678=CARTESIAN_POINT('Ctrl Pts',(-184.092436450208,2.81582557588218,
134.839101701749));
#120679=CARTESIAN_POINT('Ctrl Pts',(-184.100184346985,2.92610889510012,
134.757469494958));
#120680=CARTESIAN_POINT('Ctrl Pts',(-184.107930623069,3.03636914542542,
134.675854363865));
#120681=CARTESIAN_POINT('Ctrl Pts',(-184.115676899153,3.14324034655068,
134.589601825376));
#120682=CARTESIAN_POINT('Ctrl Pts',(-184.123423175237,3.24631817313421,
134.499032643779));
#120683=CARTESIAN_POINT('Ctrl Pts',(-184.131169508503,3.34939676061442,
134.40846279362));
#120684=CARTESIAN_POINT('Ctrl Pts',(-184.138915841768,3.44868162397767,
134.313576494829));
#120685=CARTESIAN_POINT('Ctrl Pts',(-184.146662175034,3.54380286150397,
134.214733667732));
#120686=CARTESIAN_POINT('Ctrl Pts',(-184.154410243036,3.63894540077176,
134.115868705469));
#120687=CARTESIAN_POINT('Ctrl Pts',(-184.162158311039,3.72992218775639,
134.013045733441));
#120688=CARTESIAN_POINT('Ctrl Pts',(-184.169906379042,3.81640168934142,
133.906659959682));
#120689=CARTESIAN_POINT('Ctrl Pts',(-184.177662681784,3.90297310236997,
133.800161117856));
#120690=CARTESIAN_POINT('Ctrl Pts',(-184.185418984526,3.98503743489305,
133.690092214043));
#120691=CARTESIAN_POINT('Ctrl Pts',(-184.193175287268,4.06230449550591,
133.576880274537));
#120692=CARTESIAN_POINT('Ctrl Pts',(-184.200935729782,4.13961279587571,
133.463607910411));
#120693=CARTESIAN_POINT('Ctrl Pts',(-184.208696172296,4.21211851583949,
133.34718949967));
#120694=CARTESIAN_POINT('Ctrl Pts',(-184.21645661481,4.27957654775137,133.228078347508));
#120695=CARTESIAN_POINT('Ctrl Pts',(-184.224229515076,4.34714286928472,
133.108775987551));
#120696=CARTESIAN_POINT('Ctrl Pts',(-184.232002415341,4.40964513203329,
132.986772596348));
#120697=CARTESIAN_POINT('Ctrl Pts',(-184.239775315607,4.46688528271646,
132.862544023765));
#120698=CARTESIAN_POINT('Ctrl Pts',(-184.247265651369,4.52204460974522,
132.742831472703));
#120699=CARTESIAN_POINT('Ctrl Pts',(-184.254755987131,4.57231764704277,
132.621052998097));
#120700=CARTESIAN_POINT('Ctrl Pts',(-184.262246322894,4.61757109606277,
132.497647431814));
#120701=CARTESIAN_POINT('Ctrl Pts',(-184.270020657013,4.66454034335519,
132.369562905981));
#120702=CARTESIAN_POINT('Ctrl Pts',(-184.277794991132,4.70625063758659,
132.239319737225));
#120703=CARTESIAN_POINT('Ctrl Pts',(-184.285569325251,4.74249933939709,
132.107389043318));
#120704=CARTESIAN_POINT('Ctrl Pts',(-184.293334078198,4.77870336792206,
131.975620942201));
#120705=CARTESIAN_POINT('Ctrl Pts',(-184.301098831145,4.80945909397288,
131.842169827338));
#120706=CARTESIAN_POINT('Ctrl Pts',(-184.308863584092,4.83461224377596,
131.707525893045));
#120707=CARTESIAN_POINT('Ctrl Pts',(-184.316620624977,4.85974041111613,
131.573015689005));
#120708=CARTESIAN_POINT('Ctrl Pts',(-184.324377665862,4.87927700459897,
131.437315405021));
#120709=CARTESIAN_POINT('Ctrl Pts',(-184.332134706747,4.89311789977162,
131.300929123851));
#120710=CARTESIAN_POINT('Ctrl Pts',(-184.339885897987,4.9069483574176,131.164645692637));
#120711=CARTESIAN_POINT('Ctrl Pts',(-184.347637089227,4.91509162671567,
131.027677681317));
#120712=CARTESIAN_POINT('Ctrl Pts',(-184.355388280468,4.91749494876237,
130.89053771079));
#120713=CARTESIAN_POINT('Ctrl Pts',(-184.363136177245,4.91989724933307,
130.75345602841));
#120714=CARTESIAN_POINT('Ctrl Pts',(-184.370884074022,4.9165644480558,130.616202922275));
#120715=CARTESIAN_POINT('Ctrl Pts',(-184.378631970799,4.90749578839558,
130.479294240683));
#120716=CARTESIAN_POINT('Ctrl Pts',(-184.386378246883,4.89842902570346,
130.342414197436));
#120717=CARTESIAN_POINT('Ctrl Pts',(-184.394124522967,4.88362881695607,
130.205878825291));
#120718=CARTESIAN_POINT('Ctrl Pts',(-184.401870799051,4.86314648250967,
130.070201675542));
#120719=CARTESIAN_POINT('Ctrl Pts',(-184.409617132316,4.84266399686724,
129.934523524254));
#120720=CARTESIAN_POINT('Ctrl Pts',(-184.417363465582,4.81649936018953,
129.799703994589));
#120721=CARTESIAN_POINT('Ctrl Pts',(-184.425109798847,4.78475544272591,
129.666248841067));
#120722=CARTESIAN_POINT('Ctrl Pts',(-184.43285786685,4.75300441643203,129.532763801189));
#120723=CARTESIAN_POINT('Ctrl Pts',(-184.440605934853,4.7156717135631,129.400644125729));
#120724=CARTESIAN_POINT('Ctrl Pts',(-184.448354002856,4.67291063208325,
129.270382362484));
#120725=CARTESIAN_POINT('Ctrl Pts',(-184.456110305598,4.6301041036172,129.139982155487));
#120726=CARTESIAN_POINT('Ctrl Pts',(-184.46386660834,4.58185779378596,129.011444177258));
#120727=CARTESIAN_POINT('Ctrl Pts',(-184.471622911082,4.52837411636472,
128.885243392189));
#120728=CARTESIAN_POINT('Ctrl Pts',(-184.479383353596,4.47486189309462,
128.758975249962));
#120729=CARTESIAN_POINT('Ctrl Pts',(-184.48714379611,4.41610689968782,128.635047139604));
#120730=CARTESIAN_POINT('Ctrl Pts',(-184.494904238624,4.35235802797307,
128.513910299651));
#120731=CARTESIAN_POINT('Ctrl Pts',(-184.50267713889,4.28850682091009,128.392579000088));
#120732=CARTESIAN_POINT('Ctrl Pts',(-184.510450039155,4.21964591229296,
128.274048263238));
#120733=CARTESIAN_POINT('Ctrl Pts',(-184.518222939421,4.14606859545448,
128.15874192541));
#120734=CARTESIAN_POINT('Ctrl Pts',(-184.525713275183,4.07516599941415,
128.047627263403));
#120735=CARTESIAN_POINT('Ctrl Pts',(-184.533203610945,3.99988412443292,
127.939506893194));
#120736=CARTESIAN_POINT('Ctrl Pts',(-184.540693946706,3.92052012106803,
127.83473016197));
#120737=CARTESIAN_POINT('Ctrl Pts',(-184.548468280826,3.83814700739212,
127.725980789134));
#120738=CARTESIAN_POINT('Ctrl Pts',(-184.556242614945,3.75111517370212,
127.620489123221));
#120739=CARTESIAN_POINT('Ctrl Pts',(-184.564016949064,3.65971145319893,
127.518680301129));
#120740=CARTESIAN_POINT('Ctrl Pts',(-184.571781702011,3.56842037961253,
127.41699694931));
#120741=CARTESIAN_POINT('Ctrl Pts',(-184.579546454958,3.47276839832737,
127.318987698628));
#120742=CARTESIAN_POINT('Ctrl Pts',(-184.587311207905,3.37308453496028,
127.225047305978));
#120743=CARTESIAN_POINT('Ctrl Pts',(-184.59506824879,3.27349967901132,127.13120021625));
#120744=CARTESIAN_POINT('Ctrl Pts',(-184.602825289675,3.16989119284842,
127.04141420869));
#120745=CARTESIAN_POINT('Ctrl Pts',(-184.61058233056,3.06262689376355,126.956049355194));
#120746=CARTESIAN_POINT('Ctrl Pts',(-184.6183335218,2.95544348352117,126.870748875999));
#120747=CARTESIAN_POINT('Ctrl Pts',(-184.62608471304,2.84461005242828,126.789863157161));
#120748=CARTESIAN_POINT('Ctrl Pts',(-184.63383590428,2.73052936548945,126.713713670358));
#120749=CARTESIAN_POINT('Ctrl Pts',(-184.641583801057,2.61649716588561,
126.637596549119));
#120750=CARTESIAN_POINT('Ctrl Pts',(-184.649331697835,2.49922077998541,
126.566211872763));
#120751=CARTESIAN_POINT('Ctrl Pts',(-184.657079594612,2.37913379664567,
126.499839106392));
#120752=CARTESIAN_POINT('Ctrl Pts',(-184.664825870696,2.25907193291407,
126.433480223773));
#120753=CARTESIAN_POINT('Ctrl Pts',(-184.67257214678,2.13620098310233,126.372131354849));
#120754=CARTESIAN_POINT('Ctrl Pts',(-184.680318422864,2.01098075236442,
126.316026909371));
#120755=CARTESIAN_POINT('Ctrl Pts',(-184.688064756129,1.88575959727938,
126.259922049742));
#120756=CARTESIAN_POINT('Ctrl Pts',(-184.695811089395,1.75818948345372,
126.209061850666));
#120757=CARTESIAN_POINT('Ctrl Pts',(-184.70355742266,1.62875152037251,126.163633137161));
#120758=CARTESIAN_POINT('Ctrl Pts',(-184.711305490663,1.49928457055711,
126.118194250211));
#120759=CARTESIAN_POINT('Ctrl Pts',(-184.719053558666,1.36794930796729,
126.078189398663));
#120760=CARTESIAN_POINT('Ctrl Pts',(-184.726801626669,1.23524298830775,
126.043755842715));
#120761=CARTESIAN_POINT('Ctrl Pts',(-184.734557929411,1.10239562679191,
126.009285690373));
#120762=CARTESIAN_POINT('Ctrl Pts',(-184.742314232153,0.968174676377767,
125.980398760293));
#120763=CARTESIAN_POINT('Ctrl Pts',(-184.750070534895,0.833089147649478,
125.957181485889));
#120764=CARTESIAN_POINT('Ctrl Pts',(-184.757830977409,0.697931519707528,
125.933951819726));
#120765=CARTESIAN_POINT('Ctrl Pts',(-184.765591419923,0.561908781530276,
125.916397888946));
#120766=CARTESIAN_POINT('Ctrl Pts',(-184.773351862437,0.425535104989546,
125.904554199255));
#120767=CARTESIAN_POINT('Ctrl Pts',(-184.781124762703,0.288942509316547,
125.892691497022));
#120768=CARTESIAN_POINT('Ctrl Pts',(-184.788897662968,0.1519982403108,125.886557371142));
#120769=CARTESIAN_POINT('Ctrl Pts',(-184.796670563234,0.0152174156738462,
125.886134159506));
#120770=CARTESIAN_POINT('Ctrl Pts',(-184.804160898996,-0.116591081455591,
125.885726332679));
#120771=CARTESIAN_POINT('Ctrl Pts',(-184.811651234757,-0.248247503329108,
125.89062140511));
#120772=CARTESIAN_POINT('Ctrl Pts',(-184.819141570519,-0.379297317131378,
125.900758206306));
#120773=CARTESIAN_POINT('Ctrl Pts',(-184.826915904638,-0.515315924457791,
125.9112793474));
#120774=CARTESIAN_POINT('Ctrl Pts',(-184.834690238758,-0.651111882649554,
125.92748087175));
#120775=CARTESIAN_POINT('Ctrl Pts',(-184.842464572877,-0.786172471644022,
125.949351255337));
#120776=CARTESIAN_POINT('Ctrl Pts',(-184.850229325824,-0.921066610532533,
125.971194685631));
#120777=CARTESIAN_POINT('Ctrl Pts',(-184.857994078771,-1.05522680121144,
125.998693012488));
#120778=CARTESIAN_POINT('Ctrl Pts',(-184.865758831718,-1.18814307714153,
126.031782793084));
#120779=CARTESIAN_POINT('Ctrl Pts',(-184.873515872603,-1.3209273387533,
126.064839708443));
#120780=CARTESIAN_POINT('Ctrl Pts',(-184.881272913488,-1.45246976733426,
126.103476931965));
#120781=CARTESIAN_POINT('Ctrl Pts',(-184.889029954373,-1.58226860997003,
126.147579636201));
#120782=CARTESIAN_POINT('Ctrl Pts',(-184.896781145613,-1.71196957028905,
126.191649082245));
#120783=CARTESIAN_POINT('Ctrl Pts',(-184.904532336853,-1.83992919311302,
126.241175680014));
#120784=CARTESIAN_POINT('Ctrl Pts',(-184.912283528093,-1.96565931089237,
126.295994335197));
#120785=CARTESIAN_POINT('Ctrl Pts',(-184.92003142487,-2.09133599001719,
126.350789690989));
#120786=CARTESIAN_POINT('Ctrl Pts',(-184.927779321648,-2.21478469116771,
126.410872474649));
#120787=CARTESIAN_POINT('Ctrl Pts',(-184.935527218425,-2.33553592707272,
126.476028953304));
#120788=CARTESIAN_POINT('Ctrl Pts',(-184.943273494509,-2.45626190442228,
126.541171802628));
#120789=CARTESIAN_POINT('Ctrl Pts',(-184.951019770593,-2.57429119500066,
126.611386050408));
#120790=CARTESIAN_POINT('Ctrl Pts',(-184.958766046677,-2.68917804732998,
126.686411553741));
#120791=CARTESIAN_POINT('Ctrl Pts',(-184.966512379942,-2.8040657477281,
126.761437610895));
#120792=CARTESIAN_POINT('Ctrl Pts',(-184.974258713208,-2.9158106362426,
126.8412747807));
#120793=CARTESIAN_POINT('Ctrl Pts',(-184.982005046473,-3.02399548026597,
126.925619275606));
#120794=CARTESIAN_POINT('Ctrl Pts',(-184.989753114476,-3.1322045515355,
127.009982658877));
#120795=CARTESIAN_POINT('Ctrl Pts',(-184.997501182479,-3.2368516836113,
127.098855135468));
#120796=CARTESIAN_POINT('Ctrl Pts',(-185.005249250482,-3.33755261674843,
127.19189254256));
#120797=CARTESIAN_POINT('Ctrl Pts',(-185.013005553224,-3.43836057603525,
127.285028830915));
#120798=CARTESIAN_POINT('Ctrl Pts',(-185.020761855966,-3.53521367065951,
127.382338626523));
#120799=CARTESIAN_POINT('Ctrl Pts',(-185.028518158708,-3.62776404908838,
127.483440403733));
#120800=CARTESIAN_POINT('Ctrl Pts',(-185.036278601222,-3.72036382444085,
127.584596142007));
#120801=CARTESIAN_POINT('Ctrl Pts',(-185.044039043736,-3.80865605608395,
127.689547595635));
#120802=CARTESIAN_POINT('Ctrl Pts',(-185.05179948625,-3.89233379093432,
127.797880828435));
#120803=CARTESIAN_POINT('Ctrl Pts',(-185.059572386516,-3.976145852713,127.906387967359));
#120804=CARTESIAN_POINT('Ctrl Pts',(-185.067345286781,-4.05532838899046,
128.018287414464));
#120805=CARTESIAN_POINT('Ctrl Pts',(-185.075118187046,-4.12961782569921,
128.133136239838));
#120806=CARTESIAN_POINT('Ctrl Pts',(-185.082608522808,-4.20120665425939,
128.243810021123));
#120807=CARTESIAN_POINT('Ctrl Pts',(-185.09009885857,-4.26825180309765,
128.357222203767));
#120808=CARTESIAN_POINT('Ctrl Pts',(-185.097589194332,-4.33055905059273,
128.472957312295));
#120809=CARTESIAN_POINT('Ctrl Pts',(-185.10578677954,-4.39874944774409,
128.599620314307));
#120810=CARTESIAN_POINT('Ctrl Pts',(-185.113984364748,-4.46146195184884,
128.729431206875));
#120811=CARTESIAN_POINT('Ctrl Pts',(-185.122181949956,-4.51841101832934,
128.86190214132));
#120812=CARTESIAN_POINT('Ctrl Pts',(-185.130360998453,-4.57523130928227,
128.994073527142));
#120813=CARTESIAN_POINT('Ctrl Pts',(-185.13854004695,-4.62631401768098,
129.128892662092));
#120814=CARTESIAN_POINT('Ctrl Pts',(-185.146719095448,-4.6714196002999,
129.265847705552));
#120815=CARTESIAN_POINT('Ctrl Pts',(-185.152953088293,-4.70579864566502,
129.370233534949));
#120816=CARTESIAN_POINT('Ctrl Pts',(-185.159187081138,-4.73670625024354,
129.475859598491));
#120817=CARTESIAN_POINT('Ctrl Pts',(-185.165421073984,-4.76405452823401,
129.582490119308));
#120818=CARTESIAN_POINT('Ctrl Pts',(-183.415149158805,-4.76405452823414,
129.582490119309));
#120819=CARTESIAN_POINT('Ctrl Pts',(-183.419067256354,-4.78116185622988,
129.649191331524));
#120820=CARTESIAN_POINT('Ctrl Pts',(-183.422985353904,-4.79685563415493,
129.716203290357));
#120821=CARTESIAN_POINT('Ctrl Pts',(-183.426903451454,-4.81112741488386,
129.783460984765));
#120822=CARTESIAN_POINT('Ctrl Pts',(-183.437819003722,-4.85088762159933,
129.970836329416));
#120823=CARTESIAN_POINT('Ctrl Pts',(-183.448734555991,-4.87971282541858,
130.160606736013));
#120824=CARTESIAN_POINT('Ctrl Pts',(-183.459650108259,-4.89737607248764,
130.351712114724));
#120825=CARTESIAN_POINT('Ctrl Pts',(-183.468146926843,-4.91112539109944,
130.500471214907));
#120826=CARTESIAN_POINT('Ctrl Pts',(-183.476643745428,-4.91811217802289,
130.650039045172));
#120827=CARTESIAN_POINT('Ctrl Pts',(-183.485140564012,-4.91824798071445,
130.799903858857));
#120828=CARTESIAN_POINT('',(-183.139859435957,-4.91824917715616,130.807205596086));
#120829=CARTESIAN_POINT('Ctrl Pts',(-183.069718605797,-4.76405452823406,
129.582490119308));
#120830=CARTESIAN_POINT('Ctrl Pts',(-183.077377441043,-4.79772994797449,
129.71379006978));
#120831=CARTESIAN_POINT('Ctrl Pts',(-183.085036276289,-4.825950394775,129.846394602858));
#120832=CARTESIAN_POINT('Ctrl Pts',(-183.092695111536,-4.84863804824104,
129.97980489498));
#120833=CARTESIAN_POINT('Ctrl Pts',(-183.100555832273,-4.87192374408618,
130.116731857903));
#120834=CARTESIAN_POINT('Ctrl Pts',(-183.10841655301,-4.88938085774212,
130.254507194701));
#120835=CARTESIAN_POINT('Ctrl Pts',(-183.116277273746,-4.90098218359303,
130.392587987825));
#120836=CARTESIAN_POINT('Ctrl Pts',(-183.124137994483,-4.91258350944392,
130.530668780949));
#120837=CARTESIAN_POINT('Ctrl Pts',(-183.13199871522,-4.91832909109846,
130.669054577283));
#120838=CARTESIAN_POINT('Ctrl Pts',(-183.139859435957,-4.91824917715616,
130.807205596086));
#120839=CARTESIAN_POINT('Ctrl Pts',(-183.139859435995,-4.91824917715577,
130.807205596751));
#120840=CARTESIAN_POINT('Ctrl Pts',(-183.149254565264,-4.91815366403183,
130.972323621388));
#120841=CARTESIAN_POINT('Ctrl Pts',(-183.158649694533,-4.90974370090652,
131.137198293807));
#120842=CARTESIAN_POINT('Ctrl Pts',(-183.168044823802,-4.89308820514277,
131.301221643601));
#120843=CARTESIAN_POINT('Ctrl Pts',(-183.175819157921,-4.87930602234573,
131.436948602553));
#120844=CARTESIAN_POINT('Ctrl Pts',(-183.18359349204,-4.85985043506831,
131.572316662951));
#120845=CARTESIAN_POINT('Ctrl Pts',(-183.191367826159,-4.83474526787819,
131.70681352893));
#120846=CARTESIAN_POINT('Ctrl Pts',(-183.199132579106,-4.80967104056291,
131.841144639542));
#120847=CARTESIAN_POINT('Ctrl Pts',(-183.206897332053,-4.77896115788808,
131.974606311377));
#120848=CARTESIAN_POINT('Ctrl Pts',(-183.214662085,-4.74269128219991,132.106690247209));
#120849=CARTESIAN_POINT('Ctrl Pts',(-183.222419125885,-4.70645743026349,
132.238642995413));
#120850=CARTESIAN_POINT('Ctrl Pts',(-183.23017616677,-4.664674677723,132.369220356194));
#120851=CARTESIAN_POINT('Ctrl Pts',(-183.237933207655,-4.61746985964742,
132.497923476673));
#120852=CARTESIAN_POINT('Ctrl Pts',(-183.245684398895,-4.57030063909242,
132.626529541128));
#120853=CARTESIAN_POINT('Ctrl Pts',(-183.253435590136,-4.5177176256354,
132.753263812955));
#120854=CARTESIAN_POINT('Ctrl Pts',(-183.261186781376,-4.45989758071983,
132.877642226993));
#120855=CARTESIAN_POINT('Ctrl Pts',(-183.268934678153,-4.40210211086567,
133.001967776888));
#120856=CARTESIAN_POINT('Ctrl Pts',(-183.27668257493,-4.33907420112053,
133.123939106722));
#120857=CARTESIAN_POINT('Ctrl Pts',(-183.284430471707,-4.27103878920714,
133.243091993423));
#120858=CARTESIAN_POINT('Ctrl Pts',(-183.292176747791,-4.20301760883524,
133.362219955909));
#120859=CARTESIAN_POINT('Ctrl Pts',(-183.299923023875,-4.12999120349208,
133.478530308623));
#120860=CARTESIAN_POINT('Ctrl Pts',(-183.307669299959,-4.05223033797251,
133.591583671165));
#120861=CARTESIAN_POINT('Ctrl Pts',(-183.315415633224,-3.97446889844,133.704637868242));
#120862=CARTESIAN_POINT('Ctrl Pts',(-183.32316196649,-3.89197315055749,
133.814434705049));
#120863=CARTESIAN_POINT('Ctrl Pts',(-183.330908299755,-3.80505680682347,
133.920564359196));
#120864=CARTESIAN_POINT('Ctrl Pts',(-183.338656367758,-3.7181209987768,
134.026717780342));
#120865=CARTESIAN_POINT('Ctrl Pts',(-183.346404435761,-3.62676287263744,
134.129202082239));
#120866=CARTESIAN_POINT('Ctrl Pts',(-183.354152503764,-3.53133571328797,
134.227641374757));
#120867=CARTESIAN_POINT('Ctrl Pts',(-183.361908806506,-3.43580713281808,
134.326185289727));
#120868=CARTESIAN_POINT('Ctrl Pts',(-183.369665109248,-3.33620115280986,
134.420675326271));
#120869=CARTESIAN_POINT('Ctrl Pts',(-183.37742141199,-3.23290753652007,
134.510772888592));
#120870=CARTESIAN_POINT('Ctrl Pts',(-183.385181854504,-3.12955878931717,
134.600918538695));
#120871=CARTESIAN_POINT('Ctrl Pts',(-183.392942297018,-3.02251878900405,
134.686666798853));
#120872=CARTESIAN_POINT('Ctrl Pts',(-183.400702739532,-2.91220871858613,
134.767720737703));
#120873=CARTESIAN_POINT('Ctrl Pts',(-183.408475639798,-2.80172156865031,
134.848904791531));
#120874=CARTESIAN_POINT('Ctrl Pts',(-183.416248540063,-2.68795418328053,
134.925379247005));
#120875=CARTESIAN_POINT('Ctrl Pts',(-183.424021440328,-2.57135568988743,
134.996891235055));
#120876=CARTESIAN_POINT('Ctrl Pts',(-183.43151177609,-2.45899584542431,
135.065803582211));
#120877=CARTESIAN_POINT('Ctrl Pts',(-183.439002111852,-2.34400742397867,
135.130107844031));
#120878=CARTESIAN_POINT('Ctrl Pts',(-183.446492447614,-2.22681044216329,
135.18961982509));
#120879=CARTESIAN_POINT('Ctrl Pts',(-183.454266781733,-2.1051699011596,
135.251388221));
#120880=CARTESIAN_POINT('Ctrl Pts',(-183.462041115852,-1.98076469797066,
135.308189427607));
#120881=CARTESIAN_POINT('Ctrl Pts',(-183.469815449971,-1.85403871937935,
135.359766580764));
#120882=CARTESIAN_POINT('Ctrl Pts',(-183.477580202919,-1.72746891923083,
135.41128016969));
#120883=CARTESIAN_POINT('Ctrl Pts',(-183.485344955866,-1.59858439316792,
135.457582369257));
#120884=CARTESIAN_POINT('Ctrl Pts',(-183.493109708813,-1.467853683391,135.49846208927));
#120885=CARTESIAN_POINT('Ctrl Pts',(-183.500866749698,-1.33725281719802,
135.539301206969));
#120886=CARTESIAN_POINT('Ctrl Pts',(-183.508623790583,-1.204809787081,135.57472844694));
#120887=CARTESIAN_POINT('Ctrl Pts',(-183.516380831468,-1.07101284954884,
135.60458087695));
#120888=CARTESIAN_POINT('Ctrl Pts',(-183.524132022708,-0.937316809328249,
135.634410795011));
#120889=CARTESIAN_POINT('Ctrl Pts',(-183.531883213948,-0.802269273954129,
135.65867418614));
#120890=CARTESIAN_POINT('Ctrl Pts',(-183.539634405188,-0.66637304503378,
135.677258115703));
#120891=CARTESIAN_POINT('Ctrl Pts',(-183.547382301965,-0.530534575635689,
135.695834146601));
#120892=CARTESIAN_POINT('Ctrl Pts',(-183.555130198743,-0.393848516679804,
135.708735464179));
#120893=CARTESIAN_POINT('Ctrl Pts',(-183.56287809552,-0.256827016516643,
135.715900391006));
#120894=CARTESIAN_POINT('Ctrl Pts',(-183.570624371604,-0.119834178297475,
135.723063819085));
#120895=CARTESIAN_POINT('Ctrl Pts',(-183.578370647688,0.01749357137839,
135.724493222735));
#120896=CARTESIAN_POINT('Ctrl Pts',(-183.586116923772,0.15464021435102,
135.720178908207));
#120897=CARTESIAN_POINT('Ctrl Pts',(-183.593863257037,0.291787869708826,
135.715864561833));
#120898=CARTESIAN_POINT('Ctrl Pts',(-183.601609590303,0.42875402492383,
135.705806424969));
#120899=CARTESIAN_POINT('Ctrl Pts',(-183.609355923568,0.565024315543222,
135.690046913814));
#120900=CARTESIAN_POINT('Ctrl Pts',(-183.617103991571,0.701325122949181,
135.674283873426));
#120901=CARTESIAN_POINT('Ctrl Pts',(-183.624852059574,0.836929367365514,
135.652816963002));
#120902=CARTESIAN_POINT('Ctrl Pts',(-183.632600127577,0.971329842672489,
135.625740233323));
#120903=CARTESIAN_POINT('Ctrl Pts',(-183.640356430319,1.10587316040419,
135.598634726173));
#120904=CARTESIAN_POINT('Ctrl Pts',(-183.648112733061,1.23920976945106,
135.565907567004));
#120905=CARTESIAN_POINT('Ctrl Pts',(-183.655869035803,1.37084412301909,
135.527703655382));
#120906=CARTESIAN_POINT('Ctrl Pts',(-183.663629478317,1.50254873380541,
135.489479353182));
#120907=CARTESIAN_POINT('Ctrl Pts',(-183.671389920831,1.63254890835973,
135.445772598521));
#120908=CARTESIAN_POINT('Ctrl Pts',(-183.679150363345,1.76036717021572,
135.396777245936));
#120909=CARTESIAN_POINT('Ctrl Pts',(-183.686923263611,1.88839061729247,
135.347703241661));
#120910=CARTESIAN_POINT('Ctrl Pts',(-183.694696163876,2.01422479326663,
135.293323829465));
#120911=CARTESIAN_POINT('Ctrl Pts',(-183.702469064142,2.13741418789364,
135.233880191051));
#120912=CARTESIAN_POINT('Ctrl Pts',(-183.709959399904,2.25612533772893,
135.176597478624));
#120913=CARTESIAN_POINT('Ctrl Pts',(-183.717449735665,2.37238038492857,
135.114612487253));
#120914=CARTESIAN_POINT('Ctrl Pts',(-183.724940071427,2.48579733142663,
135.048179026684));
#120915=CARTESIAN_POINT('Ctrl Pts',(-183.732714405547,2.60351451592501,
134.979226721265));
#120916=CARTESIAN_POINT('Ctrl Pts',(-183.740488739666,2.71854703082651,
134.905263540102));
#120917=CARTESIAN_POINT('Ctrl Pts',(-183.748263073785,2.83043883740145,
134.826524096371));
#120918=CARTESIAN_POINT('Ctrl Pts',(-183.756027826732,2.94219274732453,
134.747881691967));
#120919=CARTESIAN_POINT('Ctrl Pts',(-183.763792579679,3.05081333368219,
134.664474959851));
#120920=CARTESIAN_POINT('Ctrl Pts',(-183.771557332626,3.15586974181246,
134.57658399844));
#120921=CARTESIAN_POINT('Ctrl Pts',(-183.779314373511,3.26082180643742,
134.488780331571));
#120922=CARTESIAN_POINT('Ctrl Pts',(-183.787071414396,3.36221643965492,
134.396501547914));
#120923=CARTESIAN_POINT('Ctrl Pts',(-183.794828455281,3.45965264739519,
134.300070362649));
#120924=CARTESIAN_POINT('Ctrl Pts',(-183.802579646521,3.55701537773313,
134.203711896892));
#120925=CARTESIAN_POINT('Ctrl Pts',(-183.810330837761,3.65042534745426,
134.103207536208));
#120926=CARTESIAN_POINT('Ctrl Pts',(-183.818082029001,3.73951576490132,
133.998919257903));
#120927=CARTESIAN_POINT('Ctrl Pts',(-183.825829925778,3.82856831654428,
133.894675304899));
#120928=CARTESIAN_POINT('Ctrl Pts',(-183.833577822555,3.91330471401534,
133.786650929633));
#120929=CARTESIAN_POINT('Ctrl Pts',(-183.841325719332,3.99339623765048,
133.675243678859));
#120930=CARTESIAN_POINT('Ctrl Pts',(-183.849071995416,4.07347100786544,
133.56385973208));
#120931=CARTESIAN_POINT('Ctrl Pts',(-183.8568182715,4.14890260875522,133.449094634542));
#120932=CARTESIAN_POINT('Ctrl Pts',(-183.864564547585,4.21940396427489,
133.33137728723));
#120933=CARTESIAN_POINT('Ctrl Pts',(-183.87231088085,4.28990584021965,133.213659070955));
#120934=CARTESIAN_POINT('Ctrl Pts',(-183.880057214115,4.35547719729329,
133.092988896832));
#120935=CARTESIAN_POINT('Ctrl Pts',(-183.887803547381,4.41587569489273,
132.969822441232));
#120936=CARTESIAN_POINT('Ctrl Pts',(-183.895551615384,4.47628771831701,
132.846628403359));
#120937=CARTESIAN_POINT('Ctrl Pts',(-183.903299683387,4.53152440502785,
132.720937322577));
#120938=CARTESIAN_POINT('Ctrl Pts',(-183.911047751389,4.58139072531399,
132.593226762504));
#120939=CARTESIAN_POINT('Ctrl Pts',(-183.918804054131,4.63131004411868,
132.465380470129));
#120940=CARTESIAN_POINT('Ctrl Pts',(-183.926560356873,4.67584745234577,
132.335510775713));
#120941=CARTESIAN_POINT('Ctrl Pts',(-183.934316659615,4.71485700295889,
132.204112918564));
#120942=CARTESIAN_POINT('Ctrl Pts',(-183.942077102129,4.75388737414372,
132.072644930422));
#120943=CARTESIAN_POINT('Ctrl Pts',(-183.949837544643,4.78738391338526,
131.939647533283));
#120944=CARTESIAN_POINT('Ctrl Pts',(-183.957597987157,4.81525162830277,
131.805627224733));
#120945=CARTESIAN_POINT('Ctrl Pts',(-183.965370887423,4.84316407895025,
131.671391774886));
#120946=CARTESIAN_POINT('Ctrl Pts',(-183.973143787688,4.86542958515006,
131.536130518247));
#120947=CARTESIAN_POINT('Ctrl Pts',(-183.980916687954,4.88200484548556,
131.400357053089));
#120948=CARTESIAN_POINT('Ctrl Pts',(-183.988407023716,4.8979775533577,131.269519295378));
#120949=CARTESIAN_POINT('Ctrl Pts',(-183.995897359478,4.90866651731051,
131.138206229746));
#120950=CARTESIAN_POINT('Ctrl Pts',(-184.00338769524,4.91407879538588,131.006876432353));
#120951=CARTESIAN_POINT('Ctrl Pts',(-184.011162029359,4.91969628162939,
130.870567225777));
#120952=CARTESIAN_POINT('Ctrl Pts',(-184.018936363479,4.91964684670001,
130.73380820703));
#120953=CARTESIAN_POINT('Ctrl Pts',(-184.026710697598,4.91388137723509,
130.597109868563));
#120954=CARTESIAN_POINT('Ctrl Pts',(-184.034475450545,4.90812301319603,
130.460579998582));
#120955=CARTESIAN_POINT('Ctrl Pts',(-184.042240203492,4.89666264739697,
130.324111046953));
#120956=CARTESIAN_POINT('Ctrl Pts',(-184.050004956439,4.87950304710029,
130.188216903941));
#120957=CARTESIAN_POINT('Ctrl Pts',(-184.057761997324,4.86236048996048,
130.052457732909));
#120958=CARTESIAN_POINT('Ctrl Pts',(-184.065519038209,4.83953001175498,
129.917272619736));
#120959=CARTESIAN_POINT('Ctrl Pts',(-184.073276079094,4.81106637481358,
129.783173367529));
#120960=CARTESIAN_POINT('Ctrl Pts',(-184.081027270334,4.78262420252226,
129.649175240611));
#120961=CARTESIAN_POINT('Ctrl Pts',(-184.088778461574,4.74855740774753,
129.516261725672));
#120962=CARTESIAN_POINT('Ctrl Pts',(-184.096529652814,4.70897227239641,
129.384937072495));
#120963=CARTESIAN_POINT('Ctrl Pts',(-184.104277549591,4.66940396178373,
129.253668235799));
#120964=CARTESIAN_POINT('Ctrl Pts',(-184.112025446369,4.62432208809752,
129.123987291273));
#120965=CARTESIAN_POINT('Ctrl Pts',(-184.119773343146,4.57388343767266,
128.996385683812));
#120966=CARTESIAN_POINT('Ctrl Pts',(-184.12751961923,4.52345533792613,128.868810767856));
#120967=CARTESIAN_POINT('Ctrl Pts',(-184.135265895314,4.46767283385089,
128.74331468718));
#120968=CARTESIAN_POINT('Ctrl Pts',(-184.143012171398,4.40674160037786,
128.620370798451));
#120969=CARTESIAN_POINT('Ctrl Pts',(-184.150758504663,4.3458099171244,128.497426002177));
#120970=CARTESIAN_POINT('Ctrl Pts',(-184.158504837929,4.2797296022448,128.377033785747));
#120971=CARTESIAN_POINT('Ctrl Pts',(-184.166251171194,4.20875303816093,
128.259644341383));
#120972=CARTESIAN_POINT('Ctrl Pts',(-184.173999239197,4.13776057936755,
128.142228608466));
#120973=CARTESIAN_POINT('Ctrl Pts',(-184.1817473072,4.06186989174729,128.027817320214));
#120974=CARTESIAN_POINT('Ctrl Pts',(-184.189495375203,3.98137734477428,
127.916832695447));
#120975=CARTESIAN_POINT('Ctrl Pts',(-184.197251677945,3.90079924936458,
127.8057301149));
#120976=CARTESIAN_POINT('Ctrl Pts',(-184.205007980687,3.81560975438436,
127.698061789918));
#120977=CARTESIAN_POINT('Ctrl Pts',(-184.212764283429,3.72614663075139,
127.594218198819));
#120978=CARTESIAN_POINT('Ctrl Pts',(-184.220524725943,3.63663575795566,
127.490319183269));
#120979=CARTESIAN_POINT('Ctrl Pts',(-184.228285168457,3.54284697871845,
127.390249254338));
#120980=CARTESIAN_POINT('Ctrl Pts',(-184.236045610971,3.44515507810191,
127.294362106124));
#120981=CARTESIAN_POINT('Ctrl Pts',(-184.243818511237,3.34730635377383,
127.198321031346));
#120982=CARTESIAN_POINT('Ctrl Pts',(-184.251591411502,3.2455422777318,127.106476417236));
#120983=CARTESIAN_POINT('Ctrl Pts',(-184.259364311768,3.14027154927359,
127.01914230691));
#120984=CARTESIAN_POINT('Ctrl Pts',(-184.26685464753,3.03882767695724,126.934983011478));
#120985=CARTESIAN_POINT('Ctrl Pts',(-184.274344983291,2.93412792197492,
126.855012163906));
#120986=CARTESIAN_POINT('Ctrl Pts',(-184.281835319053,2.82656191248064,
126.779471697681));
#120987=CARTESIAN_POINT('Ctrl Pts',(-184.289609653172,2.71491750504099,
126.701067091717));
#120988=CARTESIAN_POINT('Ctrl Pts',(-184.297383987292,2.59983154856586,
126.627187092566));
#120989=CARTESIAN_POINT('Ctrl Pts',(-184.305158321411,2.4817069878406,126.55814895433));
#120990=CARTESIAN_POINT('Ctrl Pts',(-184.312923074358,2.36372800507934,
126.489195899429));
#120991=CARTESIAN_POINT('Ctrl Pts',(-184.320687827305,2.2427182034227,126.425073027955));
#120992=CARTESIAN_POINT('Ctrl Pts',(-184.328452580252,2.11911142907846,
126.366055781973));
#120993=CARTESIAN_POINT('Ctrl Pts',(-184.336209621137,1.99562742272505,
126.307097152752));
#120994=CARTESIAN_POINT('Ctrl Pts',(-184.343966662022,1.8695519272367,126.253234224909));
#120995=CARTESIAN_POINT('Ctrl Pts',(-184.351723702907,1.74134513743703,
126.204697567426));
#120996=CARTESIAN_POINT('Ctrl Pts',(-184.359474894147,1.61323502937467,
126.156197511813));
#120997=CARTESIAN_POINT('Ctrl Pts',(-184.367226085387,1.48299719024648,
126.113015869661));
#120998=CARTESIAN_POINT('Ctrl Pts',(-184.374977276627,1.35111330764339,
126.075335782316));
#120999=CARTESIAN_POINT('Ctrl Pts',(-184.382725173404,1.2192854792087,126.037671710014));
#121000=CARTESIAN_POINT('Ctrl Pts',(-184.390473070181,1.08581337391095,
126.005504648981));
#121001=CARTESIAN_POINT('Ctrl Pts',(-184.398220966959,0.951195205101593,
125.978968328405));
#121002=CARTESIAN_POINT('Ctrl Pts',(-184.405967243043,0.816605195511116,
125.952437558655));
#121003=CARTESIAN_POINT('Ctrl Pts',(-184.413713519127,0.680869982589351,
125.931535262159));
#121004=CARTESIAN_POINT('Ctrl Pts',(-184.421459795211,0.544498987029324,
125.916344259612));
#121005=CARTESIAN_POINT('Ctrl Pts',(-184.429206128476,0.408126984809772,
125.901153144929));
#121006=CARTESIAN_POINT('Ctrl Pts',(-184.436952461741,0.271119579148865,
125.891673451605));
#121007=CARTESIAN_POINT('Ctrl Pts',(-184.444698795007,0.133991948377302,
125.887936183054));
#121008=CARTESIAN_POINT('Ctrl Pts',(-184.45244686301,-0.00316639117658285,
125.884198077567));
#121009=CARTESIAN_POINT('Ctrl Pts',(-184.460194931013,-0.140444618670646,
125.886204966446));
#121010=CARTESIAN_POINT('Ctrl Pts',(-184.467942999016,-0.277327314513638,
125.893935725245));
#121011=CARTESIAN_POINT('Ctrl Pts',(-184.475699301758,-0.41435549091451,
125.901674700386));
#121012=CARTESIAN_POINT('Ctrl Pts',(-184.4834556045,-0.550986904952897,
125.915149675607));
#121013=CARTESIAN_POINT('Ctrl Pts',(-184.491211907241,-0.686710462729283,
125.934287537737));
#121014=CARTESIAN_POINT('Ctrl Pts',(-184.498972349756,-0.822506460255012,
125.95343561432));
#121015=CARTESIAN_POINT('Ctrl Pts',(-184.50673279227,-0.957393251687999,
125.978252529597));
#121016=CARTESIAN_POINT('Ctrl Pts',(-184.514493234784,-1.09087068368609,
126.00861414658));
#121017=CARTESIAN_POINT('Ctrl Pts',(-184.522266135049,-1.22456238550795,
126.039024502726));
#121018=CARTESIAN_POINT('Ctrl Pts',(-184.530039035315,-1.35683982936047,
126.074997244652));
#121019=CARTESIAN_POINT('Ctrl Pts',(-184.53781193558,-1.48721788992002,
126.116358270041));
#121020=CARTESIAN_POINT('Ctrl Pts',(-184.545302271342,-1.61285637957678,
126.156215717975));
#121021=CARTESIAN_POINT('Ctrl Pts',(-184.552792607104,-1.73673089353513,
126.201076390584));
#121022=CARTESIAN_POINT('Ctrl Pts',(-184.560282942866,-1.85842728276808,
126.250743253627));
#121023=CARTESIAN_POINT('Ctrl Pts',(-184.568057639186,-1.98474371230457,
126.302295652556));
#121024=CARTESIAN_POINT('Ctrl Pts',(-184.575832335506,-2.10911352182145,
126.359189682738));
#121025=CARTESIAN_POINT('Ctrl Pts',(-184.583607031826,-2.23105192754482,
126.421257794326));
#121026=CARTESIAN_POINT('Ctrl Pts',(-184.591372063905,-2.35283875923919,
126.483248752913));
#121027=CARTESIAN_POINT('Ctrl Pts',(-184.599137095985,-2.4721998557502,
126.550400819786));
#121028=CARTESIAN_POINT('Ctrl Pts',(-184.606902128064,-2.5886689263795,
126.622497844579));
#121029=CARTESIAN_POINT('Ctrl Pts',(-184.614659365366,-2.70502108178013,
126.694522496164));
#121030=CARTESIAN_POINT('Ctrl Pts',(-184.622416602668,-2.81848665856598,
126.771482022306));
#121031=CARTESIAN_POINT('Ctrl Pts',(-184.63017383997,-2.92862289471845,
126.85311385192));
#121032=CARTESIAN_POINT('Ctrl Pts',(-184.63807648539,-3.0408236162226,126.936275856545));
#121033=CARTESIAN_POINT('Ctrl Pts',(-184.645979130809,-3.1495685597896,
127.02428690553));
#121034=CARTESIAN_POINT('Ctrl Pts',(-184.653881776229,-3.25441882467343,
127.116821983719));
#121035=CARTESIAN_POINT('Ctrl Pts',(-184.66162933114,-3.35721138861581,
127.207541048209));
#121036=CARTESIAN_POINT('Ctrl Pts',(-184.669376886051,-3.45626042849622,
127.30260793449));
#121037=CARTESIAN_POINT('Ctrl Pts',(-184.677124440961,-3.55118486455092,
127.401675042864));
#121038=CARTESIAN_POINT('Ctrl Pts',(-184.684870290526,-3.64608840639422,
127.500720345166));
#121039=CARTESIAN_POINT('Ctrl Pts',(-184.69261614009,-3.73686888073763,
127.603763835403));
#121040=CARTESIAN_POINT('Ctrl Pts',(-184.700361989654,-3.82318206752826,
127.710421067247));
#121041=CARTESIAN_POINT('Ctrl Pts',(-184.708107811659,-3.90949494721215,
127.817077919599));
#121042=CARTESIAN_POINT('Ctrl Pts',(-184.715853633663,-3.99134032571703,
127.927348183657));
#121043=CARTESIAN_POINT('Ctrl Pts',(-184.723599455667,-4.06841453913728,
128.040814670737));
#121044=CARTESIAN_POINT('Ctrl Pts',(-184.731619278531,-4.1482151773007,
128.158294923565));
#121045=CARTESIAN_POINT('Ctrl Pts',(-184.739639101396,-4.22290061394825,
128.279201330047));
#121046=CARTESIAN_POINT('Ctrl Pts',(-184.74765892426,-4.29218348010272,
128.403039307197));
#121047=CARTESIAN_POINT('Ctrl Pts',(-184.755413217867,-4.35917245170187,
128.522777118212));
#121048=CARTESIAN_POINT('Ctrl Pts',(-184.763167511474,-4.42111077918117,
128.645255083161));
#121049=CARTESIAN_POINT('Ctrl Pts',(-184.770921805081,-4.4777865008787,
128.770002951115));
#121050=CARTESIAN_POINT('Ctrl Pts',(-184.779074392574,-4.53737333151672,
128.901158406353));
#121051=CARTESIAN_POINT('Ctrl Pts',(-184.787226980067,-4.59114243408741,
129.034822659559));
#121052=CARTESIAN_POINT('Ctrl Pts',(-184.79537956756,-4.63890608312226,
129.170428729612));
#121053=CARTESIAN_POINT('Ctrl Pts',(-184.803532155053,-4.68666973215712,
129.306034799666));
#121054=CARTESIAN_POINT('Ctrl Pts',(-184.811684742546,-4.72842783798587,
129.443582194741));
#121055=CARTESIAN_POINT('Ctrl Pts',(-184.819837330039,-4.76405452823405,
129.582490119308));
#121056=CARTESIAN_POINT('Origin',(213.235140564004,0.,130.804360617566));
#121057=CARTESIAN_POINT('',(-186.915092859931,-4.76405452823404,129.582490119308));
#121058=CARTESIAN_POINT('',(-186.570144995258,-4.76405452823391,129.582490119308));
#121059=CARTESIAN_POINT('',(213.235140564004,-4.76405452823405,129.582490119308));
#121060=CARTESIAN_POINT('',(-185.235140563977,-4.91824999726717,130.804196661748));
#121061=CARTESIAN_POINT('Ctrl Pts',(-185.235140564012,-4.91824999726719,
130.804196662373));
#121062=CARTESIAN_POINT('Ctrl Pts',(-185.243235275636,-4.91825478877005,
130.947929889419));
#121063=CARTESIAN_POINT('Ctrl Pts',(-185.251329987261,-4.91195447570265,
131.09154808551));
#121064=CARTESIAN_POINT('Ctrl Pts',(-185.259424698885,-4.89940510202952,
131.234491654236));
#121065=CARTESIAN_POINT('Ctrl Pts',(-185.267529366981,-4.88684029266407,
131.377611043127));
#121066=CARTESIAN_POINT('Ctrl Pts',(-185.275634035077,-4.86801111637512,
131.520053813894));
#121067=CARTESIAN_POINT('Ctrl Pts',(-185.283738703172,-4.84302506459005,
131.661268597604));
#121068=CARTESIAN_POINT('Ctrl Pts',(-185.291861849205,-4.8179820467862,
131.802805338704));
#121069=CARTESIAN_POINT('Ctrl Pts',(-185.299984995237,-4.78675414792536,
131.9431081626));
#121070=CARTESIAN_POINT('Ctrl Pts',(-185.308108141269,-4.74949972502816,
132.081637182942));
#121071=CARTESIAN_POINT('Ctrl Pts',(-185.316240943695,-4.71220101591753,
132.220330879723));
#121072=CARTESIAN_POINT('Ctrl Pts',(-185.324373746121,-4.66886158835768,
132.357246244439));
#121073=CARTESIAN_POINT('Ctrl Pts',(-185.332506548547,-4.61968871556572,
132.491861501647));
#121074=CARTESIAN_POINT('Ctrl Pts',(-185.340657905423,-4.57040365811858,
132.626783874656));
#121075=CARTESIAN_POINT('Ctrl Pts',(-185.3488092623,-4.51525867281962,132.759395335421));
#121076=CARTESIAN_POINT('Ctrl Pts',(-185.356960619176,-4.45450870042069,
132.889195215412));
#121077=CARTESIAN_POINT('Ctrl Pts',(-185.363319352166,-4.40711869413288,
132.990449864361));
#121078=CARTESIAN_POINT('Ctrl Pts',(-185.369678085156,-4.35631884409728,
133.08999403756));
#121079=CARTESIAN_POINT('Ctrl Pts',(-185.376036818146,-4.3022485761293,
133.187602160443));
#121080=CARTESIAN_POINT('Ctrl Pts',(-185.383811152265,-4.23614101511718,
133.306940110507));
#121081=CARTESIAN_POINT('Ctrl Pts',(-185.391585486384,-4.16495959670137,
133.423714411295));
#121082=CARTESIAN_POINT('Ctrl Pts',(-185.399359820503,-4.08892792282361,
133.537463525335));
#121083=CARTESIAN_POINT('Ctrl Pts',(-185.40712457345,-4.01298995118897,
133.651072453757));
#121084=CARTESIAN_POINT('Ctrl Pts',(-185.414889326397,-3.93221383272465,
133.761663291662));
#121085=CARTESIAN_POINT('Ctrl Pts',(-185.422654079344,-3.84686924586274,
133.868798586874));
#121086=CARTESIAN_POINT('Ctrl Pts',(-185.430411120229,-3.76160942444742,
133.9758274738));
#121087=CARTESIAN_POINT('Ctrl Pts',(-185.438168161114,-3.67179040642328,
134.079407344235));
#121088=CARTESIAN_POINT('Ctrl Pts',(-185.445925201999,-3.57772519128268,
134.179129575311));
#121089=CARTESIAN_POINT('Ctrl Pts',(-185.453676393239,-3.48373091145266,
134.278776605077));
#121090=CARTESIAN_POINT('Ctrl Pts',(-185.461427584479,-3.38549707525688,
134.37457150257));
#121091=CARTESIAN_POINT('Ctrl Pts',(-185.469178775719,-3.28337675376989,
134.466138895303));
#121092=CARTESIAN_POINT('Ctrl Pts',(-185.476926672496,-3.18129983614355,
134.557667369451));
#121093=CARTESIAN_POINT('Ctrl Pts',(-185.484674569273,-3.07534000912483,
134.644971652084));
#121094=CARTESIAN_POINT('Ctrl Pts',(-185.49242246605,-2.96588681661787,
134.727713578174));
#121095=CARTESIAN_POINT('Ctrl Pts',(-185.500168742134,-2.85645651935925,
134.810438196437));
#121096=CARTESIAN_POINT('Ctrl Pts',(-185.507915018218,-2.74353462176835,
134.888602120789));
#121097=CARTESIAN_POINT('Ctrl Pts',(-185.515661294302,-2.62754301228335,
134.961908065413));
#121098=CARTESIAN_POINT('Ctrl Pts',(-185.523407627568,-2.51155054657478,
135.035214551166));
#121099=CARTESIAN_POINT('Ctrl Pts',(-185.531153960833,-2.39248865425077,
135.103662776763));
#121100=CARTESIAN_POINT('Ctrl Pts',(-185.538900294098,-2.27080706495366,
135.166999536415));
#121101=CARTESIAN_POINT('Ctrl Pts',(-185.546648362101,-2.14909822590848,
135.230350479895));
#121102=CARTESIAN_POINT('Ctrl Pts',(-185.554396430104,-2.02476886923059,
135.288587499175));
#121103=CARTESIAN_POINT('Ctrl Pts',(-185.562144498107,-1.89829174083592,
135.341504160499));
#121104=CARTESIAN_POINT('Ctrl Pts',(-185.569900800848,-1.77168019104392,
135.394477062279));
#121105=CARTESIAN_POINT('Ctrl Pts',(-185.57765710359,-1.64291667088637,
135.442118159409));
#121106=CARTESIAN_POINT('Ctrl Pts',(-185.585413406332,-1.51249277472832,
135.484269662504));
#121107=CARTESIAN_POINT('Ctrl Pts',(-185.593173848846,-1.38199926740991,
135.526443663125));
#121108=CARTESIAN_POINT('Ctrl Pts',(-185.60093429136,-1.24984399481776,
135.563122127009));
#121109=CARTESIAN_POINT('Ctrl Pts',(-185.608694733874,-1.11653102912432,
135.594197934584));
#121110=CARTESIAN_POINT('Ctrl Pts',(-185.61646763414,-0.983004057623368,
135.625323627805));
#121111=CARTESIAN_POINT('Ctrl Pts',(-185.624240534405,-0.848316063641948,
135.650828619293));
#121112=CARTESIAN_POINT('Ctrl Pts',(-185.63201343467,-0.712979458432716,
135.670657295159));
#121113=CARTESIAN_POINT('Ctrl Pts',(-185.639503770433,-0.582562679703454,
135.689765148714));
#121114=CARTESIAN_POINT('Ctrl Pts',(-185.646994106196,-0.451543934645043,
135.703602186016));
#121115=CARTESIAN_POINT('Ctrl Pts',(-185.654484441958,-0.320381836731385,
135.712164458511));
#121116=CARTESIAN_POINT('Ctrl Pts',(-185.662258776077,-0.184246688020785,
135.721051372169));
#121117=CARTESIAN_POINT('Ctrl Pts',(-185.670033110196,-0.047525866190644,
135.72428379084));
#121118=CARTESIAN_POINT('Ctrl Pts',(-185.677807444315,0.0892714619018228,
135.721800364893));
#121119=CARTESIAN_POINT('Ctrl Pts',(-185.685572197262,0.225900199513344,
135.719319999546));
#121120=CARTESIAN_POINT('Ctrl Pts',(-185.69333695021,0.362604868635719,
135.711137812602));
#121121=CARTESIAN_POINT('Ctrl Pts',(-185.701101703157,0.498871660584027,
135.697244238578));
#121122=CARTESIAN_POINT('Ctrl Pts',(-185.708858744042,0.635003110433547,
135.683364463847));
#121123=CARTESIAN_POINT('Ctrl Pts',(-185.716615784927,0.770697162159242,
135.663784630225));
#121124=CARTESIAN_POINT('Ctrl Pts',(-185.724372825812,0.905440845898517,
135.638547202409));
#121125=CARTESIAN_POINT('Ctrl Pts',(-185.732124017052,1.04008291837792,
135.613328806334));
#121126=CARTESIAN_POINT('Ctrl Pts',(-185.739875208292,1.17377566665088,
135.58246137983));
#121127=CARTESIAN_POINT('Ctrl Pts',(-185.747626399532,1.3060124356725,135.546039073595));
#121128=CARTESIAN_POINT('Ctrl Pts',(-185.755374296309,1.43819300053959,
135.509632247811));
#121129=CARTESIAN_POINT('Ctrl Pts',(-185.763122193086,1.56891844082116,
135.46767534169));
#121130=CARTESIAN_POINT('Ctrl Pts',(-185.770870089863,1.69769369070752,
135.420313303094));
#121131=CARTESIAN_POINT('Ctrl Pts',(-185.778616365947,1.82644200358802,
135.372961171615));
#121132=CARTESIAN_POINT('Ctrl Pts',(-185.786362642032,1.95324057078163,
135.320206291428));
#121133=CARTESIAN_POINT('Ctrl Pts',(-185.794108918116,2.07761123630648,
135.262242918981));
#121134=CARTESIAN_POINT('Ctrl Pts',(-185.801855251381,2.20198281990683,
135.204279118662));
#121135=CARTESIAN_POINT('Ctrl Pts',(-185.809601584646,2.32392611170664,
135.141106914518));
#121136=CARTESIAN_POINT('Ctrl Pts',(-185.817347917912,2.44298499264541,
135.072967812918));
#121137=CARTESIAN_POINT('Ctrl Pts',(-185.825095985915,2.56207053599523,
135.004813452038));
#121138=CARTESIAN_POINT('Ctrl Pts',(-185.832844053918,2.67827004387223,
134.931690174513));
#121139=CARTESIAN_POINT('Ctrl Pts',(-185.840592121921,2.79115430699464,
134.853884132382));
#121140=CARTESIAN_POINT('Ctrl Pts',(-185.848348424663,2.9041585448554,134.775995397063));
#121141=CARTESIAN_POINT('Ctrl Pts',(-185.856104727404,3.01384017700653,
134.693414177478));
#121142=CARTESIAN_POINT('Ctrl Pts',(-185.863861030146,3.11980073200734,
134.606468776873));
#121143=CARTESIAN_POINT('Ctrl Pts',(-185.871621472661,3.22581784134676,
134.519476970889));
#121144=CARTESIAN_POINT('Ctrl Pts',(-185.879381915175,3.32810962470852,
134.428116602875));
#121145=CARTESIAN_POINT('Ctrl Pts',(-185.887142357689,3.42631349604209,
134.33275386228));
#121146=CARTESIAN_POINT('Ctrl Pts',(-185.894915257954,3.52467501294806,
134.237238036947));
#121147=CARTESIAN_POINT('Ctrl Pts',(-185.90268815822,3.61893523531003,134.13770728394));
#121148=CARTESIAN_POINT('Ctrl Pts',(-185.910461058485,3.70877040278946,
134.034562648692));
#121149=CARTESIAN_POINT('Ctrl Pts',(-185.917951394247,3.79533983565013,
133.935167580741));
#121150=CARTESIAN_POINT('Ctrl Pts',(-185.925441730009,3.8778001590255,133.832417056538));
#121151=CARTESIAN_POINT('Ctrl Pts',(-185.932932065771,3.9559001591004,133.726694786296));
#121152=CARTESIAN_POINT('Ctrl Pts',(-185.94070639989,4.03696134441601,133.616964024045));
#121153=CARTESIAN_POINT('Ctrl Pts',(-185.948480734009,4.11358181358176,
133.503684125752));
#121154=CARTESIAN_POINT('Ctrl Pts',(-185.956255068128,4.18543473429262,
133.38725030694));
#121155=CARTESIAN_POINT('Ctrl Pts',(-185.964019821076,4.25719910270018,
133.270959982405));
#121156=CARTESIAN_POINT('Ctrl Pts',(-185.971784574023,4.32420740995068,
133.15152380069));
#121157=CARTESIAN_POINT('Ctrl Pts',(-185.97954932697,4.38617388218686,133.029368873219));
#121158=CARTESIAN_POINT('Ctrl Pts',(-185.987306367855,4.44807880844942,
132.907335271742));
#121159=CARTESIAN_POINT('Ctrl Pts',(-185.99506340874,4.50495168936313,132.782588644633));
#121160=CARTESIAN_POINT('Ctrl Pts',(-186.002820449625,4.55655097893896,
132.655583521171));
#121161=CARTESIAN_POINT('Ctrl Pts',(-186.010571640865,4.60811135708892,
132.52867417326));
#121162=CARTESIAN_POINT('Ctrl Pts',(-186.018322832105,4.65440591302887,
132.399510079759));
#121163=CARTESIAN_POINT('Ctrl Pts',(-186.026074023345,4.69523999897835,
132.268568394657));
#121164=CARTESIAN_POINT('Ctrl Pts',(-186.033821920122,4.73605672935219,
132.137682363264));
#121165=CARTESIAN_POINT('Ctrl Pts',(-186.041569816899,4.77141748956988,
132.005020615405));
#121166=CARTESIAN_POINT('Ctrl Pts',(-186.049317713676,4.80117663320995,
131.871078011827));
#121167=CARTESIAN_POINT('Ctrl Pts',(-186.05706398976,4.83092955187871,131.737163426154));
#121168=CARTESIAN_POINT('Ctrl Pts',(-186.064810265844,4.85508309987727,
131.601968899102));
#121169=CARTESIAN_POINT('Ctrl Pts',(-186.072556541928,4.87354225566816,
131.466001717194));
#121170=CARTESIAN_POINT('Ctrl Pts',(-186.080302875194,4.89200154772027,
131.330033531608));
#121171=CARTESIAN_POINT('Ctrl Pts',(-186.088049208459,4.90476631109189,
131.193293067196));
#121172=CARTESIAN_POINT('Ctrl Pts',(-186.095795541724,4.91179318843833,
131.056294609935));
#121173=CARTESIAN_POINT('Ctrl Pts',(-186.103543609727,4.91882163940525,
130.919265472818));
#121174=CARTESIAN_POINT('Ctrl Pts',(-186.11129167773,4.92010962740263,130.781978618262));
#121175=CARTESIAN_POINT('Ctrl Pts',(-186.119039745733,4.91566590214478,
130.644949824358));
#121176=CARTESIAN_POINT('Ctrl Pts',(-186.126796048475,4.91121745404283,
130.507775394621));
#121177=CARTESIAN_POINT('Ctrl Pts',(-186.134552351217,4.90102513648487,
130.370859964803));
#121178=CARTESIAN_POINT('Ctrl Pts',(-186.142308653959,4.88514977674217,
130.234716236135));
#121179=CARTESIAN_POINT('Ctrl Pts',(-186.150069096473,4.86926594384197,
130.09849984346));
#121180=CARTESIAN_POINT('Ctrl Pts',(-186.157829538987,4.84769308629387,
129.963056358551));
#121181=CARTESIAN_POINT('Ctrl Pts',(-186.165589981501,4.82054330303636,
129.828888769663));
#121182=CARTESIAN_POINT('Ctrl Pts',(-186.173362881767,4.79334993653653,
129.694505803051));
#121183=CARTESIAN_POINT('Ctrl Pts',(-186.181135782032,4.76056184779475,
129.561403205215));
#121184=CARTESIAN_POINT('Ctrl Pts',(-186.188908682298,4.72234144732119,
129.430070139751));
#121185=CARTESIAN_POINT('Ctrl Pts',(-186.19639901806,4.68551045467694,129.303511362027));
#121186=CARTESIAN_POINT('Ctrl Pts',(-186.203889353822,4.6436353476091,129.178595988423));
#121187=CARTESIAN_POINT('Ctrl Pts',(-186.211379689583,4.59690316518476,
129.05574277698));
#121188=CARTESIAN_POINT('Ctrl Pts',(-186.219154023703,4.54839911785924,
128.928231548683));
#121189=CARTESIAN_POINT('Ctrl Pts',(-186.226928357822,4.49450876631522,
128.802538025928));
#121190=CARTESIAN_POINT('Ctrl Pts',(-186.234702691941,4.43538795572149,
128.679150805632));
#121191=CARTESIAN_POINT('Ctrl Pts',(-186.242467444888,4.37634000624273,
128.555915649057));
#121192=CARTESIAN_POINT('Ctrl Pts',(-186.250232197835,4.31207459079579,
128.434981488786));
#121193=CARTESIAN_POINT('Ctrl Pts',(-186.257996950782,4.2427965825651,128.316819618613));
#121194=CARTESIAN_POINT('Ctrl Pts',(-186.265753991667,4.17358738222901,
128.198775108475));
#121195=CARTESIAN_POINT('Ctrl Pts',(-186.273511032552,4.09937569316561,
128.083497743981));
#121196=CARTESIAN_POINT('Ctrl Pts',(-186.281268073437,4.02041336222315,
127.971436428789));
#121197=CARTESIAN_POINT('Ctrl Pts',(-186.289019264677,3.94151057738879,
127.859459619907));
#121198=CARTESIAN_POINT('Ctrl Pts',(-186.296770455917,3.85786450570213,
127.750694351319));
#121199=CARTESIAN_POINT('Ctrl Pts',(-186.304521647158,3.76977137844832,
127.645562299102));
#121200=CARTESIAN_POINT('Ctrl Pts',(-186.312269543935,3.68171569312366,
127.540474930812));
#121201=CARTESIAN_POINT('Ctrl Pts',(-186.320017440712,3.58921696210682,
127.439018006611));
#121202=CARTESIAN_POINT('Ctrl Pts',(-186.327765337489,3.49261280031067,
127.341581547281));
#121203=CARTESIAN_POINT('Ctrl Pts',(-186.335511613573,3.39602884602262,
127.244165469557));
#121204=CARTESIAN_POINT('Ctrl Pts',(-186.343257889657,3.29534144418254,
127.15076846138));
#121205=CARTESIAN_POINT('Ctrl Pts',(-186.351004165741,3.19092602784825,
127.061744667819));
#121206=CARTESIAN_POINT('Ctrl Pts',(-186.358750499007,3.08650984074266,
126.972720217104));
#121207=CARTESIAN_POINT('Ctrl Pts',(-186.366496832272,2.97836588174077,
126.888069299076));
#121208=CARTESIAN_POINT('Ctrl Pts',(-186.374243165537,2.86690339849536,
126.808106375629));
#121209=CARTESIAN_POINT('Ctrl Pts',(-186.38199123354,2.75541595399981,126.728125545041));
#121210=CARTESIAN_POINT('Ctrl Pts',(-186.389739301543,2.64060882406983,
126.652835025955));
#121211=CARTESIAN_POINT('Ctrl Pts',(-186.397487369546,2.52292067685579,
126.582506247648));
#121212=CARTESIAN_POINT('Ctrl Pts',(-186.405243672288,2.40510744927854,
126.512102723079));
#121213=CARTESIAN_POINT('Ctrl Pts',(-186.41299997503,2.2844074239254,126.44667167434));
#121214=CARTESIAN_POINT('Ctrl Pts',(-186.420756277772,2.16128482948886,
126.386439053264));
#121215=CARTESIAN_POINT('Ctrl Pts',(-186.428516720286,2.03809652081653,
126.326174284226));
#121216=CARTESIAN_POINT('Ctrl Pts',(-186.4362771628,1.9124834245532,126.271113628271));
#121217=CARTESIAN_POINT('Ctrl Pts',(-186.444037605315,1.78492931117828,
126.221434650829));
#121218=CARTESIAN_POINT('Ctrl Pts',(-186.45181050558,1.65717043661684,126.171675924281));
#121219=CARTESIAN_POINT('Ctrl Pts',(-186.459583405845,1.52746468853852,
126.127316266604));
#121220=CARTESIAN_POINT('Ctrl Pts',(-186.467356306111,1.39631140097754,
126.088483442109));
#121221=CARTESIAN_POINT('Ctrl Pts',(-186.474846641873,1.26992586577211,
126.051062288597));
#121222=CARTESIAN_POINT('Ctrl Pts',(-186.482336977635,1.14219650594113,
126.018773191476));
#121223=CARTESIAN_POINT('Ctrl Pts',(-186.489827313397,1.0135767336687,125.991685138431));
#121224=CARTESIAN_POINT('Ctrl Pts',(-186.497601647516,0.880080303639861,
125.963570033623));
#121225=CARTESIAN_POINT('Ctrl Pts',(-186.505375981635,0.745201731765015,
125.940969093346));
#121226=CARTESIAN_POINT('Ctrl Pts',(-186.513150315754,0.609436326590159,
125.924015299217));
#121227=CARTESIAN_POINT('Ctrl Pts',(-186.520915068702,0.47383824014311,
125.907082399123));
#121228=CARTESIAN_POINT('Ctrl Pts',(-186.528679821649,0.337355879254183,
125.895782845622));
#121229=CARTESIAN_POINT('Ctrl Pts',(-186.536444574596,0.200496495701578,
125.890199018909));
#121230=CARTESIAN_POINT('Ctrl Pts',(-186.544201615481,0.0637730428177244,
125.884620738132));
#121231=CARTESIAN_POINT('Ctrl Pts',(-186.551958656366,-0.0733262994167068,
125.88474690261));
#121232=CARTESIAN_POINT('Ctrl Pts',(-186.559715697251,-0.2102877262663,
125.89060826985));
#121233=CARTESIAN_POINT('Ctrl Pts',(-186.567466888491,-0.34714586943757,
125.896465216988));
#121234=CARTESIAN_POINT('Ctrl Pts',(-186.575218079731,-0.483865915208605,
125.908048741667));
#121235=CARTESIAN_POINT('Ctrl Pts',(-186.582969270971,-0.619932975308011,
125.925337542336));
#121236=CARTESIAN_POINT('Ctrl Pts',(-186.590717167748,-0.755942203277722,
125.942618994804));
#121237=CARTESIAN_POINT('Ctrl Pts',(-186.598465064525,-0.891298610539438,
125.965600851155));
#121238=CARTESIAN_POINT('Ctrl Pts',(-186.606212961302,-1.02549157245746,
125.994209882161));
#121239=CARTESIAN_POINT('Ctrl Pts',(-186.613959237386,-1.15965646410071,
126.022812928774));
#121240=CARTESIAN_POINT('Ctrl Pts',(-186.62170551347,-1.29265801234209,
126.057040727289));
#121241=CARTESIAN_POINT('Ctrl Pts',(-186.629451789554,-1.42399533416772,
126.096768839303));
#121242=CARTESIAN_POINT('Ctrl Pts',(-186.63719812282,-1.55533362549545,
126.136497244581));
#121243=CARTESIAN_POINT('Ctrl Pts',(-186.644944456085,-1.68500729167432,
126.181725931178));
#121244=CARTESIAN_POINT('Ctrl Pts',(-186.65269078935,-1.81253055865413,
126.232280561788));
#121245=CARTESIAN_POINT('Ctrl Pts',(-186.660438857353,-1.94008238358522,
126.282846513757));
#121246=CARTESIAN_POINT('Ctrl Pts',(-186.668186925356,-2.06548248767706,
126.338740639035));
#121247=CARTESIAN_POINT('Ctrl Pts',(-186.675934993359,-2.18826539894326,
126.399740587837));
#121248=CARTESIAN_POINT('Ctrl Pts',(-186.683691296101,-2.31117880534887,
126.460805368111));
#121249=CARTESIAN_POINT('Ctrl Pts',(-186.691447598843,-2.43146911172216,
126.526986637757));
#121250=CARTESIAN_POINT('Ctrl Pts',(-186.699203901585,-2.54869529143897,
126.598015960516));
#121251=CARTESIAN_POINT('Ctrl Pts',(-186.706964344099,-2.66598403829782,
126.669083193762));
#121252=CARTESIAN_POINT('Ctrl Pts',(-186.714724786613,-2.7802050743521,
126.745003419722));
#121253=CARTESIAN_POINT('Ctrl Pts',(-186.722485229127,-2.89094751901861,
126.825465607041));
#121254=CARTESIAN_POINT('Ctrl Pts',(-186.730258129393,-3.00186773728824,
126.906056959406));
#121255=CARTESIAN_POINT('Ctrl Pts',(-186.738031029658,-3.10929789869776,
126.991204600203));
#121256=CARTESIAN_POINT('Ctrl Pts',(-186.745803929924,-3.21286060927254,
127.080557485299));
#121257=CARTESIAN_POINT('Ctrl Pts',(-186.753294265686,-3.31265855445779,
127.166662167953));
#121258=CARTESIAN_POINT('Ctrl Pts',(-186.760784601447,-3.40886512528903,
127.256671450161));
#121259=CARTESIAN_POINT('Ctrl Pts',(-186.768274937209,-3.50117720011197,
127.350241152939));
#121260=CARTESIAN_POINT('Ctrl Pts',(-186.775943029108,-3.5956799694917,
127.446031395543));
#121261=CARTESIAN_POINT('Ctrl Pts',(-186.783611121006,-3.68641809312052,
127.545874838496));
#121262=CARTESIAN_POINT('Ctrl Pts',(-186.791279212905,-3.77301654595831,
127.649439191219));
#121263=CARTESIAN_POINT('Ctrl Pts',(-186.798938310547,-3.85951342349731,
127.75288206856));
#121264=CARTESIAN_POINT('Ctrl Pts',(-186.806597408188,-3.94188002817934,
127.860036873487));
#121265=CARTESIAN_POINT('Ctrl Pts',(-186.81425650583,-4.0197769009932,127.970533394756));
#121266=CARTESIAN_POINT('Ctrl Pts',(-186.821908387342,-4.09760038214203,
128.080925810129));
#121267=CARTESIAN_POINT('Ctrl Pts',(-186.829560268854,-4.17096227552672,
128.194653354138));
#121268=CARTESIAN_POINT('Ctrl Pts',(-186.837212150366,-4.23956264999936,
128.311311961958));
#121269=CARTESIAN_POINT('Ctrl Pts',(-186.844858218946,-4.30811091057845,
128.427881947313));
#121270=CARTESIAN_POINT('Ctrl Pts',(-186.852504287526,-4.37190464719919,
128.547378219883));
#121271=CARTESIAN_POINT('Ctrl Pts',(-186.860150356106,-4.43068697554932,
128.669367412144));
#121272=CARTESIAN_POINT('Ctrl Pts',(-186.867793074609,-4.48944354879428,
128.791303155613));
#121273=CARTESIAN_POINT('Ctrl Pts',(-186.875435793112,-4.54319290765865,
128.915729283918));
#121274=CARTESIAN_POINT('Ctrl Pts',(-186.883078511615,-4.59172410237677,
129.04218785925));
#121275=CARTESIAN_POINT('Ctrl Pts',(-186.890720376631,-4.64024987745937,
129.168632312543));
#121276=CARTESIAN_POINT('Ctrl Pts',(-186.898362241647,-4.68355850002953,
129.297108387139));
#121277=CARTESIAN_POINT('Ctrl Pts',(-186.906004106664,-4.72148732126051,
129.427138581119));
#121278=CARTESIAN_POINT('Ctrl Pts',(-186.909033691086,-4.73652403883128,
129.478688490636));
#121279=CARTESIAN_POINT('Ctrl Pts',(-186.912063275508,-4.75071576216139,
129.530482472835));
#121280=CARTESIAN_POINT('Ctrl Pts',(-186.915092859931,-4.76405452823404,
129.582490119308));
#121281=CARTESIAN_POINT('Ctrl Pts',(-185.165421073984,-4.76405452823401,
129.582490119308));
#121282=CARTESIAN_POINT('Ctrl Pts',(-185.17357585509,-4.79982922771808,
129.72197512964));
#121283=CARTESIAN_POINT('Ctrl Pts',(-185.181730636195,-4.82951156155369,
129.863179394967));
#121284=CARTESIAN_POINT('Ctrl Pts',(-185.189885417301,-4.85294732447109,
130.005558183663));
#121285=CARTESIAN_POINT('Ctrl Pts',(-185.198024167137,-4.87633701563996,
130.147657073652));
#121286=CARTESIAN_POINT('Ctrl Pts',(-185.206162916974,-4.89350457056318,
130.29092555989));
#121287=CARTESIAN_POINT('Ctrl Pts',(-185.21430166681,-4.90434637358492,
130.434807224395));
#121288=CARTESIAN_POINT('Ctrl Pts',(-185.221247965866,-4.9135996873744,
130.557608034144));
#121289=CARTESIAN_POINT('Ctrl Pts',(-185.228194264921,-4.91824588552851,
130.680855148721));
#121290=CARTESIAN_POINT('Ctrl Pts',(-185.235140563977,-4.91824999726717,
130.804196661748));
#121291=CARTESIAN_POINT('',(-184.889859436036,-4.91824816211532,130.800108753356));
#121292=CARTESIAN_POINT('Ctrl Pts',(-184.819837330039,-4.76405452823405,
129.582490119308));
#121293=CARTESIAN_POINT('Ctrl Pts',(-184.826135075586,-4.79157558581711,
129.689794305134));
#121294=CARTESIAN_POINT('Ctrl Pts',(-184.832432821132,-4.8154390765796,
129.797910017712));
#121295=CARTESIAN_POINT('Ctrl Pts',(-184.838730566679,-4.83561259437176,
129.906566710451));
#121296=CARTESIAN_POINT('Ctrl Pts',(-184.850410110173,-4.87302558235891,
130.108077006377));
#121297=CARTESIAN_POINT('Ctrl Pts',(-184.862089653666,-4.89785094753426,
130.311991589822));
#121298=CARTESIAN_POINT('Ctrl Pts',(-184.87376919716,-4.90985019127264,
130.517038217186));
#121299=CARTESIAN_POINT('Ctrl Pts',(-184.879132610105,-4.91536041512924,
130.611198552825));
#121300=CARTESIAN_POINT('Ctrl Pts',(-184.88449602305,-4.9181664561817,130.705597270812));
#121301=CARTESIAN_POINT('Ctrl Pts',(-184.889859435995,-4.9182481621147,
130.800108752638));
#121302=CARTESIAN_POINT('Ctrl Pts',(-184.889859436036,-4.91824816211532,
130.800108753357));
#121303=CARTESIAN_POINT('Ctrl Pts',(-184.897506058226,-4.91836465031066,
130.934853849735));
#121304=CARTESIAN_POINT('Ctrl Pts',(-184.905152680416,-4.91293956817794,
131.069789576618));
#121305=CARTESIAN_POINT('Ctrl Pts',(-184.912799302606,-4.90195264080868,
131.204414826104));
#121306=CARTESIAN_POINT('Ctrl Pts',(-184.920439094191,-4.89097552788502,
131.338919817018));
#121307=CARTESIAN_POINT('Ctrl Pts',(-184.928078885776,-4.87444648449873,
131.473114482282));
#121308=CARTESIAN_POINT('Ctrl Pts',(-184.935718677362,-4.85239729067965,
131.60649751106));
#121309=CARTESIAN_POINT('Ctrl Pts',(-184.943353957593,-4.83036111707372,
131.739801776167));
#121310=CARTESIAN_POINT('Ctrl Pts',(-184.950989237825,-4.80281134123516,
131.872294960994));
#121311=CARTESIAN_POINT('Ctrl Pts',(-184.958624518056,-4.76983155314398,
132.003481135751));
#121312=CARTESIAN_POINT('Ctrl Pts',(-184.96625747086,-4.73686181813173,
132.134627321622));
#121313=CARTESIAN_POINT('Ctrl Pts',(-184.973890423664,-4.69846545941638,
132.264466898419));
#121314=CARTESIAN_POINT('Ctrl Pts',(-184.981523376467,-4.65477702326063,
132.392514868961));
#121315=CARTESIAN_POINT('Ctrl Pts',(-184.989155769078,-4.61109179346305,
132.520553441876));
#121316=CARTESIAN_POINT('Ctrl Pts',(-184.996788161688,-4.56211538887205,
132.646800288048));
#121317=CARTESIAN_POINT('Ctrl Pts',(-185.004420554298,-4.50803182670943,
132.770786846));
#121318=CARTESIAN_POINT('Ctrl Pts',(-185.012054153287,-4.45393971608056,
132.89479300131));
#121319=CARTESIAN_POINT('Ctrl Pts',(-185.019687752276,-4.39473900456917,
133.016537788303));
#121320=CARTESIAN_POINT('Ctrl Pts',(-185.027321351264,-4.33066108607502,
133.13557438298));
#121321=CARTESIAN_POINT('Ctrl Pts',(-185.034962554895,-4.26651933273594,
133.254729562698));
#121322=CARTESIAN_POINT('Ctrl Pts',(-185.042603758525,-4.19749086029851,
133.371170805936));
#121323=CARTESIAN_POINT('Ctrl Pts',(-185.050244962156,-4.12385227870567,
133.484477302696));
#121324=CARTESIAN_POINT('Ctrl Pts',(-185.057889999776,-4.05017674879779,
133.597840651233));
#121325=CARTESIAN_POINT('Ctrl Pts',(-185.065535037397,-3.9718867376698,
133.708065792888));
#121326=CARTESIAN_POINT('Ctrl Pts',(-185.073180075017,-3.88930031472982,
133.814763601278));
#121327=CARTESIAN_POINT('Ctrl Pts',(-185.080837121003,-3.80658417000405,
133.921629004168));
#121328=CARTESIAN_POINT('Ctrl Pts',(-185.088494166989,-3.7195583925844,
134.024955697636));
#121329=CARTESIAN_POINT('Ctrl Pts',(-185.096151212975,-3.62857964916102,
134.124389652408));
#121330=CARTESIAN_POINT('Ctrl Pts',(-185.103160205481,-3.54530088447839,
134.215408022297));
#121331=CARTESIAN_POINT('Ctrl Pts',(-185.110169197986,-3.45871056569238,
134.303164978857));
#121332=CARTESIAN_POINT('Ctrl Pts',(-185.117178190492,-3.36910616455944,
134.387418908248));
#121333=CARTESIAN_POINT('Ctrl Pts',(-185.124952524611,-3.26971747889623,
134.480872881472));
#121334=CARTESIAN_POINT('Ctrl Pts',(-185.13272685873,-3.1662800113838,134.570336404582));
#121335=CARTESIAN_POINT('Ctrl Pts',(-185.140501192849,-3.05914760954894,
134.655438254474));
#121336=CARTESIAN_POINT('Ctrl Pts',(-185.148265945796,-2.95214723882493,
134.740435223941));
#121337=CARTESIAN_POINT('Ctrl Pts',(-185.156030698744,-2.84146129743104,
134.821080974734));
#121338=CARTESIAN_POINT('Ctrl Pts',(-185.163795451691,-2.7274801549028,
134.897041287629));
#121339=CARTESIAN_POINT('Ctrl Pts',(-185.171552492576,-2.61361222005217,
134.972926155671));
#121340=CARTESIAN_POINT('Ctrl Pts',(-185.179309533461,-2.4964559204001,
135.044134631363));
#121341=CARTESIAN_POINT('Ctrl Pts',(-185.187066574346,-2.37643407513157,
135.110373175496));
#121342=CARTESIAN_POINT('Ctrl Pts',(-185.194817765586,-2.25650273927002,
135.176561768628));
#121343=CARTESIAN_POINT('Ctrl Pts',(-185.202568956826,-2.13371049990436,
135.237787701952));
#121344=CARTESIAN_POINT('Ctrl Pts',(-185.210320148066,-2.00850818166039,
135.293801334037));
#121345=CARTESIAN_POINT('Ctrl Pts',(-185.218068044844,-1.88335907774139,
135.349791158833));
#121346=CARTESIAN_POINT('Ctrl Pts',(-185.225815941621,-1.75580228842462,
135.400572929258));
#121347=CARTESIAN_POINT('Ctrl Pts',(-185.233563838398,-1.62631200864633,
135.445943570938));
#121348=CARTESIAN_POINT('Ctrl Pts',(-185.241310114482,-1.49684881544309,
135.491304722058));
#121349=CARTESIAN_POINT('Ctrl Pts',(-185.249056390566,-1.36545330497909,
135.531256866629));
#121350=CARTESIAN_POINT('Ctrl Pts',(-185.25680266665,-1.23261799023726,
135.56564573323));
#121351=CARTESIAN_POINT('Ctrl Pts',(-185.264548999916,-1.09978169493548,
135.600034853681));
#121352=CARTESIAN_POINT('Ctrl Pts',(-185.272295333181,-0.965505952635501,
135.628860516231));
#121353=CARTESIAN_POINT('Ctrl Pts',(-185.280041666446,-0.830296328772982,
135.65201892534));
#121354=CARTESIAN_POINT('Ctrl Pts',(-185.287789734449,-0.695056425652861,
135.675182520613));
#121355=CARTESIAN_POINT('Ctrl Pts',(-185.295537802453,-0.558882610093101,
135.692676271008));
#121356=CARTESIAN_POINT('Ctrl Pts',(-185.303285870456,-0.42228808350065,
135.704447947097));
#121357=CARTESIAN_POINT('Ctrl Pts',(-185.311042173197,-0.285548382619655,
135.716232134264));
#121358=CARTESIAN_POINT('Ctrl Pts',(-185.318798475939,-0.148387467644769,
135.722282065073));
#121359=CARTESIAN_POINT('Ctrl Pts',(-185.326554778681,-0.0113216354735307,
135.722597586549));
#121360=CARTESIAN_POINT('Ctrl Pts',(-185.334315221195,0.125817352859683,
135.722913276428));
#121361=CARTESIAN_POINT('Ctrl Pts',(-185.34207566371,0.262860766800342,
135.717488473873));
#121362=CARTESIAN_POINT('Ctrl Pts',(-185.349836106224,0.399295898810333,
135.706375085894));
#121363=CARTESIAN_POINT('Ctrl Pts',(-185.357609006489,0.535950048605996,
135.695243857718));
#121364=CARTESIAN_POINT('Ctrl Pts',(-185.365381906755,0.671993576948554,
135.678405843878));
#121365=CARTESIAN_POINT('Ctrl Pts',(-185.37315480702,0.806921561960867,
135.655964543624));
#121366=CARTESIAN_POINT('Ctrl Pts',(-185.380645142782,0.936944574849048,
135.634339041161));
#121367=CARTESIAN_POINT('Ctrl Pts',(-185.388135478544,1.06593144034985,
135.60751062932));
#121368=CARTESIAN_POINT('Ctrl Pts',(-185.395625814305,1.19344424050067,
135.575615579032));
#121369=CARTESIAN_POINT('Ctrl Pts',(-185.403400148425,1.32579172723165,
135.542511218217));
#121370=CARTESIAN_POINT('Ctrl Pts',(-185.411174482543,1.45697040075332,
135.503843566807));
#121371=CARTESIAN_POINT('Ctrl Pts',(-185.418948816663,1.5864766773227,135.459709671591));
#121372=CARTESIAN_POINT('Ctrl Pts',(-185.42671356961,1.71582334898017,135.415630167457));
#121373=CARTESIAN_POINT('Ctrl Pts',(-185.434478322557,1.84350135810591,
135.366097948359));
#121374=CARTESIAN_POINT('Ctrl Pts',(-185.442243075504,1.9690185123329,135.31126078959));
#121375=CARTESIAN_POINT('Ctrl Pts',(-185.450000116389,2.09441100115318,
135.25647809586));
#121376=CARTESIAN_POINT('Ctrl Pts',(-185.457757157274,2.21764655014518,
135.196401103399));
#121377=CARTESIAN_POINT('Ctrl Pts',(-185.465514198159,2.33824965236156,
135.13122687685));
#121378=CARTESIAN_POINT('Ctrl Pts',(-185.473265389399,2.45876180684023,
135.066101798692));
#121379=CARTESIAN_POINT('Ctrl Pts',(-185.481016580639,2.5766451232984,134.995887322545));
#121380=CARTESIAN_POINT('Ctrl Pts',(-185.488767771879,2.69144588960641,
134.920827802644));
#121381=CARTESIAN_POINT('Ctrl Pts',(-185.496515668657,2.80619786252648,
134.84580018504));
#121382=CARTESIAN_POINT('Ctrl Pts',(-185.504263565434,2.91786956457255,
134.76593183292));
#121383=CARTESIAN_POINT('Ctrl Pts',(-185.512011462211,3.02603382957723,
134.681511933256));
#121384=CARTESIAN_POINT('Ctrl Pts',(-185.519757738295,3.13417546894943,
134.597109692414));
#121385=CARTESIAN_POINT('Ctrl Pts',(-185.527504014379,3.23881082260025,
134.508158038173));
#121386=CARTESIAN_POINT('Ctrl Pts',(-185.535250290463,3.33954388231524,
134.414987948182));
#121387=CARTESIAN_POINT('Ctrl Pts',(-185.542996623729,3.44027768561866,
134.32181717043));
#121388=CARTESIAN_POINT('Ctrl Pts',(-185.550742956994,3.53710885048758,
134.224428160262));
#121389=CARTESIAN_POINT('Ctrl Pts',(-185.558489290259,3.62967678032664,
134.123190160169));
#121390=CARTESIAN_POINT('Ctrl Pts',(-185.566237358262,3.72226544011165,
134.021929488529));
#121391=CARTESIAN_POINT('Ctrl Pts',(-185.573985426265,3.81058870130834,
133.916818400254));
#121392=CARTESIAN_POINT('Ctrl Pts',(-185.581733494268,3.89432522392317,
133.808260434939));
#121393=CARTESIAN_POINT('Ctrl Pts',(-185.58948979701,3.97815074271105,133.699587092927));
#121394=CARTESIAN_POINT('Ctrl Pts',(-185.597246099752,4.05737954572931,
133.58745986594));
#121395=CARTESIAN_POINT('Ctrl Pts',(-185.605002402494,4.13173243319085,
133.472313046493));
#121396=CARTESIAN_POINT('Ctrl Pts',(-185.612762845008,4.20612500502695,
133.357104769722));
#121397=CARTESIAN_POINT('Ctrl Pts',(-185.620523287522,4.27563627770473,
133.238874026014));
#121398=CARTESIAN_POINT('Ctrl Pts',(-185.628283730036,4.3400327911151,133.118080227749));
#121399=CARTESIAN_POINT('Ctrl Pts',(-185.636056630302,4.40453267952583,
132.997092520555));
#121400=CARTESIAN_POINT('Ctrl Pts',(-185.643829530567,4.46390123172262,
132.873533889436));
#121401=CARTESIAN_POINT('Ctrl Pts',(-185.651602430833,4.51795260194687,
132.74788508334));
#121402=CARTESIAN_POINT('Ctrl Pts',(-185.659092766595,4.57003906871526,
132.626803927838));
#121403=CARTESIAN_POINT('Ctrl Pts',(-185.666583102356,4.61718811749639,
132.50378221287));
#121404=CARTESIAN_POINT('Ctrl Pts',(-185.674073438118,4.65927769153067,
132.37926202899));
#121405=CARTESIAN_POINT('Ctrl Pts',(-185.681847772237,4.70296310455798,
132.250020624489));
#121406=CARTESIAN_POINT('Ctrl Pts',(-185.689622106357,4.74133619155718,
132.118755481185));
#121407=CARTESIAN_POINT('Ctrl Pts',(-185.697396440476,4.77420640142745,
131.985942734505));
#121408=CARTESIAN_POINT('Ctrl Pts',(-185.705161193423,4.80703610170175,
131.853293667665));
#121409=CARTESIAN_POINT('Ctrl Pts',(-185.71292594637,4.83437632559071,131.719101168244));
#121410=CARTESIAN_POINT('Ctrl Pts',(-185.720690699317,4.85608535863617,
131.583859207776));
#121411=CARTESIAN_POINT('Ctrl Pts',(-185.728447740202,4.87777282996403,
131.448751571529));
#121412=CARTESIAN_POINT('Ctrl Pts',(-185.736204781087,4.89384017916371,
131.312596932063));
#121413=CARTESIAN_POINT('Ctrl Pts',(-185.743961821972,4.90419617918031,
131.175901865092));
#121414=CARTESIAN_POINT('Ctrl Pts',(-185.751713013212,4.9145443696567,131.039309880935));
#121415=CARTESIAN_POINT('Ctrl Pts',(-185.759464204452,4.91918975430297,
130.902178668729));
#121416=CARTESIAN_POINT('Ctrl Pts',(-185.767215395692,4.91809267276772,
130.76502202877));
#121417=CARTESIAN_POINT('Ctrl Pts',(-185.774963292469,4.91699605752139,
130.627923684042));
#121418=CARTESIAN_POINT('Ctrl Pts',(-185.782711189246,4.91016183358293,
130.490800323191));
#121419=CARTESIAN_POINT('Ctrl Pts',(-185.790459086024,4.89760240839343,
130.354167645832));
#121420=CARTESIAN_POINT('Ctrl Pts',(-185.798205362108,4.88504561036494,
130.217563549084));
#121421=CARTESIAN_POINT('Ctrl Pts',(-185.805951638192,4.86676602891934,
130.081450320748));
#121422=CARTESIAN_POINT('Ctrl Pts',(-185.813697914276,4.84282807281364,
129.946340035256));
#121423=CARTESIAN_POINT('Ctrl Pts',(-185.821444247541,4.81888994000336,
129.81122875241));
#121424=CARTESIAN_POINT('Ctrl Pts',(-185.829190580807,4.78929341739268,
129.677120812149));
#121425=CARTESIAN_POINT('Ctrl Pts',(-185.836936914072,4.75415424788159,
129.54451917919));
#121426=CARTESIAN_POINT('Ctrl Pts',(-185.844684982075,4.71900720919718,
129.411887851015));
#121427=CARTESIAN_POINT('Ctrl Pts',(-185.852433050078,4.67831515382283,
129.280763879231));
#121428=CARTESIAN_POINT('Ctrl Pts',(-185.860181118081,4.63224389893416,
129.151635739286));
#121429=CARTESIAN_POINT('Ctrl Pts',(-185.867937420823,4.5861236789676,129.022370360416));
#121430=CARTESIAN_POINT('Ctrl Pts',(-185.875693723564,4.5346129705982,128.895105419515));
#121431=CARTESIAN_POINT('Ctrl Pts',(-185.883450026306,4.47792624211395,
128.770310560983));
#121432=CARTESIAN_POINT('Ctrl Pts',(-185.89121046882,4.42120925821574,128.645449095676));
#121433=CARTESIAN_POINT('Ctrl Pts',(-185.898970911335,4.35931092585522,
128.52306068839));
#121434=CARTESIAN_POINT('Ctrl Pts',(-185.906731353849,4.29249157078739,
128.403590079339));
#121435=CARTESIAN_POINT('Ctrl Pts',(-185.914504254114,4.22556495135886,
128.28392768546));
#121436=CARTESIAN_POINT('Ctrl Pts',(-185.922277154379,4.15370172825647,
128.167192782885));
#121437=CARTESIAN_POINT('Ctrl Pts',(-185.930050054645,4.07720591501325,
128.053801585463));
#121438=CARTESIAN_POINT('Ctrl Pts',(-185.937540390407,4.00349091726232,
127.944532443683));
#121439=CARTESIAN_POINT('Ctrl Pts',(-185.945030726169,3.92547447684811,
127.838368371698));
#121440=CARTESIAN_POINT('Ctrl Pts',(-185.952521061931,3.84346256241335,
127.73565102006));
#121441=CARTESIAN_POINT('Ctrl Pts',(-185.96029539605,3.75834114131641,127.629039108815));
#121442=CARTESIAN_POINT('Ctrl Pts',(-185.968069730169,3.66864564947082,
127.525802727655));
#121443=CARTESIAN_POINT('Ctrl Pts',(-185.975844064288,3.57467367557063,
127.426359555446));
#121444=CARTESIAN_POINT('Ctrl Pts',(-185.983608817235,3.48081751372976,
127.32703893806));
#121445=CARTESIAN_POINT('Ctrl Pts',(-185.991373570182,3.38269562227221,
127.231502509616));
#121446=CARTESIAN_POINT('Ctrl Pts',(-185.99913832313,3.28064699331261,127.140136502181));
#121447=CARTESIAN_POINT('Ctrl Pts',(-186.006895364015,3.17869972048965,
127.048861240753));
#121448=CARTESIAN_POINT('Ctrl Pts',(-186.0146524049,3.07283376091616,126.961748416427));
#121449=CARTESIAN_POINT('Ctrl Pts',(-186.022409445785,2.96342600063647,
126.879148597655));
#121450=CARTESIAN_POINT('Ctrl Pts',(-186.030160637025,2.85410074559971,
126.79661106805));
#121451=CARTESIAN_POINT('Ctrl Pts',(-186.037911828265,2.74123931688351,
126.718580004569));
#121452=CARTESIAN_POINT('Ctrl Pts',(-186.045663019505,2.6252525518401,126.6453664962));
#121453=CARTESIAN_POINT('Ctrl Pts',(-186.053410916282,2.50931508426635,
126.572184105526));
#121454=CARTESIAN_POINT('Ctrl Pts',(-186.061158813059,2.39025525227261,
126.503815405716));
#121455=CARTESIAN_POINT('Ctrl Pts',(-186.068906709836,2.26851363507625,
126.440528706278));
#121456=CARTESIAN_POINT('Ctrl Pts',(-186.07665298592,2.14679748360143,126.377255245054));
#121457=CARTESIAN_POINT('Ctrl Pts',(-186.084399262004,2.02240100940056,
126.319061849963));
#121458=CARTESIAN_POINT('Ctrl Pts',(-186.092145538088,1.89578984970093,
126.266171120832));
#121459=CARTESIAN_POINT('Ctrl Pts',(-186.099891871354,1.769177755387,126.213280001273));
#121460=CARTESIAN_POINT('Ctrl Pts',(-186.107638204619,1.64035130370563,
126.165691776484));
#121461=CARTESIAN_POINT('Ctrl Pts',(-186.115384537884,1.50979621498143,
126.123580933397));
#121462=CARTESIAN_POINT('Ctrl Pts',(-186.123132605887,1.37921188934978,
126.081460659879));
#121463=CARTESIAN_POINT('Ctrl Pts',(-186.13088067389,1.24689852837551,126.044820328894));
#121464=CARTESIAN_POINT('Ctrl Pts',(-186.138628741893,1.11335672851959,
126.013784466667));
#121465=CARTESIAN_POINT('Ctrl Pts',(-186.146385044635,0.979672998849801,
125.982715619156));
#121466=CARTESIAN_POINT('Ctrl Pts',(-186.154141347377,0.844758603646081,
125.957263227791));
#121467=CARTESIAN_POINT('Ctrl Pts',(-186.161897650119,0.709124593392249,
125.937500708595));
#121468=CARTESIAN_POINT('Ctrl Pts',(-186.169658092633,0.573418191182914,
125.917727641549));
#121469=CARTESIAN_POINT('Ctrl Pts',(-186.177418535147,0.436991797321192,
125.903650537974));
#121470=CARTESIAN_POINT('Ctrl Pts',(-186.185178977661,0.300360296774949,
125.895290771391));
#121471=CARTESIAN_POINT('Ctrl Pts',(-186.192951877927,0.163509463214826,
125.886917584969));
#121472=CARTESIAN_POINT('Ctrl Pts',(-186.200724778192,0.0264532561306669,
125.884280083587));
#121473=CARTESIAN_POINT('Ctrl Pts',(-186.208497678457,-0.110293825237829,
125.887347465803));
#121474=CARTESIAN_POINT('Ctrl Pts',(-186.215988014219,-0.242069805751984,
125.890303340948));
#121475=CARTESIAN_POINT('Ctrl Pts',(-186.223478349981,-0.37355843793483,
125.898556507699));
#121476=CARTESIAN_POINT('Ctrl Pts',(-186.230968685743,-0.504306897976589,
125.91203421644));
#121477=CARTESIAN_POINT('Ctrl Pts',(-186.238743019862,-0.640012725620837,
125.926022936604));
#121478=CARTESIAN_POINT('Ctrl Pts',(-186.246517353981,-0.775351021172049,
125.945684508496));
#121479=CARTESIAN_POINT('Ctrl Pts',(-186.2542916881,-0.909809525613153,
125.970994327949));
#121480=CARTESIAN_POINT('Ctrl Pts',(-186.262056441047,-1.0441023219648,
125.996272955312));
#121481=CARTESIAN_POINT('Ctrl Pts',(-186.269821193994,-1.17751710403923,
126.02718590837));
#121482=CARTESIAN_POINT('Ctrl Pts',(-186.277585946941,-1.3095456903417,
126.063656751323));
#121483=CARTESIAN_POINT('Ctrl Pts',(-186.285342987826,-1.44144314399063,
126.100091370921));
#121484=CARTESIAN_POINT('Ctrl Pts',(-186.293100028711,-1.57195676732722,
126.142072791592));
#121485=CARTESIAN_POINT('Ctrl Pts',(-186.300857069596,-1.7005879010708,
126.189473419245));
#121486=CARTESIAN_POINT('Ctrl Pts',(-186.308608260836,-1.8291220330753,
126.236838301715));
#121487=CARTESIAN_POINT('Ctrl Pts',(-186.316359452076,-1.95577613574888,
126.289614122268));
#121488=CARTESIAN_POINT('Ctrl Pts',(-186.324110643316,-2.08006641349185,
126.347623383));
#121489=CARTESIAN_POINT('Ctrl Pts',(-186.331858540093,-2.20430386455207,
126.40560798825));
#121490=CARTESIAN_POINT('Ctrl Pts',(-186.33960643687,-2.32617913539421,
126.46882144461));
#121491=CARTESIAN_POINT('Ctrl Pts',(-186.347354333647,-2.4452283458019,
126.537038108148));
#121492=CARTESIAN_POINT('Ctrl Pts',(-186.355100609731,-2.56425265368117,
126.605240502231));
#121493=CARTESIAN_POINT('Ctrl Pts',(-186.362846885815,-2.68045173795131,
126.678443827566));
#121494=CARTESIAN_POINT('Ctrl Pts',(-186.370593161899,-2.79338663077894,
126.756376651011));
#121495=CARTESIAN_POINT('Ctrl Pts',(-186.378339495165,-2.90632235726645,
126.834310049738));
#121496=CARTESIAN_POINT('Ctrl Pts',(-186.38608582843,-3.01599352244523,
126.916972794186));
#121497=CARTESIAN_POINT('Ctrl Pts',(-186.393832161695,-3.12199078181559,
127.004050548538));
#121498=CARTESIAN_POINT('Ctrl Pts',(-186.401580229698,-3.2280117785374,
127.091147803349));
#121499=CARTESIAN_POINT('Ctrl Pts',(-186.409328297701,-3.33035693024278,
127.182661787357));
#121500=CARTESIAN_POINT('Ctrl Pts',(-186.417076365704,-3.42865088487751,
127.278238644048));
#121501=CARTESIAN_POINT('Ctrl Pts',(-186.424832668446,-3.52704930749682,
127.373917080959));
#121502=CARTESIAN_POINT('Ctrl Pts',(-186.432588971188,-3.62138765127686,
127.473666743374));
#121503=CARTESIAN_POINT('Ctrl Pts',(-186.440345273929,-3.71132791396644,
127.577097353202));
#121504=CARTESIAN_POINT('Ctrl Pts',(-186.448105716444,-3.8013161804825,
127.680583167061));
#121505=CARTESIAN_POINT('Ctrl Pts',(-186.455866158958,-3.8869014446861,
127.787753537677));
#121506=CARTESIAN_POINT('Ctrl Pts',(-186.463626601472,-3.96778741652845,
127.898186830653));
#121507=CARTESIAN_POINT('Ctrl Pts',(-186.471399501737,-4.04880323371331,
128.008797400955));
#121508=CARTESIAN_POINT('Ctrl Pts',(-186.479172402003,-4.12510446603694,
128.122681035685));
#121509=CARTESIAN_POINT('Ctrl Pts',(-186.486945302268,-4.19643892821958,
128.239388223129));
#121510=CARTESIAN_POINT('Ctrl Pts',(-186.494435638031,-4.26518020302876,
128.351852810354));
#121511=CARTESIAN_POINT('Ctrl Pts',(-186.501925973793,-4.32930939758988,
128.466938958798));
#121512=CARTESIAN_POINT('Ctrl Pts',(-186.509416309556,-4.38864295588559,
128.584226372018));
#121513=CARTESIAN_POINT('Ctrl Pts',(-186.517717331537,-4.45439824205773,
128.714207914373));
#121514=CARTESIAN_POINT('Ctrl Pts',(-186.526018353518,-4.51445011624346,
128.847261066043));
#121515=CARTESIAN_POINT('Ctrl Pts',(-186.534319375498,-4.56852078633726,
128.982877461645));
#121516=CARTESIAN_POINT('Ctrl Pts',(-186.542600349557,-4.62246086954897,
129.118166328066));
#121517=CARTESIAN_POINT('Ctrl Pts',(-186.550881323616,-4.670448438029,129.256005807444));
#121518=CARTESIAN_POINT('Ctrl Pts',(-186.559162297674,-4.71225244919594,
129.39586499544));
#121519=CARTESIAN_POINT('Ctrl Pts',(-186.562823196869,-4.73073339959214,
129.45769472526));
#121520=CARTESIAN_POINT('Ctrl Pts',(-186.566484096064,-4.74800643982495,
129.519918866165));
#121521=CARTESIAN_POINT('Ctrl Pts',(-186.570144995258,-4.76405452823391,
129.582490119308));
#121522=CARTESIAN_POINT('Origin',(213.235140564004,0.,130.804360617566));
#121523=CARTESIAN_POINT('',(-188.665047832579,-4.76405452823406,129.582490119308));
#121524=CARTESIAN_POINT('',(-188.319844903182,-4.76405452823404,129.582490119308));
#121525=CARTESIAN_POINT('',(213.235140564004,-4.76405452823405,129.582490119308));
#121526=CARTESIAN_POINT('',(-186.985140563973,-4.91824792938353,130.808873666935));
#121527=CARTESIAN_POINT('Ctrl Pts',(-186.985140564012,-4.9182479293829,
130.808873667626));
#121528=CARTESIAN_POINT('Ctrl Pts',(-186.995772027482,-4.91807578782115,
130.996470718023));
#121529=CARTESIAN_POINT('Ctrl Pts',(-187.006403490951,-4.90716688700063,
131.183595083917));
#121530=CARTESIAN_POINT('Ctrl Pts',(-187.017034954421,-4.88570371797789,
131.369234269489));
#121531=CARTESIAN_POINT('Ctrl Pts',(-187.026930823288,-4.86572559297847,
131.542029016165));
#121532=CARTESIAN_POINT('Ctrl Pts',(-187.036826692156,-4.83660372490796,
131.71353778882));
#121533=CARTESIAN_POINT('Ctrl Pts',(-187.046722561023,-4.79852032900577,
131.882964212321));
#121534=CARTESIAN_POINT('Ctrl Pts',(-187.054496895142,-4.76860147618899,
132.016067999625));
#121535=CARTESIAN_POINT('Ctrl Pts',(-187.062271229261,-4.73309288657269,
132.148136813944));
#121536=CARTESIAN_POINT('Ctrl Pts',(-187.07004556338,-4.69207949437852,
132.278664887699));
#121537=CARTESIAN_POINT('Ctrl Pts',(-187.077810316327,-4.65111664752476,
132.409032097269));
#121538=CARTESIAN_POINT('Ctrl Pts',(-187.085575069274,-4.60466261265512,
132.537861974965));
#121539=CARTESIAN_POINT('Ctrl Pts',(-187.093339822221,-4.55285331124662,
132.66465892396));
#121540=CARTESIAN_POINT('Ctrl Pts',(-187.101096863106,-4.50109546756681,
132.791329936437));
#121541=CARTESIAN_POINT('Ctrl Pts',(-187.108853903991,-4.44399308917469,
132.915971678803));
#121542=CARTESIAN_POINT('Ctrl Pts',(-187.116610944876,-4.38173177310754,
133.038104052036));
#121543=CARTESIAN_POINT('Ctrl Pts',(-187.124362136116,-4.31951740878307,
133.160144324298));
#121544=CARTESIAN_POINT('Ctrl Pts',(-187.132113327356,-4.25215202722686,
133.279678647097));
#121545=CARTESIAN_POINT('Ctrl Pts',(-187.139864518596,-4.17986902446443,
133.396247575136));
#121546=CARTESIAN_POINT('Ctrl Pts',(-187.147612415373,-4.1076167439063,
133.512766958271));
#121547=CARTESIAN_POINT('Ctrl Pts',(-187.15536031215,-4.03045120483651,
133.626323121855));
#121548=CARTESIAN_POINT('Ctrl Pts',(-187.163108208927,-3.9486512601369,
133.736482083044));
#121549=CARTESIAN_POINT('Ctrl Pts',(-187.170854485011,-3.86686842622231,
133.846618001354));
#121550=CARTESIAN_POINT('Ctrl Pts',(-187.178600761095,-3.78045334783767,
133.953357817043));
#121551=CARTESIAN_POINT('Ctrl Pts',(-187.186347037179,-3.68972740421345,
134.056297693387));
#121552=CARTESIAN_POINT('Ctrl Pts',(-187.194093370445,-3.59900079087104,
134.159238329609));
#121553=CARTESIAN_POINT('Ctrl Pts',(-187.20183970371,-3.50396350729632,
134.258378677208));
#121554=CARTESIAN_POINT('Ctrl Pts',(-187.209586036975,-3.40497603632671,
134.353349382629));
#121555=CARTESIAN_POINT('Ctrl Pts',(-187.217334104978,-3.30596639779917,
134.44834135608));
#121556=CARTESIAN_POINT('Ctrl Pts',(-187.225082172981,-3.20300509365603,
134.539161558656));
#121557=CARTESIAN_POINT('Ctrl Pts',(-187.232830240984,-3.09648783601041,
134.625479059062));
#121558=CARTESIAN_POINT('Ctrl Pts',(-187.240586543725,-2.98985737055593,
134.711888298734));
#121559=CARTESIAN_POINT('Ctrl Pts',(-187.248342846467,-2.8796637062563,
134.793785030094));
#121560=CARTESIAN_POINT('Ctrl Pts',(-187.256099149209,-2.76633431053606,
134.870879711933));
#121561=CARTESIAN_POINT('Ctrl Pts',(-187.263859591723,-2.65294442750473,
134.948015541525));
#121562=CARTESIAN_POINT('Ctrl Pts',(-187.271620034237,-2.53641581021152,
135.020344008526));
#121563=CARTESIAN_POINT('Ctrl Pts',(-187.279380476751,-2.41720213633815,
135.087620695425));
#121564=CARTESIAN_POINT('Ctrl Pts',(-187.287153377017,-2.2977970900922,
135.155005380835));
#121565=CARTESIAN_POINT('Ctrl Pts',(-187.294926277282,-2.1756987223634,
135.217321902815));
#121566=CARTESIAN_POINT('Ctrl Pts',(-187.302699177547,-2.05138318386969,
135.274372932475));
#121567=CARTESIAN_POINT('Ctrl Pts',(-187.31018951331,-1.93158682832274,
135.329350013508));
#121568=CARTESIAN_POINT('Ctrl Pts',(-187.317679849073,-1.80973198772532,
135.379437666485));
#121569=CARTESIAN_POINT('Ctrl Pts',(-187.325170184835,-1.68625769629345,
135.424503260839));
#121570=CARTESIAN_POINT('Ctrl Pts',(-187.332944518954,-1.5581018395823,
135.471277530897));
#121571=CARTESIAN_POINT('Ctrl Pts',(-187.340718853073,-1.42779534567859,
135.512789568897));
#121572=CARTESIAN_POINT('Ctrl Pts',(-187.348493187192,-1.29580964019177,
135.548837452675));
#121573=CARTESIAN_POINT('Ctrl Pts',(-187.356257940139,-1.16398659529106,
135.584840910658));
#121574=CARTESIAN_POINT('Ctrl Pts',(-187.364022693087,-1.03048882998293,
135.615393511214));
#121575=CARTESIAN_POINT('Ctrl Pts',(-187.371787446034,-0.895806772792648,
135.640341726743));
#121576=CARTESIAN_POINT('Ctrl Pts',(-187.379544486919,-0.761258483720252,
135.665265163353));
#121577=CARTESIAN_POINT('Ctrl Pts',(-187.387301527804,-0.625528625504841,
135.68459522148));
#121578=CARTESIAN_POINT('Ctrl Pts',(-187.395058568689,-0.48912143878214,
135.698228543923));
#121579=CARTESIAN_POINT('Ctrl Pts',(-187.402809759929,-0.352817117779854,
135.711851585371));
#121580=CARTESIAN_POINT('Ctrl Pts',(-187.410560951169,-0.215836872397206,
135.719786403242));
#121581=CARTESIAN_POINT('Ctrl Pts',(-187.418312142409,-0.0786934032297544,
135.721981018816));
#121582=CARTESIAN_POINT('Ctrl Pts',(-187.426060039186,0.0583917763046921,
135.72417470162));
#121583=CARTESIAN_POINT('Ctrl Pts',(-187.433807935963,0.195639651546684,
135.720633028339));
#121584=CARTESIAN_POINT('Ctrl Pts',(-187.44155583274,0.33253437364453,135.711356027473));
#121585=CARTESIAN_POINT('Ctrl Pts',(-187.449302108824,0.469400460317623,
135.702080967155));
#121586=CARTESIAN_POINT('Ctrl Pts',(-187.457048384909,0.605913150958659,
135.687072991952));
#121587=CARTESIAN_POINT('Ctrl Pts',(-187.464794660993,0.741558972969566,
135.666384203698));
#121588=CARTESIAN_POINT('Ctrl Pts',(-187.472540994258,0.877205796287302,
135.645695262725));
#121589=CARTESIAN_POINT('Ctrl Pts',(-187.480287327523,1.01198535171049,
135.619325483972));
#121590=CARTESIAN_POINT('Ctrl Pts',(-187.488033660789,1.14539204185446,
135.587378507242));
#121591=CARTESIAN_POINT('Ctrl Pts',(-187.495781728792,1.27882860750151,
135.555424376208));
#121592=CARTESIAN_POINT('Ctrl Pts',(-187.503529796795,1.41089131594959,
135.517890652914));
#121593=CARTESIAN_POINT('Ctrl Pts',(-187.511277864798,1.54108785326631,
135.474931384722));
#121594=CARTESIAN_POINT('Ctrl Pts',(-187.51903416754,1.67142276501208,135.431926458909));
#121595=CARTESIAN_POINT('Ctrl Pts',(-187.526790470281,1.79988717172503,
135.383484592025));
#121596=CARTESIAN_POINT('Ctrl Pts',(-187.534546773023,1.92600641760273,
135.329808920425));
#121597=CARTESIAN_POINT('Ctrl Pts',(-187.542307215538,2.05219297711968,
135.276104600504));
#121598=CARTESIAN_POINT('Ctrl Pts',(-187.550067658052,2.17603152887269,
135.217161077647));
#121599=CARTESIAN_POINT('Ctrl Pts',(-187.557828100566,2.29707121362073,
135.153227930103));
#121600=CARTESIAN_POINT('Ctrl Pts',(-187.565601000831,2.41830520201613,
135.089192151395));
#121601=CARTESIAN_POINT('Ctrl Pts',(-187.573373901097,2.53673100702913,
135.020150938914));
#121602=CARTESIAN_POINT('Ctrl Pts',(-187.581146801362,2.65192523918329,
134.94639823066));
#121603=CARTESIAN_POINT('Ctrl Pts',(-187.588637137124,2.7629318708422,134.875326619122));
#121604=CARTESIAN_POINT('Ctrl Pts',(-187.596127472886,2.87093754965219,
134.799880290516));
#121605=CARTESIAN_POINT('Ctrl Pts',(-187.603617808648,2.9755933810453,134.720356926704));
#121606=CARTESIAN_POINT('Ctrl Pts',(-187.611392142768,3.08421727009468,
134.637818410382));
#121607=CARTESIAN_POINT('Ctrl Pts',(-187.619166476887,3.18957636621408,
134.550626137116));
#121608=CARTESIAN_POINT('Ctrl Pts',(-187.626940811006,3.29124596951094,
134.45906758676));
#121609=CARTESIAN_POINT('Ctrl Pts',(-187.634705563953,3.3927902741082,134.367621874136));
#121610=CARTESIAN_POINT('Ctrl Pts',(-187.6424703169,3.49065384526458,134.271820850219));
#121611=CARTESIAN_POINT('Ctrl Pts',(-187.650235069847,3.58444242726253,
134.171994140998));
#121612=CARTESIAN_POINT('Ctrl Pts',(-187.657992110732,3.67813785711891,
134.072266581071));
#121613=CARTESIAN_POINT('Ctrl Pts',(-187.665749151617,3.76776608622933,
133.968521575866));
#121614=CARTESIAN_POINT('Ctrl Pts',(-187.673506192502,3.85296760287033,
133.861127490216));
#121615=CARTESIAN_POINT('Ctrl Pts',(-187.681257383742,3.93810486838475,
133.753814391282));
#121616=CARTESIAN_POINT('Ctrl Pts',(-187.689008574982,4.01882182394327,
133.642857994237));
#121617=CARTESIAN_POINT('Ctrl Pts',(-187.696759766223,4.0947976111808,133.528661552846));
#121618=CARTESIAN_POINT('Ctrl Pts',(-187.704507663,4.17074110668214,133.414513647989));
#121619=CARTESIAN_POINT('Ctrl Pts',(-187.712255559777,4.24194722567974,
133.297128762567));
#121620=CARTESIAN_POINT('Ctrl Pts',(-187.720003456554,4.30813716324615,
133.176940910234));
#121621=CARTESIAN_POINT('Ctrl Pts',(-187.727749732638,4.37431325530452,
133.056778198609));
#121622=CARTESIAN_POINT('Ctrl Pts',(-187.735496008722,4.43547506451776,
132.933814028545));
#121623=CARTESIAN_POINT('Ctrl Pts',(-187.743242284806,4.4913888811533,132.808508561395));
#121624=CARTESIAN_POINT('Ctrl Pts',(-187.750988618071,4.54730311053187,
132.683202169268));
#121625=CARTESIAN_POINT('Ctrl Pts',(-187.758734951337,4.59796911071568,
132.555554802601));
#121626=CARTESIAN_POINT('Ctrl Pts',(-187.766481284602,4.64320078906951,
132.426047854639));
#121627=CARTESIAN_POINT('Ctrl Pts',(-187.774229352605,4.68844259674417,
132.296511904493));
#121628=CARTESIAN_POINT('Ctrl Pts',(-187.781977420608,4.72824753205442,
132.165115913412));
#121629=CARTESIAN_POINT('Ctrl Pts',(-187.789725488611,4.76247909170162,
132.032357345414));
#121630=CARTESIAN_POINT('Ctrl Pts',(-187.797481791353,4.79674703305773,
131.899457680029));
#121631=CARTESIAN_POINT('Ctrl Pts',(-187.805238094095,4.82542966824893,
131.765192924051));
#121632=CARTESIAN_POINT('Ctrl Pts',(-187.812994396837,4.8484413385891,131.630072219011));
#121633=CARTESIAN_POINT('Ctrl Pts',(-187.820754839351,4.87146529095061,
131.494879395982));
#121634=CARTESIAN_POINT('Ctrl Pts',(-187.828515281865,4.88881219795085,
131.358830101222));
#121635=CARTESIAN_POINT('Ctrl Pts',(-187.836275724379,4.90044833640633,
131.22243855852));
#121636=CARTESIAN_POINT('Ctrl Pts',(-187.844048624645,4.91210315422426,
131.085828068006));
#121637=CARTESIAN_POINT('Ctrl Pts',(-187.85182152491,4.9180288671356,130.948874622484));
#121638=CARTESIAN_POINT('Ctrl Pts',(-187.859594425176,4.91824392115051,
130.812093312181));
#121639=CARTESIAN_POINT('Ctrl Pts',(-187.867084760937,4.9184511574103,130.68028434704));
#121640=CARTESIAN_POINT('Ctrl Pts',(-187.874575096699,4.91335573198571,
130.548635527089));
#121641=CARTESIAN_POINT('Ctrl Pts',(-187.882065432461,4.90301950702024,
130.417601291526));
#121642=CARTESIAN_POINT('Ctrl Pts',(-187.88983976658,4.89229138094348,130.281598853093));
#121643=CARTESIAN_POINT('Ctrl Pts',(-187.897614100699,4.87588321702286,
130.145827708113));
#121644=CARTESIAN_POINT('Ctrl Pts',(-187.905388434818,4.85380731953623,
130.010800558518));
#121645=CARTESIAN_POINT('Ctrl Pts',(-187.913153187766,4.83175862862026,
129.875939817817));
#121646=CARTESIAN_POINT('Ctrl Pts',(-187.920917940713,4.80405616463346,
129.741821630265));
#121647=CARTESIAN_POINT('Ctrl Pts',(-187.92868269366,4.77076414640998,129.608955865263));
#121648=CARTESIAN_POINT('Ctrl Pts',(-187.936439734545,4.73750519428833,
129.476222064411));
#121649=CARTESIAN_POINT('Ctrl Pts',(-187.94419677543,4.69866783032351,129.344738587432));
#121650=CARTESIAN_POINT('Ctrl Pts',(-187.951953816315,4.65436764541508,
129.21500701191));
#121651=CARTESIAN_POINT('Ctrl Pts',(-187.959705007555,4.61010086762063,
129.085373267977));
#121652=CARTESIAN_POINT('Ctrl Pts',(-187.967456198795,4.56037959443934,
128.95748916438));
#121653=CARTESIAN_POINT('Ctrl Pts',(-187.975207390035,4.50536966289933,
128.831842616856));
#121654=CARTESIAN_POINT('Ctrl Pts',(-187.982955286812,4.45038311204773,
128.706249472466));
#121655=CARTESIAN_POINT('Ctrl Pts',(-187.990703183589,4.39011253005438,
128.582892350036));
#121656=CARTESIAN_POINT('Ctrl Pts',(-187.998451080366,4.32477236402399,
128.462240411028));
#121657=CARTESIAN_POINT('Ctrl Pts',(-188.006197356451,4.25944586574759,
128.341613709804));
#121658=CARTESIAN_POINT('Ctrl Pts',(-188.013943632535,4.18905207878634,
128.223691410034));
#121659=CARTESIAN_POINT('Ctrl Pts',(-188.021689908619,4.11385182410005,
128.108918866786));
#121660=CARTESIAN_POINT('Ctrl Pts',(-188.029436241884,4.03865101430267,
127.994145476313));
#121661=CARTESIAN_POINT('Ctrl Pts',(-188.03718257515,3.95864388025005,127.882522215779));
#121662=CARTESIAN_POINT('Ctrl Pts',(-188.044928908415,3.87413484409709,
127.774465854995));
#121663=CARTESIAN_POINT('Ctrl Pts',(-188.052676976418,3.78960688273153,
127.666385295739));
#121664=CARTESIAN_POINT('Ctrl Pts',(-188.060425044421,3.70057525393309,
127.561873533624));
#121665=CARTESIAN_POINT('Ctrl Pts',(-188.068173112424,3.60738470489975,
127.461314304193));
#121666=CARTESIAN_POINT('Ctrl Pts',(-188.075929415166,3.51409511184179,
127.360648199217));
#121667=CARTESIAN_POINT('Ctrl Pts',(-188.083685717908,3.416638034995,127.26394330569));
#121668=CARTESIAN_POINT('Ctrl Pts',(-188.091442020649,3.31539552893747,
127.171546894128));
#121669=CARTESIAN_POINT('Ctrl Pts',(-188.099202463164,3.21409898670611,
127.079101167818));
#121670=CARTESIAN_POINT('Ctrl Pts',(-188.106962905678,3.10901328886408,
126.990968756662));
#121671=CARTESIAN_POINT('Ctrl Pts',(-188.114723348192,3.00055283824357,
126.907455983448));
#121672=CARTESIAN_POINT('Ctrl Pts',(-188.122496248457,2.89191827727905,
126.823809148117));
#121673=CARTESIAN_POINT('Ctrl Pts',(-188.130269148723,2.77989845741056,
126.744796995441));
#121674=CARTESIAN_POINT('Ctrl Pts',(-188.138042048988,2.66493670915268,
126.670682425119));
#121675=CARTESIAN_POINT('Ctrl Pts',(-188.14553238475,2.55415411001514,126.599262106112));
#121676=CARTESIAN_POINT('Ctrl Pts',(-188.153022720512,2.44064002739613,
126.532389628946));
#121677=CARTESIAN_POINT('Ctrl Pts',(-188.160513056274,2.32481023186287,
126.470258582735));
#121678=CARTESIAN_POINT('Ctrl Pts',(-188.168287390393,2.2045887144261,126.405771819022));
#121679=CARTESIAN_POINT('Ctrl Pts',(-188.176061724512,2.0814915915248,126.346188851776));
#121680=CARTESIAN_POINT('Ctrl Pts',(-188.183836058631,1.95595686457699,
126.291776456975));
#121681=CARTESIAN_POINT('Ctrl Pts',(-188.191600811579,1.83057684796112,
126.237431120589));
#121682=CARTESIAN_POINT('Ctrl Pts',(-188.199365564526,1.70276555989438,
126.188243831725));
#121683=CARTESIAN_POINT('Ctrl Pts',(-188.207130317473,1.5729866797913,126.144436158125));
#121684=CARTESIAN_POINT('Ctrl Pts',(-188.214887358358,1.4433366979015,126.100671994924));
#121685=CARTESIAN_POINT('Ctrl Pts',(-188.222644399243,1.3117233810346,126.062276938189));
#121686=CARTESIAN_POINT('Ctrl Pts',(-188.230401440128,1.17863120032339,
126.029424852959));
#121687=CARTESIAN_POINT('Ctrl Pts',(-188.238152631368,1.04563938546079,
125.996597541742));
#121688=CARTESIAN_POINT('Ctrl Pts',(-188.245903822608,0.911171304574001,
125.969304975312));
#121689=CARTESIAN_POINT('Ctrl Pts',(-188.253655013848,0.775727093957084,
125.947671360654));
#121690=CARTESIAN_POINT('Ctrl Pts',(-188.261402910625,0.640340450742956,
125.92604694086));
#121691=CARTESIAN_POINT('Ctrl Pts',(-188.269150807402,0.503978888229026,
125.910076750604));
#121692=CARTESIAN_POINT('Ctrl Pts',(-188.276898704179,0.36715303913928,
125.899833962694));
#121693=CARTESIAN_POINT('Ctrl Pts',(-188.284644980264,0.230355811067541,
125.889593317354));
#121694=CARTESIAN_POINT('Ctrl Pts',(-188.292391256348,0.0930948792217825,
125.885077720542));
#121695=CARTESIAN_POINT('Ctrl Pts',(-188.300137532432,-0.0441140864660505,
125.886308461491));
#121696=CARTESIAN_POINT('Ctrl Pts',(-188.307883865697,-0.181324064999486,
125.887539211525));
#121697=CARTESIAN_POINT('Ctrl Pts',(-188.315630198963,-0.318481685660068,
125.894516380455));
#121698=CARTESIAN_POINT('Ctrl Pts',(-188.323376532228,-0.455071760591299,
125.907209123563));
#121699=CARTESIAN_POINT('Ctrl Pts',(-188.331124600231,-0.591692423922576,
125.919904709124));
#121700=CARTESIAN_POINT('Ctrl Pts',(-188.338872668234,-0.727744899400813,
125.938318379674));
#121701=CARTESIAN_POINT('Ctrl Pts',(-188.346620736237,-0.862719995164512,
125.962367508066));
#121702=CARTESIAN_POINT('Ctrl Pts',(-188.354377038979,-0.997838544066398,
125.986442196158));
#121703=CARTESIAN_POINT('Ctrl Pts',(-188.362133341721,-1.13187704037199,
126.016164237938));
#121704=CARTESIAN_POINT('Ctrl Pts',(-188.369889644462,-1.26433680573185,
126.051399908264));
#121705=CARTESIAN_POINT('Ctrl Pts',(-188.377650086977,-1.39686726885678,
126.086654384927));
#121706=CARTESIAN_POINT('Ctrl Pts',(-188.385410529491,-1.52781694894612,
126.12742823772));
#121707=CARTESIAN_POINT('Ctrl Pts',(-188.393170972005,-1.65670413311006,
126.173538392751));
#121708=CARTESIAN_POINT('Ctrl Pts',(-188.40094387227,-1.78579821842409,
126.219722567897));
#121709=CARTESIAN_POINT('Ctrl Pts',(-188.408716772536,-1.91282282908581,
126.271260016418));
#121710=CARTESIAN_POINT('Ctrl Pts',(-188.416489672801,-2.03731714916122,
126.327919855506));
#121711=CARTESIAN_POINT('Ctrl Pts',(-188.423980008563,-2.15728578711929,
126.382519966725));
#121712=CARTESIAN_POINT('Ctrl Pts',(-188.431470344325,-2.27490463047672,
126.441876371959));
#121713=CARTESIAN_POINT('Ctrl Pts',(-188.438960680087,-2.38978607308234,
126.505743911299));
#121714=CARTESIAN_POINT('Ctrl Pts',(-188.446736064809,-2.50903939390405,
126.572041965939));
#121715=CARTESIAN_POINT('Ctrl Pts',(-188.454511449531,-2.62572065138844,
126.643411342122));
#121716=CARTESIAN_POINT('Ctrl Pts',(-188.462286834253,-2.73936846326012,
126.719627641594));
#121717=CARTESIAN_POINT('Ctrl Pts',(-188.470052407546,-2.85287286776605,
126.795747766942));
#121718=CARTESIAN_POINT('Ctrl Pts',(-188.477817980839,-2.96335112181759,
126.876702429187));
#121719=CARTESIAN_POINT('Ctrl Pts',(-188.485583554132,-3.07036605036914,
126.96222119021));
#121720=CARTESIAN_POINT('Ctrl Pts',(-188.493339764738,-3.177251954663,127.047636844174));
#121721=CARTESIAN_POINT('Ctrl Pts',(-188.501095975344,-3.28068254643464,
127.137605394597));
#121722=CARTESIAN_POINT('Ctrl Pts',(-188.508852185949,-3.38024981628517,
127.23181331319));
#121723=CARTESIAN_POINT('Ctrl Pts',(-188.516603088238,-3.47974894273336,
127.325956756297));
#121724=CARTESIAN_POINT('Ctrl Pts',(-188.524353990527,-3.57538972474253,
127.424333527832));
#121725=CARTESIAN_POINT('Ctrl Pts',(-188.532104892816,-3.66679737349336,
127.526590020919));
#121726=CARTESIAN_POINT('Ctrl Pts',(-188.539852169042,-3.75816225948245,
127.628798675886));
#121727=CARTESIAN_POINT('Ctrl Pts',(-188.547599445267,-3.84529769319432,
127.734883149714));
#121728=CARTESIAN_POINT('Ctrl Pts',(-188.555346721492,-3.92786618611514,
127.844453476037));
#121729=CARTESIAN_POINT('Ctrl Pts',(-188.563092051104,-4.01041393253067,
127.953996271261));
#121730=CARTESIAN_POINT('Ctrl Pts',(-188.570837380716,-4.08839678790403,
128.067022863189));
#121731=CARTESIAN_POINT('Ctrl Pts',(-188.578582710328,-4.1615182156311,
128.183111067548));
#121732=CARTESIAN_POINT('Ctrl Pts',(-188.586330187877,-4.23465992141677,
128.299231465526));
#121733=CARTESIAN_POINT('Ctrl Pts',(-188.594077665427,-4.302937292578,128.41841484449));
#121734=CARTESIAN_POINT('Ctrl Pts',(-188.601825142976,-4.36609769469263,
128.540210891311));
#121735=CARTESIAN_POINT('Ctrl Pts',(-188.609573616128,-4.42926621333887,
128.662022589734));
#121736=CARTESIAN_POINT('Ctrl Pts',(-188.617322089279,-4.48731628029937,
128.78644727399));
#121737=CARTESIAN_POINT('Ctrl Pts',(-188.625070562431,-4.54004215253343,
128.913011808985));
#121738=CARTESIAN_POINT('Ctrl Pts',(-188.632825393423,-4.59281128782829,
129.03968019374));
#121739=CARTESIAN_POINT('Ctrl Pts',(-188.640580224415,-4.64024735853174,
129.168491572479));
#121740=CARTESIAN_POINT('Ctrl Pts',(-188.648335055407,-4.68219341291706,
129.298954391149));
#121741=CARTESIAN_POINT('Ctrl Pts',(-188.653905981131,-4.7123266748338,
129.392676443031));
#121742=CARTESIAN_POINT('Ctrl Pts',(-188.659476906855,-4.73962772385923,
129.487250379779));
#121743=CARTESIAN_POINT('Ctrl Pts',(-188.665047832579,-4.76405452823406,
129.582490119308));
#121744=CARTESIAN_POINT('Ctrl Pts',(-186.915092859931,-4.76405452823404,
129.582490119308));
#121745=CARTESIAN_POINT('Ctrl Pts',(-186.922737472684,-4.79771251131355,
129.713722084504));
#121746=CARTESIAN_POINT('Ctrl Pts',(-186.930382085436,-4.82593597496495,
129.846315094707));
#121747=CARTESIAN_POINT('Ctrl Pts',(-186.938026698189,-4.84863265225042,
129.979773165545));
#121748=CARTESIAN_POINT('Ctrl Pts',(-186.945879009153,-4.87194598068921,
130.116857188863));
#121749=CARTESIAN_POINT('Ctrl Pts',(-186.953731320117,-4.88942783458341,
130.2548535049));
#121750=CARTESIAN_POINT('Ctrl Pts',(-186.961583631081,-4.90103510324496,
130.393218331659));
#121751=CARTESIAN_POINT('Ctrl Pts',(-186.969435942045,-4.91264237190651,
130.531583158419));
#121752=CARTESIAN_POINT('Ctrl Pts',(-186.977288253009,-4.91837507169744,
130.670316037513));
#121753=CARTESIAN_POINT('Ctrl Pts',(-186.985140563973,-4.91824792938353,
130.808873666936));
#121754=CARTESIAN_POINT('',(-186.639859435958,-4.91824992550734,130.803504611091));
#121755=CARTESIAN_POINT('Ctrl Pts',(-186.570144995258,-4.76405452823391,
129.582490119308));
#121756=CARTESIAN_POINT('Ctrl Pts',(-186.57840025716,-4.80024267923322,
129.723587170822));
#121757=CARTESIAN_POINT('Ctrl Pts',(-186.586655519063,-4.83019874442568,
129.866450467451));
#121758=CARTESIAN_POINT('Ctrl Pts',(-186.594910780965,-4.8537620318651,
130.010523606257));
#121759=CARTESIAN_POINT('Ctrl Pts',(-186.603145195941,-4.87726581518243,
130.154232918679));
#121760=CARTESIAN_POINT('Ctrl Pts',(-186.611379610917,-4.89440896454415,
130.299145675755));
#121761=CARTESIAN_POINT('Ctrl Pts',(-186.619614025893,-4.90508133671532,
130.444693906975));
#121762=CARTESIAN_POINT('Ctrl Pts',(-186.626362495915,-4.9138278213004,
130.563977168498));
#121763=CARTESIAN_POINT('Ctrl Pts',(-186.633110965936,-4.91822907159551,
130.683686883876));
#121764=CARTESIAN_POINT('Ctrl Pts',(-186.639859435957,-4.91824992550734,
130.803504611091));
#121765=CARTESIAN_POINT('Ctrl Pts',(-186.639859435995,-4.91824992550745,
130.803504611754));
#121766=CARTESIAN_POINT('Ctrl Pts',(-186.647875869329,-4.91827469762084,
130.945834772432));
#121767=CARTESIAN_POINT('Ctrl Pts',(-186.655892302664,-4.91211675181942,
131.08808080582));
#121768=CARTESIAN_POINT('Ctrl Pts',(-186.663908735998,-4.89982403781472,
131.229692794756));
#121769=CARTESIAN_POINT('Ctrl Pts',(-186.671932409808,-4.88752022097909,
131.371432688235));
#121770=CARTESIAN_POINT('Ctrl Pts',(-186.679956083619,-4.86907061660121,
131.512537046391));
#121771=CARTESIAN_POINT('Ctrl Pts',(-186.68797975743,-4.84457475465937,
131.652463505792));
#121772=CARTESIAN_POINT('Ctrl Pts',(-186.696303438758,-4.81916298525302,
131.797621856561));
#121773=CARTESIAN_POINT('Ctrl Pts',(-186.704627120086,-4.78724414801483,
131.941512102986));
#121774=CARTESIAN_POINT('Ctrl Pts',(-186.712950801415,-4.74898628261018,
132.083544869377));
#121775=CARTESIAN_POINT('Ctrl Pts',(-186.720998349268,-4.71199760050266,
132.220865778145));
#121776=CARTESIAN_POINT('Ctrl Pts',(-186.729045897121,-4.6690839408078,
132.356450179057));
#121777=CARTESIAN_POINT('Ctrl Pts',(-186.737093444975,-4.62044665828881,
132.489785116144));
#121778=CARTESIAN_POINT('Ctrl Pts',(-186.745555193041,-4.56930605760306,
132.629982685208));
#121779=CARTESIAN_POINT('Ctrl Pts',(-186.754016941106,-4.51183726098221,
132.767692681952));
#121780=CARTESIAN_POINT('Ctrl Pts',(-186.762478689172,-4.44832931978521,
132.902347587316));
#121781=CARTESIAN_POINT('Ctrl Pts',(-186.770940437238,-4.38482137858837,
133.037002492679));
#121782=CARTESIAN_POINT('Ctrl Pts',(-186.779402185303,-4.31527456651344,
133.168601951196));
#121783=CARTESIAN_POINT('Ctrl Pts',(-186.787863933369,-4.2400305344674,
133.29661343967));
#121784=CARTESIAN_POINT('Ctrl Pts',(-186.795638267488,-4.17089916337693,
133.414225554185));
#121785=CARTESIAN_POINT('Ctrl Pts',(-186.803412601607,-4.09676100795466,
133.529145376511));
#121786=CARTESIAN_POINT('Ctrl Pts',(-186.811186935727,-4.0178513751189,
133.64091722549));
#121787=CARTESIAN_POINT('Ctrl Pts',(-186.818951688674,-3.93903899135325,
133.752551325653));
#121788=CARTESIAN_POINT('Ctrl Pts',(-186.826716441621,-3.85546705377721,
133.861044855384));
#121789=CARTESIAN_POINT('Ctrl Pts',(-186.834481194568,-3.76741631617132,
133.965967386781));
#121790=CARTESIAN_POINT('Ctrl Pts',(-186.842238235453,-3.67945303179932,
134.070785707641));
#121791=CARTESIAN_POINT('Ctrl Pts',(-186.849995276338,-3.5870200496273,
134.172039790846));
#121792=CARTESIAN_POINT('Ctrl Pts',(-186.857752317224,-3.49044069470467,
134.269329133909));
#121793=CARTESIAN_POINT('Ctrl Pts',(-186.865503508464,-3.39393417102474,
134.366545110322));
#121794=CARTESIAN_POINT('Ctrl Pts',(-186.873254699704,-3.29328777264913,
134.459802021349));
#121795=CARTESIAN_POINT('Ctrl Pts',(-186.881005890944,-3.18886403465664,
134.548733626626));
#121796=CARTESIAN_POINT('Ctrl Pts',(-186.888753787722,-3.08448467953826,
134.637627433597));
#121797=CARTESIAN_POINT('Ctrl Pts',(-186.896501684499,-2.97633147498796,
134.722199338236));
#121798=CARTESIAN_POINT('Ctrl Pts',(-186.904249581276,-2.86480246755412,
134.802121226256));
#121799=CARTESIAN_POINT('Ctrl Pts',(-186.91199585736,-2.75329678958435,
134.882026396341));
#121800=CARTESIAN_POINT('Ctrl Pts',(-186.919742133444,-2.63841703088417,
134.957283256941));
#121801=CARTESIAN_POINT('Ctrl Pts',(-186.927488409529,-2.52059252882238,
135.027605385058));
#121802=CARTESIAN_POINT('Ctrl Pts',(-186.935234742794,-2.40276715700672,
135.097928032277));
#121803=CARTESIAN_POINT('Ctrl Pts',(-186.94298107606,-2.2819973341713,135.163315673957));
#121804=CARTESIAN_POINT('Ctrl Pts',(-186.950727409325,-2.15873910496181,
135.223526663237));
#121805=CARTESIAN_POINT('Ctrl Pts',(-186.958475477328,-2.03545327292633,
135.28375113635));
#121806=CARTESIAN_POINT('Ctrl Pts',(-186.966223545331,-1.90967827685561,
135.338796478669));
#121807=CARTESIAN_POINT('Ctrl Pts',(-186.973971613335,-1.78189197661644,
135.388468387478));
#121808=CARTESIAN_POINT('Ctrl Pts',(-186.981727916077,-1.65396986357687,
135.438193088183));
#121809=CARTESIAN_POINT('Ctrl Pts',(-186.989484218819,-1.52403254119107,
135.482532805269));
#121810=CARTESIAN_POINT('Ctrl Pts',(-186.997240521561,-1.3925754703003,
135.521342345538));
#121811=CARTESIAN_POINT('Ctrl Pts',(-187.005000964075,-1.2610482368127,
135.560172599627));
#121812=CARTESIAN_POINT('Ctrl Pts',(-187.012761406589,-1.12800001764879,
135.59346670068));
#121813=CARTESIAN_POINT('Ctrl Pts',(-187.020521849103,-0.993937454370752,
135.621130427231));
#121814=CARTESIAN_POINT('Ctrl Pts',(-187.028294749369,-0.85965968196463,
135.648838562051));
#121815=CARTESIAN_POINT('Ctrl Pts',(-187.036067649635,-0.724364697643503,
135.670898197859));
#121816=CARTESIAN_POINT('Ctrl Pts',(-187.0438405499,-0.588566164980932,
135.687266814898));
#121817=CARTESIAN_POINT('Ctrl Pts',(-187.051330885661,-0.457704251061874,
135.703040391474));
#121818=CARTESIAN_POINT('Ctrl Pts',(-187.058821221422,-0.326375070731452,
135.713529506913));
#121819=CARTESIAN_POINT('Ctrl Pts',(-187.066311557182,-0.19503718887608,
135.718741917125));
#121820=CARTESIAN_POINT('Ctrl Pts',(-187.074085891301,-0.0587195912883398,
135.724151957455));
#121821=CARTESIAN_POINT('Ctrl Pts',(-187.08186022542,0.0780391938607504,
135.723894398637));
#121822=CARTESIAN_POINT('Ctrl Pts',(-187.089634559539,0.214728599968461,
135.717920904248));
#121823=CARTESIAN_POINT('Ctrl Pts',(-187.097399312486,0.351249548599797,
135.711954771656));
#121824=CARTESIAN_POINT('Ctrl Pts',(-187.105164065433,0.48770090147341,
135.700286736615));
#121825=CARTESIAN_POINT('Ctrl Pts',(-187.11292881838,0.62356877312973,135.682920348437));
#121826=CARTESIAN_POINT('Ctrl Pts',(-187.120685859265,0.759301698900149,
135.665571208801));
#121827=CARTESIAN_POINT('Ctrl Pts',(-187.12844290015,0.894451911427142,
135.642535028303));
#121828=CARTESIAN_POINT('Ctrl Pts',(-187.136199941035,1.028507691538,135.613867348089));
#121829=CARTESIAN_POINT('Ctrl Pts',(-187.143951132275,1.16246237914208,
135.585221286396));
#121830=CARTESIAN_POINT('Ctrl Pts',(-187.151702323515,1.2953238963055,135.550952259327));
#121831=CARTESIAN_POINT('Ctrl Pts',(-187.159453514755,1.42658815557148,
135.511167316049));
#121832=CARTESIAN_POINT('Ctrl Pts',(-187.167201411532,1.55779662402658,
135.471399282433));
#121833=CARTESIAN_POINT('Ctrl Pts',(-187.174949308309,1.68740881144558,
135.42612010863));
#121834=CARTESIAN_POINT('Ctrl Pts',(-187.182697205086,1.81493351210572,
135.375487328688));
#121835=CARTESIAN_POINT('Ctrl Pts',(-187.19044348117,1.94243153734725,135.324865140033));
#121836=CARTESIAN_POINT('Ctrl Pts',(-187.198189757255,2.0678425812239,135.268891716883));
#121837=CARTESIAN_POINT('Ctrl Pts',(-187.205936033339,2.19069360062039,
135.207773454299));
#121838=CARTESIAN_POINT('Ctrl Pts',(-187.213682366604,2.31354552687536,
135.146654740553));
#121839=CARTESIAN_POINT('Ctrl Pts',(-187.221428699869,2.43383704090215,
135.080391285736));
#121840=CARTESIAN_POINT('Ctrl Pts',(-187.229175033134,2.55111833508265,
135.009236157092));
#121841=CARTESIAN_POINT('Ctrl Pts',(-187.236923101137,2.66842589359566,
134.938065093751));
#121842=CARTESIAN_POINT('Ctrl Pts',(-187.24467116914,2.78272155665276,134.862000379508));
#121843=CARTESIAN_POINT('Ctrl Pts',(-187.252419237143,2.89358355694662,
134.78133902604));
#121844=CARTESIAN_POINT('Ctrl Pts',(-187.260175539885,3.00456338269382,
134.700591944726));
#121845=CARTESIAN_POINT('Ctrl Pts',(-187.267931842627,3.11210193908768,
134.615238695533));
#121846=CARTESIAN_POINT('Ctrl Pts',(-187.275688145368,3.21580926229213,
134.52561764323));
#121847=CARTESIAN_POINT('Ctrl Pts',(-187.283448587883,3.31957193721782,
134.435948757473));
#121848=CARTESIAN_POINT('Ctrl Pts',(-187.291209030397,3.41949901971309,
134.342007797447));
#121849=CARTESIAN_POINT('Ctrl Pts',(-187.298969472911,3.51523738644899,
134.244170086041));
#121850=CARTESIAN_POINT('Ctrl Pts',(-187.306742373176,3.61112944091017,
134.146175316856));
#121851=CARTESIAN_POINT('Ctrl Pts',(-187.314515273441,3.70281908106574,
134.044271586789));
#121852=CARTESIAN_POINT('Ctrl Pts',(-187.322288173707,3.7899928861312,133.938868072586));
#121853=CARTESIAN_POINT('Ctrl Pts',(-187.329778509469,3.87399770381394,
133.837296241609));
#121854=CARTESIAN_POINT('Ctrl Pts',(-187.337268845232,3.95380912358556,
133.732474905839));
#121855=CARTESIAN_POINT('Ctrl Pts',(-187.344759180995,4.02918580518921,
133.624794061163));
#121856=CARTESIAN_POINT('Ctrl Pts',(-187.352533515114,4.10742041657999,
133.513030464541));
#121857=CARTESIAN_POINT('Ctrl Pts',(-187.360307849233,4.181125188946,133.39783220855));
#121858=CARTESIAN_POINT('Ctrl Pts',(-187.368082183353,4.24998348176541,
133.279602720315));
#121859=CARTESIAN_POINT('Ctrl Pts',(-187.3758469363,4.31875691289296,133.161518939358));
#121860=CARTESIAN_POINT('Ctrl Pts',(-187.383611689247,4.38269555379604,
133.040411693732));
#121861=CARTESIAN_POINT('Ctrl Pts',(-187.391376442194,4.44152462296868,
132.916715248319));
#121862=CARTESIAN_POINT('Ctrl Pts',(-187.399133483079,4.50029526228031,
132.793141659959));
#121863=CARTESIAN_POINT('Ctrl Pts',(-187.406890523964,4.55396626230861,
132.666984340256));
#121864=CARTESIAN_POINT('Ctrl Pts',(-187.414647564849,4.60230775467839,
132.538703834385));
#121865=CARTESIAN_POINT('Ctrl Pts',(-187.42239875609,4.6506127923528,132.410520065842));
#121866=CARTESIAN_POINT('Ctrl Pts',(-187.43014994733,4.69359618468073,132.280216662417));
#121867=CARTESIAN_POINT('Ctrl Pts',(-187.43790113857,4.73107552357416,132.148275589853));
#121868=CARTESIAN_POINT('Ctrl Pts',(-187.445649035347,4.76853893274882,
132.016390595764));
#121869=CARTESIAN_POINT('Ctrl Pts',(-187.453396932125,4.80050283470879,
131.882869692232));
#121870=CARTESIAN_POINT('Ctrl Pts',(-187.461144828902,4.82683425861936,
131.748211295543));
#121871=CARTESIAN_POINT('Ctrl Pts',(-187.468891104986,4.85316017456368,
131.613581066489));
#121872=CARTESIAN_POINT('Ctrl Pts',(-187.47663738107,4.87385588096731,131.477814201007));
#121873=CARTESIAN_POINT('Ctrl Pts',(-187.484383657154,4.88883933248194,
131.34142024524));
#121874=CARTESIAN_POINT('Ctrl Pts',(-187.49212999042,4.90382289460099,131.205025282644));
#121875=CARTESIAN_POINT('Ctrl Pts',(-187.499876323685,4.91309407499838,
131.068003609154));
#121876=CARTESIAN_POINT('Ctrl Pts',(-187.507622656951,4.91662265431028,
130.930870449686));
#121877=CARTESIAN_POINT('Ctrl Pts',(-187.515370724954,4.92015202382305,
130.793706580197));
#121878=CARTESIAN_POINT('Ctrl Pts',(-187.523118792957,4.91793622317329,
130.65643156581));
#121879=CARTESIAN_POINT('Ctrl Pts',(-187.53086686096,4.90999716116407,130.519560793372));
#121880=CARTESIAN_POINT('Ctrl Pts',(-187.538623163702,4.90204966142525,
130.382544553048));
#121881=CARTESIAN_POINT('Ctrl Pts',(-187.546379466444,4.88836677205368,
130.245933803843));
#121882=CARTESIAN_POINT('Ctrl Pts',(-187.554135769186,4.86902238393298,
130.110239527799));
#121883=CARTESIAN_POINT('Ctrl Pts',(-187.5618962117,4.8496676711299,129.974472827634));
#121884=CARTESIAN_POINT('Ctrl Pts',(-187.569656654214,4.82464550985388,
129.839623959516));
#121885=CARTESIAN_POINT('Ctrl Pts',(-187.577417096728,4.79408079809747,
129.706192887293));
#121886=CARTESIAN_POINT('Ctrl Pts',(-187.585189996994,4.76346702115233,
129.572547619668));
#121887=CARTESIAN_POINT('Ctrl Pts',(-187.59296289726,4.72729301712821,129.440325073378));
#121888=CARTESIAN_POINT('Ctrl Pts',(-187.600735797525,4.6857336264191,129.310010108232));
#121889=CARTESIAN_POINT('Ctrl Pts',(-187.608226133286,4.64568502424898,
129.184432420329));
#121890=CARTESIAN_POINT('Ctrl Pts',(-187.615716469048,4.60063588766843,
129.060626320137));
#121891=CARTESIAN_POINT('Ctrl Pts',(-187.623206804809,4.55078388095632,
128.939005656351));
#121892=CARTESIAN_POINT('Ctrl Pts',(-187.630981138928,4.49904172025193,
128.812773708119));
#121893=CARTESIAN_POINT('Ctrl Pts',(-187.638755473047,4.4419613947056,128.688496324464));
#121894=CARTESIAN_POINT('Ctrl Pts',(-187.646529807166,4.37971116704724,
128.566657966242));
#121895=CARTESIAN_POINT('Ctrl Pts',(-187.654294560113,4.31753765723083,
128.444969762907));
#121896=CARTESIAN_POINT('Ctrl Pts',(-187.66205931306,4.25020709874698,128.325714949011));
#121897=CARTESIAN_POINT('Ctrl Pts',(-187.669824066007,4.17793632482349,
128.209359436792));
#121898=CARTESIAN_POINT('Ctrl Pts',(-187.677581106892,4.1057373312515,128.093119490508));
#121899=CARTESIAN_POINT('Ctrl Pts',(-187.685338147778,4.02860809172652,
127.979773445279));
#121900=CARTESIAN_POINT('Ctrl Pts',(-187.693095188663,3.94681182647804,
127.869763631799));
#121901=CARTESIAN_POINT('Ctrl Pts',(-187.700846379903,3.86507724442891,
127.759836777574));
#121902=CARTESIAN_POINT('Ctrl Pts',(-187.708597571143,3.77868287422416,
127.653241459867));
#121903=CARTESIAN_POINT('Ctrl Pts',(-187.716348762383,3.68793561126631,
127.550391658025));
#121904=CARTESIAN_POINT('Ctrl Pts',(-187.72409665916,3.59722691831658,127.447585570094));
#121905=CARTESIAN_POINT('Ctrl Pts',(-187.731844555937,3.50216927043818,
127.348522124323));
#121906=CARTESIAN_POINT('Ctrl Pts',(-187.739592452715,3.40311012538557,
127.253582599019));
#121907=CARTESIAN_POINT('Ctrl Pts',(-187.747338728799,3.30407170137063,
127.158662933017));
#121908=CARTESIAN_POINT('Ctrl Pts',(-187.755085004883,3.20103372715624,
127.067865742005));
#121909=CARTESIAN_POINT('Ctrl Pts',(-187.762831280967,3.09438055082806,
126.981535475193));
#121910=CARTESIAN_POINT('Ctrl Pts',(-187.770577614232,2.9877265872108,126.895204571112));
#121911=CARTESIAN_POINT('Ctrl Pts',(-187.778323947498,2.87745767211547,
126.813340903009));
#121912=CARTESIAN_POINT('Ctrl Pts',(-187.786070280763,2.76399094455158,
126.736248386944));
#121913=CARTESIAN_POINT('Ctrl Pts',(-187.793818348766,2.6504988069003,126.659138606544));
#121914=CARTESIAN_POINT('Ctrl Pts',(-187.801566416769,2.53380775509228,
126.586802323981));
#121915=CARTESIAN_POINT('Ctrl Pts',(-187.809314484772,2.41436324092127,
126.519499685938));
#121916=CARTESIAN_POINT('Ctrl Pts',(-187.817070787514,2.29479177969936,
126.452125517851));
#121917=CARTESIAN_POINT('Ctrl Pts',(-187.824827090256,2.17246135144864,
126.389795873351));
#121918=CARTESIAN_POINT('Ctrl Pts',(-187.832583392998,2.0478417996602,126.33272478422));
#121919=CARTESIAN_POINT('Ctrl Pts',(-187.840343835512,1.92315573466474,
126.27562323453));
#121920=CARTESIAN_POINT('Ctrl Pts',(-187.848104278026,1.79617847343045,
126.223785980392));
#121921=CARTESIAN_POINT('Ctrl Pts',(-187.855864720541,1.66739816011783,
126.177378184259));
#121922=CARTESIAN_POINT('Ctrl Pts',(-187.863637620806,1.53841111721335,
126.130895890211));
#121923=CARTESIAN_POINT('Ctrl Pts',(-187.871410521072,1.40761561151015,
126.089860588313));
#121924=CARTESIAN_POINT('Ctrl Pts',(-187.879183421337,1.27551407480012,
126.054387258958));
#121925=CARTESIAN_POINT('Ctrl Pts',(-187.886673757098,1.14821476170498,
126.02020347448));
#121926=CARTESIAN_POINT('Ctrl Pts',(-187.89416409286,1.01970302453186,125.991184367656));
#121927=CARTESIAN_POINT('Ctrl Pts',(-187.901654428621,0.890433888279403,
125.967387333259));
#121928=CARTESIAN_POINT('Ctrl Pts',(-187.90942876274,0.756263473425365,
125.942688027067));
#121929=CARTESIAN_POINT('Ctrl Pts',(-187.917203096859,0.620852080617946,
125.923536360038));
#121930=CARTESIAN_POINT('Ctrl Pts',(-187.924977430978,0.484698250610068,
125.910052630899));
#121931=CARTESIAN_POINT('Ctrl Pts',(-187.932742183925,0.34871221802889,
125.89658551925));
#121932=CARTESIAN_POINT('Ctrl Pts',(-187.940506936872,0.211985954126687,
125.888772485131));
#121933=CARTESIAN_POINT('Ctrl Pts',(-187.948271689819,0.0750286477215531,
125.886682937551));
#121934=CARTESIAN_POINT('Ctrl Pts',(-187.956028730704,-0.0617926307557264,
125.884595465339));
#121935=CARTESIAN_POINT('Ctrl Pts',(-187.963785771589,-0.198844106680892,
125.888220172887));
#121936=CARTESIAN_POINT('Ctrl Pts',(-187.971542812474,-0.33561135775171,
125.897574696105));
#121937=CARTESIAN_POINT('Ctrl Pts',(-187.979294003714,-0.472275471574414,
125.906922165004));
#121938=CARTESIAN_POINT('Ctrl Pts',(-187.987045194954,-0.608655398690284,
125.921990822516));
#121939=CARTESIAN_POINT('Ctrl Pts',(-187.994796386194,-0.744236962088531,
125.942746234795));
#121940=CARTESIAN_POINT('Ctrl Pts',(-188.002544282971,-0.879760899705762,
125.963492825471));
#121941=CARTESIAN_POINT('Ctrl Pts',(-188.010292179749,-1.01448676284468,
125.989921304604));
#121942=CARTESIAN_POINT('Ctrl Pts',(-188.018040076526,-1.14790596186375,
126.021945436382));
#121943=CARTESIAN_POINT('Ctrl Pts',(-188.02578635261,-1.28129725246294,
126.053962869403));
#121944=CARTESIAN_POINT('Ctrl Pts',(-188.033532628694,-1.41338204267613,
126.091573535708));
#121945=CARTESIAN_POINT('Ctrl Pts',(-188.041278904778,-1.54366278809802,
126.134640255581));
#121946=CARTESIAN_POINT('Ctrl Pts',(-188.049025238043,-1.67394449522224,
126.177707293362));
#121947=CARTESIAN_POINT('Ctrl Pts',(-188.056771571308,-1.80242175977307,
126.226230342367));
#121948=CARTESIAN_POINT('Ctrl Pts',(-188.064517904574,-1.928613414739,126.280022725787));
#121949=CARTESIAN_POINT('Ctrl Pts',(-188.072265972577,-2.05483332945198,
126.333827155638));
#121950=CARTESIAN_POINT('Ctrl Pts',(-188.080014040579,-2.17876625648171,
126.392903114748));
#121951=CARTESIAN_POINT('Ctrl Pts',(-188.087762108582,-2.29995254948067,
126.457016447543));
#121952=CARTESIAN_POINT('Ctrl Pts',(-188.095518411324,-2.42126764071347,
126.52119792075));
#121953=CARTESIAN_POINT('Ctrl Pts',(-188.103274714066,-2.53982992045492,
126.590427279275));
#121954=CARTESIAN_POINT('Ctrl Pts',(-188.111031016808,-2.65520535582168,
126.664424919887));
#121955=CARTESIAN_POINT('Ctrl Pts',(-188.118791459322,-2.77064237053186,
126.738462055268));
#121956=CARTESIAN_POINT('Ctrl Pts',(-188.126551901836,-2.88288883183471,
126.817272319268));
#121957=CARTESIAN_POINT('Ctrl Pts',(-188.13431234435,-2.99154193003811,
126.900534296721));
#121958=CARTESIAN_POINT('Ctrl Pts',(-188.142085244616,-3.1003694478408,
126.983929933691));
#121959=CARTESIAN_POINT('Ctrl Pts',(-188.149858144881,-3.20559177519847,
127.071791313939));
#121960=CARTESIAN_POINT('Ctrl Pts',(-188.157631045146,-3.30684059919295,
127.163757877081));
#121961=CARTESIAN_POINT('Ctrl Pts',(-188.165121380909,-3.4044087734147,
127.252381224011));
#121962=CARTESIAN_POINT('Ctrl Pts',(-188.172611716672,-3.49828710288302,
127.344816252083));
#121963=CARTESIAN_POINT('Ctrl Pts',(-188.180102052434,-3.58818134762388,
127.440711159156));
#121964=CARTESIAN_POINT('Ctrl Pts',(-188.187783968033,-3.6803748116775,
127.539058764095));
#121965=CARTESIAN_POINT('Ctrl Pts',(-188.195465883631,-3.76868519027518,
127.641374004402));
#121966=CARTESIAN_POINT('Ctrl Pts',(-188.20314779923,-3.85274535651832,
127.747313630631));
#121967=CARTESIAN_POINT('Ctrl Pts',(-188.210820609535,-3.93670588713396,
127.85312768774));
#121968=CARTESIAN_POINT('Ctrl Pts',(-188.21849341984,-4.01642597523958,
127.962557278402));
#121969=CARTESIAN_POINT('Ctrl Pts',(-188.226166230145,-4.09157506968238,
128.075222198274));
#121970=CARTESIAN_POINT('Ctrl Pts',(-188.233972786232,-4.16803409802803,
128.189850995414));
#121971=CARTESIAN_POINT('Ctrl Pts',(-188.241779342318,-4.23976097868823,
128.307828684763));
#121972=CARTESIAN_POINT('Ctrl Pts',(-188.249585898404,-4.3064496647105,
128.428718736344));
#121973=CARTESIAN_POINT('Ctrl Pts',(-188.257245164482,-4.37188010355881,
128.547327897795));
#121974=CARTESIAN_POINT('Ctrl Pts',(-188.26490443056,-4.43246057085316,
128.668740130964));
#121975=CARTESIAN_POINT('Ctrl Pts',(-188.272563696638,-4.4879455798733,
128.792513820567));
#121976=CARTESIAN_POINT('Ctrl Pts',(-188.280443897728,-4.54503107920871,
128.919857818529));
#121977=CARTESIAN_POINT('Ctrl Pts',(-188.288324098819,-4.59672247009533,
129.049701204745));
#121978=CARTESIAN_POINT('Ctrl Pts',(-188.29620429991,-4.64280362102202,
129.181536659422));
#121979=CARTESIAN_POINT('Ctrl Pts',(-188.304084501,-4.68888477194858,129.3133721141));
#121980=CARTESIAN_POINT('Ctrl Pts',(-188.311964702091,-4.72935551781386,
129.447199204311));
#121981=CARTESIAN_POINT('Ctrl Pts',(-188.319844903182,-4.76405452823404,
129.582490119308));
#121982=CARTESIAN_POINT('Origin',(213.235140564004,0.,130.804360617566));
#121983=CARTESIAN_POINT('',(-190.415359814329,-4.76405452823405,129.582490119308));
#121984=CARTESIAN_POINT('',(-190.06976504276,-4.76405452823418,129.582490119309));
#121985=CARTESIAN_POINT('',(213.235140564004,-4.76405452823405,129.582490119308));
#121986=CARTESIAN_POINT('',(-188.735140564044,-4.9182496381179,130.802473913264));
#121987=CARTESIAN_POINT('Ctrl Pts',(-188.735140564045,-4.9182496381179,
130.802473913264));
#121988=CARTESIAN_POINT('Ctrl Pts',(-188.742840932869,-4.91830150830916,
130.937688821655));
#121989=CARTESIAN_POINT('Ctrl Pts',(-188.750541301692,-4.91277307334292,
131.073131498441));
#121990=CARTESIAN_POINT('Ctrl Pts',(-188.758241670516,-4.90163420131192,
131.208297764941));
#121991=CARTESIAN_POINT('Ctrl Pts',(-188.76593290635,-4.89050854049381,
131.343303718052));
#121992=CARTESIAN_POINT('Ctrl Pts',(-188.773624142184,-4.87378571052704,
131.478033519156));
#121993=CARTESIAN_POINT('Ctrl Pts',(-188.781315378017,-4.85148756347388,
131.611981496418));
#121994=CARTESIAN_POINT('Ctrl Pts',(-188.788999416841,-4.82921028172503,
131.745804132983));
#121995=CARTESIAN_POINT('Ctrl Pts',(-188.796683455665,-4.80136812688925,
131.87884601002));
#121996=CARTESIAN_POINT('Ctrl Pts',(-188.804367494489,-4.76803483755962,
132.010605555511));
#121997=CARTESIAN_POINT('Ctrl Pts',(-188.812346179207,-4.73342337706943,
132.147417445207));
#121998=CARTESIAN_POINT('Ctrl Pts',(-188.820324863925,-4.69289129475855,
132.282846262811));
#121999=CARTESIAN_POINT('Ctrl Pts',(-188.828303548642,-4.64657983212241,
132.416340433263));
#122000=CARTESIAN_POINT('Ctrl Pts',(-188.835979763627,-4.6020240242359,
132.544773876606));
#122001=CARTESIAN_POINT('Ctrl Pts',(-188.843655978612,-4.55211916674477,
132.671416266738));
#122002=CARTESIAN_POINT('Ctrl Pts',(-188.851332193597,-4.49704201443896,
132.795791305004));
#122003=CARTESIAN_POINT('Ctrl Pts',(-188.859007503027,-4.44197135952829,
132.920151670875));
#122004=CARTESIAN_POINT('Ctrl Pts',(-188.866682812457,-4.3817297846288,
133.042244852048));
#122005=CARTESIAN_POINT('Ctrl Pts',(-188.874358121887,-4.31654198168248,
133.161615033804));
#122006=CARTESIAN_POINT('Ctrl Pts',(-188.882034263867,-4.25134710773214,
133.280998163795));
#122007=CARTESIAN_POINT('Ctrl Pts',(-188.889710405848,-4.18120513001891,
133.397657356846));
#122008=CARTESIAN_POINT('Ctrl Pts',(-188.897386547828,-4.10638618677583,
133.511162336857));
#122009=CARTESIAN_POINT('Ctrl Pts',(-188.905065260793,-4.03154218428859,
133.624705333297));
#122010=CARTESIAN_POINT('Ctrl Pts',(-188.912743973757,-3.95201832019808,
133.735091682711));
#122011=CARTESIAN_POINT('Ctrl Pts',(-188.920422686722,-3.86812714267184,
133.841921394016));
#122012=CARTESIAN_POINT('Ctrl Pts',(-188.928109823954,-3.78414392866631,
133.94886830752));
#122013=CARTESIAN_POINT('Ctrl Pts',(-188.935796961185,-3.69578408429893,
134.052250480927));
#122014=CARTESIAN_POINT('Ctrl Pts',(-188.943484098417,-3.60339959857195,
134.151702009703));
#122015=CARTESIAN_POINT('Ctrl Pts',(-188.951176241949,-3.5109549468263,
134.251218306957));
#122016=CARTESIAN_POINT('Ctrl Pts',(-188.958868385481,-3.41448071785227,
134.346798583313));
#122017=CARTESIAN_POINT('Ctrl Pts',(-188.966560529013,-3.31436367286446,
134.438115769815));
#122018=CARTESIAN_POINT('Ctrl Pts',(-188.974263479165,-3.21410597437231,
134.529561246983));
#122019=CARTESIAN_POINT('Ctrl Pts',(-188.981966429318,-3.11019555105514,
134.616731427316));
#122020=CARTESIAN_POINT('Ctrl Pts',(-188.98966937947,-3.00305014572403,
134.699341090529));
#122021=CARTESIAN_POINT('Ctrl Pts',(-188.991731562218,-2.97436588814104,
134.721456801895));
#122022=CARTESIAN_POINT('Ctrl Pts',(-188.993793744965,-2.94544992466852,
134.743245908247));
#122023=CARTESIAN_POINT('Ctrl Pts',(-188.995855927712,-2.91631057808861,
134.764703490933));
#122024=CARTESIAN_POINT('Ctrl Pts',(-189.003630261831,-2.80645658157905,
134.84559759084));
#122025=CARTESIAN_POINT('Ctrl Pts',(-189.01140459595,-2.69306021115118,
134.92204557856));
#122026=CARTESIAN_POINT('Ctrl Pts',(-189.01917893007,-2.57651717925398,
134.993721223614));
#122027=CARTESIAN_POINT('Ctrl Pts',(-189.026943683017,-2.46011777622816,
135.065308534842));
#122028=CARTESIAN_POINT('Ctrl Pts',(-189.034708435964,-2.34057975758224,
135.132135002961));
#122029=CARTESIAN_POINT('Ctrl Pts',(-189.042473188911,-2.21833066914151,
135.193915504436));
#122030=CARTESIAN_POINT('Ctrl Pts',(-189.050230229796,-2.09620300021883,
135.255634644646));
#122031=CARTESIAN_POINT('Ctrl Pts',(-189.057987270681,-1.97136996672141,
135.312317616571));
#122032=CARTESIAN_POINT('Ctrl Pts',(-189.065744311566,-1.84428646499388,
135.363723566218));
#122033=CARTESIAN_POINT('Ctrl Pts',(-189.073495502806,-1.71729879792339,
135.415090750238));
#122034=CARTESIAN_POINT('Ctrl Pts',(-189.081246694046,-1.58806440155843,
135.461188686808));
#122035=CARTESIAN_POINT('Ctrl Pts',(-189.088997885286,-1.4570607255567,
135.501823454517));
#122036=CARTESIAN_POINT('Ctrl Pts',(-189.096745782063,-1.32611272961209,
135.542440951367));
#122037=CARTESIAN_POINT('Ctrl Pts',(-189.10449367884,-1.19339732231602,
135.57759978204));
#122038=CARTESIAN_POINT('Ctrl Pts',(-189.112241575618,-1.05940958549109,
135.607155053378));
#122039=CARTESIAN_POINT('Ctrl Pts',(-189.119987851702,-0.925449876012263,
135.636704142391));
#122040=CARTESIAN_POINT('Ctrl Pts',(-189.127734127786,-0.790218747924846,
135.660651919364));
#122041=CARTESIAN_POINT('Ctrl Pts',(-189.13548040387,-0.65422363177214,
135.678904134874));
#122042=CARTESIAN_POINT('Ctrl Pts',(-189.143226737135,-0.518227511734195,
135.697156485118));
#122043=CARTESIAN_POINT('Ctrl Pts',(-189.150973070401,-0.381467779868424,
135.709713137999));
#122044=CARTESIAN_POINT('Ctrl Pts',(-189.158719403666,-0.244458787537432,
135.716531518878));
#122045=CARTESIAN_POINT('Ctrl Pts',(-189.166467471669,-0.107419112992374,
135.723351426686));
#122046=CARTESIAN_POINT('Ctrl Pts',(-189.174215539672,0.0298695426863131,
135.72443048597));
#122047=CARTESIAN_POINT('Ctrl Pts',(-189.181963607675,0.166891415319874,
135.71977823136));
#122048=CARTESIAN_POINT('Ctrl Pts',(-189.189719910417,0.304058916429691,
135.715121032278));
#122049=CARTESIAN_POINT('Ctrl Pts',(-189.197476213158,0.440958676729197,
135.704720364546));
#122050=CARTESIAN_POINT('Ctrl Pts',(-189.2052325159,0.577078088149238,135.688637835607));
#122051=CARTESIAN_POINT('Ctrl Pts',(-189.212992958415,0.713270150598,135.672546722939));
#122052=CARTESIAN_POINT('Ctrl Pts',(-189.220753400929,0.848680648448811,
135.650767768445));
#122053=CARTESIAN_POINT('Ctrl Pts',(-189.228513843443,0.982806764623835,
135.623413836395));
#122054=CARTESIAN_POINT('Ctrl Pts',(-189.236286743708,1.1171481919477,135.596015993386));
#122055=CARTESIAN_POINT('Ctrl Pts',(-189.244059643974,1.25020073776289,
135.563025383117));
#122056=CARTESIAN_POINT('Ctrl Pts',(-189.251832544239,1.38147548620193,
135.524605160333));
#122057=CARTESIAN_POINT('Ctrl Pts',(-189.259322880001,1.50797806687371,
135.487581609423));
#122058=CARTESIAN_POINT('Ctrl Pts',(-189.266813215763,1.63282956904491,
135.445516450911));
#122059=CARTESIAN_POINT('Ctrl Pts',(-189.274303551525,1.75561151980122,
135.398597360926));
#122060=CARTESIAN_POINT('Ctrl Pts',(-189.282077885644,1.88304878554009,
135.349899319384));
#122061=CARTESIAN_POINT('Ctrl Pts',(-189.289852219764,2.0086601508045,135.295817746099));
#122062=CARTESIAN_POINT('Ctrl Pts',(-189.297626553883,2.1319572564113,135.23650922962));
#122063=CARTESIAN_POINT('Ctrl Pts',(-189.30539130683,2.25510240935448,135.177273805588));
#122064=CARTESIAN_POINT('Ctrl Pts',(-189.313156059777,2.37593862856379,
135.112824423354));
#122065=CARTESIAN_POINT('Ctrl Pts',(-189.320920812724,2.49399493257179,
135.043366673094));
#122066=CARTESIAN_POINT('Ctrl Pts',(-189.328677853609,2.61193398139434,
134.973977909251));
#122067=CARTESIAN_POINT('Ctrl Pts',(-189.336434894494,2.72709827484188,
134.899590873599));
#122068=CARTESIAN_POINT('Ctrl Pts',(-189.344191935379,2.8390392930429,134.820458095847));
#122069=CARTESIAN_POINT('Ctrl Pts',(-189.351943126619,2.95089589565147,
134.741384992739));
#122070=CARTESIAN_POINT('Ctrl Pts',(-189.359694317859,3.0595337432095,134.657573495689));
#122071=CARTESIAN_POINT('Ctrl Pts',(-189.3674455091,3.16453161094203,134.569320477358));
#122072=CARTESIAN_POINT('Ctrl Pts',(-189.375193405877,3.26948485177972,
134.481104968915));
#122073=CARTESIAN_POINT('Ctrl Pts',(-189.382941302654,3.37080089117263,
134.388451944842));
#122074=CARTESIAN_POINT('Ctrl Pts',(-189.390689199431,3.46809022258434,
134.291699613207));
#122075=CARTESIAN_POINT('Ctrl Pts',(-189.398435475515,3.5653592031655,134.194967520073));
#122076=CARTESIAN_POINT('Ctrl Pts',(-189.406181751599,3.65860287410479,
134.094138100479));
#122077=CARTESIAN_POINT('Ctrl Pts',(-189.413928027683,3.74746766208944,
133.989587325996));
#122078=CARTESIAN_POINT('Ctrl Pts',(-189.421674360949,3.83633310605366,
133.885035779743));
#122079=CARTESIAN_POINT('Ctrl Pts',(-189.429420694214,3.92081934936079,
133.776763121682));
#122080=CARTESIAN_POINT('Ctrl Pts',(-189.437167027479,4.00061255328625,
133.665179077551));
#122081=CARTESIAN_POINT('Ctrl Pts',(-189.444915095482,4.08042362634638,
133.553570044946));
#122082=CARTESIAN_POINT('Ctrl Pts',(-189.452663163485,4.15553934133821,
133.438648468607));
#122083=CARTESIAN_POINT('Ctrl Pts',(-189.460411231488,4.22568893687965,
133.320853429245));
#122084=CARTESIAN_POINT('Ctrl Pts',(-189.46816753423,4.29591308824612,133.202933195913));
#122085=CARTESIAN_POINT('Ctrl Pts',(-189.475923836972,4.36116037632517,
133.08213373541));
#122086=CARTESIAN_POINT('Ctrl Pts',(-189.483680139714,4.42120555602244,
132.958919619751));
#122087=CARTESIAN_POINT('Ctrl Pts',(-189.491440582228,4.4812827836402,132.835639741008));
#122088=CARTESIAN_POINT('Ctrl Pts',(-189.499201024743,4.53615221408563,
132.709942997256));
#122089=CARTESIAN_POINT('Ctrl Pts',(-189.506961467257,4.58563701835403,
132.582313428639));
#122090=CARTESIAN_POINT('Ctrl Pts',(-189.514734367522,4.63520126002316,
132.454478977708));
#122091=CARTESIAN_POINT('Ctrl Pts',(-189.522507267788,4.67936347626291,
132.324705871978));
#122092=CARTESIAN_POINT('Ctrl Pts',(-189.530280168053,4.7179966628129,132.193493639341));
#122093=CARTESIAN_POINT('Ctrl Pts',(-189.537770503815,4.7552254357191,132.06705130187));
#122094=CARTESIAN_POINT('Ctrl Pts',(-189.545260839577,4.78732011310547,
131.939272951445));
#122095=CARTESIAN_POINT('Ctrl Pts',(-189.552751175338,4.81421239738261,
131.810612104714));
#122096=CARTESIAN_POINT('Ctrl Pts',(-189.560525509457,4.84212431079291,
131.677073042868));
#122097=CARTESIAN_POINT('Ctrl Pts',(-189.568299843577,4.86451996267185,
131.542160232397));
#122098=CARTESIAN_POINT('Ctrl Pts',(-189.576074177696,4.88126712533379,
131.406369183648));
#122099=CARTESIAN_POINT('Ctrl Pts',(-189.583838930643,4.89799364861444,
131.27074548523));
#122100=CARTESIAN_POINT('Ctrl Pts',(-189.59160368359,4.90908548611105,131.134246086389));
#122101=CARTESIAN_POINT('Ctrl Pts',(-189.599368436537,4.91446102967388,
130.997378363685));
#122102=CARTESIAN_POINT('Ctrl Pts',(-189.607125477422,4.91983123417105,
130.860646579932));
#122103=CARTESIAN_POINT('Ctrl Pts',(-189.614882518307,4.91949642797885,
130.723547588459));
#122104=CARTESIAN_POINT('Ctrl Pts',(-189.622639559192,4.91342663554939,
130.586595240213));
#122105=CARTESIAN_POINT('Ctrl Pts',(-189.630390750432,4.90736142039758,
130.449746168797));
#122106=CARTESIAN_POINT('Ctrl Pts',(-189.638141941672,4.8955698444968,130.313043909499));
#122107=CARTESIAN_POINT('Ctrl Pts',(-189.645893132912,4.87807399294504,
130.177003317574));
#122108=CARTESIAN_POINT('Ctrl Pts',(-189.653641029689,4.86058557759692,
130.04102054653));
#122109=CARTESIAN_POINT('Ctrl Pts',(-189.661388926466,4.83739775844842,
129.905699270483));
#122110=CARTESIAN_POINT('Ctrl Pts',(-189.669136823243,4.80858454172782,
129.771550002034));
#122111=CARTESIAN_POINT('Ctrl Pts',(-189.676883099327,4.77977735211094,
129.637428794719));
#122112=CARTESIAN_POINT('Ctrl Pts',(-189.684629375411,4.74534718751536,
129.504479489374));
#122113=CARTESIAN_POINT('Ctrl Pts',(-189.692375651495,4.70541924846024,
129.373202779059));
#122114=CARTESIAN_POINT('Ctrl Pts',(-189.700121984761,4.66549101466631,
129.241925099689));
#122115=CARTESIAN_POINT('Ctrl Pts',(-189.707868318026,4.62006503919849,
129.112320414033));
#122116=CARTESIAN_POINT('Ctrl Pts',(-189.715614651291,4.56931639842622,
128.984874230265));
#122117=CARTESIAN_POINT('Ctrl Pts',(-189.723362719294,4.51855639284751,
128.857399505808));
#122118=CARTESIAN_POINT('Ctrl Pts',(-189.731110787297,4.46247149468235,
128.732084608271));
#122119=CARTESIAN_POINT('Ctrl Pts',(-189.7388588553,4.40128476182806,128.609394670723));
#122120=CARTESIAN_POINT('Ctrl Pts',(-189.746615158042,4.34003299898604,
128.48657433685));
#122121=CARTESIAN_POINT('Ctrl Pts',(-189.754371460784,4.2736687446074,128.366384886397));
#122122=CARTESIAN_POINT('Ctrl Pts',(-189.762127763526,4.20246110581043,
128.249266936964));
#122123=CARTESIAN_POINT('Ctrl Pts',(-189.76988820604,4.13121546135242,128.132086478155));
#122124=CARTESIAN_POINT('Ctrl Pts',(-189.777648648554,4.0551214983341,128.017981112027));
#122125=CARTESIAN_POINT('Ctrl Pts',(-189.785409091068,3.97449087304063,
127.907361245351));
#122126=CARTESIAN_POINT('Ctrl Pts',(-189.793181991334,3.89373081230961,
127.796563801844));
#122127=CARTESIAN_POINT('Ctrl Pts',(-189.800954891599,3.80841977969454,
127.689263345051));
#122128=CARTESIAN_POINT('Ctrl Pts',(-189.808727791865,3.71890939325291,
127.585836734281));
#122129=CARTESIAN_POINT('Ctrl Pts',(-189.816218127627,3.63265293481907,
127.486169941325));
#122130=CARTESIAN_POINT('Ctrl Pts',(-189.823708463389,3.54249734681371,
127.390100460701));
#122131=CARTESIAN_POINT('Ctrl Pts',(-189.831198799151,3.44878726912054,
127.29793088993));
#122132=CARTESIAN_POINT('Ctrl Pts',(-189.83897313327,3.3515241453514,127.20226668187));
#122133=CARTESIAN_POINT('Ctrl Pts',(-189.846747467389,3.25012357385693,
127.110500916178));
#122134=CARTESIAN_POINT('Ctrl Pts',(-189.854521801508,3.14493096923238,
127.023012675196));
#122135=CARTESIAN_POINT('Ctrl Pts',(-189.862286554456,3.03986800509226,
126.935632255653));
#122136=CARTESIAN_POINT('Ctrl Pts',(-189.870051307403,2.93102260408373,
126.852519119373));
#122137=CARTESIAN_POINT('Ctrl Pts',(-189.87781606035,2.81877752527758,126.774016175029));
#122138=CARTESIAN_POINT('Ctrl Pts',(-189.885573101235,2.70664392986547,
126.695591200915));
#122139=CARTESIAN_POINT('Ctrl Pts',(-189.89333014212,2.59111769456779,126.621767529126));
#122140=CARTESIAN_POINT('Ctrl Pts',(-189.901087183005,2.47261493422438,
126.552848127928));
#122141=CARTESIAN_POINT('Ctrl Pts',(-189.908838374245,2.35420153773453,
126.483980699386));
#122142=CARTESIAN_POINT('Ctrl Pts',(-189.916589565485,2.23281642057723,
126.420010375857));
#122143=CARTESIAN_POINT('Ctrl Pts',(-189.924340756725,2.10890468259733,
126.361196868364));
#122144=CARTESIAN_POINT('Ctrl Pts',(-189.932088653502,1.98504561041135,
126.302408358181));
#122145=CARTESIAN_POINT('Ctrl Pts',(-189.93983655028,1.8586624057305,126.248772472034));
#122146=CARTESIAN_POINT('Ctrl Pts',(-189.947584447057,1.73022457943941,
126.200502890919));
#122147=CARTESIAN_POINT('Ctrl Pts',(-189.955330723141,1.60181361957279,
126.15224340676));
#122148=CARTESIAN_POINT('Ctrl Pts',(-189.963076999225,1.47134925869841,
126.109348132341));
#122149=CARTESIAN_POINT('Ctrl Pts',(-189.970823275309,1.33932041800663,
126.071982369749));
#122150=CARTESIAN_POINT('Ctrl Pts',(-189.978569608574,1.20729060270813,
126.034616331331));
#122151=CARTESIAN_POINT('Ctrl Pts',(-189.98631594184,1.07369666073754,126.002779992655));
#122152=CARTESIAN_POINT('Ctrl Pts',(-189.994062275105,0.939041696927769,
125.976588486041));
#122153=CARTESIAN_POINT('Ctrl Pts',(-190.001810343108,0.804356578073038,
125.95039111402));
#122154=CARTESIAN_POINT('Ctrl Pts',(-190.009558411111,0.668610348265179,
125.929841164149));
#122155=CARTESIAN_POINT('Ctrl Pts',(-190.017306479114,0.532314905370259,
125.915002387285));
#122156=CARTESIAN_POINT('Ctrl Pts',(-190.025062781856,0.395874606056136,
125.900147839592));
#122157=CARTESIAN_POINT('Ctrl Pts',(-190.032819084598,0.258884316919199,
125.891016632574));
#122158=CARTESIAN_POINT('Ctrl Pts',(-190.040575387339,0.12186020099531,
125.887620523366));
#122159=CARTESIAN_POINT('Ctrl Pts',(-190.048335829854,-0.0152370488249634,
125.884222601552));
#122160=CARTESIAN_POINT('Ctrl Pts',(-190.056096272368,-0.152367770690179,
125.886565870162));
#122161=CARTESIAN_POINT('Ctrl Pts',(-190.063856714882,-0.28901821992613,
125.894609958821));
#122162=CARTESIAN_POINT('Ctrl Pts',(-190.071629615147,-0.42588803259445,
125.902666960564));
#122163=CARTESIAN_POINT('Ctrl Pts',(-190.079402515413,-0.562275642767436,
125.916443030582));
#122164=CARTESIAN_POINT('Ctrl Pts',(-190.087175415678,-0.697673929887046,
125.935846044305));
#122165=CARTESIAN_POINT('Ctrl Pts',(-190.09466575144,-0.82815014822142,
125.954543709606));
#122166=CARTESIAN_POINT('Ctrl Pts',(-190.102156087202,-0.957707420585213,
125.978466258228));
#122167=CARTESIAN_POINT('Ctrl Pts',(-190.109646422964,-1.0859048768382,
126.007487296229));
#122168=CARTESIAN_POINT('Ctrl Pts',(-190.117420757083,-1.21896297860964,
126.037608675706));
#122169=CARTESIAN_POINT('Ctrl Pts',(-190.125195091202,-1.35097760196638,
126.073318210457));
#122170=CARTESIAN_POINT('Ctrl Pts',(-190.132969425321,-1.48144310917082,
126.114530196667));
#122171=CARTESIAN_POINT('Ctrl Pts',(-190.140734178268,-1.61174782929803,
126.155691392787));
#122172=CARTESIAN_POINT('Ctrl Pts',(-190.148498931215,-1.74050686267825,
126.202341431007));
#122173=CARTESIAN_POINT('Ctrl Pts',(-190.156263684163,-1.86722481990743,
126.254343635793));
#122174=CARTESIAN_POINT('Ctrl Pts',(-190.164020725047,-1.9938169190744,
126.306294191256));
#122175=CARTESIAN_POINT('Ctrl Pts',(-190.171777765932,-2.11837161700793,
126.363586187039));
#122176=CARTESIAN_POINT('Ctrl Pts',(-190.179534806817,-2.24040909768993,
126.42603329569));
#122177=CARTESIAN_POINT('Ctrl Pts',(-190.187285998058,-2.36235454895925,
126.488433312491));
#122178=CARTESIAN_POINT('Ctrl Pts',(-190.195037189298,-2.48178621469771,
126.55598052693));
#122179=CARTESIAN_POINT('Ctrl Pts',(-190.202788380538,-2.59824500532673,
126.628440844056));
#122180=CARTESIAN_POINT('Ctrl Pts',(-190.210536277315,-2.71465429786326,
126.700870363613));
#122181=CARTESIAN_POINT('Ctrl Pts',(-190.218284174092,-2.82809289713704,
126.778208626477));
#122182=CARTESIAN_POINT('Ctrl Pts',(-190.226032070869,-2.93812724517321,
126.860176119641));
#122183=CARTESIAN_POINT('Ctrl Pts',(-190.233778346953,-3.04813857639583,
126.942126466972));
#122184=CARTESIAN_POINT('Ctrl Pts',(-190.241524623037,-3.15474675944337,
127.028703885119));
#122185=CARTESIAN_POINT('Ctrl Pts',(-190.249270899121,-3.25754844714305,
127.119586380653));
#122186=CARTESIAN_POINT('Ctrl Pts',(-190.257017232387,-3.36035089370159,
127.210469547061));
#122187=CARTESIAN_POINT('Ctrl Pts',(-190.264763565652,-3.45934649593055,
127.305657595318));
#122188=CARTESIAN_POINT('Ctrl Pts',(-190.272509898917,-3.55416644929697,
127.404789480909));
#122189=CARTESIAN_POINT('Ctrl Pts',(-190.28025796692,-3.64900763693438,
127.503943566399));
#122190=CARTESIAN_POINT('Ctrl Pts',(-190.288006034923,-3.73967104476384,
127.607042964203));
#122191=CARTESIAN_POINT('Ctrl Pts',(-190.295754102926,-3.82582634408186,
127.713691459046));
#122192=CARTESIAN_POINT('Ctrl Pts',(-190.303510405668,-3.91207321027691,
127.820453301177));
#122193=CARTESIAN_POINT('Ctrl Pts',(-190.31126670841,-3.99380215080234,
127.930771470759));
#122194=CARTESIAN_POINT('Ctrl Pts',(-190.319023011152,-4.07072427531871,
128.044218060228));
#122195=CARTESIAN_POINT('Ctrl Pts',(-190.326783453666,-4.14768745548943,
128.157725199558));
#122196=CARTESIAN_POINT('Ctrl Pts',(-190.33454389618,-4.21983850201565,
128.274363753527));
#122197=CARTESIAN_POINT('Ctrl Pts',(-190.342304338694,-4.28693368809188,
128.393679673019));
#122198=CARTESIAN_POINT('Ctrl Pts',(-190.35007723896,-4.35413658131705,
128.513187129016));
#122199=CARTESIAN_POINT('Ctrl Pts',(-190.357850139225,-4.41626721820383,
128.635380190496));
#122200=CARTESIAN_POINT('Ctrl Pts',(-190.36562303949,-4.47312899471228,
128.759782406989));
#122201=CARTESIAN_POINT('Ctrl Pts',(-190.373113375253,-4.52792370242032,
128.879662289568));
#122202=CARTESIAN_POINT('Ctrl Pts',(-190.380603711015,-4.57782585506955,
129.001593213935));
#122203=CARTESIAN_POINT('Ctrl Pts',(-190.388094046777,-4.62270349038433,
129.125135944543));
#122204=CARTESIAN_POINT('Ctrl Pts',(-190.397182635961,-4.67715690927988,
129.275039655247));
#122205=CARTESIAN_POINT('Ctrl Pts',(-190.406271225145,-4.72435719403422,
129.427710815754));
#122206=CARTESIAN_POINT('Ctrl Pts',(-190.415359814329,-4.76405452823405,
129.582490119308));
#122207=CARTESIAN_POINT('Ctrl Pts',(-188.665047832579,-4.76405452823406,
129.582490119308));
#122208=CARTESIAN_POINT('Ctrl Pts',(-188.672812177752,-4.7980988056188,
129.715228240137));
#122209=CARTESIAN_POINT('Ctrl Pts',(-188.680576522925,-4.82655782458609,
129.849259699109));
#122210=CARTESIAN_POINT('Ctrl Pts',(-188.688340868098,-4.84936224031761,
129.984074737716));
#122211=CARTESIAN_POINT('Ctrl Pts',(-188.696116115444,-4.87219867648161,
130.119079074566));
#122212=CARTESIAN_POINT('Ctrl Pts',(-188.703891362791,-4.88936461210996,
130.254868801069));
#122213=CARTESIAN_POINT('Ctrl Pts',(-188.711666610137,-4.90084263355078,
130.390930401361));
#122214=CARTESIAN_POINT('Ctrl Pts',(-188.713580508058,-4.90366797921412,
130.424422328024));
#122215=CARTESIAN_POINT('Ctrl Pts',(-188.715494405978,-4.90614893497245,
130.457930736052));
#122216=CARTESIAN_POINT('Ctrl Pts',(-188.717408303899,-4.90828572440508,
130.491447993817));
#122217=CARTESIAN_POINT('Ctrl Pts',(-188.72331905727,-4.91488484090139,
130.594960434142));
#122218=CARTESIAN_POINT('Ctrl Pts',(-188.729229810641,-4.9182098228819,
130.6986838224));
#122219=CARTESIAN_POINT('Ctrl Pts',(-188.735140564012,-4.91824963811768,
130.802473912695));
#122220=CARTESIAN_POINT('',(-188.389859436034,-4.91824789781227,130.808907942626));
#122221=CARTESIAN_POINT('Ctrl Pts',(-188.319844903182,-4.76405452823404,
129.582490119308));
#122222=CARTESIAN_POINT('Ctrl Pts',(-188.327501512409,-4.79776899317125,
129.71394230641));
#122223=CARTESIAN_POINT('Ctrl Pts',(-188.335158121637,-4.82603476089132,
129.846775959306));
#122224=CARTESIAN_POINT('Ctrl Pts',(-188.342814730864,-4.84875524607537,
129.980494350411));
#122225=CARTESIAN_POINT('Ctrl Pts',(-188.350655515053,-4.87202225836387,
130.117429254037));
#122226=CARTESIAN_POINT('Ctrl Pts',(-188.358496299241,-4.88947373540814,
130.255291565461));
#122227=CARTESIAN_POINT('Ctrl Pts',(-188.36633708343,-4.90106215269356,
130.393540902929));
#122228=CARTESIAN_POINT('Ctrl Pts',(-188.374177867618,-4.91265056997894,
130.531790240396));
#122229=CARTESIAN_POINT('Ctrl Pts',(-188.382018651807,-4.91837593560674,
130.670426153596));
#122230=CARTESIAN_POINT('Ctrl Pts',(-188.389859435995,-4.91824789781291,
130.808907941932));
#122231=CARTESIAN_POINT('Ctrl Pts',(-188.389859436034,-4.91824789781227,
130.808907942627));
#122232=CARTESIAN_POINT('Ctrl Pts',(-188.399867117337,-4.9180844751749,
130.985660875825));
#122233=CARTESIAN_POINT('Ctrl Pts',(-188.409874798639,-4.90838934841572,
131.161987856138));
#122234=CARTESIAN_POINT('Ctrl Pts',(-188.419882479942,-4.88932061848566,
131.33702087716));
#122235=CARTESIAN_POINT('Ctrl Pts',(-188.430125673914,-4.86980314050388,
131.516172983589));
#122236=CARTESIAN_POINT('Ctrl Pts',(-188.440368867886,-4.84046566695456,
131.693969810191));
#122237=CARTESIAN_POINT('Ctrl Pts',(-188.450612061858,-4.80152560262522,
131.86950612398));
#122238=CARTESIAN_POINT('Ctrl Pts',(-188.453257933321,-4.79146717697613,
131.914848087107));
#122239=CARTESIAN_POINT('Ctrl Pts',(-188.455903804784,-4.78076829602226,
131.960039341272));
#122240=CARTESIAN_POINT('Ctrl Pts',(-188.458549676247,-4.76943321745608,
132.005064513923));
#122241=CARTESIAN_POINT('Ctrl Pts',(-188.466324010366,-4.73612748463049,
132.137361468194));
#122242=CARTESIAN_POINT('Ctrl Pts',(-188.474098344485,-4.69726024638632,
132.268481144229));
#122243=CARTESIAN_POINT('Ctrl Pts',(-188.481872678604,-4.65292931576995,
132.397920106556));
#122244=CARTESIAN_POINT('Ctrl Pts',(-188.489637431551,-4.60865301906372,
132.527199546929));
#122245=CARTESIAN_POINT('Ctrl Pts',(-188.497402184498,-4.55892655312866,
132.654802028599));
#122246=CARTESIAN_POINT('Ctrl Pts',(-188.505166937445,-4.503898442119,132.780235584657));
#122247=CARTESIAN_POINT('Ctrl Pts',(-188.51292397833,-4.44892498580481,
132.90554455834));
#122248=CARTESIAN_POINT('Ctrl Pts',(-188.520681019215,-4.38866051938554,
133.028688537671));
#122249=CARTESIAN_POINT('Ctrl Pts',(-188.5284380601,-4.32330283091627,133.149192316152));
#122250=CARTESIAN_POINT('Ctrl Pts',(-188.53618925134,-4.25799442918837,
133.269605221796));
#122251=CARTESIAN_POINT('Ctrl Pts',(-188.54394044258,-4.18760063600923,
133.387381547266));
#122252=CARTESIAN_POINT('Ctrl Pts',(-188.551691633821,-4.11236649580212,
133.502067952824));
#122253=CARTESIAN_POINT('Ctrl Pts',(-188.559439530598,-4.03716433211143,
133.6167056136));
#122254=CARTESIAN_POINT('Ctrl Pts',(-188.567187427375,-3.95712612715828,
133.728255640296));
#122255=CARTESIAN_POINT('Ctrl Pts',(-188.574935324152,-3.87254171765271,
133.836291307331));
#122256=CARTESIAN_POINT('Ctrl Pts',(-188.582681600236,-3.78797500138217,
133.944304375634));
#122257=CARTESIAN_POINT('Ctrl Pts',(-188.59042787632,-3.69886421295048,
134.048804238843));
#122258=CARTESIAN_POINT('Ctrl Pts',(-188.598174152404,-3.60554093228053,
134.149395392893));
#122259=CARTESIAN_POINT('Ctrl Pts',(-188.605920485669,-3.51221696271946,
134.249987289485));
#122260=CARTESIAN_POINT('Ctrl Pts',(-188.613666818935,-3.41468070477701,
134.34667013273));
#122261=CARTESIAN_POINT('Ctrl Pts',(-188.6214131522,-3.31330194928639,134.439083888374));
#122262=CARTESIAN_POINT('Ctrl Pts',(-188.629161220203,-3.21190049072653,
134.531518339438));
#122263=CARTESIAN_POINT('Ctrl Pts',(-188.636909288206,-3.10665511120062,
134.619681537175));
#122264=CARTESIAN_POINT('Ctrl Pts',(-188.644657356209,-2.99796983886249,
134.703252756081));
#122265=CARTESIAN_POINT('Ctrl Pts',(-188.652413658951,-2.88916905452341,
134.786912795473));
#122266=CARTESIAN_POINT('Ctrl Pts',(-188.660169961693,-2.77692138462799,
134.865970868193));
#122267=CARTESIAN_POINT('Ctrl Pts',(-188.667926264434,-2.661661546083,134.940148435697));
#122268=CARTESIAN_POINT('Ctrl Pts',(-188.675686706949,-2.54634018989178,
135.014365594003));
#122269=CARTESIAN_POINT('Ctrl Pts',(-188.683447149463,-2.4280037987698,
135.083696859122));
#122270=CARTESIAN_POINT('Ctrl Pts',(-188.691207591977,-2.30711213985166,
135.147909470365));
#122271=CARTESIAN_POINT('Ctrl Pts',(-188.698980492242,-2.18602641491037,
135.212225161391));
#122272=CARTESIAN_POINT('Ctrl Pts',(-188.706753392507,-2.06237757804144,
135.271405609637));
#122273=CARTESIAN_POINT('Ctrl Pts',(-188.714526292773,-1.93664666046133,
135.325265701177));
#122274=CARTESIAN_POINT('Ctrl Pts',(-188.722016628535,-1.81548637842552,
135.377167842728));
#122275=CARTESIAN_POINT('Ctrl Pts',(-188.729506964298,-1.69239305308073,
135.424129618806));
#122276=CARTESIAN_POINT('Ctrl Pts',(-188.73699730006,-1.56780896021745,
135.466029645582));
#122277=CARTESIAN_POINT('Ctrl Pts',(-188.744771634179,-1.43850122361313,
135.509518324605));
#122278=CARTESIAN_POINT('Ctrl Pts',(-188.752545968298,-1.30717783500581,
135.547691603967));
#122279=CARTESIAN_POINT('Ctrl Pts',(-188.760320302418,-1.17431521925618,
135.580359657382));
#122280=CARTESIAN_POINT('Ctrl Pts',(-188.768085055365,-1.04161634480655,
135.612987450341));
#122281=CARTESIAN_POINT('Ctrl Pts',(-188.775849808312,-0.907382393612003,
135.64012342443));
#122282=CARTESIAN_POINT('Ctrl Pts',(-188.783614561259,-0.772107552298939,
135.661626617095));
#122283=CARTESIAN_POINT('Ctrl Pts',(-188.791371602144,-0.636967067865308,
135.683108452486));
#122284=CARTESIAN_POINT('Ctrl Pts',(-188.799128643029,-0.500788134293892,
135.698968578897));
#122285=CARTESIAN_POINT('Ctrl Pts',(-188.806885683914,-0.36407746554492,
135.709116540299));
#122286=CARTESIAN_POINT('Ctrl Pts',(-188.814636875154,-0.227469891374892,
135.719256849044));
#122287=CARTESIAN_POINT('Ctrl Pts',(-188.822388066394,-0.0903317684798211,
135.72369353795));
#122288=CARTESIAN_POINT('Ctrl Pts',(-188.830139257634,0.0468230430825336,
135.722387728628));
#122289=CARTESIAN_POINT('Ctrl Pts',(-188.837887154411,0.183919560191437,
135.721082474309));
#122290=CARTESIAN_POINT('Ctrl Pts',(-188.845635051188,0.321032361730929,
135.714039579871));
#122291=CARTESIAN_POINT('Ctrl Pts',(-188.853382947965,0.457645767564134,
135.70127223755));
#122292=CARTESIAN_POINT('Ctrl Pts',(-188.861129224049,0.594230596817883,
135.688507565881));
#122293=CARTESIAN_POINT('Ctrl Pts',(-188.868875500133,0.730315849125278,
135.670020864439));
#122294=CARTESIAN_POINT('Ctrl Pts',(-188.876621776217,0.865389548668166,
135.645877321199));
#122295=CARTESIAN_POINT('Ctrl Pts',(-188.884368109483,1.0004642452946,135.621733599736));
#122296=CARTESIAN_POINT('Ctrl Pts',(-188.892114442748,1.1345269893911,135.591933021942));
#122297=CARTESIAN_POINT('Ctrl Pts',(-188.899860776013,1.26707499296545,
135.556592096009));
#122298=CARTESIAN_POINT('Ctrl Pts',(-188.907608844016,1.39965267974599,
135.52124325572));
#122299=CARTESIAN_POINT('Ctrl Pts',(-188.915356912019,1.53071457330889,
135.480351699103));
#122300=CARTESIAN_POINT('Ctrl Pts',(-188.923104980022,1.65977245111908,
135.434083986516));
#122301=CARTESIAN_POINT('Ctrl Pts',(-188.930861282764,1.7889674931778,135.387767100054));
#122302=CARTESIAN_POINT('Ctrl Pts',(-188.938617585506,1.91615389617927,
135.336062775758));
#122303=CARTESIAN_POINT('Ctrl Pts',(-188.946373888248,2.04086234265069,
135.279186196385));
#122304=CARTESIAN_POINT('Ctrl Pts',(-188.954134330762,2.16563734977488,
135.222279260269));
#122305=CARTESIAN_POINT('Ctrl Pts',(-188.961894773276,2.2879314166124,135.160194745264));
#122306=CARTESIAN_POINT('Ctrl Pts',(-188.96965521579,2.40730019963481,135.093193653642));
#122307=CARTESIAN_POINT('Ctrl Pts',(-188.977428116055,2.5268606040248,135.02608500592));
#122308=CARTESIAN_POINT('Ctrl Pts',(-188.985201016321,2.64348600783031,
134.954044215384));
#122309=CARTESIAN_POINT('Ctrl Pts',(-188.992973916586,2.75676066034094,
134.877375928622));
#122310=CARTESIAN_POINT('Ctrl Pts',(-189.000464252348,2.86591749391118,
134.803494727199));
#122311=CARTESIAN_POINT('Ctrl Pts',(-189.00795458811,2.97196271521771,134.725316813482));
#122312=CARTESIAN_POINT('Ctrl Pts',(-189.015444923872,3.07455513973725,
134.643148675693));
#122313=CARTESIAN_POINT('Ctrl Pts',(-189.023219257991,3.18103738721459,
134.557865107985));
#122314=CARTESIAN_POINT('Ctrl Pts',(-189.03099359211,3.2841371475586,134.468012611807));
#122315=CARTESIAN_POINT('Ctrl Pts',(-189.038767926229,3.38343719526661,
134.373889411145));
#122316=CARTESIAN_POINT('Ctrl Pts',(-189.046532679176,3.48261486454052,
134.279882208915));
#122317=CARTESIAN_POINT('Ctrl Pts',(-189.054297432124,3.57800185753944,
134.1816150409));
#122318=CARTESIAN_POINT('Ctrl Pts',(-189.062062185071,3.66921245853213,
134.079427486601));
#122319=CARTESIAN_POINT('Ctrl Pts',(-189.069819225956,3.76033246787007,
133.977341426422));
#122320=CARTESIAN_POINT('Ctrl Pts',(-189.077576266841,3.84728408135189,
133.87134301855));
#122321=CARTESIAN_POINT('Ctrl Pts',(-189.085333307726,3.92971730448732,
133.7618096821));
#122322=CARTESIAN_POINT('Ctrl Pts',(-189.093084498966,4.01208836408783,
133.652358945591));
#122323=CARTESIAN_POINT('Ctrl Pts',(-189.100835690206,4.0899475813276,133.539378897572));
#122324=CARTESIAN_POINT('Ctrl Pts',(-189.108586881446,4.16298449280398,
133.423280848343));
#122325=CARTESIAN_POINT('Ctrl Pts',(-189.116334778223,4.23599036164477,
133.307232143882));
#122326=CARTESIAN_POINT('Ctrl Pts',(-189.124082675,4.30417779348807,133.188068404235));
#122327=CARTESIAN_POINT('Ctrl Pts',(-189.131830571777,4.36727914962361,
133.06623061643));
#122328=CARTESIAN_POINT('Ctrl Pts',(-189.139576847861,4.43036730631575,
132.944418314464));
#122329=CARTESIAN_POINT('Ctrl Pts',(-189.147323123945,4.48837132376201,
132.819933423872));
#122330=CARTESIAN_POINT('Ctrl Pts',(-189.15506940003,4.54106931101448,132.6932419201));
#122331=CARTESIAN_POINT('Ctrl Pts',(-189.162815733295,4.59376768727144,
132.56654948112));
#122332=CARTESIAN_POINT('Ctrl Pts',(-189.17056206656,4.64115980502555,132.437650757441));
#122333=CARTESIAN_POINT('Ctrl Pts',(-189.178308399826,4.68307191672785,
132.307031734363));
#122334=CARTESIAN_POINT('Ctrl Pts',(-189.186056467829,4.72499341435691,
132.17638346006));
#122335=CARTESIAN_POINT('Ctrl Pts',(-189.193804535832,4.76143234450105,
132.044014491957));
#122336=CARTESIAN_POINT('Ctrl Pts',(-189.201552603835,4.7922649429027,131.910425615442));
#122337=CARTESIAN_POINT('Ctrl Pts',(-189.209308906576,4.82313031055689,
131.776694759079));
#122338=CARTESIAN_POINT('Ctrl Pts',(-189.217065209318,4.84837735570641,
131.641741785897));
#122339=CARTESIAN_POINT('Ctrl Pts',(-189.22482151206,4.86793344014249,131.506077857516));
#122340=CARTESIAN_POINT('Ctrl Pts',(-189.232581954574,4.8874999622497,131.37034152121));
#122341=CARTESIAN_POINT('Ctrl Pts',(-189.240342397089,4.90136943177558,
131.233893862373));
#122342=CARTESIAN_POINT('Ctrl Pts',(-189.248102839603,4.90952125879313,
131.097249797903));
#122343=CARTESIAN_POINT('Ctrl Pts',(-189.255875739868,4.91768617184709,
130.960386380249));
#122344=CARTESIAN_POINT('Ctrl Pts',(-189.263648640134,4.92011509395886,
130.823326318046));
#122345=CARTESIAN_POINT('Ctrl Pts',(-189.271421540399,4.91683960951637,
130.686584063062));
#122346=CARTESIAN_POINT('Ctrl Pts',(-189.278911876161,4.91368319718378,
130.554812733478));
#122347=CARTESIAN_POINT('Ctrl Pts',(-189.286402211923,4.90522993667453,
130.423336813468));
#122348=CARTESIAN_POINT('Ctrl Pts',(-189.293892547685,4.8915532666416,130.292609015607));
#122349=CARTESIAN_POINT('Ctrl Pts',(-189.301666881805,4.87735804150758,
130.156924633557));
#122350=CARTESIAN_POINT('Ctrl Pts',(-189.309441215924,4.85749053053571,
130.021616416288));
#122351=CARTESIAN_POINT('Ctrl Pts',(-189.317215550043,4.83197611743572,
129.887196584783));
#122352=CARTESIAN_POINT('Ctrl Pts',(-189.32498030299,4.80649314856966,129.752942413707));
#122353=CARTESIAN_POINT('Ctrl Pts',(-189.332745055937,4.77537719672058,
129.619574830376));
#122354=CARTESIAN_POINT('Ctrl Pts',(-189.340509808884,4.73870547096616,
129.487601899374));
#122355=CARTESIAN_POINT('Ctrl Pts',(-189.348266849769,4.70207016808673,
129.355760045747));
#122356=CARTESIAN_POINT('Ctrl Pts',(-189.356023890654,4.6598901765116,129.225310462118));
#122357=CARTESIAN_POINT('Ctrl Pts',(-189.363780931539,4.61229384905882,
129.096751613012));
#122358=CARTESIAN_POINT('Ctrl Pts',(-189.371532122779,4.56473341436676,
128.968289711134));
#122359=CARTESIAN_POINT('Ctrl Pts',(-189.379283314019,4.5117649089419,128.841716070937));
#122360=CARTESIAN_POINT('Ctrl Pts',(-189.387034505259,4.45356656673678,
128.717514217338));
#122361=CARTESIAN_POINT('Ctrl Pts',(-189.394782402037,4.39539296037968,
128.59336515284));
#122362=CARTESIAN_POINT('Ctrl Pts',(-189.402530298814,4.33199410380397,
128.471586223247));
#122363=CARTESIAN_POINT('Ctrl Pts',(-189.410278195591,4.26359634662585,
128.352640964845));
#122364=CARTESIAN_POINT('Ctrl Pts',(-189.418024471675,4.19521289678404,
128.233720587227));
#122365=CARTESIAN_POINT('Ctrl Pts',(-189.425770747759,4.12183282098978,
128.117633040512));
#122366=CARTESIAN_POINT('Ctrl Pts',(-189.433517023843,4.04372822010655,
128.004816878952));
#122367=CARTESIAN_POINT('Ctrl Pts',(-189.441263357108,3.9656230426728,127.891999884608));
#122368=CARTESIAN_POINT('Ctrl Pts',(-189.449009690374,3.88279349310222,
127.782454645051));
#122369=CARTESIAN_POINT('Ctrl Pts',(-189.456756023639,3.7955545297986,127.676590025942));
#122370=CARTESIAN_POINT('Ctrl Pts',(-189.464504091642,3.70829602993413,
127.570701699186));
#122371=CARTESIAN_POINT('Ctrl Pts',(-189.472252159645,3.61662639999776,
127.4684959347));
#122372=CARTESIAN_POINT('Ctrl Pts',(-189.480000227648,3.5209000673159,127.370347545594));
#122373=CARTESIAN_POINT('Ctrl Pts',(-189.48775653039,3.42507199554838,127.272094843212));
#122374=CARTESIAN_POINT('Ctrl Pts',(-189.495512833132,3.32517888174022,
127.17790841068));
#122375=CARTESIAN_POINT('Ctrl Pts',(-189.503269135873,3.22161151791196,
127.08812565592));
#122376=CARTESIAN_POINT('Ctrl Pts',(-189.511029578388,3.11798887706327,
126.998294981402));
#122377=CARTESIAN_POINT('Ctrl Pts',(-189.518790020902,3.01068838434436,
126.912872911365));
#122378=CARTESIAN_POINT('Ctrl Pts',(-189.526550463416,2.90013212456667,
126.832155093861));
#122379=CARTESIAN_POINT('Ctrl Pts',(-189.534323363681,2.78939839006606,
126.751307700949));
#122380=CARTESIAN_POINT('Ctrl Pts',(-189.542096263947,2.67539876972268,
126.675179868487));
#122381=CARTESIAN_POINT('Ctrl Pts',(-189.549869164212,2.55858315851329,
126.604023097381));
#122382=CARTESIAN_POINT('Ctrl Pts',(-189.557359499974,2.44601408901245,
126.535453054138));
#122383=CARTESIAN_POINT('Ctrl Pts',(-189.564849835736,2.33083048013107,
126.471499075371));
#122384=CARTESIAN_POINT('Ctrl Pts',(-189.572340171498,2.21345290716398,
126.412344077266));
#122385=CARTESIAN_POINT('Ctrl Pts',(-189.580114505617,2.0916249278412,126.350946199428));
#122386=CARTESIAN_POINT('Ctrl Pts',(-189.587888839736,1.96704741755451,
126.294523902565));
#122387=CARTESIAN_POINT('Ctrl Pts',(-189.595663173855,1.84016504283681,
126.243332698596));
#122388=CARTESIAN_POINT('Ctrl Pts',(-189.603427926802,1.7134390393065,126.192204583211));
#122389=CARTESIAN_POINT('Ctrl Pts',(-189.61119267975,1.58441418226004,126.146294878277));
#122390=CARTESIAN_POINT('Ctrl Pts',(-189.618957432697,1.45355965421348,
126.105813246927));
#122391=CARTESIAN_POINT('Ctrl Pts',(-189.626714473582,1.3228350927289,126.065371822503));
#122392=CARTESIAN_POINT('Ctrl Pts',(-189.634471514467,1.19028484774728,
126.030347857655));
#122393=CARTESIAN_POINT('Ctrl Pts',(-189.642228555352,1.0563976694256,126.000902797773));
#122394=CARTESIAN_POINT('Ctrl Pts',(-189.649979746592,0.922611456466401,
125.971479942639));
#122395=CARTESIAN_POINT('Ctrl Pts',(-189.657730937832,0.787490697206884,
125.94762770214));
#122396=CARTESIAN_POINT('Ctrl Pts',(-189.665482129072,0.651538534659585,
125.92945748003));
#122397=CARTESIAN_POINT('Ctrl Pts',(-189.673230025849,0.515644155408197,
125.91129498075));
#122398=CARTESIAN_POINT('Ctrl Pts',(-189.680977922626,0.378919462400322,
125.898809748275));
#122399=CARTESIAN_POINT('Ctrl Pts',(-189.688725819403,0.241876789339127,
125.892061900949));
#122400=CARTESIAN_POINT('Ctrl Pts',(-189.696472095488,0.104862782650838,
125.885315465126));
#122401=CARTESIAN_POINT('Ctrl Pts',(-189.704218371572,-0.0324686815449168,
125.884304046529));
#122402=CARTESIAN_POINT('Ctrl Pts',(-189.711964647656,-0.169601557973934,
125.889035768278));
#122403=CARTESIAN_POINT('Ctrl Pts',(-189.719710980921,-0.30673544668688,
125.893767524955));
#122404=CARTESIAN_POINT('Ctrl Pts',(-189.727457314187,-0.443670353975256,
125.904242493092));
#122405=CARTESIAN_POINT('Ctrl Pts',(-189.735203647452,-0.57989204686906,
125.92041669114));
#122406=CARTESIAN_POINT('Ctrl Pts',(-189.742951715455,-0.716144245666308,
125.936594511287));
#122407=CARTESIAN_POINT('Ctrl Pts',(-189.750699783458,-0.851682524082018,
125.958474054952));
#122408=CARTESIAN_POINT('Ctrl Pts',(-189.758447851461,-0.985999964604032,
125.985959728028));
#122409=CARTESIAN_POINT('Ctrl Pts',(-189.766204154203,-1.12046015930041,
126.013474613205));
#122410=CARTESIAN_POINT('Ctrl Pts',(-189.773960456944,-1.25369654052637,
126.046607451556));
#122411=CARTESIAN_POINT('Ctrl Pts',(-189.781716759686,-1.38521400480768,
126.085211835912));
#122412=CARTESIAN_POINT('Ctrl Pts',(-189.7894772022,-1.51680166391959,126.12383682459));
#122413=CARTESIAN_POINT('Ctrl Pts',(-189.797237644715,-1.64666820799493,
126.167939052618));
#122414=CARTESIAN_POINT('Ctrl Pts',(-189.804998087229,-1.77433675280554,
126.217323213081));
#122415=CARTESIAN_POINT('Ctrl Pts',(-189.812770987494,-1.90221024249816,
126.266786649383));
#122416=CARTESIAN_POINT('Ctrl Pts',(-189.82054388776,-2.02787832339203,
126.321548805643));
#122417=CARTESIAN_POINT('Ctrl Pts',(-189.828316788025,-2.1508862214266,
126.38136711486));
#122418=CARTESIAN_POINT('Ctrl Pts',(-189.835807123787,-2.26942247252908,
126.439010877864));
#122419=CARTESIAN_POINT('Ctrl Pts',(-189.843297459549,-2.38548832025277,
126.501349422499));
#122420=CARTESIAN_POINT('Ctrl Pts',(-189.850787795311,-2.49870254081068,
126.568127777524));
#122421=CARTESIAN_POINT('Ctrl Pts',(-189.858563333984,-2.61622751943143,
126.637448793101));
#122422=CARTESIAN_POINT('Ctrl Pts',(-189.866338872658,-2.73105175223908,
126.711774041575));
#122423=CARTESIAN_POINT('Ctrl Pts',(-189.874114411331,-2.84271970669593,
126.790867409441));
#122424=CARTESIAN_POINT('Ctrl Pts',(-189.882266520974,-2.95979576362285,
126.873791285713));
#122425=CARTESIAN_POINT('Ctrl Pts',(-189.890418630616,-3.07340178179484,
126.961956537243));
#122426=CARTESIAN_POINT('Ctrl Pts',(-189.898570740259,-3.18304092391845,
127.055036206534));
#122427=CARTESIAN_POINT('Ctrl Pts',(-189.906326693971,-3.28735209593799,
127.14359262176));
#122428=CARTESIAN_POINT('Ctrl Pts',(-189.914082647682,-3.38807246231964,
127.236596825632));
#122429=CARTESIAN_POINT('Ctrl Pts',(-189.921838601394,-3.48480374559348,
127.333722935929));
#122430=CARTESIAN_POINT('Ctrl Pts',(-189.929589286311,-3.58146931712576,
127.43078306627));
#122431=CARTESIAN_POINT('Ctrl Pts',(-189.937339971229,-3.67415092233515,
127.531959256202));
#122432=CARTESIAN_POINT('Ctrl Pts',(-189.945090656146,-3.7624847314623,
127.636886591151));
#122433=CARTESIAN_POINT('Ctrl Pts',(-189.952837754435,-3.8507776641283,
127.741765370987));
#122434=CARTESIAN_POINT('Ctrl Pts',(-189.960584852723,-3.93472655359425,
127.850391542837));
#122435=CARTESIAN_POINT('Ctrl Pts',(-189.968331951012,-4.01400597908118,
127.962365004902));
#122436=CARTESIAN_POINT('Ctrl Pts',(-189.976077142051,-4.09326588685833,
128.07431090035));
#122437=CARTESIAN_POINT('Ctrl Pts',(-189.983822333091,-4.1678583942436,
128.189602126264));
#122438=CARTESIAN_POINT('Ctrl Pts',(-189.99156752413,-4.23750000942929,
128.307807647452));
#122439=CARTESIAN_POINT('Ctrl Pts',(-189.999314507378,-4.30715773942337,
128.426040520954));
#122440=CARTESIAN_POINT('Ctrl Pts',(-190.007061490626,-4.37186208637682,
128.54718870223));
#122441=CARTESIAN_POINT('Ctrl Pts',(-190.014808473873,-4.43137434301563,
128.67079447269));
#122442=CARTESIAN_POINT('Ctrl Pts',(-190.022556509817,-4.49089468645619,
128.794417039275));
#122443=CARTESIAN_POINT('Ctrl Pts',(-190.030304545761,-4.54522137225773,
128.920497504471));
#122444=CARTESIAN_POINT('Ctrl Pts',(-190.038052581704,-4.59416325289056,
129.04855679359));
#122445=CARTESIAN_POINT('Ctrl Pts',(-190.045805933935,-4.64313871481742,
129.176703950126));
#122446=CARTESIAN_POINT('Ctrl Pts',(-190.053559286166,-4.68672186348919,
129.30683227332));
#122447=CARTESIAN_POINT('Ctrl Pts',(-190.061312638396,-4.72477092847605,
129.438446002399));
#122448=CARTESIAN_POINT('Ctrl Pts',(-190.064130106518,-4.73859746756062,
129.486272732696));
#122449=CARTESIAN_POINT('Ctrl Pts',(-190.066947574639,-4.75169371319282,
129.534295489064));
#122450=CARTESIAN_POINT('Ctrl Pts',(-190.06976504276,-4.76405452823418,
129.582490119309));
#122451=CARTESIAN_POINT('Origin',(213.235140564004,0.,130.804360617566));
#122452=CARTESIAN_POINT('',(-192.165295998532,-4.76405452823416,129.582490119309));
#122453=CARTESIAN_POINT('',(-191.820046567589,-4.76405452823394,129.582490119308));
#122454=CARTESIAN_POINT('',(213.235140564004,-4.76405452823405,129.582490119308));
#122455=CARTESIAN_POINT('',(-190.485140563957,-4.91824868249715,130.800760671037));
#122456=CARTESIAN_POINT('Ctrl Pts',(-190.485140564012,-4.91824868249786,
130.800760672006));
#122457=CARTESIAN_POINT('Ctrl Pts',(-190.492903044254,-4.9183493592558,
130.938305344235));
#122458=CARTESIAN_POINT('Ctrl Pts',(-190.500665524497,-4.91267582439302,
131.075902460375));
#122459=CARTESIAN_POINT('Ctrl Pts',(-190.508428004739,-4.90124163143306,
131.213033509752));
#122460=CARTESIAN_POINT('Ctrl Pts',(-190.516189892968,-4.88980831051287,
131.350154100696));
#122461=CARTESIAN_POINT('Ctrl Pts',(-190.523951781197,-4.87261523719499,
131.486808308646));
#122462=CARTESIAN_POINT('Ctrl Pts',(-190.531713669427,-4.8497279622425,
131.622481485619));
#122463=CARTESIAN_POINT('Ctrl Pts',(-190.539476617656,-4.8268375616964,
131.758173190757));
#122464=CARTESIAN_POINT('Ctrl Pts',(-190.547239565885,-4.7982514760145,
131.892883215297));
#122465=CARTESIAN_POINT('Ctrl Pts',(-190.555002514114,-4.76408655954542,
132.026106219424));
#122466=CARTESIAN_POINT('Ctrl Pts',(-190.562768174686,-4.72990970599202,
132.159375771132));
#122467=CARTESIAN_POINT('Ctrl Pts',(-190.570533835258,-4.69015023823709,
132.291156892345));
#122468=CARTESIAN_POINT('Ctrl Pts',(-190.57829949583,-4.64497503635937,
132.420958889895));
#122469=CARTESIAN_POINT('Ctrl Pts',(-190.586074494797,-4.59974551020291,
132.550916977504));
#122470=CARTESIAN_POINT('Ctrl Pts',(-190.593849493765,-4.54908737022984,
132.678890820855));
#122471=CARTESIAN_POINT('Ctrl Pts',(-190.601624492733,-4.49321610342936,
132.804408644585));
#122472=CARTESIAN_POINT('Ctrl Pts',(-190.609404441072,-4.4373092703673,
132.930006369846));
#122473=CARTESIAN_POINT('Ctrl Pts',(-190.617184389411,-4.37618287100597,
133.053144613246));
#122474=CARTESIAN_POINT('Ctrl Pts',(-190.62496433775,-4.31009818111834,
133.173376601391));
#122475=CARTESIAN_POINT('Ctrl Pts',(-190.632757105409,-4.24390460094357,
133.293806700412));
#122476=CARTESIAN_POINT('Ctrl Pts',(-190.640549873068,-4.17273660894555,
133.411320645231));
#122477=CARTESIAN_POINT('Ctrl Pts',(-190.648342640727,-4.09689905135302,
133.52550030996));
#122478=CARTESIAN_POINT('Ctrl Pts',(-190.654408984015,-4.0378626885938,
133.614384397484));
#122479=CARTESIAN_POINT('Ctrl Pts',(-190.660475327302,-3.97599746982579,
133.701248499452));
#122480=CARTESIAN_POINT('Ctrl Pts',(-190.66654167059,-3.91146342789147,
133.78591003268));
#122481=CARTESIAN_POINT('Ctrl Pts',(-190.674316004709,-3.82875970007991,
133.894408186373));
#122482=CARTESIAN_POINT('Ctrl Pts',(-190.682090338828,-3.74140718917245,
133.999634468692));
#122483=CARTESIAN_POINT('Ctrl Pts',(-190.689864672947,-3.64969402101185,
134.101164617729));
#122484=CARTESIAN_POINT('Ctrl Pts',(-190.697629425894,-3.55809388113412,
134.202569639932));
#122485=CARTESIAN_POINT('Ctrl Pts',(-190.705394178841,-3.46214403645708,
134.300287304914));
#122486=CARTESIAN_POINT('Ctrl Pts',(-190.713158931788,-3.36217471257771,
134.393923859049));
#122487=CARTESIAN_POINT('Ctrl Pts',(-190.720915972673,-3.26230467964042,
134.487467412037));
#122488=CARTESIAN_POINT('Ctrl Pts',(-190.728673013558,-3.15842339566355,
134.576937655122));
#122489=CARTESIAN_POINT('Ctrl Pts',(-190.736430054443,-3.05089977217039,
134.661975637584));
#122490=CARTESIAN_POINT('Ctrl Pts',(-190.744181245683,-2.94345723307797,
134.746949492243));
#122491=CARTESIAN_POINT('Ctrl Pts',(-190.751932436923,-2.83237812705361,
134.827497497584));
#122492=CARTESIAN_POINT('Ctrl Pts',(-190.759683628163,-2.7180661956855,
134.903299409299));
#122493=CARTESIAN_POINT('Ctrl Pts',(-190.76743152494,-2.60380284993743,
134.979069103179));
#122494=CARTESIAN_POINT('Ctrl Pts',(-190.775179421717,-2.48630973685419,
135.050096499908));
#122495=CARTESIAN_POINT('Ctrl Pts',(-190.782927318495,-2.36602129387989,
135.116103455376));
#122496=CARTESIAN_POINT('Ctrl Pts',(-190.790673594579,-2.24575801265473,
135.182096603612));
#122497=CARTESIAN_POINT('Ctrl Pts',(-190.798419870663,-2.12270090711924,
135.243071211466));
#122498=CARTESIAN_POINT('Ctrl Pts',(-190.806166146747,-1.99731049376025,
135.298794269765));
#122499=CARTESIAN_POINT('Ctrl Pts',(-190.813912480012,-1.87191915479789,
135.354517739398));
#122500=CARTESIAN_POINT('Ctrl Pts',(-190.821658813278,-1.74419483091776,
135.404989423349));
#122501=CARTESIAN_POINT('Ctrl Pts',(-190.829405146543,-1.61461919800756,
135.450023961796));
#122502=CARTESIAN_POINT('Ctrl Pts',(-190.837153214546,-1.4850145475326,
135.495068585417));
#122503=CARTESIAN_POINT('Ctrl Pts',(-190.844901282549,-1.35355813227166,
135.534673512303));
#122504=CARTESIAN_POINT('Ctrl Pts',(-190.852649350552,-1.22074762339899,
135.56870299637));
#122505=CARTESIAN_POINT('Ctrl Pts',(-190.860405653294,-1.0877959619372,
135.602768647377));
#122506=CARTESIAN_POINT('Ctrl Pts',(-190.868161956036,-0.953487711347482,
135.631246921252));
#122507=CARTESIAN_POINT('Ctrl Pts',(-190.875918258778,-0.818332142929902,
135.654052934234));
#122508=CARTESIAN_POINT('Ctrl Pts',(-190.883678701292,-0.683104437916002,
135.676871119472));
#122509=CARTESIAN_POINT('Ctrl Pts',(-190.891439143806,-0.54702890166007,
135.694010962518));
#122510=CARTESIAN_POINT('Ctrl Pts',(-190.89919958632,-0.410619808675805,
135.705439522789));
#122511=CARTESIAN_POINT('Ctrl Pts',(-190.906972486586,-0.273991739705651,
135.7168864292));
#122512=CARTESIAN_POINT('Ctrl Pts',(-190.914745386851,-0.137029434847546,
135.722603715419));
#122513=CARTESIAN_POINT('Ctrl Pts',(-190.922518287116,-0.00024795565964834,
135.722610611316));
#122514=CARTESIAN_POINT('Ctrl Pts',(-190.930008622879,0.131561172230973,
135.722617256529));
#122515=CARTESIAN_POINT('Ctrl Pts',(-190.937498958641,0.263202085368852,
135.717321489911));
#122516=CARTESIAN_POINT('Ctrl Pts',(-190.944989294403,0.394220439225914,
135.706785865114));
#122517=CARTESIAN_POINT('Ctrl Pts',(-190.952763628522,0.530206393788766,
135.695850778901));
#122518=CARTESIAN_POINT('Ctrl Pts',(-190.960537962641,0.665952411115588,
135.67923601341));
#122519=CARTESIAN_POINT('Ctrl Pts',(-190.96831229676,0.800945808593782,
135.656954653151));
#122520=CARTESIAN_POINT('Ctrl Pts',(-190.976077049707,0.935772838774291,
135.634700752677));
#122521=CARTESIAN_POINT('Ctrl Pts',(-190.983841802654,1.06984871258484,
135.606794215719));
#122522=CARTESIAN_POINT('Ctrl Pts',(-190.991606555601,1.20266365894648,
135.57330003697));
#122523=CARTESIAN_POINT('Ctrl Pts',(-190.999363596486,1.33534669163104,
135.539839125113));
#122524=CARTESIAN_POINT('Ctrl Pts',(-191.007120637371,1.46677091249836,
135.500801710651));
#122525=CARTESIAN_POINT('Ctrl Pts',(-191.014877678256,1.59643492045341,
135.456304147668));
#122526=CARTESIAN_POINT('Ctrl Pts',(-191.022628869497,1.7260011477716,135.411840140643));
#122527=CARTESIAN_POINT('Ctrl Pts',(-191.030380060737,1.85380943596783,
135.361924307202));
#122528=CARTESIAN_POINT('Ctrl Pts',(-191.038131251977,1.97937212224398,
135.306723226706));
#122529=CARTESIAN_POINT('Ctrl Pts',(-191.045879148754,2.10488144102913,
135.251545608142));
#122530=CARTESIAN_POINT('Ctrl Pts',(-191.053627045531,2.22814669904816,
135.191087367399));
#122531=CARTESIAN_POINT('Ctrl Pts',(-191.061374942308,2.34869906173386,
135.125563665319));
#122532=CARTESIAN_POINT('Ctrl Pts',(-191.069121218392,2.46922620746376,
135.060053669385));
#122533=CARTESIAN_POINT('Ctrl Pts',(-191.076867494477,2.58704124332095,
134.989480506272));
#122534=CARTESIAN_POINT('Ctrl Pts',(-191.084613770561,2.70169921167772,
134.914105674394));
#122535=CARTESIAN_POINT('Ctrl Pts',(-191.092360103826,2.81635802641402,
134.838730286115));
#122536=CARTESIAN_POINT('Ctrl Pts',(-191.100106437091,2.927859400452,134.758553373108));
#122537=CARTESIAN_POINT('Ctrl Pts',(-191.107852770357,3.03578702774157,
134.673879991428));
#122538=CARTESIAN_POINT('Ctrl Pts',(-191.11560083836,3.14373882467452,134.589187647732));
#122539=CARTESIAN_POINT('Ctrl Pts',(-191.123348906363,3.24811497478342,
134.49999707292));
#122540=CARTESIAN_POINT('Ctrl Pts',(-191.131096974365,3.34853226761644,
134.406653597771));
#122541=CARTESIAN_POINT('Ctrl Pts',(-191.138853277107,3.44905628514341,
134.313210916065));
#122542=CARTESIAN_POINT('Ctrl Pts',(-191.146609579849,3.54561275360605,
134.215606783686));
#122543=CARTESIAN_POINT('Ctrl Pts',(-191.154365882591,3.63785498431555,
134.114223783256));
#122544=CARTESIAN_POINT('Ctrl Pts',(-191.162126325105,3.73014644748118,
134.012786671666));
#122545=CARTESIAN_POINT('Ctrl Pts',(-191.16988676762,3.81811883403782,133.907566972984));
#122546=CARTESIAN_POINT('Ctrl Pts',(-191.177647210134,3.9014664522032,133.798979555734));
#122547=CARTESIAN_POINT('Ctrl Pts',(-191.185420110399,3.98494786736428,
133.690217824322));
#122548=CARTESIAN_POINT('Ctrl Pts',(-191.193193010664,4.06378945344856,
133.578077891125));
#122549=CARTESIAN_POINT('Ctrl Pts',(-191.20096591093,4.1377289857357,133.463003486231));
#122550=CARTESIAN_POINT('Ctrl Pts',(-191.208456246692,4.20898062978117,
133.352112325811));
#122551=CARTESIAN_POINT('Ctrl Pts',(-191.215946582454,4.27568028039896,
133.238496606114));
#122552=CARTESIAN_POINT('Ctrl Pts',(-191.223436918216,4.33763498143187,
133.122572391835));
#122553=CARTESIAN_POINT('Ctrl Pts',(-191.231211252335,4.40193871378563,
133.002252875736));
#122554=CARTESIAN_POINT('Ctrl Pts',(-191.238985586454,4.46133427916974,
132.879065220246));
#122555=CARTESIAN_POINT('Ctrl Pts',(-191.246759920573,4.51555556847681,
132.753447832264));
#122556=CARTESIAN_POINT('Ctrl Pts',(-191.25452467352,4.56971003489071,132.627985256485));
#122557=CARTESIAN_POINT('Ctrl Pts',(-191.262289426467,4.61870275977333,
132.500099261741));
#122558=CARTESIAN_POINT('Ctrl Pts',(-191.270054179414,4.66231288128167,
132.370253864098));
#122559=CARTESIAN_POINT('Ctrl Pts',(-191.277811220299,4.70587968860265,
132.240537430734));
#122560=CARTESIAN_POINT('Ctrl Pts',(-191.285568261184,4.74407440781323,
132.108865835533));
#122561=CARTESIAN_POINT('Ctrl Pts',(-191.293325302069,4.77672391135812,
131.975723813658));
#122562=CARTESIAN_POINT('Ctrl Pts',(-191.301076493309,4.80934879365846,
131.842682195218));
#122563=CARTESIAN_POINT('Ctrl Pts',(-191.30882768455,4.83643669095588,131.708172735403));
#122564=CARTESIAN_POINT('Ctrl Pts',(-191.31657887579,4.85786415753015,131.572695758949));
#122565=CARTESIAN_POINT('Ctrl Pts',(-191.324326772567,4.87928251685945,
131.437276363824));
#122566=CARTESIAN_POINT('Ctrl Pts',(-191.332074669344,4.89504516953697,
131.300890655304));
#122567=CARTESIAN_POINT('Ctrl Pts',(-191.339822566121,4.9050797199358,131.164049376877));
#122568=CARTESIAN_POINT('Ctrl Pts',(-191.347568842205,4.91511217132304,
131.027236722695));
#122569=CARTESIAN_POINT('Ctrl Pts',(-191.355315118289,4.91941887513359,
130.889969077825));
#122570=CARTESIAN_POINT('Ctrl Pts',(-191.363061394373,4.91797932692134,
130.752762144001));
#122571=CARTESIAN_POINT('Ctrl Pts',(-191.370807727638,4.91653976808269,
130.615554197346));
#122572=CARTESIAN_POINT('Ctrl Pts',(-191.378554060904,4.90935387668189,
130.478407353576));
#122573=CARTESIAN_POINT('Ctrl Pts',(-191.386300394169,4.89645328142879,
130.341836753008));
#122574=CARTESIAN_POINT('Ctrl Pts',(-191.394048462172,4.88354979717682,
130.205235568402));
#122575=CARTESIAN_POINT('Ctrl Pts',(-191.401796530175,4.86492909924203,
130.069211272942));
#122576=CARTESIAN_POINT('Ctrl Pts',(-191.409544598178,4.84067458957936,
129.934272932157));
#122577=CARTESIAN_POINT('Ctrl Pts',(-191.41730090092,4.81639430193517,129.799191177297));
#122578=CARTESIAN_POINT('Ctrl Pts',(-191.425057203662,4.78646831079896,
129.665198068094));
#122579=CARTESIAN_POINT('Ctrl Pts',(-191.432813506404,4.75103110006152,
129.532792078812));
#122580=CARTESIAN_POINT('Ctrl Pts',(-191.440573948918,4.71557497541762,
129.400315420467));
#122581=CARTESIAN_POINT('Ctrl Pts',(-191.448334391432,4.67460188671874,
129.269427942878));
#122582=CARTESIAN_POINT('Ctrl Pts',(-191.456094833946,4.6282956407281,129.14061107977));
#122583=CARTESIAN_POINT('Ctrl Pts',(-191.463867734212,4.58191505984064,
129.011587428397));
#122584=CARTESIAN_POINT('Ctrl Pts',(-191.471640634477,4.53018436116495,
128.884641396051));
#122585=CARTESIAN_POINT('Ctrl Pts',(-191.479413534742,4.47333512852615,
128.760233446768));
#122586=CARTESIAN_POINT('Ctrl Pts',(-191.486903870504,4.41855250868881,
128.640348039807));
#122587=CARTESIAN_POINT('Ctrl Pts',(-191.494394206266,4.35901717633166,
128.522819662996));
#122588=CARTESIAN_POINT('Ctrl Pts',(-191.501884542028,4.29497488095036,
128.408035548944));
#122589=CARTESIAN_POINT('Ctrl Pts',(-191.509658876147,4.22850440247415,
128.28889936032));
#122590=CARTESIAN_POINT('Ctrl Pts',(-191.517433210267,4.15696789296251,
128.172342252175));
#122591=CARTESIAN_POINT('Ctrl Pts',(-191.525207544386,4.08059035808282,
128.058825079275));
#122592=CARTESIAN_POINT('Ctrl Pts',(-191.532972297333,4.0043069516886,127.945447806144));
#122593=CARTESIAN_POINT('Ctrl Pts',(-191.54073705028,3.92319460690395,127.835103335206));
#122594=CARTESIAN_POINT('Ctrl Pts',(-191.548501803227,3.83752433236579,
127.728228295802));
#122595=CARTESIAN_POINT('Ctrl Pts',(-191.556258844112,3.75193914675227,
127.621459406194));
#122596=CARTESIAN_POINT('Ctrl Pts',(-191.564015884997,3.6618052832676,127.518153393728));
#122597=CARTESIAN_POINT('Ctrl Pts',(-191.571772925882,3.5674369836618,127.418717926717));
#122598=CARTESIAN_POINT('Ctrl Pts',(-191.579524117122,3.47313984792494,
127.319357444764));
#122599=CARTESIAN_POINT('Ctrl Pts',(-191.587275308362,3.37461490002521,
127.223861980993));
#122600=CARTESIAN_POINT('Ctrl Pts',(-191.595026499602,3.27221635190649,
127.132605831525));
#122601=CARTESIAN_POINT('Ctrl Pts',(-191.602774396379,3.16986132590188,
127.041388468354));
#122602=CARTESIAN_POINT('Ctrl Pts',(-191.610522293156,3.06363626547616,
126.954407095373));
#122603=CARTESIAN_POINT('Ctrl Pts',(-191.618270189933,2.95393174198714,
126.871998690406));
#122604=CARTESIAN_POINT('Ctrl Pts',(-191.626016466018,2.84425016631949,
126.789607523499));
#122605=CARTESIAN_POINT('Ctrl Pts',(-191.633762742102,2.73109088767587,
126.711787656611));
#122606=CARTESIAN_POINT('Ctrl Pts',(-191.641509018186,2.61487669737603,
126.638835090094));
#122607=CARTESIAN_POINT('Ctrl Pts',(-191.649255351451,2.49866164920991,
126.565881985059));
#122608=CARTESIAN_POINT('Ctrl Pts',(-191.657001684716,2.37939197551846,
126.497796459953));
#122609=CARTESIAN_POINT('Ctrl Pts',(-191.664748017982,2.25751817453226,
126.434830350574));
#122610=CARTESIAN_POINT('Ctrl Pts',(-191.672496085985,2.1356170807535,126.371850140372));
#122611=CARTESIAN_POINT('Ctrl Pts',(-191.680244153988,2.01111104650626,
126.313991806636));
#122612=CARTESIAN_POINT('Ctrl Pts',(-191.687992221991,1.88447344383008,
126.261460343292));
#122613=CARTESIAN_POINT('Ctrl Pts',(-191.695748524732,1.75770124920225,
126.208873048883));
#122614=CARTESIAN_POINT('Ctrl Pts',(-191.703504827474,1.62879332235594,
126.161624084286));
#122615=CARTESIAN_POINT('Ctrl Pts',(-191.711261130216,1.49824173563579,
126.119869741911));
#122616=CARTESIAN_POINT('Ctrl Pts',(-191.71902157273,1.36762046960263,126.078093113985));
#122617=CARTESIAN_POINT('Ctrl Pts',(-191.726782015244,1.23535417251634,
126.041817055184));
#122618=CARTESIAN_POINT('Ctrl Pts',(-191.734542457759,1.10194724024969,
126.01114715036));
#122619=CARTESIAN_POINT('Ctrl Pts',(-191.742315358024,0.968326151332061,
125.980428011482));
#122620=CARTESIAN_POINT('Ctrl Pts',(-191.750088258289,0.833561152794384,
125.955333082055));
#122621=CARTESIAN_POINT('Ctrl Pts',(-191.757861158555,0.698164822785404,
125.935916416106));
#122622=CARTESIAN_POINT('Ctrl Pts',(-191.765351494317,0.567690490411714,
125.917205594873));
#122623=CARTESIAN_POINT('Ctrl Pts',(-191.772841830079,0.436630237048816,
125.903767397656));
#122624=CARTESIAN_POINT('Ctrl Pts',(-191.780332165842,0.305442686064309,
125.895604377129));
#122625=CARTESIAN_POINT('Ctrl Pts',(-191.788106499961,0.169281119213901,
125.887131853198));
#122626=CARTESIAN_POINT('Ctrl Pts',(-191.79588083408,0.0325510922944527,
125.884315580651));
#122627=CARTESIAN_POINT('Ctrl Pts',(-191.803655168199,-0.104238043468105,
125.887215359106));
#122628=CARTESIAN_POINT('Ctrl Pts',(-191.811419921146,-0.240858598845289,
125.890111563843));
#122629=CARTESIAN_POINT('Ctrl Pts',(-191.819184674093,-0.377537730998018,
125.898709794876));
#122630=CARTESIAN_POINT('Ctrl Pts',(-191.82694942704,-0.513761604507242,
125.913018053787));
#122631=CARTESIAN_POINT('Ctrl Pts',(-191.834706467925,-0.649850178545986,
125.927312101534));
#122632=CARTESIAN_POINT('Ctrl Pts',(-191.84246350881,-0.785484007468369,
125.94730485048));
#122633=CARTESIAN_POINT('Ctrl Pts',(-191.850220549695,-0.920150253035749,
125.972952274822));
#122634=CARTESIAN_POINT('Ctrl Pts',(-191.857971740935,-1.05471494573815,
125.998580358241));
#122635=CARTESIAN_POINT('Ctrl Pts',(-191.865722932175,-1.18831312492588,
126.029854556506));
#122636=CARTESIAN_POINT('Ctrl Pts',(-191.873474123415,-1.32043842446319,
126.066679177273));
#122637=CARTESIAN_POINT('Ctrl Pts',(-191.881222020193,-1.4525075672249,
126.103488146594));
#122638=CARTESIAN_POINT('Ctrl Pts',(-191.88896991697,-1.58310469960573,
126.145842741646));
#122639=CARTESIAN_POINT('Ctrl Pts',(-191.896717813747,-1.71173519926051,
126.193596508428));
#122640=CARTESIAN_POINT('Ctrl Pts',(-191.904464089831,-1.84033879218771,
126.241340286152));
#122641=CARTESIAN_POINT('Ctrl Pts',(-191.912210365915,-1.96697620435051,
126.294480853203));
#122642=CARTESIAN_POINT('Ctrl Pts',(-191.919956641999,-2.09116987323163,
126.352822498692));
#122643=CARTESIAN_POINT('Ctrl Pts',(-191.927702975264,-2.21536445888204,
126.411164574845));
#122644=CARTESIAN_POINT('Ctrl Pts',(-191.93544930853,-2.33711491138994,
126.474707639814));
#122645=CARTESIAN_POINT('Ctrl Pts',(-191.943195641795,-2.45596584886988,
126.543208800078));
#122646=CARTESIAN_POINT('Ctrl Pts',(-191.950943709798,-2.57484340219369,
126.611725300701));
#122647=CARTESIAN_POINT('Ctrl Pts',(-191.958691777801,-2.69081980973953,
126.685201910856));
#122648=CARTESIAN_POINT('Ctrl Pts',(-191.966439845804,-2.80346673516209,
126.763351173462));
#122649=CARTESIAN_POINT('Ctrl Pts',(-191.974196148546,-2.91623338307735,
126.841583494034));
#122650=CARTESIAN_POINT('Ctrl Pts',(-191.981952451288,-3.02566315836508,
126.924498164268));
#122651=CARTESIAN_POINT('Ctrl Pts',(-191.98970875403,-3.13135859067244,
127.011765669628));
#122652=CARTESIAN_POINT('Ctrl Pts',(-191.997469196544,-3.23711043581445,
127.099079752284));
#122653=CARTESIAN_POINT('Ctrl Pts',(-192.005229639058,-3.33912367583414,
127.190751038126));
#122654=CARTESIAN_POINT('Ctrl Pts',(-192.012990081572,-3.43703684091518,
127.286412235811));
#122655=CARTESIAN_POINT('Ctrl Pts',(-192.020762981838,-3.53510718490086,
127.382226997343));
#122656=CARTESIAN_POINT('Ctrl Pts',(-192.028535882103,-3.62906403328069,
127.482044185023));
#122657=CARTESIAN_POINT('Ctrl Pts',(-192.036308782368,-3.71858484786014,
127.58546176986));
#122658=CARTESIAN_POINT('Ctrl Pts',(-192.04379911813,-3.80485135533908,
127.685119864993));
#122659=CARTESIAN_POINT('Ctrl Pts',(-192.051289453892,-3.88699855951138,
127.78812089412));
#122660=CARTESIAN_POINT('Ctrl Pts',(-192.058779789654,-3.9647764156074,
127.894080384196));
#122661=CARTESIAN_POINT('Ctrl Pts',(-192.066605571333,-4.04603746191827,
128.004785145967));
#122662=CARTESIAN_POINT('Ctrl Pts',(-192.074431353011,-4.12278666815336,
128.119070688909));
#122663=CARTESIAN_POINT('Ctrl Pts',(-192.08225713469,-4.19469433982913,
128.236536157463));
#122664=CARTESIAN_POINT('Ctrl Pts',(-192.090069792819,-4.26648142497111,
128.353804640724));
#122665=CARTESIAN_POINT('Ctrl Pts',(-192.097882450948,-4.33344294894402,
128.474242102797));
#122666=CARTESIAN_POINT('Ctrl Pts',(-192.105695109077,-4.3952906467389,
128.597416306264));
#122667=CARTESIAN_POINT('Ctrl Pts',(-192.113500201717,-4.4570784535094,
128.720471232385));
#122668=CARTESIAN_POINT('Ctrl Pts',(-192.121305294356,-4.51376211373051,
128.846257287088));
#122669=CARTESIAN_POINT('Ctrl Pts',(-192.129110386996,-4.5650974649776,
128.974314662472));
#122670=CARTESIAN_POINT('Ctrl Pts',(-192.136908171869,-4.61638475186583,
129.102252140057));
#122671=CARTESIAN_POINT('Ctrl Pts',(-192.144705956742,-4.66233355954381,
129.232456348203));
#122672=CARTESIAN_POINT('Ctrl Pts',(-192.152503741615,-4.70274661817135,
129.364444888164));
#122673=CARTESIAN_POINT('Ctrl Pts',(-192.156767827254,-4.72484580989491,
129.436620569713));
#122674=CARTESIAN_POINT('Ctrl Pts',(-192.161031912893,-4.7452904916293,
129.50932942537));
#122675=CARTESIAN_POINT('Ctrl Pts',(-192.165295998532,-4.76405452823416,
129.582490119309));
#122676=CARTESIAN_POINT('Ctrl Pts',(-190.415359814329,-4.76405452823405,
129.582490119308));
#122677=CARTESIAN_POINT('Ctrl Pts',(-190.424329050674,-4.80323055054687,
129.735236835727));
#122678=CARTESIAN_POINT('Ctrl Pts',(-190.433298287018,-4.83509936457335,
129.890036533855));
#122679=CARTESIAN_POINT('Ctrl Pts',(-190.442267523362,-4.85946771299443,
130.04623357751));
#122680=CARTESIAN_POINT('Ctrl Pts',(-190.451168803988,-4.88365143381179,
130.201247189058));
#122681=CARTESIAN_POINT('Ctrl Pts',(-190.460070084614,-4.9004478339706,
130.357636916376));
#122682=CARTESIAN_POINT('Ctrl Pts',(-190.46897136524,-4.90971529438901,
130.51474226431));
#122683=CARTESIAN_POINT('Ctrl Pts',(-190.474361098146,-4.9153267494672,
130.609869684625));
#122684=CARTESIAN_POINT('Ctrl Pts',(-190.479750831051,-4.9181787794553,
130.705259101589));
#122685=CARTESIAN_POINT('Ctrl Pts',(-190.485140563957,-4.91824868249715,
130.800760671037));
#122686=CARTESIAN_POINT('',(-190.13985943604,-4.91824986400714,130.803204030469));
#122687=CARTESIAN_POINT('Ctrl Pts',(-190.06976504276,-4.76405452823418,
129.582490119309));
#122688=CARTESIAN_POINT('Ctrl Pts',(-190.077527632497,-4.79811061399697,
129.715274280825));
#122689=CARTESIAN_POINT('Ctrl Pts',(-190.085290222234,-4.82658033576797,
129.849363494492));
#122690=CARTESIAN_POINT('Ctrl Pts',(-190.093052811971,-4.84939154448578,
129.984247996782));
#122691=CARTESIAN_POINT('Ctrl Pts',(-190.100826943755,-4.87223667075837,
130.119333056286));
#122692=CARTESIAN_POINT('Ctrl Pts',(-190.10860107554,-4.88940643253583,
130.255215378942));
#122693=CARTESIAN_POINT('Ctrl Pts',(-190.116375207325,-4.90088061235472,
130.391380852994));
#122694=CARTESIAN_POINT('Ctrl Pts',(-190.120661944591,-4.90720759465933,
130.466463914131));
#122695=CARTESIAN_POINT('Ctrl Pts',(-190.124948681858,-4.91180373898945,
130.541633066273));
#122696=CARTESIAN_POINT('Ctrl Pts',(-190.129235419125,-4.91467242218679,
130.616802506313));
#122697=CARTESIAN_POINT('Ctrl Pts',(-190.132776758081,-4.91704228507516,
130.678901125798));
#122698=CARTESIAN_POINT('Ctrl Pts',(-190.136318097038,-4.91823524652186,
130.741044945587));
#122699=CARTESIAN_POINT('Ctrl Pts',(-190.139859435995,-4.91824986400696,
130.803204029673));
#122700=CARTESIAN_POINT('Ctrl Pts',(-190.13985943604,-4.91824986400714,
130.803204030469));
#122701=CARTESIAN_POINT('Ctrl Pts',(-190.147585601233,-4.91828175505972,
130.938816960416));
#122702=CARTESIAN_POINT('Ctrl Pts',(-190.155311766426,-4.91270043226599,
131.074655996844));
#122703=CARTESIAN_POINT('Ctrl Pts',(-190.163037931618,-4.90147587807679,
131.210214383264));
#122704=CARTESIAN_POINT('Ctrl Pts',(-190.170754697744,-4.89026497882958,
131.345607859624));
#122705=CARTESIAN_POINT('Ctrl Pts',(-190.178471463869,-4.87342453696202,
131.48072097409));
#122706=CARTESIAN_POINT('Ctrl Pts',(-190.186188229995,-4.85097651155595,
131.615045480403));
#122707=CARTESIAN_POINT('Ctrl Pts',(-190.193897512807,-4.82855025506256,
131.749239725884));
#122708=CARTESIAN_POINT('Ctrl Pts',(-190.201606795619,-4.80052729930736,
131.882646496431));
#122709=CARTESIAN_POINT('Ctrl Pts',(-190.209316078432,-4.76698148662643,
132.014761612551));
#122710=CARTESIAN_POINT('Ctrl Pts',(-190.217019786611,-4.73345993114099,
132.14678119537));
#122711=CARTESIAN_POINT('Ctrl Pts',(-190.224723494791,-4.69442356335619,
132.277510599873));
#122712=CARTESIAN_POINT('Ctrl Pts',(-190.232427202971,-4.6499974110266,
132.406455227739));
#122713=CARTESIAN_POINT('Ctrl Pts',(-190.240128016859,-4.60558794964859,
132.535351410974));
#122714=CARTESIAN_POINT('Ctrl Pts',(-190.247828830748,-4.55579285811654,
132.662463776619));
#122715=CARTESIAN_POINT('Ctrl Pts',(-190.255529644636,-4.50078711110052,
132.787312569342));
#122716=CARTESIAN_POINT('Ctrl Pts',(-190.263229171694,-4.44579055572119,
132.912140499431));
#122717=CARTESIAN_POINT('Ctrl Pts',(-190.270928698752,-4.38558523610426,
133.034705246309));
#122718=CARTESIAN_POINT('Ctrl Pts',(-190.27862822581,-4.32039420672799,
133.1545471976));
#122719=CARTESIAN_POINT('Ctrl Pts',(-190.286328185659,-4.25519951295482,
133.274395885223));
#122720=CARTESIAN_POINT('Ctrl Pts',(-190.294028145508,-4.18501874133744,
133.391521124698));
#122721=CARTESIAN_POINT('Ctrl Pts',(-190.301728105358,-4.1101205931154,
133.505488488021));
#122722=CARTESIAN_POINT('Ctrl Pts',(-190.309430217604,-4.03520150834462,
133.619487709051));
#122723=CARTESIAN_POINT('Ctrl Pts',(-190.317132329851,-3.95556264143853,
133.73032696698));
#122724=CARTESIAN_POINT('Ctrl Pts',(-190.324834442098,-3.87151536636673,
133.837601760384));
#122725=CARTESIAN_POINT('Ctrl Pts',(-190.332544856977,-3.78737749100206,
133.944992192609));
#122726=CARTESIAN_POINT('Ctrl Pts',(-190.340255271856,-3.69882196354237,
134.048810176041));
#122727=CARTESIAN_POINT('Ctrl Pts',(-190.347965686736,-3.60619996799212,
134.148684892117));
#122728=CARTESIAN_POINT('Ctrl Pts',(-190.3556806963,-3.51352277841163,134.248619124166));
#122729=CARTESIAN_POINT('Ctrl Pts',(-190.363395705863,-3.41677457553636,
134.344605130585));
#122730=CARTESIAN_POINT('Ctrl Pts',(-190.371110715427,-3.31634172458628,
134.43631059358));
#122731=CARTESIAN_POINT('Ctrl Pts',(-190.378837231148,-3.21575908819369,
134.528152826001));
#122732=CARTESIAN_POINT('Ctrl Pts',(-190.386563746869,-3.11148113317161,
134.615701512883));
#122733=CARTESIAN_POINT('Ctrl Pts',(-190.394290262589,-3.00392586603647,
134.698665748633));
#122734=CARTESIAN_POINT('Ctrl Pts',(-190.398754522705,-2.94178211240861,
134.746601188372));
#122735=CARTESIAN_POINT('Ctrl Pts',(-190.403218782821,-2.87854480706385,
134.793006993218));
#122736=CARTESIAN_POINT('Ctrl Pts',(-190.407683042937,-2.81429844266184,
134.837833976612));
#122737=CARTESIAN_POINT('Ctrl Pts',(-190.415457377056,-2.70241591570069,
134.915898412238));
#122738=CARTESIAN_POINT('Ctrl Pts',(-190.423231711176,-2.58710562699183,
134.989427787118));
#122739=CARTESIAN_POINT('Ctrl Pts',(-190.431006045295,-2.46877148506654,
135.058106075045));
#122740=CARTESIAN_POINT('Ctrl Pts',(-190.438770798242,-2.35058317939566,
135.126699723119));
#122741=CARTESIAN_POINT('Ctrl Pts',(-190.446535551189,-2.2293787702848,
135.19045398537));
#122742=CARTESIAN_POINT('Ctrl Pts',(-190.454300304136,-2.1055929402831,
135.249094741485));
#122743=CARTESIAN_POINT('Ctrl Pts',(-190.462057345021,-1.98193005611249,
135.307677254775));
#122744=CARTESIAN_POINT('Ctrl Pts',(-190.469814385906,-1.85569120437271,
135.361156202688));
#122745=CARTESIAN_POINT('Ctrl Pts',(-190.477571426791,-1.72733727952841,
135.409302417986));
#122746=CARTESIAN_POINT('Ctrl Pts',(-190.485322618031,-1.59908014737782,
135.457412325848));
#122747=CARTESIAN_POINT('Ctrl Pts',(-190.493073809271,-1.46871148143803,
135.500197368803));
#122748=CARTESIAN_POINT('Ctrl Pts',(-190.500825000511,-1.3367135244881,
135.537475872443));
#122749=CARTESIAN_POINT('Ctrl Pts',(-190.508572897288,-1.2047716701905,
135.574738531725));
#122750=CARTESIAN_POINT('Ctrl Pts',(-190.516320794066,-1.07120227765744,
135.606499200586));
#122751=CARTESIAN_POINT('Ctrl Pts',(-190.524068690843,-0.9365039649583,
135.632625666848));
#122752=CARTESIAN_POINT('Ctrl Pts',(-190.531814966927,-0.80183382824242,
135.658746668017));
#122753=CARTESIAN_POINT('Ctrl Pts',(-190.539561243011,-0.666035624636225,
135.679235736398));
#122754=CARTESIAN_POINT('Ctrl Pts',(-190.547307519095,-0.529619024550856,
135.69401160218));
#122755=CARTESIAN_POINT('Ctrl Pts',(-190.55505385236,-0.39320141746932,
135.708787577034));
#122756=CARTESIAN_POINT('Ctrl Pts',(-190.562800185626,-0.25616579349155,
135.717850223034));
#122757=CARTESIAN_POINT('Ctrl Pts',(-190.570546518891,-0.119027422925699,
135.721170104936));
#122758=CARTESIAN_POINT('Ctrl Pts',(-190.578294586894,0.0181416588272017,
135.724490730303));
#122759=CARTESIAN_POINT('Ctrl Pts',(-190.586042654897,0.155413142178313,
135.722066023016));
#122760=CARTESIAN_POINT('Ctrl Pts',(-190.5937907229,0.292271674219316,135.713918676185));
#122761=CARTESIAN_POINT('Ctrl Pts',(-190.601547025642,0.429275661136996,
135.705762670257));
#122762=CARTESIAN_POINT('Ctrl Pts',(-190.609303328384,0.565865429118824,
135.691871898426));
#122763=CARTESIAN_POINT('Ctrl Pts',(-190.617059631125,0.70153010916397,
135.672321029118));
#122764=CARTESIAN_POINT('Ctrl Pts',(-190.62482007364,0.837267197534009,
135.652759724922));
#122765=CARTESIAN_POINT('Ctrl Pts',(-190.632580516154,0.972077830027677,
135.627532375601));
#122766=CARTESIAN_POINT('Ctrl Pts',(-190.640340958668,1.1054622334498,135.596764639862));
#122767=CARTESIAN_POINT('Ctrl Pts',(-190.648113858933,1.23906075735725,
135.565947513022));
#122768=CARTESIAN_POINT('Ctrl Pts',(-190.655886759199,1.37122809985715,
135.529572330681));
#122769=CARTESIAN_POINT('Ctrl Pts',(-190.663659659464,1.50147966778053,
135.487814670905));
#122770=CARTESIAN_POINT('Ctrl Pts',(-190.671149995226,1.62699626312459,
135.447575007244));
#122771=CARTESIAN_POINT('Ctrl Pts',(-190.678640330988,1.75073366284605,
135.402337511017));
#122772=CARTESIAN_POINT('Ctrl Pts',(-190.68613066675,1.8722783195407,135.352300476082));
#122773=CARTESIAN_POINT('Ctrl Pts',(-190.693905000869,1.99843137883754,
135.300366271758));
#122774=CARTESIAN_POINT('Ctrl Pts',(-190.701679334988,2.12262175204157,
135.243096883288));
#122775=CARTESIAN_POINT('Ctrl Pts',(-190.709453669107,2.24436523492668,
135.180661310475));
#122776=CARTESIAN_POINT('Ctrl Pts',(-190.717218422054,2.36595867984999,
135.118302683924));
#122777=CARTESIAN_POINT('Ctrl Pts',(-190.724983175001,2.48511089000259,
135.050790717883));
#122778=CARTESIAN_POINT('Ctrl Pts',(-190.732747927949,2.6013562836682,134.978342954366));
#122779=CARTESIAN_POINT('Ctrl Pts',(-190.740504968834,2.71748622077004,
134.90596714699));
#122780=CARTESIAN_POINT('Ctrl Pts',(-190.748262009719,2.83071475717223,
134.828665503394));
#122781=CARTESIAN_POINT('Ctrl Pts',(-190.756019050603,2.94059996327127,
134.746701916656));
#122782=CARTESIAN_POINT('Ctrl Pts',(-190.763770241844,3.05040230408146,
134.664800139296));
#122783=CARTESIAN_POINT('Ctrl Pts',(-190.771521433084,3.15686602082719,
134.578243649209));
#122784=CARTESIAN_POINT('Ctrl Pts',(-190.779272624324,3.25957760168308,
134.487339971446));
#122785=CARTESIAN_POINT('Ctrl Pts',(-190.787020521101,3.36224552737705,
134.396474930171));
#122786=CARTESIAN_POINT('Ctrl Pts',(-190.794768417878,3.46116419687574,
134.301266634669));
#122787=CARTESIAN_POINT('Ctrl Pts',(-190.802516314655,3.55595286108516,
134.20206312253));
#122788=CARTESIAN_POINT('Ctrl Pts',(-190.810262590739,3.65072169754968,
134.102880361628));
#122789=CARTESIAN_POINT('Ctrl Pts',(-190.818008866823,3.74136197716383,
133.999704328862));
#122790=CARTESIAN_POINT('Ctrl Pts',(-190.825755142907,3.82752983602749,
133.892919896068));
#122791=CARTESIAN_POINT('Ctrl Pts',(-190.833501476173,3.91369833096282,
133.786134675015));
#122792=CARTESIAN_POINT('Ctrl Pts',(-190.841247809438,3.99539409375177,
133.675741305042));
#122793=CARTESIAN_POINT('Ctrl Pts',(-190.848994142703,4.07231384350195,
133.562157387185));
#122794=CARTESIAN_POINT('Ctrl Pts',(-190.856742210706,4.14925081889687,
133.448548032997));
#122795=CARTESIAN_POINT('Ctrl Pts',(-190.864490278709,4.2214094337795,133.331747032808));
#122796=CARTESIAN_POINT('Ctrl Pts',(-190.872238346712,4.28853021966979,
133.212200233794));
#122797=CARTESIAN_POINT('Ctrl Pts',(-190.879994649454,4.3557223423298,133.092526379021));
#122798=CARTESIAN_POINT('Ctrl Pts',(-190.887750952196,4.41786574856622,
132.970101237319));
#122799=CARTESIAN_POINT('Ctrl Pts',(-190.895507254938,4.47474712186675,
132.845394977356));
#122800=CARTESIAN_POINT('Ctrl Pts',(-190.903267697452,4.53165885446903,
132.720622157908));
#122801=CARTESIAN_POINT('Ctrl Pts',(-190.911028139966,4.5833028108051,132.593566156235));
#122802=CARTESIAN_POINT('Ctrl Pts',(-190.91878858248,4.62951457148501,132.464715367283));
#122803=CARTESIAN_POINT('Ctrl Pts',(-190.926561482746,4.67580051538552,
132.335657735606));
#122804=CARTESIAN_POINT('Ctrl Pts',(-190.934334383011,4.71663672127184,
132.204799932619));
#122805=CARTESIAN_POINT('Ctrl Pts',(-190.942107283277,4.75190897349856,
132.072644564513));
#122806=CARTESIAN_POINT('Ctrl Pts',(-190.949597619039,4.78589899051188,
131.945293376915));
#122807=CARTESIAN_POINT('Ctrl Pts',(-190.957087954801,4.81472249074796,
131.816737626403));
#122808=CARTESIAN_POINT('Ctrl Pts',(-190.964578290563,4.83832277197152,
131.687432424795));
#122809=CARTESIAN_POINT('Ctrl Pts',(-190.972352624682,4.86281786503052,
131.553224577167));
#122810=CARTESIAN_POINT('Ctrl Pts',(-190.980126958801,4.88176343679289,
131.417784195585));
#122811=CARTESIAN_POINT('Ctrl Pts',(-190.98790129292,4.89503994736683,131.281610003299));
#122812=CARTESIAN_POINT('Ctrl Pts',(-190.995666045867,4.90830009582805,
131.145603633535));
#122813=CARTESIAN_POINT('Ctrl Pts',(-191.003430798814,4.91590504680117,
131.008865637851));
#122814=CARTESIAN_POINT('Ctrl Pts',(-191.011195551762,4.91778616625509,
130.871905310104));
#122815=CARTESIAN_POINT('Ctrl Pts',(-191.018952592647,4.91966541735466,
130.735081013285));
#122816=CARTESIAN_POINT('Ctrl Pts',(-191.026709633532,4.9158321449874,130.59803521225));
#122817=CARTESIAN_POINT('Ctrl Pts',(-191.034466674417,4.90626949612716,
130.461282355544));
#122818=CARTESIAN_POINT('Ctrl Pts',(-191.042217865657,4.89671405853478,
130.324632625231));
#122819=CARTESIAN_POINT('Ctrl Pts',(-191.049969056897,4.88143787143859,
130.18827578797));
#122820=CARTESIAN_POINT('Ctrl Pts',(-191.057720248137,4.86047615113323,
130.052725967776));
#122821=CARTESIAN_POINT('Ctrl Pts',(-191.065468144914,4.83952334011826,
129.917233759872));
#122822=CARTESIAN_POINT('Ctrl Pts',(-191.073216041691,4.81288986175936,
129.782548272388));
#122823=CARTESIAN_POINT('Ctrl Pts',(-191.080963938468,4.78066272575466,
129.649177963143));
#122824=CARTESIAN_POINT('Ctrl Pts',(-191.088710214552,4.74844233097209,
129.515835552091));
#122825=CARTESIAN_POINT('Ctrl Pts',(-191.096456490636,4.71063069765271,
129.383808151861));
#122826=CARTESIAN_POINT('Ctrl Pts',(-191.104202766721,4.66736576253298,
129.253593097518));
#122827=CARTESIAN_POINT('Ctrl Pts',(-191.111949099986,4.62410050804126,
129.123377081957));
#122828=CARTESIAN_POINT('Ctrl Pts',(-191.119695433251,4.57538199469793,
128.994973810001));
#122829=CARTESIAN_POINT('Ctrl Pts',(-191.127441766517,4.52139763135042,
128.868864164012));
#122830=CARTESIAN_POINT('Ctrl Pts',(-191.13518983452,4.46740117857896,128.742726276643));
#122831=CARTESIAN_POINT('Ctrl Pts',(-191.142937902523,4.40813668305963,
128.618883396679));
#122832=CARTESIAN_POINT('Ctrl Pts',(-191.150685970526,4.34383899959804,
128.49779481359));
#122833=CARTESIAN_POINT('Ctrl Pts',(-191.158442273267,4.2794729797934,128.376577536114));
#122834=CARTESIAN_POINT('Ctrl Pts',(-191.166198576009,4.21006326982718,
128.258120748965));
#122835=CARTESIAN_POINT('Ctrl Pts',(-191.173954878751,4.13589013312932,
128.142858059013));
#122836=CARTESIAN_POINT('Ctrl Pts',(-191.181715321265,4.0616774079951,128.027533849893));
#122837=CARTESIAN_POINT('Ctrl Pts',(-191.18947576378,3.98269641524828,127.915407454376));
#122838=CARTESIAN_POINT('Ctrl Pts',(-191.197236206294,3.89926918269119,
127.806881192547));
#122839=CARTESIAN_POINT('Ctrl Pts',(-191.205009106559,3.81570802533407,
127.698180714727));
#122840=CARTESIAN_POINT('Ctrl Pts',(-191.212782006825,3.72768661635664,
127.59309221928));
#122841=CARTESIAN_POINT('Ctrl Pts',(-191.22055490709,3.63556607623541,127.491983469984));
#122842=CARTESIAN_POINT('Ctrl Pts',(-191.228045242852,3.54679434978573,
127.394550278402));
#122843=CARTESIAN_POINT('Ctrl Pts',(-191.235535578614,3.4542165619243,127.300812728031));
#122844=CARTESIAN_POINT('Ctrl Pts',(-191.243025914376,3.35818496216893,
127.21106452312));
#122845=CARTESIAN_POINT('Ctrl Pts',(-191.250800248495,3.25851229511997,
127.11791348774));
#122846=CARTESIAN_POINT('Ctrl Pts',(-191.258574582614,3.15480301053301,
127.02876520709));
#122847=CARTESIAN_POINT('Ctrl Pts',(-191.266348916733,3.04741208417123,
126.943989825563));
#122848=CARTESIAN_POINT('Ctrl Pts',(-191.27411366968,2.94015350752896,126.859318922119));
#122849=CARTESIAN_POINT('Ctrl Pts',(-191.281878422628,2.82922262090105,
126.779010434803));
#122850=CARTESIAN_POINT('Ctrl Pts',(-191.289643175575,2.71501080926322,
126.703397393141));
#122851=CARTESIAN_POINT('Ctrl Pts',(-191.29740021646,2.60091243440618,126.627859451418));
#122852=CARTESIAN_POINT('Ctrl Pts',(-191.305157257345,2.48353994330888,
126.557007889035));
#122853=CARTESIAN_POINT('Ctrl Pts',(-191.31291429823,2.3633170466302,126.491134956926));
#122854=CARTESIAN_POINT('Ctrl Pts',(-191.32066548947,2.24318481097262,126.425311700106));
#122855=CARTESIAN_POINT('Ctrl Pts',(-191.32841668071,2.12020678969177,126.364459787714));
#122856=CARTESIAN_POINT('Ctrl Pts',(-191.33616787195,1.99483456514794,126.30882748787));
#122857=CARTESIAN_POINT('Ctrl Pts',(-191.343915768727,1.86951562714447,
126.253218833238));
#122858=CARTESIAN_POINT('Ctrl Pts',(-191.351663665504,1.74180486642149,
126.20282553702));
#122859=CARTESIAN_POINT('Ctrl Pts',(-191.359411562281,1.61217709380733,
126.157849229363));
#122860=CARTESIAN_POINT('Ctrl Pts',(-191.367157838366,1.48257643652876,
126.112882329779));
#122861=CARTESIAN_POINT('Ctrl Pts',(-191.37490411445,1.35105993409509,126.073330292999));
#122862=CARTESIAN_POINT('Ctrl Pts',(-191.382650390534,1.21812056675712,
126.03934589069));
#122863=CARTESIAN_POINT('Ctrl Pts',(-191.390396723799,1.08518021809113,
126.005361237516));
#122864=CARTESIAN_POINT('Ctrl Pts',(-191.398143057064,0.950817362346455,
125.976944397655));
#122865=CARTESIAN_POINT('Ctrl Pts',(-191.40588939033,0.815537878534929,
125.9541976274));
#122866=CARTESIAN_POINT('Ctrl Pts',(-191.413637458333,0.68022809982115,
125.931445763164));
#122867=CARTESIAN_POINT('Ctrl Pts',(-191.421385526336,0.544001670051006,
125.914366560051));
#122868=CARTESIAN_POINT('Ctrl Pts',(-191.429133594339,0.407371947222745,
125.90301068524));
#122869=CARTESIAN_POINT('Ctrl Pts',(-191.436889897081,0.270597012698589,
125.89164274127));
#122870=CARTESIAN_POINT('Ctrl Pts',(-191.444646199823,0.133418319135421,
125.886010309127));
#122871=CARTESIAN_POINT('Ctrl Pts',(-191.452402502564,-0.00364783849507481,
125.886111970357));
#122872=CARTESIAN_POINT('Ctrl Pts',(-191.460162945079,-0.14078715246088,
125.886213685846));
#122873=CARTESIAN_POINT('Ctrl Pts',(-191.467923387593,-0.277813420392517,
125.892055576286));
#122874=CARTESIAN_POINT('Ctrl Pts',(-191.475683830107,-0.414214095113777,
125.903584174398));
#122875=CARTESIAN_POINT('Ctrl Pts',(-191.483456730372,-0.550833732307181,
125.91513127924));
#122876=CARTESIAN_POINT('Ctrl Pts',(-191.491229630638,-0.686825381383332,
125.93238328479));
#122877=CARTESIAN_POINT('Ctrl Pts',(-191.499002530903,-0.821684437819978,
125.95523515547));
#122878=CARTESIAN_POINT('Ctrl Pts',(-191.506492866665,-0.951641027862406,
125.977256303091));
#122879=CARTESIAN_POINT('Ctrl Pts',(-191.513983202427,-1.08054563945036,
126.004477182315));
#122880=CARTESIAN_POINT('Ctrl Pts',(-191.521473538189,-1.20796077141146,
126.036760189968));
#122881=CARTESIAN_POINT('Ctrl Pts',(-191.529247872308,-1.3402068868303,
126.07026721767));
#122882=CARTESIAN_POINT('Ctrl Pts',(-191.537022206427,-1.47126726171084,
126.109333952733));
#122883=CARTESIAN_POINT('Ctrl Pts',(-191.544796540546,-1.6006386100197,
126.153861816081));
#122884=CARTESIAN_POINT('Ctrl Pts',(-191.552561293493,-1.72985051970473,
126.198334802817));
#122885=CARTESIAN_POINT('Ctrl Pts',(-191.560326046441,-1.85737717839847,
126.248255400426));
#122886=CARTESIAN_POINT('Ctrl Pts',(-191.568090799388,-1.98272684579087,
126.303474336234));
#122887=CARTESIAN_POINT('Ctrl Pts',(-191.575847840273,-2.10795201412615,
126.358638427817));
#122888=CARTESIAN_POINT('Ctrl Pts',(-191.583604881158,-2.2310041385998,
126.419090228625));
#122889=CARTESIAN_POINT('Ctrl Pts',(-191.591361922043,-2.35140831426397,
126.484631227649));
#122890=CARTESIAN_POINT('Ctrl Pts',(-191.599113113283,-2.47172169220282,
126.550122801696));
#122891=CARTESIAN_POINT('Ctrl Pts',(-191.606864304523,-2.58939075392098,
126.62069574888));
#122892=CARTESIAN_POINT('Ctrl Pts',(-191.614615495763,-2.70396253312058,
126.696104335154));
#122893=CARTESIAN_POINT('Ctrl Pts',(-191.62236339254,-2.81848561625756,
126.771480870767));
#122894=CARTESIAN_POINT('Ctrl Pts',(-191.630111289317,-2.92991370925743,
126.851688743189));
#122895=CARTESIAN_POINT('Ctrl Pts',(-191.637859186094,-3.03782052811709,
126.936437466642));
#122896=CARTESIAN_POINT('Ctrl Pts',(-191.645605462178,-3.14570477519644,
127.02116846249));
#122897=CARTESIAN_POINT('Ctrl Pts',(-191.653351738262,-3.25006890594588,
127.110438178736));
#122898=CARTESIAN_POINT('Ctrl Pts',(-191.661098014347,-3.35051792136731,
127.203914433953));
#122899=CARTESIAN_POINT('Ctrl Pts',(-191.668844347612,-3.45096767828041,
127.29739137919));
#122900=CARTESIAN_POINT('Ctrl Pts',(-191.676590680877,-3.54750197598732,
127.395074659016));
#122901=CARTESIAN_POINT('Ctrl Pts',(-191.684337014142,-3.63976134341008,
127.496593935117));
#122902=CARTESIAN_POINT('Ctrl Pts',(-191.692085082145,-3.73204137167862,
127.598135945756));
#122903=CARTESIAN_POINT('Ctrl Pts',(-191.699833150149,-3.82004430177213,
127.70351537279));
#122904=CARTESIAN_POINT('Ctrl Pts',(-191.707581218151,-3.90345002342118,
127.812327700442));
#122905=CARTESIAN_POINT('Ctrl Pts',(-191.715337520893,-3.98694438966386,
127.921255675131));
#122906=CARTESIAN_POINT('Ctrl Pts',(-191.723093823635,-4.06583154899084,
128.033623527975));
#122907=CARTESIAN_POINT('Ctrl Pts',(-191.730850126377,-4.13983362474526,
128.148996118683));
#122908=CARTESIAN_POINT('Ctrl Pts',(-191.738610568891,-4.21387519763547,
128.264430287216));
#122909=CARTESIAN_POINT('Ctrl Pts',(-191.746371011405,-4.28302629462755,
128.38287205169));
#122910=CARTESIAN_POINT('Ctrl Pts',(-191.754131453919,-4.34705485498703,
128.503861291282));
#122911=CARTESIAN_POINT('Ctrl Pts',(-191.761904354185,-4.41118619967579,
128.625044753542));
#122912=CARTESIAN_POINT('Ctrl Pts',(-191.76967725445,-4.47017840691058,
128.748783509796));
#122913=CARTESIAN_POINT('Ctrl Pts',(-191.777450154716,-4.52384709502806,
128.874596247674));
#122914=CARTESIAN_POINT('Ctrl Pts',(-191.784940490478,-4.57556479114977,
128.995835375627));
#122915=CARTESIAN_POINT('Ctrl Pts',(-191.79243082624,-4.62233918575824,
129.119000026256));
#122916=CARTESIAN_POINT('Ctrl Pts',(-191.799921162002,-4.6640495682308,
129.243647739556));
#122917=CARTESIAN_POINT('Ctrl Pts',(-191.806629630531,-4.70140607627558,
129.355284292103));
#122918=CARTESIAN_POINT('Ctrl Pts',(-191.81333809906,-4.73477224984779,
129.468318960301));
#122919=CARTESIAN_POINT('Ctrl Pts',(-191.820046567589,-4.76405452823394,
129.582490119308));
#122920=CARTESIAN_POINT('Origin',(213.235140564004,0.,130.804360617566));
#122921=CARTESIAN_POINT('',(-193.914998640423,-4.76405452823412,129.582490119309));
#122922=CARTESIAN_POINT('',(-193.570047426085,-4.7640545282341,129.582490119308));
#122923=CARTESIAN_POINT('',(213.235140564004,-4.76405452823405,129.582490119308));
#122924=CARTESIAN_POINT('',(-192.235140564068,-4.9182489107902,130.807633843951));
#122925=CARTESIAN_POINT('Ctrl Pts',(-192.235140564068,-4.9182489107902,
130.80763384395));
#122926=CARTESIAN_POINT('Ctrl Pts',(-192.243918515748,-4.9181453490622,
130.963242499187));
#122927=CARTESIAN_POINT('Ctrl Pts',(-192.252696467428,-4.91065281771742,
131.118565439462));
#122928=CARTESIAN_POINT('Ctrl Pts',(-192.261474419109,-4.89587660554873,
131.272949270588));
#122929=CARTESIAN_POINT('Ctrl Pts',(-192.270289110367,-4.88103854845119,
131.42797926576));
#122930=CARTESIAN_POINT('Ctrl Pts',(-192.279103801625,-4.85885582307568,
131.582062100835));
#122931=CARTESIAN_POINT('Ctrl Pts',(-192.287918492883,-4.8294847853578,
131.734554022454));
#122932=CARTESIAN_POINT('Ctrl Pts',(-192.296783739358,-4.79994529486645,
131.887920536499));
#122933=CARTESIAN_POINT('Ctrl Pts',(-192.305648985834,-4.76313489578936,
132.039677664175));
#122934=CARTESIAN_POINT('Ctrl Pts',(-192.314514232309,-4.71926132012198,
132.189191168536));
#122935=CARTESIAN_POINT('Ctrl Pts',(-192.322085292695,-4.68179259416399,
132.316878060629));
#122936=CARTESIAN_POINT('Ctrl Pts',(-192.329656353081,-4.63917323850466,
132.442928873986));
#122937=CARTESIAN_POINT('Ctrl Pts',(-192.337227413468,-4.59155968143751,
132.566961750635));
#122938=CARTESIAN_POINT('Ctrl Pts',(-192.345001747587,-4.54266775846242,
132.694324758674));
#122939=CARTESIAN_POINT('Ctrl Pts',(-192.352776081706,-4.48839508868817,
132.819853675534));
#122940=CARTESIAN_POINT('Ctrl Pts',(-192.360550415825,-4.42889900368266,
132.943060380899));
#122941=CARTESIAN_POINT('Ctrl Pts',(-192.368315168772,-4.3694762422846,
133.06611524501));
#122942=CARTESIAN_POINT('Ctrl Pts',(-192.376079921719,-4.30484304252658,
133.186853243304));
#122943=CARTESIAN_POINT('Ctrl Pts',(-192.383844674666,-4.23520571110023,
133.304803707733));
#122944=CARTESIAN_POINT('Ctrl Pts',(-192.391601715551,-4.16563754445317,
133.422637022098));
#122945=CARTESIAN_POINT('Ctrl Pts',(-192.399358756436,-4.09107533448945,
133.537687977781));
#122946=CARTESIAN_POINT('Ctrl Pts',(-192.407115797321,-4.01177229319911,
133.64950843974));
#122947=CARTESIAN_POINT('Ctrl Pts',(-192.414866988561,-3.9325290549492,
133.761244577018));
#122948=CARTESIAN_POINT('Ctrl Pts',(-192.422618179801,-3.84855232664149,
133.869754751943));
#122949=CARTESIAN_POINT('Ctrl Pts',(-192.430369371041,-3.76013962162594,
133.974618192019));
#122950=CARTESIAN_POINT('Ctrl Pts',(-192.438117267819,-3.67176449436839,
134.079437062336));
#122951=CARTESIAN_POINT('Ctrl Pts',(-192.445865164596,-3.57895739182149,
134.180611982277));
#122952=CARTESIAN_POINT('Ctrl Pts',(-192.453613061373,-3.4820571144234,
134.27775396045));
#122953=CARTESIAN_POINT('Ctrl Pts',(-192.461359337457,-3.38517710647442,
134.374875618616));
#122954=CARTESIAN_POINT('Ctrl Pts',(-192.469105613541,-3.28420590264548,
134.467965736369));
#122955=CARTESIAN_POINT('Ctrl Pts',(-192.476851889625,-3.17952001215119,
134.556671312968));
#122956=CARTESIAN_POINT('Ctrl Pts',(-192.48459822289,-3.07483334888957,
134.645377544372));
#122957=CARTESIAN_POINT('Ctrl Pts',(-192.492344556156,-2.96643224252753,
134.729698917291));
#122958=CARTESIAN_POINT('Ctrl Pts',(-192.500090889421,-2.85472689593607,
134.809322216897));
#122959=CARTESIAN_POINT('Ctrl Pts',(-192.507838957424,-2.7429965337069,
134.888963347589));
#122960=CARTESIAN_POINT('Ctrl Pts',(-192.515587025427,-2.62796077711468,
134.963904084522));
#122961=CARTESIAN_POINT('Ctrl Pts',(-192.52333509343,-2.51005911841526,
135.033874334834));
#122962=CARTESIAN_POINT('Ctrl Pts',(-192.531091396171,-2.39203215242945,
135.103918950361));
#122963=CARTESIAN_POINT('Ctrl Pts',(-192.538847698913,-2.27113353654513,
135.16898232667));
#122964=CARTESIAN_POINT('Ctrl Pts',(-192.546604001655,-2.14782818502421,
135.228839925927));
#122965=CARTESIAN_POINT('Ctrl Pts',(-192.554364444169,-2.02445702172452,
135.288729472987));
#122966=CARTESIAN_POINT('Ctrl Pts',(-192.562124886684,-1.89867692159537,
135.343407550848));
#122967=CARTESIAN_POINT('Ctrl Pts',(-192.569885329198,-1.77097219332344,
135.392698067337));
#122968=CARTESIAN_POINT('Ctrl Pts',(-192.577658229463,-1.64306246208459,
135.442067709339));
#122969=CARTESIAN_POINT('Ctrl Pts',(-192.585431129729,-1.51322229925508,
135.486032381865));
#122970=CARTESIAN_POINT('Ctrl Pts',(-192.593204029994,-1.38195142542684,
135.524465840997));
#122971=CARTESIAN_POINT('Ctrl Pts',(-192.600694365756,-1.25545257851221,
135.561502147082));
#122972=CARTESIAN_POINT('Ctrl Pts',(-192.608184701518,-1.12762553341084,
135.593402330408));
#122973=CARTESIAN_POINT('Ctrl Pts',(-192.61567503728,-0.998923910181445,
135.620098783639));
#122974=CARTESIAN_POINT('Ctrl Pts',(-192.623449371399,-0.865342525790616,
135.647807441008));
#122975=CARTESIAN_POINT('Ctrl Pts',(-192.631223705518,-0.730395789175812,
135.669997752622));
#122976=CARTESIAN_POINT('Ctrl Pts',(-192.638998039637,-0.594579411339083,
135.68653824503));
#122977=CARTESIAN_POINT('Ctrl Pts',(-192.646762792585,-0.45893041504978,
135.70305835276));
#122978=CARTESIAN_POINT('Ctrl Pts',(-192.654527545532,-0.32241429438374,
135.713942448564));
#122979=CARTESIAN_POINT('Ctrl Pts',(-192.662292298479,-0.185538549506594,
135.719109696527));
#122980=CARTESIAN_POINT('Ctrl Pts',(-192.670049339364,-0.0487987515492415,
135.724271812306));
#122981=CARTESIAN_POINT('Ctrl Pts',(-192.677806380249,0.0882995716484737,
135.723728365175));
#122982=CARTESIAN_POINT('Ctrl Pts',(-192.685563421134,0.225242524115774,
135.717450161614));
#122983=CARTESIAN_POINT('Ctrl Pts',(-192.693314612374,0.362082206837544,
135.711176692494));
#122984=CARTESIAN_POINT('Ctrl Pts',(-192.701065803614,0.498766363066561,
135.69917709268));
#122985=CARTESIAN_POINT('Ctrl Pts',(-192.708816994854,0.63478017175093,
135.681474230765));
#122986=CARTESIAN_POINT('Ctrl Pts',(-192.716564891631,0.770736170938507,
135.663778893039));
#122987=CARTESIAN_POINT('Ctrl Pts',(-192.724312788408,0.906022002373333,
135.640385164795));
#122988=CARTESIAN_POINT('Ctrl Pts',(-192.732060685185,1.04012726666948,
135.611367829089));
#122989=CARTESIAN_POINT('Ctrl Pts',(-192.73980696127,1.17420447903531,135.582356563184));
#122990=CARTESIAN_POINT('Ctrl Pts',(-192.747553237354,1.30710123357782,
135.547724112247));
#122991=CARTESIAN_POINT('Ctrl Pts',(-192.755299513438,1.4383170283509,135.507596438621));
#122992=CARTESIAN_POINT('Ctrl Pts',(-192.763045846703,1.56953379172899,
135.467468468782));
#122993=CARTESIAN_POINT('Ctrl Pts',(-192.770792179969,1.69906919670432,
135.421845309648));
#122994=CARTESIAN_POINT('Ctrl Pts',(-192.778538513234,1.82643800209956,
135.370902776244));
#122995=CARTESIAN_POINT('Ctrl Pts',(-192.786286581237,1.95383533085548,
135.319948834614));
#122996=CARTESIAN_POINT('Ctrl Pts',(-192.79403464924,2.07906473161203,135.263673293452));
#122997=CARTESIAN_POINT('Ctrl Pts',(-192.801782717243,2.20166141129512,
135.202299918251));
#122998=CARTESIAN_POINT('Ctrl Pts',(-192.809539019985,2.32438838818846,
135.140861314697));
#122999=CARTESIAN_POINT('Ctrl Pts',(-192.817295322727,2.44447670436585,
135.074314229283));
#123000=CARTESIAN_POINT('Ctrl Pts',(-192.825051625468,2.56148615227356,
135.002928439361));
#123001=CARTESIAN_POINT('Ctrl Pts',(-192.832812067983,2.67855805164703,
134.931504548693));
#123002=CARTESIAN_POINT('Ctrl Pts',(-192.840572510497,2.79254748358488,
134.855237024847));
#123003=CARTESIAN_POINT('Ctrl Pts',(-192.848332953011,2.90304451607954,
134.774438148315));
#123004=CARTESIAN_POINT('Ctrl Pts',(-192.856105853276,3.01371892821992,
134.693509566255));
#123005=CARTESIAN_POINT('Ctrl Pts',(-192.863878753542,3.12088943189119,
134.608035339398));
#123006=CARTESIAN_POINT('Ctrl Pts',(-192.871651653807,3.22417970332439,
134.518367658912));
#123007=CARTESIAN_POINT('Ctrl Pts',(-192.879141989569,3.32371511321709,
134.431959624473));
#123008=CARTESIAN_POINT('Ctrl Pts',(-192.886632325331,3.41964728113286,
134.341657939474));
#123009=CARTESIAN_POINT('Ctrl Pts',(-192.894122661093,3.51167413438388,
134.247807703902));
#123010=CARTESIAN_POINT('Ctrl Pts',(-192.901896995212,3.60719021374836,
134.150399108123));
#123011=CARTESIAN_POINT('Ctrl Pts',(-192.909671329331,3.69880155876895,
134.048859002174));
#123012=CARTESIAN_POINT('Ctrl Pts',(-192.91744566345,3.78612961320351,133.943533377151));
#123013=CARTESIAN_POINT('Ctrl Pts',(-192.925210416397,3.87335004361548,
133.838337556548));
#123014=CARTESIAN_POINT('Ctrl Pts',(-192.932975169344,3.95629743948013,
133.729365797536));
#123015=CARTESIAN_POINT('Ctrl Pts',(-192.940739922292,4.0346294750173,133.61700138059));
#123016=CARTESIAN_POINT('Ctrl Pts',(-192.948496963177,4.11288371007249,
133.504748565566));
#123017=CARTESIAN_POINT('Ctrl Pts',(-192.956254004062,4.18653148511081,
133.389110116985));
#123018=CARTESIAN_POINT('Ctrl Pts',(-192.964011044947,4.25527046547266,
133.27050261027));
#123019=CARTESIAN_POINT('Ctrl Pts',(-192.971762236187,4.32395760923461,
133.151984546398));
#123020=CARTESIAN_POINT('Ctrl Pts',(-192.979513427427,4.38774313120223,
133.03050221786));
#123021=CARTESIAN_POINT('Ctrl Pts',(-192.987264618667,4.44636799801797,
132.906501119222));
#123022=CARTESIAN_POINT('Ctrl Pts',(-192.995012515444,4.50496794770152,
132.782552724358));
#123023=CARTESIAN_POINT('Ctrl Pts',(-193.002760412221,4.55841143801551,
132.656088041339));
#123024=CARTESIAN_POINT('Ctrl Pts',(-193.010508308998,4.60648550272751,
132.527576905692));
#123025=CARTESIAN_POINT('Ctrl Pts',(-193.018254585082,4.65454951138154,
132.399092651803));
#123026=CARTESIAN_POINT('Ctrl Pts',(-193.026000861166,4.69724619158006,
132.268563162699));
#123027=CARTESIAN_POINT('Ctrl Pts',(-193.03374713725,4.73441098548304,132.136477610565));
#123028=CARTESIAN_POINT('Ctrl Pts',(-193.041493470516,4.77157605372813,
132.004391083406));
#123029=CARTESIAN_POINT('Ctrl Pts',(-193.049239803781,4.80320904830049,
131.870748846647));
#123030=CARTESIAN_POINT('Ctrl Pts',(-193.056986137046,4.82919560265308,
131.736054179751));
#123031=CARTESIAN_POINT('Ctrl Pts',(-193.064734205049,4.8551879765143,131.601329348918));
#123032=CARTESIAN_POINT('Ctrl Pts',(-193.072482273053,4.87553131993598,
131.465552002776));
#123033=CARTESIAN_POINT('Ctrl Pts',(-193.080230341056,4.89016266115448,
131.329234135616));
#123034=CARTESIAN_POINT('Ctrl Pts',(-193.087986643797,4.90480955273655,
131.192771388205));
#123035=CARTESIAN_POINT('Ctrl Pts',(-193.095742946539,4.91373227328045,
131.055767361558));
#123036=CARTESIAN_POINT('Ctrl Pts',(-193.103499249281,4.91691985117717,
130.918738236006));
#123037=CARTESIAN_POINT('Ctrl Pts',(-193.111259691795,4.92010913038018,
130.781635973883));
#123038=CARTESIAN_POINT('Ctrl Pts',(-193.119020134309,4.91755717486896,
130.644508976869));
#123039=CARTESIAN_POINT('Ctrl Pts',(-193.126780576824,4.90930513680369,
130.507870927605));
#123040=CARTESIAN_POINT('Ctrl Pts',(-193.134553477089,4.90103985183434,
130.371013534815));
#123041=CARTESIAN_POINT('Ctrl Pts',(-193.142326377354,4.88705623904379,
130.23464704741));
#123042=CARTESIAN_POINT('Ctrl Pts',(-193.15009927762,4.86744719464528,130.099278445164));
#123043=CARTESIAN_POINT('Ctrl Pts',(-193.157589613382,4.84855098840286,
129.968830832581));
#123044=CARTESIAN_POINT('Ctrl Pts',(-193.165079949144,4.82443130336841,
129.839310116289));
#123045=CARTESIAN_POINT('Ctrl Pts',(-193.172570284906,4.79521520426802,
129.711156973565));
#123046=CARTESIAN_POINT('Ctrl Pts',(-193.180344619025,4.76489136789024,
129.578144865484));
#123047=CARTESIAN_POINT('Ctrl Pts',(-193.188118953144,4.7289809707059,129.44618473883));
#123048=CARTESIAN_POINT('Ctrl Pts',(-193.195893287263,4.68757048592578,
129.31578210033));
#123049=CARTESIAN_POINT('Ctrl Pts',(-193.20365804021,4.64621103586719,129.185540171426));
#123050=CARTESIAN_POINT('Ctrl Pts',(-193.211422793157,4.59936510233688,
129.056852280564));
#123051=CARTESIAN_POINT('Ctrl Pts',(-193.219187546105,4.54717011460856,
128.930213608575));
#123052=CARTESIAN_POINT('Ctrl Pts',(-193.22694458699,4.49502696767788,128.8037007159));
#123053=CARTESIAN_POINT('Ctrl Pts',(-193.234701627874,4.43754548719051,
128.679233350863));
#123054=CARTESIAN_POINT('Ctrl Pts',(-193.242458668759,4.37491273058033,
128.557291045366));
#123055=CARTESIAN_POINT('Ctrl Pts',(-193.25020986,4.31232720581922,128.435440697511));
#123056=CARTESIAN_POINT('Ctrl Pts',(-193.25796105124,4.24459831493363,128.316111965434));
#123057=CARTESIAN_POINT('Ctrl Pts',(-193.26571224248,4.17196085126148,128.19976358193));
#123058=CARTESIAN_POINT('Ctrl Pts',(-193.273460139257,4.09935426044897,
128.083464649593));
#123059=CARTESIAN_POINT('Ctrl Pts',(-193.281208036034,4.02184345290365,
127.97014387735));
#123060=CARTESIAN_POINT('Ctrl Pts',(-193.288955932811,3.93970860111024,
127.860234397303));
#123061=CARTESIAN_POINT('Ctrl Pts',(-193.296702208895,3.8575909301572,127.75034790795));
#123062=CARTESIAN_POINT('Ctrl Pts',(-193.304448484979,3.77085137275848,
127.643871604446));
#123063=CARTESIAN_POINT('Ctrl Pts',(-193.312194761063,3.67981253579604,
127.541208343476));
#123064=CARTESIAN_POINT('Ctrl Pts',(-193.319941094329,3.58877302680572,
127.43854432467));
#123065=CARTESIAN_POINT('Ctrl Pts',(-193.327687427594,3.49343443432112,
127.339693697082));
#123066=CARTESIAN_POINT('Ctrl Pts',(-193.335433760859,3.39415836369511,
127.24502471537));
#123067=CARTESIAN_POINT('Ctrl Pts',(-193.343181828862,3.29486006088155,
127.150334533197));
#123068=CARTESIAN_POINT('Ctrl Pts',(-193.350929896865,3.19162280819176,
127.059828130087));
#123069=CARTESIAN_POINT('Ctrl Pts',(-193.358677964868,3.08484332314698,
126.97383523139));
#123070=CARTESIAN_POINT('Ctrl Pts',(-193.36643426761,2.97795035159466,126.887750938417));
#123071=CARTESIAN_POINT('Ctrl Pts',(-193.374190570352,2.86750793222474,
126.806189978007));
#123072=CARTESIAN_POINT('Ctrl Pts',(-193.381946873094,2.7539444117456,126.729440588962));
#123073=CARTESIAN_POINT('Ctrl Pts',(-193.389707315608,2.64032027899594,
126.652650236458));
#123074=CARTESIAN_POINT('Ctrl Pts',(-193.397467758122,2.52357205848088,
126.580676777505));
#123075=CARTESIAN_POINT('Ctrl Pts',(-193.405228200636,2.40415416970356,
126.513763247642));
#123076=CARTESIAN_POINT('Ctrl Pts',(-193.413001100902,2.28454458072975,
126.446742302241));
#123077=CARTESIAN_POINT('Ctrl Pts',(-193.420774001167,2.16225710849449,
126.384797694339));
#123078=CARTESIAN_POINT('Ctrl Pts',(-193.428546901433,2.03776850211148,
126.328125302672));
#123079=CARTESIAN_POINT('Ctrl Pts',(-193.436037237195,1.91780537013702,
126.273513095191));
#123080=CARTESIAN_POINT('Ctrl Pts',(-193.443527572957,1.79579864438425,
126.223796558439));
#123081=CARTESIAN_POINT('Ctrl Pts',(-193.451017908719,1.67218776071735,
126.179106986098));
#123082=CARTESIAN_POINT('Ctrl Pts',(-193.458792242838,1.54389013282677,
126.132722995039));
#123083=CARTESIAN_POINT('Ctrl Pts',(-193.466566576957,1.41345789412949,
126.091607757464));
#123084=CARTESIAN_POINT('Ctrl Pts',(-193.474340911076,1.28136308263296,
126.055961759744));
#123085=CARTESIAN_POINT('Ctrl Pts',(-193.482105664023,1.1494310661863,126.020359692531));
#123086=CARTESIAN_POINT('Ctrl Pts',(-193.48987041697,1.01584092762441,125.990213554768));
#123087=CARTESIAN_POINT('Ctrl Pts',(-193.497635169917,0.88108356048614,
125.965675380651));
#123088=CARTESIAN_POINT('Ctrl Pts',(-193.505392210802,0.746460036264656,
125.941161578194));
#123089=CARTESIAN_POINT('Ctrl Pts',(-193.513149251688,0.610671972693172,
125.922244724601));
#123090=CARTESIAN_POINT('Ctrl Pts',(-193.520906292573,0.47422392265558,
125.909026641862));
#123091=CARTESIAN_POINT('Ctrl Pts',(-193.528657483813,0.337878769153747,
125.895818526982));
#123092=CARTESIAN_POINT('Ctrl Pts',(-193.536408675053,0.200875007398296,
125.888300666612));
#123093=CARTESIAN_POINT('Ctrl Pts',(-193.544159866293,0.0637254938153366,
125.886523478748));
#123094=CARTESIAN_POINT('Ctrl Pts',(-193.55190776307,-0.0733657275659535,
125.884747046236));
#123095=CARTESIAN_POINT('Ctrl Pts',(-193.559655659847,-0.210602187450144,
125.888706438433));
#123096=CARTESIAN_POINT('Ctrl Pts',(-193.567403556624,-0.347468039461664,
125.898400056773));
#123097=CARTESIAN_POINT('Ctrl Pts',(-193.575149832708,-0.48430526208743,
125.908091647417));
#123098=CARTESIAN_POINT('Ctrl Pts',(-193.582896108792,-0.620771641297166,
125.923515050776));
#123099=CARTESIAN_POINT('Ctrl Pts',(-193.590642384876,-0.756353865451232,
125.944616602423));
#123100=CARTESIAN_POINT('Ctrl Pts',(-193.598388718142,-0.891937090442292,
125.965718309837));
#123101=CARTESIAN_POINT('Ctrl Pts',(-193.606135051407,-1.02663576103986,
125.992498189051));
#123102=CARTESIAN_POINT('Ctrl Pts',(-193.613881384672,-1.15994459764504,
126.02485106188));
#123103=CARTESIAN_POINT('Ctrl Pts',(-193.621629452675,-1.29328328784007,
126.05721117991));
#123104=CARTESIAN_POINT('Ctrl Pts',(-193.629377520678,-1.42523114484017,
126.095146682807));
#123105=CARTESIAN_POINT('Ctrl Pts',(-193.637125588681,-1.55529632586053,
126.138502025488));
#123106=CARTESIAN_POINT('Ctrl Pts',(-193.644881891423,-1.68549974170325,
126.181903446744));
#123107=CARTESIAN_POINT('Ctrl Pts',(-193.652638194165,-1.81381611299879,
126.230736090713));
#123108=CARTESIAN_POINT('Ctrl Pts',(-193.660394496907,-1.93977140442049,
126.284795377292));
#123109=CARTESIAN_POINT('Ctrl Pts',(-193.668154939421,-2.06579392197332,
126.33888351694));
#123110=CARTESIAN_POINT('Ctrl Pts',(-193.675915381935,-2.1894524963065,
126.398203688727));
#123111=CARTESIAN_POINT('Ctrl Pts',(-193.683675824449,-2.31029702989768,
126.462504943301));
#123112=CARTESIAN_POINT('Ctrl Pts',(-193.691448724715,-2.43133555386226,
126.526909419958));
#123113=CARTESIAN_POINT('Ctrl Pts',(-193.69922162498,-2.54955067263316,
126.596310760058));
#123114=CARTESIAN_POINT('Ctrl Pts',(-193.706994525246,-2.6645198933412,
126.670413738313));
#123115=CARTESIAN_POINT('Ctrl Pts',(-193.714484861008,-2.77530969328494,
126.741822886652));
#123116=CARTESIAN_POINT('Ctrl Pts',(-193.72197519677,-2.88308523914618,
126.817597597928));
#123117=CARTESIAN_POINT('Ctrl Pts',(-193.729465532532,-2.98749854401419,
126.897439129743));
#123118=CARTESIAN_POINT('Ctrl Pts',(-193.737196078694,-3.0952603185036,
126.97984112973));
#123119=CARTESIAN_POINT('Ctrl Pts',(-193.744926624856,-3.19980039402153,
127.066850545295));
#123120=CARTESIAN_POINT('Ctrl Pts',(-193.752657171018,-3.30069311752396,
127.158183440517));
#123121=CARTESIAN_POINT('Ctrl Pts',(-193.760334883215,-3.40089629561768,
127.248892126417));
#123122=CARTESIAN_POINT('Ctrl Pts',(-193.768012595413,-3.49750149279864,
127.343865140785));
#123123=CARTESIAN_POINT('Ctrl Pts',(-193.77569030761,-3.5901203904032,127.44278083346));
#123124=CARTESIAN_POINT('Ctrl Pts',(-193.783361016429,-3.68265480383977,
127.54160629822));
#123125=CARTESIAN_POINT('Ctrl Pts',(-193.791031725249,-3.77120987628044,
127.644366999939));
#123126=CARTESIAN_POINT('Ctrl Pts',(-193.798702434068,-3.855431774176,127.750702336557));
#123127=CARTESIAN_POINT('Ctrl Pts',(-193.80636789687,-3.93959607249805,
127.856964950164));
#123128=CARTESIAN_POINT('Ctrl Pts',(-193.814033359672,-4.01943284300044,
127.966797023577));
#123129=CARTESIAN_POINT('Ctrl Pts',(-193.821698822474,-4.09462678788818,
128.079802941464));
#123130=CARTESIAN_POINT('Ctrl Pts',(-193.829473807303,-4.17089508320833,
128.194423456868));
#123131=CARTESIAN_POINT('Ctrl Pts',(-193.837248792132,-4.24238657353508,
128.312308902551));
#123132=CARTESIAN_POINT('Ctrl Pts',(-193.845023776961,-4.30881615492087,
128.433013657378));
#123133=CARTESIAN_POINT('Ctrl Pts',(-193.852685093457,-4.37427455244702,
128.551953738889));
#123134=CARTESIAN_POINT('Ctrl Pts',(-193.860346409954,-4.43481787122632,
128.673630879259));
#123135=CARTESIAN_POINT('Ctrl Pts',(-193.86800772645,-4.49021873156322,
128.79759236856));
#123136=CARTESIAN_POINT('Ctrl Pts',(-193.875839545445,-4.54685253732966,
128.924312619201));
#123137=CARTESIAN_POINT('Ctrl Pts',(-193.883671364441,-4.5981120887347,
129.053419710477));
#123138=CARTESIAN_POINT('Ctrl Pts',(-193.891503183436,-4.64380612801652,
129.184407621984));
#123139=CARTESIAN_POINT('Ctrl Pts',(-193.899335002432,-4.68950016729845,
129.315395533491));
#123140=CARTESIAN_POINT('Ctrl Pts',(-193.907166821427,-4.72962857139135,
129.448263836065));
#123141=CARTESIAN_POINT('Ctrl Pts',(-193.914998640423,-4.76405452823412,
129.582490119309));
#123142=CARTESIAN_POINT('Ctrl Pts',(-192.165295998532,-4.76405452823416,
129.582490119309));
#123143=CARTESIAN_POINT('Ctrl Pts',(-192.173087299489,-4.79834001608084,
129.716168716068));
#123144=CARTESIAN_POINT('Ctrl Pts',(-192.180878600447,-4.82701148740486,
129.851356535398));
#123145=CARTESIAN_POINT('Ctrl Pts',(-192.188669901404,-4.84994811259561,
129.987545848092));
#123146=CARTESIAN_POINT('Ctrl Pts',(-192.196460544,-4.87288279965338,130.12372365286));
#123147=CARTESIAN_POINT('Ctrl Pts',(-192.204251186596,-4.89008353206788,
130.260902405253));
#123148=CARTESIAN_POINT('Ctrl Pts',(-192.212041829192,-4.90148064217082,
130.398564391703));
#123149=CARTESIAN_POINT('Ctrl Pts',(-192.219741407466,-4.9127445321833,
130.534617256005));
#123150=CARTESIAN_POINT('Ctrl Pts',(-192.227440985739,-4.91833974990952,
130.671141747254));
#123151=CARTESIAN_POINT('Ctrl Pts',(-192.235140564013,-4.91824891079085,
130.807633842979));
#123152=CARTESIAN_POINT('',(-191.889859435946,-4.91824838362704,130.800373206121));
#123153=CARTESIAN_POINT('Ctrl Pts',(-191.820046567589,-4.76405452823394,
129.582490119308));
#123154=CARTESIAN_POINT('Ctrl Pts',(-191.82924828616,-4.80421977364591,
129.739093801576));
#123155=CARTESIAN_POINT('Ctrl Pts',(-191.83845000473,-4.83669951198726,
129.897836547039));
#123156=CARTESIAN_POINT('Ctrl Pts',(-191.847651723301,-4.86129257036642,
130.058024495031));
#123157=CARTESIAN_POINT('Ctrl Pts',(-191.856764218548,-4.88564716520422,
130.216659200447));
#123158=CARTESIAN_POINT('Ctrl Pts',(-191.865876713795,-4.90226722063982,
130.376711144536));
#123159=CARTESIAN_POINT('Ctrl Pts',(-191.874989209043,-4.91100407682167,
130.537486077864));
#123160=CARTESIAN_POINT('Ctrl Pts',(-191.879945951344,-4.91575649023196,
130.624939611869));
#123161=CARTESIAN_POINT('Ctrl Pts',(-191.884902693645,-4.9181772279881,
130.712606716241));
#123162=CARTESIAN_POINT('Ctrl Pts',(-191.889859435946,-4.91824838362704,
130.800373206121));
#123163=CARTESIAN_POINT('Ctrl Pts',(-191.889859435995,-4.91824838362774,
130.800373206994));
#123164=CARTESIAN_POINT('Ctrl Pts',(-191.897713992238,-4.91836113829842,
130.939449799867));
#123165=CARTESIAN_POINT('Ctrl Pts',(-191.90556854848,-4.91257017733928,
131.078607516704));
#123166=CARTESIAN_POINT('Ctrl Pts',(-191.913423104722,-4.90088344947465,
131.217306712311));
#123167=CARTESIAN_POINT('Ctrl Pts',(-191.921150059273,-4.88938657908931,
131.353752661333));
#123168=CARTESIAN_POINT('Ctrl Pts',(-191.928877013823,-4.87218410818176,
131.489754471933));
#123169=CARTESIAN_POINT('Ctrl Pts',(-191.936603968374,-4.84933606598093,
131.624801219728));
#123170=CARTESIAN_POINT('Ctrl Pts',(-191.944330975815,-4.82648786738739,
131.759848891906));
#123171=CARTESIAN_POINT('Ctrl Pts',(-191.952057983256,-4.7979940857108,
131.893941100987));
#123172=CARTESIAN_POINT('Ctrl Pts',(-191.959784990697,-4.76396615906066,
132.02657561413));
#123173=CARTESIAN_POINT('Ctrl Pts',(-191.967513741978,-4.72993055294498,
132.159240060396));
#123174=CARTESIAN_POINT('Ctrl Pts',(-191.97524249326,-4.69035841421798,
132.290445775788));
#123175=CARTESIAN_POINT('Ctrl Pts',(-191.982971244541,-4.64541136803275,
132.419704631778));
#123176=CARTESIAN_POINT('Ctrl Pts',(-191.990921039647,-4.59917882738299,
132.552660316771));
#123177=CARTESIAN_POINT('Ctrl Pts',(-191.998870834754,-4.54725946423311,
132.6835556899));
#123178=CARTESIAN_POINT('Ctrl Pts',(-192.00682062986,-4.48988223286208,
132.811881625558));
#123179=CARTESIAN_POINT('Ctrl Pts',(-192.01456223062,-4.43400763331795,
132.936846879103));
#123180=CARTESIAN_POINT('Ctrl Pts',(-192.022303831381,-4.37295770825076,
133.059375276236));
#123181=CARTESIAN_POINT('Ctrl Pts',(-192.030045432141,-4.30699015546567,
133.179022459434));
#123182=CARTESIAN_POINT('Ctrl Pts',(-192.03809932442,-4.23836151127706,
133.30349613804));
#123183=CARTESIAN_POINT('Ctrl Pts',(-192.046153216699,-4.16441045295695,
133.424850879837));
#123184=CARTESIAN_POINT('Ctrl Pts',(-192.054207108978,-4.08547567197879,
133.542621305698));
#123185=CARTESIAN_POINT('Ctrl Pts',(-192.062261001257,-4.00654089100041,
133.660391731559));
#123186=CARTESIAN_POINT('Ctrl Pts',(-192.070314893536,-3.9226227251379,
133.77457750615));
#123187=CARTESIAN_POINT('Ctrl Pts',(-192.078368785815,-3.83410466332919,
133.88475417897));
#123188=CARTESIAN_POINT('Ctrl Pts',(-192.086143119934,-3.74865914652369,
133.99110651607));
#123189=CARTESIAN_POINT('Ctrl Pts',(-192.093917454053,-3.65864985410877,
134.094069416823));
#123190=CARTESIAN_POINT('Ctrl Pts',(-192.101691788172,-3.56437564467085,
134.193226110054));
#123191=CARTESIAN_POINT('Ctrl Pts',(-192.109456541119,-3.47021761977078,
134.292260601523));
#123192=CARTESIAN_POINT('Ctrl Pts',(-192.117221294066,-3.37180540278206,
134.387497938163));
#123193=CARTESIAN_POINT('Ctrl Pts',(-192.124986047013,-3.26947915980666,
134.478552921473));
#123194=CARTESIAN_POINT('Ctrl Pts',(-192.132743087898,-3.16725454869806,
134.56951746769));
#123195=CARTESIAN_POINT('Ctrl Pts',(-192.140500128783,-3.06112393801676,
134.656307668951));
#123196=CARTESIAN_POINT('Ctrl Pts',(-192.148257169668,-2.95146527907113,
134.738574105538));
#123197=CARTESIAN_POINT('Ctrl Pts',(-192.156008360908,-2.84188931457368,
134.820778504364));
#123198=CARTESIAN_POINT('Ctrl Pts',(-192.163759552148,-2.72879090890884,
134.898465695044));
#123199=CARTESIAN_POINT('Ctrl Pts',(-192.171510743389,-2.6125818443738,
134.971325840477));
#123200=CARTESIAN_POINT('Ctrl Pts',(-192.179258640166,-2.49642217179069,
135.044155018405));
#123201=CARTESIAN_POINT('Ctrl Pts',(-192.187006536943,-2.37715480046932,
135.112161024362));
#123202=CARTESIAN_POINT('Ctrl Pts',(-192.19475443372,-2.25522112422815,
135.175076891054));
#123203=CARTESIAN_POINT('Ctrl Pts',(-192.202500709804,-2.13331295388346,
135.237979597104));
#123204=CARTESIAN_POINT('Ctrl Pts',(-192.210246985888,-2.00873993520163,
135.29579410257));
#123205=CARTESIAN_POINT('Ctrl Pts',(-192.217993261972,-1.88196838077047,
135.348299225897));
#123206=CARTESIAN_POINT('Ctrl Pts',(-192.225739595237,-1.75519589054102,
135.400804736805));
#123207=CARTESIAN_POINT('Ctrl Pts',(-192.233485928503,-1.62622519338845,
135.448000637764));
#123208=CARTESIAN_POINT('Ctrl Pts',(-192.241232261768,-1.49554253846573,
135.489713921015));
#123209=CARTESIAN_POINT('Ctrl Pts',(-192.248980329771,-1.36483061806836,
135.531436545666));
#123210=CARTESIAN_POINT('Ctrl Pts',(-192.256728397774,-1.2324063493972,
135.567673990578));
#123211=CARTESIAN_POINT('Ctrl Pts',(-192.264476465777,-1.09877070560949,
135.598303253747));
#123212=CARTESIAN_POINT('Ctrl Pts',(-192.272232768519,-0.964993032269096,
135.628965070061));
#123213=CARTESIAN_POINT('Ctrl Pts',(-192.279989071261,-0.830001793655666,
135.654006710523));
#123214=CARTESIAN_POINT('Ctrl Pts',(-192.287745374002,-0.694308261338982,
135.673356314908));
#123215=CARTESIAN_POINT('Ctrl Pts',(-192.295505816517,-0.558542305298078,
135.69271624676));
#123216=CARTESIAN_POINT('Ctrl Pts',(-192.303266259031,-0.422073697493207,
135.706378050116));
#123217=CARTESIAN_POINT('Ctrl Pts',(-192.311026701545,-0.28541738556099,
135.714321918688));
#123218=CARTESIAN_POINT('Ctrl Pts',(-192.31879960181,-0.148541700785455,
135.722278539464));
#123219=CARTESIAN_POINT('Ctrl Pts',(-192.326572502076,-0.0114781008894383,
135.72449887668));
#123220=CARTESIAN_POINT('Ctrl Pts',(-192.334345402341,0.125259011019499,
135.721015297596));
#123221=CARTESIAN_POINT('Ctrl Pts',(-192.341835738103,0.257025384489433,
135.717658355386));
#123222=CARTESIAN_POINT('Ctrl Pts',(-192.349326073865,0.388488287825575,
135.709005020696));
#123223=CARTESIAN_POINT('Ctrl Pts',(-192.356816409627,0.519195120740406,
135.695129421047));
#123224=CARTESIAN_POINT('Ctrl Pts',(-192.364590743746,0.654857742953279,
135.680727723819));
#123225=CARTESIAN_POINT('Ctrl Pts',(-192.372365077865,0.790135568566218,
135.66065431978));
#123226=CARTESIAN_POINT('Ctrl Pts',(-192.380139411984,0.924516415821493,
135.634935372124));
#123227=CARTESIAN_POINT('Ctrl Pts',(-192.387904164931,1.05873165069249,
135.609248120773));
#123228=CARTESIAN_POINT('Ctrl Pts',(-192.395668917878,1.19205172640386,
135.577929242197));
#123229=CARTESIAN_POINT('Ctrl Pts',(-192.403433670826,1.32396869645902,
135.541056718573));
#123230=CARTESIAN_POINT('Ctrl Pts',(-192.411190711711,1.45575464472018,
135.504220817259));
#123231=CARTESIAN_POINT('Ctrl Pts',(-192.418947752595,1.58613988652435,
135.461842352468));
#123232=CARTESIAN_POINT('Ctrl Pts',(-192.42670479348,1.71462615325309,135.414050435448));
#123233=CARTESIAN_POINT('Ctrl Pts',(-192.43445598472,1.84301552748845,135.366294558683));
#123234=CARTESIAN_POINT('Ctrl Pts',(-192.442207175961,1.96950841206677,
135.313133491062));
#123235=CARTESIAN_POINT('Ctrl Pts',(-192.449958367201,2.0936215538718,135.254746202171));
#123236=CARTESIAN_POINT('Ctrl Pts',(-192.457706263978,2.21768194428091,
135.196383729436));
#123237=CARTESIAN_POINT('Ctrl Pts',(-192.465454160755,2.33936425058921,
135.132799619475));
#123238=CARTESIAN_POINT('Ctrl Pts',(-192.473202057532,2.45820528151151,
135.064220927065));
#123239=CARTESIAN_POINT('Ctrl Pts',(-192.480948333616,2.57702145345207,
134.99565657984));
#123240=CARTESIAN_POINT('Ctrl Pts',(-192.4886946097,2.6929971937552,134.922099923534));
#123241=CARTESIAN_POINT('Ctrl Pts',(-192.496440885784,2.80569436276991,
134.843823726102));
#123242=CARTESIAN_POINT('Ctrl Pts',(-192.50418721905,2.91839236368936,134.765546950852));
#123243=CARTESIAN_POINT('Ctrl Pts',(-192.511933552315,3.0278114239197,134.682550787991));
#123244=CARTESIAN_POINT('Ctrl Pts',(-192.51967988558,3.13354315758743,134.59515081778));
#123245=CARTESIAN_POINT('Ctrl Pts',(-192.527427953583,3.23929856914339,
134.507731274952));
#123246=CARTESIAN_POINT('Ctrl Pts',(-192.535176021586,3.34136470970479,
134.415906211393));
#123247=CARTESIAN_POINT('Ctrl Pts',(-192.542924089589,3.43936730597353,
134.320030624421));
#123248=CARTESIAN_POINT('Ctrl Pts',(-192.550680392331,3.53747406056822,
134.224053139734));
#123249=CARTESIAN_POINT('Ctrl Pts',(-192.558436695073,3.63150836371962,
134.124016805884));
#123250=CARTESIAN_POINT('Ctrl Pts',(-192.566192997815,3.72113340261438,
134.020312927916));
#123251=CARTESIAN_POINT('Ctrl Pts',(-192.573953440329,3.81080627709143,
133.916553700066));
#123252=CARTESIAN_POINT('Ctrl Pts',(-192.581713882843,3.896064955127,133.80912333375));
#123253=CARTESIAN_POINT('Ctrl Pts',(-192.589474325357,3.97661443135476,
133.698444363217));
#123254=CARTESIAN_POINT('Ctrl Pts',(-192.597247225623,4.05729321275217,
133.587587720975));
#123255=CARTESIAN_POINT('Ctrl Pts',(-192.605020125888,4.13324746904369,
133.47347237904));
#123256=CARTESIAN_POINT('Ctrl Pts',(-192.612793026153,4.20422638427667,
133.356548614609));
#123257=CARTESIAN_POINT('Ctrl Pts',(-192.620283361916,4.27262503715757,
133.243875323526));
#123258=CARTESIAN_POINT('Ctrl Pts',(-192.627773697678,4.3364036520234,133.128594520953));
#123259=CARTESIAN_POINT('Ctrl Pts',(-192.63526403344,4.39537995294483,133.011127060068));
#123260=CARTESIAN_POINT('Ctrl Pts',(-192.643038367559,4.45659235823986,
132.889205784701));
#123261=CARTESIAN_POINT('Ctrl Pts',(-192.650812701678,4.51282500400254,
132.764542553542));
#123262=CARTESIAN_POINT('Ctrl Pts',(-192.658587035797,4.56382305531772,
132.637582421454));
#123263=CARTESIAN_POINT('Ctrl Pts',(-192.666351788744,4.6147582560922,132.510778756383));
#123264=CARTESIAN_POINT('Ctrl Pts',(-192.674116541692,4.66047155399552,
132.381684181989));
#123265=CARTESIAN_POINT('Ctrl Pts',(-192.681881294639,4.70075400015228,
132.250768199319));
#123266=CARTESIAN_POINT('Ctrl Pts',(-192.689638335524,4.74099643721574,
132.119982244248));
#123267=CARTESIAN_POINT('Ctrl Pts',(-192.697395376409,4.77581864259817,
131.987378852245));
#123268=CARTESIAN_POINT('Ctrl Pts',(-192.705152417294,4.80505991488965,
131.853447018593));
#123269=CARTESIAN_POINT('Ctrl Pts',(-192.712903608534,4.83427913611028,
131.71961618398));
#123270=CARTESIAN_POINT('Ctrl Pts',(-192.720654799774,4.85792571819555,
131.584459282138));
#123271=CARTESIAN_POINT('Ctrl Pts',(-192.728405991014,4.87588902321573,
131.448479625036));
#123272=CARTESIAN_POINT('Ctrl Pts',(-192.736153887791,4.89384469335207,
131.312557762916));
#123273=CARTESIAN_POINT('Ctrl Pts',(-192.743901784568,4.90612183966131,
131.175814227835));
#123274=CARTESIAN_POINT('Ctrl Pts',(-192.751649681345,4.91266112355447,
131.038761444392));
#123275=CARTESIAN_POINT('Ctrl Pts',(-192.759395957429,4.9191990395704,130.901737329437));
#123276=CARTESIAN_POINT('Ctrl Pts',(-192.767142233513,4.92000146188634,
130.764404485061));
#123277=CARTESIAN_POINT('Ctrl Pts',(-192.774888509598,4.91506105272305,
130.627278968305));
#123278=CARTESIAN_POINT('Ctrl Pts',(-192.782634842863,4.91012060709078,
130.490152439319));
#123279=CARTESIAN_POINT('Ctrl Pts',(-192.790381176128,4.89943725946526,
130.353233631717));
#123280=CARTESIAN_POINT('Ctrl Pts',(-192.798127509394,4.88305577391945,
130.217036710942));
#123281=CARTESIAN_POINT('Ctrl Pts',(-192.805875577397,4.86667061985355,
130.080809289811));
#123282=CARTESIAN_POINT('Ctrl Pts',(-192.8136236454,4.84458483533778,129.945304465287));
#123283=CARTESIAN_POINT('Ctrl Pts',(-192.821371713403,4.81689478580987,
129.811029008818));
#123284=CARTESIAN_POINT('Ctrl Pts',(-192.829128016144,4.78917530696777,
129.676610842796));
#123285=CARTESIAN_POINT('Ctrl Pts',(-192.836884318886,4.75583974389208,
129.543425038395));
#123286=CARTESIAN_POINT('Ctrl Pts',(-192.844640621628,4.71703525704713,
129.41196647571));
#123287=CARTESIAN_POINT('Ctrl Pts',(-192.852401064142,4.67821005907918,
129.280437749632));
#123288=CARTESIAN_POINT('Ctrl Pts',(-192.860161506656,4.63391024734856,
129.150638472024));
#123289=CARTESIAN_POINT('Ctrl Pts',(-192.867921949171,4.58433185427907,
129.023045229337));
#123290=CARTESIAN_POINT('Ctrl Pts',(-192.875694849436,4.53467387357166,
128.895247162649));
#123291=CARTESIAN_POINT('Ctrl Pts',(-192.883467749701,4.47972053529839,
128.769662565957));
#123292=CARTESIAN_POINT('Ctrl Pts',(-192.891240649967,4.41971509826897,
128.646745843647));
#123293=CARTESIAN_POINT('Ctrl Pts',(-192.898730985729,4.36189101002015,
128.528297453802));
#123294=CARTESIAN_POINT('Ctrl Pts',(-192.906221321491,4.29937590510965,
128.412326609133));
#123295=CARTESIAN_POINT('Ctrl Pts',(-192.913711657253,4.23242533464076,
128.299214144964));
#123296=CARTESIAN_POINT('Ctrl Pts',(-192.921485991372,4.16293631294325,
128.181812987336));
#123297=CARTESIAN_POINT('Ctrl Pts',(-192.929260325491,4.08844872451645,
128.067119348354));
#123298=CARTESIAN_POINT('Ctrl Pts',(-192.93703465961,4.00919926212544,127.955588190875));
#123299=CARTESIAN_POINT('Ctrl Pts',(-192.944799412557,3.93004746761452,
127.844194485581));
#123300=CARTESIAN_POINT('Ctrl Pts',(-192.952564165504,3.84614570015536,
127.735955822617));
#123301=CARTESIAN_POINT('Ctrl Pts',(-192.960328918452,3.75777602230254,
127.631301773374));
#123302=CARTESIAN_POINT('Ctrl Pts',(-192.968085959337,3.66949411445908,
127.526751668006));
#123303=CARTESIAN_POINT('Ctrl Pts',(-192.975843000222,3.57675337783237,
127.425779388006));
#123304=CARTESIAN_POINT('Ctrl Pts',(-192.983600041107,3.47987835496601,
127.328784449916));
#123305=CARTESIAN_POINT('Ctrl Pts',(-192.991351232347,3.38307638630784,
127.231862656463));
#123306=CARTESIAN_POINT('Ctrl Pts',(-192.999102423587,3.28214661216284,
127.138912510412));
#123307=CARTESIAN_POINT('Ctrl Pts',(-193.006853614827,3.17745268064025,
127.050299146999));
#123308=CARTESIAN_POINT('Ctrl Pts',(-193.014601511604,3.07280324683178,
126.961723446631));
#123309=CARTESIAN_POINT('Ctrl Pts',(-193.022349408381,2.96439313545571,
126.877481114876));
#123310=CARTESIAN_POINT('Ctrl Pts',(-193.030097305158,2.85262138988372,
126.797899052983));
#123311=CARTESIAN_POINT('Ctrl Pts',(-193.037843581242,2.74087302455107,
126.718333637942));
#123312=CARTESIAN_POINT('Ctrl Pts',(-193.045589857326,2.62576474197169,
126.643426780396));
#123313=CARTESIAN_POINT('Ctrl Pts',(-193.053336133411,2.50772674929877,
126.573463595261));
#123314=CARTESIAN_POINT('Ctrl Pts',(-193.061082466676,2.38968788529636,
126.503499893673));
#123315=CARTESIAN_POINT('Ctrl Pts',(-193.068828799941,2.26871960437203,
126.438480136662));
#123316=CARTESIAN_POINT('Ctrl Pts',(-193.076575133207,2.145278684549,126.378644581926));
#123317=CARTESIAN_POINT('Ctrl Pts',(-193.08432320121,2.02181012098801,126.318795627432));
#123318=CARTESIAN_POINT('Ctrl Pts',(-193.092071269213,1.89586816841405,
126.264133355903));
#123319=CARTESIAN_POINT('Ctrl Pts',(-193.099819337216,1.7679312758711,126.214850614712));
#123320=CARTESIAN_POINT('Ctrl Pts',(-193.107575639958,1.63985841047612,
126.165515495237));
#123321=CARTESIAN_POINT('Ctrl Pts',(-193.115331942699,1.50978673510698,
126.121571468042));
#123322=CARTESIAN_POINT('Ctrl Pts',(-193.123088245441,1.37821215022817,
126.08316221764));
#123323=CARTESIAN_POINT('Ctrl Pts',(-193.130848687956,1.24656734003178,
126.044732467064));
#123324=CARTESIAN_POINT('Ctrl Pts',(-193.13860913047,1.11341840134966,126.011843473238));
#123325=CARTESIAN_POINT('Ctrl Pts',(-193.146369572984,0.979272260174981,
125.98458791515));
#123326=CARTESIAN_POINT('Ctrl Pts',(-193.154142473249,0.844910775705553,
125.957288604021));
#123327=CARTESIAN_POINT('Ctrl Pts',(-193.161915373515,0.70954927612074,
125.935640861783));
#123328=CARTESIAN_POINT('Ctrl Pts',(-193.16968827378,0.573701552030352,
125.919685644582));
#123329=CARTESIAN_POINT('Ctrl Pts',(-193.177178609542,0.442792234891523,
125.904310439715));
#123330=CARTESIAN_POINT('Ctrl Pts',(-193.184668945304,0.311431737587399,
125.894221093707));
#123331=CARTESIAN_POINT('Ctrl Pts',(-193.192159281066,0.180078599274265,
125.889408454972));
#123332=CARTESIAN_POINT('Ctrl Pts',(-193.199933615185,0.0437451667967284,
125.884413343577));
#123333=CARTESIAN_POINT('Ctrl Pts',(-193.207707949304,-0.0930122009763956,
125.885087147901));
#123334=CARTESIAN_POINT('Ctrl Pts',(-193.215482283423,-0.229682792687816,
125.891476650155));
#123335=CARTESIAN_POINT('Ctrl Pts',(-193.22324703637,-0.366184950108441,
125.897858277918));
#123336=CARTESIAN_POINT('Ctrl Pts',(-193.231011789318,-0.502600157464022,
125.909941569895));
#123337=CARTESIAN_POINT('Ctrl Pts',(-193.238776542265,-0.638414542478167,
125.927721412698));
#123338=CARTESIAN_POINT('Ctrl Pts',(-193.24653358315,-0.774094034730837,
125.945483596311));
#123339=CARTESIAN_POINT('Ctrl Pts',(-193.254290624035,-0.909173507043042,
125.968931020864));
#123340=CARTESIAN_POINT('Ctrl Pts',(-193.26204766492,-1.04314141166046,
125.998006587974));
#123341=CARTESIAN_POINT('Ctrl Pts',(-193.26979885616,-1.17700829003943,
126.027060228972));
#123342=CARTESIAN_POINT('Ctrl Pts',(-193.2775500474,-1.30976488866881,126.061733482066));
#123343=CARTESIAN_POINT('Ctrl Pts',(-193.28530123864,-1.44090744824757,
126.101917764316));
#123344=CARTESIAN_POINT('Ctrl Pts',(-193.293049135417,-1.57199426873999,
126.142084967174));
#123345=CARTESIAN_POINT('Ctrl Pts',(-193.300797032194,-1.70146804157518,
126.187758426161));
#123346=CARTESIAN_POINT('Ctrl Pts',(-193.308544928971,-1.82883804278507,
126.238779112898));
#123347=CARTESIAN_POINT('Ctrl Pts',(-193.316291205055,-1.95618140093683,
126.289789127208));
#123348=CARTESIAN_POINT('Ctrl Pts',(-193.324037481139,-2.08142150007336,
126.346143999172));
#123349=CARTESIAN_POINT('Ctrl Pts',(-193.331783757224,-2.20408592746605,
126.407635894906));
#123350=CARTESIAN_POINT('Ctrl Pts',(-193.339530090489,-2.32675126033885,
126.469128244559));
#123351=CARTESIAN_POINT('Ctrl Pts',(-193.347276423754,-2.44684053402099,
126.53575751844));
#123352=CARTESIAN_POINT('Ctrl Pts',(-193.35502275702,-2.5639047132275,126.607269281415));
#123353=CARTESIAN_POINT('Ctrl Pts',(-193.362770825023,-2.68099510814607,
126.678797058955));
#123354=CARTESIAN_POINT('Ctrl Pts',(-193.370518893026,-2.79505872696956,
126.755209297555));
#123355=CARTESIAN_POINT('Ctrl Pts',(-193.378266961029,-2.90567470834559,
126.836207703201));
#123356=CARTESIAN_POINT('Ctrl Pts',(-193.38602326377,-3.01640825370252,
126.917292194916));
#123357=CARTESIAN_POINT('Ctrl Pts',(-193.393779566512,-3.12368652605522,
127.002972359134));
#123358=CARTESIAN_POINT('Ctrl Pts',(-193.401535869254,-3.22712059323985,
127.092908645738));
#123359=CARTESIAN_POINT('Ctrl Pts',(-193.409296311768,-3.33060986630048,
127.182892934046));
#123360=CARTESIAN_POINT('Ctrl Pts',(-193.417056754283,-3.4302505619723,
127.277137602611));
#123361=CARTESIAN_POINT('Ctrl Pts',(-193.424817196797,-3.52569070091577,
127.375266255497));
#123362=CARTESIAN_POINT('Ctrl Pts',(-193.432590097062,-3.62128404884331,
127.473552433207));
#123363=CARTESIAN_POINT('Ctrl Pts',(-193.440362997328,-3.71266310439815,
127.57573476299));
#123364=CARTESIAN_POINT('Ctrl Pts',(-193.448135897593,-3.79951569364077,
127.68140311605));
#123365=CARTESIAN_POINT('Ctrl Pts',(-193.455626233355,-3.88321097249688,
127.783230158314));
#123366=CARTESIAN_POINT('Ctrl Pts',(-193.463116569117,-3.9627029824913,
127.888293927058));
#123367=CARTESIAN_POINT('Ctrl Pts',(-193.470606904879,-4.03775157149843,
127.996203693646));
#123368=CARTESIAN_POINT('Ctrl Pts',(-193.47889361498,-4.12077934492612,
128.115586453127));
#123369=CARTESIAN_POINT('Ctrl Pts',(-193.48718032508,-4.19864109136327,
128.238845638589));
#123370=CARTESIAN_POINT('Ctrl Pts',(-193.495467035181,-4.27096326554449,
128.365496979133));
#123371=CARTESIAN_POINT('Ctrl Pts',(-193.503328207986,-4.33957156751243,
128.485644548189));
#123372=CARTESIAN_POINT('Ctrl Pts',(-193.511189380792,-4.40319473039249,
128.608844226595));
#123373=CARTESIAN_POINT('Ctrl Pts',(-193.519050553597,-4.46155570869261,
128.734649594082));
#123374=CARTESIAN_POINT('Ctrl Pts',(-193.526903815789,-4.51985795897289,
128.86032836499));
#123375=CARTESIAN_POINT('Ctrl Pts',(-193.534757077982,-4.57290840298805,
128.988607267093));
#123376=CARTESIAN_POINT('Ctrl Pts',(-193.542610340174,-4.62047497514472,
129.119013749244));
#123377=CARTESIAN_POINT('Ctrl Pts',(-193.550455704939,-4.66799371322391,
129.249289091533));
#123378=CARTESIAN_POINT('Ctrl Pts',(-193.558301069704,-4.71003943508657,
129.381687398499));
#123379=CARTESIAN_POINT('Ctrl Pts',(-193.566146434469,-4.74642766497959,
129.515715017094));
#123380=CARTESIAN_POINT('Ctrl Pts',(-193.567446765008,-4.75245883472166,
129.537929434235));
#123381=CARTESIAN_POINT('Ctrl Pts',(-193.568747095547,-4.75833469270917,
129.560188567407));
#123382=CARTESIAN_POINT('Ctrl Pts',(-193.570047426085,-4.76405452823409,
129.582490119308));
#123383=CARTESIAN_POINT('Origin',(213.235140564004,0.,130.804360617566));
#123384=CARTESIAN_POINT('',(-195.665141276266,-4.76405452823396,129.582490119308));
#123385=CARTESIAN_POINT('',(-195.319719904489,-4.76405452823413,129.582490119309));
#123386=CARTESIAN_POINT('',(213.235140564004,-4.76405452823405,129.582490119308));
#123387=CARTESIAN_POINT('',(-193.985140563976,-4.91824942956879,130.80672938227));
#123388=CARTESIAN_POINT('Ctrl Pts',(-193.985140564012,-4.91824942956849,
130.806729382913));
#123389=CARTESIAN_POINT('Ctrl Pts',(-193.992731428123,-4.91818520775937,
130.940072635538));
#123390=CARTESIAN_POINT('Ctrl Pts',(-194.000322292233,-4.91269870967798,
131.073280898492));
#123391=CARTESIAN_POINT('Ctrl Pts',(-194.007913156344,-4.90181963422078,
131.206041256965));
#123392=CARTESIAN_POINT('Ctrl Pts',(-194.015687490463,-4.89067761319646,
131.342010412719));
#123393=CARTESIAN_POINT('Ctrl Pts',(-194.023461824582,-4.87385628461547,
131.47773098801));
#123394=CARTESIAN_POINT('Ctrl Pts',(-194.031236158701,-4.85136951318697,
131.612690320732));
#123395=CARTESIAN_POINT('Ctrl Pts',(-194.039000911648,-4.82891045469462,
131.747483328137));
#123396=CARTESIAN_POINT('Ctrl Pts',(-194.046765664595,-4.80079990939565,
131.881516577692));
#123397=CARTESIAN_POINT('Ctrl Pts',(-194.054530417543,-4.76710364769382,
132.014280397818));
#123398=CARTESIAN_POINT('Ctrl Pts',(-194.062287458428,-4.73344085359424,
132.146912355046));
#123399=CARTESIAN_POINT('Ctrl Pts',(-194.070044499313,-4.69420347904607,
132.278277015427));
#123400=CARTESIAN_POINT('Ctrl Pts',(-194.077801540198,-4.64950864104312,
132.407873155517));
#123401=CARTESIAN_POINT('Ctrl Pts',(-194.085552731438,-4.604847507765,132.53737156615));
#123402=CARTESIAN_POINT('Ctrl Pts',(-194.093303922678,-4.55473722966819,
132.665103742946));
#123403=CARTESIAN_POINT('Ctrl Pts',(-194.101055113918,-4.49934512806033,
132.790582277175));
#123404=CARTESIAN_POINT('Ctrl Pts',(-194.108803010695,-4.44397656957337,
132.91600747968));
#123405=CARTESIAN_POINT('Ctrl Pts',(-194.116550907472,-4.38333081010158,
133.039180587809));
#123406=CARTESIAN_POINT('Ctrl Pts',(-194.124298804249,-4.3176237237225,
133.159633094977));
#123407=CARTESIAN_POINT('Ctrl Pts',(-194.132045080334,-4.25193038184923,
133.280060406077));
#123408=CARTESIAN_POINT('Ctrl Pts',(-194.139791356418,-4.18117800603018,
133.397767905166));
#123409=CARTESIAN_POINT('Ctrl Pts',(-194.147537632502,-4.10562877152469,
133.512311033089));
#123410=CARTESIAN_POINT('Ctrl Pts',(-194.155283965767,-4.03007897933201,
133.626855006542));
#123411=CARTESIAN_POINT('Ctrl Pts',(-194.163030299033,-3.94973247305859,
133.73823423585));
#123412=CARTESIAN_POINT('Ctrl Pts',(-194.170776632298,-3.86489494195318,
133.846032879688));
#123413=CARTESIAN_POINT('Ctrl Pts',(-194.178524700301,-3.78003841207102,
133.953855664285));
#123414=CARTESIAN_POINT('Ctrl Pts',(-194.186272768304,-3.69068909780753,
134.058095960657));
#123415=CARTESIAN_POINT('Ctrl Pts',(-194.194020836307,-3.59719291272284,
134.158371084329));
#123416=CARTESIAN_POINT('Ctrl Pts',(-194.201777139049,-3.50359735877989,
134.258752781596));
#123417=CARTESIAN_POINT('Ctrl Pts',(-194.209533441791,-3.40584639691667,
134.355160601374));
#123418=CARTESIAN_POINT('Ctrl Pts',(-194.217289744533,-3.30432313691359,
134.447248437601));
#123419=CARTESIAN_POINT('Ctrl Pts',(-194.225050187047,-3.20274569088985,
134.539385423878));
#123420=CARTESIAN_POINT('Ctrl Pts',(-194.232810629561,-3.09739223505416,
134.627197582094));
#123421=CARTESIAN_POINT('Ctrl Pts',(-194.240571072075,-2.9886781026604,
134.71037985218));
#123422=CARTESIAN_POINT('Ctrl Pts',(-194.248343972341,-2.87978945269014,
134.793695653831));
#123423=CARTESIAN_POINT('Ctrl Pts',(-194.256116872606,-2.76752966587593,
134.87236649073));
#123424=CARTESIAN_POINT('Ctrl Pts',(-194.263889772872,-2.65234287085514,
134.946130813741));
#123425=CARTESIAN_POINT('Ctrl Pts',(-194.271380108634,-2.54134340597169,
135.01721361781));
#123426=CARTESIAN_POINT('Ctrl Pts',(-194.278870444396,-2.427626312325,135.083740287406));
#123427=CARTESIAN_POINT('Ctrl Pts',(-194.286360780158,-2.31160794777514,
135.145518499777));
#123428=CARTESIAN_POINT('Ctrl Pts',(-194.294135114277,-2.19119071166986,
135.209639051847));
#123429=CARTESIAN_POINT('Ctrl Pts',(-194.301909448396,-2.06791280888925,
135.268847077811));
#123430=CARTESIAN_POINT('Ctrl Pts',(-194.309683782515,-1.94221305079689,
135.32287713605));
#123431=CARTESIAN_POINT('Ctrl Pts',(-194.317448535462,-1.81666820642226,
135.376840607072));
#123432=CARTESIAN_POINT('Ctrl Pts',(-194.325213288409,-1.68870780118061,
135.425638654508));
#123433=CARTESIAN_POINT('Ctrl Pts',(-194.332978041356,-1.55879618671472,
135.469051122925));
#123434=CARTESIAN_POINT('Ctrl Pts',(-194.340735082241,-1.42901360229611,
135.512420473466));
#123435=CARTESIAN_POINT('Ctrl Pts',(-194.348492123126,-1.29728403370762,
135.550414766694));
#123436=CARTESIAN_POINT('Ctrl Pts',(-194.356249164011,-1.1640924790234,
135.582861612939));
#123437=CARTESIAN_POINT('Ctrl Pts',(-194.364000355251,-1.03100136512646,
135.615283990765));
#123438=CARTESIAN_POINT('Ctrl Pts',(-194.371751546491,-0.896450837902563,
135.642167156194));
#123439=CARTESIAN_POINT('Ctrl Pts',(-194.379502737732,-0.760941409372517,
135.66338842506));
#123440=CARTESIAN_POINT('Ctrl Pts',(-194.387250634509,-0.625489575964244,
135.684600674321));
#123441=CARTESIAN_POINT('Ctrl Pts',(-194.394998531286,-0.489080037301672,
135.700155752914));
#123442=CARTESIAN_POINT('Ctrl Pts',(-194.402746428063,-0.352223646456436,
135.709982042562));
#123443=CARTESIAN_POINT('Ctrl Pts',(-194.410492704147,-0.215395883017882,
135.719806276762));
#123444=CARTESIAN_POINT('Ctrl Pts',(-194.418238980231,-0.0781218430315514,
135.723904077597));
#123445=CARTESIAN_POINT('Ctrl Pts',(-194.425985256315,0.0590827411620631,
135.722255725455));
#123446=CARTESIAN_POINT('Ctrl Pts',(-194.433731589581,0.196288338168563,
135.720607361145));
#123447=CARTESIAN_POINT('Ctrl Pts',(-194.441477922846,0.333424087422282,
135.713212763916));
#123448=CARTESIAN_POINT('Ctrl Pts',(-194.449224256111,0.469974897333745,
135.700104346396));
#123449=CARTESIAN_POINT('Ctrl Pts',(-194.456972324114,0.606556286852497,
135.686992993336));
#123450=CARTESIAN_POINT('Ctrl Pts',(-194.464720392117,0.742552087266234,
135.668165311142));
#123451=CARTESIAN_POINT('Ctrl Pts',(-194.47246846012,0.877453360560609,
135.643705476381));
#123452=CARTESIAN_POINT('Ctrl Pts',(-194.480224762862,1.0124980085334,135.619219645417));
#123453=CARTESIAN_POINT('Ctrl Pts',(-194.487981065604,1.1464454203106,135.589089774232));
#123454=CARTESIAN_POINT('Ctrl Pts',(-194.495737368346,1.27879732686596,
135.553451105154));
#123455=CARTESIAN_POINT('Ctrl Pts',(-194.50349781086,1.41121987361924,135.517793414645));
#123456=CARTESIAN_POINT('Ctrl Pts',(-194.511258253374,1.54204484557664,
135.476621184933));
#123457=CARTESIAN_POINT('Ctrl Pts',(-194.519018695888,1.67079108929357,
135.430118955227));
#123458=CARTESIAN_POINT('Ctrl Pts',(-194.526791596154,1.79974400791011,
135.383542076013));
#123459=CARTESIAN_POINT('Ctrl Pts',(-194.534564496419,1.92661116793729,
135.33161824699));
#123460=CARTESIAN_POINT('Ctrl Pts',(-194.542337396684,2.05093245830343,
135.274579752461));
#123461=CARTESIAN_POINT('Ctrl Pts',(-194.549827732446,2.17073435661631,
135.21961475088));
#123462=CARTESIAN_POINT('Ctrl Pts',(-194.557318068208,2.28817199468981,
135.159900629281));
#123463=CARTESIAN_POINT('Ctrl Pts',(-194.56480840397,2.40285851435058,135.095683726179));
#123464=CARTESIAN_POINT('Ctrl Pts',(-194.572582738089,2.52189340826435,
135.029032019675));
#123465=CARTESIAN_POINT('Ctrl Pts',(-194.580357072209,2.63834151504885,
134.957318212925));
#123466=CARTESIAN_POINT('Ctrl Pts',(-194.588131406328,2.75174232289214,
134.880768012676));
#123467=CARTESIAN_POINT('Ctrl Pts',(-194.595896159275,2.86500337437468,
134.804312153707));
#123468=CARTESIAN_POINT('Ctrl Pts',(-194.603660912222,2.97522427835457,
134.723031977348));
#123469=CARTESIAN_POINT('Ctrl Pts',(-194.611425665169,3.08196881842492,
134.637199156398));
#123470=CARTESIAN_POINT('Ctrl Pts',(-194.619182706054,3.18860733831322,
134.551451585816));
#123471=CARTESIAN_POINT('Ctrl Pts',(-194.626939746939,3.29177606275606,
134.461160612539));
#123472=CARTESIAN_POINT('Ctrl Pts',(-194.634696787824,3.39106780213559,
134.366641098356));
#123473=CARTESIAN_POINT('Ctrl Pts',(-194.642447979064,3.49028466484221,
134.272192862074));
#123474=CARTESIAN_POINT('Ctrl Pts',(-194.650199170304,3.58563007983292,
134.173522700424));
#123475=CARTESIAN_POINT('Ctrl Pts',(-194.657950361544,3.6767302904695,134.070985394556));
#123476=CARTESIAN_POINT('Ctrl Pts',(-194.665698258321,3.76779178108626,
133.968491669778));
#123477=CARTESIAN_POINT('Ctrl Pts',(-194.673446155098,3.85461139688462,
133.862134361516));
#123478=CARTESIAN_POINT('Ctrl Pts',(-194.681194051876,3.93685275481512,
133.752304553499));
#123479=CARTESIAN_POINT('Ctrl Pts',(-194.68894032796,4.01907690962669,133.64249771951));
#123480=CARTESIAN_POINT('Ctrl Pts',(-194.696686604044,4.09672447724247,
133.529220143312));
#123481=CARTESIAN_POINT('Ctrl Pts',(-194.704432880128,4.1695001010668,133.412895066199));
#123482=CARTESIAN_POINT('Ctrl Pts',(-194.712179213393,4.24227626210415,
133.2965691304));
#123483=CARTESIAN_POINT('Ctrl Pts',(-194.719925546659,4.31018020022778,
133.177195980241));
#123484=CARTESIAN_POINT('Ctrl Pts',(-194.727671879924,4.3729607655146,133.055226496682));
#123485=CARTESIAN_POINT('Ctrl Pts',(-194.735419947927,4.43575539007363,
132.933229698903));
#123486=CARTESIAN_POINT('Ctrl Pts',(-194.74316801593,4.49342417982122,132.808635758297));
#123487=CARTESIAN_POINT('Ctrl Pts',(-194.750916083933,4.54576286146099,
132.681918358319));
#123488=CARTESIAN_POINT('Ctrl Pts',(-194.758672386675,4.59815716927451,
132.555066281581));
#123489=CARTESIAN_POINT('Ctrl Pts',(-194.766428689417,4.64520990323737,
132.426086599126));
#123490=CARTESIAN_POINT('Ctrl Pts',(-194.774184992159,4.68676551997081,
132.295471620581));
#123491=CARTESIAN_POINT('Ctrl Pts',(-194.781945434673,4.72834331618813,
132.164786928889));
#123492=CARTESIAN_POINT('Ctrl Pts',(-194.789705877187,4.76441804619331,
132.032465578979));
#123493=CARTESIAN_POINT('Ctrl Pts',(-194.797466319701,4.79488489286097,
131.899012126821));
#123494=CARTESIAN_POINT('Ctrl Pts',(-194.805239219967,4.82540064761563,
131.765344443334));
#123495=CARTESIAN_POINT('Ctrl Pts',(-194.813012120232,4.85029045859629,
131.630541410641));
#123496=CARTESIAN_POINT('Ctrl Pts',(-194.820785020498,4.86950105189414,
131.495115688559));
#123497=CARTESIAN_POINT('Ctrl Pts',(-194.82827535626,4.88801329173705,131.36461303259));
#123498=CARTESIAN_POINT('Ctrl Pts',(-194.835765692022,4.90125202199734,
131.233532480348));
#123499=CARTESIAN_POINT('Ctrl Pts',(-194.843256027784,4.90921538795057,
131.102332658552));
#123500=CARTESIAN_POINT('Ctrl Pts',(-194.851030361903,4.91748068734433,
130.966158355635));
#123501=CARTESIAN_POINT('Ctrl Pts',(-194.858804696022,4.92008887680447,
130.82942420116));
#123502=CARTESIAN_POINT('Ctrl Pts',(-194.866579030141,4.91698093192857,
130.692639636767));
#123503=CARTESIAN_POINT('Ctrl Pts',(-194.874343783088,4.91387681731697,
130.556023647124));
#123504=CARTESIAN_POINT('Ctrl Pts',(-194.882108536035,4.90507059386854,
130.419357758287));
#123505=CARTESIAN_POINT('Ctrl Pts',(-194.889873288982,4.89055504197982,
130.283155817256));
#123506=CARTESIAN_POINT('Ctrl Pts',(-194.897630329867,4.87605390714187,
130.147089153914));
#123507=CARTESIAN_POINT('Ctrl Pts',(-194.905387370752,4.85585476974856,
130.011485907615));
#123508=CARTESIAN_POINT('Ctrl Pts',(-194.913144411637,4.83000243600482,
129.876858849003));
#123509=CARTESIAN_POINT('Ctrl Pts',(-194.920895602877,4.80416959770702,
129.742333313703));
#123510=CARTESIAN_POINT('Ctrl Pts',(-194.928646794117,4.77269212197063,
129.608782883225));
#123511=CARTESIAN_POINT('Ctrl Pts',(-194.936397985358,4.73566647163151,
129.476713777489));
#123512=CARTESIAN_POINT('Ctrl Pts',(-194.944145882135,4.69865655818142,
129.344700804647));
#123513=CARTESIAN_POINT('Ctrl Pts',(-194.951893778912,4.6561032655712,129.214168279979));
#123514=CARTESIAN_POINT('Ctrl Pts',(-194.959641675689,4.6081538003628,129.08561060238));
#123515=CARTESIAN_POINT('Ctrl Pts',(-194.967387951773,4.56021436514899,
128.957079816276));
#123516=CARTESIAN_POINT('Ctrl Pts',(-194.975134227857,4.50688113905005,
128.830523421655));
#123517=CARTESIAN_POINT('Ctrl Pts',(-194.982880503941,4.44835055949762,
128.706418682641));
#123518=CARTESIAN_POINT('Ctrl Pts',(-194.990626837206,4.38981954788566,
128.582313027514));
#123519=CARTESIAN_POINT('Ctrl Pts',(-194.998373170472,4.32609127303541,
128.460659417719));
#123520=CARTESIAN_POINT('Ctrl Pts',(-195.006119503737,4.25740932120014,
128.341912864971));
#123521=CARTESIAN_POINT('Ctrl Pts',(-195.01386757174,4.18871198851806,128.223139719757));
#123522=CARTESIAN_POINT('Ctrl Pts',(-195.021615639743,4.11505896709885,
128.107275265403));
#123523=CARTESIAN_POINT('Ctrl Pts',(-195.029363707746,4.03673836554418,
127.994747400299));
#123524=CARTESIAN_POINT('Ctrl Pts',(-195.037120010488,3.95833452392204,
127.88209993924));
#123525=CARTESIAN_POINT('Ctrl Pts',(-195.04487631323,3.87525341621253,127.772796472684));
#123526=CARTESIAN_POINT('Ctrl Pts',(-195.052632615971,3.78782516145076,
127.667233969058));
#123527=CARTESIAN_POINT('Ctrl Pts',(-195.060393058486,3.70035024359701,
127.561615123545));
#123528=CARTESIAN_POINT('Ctrl Pts',(-195.068153501,3.60852381712407,127.459741509747));
#123529=CARTESIAN_POINT('Ctrl Pts',(-195.075913943514,3.51271372304341,
127.361974038107));
#123530=CARTESIAN_POINT('Ctrl Pts',(-195.083686843779,3.41674982609412,
127.264049621441));
#123531=CARTESIAN_POINT('Ctrl Pts',(-195.091459744045,3.31678976767184,
127.170244786629));
#123532=CARTESIAN_POINT('Ctrl Pts',(-195.09923264431,3.21323606715028,127.080881459673));
#123533=CARTESIAN_POINT('Ctrl Pts',(-195.106722980072,3.11344680447899,
126.994766714744));
#123534=CARTESIAN_POINT('Ctrl Pts',(-195.114213315834,3.01032088056308,
126.912776355728));
#123535=CARTESIAN_POINT('Ctrl Pts',(-195.121703651596,2.90424314852822,
126.835159842003));
#123536=CARTESIAN_POINT('Ctrl Pts',(-195.129477985715,2.79414344704178,
126.75460047457));
#123537=CARTESIAN_POINT('Ctrl Pts',(-195.137252319834,2.68051492048119,
126.678497980498));
#123538=CARTESIAN_POINT('Ctrl Pts',(-195.145026653953,2.56375427239589,
126.60717738434));
#123539=CARTESIAN_POINT('Ctrl Pts',(-195.1527914069,2.44713752137415,126.535944684443));
#123540=CARTESIAN_POINT('Ctrl Pts',(-195.160556159847,2.32739665963895,
126.469482358469));
#123541=CARTESIAN_POINT('Ctrl Pts',(-195.168320912794,2.20496009885318,
126.408074227331));
#123542=CARTESIAN_POINT('Ctrl Pts',(-195.176077953679,2.0826451437853,126.346727087614));
#123543=CARTESIAN_POINT('Ctrl Pts',(-195.183834994564,1.95764016503764,
126.290424327054));
#123544=CARTESIAN_POINT('Ctrl Pts',(-195.191592035449,1.83040078992447,
126.23940541398));
#123545=CARTESIAN_POINT('Ctrl Pts',(-195.19934322669,1.70325736701403,126.188424974666));
#123546=CARTESIAN_POINT('Ctrl Pts',(-195.20709441793,1.57388326299252,126.142720596667));
#123547=CARTESIAN_POINT('Ctrl Pts',(-195.21484560917,1.44275651553619,126.102484747301));
#123548=CARTESIAN_POINT('Ctrl Pts',(-195.222593505947,1.31168550044528,
126.062265999245));
#123549=CARTESIAN_POINT('Ctrl Pts',(-195.230341402724,1.17886369649157,
126.027511271472));
#123550=CARTESIAN_POINT('Ctrl Pts',(-195.238089299501,1.04478662420943,
125.998363949613));
#123551=CARTESIAN_POINT('Ctrl Pts',(-195.245835575585,0.910737597960802,
125.969222724746));
#123552=CARTESIAN_POINT('Ctrl Pts',(-195.253581851669,0.775434207459803,
125.945686655733));
#123553=CARTESIAN_POINT('Ctrl Pts',(-195.261328127753,0.63938416776216,
125.927848447119));
#123554=CARTESIAN_POINT('Ctrl Pts',(-195.269074461019,0.503333123773844,
125.910010106827));
#123555=CARTESIAN_POINT('Ctrl Pts',(-195.276820794284,0.366535807238244,
125.897869761689));
#123556=CARTESIAN_POINT('Ctrl Pts',(-195.284567127549,0.229506696718071,
125.891468420635));
#123557=CARTESIAN_POINT('Ctrl Pts',(-195.292315195552,0.0924468994788774,
125.885065646046));
#123558=CARTESIAN_POINT('Ctrl Pts',(-195.300063263555,-0.0448444045725537,
125.884404451203));
#123559=CARTESIAN_POINT('Ctrl Pts',(-195.307811331558,-0.181851482666569,
125.889473731711));
#123560=CARTESIAN_POINT('Ctrl Pts',(-195.3155676343,-0.319004173513774,
125.89454839991));
#123561=CARTESIAN_POINT('Ctrl Pts',(-195.323323937042,-0.455871643647917,
125.905365695246));
#123562=CARTESIAN_POINT('Ctrl Pts',(-195.331080239784,-0.591941474886092,
125.921862450356));
#123563=CARTESIAN_POINT('Ctrl Pts',(-195.338840682298,-0.728083930690183,
125.938368010281));
#123564=CARTESIAN_POINT('Ctrl Pts',(-195.346601124812,-0.863427513682498,
125.960559006873));
#123565=CARTESIAN_POINT('Ctrl Pts',(-195.354361567326,-0.997469752634241,
125.98832104598));
#123566=CARTESIAN_POINT('Ctrl Pts',(-195.362134467592,-1.13172716808766,
126.016127651178));
#123567=CARTESIAN_POINT('Ctrl Pts',(-195.369907367857,-1.26467868554271,
126.049523074818));
#123568=CARTESIAN_POINT('Ctrl Pts',(-195.377680268122,-1.39583588798348,
126.088342674818));
#123569=CARTESIAN_POINT('Ctrl Pts',(-195.385170603885,-1.52222519575403,
126.12575108458));
#123570=CARTESIAN_POINT('Ctrl Pts',(-195.392660939647,-1.64694808775228,
126.168196053275));
#123571=CARTESIAN_POINT('Ctrl Pts',(-195.400151275409,-1.76958666422382,
126.215488631958));
#123572=CARTESIAN_POINT('Ctrl Pts',(-195.407925865569,-1.89687931172836,
126.264575939728));
#123573=CARTESIAN_POINT('Ctrl Pts',(-195.415700455729,-2.02232956017334,
126.319041551411));
#123574=CARTESIAN_POINT('Ctrl Pts',(-195.423475045889,-2.1454494812566,
126.378727376336));
#123575=CARTESIAN_POINT('Ctrl Pts',(-195.431239995709,-2.26841673604816,
126.438339192008));
#123576=CARTESIAN_POINT('Ctrl Pts',(-195.43900494553,-2.38905906452119,
126.503158172355));
#123577=CARTESIAN_POINT('Ctrl Pts',(-195.44676989535,-2.50690607821073,
126.57297727668));
#123578=CARTESIAN_POINT('Ctrl Pts',(-195.454527074191,-2.62463515337862,
126.642726507686));
#123579=CARTESIAN_POINT('Ctrl Pts',(-195.462284253032,-2.73957414685786,
126.717465706102));
#123580=CARTESIAN_POINT('Ctrl Pts',(-195.470041431874,-2.85127528719056,
126.796940961583));
#123581=CARTESIAN_POINT('Ctrl Pts',(-195.478170592057,-2.96833285167254,
126.880227307771));
#123582=CARTESIAN_POINT('Ctrl Pts',(-195.48629975224,-3.08183394409786,
126.968714999343));
#123583=CARTESIAN_POINT('Ctrl Pts',(-195.494428912423,-3.19129454302132,
127.0620588924));
#123584=CARTESIAN_POINT('Ctrl Pts',(-195.50217647144,-3.29561681384803,
127.151021011987));
#123585=CARTESIAN_POINT('Ctrl Pts',(-195.509924030457,-3.39626895266872,
127.244393515566));
#123586=CARTESIAN_POINT('Ctrl Pts',(-195.517671589474,-3.49286418306127,
127.341835114239));
#123587=CARTESIAN_POINT('Ctrl Pts',(-195.525417525999,-3.58943918449754,
127.43925630671));
#123588=CARTESIAN_POINT('Ctrl Pts',(-195.533163462523,-3.68195869289281,
127.540744621327));
#123589=CARTESIAN_POINT('Ctrl Pts',(-195.540909399048,-3.77007218189079,
127.645921318508));
#123590=CARTESIAN_POINT('Ctrl Pts',(-195.548655390858,-3.85818629978034,
127.751098766365));
#123591=CARTESIAN_POINT('Ctrl Pts',(-195.556401382667,-3.94189408507239,
127.859964349216));
#123592=CARTESIAN_POINT('Ctrl Pts',(-195.564147374477,-4.02088502556128,
127.972105919677));
#123593=CARTESIAN_POINT('Ctrl Pts',(-195.571895099012,-4.09989363577994,
128.084272575435));
#123594=CARTESIAN_POINT('Ctrl Pts',(-195.579642823547,-4.17418307720177,
128.199716357132));
#123595=CARTESIAN_POINT('Ctrl Pts',(-195.587390548081,-4.24348615363837,
128.317996137772));
#123596=CARTESIAN_POINT('Ctrl Pts',(-195.595145422041,-4.31285318138828,
128.436385064323));
#123597=CARTESIAN_POINT('Ctrl Pts',(-195.602900296001,-4.37722445952681,
128.557614877344));
#123598=CARTESIAN_POINT('Ctrl Pts',(-195.610655169961,-4.43637859937377,
128.681219551711));
#123599=CARTESIAN_POINT('Ctrl Pts',(-195.61841422265,-4.49556461454609,
128.804890830702));
#123600=CARTESIAN_POINT('Ctrl Pts',(-195.626173275339,-4.54952773652002,
128.930939161969));
#123601=CARTESIAN_POINT('Ctrl Pts',(-195.633932328028,-4.59809510986851,
129.05887947384));
#123602=CARTESIAN_POINT('Ctrl Pts',(-195.64170116025,-4.64672369767602,
129.186981042053));
#123603=CARTESIAN_POINT('Ctrl Pts',(-195.649469992472,-4.68994283555458,
129.316978981968));
#123604=CARTESIAN_POINT('Ctrl Pts',(-195.657238824693,-4.72762969271982,
129.448373688789));
#123605=CARTESIAN_POINT('Ctrl Pts',(-195.659872975218,-4.74040804237829,
129.492925228326));
#123606=CARTESIAN_POINT('Ctrl Pts',(-195.662507125742,-4.7525508024199,
129.537637266952));
#123607=CARTESIAN_POINT('Ctrl Pts',(-195.665141276266,-4.76405452823396,
129.582490119308));
#123608=CARTESIAN_POINT('Ctrl Pts',(-193.914998640423,-4.76405452823412,
129.582490119309));
#123609=CARTESIAN_POINT('Ctrl Pts',(-193.92267052425,-4.79777746561117,
129.713975340325));
#123610=CARTESIAN_POINT('Ctrl Pts',(-193.930342408077,-4.82602859703584,
129.84676320345));
#123611=CARTESIAN_POINT('Ctrl Pts',(-193.938014291904,-4.84873130167584,
129.980353441233));
#123612=CARTESIAN_POINT('Ctrl Pts',(-193.945868670583,-4.87197404665051,
130.117121455314));
#123613=CARTESIAN_POINT('Ctrl Pts',(-193.953723049261,-4.88940102937192,
130.254730049252));
#123614=CARTESIAN_POINT('Ctrl Pts',(-193.96157742794,-4.90098647655538,
130.392639086527));
#123615=CARTESIAN_POINT('Ctrl Pts',(-193.969431806619,-4.91257192373883,
130.530548123802));
#123616=CARTESIAN_POINT('Ctrl Pts',(-193.977286185297,-4.91831588080072,
130.668757158678));
#123617=CARTESIAN_POINT('Ctrl Pts',(-193.985140563975,-4.91824942956879,
130.806729382271));
#123618=CARTESIAN_POINT('',(-193.639859436047,-4.91824923219391,130.807108803159));
#123619=CARTESIAN_POINT('Ctrl Pts',(-193.570047426085,-4.76405452823409,
129.582490119308));
#123620=CARTESIAN_POINT('Ctrl Pts',(-193.577886143416,-4.79853512568151,
129.71692944544));
#123621=CARTESIAN_POINT('Ctrl Pts',(-193.585724860747,-4.82734183515294,
129.852911410386));
#123622=CARTESIAN_POINT('Ctrl Pts',(-193.593563578078,-4.85034802871446,
129.989923963893));
#123623=CARTESIAN_POINT('Ctrl Pts',(-193.601399678027,-4.87334654040656,
130.126890768305));
#123624=CARTESIAN_POINT('Ctrl Pts',(-193.609235777976,-4.8905483261116,
130.264887104432));
#123625=CARTESIAN_POINT('Ctrl Pts',(-193.617071877925,-4.90187780366035,
130.40339046845));
#123626=CARTESIAN_POINT('Ctrl Pts',(-193.624667730615,-4.91285993036604,
130.537647453052));
#123627=CARTESIAN_POINT('Ctrl Pts',(-193.632263583305,-4.91832451473222,
130.672380489236));
#123628=CARTESIAN_POINT('Ctrl Pts',(-193.639859435995,-4.91824923219442,
130.807108802231));
#123629=CARTESIAN_POINT('Ctrl Pts',(-193.639859436047,-4.91824923219391,
130.80710880316));
#123630=CARTESIAN_POINT('Ctrl Pts',(-193.648453682647,-4.91816405453979,
130.959545717499));
#123631=CARTESIAN_POINT('Ctrl Pts',(-193.657047929247,-4.91098784782448,
131.11172896582));
#123632=CARTESIAN_POINT('Ctrl Pts',(-193.665642175847,-4.89681553245056,
131.263033380711));
#123633=CARTESIAN_POINT('Ctrl Pts',(-193.674285738832,-4.88256189204551,
131.415206026086));
#123634=CARTESIAN_POINT('Ctrl Pts',(-193.682929301818,-4.86123170846623,
131.566489499949));
#123635=CARTESIAN_POINT('Ctrl Pts',(-193.691572864804,-4.83297164334981,
131.716264207359));
#123636=CARTESIAN_POINT('Ctrl Pts',(-193.700242045639,-4.8046278208643,
131.866482818043));
#123637=CARTESIAN_POINT('Ctrl Pts',(-193.708911226474,-4.76931309557723,
132.015183498403));
#123638=CARTESIAN_POINT('Ctrl Pts',(-193.717580407309,-4.7272241103825,
132.161760806426));
#123639=CARTESIAN_POINT('Ctrl Pts',(-193.726281692355,-4.6849792588291,
132.308880927995));
#123640=CARTESIAN_POINT('Ctrl Pts',(-193.734982977401,-4.63590999828547,
132.453861718932));
#123641=CARTESIAN_POINT('Ctrl Pts',(-193.743684262447,-4.5802623667498,
132.596113869059));
#123642=CARTESIAN_POINT('Ctrl Pts',(-193.745474351195,-4.56881414978355,
132.625378968644));
#123643=CARTESIAN_POINT('Ctrl Pts',(-193.747264439944,-4.55708766805062,
132.654528665305));
#123644=CARTESIAN_POINT('Ctrl Pts',(-193.749054528692,-4.5450853031912,
132.683557959309));
#123645=CARTESIAN_POINT('Ctrl Pts',(-193.756828862811,-4.49295917552469,
132.809631837505));
#123646=CARTESIAN_POINT('Ctrl Pts',(-193.76460319693,-4.4355008567645,132.933734912639));
#123647=CARTESIAN_POINT('Ctrl Pts',(-193.772377531049,-4.37288008339332,
133.055383238235));
#123648=CARTESIAN_POINT('Ctrl Pts',(-193.780142283997,-4.31033648452892,
133.17688164314));
#123649=CARTESIAN_POINT('Ctrl Pts',(-193.787907036944,-4.24264326728463,
133.295930973597));
#123650=CARTESIAN_POINT('Ctrl Pts',(-193.795671789891,-4.17001868196047,
133.412065979489));
#123651=CARTESIAN_POINT('Ctrl Pts',(-193.803428830776,-4.09746622839829,
133.528085638456));
#123652=CARTESIAN_POINT('Ctrl Pts',(-193.811185871661,-4.01999235975909,
133.641196403798));
#123653=CARTESIAN_POINT('Ctrl Pts',(-193.818942912546,-3.93786164135559,
133.750956748026));
#123654=CARTESIAN_POINT('Ctrl Pts',(-193.826694103786,-3.8557928583656,
133.860634321124));
#123655=CARTESIAN_POINT('Ctrl Pts',(-193.834445295026,-3.76907444885508,
133.966966190343));
#123656=CARTESIAN_POINT('Ctrl Pts',(-193.842196486266,-3.67801456681571,
134.069539312338));
#123657=CARTESIAN_POINT('Ctrl Pts',(-193.849944383043,-3.58699338765545,
134.172068838019));
#123658=CARTESIAN_POINT('Ctrl Pts',(-193.85769227982,-3.4916346650259,134.270842502153));
#123659=CARTESIAN_POINT('Ctrl Pts',(-193.865440176597,-3.39228701555218,
134.365480085741));
#123660=CARTESIAN_POINT('Ctrl Pts',(-193.873186452681,-3.29296014746504,
134.460097873187));
#123661=CARTESIAN_POINT('Ctrl Pts',(-193.880932728766,-3.18964629509992,
134.550581031482));
#123662=CARTESIAN_POINT('Ctrl Pts',(-193.88867900485,-3.0827308531471,134.636586282836));
#123663=CARTESIAN_POINT('Ctrl Pts',(-193.896425338115,-2.97581462196864,
134.722592169061));
#123664=CARTESIAN_POINT('Ctrl Pts',(-193.90417167138,-2.86529705278595,
134.804119837331));
#123665=CARTESIAN_POINT('Ctrl Pts',(-193.911918004646,-2.75159620769232,
134.880866642621));
#123666=CARTESIAN_POINT('Ctrl Pts',(-193.919666072649,-2.63786990008324,
134.957630634827));
#123667=CARTESIAN_POINT('Ctrl Pts',(-193.927414140652,-2.52095922202,135.029611414911));
#123668=CARTESIAN_POINT('Ctrl Pts',(-193.935162208655,-2.40131041503007,
135.096550193198));
#123669=CARTESIAN_POINT('Ctrl Pts',(-193.942918511396,-2.28153444386374,
135.163560114816));
#123670=CARTESIAN_POINT('Ctrl Pts',(-193.950674814138,-2.15901487224249,
135.225517138867));
#123671=CARTESIAN_POINT('Ctrl Pts',(-193.95843111688,-2.03422219292027,
135.2822086646));
#123672=CARTESIAN_POINT('Ctrl Pts',(-193.966191559394,-1.90936290798765,
135.338930448309));
#123673=CARTESIAN_POINT('Ctrl Pts',(-193.973952001908,-1.78222846013368,
135.390380987236));
#123674=CARTESIAN_POINT('Ctrl Pts',(-193.981712444423,-1.65330749395548,
135.436396605437));
#123675=CARTESIAN_POINT('Ctrl Pts',(-193.989485344688,-1.52417957239731,
135.482486091993));
#123676=CARTESIAN_POINT('Ctrl Pts',(-193.997258244953,-1.39325977518751,
135.523123107292));
#123677=CARTESIAN_POINT('Ctrl Pts',(-194.005031145219,-1.26105088175151,
135.5581942007));
#123678=CARTESIAN_POINT('Ctrl Pts',(-194.012521480981,-1.133648114606,135.591990371525));
#123679=CARTESIAN_POINT('Ctrl Pts',(-194.020011816743,-1.00504864850035,
135.620618198415));
#123680=CARTESIAN_POINT('Ctrl Pts',(-194.027502152505,-0.875707681015639,
135.644021671804));
#123681=CARTESIAN_POINT('Ctrl Pts',(-194.035276486624,-0.741462711436587,
135.668312495));
#123682=CARTESIAN_POINT('Ctrl Pts',(-194.043050820743,-0.605993654757619,
135.687051927619));
#123683=CARTESIAN_POINT('Ctrl Pts',(-194.050825154862,-0.469799415570403,
135.70012118888));
#123684=CARTESIAN_POINT('Ctrl Pts',(-194.058589907809,-0.333773023610957,
135.713174343443));
#123685=CARTESIAN_POINT('Ctrl Pts',(-194.066354660756,-0.197023612826312,
135.720571193658));
#123686=CARTESIAN_POINT('Ctrl Pts',(-194.074119413703,-0.0600605809332014,
135.722243880629));
#123687=CARTESIAN_POINT('Ctrl Pts',(-194.081876454588,0.0767664173457922,
135.723914906265));
#123688=CARTESIAN_POINT('Ctrl Pts',(-194.089633495473,0.213806226096077,
135.719873077956));
#123689=CARTESIAN_POINT('Ctrl Pts',(-194.097390536358,0.35054437172053,
135.710102325601));
#123690=CARTESIAN_POINT('Ctrl Pts',(-194.105141727599,0.487179402045514,
135.700338941446));
#123691=CARTESIAN_POINT('Ctrl Pts',(-194.112892918839,0.6235128336498,135.684855260145));
#123692=CARTESIAN_POINT('Ctrl Pts',(-194.120644110079,0.759030596709005,
135.663687280362));
#123693=CARTESIAN_POINT('Ctrl Pts',(-194.128392006856,0.894490761104039,
135.642528297535));
#123694=CARTESIAN_POINT('Ctrl Pts',(-194.136139903633,1.02913556100334,
135.615689881632));
#123695=CARTESIAN_POINT('Ctrl Pts',(-194.14388780041,1.16245667159326,135.583259816039));
#123696=CARTESIAN_POINT('Ctrl Pts',(-194.151634076494,1.29574989428092,
135.550836534117));
#123697=CARTESIAN_POINT('Ctrl Pts',(-194.159380352578,1.42771959875601,
135.512824021355));
#123698=CARTESIAN_POINT('Ctrl Pts',(-194.167126628662,1.55786866044568,
135.469360971189));
#123699=CARTESIAN_POINT('Ctrl Pts',(-194.174872961928,1.68801868286598,
135.425897600189));
#123700=CARTESIAN_POINT('Ctrl Pts',(-194.182619295193,1.81634766484947,
135.376983735339));
#123701=CARTESIAN_POINT('Ctrl Pts',(-194.190365628458,1.9423750097934,135.322807517091));
#123702=CARTESIAN_POINT('Ctrl Pts',(-194.198113696461,2.06843057768725,
135.268619166455));
#123703=CARTESIAN_POINT('Ctrl Pts',(-194.205861764464,2.19218312376924,
135.209166271782));
#123704=CARTESIAN_POINT('Ctrl Pts',(-194.213609832467,2.31317371650994,
135.144684386566));
#123705=CARTESIAN_POINT('Ctrl Pts',(-194.221366135209,2.43429289949258,
135.080133969235));
#123706=CARTESIAN_POINT('Ctrl Pts',(-194.229122437951,2.55264391970813,
135.010544068579));
#123707=CARTESIAN_POINT('Ctrl Pts',(-194.236878740693,2.66779359729971,
134.93619560758));
#123708=CARTESIAN_POINT('Ctrl Pts',(-194.244639183207,2.78300473374162,
134.861807464569));
#123709=CARTESIAN_POINT('Ctrl Pts',(-194.252399625721,2.8950108037929,134.782655925994));
#123710=CARTESIAN_POINT('Ctrl Pts',(-194.260160068235,3.00340997790441,
134.699063631548));
#123711=CARTESIAN_POINT('Ctrl Pts',(-194.2679329685,3.11198316399314,134.615337147331));
#123712=CARTESIAN_POINT('Ctrl Pts',(-194.275705868766,3.2169375841494,134.527155913481));
#123713=CARTESIAN_POINT('Ctrl Pts',(-194.283478769031,3.3179060245828,134.434881609729));
#123714=CARTESIAN_POINT('Ctrl Pts',(-194.290969104794,3.41520400788394,
134.345961709343));
#123715=CARTESIAN_POINT('Ctrl Pts',(-194.298459440556,3.50880056207708,
134.253241376088));
#123716=CARTESIAN_POINT('Ctrl Pts',(-194.305949776318,3.59840251931591,
134.157073306044));
#123717=CARTESIAN_POINT('Ctrl Pts',(-194.313724110437,3.69140176199619,
134.057258994396));
#123718=CARTESIAN_POINT('Ctrl Pts',(-194.321498444556,3.78039211153777,
133.953414161395));
#123719=CARTESIAN_POINT('Ctrl Pts',(-194.329272778675,3.8650039641869,133.845894345691));
#123720=CARTESIAN_POINT('Ctrl Pts',(-194.337037531622,3.94951154028939,
133.73850703855));
#123721=CARTESIAN_POINT('Ctrl Pts',(-194.344802284569,4.02965111668345,
133.627454064531));
#123722=CARTESIAN_POINT('Ctrl Pts',(-194.352567037516,4.10509025985185,
133.513127314971));
#123723=CARTESIAN_POINT('Ctrl Pts',(-194.360324078401,4.18045447579975,
133.39891411635));
#123724=CARTESIAN_POINT('Ctrl Pts',(-194.368081119286,4.25112733518645,
133.281433937151));
#123725=CARTESIAN_POINT('Ctrl Pts',(-194.375838160171,4.31681723223276,
133.1611109323));
#123726=CARTESIAN_POINT('Ctrl Pts',(-194.383589351411,4.38245759201679,
133.040878663962));
#123727=CARTESIAN_POINT('Ctrl Pts',(-194.391340542651,4.44312228232928,
132.917808178837));
#123728=CARTESIAN_POINT('Ctrl Pts',(-194.399091733892,4.49856372256806,
132.792351436583));
#123729=CARTESIAN_POINT('Ctrl Pts',(-194.406839630669,4.55398159871571,
132.666948016791));
#123730=CARTESIAN_POINT('Ctrl Pts',(-194.414587527446,4.60418048254142,
132.539160713937));
#123731=CARTESIAN_POINT('Ctrl Pts',(-194.422335424223,4.64895946671369,
132.409464645146));
#123732=CARTESIAN_POINT('Ctrl Pts',(-194.430081700307,4.69372908408779,
132.279795705977));
#123733=CARTESIAN_POINT('Ctrl Pts',(-194.437827976391,4.73308092933866,
132.14821916437));
#123734=CARTESIAN_POINT('Ctrl Pts',(-194.445574252475,4.76686298120744,
132.015228232499));
#123735=CARTESIAN_POINT('Ctrl Pts',(-194.45332058574,4.80064528244769,131.882236318919));
#123736=CARTESIAN_POINT('Ctrl Pts',(-194.461066919006,4.82885761200875,
131.747830373172));
#123737=CARTESIAN_POINT('Ctrl Pts',(-194.468813252271,4.85139848357786,
131.612516429299));
#123738=CARTESIAN_POINT('Ctrl Pts',(-194.476561320274,4.87394440301884,
131.477172182808));
#123739=CARTESIAN_POINT('Ctrl Pts',(-194.484309388277,4.89081627291814,
131.340919919146));
#123740=CARTESIAN_POINT('Ctrl Pts',(-194.49205745628,4.90196420739985,131.204273072824));
#123741=CARTESIAN_POINT('Ctrl Pts',(-194.499813759022,4.913123990039,131.067480996608));
#123742=CARTESIAN_POINT('Ctrl Pts',(-194.507570061764,4.91854765303973,
130.930293890293));
#123743=CARTESIAN_POINT('Ctrl Pts',(-194.515326364506,4.91823740056867,
130.793228046095));
#123744=CARTESIAN_POINT('Ctrl Pts',(-194.52308680702,4.91792698250651,130.656089045728));
#123745=CARTESIAN_POINT('Ctrl Pts',(-194.530847249534,4.91187656817852,
130.519071826834));
#123746=CARTESIAN_POINT('Ctrl Pts',(-194.538607692048,4.90014040480876,
130.382688854626));
#123747=CARTESIAN_POINT('Ctrl Pts',(-194.546380592313,4.88838540150768,
130.246086948365));
#123748=CARTESIAN_POINT('Ctrl Pts',(-194.554153492579,4.8709264597954,130.110121711381));
#123749=CARTESIAN_POINT('Ctrl Pts',(-194.561926392844,4.84786938305054,
129.975297587766));
#123750=CARTESIAN_POINT('Ctrl Pts',(-194.569416728606,4.8256504891227,129.845374660647));
#123751=CARTESIAN_POINT('Ctrl Pts',(-194.576907064368,4.79823347054425,
129.71651162387));
#123752=CARTESIAN_POINT('Ctrl Pts',(-194.58439740013,4.76575659613236,129.589145768693));
#123753=CARTESIAN_POINT('Ctrl Pts',(-194.592171734249,4.73204835115597,
129.456950798405));
#123754=CARTESIAN_POINT('Ctrl Pts',(-194.599946068368,4.69278220975143,
129.325950028211));
#123755=CARTESIAN_POINT('Ctrl Pts',(-194.607720402487,4.64805751679649,
129.196646593539));
#123756=CARTESIAN_POINT('Ctrl Pts',(-194.615485155434,4.60338794302845,
129.067502513795));
#123757=CARTESIAN_POINT('Ctrl Pts',(-194.623249908382,4.55327332936175,
128.940051973427));
#123758=CARTESIAN_POINT('Ctrl Pts',(-194.631014661329,4.49786369664073,
128.814786485009));
#123759=CARTESIAN_POINT('Ctrl Pts',(-194.638771702214,4.44250909754792,
128.689645412039));
#123760=CARTESIAN_POINT('Ctrl Pts',(-194.646528743099,4.38187010235564,
128.566685427407));
#123761=CARTESIAN_POINT('Ctrl Pts',(-194.654285783984,4.31614594456795,
128.446381133412));
#123762=CARTESIAN_POINT('Ctrl Pts',(-194.662036975224,4.250471349879,128.326167561822));
#123763=CARTESIAN_POINT('Ctrl Pts',(-194.669788166464,4.17971941213704,
128.208606036374));
#123764=CARTESIAN_POINT('Ctrl Pts',(-194.677539357704,4.10413655444054,
128.094149148879));
#123765=CARTESIAN_POINT('Ctrl Pts',(-194.685287254481,4.0285858214747,127.979740908613));
#123766=CARTESIAN_POINT('Ctrl Pts',(-194.693035151258,3.94820846734261,
127.868435007373));
#123767=CARTESIAN_POINT('Ctrl Pts',(-194.700783048035,3.86329562621768,
127.760657286598));
#123768=CARTESIAN_POINT('Ctrl Pts',(-194.708529324119,3.77840054702884,
127.652902110599));
#123769=CARTESIAN_POINT('Ctrl Pts',(-194.716275600204,3.68897210971447,
127.548673954013));
#123770=CARTESIAN_POINT('Ctrl Pts',(-194.724021876288,3.59534309643996,
127.448367309858));
#123771=CARTESIAN_POINT('Ctrl Pts',(-194.731768209553,3.50171339201721,
127.348059925262));
#123772=CARTESIAN_POINT('Ctrl Pts',(-194.739514542818,3.40388331653783,
127.251674396663));
#123773=CARTESIAN_POINT('Ctrl Pts',(-194.747260876084,3.3022237549426,127.159569631132));
#123774=CARTESIAN_POINT('Ctrl Pts',(-194.755008944087,3.20054142739355,
127.067444239377));
#123775=CARTESIAN_POINT('Ctrl Pts',(-194.76275701209,3.09502819690908,126.979601780738));
#123776=CARTESIAN_POINT('Ctrl Pts',(-194.770505080093,2.98608906594972,
126.896361749511));
#123777=CARTESIAN_POINT('Ctrl Pts',(-194.778261382835,2.87703415318544,
126.813033249789));
#123778=CARTESIAN_POINT('Ctrl Pts',(-194.786017685576,2.76454637763411,
126.734317186555));
#123779=CARTESIAN_POINT('Ctrl Pts',(-194.793773988318,2.6490613019644,126.660490773937));
#123780=CARTESIAN_POINT('Ctrl Pts',(-194.801534430832,2.53351458843263,
126.58662495794));
#123781=CARTESIAN_POINT('Ctrl Pts',(-194.809294873347,2.41496772491371,
126.517654189227));
#123782=CARTESIAN_POINT('Ctrl Pts',(-194.817055315861,2.29388118485612,
126.453809828038));
#123783=CARTESIAN_POINT('Ctrl Pts',(-194.824828216126,2.17260026593488,
126.389862978213));
#123784=CARTESIAN_POINT('Ctrl Pts',(-194.832601116392,2.04877187687075,
126.331059148613));
#123785=CARTESIAN_POINT('Ctrl Pts',(-194.840374016657,1.92287761007517,
126.277581988213));
#123786=CARTESIAN_POINT('Ctrl Pts',(-194.847864352419,1.80155991698648,
126.226048857294));
#123787=CARTESIAN_POINT('Ctrl Pts',(-194.855354688181,1.67832422631585,
126.179461952482));
#123788=CARTESIAN_POINT('Ctrl Pts',(-194.862845023943,1.55361318125574,
126.13794131091));
#123789=CARTESIAN_POINT('Ctrl Pts',(-194.870619358062,1.42417367901689,
126.094846401594));
#123790=CARTESIAN_POINT('Ctrl Pts',(-194.878393692181,1.29273471235955,
126.05707300227));
#123791=CARTESIAN_POINT('Ctrl Pts',(-194.886168026301,1.15977328170358,
126.024809488271));
#123792=CARTESIAN_POINT('Ctrl Pts',(-194.893932779248,1.02697571412778,
125.992585736169));
#123793=CARTESIAN_POINT('Ctrl Pts',(-194.901697532195,0.892659792124973,
125.965858449745));
#123794=CARTESIAN_POINT('Ctrl Pts',(-194.909462285142,0.757320129074038,
125.944767086765));
#123795=CARTESIAN_POINT('Ctrl Pts',(-194.917219326027,0.6221148872844,125.923696672025));
#123796=CARTESIAN_POINT('Ctrl Pts',(-194.924976366912,0.485888311715355,
125.908251100908));
#123797=CARTESIAN_POINT('Ctrl Pts',(-194.932733407797,0.349147389297095,
125.89851928676));
#123798=CARTESIAN_POINT('Ctrl Pts',(-194.940484599037,0.212509584271935,
125.888794811448));
#123799=CARTESIAN_POINT('Ctrl Pts',(-194.948235790277,0.0753585928360218,
125.884775544365));
#123800=CARTESIAN_POINT('Ctrl Pts',(-194.955986981517,-0.0617916090006001,
125.886498799707));
#123801=CARTESIAN_POINT('Ctrl Pts',(-194.963734878294,-0.198883518342653,
125.888221322619));
#123802=CARTESIAN_POINT('Ctrl Pts',(-194.971482775071,-0.335974248637008,
125.895681508637));
#123803=CARTESIAN_POINT('Ctrl Pts',(-194.979230671849,-0.472548162288011,
125.908864596036));
#123804=CARTESIAN_POINT('Ctrl Pts',(-194.986976947933,-0.60909350762047,
125.922044925817));
#123805=CARTESIAN_POINT('Ctrl Pts',(-194.994723224017,-0.745121862430249,
125.940945738326));
#123806=CARTESIAN_POINT('Ctrl Pts',(-195.002469500101,-0.880121451680396,
125.965500287613));
#123807=CARTESIAN_POINT('Ctrl Pts',(-195.010215833366,-1.01512203746703,
125.990055018157));
#123808=CARTESIAN_POINT('Ctrl Pts',(-195.017962166632,-1.14909345788622,
126.020263498794));
#123809=CARTESIAN_POINT('Ctrl Pts',(-195.025708499897,-1.28153328188549,
126.056007691559));
#123810=CARTESIAN_POINT('Ctrl Pts',(-195.0334565679,-1.41400276486489,126.091759888988));
#123811=CARTESIAN_POINT('Ctrl Pts',(-195.041204635903,-1.54493959152582,
126.133050163519));
#123812=CARTESIAN_POINT('Ctrl Pts',(-195.048952703906,-1.67385604854705,
126.179710469583));
#123813=CARTESIAN_POINT('Ctrl Pts',(-195.056709006648,-1.80290951951275,
126.226420366775));
#123814=CARTESIAN_POINT('Ctrl Pts',(-195.06446530939,-1.92993796321751,
126.278511563241));
#123815=CARTESIAN_POINT('Ctrl Pts',(-195.072221612131,-2.0544727193047,
126.335767448779));
#123816=CARTESIAN_POINT('Ctrl Pts',(-195.079982054646,-2.17907394334121,
126.393053893507));
#123817=CARTESIAN_POINT('Ctrl Pts',(-195.08774249716,-2.30117847981346,
126.455510342012));
#123818=CARTESIAN_POINT('Ctrl Pts',(-195.095502939674,-2.42034278165234,
126.522874440804));
#123819=CARTESIAN_POINT('Ctrl Pts',(-195.10327583994,-2.53969837660744,
126.590346678427));
#123820=CARTESIAN_POINT('Ctrl Pts',(-195.111048740205,-2.65610397282664,
126.662742102887));
#123821=CARTESIAN_POINT('Ctrl Pts',(-195.11882164047,-2.76914474876468,
126.739754803605));
#123822=CARTESIAN_POINT('Ctrl Pts',(-195.126311976232,-2.87807620776515,
126.813967898668));
#123823=CARTESIAN_POINT('Ctrl Pts',(-195.133802311994,-2.98388299120046,
126.892468215446));
#123824=CARTESIAN_POINT('Ctrl Pts',(-195.141292647756,-3.08622484897237,
126.974948228689));
#123825=CARTESIAN_POINT('Ctrl Pts',(-195.148964038384,-3.19104049321887,
127.059421931958));
#123826=CARTESIAN_POINT('Ctrl Pts',(-195.156635429012,-3.29257225117811,
127.148353103153));
#123827=CARTESIAN_POINT('Ctrl Pts',(-195.164306819639,-3.39040972582631,
127.241453805211));
#123828=CARTESIAN_POINT('Ctrl Pts',(-195.171969427545,-3.48813518957756,
127.334447919347));
#123829=CARTESIAN_POINT('Ctrl Pts',(-195.17963203545,-3.58217448966821,
127.431601801204));
#123830=CARTESIAN_POINT('Ctrl Pts',(-195.187294643356,-3.67214823682183,
127.532585810324));
#123831=CARTESIAN_POINT('Ctrl Pts',(-195.194950242633,-3.76203968920446,
127.633477454101));
#123832=CARTESIAN_POINT('Ctrl Pts',(-195.20260584191,-3.84787271682651,
127.738191961579));
#123833=CARTESIAN_POINT('Ctrl Pts',(-195.210261441187,-3.92930333398827,
127.846361568883));
#123834=CARTESIAN_POINT('Ctrl Pts',(-195.217911799506,-4.01067820443681,
127.954457124187));
#123835=CARTESIAN_POINT('Ctrl Pts',(-195.225562157824,-4.0876564179061,
128.066002754977));
#123836=CARTESIAN_POINT('Ctrl Pts',(-195.233212516142,-4.15993336229173,
128.180596625933));
#123837=CARTESIAN_POINT('Ctrl Pts',(-195.24086026656,-4.23218566846759,
128.295151433424));
#123838=CARTESIAN_POINT('Ctrl Pts',(-195.248508016977,-4.29973967457936,
128.412752077692));
#123839=CARTESIAN_POINT('Ctrl Pts',(-195.256155767394,-4.36233354812221,
128.532966975454));
#123840=CARTESIAN_POINT('Ctrl Pts',(-195.263801822143,-4.42491354327928,
128.65315521903));
#123841=CARTESIAN_POINT('Ctrl Pts',(-195.271447876892,-4.48253541118757,
128.775956204889));
#123842=CARTESIAN_POINT('Ctrl Pts',(-195.279093931642,-4.53498317575593,
128.900913571255));
#123843=CARTESIAN_POINT('Ctrl Pts',(-195.286742468474,-4.58744796606283,
129.025911501627));
#123844=CARTESIAN_POINT('Ctrl Pts',(-195.294391005307,-4.63473514030973,
129.153066840563));
#123845=CARTESIAN_POINT('Ctrl Pts',(-195.30203954214,-4.67667684027603,
129.281903132404));
#123846=CARTESIAN_POINT('Ctrl Pts',(-195.307932996256,-4.70899432657831,
129.38117581568));
#123847=CARTESIAN_POINT('Ctrl Pts',(-195.313826450373,-4.73813905169708,
129.481446069613));
#123848=CARTESIAN_POINT('Ctrl Pts',(-195.319719904489,-4.76405452823413,
129.582490119309));
#123849=CARTESIAN_POINT('Origin',(213.235140564004,0.,130.804360617566));
#123850=CARTESIAN_POINT('',(-197.415422870675,-4.76405452823413,129.582490119309));
#123851=CARTESIAN_POINT('',(-197.069830899744,-4.76405452823391,129.582490119308));
#123852=CARTESIAN_POINT('',(213.235140564004,-4.76405452823405,129.582490119308));
#123853=CARTESIAN_POINT('',(-195.735140564062,-4.91824801533315,130.799942227414));
#123854=CARTESIAN_POINT('Ctrl Pts',(-195.735140564062,-4.91824801533315,
130.799942227414));
#123855=CARTESIAN_POINT('Ctrl Pts',(-195.742788954033,-4.91836917860973,
130.934812853151));
#123856=CARTESIAN_POINT('Ctrl Pts',(-195.750437344004,-4.91293844047973,
131.069862221547));
#123857=CARTESIAN_POINT('Ctrl Pts',(-195.758085733975,-4.90193846711678,
131.204588461551));
#123858=CARTESIAN_POINT('Ctrl Pts',(-195.765727802631,-4.89094758511626,
131.339203351733));
#123859=CARTESIAN_POINT('Ctrl Pts',(-195.773369871288,-4.87439665663672,
131.473495244947));
#123860=CARTESIAN_POINT('Ctrl Pts',(-195.781011939945,-4.85232041130353,
131.606962441977));
#123861=CARTESIAN_POINT('Ctrl Pts',(-195.788650174382,-4.83025524218319,
131.740362675125));
#123862=CARTESIAN_POINT('Ctrl Pts',(-195.796288408819,-4.80267033378295,
131.872938638019));
#123863=CARTESIAN_POINT('Ctrl Pts',(-195.803926643255,-4.7696521975637,
132.00419434637));
#123864=CARTESIAN_POINT('Ctrl Pts',(-195.811563004816,-4.73664215730885,
132.13541787115));
#123865=CARTESIAN_POINT('Ctrl Pts',(-195.819199366377,-4.69820163590381,
132.265321394214));
#123866=CARTESIAN_POINT('Ctrl Pts',(-195.826835727938,-4.65446802695667,
132.393420228952));
#123867=CARTESIAN_POINT('Ctrl Pts',(-195.834471981253,-4.6107350379391,
132.521517247872));
#123868=CARTESIAN_POINT('Ctrl Pts',(-195.842108234567,-4.56170924103285,
132.647809247807));
#123869=CARTESIAN_POINT('Ctrl Pts',(-195.849744487881,-4.50757738476626,
132.771828325775));
#123870=CARTESIAN_POINT('Ctrl Pts',(-195.857382397285,-4.4534337888199,
132.895874299998));
#123871=CARTESIAN_POINT('Ctrl Pts',(-195.865020306688,-4.39418209327545,
133.01764600283));
#123872=CARTESIAN_POINT('Ctrl Pts',(-195.872658216092,-4.33005626833118,
133.136697594846));
#123873=CARTESIAN_POINT('Ctrl Pts',(-195.880303983217,-4.26586447207508,
133.255871664657));
#123874=CARTESIAN_POINT('Ctrl Pts',(-195.887949750342,-4.19678872589688,
133.37231968092));
#123875=CARTESIAN_POINT('Ctrl Pts',(-195.895595517468,-4.12310800759558,
133.485622152777));
#123876=CARTESIAN_POINT('Ctrl Pts',(-195.903245518399,-4.04938648895914,
133.59898736532));
#123877=CARTESIAN_POINT('Ctrl Pts',(-195.91089551933,-3.9710551549251,133.709203237835));
#123878=CARTESIAN_POINT('Ctrl Pts',(-195.918545520261,-3.88843420921999,
133.815882236792));
#123879=CARTESIAN_POINT('Ctrl Pts',(-195.926207035089,-3.8056889120232,
133.922721796641));
#123880=CARTESIAN_POINT('Ctrl Pts',(-195.933868549917,-3.71864137075232,
134.026013545911));
#123881=CARTESIAN_POINT('Ctrl Pts',(-195.941530064745,-3.62765000128713,
134.125405412606));
#123882=CARTESIAN_POINT('Ctrl Pts',(-195.946702217508,-3.56622334173219,
134.192503098836));
#123883=CARTESIAN_POINT('Ctrl Pts',(-195.951874370271,-3.50300009789946,
134.257824245905));
#123884=CARTESIAN_POINT('Ctrl Pts',(-195.957046523035,-3.43809892864949,
134.321271025768));
#123885=CARTESIAN_POINT('Ctrl Pts',(-195.964820857154,-3.34054508645473,
134.416638755225));
#123886=CARTESIAN_POINT('Ctrl Pts',(-195.972595191273,-3.23886568121659,
134.508095467405));
#123887=CARTESIAN_POINT('Ctrl Pts',(-195.980369525392,-3.13340727972664,
134.595263133044));
#123888=CARTESIAN_POINT('Ctrl Pts',(-195.988134278339,-3.02807884629143,
134.682323372325));
#123889=CARTESIAN_POINT('Ctrl Pts',(-195.995899031286,-2.91898098165016,
134.765104835671));
#123890=CARTESIAN_POINT('Ctrl Pts',(-196.003663784233,-2.80649748679672,
134.843265780986));
#123891=CARTESIAN_POINT('Ctrl Pts',(-196.011420825118,-2.69412571213581,
134.921349095749));
#123892=CARTESIAN_POINT('Ctrl Pts',(-196.019177866003,-2.5783753180853,
134.994820803471));
#123893=CARTESIAN_POINT('Ctrl Pts',(-196.026934906888,-2.45966333968881,
135.063379203801));
#123894=CARTESIAN_POINT('Ctrl Pts',(-196.034686098128,-2.34104088291883,
135.131885903706));
#123895=CARTESIAN_POINT('Ctrl Pts',(-196.042437289368,-2.21946162434935,
135.195486476388));
#123896=CARTESIAN_POINT('Ctrl Pts',(-196.050188480608,-2.09537145223453,
135.253922566754));
#123897=CARTESIAN_POINT('Ctrl Pts',(-196.057936377386,-1.9713340217529,
135.312333820223));
#123898=CARTESIAN_POINT('Ctrl Pts',(-196.065684274163,-1.84478815328316,
135.365584790931));
#123899=CARTESIAN_POINT('Ctrl Pts',(-196.07343217094,-1.71620400590661,
135.413463227902));
#123900=CARTESIAN_POINT('Ctrl Pts',(-196.081178447024,-1.58764675556175,
135.461331649737));
#123901=CARTESIAN_POINT('Ctrl Pts',(-196.088924723108,-1.45705244052956,
135.503829636831));
#123902=CARTESIAN_POINT('Ctrl Pts',(-196.096670999192,-1.32491048285849,
135.540793375973));
#123903=CARTESIAN_POINT('Ctrl Pts',(-196.104417332458,-1.19276754974533,
135.577757387973));
#123904=CARTESIAN_POINT('Ctrl Pts',(-196.112163665723,-1.05907732770887,
135.60918696518));
#123905=CARTESIAN_POINT('Ctrl Pts',(-196.119909998988,-0.92434326967486,
135.634968507087));
#123906=CARTESIAN_POINT('Ctrl Pts',(-196.127658066991,-0.789579038882551,
135.660755822592));
#123907=CARTESIAN_POINT('Ctrl Pts',(-196.135406134994,-0.653770890862492,
135.680892512449));
#123908=CARTESIAN_POINT('Ctrl Pts',(-196.143154202997,-0.517430915145343,
135.695316384137));
#123909=CARTESIAN_POINT('Ctrl Pts',(-196.150910505739,-0.380946035680092,
135.709755585687));
#123910=CARTESIAN_POINT('Ctrl Pts',(-196.158666808481,-0.243928588819814,
135.718469799092));
#123911=CARTESIAN_POINT('Ctrl Pts',(-196.166423111223,-0.106894770994205,
135.721448838295));
#123912=CARTESIAN_POINT('Ctrl Pts',(-196.174183553737,0.0302121859059867,
135.724429467501));
#123913=CARTESIAN_POINT('Ctrl Pts',(-196.181943996251,0.167335140487332,
135.721668830999));
#123914=CARTESIAN_POINT('Ctrl Pts',(-196.189704438765,0.303960473328762,
135.713208862639));
#123915=CARTESIAN_POINT('Ctrl Pts',(-196.197477339031,0.440805129283496,
135.704735313586));
#123916=CARTESIAN_POINT('Ctrl Pts',(-196.205250239296,0.577150178099871,
135.690544190408));
#123917=CARTESIAN_POINT('Ctrl Pts',(-196.213023139562,0.712488781964307,
135.670729160748));
#123918=CARTESIAN_POINT('Ctrl Pts',(-196.220513475324,0.842907486683093,
135.651634457327));
#123919=CARTESIAN_POINT('Ctrl Pts',(-196.228003811086,0.972391346940213,
135.627317691741));
#123920=CARTESIAN_POINT('Ctrl Pts',(-196.235494146848,1.10049987933717,
135.597906599204));
#123921=CARTESIAN_POINT('Ctrl Pts',(-196.243268480967,1.23346568567565,
135.567380376155));
#123922=CARTESIAN_POINT('Ctrl Pts',(-196.251042815086,1.3653710100103,135.531269199705));
#123923=CARTESIAN_POINT('Ctrl Pts',(-196.258817149205,1.49571047779856,
135.48966031226));
#123924=CARTESIAN_POINT('Ctrl Pts',(-196.266581902152,1.62588931384153,
135.448102704051));
#123925=CARTESIAN_POINT('Ctrl Pts',(-196.274346655099,1.75450576414976,
135.401060983704));
#123926=CARTESIAN_POINT('Ctrl Pts',(-196.282111408047,1.88106485760708,
135.348673333915));
#123927=CARTESIAN_POINT('Ctrl Pts',(-196.289868448932,2.00749825078861,
135.296337716279));
#123928=CARTESIAN_POINT('Ctrl Pts',(-196.297625489817,2.1318779946668,135.238666884213));
#123929=CARTESIAN_POINT('Ctrl Pts',(-196.305382530702,2.25372484256268,
135.1758486247));
#123930=CARTESIAN_POINT('Ctrl Pts',(-196.313133721942,2.37547980480323,
135.113077736925));
#123931=CARTESIAN_POINT('Ctrl Pts',(-196.320884913182,2.49470532685751,
135.045167326451));
#123932=CARTESIAN_POINT('Ctrl Pts',(-196.328636104422,2.61094303377791,
134.972352884457));
#123933=CARTESIAN_POINT('Ctrl Pts',(-196.336384001199,2.72713133657197,
134.899569390544));
#123934=CARTESIAN_POINT('Ctrl Pts',(-196.344131897976,2.8403340193372,134.82188621783));
#123935=CARTESIAN_POINT('Ctrl Pts',(-196.351879794753,2.95011837684841,
134.739584197629));
#123936=CARTESIAN_POINT('Ctrl Pts',(-196.359626070838,3.05987976983901,
134.657299393235));
#123937=CARTESIAN_POINT('Ctrl Pts',(-196.367372346922,3.16622394720568,
134.57039789747));
#123938=CARTESIAN_POINT('Ctrl Pts',(-196.375118623006,3.26874854368119,
134.479202929922));
#123939=CARTESIAN_POINT('Ctrl Pts',(-196.382864956271,3.37127389696957,
134.388007289193));
#123940=CARTESIAN_POINT('Ctrl Pts',(-196.390611289537,3.46997932098188,
134.292518373281));
#123941=CARTESIAN_POINT('Ctrl Pts',(-196.398357622802,3.56449711178872,
134.19309834754));
#123942=CARTESIAN_POINT('Ctrl Pts',(-196.406105690805,3.6590360691996,134.093656057373));
#123943=CARTESIAN_POINT('Ctrl Pts',(-196.413853758808,3.74938525798013,
133.990281188891));
#123944=CARTESIAN_POINT('Ctrl Pts',(-196.421601826811,3.83521555689988,
133.883370960941));
#123945=CARTESIAN_POINT('Ctrl Pts',(-196.429358129553,3.92113707728282,
133.776347107529));
#123946=CARTESIAN_POINT('Ctrl Pts',(-196.437114432295,4.00252986868535,
133.665780694151));
#123947=CARTESIAN_POINT('Ctrl Pts',(-196.444870735037,4.07910634450957,
133.552100505671));
#123948=CARTESIAN_POINT('Ctrl Pts',(-196.452631177551,4.1557236915046,133.438359642651));
#123949=CARTESIAN_POINT('Ctrl Pts',(-196.460391620065,4.22751939619557,
133.321502025975));
#123950=CARTESIAN_POINT('Ctrl Pts',(-196.468152062579,4.29425111487522,
133.20198244448));
#123951=CARTESIAN_POINT('Ctrl Pts',(-196.475924962845,4.36108995723385,
133.082270999541));
#123952=CARTESIAN_POINT('Ctrl Pts',(-196.48369786311,4.42284839268908,132.959889399764));
#123953=CARTESIAN_POINT('Ctrl Pts',(-196.491470763375,4.47933126826296,
132.835314691803));
#123954=CARTESIAN_POINT('Ctrl Pts',(-196.498961099137,4.53376084903658,
132.715268588265));
#123955=CARTESIAN_POINT('Ctrl Pts',(-196.506451434899,4.58329165474819,
132.593186343692));
#123956=CARTESIAN_POINT('Ctrl Pts',(-196.513941770661,4.62779306061534,
132.469507593247));
#123957=CARTESIAN_POINT('Ctrl Pts',(-196.52171610478,4.67398175081282,132.341139525385));
#123958=CARTESIAN_POINT('Ctrl Pts',(-196.529490438899,4.71489844511337,
132.210644867334));
#123959=CARTESIAN_POINT('Ctrl Pts',(-196.537264773018,4.75034337573913,
132.078495961661));
#123960=CARTESIAN_POINT('Ctrl Pts',(-196.545029525966,4.7857446236558,131.946509917703));
#123961=CARTESIAN_POINT('Ctrl Pts',(-196.552794278913,4.81568742506033,
131.812874056546));
#123962=CARTESIAN_POINT('Ctrl Pts',(-196.56055903186,4.84002049298939,131.67807950253));
#123963=CARTESIAN_POINT('Ctrl Pts',(-196.568316072745,4.86432939297227,
131.543418828366));
#123964=CARTESIAN_POINT('Ctrl Pts',(-196.57607311363,4.88303957834233,131.407602133804));
#123965=CARTESIAN_POINT('Ctrl Pts',(-196.583830154515,4.89604999507073,
131.271134126099));
#123966=CARTESIAN_POINT('Ctrl Pts',(-196.591581345755,4.90905060054271,
131.134769029979));
#123967=CARTESIAN_POINT('Ctrl Pts',(-196.599332536995,4.91635995580379,
130.997753985968));
#123968=CARTESIAN_POINT('Ctrl Pts',(-196.607083728235,4.91792842339693,
130.860601926624));
#123969=CARTESIAN_POINT('Ctrl Pts',(-196.614831625012,4.91949622434951,
130.723508160564));
#123970=CARTESIAN_POINT('Ctrl Pts',(-196.622579521789,4.91532798620717,
130.586277885118));
#123971=CARTESIAN_POINT('Ctrl Pts',(-196.630327418567,4.90542609256398,
130.449426943632));
#123972=CARTESIAN_POINT('Ctrl Pts',(-196.638073694651,4.89552627018349,
130.312604628412));
#123973=CARTESIAN_POINT('Ctrl Pts',(-196.645819970735,4.87989520608599,
130.176161879023));
#123974=CARTESIAN_POINT('Ctrl Pts',(-196.653566246819,4.85858734580939,
130.04061192484));
#123975=CARTESIAN_POINT('Ctrl Pts',(-196.661312580084,4.83727932824304,
129.905060970058));
#123976=CARTESIAN_POINT('Ctrl Pts',(-196.669058913349,4.81029449159206,
129.770403209857));
#123977=CARTESIAN_POINT('Ctrl Pts',(-196.676805246615,4.77773878287119,
129.637143763186));
#123978=CARTESIAN_POINT('Ctrl Pts',(-196.684553314618,4.74517578352494,
129.503854473986));
#123979=CARTESIAN_POINT('Ctrl Pts',(-196.692301382621,4.70703952237994,
129.371964501156));
#123980=CARTESIAN_POINT('Ctrl Pts',(-196.700049450624,4.6634862928383,129.2419654502));
#123981=CARTESIAN_POINT('Ctrl Pts',(-196.707805753366,4.61988677440618,
129.111828234706));
#123982=CARTESIAN_POINT('Ctrl Pts',(-196.715562056108,4.57085891131053,
128.98358632697));
#123983=CARTESIAN_POINT('Ctrl Pts',(-196.723318358849,4.51660800481933,
128.857713450434));
#123984=CARTESIAN_POINT('Ctrl Pts',(-196.731078801364,4.46232814298588,
128.731773391754));
#123985=CARTESIAN_POINT('Ctrl Pts',(-196.738839243878,4.40281985259029,
128.608205235819));
#123986=CARTESIAN_POINT('Ctrl Pts',(-196.746599686392,4.33833476766696,
128.487458697727));
#123987=CARTESIAN_POINT('Ctrl Pts',(-196.754372586657,4.27374616556059,
128.366518326573));
#123988=CARTESIAN_POINT('Ctrl Pts',(-196.762145486923,4.20416500253837,
128.248408961719));
#123989=CARTESIAN_POINT('Ctrl Pts',(-196.769918387188,4.12988714651096,
128.133552646262));
#123990=CARTESIAN_POINT('Ctrl Pts',(-196.77740872295,4.05830947764578,128.022871647178));
#123991=CARTESIAN_POINT('Ctrl Pts',(-196.784899058712,3.98237083808165,
127.915211542331));
#123992=CARTESIAN_POINT('Ctrl Pts',(-196.792389394474,3.90237049944579,
127.810919863592));
#123993=CARTESIAN_POINT('Ctrl Pts',(-196.800163728593,3.81933692365392,
127.702673934153));
#123994=CARTESIAN_POINT('Ctrl Pts',(-196.807938062712,3.73166454474996,
127.597714010231));
#123995=CARTESIAN_POINT('Ctrl Pts',(-196.815712396831,3.63964277854941,
127.49646347481));
#123996=CARTESIAN_POINT('Ctrl Pts',(-196.823477149778,3.54773442095174,
127.395337721625));
#123997=CARTESIAN_POINT('Ctrl Pts',(-196.831241902725,3.4514876017493,127.297912547587));
#123998=CARTESIAN_POINT('Ctrl Pts',(-196.839006655673,3.35123374346011,
127.204580699405));
#123999=CARTESIAN_POINT('Ctrl Pts',(-196.846763696558,3.25107945871658,
127.111341549731));
#124000=CARTESIAN_POINT('Ctrl Pts',(-196.854520737442,3.14692633926754,
127.022187899961));
#124001=CARTESIAN_POINT('Ctrl Pts',(-196.862277778327,3.03914438745001,
126.937477576313));
#124002=CARTESIAN_POINT('Ctrl Pts',(-196.870028969567,2.93144371484062,
126.852831133378));
#124003=CARTESIAN_POINT('Ctrl Pts',(-196.877780160808,2.82011996290654,
126.772621587719));
#124004=CARTESIAN_POINT('Ctrl Pts',(-196.885531352048,2.70557784607938,
126.697167953312));
#124005=CARTESIAN_POINT('Ctrl Pts',(-196.893279248825,2.59108441270722,
126.621746388711));
#124006=CARTESIAN_POINT('Ctrl Pts',(-196.901027145602,2.47337566088124,
126.551076929597));
#124007=CARTESIAN_POINT('Ctrl Pts',(-196.908775042379,2.35288687260822,
126.485436396512));
#124008=CARTESIAN_POINT('Ctrl Pts',(-196.916521318463,2.23242328799227,
126.419809594011));
#124009=CARTESIAN_POINT('Ctrl Pts',(-196.924267594547,2.10918116671744,
126.359209812087));
#124010=CARTESIAN_POINT('Ctrl Pts',(-196.932013870631,1.98362173233724,
126.30386865718));
#124011=CARTESIAN_POINT('Ctrl Pts',(-196.939760203896,1.85806137110565,
126.248527093757));
#124012=CARTESIAN_POINT('Ctrl Pts',(-196.947506537162,1.73018402039162,
126.198444392494));
#124013=CARTESIAN_POINT('Ctrl Pts',(-196.955252870427,1.60047191802326,
126.153804446298));
#124014=CARTESIAN_POINT('Ctrl Pts',(-196.96300093843,1.47073076752877,126.109154503295));
#124015=CARTESIAN_POINT('Ctrl Pts',(-196.970749006433,1.33915441739122,
126.069949867965));
#124016=CARTESIAN_POINT('Ctrl Pts',(-196.978497074436,1.2062409496441,126.036324771025));
#124017=CARTESIAN_POINT('Ctrl Pts',(-196.986253377178,1.07318621988194,
126.002663936931));
#124018=CARTESIAN_POINT('Ctrl Pts',(-196.99400967992,0.938791913329507,
125.974594583081));
#124019=CARTESIAN_POINT('Ctrl Pts',(-197.001765982662,0.803567557284923,
125.952200042793));
#124020=CARTESIAN_POINT('Ctrl Pts',(-197.009526425176,0.668271027929991,
125.929793549866));
#124021=CARTESIAN_POINT('Ctrl Pts',(-197.01728686769,0.532143954180493,
125.913067953334));
#124022=CARTESIAN_POINT('Ctrl Pts',(-197.025047310204,0.395700708427855,
125.902054628355));
#124023=CARTESIAN_POINT('Ctrl Pts',(-197.032820210469,0.259038431864272,
125.89102362381));
#124024=CARTESIAN_POINT('Ctrl Pts',(-197.040593110735,0.122059359953858,
125.885723230215));
#124025=CARTESIAN_POINT('Ctrl Pts',(-197.048366011,-0.0147215066600589,
125.886132650123));
#124026=CARTESIAN_POINT('Ctrl Pts',(-197.055856346762,-0.146530044246793,
125.886527186585));
#124027=CARTESIAN_POINT('Ctrl Pts',(-197.063346682525,-0.27815422914227,
125.89222359833));
#124028=CARTESIAN_POINT('Ctrl Pts',(-197.070837018287,-0.409139909314695,
125.903157949128));
#124029=CARTESIAN_POINT('Ctrl Pts',(-197.078611352406,-0.545091951359064,
125.914506879159));
#124030=CARTESIAN_POINT('Ctrl Pts',(-197.086385686525,-0.680786770288788,
125.931534731873));
#124031=CARTESIAN_POINT('Ctrl Pts',(-197.094160020644,-0.815711725690703,
125.954226862393));
#124032=CARTESIAN_POINT('Ctrl Pts',(-197.101924773591,-0.950470398142942,
125.976891026889));
#124033=CARTESIAN_POINT('Ctrl Pts',(-197.109689526538,-1.08446071302349,
126.005205515426));
#124034=CARTESIAN_POINT('Ctrl Pts',(-197.117454279485,-1.21717309943613,
126.039103782042));
#124035=CARTESIAN_POINT('Ctrl Pts',(-197.12521132037,-1.3497536740364,126.072968380422));
#124036=CARTESIAN_POINT('Ctrl Pts',(-197.132968361255,-1.48105846969448,
126.112405624185));
#124037=CARTESIAN_POINT('Ctrl Pts',(-197.14072540214,-1.61058644177957,
126.157297633696));
#124038=CARTESIAN_POINT('Ctrl Pts',(-197.148476593381,-1.74001673581351,
126.202155789794));
#124039=CARTESIAN_POINT('Ctrl Pts',(-197.156227784621,-1.86767250538385,
126.252460396493));
#124040=CARTESIAN_POINT('Ctrl Pts',(-197.163978975861,-1.99306659696161,
126.308043390926));
#124041=CARTESIAN_POINT('Ctrl Pts',(-197.171726872638,-2.11840739270528,
126.363602761105));
#124042=CARTESIAN_POINT('Ctrl Pts',(-197.179474769415,-2.24148806567971,
126.424435898852));
#124043=CARTESIAN_POINT('Ctrl Pts',(-197.187222666192,-2.3618404383649,
126.490326217355));
#124044=CARTESIAN_POINT('Ctrl Pts',(-197.194968942276,-2.48216763592822,
126.556202753023));
#124045=CARTESIAN_POINT('Ctrl Pts',(-197.20271521836,-2.59976732564188,
126.627134177688));
#124046=CARTESIAN_POINT('Ctrl Pts',(-197.210461494444,-2.71419534785042,
126.702857639851));
#124047=CARTESIAN_POINT('Ctrl Pts',(-197.21820782771,-2.82862421474047,
126.778581660986));
#124048=CARTESIAN_POINT('Ctrl Pts',(-197.225954160975,-2.93988104136766,
126.859097574447));
#124049=CARTESIAN_POINT('Ctrl Pts',(-197.23370049424,-3.0475504520959,126.944099058496));
#124050=CARTESIAN_POINT('Ctrl Pts',(-197.241448562243,-3.15524397464228,
127.029119578039));
#124051=CARTESIAN_POINT('Ctrl Pts',(-197.249196630246,-3.25934817585858,
127.118627424824));
#124052=CARTESIAN_POINT('Ctrl Pts',(-197.256944698249,-3.35948089813607,
127.21227610331));
#124053=CARTESIAN_POINT('Ctrl Pts',(-197.264701000991,-3.45972004266226,
127.306024312726));
#124054=CARTESIAN_POINT('Ctrl Pts',(-197.272457303733,-3.55597899047717,
127.403921877684));
#124055=CARTESIAN_POINT('Ctrl Pts',(-197.280213606475,-3.64791221894775,
127.505585162135));
#124056=CARTESIAN_POINT('Ctrl Pts',(-197.287974048989,-3.73989451495042,
127.607302707342));
#124057=CARTESIAN_POINT('Ctrl Pts',(-197.295734491503,-3.82754624145586,
127.712789676336));
#124058=CARTESIAN_POINT('Ctrl Pts',(-197.303494934017,-3.91056297081482,
127.821630272095));
#124059=CARTESIAN_POINT('Ctrl Pts',(-197.311267834283,-3.99371296599786,
127.930645588441));
#124060=CARTESIAN_POINT('Ctrl Pts',(-197.319040734548,-4.07221287151127,
128.043024968882));
#124061=CARTESIAN_POINT('Ctrl Pts',(-197.326813634813,-4.14580181441111,
128.158323887261));
#124062=CARTESIAN_POINT('Ctrl Pts',(-197.334303970575,-4.21671561387579,
128.269431399534));
#124063=CARTESIAN_POINT('Ctrl Pts',(-197.341794306337,-4.2830691483762,
128.383249603762));
#124064=CARTESIAN_POINT('Ctrl Pts',(-197.349284642099,-4.3446707290067,
128.499361849885));
#124065=CARTESIAN_POINT('Ctrl Pts',(-197.357505688457,-4.41228177691909,
128.626801284969));
#124066=CARTESIAN_POINT('Ctrl Pts',(-197.365726734815,-4.47436294437082,
128.757370335874));
#124067=CARTESIAN_POINT('Ctrl Pts',(-197.373947781172,-4.5306305492326,
128.890576437242));
#124068=CARTESIAN_POINT('Ctrl Pts',(-197.382149938232,-4.58676886939006,
129.023476474196));
#124069=CARTESIAN_POINT('Ctrl Pts',(-197.390352095292,-4.63712013449305,
129.159001183372));
#124070=CARTESIAN_POINT('Ctrl Pts',(-197.398554252352,-4.68144684635498,
129.296634353534));
#124071=CARTESIAN_POINT('Ctrl Pts',(-197.404177125126,-4.71183439678685,
129.390986826878));
#124072=CARTESIAN_POINT('Ctrl Pts',(-197.409799997901,-4.73939157229638,
129.48632962842));
#124073=CARTESIAN_POINT('Ctrl Pts',(-197.415422870675,-4.76405452823413,
129.582490119309));
#124074=CARTESIAN_POINT('Ctrl Pts',(-195.665141276266,-4.76405452823396,
129.582490119308));
#124075=CARTESIAN_POINT('Ctrl Pts',(-195.669627150585,-4.78364500634694,
129.658873096143));
#124076=CARTESIAN_POINT('Ctrl Pts',(-195.674113024903,-4.80138190659694,
129.735664461695));
#124077=CARTESIAN_POINT('Ctrl Pts',(-195.678598899222,-4.81725278166829,
129.812766597813));
#124078=CARTESIAN_POINT('Ctrl Pts',(-195.689674595893,-4.85643823041579,
130.00313302623));
#124079=CARTESIAN_POINT('Ctrl Pts',(-195.700750292564,-4.88435001913631,
130.195892860283));
#124080=CARTESIAN_POINT('Ctrl Pts',(-195.711825989234,-4.90075931060626,
130.38994386838));
#124081=CARTESIAN_POINT('Ctrl Pts',(-195.71959751416,-4.91227327866349,
130.526104354821));
#124082=CARTESIAN_POINT('Ctrl Pts',(-195.727369039086,-4.91812490136763,
130.662900256424));
#124083=CARTESIAN_POINT('Ctrl Pts',(-195.735140564012,-4.91824801533235,
130.799942226527));
#124084=CARTESIAN_POINT('',(-195.389859435957,-4.9182490946383,130.807344841003));
#124085=CARTESIAN_POINT('Ctrl Pts',(-195.319719904489,-4.76405452823413,
129.582490119309));
#124086=CARTESIAN_POINT('Ctrl Pts',(-195.327375268945,-4.79771771013328,
129.713742354623));
#124087=CARTESIAN_POINT('Ctrl Pts',(-195.335030633401,-4.82593039702568,
129.846300244023));
#124088=CARTESIAN_POINT('Ctrl Pts',(-195.342685997857,-4.84861431659377,
129.979665357836));
#124089=CARTESIAN_POINT('Ctrl Pts',(-195.35054823754,-4.87191123650242,
130.116634472268));
#124090=CARTESIAN_POINT('Ctrl Pts',(-195.358410477224,-4.88937627244404,
130.25445460389));
#124091=CARTESIAN_POINT('Ctrl Pts',(-195.366272716907,-4.90098169012487,
130.392582114532));
#124092=CARTESIAN_POINT('Ctrl Pts',(-195.37413495659,-4.91258710780571,
130.530709625174));
#124093=CARTESIAN_POINT('Ctrl Pts',(-195.381997196274,-4.91833295009223,
130.669144059767));
#124094=CARTESIAN_POINT('Ctrl Pts',(-195.389859435957,-4.9182490946383,
130.807344841003));
#124095=CARTESIAN_POINT('Ctrl Pts',(-195.389859435995,-4.9182490946379,
130.807344841668));
#124096=CARTESIAN_POINT('Ctrl Pts',(-195.39981971452,-4.91814286233046,
130.982424504574));
#124097=CARTESIAN_POINT('Ctrl Pts',(-195.409779993045,-4.90868858456078,
131.157218844946));
#124098=CARTESIAN_POINT('Ctrl Pts',(-195.41974027157,-4.88997301345931,
131.330998054651));
#124099=CARTESIAN_POINT('Ctrl Pts',(-195.427514605689,-4.87536487749105,
131.466638602838));
#124100=CARTESIAN_POINT('Ctrl Pts',(-195.435288939808,-4.85508562687483,
131.601885723498));
#124101=CARTESIAN_POINT('Ctrl Pts',(-195.443063273927,-4.82916220422726,
131.736227275282));
#124102=CARTESIAN_POINT('Ctrl Pts',(-195.450828026874,-4.80327072988126,
131.87040326311));
#124103=CARTESIAN_POINT('Ctrl Pts',(-195.458592779821,-4.77174899711198,
132.003675522438));
#124104=CARTESIAN_POINT('Ctrl Pts',(-195.466357532768,-4.73467576101327,
132.135536226031));
#124105=CARTESIAN_POINT('Ctrl Pts',(-195.474114573653,-4.69763934657529,
132.267265963715));
#124106=CARTESIAN_POINT('Ctrl Pts',(-195.481871614538,-4.65506250671518,
132.397586561726));
#124107=CARTESIAN_POINT('Ctrl Pts',(-195.489628655423,-4.60707511081103,
132.525999948508));
#124108=CARTESIAN_POINT('Ctrl Pts',(-195.497379846663,-4.55912390257549,
132.654316497755));
#124109=CARTESIAN_POINT('Ctrl Pts',(-195.505131037903,-4.50577039587603,
132.780728333762));
#124110=CARTESIAN_POINT('Ctrl Pts',(-195.512882229143,-4.44719429552313,
132.904752476331));
#124111=CARTESIAN_POINT('Ctrl Pts',(-195.52063012592,-4.38864309157538,
133.028723905332));
#124112=CARTESIAN_POINT('Ctrl Pts',(-195.528378022698,-4.32487387548738,
133.150309306542));
#124113=CARTESIAN_POINT('Ctrl Pts',(-195.536125919475,-4.2561144066719,
133.269045834753));
#124114=CARTESIAN_POINT('Ctrl Pts',(-195.543872195559,-4.18736932085501,
133.387757525841));
#124115=CARTESIAN_POINT('Ctrl Pts',(-195.551618471643,-4.11363625439252,
133.503621191137));
#124116=CARTESIAN_POINT('Ctrl Pts',(-195.559364747727,-4.03518864169585,
133.616199106603));
#124117=CARTESIAN_POINT('Ctrl Pts',(-195.567111080992,-3.95674044991661,
133.728777853093));
#124118=CARTESIAN_POINT('Ctrl Pts',(-195.574857414257,-3.87357786597965,
133.838070480587));
#124119=CARTESIAN_POINT('Ctrl Pts',(-195.582603747523,-3.78601709127631,
133.943669083943));
#124120=CARTESIAN_POINT('Ctrl Pts',(-195.590351815526,-3.69843670794469,
134.049291335373));
#124121=CARTESIAN_POINT('Ctrl Pts',(-195.598099883529,-3.60645642342602,
134.151217615629));
#124122=CARTESIAN_POINT('Ctrl Pts',(-195.605847951532,-3.51043180420721,
134.24907419209));
#124123=CARTESIAN_POINT('Ctrl Pts',(-195.613604254274,-3.41430512888052,
134.347034771685));
#124124=CARTESIAN_POINT('Ctrl Pts',(-195.621360557015,-3.3141258066689,
134.440916727675));
#124125=CARTESIAN_POINT('Ctrl Pts',(-195.629116859757,-3.21028565473641,
134.530383843137));
#124126=CARTESIAN_POINT('Ctrl Pts',(-195.636877302271,-3.10639008018798,
134.619898709892));
#124127=CARTESIAN_POINT('Ctrl Pts',(-195.644637744786,-2.99883008908042,
134.704993798469));
#124128=CARTESIAN_POINT('Ctrl Pts',(-195.6523981873,-2.88802866412109,134.78537474687));
#124129=CARTESIAN_POINT('Ctrl Pts',(-195.660171087565,-2.77704937087823,
134.865884729904));
#124130=CARTESIAN_POINT('Ctrl Pts',(-195.667943987831,-2.66281857163852,
134.941665234117));
#124131=CARTESIAN_POINT('Ctrl Pts',(-195.675716888096,-2.54578692477708,
135.012466129092));
#124132=CARTESIAN_POINT('Ctrl Pts',(-195.683207223858,-2.43300967306273,
135.080693233198));
#124133=CARTESIAN_POINT('Ctrl Pts',(-195.69069755962,-2.31763194379055,
135.144296336452));
#124134=CARTESIAN_POINT('Ctrl Pts',(-195.698187895382,-2.20007486704126,
135.2030938036));
#124135=CARTESIAN_POINT('Ctrl Pts',(-195.705962229501,-2.07806057799752,
135.264120594585));
#124136=CARTESIAN_POINT('Ctrl Pts',(-195.71373656362,-1.95331191468248,
135.320163459015));
#124137=CARTESIAN_POINT('Ctrl Pts',(-195.721510897739,-1.82627431925977,
135.370968239566));
#124138=CARTESIAN_POINT('Ctrl Pts',(-195.729275650686,-1.69939328631975,
135.421710407767));
#124139=CARTESIAN_POINT('Ctrl Pts',(-195.737040403634,-1.57022929355805,
135.467227192768));
#124140=CARTESIAN_POINT('Ctrl Pts',(-195.744805156581,-1.43925215945998,
135.507310360439));
#124141=CARTESIAN_POINT('Ctrl Pts',(-195.752562197466,-1.30840511369795,
135.547353716943));
#124142=CARTESIAN_POINT('Ctrl Pts',(-195.760319238351,-1.17574888177873,
135.581974082212));
#124143=CARTESIAN_POINT('Ctrl Pts',(-195.768076279236,-1.04177270297969,
135.611011499191));
#124144=CARTESIAN_POINT('Ctrl Pts',(-195.775827470476,-0.907897556659447,
135.640027018828));
#124145=CARTESIAN_POINT('Ctrl Pts',(-195.783578661716,-0.772704825255148,
135.663467887734));
#124146=CARTESIAN_POINT('Ctrl Pts',(-195.791329852956,-0.63669798852352,
135.681224234063));
#124147=CARTESIAN_POINT('Ctrl Pts',(-195.799077749733,-0.500748958325419,
135.698973033471));
#124148=CARTESIAN_POINT('Ctrl Pts',(-195.80682564651,-0.363986897864043,
135.711042065181));
#124149=CARTESIAN_POINT('Ctrl Pts',(-195.814573543287,-0.226924321449017,
135.717372770496));
#124150=CARTESIAN_POINT('Ctrl Pts',(-195.822319819371,-0.0898904155702491,
135.723702151564));
#124151=CARTESIAN_POINT('Ctrl Pts',(-195.830066095455,0.0474434909258787,
135.724295575739));
#124152=CARTESIAN_POINT('Ctrl Pts',(-195.837812371539,0.184561330431458,
135.719146490604));
#124153=CARTESIAN_POINT('Ctrl Pts',(-195.845558704805,0.321680182109967,
135.713997367458));
#124154=CARTESIAN_POINT('Ctrl Pts',(-195.85330503807,0.458582572925475,
135.703105665086));
#124155=CARTESIAN_POINT('Ctrl Pts',(-195.861051371335,0.594754406154578,
135.686516929982));
#124156=CARTESIAN_POINT('Ctrl Pts',(-195.868799439338,0.730956734121398,
135.669924479945));
#124157=CARTESIAN_POINT('Ctrl Pts',(-195.876547507341,0.866427790928436,
135.647632505728));
#124158=CARTESIAN_POINT('Ctrl Pts',(-195.884295575344,1.00066095236712,
135.619738143878));
#124159=CARTESIAN_POINT('Ctrl Pts',(-195.892051878086,1.13503677840698,
135.591814135568));
#124160=CARTESIAN_POINT('Ctrl Pts',(-195.899808180828,1.26817169752809,
135.558275924972));
#124161=CARTESIAN_POINT('Ctrl Pts',(-195.90756448357,1.39957105416255,135.519271425508));
#124162=CARTESIAN_POINT('Ctrl Pts',(-195.915324926084,1.53104054259037,
135.480246108168));
#124163=CARTESIAN_POINT('Ctrl Pts',(-195.923085368598,1.66077225312122,
135.435748815331));
#124164=CARTESIAN_POINT('Ctrl Pts',(-195.930845811113,1.78828989818289,
135.385976304478));
#124165=CARTESIAN_POINT('Ctrl Pts',(-195.938618711378,1.91601224588891,
135.336123894371));
#124166=CARTESIAN_POINT('Ctrl Pts',(-195.946391611643,2.04151306753059,
135.280979501355));
#124167=CARTESIAN_POINT('Ctrl Pts',(-195.954164511909,2.16433832944441,
135.220787075484));
#124168=CARTESIAN_POINT('Ctrl Pts',(-195.961654847671,2.28269858371017,
135.162782795908));
#124169=CARTESIAN_POINT('Ctrl Pts',(-195.969145183433,2.39857415673948,
135.100091275505));
#124170=CARTESIAN_POINT('Ctrl Pts',(-195.976635519195,2.5115846025559,135.032968644648));
#124171=CARTESIAN_POINT('Ctrl Pts',(-195.984409853314,2.6288798737734,134.963301038841));
#124172=CARTESIAN_POINT('Ctrl Pts',(-195.992184187433,2.74346002251183,
134.888638992476));
#124173=CARTESIAN_POINT('Ctrl Pts',(-195.999958521552,2.85487044664782,
134.809219890419));
#124174=CARTESIAN_POINT('Ctrl Pts',(-196.007723274499,2.9661435673931,134.729898665308));
#124175=CARTESIAN_POINT('Ctrl Pts',(-196.015488027446,3.07425442081109,
134.645832274185));
#124176=CARTESIAN_POINT('Ctrl Pts',(-196.023252780394,3.17877386526114,
134.557303433015));
#124177=CARTESIAN_POINT('Ctrl Pts',(-196.031009821279,3.2831894995255,134.468862519938));
#124178=CARTESIAN_POINT('Ctrl Pts',(-196.038766862164,3.38402052698728,
134.375968228082));
#124179=CARTESIAN_POINT('Ctrl Pts',(-196.046523903049,3.48086792546511,
134.278945707612));
#124180=CARTESIAN_POINT('Ctrl Pts',(-196.054275094289,3.57764229056651,
134.181996352578));
#124181=CARTESIAN_POINT('Ctrl Pts',(-196.062026285529,3.67043873104742,
134.080925241009));
#124182=CARTESIAN_POINT('Ctrl Pts',(-196.069777476769,3.75889266550496,
133.976096576266));
#124183=CARTESIAN_POINT('Ctrl Pts',(-196.077525373546,3.84730900468066,
133.871312466503));
#124184=CARTESIAN_POINT('Ctrl Pts',(-196.085273270323,3.93138625714945,
133.762774278175));
#124185=CARTESIAN_POINT('Ctrl Pts',(-196.0930211671,4.01079812931765,133.650881551682));
#124186=CARTESIAN_POINT('Ctrl Pts',(-196.100767443184,4.09019339023412,
133.539012230735));
#124187=CARTESIAN_POINT('Ctrl Pts',(-196.108513719268,4.16492498582819,
133.423790085964));
#124188=CARTESIAN_POINT('Ctrl Pts',(-196.116259995352,4.23470845621583,
133.30564575792));
#124189=CARTESIAN_POINT('Ctrl Pts',(-196.124006328618,4.30449244172929,
133.187500557761));
#124190=CARTESIAN_POINT('Ctrl Pts',(-196.131752661883,4.36932803031741,
133.066433467914));
#124191=CARTESIAN_POINT('Ctrl Pts',(-196.139498995149,4.42897565969853,
132.942901631505));
#124192=CARTESIAN_POINT('Ctrl Pts',(-196.147247063151,4.48863664675259,
132.819342130998));
#124193=CARTESIAN_POINT('Ctrl Pts',(-196.154995131154,4.54310719277129,
132.69331713759));
#124194=CARTESIAN_POINT('Ctrl Pts',(-196.162743199157,4.59219517872211,
132.565305393254));
#124195=CARTESIAN_POINT('Ctrl Pts',(-196.170499501899,4.64133533596847,
132.437157596512));
#124196=CARTESIAN_POINT('Ctrl Pts',(-196.178255804641,4.68508136532905,
132.307019196435));
#124197=CARTESIAN_POINT('Ctrl Pts',(-196.186012107383,4.72329033713375,
132.175386311577));
#124198=CARTESIAN_POINT('Ctrl Pts',(-196.193772549897,4.76151970221726,
132.043683170285));
#124199=CARTESIAN_POINT('Ctrl Pts',(-196.201532992411,4.79420602793986,
131.910484334337));
#124200=CARTESIAN_POINT('Ctrl Pts',(-196.209293434926,4.8212574068754,131.776296870182));
#124201=CARTESIAN_POINT('Ctrl Pts',(-196.217066335191,4.84835221108591,
131.641893996397));
#124202=CARTESIAN_POINT('Ctrl Pts',(-196.224839235456,4.86979393109643,
131.50649970938));
#124203=CARTESIAN_POINT('Ctrl Pts',(-196.232612135722,4.88554239271103,
131.370627861474));
#124204=CARTESIAN_POINT('Ctrl Pts',(-196.240102471484,4.900718358078,131.23969529748));
#124205=CARTESIAN_POINT('Ctrl Pts',(-196.247592807246,4.91060778408717,
131.108319598021));
#124206=CARTESIAN_POINT('Ctrl Pts',(-196.255083143008,4.91522052013289,
130.976959287794));
#124207=CARTESIAN_POINT('Ctrl Pts',(-196.262857477127,4.92000814946778,
130.84061841148));
#124208=CARTESIAN_POINT('Ctrl Pts',(-196.270631811246,4.91912622449037,
130.703862227485));
#124209=CARTESIAN_POINT('Ctrl Pts',(-196.278406145365,4.91252874026042,
130.567201517771));
#124210=CARTESIAN_POINT('Ctrl Pts',(-196.286170898312,4.90593938684015,
130.430709230169));
#124211=CARTESIAN_POINT('Ctrl Pts',(-196.293935651259,4.89364850813207,
130.294312569492));
#124212=CARTESIAN_POINT('Ctrl Pts',(-196.301700404207,4.87566199954319,
130.158525399642));
#124213=CARTESIAN_POINT('Ctrl Pts',(-196.309457445092,4.85769335540821,
130.022873095524));
#124214=CARTESIAN_POINT('Ctrl Pts',(-196.317214485976,4.8340403900447,129.88782946262));
#124215=CARTESIAN_POINT('Ctrl Pts',(-196.324971526861,4.8047609802586,129.753905961198));
#124216=CARTESIAN_POINT('Ctrl Pts',(-196.332722718102,4.77550365030315,
129.620083452531));
#124217=CARTESIAN_POINT('Ctrl Pts',(-196.340473909342,4.74062840441648,
129.48737977442));
#124218=CARTESIAN_POINT('Ctrl Pts',(-196.348225100582,4.70024459204801,
129.35629852034));
#124219=CARTESIAN_POINT('Ctrl Pts',(-196.355972997359,4.65987794387701,
129.225272979288));
#124220=CARTESIAN_POINT('Ctrl Pts',(-196.363720894136,4.61400750073638,
129.095868863611));
#124221=CARTESIAN_POINT('Ctrl Pts',(-196.371468790913,4.56279303762065,
128.968576654693));
#124222=CARTESIAN_POINT('Ctrl Pts',(-196.379215066997,4.51158928746668,
128.841311072562));
#124223=CARTESIAN_POINT('Ctrl Pts',(-196.386961343081,4.45504388664914,
128.716156880974));
#124224=CARTESIAN_POINT('Ctrl Pts',(-196.394707619166,4.39336538774464,
128.593586175822));
#124225=CARTESIAN_POINT('Ctrl Pts',(-196.402453952431,4.33168643354339,
128.471014565882));
#124226=CARTESIAN_POINT('Ctrl Pts',(-196.410200285696,4.26487448138624,
128.351026829673));
#124227=CARTESIAN_POINT('Ctrl Pts',(-196.417946618962,4.19318464946682,
128.234071614754));
#124228=CARTESIAN_POINT('Ctrl Pts',(-196.425694686965,4.1214787631067,128.117090208526));
#124229=CARTESIAN_POINT('Ctrl Pts',(-196.433442754968,4.04489302757999,
128.003143008206));
#124230=CARTESIAN_POINT('Ctrl Pts',(-196.441190822971,3.96372637703559,
127.892650420707));
#124231=CARTESIAN_POINT('Ctrl Pts',(-196.448947125713,3.88247346160899,
127.782040400371));
#124232=CARTESIAN_POINT('Ctrl Pts',(-196.456703428454,3.79663013733879,
127.674892642869));
#124233=CARTESIAN_POINT('Ctrl Pts',(-196.464459731196,3.70653654583702,
127.571595563178));
#124234=CARTESIAN_POINT('Ctrl Pts',(-196.47222017371,3.6163948686728,127.468243350725));
#124235=CARTESIAN_POINT('Ctrl Pts',(-196.479980616225,3.52199867306387,
127.368746194777));
#124236=CARTESIAN_POINT('Ctrl Pts',(-196.487741058739,3.42372489016486,
127.273455501457));
#124237=CARTESIAN_POINT('Ctrl Pts',(-196.495513959004,3.32529334946519,
127.178011839056));
#124238=CARTESIAN_POINT('Ctrl Pts',(-196.50328685927,3.22297207464116,127.086788393428));
#124239=CARTESIAN_POINT('Ctrl Pts',(-196.511059759535,3.11717166908787,
127.000096714005));
#124240=CARTESIAN_POINT('Ctrl Pts',(-196.518550095297,3.01521737477187,
126.916556495492));
#124241=CARTESIAN_POINT('Ctrl Pts',(-196.526040431059,2.91003275438475,
126.837224466721));
#124242=CARTESIAN_POINT('Ctrl Pts',(-196.533530766821,2.80200890157942,
126.762340184915));
#124243=CARTESIAN_POINT('Ctrl Pts',(-196.54130510094,2.68988929156167,126.684616642804));
#124244=CARTESIAN_POINT('Ctrl Pts',(-196.549079435059,2.57435573883828,
126.61143857336));
#124245=CARTESIAN_POINT('Ctrl Pts',(-196.556853769178,2.45581311194474,
126.543120771969));
#124246=CARTESIAN_POINT('Ctrl Pts',(-196.564618522125,2.33741657824439,
126.474887166163));
#124247=CARTESIAN_POINT('Ctrl Pts',(-196.572383275073,2.2160186845002,126.411502103747));
#124248=CARTESIAN_POINT('Ctrl Pts',(-196.58014802802,2.09205494557583,126.353238380737));
#124249=CARTESIAN_POINT('Ctrl Pts',(-196.587905068905,1.96821432918454,
126.295032526079));
#124250=CARTESIAN_POINT('Ctrl Pts',(-196.59566210979,1.84181329065324,126.241938053517));
#124251=CARTESIAN_POINT('Ctrl Pts',(-196.603419150675,1.71331341981801,
126.194182726424));
#124252=CARTESIAN_POINT('Ctrl Pts',(-196.611170341915,1.58491045173478,
126.146463411995));
#124253=CARTESIAN_POINT('Ctrl Pts',(-196.618921533155,1.45441216669993,
126.104075364592));
#124254=CARTESIAN_POINT('Ctrl Pts',(-196.626672724395,1.32230135821319,
126.067198789998));
#124255=CARTESIAN_POINT('Ctrl Pts',(-196.634420621172,1.19024670034405,
126.030337888932));
#124256=CARTESIAN_POINT('Ctrl Pts',(-196.642168517949,1.05658125794433,
125.99898390647));
#124257=CARTESIAN_POINT('Ctrl Pts',(-196.649916414726,0.921804049182246,
125.973267536553));
#124258=CARTESIAN_POINT('Ctrl Pts',(-196.65766269081,0.78705503290714,125.947556545946));
#124259=CARTESIAN_POINT('Ctrl Pts',(-196.665408966895,0.651195096632955,
125.927480895489));
#124260=CARTESIAN_POINT('Ctrl Pts',(-196.673155242979,0.514734155767422,
125.913120303353));
#124261=CARTESIAN_POINT('Ctrl Pts',(-196.680901576244,0.378272207578036,
125.89875960521));
#124262=CARTESIAN_POINT('Ctrl Pts',(-196.688647909509,0.241209634762758,
125.890114090488));
#124263=CARTESIAN_POINT('Ctrl Pts',(-196.696394242775,0.104061794833803,
125.88721162599));
#124264=CARTESIAN_POINT('Ctrl Pts',(-196.704142310778,-0.0331167584028003,
125.884308511505));
#124265=CARTESIAN_POINT('Ctrl Pts',(-196.711890378781,-0.170380225947006,
125.887151014736));
#124266=CARTESIAN_POINT('Ctrl Pts',(-196.719638446784,-0.307213326347598,
125.895714874124));
#124267=CARTESIAN_POINT('Ctrl Pts',(-196.727394749525,-0.444191854595816,
125.904287835283));
#124268=CARTESIAN_POINT('Ctrl Pts',(-196.735151052267,-0.580738711172077,
125.918594275041));
#124269=CARTESIAN_POINT('Ctrl Pts',(-196.742907355009,-0.716343256706872,
125.93855797041));
#124270=CARTESIAN_POINT('Ctrl Pts',(-196.750667797523,-0.852020178470593,
125.958532321004));
#124271=CARTESIAN_POINT('Ctrl Pts',(-196.758428240037,-0.986753403156911,
125.984169870666));
#124272=CARTESIAN_POINT('Ctrl Pts',(-196.766188682552,-1.12004354234743,
126.015343440133));
#124273=CARTESIAN_POINT('Ctrl Pts',(-196.773961582817,-1.25354765070231,
126.046567052181));
#124274=CARTESIAN_POINT('Ctrl Pts',(-196.781734483082,-1.38560366746973,
126.083344337961));
#124275=CARTESIAN_POINT('Ctrl Pts',(-196.789507383348,-1.51572753612455,
126.125498245286));
#124276=CARTESIAN_POINT('Ctrl Pts',(-196.79699771911,-1.64112107439117,
126.166119751901));
#124277=CARTESIAN_POINT('Ctrl Pts',(-196.804488054872,-1.76472021359313,
126.211733652672));
#124278=CARTESIAN_POINT('Ctrl Pts',(-196.811978390634,-1.88611201178001,
126.262140395965));
#124279=CARTESIAN_POINT('Ctrl Pts',(-196.819753120516,-2.01211283081602,
126.31446098957));
#124280=CARTESIAN_POINT('Ctrl Pts',(-196.827527850399,-2.13613453277524,
126.372111311885));
#124281=CARTESIAN_POINT('Ctrl Pts',(-196.835302580282,-2.25769335655606,
126.434920862831));
#124282=CARTESIAN_POINT('Ctrl Pts',(-196.84306763844,-2.37910096178886,
126.49765227902));
#124283=CARTESIAN_POINT('Ctrl Pts',(-196.850832696599,-2.49805144108238,
126.565529975486));
#124284=CARTESIAN_POINT('Ctrl Pts',(-196.858597754758,-2.61407982358089,
126.638334964927));
#124285=CARTESIAN_POINT('Ctrl Pts',(-196.866355010688,-2.72999162227744,
126.711066800866));
#124286=CARTESIAN_POINT('Ctrl Pts',(-196.874112266618,-2.84298683835341,
126.788715870278));
#124287=CARTESIAN_POINT('Ctrl Pts',(-196.881869522548,-2.95262431338359,
126.871016909407));
#124288=CARTESIAN_POINT('Ctrl Pts',(-196.889701246598,-3.06331428645066,
126.954108022204));
#124289=CARTESIAN_POINT('Ctrl Pts',(-196.897532970648,-3.17058134690447,
127.041940717171));
#124290=CARTESIAN_POINT('Ctrl Pts',(-196.905364694697,-3.27400009449339,
127.134196255612));
#124291=CARTESIAN_POINT('Ctrl Pts',(-196.913112250324,-3.37630738911646,
127.225460313357));
#124292=CARTESIAN_POINT('Ctrl Pts',(-196.92085980595,-3.47484838652523,
127.321052344723));
#124293=CARTESIAN_POINT('Ctrl Pts',(-196.928607361577,-3.56924381249012,
127.420622792394));
#124294=CARTESIAN_POINT('Ctrl Pts',(-196.936353185915,-3.66361814461469,
127.520170989801));
#124295=CARTESIAN_POINT('Ctrl Pts',(-196.944099010253,-3.75384847999537,
127.623695550915));
#124296=CARTESIAN_POINT('Ctrl Pts',(-196.951844834592,-3.83959259305698,
127.730810263034));
#124297=CARTESIAN_POINT('Ctrl Pts',(-196.959590605432,-3.92533611390858,
127.837924235343));
#124298=CARTESIAN_POINT('Ctrl Pts',(-196.967336376272,-4.00659323053975,
127.948628003653));
#124299=CARTESIAN_POINT('Ctrl Pts',(-196.975082147112,-4.08306244107213,
128.062502823149));
#124300=CARTESIAN_POINT('Ctrl Pts',(-196.982977876498,-4.16101209969199,
128.178582265363));
#124301=CARTESIAN_POINT('Ctrl Pts',(-196.990873605884,-4.23398630132602,
128.297956468713));
#124302=CARTESIAN_POINT('Ctrl Pts',(-196.99876933527,-4.30171285759348,
128.420152247202));
#124303=CARTESIAN_POINT('Ctrl Pts',(-197.006523360613,-4.36822393061056,
128.540154987535));
#124304=CARTESIAN_POINT('Ctrl Pts',(-197.014277385956,-4.42967400356862,
128.662878498698));
#124305=CARTESIAN_POINT('Ctrl Pts',(-197.0220314113,-4.48585278789196,128.787851795899));
#124306=CARTESIAN_POINT('Ctrl Pts',(-197.029997992707,-4.54357156476701,
128.916250904981));
#124307=CARTESIAN_POINT('Ctrl Pts',(-197.037964574115,-4.59572572575124,
129.047024507953));
#124308=CARTESIAN_POINT('Ctrl Pts',(-197.045931155522,-4.64214130697621,
129.179643057938));
#124309=CARTESIAN_POINT('Ctrl Pts',(-197.053897736929,-4.68855688820118,
129.312261607922));
#124310=CARTESIAN_POINT('Ctrl Pts',(-197.061864318336,-4.72923380978975,
129.446724666572));
#124311=CARTESIAN_POINT('Ctrl Pts',(-197.069830899744,-4.76405452823391,
129.582490119308));
#124312=CARTESIAN_POINT('Origin',(213.235140564004,0.,130.804360617566));
#124313=CARTESIAN_POINT('',(-199.165100499421,-4.76405452823391,129.582490119308));
#124314=CARTESIAN_POINT('',(-198.820145221536,-4.76405452823399,129.582490119308));
#124315=CARTESIAN_POINT('',(213.235140564004,-4.76405452823405,129.582490119308));
#124316=CARTESIAN_POINT('',(-197.485140563979,-4.91824998893204,130.804030662974));
#124317=CARTESIAN_POINT('Ctrl Pts',(-197.485140564012,-4.91824998893207,
130.804030663556));
#124318=CARTESIAN_POINT('Ctrl Pts',(-197.493215691151,-4.91825960822969,
130.947414616808));
#124319=CARTESIAN_POINT('Ctrl Pts',(-197.501290818289,-4.91199470079414,
131.0906909398));
#124320=CARTESIAN_POINT('Ctrl Pts',(-197.509365945428,-4.8995093582954,
131.233302467326));
#124321=CARTESIAN_POINT('Ctrl Pts',(-197.517450328902,-4.88700970413012,
131.37607746723));
#124322=CARTESIAN_POINT('Ctrl Pts',(-197.525534712377,-4.86827541990526,
131.518185812766));
#124323=CARTESIAN_POINT('Ctrl Pts',(-197.533619095851,-4.84341207736157,
131.659078413899));
#124324=CARTESIAN_POINT('Ctrl Pts',(-197.541721259799,-4.81849405136742,
131.800280888636));
#124325=CARTESIAN_POINT('Ctrl Pts',(-197.549823423746,-4.78742007700962,
131.940261937201));
#124326=CARTESIAN_POINT('Ctrl Pts',(-197.557925587693,-4.75034662328381,
132.078483853818));
#124327=CARTESIAN_POINT('Ctrl Pts',(-197.566036944332,-4.71323110612685,
132.216862596612));
#124328=CARTESIAN_POINT('Ctrl Pts',(-197.57414830097,-4.67010262962301,
132.353477900727));
#124329=CARTESIAN_POINT('Ctrl Pts',(-197.582259657609,-4.62116662589813,
132.487810075728));
#124330=CARTESIAN_POINT('Ctrl Pts',(-197.590389437885,-4.57211947193716,
132.622447364588));
#124331=CARTESIAN_POINT('Ctrl Pts',(-197.598519218162,-4.51723854412096,
132.754790839472));
#124332=CARTESIAN_POINT('Ctrl Pts',(-197.606648998438,-4.45677700646237,
132.884341813916));
#124333=CARTESIAN_POINT('Ctrl Pts',(-197.613676754263,-4.40451127368774,
132.996331632124));
#124334=CARTESIAN_POINT('Ctrl Pts',(-197.620704510087,-4.34807614872925,
133.106234993745));
#124335=CARTESIAN_POINT('Ctrl Pts',(-197.627732265912,-4.28766139771813,
133.213747012692));
#124336=CARTESIAN_POINT('Ctrl Pts',(-197.635506600031,-4.22082861755148,
133.332680336215));
#124337=CARTESIAN_POINT('Ctrl Pts',(-197.64328093415,-4.14893767964865,
133.449019171949));
#124338=CARTESIAN_POINT('Ctrl Pts',(-197.651055268269,-4.0722149913182,
133.562303352103));
#124339=CARTESIAN_POINT('Ctrl Pts',(-197.658820021216,-3.99558685684443,
133.675447919629));
#124340=CARTESIAN_POINT('Ctrl Pts',(-197.666584774163,-3.91413903715416,
133.785545001383));
#124341=CARTESIAN_POINT('Ctrl Pts',(-197.67434952711,-3.82814386857856,
133.892158794903));
#124342=CARTESIAN_POINT('Ctrl Pts',(-197.682106567995,-3.74223411161671,
133.9986666981));
#124343=CARTESIAN_POINT('Ctrl Pts',(-197.68986360888,-3.65178623765968,
134.101697895584));
#124344=CARTESIAN_POINT('Ctrl Pts',(-197.697620649765,-3.55711572780408,
134.200845677375));
#124345=CARTESIAN_POINT('Ctrl Pts',(-197.705371841005,-3.46251660971625,
134.299918691053));
#124346=CARTESIAN_POINT('Ctrl Pts',(-197.713123032246,-3.36370146283428,
134.395113836446));
#124347=CARTESIAN_POINT('Ctrl Pts',(-197.720874223486,-3.26102563669002,
134.486057897266));
#124348=CARTESIAN_POINT('Ctrl Pts',(-197.728622120263,-3.15839345051069,
134.576963304434));
#124349=CARTESIAN_POINT('Ctrl Pts',(-197.73637001704,-3.05190414073299,
134.663620961979));
#124350=CARTESIAN_POINT('Ctrl Pts',(-197.744117913817,-2.94194930255022,
134.745695082405));
#124351=CARTESIAN_POINT('Ctrl Pts',(-197.751864189901,-2.83201746454923,
134.827752034693));
#124352=CARTESIAN_POINT('Ctrl Pts',(-197.759610465985,-2.71862185314553,
134.905227123207));
#124353=CARTESIAN_POINT('Ctrl Pts',(-197.767356742069,-2.6021861586238,
134.977825635793));
#124354=CARTESIAN_POINT('Ctrl Pts',(-197.775103075335,-2.48574960460007,
135.050424684285));
#124355=CARTESIAN_POINT('Ctrl Pts',(-197.7828494086,-2.3662732544387,135.118146878164));
#124356=CARTESIAN_POINT('Ctrl Pts',(-197.790595741865,-2.24420837078515,
135.180741753961));
#124357=CARTESIAN_POINT('Ctrl Pts',(-197.798343809868,-2.12211615154708,
135.243350647447));
#124358=CARTESIAN_POINT('Ctrl Pts',(-197.806091877871,-1.9974345931365,
135.300829759648));
#124359=CARTESIAN_POINT('Ctrl Pts',(-197.813839945874,-1.87063768933132,
135.352975538369));
#124360=CARTESIAN_POINT('Ctrl Pts',(-197.821596248616,-1.74370602426839,
135.405176738244));
#124361=CARTESIAN_POINT('Ctrl Pts',(-197.829352551358,-1.61465488491918,
135.452033132601));
#124362=CARTESIAN_POINT('Ctrl Pts',(-197.8371088541,-1.48397681704943,135.493389927451));
#124363=CARTESIAN_POINT('Ctrl Pts',(-197.844869296614,-1.35322900236022,
135.534768795668));
#124364=CARTESIAN_POINT('Ctrl Pts',(-197.852629739128,-1.22085290607787,
135.57064211333));
#124365=CARTESIAN_POINT('Ctrl Pts',(-197.860390181642,-1.08735324310278,
135.600905831281));
#124366=CARTESIAN_POINT('Ctrl Pts',(-197.868163081908,-0.953639274617129,
135.631218131239));
#124367=CARTESIAN_POINT('Ctrl Pts',(-197.875935982173,-0.818798519968866,
135.65590276613));
#124368=CARTESIAN_POINT('Ctrl Pts',(-197.883708882439,-0.683343719454388,
135.674907242287));
#124369=CARTESIAN_POINT('Ctrl Pts',(-197.891199218201,-0.55281304212647,
135.693220857867));
#124370=CARTESIAN_POINT('Ctrl Pts',(-197.898689553963,-0.421712494577103,
135.706260090511));
#124371=CARTESIAN_POINT('Ctrl Pts',(-197.906179889725,-0.290500705819022,
135.714023783448));
#124372=CARTESIAN_POINT('Ctrl Pts',(-197.913954223844,-0.154313982210954,
135.722081839163));
#124373=CARTESIAN_POINT('Ctrl Pts',(-197.921728557963,-0.0175760168504587,
135.724481939496));
#124374=CARTESIAN_POINT('Ctrl Pts',(-197.929502892082,0.119203659386324,
135.721165835397));
#124375=CARTESIAN_POINT('Ctrl Pts',(-197.937267645029,0.255814766896124,
135.7178538181));
#124376=CARTESIAN_POINT('Ctrl Pts',(-197.945032397976,0.392467095903496,
135.708839622631));
#124377=CARTESIAN_POINT('Ctrl Pts',(-197.952797150924,0.528646789015383,
135.694116811382));
#124378=CARTESIAN_POINT('Ctrl Pts',(-197.960554191809,0.664691226536644,
135.679408623037));
#124379=CARTESIAN_POINT('Ctrl Pts',(-197.968311232694,0.800263576161697,
135.659003143977));
#124380=CARTESIAN_POINT('Ctrl Pts',(-197.976068273579,0.93485113602674,
135.632945960704));
#124381=CARTESIAN_POINT('Ctrl Pts',(-197.983819464819,1.0693372023654,135.606908427356));
#124382=CARTESIAN_POINT('Ctrl Pts',(-197.991570656059,1.20283957483479,
135.575227747049));
#124383=CARTESIAN_POINT('Ctrl Pts',(-197.999321847299,1.33485218089917,
135.538001152889));
#124384=CARTESIAN_POINT('Ctrl Pts',(-198.007069744076,1.46680867808496,
135.500790381023));
#124385=CARTESIAN_POINT('Ctrl Pts',(-198.014817640853,1.59727629273097,
135.458038489407));
#124386=CARTESIAN_POINT('Ctrl Pts',(-198.02256553763,1.72576085053872,135.409893436822));
#124387=CARTESIAN_POINT('Ctrl Pts',(-198.030311813714,1.85421853214679,
135.361758455145));
#124388=CARTESIAN_POINT('Ctrl Pts',(-198.038058089798,1.98069361612735,
135.308232693516));
#124389=CARTESIAN_POINT('Ctrl Pts',(-198.045804365883,2.1047091378518,135.249513315454));
#124390=CARTESIAN_POINT('Ctrl Pts',(-198.053550699148,2.22872557503048,
135.19079350394));
#124391=CARTESIAN_POINT('Ctrl Pts',(-198.061297032413,2.35028206036682,
135.126880166801));
#124392=CARTESIAN_POINT('Ctrl Pts',(-198.069043365679,2.46892395336895,
135.058017582459));
#124393=CARTESIAN_POINT('Ctrl Pts',(-198.076791433682,2.58759241540058,
134.989139576819));
#124394=CARTESIAN_POINT('Ctrl Pts',(-198.084539501685,2.70334464822494,
134.915310314712));
#124395=CARTESIAN_POINT('Ctrl Pts',(-198.092287569688,2.8157531924012,134.836818555596));
#124396=CARTESIAN_POINT('Ctrl Pts',(-198.10004387243,2.92828120571605,134.758243374504));
#124397=CARTESIAN_POINT('Ctrl Pts',(-198.107800175171,3.03745811039781,
134.674996021732));
#124398=CARTESIAN_POINT('Ctrl Pts',(-198.115556477913,3.14288744086359,
134.587407220049));
#124399=CARTESIAN_POINT('Ctrl Pts',(-198.123316920427,3.24837304213745,
134.499771669587));
#124400=CARTESIAN_POINT('Ctrl Pts',(-198.131077362942,3.35010679377825,
134.407790315149));
#124401=CARTESIAN_POINT('Ctrl Pts',(-198.138837805456,3.44772834555247,
134.311831546565));
#124402=CARTESIAN_POINT('Ctrl Pts',(-198.146610705722,3.54550660810803,
134.215718736448));
#124403=CARTESIAN_POINT('Ctrl Pts',(-198.154383605987,3.6391592121027,134.115616038787));
#124404=CARTESIAN_POINT('Ctrl Pts',(-198.162156506252,3.7283648444739,134.011926462407));
#124405=CARTESIAN_POINT('Ctrl Pts',(-198.169646842014,3.81432762741104,
133.912006263309));
#124406=CARTESIAN_POINT('Ctrl Pts',(-198.177137177776,3.89616095138074,
133.808755683444));
#124407=CARTESIAN_POINT('Ctrl Pts',(-198.184627513538,3.97361594297526,
133.702559955126));
#124408=CARTESIAN_POINT('Ctrl Pts',(-198.192401847657,4.05400766411971,
133.592337783489));
#124409=CARTESIAN_POINT('Ctrl Pts',(-198.200176181776,4.12993714679204,
133.478593573467));
#124410=CARTESIAN_POINT('Ctrl Pts',(-198.207950515895,4.20107997053173,
133.361724522781));
#124411=CARTESIAN_POINT('Ctrl Pts',(-198.215715268842,4.27213511709918,
133.244999502756));
#124412=CARTESIAN_POINT('Ctrl Pts',(-198.22348002179,4.33841514090281,133.125157635332));
#124413=CARTESIAN_POINT('Ctrl Pts',(-198.231244774737,4.39963687332856,
133.002627763603));
#124414=CARTESIAN_POINT('Ctrl Pts',(-198.239001815622,4.46079779946676,
132.88021959027));
#124415=CARTESIAN_POINT('Ctrl Pts',(-198.246758856507,4.5169102585312,132.755129073059));
#124416=CARTESIAN_POINT('Ctrl Pts',(-198.254515897392,4.56773547585683,
132.627812203186));
#124417=CARTESIAN_POINT('Ctrl Pts',(-198.262267088632,4.61852236549037,
132.500591343955));
#124418=CARTESIAN_POINT('Ctrl Pts',(-198.270018279872,4.66402980520103,
132.371147835464));
#124419=CARTESIAN_POINT('Ctrl Pts',(-198.277769471112,4.70406605538651,
132.239960007737));
#124420=CARTESIAN_POINT('Ctrl Pts',(-198.285517367889,4.74408528909782,
132.108827938336));
#124421=CARTESIAN_POINT('Ctrl Pts',(-198.293265264666,4.77863784444936,
131.975953397409));
#124422=CARTESIAN_POINT('Ctrl Pts',(-198.301013161443,4.80758109007599,
131.841832123124));
#124423=CARTESIAN_POINT('Ctrl Pts',(-198.308759437527,4.83651828139958,
131.707738904118));
#124424=CARTESIAN_POINT('Ctrl Pts',(-198.316505713611,4.8598484144299,131.572399852405));
#124425=CARTESIAN_POINT('Ctrl Pts',(-198.324251989695,4.87747955738707,
131.436322823533));
#124426=CARTESIAN_POINT('Ctrl Pts',(-198.331998322961,4.89511083049331,
131.300244790173));
#124427=CARTESIAN_POINT('Ctrl Pts',(-198.339744656226,4.90704297934507,
131.163429156507));
#124428=CARTESIAN_POINT('Ctrl Pts',(-198.347490989491,4.91323577800568,
131.026390462913));
#124429=CARTESIAN_POINT('Ctrl Pts',(-198.355239057494,4.91942996350062,
130.889321080454));
#124430=CARTESIAN_POINT('Ctrl Pts',(-198.362987125497,4.91988222358433,
130.752028929157));
#124431=CARTESIAN_POINT('Ctrl Pts',(-198.3707351935,4.91460444749664,130.615029724296));
#124432=CARTESIAN_POINT('Ctrl Pts',(-198.378491496242,4.9093210621257,130.47788491505));
#124433=CARTESIAN_POINT('Ctrl Pts',(-198.386247798984,4.8982954903254,130.341034065488));
#124434=CARTESIAN_POINT('Ctrl Pts',(-198.394004101726,4.88159167919793,
130.204989497069));
#124435=CARTESIAN_POINT('Ctrl Pts',(-198.40176454424,4.86487895274352,130.068872317568));
#124436=CARTESIAN_POINT('Ctrl Pts',(-198.409524986754,4.84248201195462,
129.93356266222));
#124437=CARTESIAN_POINT('Ctrl Pts',(-198.417285429268,4.8145160155251,129.799562827584));
#124438=CARTESIAN_POINT('Ctrl Pts',(-198.425058329534,4.78650512559541,
129.665347884518));
#124439=CARTESIAN_POINT('Ctrl Pts',(-198.432831229799,4.7529074110492,129.532447343168));
#124440=CARTESIAN_POINT('Ctrl Pts',(-198.440604130065,4.71388825706518,
129.401349369428));
#124441=CARTESIAN_POINT('Ctrl Pts',(-198.448094465827,4.67628754761169,
129.275017137248));
#124442=CARTESIAN_POINT('Ctrl Pts',(-198.455584801589,4.6336528210575,129.150358983697));
#124443=CARTESIAN_POINT('Ctrl Pts',(-198.463075137351,4.58617366210336,
129.027792520495));
#124444=CARTESIAN_POINT('Ctrl Pts',(-198.47084947147,4.53689431640671,128.900578912589));
#124445=CARTESIAN_POINT('Ctrl Pts',(-198.478623805589,4.48223983117683,
128.775215764509));
#124446=CARTESIAN_POINT('Ctrl Pts',(-198.486398139708,4.42236902292319,
128.652190715446));
#124447=CARTESIAN_POINT('Ctrl Pts',(-198.494162892655,4.36257200009024,
128.529317283763));
#124448=CARTESIAN_POINT('Ctrl Pts',(-198.501927645602,4.29757161477436,
128.408776565947));
#124449=CARTESIAN_POINT('Ctrl Pts',(-198.509692398549,4.22757560526325,
128.29103859994));
#124450=CARTESIAN_POINT('Ctrl Pts',(-198.517449439434,4.15764911677518,
128.173417572941));
#124451=CARTESIAN_POINT('Ctrl Pts',(-198.525206480319,4.08273707664526,
128.058594091884));
#124452=CARTESIAN_POINT('Ctrl Pts',(-198.532963521204,4.0030940596596,127.947015519049));
#124453=CARTESIAN_POINT('Ctrl Pts',(-198.540714712445,3.92351110209268,
127.835521088484));
#124454=CARTESIAN_POINT('Ctrl Pts',(-198.548465903685,3.8392044951129,127.727267012445));
#124455=CARTESIAN_POINT('Ctrl Pts',(-198.556217094925,3.7504730313789,127.622673155951));
#124456=CARTESIAN_POINT('Ctrl Pts',(-198.563964991702,3.66177928088409,
127.518123754636));
#124457=CARTESIAN_POINT('Ctrl Pts',(-198.571712888479,3.56866466656006,
127.417231776227));
#124458=CARTESIAN_POINT('Ctrl Pts',(-198.579460785256,3.47146917123165,
127.320385179121));
#124459=CARTESIAN_POINT('Ctrl Pts',(-198.58720706134,3.37429400710557,127.223558840235));
#124460=CARTESIAN_POINT('Ctrl Pts',(-198.594953337424,3.27303993667195,
127.130776475282));
#124461=CARTESIAN_POINT('Ctrl Pts',(-198.602699613508,3.16808454181421,
127.042389937401));
#124462=CARTESIAN_POINT('Ctrl Pts',(-198.610445946774,3.06312837219946,
126.954002747071));
#124463=CARTESIAN_POINT('Ctrl Pts',(-198.618192280039,2.95447112269024,
126.870011700402));
#124464=CARTESIAN_POINT('Ctrl Pts',(-198.625938613304,2.84252394757572,
126.790728762256));
#124465=CARTESIAN_POINT('Ctrl Pts',(-198.633686681307,2.73055170266768,
126.711428069246));
#124466=CARTESIAN_POINT('Ctrl Pts',(-198.64143474931,2.61528838508869,126.636837808705));
#124467=CARTESIAN_POINT('Ctrl Pts',(-198.649182817313,2.49717430712868,
126.567226734584));
#124468=CARTESIAN_POINT('Ctrl Pts',(-198.656939120055,2.37893469612088,
126.497541676984));
#124469=CARTESIAN_POINT('Ctrl Pts',(-198.664695422797,2.2578386096946,126.432846575844));
#124470=CARTESIAN_POINT('Ctrl Pts',(-198.672451725539,2.13435164337421,
126.373364552918));
#124471=CARTESIAN_POINT('Ctrl Pts',(-198.680212168053,2.01079876834144,
126.313850782646));
#124472=CARTESIAN_POINT('Ctrl Pts',(-198.687972610567,1.88485282955681,
126.259555789408));
#124473=CARTESIAN_POINT('Ctrl Pts',(-198.695733053081,1.75699866942774,
126.210654190493));
#124474=CARTESIAN_POINT('Ctrl Pts',(-198.703505953346,1.62893926645082,
126.161674090391));
#124475=CARTESIAN_POINT('Ctrl Pts',(-198.711278853612,1.49896589169275,
126.1181048103));
#124476=CARTESIAN_POINT('Ctrl Pts',(-198.719051753877,1.36757864767384,
126.080071072573));
#124477=CARTESIAN_POINT('Ctrl Pts',(-198.726542089639,1.24096766091596,
126.043419957014));
#124478=CARTESIAN_POINT('Ctrl Pts',(-198.734032425402,1.11304411471436,
126.011908983002));
#124479=CARTESIAN_POINT('Ctrl Pts',(-198.741522761164,0.984261832800122,
125.985604376896));
#124480=CARTESIAN_POINT('Ctrl Pts',(-198.749297095283,0.850596731528147,
125.958302423656));
#124481=CARTESIAN_POINT('Ctrl Pts',(-198.757071429402,0.715583080302673,
125.936522946273));
#124482=CARTESIAN_POINT('Ctrl Pts',(-198.764845763521,0.579716987989611,
125.920395908814));
#124483=CARTESIAN_POINT('Ctrl Pts',(-198.772610516468,0.444018338491886,
125.904288746487));
#124484=CARTESIAN_POINT('Ctrl Pts',(-198.780375269415,0.307469722715481,
125.89382020921));
#124485=CARTESIAN_POINT('Ctrl Pts',(-198.788140022362,0.170578884512039,
125.889069587865));
#124486=CARTESIAN_POINT('Ctrl Pts',(-198.795897063247,0.0338240082189226,
125.884323684905));
#124487=CARTESIAN_POINT('Ctrl Pts',(-198.803654104132,-0.103272025883022,
125.885284409655));
#124488=CARTESIAN_POINT('Ctrl Pts',(-198.811411145017,-0.240195235348314,
125.891979391377));
#124489=CARTESIAN_POINT('Ctrl Pts',(-198.819162336258,-0.377015189955682,
125.898669324361));
#124490=CARTESIAN_POINT('Ctrl Pts',(-198.826913527498,-0.513662190418549,
125.911084888148));
#124491=CARTESIAN_POINT('Ctrl Pts',(-198.834664718738,-0.649621487673782,
125.929201647312));
#124492=CARTESIAN_POINT('Ctrl Pts',(-198.842412615515,-0.785522998601034,
125.947310706369));
#124493=CARTESIAN_POINT('Ctrl Pts',(-198.850160512292,-0.920737000939123,
125.971116089789));
#124494=CARTESIAN_POINT('Ctrl Pts',(-198.857908409069,-1.05475332528018,
126.000541461383));
#124495=CARTESIAN_POINT('Ctrl Pts',(-198.865654685153,-1.18874161629487,
126.029960677823));
#124496=CARTESIAN_POINT('Ctrl Pts',(-198.873400961237,-1.32153234600044,
126.064997460351));
#124497=CARTESIAN_POINT('Ctrl Pts',(-198.881147237321,-1.45262539815508,
126.105524323851));
#124498=CARTESIAN_POINT('Ctrl Pts',(-198.888893570586,-1.58371941800903,
126.14605148651));
#124499=CARTESIAN_POINT('Ctrl Pts',(-198.896639903852,-1.71311536178222,
126.192068695536));
#124500=CARTESIAN_POINT('Ctrl Pts',(-198.904386237117,-1.84032852566538,
126.243398659807));
#124501=CARTESIAN_POINT('Ctrl Pts',(-198.91213430512,-1.96757017805508,
126.294740119068));
#124502=CARTESIAN_POINT('Ctrl Pts',(-198.919882373123,-2.09262771536865,
126.351396554784));
#124503=CARTESIAN_POINT('Ctrl Pts',(-198.927630441126,-2.2150370277501,
126.413142787829));
#124504=CARTESIAN_POINT('Ctrl Pts',(-198.935386743868,-2.33757643820495,
126.474954645506));
#124505=CARTESIAN_POINT('Ctrl Pts',(-198.94314304661,-2.4574616517044,126.541866930204));
#124506=CARTESIAN_POINT('Ctrl Pts',(-198.950899349351,-2.57425328384323,
126.613608525981));
#124507=CARTESIAN_POINT('Ctrl Pts',(-198.958659791866,-2.69110725119298,
126.685388412409));
#124508=CARTESIAN_POINT('Ctrl Pts',(-198.96642023438,-2.80486402303167,
126.762002527609));
#124509=CARTESIAN_POINT('Ctrl Pts',(-198.974180676894,-2.91511461972486,
126.843137344842));
#124510=CARTESIAN_POINT('Ctrl Pts',(-198.981953577159,-3.02554220046346,
126.924402406887));
#124511=CARTESIAN_POINT('Ctrl Pts',(-198.989726477425,-3.13245205358369,
127.010202427981));
#124512=CARTESIAN_POINT('Ctrl Pts',(-198.99749937769,-3.23546892900845,
127.100184073188));
#124513=CARTESIAN_POINT('Ctrl Pts',(-199.004989713452,-3.33474088152516,
127.186894658939));
#124514=CARTESIAN_POINT('Ctrl Pts',(-199.012480049214,-3.43039775782205,
127.277487910186));
#124515=CARTESIAN_POINT('Ctrl Pts',(-199.019970384976,-3.52213853697615,
127.371617809133));
#124516=CARTESIAN_POINT('Ctrl Pts',(-199.027641276347,-3.6160907406696,
127.468016722693));
#124517=CARTESIAN_POINT('Ctrl Pts',(-199.035312167719,-3.70625045185473,
127.568448295507));
#124518=CARTESIAN_POINT('Ctrl Pts',(-199.04298305909,-3.79224452810265,
127.672577658679));
#124519=CARTESIAN_POINT('Ctrl Pts',(-199.0506449325,-3.87813750901698,127.776584606526));
#124520=CARTESIAN_POINT('Ctrl Pts',(-199.058306805909,-3.9598743377894,
127.884280395336));
#124521=CARTESIAN_POINT('Ctrl Pts',(-199.065968679319,-4.03711767976908,
127.995292462075));
#124522=CARTESIAN_POINT('Ctrl Pts',(-199.073623311162,-4.11428801574521,
128.106199606536));
#124523=CARTESIAN_POINT('Ctrl Pts',(-199.081277943005,-4.1869730825278,
128.220416467907));
#124524=CARTESIAN_POINT('Ctrl Pts',(-199.088932574849,-4.25487528640376,
128.337536878494));
#124525=CARTESIAN_POINT('Ctrl Pts',(-199.096581319393,-4.32272526561704,
128.454567209913));
#124526=CARTESIAN_POINT('Ctrl Pts',(-199.104230063938,-4.38579950174855,
128.574496299718));
#124527=CARTESIAN_POINT('Ctrl Pts',(-199.111878808483,-4.44384363448245,
128.696888953517));
#124528=CARTESIAN_POINT('Ctrl Pts',(-199.119524183703,-4.50186219837772,
128.819227692512));
#124529=CARTESIAN_POINT('Ctrl Pts',(-199.127169558923,-4.55485489515574,
128.944027473816));
#124530=CARTESIAN_POINT('Ctrl Pts',(-199.134814934143,-4.60261344758878,
129.070828813827));
#124531=CARTESIAN_POINT('Ctrl Pts',(-199.142459303634,-4.65036571750983,
129.197613473455));
#124532=CARTESIAN_POINT('Ctrl Pts',(-199.150103673125,-4.69288506876711,
129.32639879276));
#124533=CARTESIAN_POINT('Ctrl Pts',(-199.157748042617,-4.73001164933185,
129.456706040278));
#124534=CARTESIAN_POINT('Ctrl Pts',(-199.160198861551,-4.74191459655825,
129.498483124697));
#124535=CARTESIAN_POINT('Ctrl Pts',(-199.162649680486,-4.75326361641396,
129.540416517897));
#124536=CARTESIAN_POINT('Ctrl Pts',(-199.165100499421,-4.76405452823391,
129.582490119308));
#124537=CARTESIAN_POINT('Ctrl Pts',(-197.415422870675,-4.76405452823413,
129.582490119309));
#124538=CARTESIAN_POINT('Ctrl Pts',(-197.423600431488,-4.79992281658223,
129.722340031201));
#124539=CARTESIAN_POINT('Ctrl Pts',(-197.431777992302,-4.82966733555782,
129.863920110019));
#124540=CARTESIAN_POINT('Ctrl Pts',(-197.439955553115,-4.85313234200592,
130.006683030144));
#124541=CARTESIAN_POINT('Ctrl Pts',(-197.448116021641,-4.87654830318953,
130.149147555073));
#124542=CARTESIAN_POINT('Ctrl Pts',(-197.456276490167,-4.89371087298272,
130.292789672346));
#124543=CARTESIAN_POINT('Ctrl Pts',(-197.464436958693,-4.90451488430555,
130.437050377952));
#124544=CARTESIAN_POINT('Ctrl Pts',(-197.471338160455,-4.91365169572061,
130.559049774504));
#124545=CARTESIAN_POINT('Ctrl Pts',(-197.478239362217,-4.91824176802981,
130.681491218841));
#124546=CARTESIAN_POINT('Ctrl Pts',(-197.485140563979,-4.91824998893204,
130.804030662974));
#124547=CARTESIAN_POINT('',(-197.13985943604,-4.91824821858491,130.800174582878));
#124548=CARTESIAN_POINT('Ctrl Pts',(-197.069830899744,-4.76405452823391,
129.582490119308));
#124549=CARTESIAN_POINT('Ctrl Pts',(-197.076695937978,-4.79406056862158,
129.699483215374));
#124550=CARTESIAN_POINT('Ctrl Pts',(-197.083560976212,-4.81971881788819,
129.817443076));
#124551=CARTESIAN_POINT('Ctrl Pts',(-197.090426014446,-4.84098812800867,
129.936019090873));
#124552=CARTESIAN_POINT('Ctrl Pts',(-197.102330337474,-4.87787018599897,
130.14163588954));
#124553=CARTESIAN_POINT('Ctrl Pts',(-197.114234660503,-4.90165998726396,
130.349666738386));
#124554=CARTESIAN_POINT('Ctrl Pts',(-197.126138983531,-4.91211451822462,
130.558771484364));
#124555=CARTESIAN_POINT('Ctrl Pts',(-197.130712467685,-4.91613101135752,
130.639106774339));
#124556=CARTESIAN_POINT('Ctrl Pts',(-197.13528595184,-4.91817963992249,
130.719600281634));
#124557=CARTESIAN_POINT('Ctrl Pts',(-197.139859435995,-4.91824821858423,
130.80017458208));
#124558=CARTESIAN_POINT('Ctrl Pts',(-197.13985943604,-4.91824821858491,
130.800174582878));
#124559=CARTESIAN_POINT('Ctrl Pts',(-197.147506112978,-4.91836287925791,
130.93489149106));
#124560=CARTESIAN_POINT('Ctrl Pts',(-197.155152789915,-4.91293828803124,
131.069802457209));
#124561=CARTESIAN_POINT('Ctrl Pts',(-197.162799466852,-4.9019533167259,
131.204406543854));
#124562=CARTESIAN_POINT('Ctrl Pts',(-197.170439161222,-4.89097837635308,
131.338887716705));
#124563=CARTESIAN_POINT('Ctrl Pts',(-197.178078855592,-4.87445318757935,
131.473062167562));
#124564=CARTESIAN_POINT('Ctrl Pts',(-197.185718549962,-4.85240867394315,
131.606428646814));
#124565=CARTESIAN_POINT('Ctrl Pts',(-197.193353528545,-4.83037776781788,
131.73971280237));
#124566=CARTESIAN_POINT('Ctrl Pts',(-197.200988507129,-4.80283437820965,
131.872189581299));
#124567=CARTESIAN_POINT('Ctrl Pts',(-197.208623485712,-4.76986124614636,
132.003363017485));
#124568=CARTESIAN_POINT('Ctrl Pts',(-197.216256000669,-4.73689875372977,
132.134494127118));
#124569=CARTESIAN_POINT('Ctrl Pts',(-197.223888515626,-4.69851009985092,
132.264322339006));
#124570=CARTESIAN_POINT('Ctrl Pts',(-197.231521030583,-4.6548290030468,
132.392362511423));
#124571=CARTESIAN_POINT('Ctrl Pts',(-197.239152849597,-4.61115188914653,
132.520391008958));
#124572=CARTESIAN_POINT('Ctrl Pts',(-197.24678466861,-4.56218342217936,
132.646631409198));
#124573=CARTESIAN_POINT('Ctrl Pts',(-197.254416487624,-4.50810682560393,
132.770614902099));
#124574=CARTESIAN_POINT('Ctrl Pts',(-197.262049377602,-4.45402264051946,
132.894615793466));
#124575=CARTESIAN_POINT('Ctrl Pts',(-197.26968226758,-4.39482906232151,
133.016358777953));
#124576=CARTESIAN_POINT('Ctrl Pts',(-197.277315157558,-4.33075673716147,
133.135396684647));
#124577=CARTESIAN_POINT('Ctrl Pts',(-197.284955576458,-4.26662121241328,
133.254552007817));
#124578=CARTESIAN_POINT('Ctrl Pts',(-197.292595995358,-4.19759752046628,
133.37099656774));
#124579=CARTESIAN_POINT('Ctrl Pts',(-197.300236414258,-4.1239615861599,
133.484309105574));
#124580=CARTESIAN_POINT('Ctrl Pts',(-197.307880546064,-4.05028986803414,
133.597676708309));
#124581=CARTESIAN_POINT('Ctrl Pts',(-197.315524677871,-3.97200167824627,
133.707908929455));
#124582=CARTESIAN_POINT('Ctrl Pts',(-197.323168809677,-3.88941447193958,
133.814616109707));
#124583=CARTESIAN_POINT('Ctrl Pts',(-197.330825110679,-3.8066957896451,
133.921493164115));
#124584=CARTESIAN_POINT('Ctrl Pts',(-197.33848141168,-3.71966467800465,
134.024833657621));
#124585=CARTESIAN_POINT('Ctrl Pts',(-197.346137712681,-3.62867730838004,
134.124282913968));
#124586=CARTESIAN_POINT('Ctrl Pts',(-197.35371635454,-3.53861283886426,
134.222723439874));
#124587=CARTESIAN_POINT('Ctrl Pts',(-197.3612949964,-3.44467233174058,134.317351104802));
#124588=CARTESIAN_POINT('Ctrl Pts',(-197.368873638259,-3.34723265001436,
134.407861227969));
#124589=CARTESIAN_POINT('Ctrl Pts',(-197.376647972378,-3.24727692493325,
134.500708462567));
#124590=CARTESIAN_POINT('Ctrl Pts',(-197.384422306497,-3.14329678401998,
134.589540674901));
#124591=CARTESIAN_POINT('Ctrl Pts',(-197.392196640617,-3.03564832798573,
134.673988802715));
#124592=CARTESIAN_POINT('Ctrl Pts',(-197.399961393564,-2.92813253905301,
134.758332855758));
#124593=CARTESIAN_POINT('Ctrl Pts',(-197.407726146511,-2.81695773483861,
134.83830333563));
#124594=CARTESIAN_POINT('Ctrl Pts',(-197.415490899458,-2.70251631213269,
134.91356840559));
#124595=CARTESIAN_POINT('Ctrl Pts',(-197.423247940343,-2.58818855426113,
134.988758721222));
#124596=CARTESIAN_POINT('Ctrl Pts',(-197.431004981228,-2.47060095904148,
135.059252713936));
#124597=CARTESIAN_POINT('Ctrl Pts',(-197.438762022113,-2.35017812468133,
135.124759423784));
#124598=CARTESIAN_POINT('Ctrl Pts',(-197.446513213353,-2.22984610211716,
135.190216734512));
#124599=CARTESIAN_POINT('Ctrl Pts',(-197.454264404593,-2.1066834381736,
135.250694062248));
#124600=CARTESIAN_POINT('Ctrl Pts',(-197.462015595833,-1.98114246876202,
135.305944514481));
#124601=CARTESIAN_POINT('Ctrl Pts',(-197.46976349261,-1.85565485761151,
135.361171483799));
#124602=CARTESIAN_POINT('Ctrl Pts',(-197.477511389387,-1.72779130857727,
135.411175838973));
#124603=CARTESIAN_POINT('Ctrl Pts',(-197.485259286164,-1.59802724398115,
135.455757395954));
#124604=CARTESIAN_POINT('Ctrl Pts',(-197.493005562248,-1.46829032322996,
135.500329627433));
#124605=CARTESIAN_POINT('Ctrl Pts',(-197.500751838333,-1.33665404717749,
135.539481190017));
#124606=CARTESIAN_POINT('Ctrl Pts',(-197.508498114417,-1.20361185877549,
135.573060813208));
#124607=CARTESIAN_POINT('Ctrl Pts',(-197.516244447682,-1.0705686882861,
135.606640684276));
#124608=CARTESIAN_POINT('Ctrl Pts',(-197.523990780947,-0.936119963815441,
135.634648438198));
#124609=CARTESIAN_POINT('Ctrl Pts',(-197.531737114213,-0.800771873265166,
135.656983358877));
#124610=CARTESIAN_POINT('Ctrl Pts',(-197.539485182216,-0.665393472448266,
135.679323281307));
#124611=CARTESIAN_POINT('Ctrl Pts',(-197.547233250219,-0.52911569045003,
135.695987778918));
#124612=CARTESIAN_POINT('Ctrl Pts',(-197.554981318222,-0.392452037104296,
135.706927747252));
#124613=CARTESIAN_POINT('Ctrl Pts',(-197.562737620963,-0.255643136002026,
135.717879342714));
#124614=CARTESIAN_POINT('Ctrl Pts',(-197.570493923705,-0.118447934655994,
135.723094224012));
#124615=CARTESIAN_POINT('Ctrl Pts',(-197.578250226447,0.0186172786708312,
135.722575381018));
#124616=CARTESIAN_POINT('Ctrl Pts',(-197.586010668961,0.155755647829336,
135.722056261102));
#124617=CARTESIAN_POINT('Ctrl Pts',(-197.593771111476,0.292763500359275,
135.715797336897));
#124618=CARTESIAN_POINT('Ctrl Pts',(-197.60153155399,0.429128454194537,
135.703853635451));
#124619=CARTESIAN_POINT('Ctrl Pts',(-197.609304454255,0.565712313159607,
135.691890760914));
#124620=CARTESIAN_POINT('Ctrl Pts',(-197.617077354521,0.701650823160877,
135.674224923474));
#124621=CARTESIAN_POINT('Ctrl Pts',(-197.624850254786,0.836439701705548,
135.650962694064));
#124622=CARTESIAN_POINT('Ctrl Pts',(-197.632340590548,0.966328665002057,
135.628546105287));
#124623=CARTESIAN_POINT('Ctrl Pts',(-197.63983092631,1.09514982852237,135.600933010851));
#124624=CARTESIAN_POINT('Ctrl Pts',(-197.647321262072,1.2224661119373,135.568262344897));
#124625=CARTESIAN_POINT('Ctrl Pts',(-197.655095596191,1.35460963093539,
135.534352960713));
#124626=CARTESIAN_POINT('Ctrl Pts',(-197.66286993031,1.48555049305068,135.494887503906));
#124627=CARTESIAN_POINT('Ctrl Pts',(-197.670644264429,1.61478571462178,
135.449966084925));
#124628=CARTESIAN_POINT('Ctrl Pts',(-197.678409017376,1.74386166533168,
135.405100027578));
#124629=CARTESIAN_POINT('Ctrl Pts',(-197.686173770323,1.87123579220267,
135.354791513917));
#124630=CARTESIAN_POINT('Ctrl Pts',(-197.693938523271,1.99641681153709,
135.29919131261));
#124631=CARTESIAN_POINT('Ctrl Pts',(-197.701695564156,2.1214734993187,135.243646334207));
#124632=CARTESIAN_POINT('Ctrl Pts',(-197.70945260504,2.24434105933608,135.182820285069));
#124633=CARTESIAN_POINT('Ctrl Pts',(-197.717209645925,2.36454519304033,
135.116913120733));
#124634=CARTESIAN_POINT('Ctrl Pts',(-197.724960837166,2.4846586798728,135.051055657502));
#124635=CARTESIAN_POINT('Ctrl Pts',(-197.732712028406,2.60211239678094,
134.98012489306));
#124636=CARTESIAN_POINT('Ctrl Pts',(-197.740463219646,2.7164541274949,134.904367938988));
#124637=CARTESIAN_POINT('Ctrl Pts',(-197.748211116423,2.83074725992267,
134.828643183643));
#124638=CARTESIAN_POINT('Ctrl Pts',(-197.7559590132,2.94193071162179,134.748096533953));
#124639=CARTESIAN_POINT('Ctrl Pts',(-197.763706909977,3.04957908470244,
134.663019771812));
#124640=CARTESIAN_POINT('Ctrl Pts',(-197.771453186061,3.15720494006407,
134.577960805895));
#124641=CARTESIAN_POINT('Ctrl Pts',(-197.779199462145,3.26129688109708,
134.488373854626));
#124642=CARTESIAN_POINT('Ctrl Pts',(-197.786945738229,3.361460921679,134.394592300135));
#124643=CARTESIAN_POINT('Ctrl Pts',(-197.794692071495,3.46162570164924,
134.30081005337));
#124644=CARTESIAN_POINT('Ctrl Pts',(-197.80243840476,3.55786223791384,134.20283340881));
#124645=CARTESIAN_POINT('Ctrl Pts',(-197.810184738026,3.64981218824234,
134.101033797161));
#124646=CARTESIAN_POINT('Ctrl Pts',(-197.817932806029,3.74178273012479,
133.999211388194));
#124647=CARTESIAN_POINT('Ctrl Pts',(-197.825680874032,3.82946451386792,
133.893564598623));
#124648=CARTESIAN_POINT('Ctrl Pts',(-197.833428942035,3.91253866189194,
133.784498916656));
#124649=CARTESIAN_POINT('Ctrl Pts',(-197.841185244776,3.99570110210896,
133.675317318384));
#124650=CARTESIAN_POINT('Ctrl Pts',(-197.848941547518,4.07424588694472,
133.562709880643));
#124651=CARTESIAN_POINT('Ctrl Pts',(-197.85669785026,4.14789646544683,133.44711258747));
#124652=CARTESIAN_POINT('Ctrl Pts',(-197.864458292774,4.22158635348026,
133.331453596542));
#124653=CARTESIAN_POINT('Ctrl Pts',(-197.872218735289,4.29037663418042,
133.212801908529));
#124654=CARTESIAN_POINT('Ctrl Pts',(-197.879979177803,4.35403664833725,
133.091618348439));
#124655=CARTESIAN_POINT('Ctrl Pts',(-197.887752078068,4.41779885520026,
132.970240253739));
#124656=CARTESIAN_POINT('Ctrl Pts',(-197.895524978334,4.4764141709775,132.846322518647));
#124657=CARTESIAN_POINT('Ctrl Pts',(-197.903297878599,4.52969967980894,
132.720347014501));
#124658=CARTESIAN_POINT('Ctrl Pts',(-197.910788214361,4.58104812617597,
132.598951037243));
#124659=CARTESIAN_POINT('Ctrl Pts',(-197.918278550123,4.62744743329827,
132.475644591939));
#124660=CARTESIAN_POINT('Ctrl Pts',(-197.925768885885,4.66877823780837,
132.350870503945));
#124661=CARTESIAN_POINT('Ctrl Pts',(-197.933543220004,4.71167611233399,
132.221365568478));
#124662=CARTESIAN_POINT('Ctrl Pts',(-197.941317554123,4.74924944018407,
132.089869269341));
#124663=CARTESIAN_POINT('Ctrl Pts',(-197.949091888242,4.78131057215974,
131.956858893076));
#124664=CARTESIAN_POINT('Ctrl Pts',(-197.956856641189,4.81333219165545,
131.824012440213));
#124665=CARTESIAN_POINT('Ctrl Pts',(-197.964621394136,4.83985504116094,
131.689655999366));
#124666=CARTESIAN_POINT('Ctrl Pts',(-197.972386147084,4.86074041578861,
131.554284395572));
#124667=CARTESIAN_POINT('Ctrl Pts',(-197.980143187969,4.88160504676788,
131.419047244763));
#124668=CARTESIAN_POINT('Ctrl Pts',(-197.987900228854,4.89684328634105,
131.282797321412));
#124669=CARTESIAN_POINT('Ctrl Pts',(-197.995657269739,4.90636699281359,
131.146041747173));
#124670=CARTESIAN_POINT('Ctrl Pts',(-198.003408460979,4.91588351738501,
131.009389301376));
#124671=CARTESIAN_POINT('Ctrl Pts',(-198.011159652219,4.91969405935185,
130.872232352118));
#124672=CARTESIAN_POINT('Ctrl Pts',(-198.018910843459,4.91776208674575,
130.7350849316));
#124673=CARTESIAN_POINT('Ctrl Pts',(-198.026658740236,4.91583093527955,
130.597995802394));
#124674=CARTESIAN_POINT('Ctrl Pts',(-198.034406637013,4.90816212914558,
130.460916583982));
#124675=CARTESIAN_POINT('Ctrl Pts',(-198.04215453379,4.89477121476498,130.324362890896));
#124676=CARTESIAN_POINT('Ctrl Pts',(-198.049900809875,4.881383101475,130.187837761899));
#124677=CARTESIAN_POINT('Ctrl Pts',(-198.057647085959,4.86227529885319,
130.051838328427));
#124678=CARTESIAN_POINT('Ctrl Pts',(-198.065393362043,4.83751533160561,
129.916876263349));
#124679=CARTESIAN_POINT('Ctrl Pts',(-198.073139695308,4.81275518158554,
129.78191320201));
#124680=CARTESIAN_POINT('Ctrl Pts',(-198.080886028573,4.78234285423304,
129.647987908893));
#124681=CARTESIAN_POINT('Ctrl Pts',(-198.088632361839,4.74639715199262,
129.515602634834));
#124682=CARTESIAN_POINT('Ctrl Pts',(-198.096380429842,4.71044339996136,
129.38318771401));
#124683=CARTESIAN_POINT('Ctrl Pts',(-198.104128497845,4.66895390968266,
129.25231387574));
#124684=CARTESIAN_POINT('Ctrl Pts',(-198.111876565848,4.62209746874859,
129.123468577045));
#124685=CARTESIAN_POINT('Ctrl Pts',(-198.11963286859,4.57519122823157,128.994486340033));
#124686=CARTESIAN_POINT('Ctrl Pts',(-198.127389171331,4.52290677641864,
128.867537317358));
#124687=CARTESIAN_POINT('Ctrl Pts',(-198.135145474073,4.46546143648297,
128.743089839191));
#124688=CARTESIAN_POINT('Ctrl Pts',(-198.142905916588,4.40798543623973,
128.618575939658));
#124689=CARTESIAN_POINT('Ctrl Pts',(-198.150666359102,4.34534323773866,
128.496566592663));
#124690=CARTESIAN_POINT('Ctrl Pts',(-198.158426801616,4.27779786917148,
128.377504945506));
#124691=CARTESIAN_POINT('Ctrl Pts',(-198.166199701881,4.21014407078227,
128.258252170022));
#124692=CARTESIAN_POINT('Ctrl Pts',(-198.173972602147,4.13757158065354,
128.141956882111));
#124693=CARTESIAN_POINT('Ctrl Pts',(-198.181745502412,4.06038694029745,
128.029033437293));
#124694=CARTESIAN_POINT('Ctrl Pts',(-198.189235838174,3.98600815603532,
127.920215044132));
#124695=CARTESIAN_POINT('Ctrl Pts',(-198.196726173936,3.90734691024696,
127.81452784734));
#124696=CARTESIAN_POINT('Ctrl Pts',(-198.204216509698,3.8247112456301,127.712311628619));
#124697=CARTESIAN_POINT('Ctrl Pts',(-198.211990843817,3.73894242467187,
127.606219850896));
#124698=CARTESIAN_POINT('Ctrl Pts',(-198.219765177936,3.64862016552164,
127.503531384384));
#124699=CARTESIAN_POINT('Ctrl Pts',(-198.227539512055,3.55404459388961,
127.404662088704));
#124700=CARTESIAN_POINT('Ctrl Pts',(-198.235304265002,3.45958557819766,
127.305914640596));
#124701=CARTESIAN_POINT('Ctrl Pts',(-198.24306901795,3.36088394735533,127.210977278024));
#124702=CARTESIAN_POINT('Ctrl Pts',(-198.250833770897,3.25828103830071,
127.12023416236));
#124703=CARTESIAN_POINT('Ctrl Pts',(-198.258590811782,3.15578003590126,
127.029581174037));
#124704=CARTESIAN_POINT('Ctrl Pts',(-198.266347852667,3.04938575729155,
126.943114399854));
#124705=CARTESIAN_POINT('Ctrl Pts',(-198.274104893552,2.93947721554274,
126.861182107556));
#124706=CARTESIAN_POINT('Ctrl Pts',(-198.281856084792,2.82965155668068,
126.779311601038));
#124707=CARTESIAN_POINT('Ctrl Pts',(-198.289607276032,2.71631722179468,
126.701969002842));
#124708=CARTESIAN_POINT('Ctrl Pts',(-198.297358467272,2.59988693431213,
126.629462895311));
#124709=CARTESIAN_POINT('Ctrl Pts',(-198.305106364049,2.48350613280748,
126.556987604809));
#124710=CARTESIAN_POINT('Ctrl Pts',(-198.312854260826,2.36403232703562,
126.489344922703));
#124711=CARTESIAN_POINT('Ctrl Pts',(-198.320602157603,2.24190772132709,
126.4268004716));
#124712=CARTESIAN_POINT('Ctrl Pts',(-198.328348433687,2.11980866145337,
126.364269103447));
#124713=CARTESIAN_POINT('Ctrl Pts',(-198.336094709771,1.99506025231821,
126.306834023191));
#124714=CARTESIAN_POINT('Ctrl Pts',(-198.343840985855,1.8681294775501,126.254714992069));
#124715=CARTESIAN_POINT('Ctrl Pts',(-198.351587319121,1.74119776580766,
126.202595576215));
#124716=CARTESIAN_POINT('Ctrl Pts',(-198.359333652386,1.61208401795031,
126.155792436301));
#124717=CARTESIAN_POINT('Ctrl Pts',(-198.367079985652,1.48127500745482,
126.114477099312));
#124718=CARTESIAN_POINT('Ctrl Pts',(-198.374828053655,1.35043670318858,
126.07315251004));
#124719=CARTESIAN_POINT('Ctrl Pts',(-198.382576121657,1.21790275358034,
126.037318286899));
#124720=CARTESIAN_POINT('Ctrl Pts',(-198.39032418966,1.08417450384265,126.007095906534));
#124721=CARTESIAN_POINT('Ctrl Pts',(-198.398080492402,0.950304126129575,
125.976841405463));
#124722=CARTESIAN_POINT('Ctrl Pts',(-198.405836795144,0.81523729464666,
125.952210747888));
#124723=CARTESIAN_POINT('Ctrl Pts',(-198.413593097886,0.679485497313303,
125.933274237564));
#124724=CARTESIAN_POINT('Ctrl Pts',(-198.4213535404,0.543661245157932,125.914327620255));
#124725=CARTESIAN_POINT('Ctrl Pts',(-198.429113982914,0.407151687636302,
125.901081243678));
#124726=CARTESIAN_POINT('Ctrl Pts',(-198.436874425429,0.270471830283358,
125.893553346707));
#124727=CARTESIAN_POINT('Ctrl Pts',(-198.444647325694,0.133572562289896,
125.886013365287));
#124728=CARTESIAN_POINT('Ctrl Pts',(-198.45242022596,-0.00349716067967948,
125.884210212806));
#124729=CARTESIAN_POINT('Ctrl Pts',(-198.460193126225,-0.140223036415281,
125.888109956487));
#124730=CARTESIAN_POINT('Ctrl Pts',(-198.467683461987,-0.271978582175825,
125.891867934663));
#124731=CARTESIAN_POINT('Ctrl Pts',(-198.475173797749,-0.403414538811383,
125.900921357127));
#124732=CARTESIAN_POINT('Ctrl Pts',(-198.482664133511,-0.534078533749533,
125.915194719144));
#124733=CARTESIAN_POINT('Ctrl Pts',(-198.49043846763,-0.669696693770792,
125.930009260021));
#124734=CARTESIAN_POINT('Ctrl Pts',(-198.498212801749,-0.804912796249909,
125.950494310249));
#124735=CARTESIAN_POINT('Ctrl Pts',(-198.505987135868,-0.939214741433294,
125.97662214785));
#124736=CARTESIAN_POINT('Ctrl Pts',(-198.513751888815,-1.07335117147142,
126.002717785227));
#124737=CARTESIAN_POINT('Ctrl Pts',(-198.521516641762,-1.20657530576016,
126.034442299186));
#124738=CARTESIAN_POINT('Ctrl Pts',(-198.529281394709,-1.33837943750662,
126.071716161899));
#124739=CARTESIAN_POINT('Ctrl Pts',(-198.537038435594,-1.47005265953166,
126.108953003685));
#124740=CARTESIAN_POINT('Ctrl Pts',(-198.544795476479,-1.60030831193102,
126.151728120008));
#124741=CARTESIAN_POINT('Ctrl Pts',(-198.552552517364,-1.72864852136443,
126.199910883658));
#124742=CARTESIAN_POINT('Ctrl Pts',(-198.560303708605,-1.85689194844843,
126.248057312312));
#124743=CARTESIAN_POINT('Ctrl Pts',(-198.568054899845,-1.9832224431181,
126.301603134525));
#124744=CARTESIAN_POINT('Ctrl Pts',(-198.575806091085,-2.10715729921745,
126.36036791068));
#124745=CARTESIAN_POINT('Ctrl Pts',(-198.583553987862,-2.23103947969604,
126.419107710238));
#124746=CARTESIAN_POINT('Ctrl Pts',(-198.591301884639,-2.3525276942214,
126.483061884765));
#124747=CARTESIAN_POINT('Ctrl Pts',(-198.599049781416,-2.47115944473042,
126.552001970742));
#124748=CARTESIAN_POINT('Ctrl Pts',(-198.6067960575,-2.58976638003497,126.620927635939));
#124749=CARTESIAN_POINT('Ctrl Pts',(-198.614542333584,-2.70551770198718,
126.694836941795));
#124750=CARTESIAN_POINT('Ctrl Pts',(-198.622288609669,-2.81797610317734,
126.773455788074));
#124751=CARTESIAN_POINT('Ctrl Pts',(-198.630034942934,-2.93043533450971,
126.852075214699));
#124752=CARTESIAN_POINT('Ctrl Pts',(-198.637781276199,-3.03960127614829,
126.93540402711));
#124753=CARTESIAN_POINT('Ctrl Pts',(-198.645527609465,-3.14506650462893,
127.023125403517));
#124754=CARTESIAN_POINT('Ctrl Pts',(-198.653275677468,-3.25055535131611,
127.110866424519));
#124755=CARTESIAN_POINT('Ctrl Pts',(-198.661023745471,-3.35234153520745,
127.203001716974));
#124756=CARTESIAN_POINT('Ctrl Pts',(-198.668771813474,-3.4500518652282,
127.299175146049));
#124757=CARTESIAN_POINT('Ctrl Pts',(-198.676528116215,-3.54786604295059,
127.395450789389));
#124758=CARTESIAN_POINT('Ctrl Pts',(-198.684284418957,-3.64159543435231,
127.49577286795));
#124759=CARTESIAN_POINT('Ctrl Pts',(-198.692040721699,-3.73090441917804,
127.599749053358));
#124760=CARTESIAN_POINT('Ctrl Pts',(-198.699801164213,-3.82026107089802,
127.703780733986));
#124761=CARTESIAN_POINT('Ctrl Pts',(-198.707561606727,-3.90519237294011,
127.81147010078));
#124762=CARTESIAN_POINT('Ctrl Pts',(-198.715322049242,-3.98540460735336,
127.922393723553));
#124763=CARTESIAN_POINT('Ctrl Pts',(-198.723094949507,-4.06574560556619,
128.033495410773));
#124764=CARTESIAN_POINT('Ctrl Pts',(-198.730867849773,-4.14135218219585,
128.147841402763));
#124765=CARTESIAN_POINT('Ctrl Pts',(-198.738640750038,-4.21197489294038,
128.264980661014));
#124766=CARTESIAN_POINT('Ctrl Pts',(-198.7461310858,-4.28003029026089,128.37786161217));
#124767=CARTESIAN_POINT('Ctrl Pts',(-198.753621421562,-4.34345773459829,
128.493336000931));
#124768=CARTESIAN_POINT('Ctrl Pts',(-198.761111757324,-4.40207623179987,
128.610982421285));
#124769=CARTESIAN_POINT('Ctrl Pts',(-198.769439516326,-4.46724830596083,
128.741781769581));
#124770=CARTESIAN_POINT('Ctrl Pts',(-198.777767275329,-4.52666005472299,
128.87563467257));
#124771=CARTESIAN_POINT('Ctrl Pts',(-198.786095034331,-4.58003551060785,
129.012027561443));
#124772=CARTESIAN_POINT('Ctrl Pts',(-198.794402369264,-4.63328006164643,
129.148085942819));
#124773=CARTESIAN_POINT('Ctrl Pts',(-198.802709704197,-4.6805177289175,
129.2866716051));
#124774=CARTESIAN_POINT('Ctrl Pts',(-198.811017039129,-4.72151946632294,
129.427248787817));
#124775=CARTESIAN_POINT('Ctrl Pts',(-198.814059766598,-4.73653717220337,
129.478737990889));
#124776=CARTESIAN_POINT('Ctrl Pts',(-198.817102494067,-4.75071875239664,
129.530494131717));
#124777=CARTESIAN_POINT('Ctrl Pts',(-198.820145221536,-4.76405452823399,
129.582490119308));
#124778=CARTESIAN_POINT('Origin',(213.235140564004,0.,130.804360617566));
#124779=CARTESIAN_POINT('',(-200.91504706349,-4.76405452823395,129.582490119308));
#124780=CARTESIAN_POINT('',(-200.569853205643,-4.76405452823395,129.582490119308));
#124781=CARTESIAN_POINT('',(213.235140564004,-4.76405452823405,129.582490119308));
#124782=CARTESIAN_POINT('',(-199.235140563976,-4.91824791219353,130.808892361601));
#124783=CARTESIAN_POINT('Ctrl Pts',(-199.235140564013,-4.91824791219293,
130.80889236225));
#124784=CARTESIAN_POINT('Ctrl Pts',(-199.245686804809,-4.91807640527225,
130.995026757141));
#124785=CARTESIAN_POINT('Ctrl Pts',(-199.256233045605,-4.90733475277425,
131.180693350563));
#124786=CARTESIAN_POINT('Ctrl Pts',(-199.266779286401,-4.88620319730163,
131.364897304304));
#124787=CARTESIAN_POINT('Ctrl Pts',(-199.277325527197,-4.86507164182904,
131.549101258045));
#124788=CARTESIAN_POINT('Ctrl Pts',(-199.287871767993,-4.83355032983892,
131.731843197017));
#124789=CARTESIAN_POINT('Ctrl Pts',(-199.298418008789,-4.79186565731639,
131.912154183503));
#124790=CARTESIAN_POINT('Ctrl Pts',(-199.306192342908,-4.76113711829408,
132.045073380155));
#124791=CARTESIAN_POINT('Ctrl Pts',(-199.313966677027,-4.72482524621133,
132.176923596683));
#124792=CARTESIAN_POINT('Ctrl Pts',(-199.321741011146,-4.68301805246697,
132.307199591897));
#124793=CARTESIAN_POINT('Ctrl Pts',(-199.329505764093,-4.64126238235248,
132.43731503359));
#124794=CARTESIAN_POINT('Ctrl Pts',(-199.337270517041,-4.59402498413645,
132.565859745473));
#124795=CARTESIAN_POINT('Ctrl Pts',(-199.345035269988,-4.54144479361619,
132.692338967293));
#124796=CARTESIAN_POINT('Ctrl Pts',(-199.352792310873,-4.48891682648241,
132.818692568166));
#124797=CARTESIAN_POINT('Ctrl Pts',(-199.360549351758,-4.43105677640118,
132.942984402826));
#124798=CARTESIAN_POINT('Ctrl Pts',(-199.368306392643,-4.36805315947013,
133.064735510928));
#124799=CARTESIAN_POINT('Ctrl Pts',(-199.376057583883,-4.3050970540568,
133.186394805573));
#124800=CARTESIAN_POINT('Ctrl Pts',(-199.383808775123,-4.2370052812737,
133.305516841482));
#124801=CARTESIAN_POINT('Ctrl Pts',(-199.391559966363,-4.16401402959605,
133.421643602615));
#124802=CARTESIAN_POINT('Ctrl Pts',(-199.39930786314,-4.09105380114736,
133.537721006777));
#124803=CARTESIAN_POINT('Ctrl Pts',(-199.407055759917,-4.01319844317672,
133.650805337891));
#124804=CARTESIAN_POINT('Ctrl Pts',(-199.414803656695,-3.93072944517622,
133.76046431861));
#124805=CARTESIAN_POINT('Ctrl Pts',(-199.422549932779,-3.84827769791228,
133.870100361034));
#124806=CARTESIAN_POINT('Ctrl Pts',(-199.430296208863,-3.76121446504357,
133.976312165972));
#124807=CARTESIAN_POINT('Ctrl Pts',(-199.438042484947,-3.66986357811492,
134.078697860509));
#124808=CARTESIAN_POINT('Ctrl Pts',(-199.445788818212,-3.57851201685465,
134.181084310835));
#124809=CARTESIAN_POINT('Ctrl Pts',(-199.453535151478,-3.48287299866424,
134.279644302673));
#124810=CARTESIAN_POINT('Ctrl Pts',(-199.461281484743,-3.38330924806213,
134.374010683676));
#124811=CARTESIAN_POINT('Ctrl Pts',(-199.469029552746,-3.28372320084826,
134.468398197375));
#124812=CARTESIAN_POINT('Ctrl Pts',(-199.476777620749,-3.18021095598737,
134.558589962581));
#124813=CARTESIAN_POINT('Ctrl Pts',(-199.484525688752,-3.07317023273365,
134.644257462943));
#124814=CARTESIAN_POINT('Ctrl Pts',(-199.492281991494,-2.9660157453259,
134.730016011745));
#124815=CARTESIAN_POINT('Ctrl Pts',(-199.500038294236,-2.85532559400969,
134.811240445636));
#124816=CARTESIAN_POINT('Ctrl Pts',(-199.507794596978,-2.74152900080911,
134.887643830891));
#124817=CARTESIAN_POINT('Ctrl Pts',(-199.515555039492,-2.62767167094008,
134.964087994933));
#124818=CARTESIAN_POINT('Ctrl Pts',(-199.523315482006,-2.51070492874323,
135.035705779087));
#124819=CARTESIAN_POINT('Ctrl Pts',(-199.53107592452,-2.39108393133343,
135.102255532035));
#124820=CARTESIAN_POINT('Ctrl Pts',(-199.538848824786,-2.27127090767914,
135.168912116555));
#124821=CARTESIAN_POINT('Ctrl Pts',(-199.546621725051,-2.14879546379233,
135.230484236534));
#124822=CARTESIAN_POINT('Ctrl Pts',(-199.554394625317,-2.02413494276591,
135.286777465202));
#124823=CARTESIAN_POINT('Ctrl Pts',(-199.561884961079,-1.90400614567938,
135.341024293215));
#124824=CARTESIAN_POINT('Ctrl Pts',(-199.569375296841,-1.781848665018,135.390369253178));
#124825=CARTESIAN_POINT('Ctrl Pts',(-199.576865632603,-1.65810233422333,
135.43468238951));
#124826=CARTESIAN_POINT('Ctrl Pts',(-199.584639966722,-1.52966412368488,
135.480675671875));
#124827=CARTESIAN_POINT('Ctrl Pts',(-199.592414300841,-1.39910734850033,
135.52139372814));
#124828=CARTESIAN_POINT('Ctrl Pts',(-199.60018863496,-1.26690465470224,
135.556637509582));
#124829=CARTESIAN_POINT('Ctrl Pts',(-199.607953387907,-1.13486488890897,
135.591837856214));
#124830=CARTESIAN_POINT('Ctrl Pts',(-199.615718140854,-1.00118361465327,
135.621577251914));
#124831=CARTESIAN_POINT('Ctrl Pts',(-199.623482893801,-0.866352185939986,
135.645705157301));
#124832=CARTESIAN_POINT('Ctrl Pts',(-199.631239934686,-0.731654673702493,
135.669809098511));
#124833=CARTESIAN_POINT('Ctrl Pts',(-199.638996975571,-0.595809662696144,
135.688312572326));
#124834=CARTESIAN_POINT('Ctrl Pts',(-199.646754016456,-0.459322013378897,
135.701115292912));
#124835=CARTESIAN_POINT('Ctrl Pts',(-199.654505207696,-0.322937290459533,
135.713908358867));
#124836=CARTESIAN_POINT('Ctrl Pts',(-199.662256398937,-0.185911281514558,
135.721009192091));
#124837=CARTESIAN_POINT('Ctrl Pts',(-199.670007590177,-0.0487569940496048,
135.722368935781));
#124838=CARTESIAN_POINT('Ctrl Pts',(-199.677755486954,0.0883389991842788,
135.723728101544));
#124839=CARTESIAN_POINT('Ctrl Pts',(-199.685503383731,0.225562772370937,
135.719351027109));
#124840=CARTESIAN_POINT('Ctrl Pts',(-199.693251280508,0.362398486389647,
135.709240881096));
#124841=CARTESIAN_POINT('Ctrl Pts',(-199.700997556592,0.499205577326821,
135.699132849906));
#124842=CARTESIAN_POINT('Ctrl Pts',(-199.708743832676,0.635624380899426,
135.683294161272));
#124843=CARTESIAN_POINT('Ctrl Pts',(-199.71649010876,0.771141751181498,
135.661780041713));
#124844=CARTESIAN_POINT('Ctrl Pts',(-199.724236442026,0.906660121822196,
135.640265763343));
#124845=CARTESIAN_POINT('Ctrl Pts',(-199.731982775291,1.04127665976482,
135.613076031752));
#124846=CARTESIAN_POINT('Ctrl Pts',(-199.739729108556,1.17448640787711,
135.580317562536));
#124847=CARTESIAN_POINT('Ctrl Pts',(-199.747477176559,1.3077259873887,135.547551757289));
#124848=CARTESIAN_POINT('Ctrl Pts',(-199.755225244562,1.43955777059391,
135.509214826219));
#124849=CARTESIAN_POINT('Ctrl Pts',(-199.762973312565,1.56949039041183,
135.465463810685));
#124850=CARTESIAN_POINT('Ctrl Pts',(-199.770729615307,1.69956110416447,
135.421666296052));
#124851=CARTESIAN_POINT('Ctrl Pts',(-199.778485918049,1.82772825133692,
135.372443327376));
#124852=CARTESIAN_POINT('Ctrl Pts',(-199.786242220791,1.95351842146964,
135.318000926616));
#124853=CARTESIAN_POINT('Ctrl Pts',(-199.794002663305,2.07937572960363,
135.263529468307));
#124854=CARTESIAN_POINT('Ctrl Pts',(-199.801763105819,2.20285318096146,
135.203833197122));
#124855=CARTESIAN_POINT('Ctrl Pts',(-199.809523548333,2.32350144390913,
135.139164431195));
#124856=CARTESIAN_POINT('Ctrl Pts',(-199.817296448599,2.44434338215913,
135.074391853224));
#124857=CARTESIAN_POINT('Ctrl Pts',(-199.825069348864,2.56234671955976,
135.004631028427));
#124858=CARTESIAN_POINT('Ctrl Pts',(-199.83284224913,2.67708986376302,134.930178466652));
#124859=CARTESIAN_POINT('Ctrl Pts',(-199.840332584892,2.78766180565022,
134.858432443034));
#124860=CARTESIAN_POINT('Ctrl Pts',(-199.847822920653,2.89520622014493,
134.782330051055));
#124861=CARTESIAN_POINT('Ctrl Pts',(-199.855313256415,2.99937603121739,
134.702171090878));
#124862=CARTESIAN_POINT('Ctrl Pts',(-199.863087590534,3.1074954723416,134.618972879359));
#124863=CARTESIAN_POINT('Ctrl Pts',(-199.870861924653,3.21232185228549,
134.531140870842));
#124864=CARTESIAN_POINT('Ctrl Pts',(-199.878636258772,3.31343222899665,
134.438965125122));
#124865=CARTESIAN_POINT('Ctrl Pts',(-199.886401011719,3.414417996205,134.346902977771));
#124866=CARTESIAN_POINT('Ctrl Pts',(-199.894165764666,3.51169658615192,
134.25050800549));
#124867=CARTESIAN_POINT('Ctrl Pts',(-199.901930517614,3.60487575695146,
134.150112228108));
#124868=CARTESIAN_POINT('Ctrl Pts',(-199.909687558499,3.69796238088497,
134.049816165227));
#124869=CARTESIAN_POINT('Ctrl Pts',(-199.917444599384,3.78695742409865,
133.945527489707));
#124870=CARTESIAN_POINT('Ctrl Pts',(-199.925201640269,3.87150362387128,
133.837616748006));
#124871=CARTESIAN_POINT('Ctrl Pts',(-199.932952831509,3.95598606669709,
133.729787382635));
#124872=CARTESIAN_POINT('Ctrl Pts',(-199.940704022749,4.03602610367543,
133.618341694337));
#124873=CARTESIAN_POINT('Ctrl Pts',(-199.948455213989,4.11130533710608,
133.50368488256));
#124874=CARTESIAN_POINT('Ctrl Pts',(-199.956203110766,4.18655257485428,
133.389076802986));
#124875=CARTESIAN_POINT('Ctrl Pts',(-199.963951007543,4.25704281945193,
133.271260640578));
#124876=CARTESIAN_POINT('Ctrl Pts',(-199.97169890432,4.32249991310147,133.150672098111));
#124877=CARTESIAN_POINT('Ctrl Pts',(-199.979445180404,4.38794331453812,
133.030108780168));
#124878=CARTESIAN_POINT('Ctrl Pts',(-199.987191456488,4.44835547276005,
132.906774579053));
#124879=CARTESIAN_POINT('Ctrl Pts',(-199.994937732572,4.50350548349756,
132.781131070251));
#124880=CARTESIAN_POINT('Ctrl Pts',(-200.002684065838,4.55865590134,132.655486633977));
#124881=CARTESIAN_POINT('Ctrl Pts',(-200.010430399103,4.60854393704874,
132.527533213996));
#124882=CARTESIAN_POINT('Ctrl Pts',(-200.018176732369,4.65298643181374,
132.397753327433));
#124883=CARTESIAN_POINT('Ctrl Pts',(-200.025924800372,4.69743887916725,
132.267944377564));
#124884=CARTESIAN_POINT('Ctrl Pts',(-200.033672868375,4.73644323229192,
132.136308517008));
#124885=CARTESIAN_POINT('Ctrl Pts',(-200.041420936378,4.76986601862287,
132.003344031499));
#124886=CARTESIAN_POINT('Ctrl Pts',(-200.04917723912,4.80332432708882,131.870238229753));
#124887=CARTESIAN_POINT('Ctrl Pts',(-200.056933541861,4.83118912317878,
131.735801362048));
#124888=CARTESIAN_POINT('Ctrl Pts',(-200.064689844603,4.85337784908269,
131.600543081913));
#124889=CARTESIAN_POINT('Ctrl Pts',(-200.072450287117,4.87557841777776,
131.465212610361));
#124890=CARTESIAN_POINT('Ctrl Pts',(-200.080210729631,4.89209683270756,
131.329060240733));
#124891=CARTESIAN_POINT('Ctrl Pts',(-200.087971172146,4.90290250153954,
131.192600392573));
#124892=CARTESIAN_POINT('Ctrl Pts',(-200.095744072411,4.9137255165904,131.05592148695));
#124893=CARTESIAN_POINT('Ctrl Pts',(-200.103516972676,4.91881744521724,
130.918934507362));
#124894=CARTESIAN_POINT('Ctrl Pts',(-200.111289872942,4.91819986858887,
130.782154422205));
#124895=CARTESIAN_POINT('Ctrl Pts',(-200.118780208704,4.91760474242652,
130.650346637671));
#124896=CARTESIAN_POINT('Ctrl Pts',(-200.126270544466,4.91170802767491,
130.518731274167));
#124897=CARTESIAN_POINT('Ctrl Pts',(-200.133760880228,4.90057435163176,
130.387762385898));
#124898=CARTESIAN_POINT('Ctrl Pts',(-200.141535214347,4.88901853887747,
130.251827772423));
#124899=CARTESIAN_POINT('Ctrl Pts',(-200.149309548466,4.87178420146617,
130.116159024119));
#124900=CARTESIAN_POINT('Ctrl Pts',(-200.157083882586,4.8488867644099,129.981268758518));
#124901=CARTESIAN_POINT('Ctrl Pts',(-200.164848635533,4.8260175463984,129.846544733114));
#124902=CARTESIAN_POINT('Ctrl Pts',(-200.17261338848,4.79749918019917,129.712597663223));
#124903=CARTESIAN_POINT('Ctrl Pts',(-200.180378141427,4.76339898717628,
129.57993701788));
#124904=CARTESIAN_POINT('Ctrl Pts',(-200.188135182312,4.72933266294583,
129.44740813296));
#124905=CARTESIAN_POINT('Ctrl Pts',(-200.195892223197,4.68969564130355,
129.316163506122));
#124906=CARTESIAN_POINT('Ctrl Pts',(-200.203649264082,4.64460656425249,
129.186704002025));
#124907=CARTESIAN_POINT('Ctrl Pts',(-200.211400455322,4.59955148922512,
129.057342124347));
#124908=CARTESIAN_POINT('Ctrl Pts',(-200.219151646562,4.5490526704274,128.929763057648));
#124909=CARTESIAN_POINT('Ctrl Pts',(-200.226902837802,4.49327891189645,
128.80445369913));
#124910=CARTESIAN_POINT('Ctrl Pts',(-200.23465073458,4.43752885870062,128.679197600433));
#124911=CARTESIAN_POINT('Ctrl Pts',(-200.242398631357,4.37650848356419,
128.556209647663));
#124912=CARTESIAN_POINT('Ctrl Pts',(-200.250146528134,4.31043508553766,
128.435957688192));
#124913=CARTESIAN_POINT('Ctrl Pts',(-200.257892804218,4.2443755086418,128.315730882839));
#124914=CARTESIAN_POINT('Ctrl Pts',(-200.265639080302,4.17326519940549,
128.198239274858));
#124915=CARTESIAN_POINT('Ctrl Pts',(-200.273385356386,4.09736768495884,
128.083926623374));
#124916=CARTESIAN_POINT('Ctrl Pts',(-200.281131689651,4.02146961025387,
127.96961312806));
#124917=CARTESIAN_POINT('Ctrl Pts',(-200.288878022917,3.94078447607879,
127.85847896178));
#124918=CARTESIAN_POINT('Ctrl Pts',(-200.296624356182,3.85561923594436,
127.75093903352));
#124919=CARTESIAN_POINT('Ctrl Pts',(-200.304372424185,3.770434923645,127.643375022439));
#124920=CARTESIAN_POINT('Ctrl Pts',(-200.312120492188,3.68076875163644,
127.53940715748));
#124921=CARTESIAN_POINT('Ctrl Pts',(-200.319868560191,3.58696779663645,
127.439417068501));
#124922=CARTESIAN_POINT('Ctrl Pts',(-200.327624862933,3.49306714886511,
127.339320708866));
#124923=CARTESIAN_POINT('Ctrl Pts',(-200.335381165675,3.39502320753719,
127.243210855946));
#124924=CARTESIAN_POINT('Ctrl Pts',(-200.343137468417,3.29322013408638,
127.151432448145));
#124925=CARTESIAN_POINT('Ctrl Pts',(-200.350897910931,3.19136272527004,
127.059605055445));
#124926=CARTESIAN_POINT('Ctrl Pts',(-200.358658353445,3.08574248742091,
126.972113963648));
#124927=CARTESIAN_POINT('Ctrl Pts',(-200.366418795959,2.97677568036702,
126.88926296728));
#124928=CARTESIAN_POINT('Ctrl Pts',(-200.374191696225,2.86763395012082,
126.806278971137));
#124929=CARTESIAN_POINT('Ctrl Pts',(-200.38196459649,2.75513523632046,126.727950178812));
#124930=CARTESIAN_POINT('Ctrl Pts',(-200.389737496756,2.63972446161173,
126.654536786454));
#124931=CARTESIAN_POINT('Ctrl Pts',(-200.397227832518,2.52850915926618,
126.583792155825));
#124932=CARTESIAN_POINT('Ctrl Pts',(-200.40471816828,2.41459010805134,126.517611910091));
#124933=CARTESIAN_POINT('Ctrl Pts',(-200.412208504042,2.29838424926308,
126.456187103866));
#124934=CARTESIAN_POINT('Ctrl Pts',(-200.419982838161,2.17777241001932,
126.392433357444));
#124935=CARTESIAN_POINT('Ctrl Pts',(-200.42775717228,2.05431486939034,126.333600821259));
#124936=CARTESIAN_POINT('Ctrl Pts',(-200.435531506399,1.92845124462011,
126.279953600108));
#124937=CARTESIAN_POINT('Ctrl Pts',(-200.443296259346,1.8027427355183,126.226372494363));
#124938=CARTESIAN_POINT('Ctrl Pts',(-200.451061012293,1.67463439851077,
126.177964140413));
#124939=CARTESIAN_POINT('Ctrl Pts',(-200.45882576524,1.54459125316685,126.134947279347));
#124940=CARTESIAN_POINT('Ctrl Pts',(-200.466582806125,1.41467726850817,
126.091973143233));
#124941=CARTESIAN_POINT('Ctrl Pts',(-200.47433984701,1.28283266852345,126.054379965485));
#124942=CARTESIAN_POINT('Ctrl Pts',(-200.482096887895,1.14954297373518,
126.022338658809));
#124943=CARTESIAN_POINT('Ctrl Pts',(-200.489848079135,1.01635379374277,
125.990321514731));
#124944=CARTESIAN_POINT('Ctrl Pts',(-200.497599270375,0.881722066640452,
125.963847999343));
#124945=CARTESIAN_POINT('Ctrl Pts',(-200.505350461615,0.746148675539075,
125.94303927286));
#124946=CARTESIAN_POINT('Ctrl Pts',(-200.513098358392,0.61063290674527,
125.922239390641));
#124947=CARTESIAN_POINT('Ctrl Pts',(-200.520846255169,0.474176655614721,
125.90709956781));
#124948=CARTESIAN_POINT('Ctrl Pts',(-200.528594151946,0.337290990834222,
125.897689867454));
#124949=CARTESIAN_POINT('Ctrl Pts',(-200.53634042803,0.200433959583882,
125.888282135405));
#124950=CARTESIAN_POINT('Ctrl Pts',(-200.544086704114,0.0631480831462334,
125.884602168507));
#124951=CARTESIAN_POINT('Ctrl Pts',(-200.551832980198,-0.0740508485073515,
125.886668116572));
#124952=CARTESIAN_POINT('Ctrl Pts',(-200.559579313464,-0.211250792932096,
125.888734079886));
#124953=CARTESIAN_POINT('Ctrl Pts',(-200.567325646729,-0.348363400371211,
125.896546036912));
#124954=CARTESIAN_POINT('Ctrl Pts',(-200.575071979994,-0.484873680273991,
125.910070007408));
#124955=CARTESIAN_POINT('Ctrl Pts',(-200.582820047997,-0.621414530707646,
125.923597006504));
#124956=CARTESIAN_POINT('Ctrl Pts',(-200.590568116,-0.757352396209157,125.942838525925));
#124957=CARTESIAN_POINT('Ctrl Pts',(-200.598316184003,-0.892178597326069,
125.967708840461));
#124958=CARTESIAN_POINT('Ctrl Pts',(-200.606072486745,-1.0271480933338,
125.992605587463));
#124959=CARTESIAN_POINT('Ctrl Pts',(-200.613828789487,-1.16100317971131,
126.023143008933));
#124960=CARTESIAN_POINT('Ctrl Pts',(-200.621585092229,-1.29324600137144,
126.059184346611));
#124961=CARTESIAN_POINT('Ctrl Pts',(-200.629345534743,-1.42555940500761,
126.095244920636));
#124962=CARTESIAN_POINT('Ctrl Pts',(-200.637105977257,-1.55625845688736,
126.136815145853));
#124963=CARTESIAN_POINT('Ctrl Pts',(-200.644866419771,-1.68486256746866,
126.183709019442));
#124964=CARTESIAN_POINT('Ctrl Pts',(-200.652639320036,-1.8136731247852,
126.23067817124));
#124965=CARTESIAN_POINT('Ctrl Pts',(-200.660412220302,-1.94038165889755,
126.28298789975));
#124966=CARTESIAN_POINT('Ctrl Pts',(-200.668185120567,-2.06452876785875,
126.340404521323));
#124967=CARTESIAN_POINT('Ctrl Pts',(-200.675675456329,-2.18416281670689,
126.395733904081));
#124968=CARTESIAN_POINT('Ctrl Pts',(-200.683165792092,-2.30141816157879,
126.455805188864));
#124969=CARTESIAN_POINT('Ctrl Pts',(-200.690656127854,-2.41590869586259,
126.520370860837));
#124970=CARTESIAN_POINT('Ctrl Pts',(-200.698431549059,-2.53475678976688,
126.587393930419));
#124971=CARTESIAN_POINT('Ctrl Pts',(-200.706206970264,-2.65100197297227,
126.659472618184));
#124972=CARTESIAN_POINT('Ctrl Pts',(-200.713982391469,-2.7641842313008,
126.736379718161));
#124973=CARTESIAN_POINT('Ctrl Pts',(-200.721747993784,-2.87722356178429,
126.813189698976));
#124974=CARTESIAN_POINT('Ctrl Pts',(-200.729513596099,-2.98720734372281,
126.894815740927));
#124975=CARTESIAN_POINT('Ctrl Pts',(-200.737279198413,-3.09370005168907,
126.980984746339));
#124976=CARTESIAN_POINT('Ctrl Pts',(-200.745035419852,-3.20006411607945,
127.067049659281));
#124977=CARTESIAN_POINT('Ctrl Pts',(-200.752791641291,-3.30294520389971,
127.15764636104));
#124978=CARTESIAN_POINT('Ctrl Pts',(-200.76054786273,-3.40193722042223,
127.252458843754));
#124979=CARTESIAN_POINT('Ctrl Pts',(-200.768298765275,-3.50086135232833,
127.347206308003));
#124980=CARTESIAN_POINT('Ctrl Pts',(-200.776049667819,-3.5959014377128,
127.446163532372));
#124981=CARTESIAN_POINT('Ctrl Pts',(-200.783800570363,-3.68668484751337,
127.548974634673));
#124982=CARTESIAN_POINT('Ctrl Pts',(-200.791547836284,-3.77742566291104,
127.651737499334));
#124983=CARTESIAN_POINT('Ctrl Pts',(-200.799295102205,-3.86391351900049,
127.758350351215));
#124984=CARTESIAN_POINT('Ctrl Pts',(-200.807042368126,-3.94581330905367,
127.868421178035));
#124985=CARTESIAN_POINT('Ctrl Pts',(-200.814787676884,-4.0276924090674,
127.97846419807));
#124986=CARTESIAN_POINT('Ctrl Pts',(-200.822532985642,-4.10498551777313,
128.091963140353));
#124987=CARTESIAN_POINT('Ctrl Pts',(-200.8302782944,-4.17739867669816,128.208494026537));
#124988=CARTESIAN_POINT('Ctrl Pts',(-200.838025646966,-4.24983094378865,
128.325055662539));
#124989=CARTESIAN_POINT('Ctrl Pts',(-200.845772999533,-4.31738047721026,
128.444650511683));
#124990=CARTESIAN_POINT('Ctrl Pts',(-200.8535203521,-4.37979740039574,128.566826753244));
#124991=CARTESIAN_POINT('Ctrl Pts',(-200.861268696023,-4.4422223104952,
128.689018628564));
#124992=CARTESIAN_POINT('Ctrl Pts',(-200.869017039946,-4.49951313147677,
128.813792202435));
#124993=CARTESIAN_POINT('Ctrl Pts',(-200.87676538387,-4.55146701346846,
128.940673120208));
#124994=CARTESIAN_POINT('Ctrl Pts',(-200.884519834436,-4.60346184147747,
129.067654035672));
#124995=CARTESIAN_POINT('Ctrl Pts',(-200.892274285003,-4.65011118842505,
129.19674524743));
#124996=CARTESIAN_POINT('Ctrl Pts',(-200.90002873557,-4.69126111778874,
129.327454328317));
#124997=CARTESIAN_POINT('Ctrl Pts',(-200.905034844876,-4.71782664201108,
129.411837346905));
#124998=CARTESIAN_POINT('Ctrl Pts',(-200.910040954183,-4.74210117247926,
129.496894318409));
#124999=CARTESIAN_POINT('Ctrl Pts',(-200.91504706349,-4.76405452823395,
129.582490119308));
#125000=CARTESIAN_POINT('Ctrl Pts',(-199.165100499421,-4.76405452823391,
129.582490119308));
#125001=CARTESIAN_POINT('Ctrl Pts',(-199.172747479307,-4.79772404353953,
129.713767048478));
#125002=CARTESIAN_POINT('Ctrl Pts',(-199.180394459193,-4.8259562660387,
129.846409655637));
#125003=CARTESIAN_POINT('Ctrl Pts',(-199.188041439078,-4.84865793162383,
129.979921823839));
#125004=CARTESIAN_POINT('Ctrl Pts',(-199.195891293228,-4.87196187206307,
130.116976067901));
#125005=CARTESIAN_POINT('Ctrl Pts',(-199.203741147378,-4.8894376250516,
130.254946212889));
#125006=CARTESIAN_POINT('Ctrl Pts',(-199.211591001527,-4.90104104578751,
130.393289176079));
#125007=CARTESIAN_POINT('Ctrl Pts',(-199.219440855677,-4.91264446652345,
130.53163213927));
#125008=CARTESIAN_POINT('Ctrl Pts',(-199.227290709826,-4.91837556944563,
130.67034746391));
#125009=CARTESIAN_POINT('Ctrl Pts',(-199.235140563976,-4.91824791219353,
130.808892361601));
#125010=CARTESIAN_POINT('',(-198.889859435951,-4.91824989448309,130.8033418354));
#125011=CARTESIAN_POINT('Ctrl Pts',(-198.820145221536,-4.76405452823399,
129.582490119308));
#125012=CARTESIAN_POINT('Ctrl Pts',(-198.828426476198,-4.80034991023985,
129.72400526289));
#125013=CARTESIAN_POINT('Ctrl Pts',(-198.836707730859,-4.83037656394087,
129.867298369273));
#125014=CARTESIAN_POINT('Ctrl Pts',(-198.844988985521,-4.85397223469977,
130.011809920598));
#125015=CARTESIAN_POINT('Ctrl Pts',(-198.853248087719,-4.87750478673457,
130.155934901657));
#125016=CARTESIAN_POINT('Ctrl Pts',(-198.861507189918,-4.89464061291577,
130.301271527841));
#125017=CARTESIAN_POINT('Ctrl Pts',(-198.869766292116,-4.90526800462946,
130.44724877898));
#125018=CARTESIAN_POINT('Ctrl Pts',(-198.876464006728,-4.91388628238558,
130.5656289545));
#125019=CARTESIAN_POINT('Ctrl Pts',(-198.883161721339,-4.91822526271462,
130.684430063471));
#125020=CARTESIAN_POINT('Ctrl Pts',(-198.889859435951,-4.91824989448309,
130.803341835399));
#125021=CARTESIAN_POINT('Ctrl Pts',(-198.889859435995,-4.91824989448325,
130.803341836187));
#125022=CARTESIAN_POINT('Ctrl Pts',(-198.897858632837,-4.91827931260921,
130.945360229872));
#125023=CARTESIAN_POINT('Ctrl Pts',(-198.905857829679,-4.91215304597155,
131.087301810736));
#125024=CARTESIAN_POINT('Ctrl Pts',(-198.913857026521,-4.89991714960293,
131.228618781338));
#125025=CARTESIAN_POINT('Ctrl Pts',(-198.921862893465,-4.88767105037535,
131.370053588597));
#125026=CARTESIAN_POINT('Ctrl Pts',(-198.929868760409,-4.86930519372858,
131.510862395327));
#125027=CARTESIAN_POINT('Ctrl Pts',(-198.937874627353,-4.84491724488214,
131.650504785391));
#125028=CARTESIAN_POINT('Ctrl Pts',(-198.945888336214,-4.82050540752001,
131.790283958152));
#125029=CARTESIAN_POINT('Ctrl Pts',(-198.953902045075,-4.79005977639878,
131.928894088689));
#125030=CARTESIAN_POINT('Ctrl Pts',(-198.961915753937,-4.75372862315488,
132.065807104698));
#125031=CARTESIAN_POINT('Ctrl Pts',(-198.969944216913,-4.71733058028216,
132.202972192552));
#125032=CARTESIAN_POINT('Ctrl Pts',(-198.977972679889,-4.67502545496002,
132.338433581101));
#125033=CARTESIAN_POINT('Ctrl Pts',(-198.986001142865,-4.62701107698537,
132.471679290152));
#125034=CARTESIAN_POINT('Ctrl Pts',(-198.994038134277,-4.57894569453759,
132.605066542788));
#125035=CARTESIAN_POINT('Ctrl Pts',(-199.002075125689,-4.52515909597119,
132.736233095487));
#125036=CARTESIAN_POINT('Ctrl Pts',(-199.0101121171,-4.46589624387441,132.864689183948));
#125037=CARTESIAN_POINT('Ctrl Pts',(-199.018163714144,-4.40652569334159,
132.993378715777));
#125038=CARTESIAN_POINT('Ctrl Pts',(-199.026215311188,-4.34165916726409,
133.119347629071));
#125039=CARTESIAN_POINT('Ctrl Pts',(-199.034266908231,-4.27158681882194,
133.242131958723));
#125040=CARTESIAN_POINT('Ctrl Pts',(-199.036031065866,-4.25623350843576,
133.269034809357));
#125041=CARTESIAN_POINT('Ctrl Pts',(-199.037795223501,-4.2406304385508,
133.295784893293));
#125042=CARTESIAN_POINT('Ctrl Pts',(-199.039559381137,-4.2247809262074,
133.322377533326));
#125043=CARTESIAN_POINT('Ctrl Pts',(-199.047333715256,-4.15493489763892,
133.439566646481));
#125044=CARTESIAN_POINT('Ctrl Pts',(-199.055108049375,-4.08009856624961,
133.554033039613));
#125045=CARTESIAN_POINT('Ctrl Pts',(-199.062882383494,-4.00051000845862,
133.665322472384));
#125046=CARTESIAN_POINT('Ctrl Pts',(-199.070647136441,-3.92101953645207,
133.776474750875));
#125047=CARTESIAN_POINT('Ctrl Pts',(-199.078411889388,-3.83678871636238,
133.884457544366));
#125048=CARTESIAN_POINT('Ctrl Pts',(-199.086176642335,-3.74810091690515,
133.988842141958));
#125049=CARTESIAN_POINT('Ctrl Pts',(-199.09393368322,-3.65950120342062,
134.093123063297));
#125050=CARTESIAN_POINT('Ctrl Pts',(-199.101690724105,-3.56645357147556,
134.193812604699));
#125051=CARTESIAN_POINT('Ctrl Pts',(-199.10944776499,-3.46928377810122,
134.290512239269));
#125052=CARTESIAN_POINT('Ctrl Pts',(-199.11719895623,-3.37218726122407,
134.387138951893));
#125053=CARTESIAN_POINT('Ctrl Pts',(-199.12495014747,-3.27097504630834,
134.47978147189));
#125054=CARTESIAN_POINT('Ctrl Pts',(-199.132701338711,-3.16601189112494,
134.568075772537));
#125055=CARTESIAN_POINT('Ctrl Pts',(-199.140449235488,-3.06109334808233,
134.65633254575));
#125056=CARTESIAN_POINT('Ctrl Pts',(-199.148197132265,-2.95242733417478,
134.740244524213));
#125057=CARTESIAN_POINT('Ctrl Pts',(-199.155945029042,-2.84041388590054,
134.819486022741));
#125058=CARTESIAN_POINT('Ctrl Pts',(-199.163691305126,-2.72842386842495,
134.898710945656));
#125059=CARTESIAN_POINT('Ctrl Pts',(-199.17143758121,-2.61308812831208,
134.973267106223));
#125060=CARTESIAN_POINT('Ctrl Pts',(-199.179183857294,-2.49483773851418,
135.042870700247));
#125061=CARTESIAN_POINT('Ctrl Pts',(-199.186930190559,-2.3765864758186,
135.112474808069));
#125062=CARTESIAN_POINT('Ctrl Pts',(-199.194676523825,-2.25542085743659,
135.177126078077));
#125063=CARTESIAN_POINT('Ctrl Pts',(-199.20242285709,-2.13179839053741,
135.236585643961));
#125064=CARTESIAN_POINT('Ctrl Pts',(-199.210170925093,-2.0081482392444,
135.296058525402));
#125065=CARTESIAN_POINT('Ctrl Pts',(-199.217918993096,-1.88204049687381,
135.350337219758));
#125066=CARTESIAN_POINT('Ctrl Pts',(-199.225667061099,-1.75395419721453,
135.399230336783));
#125067=CARTESIAN_POINT('Ctrl Pts',(-199.233423363841,-1.6257317659112,
135.448175417994));
#125068=CARTESIAN_POINT('Ctrl Pts',(-199.241179666583,-1.49552694252251,
135.491723348206));
#125069=CARTESIAN_POINT('Ctrl Pts',(-199.248935969325,-1.3638360625422,
135.529731952923));
#125070=CARTESIAN_POINT('Ctrl Pts',(-199.256696411839,-1.23207489517375,
135.567760843976));
#125071=CARTESIAN_POINT('Ctrl Pts',(-199.264456854353,-1.0988264704442,
135.600244425895));
#125072=CARTESIAN_POINT('Ctrl Pts',(-199.272217296867,-0.96459799408161,
135.627091563028));
#125073=CARTESIAN_POINT('Ctrl Pts',(-199.279990197133,-0.830154042252889,
135.653981797568));
#125074=CARTESIAN_POINT('Ctrl Pts',(-199.287763097398,-0.694727281372439,
135.675217445693));
#125075=CARTESIAN_POINT('Ctrl Pts',(-199.295535997664,-0.558831624326638,
135.690759115248));
#125076=CARTESIAN_POINT('Ctrl Pts',(-199.303026333426,-0.427876116714585,
135.705735805968));
#125077=CARTESIAN_POINT('Ctrl Pts',(-199.310516669188,-0.296485519363162,
135.715425289075));
#125078=CARTESIAN_POINT('Ctrl Pts',(-199.31800700495,-0.16511834145049,
135.719838111749));
#125079=CARTESIAN_POINT('Ctrl Pts',(-199.325781339069,-0.0287703370596385,
135.724418247935));
#125080=CARTESIAN_POINT('Ctrl Pts',(-199.333555673188,0.10798434643372,
135.723328204347));
#125081=CARTESIAN_POINT('Ctrl Pts',(-199.341330007307,0.244634857648935,
135.716522753421));
#125082=CARTESIAN_POINT('Ctrl Pts',(-199.349094760254,0.381116959321885,
135.709725689604));
#125083=CARTESIAN_POINT('Ctrl Pts',(-199.356859513201,0.517494757427955,
135.69722725263));
#125084=CARTESIAN_POINT('Ctrl Pts',(-199.364624266149,0.653254397634356,
135.679034119912));
#125085=CARTESIAN_POINT('Ctrl Pts',(-199.372381307034,0.788879199452228,
135.660859056869));
#125086=CARTESIAN_POINT('Ctrl Pts',(-199.380138347918,0.923886680191096,
135.637000605475));
#125087=CARTESIAN_POINT('Ctrl Pts',(-199.387895388803,1.05776546825392,
135.607517420823));
#125088=CARTESIAN_POINT('Ctrl Pts',(-199.395646580044,1.19154329728142,
135.578056469669));
#125089=CARTESIAN_POINT('Ctrl Pts',(-199.403397771284,1.32419374753591,
135.542979311759));
#125090=CARTESIAN_POINT('Ctrl Pts',(-199.411148962524,1.45521339253885,
135.5023960628));
#125091=CARTESIAN_POINT('Ctrl Pts',(-199.418896859301,1.58617735069778,
135.461830062804));
#125092=CARTESIAN_POINT('Ctrl Pts',(-199.426644756078,1.71551150952141,
135.415762741745));
#125093=CARTESIAN_POINT('Ctrl Pts',(-199.434392652855,1.84272563134234,
135.364354620862));
#125094=CARTESIAN_POINT('Ctrl Pts',(-199.442138928939,1.96991314271106,
135.312957253449));
#125095=CARTESIAN_POINT('Ctrl Pts',(-199.449885205023,2.09498113689857,
135.256221454736));
#125096=CARTESIAN_POINT('Ctrl Pts',(-199.457631481108,2.21745783593928,
135.194356495506));
#125097=CARTESIAN_POINT('Ctrl Pts',(-199.465377814373,2.33993543907532,
135.132491079603));
#125098=CARTESIAN_POINT('Ctrl Pts',(-199.473124147638,2.45982135992249,
135.065496603904));
#125099=CARTESIAN_POINT('Ctrl Pts',(-199.480870480904,2.57666733968873,
134.993628869073));
#125100=CARTESIAN_POINT('Ctrl Pts',(-199.488618548907,2.69353948630213,
134.92174503996));
#125101=CARTESIAN_POINT('Ctrl Pts',(-199.49636661691,2.80737000422098,134.844985984877));
#125102=CARTESIAN_POINT('Ctrl Pts',(-199.504114684913,2.91773894194668,
134.763651277413));
#125103=CARTESIAN_POINT('Ctrl Pts',(-199.511870987655,3.02822518109265,
134.682230126454));
#125104=CARTESIAN_POINT('Ctrl Pts',(-199.519627290396,3.13524217559271,
134.596223840941));
#125105=CARTESIAN_POINT('Ctrl Pts',(-199.527383593138,3.23840202855827,
134.505973153196));
#125106=CARTESIAN_POINT('Ctrl Pts',(-199.535144035652,3.34161694104344,
134.41567429594));
#125107=CARTESIAN_POINT('Ctrl Pts',(-199.542904478166,3.44097032683412,
134.321126791907));
#125108=CARTESIAN_POINT('Ctrl Pts',(-199.550664920681,3.5361113538409,134.222708106593));
#125109=CARTESIAN_POINT('Ctrl Pts',(-199.558437820946,3.63140510967045,
134.124131430869));
#125110=CARTESIAN_POINT('Ctrl Pts',(-199.566210721212,3.72247273410093,
134.021671447976));
#125111=CARTESIAN_POINT('Ctrl Pts',(-199.573983621477,3.80900330292975,
133.915739234959));
#125112=CARTESIAN_POINT('Ctrl Pts',(-199.581473957239,3.89238826762382,
133.813657924713));
#125113=CARTESIAN_POINT('Ctrl Pts',(-199.588964293001,3.97156013144357,
133.708352696285));
#125114=CARTESIAN_POINT('Ctrl Pts',(-199.596454628763,4.04627993261936,
133.600215007441));
#125115=CARTESIAN_POINT('Ctrl Pts',(-199.604228962882,4.12383275776765,
133.487977245255));
#125116=CARTESIAN_POINT('Ctrl Pts',(-199.612003297001,4.1968349200723,133.372332461753));
#125117=CARTESIAN_POINT('Ctrl Pts',(-199.61977763112,4.26497224065351,133.253686004066));
#125118=CARTESIAN_POINT('Ctrl Pts',(-199.627542384067,4.33302558807671,
133.135185767535));
#125119=CARTESIAN_POINT('Ctrl Pts',(-199.635307137014,4.39622583016546,
133.013691553092));
#125120=CARTESIAN_POINT('Ctrl Pts',(-199.643071889961,4.45430083399845,
132.889639290248));
#125121=CARTESIAN_POINT('Ctrl Pts',(-199.650828930846,4.51231815691907,
132.765710237859));
#125122=CARTESIAN_POINT('Ctrl Pts',(-199.658585971731,4.56522020713492,
132.639228544949));
#125123=CARTESIAN_POINT('Ctrl Pts',(-199.666343012616,4.61277992399897,
132.510656147435));
#125124=CARTESIAN_POINT('Ctrl Pts',(-199.674094203857,4.66030377571063,
132.382180707367));
#125125=CARTESIAN_POINT('Ctrl Pts',(-199.681845395097,4.70249317785453,
132.251618066054));
#125126=CARTESIAN_POINT('Ctrl Pts',(-199.689596586337,4.73916865958453,
132.11945129068));
#125127=CARTESIAN_POINT('Ctrl Pts',(-199.697344483114,4.77582855325628,
131.987340689712));
#125128=CARTESIAN_POINT('Ctrl Pts',(-199.705092379891,4.80697908336153,
131.853627686671));
#125129=CARTESIAN_POINT('Ctrl Pts',(-199.712840276668,4.83249031553063,
131.718811498042));
#125130=CARTESIAN_POINT('Ctrl Pts',(-199.720586552752,4.85799621129998,
131.584023510052));
#125131=CARTESIAN_POINT('Ctrl Pts',(-199.728332828836,4.87786508281496,
131.448133179379));
#125132=CARTESIAN_POINT('Ctrl Pts',(-199.73607910492,4.89201798799939,131.311650542156));
#125133=CARTESIAN_POINT('Ctrl Pts',(-199.743825438185,4.9061709976573,131.17516689745));
#125134=CARTESIAN_POINT('Ctrl Pts',(-199.751571771451,4.91460791646383,
131.038091326349));
#125135=CARTESIAN_POINT('Ctrl Pts',(-199.759318104716,4.91730166193535,
130.900939228179));
#125136=CARTESIAN_POINT('Ctrl Pts',(-199.767066172719,4.91999601065249,
130.763756415746));
#125137=CARTESIAN_POINT('Ctrl Pts',(-199.774814240722,4.91694461908141,
130.626497432957));
#125138=CARTESIAN_POINT('Ctrl Pts',(-199.782562308725,4.90817253292527,
130.489677523743));
#125139=CARTESIAN_POINT('Ctrl Pts',(-199.790318611467,4.89939112369156,
130.352712200701));
#125140=CARTESIAN_POINT('Ctrl Pts',(-199.798074914209,4.88487689942825,
130.21618727421));
#125141=CARTESIAN_POINT('Ctrl Pts',(-199.805831216951,4.8647068601427,130.080613267049));
#125142=CARTESIAN_POINT('Ctrl Pts',(-199.813591659465,4.84452605549987,
129.944966899958));
#125143=CARTESIAN_POINT('Ctrl Pts',(-199.821352101979,4.81868349449313,
129.810272847277));
#125144=CARTESIAN_POINT('Ctrl Pts',(-199.829112544493,4.78730711622281,
129.6770303033));
#125145=CARTESIAN_POINT('Ctrl Pts',(-199.836885444758,4.75588036980463,
129.543573866563));
#125146=CARTESIAN_POINT('Ctrl Pts',(-199.844658345024,4.71890215983434,
129.411573971483));
#125147=CARTESIAN_POINT('Ctrl Pts',(-199.852431245289,4.67655027494581,
129.281514404581));
#125148=CARTESIAN_POINT('Ctrl Pts',(-199.859921581051,4.63573798775117,
129.156182830536));
#125149=CARTESIAN_POINT('Ctrl Pts',(-199.867411916813,4.58993604295062,
129.032653251052));
#125150=CARTESIAN_POINT('Ctrl Pts',(-199.874902252575,4.53934462037534,
128.911338303918));
#125151=CARTESIAN_POINT('Ctrl Pts',(-199.882676586694,4.48683500863597,
128.78542366369));
#125152=CARTESIAN_POINT('Ctrl Pts',(-199.890450920813,4.42899922894786,
128.66149604675));
#125153=CARTESIAN_POINT('Ctrl Pts',(-199.898225254932,4.36600848997413,
128.540038880715));
#125154=CARTESIAN_POINT('Ctrl Pts',(-199.905990007879,4.30309538145654,
128.418731399783));
#125155=CARTESIAN_POINT('Ctrl Pts',(-199.913754760827,4.23504013255191,
128.299888655622));
#125156=CARTESIAN_POINT('Ctrl Pts',(-199.921519513774,4.16206240861067,
128.183975231916));
#125157=CARTESIAN_POINT('Ctrl Pts',(-199.929276554659,4.08915716717364,
128.068176935055));
#125158=CARTESIAN_POINT('Ctrl Pts',(-199.937033595544,4.01133938712683,
127.95530249744));
#125159=CARTESIAN_POINT('Ctrl Pts',(-199.944790636429,3.9288749764153,127.84579263927));
#125160=CARTESIAN_POINT('Ctrl Pts',(-199.952541827669,3.84647275275725,
127.736365363336));
#125161=CARTESIAN_POINT('Ctrl Pts',(-199.960293018909,3.75943110728714,
127.630297927647));
#125162=CARTESIAN_POINT('Ctrl Pts',(-199.968044210149,3.6680594497312,127.528002435722));
#125163=CARTESIAN_POINT('Ctrl Pts',(-199.975792106926,3.57672662756702,
127.425750422109));
#125164=CARTESIAN_POINT('Ctrl Pts',(-199.983540003703,3.48106771357534,
127.327267454637));
#125165=CARTESIAN_POINT('Ctrl Pts',(-199.99128790048,3.38143248002231,127.232932689475));
#125166=CARTESIAN_POINT('Ctrl Pts',(-199.999034176564,3.2818180880128,127.138617657112));
#125167=CARTESIAN_POINT('Ctrl Pts',(-200.006780452648,3.17822931458165,
127.048449369756));
#125168=CARTESIAN_POINT('Ctrl Pts',(-200.014526728732,3.07105259745354,
126.962769930601));
#125169=CARTESIAN_POINT('Ctrl Pts',(-200.022273061998,2.9638750891711,126.87708985898));
#125170=CARTESIAN_POINT('Ctrl Pts',(-200.030019395263,2.85310988972064,
126.795898945805));
#125171=CARTESIAN_POINT('Ctrl Pts',(-200.037765728529,2.73917598040633,
126.719498562262));
#125172=CARTESIAN_POINT('Ctrl Pts',(-200.045513796531,2.62521655638345,
126.643081069382));
#125173=CARTESIAN_POINT('Ctrl Pts',(-200.053261864534,2.50808733510855,
126.571456458597));
#125174=CARTESIAN_POINT('Ctrl Pts',(-200.061009932537,2.38823534370891,
126.504882160176));
#125175=CARTESIAN_POINT('Ctrl Pts',(-200.068766235279,2.26825597218606,
126.438237105799));
#125176=CARTESIAN_POINT('Ctrl Pts',(-200.076522538021,2.14554839219856,
126.37665327616));
#125177=CARTESIAN_POINT('Ctrl Pts',(-200.084278840763,2.02058374140458,
126.320341839007));
#125178=CARTESIAN_POINT('Ctrl Pts',(-200.092039283277,1.89555239321386,
126.264000346744));
#125179=CARTESIAN_POINT('Ctrl Pts',(-200.099799725791,1.76826193649607,
126.212936999659));
#125180=CARTESIAN_POINT('Ctrl Pts',(-200.107560168305,1.63920151175827,
126.167313985673));
#125181=CARTESIAN_POINT('Ctrl Pts',(-200.115333068571,1.50993390776888,
126.121617733575));
#125182=CARTESIAN_POINT('Ctrl Pts',(-200.123105968836,1.37889103187466,
126.081379381333));
#125183=CARTESIAN_POINT('Ctrl Pts',(-200.130878869102,1.24657600647687,
126.046710848765));
#125184=CARTESIAN_POINT('Ctrl Pts',(-200.138369204864,1.11907096553192,
126.01330260468));
#125185=CARTESIAN_POINT('Ctrl Pts',(-200.145859540626,0.99038496183093,
125.985066322929));
#125186=CARTESIAN_POINT('Ctrl Pts',(-200.153349876388,0.860973361320397,
125.962056627357));
#125187=CARTESIAN_POINT('Ctrl Pts',(-200.161124210507,0.726655080644413,
125.938174512183));
#125188=CARTESIAN_POINT('Ctrl Pts',(-200.168898544626,0.591129615061729,
125.919847487573));
#125189=CARTESIAN_POINT('Ctrl Pts',(-200.176672878745,0.454896228380958,
125.907192815264));
#125190=CARTESIAN_POINT('Ctrl Pts',(-200.184437631692,0.318830737174114,
125.894553738707));
#125191=CARTESIAN_POINT('Ctrl Pts',(-200.19220238464,0.182059446335804,
125.887573140922));
#125192=CARTESIAN_POINT('Ctrl Pts',(-200.199967137587,0.0450919577624086,
125.886317330054));
#125193=CARTESIAN_POINT('Ctrl Pts',(-200.207724178472,-0.0917394927708051,
125.885062766475));
#125194=CARTESIAN_POINT('Ctrl Pts',(-200.215481219357,-0.228766364827308,
125.8895216781));
#125195=CARTESIAN_POINT('Ctrl Pts',(-200.223238260242,-0.365474138281122,
125.899708569077));
#125196=CARTESIAN_POINT('Ctrl Pts',(-200.230989451482,-0.502078819338985,
125.90988777804));
#125197=CARTESIAN_POINT('Ctrl Pts',(-200.238740642722,-0.638364492456307,
125.925786339691));
#125198=CARTESIAN_POINT('Ctrl Pts',(-200.246491833962,-0.773817199757398,
125.947366690881));
#125199=CARTESIAN_POINT('Ctrl Pts',(-200.254239730739,-0.909212336044752,
125.968937869845));
#125200=CARTESIAN_POINT('Ctrl Pts',(-200.261987627516,-1.04377482537243,
125.996185973889));
#125201=CARTESIAN_POINT('Ctrl Pts',(-200.269735524293,-1.17699661246376,
126.029021672868));
#125202=CARTESIAN_POINT('Ctrl Pts',(-200.277481800377,-1.31019053242917,
126.061850503327));
#125203=CARTESIAN_POINT('Ctrl Pts',(-200.285228076462,-1.44204392861639,
126.100264510403));
#125204=CARTESIAN_POINT('Ctrl Pts',(-200.292974352546,-1.57206010089031,
126.144123488225));
#125205=CARTESIAN_POINT('Ctrl Pts',(-200.300720685811,-1.70207723291426,
126.187982789804));
#125206=CARTESIAN_POINT('Ctrl Pts',(-200.308467019076,-1.83025674350794,
126.237287017366));
#125207=CARTESIAN_POINT('Ctrl Pts',(-200.316213352342,-1.9561186109295,
126.29184656856));
#125208=CARTESIAN_POINT('Ctrl Pts',(-200.323961420345,-2.08200866424412,
126.346418337987));
#125209=CARTESIAN_POINT('Ctrl Pts',(-200.331709488348,-2.20557968295316,
126.40624761746));
#125210=CARTESIAN_POINT('Ctrl Pts',(-200.339457556351,-2.32637345459673,
126.471097457747));
#125211=CARTESIAN_POINT('Ctrl Pts',(-200.347213859093,-2.44729560729777,
126.536016221215));
#125212=CARTESIAN_POINT('Ctrl Pts',(-200.354970161835,-2.56543427159992,
126.605966019329));
#125213=CARTESIAN_POINT('Ctrl Pts',(-200.362726464576,-2.68035712468567,
126.68066461196));
#125214=CARTESIAN_POINT('Ctrl Pts',(-200.370486907091,-2.79534131555868,
126.75540307348));
#125215=CARTESIAN_POINT('Ctrl Pts',(-200.378247349605,-2.90710595674912,
126.834895153379));
#125216=CARTESIAN_POINT('Ctrl Pts',(-200.386007792119,-3.01525020257337,
126.918816990429));
#125217=CARTESIAN_POINT('Ctrl Pts',(-200.393780692384,-3.12356805114131,
127.002873546263));
#125218=CARTESIAN_POINT('Ctrl Pts',(-200.40155359265,-3.22825359181314,
127.091373816816));
#125219=CARTESIAN_POINT('Ctrl Pts',(-200.409326492915,-3.32894071332805,
127.183955006361));
#125220=CARTESIAN_POINT('Ctrl Pts',(-200.416816828677,-3.42596760435925,
127.273170636466));
#125221=CARTESIAN_POINT('Ctrl Pts',(-200.424307164439,-3.51928151621706,
127.366175415959));
#125222=CARTESIAN_POINT('Ctrl Pts',(-200.431797500201,-3.60859035589865,
127.462615758093));
#125223=CARTESIAN_POINT('Ctrl Pts',(-200.439483530572,-3.70023250333136,
127.561575727608));
#125224=CARTESIAN_POINT('Ctrl Pts',(-200.447169560944,-3.78796263802236,
127.664483128439));
#125225=CARTESIAN_POINT('Ctrl Pts',(-200.454855591315,-3.87141551944836,
127.770992038202));
#125226=CARTESIAN_POINT('Ctrl Pts',(-200.462532485089,-3.95476919812291,
127.877374337873));
#125227=CARTESIAN_POINT('Ctrl Pts',(-200.470209378863,-4.03385548881044,
127.987349321958));
#125228=CARTESIAN_POINT('Ctrl Pts',(-200.477886272637,-4.10834596593192,
128.100534349717));
#125229=CARTESIAN_POINT('Ctrl Pts',(-200.48555463187,-4.18275363065011,
128.213593547645));
#125230=CARTESIAN_POINT('Ctrl Pts',(-200.493222991104,-4.25257543216279,
128.329855354119));
#125231=CARTESIAN_POINT('Ctrl Pts',(-200.500891350337,-4.3175236951057,
128.44890477958));
#125232=CARTESIAN_POINT('Ctrl Pts',(-200.508554665913,-4.38242924007743,
128.567875903488));
#125233=CARTESIAN_POINT('Ctrl Pts',(-200.516217981489,-4.44246742915597,
128.689630650553));
#125234=CARTESIAN_POINT('Ctrl Pts',(-200.523881297066,-4.49739444895502,
128.813725986849));
#125235=CARTESIAN_POINT('Ctrl Pts',(-200.531543281829,-4.55231193011296,
128.937799772716));
#125236=CARTESIAN_POINT('Ctrl Pts',(-200.539205266592,-4.60211982992361,
129.064212980692));
#125237=CARTESIAN_POINT('Ctrl Pts',(-200.546867251355,-4.64662086241272,
129.192499077765));
#125238=CARTESIAN_POINT('Ctrl Pts',(-200.554529236118,-4.69112189490171,
129.320785174837));
#125239=CARTESIAN_POINT('Ctrl Pts',(-200.56219122088,-4.73031591701161,
129.450943786207));
#125240=CARTESIAN_POINT('Ctrl Pts',(-200.569853205643,-4.76405452823395,
129.582490119308));
#125241=CARTESIAN_POINT('Origin',(213.235140564004,0.,130.804360617566));
#125242=CARTESIAN_POINT('',(-202.665364488388,-4.77027151308326,129.580941132323));
#125243=CARTESIAN_POINT('',(-202.319765235154,-4.76405452823411,129.582490119309));
#125244=CARTESIAN_POINT('',(213.235140564004,-4.76405452823405,129.582490119308));
#125245=CARTESIAN_POINT('',(-200.985142080239,-4.92392244591489,130.802667972596));
#125246=CARTESIAN_POINT('Ctrl Pts',(-200.985142543985,-4.92565748492521,
130.802675521279));
#125247=CARTESIAN_POINT('Ctrl Pts',(-201.072612154484,-4.9187069394712,
132.340745200837));
#125248=CARTESIAN_POINT('Ctrl Pts',(-201.252897639586,-3.31467917127183,
135.523358464972));
#125249=CARTESIAN_POINT('Ctrl Pts',(-201.525998999293,2.10959714028603,
136.225733113176));
#125250=CARTESIAN_POINT('Ctrl Pts',(-201.804446623106,5.70144300590434,
131.959881054809));
#125251=CARTESIAN_POINT('Ctrl Pts',(-202.082894246919,4.05394128007133,
126.632162164928));
#125252=CARTESIAN_POINT('Ctrl Pts',(-202.361341870732,-1.31893443610527,
125.138489829794));
#125253=CARTESIAN_POINT('Ctrl Pts',(-202.555498617888,-4.22021631041374,
127.727491303473));
#125254=CARTESIAN_POINT('Ctrl Pts',(-202.65683949044,-4.73402528963851,
129.435398865923));
#125255=CARTESIAN_POINT('Ctrl Pts',(-202.665364488388,-4.77027151308407,
129.580941132326));
#125256=CARTESIAN_POINT('Ctrl Pts',(-200.91504706349,-4.76405452823395,
129.582490119308));
#125257=CARTESIAN_POINT('Ctrl Pts',(-200.922810977094,-4.79810171876979,
129.715239598469));
#125258=CARTESIAN_POINT('Ctrl Pts',(-200.930574890699,-4.82656335624725,
129.849285219688));
#125259=CARTESIAN_POINT('Ctrl Pts',(-200.938338804304,-4.84936942606639,
129.984117219523));
#125260=CARTESIAN_POINT('Ctrl Pts',(-200.946113769782,-4.87220796015882,
130.119141151722));
#125261=CARTESIAN_POINT('Ctrl Pts',(-200.953888735261,-4.88937480602331,
130.254953310856));
#125262=CARTESIAN_POINT('Ctrl Pts',(-200.96166370074,-4.90085188096385,
130.39104003575));
#125263=CARTESIAN_POINT('Ctrl Pts',(-200.964143717715,-4.90451277704879,
130.434448252648));
#125264=CARTESIAN_POINT('Ctrl Pts',(-200.966623734691,-4.90759516567256,
130.477884416332));
#125265=CARTESIAN_POINT('Ctrl Pts',(-200.969103751666,-4.91009957319356,
130.521331919685));
#125266=CARTESIAN_POINT('Ctrl Pts',(-200.974449355782,-4.91549775041753,
130.614981743472));
#125267=CARTESIAN_POINT('Ctrl Pts',(-200.979794959898,-4.91821692815383,
130.708787473997));
#125268=CARTESIAN_POINT('Ctrl Pts',(-200.985140564013,-4.91824970017718,
130.802643292019));
#125269=CARTESIAN_POINT('',(-200.639859436051,-4.91824790596759,130.808899113513));
#125270=CARTESIAN_POINT('Ctrl Pts',(-200.569853205643,-4.76405452823395,
129.582490119308));
#125271=CARTESIAN_POINT('Ctrl Pts',(-200.577513488277,-4.79778564433713,
129.714007229053));
#125272=CARTESIAN_POINT('Ctrl Pts',(-200.58517377091,-4.82606367990543,
129.846911054034));
#125273=CARTESIAN_POINT('Ctrl Pts',(-200.592834053543,-4.84879096813837,
129.980704615463));
#125274=CARTESIAN_POINT('Ctrl Pts',(-200.600671617285,-4.87204423159276,
130.117594547097));
#125275=CARTESIAN_POINT('Ctrl Pts',(-200.608509181027,-4.88948659380923,
130.255415469519));
#125276=CARTESIAN_POINT('Ctrl Pts',(-200.616346744769,-4.90106945198536,
130.393627992473));
#125277=CARTESIAN_POINT('Ctrl Pts',(-200.624184308511,-4.9126523101615,
130.531840515427));
#125278=CARTESIAN_POINT('Ctrl Pts',(-200.632021872253,-4.91837567036258,
130.670444191001));
#125279=CARTESIAN_POINT('Ctrl Pts',(-200.639859435995,-4.91824790596849,
130.808899112527));
#125280=CARTESIAN_POINT('Ctrl Pts',(-200.639859436051,-4.91824790596758,
130.808899113514));
#125281=CARTESIAN_POINT('Ctrl Pts',(-200.649775499558,-4.91808625878195,
130.984071889128));
#125282=CARTESIAN_POINT('Ctrl Pts',(-200.659691563065,-4.9085624689396,
131.15882584626));
#125283=CARTESIAN_POINT('Ctrl Pts',(-200.669607626572,-4.8898314044626,
131.332311276654));
#125284=CARTESIAN_POINT('Ctrl Pts',(-200.679740109887,-4.87069153125199,
131.50958305668));
#125285=CARTESIAN_POINT('Ctrl Pts',(-200.689872593201,-4.84193809215862,
131.685530583323));
#125286=CARTESIAN_POINT('Ctrl Pts',(-200.700005076516,-4.80378435667934,
131.859272422895));
#125287=CARTESIAN_POINT('Ctrl Pts',(-200.703418425682,-4.7909314343376,
131.917801170958));
#125288=CARTESIAN_POINT('Ctrl Pts',(-200.706831774848,-4.77701213815199,
131.976079801564));
#125289=CARTESIAN_POINT('Ctrl Pts',(-200.710245124013,-4.76203582549044,
132.034075161371));
#125290=CARTESIAN_POINT('Ctrl Pts',(-200.718019458133,-4.72792538063196,
132.166166923039));
#125291=CARTESIAN_POINT('Ctrl Pts',(-200.725793792252,-4.68826069982342,
132.297047573819));
#125292=CARTESIAN_POINT('Ctrl Pts',(-200.733568126371,-4.64314265885356,
132.426214282985));
#125293=CARTESIAN_POINT('Ctrl Pts',(-200.741332879318,-4.59808022183689,
132.555221805726));
#125294=CARTESIAN_POINT('Ctrl Pts',(-200.749097632265,-4.5475779246939,
132.682519224107));
#125295=CARTESIAN_POINT('Ctrl Pts',(-200.756862385212,-4.49178728356926,
132.807615484443));
#125296=CARTESIAN_POINT('Ctrl Pts',(-200.764619426097,-4.43605205449589,
132.932587497409));
#125297=CARTESIAN_POINT('Ctrl Pts',(-200.772376466982,-4.37503909228266,
133.055362348256));
#125298=CARTESIAN_POINT('Ctrl Pts',(-200.780133507867,-4.30894907403695,
133.175466043281));
#125299=CARTESIAN_POINT('Ctrl Pts',(-200.787884699107,-4.2429088947882,
133.295479167176));
#125300=CARTESIAN_POINT('Ctrl Pts',(-200.795635890348,-4.17179946792055,
133.412824803525));
#125301=CARTESIAN_POINT('Ctrl Pts',(-200.803387081588,-4.09586859292485,
133.527051112645));
#125302=CARTESIAN_POINT('Ctrl Pts',(-200.811134978365,-4.01996999057645,
133.641228872536));
#125303=CARTESIAN_POINT('Ctrl Pts',(-200.818882875142,-3.93925423187122,
133.752289617197));
#125304=CARTESIAN_POINT('Ctrl Pts',(-200.826630771919,-3.85401374574893,
133.859808393274));
#125305=CARTESIAN_POINT('Ctrl Pts',(-200.834377048003,-3.76879109009876,
133.96730467874));
#125306=CARTESIAN_POINT('Ctrl Pts',(-200.842123324087,-3.67904583235511,
134.071260163147));
#125307=CARTESIAN_POINT('Ctrl Pts',(-200.849869600171,-3.58511195384299,
134.17128136818));
#125308=CARTESIAN_POINT('Ctrl Pts',(-200.857615933436,-3.49117738193219,
134.271303311546));
#125309=CARTESIAN_POINT('Ctrl Pts',(-200.865362266702,-3.39305439520117,
134.367390632596));
#125310=CARTESIAN_POINT('Ctrl Pts',(-200.873108599967,-3.29111496926247,
134.459185554768));
#125311=CARTESIAN_POINT('Ctrl Pts',(-200.88085666797,-3.18915271469628,
134.551001033777));
#125312=CARTESIAN_POINT('Ctrl Pts',(-200.888604735973,-3.08337261071428,
134.638521939557));
#125313=CARTESIAN_POINT('Ctrl Pts',(-200.896352803976,-2.9741806303318,
134.721430011981));
#125314=CARTESIAN_POINT('Ctrl Pts',(-200.904109106718,-2.86487259941302,
134.80442620009));
#125315=CARTESIAN_POINT('Ctrl Pts',(-200.91186540946,-2.75214576027803,
134.882799524622));
#125316=CARTESIAN_POINT('Ctrl Pts',(-200.919621712202,-2.63643651732246,
134.956274098436));
#125317=CARTESIAN_POINT('Ctrl Pts',(-200.927382154716,-2.52066551685999,
135.029787887842));
#125318=CARTESIAN_POINT('Ctrl Pts',(-200.93514259723,-2.40190927914698,
135.098397521213));
#125319=CARTESIAN_POINT('Ctrl Pts',(-200.942903039744,-2.28062897968,135.161873040904));
#125320=CARTESIAN_POINT('Ctrl Pts',(-200.95067594001,-2.15915399030956,
135.225450457134));
#125321=CARTESIAN_POINT('Ctrl Pts',(-200.958448840275,-2.03514719618037,
135.283877123337));
#125322=CARTESIAN_POINT('Ctrl Pts',(-200.966221740541,-1.90909074643751,
135.336970857192));
#125323=CARTESIAN_POINT('Ctrl Pts',(-200.973712076303,-1.78761676615949,
135.388134500087));
#125324=CARTESIAN_POINT('Ctrl Pts',(-200.981202412065,-1.66423985179437,
135.434346102061));
#125325=CARTESIAN_POINT('Ctrl Pts',(-200.988692747827,-1.5394030098361,
135.47548697379));
#125326=CARTESIAN_POINT('Ctrl Pts',(-200.996467081946,-1.40983294107218,
135.518187714174));
#125327=CARTESIAN_POINT('Ctrl Pts',(-201.004241416065,-1.27827961399708,
135.555560883532));
#125328=CARTESIAN_POINT('Ctrl Pts',(-201.012015750184,-1.14522060017088,
135.587419559231));
#125329=CARTESIAN_POINT('Ctrl Pts',(-201.019780503131,-1.01232556968741,
135.61923897196));
#125330=CARTESIAN_POINT('Ctrl Pts',(-201.027545256078,-0.877928921160667,
135.645557323121));
#125331=CARTESIAN_POINT('Ctrl Pts',(-201.035310009025,-0.742525690139992,
135.666236661027));
#125332=CARTESIAN_POINT('Ctrl Pts',(-201.04306704991,-0.607256943517217,
135.686895459924));
#125333=CARTESIAN_POINT('Ctrl Pts',(-201.050824090795,-0.470983987934914,
135.701926332662));
#125334=CARTESIAN_POINT('Ctrl Pts',(-201.05858113168,-0.33421407859659,
135.711241909402));
#125335=CARTESIAN_POINT('Ctrl Pts',(-201.066332322921,-0.197547308510626,
135.720550461193));
#125336=CARTESIAN_POINT('Ctrl Pts',(-201.074083514161,-0.0603847190823009,
135.724152269219));
#125337=CARTESIAN_POINT('Ctrl Pts',(-201.081834705401,0.076759602487468,
135.722011583823));
#125338=CARTESIAN_POINT('Ctrl Pts',(-201.089582602178,0.213845634062312,
135.719871808275));
#125339=CARTESIAN_POINT('Ctrl Pts',(-201.097330498955,0.350913023122092,
135.711994399786));
#125340=CARTESIAN_POINT('Ctrl Pts',(-201.105078395732,0.487446179389158,
135.698395689437));
#125341=CARTESIAN_POINT('Ctrl Pts',(-201.112824671816,0.623950775863247,
135.684799823644));
#125342=CARTESIAN_POINT('Ctrl Pts',(-201.1205709479,0.759920973027649,135.665485075162));
#125343=CARTESIAN_POINT('Ctrl Pts',(-201.128317223985,0.894845201367628,
135.640519747298));
#125344=CARTESIAN_POINT('Ctrl Pts',(-201.13606355725,1.02977042568743,135.615554235145));
#125345=CARTESIAN_POINT('Ctrl Pts',(-201.143809890515,1.16364928133632,
135.584938131512));
#125346=CARTESIAN_POINT('Ctrl Pts',(-201.151556223781,1.29597969885603,
135.548791003045));
#125347=CARTESIAN_POINT('Ctrl Pts',(-201.159304291784,1.42833975085505,
135.512635779679));
#125348=CARTESIAN_POINT('Ctrl Pts',(-201.167052359787,1.55915029763305,
135.470947169741));
#125349=CARTESIAN_POINT('Ctrl Pts',(-201.17480042779,1.68792413960081,135.423894702455));
#125350=CARTESIAN_POINT('Ctrl Pts',(-201.182556730532,1.81683484394041,
135.376792227247));
#125351=CARTESIAN_POINT('Ctrl Pts',(-201.190313033273,1.94370415157494,
135.324314641176));
#125352=CARTESIAN_POINT('Ctrl Pts',(-201.198069336015,2.06806406360551,
135.266679979885));
#125353=CARTESIAN_POINT('Ctrl Pts',(-201.205829778529,2.19249035026554,
135.209014557239));
#125354=CARTESIAN_POINT('Ctrl Pts',(-201.213590221043,2.31440422521268,
135.14618675382));
#125355=CARTESIAN_POINT('Ctrl Pts',(-201.221350663558,2.4333629419461,135.07846027191));
#125356=CARTESIAN_POINT('Ctrl Pts',(-201.229123563823,2.55251262177229,
135.010625069439));
#125357=CARTESIAN_POINT('Ctrl Pts',(-201.236896464089,2.66869733203954,
134.937875681717));
#125358=CARTESIAN_POINT('Ctrl Pts',(-201.244669364354,2.7815031842106,134.860519280479));
#125359=CARTESIAN_POINT('Ctrl Pts',(-201.252159700116,2.89020825951414,
134.785974979276));
#125360=CARTESIAN_POINT('Ctrl Pts',(-201.259650035878,2.99577562489767,
134.707152986653));
#125361=CARTESIAN_POINT('Ctrl Pts',(-201.26714037164,3.09786596784007,134.624361862042));
#125362=CARTESIAN_POINT('Ctrl Pts',(-201.274914705759,3.20382709716525,
134.538431686777));
#125363=CARTESIAN_POINT('Ctrl Pts',(-201.282689039878,3.30637798966232,
134.447953257853));
#125364=CARTESIAN_POINT('Ctrl Pts',(-201.290463373997,3.40510324293289,
134.353227333501));
#125365=CARTESIAN_POINT('Ctrl Pts',(-201.298228126944,3.50370682615185,
134.258618150384));
#125366=CARTESIAN_POINT('Ctrl Pts',(-201.305992879892,3.59849387170741,
134.159772155332));
#125367=CARTESIAN_POINT('Ctrl Pts',(-201.313757632839,3.68908073813156,
134.057031269514));
#125368=CARTESIAN_POINT('Ctrl Pts',(-201.321514673724,3.77957763240292,
133.954392427393));
#125369=CARTESIAN_POINT('Ctrl Pts',(-201.329271714609,3.86588239247803,
133.847866684276));
#125370=CARTESIAN_POINT('Ctrl Pts',(-201.337028755494,3.94764732780846,
133.737833582798));
#125371=CARTESIAN_POINT('Ctrl Pts',(-201.344779946734,4.02935060356523,
133.627883458138));
#125372=CARTESIAN_POINT('Ctrl Pts',(-201.352531137974,4.10652063663432,
133.514431552222));
#125373=CARTESIAN_POINT('Ctrl Pts',(-201.360282329214,4.1788494731278,133.397891057611));
#125374=CARTESIAN_POINT('Ctrl Pts',(-201.368030225991,4.25114756793644,
133.281400095818));
#125375=CARTESIAN_POINT('Ctrl Pts',(-201.375778122768,4.31860835291871,
133.161823487747));
#125376=CARTESIAN_POINT('Ctrl Pts',(-201.383526019545,4.38096687873627,
133.039603841449));
#125377=CARTESIAN_POINT('Ctrl Pts',(-201.39127229563,4.44331236049435,132.917409760867));
#125378=CARTESIAN_POINT('Ctrl Pts',(-201.399018571714,4.50055752839833,
132.792574089773));
#125379=CARTESIAN_POINT('Ctrl Pts',(-201.406764847798,4.55248333213625,
132.665564145695));
#125380=CARTESIAN_POINT('Ctrl Pts',(-201.414511181063,4.60440951917872,
132.538553264059));
#125381=CARTESIAN_POINT('Ctrl Pts',(-201.422257514328,4.65101611574979,
132.409368439302));
#125382=CARTESIAN_POINT('Ctrl Pts',(-201.430003847594,4.69213233585013,
132.278496705371));
#125383=CARTESIAN_POINT('Ctrl Pts',(-201.437751915597,4.73325776364294,
132.147595663623));
#125384=CARTESIAN_POINT('Ctrl Pts',(-201.4454999836,4.76889025117849,132.015007333899));
#125385=CARTESIAN_POINT('Ctrl Pts',(-201.453248051603,4.79890908491508,
131.881233245698));
#125386=CARTESIAN_POINT('Ctrl Pts',(-201.461004354345,4.82895982302535,
131.747316980804));
#125387=CARTESIAN_POINT('Ctrl Pts',(-201.468760657086,4.85338490335348,
131.612212822058));
#125388=CARTESIAN_POINT('Ctrl Pts',(-201.476516959828,4.87211480062235,
131.476432363778));
#125389=CARTESIAN_POINT('Ctrl Pts',(-201.484277402342,4.89085469460135,
131.340579435379));
#125390=CARTESIAN_POINT('Ctrl Pts',(-201.492037844857,4.90389331153006,
131.204049877203));
#125391=CARTESIAN_POINT('Ctrl Pts',(-201.499798287371,4.91121319630827,
131.067358721946));
#125392=CARTESIAN_POINT('Ctrl Pts',(-201.507571187636,4.91854483161535,
130.930448137912));
#125393=CARTESIAN_POINT('Ctrl Pts',(-201.515344087902,4.92013938522368,
130.793375829575));
#125394=CARTESIAN_POINT('Ctrl Pts',(-201.523116988167,4.91603157254995,
130.656656046912));
#125395=CARTESIAN_POINT('Ctrl Pts',(-201.530607323929,4.9120730892139,130.524906372726));
#125396=CARTESIAN_POINT('Ctrl Pts',(-201.538097659691,4.90281965408166,
130.39348434606));
#125397=CARTESIAN_POINT('Ctrl Pts',(-201.545587995453,4.88834746023548,
130.262842224056));
#125398=CARTESIAN_POINT('Ctrl Pts',(-201.553362329572,4.87332654876078,
130.127246766288));
#125399=CARTESIAN_POINT('Ctrl Pts',(-201.561136663691,4.8526357463644,129.992061995147));
#125400=CARTESIAN_POINT('Ctrl Pts',(-201.56891099781,4.82630355432022,129.857799967604));
#125401=CARTESIAN_POINT('Ctrl Pts',(-201.576675750757,4.80000381434937,
129.723703406011));
#125402=CARTESIAN_POINT('Ctrl Pts',(-201.584440503704,4.76807659267288,
129.590527705303));
#125403=CARTESIAN_POINT('Ctrl Pts',(-201.592205256651,4.73060218967124,
129.458780450657));
#125404=CARTESIAN_POINT('Ctrl Pts',(-201.599962297536,4.69316500677496,
129.327164049242));
#125405=CARTESIAN_POINT('Ctrl Pts',(-201.607719338421,4.65019171305585,
129.196973644122));
#125406=CARTESIAN_POINT('Ctrl Pts',(-201.615476379306,4.60181369324896,
129.068706909269));
#125407=CARTESIAN_POINT('Ctrl Pts',(-201.623227570546,4.5534721556832,128.940536901358));
#125408=CARTESIAN_POINT('Ctrl Pts',(-201.630978761786,4.49973414196849,
128.814288040604));
#125409=CARTESIAN_POINT('Ctrl Pts',(-201.638729953027,4.44078082610854,
128.690442758006));
#125410=CARTESIAN_POINT('Ctrl Pts',(-201.646477849804,4.38185256698038,
128.566650112956));
#125411=CARTESIAN_POINT('Ctrl Pts',(-201.654225746581,4.31771358212929,
128.445259366479));
#125412=CARTESIAN_POINT('Ctrl Pts',(-201.661973643358,4.24859303865466,
128.326732668419));
#125413=CARTESIAN_POINT('Ctrl Pts',(-201.669719919442,4.17948695370766,
128.208230763589));
#125414=CARTESIAN_POINT('Ctrl Pts',(-201.677466195526,4.10540157962988,
128.092592053057));
#125415=CARTESIAN_POINT('Ctrl Pts',(-201.68521247161,4.0266116818476,127.980253426592));
#125416=CARTESIAN_POINT('Ctrl Pts',(-201.692958804875,3.9478212024563,127.86791397087));
#125417=CARTESIAN_POINT('Ctrl Pts',(-201.700705138141,3.86432635455989,
127.758874967912));
#125418=CARTESIAN_POINT('Ctrl Pts',(-201.708451471406,3.77644457960803,
127.65354335856));
#125419=CARTESIAN_POINT('Ctrl Pts',(-201.716199539409,3.68854312414213,
127.548188160925));
#125420=CARTESIAN_POINT('Ctrl Pts',(-201.723947607412,3.59625303713412,
127.446542309132));
#125421=CARTESIAN_POINT('Ctrl Pts',(-201.731695675415,3.49993102093752,
127.348978451846));
#125422=CARTESIAN_POINT('Ctrl Pts',(-201.739451978156,3.40350663255572,
127.251310902531));
#125423=CARTESIAN_POINT('Ctrl Pts',(-201.747208280898,3.30304202998784,
127.157734292792));
#125424=CARTESIAN_POINT('Ctrl Pts',(-201.75496458364,3.19893005191173,127.068583645439));
#125425=CARTESIAN_POINT('Ctrl Pts',(-201.762725026154,3.09476250613789,
126.979385415701));
#125426=CARTESIAN_POINT('Ctrl Pts',(-201.770485468669,2.98694401306269,
126.894618096892));
#125427=CARTESIAN_POINT('Ctrl Pts',(-201.778245911183,2.87589844937092,
126.814574762234));
#125428=CARTESIAN_POINT('Ctrl Pts',(-201.786018811448,2.76467462548215,
126.73440293491));
#125429=CARTESIAN_POINT('Ctrl Pts',(-201.793791711714,2.65021370556392,
126.658970460966));
#125430=CARTESIAN_POINT('Ctrl Pts',(-201.801564611979,2.5329671072149,126.588526098011));
#125431=CARTESIAN_POINT('Ctrl Pts',(-201.809054947741,2.41998271804094,
126.520642565088));
#125432=CARTESIAN_POINT('Ctrl Pts',(-201.816545283503,2.3044119372224,126.45739092656));
#125433=CARTESIAN_POINT('Ctrl Pts',(-201.824035619265,2.18667644572457,
126.398951535061));
#125434=CARTESIAN_POINT('Ctrl Pts',(-201.831809953384,2.06447697728321,
126.338296396273));
#125435=CARTESIAN_POINT('Ctrl Pts',(-201.839584287503,1.93955831659402,
126.282633483449));
#125436=CARTESIAN_POINT('Ctrl Pts',(-201.847358621622,1.81236667732486,
126.232215596963));
#125437=CARTESIAN_POINT('Ctrl Pts',(-201.85512337457,1.68533179038399,126.181859846017));
#125438=CARTESIAN_POINT('Ctrl Pts',(-201.862888127517,1.55602985846499,
126.136736402609));
#125439=CARTESIAN_POINT('Ctrl Pts',(-201.870652880464,1.42493133167005,
126.097052069943));
#125440=CARTESIAN_POINT('Ctrl Pts',(-201.878409921349,1.29396301378008,
126.057407152316));
#125441=CARTESIAN_POINT('Ctrl Pts',(-201.886166962234,1.16120202383286,
126.023190707344));
#125442=CARTESIAN_POINT('Ctrl Pts',(-201.893924003119,1.02713808569387,
125.994561202266));
#125443=CARTESIAN_POINT('Ctrl Pts',(-201.901675194359,0.893175246212959,
125.965953286921));
#125444=CARTESIAN_POINT('Ctrl Pts',(-201.909426385599,0.757911795070179,
125.942924006762));
#125445=CARTESIAN_POINT('Ctrl Pts',(-201.917177576839,0.621851544102284,
125.925581700706));
#125446=CARTESIAN_POINT('Ctrl Pts',(-201.924925473616,0.485849122370762,
125.908246765593));
#125447=CARTESIAN_POINT('Ctrl Pts',(-201.932673370393,0.349050961400987,
125.896594046454));
#125448=CARTESIAN_POINT('Ctrl Pts',(-201.940421267171,0.211969751361186,
125.890680541797));
#125449=CARTESIAN_POINT('Ctrl Pts',(-201.948167543255,0.0749172157553973,
125.884768274118));
#125450=CARTESIAN_POINT('Ctrl Pts',(-201.955913819339,-0.0624178607984672,
125.884592849862));
#125451=CARTESIAN_POINT('Ctrl Pts',(-201.963660095423,-0.199519393139578,
125.890159250684));
#125452=CARTESIAN_POINT('Ctrl Pts',(-201.971406428688,-0.336621937532869,
125.895725692597));
#125453=CARTESIAN_POINT('Ctrl Pts',(-201.979152761954,-0.473490543629981,
125.907034028304));
#125454=CARTESIAN_POINT('Ctrl Pts',(-201.986899095219,-0.609611255716637,
125.92403714679));
#125455=CARTESIAN_POINT('Ctrl Pts',(-201.994647163222,-0.745762451093156,
125.941044073007));
#125456=CARTESIAN_POINT('Ctrl Pts',(-202.002395231225,-0.881165031306035,
125.963748271266));
#125457=CARTESIAN_POINT('Ctrl Pts',(-202.010143299228,-1.01531267014358,
125.99205106348));
#125458=CARTESIAN_POINT('Ctrl Pts',(-202.01789960197,-1.14960288268788,
126.020383936239));
#125459=CARTESIAN_POINT('Ctrl Pts',(-202.025655904712,-1.28263510636064,
126.054327208385));
#125460=CARTESIAN_POINT('Ctrl Pts',(-202.033412207453,-1.41391513808278,
126.093731461625));
#125461=CARTESIAN_POINT('Ctrl Pts',(-202.041172649968,-1.54526523791097,
126.133156746102));
#125462=CARTESIAN_POINT('Ctrl Pts',(-202.048933092482,-1.67486091308033,
126.178048691531));
#125463=CARTESIAN_POINT('Ctrl Pts',(-202.056693534996,-1.80222647708686,
126.228209091689));
#125464=CARTESIAN_POINT('Ctrl Pts',(-202.064466435261,-1.92979649960372,
126.278450013774));
#125465=CARTESIAN_POINT('Ctrl Pts',(-202.072239335527,-2.0551288993706,
126.333976132696));
#125466=CARTESIAN_POINT('Ctrl Pts',(-202.080012235792,-2.17777038732706,
126.394542117607));
#125467=CARTESIAN_POINT('Ctrl Pts',(-202.087502571554,-2.29595354828237,
126.452906376411));
#125468=CARTESIAN_POINT('Ctrl Pts',(-202.094992907316,-2.41163777316133,
126.515950291816));
#125469=CARTESIAN_POINT('Ctrl Pts',(-202.102483243079,-2.52444339732246,
126.583416576689));
#125470=CARTESIAN_POINT('Ctrl Pts',(-202.110258818857,-2.64154478059957,
126.653452050026));
#125471=CARTESIAN_POINT('Ctrl Pts',(-202.118034394636,-2.7559149798318,
126.728475270979));
#125472=CARTESIAN_POINT('Ctrl Pts',(-202.125809970415,-2.86709990176267,
126.808247353929));
#125473=CARTESIAN_POINT('Ctrl Pts',(-202.133891439779,-2.98265887332797,
126.891157695595));
#125474=CARTESIAN_POINT('Ctrl Pts',(-202.141972909144,-3.09477643568045,
126.979198038385));
#125475=CARTESIAN_POINT('Ctrl Pts',(-202.150054378508,-3.20297036422735,
127.072047138183));
#125476=CARTESIAN_POINT('Ctrl Pts',(-202.157810400925,-3.30680724058814,
127.161157133776));
#125477=CARTESIAN_POINT('Ctrl Pts',(-202.165566423341,-3.40702999075184,
127.254695853762));
#125478=CARTESIAN_POINT('Ctrl Pts',(-202.173322445758,-3.50324203012239,
127.352335365503));
#125479=CARTESIAN_POINT('Ctrl Pts',(-202.181073173471,-3.59938838965428,
127.44990822293));
#125480=CARTESIAN_POINT('Ctrl Pts',(-202.188823901183,-3.69152921254174,
127.551576025106));
#125481=CARTESIAN_POINT('Ctrl Pts',(-202.196574628896,-3.77930256283194,
127.65697198553));
#125482=CARTESIAN_POINT('Ctrl Pts',(-202.20432174412,-3.86703500338546,
127.762318822604));
#125483=CARTESIAN_POINT('Ctrl Pts',(-202.212068859344,-3.95040377296826,
127.871390059986));
#125484=CARTESIAN_POINT('Ctrl Pts',(-202.219815974568,-4.02908552554411,
127.983783922925));
#125485=CARTESIAN_POINT('Ctrl Pts',(-202.227561156713,-4.10774764526049,
128.096149741079));
#125486=CARTESIAN_POINT('Ctrl Pts',(-202.235306338858,-4.18172485302055,
128.211836213856));
#125487=CARTESIAN_POINT('Ctrl Pts',(-202.243051521003,-4.25073589056795,
128.330410850263));
#125488=CARTESIAN_POINT('Ctrl Pts',(-202.250798386813,-4.31976192988371,
128.449011262681));
#125489=CARTESIAN_POINT('Ctrl Pts',(-202.258545252622,-4.38381944209067,
128.570500757135));
#125490=CARTESIAN_POINT('Ctrl Pts',(-202.266292118432,-4.44267209747922,
128.694420405906));
#125491=CARTESIAN_POINT('Ctrl Pts',(-202.274040018994,-4.50153261384766,
128.818356606689));
#125492=CARTESIAN_POINT('Ctrl Pts',(-202.281787919557,-4.55518672851136,
128.944723251757));
#125493=CARTESIAN_POINT('Ctrl Pts',(-202.289535820119,-4.60344577788972,
129.07304030274));
#125494=CARTESIAN_POINT('Ctrl Pts',(-202.297288826251,-4.6517366281298,
129.201441909736));
#125495=CARTESIAN_POINT('Ctrl Pts',(-202.305041832382,-4.6946251865411,
129.331796119675));
#125496=CARTESIAN_POINT('Ctrl Pts',(-202.312794838514,-4.73197225875476,
129.463606499588));
#125497=CARTESIAN_POINT('Ctrl Pts',(-202.315118304061,-4.74316464453239,
129.503108193671));
#125498=CARTESIAN_POINT('Ctrl Pts',(-202.317441769608,-4.75385968611253,
129.542740584605));
#125499=CARTESIAN_POINT('Ctrl Pts',(-202.319765235154,-4.76405452823412,
129.582490119309));
#125500=CARTESIAN_POINT('Origin',(213.235140564004,0.,130.804360617566));
#125501=CARTESIAN_POINT('',(-204.415385129731,-4.7580624943176,129.583982083009));
#125502=CARTESIAN_POINT('',(-204.070038127516,-4.76405452823409,129.582490119308));
#125503=CARTESIAN_POINT('',(213.235140564004,-4.76405452823405,129.582490119308));
#125504=CARTESIAN_POINT('',(-202.735140564013,-4.91326211273809,130.800663901985));
#125505=CARTESIAN_POINT('Ctrl Pts',(-202.735140564013,-4.91326211273809,
130.800663901985));
#125506=CARTESIAN_POINT('Ctrl Pts',(-202.796172748794,-4.90575607440281,
131.880836901629));
#125507=CARTESIAN_POINT('Ctrl Pts',(-202.950020808181,-4.02207680521533,
134.614867738963));
#125508=CARTESIAN_POINT('Ctrl Pts',(-203.19668474217,0.501577616433585,
136.600057273287));
#125509=CARTESIAN_POINT('Ctrl Pts',(-203.475132365984,5.14719869251641,
133.515084773622));
#125510=CARTESIAN_POINT('Ctrl Pts',(-203.753579989796,5.06279562480976,
127.939089200777));
#125511=CARTESIAN_POINT('Ctrl Pts',(-204.032027613609,0.325930709221482,
124.996138083671));
#125512=CARTESIAN_POINT('Ctrl Pts',(-204.25262932692,-3.66416944143293,
126.893211472255));
#125513=CARTESIAN_POINT('Ctrl Pts',(-204.380415165628,-4.60798580335201,
128.983142737816));
#125514=CARTESIAN_POINT('Ctrl Pts',(-204.415385129731,-4.7580624943176,
129.583982083009));
#125515=CARTESIAN_POINT('Ctrl Pts',(-202.665364488388,-4.77027151308407,
129.580941132326));
#125516=CARTESIAN_POINT('Ctrl Pts',(-202.688623180263,-4.86916182929373,
129.978023072962));
#125517=CARTESIAN_POINT('Ctrl Pts',(-202.711881872138,-4.91612258108715,
130.389021896046));
#125518=CARTESIAN_POINT('Ctrl Pts',(-202.735140564013,-4.91326211273809,
130.800663901985));
#125519=CARTESIAN_POINT('',(-202.389859436034,-4.91824990320504,130.803384849354));
#125520=CARTESIAN_POINT('Ctrl Pts',(-202.319765235154,-4.76405452823412,
129.582490119309));
#125521=CARTESIAN_POINT('Ctrl Pts',(-202.327527427096,-4.79811327357253,
129.715284650469));
#125522=CARTESIAN_POINT('Ctrl Pts',(-202.335289619037,-4.82658544150759,
129.849387011775));
#125523=CARTESIAN_POINT('Ctrl Pts',(-202.343051810979,-4.84939821559733,
129.984287444574));
#125524=CARTESIAN_POINT('Ctrl Pts',(-202.350825702342,-4.87224537382299,
130.11939120358));
#125525=CARTESIAN_POINT('Ctrl Pts',(-202.358599593705,-4.88941605217232,
130.255295049384));
#125526=CARTESIAN_POINT('Ctrl Pts',(-202.366373485068,-4.90088936486764,
130.391484733277));
#125527=CARTESIAN_POINT('Ctrl Pts',(-202.371225945676,-4.90805100313769,
130.476494292247));
#125528=CARTESIAN_POINT('Ctrl Pts',(-202.376078406283,-4.91299384376543,
130.561615199731));
#125529=CARTESIAN_POINT('Ctrl Pts',(-202.380930866891,-4.91572308414765,
130.646722987294));
#125530=CARTESIAN_POINT('Ctrl Pts',(-202.383907056592,-4.91739702604547,
130.698922673462));
#125531=CARTESIAN_POINT('Ctrl Pts',(-202.386883246294,-4.9182395397714,
130.751149164821));
#125532=CARTESIAN_POINT('Ctrl Pts',(-202.389859435995,-4.9182499032049,
130.803384848665));
#125533=CARTESIAN_POINT('Ctrl Pts',(-202.389859436034,-4.91824990320504,
130.803384849353));
#125534=CARTESIAN_POINT('Ctrl Pts',(-202.397592511015,-4.91827683063906,
130.939109551199));
#125535=CARTESIAN_POINT('Ctrl Pts',(-202.405325585996,-4.91268128621269,
131.075059385912));
#125536=CARTESIAN_POINT('Ctrl Pts',(-202.413058660977,-4.90143341606133,
131.210726869139));
#125537=CARTESIAN_POINT('Ctrl Pts',(-202.42078228894,-4.89019928673439,
131.346228615827));
#125538=CARTESIAN_POINT('Ctrl Pts',(-202.428505916903,-4.87332660037077,
131.481448306892));
#125539=CARTESIAN_POINT('Ctrl Pts',(-202.436229544867,-4.8508374788153,
131.615876986237));
#125540=CARTESIAN_POINT('Ctrl Pts',(-202.443945635588,-4.82837030367676,
131.750174480918));
#125541=CARTESIAN_POINT('Ctrl Pts',(-202.451661726309,-4.80029766335863,
131.883682112162));
#125542=CARTESIAN_POINT('Ctrl Pts',(-202.45937781703,-4.76669356115084,
132.015894998664));
#125543=CARTESIAN_POINT('Ctrl Pts',(-202.467088273264,-4.73311399751808,
132.148011339935));
#125544=CARTESIAN_POINT('Ctrl Pts',(-202.474798729498,-4.69401110747945,
132.278834436168));
#125545=CARTESIAN_POINT('Ctrl Pts',(-202.482509185732,-4.64951007925511,
132.407868985304));
#125546=CARTESIAN_POINT('Ctrl Pts',(-202.490216665053,-4.6050262323335,
132.536853715778));
#125547=CARTESIAN_POINT('Ctrl Pts',(-202.497924144375,-4.55514851955673,
132.664050898828));
#125548=CARTESIAN_POINT('Ctrl Pts',(-202.505631623696,-4.50005207787166,
132.788980066968));
#125549=CARTESIAN_POINT('Ctrl Pts',(-202.513337751278,-4.44496529901407,
132.913887324999));
#125550=CARTESIAN_POINT('Ctrl Pts',(-202.521043878859,-4.38466177095691,
133.036526997411));
#125551=CARTESIAN_POINT('Ctrl Pts',(-202.528750006441,-4.31936471923195,
133.156438738028));
#125552=CARTESIAN_POINT('Ctrl Pts',(-202.536456496514,-4.25406459597308,
133.27635611922));
#125553=CARTESIAN_POINT('Ctrl Pts',(-202.544162986588,-4.18377067092648,
133.39354496595));
#125554=CARTESIAN_POINT('Ctrl Pts',(-202.551869476661,-4.10875183304938,
133.507570087236));
#125555=CARTESIAN_POINT('Ctrl Pts',(-202.559578043381,-4.03371278004685,
133.621625934566));
#125556=CARTESIAN_POINT('Ctrl Pts',(-202.567286610102,-3.95394649875435,
133.732516030231));
#125557=CARTESIAN_POINT('Ctrl Pts',(-202.574995176822,-3.86976457714697,
133.839835074708));
#125558=CARTESIAN_POINT('Ctrl Pts',(-202.582712029366,-3.78549216965473,
133.947269474815));
#125559=CARTESIAN_POINT('Ctrl Pts',(-202.590428881909,-3.69679488857133,
134.051124847371));
#125560=CARTESIAN_POINT('Ctrl Pts',(-202.598145734452,-3.60402417816858,
134.151029526448));
#125561=CARTESIAN_POINT('Ctrl Pts',(-202.605867103336,-3.51119917307237,
134.250992675422));
#125562=CARTESIAN_POINT('Ctrl Pts',(-202.61358847222,-3.41429627095629,
134.347000247896));
#125563=CARTESIAN_POINT('Ctrl Pts',(-202.621309841104,-3.31370214936235,
134.438719037949));
#125564=CARTESIAN_POINT('Ctrl Pts',(-202.629042866836,-3.21295616217193,
134.530576294631));
#125565=CARTESIAN_POINT('Ctrl Pts',(-202.636775892567,-3.10850812896895,
134.618131584567));
#125566=CARTESIAN_POINT('Ctrl Pts',(-202.644508918298,-3.00077647222385,
134.701093046954));
#125567=CARTESIAN_POINT('Ctrl Pts',(-202.649465442433,-2.93172529156538,
134.754267639271));
#125568=CARTESIAN_POINT('Ctrl Pts',(-202.654421966569,-2.86132571321719,
134.80555585624));
#125569=CARTESIAN_POINT('Ctrl Pts',(-202.659378490704,-2.7896934030652,
134.8548906791));
#125570=CARTESIAN_POINT('Ctrl Pts',(-202.667152824823,-2.67733774865093,
134.932272607676));
#125571=CARTESIAN_POINT('Ctrl Pts',(-202.674927158942,-2.56158200219939,
135.005098693772));
#125572=CARTESIAN_POINT('Ctrl Pts',(-202.682701493061,-2.4428319884996,
135.07305537574));
#125573=CARTESIAN_POINT('Ctrl Pts',(-202.690466246008,-2.32422832357901,
135.140928307171));
#125574=CARTESIAN_POINT('Ctrl Pts',(-202.698230998955,-2.20263806981494,
135.203943582563));
#125575=CARTESIAN_POINT('Ctrl Pts',(-202.705995751903,-2.078497570351,135.261829732719));
#125576=CARTESIAN_POINT('Ctrl Pts',(-202.713752792788,-1.95448036898086,
135.319658389536));
#125577=CARTESIAN_POINT('Ctrl Pts',(-202.721509833673,-1.82791831461926,
135.372367894886));
#125578=CARTESIAN_POINT('Ctrl Pts',(-202.729266874558,-1.69927368819759,
135.419731891375));
#125579=CARTESIAN_POINT('Ctrl Pts',(-202.737018065798,-1.57072607368995,
135.467060170305));
#125580=CARTESIAN_POINT('Ctrl Pts',(-202.744769257038,-1.44009937847901,
135.50905082948));
#125581=CARTESIAN_POINT('Ctrl Pts',(-202.752520448278,-1.30787694231266,
135.545525133407));
#125582=CARTESIAN_POINT('Ctrl Pts',(-202.760268345055,-1.17571070420829,
135.581983934782));
#125583=CARTESIAN_POINT('Ctrl Pts',(-202.768016241832,-1.04195045020032,
135.612930940387));
#125584=CARTESIAN_POINT('Ctrl Pts',(-202.77576413861,-0.907095593932953,
135.638236975725));
#125585=CARTESIAN_POINT('Ctrl Pts',(-202.783510414694,-0.772268946394382,
135.663537717586));
#125586=CARTESIAN_POINT('Ctrl Pts',(-202.791256690778,-0.636348536039387,
135.683199764143));
#125587=CARTESIAN_POINT('Ctrl Pts',(-202.799002966862,-0.49984451854849,
135.697144949598));
#125588=CARTESIAN_POINT('Ctrl Pts',(-202.806749300127,-0.363339493416131,
135.711090237993));
#125589=CARTESIAN_POINT('Ctrl Pts',(-202.814495633393,-0.226251241492333,
135.719318541345));
#125590=CARTESIAN_POINT('Ctrl Pts',(-202.822241966658,-0.0890952027191759,
135.721803561551));
#125591=CARTESIAN_POINT('Ctrl Pts',(-202.829990034661,0.0480915511977042,
135.724289138261));
#125592=CARTESIAN_POINT('Ctrl Pts',(-202.837738102664,0.18534573134494,
135.721028865417));
#125593=CARTESIAN_POINT('Ctrl Pts',(-202.845486170667,0.322152132501905,
135.712048572808));
#125594=CARTESIAN_POINT('Ctrl Pts',(-202.853242473409,0.459103933130223,
135.703058735837));
#125595=CARTESIAN_POINT('Ctrl Pts',(-202.860998776151,0.595606613349426,
135.688336760683));
#125596=CARTESIAN_POINT('Ctrl Pts',(-202.868755078893,0.731149768151804,
135.667960424194));
#125597=CARTESIAN_POINT('Ctrl Pts',(-202.876515521407,0.866765266417027,
135.647573212241));
#125598=CARTESIAN_POINT('Ctrl Pts',(-202.884275963921,1.00141983514607,
135.62152569974));
#125599=CARTESIAN_POINT('Ctrl Pts',(-202.892036406435,1.1346144753236,135.589946585333));
#125600=CARTESIAN_POINT('Ctrl Pts',(-202.899809306701,1.268022931362,135.558316777328));
#125601=CARTESIAN_POINT('Ctrl Pts',(-202.907582206966,1.39996639904794,
135.521137728808));
#125602=CARTESIAN_POINT('Ctrl Pts',(-202.915355107232,1.52996136298433,
135.478587964441));
#125603=CARTESIAN_POINT('Ctrl Pts',(-202.922845442994,1.65523068254303,
135.437584991186));
#125604=CARTESIAN_POINT('Ctrl Pts',(-202.930335778755,1.77869041621811,
135.391595108432));
#125605=CARTESIAN_POINT('Ctrl Pts',(-202.937826114517,1.89992823133841,
135.340819123743));
#125606=CARTESIAN_POINT('Ctrl Pts',(-202.945600448637,2.02576281507001,
135.28811795216));
#125607=CARTESIAN_POINT('Ctrl Pts',(-202.953374782756,2.14960227229255,
135.230093642708));
#125608=CARTESIAN_POINT('Ctrl Pts',(-202.961149116875,2.27096343650089,
135.166918139545));
#125609=CARTESIAN_POINT('Ctrl Pts',(-202.968913869822,2.39217503392037,
135.103820494544));
#125610=CARTESIAN_POINT('Ctrl Pts',(-202.976678622769,2.51091407195934,
135.03558446602));
#125611=CARTESIAN_POINT('Ctrl Pts',(-202.984443375716,2.62671630176767,
134.962430426086));
#125612=CARTESIAN_POINT('Ctrl Pts',(-202.992200416601,2.74240351516851,
134.889349043777));
#125613=CARTESIAN_POINT('Ctrl Pts',(-202.999957457486,2.85515939666273,
134.811359578162));
#125614=CARTESIAN_POINT('Ctrl Pts',(-203.007714498371,2.96454363122682,
134.728728607581));
#125615=CARTESIAN_POINT('Ctrl Pts',(-203.015465689611,3.07384537828889,
134.646159949657));
#125616=CARTESIAN_POINT('Ctrl Pts',(-203.023216880851,3.1797802285859,134.558956988398));
#125617=CARTESIAN_POINT('Ctrl Pts',(-203.030968072092,3.28193654994615,
134.467429760324));
#125618=CARTESIAN_POINT('Ctrl Pts',(-203.038715968869,3.38404945214513,
134.375941433763));
#125619=CARTESIAN_POINT('Ctrl Pts',(-203.046463865646,3.48238672899254,
134.280132756231));
#125620=CARTESIAN_POINT('Ctrl Pts',(-203.054211762423,3.57656975705238,
134.1803540766));
#125621=CARTESIAN_POINT('Ctrl Pts',(-203.061958038507,3.67073308405285,
134.080596268517));
#125622=CARTESIAN_POINT('Ctrl Pts',(-203.069704314591,3.76074362251624,
133.976870394256));
#125623=CARTESIAN_POINT('Ctrl Pts',(-203.077450590675,3.84625985773754,
133.869563411715));
#125624=CARTESIAN_POINT('Ctrl Pts',(-203.085196923941,3.93177672422038,
133.762255637058));
#125625=CARTESIAN_POINT('Ctrl Pts',(-203.092943257206,4.01279897759957,
133.651367007122));
#125626=CARTESIAN_POINT('Ctrl Pts',(-203.100689590471,4.08902588465788,
133.537316961363));
#125627=CARTESIAN_POINT('Ctrl Pts',(-203.108437658474,4.1652698622036,133.423241374886));
#125628=CARTESIAN_POINT('Ctrl Pts',(-203.116185726477,4.23671613931385,
133.306003288778));
#125629=CARTESIAN_POINT('Ctrl Pts',(-203.12393379448,4.30310796631424,133.186050121415));
#125630=CARTESIAN_POINT('Ctrl Pts',(-203.131690097222,4.36957035533834,
133.065969466397));
#125631=CARTESIAN_POINT('Ctrl Pts',(-203.139446399964,4.43096737361537,
132.943168308397));
#125632=CARTESIAN_POINT('Ctrl Pts',(-203.147202702706,4.48708857063544,
132.818118105888));
#125633=CARTESIAN_POINT('Ctrl Pts',(-203.15496314522,4.54323972122798,132.693001160321));
#125634=CARTESIAN_POINT('Ctrl Pts',(-203.162723587734,4.59410929477576,
132.565633141281));
#125635=CARTESIAN_POINT('Ctrl Pts',(-203.170484030249,4.63953584793378,
132.436503435532));
#125636=CARTESIAN_POINT('Ctrl Pts',(-203.178256930514,4.68503532382784,
132.307166439315));
#125637=CARTESIAN_POINT('Ctrl Pts',(-203.18602983078,4.72507420452498,132.176062479243));
#125638=CARTESIAN_POINT('Ctrl Pts',(-203.193802731045,4.75954133600245,
132.043694847459));
#125639=CARTESIAN_POINT('Ctrl Pts',(-203.201293066807,4.79275550043213,
131.916139112508));
#125640=CARTESIAN_POINT('Ctrl Pts',(-203.208783402569,4.82079591129226,
131.787410287015));
#125641=CARTESIAN_POINT('Ctrl Pts',(-203.21627373833,4.84360863779292,131.657963819527));
#125642=CARTESIAN_POINT('Ctrl Pts',(-203.224048072449,4.86728631575333,
131.523609349876));
#125643=CARTESIAN_POINT('Ctrl Pts',(-203.231822406569,4.8854070724529,131.388056150618));
#125644=CARTESIAN_POINT('Ctrl Pts',(-203.239596740688,4.89785440608457,
131.251803663437));
#125645=CARTESIAN_POINT('Ctrl Pts',(-203.247361493635,4.91028639949003,
131.115719095268));
#125646=CARTESIAN_POINT('Ctrl Pts',(-203.255126246582,4.91705884657044,
130.978937339527));
#125647=CARTESIAN_POINT('Ctrl Pts',(-203.262890999529,4.91810621478259,
130.841968098429));
#125648=CARTESIAN_POINT('Ctrl Pts',(-203.270648040414,4.91915254273387,
130.705134897112));
#125649=CARTESIAN_POINT('Ctrl Pts',(-203.278405081299,4.91448510469911,
130.568114969434));
#125650=CARTESIAN_POINT('Ctrl Pts',(-203.286162122184,4.90409017955869,
130.431422857));
#125651=CARTESIAN_POINT('Ctrl Pts',(-203.293913313424,4.89370309331222,
130.294833825151));
#125652=CARTESIAN_POINT('Ctrl Pts',(-203.301664504664,4.8775971464774,130.158572504755));
#125653=CARTESIAN_POINT('Ctrl Pts',(-203.309415695904,4.85581068431517,
130.023152795927));
#125654=CARTESIAN_POINT('Ctrl Pts',(-203.317163592681,4.8340334819805,129.887790644087));
#125655=CARTESIAN_POINT('Ctrl Pts',(-203.324911489458,4.8065806282877,129.753269777556));
#125656=CARTESIAN_POINT('Ctrl Pts',(-203.332659386236,4.77354222644985,
129.620098115078));
#125657=CARTESIAN_POINT('Ctrl Pts',(-203.34040566232,4.74051073553344,129.48695430924));
#125658=CARTESIAN_POINT('Ctrl Pts',(-203.348151938404,4.70189611451706,
129.355159525316));
#125659=CARTESIAN_POINT('Ctrl Pts',(-203.355898214488,4.65783932500118,
129.225210249497));
#125660=CARTESIAN_POINT('Ctrl Pts',(-203.363644547753,4.61378221026816,
129.095260014422));
#125661=CARTESIAN_POINT('Ctrl Pts',(-203.371390881019,4.56428297240465,
128.967155684899));
#125662=CARTESIAN_POINT('Ctrl Pts',(-203.379137214284,4.50953194405326,
128.841376993573));
#125663=CARTESIAN_POINT('Ctrl Pts',(-203.386885282287,4.45476865458861,
128.715570134981));
#125664=CARTESIAN_POINT('Ctrl Pts',(-203.39463335029,4.39475139034221,128.592090309345));
#125665=CARTESIAN_POINT('Ctrl Pts',(-203.402381418293,4.32971779759376,
128.471395367996));
#125666=CARTESIAN_POINT('Ctrl Pts',(-203.410137721035,4.26461508636893,
128.350572150628));
#125667=CARTESIAN_POINT('Ctrl Pts',(-203.417894023777,4.19448558231854,
128.232540074813));
#125668=CARTESIAN_POINT('Ctrl Pts',(-203.425650326518,4.11961218316801,
128.117731033348));
#125669=CARTESIAN_POINT('Ctrl Pts',(-203.433410769033,4.04469882182997,
128.002860714841));
#125670=CARTESIAN_POINT('Ctrl Pts',(-203.441171211547,3.96503674722332,
127.891217176486));
#125671=CARTESIAN_POINT('Ctrl Pts',(-203.448931654061,3.88095043022052,
127.783200770641));
#125672=CARTESIAN_POINT('Ctrl Pts',(-203.456704554326,3.79672913039707,
127.675010967273));
#125673=CARTESIAN_POINT('Ctrl Pts',(-203.464477454592,3.70806964875335,
127.570460230171));
#125674=CARTESIAN_POINT('Ctrl Pts',(-203.472250354857,3.61533533775766,
127.469914118061));
#125675=CARTESIAN_POINT('Ctrl Pts',(-203.479740690619,3.52597215254956,
127.373023110385));
#125676=CARTESIAN_POINT('Ctrl Pts',(-203.487231026381,3.4328254728641,127.279850844024));
#125677=CARTESIAN_POINT('Ctrl Pts',(-203.494721362143,3.3362493295539,127.190688873543));
#125678=CARTESIAN_POINT('Ctrl Pts',(-203.502495696262,3.23601147241738,
127.098146299852));
#125679=CARTESIAN_POINT('Ctrl Pts',(-203.510270030382,3.13176143843621,
127.009630978764));
#125680=CARTESIAN_POINT('Ctrl Pts',(-203.518044364501,3.0238564499707,126.92551088698));
#125681=CARTESIAN_POINT('Ctrl Pts',(-203.525809117448,2.91608444475944,
126.84149446569));
#125682=CARTESIAN_POINT('Ctrl Pts',(-203.533573870395,2.80466675286709,
126.761862734097));
#125683=CARTESIAN_POINT('Ctrl Pts',(-203.541338623342,2.68999677926315,
126.686946333084));
#125684=CARTESIAN_POINT('Ctrl Pts',(-203.549095664227,2.57544069749386,
126.612104340097));
#125685=CARTESIAN_POINT('Ctrl Pts',(-203.556852705112,2.45763908746732,
126.541968570097));
#125686=CARTESIAN_POINT('Ctrl Pts',(-203.564609745997,2.33701743100642,
126.476828689357));
#125687=CARTESIAN_POINT('Ctrl Pts',(-203.572360937237,2.2164867362748,126.411737931106));
#125688=CARTESIAN_POINT('Ctrl Pts',(-203.580112128477,2.09314057063032,
126.35163574828));
#125689=CARTESIAN_POINT('Ctrl Pts',(-203.587863319717,1.96743201934503,
126.29676765549));
#125690=CARTESIAN_POINT('Ctrl Pts',(-203.595611216494,1.84177689754726,
126.241922883103));
#125691=CARTESIAN_POINT('Ctrl Pts',(-203.603359113271,1.71376174471187,
126.192307932205));
#125692=CARTESIAN_POINT('Ctrl Pts',(-203.611107010048,1.58386259025,126.148121538899));
#125693=CARTESIAN_POINT('Ctrl Pts',(-203.618853286132,1.45399060789093,
126.103944388434));
#125694=CARTESIAN_POINT('Ctrl Pts',(-203.626599562217,1.32223577767975,
126.06519366274));
#125695=CARTESIAN_POINT('Ctrl Pts',(-203.634345838301,1.18909200069798,
126.032019129745));
#125696=CARTESIAN_POINT('Ctrl Pts',(-203.642092171566,1.05594724087891,
125.998844351863));
#125697=CARTESIAN_POINT('Ctrl Pts',(-203.649838504831,0.921413893196879,
125.97124594334));
#125698=CARTESIAN_POINT('Ctrl Pts',(-203.657584838097,0.785998449754042,
125.949323079144));
#125699=CARTESIAN_POINT('Ctrl Pts',(-203.6653329061,0.650552680961736,125.927395305475));
#125700=CARTESIAN_POINT('Ctrl Pts',(-203.673080974103,0.514224809194846,
125.911145667744));
#125701=CARTESIAN_POINT('Ctrl Pts',(-203.680829042106,0.377528491365758,
125.900621707234));
#125702=CARTESIAN_POINT('Ctrl Pts',(-203.688585344847,0.240686891063561,
125.890086561733));
#125703=CARTESIAN_POINT('Ctrl Pts',(-203.696341647589,0.103476452891485,
125.88528927959));
#125704=CARTESIAN_POINT('Ctrl Pts',(-203.704097950331,-0.0335865463790532,
125.886225299541));
#125705=CARTESIAN_POINT('Ctrl Pts',(-203.711858392845,-0.17072270029919,
125.887161819075));
#125706=CARTESIAN_POINT('Ctrl Pts',(-203.719618835359,-0.307710868205461,
125.893837719063));
#125707=CARTESIAN_POINT('Ctrl Pts',(-203.727379277873,-0.44403883788848,
125.906196413199));
#125708=CARTESIAN_POINT('Ctrl Pts',(-203.735152178139,-0.580585653331063,
125.918574946608));
#125709=CARTESIAN_POINT('Ctrl Pts',(-203.742925078404,-0.716469764941721,
125.936654452284));
#125710=CARTESIAN_POINT('Ctrl Pts',(-203.75069797867,-0.851187216928724,
125.960326824926));
#125711=CARTESIAN_POINT('Ctrl Pts',(-203.758188314432,-0.981007350205763,
125.983138647196));
#125712=CARTESIAN_POINT('Ctrl Pts',(-203.765678650194,-1.10974387227684,
126.011143701039));
#125713=CARTESIAN_POINT('Ctrl Pts',(-203.773168985956,-1.23696012770498,
126.044201722637));
#125714=CARTESIAN_POINT('Ctrl Pts',(-203.780943320075,-1.36899982612075,
126.078513149172));
#125715=CARTESIAN_POINT('Ctrl Pts',(-203.788717654194,-1.4998199624505,
126.118376962119));
#125716=CARTESIAN_POINT('Ctrl Pts',(-203.796491988313,-1.62891786006441,
126.163691520586));
#125717=CARTESIAN_POINT('Ctrl Pts',(-203.80425674126,-1.75785665605768,
126.20895023291));
#125718=CARTESIAN_POINT('Ctrl Pts',(-203.812021494207,-1.88507707112989,
126.259646196572));
#125719=CARTESIAN_POINT('Ctrl Pts',(-203.819786247154,-2.01008828274693,
126.315627148305));
#125720=CARTESIAN_POINT('Ctrl Pts',(-203.827543288039,-2.13497533146623,
126.371552498967));
#125721=CARTESIAN_POINT('Ctrl Pts',(-203.835300328924,-2.25765718879851,
126.432752232951));
#125722=CARTESIAN_POINT('Ctrl Pts',(-203.843057369809,-2.37766016698767,
126.499024952043));
#125723=CARTESIAN_POINT('Ctrl Pts',(-203.850808561049,-2.49757264999765,
126.565247694363));
#125724=CARTESIAN_POINT('Ctrl Pts',(-203.858559752289,-2.61480993401946,
126.63653561897));
#125725=CARTESIAN_POINT('Ctrl Pts',(-203.866310943529,-2.72892055700057,
126.712640239036));
#125726=CARTESIAN_POINT('Ctrl Pts',(-203.874058840306,-2.84298267992244,
126.788712512608));
#125727=CARTESIAN_POINT('Ctrl Pts',(-203.881806737083,-2.95392046033182,
126.869597193392));
#125728=CARTESIAN_POINT('Ctrl Pts',(-203.88955463386,-3.06130939039301,
126.955001206081));
#125729=CARTESIAN_POINT('Ctrl Pts',(-203.897300909944,-3.16867585700537,
127.040387354091));
#125730=CARTESIAN_POINT('Ctrl Pts',(-203.905047186028,-3.27249464402813,
127.130290710461));
#125731=CARTESIAN_POINT('Ctrl Pts',(-203.912793462112,-3.3723727818643,
127.224376695446));
#125732=CARTESIAN_POINT('Ctrl Pts',(-203.920539795377,-3.47225165697833,
127.318463374952));
#125733=CARTESIAN_POINT('Ctrl Pts',(-203.928286128643,-3.56818954027803,
127.416732476603));
#125734=CARTESIAN_POINT('Ctrl Pts',(-203.936032461908,-3.65982922170008,
127.518811480741));
#125735=CARTESIAN_POINT('Ctrl Pts',(-203.943780529911,-3.75148942519278,
127.620913344764));
#125736=CARTESIAN_POINT('Ctrl Pts',(-203.951528597914,-3.83884925031249,
127.726826518173));
#125737=CARTESIAN_POINT('Ctrl Pts',(-203.959276665916,-3.92159105512307,
127.836144544084));
#125738=CARTESIAN_POINT('Ctrl Pts',(-203.967032968658,-4.00442079890878,
127.945578754494));
#125739=CARTESIAN_POINT('Ctrl Pts',(-203.9747892714,-4.08262248162509,128.05842473395));
#125740=CARTESIAN_POINT('Ctrl Pts',(-203.982545574142,-4.15592088058601,
128.174245658708));
#125741=CARTESIAN_POINT('Ctrl Pts',(-203.990306016656,-4.22925840110944,
128.290128400581));
#125742=CARTESIAN_POINT('Ctrl Pts',(-203.99806645917,-4.29768722825386,
128.408988912957));
#125743=CARTESIAN_POINT('Ctrl Pts',(-204.005826901684,-4.36097810647042,
128.530365670917));
#125744=CARTESIAN_POINT('Ctrl Pts',(-204.013599801949,-4.42437058482357,
128.651937273624));
#125745=CARTESIAN_POINT('Ctrl Pts',(-204.021372702215,-4.48260846613932,
128.776032839594));
#125746=CARTESIAN_POINT('Ctrl Pts',(-204.02914560248,-4.53551030205551,
128.902169942989));
#125747=CARTESIAN_POINT('Ctrl Pts',(-204.036635938243,-4.58648902298876,
129.023721644965));
#125748=CARTESIAN_POINT('Ctrl Pts',(-204.044126274005,-4.63251281279301,
129.147168742662));
#125749=CARTESIAN_POINT('Ctrl Pts',(-204.051616609768,-4.67346365646167,
129.272068049473));
#125750=CARTESIAN_POINT('Ctrl Pts',(-204.057757115684,-4.70703476806217,
129.374459311585));
#125751=CARTESIAN_POINT('Ctrl Pts',(-204.0638976216,-4.73725521212647,129.477999992541));
#125752=CARTESIAN_POINT('Ctrl Pts',(-204.070038127516,-4.76405452823409,
129.582490119308));
#125753=CARTESIAN_POINT('Origin',(213.235140564004,0.,130.804360617566));
#125754=CARTESIAN_POINT('',(-206.164998470905,-4.76405452823394,129.582490119308));
#125755=CARTESIAN_POINT('',(-205.820054717884,-4.76405452823395,129.582490119308));
#125756=CARTESIAN_POINT('',(213.235140564004,-4.76405452823405,129.582490119308));
#125757=CARTESIAN_POINT('',(-204.485140564013,-4.91519744545431,130.807513129082));
#125758=CARTESIAN_POINT('Ctrl Pts',(-204.485140564013,-4.91824898839283,
130.807515086282));
#125759=CARTESIAN_POINT('Ctrl Pts',(-204.49387773296,-4.91814963363141,
130.962422774028));
#125760=CARTESIAN_POINT('Ctrl Pts',(-204.502614901907,-4.91072767197462,
131.117052050995));
#125761=CARTESIAN_POINT('Ctrl Pts',(-204.511352070854,-4.8960860736549,
131.27075553806));
#125762=CARTESIAN_POINT('Ctrl Pts',(-204.520123591854,-4.88138690875277,
131.425063343332));
#125763=CARTESIAN_POINT('Ctrl Pts',(-204.528895112854,-4.85941133515114,
131.578437879815));
#125764=CARTESIAN_POINT('Ctrl Pts',(-204.537666633853,-4.83031338638245,
131.73024163143));
#125765=CARTESIAN_POINT('Ctrl Pts',(-204.546486847053,-4.8010539099665,
131.882888071409));
#125766=CARTESIAN_POINT('Ctrl Pts',(-204.555307060253,-4.76459286084652,
132.033946055602));
#125767=CARTESIAN_POINT('Ctrl Pts',(-204.564127273453,-4.72113560423765,
132.182787862255));
#125768=CARTESIAN_POINT('Ctrl Pts',(-204.572392469381,-4.68041292189577,
132.322263707821));
#125769=CARTESIAN_POINT('Ctrl Pts',(-204.580657665308,-4.63354733828304,
132.459793589481));
#125770=CARTESIAN_POINT('Ctrl Pts',(-204.588922861235,-4.58074515708572,
132.594879220747));
#125771=CARTESIAN_POINT('Ctrl Pts',(-204.596697195354,-4.53107884518496,
132.721942250031));
#125772=CARTESIAN_POINT('Ctrl Pts',(-204.604471529473,-4.47604305081149,
132.847138467984));
#125773=CARTESIAN_POINT('Ctrl Pts',(-204.612245863592,-4.41579807394511,
132.969980721057));
#125774=CARTESIAN_POINT('Ctrl Pts',(-204.620010616539,-4.35562734362847,
133.092671582031));
#125775=CARTESIAN_POINT('Ctrl Pts',(-204.627775369486,-4.29026037490912,
133.213013902697));
#125776=CARTESIAN_POINT('Ctrl Pts',(-204.635540122433,-4.21990633574634,
133.330538279574));
#125777=CARTESIAN_POINT('Ctrl Pts',(-204.643297163318,-4.14962217320707,
133.447945929583));
#125778=CARTESIAN_POINT('Ctrl Pts',(-204.651054204203,-4.07436099688629,
133.562540872303));
#125779=CARTESIAN_POINT('Ctrl Pts',(-204.658811245088,-3.99437874200781,
133.673876522365));
#125780=CARTESIAN_POINT('Ctrl Pts',(-204.666562436328,-3.91445680236981,
133.785128213348));
#125781=CARTESIAN_POINT('Ctrl Pts',(-204.674313627568,-3.82982109772313,
133.89312518765));
#125782=CARTESIAN_POINT('Ctrl Pts',(-204.682064818808,-3.74077169726714,
133.997448491619));
#125783=CARTESIAN_POINT('Ctrl Pts',(-204.689812715585,-3.65176014518169,
134.101727455401));
#125784=CARTESIAN_POINT('Ctrl Pts',(-204.697560612362,-3.55833888168141,
134.202335557629));
#125785=CARTESIAN_POINT('Ctrl Pts',(-204.705308509139,-3.46084906882826,
134.298885876495));
#125786=CARTESIAN_POINT('Ctrl Pts',(-204.713054785223,-3.36337964874233,
134.395415999115));
#125787=CARTESIAN_POINT('Ctrl Pts',(-204.720801061307,-3.26184364970766,
134.487889751746));
#125788=CARTESIAN_POINT('Ctrl Pts',(-204.728547337392,-3.15661972277871,
134.575956432107));
#125789=CARTESIAN_POINT('Ctrl Pts',(-204.736293670657,-3.05139501911078,
134.664023762557));
#125790=CARTESIAN_POINT('Ctrl Pts',(-204.744040003922,-2.94248263304068,
134.747683704894));
#125791=CARTESIAN_POINT('Ctrl Pts',(-204.751786337187,-2.83029466646686,
134.826625547114));
#125792=CARTESIAN_POINT('Ctrl Pts',(-204.75953440519,-2.71808157617563,
134.905585067812));
#125793=CARTESIAN_POINT('Ctrl Pts',(-204.767282473193,-2.60259176539364,
134.979824160965));
#125794=CARTESIAN_POINT('Ctrl Pts',(-204.775030541196,-2.48426636236587,
135.04907541403));
#125795=CARTESIAN_POINT('Ctrl Pts',(-204.782786843938,-2.36581520169152,
135.11840026815));
#125796=CARTESIAN_POINT('Ctrl Pts',(-204.79054314668,-2.24452276654071,
135.182726494795));
#125797=CARTESIAN_POINT('Ctrl Pts',(-204.798299449421,-2.12085532938707,
135.241832390356));
#125798=CARTESIAN_POINT('Ctrl Pts',(-204.806059891935,-1.99712188719867,
135.300969832514));
#125799=CARTESIAN_POINT('Ctrl Pts',(-204.81382033445,-1.87101127650509,
135.354881238147));
#125800=CARTESIAN_POINT('Ctrl Pts',(-204.821580776964,-1.74300886894293,
135.403393466469));
#125801=CARTESIAN_POINT('Ctrl Pts',(-204.829353677229,-1.61480098055263,
135.451983570926));
#125802=CARTESIAN_POINT('Ctrl Pts',(-204.837126577494,-1.48469559792147,
135.495157054964));
#125803=CARTESIAN_POINT('Ctrl Pts',(-204.84489947776,-1.35319320086527,
135.532790718946));
#125804=CARTESIAN_POINT('Ctrl Pts',(-204.852389813522,-1.22647124717054,
135.569056304449));
#125805=CARTESIAN_POINT('Ctrl Pts',(-204.859880149284,-1.09845238493452,
135.600177777234));
#125806=CARTESIAN_POINT('Ctrl Pts',(-204.867370485047,-0.969590637356454,
135.626090292532));
#125807=CARTESIAN_POINT('Ctrl Pts',(-204.875144819166,-0.835843057454864,
135.652985288723));
#125808=CARTESIAN_POINT('Ctrl Pts',(-204.882919153285,-0.700763742363002,
135.674353730114));
#125809=CARTESIAN_POINT('Ctrl Pts',(-204.890693487405,-0.564849194214768,
135.690067163225));
#125810=CARTESIAN_POINT('Ctrl Pts',(-204.898458240352,-0.42910214860009,
135.705761230934));
#125811=CARTESIAN_POINT('Ctrl Pts',(-204.906222993299,-0.292522302678767,
135.715814112706));
#125812=CARTESIAN_POINT('Ctrl Pts',(-204.913987746246,-0.155617639284803,
135.720148063423));
#125813=CARTESIAN_POINT('Ctrl Pts',(-204.921744787131,-0.0188489515325352,
135.724477709599));
#125814=CARTESIAN_POINT('Ctrl Pts',(-204.929501828017,0.118243523436565,
135.723099716129));
#125815=CARTESIAN_POINT('Ctrl Pts',(-204.937258868902,0.255145721463766,
135.715988018267));
#125816=CARTESIAN_POINT('Ctrl Pts',(-204.945010060142,0.391944680478308,
135.708881683392));
#125817=CARTESIAN_POINT('Ctrl Pts',(-204.952761251382,0.528553259298798,
135.696050270647));
#125818=CARTESIAN_POINT('Ctrl Pts',(-204.960512442623,0.664456785619391,
135.677519782065));
#125819=CARTESIAN_POINT('Ctrl Pts',(-204.9682603394,0.80030254931577,135.658997169436));
#125820=CARTESIAN_POINT('Ctrl Pts',(-204.976008236177,0.935443469955528,
135.634780351368));
#125821=CARTESIAN_POINT('Ctrl Pts',(-204.983756132954,1.06936961283493,
135.604947216477));
#125822=CARTESIAN_POINT('Ctrl Pts',(-204.991502409038,1.20326774125236,
135.575120322035));
#125823=CARTESIAN_POINT('Ctrl Pts',(-204.999248685123,1.33595121596879,
135.53967953249));
#125824=CARTESIAN_POINT('Ctrl Pts',(-205.006994961207,1.46692031107978,
135.49875385455));
#125825=CARTESIAN_POINT('Ctrl Pts',(-205.014741294472,1.59789037297505,
135.457827874506));
#125826=CARTESIAN_POINT('Ctrl Pts',(-205.022487627738,1.72714565684219,
135.411417041884));
#125827=CARTESIAN_POINT('Ctrl Pts',(-205.030233961003,1.85420200073023,
135.359700122256));
#125828=CARTESIAN_POINT('Ctrl Pts',(-205.037982029006,1.98128679800571,
135.307971620982));
#125829=CARTESIAN_POINT('Ctrl Pts',(-205.04573009701,2.10617131336159,135.250934815567));
#125830=CARTESIAN_POINT('Ctrl Pts',(-205.053478165013,2.22839212445938,
135.188816296684));
#125831=CARTESIAN_POINT('Ctrl Pts',(-205.061234467755,2.35074283328949,
135.1266317575));
#125832=CARTESIAN_POINT('Ctrl Pts',(-205.068990770497,2.47042383351275,
135.059354893381));
#125833=CARTESIAN_POINT('Ctrl Pts',(-205.076747073239,2.58699656794278,
134.987258156348));
#125834=CARTESIAN_POINT('Ctrl Pts',(-205.084507515753,2.70363152075111,
134.915122939117));
#125835=CARTESIAN_POINT('Ctrl Pts',(-205.092267958267,2.81715457866475,
134.838162942302));
#125836=CARTESIAN_POINT('Ctrl Pts',(-205.100028400782,2.9271577182112,134.756692935985));
#125837=CARTESIAN_POINT('Ctrl Pts',(-205.107801301047,3.03733744456286,
134.67509214678));
#125838=CARTESIAN_POINT('Ctrl Pts',(-205.115574201313,3.1439856567345,134.588967126286));
#125839=CARTESIAN_POINT('Ctrl Pts',(-205.123347101578,3.24672818181712,
134.498672349932));
#125840=CARTESIAN_POINT('Ctrl Pts',(-205.130837437339,3.3457357573013,134.411660016153));
#125841=CARTESIAN_POINT('Ctrl Pts',(-205.1383277731,3.4411164558133,134.320776037914));
#125842=CARTESIAN_POINT('Ctrl Pts',(-205.145818108861,3.53257031098373,
134.226367347609));
#125843=CARTESIAN_POINT('Ctrl Pts',(-205.15359244298,3.62749166688566,134.128379123099));
#125844=CARTESIAN_POINT('Ctrl Pts',(-205.161366777099,3.71848321111434,
134.026283234194));
#125845=CARTESIAN_POINT('Ctrl Pts',(-205.169141111218,3.80516850058741,
133.920427969957));
#125846=CARTESIAN_POINT('Ctrl Pts',(-205.176905864165,3.89174695818848,
133.814703162873));
#125847=CARTESIAN_POINT('Ctrl Pts',(-205.184670617112,3.97402947520282,
133.705228498512));
#125848=CARTESIAN_POINT('Ctrl Pts',(-205.192435370059,4.05167606532983,
133.592389334085));
#125849=CARTESIAN_POINT('Ctrl Pts',(-205.200192410944,4.1292455357689,133.479662243106));
#125850=CARTESIAN_POINT('Ctrl Pts',(-205.207949451829,4.2021880222257,133.363577622127));
#125851=CARTESIAN_POINT('Ctrl Pts',(-205.215706492714,4.27020373145505,
133.24455387925));
#125852=CARTESIAN_POINT('Ctrl Pts',(-205.223457683954,4.33816814950907,
133.125619893103));
#125853=CARTESIAN_POINT('Ctrl Pts',(-205.231208875195,4.40121299226405,
133.003751534774));
#125854=CARTESIAN_POINT('Ctrl Pts',(-205.238960066435,4.45908194301358,
132.879395867385));
#125855=CARTESIAN_POINT('Ctrl Pts',(-205.246707963212,4.51692629791526,
132.755093054471));
#125856=CARTESIAN_POINT('Ctrl Pts',(-205.254455859989,4.56959897162442,
132.628305388855));
#125857=CARTESIAN_POINT('Ctrl Pts',(-205.262203756766,4.61688986187661,
132.499503993744));
#125858=CARTESIAN_POINT('Ctrl Pts',(-205.26995003285,4.66417085989403,132.370729541109));
#125859=CARTESIAN_POINT('Ctrl Pts',(-205.277696308934,4.70607217897284,
132.239942563603));
#125860=CARTESIAN_POINT('Ctrl Pts',(-205.285442585018,4.74243224205182,
132.107633226059));
#125861=CARTESIAN_POINT('Ctrl Pts',(-205.293188918284,4.77879257353258,
131.975322911837));
#125862=CARTESIAN_POINT('Ctrl Pts',(-205.300935251549,4.80961146379121,
131.841490592143));
#125863=CARTESIAN_POINT('Ctrl Pts',(-205.308681584814,4.83477761200457,
131.706640233295));
#125864=CARTESIAN_POINT('Ctrl Pts',(-205.316429652817,4.8599493960023,131.571759675644));
#125865=CARTESIAN_POINT('Ctrl Pts',(-205.32417772082,4.8794658472645,131.435861009436));
#125866=CARTESIAN_POINT('Ctrl Pts',(-205.331925788823,4.89326711184883,
131.299456602804));
#125867=CARTESIAN_POINT('Ctrl Pts',(-205.339682091565,4.90708304458142,
131.162907223945));
#125868=CARTESIAN_POINT('Ctrl Pts',(-205.347438394307,4.91517161741112,
131.025851420532));
#125869=CARTESIAN_POINT('Ctrl Pts',(-205.355194697049,4.91752500106838,
130.888805430121));
#125870=CARTESIAN_POINT('Ctrl Pts',(-205.362955139563,4.91987964079736,
130.751686294138));
#125871=CARTESIAN_POINT('Ctrl Pts',(-205.370715582077,4.91649300161557,
130.614577372247));
#125872=CARTESIAN_POINT('Ctrl Pts',(-205.378476024592,4.9074093618528,130.477992087068));
#125873=CARTESIAN_POINT('Ctrl Pts',(-205.386248924857,4.89831114022507,
130.341187543064));
#125874=CARTESIAN_POINT('Ctrl Pts',(-205.394021825122,4.88349768500393,
130.204908704434));
#125875=CARTESIAN_POINT('Ctrl Pts',(-205.401794725388,4.86306497681123,
130.069661976073));
#125876=CARTESIAN_POINT('Ctrl Pts',(-205.40928506115,4.84337504902889,129.939331806958));
#125877=CARTESIAN_POINT('Ctrl Pts',(-205.416775396912,4.81846738151463,
129.809960313757));
#125878=CARTESIAN_POINT('Ctrl Pts',(-205.424265732673,4.78847171916799,
129.681987392107));
#125879=CARTESIAN_POINT('Ctrl Pts',(-205.432040066792,4.75733876216599,
129.549162338233));
#125880=CARTESIAN_POINT('Ctrl Pts',(-205.439814400911,4.72062575157316,
129.417423253277));
#125881=CARTESIAN_POINT('Ctrl Pts',(-205.44758873503,4.67842223616104,129.287275108211));
#125882=CARTESIAN_POINT('Ctrl Pts',(-205.455353487977,4.63627073280972,
129.157287359103));
#125883=CARTESIAN_POINT('Ctrl Pts',(-205.463118240924,4.58864230750925,
129.028887017024));
#125884=CARTESIAN_POINT('Ctrl Pts',(-205.470882993871,4.53567740129338,
128.902568417062));
#125885=CARTESIAN_POINT('Ctrl Pts',(-205.478640034756,4.48276510056905,
128.776375278515));
#125886=CARTESIAN_POINT('Ctrl Pts',(-205.486397075641,4.4245270169024,128.652260125658));
#125887=CARTESIAN_POINT('Ctrl Pts',(-205.494154116526,4.36115312330836,
128.530701342838));
#125888=CARTESIAN_POINT('Ctrl Pts',(-205.501905307766,4.29782702046055,
128.409234228441));
#125889=CARTESIAN_POINT('Ctrl Pts',(-205.509656499006,4.22937299657398,
128.290319992233));
#125890=CARTESIAN_POINT('Ctrl Pts',(-205.517407690246,4.15602863307309,
128.174415929255));
#125891=CARTESIAN_POINT('Ctrl Pts',(-205.525155587023,4.08271544288332,
128.058561128595));
#125892=CARTESIAN_POINT('Ctrl Pts',(-205.5329034838,4.00451625573041,127.94571428621));
#125893=CARTESIAN_POINT('Ctrl Pts',(-205.540651380577,3.92171387550616,
127.836306820688));
#125894=CARTESIAN_POINT('Ctrl Pts',(-205.548397656661,3.83892881575483,
127.726922240849));
#125895=CARTESIAN_POINT('Ctrl Pts',(-205.556143932745,3.75154271395995,
127.62097591841));
#125896=CARTESIAN_POINT('Ctrl Pts',(-205.563890208829,3.65988062332928,
127.518868738794));
#125897=CARTESIAN_POINT('Ctrl Pts',(-205.571636542094,3.56821785606976,
127.416760805445));
#125898=CARTESIAN_POINT('Ctrl Pts',(-205.579382875359,3.47227929816279,
127.318492362404));
#125899=CARTESIAN_POINT('Ctrl Pts',(-205.587129208625,3.37242878993213,
127.224429456309));
#125900=CARTESIAN_POINT('Ctrl Pts',(-205.594877276628,3.27255592087287,
127.130345485479));
#125901=CARTESIAN_POINT('Ctrl Pts',(-205.60262534463,3.16876964276772,127.040469193703));
#125902=CARTESIAN_POINT('Ctrl Pts',(-205.610373412633,3.06146867291942,
126.955127885289));
#125903=CARTESIAN_POINT('Ctrl Pts',(-205.618129715375,2.95405366232302,
126.869695875116));
#125904=CARTESIAN_POINT('Ctrl Pts',(-205.625886018117,2.84311680448129,
126.788808720195));
#125905=CARTESIAN_POINT('Ctrl Pts',(-205.633642320859,2.72908819275771,
126.712752046521));
#125906=CARTESIAN_POINT('Ctrl Pts',(-205.641402763373,2.61499872053071,
126.63665477911));
#125907=CARTESIAN_POINT('Ctrl Pts',(-205.649163205887,2.4978145402187,126.565393333214));
#125908=CARTESIAN_POINT('Ctrl Pts',(-205.656923648401,2.37799154233177,
126.499207973687));
#125909=CARTESIAN_POINT('Ctrl Pts',(-205.664696548666,2.25797619393123,
126.432916367546));
#125910=CARTESIAN_POINT('Ctrl Pts',(-205.672469448932,2.13531391299143,
126.371717305886));
#125911=CARTESIAN_POINT('Ctrl Pts',(-205.680242349197,2.01048263216247,
126.315803761708));
#125912=CARTESIAN_POINT('Ctrl Pts',(-205.68773268496,1.89018928280237,126.261922815689));
#125913=CARTESIAN_POINT('Ctrl Pts',(-205.695223020723,1.76788217886368,
126.212949889631));
#125914=CARTESIAN_POINT('Ctrl Pts',(-205.702713356486,1.64400154729095,
126.169013599812));
#125915=CARTESIAN_POINT('Ctrl Pts',(-205.710487690606,1.5154239439371,126.123411452216));
#125916=CARTESIAN_POINT('Ctrl Pts',(-205.718262024725,1.38474384172379,
126.083090954468));
#125917=CARTESIAN_POINT('Ctrl Pts',(-205.726036358844,1.25243449033019,
126.048249715796));
#125918=CARTESIAN_POINT('Ctrl Pts',(-205.733801111791,1.12028819838735,
126.013451415837));
#125919=CARTESIAN_POINT('Ctrl Pts',(-205.741565864738,0.986517026841535,
125.984119037703));
#125920=CARTESIAN_POINT('Ctrl Pts',(-205.749330617686,0.85161278561181,
125.960401624564));
#125921=CARTESIAN_POINT('Ctrl Pts',(-205.757087658571,0.716842533176288,
125.936707767895));
#125922=CARTESIAN_POINT('Ctrl Pts',(-205.764844699456,0.5809418331833,125.918617845271));
#125923=CARTESIAN_POINT('Ctrl Pts',(-205.772601740341,0.444415848987914,
125.906230605442));
#125924=CARTESIAN_POINT('Ctrl Pts',(-205.780352931581,0.307992820099411,
125.893852706927));
#125925=CARTESIAN_POINT('Ctrl Pts',(-205.788104122822,0.170945833354071,
125.88716896663));
#125926=CARTESIAN_POINT('Ctrl Pts',(-205.795855314062,0.0337880425846281,
125.886226679711));
#125927=CARTESIAN_POINT('Ctrl Pts',(-205.803603210839,-0.103311452464748,
125.885284793289));
#125928=CARTESIAN_POINT('Ctrl Pts',(-205.811351107616,-0.240521267733049,
125.890079509413));
#125929=CARTESIAN_POINT('Ctrl Pts',(-205.819099004394,-0.377325576133052,
125.900606089442));
#125930=CARTESIAN_POINT('Ctrl Pts',(-205.826845280478,-0.514101268020897,
125.911130467538));
#125931=CARTESIAN_POINT('Ctrl Pts',(-205.834591556562,-0.650471232192675,
125.927384294722));
#125932=CARTESIAN_POINT('Ctrl Pts',(-205.842337832646,-0.785922493189801,
125.949310782889));
#125933=CARTESIAN_POINT('Ctrl Pts',(-205.850084165912,-0.921374754057551,
125.971237432912));
#125934=CARTESIAN_POINT('Ctrl Pts',(-205.857830499177,-1.05590791227709,
125.998836764999));
#125935=CARTESIAN_POINT('Ctrl Pts',(-205.865576832443,-1.18901733786065,
126.032000527132));
#125936=CARTESIAN_POINT('Ctrl Pts',(-205.873324900446,-1.32215657237697,
126.065171716059));
#125937=CARTESIAN_POINT('Ctrl Pts',(-205.881072968449,-1.45387106051707,
126.103909720158));
#125938=CARTESIAN_POINT('Ctrl Pts',(-205.888821036452,-1.58366991545586,
126.148056003241));
#125939=CARTESIAN_POINT('Ctrl Pts',(-205.896577339194,-1.71360672216248,
126.19224920552));
#125940=CARTESIAN_POINT('Ctrl Pts',(-205.904333641936,-1.8416234578902,
126.241862042909));
#125941=CARTESIAN_POINT('Ctrl Pts',(-205.912089944678,-1.96724734143226,
126.296687053506));
#125942=CARTESIAN_POINT('Ctrl Pts',(-205.919850387192,-2.09293827422343,
126.351541325862));
#125943=CARTESIAN_POINT('Ctrl Pts',(-205.927610829707,-2.21623345872856,
126.411613143427));
#125944=CARTESIAN_POINT('Ctrl Pts',(-205.935371272221,-2.33668433336452,
126.476648821627));
#125945=CARTESIAN_POINT('Ctrl Pts',(-205.943144172487,-2.45732856643756,
126.541788900871));
#125946=CARTESIAN_POINT('Ctrl Pts',(-205.950917072752,-2.57511902930189,
126.61190856411));
#125947=CARTESIAN_POINT('Ctrl Pts',(-205.958689973018,-2.68963503403625,
126.68671001969));
#125948=CARTESIAN_POINT('Ctrl Pts',(-205.966180308779,-2.79998809352685,
126.758792253932));
#125949=CARTESIAN_POINT('Ctrl Pts',(-205.973670644539,-2.90730038036246,
126.835221621603));
#125950=CARTESIAN_POINT('Ctrl Pts',(-205.9811609803,-3.0112257326097,126.915697267549));
#125951=CARTESIAN_POINT('Ctrl Pts',(-205.988843416406,-3.11781639876974,
126.998236826237));
#125952=CARTESIAN_POINT('Ctrl Pts',(-205.996525852513,-3.22119867281582,
127.085307874707));
#125953=CARTESIAN_POINT('Ctrl Pts',(-206.004208288619,-3.32095599792357,
127.1766293262));
#125954=CARTESIAN_POINT('Ctrl Pts',(-206.01188194727,-3.42059934675241,
127.267846439699));
#125955=CARTESIAN_POINT('Ctrl Pts',(-206.019555605921,-3.5166256876976,
127.363304034671));
#125956=CARTESIAN_POINT('Ctrl Pts',(-206.027229264572,-3.60864870074115,
127.462678762999));
#125957=CARTESIAN_POINT('Ctrl Pts',(-206.034895912193,-3.70058763704767,
127.561962697703));
#125958=CARTESIAN_POINT('Ctrl Pts',(-206.042562559813,-3.78853024788272,
127.665156357538));
#125959=CARTESIAN_POINT('Ctrl Pts',(-206.050229207433,-3.87212489877666,
127.771897620137));
#125960=CARTESIAN_POINT('Ctrl Pts',(-206.057890604246,-3.95566229656263,
127.878565776755));
#125961=CARTESIAN_POINT('Ctrl Pts',(-206.065552001059,-4.03485741114901,
127.988776389217));
#125962=CARTESIAN_POINT('Ctrl Pts',(-206.073213397872,-4.10939732791692,
128.102132525082));
#125963=CARTESIAN_POINT('Ctrl Pts',(-206.080872341447,-4.18391337642932,
128.215452363439));
#125964=CARTESIAN_POINT('Ctrl Pts',(-206.088531285021,-4.25377696648902,
128.331915391257));
#125965=CARTESIAN_POINT('Ctrl Pts',(-206.096190228596,-4.31871736387104,
128.451094080707));
#125966=CARTESIAN_POINT('Ctrl Pts',(-206.103847441602,-4.38364308771443,
128.570245841263));
#125967=CARTESIAN_POINT('Ctrl Pts',(-206.111504654608,-4.44364764309317,
128.692111689209));
#125968=CARTESIAN_POINT('Ctrl Pts',(-206.119161867614,-4.49850566380742,
128.816238424341));
#125969=CARTESIAN_POINT('Ctrl Pts',(-206.1268221242,-4.55338548942266,128.940414497221));
#125970=CARTESIAN_POINT('Ctrl Pts',(-206.134482380787,-4.60311452764392,
129.066852887145));
#125971=CARTESIAN_POINT('Ctrl Pts',(-206.142142637373,-4.64751508729958,
129.195079232654));
#125972=CARTESIAN_POINT('Ctrl Pts',(-206.14976124855,-4.69167426085744,
129.322608468546));
#125973=CARTESIAN_POINT('Ctrl Pts',(-206.157379859728,-4.73056267205465,
129.451905880375));
#125974=CARTESIAN_POINT('Ctrl Pts',(-206.164998470905,-4.76405452823394,
129.582490119308));
#125975=CARTESIAN_POINT('Ctrl Pts',(-204.415385129731,-4.7580624943176,
129.583982083009));
#125976=CARTESIAN_POINT('Ctrl Pts',(-204.438636941158,-4.85784969763347,
129.983485013898));
#125977=CARTESIAN_POINT('Ctrl Pts',(-204.461888752586,-4.90979750657223,
130.395767923279));
#125978=CARTESIAN_POINT('Ctrl Pts',(-204.485140564013,-4.91220180825584,
130.807511207739));
#125979=CARTESIAN_POINT('',(-204.139859435948,-4.91824831916273,130.80029447038));
#125980=CARTESIAN_POINT('Ctrl Pts',(-204.070038127516,-4.76405452823409,
129.582490119308));
#125981=CARTESIAN_POINT('Ctrl Pts',(-204.079301788646,-4.80448438634937,
129.740125522491));
#125982=CARTESIAN_POINT('Ctrl Pts',(-204.088565449776,-4.837125792116,129.899922785572));
#125983=CARTESIAN_POINT('Ctrl Pts',(-204.097829110906,-4.86177557562907,
130.061177386649));
#125984=CARTESIAN_POINT('Ctrl Pts',(-204.106997320508,-4.88617137106238,
130.220770441836));
#125985=CARTESIAN_POINT('Ctrl Pts',(-204.11616553011,-4.9027393278596,130.381790901728));
#125986=CARTESIAN_POINT('Ctrl Pts',(-204.125333739712,-4.91132906577983,
130.543535254293));
#125987=CARTESIAN_POINT('Ctrl Pts',(-204.130175638457,-4.91586546307692,
130.628955397563));
#125988=CARTESIAN_POINT('Ctrl Pts',(-204.135017537202,-4.91817745258136,
130.71457709991));
#125989=CARTESIAN_POINT('Ctrl Pts',(-204.139859435948,-4.91824831916273,
130.80029447038));
#125990=CARTESIAN_POINT('Ctrl Pts',(-204.139859435995,-4.91824831916343,
130.800294471219));
#125991=CARTESIAN_POINT('Ctrl Pts',(-204.147784635894,-4.91836431326766,
130.94059630973));
#125992=CARTESIAN_POINT('Ctrl Pts',(-204.155709835794,-4.91247201397862,
131.080987232013));
#125993=CARTESIAN_POINT('Ctrl Pts',(-204.163635035693,-4.900578301156,131.220912387145));
#125994=CARTESIAN_POINT('Ctrl Pts',(-204.171354581511,-4.88899322289429,
131.357206570228));
#125995=CARTESIAN_POINT('Ctrl Pts',(-204.179074127329,-4.87171440627009,
131.493058448163));
#125996=CARTESIAN_POINT('Ctrl Pts',(-204.186793673146,-4.84880093828704,
131.627957924122));
#125997=CARTESIAN_POINT('Ctrl Pts',(-204.194513059106,-4.8258879448005,
131.762854606557));
#125998=CARTESIAN_POINT('Ctrl Pts',(-204.202232445066,-4.79734059760185,
131.896798538118));
#125999=CARTESIAN_POINT('Ctrl Pts',(-204.209951831025,-4.76326941003805,
132.029288203138));
#126000=CARTESIAN_POINT('Ctrl Pts',(-204.217672755543,-4.72919143171145,
132.161804274807));
#126001=CARTESIAN_POINT('Ctrl Pts',(-204.225393680062,-4.68958752045796,
132.29286512203));
#126002=CARTESIAN_POINT('Ctrl Pts',(-204.23311460458,-4.6446184041067,132.421983238183));
#126003=CARTESIAN_POINT('Ctrl Pts',(-204.24119374033,-4.59756295178294,
132.55709177159));
#126004=CARTESIAN_POINT('Ctrl Pts',(-204.24927287608,-4.54463267751754,
132.69007253139));
#126005=CARTESIAN_POINT('Ctrl Pts',(-204.25735201183,-4.48606813212016,
132.820390323814));
#126006=CARTESIAN_POINT('Ctrl Pts',(-204.265085528802,-4.43000892977471,
132.945133228333));
#126007=CARTESIAN_POINT('Ctrl Pts',(-204.272819045774,-4.36878776769414,
133.067435961724));
#126008=CARTESIAN_POINT('Ctrl Pts',(-204.280552562746,-4.30266231755848,
133.186855117783));
#126009=CARTESIAN_POINT('Ctrl Pts',(-204.288291669847,-4.23648906901836,
133.306360595297));
#126010=CARTESIAN_POINT('Ctrl Pts',(-204.296030776948,-4.16540467691822,
133.422978009958));
#126011=CARTESIAN_POINT('Ctrl Pts',(-204.303769884048,-4.08970977527734,
133.53629345285));
#126012=CARTESIAN_POINT('Ctrl Pts',(-204.311519964139,-4.01390754867324,
133.649769561459));
#126013=CARTESIAN_POINT('Ctrl Pts',(-204.319270044229,-3.93348199885383,
133.759934040129));
#126014=CARTESIAN_POINT('Ctrl Pts',(-204.32702012432,-3.84877374515481,
133.866406293435));
#126015=CARTESIAN_POINT('Ctrl Pts',(-204.328034827407,-3.83768305634567,
133.880346500872));
#126016=CARTESIAN_POINT('Ctrl Pts',(-204.329049530494,-3.82651900354742,
133.894223468265));
#126017=CARTESIAN_POINT('Ctrl Pts',(-204.330064233581,-3.81528239632779,
133.908036389739));
#126018=CARTESIAN_POINT('Ctrl Pts',(-204.3378385677,-3.72919106576708,134.013866625264));
#126019=CARTESIAN_POINT('Ctrl Pts',(-204.345612901819,-3.63855667661419,
134.116279706243));
#126020=CARTESIAN_POINT('Ctrl Pts',(-204.353387235938,-3.54368061892281,
134.21486068846));
#126021=CARTESIAN_POINT('Ctrl Pts',(-204.361151988886,-3.44892148749296,
134.313320178428));
#126022=CARTESIAN_POINT('Ctrl Pts',(-204.368916741833,-3.3499313571539,
134.407956687445));
#126023=CARTESIAN_POINT('Ctrl Pts',(-204.37668149478,-3.24705273251776,
134.498387094833));
#126024=CARTESIAN_POINT('Ctrl Pts',(-204.384438535665,-3.14427628838194,
134.588727685466));
#126025=CARTESIAN_POINT('Ctrl Pts',(-204.39219557655,-3.03761932746507,
134.674870231555));
#126026=CARTESIAN_POINT('Ctrl Pts',(-204.399952617435,-2.92746192108998,
134.756467620554));
#126027=CARTESIAN_POINT('Ctrl Pts',(-204.407703808675,-2.81738758527178,
134.838003476328));
#126028=CARTESIAN_POINT('Ctrl Pts',(-204.415454999916,-2.70381837107695,
134.915000765548));
#126029=CARTESIAN_POINT('Ctrl Pts',(-204.423206191156,-2.58716793923965,
134.987152163492));
#126030=CARTESIAN_POINT('Ctrl Pts',(-204.430954087933,-2.47056708694779,
135.059272895167));
#126031=CARTESIAN_POINT('Ctrl Pts',(-204.43870198471,-2.35088795351289,
135.126551626789));
#126032=CARTESIAN_POINT('Ctrl Pts',(-204.446449881487,-2.22857354968108,
135.188724082901));
#126033=CARTESIAN_POINT('Ctrl Pts',(-204.454196157571,-2.1062847313861,
135.250883533874));
#126034=CARTESIAN_POINT('Ctrl Pts',(-204.461942433656,-1.98136208744859,
135.307938656849));
#126035=CARTESIAN_POINT('Ctrl Pts',(-204.46968870974,-1.85427326821161,
135.359671112943));
#126036=CARTESIAN_POINT('Ctrl Pts',(-204.477435043005,-1.72718351083332,
135.411403950916));
#126037=CARTESIAN_POINT('Ctrl Pts',(-204.485181376271,-1.59792790836239,
135.457813896205));
#126038=CARTESIAN_POINT('Ctrl Pts',(-204.492927709536,-1.46699375409005,
135.498730904192));
#126039=CARTESIAN_POINT('Ctrl Pts',(-204.500675777539,-1.33603027802187,
135.53965707526));
#126040=CARTESIAN_POINT('Ctrl Pts',(-204.508423845542,-1.20338787525171,
135.575087744666));
#126041=CARTESIAN_POINT('Ctrl Pts',(-204.516171913545,-1.06956825840305,
135.604902962251));
#126042=CARTESIAN_POINT('Ctrl Pts',(-204.523928216287,-0.935606416472946,
135.634749867804));
#126043=CARTESIAN_POINT('Ctrl Pts',(-204.531684519029,-0.800465243359993,
135.658969314318));
#126044=CARTESIAN_POINT('Ctrl Pts',(-204.539440821771,-0.664656438594865,
135.677492555153));
#126045=CARTESIAN_POINT('Ctrl Pts',(-204.547201264285,-0.528775148581879,
135.696025682401));
#126046=CARTESIAN_POINT('Ctrl Pts',(-204.5549617068,-0.392225905948943,
135.708856509484));
#126047=CARTESIAN_POINT('Ctrl Pts',(-204.562722149314,-0.255523769358385,
135.715968365116));
#126048=CARTESIAN_POINT('Ctrl Pts',(-204.570495049579,-0.118602186361955,
135.72309163733));
#126049=CARTESIAN_POINT('Ctrl Pts',(-204.578267949845,0.0184723898871198,
135.724477588372));
#126050=CARTESIAN_POINT('Ctrl Pts',(-204.58604085011,0.155185762840657,
135.720161716218));
#126051=CARTESIAN_POINT('Ctrl Pts',(-204.593531185872,0.286929260314916,
135.716002736889));
#126052=CARTESIAN_POINT('Ctrl Pts',(-204.601021521633,0.418337052633677,
135.70654931052));
#126053=CARTESIAN_POINT('Ctrl Pts',(-204.608511857394,0.548956999130425,
135.691878318363));
#126054=CARTESIAN_POINT('Ctrl Pts',(-204.616286191514,0.684529440611316,
135.676651071078));
#126055=CARTESIAN_POINT('Ctrl Pts',(-204.624060525633,0.819682567332442,
135.655754564432));
#126056=CARTESIAN_POINT('Ctrl Pts',(-204.631834859752,0.953904366288411,
135.62921807893));
#126057=CARTESIAN_POINT('Ctrl Pts',(-204.639599612699,1.08796074887291,
135.602714297274));
#126058=CARTESIAN_POINT('Ctrl Pts',(-204.647364365646,1.22108770756962,
135.570584441822));
#126059=CARTESIAN_POINT('Ctrl Pts',(-204.655129118593,1.35277777999265,
135.532909585321));
#126060=CARTESIAN_POINT('Ctrl Pts',(-204.662886159478,1.48433705597924,
135.495272148018));
#126061=CARTESIAN_POINT('Ctrl Pts',(-204.670643200363,1.6144619123036,135.452100776427));
#126062=CARTESIAN_POINT('Ctrl Pts',(-204.678400241248,1.74265487551586,
135.403527612506));
#126063=CARTESIAN_POINT('Ctrl Pts',(-204.686151432488,1.8707511674172,135.354991077985));
#126064=CARTESIAN_POINT('Ctrl Pts',(-204.693902623728,1.99691810186812,
135.301060997223));
#126065=CARTESIAN_POINT('Ctrl Pts',(-204.701653814969,2.12067352414457,
135.241919278191));
#126066=CARTESIAN_POINT('Ctrl Pts',(-204.709401711746,2.24437634706579,
135.182802695968));
#126067=CARTESIAN_POINT('Ctrl Pts',(-204.717149608523,2.36566934435866,
135.118479049337));
#126068=CARTESIAN_POINT('Ctrl Pts',(-204.7248975053,2.48409071546674,135.049178208445));
#126069=CARTESIAN_POINT('Ctrl Pts',(-204.732643781384,2.60248731537686,
134.979891863794));
#126070=CARTESIAN_POINT('Ctrl Pts',(-204.740390057468,2.71801314667377,
134.905630593073));
#126071=CARTESIAN_POINT('Ctrl Pts',(-204.748136333552,2.83023173824012,
134.826669826262));
#126072=CARTESIAN_POINT('Ctrl Pts',(-204.755882666818,2.94245115817848,
134.74770847658));
#126073=CARTESIAN_POINT('Ctrl Pts',(-204.763629000083,3.05136296992693,
134.664047786568));
#126074=CARTESIAN_POINT('Ctrl Pts',(-204.771375333349,3.15656071620505,
134.576005816602));
#126075=CARTESIAN_POINT('Ctrl Pts',(-204.779123401352,3.26178202078891,
134.487944130248));
#126076=CARTESIAN_POINT('Ctrl Pts',(-204.786871469354,3.36328730507665,
134.395499462426));
#126077=CARTESIAN_POINT('Ctrl Pts',(-204.794619537357,3.46070446367402,
134.299029082186));
#126078=CARTESIAN_POINT('Ctrl Pts',(-204.802375840099,3.55822515838696,
134.202456172077));
#126079=CARTESIAN_POINT('Ctrl Pts',(-204.810132142841,3.65164876974275,
134.101849278174));
#126080=CARTESIAN_POINT('Ctrl Pts',(-204.817888445583,3.74064087315327,
133.997601748548));
#126081=CARTESIAN_POINT('Ctrl Pts',(-204.825648888097,3.82968047432912,
133.893298578876));
#126082=CARTESIAN_POINT('Ctrl Pts',(-204.833409330612,3.91428361358645,
133.785351209223));
#126083=CARTESIAN_POINT('Ctrl Pts',(-204.841169773126,3.99415786311061,
133.67418396179));
#126084=CARTESIAN_POINT('Ctrl Pts',(-204.848942673391,4.07416033387079,
133.562838258822));
#126085=CARTESIAN_POINT('Ctrl Pts',(-204.856715573657,4.14941853042956,
133.448262676063));
#126086=CARTESIAN_POINT('Ctrl Pts',(-204.864488473922,4.21968438244643,
133.330909009154));
#126087=CARTESIAN_POINT('Ctrl Pts',(-204.871978809684,4.28739589375082,
133.217821443638));
#126088=CARTESIAN_POINT('Ctrl Pts',(-204.879469145446,4.35047157997676,
133.102154538428));
#126089=CARTESIAN_POINT('Ctrl Pts',(-204.886959481207,4.40873173042483,
132.984330248466));
#126090=CARTESIAN_POINT('Ctrl Pts',(-204.894733815326,4.4692008321869,132.862038614734));
#126091=CARTESIAN_POINT('Ctrl Pts',(-204.902508149446,4.52467357561692,
132.737035389221));
#126092=CARTESIAN_POINT('Ctrl Pts',(-204.910282483565,4.57489783969652,
132.609767169797));
#126093=CARTESIAN_POINT('Ctrl Pts',(-204.918047236512,4.62506020685945,
132.48265579708));
#126094=CARTESIAN_POINT('Ctrl Pts',(-204.925811989459,4.66998682248568,
132.35328534469));
#126095=CARTESIAN_POINT('Ctrl Pts',(-204.933576742406,4.70947159955726,
132.222126576906));
#126096=CARTESIAN_POINT('Ctrl Pts',(-204.941333783291,4.74891715979151,
132.091098077859));
#126097=CARTESIAN_POINT('Ctrl Pts',(-204.949090824176,4.78293152551465,
131.958285170043));
#126098=CARTESIAN_POINT('Ctrl Pts',(-204.956847865061,4.81135697494726,
131.824177817914));
#126099=CARTESIAN_POINT('Ctrl Pts',(-204.964599056301,4.8397609885273,131.690171597184));
#126100=CARTESIAN_POINT('Ctrl Pts',(-204.972350247541,4.86258439407255,
131.55487325603));
#126101=CARTESIAN_POINT('Ctrl Pts',(-204.980101438781,4.87971961950594,
131.418786770581));
#126102=CARTESIAN_POINT('Ctrl Pts',(-204.987849335558,4.89684756201144,
131.282758125518));
#126103=CARTESIAN_POINT('Ctrl Pts',(-204.995597232335,4.90829208414323,
131.145942389504));
#126104=CARTESIAN_POINT('Ctrl Pts',(-205.003345129112,4.91399696768572,
131.008852338855));
#126105=CARTESIAN_POINT('Ctrl Pts',(-205.011091405196,4.91970065788955,
130.871790964489));
#126106=CARTESIAN_POINT('Ctrl Pts',(-205.01883768128,4.91966708133521,130.734455780001));
#126107=CARTESIAN_POINT('Ctrl Pts',(-205.026583957365,4.91389204176511,
130.597362877536));
#126108=CARTESIAN_POINT('Ctrl Pts',(-205.03433029063,4.90811695956499,130.460268963083));
#126109=CARTESIAN_POINT('Ctrl Pts',(-205.042076623895,4.89660034623337,
130.323417724839));
#126110=CARTESIAN_POINT('Ctrl Pts',(-205.04982295716,4.87939009488483,130.18732304623));
#126111=CARTESIAN_POINT('Ctrl Pts',(-205.057571025163,4.86217598941975,
130.051197890161));
#126112=CARTESIAN_POINT('Ctrl Pts',(-205.065319093166,4.83926575777492,
129.915830018667));
#126113=CARTESIAN_POINT('Ctrl Pts',(-205.073067161169,4.81075884846427,
129.781725607202));
#126114=CARTESIAN_POINT('Ctrl Pts',(-205.080823463911,4.78222164167122,
129.647478667972));
#126115=CARTESIAN_POINT('Ctrl Pts',(-205.088579766653,4.74807595643261,
129.514498254231));
#126116=CARTESIAN_POINT('Ctrl Pts',(-205.096336069395,4.70847196296183,
129.383278341094));
#126117=CARTESIAN_POINT('Ctrl Pts',(-205.104096511909,4.66884683164728,
129.251988391939));
#126118=CARTESIAN_POINT('Ctrl Pts',(-205.111856954423,4.62375771564571,
129.122461184739));
#126119=CARTESIAN_POINT('Ctrl Pts',(-205.119617396937,4.5734035448659,128.99517210381));
#126120=CARTESIAN_POINT('Ctrl Pts',(-205.127390297203,4.52296854110091,
128.867678687148));
#126121=CARTESIAN_POINT('Ctrl Pts',(-205.135163197468,4.46725175190091,
128.742430933815));
#126122=CARTESIAN_POINT('Ctrl Pts',(-205.142936097734,4.40649919765708,
128.619881758994));
#126123=CARTESIAN_POINT('Ctrl Pts',(-205.150426433496,4.34795515178448,
128.501787555357));
#126124=CARTESIAN_POINT('Ctrl Pts',(-205.157916769258,4.28473525768429,
128.386199406543));
#126125=CARTESIAN_POINT('Ctrl Pts',(-205.16540710502,4.21709737997774,128.273496585208));
#126126=CARTESIAN_POINT('Ctrl Pts',(-205.17318143914,4.14689499158213,128.15652060215));
#126127=CARTESIAN_POINT('Ctrl Pts',(-205.180955773259,4.0717106105036,128.042282515269));
#126128=CARTESIAN_POINT('Ctrl Pts',(-205.188730107378,3.9917836946099,127.931235838176));
#126129=CARTESIAN_POINT('Ctrl Pts',(-205.196494860325,3.91195528149677,
127.820326016188));
#126130=CARTESIAN_POINT('Ctrl Pts',(-205.204259613272,3.82739618907955,
127.712600092508));
#126131=CARTESIAN_POINT('Ctrl Pts',(-205.212024366219,3.73839108960982,
127.608485913572));
#126132=CARTESIAN_POINT('Ctrl Pts',(-205.219781407104,3.64947439125963,
127.504475142307));
#126133=CARTESIAN_POINT('Ctrl Pts',(-205.227538447989,3.55612072597651,
127.404069272277));
#126134=CARTESIAN_POINT('Ctrl Pts',(-205.235295488874,3.45865706226162,
127.307665837039));
#126135=CARTESIAN_POINT('Ctrl Pts',(-205.243046680114,3.36126689665303,
127.21133510038));
#126136=CARTESIAN_POINT('Ctrl Pts',(-205.250797871354,3.2597731785813,127.119001064663));
#126137=CARTESIAN_POINT('Ctrl Pts',(-205.258549062594,3.15454177209991,
127.031026644728));
#126138=CARTESIAN_POINT('Ctrl Pts',(-205.266296959371,3.04935509177414,
126.943089616268));
#126139=CARTESIAN_POINT('Ctrl Pts',(-205.274044856149,2.94043418200212,
126.859508768447));
#126140=CARTESIAN_POINT('Ctrl Pts',(-205.281792752926,2.82818006870287,
126.780608567366));
#126141=CARTESIAN_POINT('Ctrl Pts',(-205.28953902901,2.71594943654389,126.701724870505));
#126142=CARTESIAN_POINT('Ctrl Pts',(-205.297285305094,2.60038730735141,
126.627520097597));
#126143=CARTESIAN_POINT('Ctrl Pts',(-205.305031581178,2.48192561588327,
126.558276739482));
#126144=CARTESIAN_POINT('Ctrl Pts',(-205.312777914443,2.36346304995832,
126.489032870229));
#126145=CARTESIAN_POINT('Ctrl Pts',(-205.320524247709,2.24210121658067,
126.424750686145));
#126146=CARTESIAN_POINT('Ctrl Pts',(-205.328270580974,2.11829834782731,
126.365667659938));
#126147=CARTESIAN_POINT('Ctrl Pts',(-205.336018648977,1.99446775428004,
126.306571402498));
#126148=CARTESIAN_POINT('Ctrl Pts',(-205.34376671698,1.86819539035735,126.252676788146));
#126149=CARTESIAN_POINT('Ctrl Pts',(-205.351514784983,1.73996087015536,
126.204173748228));
#126150=CARTESIAN_POINT('Ctrl Pts',(-205.359271087725,1.61159006077877,
126.155619158702));
#126151=CARTESIAN_POINT('Ctrl Pts',(-205.367027390467,1.48125329557024,
126.112467728895));
#126152=CARTESIAN_POINT('Ctrl Pts',(-205.374783693208,1.34944734045477,
126.07486012197));
#126153=CARTESIAN_POINT('Ctrl Pts',(-205.382544135723,1.21757103653245,
126.037232442734));
#126154=CARTESIAN_POINT('Ctrl Pts',(-205.390304578237,1.0842243601514,126.005154573647));
#126155=CARTESIAN_POINT('Ctrl Pts',(-205.398065020751,0.94991479207595,
125.978716106177));
#126156=CARTESIAN_POINT('Ctrl Pts',(-205.405837921016,0.815389618358384,
125.952235197333));
#126157=CARTESIAN_POINT('Ctrl Pts',(-205.413610821282,0.679898850757354,
125.931411840046));
#126158=CARTESIAN_POINT('Ctrl Pts',(-205.421383721547,0.543956519674996,
125.916283862113));
#126159=CARTESIAN_POINT('Ctrl Pts',(-205.428874057309,0.412956034745918,
125.901705824283));
#126160=CARTESIAN_POINT('Ctrl Pts',(-205.436364393071,0.281536554534047,
125.892416293839));
#126161=CARTESIAN_POINT('Ctrl Pts',(-205.443854728833,0.150156553991709,
125.888403328106));
#126162=CARTESIAN_POINT('Ctrl Pts',(-205.451629062952,0.0137952407976317,
125.884238209558));
#126163=CARTESIAN_POINT('Ctrl Pts',(-205.459403397071,-0.122955491538462,
125.885744482312));
#126164=CARTESIAN_POINT('Ctrl Pts',(-205.46717773119,-0.259584656345014,
125.892965818867));
#126165=CARTESIAN_POINT('Ctrl Pts',(-205.474942484137,-0.396045437916839,
125.900178255769));
#126166=CARTESIAN_POINT('Ctrl Pts',(-205.482707237084,-0.532384563386209,
125.913091721957));
#126167=CARTESIAN_POINT('Ctrl Pts',(-205.490471990031,-0.668088201124236,
125.931697976051));
#126168=CARTESIAN_POINT('Ctrl Pts',(-205.498229030916,-0.803657056095805,
125.950285750151));
#126169=CARTESIAN_POINT('Ctrl Pts',(-205.505986071801,-0.938591294568638,
125.974555007365));
#126170=CARTESIAN_POINT('Ctrl Pts',(-205.513743112686,-1.07237972584027,
126.004445536431));
#126171=CARTESIAN_POINT('Ctrl Pts',(-205.521494303926,-1.20606726621606,
126.034313524817));
#126172=CARTESIAN_POINT('Ctrl Pts',(-205.529245495166,-1.33861033923932,
126.069794262592));
#126173=CARTESIAN_POINT('Ctrl Pts',(-205.536996686406,-1.4695058559177,
126.110776102302));
#126174=CARTESIAN_POINT('Ctrl Pts',(-205.544744583183,-1.60034573850956,
126.151740523638));
#126175=CARTESIAN_POINT('Ctrl Pts',(-205.55249247996,-1.72953908518632,
126.198201280005));
#126176=CARTESIAN_POINT('Ctrl Pts',(-205.560240376737,-1.85659614912279,
126.249996358796));
#126177=CARTESIAN_POINT('Ctrl Pts',(-205.567986652821,-1.98362663546017,
126.301780603172));
#126178=CARTESIAN_POINT('Ctrl Pts',(-205.575732928906,-2.10852136608529,
126.358896803041));
#126179=CARTESIAN_POINT('Ctrl Pts',(-205.58347920499,-2.23080920216611,
126.421134252657));
#126180=CARTESIAN_POINT('Ctrl Pts',(-205.591225538255,-2.35309794094813,
126.483372161696));
#126181=CARTESIAN_POINT('Ctrl Pts',(-205.59897187152,-2.47277939835213,
126.550731218584));
#126182=CARTESIAN_POINT('Ctrl Pts',(-205.606718204785,-2.58940609623158,
126.622954259497));
#126183=CARTESIAN_POINT('Ctrl Pts',(-205.614466272788,-2.70605891185186,
126.69519347426));
#126184=CARTESIAN_POINT('Ctrl Pts',(-205.622214340791,-2.81965527435539,
126.77229863474));
#126185=CARTESIAN_POINT('Ctrl Pts',(-205.629962408794,-2.92977614598774,
126.853968890547));
#126186=CARTESIAN_POINT('Ctrl Pts',(-205.637718711536,-3.04001405539247,
126.935725946473));
#126187=CARTESIAN_POINT('Ctrl Pts',(-205.645475014278,-3.14676878064829,
127.022057556528));
#126188=CARTESIAN_POINT('Ctrl Pts',(-205.65323131702,-3.24965346373534,
127.112621809344));
#126189=CARTESIAN_POINT('Ctrl Pts',(-205.660991759534,-3.35259305947554,
127.203234399029));
#126190=CARTESIAN_POINT('Ctrl Pts',(-205.668752202048,-3.45165821498836,
127.298083862653));
#126191=CARTESIAN_POINT('Ctrl Pts',(-205.676512644562,-3.54649924868453,
127.396791668655));
#126192=CARTESIAN_POINT('Ctrl Pts',(-205.684285544827,-3.64149252962784,
127.495657929191));
#126193=CARTESIAN_POINT('Ctrl Pts',(-205.692058445093,-3.73224787929608,
127.598394616017));
#126194=CARTESIAN_POINT('Ctrl Pts',(-205.699831345358,-3.81845562610398,
127.704589707648));
#126195=CARTESIAN_POINT('Ctrl Pts',(-205.707321681121,-3.90152950417868,
127.806924340218));
#126196=CARTESIAN_POINT('Ctrl Pts',(-205.714812016883,-3.98038048839516,
127.912470052807));
#126197=CARTESIAN_POINT('Ctrl Pts',(-205.722302352646,-4.05477080955335,
128.020834662146));
#126198=CARTESIAN_POINT('Ctrl Pts',(-205.730448383082,-4.13567316687673,
128.138685374571));
#126199=CARTESIAN_POINT('Ctrl Pts',(-205.738594413519,-4.21155944536966,
128.260249366182));
#126200=CARTESIAN_POINT('Ctrl Pts',(-205.746740443956,-4.28207823747369,
128.385065465946));
#126201=CARTESIAN_POINT('Ctrl Pts',(-205.754614573043,-4.35024322610434,
128.505715405734));
#126202=CARTESIAN_POINT('Ctrl Pts',(-205.76248870213,-4.41339304358188,
128.629403491818));
#126203=CARTESIAN_POINT('Ctrl Pts',(-205.770362831217,-4.47125192901984,
128.755680737805));
#126204=CARTESIAN_POINT('Ctrl Pts',(-205.778228904709,-4.52905162216871,
128.881828796388));
#126205=CARTESIAN_POINT('Ctrl Pts',(-205.786094978202,-4.58157099847426,
129.010560404246));
#126206=CARTESIAN_POINT('Ctrl Pts',(-205.793961051694,-4.62857939142672,
129.141400642173));
#126207=CARTESIAN_POINT('Ctrl Pts',(-205.801819026306,-4.67553938470417,
129.272106167454));
#126208=CARTESIAN_POINT('Ctrl Pts',(-205.809677000917,-4.7169995704176,
129.404915645517));
#126209=CARTESIAN_POINT('Ctrl Pts',(-205.817534975528,-4.75277695961418,
129.539333252383));
#126210=CARTESIAN_POINT('Ctrl Pts',(-205.818374889647,-4.75660109188932,
129.553700726375));
#126211=CARTESIAN_POINT('Ctrl Pts',(-205.819214803765,-4.76036034493871,
129.568086554707));
#126212=CARTESIAN_POINT('Ctrl Pts',(-205.820054717884,-4.76405452823395,
129.582490119308));
#126213=CARTESIAN_POINT('Origin',(213.235140564004,0.,130.804360617566));
#126214=CARTESIAN_POINT('',(-207.915133748109,-4.76405452823406,129.582490119308));
#126215=CARTESIAN_POINT('',(-207.569721641055,-4.76405452823393,129.582490119308));
#126216=CARTESIAN_POINT('',(213.235140564004,-4.76405452823405,129.582490119308));
#126217=CARTESIAN_POINT('',(-206.235140563976,-4.91824935292959,130.806883494435));
#126218=CARTESIAN_POINT('Ctrl Pts',(-206.235140564013,-4.91824935292925,
130.806883495092));
#126219=CARTESIAN_POINT('Ctrl Pts',(-206.243296577379,-4.91817584971133,
130.950175093808));
#126220=CARTESIAN_POINT('Ctrl Pts',(-206.251452590746,-4.9118408081057,
131.09330184757));
#126221=CARTESIAN_POINT('Ctrl Pts',(-206.259608604113,-4.89928367079141,
131.235872582194));
#126222=CARTESIAN_POINT('Ctrl Pts',(-206.267382938232,-4.88731417335877,
131.371771394107));
#126223=CARTESIAN_POINT('Ctrl Pts',(-206.275157272351,-4.86966698677397,
131.507387058606));
#126224=CARTESIAN_POINT('Ctrl Pts',(-206.28293160647,-4.846359096209,131.64220700748));
#126225=CARTESIAN_POINT('Ctrl Pts',(-206.290696359417,-4.82307993053606,
131.776860802817));
#126226=CARTESIAN_POINT('Ctrl Pts',(-206.298461112364,-4.79415400762733,
131.910720452176));
#126227=CARTESIAN_POINT('Ctrl Pts',(-206.306225865311,-4.75965019918353,
132.043276693784));
#126228=CARTESIAN_POINT('Ctrl Pts',(-206.313982906196,-4.72518066040869,
132.175701278665));
#126229=CARTESIAN_POINT('Ctrl Pts',(-206.321739947081,-4.68514435886508,
132.306824656126));
#126230=CARTESIAN_POINT('Ctrl Pts',(-206.329496987965,-4.63966146046592,
132.436146324933));
#126231=CARTESIAN_POINT('Ctrl Pts',(-206.337248179205,-4.59421286107431,
132.565370471264));
#126232=CARTESIAN_POINT('Ctrl Pts',(-206.344999370445,-4.5433259693909,
132.69279524599));
#126233=CARTESIAN_POINT('Ctrl Pts',(-206.352750561685,-4.48717107061851,
132.817934267946));
#126234=CARTESIAN_POINT('Ctrl Pts',(-206.360498458462,-4.43104003917615,
132.943020102479));
#126235=CARTESIAN_POINT('Ctrl Pts',(-206.368246355239,-4.36964561366111,
133.065821760543));
#126236=CARTESIAN_POINT('Ctrl Pts',(-206.375994252016,-4.30320651608381,
133.185872058318));
#126237=CARTESIAN_POINT('Ctrl Pts',(-206.3837405281,-4.23678131613346,133.305897244159));
#126238=CARTESIAN_POINT('Ctrl Pts',(-206.391486804184,-4.16531373223735,
133.423171872606));
#126239=CARTESIAN_POINT('Ctrl Pts',(-206.399233080268,-4.08906864095504,
133.537252988674));
#126240=CARTESIAN_POINT('Ctrl Pts',(-206.406979413534,-4.01282298684869,
133.651334946862));
#126241=CARTESIAN_POINT('Ctrl Pts',(-206.414725746799,-3.93179997222957,
133.762223020581));
#126242=CARTESIAN_POINT('Ctrl Pts',(-206.422472080064,-3.84630781202687,
133.869503237028));
#126243=CARTESIAN_POINT('Ctrl Pts',(-206.430220148067,-3.76079650644777,
133.976807478135));
#126244=CARTESIAN_POINT('Ctrl Pts',(-206.43796821607,-3.67081430735097,
134.080501948538));
#126245=CARTESIAN_POINT('Ctrl Pts',(-206.445716284073,-3.5767094513966,
134.180206076527));
#126246=CARTESIAN_POINT('Ctrl Pts',(-206.453472586815,-3.48250457968159,
134.280016171251));
#126247=CARTESIAN_POINT('Ctrl Pts',(-206.461228889557,-3.38416856715666,
134.375827166964));
#126248=CARTESIAN_POINT('Ctrl Pts',(-206.468985192298,-3.28208662334993,
134.467295296116));
#126249=CARTESIAN_POINT('Ctrl Pts',(-206.476745634812,-3.17995019533615,
134.558812244563));
#126250=CARTESIAN_POINT('Ctrl Pts',(-206.484506077326,-3.07406415392714,
134.645981459434));
#126251=CARTESIAN_POINT('Ctrl Pts',(-206.49226651984,-2.96484568166884,
134.728500414565));
#126252=CARTESIAN_POINT('Ctrl Pts',(-206.500039420106,-2.8554518822229,
134.811151836448));
#126253=CARTESIAN_POINT('Ctrl Pts',(-206.507812320371,-2.74271528361125,
134.889137858572));
#126254=CARTESIAN_POINT('Ctrl Pts',(-206.515585220636,-2.62708159836639,
134.962199640186));
#126255=CARTESIAN_POINT('Ctrl Pts',(-206.523075556399,-2.51565148882853,
135.032605442017));
#126256=CARTESIAN_POINT('Ctrl Pts',(-206.530565892162,-2.40153153536177,
135.098438650812));
#126257=CARTESIAN_POINT('Ctrl Pts',(-206.538056227925,-2.2851392588354,
135.159509481868));
#126258=CARTESIAN_POINT('Ctrl Pts',(-206.545830562044,-2.16433393378268,
135.222895832038));
#126259=CARTESIAN_POINT('Ctrl Pts',(-206.553604896163,-2.04069789899693,
135.281352333429));
#126260=CARTESIAN_POINT('Ctrl Pts',(-206.561379230282,-1.91467157352999,
135.334616220511));
#126261=CARTESIAN_POINT('Ctrl Pts',(-206.56914398323,-1.78880056424624,
135.387814464613));
#126262=CARTESIAN_POINT('Ctrl Pts',(-206.576908736177,-1.66054548224971,
135.435832676627));
#126263=CARTESIAN_POINT('Ctrl Pts',(-206.584673489124,-1.53037201072842,
135.478453531841));
#126264=CARTESIAN_POINT('Ctrl Pts',(-206.592430530009,-1.40032782933418,
135.521032055421));
#126265=CARTESIAN_POINT('Ctrl Pts',(-206.600187570894,-1.26836941934266,
135.55822376943));
#126266=CARTESIAN_POINT('Ctrl Pts',(-206.607944611779,-1.13498281922694,
135.589859239712));
#126267=CARTESIAN_POINT('Ctrl Pts',(-206.615695803019,-1.00169680698415,
135.62147085344));
#126268=CARTESIAN_POINT('Ctrl Pts',(-206.623446994259,-0.866985127212026,
135.647534473537));
#126269=CARTESIAN_POINT('Ctrl Pts',(-206.631198185499,-0.731349029471388,
135.667930464869));
#126270=CARTESIAN_POINT('Ctrl Pts',(-206.638946082276,-0.595770580690315,
135.688317787359));
#126271=CARTESIAN_POINT('Ctrl Pts',(-206.646693979053,-0.459268881202547,
135.703042214174));
#126272=CARTESIAN_POINT('Ctrl Pts',(-206.65444187583,-0.322355210575576,
135.712035238068));
#126273=CARTESIAN_POINT('Ctrl Pts',(-206.662188151914,-0.185470179336983,
135.721026380815));
#126274=CARTESIAN_POINT('Ctrl Pts',(-206.669934427998,-0.0481737382443191,
135.724288479683));
#126275=CARTESIAN_POINT('Ctrl Pts',(-206.677680704082,0.0890182698783709,
135.721804954834));
#126276=CARTESIAN_POINT('Ctrl Pts',(-206.685427037348,0.226211290721486,
135.719321411652));
#126277=CARTESIAN_POINT('Ctrl Pts',(-206.693173370613,0.36329948615519,
135.711092167198));
#126278=CARTESIAN_POINT('Ctrl Pts',(-206.700919703878,0.499767971438338,
135.697152769009));
#126279=CARTESIAN_POINT('Ctrl Pts',(-206.708667771881,0.636267017892372,
135.683210249189));
#126280=CARTESIAN_POINT('Ctrl Pts',(-206.716415839884,0.772145689173082,
135.66355507079));
#126281=CARTESIAN_POINT('Ctrl Pts',(-206.724163907887,0.906895569102237,
135.638274506874));
#126282=CARTESIAN_POINT('Ctrl Pts',(-206.731920210629,1.04178866280751,
135.612967074473));
#126283=CARTESIAN_POINT('Ctrl Pts',(-206.739676513371,1.17555018377165,
135.582022385611));
#126284=CARTESIAN_POINT('Ctrl Pts',(-206.747432816113,1.30768269545861,
135.545578713214));
#126285=CARTESIAN_POINT('Ctrl Pts',(-206.755193258627,1.4398857302455,135.509115589732));
#126286=CARTESIAN_POINT('Ctrl Pts',(-206.762953701141,1.57045765127054,
135.467147754108));
#126287=CARTESIAN_POINT('Ctrl Pts',(-206.770714143655,1.69891843734635,
135.419862671053));
#126288=CARTESIAN_POINT('Ctrl Pts',(-206.77848704392,1.82758544008018,135.372501681785));
#126289=CARTESIAN_POINT('Ctrl Pts',(-206.786259944186,1.9541341744678,135.319806538378));
#126290=CARTESIAN_POINT('Ctrl Pts',(-206.794032844451,2.07810595194281,
135.262012321659));
#126291=CARTESIAN_POINT('Ctrl Pts',(-206.801523180213,2.19757104304053,
135.206319070292));
#126292=CARTESIAN_POINT('Ctrl Pts',(-206.809013515975,2.31464300846158,
135.145891178822));
#126293=CARTESIAN_POINT('Ctrl Pts',(-206.816503851737,2.42893649673259,
135.080977336111));
#126294=CARTESIAN_POINT('Ctrl Pts',(-206.824278185856,2.5475634573503,135.013602265324));
#126295=CARTESIAN_POINT('Ctrl Pts',(-206.832052519975,2.66357286432491,
134.941180934586));
#126296=CARTESIAN_POINT('Ctrl Pts',(-206.839826854094,2.77650558831772,
134.86394184973));
#126297=CARTESIAN_POINT('Ctrl Pts',(-206.847591607042,2.88929913282099,
134.786797955144));
#126298=CARTESIAN_POINT('Ctrl Pts',(-206.855356359989,2.99902321915925,
134.704848338791));
#126299=CARTESIAN_POINT('Ctrl Pts',(-206.863121112936,3.1052432927571,134.618367323812));
#126300=CARTESIAN_POINT('Ctrl Pts',(-206.870878153821,3.21135786708041,
134.531972202995));
#126301=CARTESIAN_POINT('Ctrl Pts',(-206.878635194706,3.31397505326374,
134.441054885293));
#126302=CARTESIAN_POINT('Ctrl Pts',(-206.886392235591,3.41268958588663,
134.345932705337));
#126303=CARTESIAN_POINT('Ctrl Pts',(-206.894143426831,3.51132967711271,
134.250882257758));
#126304=CARTESIAN_POINT('Ctrl Pts',(-206.901894618071,3.6060726922938,134.151633529634));
#126305=CARTESIAN_POINT('Ctrl Pts',(-206.909645809311,3.69654704137007,
134.048543570705));
#126306=CARTESIAN_POINT('Ctrl Pts',(-206.917393706088,3.78698293643439,
133.945497427759));
#126307=CARTESIAN_POINT('Ctrl Pts',(-206.925141602865,3.87315351654314,
133.838613594408));
#126308=CARTESIAN_POINT('Ctrl Pts',(-206.932889499642,3.95472478551692,
133.728285194794));
#126309=CARTESIAN_POINT('Ctrl Pts',(-206.940635775726,4.0362789915397,133.617979873503));
#126310=CARTESIAN_POINT('Ctrl Pts',(-206.948382051811,4.11323556776735,
133.504231733294));
#126311=CARTESIAN_POINT('Ctrl Pts',(-206.956128327895,4.18530173946635,
133.387465805536));
#126312=CARTESIAN_POINT('Ctrl Pts',(-206.96387466116,4.25736844314155,133.270699015839));
#126313=CARTESIAN_POINT('Ctrl Pts',(-206.971620994426,4.32454446491532,
133.150914726844));
#126314=CARTESIAN_POINT('Ctrl Pts',(-206.979367327691,4.38658140415818,
133.028565339977));
#126315=CARTESIAN_POINT('Ctrl Pts',(-206.987115395694,4.44863223614336,
132.906188553813));
#126316=CARTESIAN_POINT('Ctrl Pts',(-206.994863463697,4.50554151874139,
132.781245875352));
#126317=CARTESIAN_POINT('Ctrl Pts',(-207.0026115317,4.55710786588625,132.654212222743));
#126318=CARTESIAN_POINT('Ctrl Pts',(-207.010367834442,4.60872901835857,
132.527043557257));
#126319=CARTESIAN_POINT('Ctrl Pts',(-207.018124137184,4.65499574460735,
132.397779841151));
#126320=CARTESIAN_POINT('Ctrl Pts',(-207.025880439925,4.69575550096411,
132.266914321765));
#126321=CARTESIAN_POINT('Ctrl Pts',(-207.03364088244,4.73653701203008,132.13597895551));
#126322=CARTESIAN_POINT('Ctrl Pts',(-207.041401324954,4.77180559603988,
132.003440460087));
#126323=CARTESIAN_POINT('Ctrl Pts',(-207.049161767468,4.80145950918554,
131.86980402017));
#126324=CARTESIAN_POINT('Ctrl Pts',(-207.056934667734,4.83116102542514,
131.735953055175));
#126325=CARTESIAN_POINT('Ctrl Pts',(-207.064707567999,4.85522979093357,
131.601001008726));
#126326=CARTESIAN_POINT('Ctrl Pts',(-207.072480468265,4.87361565349489,
131.465460855434));
#126327=CARTESIAN_POINT('Ctrl Pts',(-207.079970804027,4.89133314364086,
131.33484792812));
#126328=CARTESIAN_POINT('Ctrl Pts',(-207.087461139788,4.90377370409151,
131.203689216588));
#126329=CARTESIAN_POINT('Ctrl Pts',(-207.09495147555,4.91093827194779,131.072443350353));
#126330=CARTESIAN_POINT('Ctrl Pts',(-207.102725809669,4.91837448657198,
130.936221257207));
#126331=CARTESIAN_POINT('Ctrl Pts',(-207.110500143789,4.92015028810036,
130.79947375931));
#126332=CARTESIAN_POINT('Ctrl Pts',(-207.118274477908,4.91620975433994,
130.66271064816));
#126333=CARTESIAN_POINT('Ctrl Pts',(-207.126039230855,4.91227407693521,
130.526116085322));
#126334=CARTESIAN_POINT('Ctrl Pts',(-207.133803983802,4.90263609258996,
130.389506334569));
#126335=CARTESIAN_POINT('Ctrl Pts',(-207.141568736749,4.88729170976703,
130.253395277329));
#126336=CARTESIAN_POINT('Ctrl Pts',(-207.149325777634,4.87196256720145,
130.11741940751));
#126337=CARTESIAN_POINT('Ctrl Pts',(-207.157082818519,4.85093834860235,
129.981941631508));
#126338=CARTESIAN_POINT('Ctrl Pts',(-207.164839859404,4.824266980725,129.847474437717));
#126339=CARTESIAN_POINT('Ctrl Pts',(-207.172591050644,4.79761572593367,
129.713108646683));
#126340=CARTESIAN_POINT('Ctrl Pts',(-207.180342241884,4.76532587402565,
129.579752302914));
#126341=CARTESIAN_POINT('Ctrl Pts',(-207.188093433124,4.72749696755391,
129.447911029756));
#126342=CARTESIAN_POINT('Ctrl Pts',(-207.195841329901,4.68968413937648,
129.316125792657));
#126343=CARTESIAN_POINT('Ctrl Pts',(-207.203589226679,4.64633704665318,
129.185854720425));
#126344=CARTESIAN_POINT('Ctrl Pts',(-207.211337123456,4.59760590276493,
129.057591306706));
#126345=CARTESIAN_POINT('Ctrl Pts',(-207.21908339954,4.54888495238146,128.929354722929));
#126346=CARTESIAN_POINT('Ctrl Pts',(-207.226829675624,4.49478232972868,
128.80312532759));
#126347=CARTESIAN_POINT('Ctrl Pts',(-207.234575951708,4.43549737384086,
128.6793791802));
#126348=CARTESIAN_POINT('Ctrl Pts',(-207.242322284973,4.37621198032504,
128.555632119344));
#126349=CARTESIAN_POINT('Ctrl Pts',(-207.250068618239,4.31174434616013,
128.434368695606));
#126350=CARTESIAN_POINT('Ctrl Pts',(-207.257814951504,4.24234082287173,
128.316042429493));
#126351=CARTESIAN_POINT('Ctrl Pts',(-207.265563019507,4.17292175714561,
128.197689665032));
#126352=CARTESIAN_POINT('Ctrl Pts',(-207.27331108751,4.09856480052667,128.082275704225));
#126353=CARTESIAN_POINT('Ctrl Pts',(-207.281059155513,4.01956066101754,
127.970226683734));
#126354=CARTESIAN_POINT('Ctrl Pts',(-207.288815458255,3.94047255496867,
127.858058576209));
#126355=CARTESIAN_POINT('Ctrl Pts',(-207.296571760996,3.85672762533503,
127.749262873077));
#126356=CARTESIAN_POINT('Ctrl Pts',(-207.304328063738,3.76865840149489,
127.644234525882));
#126357=CARTESIAN_POINT('Ctrl Pts',(-207.312088506252,3.68054217245802,
127.539150121895));
#126358=CARTESIAN_POINT('Ctrl Pts',(-207.319848948767,3.58809731371382,
127.437837369101));
#126359=CARTESIAN_POINT('Ctrl Pts',(-207.327609391281,3.4916938564228,127.340654932101));
#126360=CARTESIAN_POINT('Ctrl Pts',(-207.335382291546,3.3951356437441,127.243316489227));
#126361=CARTESIAN_POINT('Ctrl Pts',(-207.343155191811,3.29460642069608,
127.15012187765));
#126362=CARTESIAN_POINT('Ctrl Pts',(-207.350928092077,3.19051065884962,
127.061390567156));
#126363=CARTESIAN_POINT('Ctrl Pts',(-207.358418427839,3.090199040146,126.975884863298));
#126364=CARTESIAN_POINT('Ctrl Pts',(-207.365908763601,2.98657592832593,
126.894523780142));
#126365=CARTESIAN_POINT('Ctrl Pts',(-207.373399099363,2.88002768791472,
126.817554429733));
#126366=CARTESIAN_POINT('Ctrl Pts',(-207.381173433482,2.7694396385851,126.73766676301));
#126367=CARTESIAN_POINT('Ctrl Pts',(-207.388947767602,2.65534995981542,
126.662257368034));
#126368=CARTESIAN_POINT('Ctrl Pts',(-207.396722101721,2.53815732632183,
126.591648848487));
#126369=CARTESIAN_POINT('Ctrl Pts',(-207.404486854668,2.42110912227552,
126.52112734763));
#126370=CARTESIAN_POINT('Ctrl Pts',(-207.412251607615,2.30096590401835,
126.455395149661));
#126371=CARTESIAN_POINT('Ctrl Pts',(-207.420016360562,2.17815780297416,
126.39473346237));
#126372=CARTESIAN_POINT('Ctrl Pts',(-207.427773401447,2.05547167666722,
126.334132025122));
#126373=CARTESIAN_POINT('Ctrl Pts',(-207.435530442332,1.93012628308811,
126.278591248508));
#126374=CARTESIAN_POINT('Ctrl Pts',(-207.443287483217,1.80257869882107,
126.228347822888));
#126375=CARTESIAN_POINT('Ctrl Pts',(-207.451038674457,1.67512729917933,
126.178142286226));
#126376=CARTESIAN_POINT('Ctrl Pts',(-207.458789865697,1.54547737663862,
126.133226291915));
#126377=CARTESIAN_POINT('Ctrl Pts',(-207.466541056937,1.41410813162145,
126.093789393757));
#126378=CARTESIAN_POINT('Ctrl Pts',(-207.474288953714,1.28279472203762,
126.054369257331));
#126379=CARTESIAN_POINT('Ctrl Pts',(-207.482036850492,1.1497638170714,126.020423697504));
#126380=CARTESIAN_POINT('Ctrl Pts',(-207.489784747269,1.01551180090532,
125.992093080872));
#126381=CARTESIAN_POINT('Ctrl Pts',(-207.497531023353,0.881287867367254,
125.963768390394));
#126382=CARTESIAN_POINT('Ctrl Pts',(-207.505277299437,0.745843712991892,
125.941056387592));
#126383=CARTESIAN_POINT('Ctrl Pts',(-207.513023575521,0.609687607747052,
125.924046684686));
#126384=CARTESIAN_POINT('Ctrl Pts',(-207.520769908786,0.473530497428588,
125.907036856218));
#126385=CARTESIAN_POINT('Ctrl Pts',(-207.528516242052,0.33666181370332,
125.895729460106));
#126386=CARTESIAN_POINT('Ctrl Pts',(-207.536262575317,0.199596275234876,
125.890162372744));
#126387=CARTESIAN_POINT('Ctrl Pts',(-207.54401064332,0.0625000418892514,
125.884594038672));
#126388=CARTESIAN_POINT('Ctrl Pts',(-207.551758711323,-0.0747927433537585,
125.884768587215));
#126389=CARTESIAN_POINT('Ctrl Pts',(-207.559506779326,-0.211766424875434,
125.890671774772));
#126390=CARTESIAN_POINT('Ctrl Pts',(-207.567263082068,-0.348885683655652,
125.896581236308));
#126391=CARTESIAN_POINT('Ctrl Pts',(-207.57501938481,-0.485684770005954,
125.908231482363));
#126392=CARTESIAN_POINT('Ctrl Pts',(-207.582775687552,-0.621651659755012,
125.925556227511));
#126393=CARTESIAN_POINT('Ctrl Pts',(-207.590536130066,-0.757691119127012,
125.942890219397));
#126394=CARTESIAN_POINT('Ctrl Pts',(-207.59829657258,-0.892897111621781,
125.965904679646));
#126395=CARTESIAN_POINT('Ctrl Pts',(-207.606057015094,-1.02676787166982,
125.994482157542));
#126396=CARTESIAN_POINT('Ctrl Pts',(-207.61382991536,-1.16085353294637,
126.023105510542));
#126397=CARTESIAN_POINT('Ctrl Pts',(-207.621602815625,-1.29359929969567,
126.057309629066));
#126398=CARTESIAN_POINT('Ctrl Pts',(-207.629375715891,-1.42451776617409,
126.096926900948));
#126399=CARTESIAN_POINT('Ctrl Pts',(-207.636866051653,-1.55067701663124,
126.135103985207));
#126400=CARTESIAN_POINT('Ctrl Pts',(-207.644356387415,-1.67513922322726,
126.178307391138));
#126401=CARTESIAN_POINT('Ctrl Pts',(-207.651846723176,-1.79748764413635,
126.226345629421));
#126402=CARTESIAN_POINT('Ctrl Pts',(-207.659621346427,-1.92447966532862,
126.276207106413));
#126403=CARTESIAN_POINT('Ctrl Pts',(-207.667395969677,-2.0495965663628,
126.331435618184));
#126404=CARTESIAN_POINT('Ctrl Pts',(-207.675170592927,-2.17235138413133,
126.391870104674));
#126405=CARTESIAN_POINT('Ctrl Pts',(-207.68293556835,-2.29495387074919,
126.452229595697));
#126406=CARTESIAN_POINT('Ctrl Pts',(-207.690700543772,-2.41519975904507,
126.517782035912));
#126407=CARTESIAN_POINT('Ctrl Pts',(-207.698465519195,-2.53261992505663,
126.588317522707));
#126408=CARTESIAN_POINT('Ctrl Pts',(-207.706222716183,-2.64992246736666,
126.65878235175));
#126409=CARTESIAN_POINT('Ctrl Pts',(-207.71397991317,-2.7644045876617,126.734220093246));
#126410=CARTESIAN_POINT('Ctrl Pts',(-207.721737110158,-2.87562006548463,
126.814374113644));
#126411=CARTESIAN_POINT('Ctrl Pts',(-207.729795303405,-2.99115094782568,
126.89763828587));
#126412=CARTESIAN_POINT('Ctrl Pts',(-207.737853496653,-3.10315618232721,
126.985991940956));
#126413=CARTESIAN_POINT('Ctrl Pts',(-207.745911689901,-3.2111662156833,
127.07909625141));
#126414=CARTESIAN_POINT('Ctrl Pts',(-207.753659246585,-3.31501255320105,
127.168611469092));
#126415=CARTESIAN_POINT('Ctrl Pts',(-207.761406803268,-3.41516565824468,
127.262517606759));
#126416=CARTESIAN_POINT('Ctrl Pts',(-207.769154359952,-3.51124052762793,
127.360471388853));
#126417=CARTESIAN_POINT('Ctrl Pts',(-207.776900268185,-3.60729495512799,
127.458404329287));
#126418=CARTESIAN_POINT('Ctrl Pts',(-207.784646176418,-3.69927259997578,
127.560382921643));
#126419=CARTESIAN_POINT('Ctrl Pts',(-207.792392084651,-3.78682490105777,
127.666026627815));
#126420=CARTESIAN_POINT('Ctrl Pts',(-207.800138022213,-3.87437753365062,
127.771670733999));
#126421=CARTESIAN_POINT('Ctrl Pts',(-207.807883959776,-3.95750454018412,
127.880979680284));
#126422=CARTESIAN_POINT('Ctrl Pts',(-207.815629897339,-4.0358975446204,
127.993539728248));
#126423=CARTESIAN_POINT('Ctrl Pts',(-207.823377541653,-4.114307822298,128.106124577875));
#126424=CARTESIAN_POINT('Ctrl Pts',(-207.831125185968,-4.18798179960877,
128.221961633515));
#126425=CARTESIAN_POINT('Ctrl Pts',(-207.838872830283,-4.25665456438336,
128.340608401532));
#126426=CARTESIAN_POINT('Ctrl Pts',(-207.846627482129,-4.3253894417789,
128.459362482276));
#126427=CARTESIAN_POINT('Ctrl Pts',(-207.854382133974,-4.38911387975285,
128.580931010513));
#126428=CARTESIAN_POINT('Ctrl Pts',(-207.86213678582,-4.44760890967717,
128.704846852653));
#126429=CARTESIAN_POINT('Ctrl Pts',(-207.869895598211,-4.50613532350585,
128.82882917844));
#126430=CARTESIAN_POINT('Ctrl Pts',(-207.877654410602,-4.55942658739599,
128.955160967813));
#126431=CARTESIAN_POINT('Ctrl Pts',(-207.885413222994,-4.60731235870681,
129.083356291073));
#126432=CARTESIAN_POINT('Ctrl Pts',(-207.893181538738,-4.65525678273092,
129.21170863391));
#126433=CARTESIAN_POINT('Ctrl Pts',(-207.900949854483,-4.6977823753859,
129.34192869686));
#126434=CARTESIAN_POINT('Ctrl Pts',(-207.908718170227,-4.73476889932119,
129.473516324449));
#126435=CARTESIAN_POINT('Ctrl Pts',(-207.910856696188,-4.74495085435851,
129.50974085071));
#126436=CARTESIAN_POINT('Ctrl Pts',(-207.912995222148,-4.7547133384679,
129.546068962182));
#126437=CARTESIAN_POINT('Ctrl Pts',(-207.915133748109,-4.76405452823406,
129.582490119308));
#126438=CARTESIAN_POINT('Ctrl Pts',(-206.164998470905,-4.76405452823394,
129.582490119308));
#126439=CARTESIAN_POINT('Ctrl Pts',(-206.172665944474,-4.79776118631657,
129.713911867602));
#126440=CARTESIAN_POINT('Ctrl Pts',(-206.180333418043,-4.82600172992664,
129.846636618208));
#126441=CARTESIAN_POINT('Ctrl Pts',(-206.188000891612,-4.84869920343357,
129.980164586805));
#126442=CARTESIAN_POINT('Ctrl Pts',(-206.195857503673,-4.87195657008729,
130.116986375504));
#126443=CARTESIAN_POINT('Ctrl Pts',(-206.203714115733,-4.88939378574457,
130.254651075192));
#126444=CARTESIAN_POINT('Ctrl Pts',(-206.211570727794,-4.90098467145666,
130.392617599839));
#126445=CARTESIAN_POINT('Ctrl Pts',(-206.219427339854,-4.91257555716875,
130.530584124486));
#126446=CARTESIAN_POINT('Ctrl Pts',(-206.227283951915,-4.91832015787954,
130.668852025862));
#126447=CARTESIAN_POINT('Ctrl Pts',(-206.235140563975,-4.91824935292959,
130.806883494435));
#126448=CARTESIAN_POINT('',(-205.889859436046,-4.91824930584068,130.806973680448));
#126449=CARTESIAN_POINT('Ctrl Pts',(-205.820054717884,-4.76405452823395,
129.582490119308));
#126450=CARTESIAN_POINT('Ctrl Pts',(-205.827905852165,-4.79858606955834,
129.717128074842));
#126451=CARTESIAN_POINT('Ctrl Pts',(-205.835756986446,-4.82742791349959,
129.853316954026));
#126452=CARTESIAN_POINT('Ctrl Pts',(-205.843608120727,-4.85045202410955,
129.99054354702));
#126453=CARTESIAN_POINT('Ctrl Pts',(-205.851456131429,-4.87346697456125,
130.12771554432));
#126454=CARTESIAN_POINT('Ctrl Pts',(-205.859304142131,-4.8906687356244,
130.265924063211));
#126455=CARTESIAN_POINT('Ctrl Pts',(-205.867152152832,-4.9019802890764,
130.404645333887));
#126456=CARTESIAN_POINT('Ctrl Pts',(-205.87472124722,-4.91288983278145,
130.538436485711));
#126457=CARTESIAN_POINT('Ctrl Pts',(-205.882290341607,-4.91832064309359,
130.672704230441));
#126458=CARTESIAN_POINT('Ctrl Pts',(-205.889859435995,-4.91824930584116,
130.806973679544));
#126459=CARTESIAN_POINT('Ctrl Pts',(-205.889859436046,-4.91824930584068,
130.806973680447));
#126460=CARTESIAN_POINT('Ctrl Pts',(-205.898419073697,-4.91816863288146,
130.958814544507));
#126461=CARTESIAN_POINT('Ctrl Pts',(-205.906978711349,-4.91105222461682,
131.11040905316));
#126462=CARTESIAN_POINT('Ctrl Pts',(-205.915538349,-4.89699280558849,131.261136847809));
#126463=CARTESIAN_POINT('Ctrl Pts',(-205.924144711242,-4.88285664025042,
131.412687421976));
#126464=CARTESIAN_POINT('Ctrl Pts',(-205.932751073485,-4.86170154469193,
131.563361562213));
#126465=CARTESIAN_POINT('Ctrl Pts',(-205.941357435727,-4.8336719627189,
131.712544750507));
#126466=CARTESIAN_POINT('Ctrl Pts',(-205.949987994199,-4.80556357739427,
131.862147357658));
#126467=CARTESIAN_POINT('Ctrl Pts',(-205.95861855267,-4.77054211518795,
132.010250401408));
#126468=CARTESIAN_POINT('Ctrl Pts',(-205.967249111142,-4.72880199806623,
132.15625363315));
#126469=CARTESIAN_POINT('Ctrl Pts',(-205.975911032462,-4.68691020026427,
132.302787430473));
#126470=CARTESIAN_POINT('Ctrl Pts',(-205.984572953782,-4.63825094856085,
132.447205915682));
#126471=CARTESIAN_POINT('Ctrl Pts',(-205.993234875102,-4.58306805029199,
132.588925076725));
#126472=CARTESIAN_POINT('Ctrl Pts',(-205.995739908888,-4.5671091169981,
132.629910358551));
#126473=CARTESIAN_POINT('Ctrl Pts',(-205.998244942673,-4.55060485959071,
132.67067003316));
#126474=CARTESIAN_POINT('Ctrl Pts',(-206.000749976459,-4.53356188569129,
132.711190366418));
#126475=CARTESIAN_POINT('Ctrl Pts',(-206.008524310578,-4.48066927631869,
132.836944602228));
#126476=CARTESIAN_POINT('Ctrl Pts',(-206.016298644698,-4.42245657148283,
132.960695612929));
#126477=CARTESIAN_POINT('Ctrl Pts',(-206.024072978817,-4.35909645044119,
133.081960494246));
#126478=CARTESIAN_POINT('Ctrl Pts',(-206.031837731764,-4.29581441508608,
133.203075927434));
#126479=CARTESIAN_POINT('Ctrl Pts',(-206.039602484712,-4.22739776497256,
133.321710984359));
#126480=CARTESIAN_POINT('Ctrl Pts',(-206.047367237659,-4.15406757846652,
133.437401752078));
#126481=CARTESIAN_POINT('Ctrl Pts',(-206.055124278544,-4.0808102245355,
133.552977614096));
#126482=CARTESIAN_POINT('Ctrl Pts',(-206.06288131943,-4.00264925397073,
133.665614678334));
#126483=CARTESIAN_POINT('Ctrl Pts',(-206.070638360315,-3.91985191488636,
133.774873035965));
#126484=CARTESIAN_POINT('Ctrl Pts',(-206.078389551555,-3.83711701391935,
133.884049001019));
#126485=CARTESIAN_POINT('Ctrl Pts',(-206.086140742796,-3.7497529388275,
133.989851020585));
#126486=CARTESIAN_POINT('Ctrl Pts',(-206.093891934036,-3.65807035220528,
134.091867934792));
#126487=CARTESIAN_POINT('Ctrl Pts',(-206.101639830814,-3.5664267331282,
134.193841489089));
#126488=CARTESIAN_POINT('Ctrl Pts',(-206.109387727591,-3.47046851394157,
134.292032847568));
#126489=CARTESIAN_POINT('Ctrl Pts',(-206.117135624368,-3.37054661931243,
134.386063920401));
#126490=CARTESIAN_POINT('Ctrl Pts',(-206.124881900453,-3.2706456261893,
134.480075323962));
#126491=CARTESIAN_POINT('Ctrl Pts',(-206.132628176537,-3.16678289131879,
134.569927905073));
#126492=CARTESIAN_POINT('Ctrl Pts',(-206.140374452621,-3.0593458918801,
134.655280738308));
#126493=CARTESIAN_POINT('Ctrl Pts',(-206.148120785887,-2.95190809936603,
134.740634201599));
#126494=CARTESIAN_POINT('Ctrl Pts',(-206.155867119153,-2.84089629575584,
134.821487607538));
#126495=CARTESIAN_POINT('Ctrl Pts',(-206.163613452418,-2.72673037768329,
134.897540861572));
#126496=CARTESIAN_POINT('Ctrl Pts',(-206.171361520422,-2.61253889294479,
134.973611147205));
#126497=CARTESIAN_POINT('Ctrl Pts',(-206.179109588425,-2.49519221352086,
135.044878925172));
#126498=CARTESIAN_POINT('Ctrl Pts',(-206.186857656428,-2.37513814799737,
135.11108812699));
#126499=CARTESIAN_POINT('Ctrl Pts',(-206.19461395917,-2.25495648758455,
135.177367696735));
#126500=CARTESIAN_POINT('Ctrl Pts',(-206.202370261912,-2.13206203597101,
135.238577761457));
#126501=CARTESIAN_POINT('Ctrl Pts',(-206.210126564654,-2.00692657135467,
135.294508588367));
#126502=CARTESIAN_POINT('Ctrl Pts',(-206.217887007169,-1.88172431817278,
135.350469267244));
#126503=CARTESIAN_POINT('Ctrl Pts',(-206.225647449683,-1.75427903178613,
135.401144949441));
#126504=CARTESIAN_POINT('Ctrl Pts',(-206.233407892198,-1.6250803440804,
135.446374936564));
#126505=CARTESIAN_POINT('Ctrl Pts',(-206.241180792463,-1.49567425517145,
135.491677530877));
#126506=CARTESIAN_POINT('Ctrl Pts',(-206.248953692729,-1.36450951455032,
135.531516847299));
#126507=CARTESIAN_POINT('Ctrl Pts',(-206.256726592995,-1.23208958293334,
135.565782497858));
#126508=CARTESIAN_POINT('Ctrl Pts',(-206.264216928754,-1.10448344942972,
135.598802505697));
#126509=CARTESIAN_POINT('Ctrl Pts',(-206.271707264513,-0.975712100315515,
135.626646980716));
#126510=CARTESIAN_POINT('Ctrl Pts',(-206.279197600272,-0.846231065683617,
135.649262685304));
#126511=CARTESIAN_POINT('Ctrl Pts',(-206.286971934391,-0.711840718217051,
135.672735871215));
#126512=CARTESIAN_POINT('Ctrl Pts',(-206.29474626851,-0.576260099220195,
135.690650318037));
#126513=CARTESIAN_POINT('Ctrl Pts',(-206.302520602629,-0.439988827093508,
135.702890284163));
#126514=CARTESIAN_POINT('Ctrl Pts',(-206.310285355577,-0.303885497130804,
135.715115165626));
#126515=CARTESIAN_POINT('Ctrl Pts',(-206.318050108524,-0.16709359326881,
135.721679446316));
#126516=CARTESIAN_POINT('Ctrl Pts',(-206.325814861471,-0.030122916862644,
135.722518369446));
#126517=CARTESIAN_POINT('Ctrl Pts',(-206.333571902356,0.106711718336767,
135.723356459347));
#126518=CARTESIAN_POINT('Ctrl Pts',(-206.341328943241,0.243724384301109,
135.718480505712));
#126519=CARTESIAN_POINT('Ctrl Pts',(-206.349085984126,0.380400519141976,
135.707877570482));
#126520=CARTESIAN_POINT('Ctrl Pts',(-206.356837175366,0.516973585446189,
135.697282631009));
#126521=CARTESIAN_POINT('Ctrl Pts',(-206.364588366606,0.653210237545264,
135.68096933629));
#126522=CARTESIAN_POINT('Ctrl Pts',(-206.372339557846,0.78859663427342,
135.658976813612));
#126523=CARTESIAN_POINT('Ctrl Pts',(-206.380087454624,0.9239254881716,135.636993638342));
#126524=CARTESIAN_POINT('Ctrl Pts',(-206.387835351401,1.0584044203597,135.60933609858));
#126525=CARTESIAN_POINT('Ctrl Pts',(-206.395583248178,1.19152564980452,
135.576095070399));
#126526=CARTESIAN_POINT('Ctrl Pts',(-206.403329524262,1.3246190331579,135.542860995525));
#126527=CARTESIAN_POINT('Ctrl Pts',(-206.411075800346,1.45635489958587,
135.504045849998));
#126528=CARTESIAN_POINT('Ctrl Pts',(-206.41882207643,1.58623697799247,135.459791350823));
#126529=CARTESIAN_POINT('Ctrl Pts',(-206.426568409696,1.71612001515889,
135.41553652497));
#126530=CARTESIAN_POINT('Ctrl Pts',(-206.434314742961,1.84414886692504,
135.365842391443));
#126531=CARTESIAN_POINT('Ctrl Pts',(-206.442061076226,1.96984409085683,
135.310900012736));
#126532=CARTESIAN_POINT('Ctrl Pts',(-206.449809144229,2.09556746336268,
135.255945330063));
#126533=CARTESIAN_POINT('Ctrl Pts',(-206.457557212232,2.21895580995249,
135.195740220041));
#126534=CARTESIAN_POINT('Ctrl Pts',(-206.465305280235,2.33955164148073,
135.130523025445));
#126535=CARTESIAN_POINT('Ctrl Pts',(-206.473061582977,2.46027564369365,
135.065236517239));
#126536=CARTESIAN_POINT('Ctrl Pts',(-206.480817885719,2.57820085766173,
134.99492746967));
#126537=CARTESIAN_POINT('Ctrl Pts',(-206.488574188461,2.69289582161183,
134.919879437405));
#126538=CARTESIAN_POINT('Ctrl Pts',(-206.496334630975,2.80765200171758,
134.844791349744));
#126539=CARTESIAN_POINT('Ctrl Pts',(-206.504095073489,2.91917417867433,
134.764959464925));
#126540=CARTESIAN_POINT('Ctrl Pts',(-206.511855516003,3.02706249437732,
134.68070886271));
#126541=CARTESIAN_POINT('Ctrl Pts',(-206.519628416269,3.13512400198284,
134.59632301395));
#126542=CARTESIAN_POINT('Ctrl Pts',(-206.527401316534,3.23953969337777,
134.507504526547));
#126543=CARTESIAN_POINT('Ctrl Pts',(-206.5351742168,3.33994456322253,134.414617308869));
#126544=CARTESIAN_POINT('Ctrl Pts',(-206.542664552561,3.43669946314165,
134.325106775525));
#126545=CARTESIAN_POINT('Ctrl Pts',(-206.550154888323,3.52972986821838,
134.231818411375));
#126546=CARTESIAN_POINT('Ctrl Pts',(-206.557645224085,3.61874476299928,
134.13510669056));
#126547=CARTESIAN_POINT('Ctrl Pts',(-206.565419558204,3.71113468457249,
134.034728115454));
#126548=CARTESIAN_POINT('Ctrl Pts',(-206.573193892323,3.79949125235512,
133.930343496942));
#126549=CARTESIAN_POINT('Ctrl Pts',(-206.580968226442,3.88344703370601,
133.82231061697));
#126550=CARTESIAN_POINT('Ctrl Pts',(-206.588732979389,3.9672993470595,133.714410877866));
#126551=CARTESIAN_POINT('Ctrl Pts',(-206.596497732336,4.04676142767885,
133.602872129055));
#126552=CARTESIAN_POINT('Ctrl Pts',(-206.604262485283,4.12150323375985,
133.488088278229));
#126553=CARTESIAN_POINT('Ctrl Pts',(-206.612019526168,4.19617080522537,
133.373418432341));
#126554=CARTESIAN_POINT('Ctrl Pts',(-206.619776567053,4.2661272200117,133.255510224025));
#126555=CARTESIAN_POINT('Ctrl Pts',(-206.627533607938,4.33108345969385,
133.134789575433));
#126556=CARTESIAN_POINT('Ctrl Pts',(-206.635284799178,4.39599071537045,
133.014159963221));
#126557=CARTESIAN_POINT('Ctrl Pts',(-206.643035990418,4.45590511673205,
132.890722475119));
#126558=CARTESIAN_POINT('Ctrl Pts',(-206.650787181658,4.51058183897033,
132.764930569506));
#126559=CARTESIAN_POINT('Ctrl Pts',(-206.658535078435,4.56523532214318,
132.639192128808));
#126560=CARTESIAN_POINT('Ctrl Pts',(-206.666282975212,4.61465539831717,
132.511101618704));
#126561=CARTESIAN_POINT('Ctrl Pts',(-206.674030871989,4.65864405605593,
132.381135370495));
#126562=CARTESIAN_POINT('Ctrl Pts',(-206.681777148073,4.70262351231578,
132.251196308424));
#126563=CARTESIAN_POINT('Ctrl Pts',(-206.689523424157,4.74117368471374,
132.119382658775));
#126564=CARTESIAN_POINT('Ctrl Pts',(-206.697269700241,4.77414555713005,
131.986188549981));
#126565=CARTESIAN_POINT('Ctrl Pts',(-206.705016033506,4.80711767293719,
131.852993457978));
#126566=CARTESIAN_POINT('Ctrl Pts',(-206.712762366772,4.83451131264874,
131.718418266004));
#126567=CARTESIAN_POINT('Ctrl Pts',(-206.720508700037,4.8562280722051,131.582969616504));
#126568=CARTESIAN_POINT('Ctrl Pts',(-206.72825676804,4.87794969507915,131.447490634218));
#126569=CARTESIAN_POINT('Ctrl Pts',(-206.736004836043,4.89399184618037,
131.311138191135));
#126570=CARTESIAN_POINT('Ctrl Pts',(-206.743752904046,4.90430776597871,
131.174426015923));
#126571=CARTESIAN_POINT('Ctrl Pts',(-206.751509206787,4.91463464965938,
131.037568541384));
#126572=CARTESIAN_POINT('Ctrl Pts',(-206.759265509529,4.91922311531838,
130.900350961453));
#126573=CARTESIAN_POINT('Ctrl Pts',(-206.767021812271,4.91807850989876,
130.763289545363));
#126574=CARTESIAN_POINT('Ctrl Pts',(-206.774782254785,4.91693329356877,
130.626154975468));
#126575=CARTESIAN_POINT('Ctrl Pts',(-206.782542697299,4.91004892864024,
130.489177125775));
#126576=CARTESIAN_POINT('Ctrl Pts',(-206.790303139813,4.89748278085339,
130.352868121787));
#126577=CARTESIAN_POINT('Ctrl Pts',(-206.798076040079,4.88489646077053,
130.216340302485));
#126578=CARTESIAN_POINT('Ctrl Pts',(-206.805848940344,4.86661018354394,
130.080483862156));
#126579=CARTESIAN_POINT('Ctrl Pts',(-206.813621840609,4.84273282128629,
129.945802591492));
#126580=CARTESIAN_POINT('Ctrl Pts',(-206.821112176372,4.81972346128801,
129.816017324245));
#126581=CARTESIAN_POINT('Ctrl Pts',(-206.828602512135,4.79152252480077,
129.687323570165));
#126582=CARTESIAN_POINT('Ctrl Pts',(-206.836092847897,4.75827093999596,
129.560157770724));
#126583=CARTESIAN_POINT('Ctrl Pts',(-206.843867182016,4.72375861124946,
129.428170441356));
#126584=CARTESIAN_POINT('Ctrl Pts',(-206.851641516135,4.68369575848463,
129.29741112245));
#126585=CARTESIAN_POINT('Ctrl Pts',(-206.859415850255,4.63818478746673,
129.168382335371));
#126586=CARTESIAN_POINT('Ctrl Pts',(-206.867180603202,4.59272990465331,
129.039512564742));
#126587=CARTESIAN_POINT('Ctrl Pts',(-206.874945356149,4.54184039188006,
128.912369447615));
#126588=CARTESIAN_POINT('Ctrl Pts',(-206.882710109096,4.4856692591883,128.787443574236));
#126589=CARTESIAN_POINT('Ctrl Pts',(-206.890467149981,4.42955391645741,
128.662641778997));
#126590=CARTESIAN_POINT('Ctrl Pts',(-206.898224190866,4.36816755243845,
128.540053199304));
#126591=CARTESIAN_POINT('Ctrl Pts',(-206.905981231751,4.30171228598306,
128.420151215873));
#126592=CARTESIAN_POINT('Ctrl Pts',(-206.913732422991,4.23530713396096,
128.300339651459));
#126593=CARTESIAN_POINT('Ctrl Pts',(-206.921483614231,4.16384087671486,
128.183210991282));
#126594=CARTESIAN_POINT('Ctrl Pts',(-206.929234805471,4.08756268783238,
128.069216318714));
#126595=CARTESIAN_POINT('Ctrl Pts',(-206.936982702249,4.01131691921485,
127.955270096924));
#126596=CARTESIAN_POINT('Ctrl Pts',(-206.944730599026,3.93026350367536,
127.844455537692));
#126597=CARTESIAN_POINT('Ctrl Pts',(-206.952478495803,3.844696162211,127.737196702354));
#126598=CARTESIAN_POINT('Ctrl Pts',(-206.960224771887,3.75914671958986,
127.629960303251));
#126599=CARTESIAN_POINT('Ctrl Pts',(-206.967971047971,3.66908547280403,
127.526278454052));
#126600=CARTESIAN_POINT('Ctrl Pts',(-206.975717324055,3.5748475992442,127.426543614726));
#126601=CARTESIAN_POINT('Ctrl Pts',(-206.983463657321,3.48060903004192,
127.326808039179));
#126602=CARTESIAN_POINT('Ctrl Pts',(-206.991209990586,3.38219404105675,
127.231019815818));
#126603=CARTESIAN_POINT('Ctrl Pts',(-206.998956323851,3.27997569512705,
127.13953558738));
#126604=CARTESIAN_POINT('Ctrl Pts',(-207.006704391854,3.17773445810738,
127.048030871684));
#126605=CARTESIAN_POINT('Ctrl Pts',(-207.014452459857,3.07168846055954,
126.960832329545));
#126606=CARTESIAN_POINT('Ctrl Pts',(-207.022200527861,2.96224464229277,
126.878256983974));
#126607=CARTESIAN_POINT('Ctrl Pts',(-207.029956830602,2.85268450583369,
126.795593876342));
#126608=CARTESIAN_POINT('Ctrl Pts',(-207.037713133344,2.73971964740064,
126.717564016553));
#126609=CARTESIAN_POINT('Ctrl Pts',(-207.045469436086,2.62378730907338,
126.644441962202));
#126610=CARTESIAN_POINT('Ctrl Pts',(-207.0532298786,2.50779309416619,126.571280880408));
#126611=CARTESIAN_POINT('Ctrl Pts',(-207.060990321115,2.38882858239987,
126.50303301797));
#126612=CARTESIAN_POINT('Ctrl Pts',(-207.068750763629,2.26735564704684,
126.439926927807));
#126613=CARTESIAN_POINT('Ctrl Pts',(-207.076523663894,2.14568771255446,
126.376719534146));
#126614=CARTESIAN_POINT('Ctrl Pts',(-207.08429656416,2.02150366214178,126.318670572596));
#126615=CARTESIAN_POINT('Ctrl Pts',(-207.092069464425,1.89528619722091,
126.265960757139));
#126616=CARTESIAN_POINT('Ctrl Pts',(-207.099559800187,1.77365705507833,
126.215167076244));
#126617=CARTESIAN_POINT('Ctrl Pts',(-207.107050135949,1.65014005997225,
126.16933120521));
#126618=CARTESIAN_POINT('Ctrl Pts',(-207.11454047171,1.52517857759403,126.12857048445));
#126619=CARTESIAN_POINT('Ctrl Pts',(-207.122314805829,1.39547914262526,
126.086264308572));
#126620=CARTESIAN_POINT('Ctrl Pts',(-207.130089139948,1.26381267382523,
126.049291715399));
#126621=CARTESIAN_POINT('Ctrl Pts',(-207.137863474068,1.13065730947015,
126.017838173135));
#126622=CARTESIAN_POINT('Ctrl Pts',(-207.145628227015,0.997666047201566,
125.986423394551));
#126623=CARTESIAN_POINT('Ctrl Pts',(-207.153392979962,0.863189917184256,
125.960514222462));
#126624=CARTESIAN_POINT('Ctrl Pts',(-207.161157732909,0.727724372552056,
125.9402471012));
#126625=CARTESIAN_POINT('Ctrl Pts',(-207.168914773794,0.592393374208515,
125.920000109528));
#126626=CARTESIAN_POINT('Ctrl Pts',(-207.176671814678,0.45607530102819,
125.905384074413));
#126627=CARTESIAN_POINT('Ctrl Pts',(-207.184428855563,0.319277671788742,
125.896484821379));
#126628=CARTESIAN_POINT('Ctrl Pts',(-207.192180046803,0.182583202705448,
125.887592279341));
#126629=CARTESIAN_POINT('Ctrl Pts',(-207.199931238044,0.0454102859413843,
125.884407963739));
#126630=CARTESIAN_POINT('Ctrl Pts',(-207.207682429284,-0.0917268848740953,
125.886966059358));
#126631=CARTESIAN_POINT('Ctrl Pts',(-207.215430326061,-0.228805768733537,
125.889523067719));
#126632=CARTESIAN_POINT('Ctrl Pts',(-207.223178222838,-0.365848546783255,
125.897817625703));
#126633=CARTESIAN_POINT('Ctrl Pts',(-207.230926119615,-0.502339680839985,
125.911831833026));
#126634=CARTESIAN_POINT('Ctrl Pts',(-207.238672395699,-0.638802263893879,
125.925843108879));
#126635=CARTESIAN_POINT('Ctrl Pts',(-207.246418671783,-0.774713043801706,
125.945571614404));
#126636=CARTESIAN_POINT('Ctrl Pts',(-207.254164947867,-0.909560661310067,
125.970947489569));
#126637=CARTESIAN_POINT('Ctrl Pts',(-207.261911281132,-1.04440927423309,
125.996323552053));
#126638=CARTESIAN_POINT('Ctrl Pts',(-207.269657614397,-1.17819432487519,
126.027346995058));
#126639=CARTESIAN_POINT('Ctrl Pts',(-207.277403947663,-1.3104141100234,
126.063896724364));
#126640=CARTESIAN_POINT('Ctrl Pts',(-207.285152015665,-1.44266350487555,
126.100454638729));
#126641=CARTESIAN_POINT('Ctrl Pts',(-207.292900083668,-1.57334655995862,
126.142541197874));
#126642=CARTESIAN_POINT('Ctrl Pts',(-207.300648151671,-1.70197659392866,
126.189985390494));
#126643=CARTESIAN_POINT('Ctrl Pts',(-207.308404454413,-1.8307433374297,
126.237480007366));
#126644=CARTESIAN_POINT('Ctrl Pts',(-207.316160757155,-1.95745233369282,
126.290343496894));
#126645=CARTESIAN_POINT('Ctrl Pts',(-207.323917059897,-2.08163624961235,
126.348356400019));
#126646=CARTESIAN_POINT('Ctrl Pts',(-207.331677502411,-2.20588644622692,
126.406400266377));
#126647=CARTESIAN_POINT('Ctrl Pts',(-207.339437944925,-2.32760853025468,
126.469598842679));
#126648=CARTESIAN_POINT('Ctrl Pts',(-207.347198387439,-2.44636055986463,
126.537687080296));
#126649=CARTESIAN_POINT('Ctrl Pts',(-207.354971287704,-2.56530322077482,
126.605884619197));
#126650=CARTESIAN_POINT('Ctrl Pts',(-207.36274418797,-2.68126596877018,
126.67898729624));
#126651=CARTESIAN_POINT('Ctrl Pts',(-207.370517088235,-2.79383585215566,
126.756686681376));
#126652=CARTESIAN_POINT('Ctrl Pts',(-207.378007423998,-2.90231353674432,
126.831561498158));
#126653=CARTESIAN_POINT('Ctrl Pts',(-207.38549775976,-3.00764050612485,
126.910704436435));
#126654=CARTESIAN_POINT('Ctrl Pts',(-207.392988095523,-3.10947838849646,
126.993805905457));
#126655=CARTESIAN_POINT('Ctrl Pts',(-207.400656660266,-3.21373945489434,
127.078884734452));
#126656=CARTESIAN_POINT('Ctrl Pts',(-207.40832522501,-3.31469263021925,
127.168398207827));
#126657=CARTESIAN_POINT('Ctrl Pts',(-207.415993789753,-3.41192943455653,
127.262056198673));
#126658=CARTESIAN_POINT('Ctrl Pts',(-207.423653568804,-3.50905483699829,
127.355606887786));
#126659=CARTESIAN_POINT('Ctrl Pts',(-207.431313347855,-3.60247204570966,
127.453292379642));
#126660=CARTESIAN_POINT('Ctrl Pts',(-207.438973126906,-3.69180383118984,
127.554781024063));
#126661=CARTESIAN_POINT('Ctrl Pts',(-207.446625896291,-3.78105386678786,
127.656176793538));
#126662=CARTESIAN_POINT('Ctrl Pts',(-207.454278665675,-3.86622564885268,
127.761368495727));
#126663=CARTESIAN_POINT('Ctrl Pts',(-207.461931435059,-3.946977576186,127.869986565816));
#126664=CARTESIAN_POINT('Ctrl Pts',(-207.469578964315,-4.02767420974882,
127.978530261176));
#126665=CARTESIAN_POINT('Ctrl Pts',(-207.477226493571,-4.10395676880122,
128.090495336564));
#126666=CARTESIAN_POINT('Ctrl Pts',(-207.484874022827,-4.17552322907947,
128.205478391316));
#126667=CARTESIAN_POINT('Ctrl Pts',(-207.49251889284,-4.24706480385526,
128.320421463497));
#126668=CARTESIAN_POINT('Ctrl Pts',(-207.500163762853,-4.31389332535797,
128.438380089298));
#126669=CARTESIAN_POINT('Ctrl Pts',(-207.507808632866,-4.37574973386624,
128.558921389025));
#126670=CARTESIAN_POINT('Ctrl Pts',(-207.515451815557,-4.4375924898678,
128.679436083734));
#126671=CARTESIAN_POINT('Ctrl Pts',(-207.523094998249,-4.49446513553793,
128.802531958918));
#126672=CARTESIAN_POINT('Ctrl Pts',(-207.53073818094,-4.54615461705261,
128.927751638489));
#126673=CARTESIAN_POINT('Ctrl Pts',(-207.538383674744,-4.59785972820617,
129.053009181439));
#126674=CARTESIAN_POINT('Ctrl Pts',(-207.546029168548,-4.64437838974133,
129.180391439886));
#126675=CARTESIAN_POINT('Ctrl Pts',(-207.553674662351,-4.68554579883754,
129.309421277828));
#126676=CARTESIAN_POINT('Ctrl Pts',(-207.559023655253,-4.71434762441938,
129.399694019515));
#126677=CARTESIAN_POINT('Ctrl Pts',(-207.564372648154,-4.74053114460319,
129.490772803549));
#126678=CARTESIAN_POINT('Ctrl Pts',(-207.569721641055,-4.76405452823393,
129.582490119308));
#126679=CARTESIAN_POINT('Origin',(213.235140564004,0.,130.804360617566));
#126680=CARTESIAN_POINT('',(-209.665424299527,-4.76405452823394,129.582490119308));
#126681=CARTESIAN_POINT('',(-209.319824802869,-4.76405452823399,129.582490119308));
#126682=CARTESIAN_POINT('',(213.235140564004,-4.76405452823405,129.582490119308));
#126683=CARTESIAN_POINT('',(-207.985140564043,-4.91824805552431,130.799987194266));
#126684=CARTESIAN_POINT('Ctrl Pts',(-207.985140564043,-4.91824805552431,
130.799987194267));
#126685=CARTESIAN_POINT('Ctrl Pts',(-207.992788080768,-4.91836794557653,
130.93481270186));
#126686=CARTESIAN_POINT('Ctrl Pts',(-208.000435597493,-4.91293964861326,
131.069820827236));
#126687=CARTESIAN_POINT('Ctrl Pts',(-208.008083114218,-4.90194487473793,
131.204509974095));
#126688=CARTESIAN_POINT('Ctrl Pts',(-208.015724146108,-4.89095942405694,
131.339084909138));
#126689=CARTESIAN_POINT('Ctrl Pts',(-208.023365177999,-4.87441691822112,
131.473341003815));
#126690=CARTESIAN_POINT('Ctrl Pts',(-208.03100620989,-4.85235112844437,
131.606776712111));
#126691=CARTESIAN_POINT('Ctrl Pts',(-208.038643191443,-4.83029703524341,
131.740141689157));
#126692=CARTESIAN_POINT('Ctrl Pts',(-208.046280172995,-4.8027255454322,
131.872686747673));
#126693=CARTESIAN_POINT('Ctrl Pts',(-208.053917154548,-4.76972222154673,
132.003915948421));
#126694=CARTESIAN_POINT('Ctrl Pts',(-208.06155211758,-4.73672762072607,
132.135110464153));
#126695=CARTESIAN_POINT('Ctrl Pts',(-208.069187080612,-4.69830413812791,
132.264989422662));
#126696=CARTESIAN_POINT('Ctrl Pts',(-208.076822043645,-4.6545882427032,
132.393068064955));
#126697=CARTESIAN_POINT('Ctrl Pts',(-208.084456753798,-4.61087379520155,
132.52114246513));
#126698=CARTESIAN_POINT('Ctrl Pts',(-208.092091463951,-4.56186741386925,
132.647416285964));
#126699=CARTESIAN_POINT('Ctrl Pts',(-208.099726174104,-4.50775496015573,
132.771421440645));
#126700=CARTESIAN_POINT('Ctrl Pts',(-208.107362396608,-4.45363178736365,
132.895451159376));
#126701=CARTESIAN_POINT('Ctrl Pts',(-208.114998619113,-4.39440069272263,
133.017210948925));
#126702=CARTESIAN_POINT('Ctrl Pts',(-208.122634841618,-4.33029480919843,
133.13625468204));
#126703=CARTESIAN_POINT('Ctrl Pts',(-208.130278840718,-4.26612364136049,
133.255419647217));
#126704=CARTESIAN_POINT('Ctrl Pts',(-208.137922839819,-4.19706796319404,
133.371862677257));
#126705=CARTESIAN_POINT('Ctrl Pts',(-208.145566838919,-4.12340598189315,
133.485163887295));
#126706=CARTESIAN_POINT('Ctrl Pts',(-208.153214944412,-4.04970442903014,
133.598525963275));
#126707=CARTESIAN_POINT('Ctrl Pts',(-208.160863049905,-3.97139187990211,
133.708742530803));
#126708=CARTESIAN_POINT('Ctrl Pts',(-208.168511155397,-3.88878784192218,
133.815425575852));
#126709=CARTESIAN_POINT('Ctrl Pts',(-208.176170926514,-3.80605780834674,
133.922271344106));
#126710=CARTESIAN_POINT('Ctrl Pts',(-208.18383069763,-3.71902347321935,
134.025572518618));
#126711=CARTESIAN_POINT('Ctrl Pts',(-208.191490468746,-3.62804267754195,
134.124976432808));
#126712=CARTESIAN_POINT('Ctrl Pts',(-208.197240969432,-3.55973970608588,
134.199602980784));
#126713=CARTESIAN_POINT('Ctrl Pts',(-208.202991470117,-3.48921325557276,
134.272033733371));
#126714=CARTESIAN_POINT('Ctrl Pts',(-208.208741970803,-3.4166267967544,
134.342134549603));
#126715=CARTESIAN_POINT('Ctrl Pts',(-208.216516304922,-3.31849423156944,
134.436906674189));
#126716=CARTESIAN_POINT('Ctrl Pts',(-208.224290639041,-3.21625998725054,
134.527742740487));
#126717=CARTESIAN_POINT('Ctrl Pts',(-208.23206497316,-3.1102729253396,134.614266835887));
#126718=CARTESIAN_POINT('Ctrl Pts',(-208.239829726106,-3.00441648301042,
134.700684298072));
#126719=CARTESIAN_POINT('Ctrl Pts',(-208.247594479054,-2.89481672543764,
134.782800118));
#126720=CARTESIAN_POINT('Ctrl Pts',(-208.255359232,-2.78185952678535,134.860274896213));
#126721=CARTESIAN_POINT('Ctrl Pts',(-208.263116272885,-2.66901451881519,
134.937672725384));
#126722=CARTESIAN_POINT('Ctrl Pts',(-208.27087331377,-2.55281902621447,
135.010438466342));
#126723=CARTESIAN_POINT('Ctrl Pts',(-208.278630354655,-2.43369191283578,
135.078272962935));
#126724=CARTESIAN_POINT('Ctrl Pts',(-208.286381545895,-2.31465463414012,
135.146056305006));
#126725=CARTESIAN_POINT('Ctrl Pts',(-208.294132737135,-2.19269047341665,
135.20891561186));
#126726=CARTESIAN_POINT('Ctrl Pts',(-208.301883928375,-2.06824688333898,
135.266595247441));
#126727=CARTESIAN_POINT('Ctrl Pts',(-208.309631825152,-1.94385618510623,
135.324250367639));
#126728=CARTESIAN_POINT('Ctrl Pts',(-208.317379721929,-1.81698850746676,
135.37673003111));
#126729=CARTESIAN_POINT('Ctrl Pts',(-208.325127618706,-1.68811529282284,
135.423824852803));
#126730=CARTESIAN_POINT('Ctrl Pts',(-208.33287389479,-1.55926903567759,
135.470909823275));
#126731=CARTESIAN_POINT('Ctrl Pts',(-208.340620170874,-1.4284184429477,
135.512612058317));
#126732=CARTESIAN_POINT('Ctrl Pts',(-208.348366446958,-1.29605392479125,
135.548770727004));
#126733=CARTESIAN_POINT('Ctrl Pts',(-208.356112780224,-1.16368842954982,
135.584929662605));
#126734=CARTESIAN_POINT('Ctrl Pts',(-208.363859113489,-1.0298093637282,
135.615544847168));
#126735=CARTESIAN_POINT('Ctrl Pts',(-208.371605446754,-0.894920862442862,
135.64050574695));
#126736=CARTESIAN_POINT('Ctrl Pts',(-208.379353514757,-0.760002153813462,
135.665472236552));
#126737=CARTESIAN_POINT('Ctrl Pts',(-208.38710158276,-0.624073944259812,
135.684781850579));
#126738=CARTESIAN_POINT('Ctrl Pts',(-208.394849650763,-0.487648692408282,
135.698375514896));
#126739=CARTESIAN_POINT('Ctrl Pts',(-208.402605953505,-0.351078446175044,
135.711983626722));
#126740=CARTESIAN_POINT('Ctrl Pts',(-208.410362256246,-0.214010492041764,
135.719863614585));
#126741=CARTESIAN_POINT('Ctrl Pts',(-208.418118558988,-0.0769610788796258,
135.72200843485));
#126742=CARTESIAN_POINT('Ctrl Pts',(-208.425879001502,0.0601614816807967,
135.724154399871));
#126743=CARTESIAN_POINT('Ctrl Pts',(-208.433639444016,0.197265090912087,
135.720559108173));
#126744=CARTESIAN_POINT('Ctrl Pts',(-208.44139988653,0.333836394172614,
135.711267619377));
#126745=CARTESIAN_POINT('Ctrl Pts',(-208.449172786796,0.470626933813368,
135.701961215059));
#126746=CARTESIAN_POINT('Ctrl Pts',(-208.456945687061,0.606883071075844,
135.6869403838));
#126747=CARTESIAN_POINT('Ctrl Pts',(-208.464718587327,0.742098547718523,
135.666301876772));
#126748=CARTESIAN_POINT('Ctrl Pts',(-208.47220892309,0.872398601215581,
135.646413631458));
#126749=CARTESIAN_POINT('Ctrl Pts',(-208.479699258852,1.00173203939671,
135.621309111393));
#126750=CARTESIAN_POINT('Ctrl Pts',(-208.487189594615,1.12965916458491,
135.591118730775));
#126751=CARTESIAN_POINT('Ctrl Pts',(-208.494963928734,1.26243668558986,
135.559783672703));
#126752=CARTESIAN_POINT('Ctrl Pts',(-208.502738262854,1.39411974704277,
135.522870220161));
#126753=CARTESIAN_POINT('Ctrl Pts',(-208.510512596973,1.52420351483378,
135.480468690298));
#126754=CARTESIAN_POINT('Ctrl Pts',(-208.51827734992,1.65412696600691,135.438119416531));
#126755=CARTESIAN_POINT('Ctrl Pts',(-208.526042102867,1.78245467704559,
135.39029564292));
#126756=CARTESIAN_POINT('Ctrl Pts',(-208.533806855814,1.90869252716161,
135.33713856263));
#126757=CARTESIAN_POINT('Ctrl Pts',(-208.541563896699,2.03480499606526,
135.284034278702));
#126758=CARTESIAN_POINT('Ctrl Pts',(-208.549320937584,2.15883137675045,
135.225607380339));
#126759=CARTESIAN_POINT('Ctrl Pts',(-208.557077978469,2.28029357453021,
135.162048568356));
#126760=CARTESIAN_POINT('Ctrl Pts',(-208.564829169709,2.40166417672196,
135.098537686567));
#126761=CARTESIAN_POINT('Ctrl Pts',(-208.572580360949,2.52047409985873,
135.029902774723));
#126762=CARTESIAN_POINT('Ctrl Pts',(-208.580331552189,2.63626641098722,
134.9563821099));
#126763=CARTESIAN_POINT('Ctrl Pts',(-208.588079448966,2.75200950729446,
134.88289269332));
#126764=CARTESIAN_POINT('Ctrl Pts',(-208.595827345743,2.86473721315403,
134.804521863035));
#126765=CARTESIAN_POINT('Ctrl Pts',(-208.60357524252,2.97401854085767,134.721553079156));
#126766=CARTESIAN_POINT('Ctrl Pts',(-208.611321518604,3.08327700926309,
134.638601650557));
#126767=CARTESIAN_POINT('Ctrl Pts',(-208.619067794688,3.18909022224706,
134.551054417686));
#126768=CARTESIAN_POINT('Ctrl Pts',(-208.626814070772,3.2910577895266,134.459237043452));
#126769=CARTESIAN_POINT('Ctrl Pts',(-208.634560404037,3.3930261095077,134.367418991443));
#126770=CARTESIAN_POINT('Ctrl Pts',(-208.642306737303,3.49114843660265,
134.271330996788));
#126771=CARTESIAN_POINT('Ctrl Pts',(-208.650053070568,3.58505927829805,
134.171337456451));
#126772=CARTESIAN_POINT('Ctrl Pts',(-208.657801138571,3.67899115067519,
134.071321523254));
#126773=CARTESIAN_POINT('Ctrl Pts',(-208.665549206574,3.7687093933284,133.967398588914));
#126774=CARTESIAN_POINT('Ctrl Pts',(-208.673297274577,3.85388730910897,
133.859967868374));
#126775=CARTESIAN_POINT('Ctrl Pts',(-208.681053577318,3.93915575299218,
133.752422969185));
#126776=CARTESIAN_POINT('Ctrl Pts',(-208.68880988006,4.01987398723393,133.641363143325));
#126777=CARTESIAN_POINT('Ctrl Pts',(-208.696566182802,4.09575704069982,
133.527218918333));
#126778=CARTESIAN_POINT('Ctrl Pts',(-208.704326625316,4.17168059523614,
133.413013771132));
#126779=CARTESIAN_POINT('Ctrl Pts',(-208.71208706783,4.24276362423822,133.295721278727));
#126780=CARTESIAN_POINT('Ctrl Pts',(-208.719847510344,4.30876655691763,
133.175797696741));
#126781=CARTESIAN_POINT('Ctrl Pts',(-208.72762041061,4.37487544336421,133.055681602776));
#126782=CARTESIAN_POINT('Ctrl Pts',(-208.735393310875,4.43588776304528,
132.932926329322));
#126783=CARTESIAN_POINT('Ctrl Pts',(-208.743166211141,4.49161127051699,
132.808010102148));
#126784=CARTESIAN_POINT('Ctrl Pts',(-208.750656546903,4.54530908813745,
132.687634894467));
#126785=CARTESIAN_POINT('Ctrl Pts',(-208.758146882666,4.59409582688949,
132.56525340371));
#126786=CARTESIAN_POINT('Ctrl Pts',(-208.765637218428,4.6378435405948,132.441306052045));
#126787=CARTESIAN_POINT('Ctrl Pts',(-208.773411552547,4.68324996215869,
132.312659198879));
#126788=CARTESIAN_POINT('Ctrl Pts',(-208.781185886666,4.72337154034538,
132.181917887059));
#126789=CARTESIAN_POINT('Ctrl Pts',(-208.788960220785,4.75801138636156,
132.049555666445));
#126790=CARTESIAN_POINT('Ctrl Pts',(-208.796724973733,4.79260854186337,
131.917356570439));
#126791=CARTESIAN_POINT('Ctrl Pts',(-208.80448972668,4.82173730907985,131.783540914914));
#126792=CARTESIAN_POINT('Ctrl Pts',(-208.812254479627,4.8452493934639,131.648600736038));
#126793=CARTESIAN_POINT('Ctrl Pts',(-208.820011520512,4.86873812531435,
131.51379458165));
#126794=CARTESIAN_POINT('Ctrl Pts',(-208.827768561397,4.88662120925884,
131.377866509247));
#126795=CARTESIAN_POINT('Ctrl Pts',(-208.835525602282,4.89880066543715,
131.241321831877));
#126796=CARTESIAN_POINT('Ctrl Pts',(-208.843276793522,4.91097093699282,
131.104880123912));
#126797=CARTESIAN_POINT('Ctrl Pts',(-208.851027984762,4.91744610736595,
130.967823124351));
#126798=CARTESIAN_POINT('Ctrl Pts',(-208.858779176003,4.91817966238524,
130.830664058409));
#126799=CARTESIAN_POINT('Ctrl Pts',(-208.86652707278,4.91891290562408,130.693563288729));
#126800=CARTESIAN_POINT('Ctrl Pts',(-208.874274969557,4.91390938507212,
130.556360929091));
#126801=CARTESIAN_POINT('Ctrl Pts',(-208.882022866334,4.90317462436412,
130.419572798773));
#126802=CARTESIAN_POINT('Ctrl Pts',(-208.889769142418,4.89244210913667,
130.282813281582));
#126803=CARTESIAN_POINT('Ctrl Pts',(-208.897515418502,4.87598076890379,
130.146468210885));
#126804=CARTESIAN_POINT('Ctrl Pts',(-208.905261694586,4.85384817236754,
130.011050475122));
#126805=CARTESIAN_POINT('Ctrl Pts',(-208.913008027852,4.83171541245352,
129.875631739737));
#126806=CARTESIAN_POINT('Ctrl Pts',(-208.920754361117,4.80391137576211,
129.741140738792));
#126807=CARTESIAN_POINT('Ctrl Pts',(-208.928500694382,4.77054508214752,
129.608081936949));
#126808=CARTESIAN_POINT('Ctrl Pts',(-208.936248762385,4.73717131638278,
129.474993337511));
#126809=CARTESIAN_POINT('Ctrl Pts',(-208.943996830388,4.69823291011487,
129.343337954543));
#126810=CARTESIAN_POINT('Ctrl Pts',(-208.951744898391,4.65388914639238,
129.213606433039));
#126811=CARTESIAN_POINT('Ctrl Pts',(-208.959501201133,4.60949825359005,
129.083737031329));
#126812=CARTESIAN_POINT('Ctrl Pts',(-208.967257503875,4.55969065397508,
128.955795946137));
#126813=CARTESIAN_POINT('Ctrl Pts',(-208.975013806617,4.50467452870077,
128.8302556424));
#126814=CARTESIAN_POINT('Ctrl Pts',(-208.982774249131,4.44962903966375,
128.704648334023));
#126815=CARTESIAN_POINT('Ctrl Pts',(-208.990534691645,4.38936965738045,
128.581444711373));
#126816=CARTESIAN_POINT('Ctrl Pts',(-208.99829513416,4.32415074876651,128.461092949449));
#126817=CARTESIAN_POINT('Ctrl Pts',(-209.006068034425,4.25882714497078,
128.340547988193));
#126818=CARTESIAN_POINT('Ctrl Pts',(-209.013840934691,4.18852830589864,
128.22286437192));
#126819=CARTESIAN_POINT('Ctrl Pts',(-209.021613834956,4.11355266307514,
128.108462334877));
#126820=CARTESIAN_POINT('Ctrl Pts',(-209.029104170718,4.04130257372357,
127.998219100045));
#126821=CARTESIAN_POINT('Ctrl Pts',(-209.036594506479,3.96470998351261,
127.891023249946));
#126822=CARTESIAN_POINT('Ctrl Pts',(-209.044084842241,3.88407627404977,
127.787220488261));
#126823=CARTESIAN_POINT('Ctrl Pts',(-209.05185917636,3.80038531298161,127.679482013312));
#126824=CARTESIAN_POINT('Ctrl Pts',(-209.059633510479,3.71207563759592,
127.57505772071));
#126825=CARTESIAN_POINT('Ctrl Pts',(-209.067407844598,3.6194392355984,127.474369223837));
#126826=CARTESIAN_POINT('Ctrl Pts',(-209.075172597545,3.52691699968669,
127.373804816537));
#126827=CARTESIAN_POINT('Ctrl Pts',(-209.082937350492,3.43007890902742,
127.276967329268));
#126828=CARTESIAN_POINT('Ctrl Pts',(-209.090702103439,3.32925877075882,
127.184247483999));
#126829=CARTESIAN_POINT('Ctrl Pts',(-209.098459144324,3.22853876847313,
127.091619729388));
#126830=CARTESIAN_POINT('Ctrl Pts',(-209.106216185209,3.12384487516857,
127.003101741029));
#126831=CARTESIAN_POINT('Ctrl Pts',(-209.113973226094,3.0155492645166,126.919049086199));
#126832=CARTESIAN_POINT('Ctrl Pts',(-209.121724417335,2.9073353204266,126.83505981613));
#126833=CARTESIAN_POINT('Ctrl Pts',(-209.129475608575,2.79552537279217,
126.755529415843));
#126834=CARTESIAN_POINT('Ctrl Pts',(-209.137226799815,2.68052607047514,
126.680774429792));
#126835=CARTESIAN_POINT('Ctrl Pts',(-209.144974696592,2.56557564592976,
126.606051216604));
#126836=CARTESIAN_POINT('Ctrl Pts',(-209.152722593369,2.44743888991785,
126.536099593413));
#126837=CARTESIAN_POINT('Ctrl Pts',(-209.160470490146,2.32655276146665,
126.471193725948));
#126838=CARTESIAN_POINT('Ctrl Pts',(-209.16821676623,2.20569191978752,126.406301435392));
#126839=CARTESIAN_POINT('Ctrl Pts',(-209.175963042314,2.08208319383041,
126.346452986013));
#126840=CARTESIAN_POINT('Ctrl Pts',(-209.183709318398,1.95618920845762,
126.291877172365));
#126841=CARTESIAN_POINT('Ctrl Pts',(-209.191455651664,1.83029429376386,
126.23730095585));
#126842=CARTESIAN_POINT('Ctrl Pts',(-209.199201984929,1.7021144447027,126.187997608234));
#126843=CARTESIAN_POINT('Ctrl Pts',(-209.206948318194,1.57213300957585,
126.144148083496));
#126844=CARTESIAN_POINT('Ctrl Pts',(-209.214696386197,1.44212246600765,
126.100288738961));
#126845=CARTESIAN_POINT('Ctrl Pts',(-209.2224444542,1.31030990393177,126.061885772592));
#126846=CARTESIAN_POINT('Ctrl Pts',(-209.230192522203,1.17719421325383,
126.02907038065));
#126847=CARTESIAN_POINT('Ctrl Pts',(-209.237948824945,1.04393704563628,
125.99622011212));
#126848=CARTESIAN_POINT('Ctrl Pts',(-209.245705127687,0.90937436297501,
125.968969374619));
#126849=CARTESIAN_POINT('Ctrl Pts',(-209.253461430428,0.774016190401353,
125.947398398288));
#126850=CARTESIAN_POINT('Ctrl Pts',(-209.261221872943,0.63858577309507,
125.925815908877));
#126851=CARTESIAN_POINT('Ctrl Pts',(-209.268982315457,0.502359408011086,
125.909919266368));
#126852=CARTESIAN_POINT('Ctrl Pts',(-209.276742757971,0.365851649000174,
125.899736714205));
#126853=CARTESIAN_POINT('Ctrl Pts',(-209.284515658236,0.229124755615908,
125.889537816105));
#126854=CARTESIAN_POINT('Ctrl Pts',(-209.292288558502,0.092115956609699,
125.885071351205));
#126855=CARTESIAN_POINT('Ctrl Pts',(-209.300061458767,-0.0446598835168608,
125.886313387485));
#126856=CARTESIAN_POINT('Ctrl Pts',(-209.307551794529,-0.176463577336899,
125.887510272618));
#126857=CARTESIAN_POINT('Ctrl Pts',(-209.315042130291,-0.308050647861612,
125.894007812595));
#126858=CARTESIAN_POINT('Ctrl Pts',(-209.322532466053,-0.438967340671629,
125.905739307817));
#126859=CARTESIAN_POINT('Ctrl Pts',(-209.330306800172,-0.57484777968248,
125.917915606247));
#126860=CARTESIAN_POINT('Ctrl Pts',(-209.338081134292,-0.710436431130188,
125.935769156352));
#126861=CARTESIAN_POINT('Ctrl Pts',(-209.345855468411,-0.845220753247153,
125.95928219294));
#126862=CARTESIAN_POINT('Ctrl Pts',(-209.353620221358,-0.979838965733497,
125.982766251811));
#126863=CARTESIAN_POINT('Ctrl Pts',(-209.361384974305,-1.11365443975783,
126.011895852824));
#126864=CARTESIAN_POINT('Ctrl Pts',(-209.369149727252,-1.24615801894924,
126.046601349349));
#126865=CARTESIAN_POINT('Ctrl Pts',(-209.376906768137,-1.37852999371783,
126.081272375885));
#126866=CARTESIAN_POINT('Ctrl Pts',(-209.384663809022,-1.50959229090726,
126.121508178528));
#126867=CARTESIAN_POINT('Ctrl Pts',(-209.392420849908,-1.63884459273675,
126.167187829826));
#126868=CARTESIAN_POINT('Ctrl Pts',(-209.400172041148,-1.76799942440017,
126.212833033743));
#126869=CARTESIAN_POINT('Ctrl Pts',(-209.407923232388,-1.8953466103871,
126.263913785318));
#126870=CARTESIAN_POINT('Ctrl Pts',(-209.415674423628,-2.02040002924071,
126.320259059356));
#126871=CARTESIAN_POINT('Ctrl Pts',(-209.423422320405,-2.14540029705488,
126.376580385148));
#126872=CARTESIAN_POINT('Ctrl Pts',(-209.431170217183,-2.26810838105454,
126.438161622791));
#126873=CARTESIAN_POINT('Ctrl Pts',(-209.43891811396,-2.38805743081934,
126.504783339553));
#126874=CARTESIAN_POINT('Ctrl Pts',(-209.446664390044,-2.50798138982873,
126.571391120487));
#126875=CARTESIAN_POINT('Ctrl Pts',(-209.454410666128,-2.62514712097876,
126.643037093649));
#126876=CARTESIAN_POINT('Ctrl Pts',(-209.462156942213,-2.73911207289486,
126.719455708682));
#126877=CARTESIAN_POINT('Ctrl Pts',(-209.469903275478,-2.85307786607418,
126.795874887821));
#126878=CARTESIAN_POINT('Ctrl Pts',(-209.477649608743,-2.96384250815246,
126.877066561391));
#126879=CARTESIAN_POINT('Ctrl Pts',(-209.485395942009,-3.07099249585687,
126.962721884826));
#126880=CARTESIAN_POINT('Ctrl Pts',(-209.493144010012,-3.17816647905854,
127.048396390176));
#126881=CARTESIAN_POINT('Ctrl Pts',(-209.500892078015,-3.28172389179726,
127.138536290411));
#126882=CARTESIAN_POINT('Ctrl Pts',(-209.508640146018,-3.38128469276149,
127.232792770108));
#126883=CARTESIAN_POINT('Ctrl Pts',(-209.51639644876,-3.48095130812937,
127.327149426712));
#126884=CARTESIAN_POINT('Ctrl Pts',(-209.524152751502,-3.57661254222479,
127.425631133395));
#126885=CARTESIAN_POINT('Ctrl Pts',(-209.531909054244,-3.66792521411793,
127.527852157919));
#126886=CARTESIAN_POINT('Ctrl Pts',(-209.539669496758,-3.75928662233343,
127.630127740881));
#126887=CARTESIAN_POINT('Ctrl Pts',(-209.547429939272,-3.84629459573451,
127.736146316386));
#126888=CARTESIAN_POINT('Ctrl Pts',(-209.555190381787,-3.92864724338677,
127.845490241978));
#126889=CARTESIAN_POINT('Ctrl Pts',(-209.562963282052,-4.01113209081997,
127.955009696147));
#126890=CARTESIAN_POINT('Ctrl Pts',(-209.570736182318,-4.08894645672586,
128.067864845666));
#126891=CARTESIAN_POINT('Ctrl Pts',(-209.578509082584,-4.1618321789507,
128.183609584608));
#126892=CARTESIAN_POINT('Ctrl Pts',(-209.585999418345,-4.23206832157534,
128.295146710731));
#126893=CARTESIAN_POINT('Ctrl Pts',(-209.593489754106,-4.29772778297644,
128.409366718959));
#126894=CARTESIAN_POINT('Ctrl Pts',(-209.600980089867,-4.35862141406717,
128.525851800086));
#126895=CARTESIAN_POINT('Ctrl Pts',(-209.609225337078,-4.42565219318398,
128.654076798391));
#126896=CARTESIAN_POINT('Ctrl Pts',(-209.617470584289,-4.48710001139767,
128.785413186329));
#126897=CARTESIAN_POINT('Ctrl Pts',(-209.6257158315,-4.5426830412027,128.919363575216));
#126898=CARTESIAN_POINT('Ctrl Pts',(-209.633941832449,-4.59813632770947,
129.053001293755));
#126899=CARTESIAN_POINT('Ctrl Pts',(-209.642167833397,-4.64775199956008,
129.189240552761));
#126900=CARTESIAN_POINT('Ctrl Pts',(-209.650393834346,-4.69129459316533,
129.327560664073));
#126901=CARTESIAN_POINT('Ctrl Pts',(-209.655403989406,-4.71781478773465,
129.411806363769));
#126902=CARTESIAN_POINT('Ctrl Pts',(-209.660414144467,-4.74208300097035,
129.496823467972));
#126903=CARTESIAN_POINT('Ctrl Pts',(-209.665424299527,-4.76405452823394,
129.582490119308));
#126904=CARTESIAN_POINT('Ctrl Pts',(-207.915133748109,-4.76405452823406,
129.582490119308));
#126905=CARTESIAN_POINT('Ctrl Pts',(-207.920187281069,-4.78612861629524,
129.668556653638));
#126906=CARTESIAN_POINT('Ctrl Pts',(-207.92524081403,-4.8058494769431,129.755142810851));
#126907=CARTESIAN_POINT('Ctrl Pts',(-207.930294346991,-4.82319964338405,
129.842108954767));
#126908=CARTESIAN_POINT('Ctrl Pts',(-207.94154281492,-4.86181872280981,
130.035683606093));
#126909=CARTESIAN_POINT('Ctrl Pts',(-207.95279128285,-4.88879425702603,
130.231652183515));
#126910=CARTESIAN_POINT('Ctrl Pts',(-207.96403975078,-4.90389504104624,
130.428865625719));
#126911=CARTESIAN_POINT('Ctrl Pts',(-207.971073355191,-4.91333747727461,
130.552182093851));
#126912=CARTESIAN_POINT('Ctrl Pts',(-207.978106959602,-4.91813778975611,
130.675984943192));
#126913=CARTESIAN_POINT('Ctrl Pts',(-207.985140564013,-4.91824805552383,
130.799987193734));
#126914=CARTESIAN_POINT('',(-207.639859435957,-4.91824901139309,130.80747901955));
#126915=CARTESIAN_POINT('Ctrl Pts',(-207.569721641055,-4.76405452823393,
129.582490119308));
#126916=CARTESIAN_POINT('Ctrl Pts',(-207.577373827926,-4.79770671860123,
129.713699498807));
#126917=CARTESIAN_POINT('Ctrl Pts',(-207.585026014798,-4.8259125172616,
129.846215817631));
#126918=CARTESIAN_POINT('Ctrl Pts',(-207.592678201669,-4.84859316521369,
129.979541012596));
#126919=CARTESIAN_POINT('Ctrl Pts',(-207.600541740717,-4.87190024903275,
130.11654862811));
#126920=CARTESIAN_POINT('Ctrl Pts',(-207.608405279765,-4.88937248762533,
130.254409993629));
#126921=CARTESIAN_POINT('Ctrl Pts',(-207.616268818813,-4.90098158156969,
130.392580822512));
#126922=CARTESIAN_POINT('Ctrl Pts',(-207.624132357861,-4.91259067551404,
130.530751651395));
#126923=CARTESIAN_POINT('Ctrl Pts',(-207.631995896909,-4.91833666685329,
130.669231486794));
#126924=CARTESIAN_POINT('Ctrl Pts',(-207.639859435957,-4.91824901139309,
130.80747901955));
#126925=CARTESIAN_POINT('Ctrl Pts',(-207.639859435995,-4.91824901139267,
130.807479020212));
#126926=CARTESIAN_POINT('Ctrl Pts',(-207.650384863776,-4.91813168363402,
130.992524762711));
#126927=CARTESIAN_POINT('Ctrl Pts',(-207.660910291556,-4.90757161966847,
131.177239249296));
#126928=CARTESIAN_POINT('Ctrl Pts',(-207.671435719336,-4.88667662202955,
131.360754950939));
#126929=CARTESIAN_POINT('Ctrl Pts',(-207.679210053455,-4.87124307420014,
131.496304062153));
#126930=CARTESIAN_POINT('Ctrl Pts',(-207.686984387574,-4.85014091170025,
131.631425231444));
#126931=CARTESIAN_POINT('Ctrl Pts',(-207.694758721693,-4.82340019419708,
131.765606490961));
#126932=CARTESIAN_POINT('Ctrl Pts',(-207.702523474641,-4.79669243223834,
131.899622384068));
#126933=CARTESIAN_POINT('Ctrl Pts',(-207.710288227588,-4.76436001742371,
132.032700292437));
#126934=CARTESIAN_POINT('Ctrl Pts',(-207.718052980535,-4.72648479467642,
132.164332877648));
#126935=CARTESIAN_POINT('Ctrl Pts',(-207.72581002142,-4.68864719013421,
132.29583472352));
#126936=CARTESIAN_POINT('Ctrl Pts',(-207.733567062305,-4.64527784065412,
132.425893729685));
#126937=CARTESIAN_POINT('Ctrl Pts',(-207.74132410319,-4.59650964511101,
132.554012624367));
#126938=CARTESIAN_POINT('Ctrl Pts',(-207.749075294431,-4.54777822604359,
132.682034903593));
#126939=CARTESIAN_POINT('Ctrl Pts',(-207.756826485671,-4.49365620313431,
132.808119619543));
#126940=CARTESIAN_POINT('Ctrl Pts',(-207.764577676911,-4.4343262179017,
132.931784894886));
#126941=CARTESIAN_POINT('Ctrl Pts',(-207.772325573688,-4.37502144949558,
133.055397609187));
#126942=CARTESIAN_POINT('Ctrl Pts',(-207.780073470465,-4.3105132900552,
133.176592576385));
#126943=CARTESIAN_POINT('Ctrl Pts',(-207.787821367242,-4.24103231224365,
133.294908346281));
#126944=CARTESIAN_POINT('Ctrl Pts',(-207.795567643327,-4.17156586835463,
133.413199367068));
#126945=CARTESIAN_POINT('Ctrl Pts',(-207.803313919411,-4.09712887297701,
133.528612051576));
#126946=CARTESIAN_POINT('Ctrl Pts',(-207.811060195495,-4.01799742000656,
133.64071034835));
#126947=CARTESIAN_POINT('Ctrl Pts',(-207.818806528761,-3.93886538290582,
133.752809472609));
#126948=CARTESIAN_POINT('Ctrl Pts',(-207.826552862026,-3.85503904453311,
133.861593840911));
#126949=CARTESIAN_POINT('Ctrl Pts',(-207.834299195291,-3.76683708345568,
133.966657480481));
#126950=CARTESIAN_POINT('Ctrl Pts',(-207.842047263294,-3.6786153701605,
134.071744648325));
#126951=CARTESIAN_POINT('Ctrl Pts',(-207.849795331298,-3.58601633562376,
134.173109130025));
#126952=CARTESIAN_POINT('Ctrl Pts',(-207.857543399301,-3.4893978147611,
134.270379364319));
#126953=CARTESIAN_POINT('Ctrl Pts',(-207.865299702043,-3.39267660658457,
134.367752978575));
#126954=CARTESIAN_POINT('Ctrl Pts',(-207.873056004784,-3.29192765434873,
134.461023375182));
#126955=CARTESIAN_POINT('Ctrl Pts',(-207.880812307526,-3.18754481460604,
134.549856728548));
#126956=CARTESIAN_POINT('Ctrl Pts',(-207.888572750041,-3.08310626259888,
134.638737494948));
#126957=CARTESIAN_POINT('Ctrl Pts',(-207.896333192555,-2.97503026636996,
134.723176258716));
#126958=CARTESIAN_POINT('Ctrl Pts',(-207.904093635069,-2.86374159265479,
134.80288123812));
#126959=CARTESIAN_POINT('Ctrl Pts',(-207.911866535335,-2.75227426848084,
134.882714167034));
#126960=CARTESIAN_POINT('Ctrl Pts',(-207.9196394356,-2.63758428823285,134.957797911912));
#126961=CARTESIAN_POINT('Ctrl Pts',(-207.927412335866,-2.52012382455114,
135.027885090258));
#126962=CARTESIAN_POINT('Ctrl Pts',(-207.934902671627,-2.40693334460267,
135.095424423125));
#126963=CARTESIAN_POINT('Ctrl Pts',(-207.942393007388,-2.29117058288348,
135.158324010965));
#126964=CARTESIAN_POINT('Ctrl Pts',(-207.949883343149,-2.17325776733692,
135.216404785433));
#126965=CARTESIAN_POINT('Ctrl Pts',(-207.957657677268,-2.05087425153848,
135.276687710124));
#126966=CARTESIAN_POINT('Ctrl Pts',(-207.965432011387,-1.92578675070595,
135.331970155687));
#126967=CARTESIAN_POINT('Ctrl Pts',(-207.973206345506,-1.79844224587773,
135.382000681042));
#126968=CARTESIAN_POINT('Ctrl Pts',(-207.980971098453,-1.67125468177061,
135.431969548246));
#126969=CARTESIAN_POINT('Ctrl Pts',(-207.9887358514,-1.54181600853049,135.476699232042));
#126970=CARTESIAN_POINT('Ctrl Pts',(-207.996500604347,-1.41059730351827,
135.515984362074));
#126971=CARTESIAN_POINT('Ctrl Pts',(-208.004257645232,-1.27950892677373,
135.55523047356));
#126972=CARTESIAN_POINT('Ctrl Pts',(-208.012014686117,-1.14664440867894,
135.589042681258));
#126973=CARTESIAN_POINT('Ctrl Pts',(-208.019771727002,-1.01249395315079,
135.617264009214));
#126974=CARTESIAN_POINT('Ctrl Pts',(-208.027522918242,-0.878444661524504,
135.645464055246));
#126975=CARTESIAN_POINT('Ctrl Pts',(-208.035274109482,-0.743111743707259,
135.668081533319));
#126976=CARTESIAN_POINT('Ctrl Pts',(-208.043025300722,-0.60699933894857,
135.685009638446));
#126977=CARTESIAN_POINT('Ctrl Pts',(-208.050773197499,-0.470944785593006,
135.701930548676));
#126978=CARTESIAN_POINT('Ctrl Pts',(-208.058521094276,-0.334111791395838,
135.713166847296));
#126979=CARTESIAN_POINT('Ctrl Pts',(-208.066268991053,-0.197013217634391,
135.718663096512));
#126980=CARTESIAN_POINT('Ctrl Pts',(-208.074015267137,-0.0599433219390715,
135.724158196032));
#126981=CARTESIAN_POINT('Ctrl Pts',(-208.081761543221,0.0773916524176224,
135.723915618745));
#126982=CARTESIAN_POINT('Ctrl Pts',(-208.089507819305,0.214475607502896,
135.717931953803));
#126983=CARTESIAN_POINT('Ctrl Pts',(-208.09725415257,0.351560574510971,
135.71194824469));
#126984=CARTESIAN_POINT('Ctrl Pts',(-208.105000485836,0.488394127956879,
135.700223380407));
#126985=CARTESIAN_POINT('Ctrl Pts',(-208.112746819101,0.624462457896682,
135.682806036055));
#126986=CARTESIAN_POINT('Ctrl Pts',(-208.120494887104,0.760561259395359,
135.66538479121));
#126987=CARTESIAN_POINT('Ctrl Pts',(-208.128242955107,0.895894108661634,
135.642268579239));
#126988=CARTESIAN_POINT('Ctrl Pts',(-208.13599102311,1.02995498217124,135.613557618854));
#126989=CARTESIAN_POINT('Ctrl Pts',(-208.143747325851,1.16415833717274,
135.584816144119));
#126990=CARTESIAN_POINT('Ctrl Pts',(-208.151503628593,1.29708663300382,
135.55046812487));
#126991=CARTESIAN_POINT('Ctrl Pts',(-208.159259931335,1.42824612365238,
135.510664482891));
#126992=CARTESIAN_POINT('Ctrl Pts',(-208.167020373849,1.55947561807024,
135.47083959651));
#126993=CARTESIAN_POINT('Ctrl Pts',(-208.174780816363,1.6889340573202,135.425553414362));
#126994=CARTESIAN_POINT('Ctrl Pts',(-208.182541258877,1.8161463603732,135.375005589581));
#126995=CARTESIAN_POINT('Ctrl Pts',(-208.190314159142,1.94356287590843,
135.324376620943));
#126996=CARTESIAN_POINT('Ctrl Pts',(-208.198087059408,2.06872569273712,
135.268469290505));
#126997=CARTESIAN_POINT('Ctrl Pts',(-208.205859959673,2.19118227060116,
135.207530307631));
#126998=CARTESIAN_POINT('Ctrl Pts',(-208.213350295436,2.30918724342625,
135.148806610272));
#126999=CARTESIAN_POINT('Ctrl Pts',(-208.220840631199,2.42467904848438,
135.085410883889));
#127000=CARTESIAN_POINT('Ctrl Pts',(-208.228330966962,2.53727880598606,
135.017601569991));
#127001=CARTESIAN_POINT('Ctrl Pts',(-208.236105301081,2.65414781750716,
134.947221245354));
#127002=CARTESIAN_POINT('Ctrl Pts',(-208.243879635201,2.76827135427662,
134.871863100413));
#127003=CARTESIAN_POINT('Ctrl Pts',(-208.25165396932,2.87919626762285,134.791767282932));
#127004=CARTESIAN_POINT('Ctrl Pts',(-208.259418722267,2.98998447592703,
134.711770176388));
#127005=CARTESIAN_POINT('Ctrl Pts',(-208.267183475215,3.09758159032083,
134.627047241368));
#127006=CARTESIAN_POINT('Ctrl Pts',(-208.274948228162,3.20156019808689,
134.537883800904));
#127007=CARTESIAN_POINT('Ctrl Pts',(-208.282705269047,3.30543553283387,
134.448808918827));
#127008=CARTESIAN_POINT('Ctrl Pts',(-208.290462309932,3.40569921821184,
134.355302561001));
#127009=CARTESIAN_POINT('Ctrl Pts',(-208.298219350818,3.50195421871368,
134.257692300526));
#127010=CARTESIAN_POINT('Ctrl Pts',(-208.305970542058,3.59813663257102,
134.160155648707));
#127011=CARTESIAN_POINT('Ctrl Pts',(-208.313721733299,3.6903161052074,134.058521531476));
#127012=CARTESIAN_POINT('Ctrl Pts',(-208.321472924539,3.778130278984,133.953156364756));
#127013=CARTESIAN_POINT('Ctrl Pts',(-208.329220821316,3.86590712939388,
133.847835981044));
#127014=CARTESIAN_POINT('Ctrl Pts',(-208.336968718093,3.94932212134805,
133.738788001574));
#127015=CARTESIAN_POINT('Ctrl Pts',(-208.344716614871,4.02805139941409,
133.626413945584));
#127016=CARTESIAN_POINT('Ctrl Pts',(-208.352462890955,4.10676420901237,
133.514063395824));
#127017=CARTESIAN_POINT('Ctrl Pts',(-208.360209167039,4.18079303010462,
133.398388473415));
#127018=CARTESIAN_POINT('Ctrl Pts',(-208.367955443124,4.24985602950842,
133.279821542515));
#127019=CARTESIAN_POINT('Ctrl Pts',(-208.375701776389,4.3189195387197,133.161253736382));
#127020=CARTESIAN_POINT('Ctrl Pts',(-208.383448109655,4.38301695631581,
133.039794216993));
#127021=CARTESIAN_POINT('Ctrl Pts',(-208.39119444292,4.44191150721355,132.915901577288));
#127022=CARTESIAN_POINT('Ctrl Pts',(-208.398942510924,4.50081924713754,
132.791981192686));
#127023=CARTESIAN_POINT('Ctrl Pts',(-208.406690578927,4.55452163403762,
132.665626956551));
#127024=CARTESIAN_POINT('Ctrl Pts',(-208.41443864693,4.60282946667902,132.537318771467));
#127025=CARTESIAN_POINT('Ctrl Pts',(-208.422194949672,4.65118864145976,
132.408874218917));
#127026=CARTESIAN_POINT('Ctrl Pts',(-208.429951252414,4.69414167092756,
132.278471935501));
#127027=CARTESIAN_POINT('Ctrl Pts',(-208.437707555156,4.73154864807493,
132.146608900635));
#127028=CARTESIAN_POINT('Ctrl Pts',(-208.445467997671,4.76897559045231,
132.014675486496));
#127029=CARTESIAN_POINT('Ctrl Pts',(-208.453228440185,4.80085049145022,
131.881280147467));
#127030=CARTESIAN_POINT('Ctrl Pts',(-208.460988882699,4.82708453200273,
131.746930500068));
#127031=CARTESIAN_POINT('Ctrl Pts',(-208.468761782965,4.85336068576608,
131.612365182688));
#127032=CARTESIAN_POINT('Ctrl Pts',(-208.476534683231,4.87397782505391,
131.476842882373));
#127033=CARTESIAN_POINT('Ctrl Pts',(-208.484307583496,4.88889890437966,
131.340877686498));
#127034=CARTESIAN_POINT('Ctrl Pts',(-208.491797919256,4.90327756488348,
131.209855168009));
#127035=CARTESIAN_POINT('Ctrl Pts',(-208.499288255016,4.91236708648847,
131.078421702932));
#127036=CARTESIAN_POINT('Ctrl Pts',(-208.506778590776,4.91618010957647,
130.947035747511));
#127037=CARTESIAN_POINT('Ctrl Pts',(-208.514552924895,4.92013770459477,
130.810668253622));
#127038=CARTESIAN_POINT('Ctrl Pts',(-208.522327259014,4.9184233222491,130.673919971935));
#127039=CARTESIAN_POINT('Ctrl Pts',(-208.530101593133,4.91099406772633,
130.53730195499));
#127040=CARTESIAN_POINT('Ctrl Pts',(-208.53786634608,4.90357396909578,130.400852307542));
#127041=CARTESIAN_POINT('Ctrl Pts',(-208.545631099026,4.89045303292205,
130.264532992051));
#127042=CARTESIAN_POINT('Ctrl Pts',(-208.553395851973,4.87164028253833,
130.128857827009));
#127043=CARTESIAN_POINT('Ctrl Pts',(-208.561152892858,4.8528462172435,129.993317416455));
#127044=CARTESIAN_POINT('Ctrl Pts',(-208.568909933743,4.82837164119221,
129.858420267914));
#127045=CARTESIAN_POINT('Ctrl Pts',(-208.576666974628,4.7982775435219,129.724677479866));
#127046=CARTESIAN_POINT('Ctrl Pts',(-208.584418165868,4.76820614004469,
129.591035548295));
#127047=CARTESIAN_POINT('Ctrl Pts',(-208.592169357107,4.73252373536271,
129.4585466244));
#127048=CARTESIAN_POINT('Ctrl Pts',(-208.599920548347,4.69134274241578,
129.327713626683));
#127049=CARTESIAN_POINT('Ctrl Pts',(-208.607668445124,4.65017925248945,
129.196936236481));
#127050=CARTESIAN_POINT('Ctrl Pts',(-208.615416341901,4.60352193964285,
129.067813744772));
#127051=CARTESIAN_POINT('Ctrl Pts',(-208.623164238678,4.55153356160966,
128.940835651261));
#127052=CARTESIAN_POINT('Ctrl Pts',(-208.630910514762,4.49955605842443,
128.81388411883));
#127053=CARTESIAN_POINT('Ctrl Pts',(-208.638656790846,4.44224985617784,
128.689076453966));
#127054=CARTESIAN_POINT('Ctrl Pts',(-208.64640306693,4.37982637736422,128.566883474298));
#127055=CARTESIAN_POINT('Ctrl Pts',(-208.654149400195,4.31740243775458,
128.44468959263));
#127056=CARTESIAN_POINT('Ctrl Pts',(-208.66189573346,4.24986132406468,128.325110782835));
#127057=CARTESIAN_POINT('Ctrl Pts',(-208.669642066725,4.17746088080643,
128.208594131182));
#127058=CARTESIAN_POINT('Ctrl Pts',(-208.677390134728,4.105044223971,128.092051386434));
#127059=CARTESIAN_POINT('Ctrl Pts',(-208.685138202731,4.02776627845415,
127.978572496404));
#127060=CARTESIAN_POINT('Ctrl Pts',(-208.692886270733,3.94592853200238,
127.868576040519));
#127061=CARTESIAN_POINT('Ctrl Pts',(-208.700642573475,3.86400380741969,
127.758462679091));
#127062=CARTESIAN_POINT('Ctrl Pts',(-208.708398876217,3.7775098348199,127.65183945947));
#127063=CARTESIAN_POINT('Ctrl Pts',(-208.716155178958,3.68678911390519,
127.549092718899));
#127064=CARTESIAN_POINT('Ctrl Pts',(-208.723915621472,3.59601997261018,
127.446291139299));
#127065=CARTESIAN_POINT('Ctrl Pts',(-208.731676063986,3.50101985852024,
127.34737044324));
#127066=CARTESIAN_POINT('Ctrl Pts',(-208.7394365065,3.40216783491512,127.252679735847));
#127067=CARTESIAN_POINT('Ctrl Pts',(-208.747209406765,3.30315712526576,
127.157837022523));
#127068=CARTESIAN_POINT('Ctrl Pts',(-208.754982307031,3.20028244321735,
127.067238125697));
#127069=CARTESIAN_POINT('Ctrl Pts',(-208.762755207296,3.0939562810473,126.981192089569));
#127070=CARTESIAN_POINT('Ctrl Pts',(-208.77024554306,2.99149534266338,126.898274043568));
#127071=CARTESIAN_POINT('Ctrl Pts',(-208.777735878824,2.8858297545026,126.819583773253));
#127072=CARTESIAN_POINT('Ctrl Pts',(-208.785226214587,2.77735206122495,
126.745358450714));
#127073=CARTESIAN_POINT('Ctrl Pts',(-208.793000548707,2.66476140326243,
126.668318852529));
#127074=CARTESIAN_POINT('Ctrl Pts',(-208.800774882826,2.54878453542897,
126.595845424432));
#127075=CARTESIAN_POINT('Ctrl Pts',(-208.808549216945,2.42982823500761,
126.528250491428));
#127076=CARTESIAN_POINT('Ctrl Pts',(-208.816313969892,2.31101853759509,
126.460738863137));
#127077=CARTESIAN_POINT('Ctrl Pts',(-208.824078722839,2.18923705020673,
126.398093958535));
#127078=CARTESIAN_POINT('Ctrl Pts',(-208.831843475786,2.06492094022386,
126.34058591748));
#127079=CARTESIAN_POINT('Ctrl Pts',(-208.839600516671,1.94072830275398,
126.283134994223));
#127080=CARTESIAN_POINT('Ctrl Pts',(-208.847357557556,1.81400640501634,
126.230810944377));
#127081=CARTESIAN_POINT('Ctrl Pts',(-208.855114598441,1.68521821475511,
126.183838717265));
#127082=CARTESIAN_POINT('Ctrl Pts',(-208.862865789681,1.55652714467016,
126.136901912276));
#127083=CARTESIAN_POINT('Ctrl Pts',(-208.870616980922,1.42577324939049,
126.095309030325));
#127084=CARTESIAN_POINT('Ctrl Pts',(-208.878368172162,1.29344041043454,
126.059237334957));
#127085=CARTESIAN_POINT('Ctrl Pts',(-208.886116068939,1.16116381646543,
126.023180971022));
#127086=CARTESIAN_POINT('Ctrl Pts',(-208.893863965716,1.02730998998639,
125.992641228963));
#127087=CARTESIAN_POINT('Ctrl Pts',(-208.901611862493,0.892378735491116,
125.967745762635));
#127088=CARTESIAN_POINT('Ctrl Pts',(-208.909358138577,0.7574757057055,125.942855503901));
#127089=CARTESIAN_POINT('Ctrl Pts',(-208.917104414661,0.621496080418521,
125.923607243392));
#127090=CARTESIAN_POINT('Ctrl Pts',(-208.924850690745,0.484950250857501,
125.910077593803));
#127091=CARTESIAN_POINT('Ctrl Pts',(-208.932597024011,0.348403413345999,
125.896547844342));
#127092=CARTESIAN_POINT('Ctrl Pts',(-208.940343357276,0.211290752280387,
125.888736828585));
#127093=CARTESIAN_POINT('Ctrl Pts',(-208.948089690541,0.0741277852576398,
125.886669275691));
#127094=CARTESIAN_POINT('Ctrl Pts',(-208.955837758544,-0.0630658984603644,
125.884601259783));
#127095=CARTESIAN_POINT('Ctrl Pts',(-208.963585826547,-0.200309519706907,
125.888279272036));
#127096=CARTESIAN_POINT('Ctrl Pts',(-208.97133389455,-0.337087954264749,
125.897675914674));
#127097=CARTESIAN_POINT('Ctrl Pts',(-208.979090197292,-0.474011758570708,
125.907082544177));
#127098=CARTESIAN_POINT('Ctrl Pts',(-208.986846500034,-0.610468997891036,
125.922219918342));
#127099=CARTESIAN_POINT('Ctrl Pts',(-208.994602802776,-0.745949506308154,
125.943008707188));
#127100=CARTESIAN_POINT('Ctrl Pts',(-209.00236324529,-0.881502324751852,
125.963808591636));
#127101=CARTESIAN_POINT('Ctrl Pts',(-209.010123687804,-1.01607699010257,
125.990265825674));
#127102=CARTESIAN_POINT('Ctrl Pts',(-209.017884130318,-1.14917489737068,
126.022250192476));
#127103=CARTESIAN_POINT('Ctrl Pts',(-209.025657030584,-1.28248646521542,
126.054285903423));
#127104=CARTESIAN_POINT('Ctrl Pts',(-209.033429930849,-1.41431616151418,
126.091866370262));
#127105=CARTESIAN_POINT('Ctrl Pts',(-209.041202831114,-1.54418101647718,
126.134811597494));
#127106=CARTESIAN_POINT('Ctrl Pts',(-209.048693166877,-1.66932495685847,
126.176195657547));
#127107=CARTESIAN_POINT('Ctrl Pts',(-209.056183502639,-1.79264414130074,
126.222561096243));
#127108=CARTESIAN_POINT('Ctrl Pts',(-209.063673838402,-1.91372685023181,
126.27370585195));
#127109=CARTESIAN_POINT('Ctrl Pts',(-209.071448601995,-2.03940738940923,
126.326792709108));
#127110=CARTESIAN_POINT('Ctrl Pts',(-209.079223365589,-2.1630763871519,
126.385197194931));
#127111=CARTESIAN_POINT('Ctrl Pts',(-209.086998129183,-2.28425112295715,
126.448745865345));
#127112=CARTESIAN_POINT('Ctrl Pts',(-209.094763213571,-2.4052750020561,
126.512215420726));
#127113=CARTESIAN_POINT('Ctrl Pts',(-209.102528297959,-2.52381045499339,
126.580816237645));
#127114=CARTESIAN_POINT('Ctrl Pts',(-209.110293382346,-2.63939384798977,
126.654326499912));
#127115=CARTESIAN_POINT('Ctrl Pts',(-209.118050657055,-2.75486099380381,
126.727762829751));
#127116=CARTESIAN_POINT('Ctrl Pts',(-209.125807931764,-2.86738166066909,
126.806098569736));
#127117=CARTESIAN_POINT('Ctrl Pts',(-209.133565206473,-2.97651631010486,
126.889065773218));
#127118=CARTESIAN_POINT('Ctrl Pts',(-209.14132602299,-3.08570078811257,
126.97207085777));
#127119=CARTESIAN_POINT('Ctrl Pts',(-209.149086839506,-3.19149581646136,
127.059711439138));
#127120=CARTESIAN_POINT('Ctrl Pts',(-209.156847656023,-3.29348919977197,
127.151675036588));
#127121=CARTESIAN_POINT('Ctrl Pts',(-209.164595213319,-3.39530832916146,
127.243481515832));
#127122=CARTESIAN_POINT('Ctrl Pts',(-209.172342770616,-3.49333849204953,
127.339596001324));
#127123=CARTESIAN_POINT('Ctrl Pts',(-209.180090327912,-3.58720222976018,
127.439666987337));
#127124=CARTESIAN_POINT('Ctrl Pts',(-209.187836127983,-3.68104467821264,
127.539715276224));
#127125=CARTESIAN_POINT('Ctrl Pts',(-209.195581928054,-3.77072231479238,
127.643717994952));
#127126=CARTESIAN_POINT('Ctrl Pts',(-209.203327728125,-3.85589491745125,
127.751287174612));
#127127=CARTESIAN_POINT('Ctrl Pts',(-209.211073448765,-3.94106664669009,
127.858855251181));
#127128=CARTESIAN_POINT('Ctrl Pts',(-209.218819169406,-4.0217331920826,
127.969989408906));
#127129=CARTESIAN_POINT('Ctrl Pts',(-209.226564890046,-4.09759522176032,
128.084269357864));
#127130=CARTESIAN_POINT('Ctrl Pts',(-209.234336549448,-4.17371129715035,
128.19893200593));
#127131=CARTESIAN_POINT('Ctrl Pts',(-209.24210820885,-4.24499039396231,
128.316761227611));
#127132=CARTESIAN_POINT('Ctrl Pts',(-209.249879868252,-4.31117491106617,
128.437304651034));
#127133=CARTESIAN_POINT('Ctrl Pts',(-209.257633629026,-4.37720700100607,
128.557570455265));
#127134=CARTESIAN_POINT('Ctrl Pts',(-209.265387389801,-4.43816780660334,
128.680537606677));
#127135=CARTESIAN_POINT('Ctrl Pts',(-209.273141150576,-4.49384871502306,
128.805734392134));
#127136=CARTESIAN_POINT('Ctrl Pts',(-209.280921759291,-4.5497224224962,
128.931364680247));
#127137=CARTESIAN_POINT('Ctrl Pts',(-209.288702368007,-4.60027945897932,
129.059239701905));
#127138=CARTESIAN_POINT('Ctrl Pts',(-209.296482976722,-4.64535888444512,
129.188865678791));
#127139=CARTESIAN_POINT('Ctrl Pts',(-209.304263585438,-4.69043830991079,
129.318491655677));
#127140=CARTESIAN_POINT('Ctrl Pts',(-209.312044194154,-4.73004005339845,
129.449868198166));
#127141=CARTESIAN_POINT('Ctrl Pts',(-209.319824802869,-4.76405452823398,
129.582490119308));
#127142=CARTESIAN_POINT('Origin',(213.235140564004,0.,130.804360617566));
#127143=CARTESIAN_POINT('',(-211.415108320184,-4.76405452823408,129.582490119308));
#127144=CARTESIAN_POINT('',(-211.070145064099,-4.76405452823395,129.582490119308));
#127145=CARTESIAN_POINT('',(213.235140564004,-4.76405452823405,129.582490119308));
#127146=CARTESIAN_POINT('',(-209.735140563965,-4.91824997503721,130.803865091055));
#127147=CARTESIAN_POINT('Ctrl Pts',(-209.735140564013,-4.91824997503729,
130.803865091902));
#127148=CARTESIAN_POINT('Ctrl Pts',(-209.743196689866,-4.91826438707087,
130.946909113438));
#127149=CARTESIAN_POINT('Ctrl Pts',(-209.751252815718,-4.91203396140685,
131.089852888571));
#127150=CARTESIAN_POINT('Ctrl Pts',(-209.759308941571,-4.89961085085684,
131.232141604364));
#127151=CARTESIAN_POINT('Ctrl Pts',(-209.767373658041,-4.88717449297359,
131.374582049149));
#127152=CARTESIAN_POINT('Ctrl Pts',(-209.77543837451,-4.86853230799063,
131.516365699231));
#127153=CARTESIAN_POINT('Ctrl Pts',(-209.78350309098,-4.84378796086789,
131.656945658868));
#127154=CARTESIAN_POINT('Ctrl Pts',(-209.791584921351,-4.81899110448103,
131.797823939175));
#127155=CARTESIAN_POINT('Ctrl Pts',(-209.799666751723,-4.78806625848942,
131.937493083153));
#127156=CARTESIAN_POINT('Ctrl Pts',(-209.807748582094,-4.75116801749538,
132.075417473898));
#127157=CARTESIAN_POINT('Ctrl Pts',(-209.815839159132,-4.71422984289908,
132.213491135113));
#127158=CARTESIAN_POINT('Ctrl Pts',(-209.82392973617,-4.67130547793691,
132.349815948105));
#127159=CARTESIAN_POINT('Ctrl Pts',(-209.832020313208,-4.62259852859672,
132.483874209626));
#127160=CARTESIAN_POINT('Ctrl Pts',(-209.840129193615,-4.57378138918253,
132.618235752095));
#127161=CARTESIAN_POINT('Ctrl Pts',(-209.848238074022,-4.5191556368364,
132.750320170896));
#127162=CARTESIAN_POINT('Ctrl Pts',(-209.856346954429,-4.45897267597615,
132.879630657199));
#127163=CARTESIAN_POINT('Ctrl Pts',(-209.864040540846,-4.40187196823782,
133.002318543942));
#127164=CARTESIAN_POINT('Ctrl Pts',(-209.871734127263,-4.3397691994306,
133.122509340562));
#127165=CARTESIAN_POINT('Ctrl Pts',(-209.87942771368,-4.27291533841665,
133.239802584278));
#127166=CARTESIAN_POINT('Ctrl Pts',(-209.887202047799,-4.20535981560865,
133.358326874139));
#127167=CARTESIAN_POINT('Ctrl Pts',(-209.894976381918,-4.13276202216405,
133.474225933839));
#127168=CARTESIAN_POINT('Ctrl Pts',(-209.902750716037,-4.05535116236854,
133.587040982318));
#127169=CARTESIAN_POINT('Ctrl Pts',(-209.910515468984,-3.97803570453932,
133.699716996333));
#127170=CARTESIAN_POINT('Ctrl Pts',(-209.918280221931,-3.8959192017021,
133.809316242246));
#127171=CARTESIAN_POINT('Ctrl Pts',(-209.926044974879,-3.80927663799556,
133.915404583459));
#127172=CARTESIAN_POINT('Ctrl Pts',(-209.933802015764,-3.72272012890474,
134.021387556237));
#127173=CARTESIAN_POINT('Ctrl Pts',(-209.941559056648,-3.63164675059403,
134.12386626291));
#127174=CARTESIAN_POINT('Ctrl Pts',(-209.949316097533,-3.53637445407398,
134.222435921458));
#127175=CARTESIAN_POINT('Ctrl Pts',(-209.957067288774,-3.44117400313397,
134.320931247859));
#127176=CARTESIAN_POINT('Ctrl Pts',(-209.964818480014,-3.34178120719801,
134.415523113659));
#127177=CARTESIAN_POINT('Ctrl Pts',(-209.972569671254,-3.23855368108763,
134.505840472599));
#127178=CARTESIAN_POINT('Ctrl Pts',(-209.980317568031,-3.13537002942939,
134.596119444252));
#127179=CARTESIAN_POINT('Ctrl Pts',(-209.988065464808,-3.02835518289397,
134.682127265576));
#127180=CARTESIAN_POINT('Ctrl Pts',(-209.995813361585,-2.91790277345313,
134.763530539049));
#127181=CARTESIAN_POINT('Ctrl Pts',(-210.003559637669,-2.80747346827526,
134.844916784711));
#127182=CARTESIAN_POINT('Ctrl Pts',(-210.011305913753,-2.69360834497568,
134.921700166518));
#127183=CARTESIAN_POINT('Ctrl Pts',(-210.019052189837,-2.5767328799856,
134.993588556901));
#127184=CARTESIAN_POINT('Ctrl Pts',(-210.026798523103,-2.45985655224754,
135.065477477947));
#127185=CARTESIAN_POINT('Ctrl Pts',(-210.034544856368,-2.33997017149051,
135.132471130634));
#127186=CARTESIAN_POINT('Ctrl Pts',(-210.042291189633,-2.21752651664132,
135.1943218031));
#127187=CARTESIAN_POINT('Ctrl Pts',(-210.050039257636,-2.09505544138409,
135.256186326595));
#127188=CARTESIAN_POINT('Ctrl Pts',(-210.057787325639,-1.97002630136351,
135.312905401805));
#127189=CARTESIAN_POINT('Ctrl Pts',(-210.065535393642,-1.84291432065546,
135.364278365642));
#127190=CARTESIAN_POINT('Ctrl Pts',(-210.073291696384,-1.71566724382218,
135.415705929277));
#127191=CARTESIAN_POINT('Ctrl Pts',(-210.081047999126,-1.58633326731982,
135.461775884578));
#127192=CARTESIAN_POINT('Ctrl Pts',(-210.088804301868,-1.4554058700633,
135.502336438692));
#127193=CARTESIAN_POINT('Ctrl Pts',(-210.096564744382,-1.32440859291271,
135.542918641195));
#127194=CARTESIAN_POINT('Ctrl Pts',(-210.104325186896,-1.19181657818618,
135.577985483336));
#127195=CARTESIAN_POINT('Ctrl Pts',(-210.11208562941,-1.05813516480963,
135.60743599023));
#127196=CARTESIAN_POINT('Ctrl Pts',(-210.119858529675,-0.924239154160643,
135.636933773692));
#127197=CARTESIAN_POINT('Ctrl Pts',(-210.127631429941,-0.789250635420359,
135.660797137288));
#127198=CARTESIAN_POINT('Ctrl Pts',(-210.135404330206,-0.653682658929158,
135.678976709518));
#127199=CARTESIAN_POINT('Ctrl Pts',(-210.142894665968,-0.523042919860747,
135.696495408506));
#127200=CARTESIAN_POINT('Ctrl Pts',(-210.15038500173,-0.391865427795292,
135.708736353318));
#127201=CARTESIAN_POINT('Ctrl Pts',(-210.157875337492,-0.26060881028972,
135.715701179011));
#127202=CARTESIAN_POINT('Ctrl Pts',(-210.165649671611,-0.12437555823472,
135.722930078188));
#127203=CARTESIAN_POINT('Ctrl Pts',(-210.17342400573,0.0123744837791795,
135.724497771247));
#127204=CARTESIAN_POINT('Ctrl Pts',(-210.181198339849,0.149131439737756,
135.720349111875));
#127205=CARTESIAN_POINT('Ctrl Pts',(-210.188963092796,0.285719854970061,
135.716205565356));
#127206=CARTESIAN_POINT('Ctrl Pts',(-210.196727845743,0.422314780159226,
135.706359695386));
#127207=CARTESIAN_POINT('Ctrl Pts',(-210.20449259869,0.558402328245245,
135.690808192473));
#127208=CARTESIAN_POINT('Ctrl Pts',(-210.212249639575,0.694354712260006,
135.675272135531));
#127209=CARTESIAN_POINT('Ctrl Pts',(-210.22000668046,0.82980033609962,135.654041767165));
#127210=CARTESIAN_POINT('Ctrl Pts',(-210.227763721345,0.96422678489746,
135.627165793995));
#127211=CARTESIAN_POINT('Ctrl Pts',(-210.235514912586,1.09855186166439,
135.600310088204));
#127212=CARTESIAN_POINT('Ctrl Pts',(-210.243266103826,1.23185891135041,
135.567817328034));
#127213=CARTESIAN_POINT('Ctrl Pts',(-210.251017295066,1.36364246268163,
135.529787825393));
#127214=CARTESIAN_POINT('Ctrl Pts',(-210.258765191843,1.49537000248827,
135.491774486305));
#127215=CARTESIAN_POINT('Ctrl Pts',(-210.26651308862,1.62557495697206,135.448229193382));
#127216=CARTESIAN_POINT('Ctrl Pts',(-210.274260985397,1.7537640616575,135.399302910842));
#127217=CARTESIAN_POINT('Ctrl Pts',(-210.282007261481,1.88192635194604,
135.350386862626));
#127218=CARTESIAN_POINT('Ctrl Pts',(-210.289753537565,2.0080732661324,135.296092202972));
#127219=CARTESIAN_POINT('Ctrl Pts',(-210.297499813649,2.13172904861533,
135.236618995164));
#127220=CARTESIAN_POINT('Ctrl Pts',(-210.305246146914,2.255385743897,135.177145348339));
#127221=CARTESIAN_POINT('Ctrl Pts',(-210.31299248018,2.37655091844898,135.112493246538));
#127222=CARTESIAN_POINT('Ctrl Pts',(-210.320738813445,2.49477142719497,
135.042909731184));
#127223=CARTESIAN_POINT('Ctrl Pts',(-210.328486881448,2.61301841060405,
134.973310633084));
#127224=CARTESIAN_POINT('Ctrl Pts',(-210.336234949451,2.72831907913344,
134.898778122168));
#127225=CARTESIAN_POINT('Ctrl Pts',(-210.343983017454,2.84024773902294,
134.819603554609));
#127226=CARTESIAN_POINT('Ctrl Pts',(-210.351739320196,2.95229535802428,
134.740344839378));
#127227=CARTESIAN_POINT('Ctrl Pts',(-210.359495622938,3.06096348964574,
134.65643443818));
#127228=CARTESIAN_POINT('Ctrl Pts',(-210.36725192568,3.16585768885339,134.568205481057));
#127229=CARTESIAN_POINT('Ctrl Pts',(-210.375012368194,3.27080787325346,
134.479929433483));
#127230=CARTESIAN_POINT('Ctrl Pts',(-210.382772810708,3.37197982339132,
134.387330501026));
#127231=CARTESIAN_POINT('Ctrl Pts',(-210.390533253222,3.46901543820338,
134.290779260243));
#127232=CARTESIAN_POINT('Ctrl Pts',(-210.398306153487,3.56620682319875,
134.194073026837));
#127233=CARTESIAN_POINT('Ctrl Pts',(-210.406079053753,3.65924833849426,
134.093402093866));
#127234=CARTESIAN_POINT('Ctrl Pts',(-210.413851954018,3.74782113020959,
133.989171418611));
#127235=CARTESIAN_POINT('Ctrl Pts',(-210.421342289781,3.83317407784731,
133.88872979094));
#127236=CARTESIAN_POINT('Ctrl Pts',(-210.428832625543,3.91437737005352,
133.784982981394));
#127237=CARTESIAN_POINT('Ctrl Pts',(-210.436322961305,3.9911844830499,133.678317730113));
#127238=CARTESIAN_POINT('Ctrl Pts',(-210.444097295424,4.07090376107842,
133.567608233413));
#127239=CARTESIAN_POINT('Ctrl Pts',(-210.451871629543,4.14613944366244,
133.453403926496));
#127240=CARTESIAN_POINT('Ctrl Pts',(-210.459645963662,4.21656953420747,
133.336103974562));
#127241=CARTESIAN_POINT('Ctrl Pts',(-210.467410716609,4.28691282596003,
133.218948584336));
#127242=CARTESIAN_POINT('Ctrl Pts',(-210.475175469556,4.352462110286,133.098705471988));
#127243=CARTESIAN_POINT('Ctrl Pts',(-210.482940222504,4.41293683430738,
132.975805196392));
#127244=CARTESIAN_POINT('Ctrl Pts',(-210.490697263389,4.47335149398065,
132.853026987082));
#127245=CARTESIAN_POINT('Ctrl Pts',(-210.498454304274,4.52870145192803,
132.727597215043));
#127246=CARTESIAN_POINT('Ctrl Pts',(-210.506211345159,4.57875071365639,
132.599973316533));
#127247=CARTESIAN_POINT('Ctrl Pts',(-210.513962536399,4.62876223284708,
132.472445660197));
#127248=CARTESIAN_POINT('Ctrl Pts',(-210.521713727639,4.6734808700339,132.342727533292));
#127249=CARTESIAN_POINT('Ctrl Pts',(-210.529464918879,4.71271780089766,
132.211298424152));
#127250=CARTESIAN_POINT('Ctrl Pts',(-210.537212815656,4.75193805501908,
132.079925175891));
#127251=CARTESIAN_POINT('Ctrl Pts',(-210.544960712433,4.78568112514685,
131.946842765609));
#127252=CARTESIAN_POINT('Ctrl Pts',(-210.55270860921,4.81380740025742,131.812547790529));
#127253=CARTESIAN_POINT('Ctrl Pts',(-210.560454885294,4.84192779195757,
131.678280907063));
#127254=CARTESIAN_POINT('Ctrl Pts',(-210.568201161378,4.86443364551295,
131.542802345727));
#127255=CARTESIAN_POINT('Ctrl Pts',(-210.575947437463,4.88123612230785,
131.406620512277));
#127256=CARTESIAN_POINT('Ctrl Pts',(-210.583693770728,4.89803872313483,
131.270437673563));
#127257=CARTESIAN_POINT('Ctrl Pts',(-210.591440103993,4.90913781531647,
131.133551940397));
#127258=CARTESIAN_POINT('Ctrl Pts',(-210.599186437259,4.91449630581469,
130.996478088489));
#127259=CARTESIAN_POINT('Ctrl Pts',(-210.606934505262,4.91985599630972,
130.859373539841));
#127260=CARTESIAN_POINT('Ctrl Pts',(-210.614682573265,4.9194725117209,130.722081179214));
#127261=CARTESIAN_POINT('Ctrl Pts',(-210.622430641268,4.91336088037301,
130.585116639952));
#127262=CARTESIAN_POINT('Ctrl Pts',(-210.630186944009,4.90724275351062,
130.448006533148));
#127263=CARTESIAN_POINT('Ctrl Pts',(-210.637943246751,4.89538433602431,
130.3112253349));
#127264=CARTESIAN_POINT('Ctrl Pts',(-210.645699549493,4.87785269247762,
130.175284967911));
#127265=CARTESIAN_POINT('Ctrl Pts',(-210.653459992007,4.8603116917649,130.039272045455));
#127266=CARTESIAN_POINT('Ctrl Pts',(-210.661220434522,4.83709149766175,
129.904101233618));
#127267=CARTESIAN_POINT('Ctrl Pts',(-210.668980877036,4.80831032435012,
129.770274118646));
#127268=CARTESIAN_POINT('Ctrl Pts',(-210.676753777301,4.77948294894402,
129.636232172509));
#127269=CARTESIAN_POINT('Ctrl Pts',(-210.684526677567,4.74507685356864,
129.503538612323));
#127270=CARTESIAN_POINT('Ctrl Pts',(-210.692299577832,4.70526039194284,
129.37268058819));
#127271=CARTESIAN_POINT('Ctrl Pts',(-210.699789913594,4.66689135898908,
129.246579582847));
#127272=CARTESIAN_POINT('Ctrl Pts',(-210.707280249356,4.62349859279517,
129.122183268605));
#127273=CARTESIAN_POINT('Ctrl Pts',(-210.714770585118,4.5752742166704,128.999908095395));
#127274=CARTESIAN_POINT('Ctrl Pts',(-210.722544919237,4.52522139866675,
128.872996821825));
#127275=CARTESIAN_POINT('Ctrl Pts',(-210.730319253356,4.46980480499287,
128.747968693797));
#127276=CARTESIAN_POINT('Ctrl Pts',(-210.738093587475,4.40918621761393,
128.625310374707));
#127277=CARTESIAN_POINT('Ctrl Pts',(-210.745858340422,4.34864233722662,
128.502803221033));
#127278=CARTESIAN_POINT('Ctrl Pts',(-210.75362309337,4.282909390654,128.382660412352));
#127279=CARTESIAN_POINT('Ctrl Pts',(-210.761387846317,4.21219797358922,
128.265350713333));
#127280=CARTESIAN_POINT('Ctrl Pts',(-210.769144887202,4.14155678810053,
128.148157527962));
#127281=CARTESIAN_POINT('Ctrl Pts',(-210.776901928087,4.06594717279689,
128.033792185169));
#127282=CARTESIAN_POINT('Ctrl Pts',(-210.784658968972,3.98562642096889,
127.922700489276));
#127283=CARTESIAN_POINT('Ctrl Pts',(-210.792410160212,3.90536623964476,
127.811692568496));
#127284=CARTESIAN_POINT('Ctrl Pts',(-210.800161351452,3.82040222138373,
127.703953696399));
#127285=CARTESIAN_POINT('Ctrl Pts',(-210.807912542692,3.73103570914607,
127.599901911392));
#127286=CARTESIAN_POINT('Ctrl Pts',(-210.815660439469,3.64170718005991,
127.495894351168));
#127287=CARTESIAN_POINT('Ctrl Pts',(-210.823408336246,3.54798013282419,
127.39557105714));
#127288=CARTESIAN_POINT('Ctrl Pts',(-210.831156233023,3.45019690557752,
127.299317910944));
#127289=CARTESIAN_POINT('Ctrl Pts',(-210.838902509108,3.35243413247403,
127.203084898831));
#127290=CARTESIAN_POINT('Ctrl Pts',(-210.846648785192,3.25061714545276,
127.110920615187));
#127291=CARTESIAN_POINT('Ctrl Pts',(-210.854395061276,3.1451256612314,127.023174608182));
#127292=CARTESIAN_POINT('Ctrl Pts',(-210.862141394541,3.03963339829572,
126.935427953456));
#127293=CARTESIAN_POINT('Ctrl Pts',(-210.869887727807,2.93046688461224,
126.852099890465));
#127294=CARTESIAN_POINT('Ctrl Pts',(-210.877634061072,2.81803916587099,
126.773499875477));
#127295=CARTESIAN_POINT('Ctrl Pts',(-210.885382129075,2.70558626972242,
126.694882258561));
#127296=CARTESIAN_POINT('Ctrl Pts',(-210.893130197078,2.58987103561829,
126.620995020536));
#127297=CARTESIAN_POINT('Ctrl Pts',(-210.900878265081,2.4713354036721,126.552104230063));
#127298=CARTESIAN_POINT('Ctrl Pts',(-210.908634567823,2.35267379064488,
126.483140221639));
#127299=CARTESIAN_POINT('Ctrl Pts',(-210.916390870565,2.23118613040431,
126.419183465398));
#127300=CARTESIAN_POINT('Ctrl Pts',(-210.924147173307,2.1073393680538,126.36045424475));
#127301=CARTESIAN_POINT('Ctrl Pts',(-210.931907615821,1.9834265049576,126.301693678549));
#127302=CARTESIAN_POINT('Ctrl Pts',(-210.939668058335,1.85715239062455,
126.24816635995));
#127303=CARTESIAN_POINT('Ctrl Pts',(-210.947428500849,1.72900292142403,
126.200043951631));
#127304=CARTESIAN_POINT('Ctrl Pts',(-210.955201401115,1.60064773531863,
126.15184429295));
#127305=CARTESIAN_POINT('Ctrl Pts',(-210.96297430138,1.4704115500907,126.10906700492));
#127306=CARTESIAN_POINT('Ctrl Pts',(-210.970747201646,1.33879521821518,
126.071833763317));
#127307=CARTESIAN_POINT('Ctrl Pts',(-210.978237537407,1.2119634715277,126.035954043833));
#127308=CARTESIAN_POINT('Ctrl Pts',(-210.985727873169,1.08385047921586,
126.005222360583));
#127309=CARTESIAN_POINT('Ctrl Pts',(-210.993218208931,0.954910459740987,
125.979702176145));
#127310=CARTESIAN_POINT('Ctrl Pts',(-211.00099254305,0.821081640234792,
125.953214386157));
#127311=CARTESIAN_POINT('Ctrl Pts',(-211.008766877169,0.685937912638592,
125.932257178713));
#127312=CARTESIAN_POINT('Ctrl Pts',(-211.016541211288,0.549976167754722,
125.916957495518));
#127313=CARTESIAN_POINT('Ctrl Pts',(-211.024305964236,0.414181983569803,
125.901676667816));
#127314=CARTESIAN_POINT('Ctrl Pts',(-211.032070717183,0.277572172765213,
125.892039534677));
#127315=CARTESIAN_POINT('Ctrl Pts',(-211.03983547013,0.140654952451376,
125.888122294737));
#127316=CARTESIAN_POINT('Ctrl Pts',(-211.047592511015,0.00387372025132052,
125.884208945455));
#127317=CARTESIAN_POINT('Ctrl Pts',(-211.0553495519,-0.13321392557411,125.886004194877));
#127318=CARTESIAN_POINT('Ctrl Pts',(-211.063106592785,-0.270093843915168,
125.893532542997));
#127319=CARTESIAN_POINT('Ctrl Pts',(-211.070857784025,-0.40687054004522,
125.90105521393));
#127320=CARTESIAN_POINT('Ctrl Pts',(-211.078608975265,-0.543439431695396,
125.914302356763));
#127321=CARTESIAN_POINT('Ctrl Pts',(-211.086360166505,-0.67928592808505,
125.933246403097));
#127322=CARTESIAN_POINT('Ctrl Pts',(-211.094108063282,-0.815074686089728,
125.952182397706));
#127323=CARTESIAN_POINT('Ctrl Pts',(-211.101855960059,-0.950141273099997,
125.976810426078));
#127324=CARTESIAN_POINT('Ctrl Pts',(-211.109603856837,-1.08397599384027,
126.007051047893));
#127325=CARTESIAN_POINT('Ctrl Pts',(-211.117350132921,-1.21778271924211,
126.037285344021));
#127326=CARTESIAN_POINT('Ctrl Pts',(-211.125096409005,-1.35035770980363,
126.073129812261));
#127327=CARTESIAN_POINT('Ctrl Pts',(-211.132842685089,-1.48120163458712,
126.114453925509));
#127328=CARTESIAN_POINT('Ctrl Pts',(-211.140589018354,-1.61204652523055,
126.155778343803));
#127329=CARTESIAN_POINT('Ctrl Pts',(-211.14833535162,-1.74115995178414,
126.202582370073));
#127330=CARTESIAN_POINT('Ctrl Pts',(-211.156081684885,-1.86805829864045,
126.254685765955));
#127331=CARTESIAN_POINT('Ctrl Pts',(-211.163829752888,-1.99498506350151,
126.306800830031));
#127332=CARTESIAN_POINT('Ctrl Pts',(-211.171577820891,-2.11969539998282,
126.36421747676));
#127333=CARTESIAN_POINT('Ctrl Pts',(-211.179325888894,-2.24172657755652,
126.426707706019));
#127334=CARTESIAN_POINT('Ctrl Pts',(-211.187082191636,-2.3638874513181,
126.489264350637));
#127335=CARTESIAN_POINT('Ctrl Pts',(-211.194838494378,-2.48336312955346,
126.556905170928));
#127336=CARTESIAN_POINT('Ctrl Pts',(-211.20259479712,-2.59971588635782,
126.629356381314));
#127337=CARTESIAN_POINT('Ctrl Pts',(-211.210355239634,-2.71613074413179,
126.701846261094));
#127338=CARTESIAN_POINT('Ctrl Pts',(-211.218115682148,-2.82941903645592,
126.77915142657));
#127339=CARTESIAN_POINT('Ctrl Pts',(-211.225876124662,-2.93917369979947,
126.860955867238));
#127340=CARTESIAN_POINT('Ctrl Pts',(-211.233649024928,-3.04910455107218,
126.942891627657));
#127341=CARTESIAN_POINT('Ctrl Pts',(-211.241421925193,-3.15549013431897,
127.029340849696));
#127342=CARTESIAN_POINT('Ctrl Pts',(-211.249194825458,-3.2579573572653,
127.119947920712));
#127343=CARTESIAN_POINT('Ctrl Pts',(-211.256685161221,-3.35669963855956,
127.207261196472));
#127344=CARTESIAN_POINT('Ctrl Pts',(-211.264175496983,-3.45180327572581,
127.298435059796));
#127345=CARTESIAN_POINT('Ctrl Pts',(-211.271665832745,-3.54296935972677,
127.393121666901));
#127346=CARTESIAN_POINT('Ctrl Pts',(-211.279339833884,-3.63637086463484,
127.49013001924));
#127347=CARTESIAN_POINT('Ctrl Pts',(-211.287013835023,-3.72595178177155,
127.591150574736));
#127348=CARTESIAN_POINT('Ctrl Pts',(-211.294687836162,-3.81134085198831,
127.695845864108));
#127349=CARTESIAN_POINT('Ctrl Pts',(-211.30235279395,-3.89662929630337,
127.800417776356));
#127350=CARTESIAN_POINT('Ctrl Pts',(-211.310017751738,-3.97773546367402,
127.908655504759));
#127351=CARTESIAN_POINT('Ctrl Pts',(-211.317682709527,-4.05432414393831,
128.020184114832));
#127352=CARTESIAN_POINT('Ctrl Pts',(-211.3253403984,-4.13084019279955,128.131606958891));
#127353=CARTESIAN_POINT('Ctrl Pts',(-211.332998087273,-4.20284704831621,
128.246314149174));
#127354=CARTESIAN_POINT('Ctrl Pts',(-211.340655776146,-4.27004945328258,
128.363897397392));
#127355=CARTESIAN_POINT('Ctrl Pts',(-211.348307502504,-4.33719953236235,
128.48138909163));
#127356=CARTESIAN_POINT('Ctrl Pts',(-211.355959228862,-4.39955240749439,
128.601752039367));
#127357=CARTESIAN_POINT('Ctrl Pts',(-211.36361095522,-4.45685623973759,
128.724549202843));
#127358=CARTESIAN_POINT('Ctrl Pts',(-211.371259291001,-4.5141346799327,
128.847291953353));
#127359=CARTESIAN_POINT('Ctrl Pts',(-211.378907626783,-4.56636835876335,
128.972466410226));
#127360=CARTESIAN_POINT('Ctrl Pts',(-211.386555962565,-4.61335166716167,
129.099611528229));
#127361=CARTESIAN_POINT('Ctrl Pts',(-211.394203146325,-4.66032789875526,
129.226737495149));
#127362=CARTESIAN_POINT('Ctrl Pts',(-211.401850330086,-4.70205519260479,
129.35583315652));
#127363=CARTESIAN_POINT('Ctrl Pts',(-211.409497513846,-4.73837648641222,
129.486418534045));
#127364=CARTESIAN_POINT('Ctrl Pts',(-211.411367782625,-4.74725957121321,
129.518355749401));
#127365=CARTESIAN_POINT('Ctrl Pts',(-211.413238051405,-4.75581953262355,
129.550381996406));
#127366=CARTESIAN_POINT('Ctrl Pts',(-211.415108320184,-4.76405452823408,
129.582490119308));
#127367=CARTESIAN_POINT('Ctrl Pts',(-209.665424299527,-4.76405452823394,
129.582490119308));
#127368=CARTESIAN_POINT('Ctrl Pts',(-209.673625365142,-4.80001947035231,
129.722716882783));
#127369=CARTESIAN_POINT('Ctrl Pts',(-209.681826430757,-4.82982807170211,
129.86468490532));
#127370=CARTESIAN_POINT('Ctrl Pts',(-209.690027496371,-4.85332304546196,
130.007844152647));
#127371=CARTESIAN_POINT('Ctrl Pts',(-209.698210356522,-4.87676586296161,
130.150685602174));
#127372=CARTESIAN_POINT('Ctrl Pts',(-209.706393216672,-4.89392295084962,
130.294712688466));
#127373=CARTESIAN_POINT('Ctrl Pts',(-209.714576076822,-4.90468758703764,
130.439363718868));
#127374=CARTESIAN_POINT('Ctrl Pts',(-209.72143090587,-4.91370518473249,
130.560538719633));
#127375=CARTESIAN_POINT('Ctrl Pts',(-209.728285734918,-4.91823771204663,
130.68215121371));
#127376=CARTESIAN_POINT('Ctrl Pts',(-209.735140563965,-4.91824997503721,
130.803865091054));
#127377=CARTESIAN_POINT('',(-209.389859436045,-4.91824827956038,130.80024684784));
#127378=CARTESIAN_POINT('Ctrl Pts',(-209.319824802869,-4.76405452823398,
129.582490119308));
#127379=CARTESIAN_POINT('Ctrl Pts',(-209.327257022651,-4.79654595171651,
129.70917368634));
#127380=CARTESIAN_POINT('Ctrl Pts',(-209.334689242432,-4.82393958829447,
129.836993228704));
#127381=CARTESIAN_POINT('Ctrl Pts',(-209.342121462214,-4.84618427704989,
129.965503648009));
#127382=CARTESIAN_POINT('Ctrl Pts',(-209.354271274709,-4.8825487556775,
130.17558590394));
#127383=CARTESIAN_POINT('Ctrl Pts',(-209.366421087205,-4.90525992748157,
130.388095669113));
#127384=CARTESIAN_POINT('Ctrl Pts',(-209.378570899701,-4.91406934757996,
130.601615680083));
#127385=CARTESIAN_POINT('Ctrl Pts',(-209.382333745132,-4.91679766015132,
130.667743679844));
#127386=CARTESIAN_POINT('Ctrl Pts',(-209.386096590564,-4.91819284223868,
130.7339683558));
#127387=CARTESIAN_POINT('Ctrl Pts',(-209.389859435995,-4.91824827955965,
130.800246846965));
#127388=CARTESIAN_POINT('Ctrl Pts',(-209.389859436045,-4.91824827956038,
130.80024684784));
#127389=CARTESIAN_POINT('Ctrl Pts',(-209.397506456235,-4.91836094170136,
130.934940916295));
#127390=CARTESIAN_POINT('Ctrl Pts',(-209.405153476426,-4.91293622999767,
131.069832323817));
#127391=CARTESIAN_POINT('Ctrl Pts',(-209.412800496617,-4.90195219649436,
131.204420270348));
#127392=CARTESIAN_POINT('Ctrl Pts',(-209.420440385843,-4.89097840577219,
131.338882711537));
#127393=CARTESIAN_POINT('Ctrl Pts',(-209.428080275069,-4.87445563693796,
131.473041854784));
#127394=CARTESIAN_POINT('Ctrl Pts',(-209.435720164295,-4.85241399032164,
131.606396482743));
#127395=CARTESIAN_POINT('Ctrl Pts',(-209.4434222027,-4.83019303871642,131.740835927572));
#127396=CARTESIAN_POINT('Ctrl Pts',(-209.451124241106,-4.80236300573932,
131.874457293552));
#127397=CARTESIAN_POINT('Ctrl Pts',(-209.458826279512,-4.7690082265291,
132.006751401711));
#127398=CARTESIAN_POINT('Ctrl Pts',(-209.466458640287,-4.73595519626658,
132.137848691638));
#127399=CARTESIAN_POINT('Ctrl Pts',(-209.474091001061,-4.69747708121146,
132.267642243255));
#127400=CARTESIAN_POINT('Ctrl Pts',(-209.481723361836,-4.65370724643205,
132.395646866801));
#127401=CARTESIAN_POINT('Ctrl Pts',(-209.489354909185,-4.60994207646628,
132.523637848128));
#127402=CARTESIAN_POINT('Ctrl Pts',(-209.496986456533,-4.56088643870788,
132.649839898546));
#127403=CARTESIAN_POINT('Ctrl Pts',(-209.504618003882,-4.50672322038455,
132.77378410614));
#127404=CARTESIAN_POINT('Ctrl Pts',(-209.512250504877,-4.45255323376128,
132.897743801949));
#127405=CARTESIAN_POINT('Ctrl Pts',(-209.519883005873,-4.39327455956056,
133.0194447242));
#127406=CARTESIAN_POINT('Ctrl Pts',(-209.527515506869,-4.32911753163796,
133.138439549343));
#127407=CARTESIAN_POINT('Ctrl Pts',(-209.535269971799,-4.26393530325576,
133.259335858289));
#127408=CARTESIAN_POINT('Ctrl Pts',(-209.543024436729,-4.19371767192674,
133.377438459046));
#127409=CARTESIAN_POINT('Ctrl Pts',(-209.550778901658,-4.1187531996581,
133.492306886152));
#127410=CARTESIAN_POINT('Ctrl Pts',(-209.558422540026,-4.04486011720237,
133.605533617413));
#127411=CARTESIAN_POINT('Ctrl Pts',(-209.566066178394,-3.96635527115312,
133.715617718784));
#127412=CARTESIAN_POINT('Ctrl Pts',(-209.573709816762,-3.88355647376137,
133.822169786086));
#127413=CARTESIAN_POINT('Ctrl Pts',(-209.581519694973,-3.79895690317604,
133.931039231329));
#127414=CARTESIAN_POINT('Ctrl Pts',(-209.589329573184,-3.70987474966135,
134.036220898821));
#127415=CARTESIAN_POINT('Ctrl Pts',(-209.597139451395,-3.61668886684718,
134.13733897077));
#127416=CARTESIAN_POINT('Ctrl Pts',(-209.604949329605,-3.52350298403301,
134.238457042718));
#127417=CARTESIAN_POINT('Ctrl Pts',(-209.612759207816,-3.42621373416068,
134.335511257294));
#127418=CARTESIAN_POINT('Ctrl Pts',(-209.620569086027,-3.32523510253084,
134.428170018652));
#127419=CARTESIAN_POINT('Ctrl Pts',(-209.628343420146,-3.22471604192765,
134.520407074136));
#127420=CARTESIAN_POINT('Ctrl Pts',(-209.636117754265,-3.12019708063552,
134.608604683983));
#127421=CARTESIAN_POINT('Ctrl Pts',(-209.643892088384,-3.01203655935464,
134.692395960462));
#127422=CARTESIAN_POINT('Ctrl Pts',(-209.651656841331,-2.90400933624994,
134.776083971682));
#127423=CARTESIAN_POINT('Ctrl Pts',(-209.659421594278,-2.7923497888379,
134.855376217297));
#127424=CARTESIAN_POINT('Ctrl Pts',(-209.667186347225,-2.67745232662292,
134.929943255347));
#127425=CARTESIAN_POINT('Ctrl Pts',(-209.67494338811,-2.56266898218686,
135.004436232364));
#127426=CARTESIAN_POINT('Ctrl Pts',(-209.682700428995,-2.44465444865051,
135.074213129921));
#127427=CARTESIAN_POINT('Ctrl Pts',(-209.69045746988,-2.32383508751043,
135.138985578108));
#127428=CARTESIAN_POINT('Ctrl Pts',(-209.698208661121,-2.20310683719059,
135.203709180888));
#127429=CARTESIAN_POINT('Ctrl Pts',(-209.705959852361,-2.07957831250657,
135.263435662026));
#127430=CARTESIAN_POINT('Ctrl Pts',(-209.713711043601,-1.95370334389376,
135.317920887083));
#127431=CARTESIAN_POINT('Ctrl Pts',(-209.721458940378,-1.82788187550026,
135.372382954465));
#127432=CARTESIAN_POINT('Ctrl Pts',(-209.729206837155,-1.69971630477828,
135.42160804146));
#127433=CARTESIAN_POINT('Ctrl Pts',(-209.736954733932,-1.56968326381835,
135.465398861755));
#127434=CARTESIAN_POINT('Ctrl Pts',(-209.744701010016,-1.43967742296741,
135.509180521954));
#127435=CARTESIAN_POINT('Ctrl Pts',(-209.7524472861,-1.30780525915599,135.547530051775));
#127436=CARTESIAN_POINT('Ctrl Pts',(-209.760193562184,-1.17456112701993,
135.58029918725));
#127437=CARTESIAN_POINT('Ctrl Pts',(-209.76793989545,-1.04131601130613,
135.613068564619));
#127438=CARTESIAN_POINT('Ctrl Pts',(-209.775686228715,-0.906699286711348,
135.640257372075));
#127439=CARTESIAN_POINT('Ctrl Pts',(-209.78343256198,-0.771217744846221,
135.661767976696));
#127440=CARTESIAN_POINT('Ctrl Pts',(-209.791180629983,-0.635705862828972,
135.683283398468));
#127441=CARTESIAN_POINT('Ctrl Pts',(-209.798928697986,-0.499329164215588,
135.699118025785));
#127442=CARTESIAN_POINT('Ctrl Pts',(-209.806676765989,-0.362601448238541,
135.709225880979));
#127443=CARTESIAN_POINT('Ctrl Pts',(-209.814433068731,-0.22572841641806,
135.719344478922));
#127444=CARTESIAN_POINT('Ctrl Pts',(-209.822189371473,-0.0885040125184699,
135.723724117468));
#127445=CARTESIAN_POINT('Ctrl Pts',(-209.829945674215,0.0485555029631042,
135.72237092923));
#127446=CARTESIAN_POINT('Ctrl Pts',(-209.837706116729,0.185688171234873,
135.721017018754));
#127447=CARTESIAN_POINT('Ctrl Pts',(-209.845466559243,0.322655385478393,
135.713924204827));
#127448=CARTESIAN_POINT('Ctrl Pts',(-209.853227001757,0.458945108086046,
135.70115063249));
#127449=CARTESIAN_POINT('Ctrl Pts',(-209.860999902023,0.595453615055662,
135.688356554881));
#127450=CARTESIAN_POINT('Ctrl Pts',(-209.868772802288,0.731282069464407,
135.669863548454));
#127451=CARTESIAN_POINT('Ctrl Pts',(-209.876545702554,0.865926846890192,
135.645781251877));
#127452=CARTESIAN_POINT('Ctrl Pts',(-209.884036038315,0.995676947504995,
135.622574407441));
#127453=CARTESIAN_POINT('Ctrl Pts',(-209.891526374077,1.12432763552259,
135.594177653627));
#127454=CARTESIAN_POINT('Ctrl Pts',(-209.899016709839,1.25144268444344,
135.560732582631));
#127455=CARTESIAN_POINT('Ctrl Pts',(-209.906791043958,1.38337733908158,
135.526019431602));
#127456=CARTESIAN_POINT('Ctrl Pts',(-209.914565378078,1.51407553772831,
135.485757631805));
#127457=CARTESIAN_POINT('Ctrl Pts',(-209.922339712197,1.64303491544211,
135.44005035364));
#127458=CARTESIAN_POINT('Ctrl Pts',(-209.930104465144,1.7718353622483,135.394399405609));
#127459=CARTESIAN_POINT('Ctrl Pts',(-209.937869218091,1.8989008869701,135.343316461585));
#127460=CARTESIAN_POINT('Ctrl Pts',(-209.945633971038,2.02374113278387,
135.286955278025));
#127461=CARTESIAN_POINT('Ctrl Pts',(-209.953391011923,2.14845738550555,
135.230650073188));
#127462=CARTESIAN_POINT('Ctrl Pts',(-209.961148052808,2.27095240364596,
135.169077221304));
#127463=CARTESIAN_POINT('Ctrl Pts',(-209.968905093693,2.39075311462998,
135.102439561395));
#127464=CARTESIAN_POINT('Ctrl Pts',(-209.976656284933,2.51046348296641,
135.035852153464));
#127465=CARTESIAN_POINT('Ctrl Pts',(-209.984407476173,2.62748324803347,
134.964207729093));
#127466=CARTESIAN_POINT('Ctrl Pts',(-209.992158667413,2.74136170617812,
134.887756148053));
#127467=CARTESIAN_POINT('Ctrl Pts',(-209.99990656419,2.8551917629398,134.811337060975));
#127468=CARTESIAN_POINT('Ctrl Pts',(-210.007654460968,2.9658828443485,134.730115098399));
#127469=CARTESIAN_POINT('Ctrl Pts',(-210.015402357745,3.07301133655527,
134.644384626332));
#127470=CARTESIAN_POINT('Ctrl Pts',(-210.023148633829,3.1801174197909,134.558672087232));
#127471=CARTESIAN_POINT('Ctrl Pts',(-210.030894909913,3.28366209104112,
134.468453158612));
#127472=CARTESIAN_POINT('Ctrl Pts',(-210.038641185997,3.38325340087477,
134.374063614731));
#127473=CARTESIAN_POINT('Ctrl Pts',(-210.046387519262,3.48284544586898,
134.279673374088));
#127474=CARTESIAN_POINT('Ctrl Pts',(-210.054133852528,3.57848378744892,
134.181112725696));
#127475=CARTESIAN_POINT('Ctrl Pts',(-210.061880185793,3.6698123510275,134.078755274712));
#127476=CARTESIAN_POINT('Ctrl Pts',(-210.069628253796,3.76116136700454,
133.976374901486));
#127477=CARTESIAN_POINT('Ctrl Pts',(-210.077376321799,3.84819842421281,
133.870196325401));
#127478=CARTESIAN_POINT('Ctrl Pts',(-210.085124389802,3.93060711930239,
133.76062696825));
#127479=CARTESIAN_POINT('Ctrl Pts',(-210.092880692544,4.01310339933368,
133.650941159483));
#127480=CARTESIAN_POINT('Ctrl Pts',(-210.100636995286,4.090961255481,133.537857683699));
#127481=CARTESIAN_POINT('Ctrl Pts',(-210.108393298028,4.16390679587436,
133.421814200301));
#127482=CARTESIAN_POINT('Ctrl Pts',(-210.116153740542,4.23689126949917,
133.305708781002));
#127483=CARTESIAN_POINT('Ctrl Pts',(-210.123914183056,4.30495800917251,
133.186640545366));
#127484=CARTESIAN_POINT('Ctrl Pts',(-210.13167462557,4.3678791651305,133.065071713951));
#127485=CARTESIAN_POINT('Ctrl Pts',(-210.139447525836,4.43090132771374,
132.943307729456));
#127486=CARTESIAN_POINT('Ctrl Pts',(-210.147220426101,4.4887612350593,132.819035482209));
#127487=CARTESIAN_POINT('Ctrl Pts',(-210.154993326366,4.54127890798377,
132.692737948081));
#127488=CARTESIAN_POINT('Ctrl Pts',(-210.162483662128,4.59188743121382,
132.571031647441));
#127489=CARTESIAN_POINT('Ctrl Pts',(-210.169973997891,4.63753527733388,
132.447445040966));
#127490=CARTESIAN_POINT('Ctrl Pts',(-210.177464333653,4.67810578079159,
132.322421672407));
#127491=CARTESIAN_POINT('Ctrl Pts',(-210.185238667772,4.72021452721886,
132.192658004829));
#127492=CARTESIAN_POINT('Ctrl Pts',(-210.193013001891,4.75698670362623,
132.060935422502));
#127493=CARTESIAN_POINT('Ctrl Pts',(-210.20078733601,4.78823756967018,131.927732345401));
#127494=CARTESIAN_POINT('Ctrl Pts',(-210.208552088957,4.81944992181453,
131.794693429188));
#127495=CARTESIAN_POINT('Ctrl Pts',(-210.216316841904,4.84515441412268,
131.660178025542));
#127496=CARTESIAN_POINT('Ctrl Pts',(-210.224081594851,4.86521535641737,
131.524681794667));
#127497=CARTESIAN_POINT('Ctrl Pts',(-210.231838635736,4.88525637390142,
131.389320140559));
#127498=CARTESIAN_POINT('Ctrl Pts',(-210.239595676621,4.89966493918948,
131.252979982114));
#127499=CARTESIAN_POINT('Ctrl Pts',(-210.247352717506,4.90835599921353,
131.116168968135));
#127500=CARTESIAN_POINT('Ctrl Pts',(-210.255103908746,4.91704050524162,
130.979461124405));
#127501=CARTESIAN_POINT('Ctrl Pts',(-210.262855099986,4.92001606332805,
130.842283520498));
#127502=CARTESIAN_POINT('Ctrl Pts',(-210.270606291227,4.9172492712412,130.70515040147));
#127503=CARTESIAN_POINT('Ctrl Pts',(-210.278354188004,4.91448365511481,
130.568075567676));
#127504=CARTESIAN_POINT('Ctrl Pts',(-210.286102084781,4.9059805509559,130.431045571223));
#127505=CARTESIAN_POINT('Ctrl Pts',(-210.293849981558,4.8917586435896,130.294575922458));
#127506=CARTESIAN_POINT('Ctrl Pts',(-210.301596257642,4.87753971113974,
130.158134820201));
#127507=CARTESIAN_POINT('Ctrl Pts',(-210.309342533726,4.85760439538852,
130.022254221102));
#127508=CARTESIAN_POINT('Ctrl Pts',(-210.31708880981,4.83202333448889,129.887445377506));
#127509=CARTESIAN_POINT('Ctrl Pts',(-210.324835143075,4.80644208475572,
129.752635538782));
#127510=CARTESIAN_POINT('Ctrl Pts',(-210.332581476341,4.77521507960163,
129.618897855459));
#127511=CARTESIAN_POINT('Ctrl Pts',(-210.340327809606,4.73846417661337,
129.486733845885));
#127512=CARTESIAN_POINT('Ctrl Pts',(-210.348075877609,4.70170504351525,
129.354540239097));
#127513=CARTESIAN_POINT('Ctrl Pts',(-210.355823945612,4.65941965574108,
129.22392138392));
#127514=CARTESIAN_POINT('Ctrl Pts',(-210.363572013615,4.61177976504491,
129.095363700886));
#127515=CARTESIAN_POINT('Ctrl Pts',(-210.371328316357,4.56408924210593,
128.966669385216));
#127516=CARTESIAN_POINT('Ctrl Pts',(-210.379084619098,4.51103298426964,
128.840040984911));
#127517=CARTESIAN_POINT('Ctrl Pts',(-210.38684092184,4.45283116154137,128.715945498557));
#127518=CARTESIAN_POINT('Ctrl Pts',(-210.394601364354,4.39459827474774,
128.591783778705));
#127519=CARTESIAN_POINT('Ctrl Pts',(-210.402361806869,4.33121453133613,
128.470158013103));
#127520=CARTESIAN_POINT('Ctrl Pts',(-210.410122249383,4.26294565218836,
128.351509739712));
#127521=CARTESIAN_POINT('Ctrl Pts',(-210.417895149648,4.19456718177516,
128.23267100158));
#127522=CARTESIAN_POINT('Ctrl Pts',(-210.425668049914,4.12128811382067,
128.116819637697));
#127523=CARTESIAN_POINT('Ctrl Pts',(-210.433440950179,4.04341750645725,
128.004368129902));
#127524=CARTESIAN_POINT('Ctrl Pts',(-210.440931285941,3.96837769181507,
127.896004517663));
#127525=CARTESIAN_POINT('Ctrl Pts',(-210.448421621703,3.88907455547164,
127.790798112337));
#127526=CARTESIAN_POINT('Ctrl Pts',(-210.455911957465,3.80581820276506,
127.68908681419));
#127527=CARTESIAN_POINT('Ctrl Pts',(-210.463686291584,3.71940516014076,
127.583519101259));
#127528=CARTESIAN_POINT('Ctrl Pts',(-210.471460625704,3.6284594806104,127.481382354555));
#127529=CARTESIAN_POINT('Ctrl Pts',(-210.479234959823,3.53328381577912,
127.383090599042));
#127530=CARTESIAN_POINT('Ctrl Pts',(-210.48699971277,3.43822544644917,127.284919979333));
#127531=CARTESIAN_POINT('Ctrl Pts',(-210.494764465717,3.33894773364673,
127.190585200573));
#127532=CARTESIAN_POINT('Ctrl Pts',(-210.502529218664,3.23579434648503,
127.100468339198));
#127533=CARTESIAN_POINT('Ctrl Pts',(-210.510286259549,3.13274341272166,
127.01044098316));
#127534=CARTESIAN_POINT('Ctrl Pts',(-210.518043300434,3.02582475755512,
126.924623463178));
#127535=CARTESIAN_POINT('Ctrl Pts',(-210.525800341319,2.91541950703893,
126.843361733386));
#127536=CARTESIAN_POINT('Ctrl Pts',(-210.533551532559,2.80509751398143,
126.762161283696));
#127537=CARTESIAN_POINT('Ctrl Pts',(-210.541302723799,2.6912944725708,126.685510016745));
#127538=CARTESIAN_POINT('Ctrl Pts',(-210.549053915039,2.57442497701588,
126.613713996791));
#127539=CARTESIAN_POINT('Ctrl Pts',(-210.556801811817,2.45760515411368,
126.541948492059));
#127540=CARTESIAN_POINT('Ctrl Pts',(-210.564549708594,2.33772180170944,
126.475034334182));
#127541=CARTESIAN_POINT('Ctrl Pts',(-210.572297605371,2.21521873286088,
126.413234449021));
#127542=CARTESIAN_POINT('Ctrl Pts',(-210.580043881455,2.09274128901346,
126.351447491063));
#127543=CARTESIAN_POINT('Ctrl Pts',(-210.587790157539,1.96764556754184,
126.29477285392));
#127544=CARTESIAN_POINT('Ctrl Pts',(-210.595536433623,1.84039988117138,
126.243427452096));
#127545=CARTESIAN_POINT('Ctrl Pts',(-210.603282766888,1.71315325550235,
126.192081671251));
#127546=CARTESIAN_POINT('Ctrl Pts',(-210.611029100154,1.58375699582705,
126.146065350522));
#127547=CARTESIAN_POINT('Ctrl Pts',(-210.618775433419,1.45269891073695,
126.105547050585));
#127548=CARTESIAN_POINT('Ctrl Pts',(-210.626523501422,1.32161147609756,
126.065019676856));
#127549=CARTESIAN_POINT('Ctrl Pts',(-210.634271569425,1.18886184894955,
126.029992889409));
#127550=CARTESIAN_POINT('Ctrl Pts',(-210.642019637428,1.05495210467951,
126.000585110808));
#127551=CARTESIAN_POINT('Ctrl Pts',(-210.64977594017,0.920900039539174,
125.971146077269));
#127552=CARTESIAN_POINT('Ctrl Pts',(-210.657532242912,0.785685776728094,
125.947338066182));
#127553=CARTESIAN_POINT('Ctrl Pts',(-210.665288545654,0.649821222647911,
125.92922826643));
#127554=CARTESIAN_POINT('Ctrl Pts',(-210.673048988168,0.513884153564413,
125.911108800932));
#127555=CARTESIAN_POINT('Ctrl Pts',(-210.680809430682,0.377296490795038,
125.898693642202));
#127556=CARTESIAN_POINT('Ctrl Pts',(-210.688569873196,0.240573341358052,
125.891997893792));
#127557=CARTESIAN_POINT('Ctrl Pts',(-210.696342773462,0.103630711783879,
125.885291396771));
#127558=CARTESIAN_POINT('Ctrl Pts',(-210.704115673727,-0.033447447902223,
125.884322660007));
#127559=CARTESIAN_POINT('Ctrl Pts',(-210.711888573992,-0.17014705157744,
125.889054620648));
#127560=CARTESIAN_POINT('Ctrl Pts',(-210.719378909755,-0.301877280334283,
125.893614562601));
#127561=CARTESIAN_POINT('Ctrl Pts',(-210.726869245517,-0.433255691014989,
125.9034679053));
#127562=CARTESIAN_POINT('Ctrl Pts',(-210.734359581279,-0.563830379047278,
125.918536391689));
#127563=CARTESIAN_POINT('Ctrl Pts',(-210.742133915398,-0.699355846063048,
125.93417620432));
#127564=CARTESIAN_POINT('Ctrl Pts',(-210.749908249517,-0.834444744985957,
125.955483973802));
#127565=CARTESIAN_POINT('Ctrl Pts',(-210.757682583636,-0.968585154302004,
125.982428861375));
#127566=CARTESIAN_POINT('Ctrl Pts',(-210.765447336583,-1.10256024755131,
126.009340541782));
#127567=CARTESIAN_POINT('Ctrl Pts',(-210.77321208953,-1.23558879738455,
126.041875441078));
#127568=CARTESIAN_POINT('Ctrl Pts',(-210.780976842477,-1.36716359052389,
126.079950942353));
#127569=CARTESIAN_POINT('Ctrl Pts',(-210.788733883362,-1.49860770172451,
126.117988626503));
#127570=CARTESIAN_POINT('Ctrl Pts',(-210.796490924247,-1.62860055651468,
126.161555853429));
#127571=CARTESIAN_POINT('Ctrl Pts',(-210.804247965132,-1.75664508594344,
126.210518967647));
#127572=CARTESIAN_POINT('Ctrl Pts',(-210.811999156372,-1.88459305599669,
126.259445158399));
#127573=CARTESIAN_POINT('Ctrl Pts',(-210.819750347612,-2.01059526143671,
126.31375899811));
#127574=CARTESIAN_POINT('Ctrl Pts',(-210.827501538852,-2.13417010343808,
126.373277112136));
#127575=CARTESIAN_POINT('Ctrl Pts',(-210.835249435629,-2.25769242283462,
126.432769929376));
#127576=CARTESIAN_POINT('Ctrl Pts',(-210.842997332407,-2.3787890792521,
126.497462452225));
#127577=CARTESIAN_POINT('Ctrl Pts',(-210.850745229184,-2.49699897391876,
126.567123406039));
#127578=CARTESIAN_POINT('Ctrl Pts',(-210.858491505268,-2.61518414162376,
126.636769788283));
#127579=CARTESIAN_POINT('Ctrl Pts',(-210.866237781352,-2.73048341204913,
126.711382335922));
#127580=CARTESIAN_POINT('Ctrl Pts',(-210.873984057436,-2.84246115441336,
126.790684291783));
#127581=CARTESIAN_POINT('Ctrl Pts',(-210.881730390701,-2.9544397233717,
126.869986833033));
#127582=CARTESIAN_POINT('Ctrl Pts',(-210.889476723967,-3.06309639628533,
126.953978625625));
#127583=CARTESIAN_POINT('Ctrl Pts',(-210.897223057232,-3.16802568582288,
127.042340373539));
#127584=CARTESIAN_POINT('Ctrl Pts',(-210.904971125235,-3.272978473548,127.130721909455));
#127585=CARTESIAN_POINT('Ctrl Pts',(-210.912719193238,-3.37420191790143,
127.223475096248));
#127586=CARTESIAN_POINT('Ctrl Pts',(-210.920467261241,-3.47132500261658,
127.320241533966));
#127587=CARTESIAN_POINT('Ctrl Pts',(-210.928223563983,-3.56855131090154,
127.417110816204));
#127588=CARTESIAN_POINT('Ctrl Pts',(-210.935979866725,-3.66166827674774,
127.518001593439));
#127589=CARTESIAN_POINT('Ctrl Pts',(-210.943736169466,-3.75034267433231,
127.622519501548));
#127590=CARTESIAN_POINT('Ctrl Pts',(-210.951496611981,-3.8390644001128,
127.727093194012));
#127591=CARTESIAN_POINT('Ctrl Pts',(-210.959257054495,-3.92333859283302,
127.835297566513));
#127592=CARTESIAN_POINT('Ctrl Pts',(-210.967017497009,-4.00287411752363,
127.946707408767));
#127593=CARTESIAN_POINT('Ctrl Pts',(-210.974790397274,-4.08253731969931,
128.05829609599));
#127594=CARTESIAN_POINT('Ctrl Pts',(-210.98256329754,-4.15744643900569,
128.173100208105));
#127595=CARTESIAN_POINT('Ctrl Pts',(-210.990336197805,-4.22735478136186,
128.290667196523));
#127596=CARTESIAN_POINT('Ctrl Pts',(-210.997826533567,-4.29472177938432,
128.403960328777));
#127597=CARTESIAN_POINT('Ctrl Pts',(-211.005316869329,-4.3574451231781,
128.519818678921));
#127598=CARTESIAN_POINT('Ctrl Pts',(-211.012807205091,-4.41534638716189,
128.63781974699));
#127599=CARTESIAN_POINT('Ctrl Pts',(-211.021162556032,-4.47993433033233,
128.769448070002));
#127600=CARTESIAN_POINT('Ctrl Pts',(-211.029517906973,-4.53870371440234,
128.904111953051));
#127601=CARTESIAN_POINT('Ctrl Pts',(-211.037873257915,-4.59138038536787,
129.041292490873));
#127602=CARTESIAN_POINT('Ctrl Pts',(-211.046207800767,-4.64392587083518,
129.178131395543));
#127603=CARTESIAN_POINT('Ctrl Pts',(-211.054542343618,-4.69040879233743,
129.317474177873));
#127604=CARTESIAN_POINT('Ctrl Pts',(-211.06287688647,-4.73060208665202,
129.458780088477));
#127605=CARTESIAN_POINT('Ctrl Pts',(-211.065299612346,-4.74228567097247,
129.499855585016));
#127606=CARTESIAN_POINT('Ctrl Pts',(-211.067722338222,-4.75343809550135,
129.54109680921));
#127607=CARTESIAN_POINT('Ctrl Pts',(-211.070145064099,-4.76405452823395,
129.582490119308));
#127608=CARTESIAN_POINT('Origin',(213.235140564004,0.,130.804360617566));
#127609=CARTESIAN_POINT('',(-213.165046531412,-4.76405452823396,129.582490119308));
#127610=CARTESIAN_POINT('',(-212.819861628446,-4.76405452823406,129.582490119308));
#127611=CARTESIAN_POINT('',(213.235140564004,-4.76405452823405,129.582490119308));
#127612=CARTESIAN_POINT('',(-211.485140564044,-4.91824790103933,130.808904450997));
#127613=CARTESIAN_POINT('Ctrl Pts',(-211.485140564044,-4.91824790103933,
130.808904450997));
#127614=CARTESIAN_POINT('Ctrl Pts',(-211.495366712974,-4.91808111918583,
130.98942922449));
#127615=CARTESIAN_POINT('Ctrl Pts',(-211.505592861904,-4.90797173471146,
131.169512207673));
#127616=CARTESIAN_POINT('Ctrl Pts',(-211.515819010834,-4.88808531502141,
131.348240214142));
#127617=CARTESIAN_POINT('Ctrl Pts',(-211.526332245936,-4.86764060929875,
131.531985782908));
#127618=CARTESIAN_POINT('Ctrl Pts',(-211.536845481038,-4.8368621460543,
131.714299654373));
#127619=CARTESIAN_POINT('Ctrl Pts',(-211.547358716141,-4.79597733691819,
131.894215858535));
#127620=CARTESIAN_POINT('Ctrl Pts',(-211.548276962946,-4.79240637659797,
131.909930096649));
#127621=CARTESIAN_POINT('Ctrl Pts',(-211.549195209752,-4.78875834852051,
131.925626057538));
#127622=CARTESIAN_POINT('Ctrl Pts',(-211.550113456558,-4.7850334212715,
131.941303105036));
#127623=CARTESIAN_POINT('Ctrl Pts',(-211.557887790677,-4.75349633470017,
132.074032785663));
#127624=CARTESIAN_POINT('Ctrl Pts',(-211.565662124796,-4.71638252570012,
132.205659518639));
#127625=CARTESIAN_POINT('Ctrl Pts',(-211.573436458915,-4.67378307958606,
132.335678607885));
#127626=CARTESIAN_POINT('Ctrl Pts',(-211.581201211862,-4.63123613348211,
132.465537460224));
#127627=CARTESIAN_POINT('Ctrl Pts',(-211.588965964809,-4.58321712231859,
132.593792243019));
#127628=CARTESIAN_POINT('Ctrl Pts',(-211.596730717756,-4.52986799106473,
132.719949050927));
#127629=CARTESIAN_POINT('Ctrl Pts',(-211.604487758641,-4.47657184692026,
132.845980558115));
#127630=CARTESIAN_POINT('Ctrl Pts',(-211.612244799526,-4.4179562691757,
132.969917879386));
#127631=CARTESIAN_POINT('Ctrl Pts',(-211.620001840411,-4.35421268600348,
133.091283210822));
#127632=CARTESIAN_POINT('Ctrl Pts',(-211.627753031651,-4.2905171723631,
133.212557019718));
#127633=CARTESIAN_POINT('Ctrl Pts',(-211.635504222891,-4.2217015315191,
133.331262354623));
#127634=CARTESIAN_POINT('Ctrl Pts',(-211.643255414131,-4.14800473564428,
133.446942645729));
#127635=CARTESIAN_POINT('Ctrl Pts',(-211.651003310908,-4.07433926287374,
133.562573769626));
#127636=CARTESIAN_POINT('Ctrl Pts',(-211.658751207686,-3.9957969709619,
133.675182077886));
#127637=CARTESIAN_POINT('Ctrl Pts',(-211.666499104463,-3.9126619755804,
133.784337014678));
#127638=CARTESIAN_POINT('Ctrl Pts',(-211.674245380547,-3.82954437024774,
133.893469118611));
#127639=CARTESIAN_POINT('Ctrl Pts',(-211.681991656631,-3.741836209056,133.99914897708));
#127640=CARTESIAN_POINT('Ctrl Pts',(-211.689737932715,-3.64986376386465,
134.100976695869));
#127641=CARTESIAN_POINT('Ctrl Pts',(-211.69748426598,-3.55789063975373,
134.202805166328));
#127642=CARTESIAN_POINT('Ctrl Pts',(-211.705230599245,-3.46165343088827,
134.300781150227));
#127643=CARTESIAN_POINT('Ctrl Pts',(-211.712976932511,-3.36151709002681,
134.394539710029));
#127644=CARTESIAN_POINT('Ctrl Pts',(-211.720725000514,-3.26135832432624,
134.48831926641));
#127645=CARTESIAN_POINT('Ctrl Pts',(-211.728473068517,-3.15729897443404,
134.577879252155));
#127646=CARTESIAN_POINT('Ctrl Pts',(-211.73622113652,-3.04973875200786,
134.662893578032));
#127647=CARTESIAN_POINT('Ctrl Pts',(-211.743977439262,-2.94206421329685,
134.747998258146));
#127648=CARTESIAN_POINT('Ctrl Pts',(-211.751733742003,-2.83088167662946,
134.828547384768));
#127649=CARTESIAN_POINT('Ctrl Pts',(-211.759490044745,-2.71662210272428,
134.904256642283));
#127650=CARTESIAN_POINT('Ctrl Pts',(-211.767250487259,-2.60230154504422,
134.980006308108));
#127651=CARTESIAN_POINT('Ctrl Pts',(-211.775010929774,-2.48490101219084,
135.05091075559));
#127652=CARTESIAN_POINT('Ctrl Pts',(-211.782771372288,-2.36487712384615,
135.116731108562));
#127653=CARTESIAN_POINT('Ctrl Pts',(-211.790544272553,-2.24466056250067,
135.182657122207));
#127654=CARTESIAN_POINT('Ctrl Pts',(-211.798317172819,-2.12181258082996,
135.243482558607));
#127655=CARTESIAN_POINT('Ctrl Pts',(-211.806090073084,-1.99681169661381,
135.299015900318));
#127656=CARTESIAN_POINT('Ctrl Pts',(-211.813580408846,-1.87635490939715,
135.352530465177));
#127657=CARTESIAN_POINT('Ctrl Pts',(-211.821070744608,-1.7538993152546,
135.401130903635));
#127658=CARTESIAN_POINT('Ctrl Pts',(-211.82856108037,-1.62988553055513,
135.444689939908));
#127659=CARTESIAN_POINT('Ctrl Pts',(-211.836335414489,-1.50116972551577,
135.489900530281));
#127660=CARTESIAN_POINT('Ctrl Pts',(-211.844109748608,-1.37036750688096,
135.529823095987));
#127661=CARTESIAN_POINT('Ctrl Pts',(-211.851884082727,-1.23795272359228,
135.564261469123));
#127662=CARTESIAN_POINT('Ctrl Pts',(-211.859648835674,-1.10570112969012,
135.598657400042));
#127663=CARTESIAN_POINT('Ctrl Pts',(-211.867413588621,-0.971841300097183,
135.627582488879));
#127664=CARTESIAN_POINT('Ctrl Pts',(-211.875178341568,-0.836865496090621,
135.650889190055));
#127665=CARTESIAN_POINT('Ctrl Pts',(-211.882935382453,-0.702023751955058,
135.674172742687));
#127666=CARTESIAN_POINT('Ctrl Pts',(-211.890692423338,-0.566068621945752,
135.691848946536));
#127667=CARTESIAN_POINT('Ctrl Pts',(-211.898449464223,-0.429505567635087,
135.703820590856));
#127668=CARTESIAN_POINT('Ctrl Pts',(-211.906200655464,-0.29304549658617,
135.715783207266));
#127669=CARTESIAN_POINT('Ctrl Pts',(-211.913951846704,-0.155978801629436,
135.722049792719));
#127670=CARTESIAN_POINT('Ctrl Pts',(-211.921703037944,-0.0188187781709079,
135.722574614139));
#127671=CARTESIAN_POINT('Ctrl Pts',(-211.929450934721,0.1182829486186,135.723099212496));
#127672=CARTESIAN_POINT('Ctrl Pts',(-211.937198831498,0.25547753487123,
135.717886899103));
#127673=CARTESIAN_POINT('Ctrl Pts',(-211.944946728275,0.392249170311845,
135.706943982578));
#127674=CARTESIAN_POINT('Ctrl Pts',(-211.952693004359,0.528992196074782,
135.696003355074));
#127675=CARTESIAN_POINT('Ctrl Pts',(-211.960439280443,0.665312057528826,
135.679334539916));
#127676=CARTESIAN_POINT('Ctrl Pts',(-211.968185556527,0.800695954434944,
135.656995886268));
#127677=CARTESIAN_POINT('Ctrl Pts',(-211.975931889793,0.936080850714418,
135.634657067721));
#127678=CARTESIAN_POINT('Ctrl Pts',(-211.983678223058,1.07052938291009,
135.606648390818));
#127679=CARTESIAN_POINT('Ctrl Pts',(-211.991424556323,1.20353725285352,
135.573079642996));
#127680=CARTESIAN_POINT('Ctrl Pts',(-211.999172624326,1.3365749089874,135.539503377685));
#127681=CARTESIAN_POINT('Ctrl Pts',(-212.006920692329,1.46817088187399,
135.500364659427));
#127682=CARTESIAN_POINT('Ctrl Pts',(-212.014668760332,1.59783476949158,
135.455823517762));
#127683=CARTESIAN_POINT('Ctrl Pts',(-212.022425063074,1.72763646543178,
135.411235037243));
#127684=CARTESIAN_POINT('Ctrl Pts',(-212.030181365816,1.85550160378182,
135.361232790753));
#127685=CARTESIAN_POINT('Ctrl Pts',(-212.037937668558,1.98095803696752,
135.306025678216));
#127686=CARTESIAN_POINT('Ctrl Pts',(-212.045698111072,2.10648143002903,
135.25078909998));
#127687=CARTESIAN_POINT('Ctrl Pts',(-212.053458553586,2.22959320548871,
135.190342292537));
#127688=CARTESIAN_POINT('Ctrl Pts',(-212.0612189961,2.34984557596974,135.124940304552));
#127689=CARTESIAN_POINT('Ctrl Pts',(-212.068991896365,2.47029098623136,
135.05943332749));
#127690=CARTESIAN_POINT('Ctrl Pts',(-212.076764796631,2.58786748336211,
134.988955475393));
#127691=CARTESIAN_POINT('Ctrl Pts',(-212.084537696896,2.70215528776471,
134.913805818965));
#127692=CARTESIAN_POINT('Ctrl Pts',(-212.092028032659,2.81228844260644,
134.841388041838));
#127693=CARTESIAN_POINT('Ctrl Pts',(-212.099518368421,2.91936760769774,
134.764632406479));
#127694=CARTESIAN_POINT('Ctrl Pts',(-212.107008704183,3.02304753840801,
134.683840820251));
#127695=CARTESIAN_POINT('Ctrl Pts',(-212.114783038302,3.13065852520142,
134.599985996477));
#127696=CARTESIAN_POINT('Ctrl Pts',(-212.122557372421,3.23494830458973,
134.511517507355));
#127697=CARTESIAN_POINT('Ctrl Pts',(-212.13033170654,3.335495708033,134.418727981877));
#127698=CARTESIAN_POINT('Ctrl Pts',(-212.138096459487,3.4359191957877,134.326052811196));
#127699=CARTESIAN_POINT('Ctrl Pts',(-212.145861212434,3.53260919983123,
134.229067462502));
#127700=CARTESIAN_POINT('Ctrl Pts',(-212.153625965381,3.62517550664391,
134.128106337161));
#127701=CARTESIAN_POINT('Ctrl Pts',(-212.161383006266,3.7176498752957,134.027245487833));
#127702=CARTESIAN_POINT('Ctrl Pts',(-212.169140047151,3.8060084348688,133.922417006453));
#127703=CARTESIAN_POINT('Ctrl Pts',(-212.176897088036,3.88989618488271,
133.813993607373));
#127704=CARTESIAN_POINT('Ctrl Pts',(-212.184648279277,3.97372067449189,
133.705651971222));
#127705=CARTESIAN_POINT('Ctrl Pts',(-212.192399470517,4.053080826977,133.593721121331));
#127706=CARTESIAN_POINT('Ctrl Pts',(-212.200150661757,4.12766071710104,
133.478608187818));
#127707=CARTESIAN_POINT('Ctrl Pts',(-212.207898558534,4.20220890878219,
133.363544180373));
#127708=CARTESIAN_POINT('Ctrl Pts',(-212.215646455311,4.27198066693807,
133.245301106699));
#127709=CARTESIAN_POINT('Ctrl Pts',(-212.223394352088,4.33670249113417,
133.124316342551));
#127710=CARTESIAN_POINT('Ctrl Pts',(-212.231140628172,4.40141077691988,
133.003356885807));
#127711=CARTESIAN_POINT('Ctrl Pts',(-212.238886904256,4.46107104555584,
132.879657223835));
#127712=CARTESIAN_POINT('Ctrl Pts',(-212.246633180341,4.51545520679142,
132.753680329148));
#127713=CARTESIAN_POINT('Ctrl Pts',(-212.254379513606,4.56983976947861,
132.627702504527));
#127714=CARTESIAN_POINT('Ctrl Pts',(-212.262125846871,4.61894799209267,
132.499447772594));
#127715=CARTESIAN_POINT('Ctrl Pts',(-212.269872180137,4.66259965643574,
132.369399756471));
#127716=CARTESIAN_POINT('Ctrl Pts',(-212.277620248139,4.70626109626633,
132.239322616997));
#127717=CARTESIAN_POINT('Ctrl Pts',(-212.285368316143,4.74446342188477,
132.107451764781));
#127718=CARTESIAN_POINT('Ctrl Pts',(-212.293116384146,4.77707619640578,
131.974286288809));
#127719=CARTESIAN_POINT('Ctrl Pts',(-212.300872686887,4.8097236321717,131.840979282984));
#127720=CARTESIAN_POINT('Ctrl Pts',(-212.308628989629,4.83676955662014,
131.70637528516));
#127721=CARTESIAN_POINT('Ctrl Pts',(-212.316385292371,4.85813451587632,
131.570984441975));
#127722=CARTESIAN_POINT('Ctrl Pts',(-212.324145734885,4.87951087825454,
131.43552133662));
#127723=CARTESIAN_POINT('Ctrl Pts',(-212.331906177399,4.89520018901777,
131.2992709373));
#127724=CARTESIAN_POINT('Ctrl Pts',(-212.339666619914,4.90517498781803,
131.162747840252));
#127725=CARTESIAN_POINT('Ctrl Pts',(-212.347439520179,4.91516579905085,
131.026005584208));
#127726=CARTESIAN_POINT('Ctrl Pts',(-212.355212420445,4.91942375470973,
130.888990146657));
#127727=CARTESIAN_POINT('Ctrl Pts',(-212.36298532071,4.91797357032243,130.752216355082));
#127728=CARTESIAN_POINT('Ctrl Pts',(-212.370475656472,4.91657610379041,
130.620414635343));
#127729=CARTESIAN_POINT('Ctrl Pts',(-212.377965992234,4.9098783182167,130.488837605343));
#127730=CARTESIAN_POINT('Ctrl Pts',(-212.385456327996,4.89794760365846,
130.35793891747));
#127731=CARTESIAN_POINT('Ctrl Pts',(-212.393230662115,4.88556453243154,
130.222077166062));
#127732=CARTESIAN_POINT('Ctrl Pts',(-212.401004996234,4.86750466015426,
130.086515841689));
#127733=CARTESIAN_POINT('Ctrl Pts',(-212.408779330353,4.84378653200132,
129.95176745849));
#127734=CARTESIAN_POINT('Ctrl Pts',(-212.4165440833,4.82009763432157,129.817185140631));
#127735=CARTESIAN_POINT('Ctrl Pts',(-212.424308836247,4.79076442266846,
129.683414151859));
#127736=CARTESIAN_POINT('Ctrl Pts',(-212.432073589195,4.75585731844136,
129.550963541964));
#127737=CARTESIAN_POINT('Ctrl Pts',(-212.43983063008,4.72098488444229,129.418644483882));
#127738=CARTESIAN_POINT('Ctrl Pts',(-212.447587670965,4.68054967388698,
129.287643570505));
#127739=CARTESIAN_POINT('Ctrl Pts',(-212.45534471185,4.63467337548564,129.158460935002));
#127740=CARTESIAN_POINT('Ctrl Pts',(-212.46309590309,4.58883167275773,129.029375717129));
#127741=CARTESIAN_POINT('Ctrl Pts',(-212.47084709433,4.5375571795959,128.902106414819));
#127742=CARTESIAN_POINT('Ctrl Pts',(-212.47859828557,4.48102166079118,128.777138888692));
#127743=CARTESIAN_POINT('Ctrl Pts',(-212.486346182347,4.42451017109,128.652224477097));
#127744=CARTESIAN_POINT('Ctrl Pts',(-212.494094079124,4.36274226394313,
128.529610251353));
#127745=CARTESIAN_POINT('Ctrl Pts',(-212.501841975901,4.29593808229475,
128.4097627274));
#127746=CARTESIAN_POINT('Ctrl Pts',(-212.509588251985,4.22914787464121,
128.289940272965));
#127747=CARTESIAN_POINT('Ctrl Pts',(-212.517334528069,4.15732367814835,
128.172883710467));
#127748=CARTESIAN_POINT('Ctrl Pts',(-212.525080804154,4.08073171635147,
128.059035186645));
#127749=CARTESIAN_POINT('Ctrl Pts',(-212.532827137419,4.00413918917002,
127.945185822418));
#127750=CARTESIAN_POINT('Ctrl Pts',(-212.540573470684,3.9227790446898,127.83454486851));
#127751=CARTESIAN_POINT('Ctrl Pts',(-212.54831980395,3.83696075640322,127.727525357705));
#127752=CARTESIAN_POINT('Ctrl Pts',(-212.556067871953,3.75112324970611,
127.620481880623));
#127753=CARTESIAN_POINT('Ctrl Pts',(-212.563815939956,3.66082585710043,
127.517061765387));
#127754=CARTESIAN_POINT('Ctrl Pts',(-212.571564007959,3.56641797196269,
127.41764452203));
#127755=CARTESIAN_POINT('Ctrl Pts',(-212.5793203107,3.47190974900103,127.318121616844));
#127756=CARTESIAN_POINT('Ctrl Pts',(-212.587076613442,3.37328257624632,
127.222610365916));
#127757=CARTESIAN_POINT('Ctrl Pts',(-212.594832916184,3.27092270775256,
127.13145336276));
#127758=CARTESIAN_POINT('Ctrl Pts',(-212.602593358698,3.168508206715,127.040247706366));
#127759=CARTESIAN_POINT('Ctrl Pts',(-212.610353801213,3.06235734265556,
126.953401175943));
#127760=CARTESIAN_POINT('Ctrl Pts',(-212.618114243727,2.95288821697341,
126.871215026495));
#127761=CARTESIAN_POINT('Ctrl Pts',(-212.625887143992,2.8432433617325,126.788896944544));
#127762=CARTESIAN_POINT('Ctrl Pts',(-212.633660044258,2.73026992268151,
126.711254415072));
#127763=CARTESIAN_POINT('Ctrl Pts',(-212.641432944523,2.61441439811064,
126.638544921036));
#127764=CARTESIAN_POINT('Ctrl Pts',(-212.648923280285,2.50277051368069,
126.568478600254));
#127765=CARTESIAN_POINT('Ctrl Pts',(-212.656413616047,2.38845071518206,
126.502993038286));
#127766=CARTESIAN_POINT('Ctrl Pts',(-212.663903951809,2.27187309918929,
126.442276748166));
#127767=CARTESIAN_POINT('Ctrl Pts',(-212.671678285928,2.15087540745265,
126.379258381452));
#127768=CARTESIAN_POINT('Ctrl Pts',(-212.679452620047,2.02706202385851,
126.321178456388));
#127769=CARTESIAN_POINT('Ctrl Pts',(-212.687226954166,1.90087416518663,
126.268298396804));
#127770=CARTESIAN_POINT('Ctrl Pts',(-212.694991707113,1.77484182177283,
126.215483507167));
#127771=CARTESIAN_POINT('Ctrl Pts',(-212.70275646006,1.64644118292491,126.167855881921));
#127772=CARTESIAN_POINT('Ctrl Pts',(-212.710521213007,1.51613859113558,
126.125631427394));
#127773=CARTESIAN_POINT('Ctrl Pts',(-212.718278253892,1.38596541771736,
126.08344891079));
#127774=CARTESIAN_POINT('Ctrl Pts',(-212.726035294777,1.25389442016377,
126.046659005059));
#127775=CARTESIAN_POINT('Ctrl Pts',(-212.733792335662,1.12041215039591,
126.015429664238));
#127776=CARTESIAN_POINT('Ctrl Pts',(-212.741543526903,0.987030540646194,
125.984223873706));
#127777=CARTESIAN_POINT('Ctrl Pts',(-212.749294718143,0.852240156154917,
125.958570390347));
#127778=CARTESIAN_POINT('Ctrl Pts',(-212.757045909383,0.716542608289347,
125.938587323114));
#127779=CARTESIAN_POINT('Ctrl Pts',(-212.76479380616,0.580902735501286,
125.918612749217));
#127780=CARTESIAN_POINT('Ctrl Pts',(-212.772541702937,0.444356852189445,
125.904303854824));
#127781=CARTESIAN_POINT('Ctrl Pts',(-212.780289599714,0.307416444065595,
125.895727590702));
#127782=CARTESIAN_POINT('Ctrl Pts',(-212.788035875798,0.17050468092303,
125.88715312055));
#127783=CARTESIAN_POINT('Ctrl Pts',(-212.795782151882,0.0331989470708777,
125.884308919931));
#127784=CARTESIAN_POINT('Ctrl Pts',(-212.803528427967,-0.103984866592843,
125.887209998557));
#127785=CARTESIAN_POINT('Ctrl Pts',(-212.811274761232,-0.241169692916126,
125.890111098598));
#127786=CARTESIAN_POINT('Ctrl Pts',(-212.819021094497,-0.378232206377305,
125.898757554246));
#127787=CARTESIAN_POINT('Ctrl Pts',(-212.826767427762,-0.514657632814622,
125.913112250995));
#127788=CARTESIAN_POINT('Ctrl Pts',(-212.834515495765,-0.651113610780467,
125.927470162379));
#127789=CARTESIAN_POINT('Ctrl Pts',(-212.842263563768,-0.786931829078878,
125.947538817671));
#127790=CARTESIAN_POINT('Ctrl Pts',(-212.850011631771,-0.921604139515747,
125.973229396772));
#127791=CARTESIAN_POINT('Ctrl Pts',(-212.857767934513,-1.05641958128695,
125.998947280127));
#127792=CARTESIAN_POINT('Ctrl Pts',(-212.865524237255,-1.19008629768885,
126.030298949714));
#127793=CARTESIAN_POINT('Ctrl Pts',(-212.873280539997,-1.32210727534472,
126.06714461922));
#127794=CARTESIAN_POINT('Ctrl Pts',(-212.881040982511,-1.45419871657143,
126.10400995437));
#127795=CARTESIAN_POINT('Ctrl Pts',(-212.888801425025,-1.58464229714127,
126.146375011615));
#127796=CARTESIAN_POINT('Ctrl Pts',(-212.89656186754,-1.71295856866838,
126.194050866093));
#127797=CARTESIAN_POINT('Ctrl Pts',(-212.904334767805,-1.84148082486593,
126.241803254086));
#127798=CARTESIAN_POINT('Ctrl Pts',(-212.912107668071,-1.96786858719859,
126.29488332423));
#127799=CARTESIAN_POINT('Ctrl Pts',(-212.919880568336,-2.09166388472976,
126.353054600697));
#127800=CARTESIAN_POINT('Ctrl Pts',(-212.927370904098,-2.21095891137079,
126.409111204738));
#127801=CARTESIAN_POINT('Ctrl Pts',(-212.93486123986,-2.32784641280421,
126.469895143101));
#127802=CARTESIAN_POINT('Ctrl Pts',(-212.942351575622,-2.44194179626499,
126.535156555196));
#127803=CARTESIAN_POINT('Ctrl Pts',(-212.950127033458,-2.56038025772637,
126.602902164238));
#127804=CARTESIAN_POINT('Ctrl Pts',(-212.957902491295,-2.6761850569002,
126.675687500662));
#127805=CARTESIAN_POINT('Ctrl Pts',(-212.965677949132,-2.78889756476613,
126.753282559105));
#127806=CARTESIAN_POINT('Ctrl Pts',(-212.973443580617,-2.90146763051654,
126.830779555635));
#127807=CARTESIAN_POINT('Ctrl Pts',(-212.981209212103,-3.01095286230411,
126.913073958956));
#127808=CARTESIAN_POINT('Ctrl Pts',(-212.988974843589,-3.11691940047498,
126.99989002188));
#127809=CARTESIAN_POINT('Ctrl Pts',(-212.996731076475,-3.22275768931839,
127.086601012939));
#127810=CARTESIAN_POINT('Ctrl Pts',(-213.004487309362,-3.32508546591033,
127.177822517787));
#127811=CARTESIAN_POINT('Ctrl Pts',(-213.012243542249,-3.42349856516967,
127.273236060604));
#127812=CARTESIAN_POINT('Ctrl Pts',(-213.019994445663,-3.52184404270403,
127.368584042755));
#127813=CARTESIAN_POINT('Ctrl Pts',(-213.027745349078,-3.61627991492908,
127.468118061299));
#127814=CARTESIAN_POINT('Ctrl Pts',(-213.035496252493,-3.70643572626988,
127.571479971837));
#127815=CARTESIAN_POINT('Ctrl Pts',(-213.043243508726,-3.7965491148681,
127.674793245513));
#127816=CARTESIAN_POINT('Ctrl Pts',(-213.05099076496,-3.88238619414116,
127.781930532739));
#127817=CARTESIAN_POINT('Ctrl Pts',(-213.058738021193,-3.96361425147899,
127.892497789758));
#127818=CARTESIAN_POINT('Ctrl Pts',(-213.066483309715,-4.04482167785262,
128.003036964002));
#127819=CARTESIAN_POINT('Ctrl Pts',(-213.074228598237,-4.12142218203461,
128.117004058679));
#127820=CARTESIAN_POINT('Ctrl Pts',(-213.08197388676,-4.19312439448118,
128.233973317001));
#127821=CARTESIAN_POINT('Ctrl Pts',(-213.089721116824,-4.26484458080633,
128.350971896472));
#127822=CARTESIAN_POINT('Ctrl Pts',(-213.097468346889,-4.33166381333356,
128.470973812513));
#127823=CARTESIAN_POINT('Ctrl Pts',(-213.105215576953,-4.39333498212897,
128.593525753244));
#127824=CARTESIAN_POINT('Ctrl Pts',(-213.112963794129,-4.45501400874135,
128.7160933089));
#127825=CARTESIAN_POINT('Ctrl Pts',(-213.120712011305,-4.5115434965853,
128.841211183594));
#127826=CARTESIAN_POINT('Ctrl Pts',(-213.128460228481,-4.56272349602907,
128.968403820339));
#127827=CARTESIAN_POINT('Ctrl Pts',(-213.13621430851,-4.61394222190882,
129.0956927001));
#127828=CARTESIAN_POINT('Ctrl Pts',(-213.143968388539,-4.65980323682197,
129.225059111539));
#127829=CARTESIAN_POINT('Ctrl Pts',(-213.151722468569,-4.70015562376695,
129.356009770957));
#127830=CARTESIAN_POINT('Ctrl Pts',(-213.15616382285,-4.72326851992387,
129.431015222232));
#127831=CARTESIAN_POINT('Ctrl Pts',(-213.160605177131,-4.74457510560391,
129.506540146115));
#127832=CARTESIAN_POINT('Ctrl Pts',(-213.165046531412,-4.76405452823396,
129.582490119308));
#127833=CARTESIAN_POINT('Ctrl Pts',(-211.415108320184,-4.76405452823408,
129.582490119308));
#127834=CARTESIAN_POINT('Ctrl Pts',(-211.422757975275,-4.79773678652557,
129.713816733187));
#127835=CARTESIAN_POINT('Ctrl Pts',(-211.430407630367,-4.8259785998609,
129.846513808639));
#127836=CARTESIAN_POINT('Ctrl Pts',(-211.438057285458,-4.84868568598776,
129.980085068373));
#127837=CARTESIAN_POINT('Ctrl Pts',(-211.44590449855,-4.87197919941048,
130.117105904694));
#127838=CARTESIAN_POINT('Ctrl Pts',(-211.453751711643,-4.88944813592392,
130.255046251775));
#127839=CARTESIAN_POINT('Ctrl Pts',(-211.461598924736,-4.90104730394483,
130.393363796416));
#127840=CARTESIAN_POINT('Ctrl Pts',(-211.469446137828,-4.91264647196571,
130.531681341057));
#127841=CARTESIAN_POINT('Ctrl Pts',(-211.477293350921,-4.91837588397801,
130.670375628325));
#127842=CARTESIAN_POINT('Ctrl Pts',(-211.485140564013,-4.91824790103983,
130.808904450448));
#127843=CARTESIAN_POINT('',(-211.139859435944,-4.91824985838884,130.803180381106));
#127844=CARTESIAN_POINT('Ctrl Pts',(-211.070145064099,-4.76405452823395,
129.582490119308));
#127845=CARTESIAN_POINT('Ctrl Pts',(-211.078453150991,-4.80046072940634,
129.724437345138));
#127846=CARTESIAN_POINT('Ctrl Pts',(-211.086761237883,-4.83056016471545,
129.868174465631));
#127847=CARTESIAN_POINT('Ctrl Pts',(-211.095069324776,-4.85418901054387,
130.013138706586));
#127848=CARTESIAN_POINT('Ctrl Pts',(-211.103353884107,-4.87775094215576,
130.157692425221));
#127849=CARTESIAN_POINT('Ctrl Pts',(-211.111638443438,-4.89487877747,130.30346603943));
#127850=CARTESIAN_POINT('Ctrl Pts',(-211.119923002769,-4.90545923950509,
130.449885354601));
#127851=CARTESIAN_POINT('Ctrl Pts',(-211.126568480494,-4.91394638069955,
130.567335934484));
#127852=CARTESIAN_POINT('Ctrl Pts',(-211.133213958219,-4.91822154692877,
130.685201620831));
#127853=CARTESIAN_POINT('Ctrl Pts',(-211.139859435944,-4.91824985838884,
130.803180381105));
#127854=CARTESIAN_POINT('Ctrl Pts',(-211.139859435995,-4.91824985838906,
130.803180382015));
#127855=CARTESIAN_POINT('Ctrl Pts',(-211.147841921195,-4.91828386582182,
130.944895356739));
#127856=CARTESIAN_POINT('Ctrl Pts',(-211.155824406396,-4.91218844142533,
131.086540806449));
#127857=CARTESIAN_POINT('Ctrl Pts',(-211.163806891596,-4.90000775983892,
131.227570986081));
#127858=CARTESIAN_POINT('Ctrl Pts',(-211.171795502414,-4.88781773101396,
131.368709389765));
#127859=CARTESIAN_POINT('Ctrl Pts',(-211.179784113232,-4.86953316549332,
131.509231227511));
#127860=CARTESIAN_POINT('Ctrl Pts',(-211.187772724049,-4.84524987723052,
131.648597959608));
#127861=CARTESIAN_POINT('Ctrl Pts',(-211.195768680695,-4.82094425957045,
131.788092844658));
#127862=CARTESIAN_POINT('Ctrl Pts',(-211.203764637341,-4.79062898235596,
131.926430156233));
#127863=CARTESIAN_POINT('Ctrl Pts',(-211.211760593987,-4.75445050736873,
132.063083555897));
#127864=CARTESIAN_POINT('Ctrl Pts',(-211.219770864681,-4.71820726709368,
132.199981587122));
#127865=CARTESIAN_POINT('Ctrl Pts',(-211.227781135375,-4.6760799487421,
132.335189339058));
#127866=CARTESIAN_POINT('Ctrl Pts',(-211.235791406069,-4.62826461706551,
132.468196455898));
#127867=CARTESIAN_POINT('Ctrl Pts',(-211.243809861851,-4.58040042652914,
132.60133948262));
#127868=CARTESIAN_POINT('Ctrl Pts',(-211.251828317633,-4.5268367648255,
132.732277060875));
#127869=CARTESIAN_POINT('Ctrl Pts',(-211.259846773415,-4.46781688210603,
132.860520964054));
#127870=CARTESIAN_POINT('Ctrl Pts',(-211.267879825772,-4.40868956121954,
132.988998318897));
#127871=CARTESIAN_POINT('Ctrl Pts',(-211.27591287813,-4.34408633677997,
133.114771885697));
#127872=CARTESIAN_POINT('Ctrl Pts',(-211.283945930488,-4.27429572649051,
133.237379134759));
#127873=CARTESIAN_POINT('Ctrl Pts',(-211.28638222996,-4.25312932305676,
133.274564000843));
#127874=CARTESIAN_POINT('Ctrl Pts',(-211.288818529432,-4.23148607004176,
133.311457838392));
#127875=CARTESIAN_POINT('Ctrl Pts',(-211.291254828904,-4.20937476713397,
133.348048320944));
#127876=CARTESIAN_POINT('Ctrl Pts',(-211.299029163023,-4.13881666925639,
133.464810090256));
#127877=CARTESIAN_POINT('Ctrl Pts',(-211.306803497142,-4.0632849349863,
133.5788188126));
#127878=CARTESIAN_POINT('Ctrl Pts',(-211.314577831261,-3.98302040142171,
133.689621705294));
#127879=CARTESIAN_POINT('Ctrl Pts',(-211.322342584209,-3.90285478672151,
133.800288043326));
#127880=CARTESIAN_POINT('Ctrl Pts',(-211.330107337156,-3.81796820532065,
133.907756099236));
#127881=CARTESIAN_POINT('Ctrl Pts',(-211.337872090103,-3.72864663036949,
134.011598895015));
#127882=CARTESIAN_POINT('Ctrl Pts',(-211.345629130988,-3.63941377086579,
134.115338552666));
#127883=CARTESIAN_POINT('Ctrl Pts',(-211.353386171873,-3.54575493706022,
134.215459821178));
#127884=CARTESIAN_POINT('Ctrl Pts',(-211.361143212758,-3.44799830589485,
134.311566164016));
#127885=CARTESIAN_POINT('Ctrl Pts',(-211.368894403998,-3.35031539376534,
134.407600032312));
#127886=CARTESIAN_POINT('Ctrl Pts',(-211.376645595238,-3.24854111276296,
134.499624728379));
#127887=CARTESIAN_POINT('Ctrl Pts',(-211.384396786478,-3.14304242983449,
134.587278452619));
#127888=CARTESIAN_POINT('Ctrl Pts',(-211.392144683255,-3.03758858666068,
134.674894921687));
#127889=CARTESIAN_POINT('Ctrl Pts',(-211.399892580032,-2.92841379005274,
134.758143864586));
#127890=CARTESIAN_POINT('Ctrl Pts',(-211.407640476809,-2.81592005163532,
134.836702037299));
#127891=CARTESIAN_POINT('Ctrl Pts',(-211.415386752893,-2.7034498444829,
134.915243777337));
#127892=CARTESIAN_POINT('Ctrl Pts',(-211.423133028978,-2.58766239676326,
134.989096475164));
#127893=CARTESIAN_POINT('Ctrl Pts',(-211.430879305062,-2.46899050103855,
135.057978955908));
#127894=CARTESIAN_POINT('Ctrl Pts',(-211.438625638327,-2.3503177293047,
135.126861945128));
#127895=CARTESIAN_POINT('Ctrl Pts',(-211.446371971592,-2.22876080521027,
135.190774447787));
#127896=CARTESIAN_POINT('Ctrl Pts',(-211.454118304858,-2.10477868149494,
135.249480386979));
#127897=CARTESIAN_POINT('Ctrl Pts',(-211.461866372861,-1.98076879284282,
135.308199472958));
#127898=CARTESIAN_POINT('Ctrl Pts',(-211.469614440864,-1.85433297713764,
135.361709508034));
#127899=CARTESIAN_POINT('Ctrl Pts',(-211.477362508867,-1.72595142433968,
135.409822021521));
#127900=CARTESIAN_POINT('Ctrl Pts',(-211.485118811609,-1.59743342609947,
135.45798566956));
#127901=CARTESIAN_POINT('Ctrl Pts',(-211.49287511435,-1.46696592649307,
135.500740199213));
#127902=CARTESIAN_POINT('Ctrl Pts',(-211.500631417092,-1.33504611727477,
135.537946459953));
#127903=CARTESIAN_POINT('Ctrl Pts',(-211.508391859606,-1.20305589848227,
135.575172578795));
#127904=CARTESIAN_POINT('Ctrl Pts',(-211.516152302121,-1.06961220575475,
135.606844437886));
#127905=CARTESIAN_POINT('Ctrl Pts',(-211.523912744635,-0.935222790191522,
135.63287399077));
#127906=CARTESIAN_POINT('Ctrl Pts',(-211.5316856449,-0.800617640807904,
135.658945328602));
#127907=CARTESIAN_POINT('Ctrl Pts',(-211.539458545166,-0.665064121654209,
135.679356202147));
#127908=CARTESIAN_POINT('Ctrl Pts',(-211.547231445431,-0.529076375886424,
135.694070348315));
#127909=CARTESIAN_POINT('Ctrl Pts',(-211.554721781193,-0.398032127210128,
135.708249598206));
#127910=CARTESIAN_POINT('Ctrl Pts',(-211.562212116955,-0.266584981589111,
135.71713908993));
#127911=CARTESIAN_POINT('Ctrl Pts',(-211.569702452717,-0.135193375502677,
135.720752161546));
#127912=CARTESIAN_POINT('Ctrl Pts',(-211.577476786836,0.00117998326470839,
135.72450222387));
#127913=CARTESIAN_POINT('Ctrl Pts',(-211.585251120955,0.137925497606106,
135.722579735904));
#127914=CARTESIAN_POINT('Ctrl Pts',(-211.593025455074,0.274532050292743,
135.714942580619));
#127915=CARTESIAN_POINT('Ctrl Pts',(-211.600790208021,0.410970247611329,
135.707314837445));
#127916=CARTESIAN_POINT('Ctrl Pts',(-211.608554960968,0.547269437418897,
135.693986461672));
#127917=CARTESIAN_POINT('Ctrl Pts',(-211.616319713915,0.682915815550491,
135.674967258568));
#127918=CARTESIAN_POINT('Ctrl Pts',(-211.6240767548,0.818427467787413,135.655966945604));
#127919=CARTESIAN_POINT('Ctrl Pts',(-211.631833795686,0.953287213984832,
135.631287107396));
#127920=CARTESIAN_POINT('Ctrl Pts',(-211.639590836571,1.08698404907044,
135.600989510817));
#127921=CARTESIAN_POINT('Ctrl Pts',(-211.647342027811,1.22058006233288,
135.57071476189));
#127922=CARTESIAN_POINT('Ctrl Pts',(-211.655093219051,1.35301453026544,
135.534830772938));
#127923=CARTESIAN_POINT('Ctrl Pts',(-211.662844410291,1.48378470602246,
135.493450722125));
#127924=CARTESIAN_POINT('Ctrl Pts',(-211.670592307068,1.61449930096619,
135.452088258938));
#127925=CARTESIAN_POINT('Ctrl Pts',(-211.678340203845,1.74355063866827,
135.405234497666));
#127926=CARTESIAN_POINT('Ctrl Pts',(-211.686088100622,1.87044946768263,
135.353052940789));
#127927=CARTESIAN_POINT('Ctrl Pts',(-211.693834376706,1.99732175219757,
135.300882299169));
#127928=CARTESIAN_POINT('Ctrl Pts',(-211.70158065279,2.12204206225449,135.243386227259));
#127929=CARTESIAN_POINT('Ctrl Pts',(-211.709326928874,2.24413990251942,
135.180776863814));
#127930=CARTESIAN_POINT('Ctrl Pts',(-211.71707326214,2.36623864408271,135.1181670382));
#127931=CARTESIAN_POINT('Ctrl Pts',(-211.724819595405,2.48571452933222,
135.050444024126));
#127932=CARTESIAN_POINT('Ctrl Pts',(-211.73256592867,2.60212086491236,134.977866346194));
#127933=CARTESIAN_POINT('Ctrl Pts',(-211.740313996673,2.71855326888377,
134.905272414994));
#127934=CARTESIAN_POINT('Ctrl Pts',(-211.748062064676,2.83191442363078,
134.827821863407));
#127935=CARTESIAN_POINT('Ctrl Pts',(-211.755810132679,2.94178620902499,
134.745816815837));
#127936=CARTESIAN_POINT('Ctrl Pts',(-211.763566435421,3.05177476746066,
134.663724612327));
#127937=CARTESIAN_POINT('Ctrl Pts',(-211.771322738163,3.15826623451207,
134.577068477491));
#127938=CARTESIAN_POINT('Ctrl Pts',(-211.779079040905,3.26087479461181,
134.486191498577));
#127939=CARTESIAN_POINT('Ctrl Pts',(-211.786839483419,3.36353811998983,
134.395266015882));
#127940=CARTESIAN_POINT('Ctrl Pts',(-211.794599925933,3.46231412749967,
134.300115471336));
#127941=CARTESIAN_POINT('Ctrl Pts',(-211.802360368447,3.55685428929164,
134.201119459057));
#127942=CARTESIAN_POINT('Ctrl Pts',(-211.810133268713,3.6515462153442,134.101964529591));
#127943=CARTESIAN_POINT('Ctrl Pts',(-211.817906168978,3.74198844950517,
133.998952090566));
#127944=CARTESIAN_POINT('Ctrl Pts',(-211.825679069244,3.82787257567532,
133.892495104096));
#127945=CARTESIAN_POINT('Ctrl Pts',(-211.833169405006,3.91063459753106,
133.789908097231));
#127946=CARTESIAN_POINT('Ctrl Pts',(-211.840659740768,3.98916397166631,
133.684122878256));
#127947=CARTESIAN_POINT('Ctrl Pts',(-211.84815007653,4.06322412365334,133.575532352313));
#127948=CARTESIAN_POINT('Ctrl Pts',(-211.855924410649,4.1400922888123,133.462824583575));
#127949=CARTESIAN_POINT('Ctrl Pts',(-211.863698744768,4.21238913593506,
133.34673755782));
#127950=CARTESIAN_POINT('Ctrl Pts',(-211.871473078887,4.27980295942585,
133.227678527166));
#127951=CARTESIAN_POINT('Ctrl Pts',(-211.879237831834,4.34713370140377,
133.108766226128));
#127952=CARTESIAN_POINT('Ctrl Pts',(-211.887002584781,4.40959320277074,
132.986889544881));
#127953=CARTESIAN_POINT('Ctrl Pts',(-211.894767337728,4.46691198927408,
132.862486061405));
#127954=CARTESIAN_POINT('Ctrl Pts',(-211.902524378613,4.52417384595077,
132.738206137224));
#127955=CARTESIAN_POINT('Ctrl Pts',(-211.910281419498,4.57630498604949,
132.611404757931));
#127956=CARTESIAN_POINT('Ctrl Pts',(-211.918038460383,4.62308116506517,
132.482545233072));
#127957=CARTESIAN_POINT('Ctrl Pts',(-211.925789651624,4.66982206980045,
132.353782882182));
#127958=CARTESIAN_POINT('Ctrl Pts',(-211.933540842864,4.71121591841661,
132.222965841027));
#127959=CARTESIAN_POINT('Ctrl Pts',(-211.941292034104,4.74708618395972,
132.090578260331));
#127960=CARTESIAN_POINT('Ctrl Pts',(-211.949039930881,4.78294120368305,
131.958246947888));
#127961=CARTESIAN_POINT('Ctrl Pts',(-211.956787827658,4.81327720763939,
131.824346800121));
#127962=CARTESIAN_POINT('Ctrl Pts',(-211.964535724435,4.83796730273891,
131.689377815212));
#127963=CARTESIAN_POINT('Ctrl Pts',(-211.972282000519,4.8626522332028,131.554437062905));
#127964=CARTESIAN_POINT('Ctrl Pts',(-211.980028276603,4.88169353358055,
131.418428302505));
#127965=CARTESIAN_POINT('Ctrl Pts',(-211.987774552687,4.89501536799332,
131.281862041238));
#127966=CARTESIAN_POINT('Ctrl Pts',(-211.995520885953,4.90833730074482,
131.145294771871));
#127967=CARTESIAN_POINT('Ctrl Pts',(-212.003267219218,4.9159396453269,131.008170382544));
#127968=CARTESIAN_POINT('Ctrl Pts',(-212.011013552483,4.91779845713967,
130.871004427891));
#127969=CARTESIAN_POINT('Ctrl Pts',(-212.018761620486,4.91965768522046,
130.733807755874));
#127970=CARTESIAN_POINT('Ctrl Pts',(-212.026509688489,4.91577081579773,
130.596569890862));
#127971=CARTESIAN_POINT('Ctrl Pts',(-212.034257756492,4.90616603054668,
130.459805914783));
#127972=CARTESIAN_POINT('Ctrl Pts',(-212.042014059234,4.89655103721554,
130.322896584322));
#127973=CARTESIAN_POINT('Ctrl Pts',(-212.049770361976,4.88120601588943,
130.186462539525));
#127974=CARTESIAN_POINT('Ctrl Pts',(-212.057526664718,4.86021107284611,
130.05101382499));
#127975=CARTESIAN_POINT('Ctrl Pts',(-212.065287107232,4.83920492416949,
129.915492817398));
#127976=CARTESIAN_POINT('Ctrl Pts',(-212.073047549746,4.81254292103631,
129.78095857129));
#127977=CARTESIAN_POINT('Ctrl Pts',(-212.08080799226,4.78035603891383,129.647909492909));
#127978=CARTESIAN_POINT('Ctrl Pts',(-212.088580892526,4.74811748755075,
129.514646832336));
#127979=CARTESIAN_POINT('Ctrl Pts',(-212.096353792791,4.7103364418738,129.382874479768));
#127980=CARTESIAN_POINT('Ctrl Pts',(-212.104126693057,4.66719363216871,
129.253075130512));
#127981=CARTESIAN_POINT('Ctrl Pts',(-212.111617028819,4.62561917226623,
129.127994314546));
#127982=CARTESIAN_POINT('Ctrl Pts',(-212.119107364581,4.57906611645686,
129.004745833215));
#127983=CARTESIAN_POINT('Ctrl Pts',(-212.126597700343,4.52773715270625,
128.883741098113));
#127984=CARTESIAN_POINT('Ctrl Pts',(-212.134372034462,4.47446203569445,
128.758148431702));
#127985=CARTESIAN_POINT('Ctrl Pts',(-212.142146368581,4.41587294499023,
128.634575173661));
#127986=CARTESIAN_POINT('Ctrl Pts',(-212.1499207027,4.35214402884569,128.513503700453));
#127987=CARTESIAN_POINT('Ctrl Pts',(-212.157685455647,4.28849365289468,
128.392581437016));
#127988=CARTESIAN_POINT('Ctrl Pts',(-212.165450208594,4.2197162353809,128.274155166353));
#127989=CARTESIAN_POINT('Ctrl Pts',(-212.173214961542,4.14603426563759,
128.158688126372));
#127990=CARTESIAN_POINT('Ctrl Pts',(-212.180972002427,4.07242547786517,
128.043335769884));
#127991=CARTESIAN_POINT('Ctrl Pts',(-212.188729043312,3.99392204086201,
127.930937122484));
#127992=CARTESIAN_POINT('Ctrl Pts',(-212.196486084197,3.91079254043548,
127.821931277552));
#127993=CARTESIAN_POINT('Ctrl Pts',(-212.204237275437,3.82772572861176,
127.713007634776));
#127994=CARTESIAN_POINT('Ctrl Pts',(-212.211988466677,3.74004003323491,
127.607472011472));
#127995=CARTESIAN_POINT('Ctrl Pts',(-212.219739657917,3.64804736688959,
127.505734620059));
#127996=CARTESIAN_POINT('Ctrl Pts',(-212.227487554694,3.55609379988157,
127.404040469751));
#127997=CARTESIAN_POINT('Ctrl Pts',(-212.235235451471,3.45983716445215,
127.306141629901));
#127998=CARTESIAN_POINT('Ctrl Pts',(-212.242983348248,3.35962953441825,
127.21241512049));
#127999=CARTESIAN_POINT('Ctrl Pts',(-212.250729624333,3.25944286566032,
127.118708216644));
#128000=CARTESIAN_POINT('Ctrl Pts',(-212.258475900417,3.15530713153065,
127.029172174163));
#128001=CARTESIAN_POINT('Ctrl Pts',(-212.266222176501,3.04761084507334,
126.944146737547));
#128002=CARTESIAN_POINT('Ctrl Pts',(-212.273968509766,2.93991376362695,
126.859120673292));
#128003=CARTESIAN_POINT('Ctrl Pts',(-212.281714843031,2.82865638426578,
126.778605523605));
#128004=CARTESIAN_POINT('Ctrl Pts',(-212.289461176297,2.71425951506319,
126.702900103628));
#128005=CARTESIAN_POINT('Ctrl Pts',(-212.2972092443,2.59983702747476,126.627177729947));
#128006=CARTESIAN_POINT('Ctrl Pts',(-212.304957312303,2.48227397699698,
126.556267445015));
#128007=CARTESIAN_POINT('Ctrl Pts',(-212.312705380306,2.36201894952585,
126.490423953151));
#128008=CARTESIAN_POINT('Ctrl Pts',(-212.320461683048,2.24163611358032,
126.424510482041));
#128009=CARTESIAN_POINT('Ctrl Pts',(-212.328217985789,2.11855592882903,
126.363674749277));
#128010=CARTESIAN_POINT('Ctrl Pts',(-212.335974288531,1.99325080963909,
126.308125050742));
#128011=CARTESIAN_POINT('Ctrl Pts',(-212.343734731046,1.86787881133419,
126.252545703661));
#128012=CARTESIAN_POINT('Ctrl Pts',(-212.35149517356,1.74027987592607,126.202258155801));
#128013=CARTESIAN_POINT('Ctrl Pts',(-212.359255616074,1.61094412214307,
126.157421614541));
#128014=CARTESIAN_POINT('Ctrl Pts',(-212.367028516339,1.4814007471262,126.112513097685));
#128015=CARTESIAN_POINT('Ctrl Pts',(-212.374801416605,1.35011535688172,
126.073073186146));
#128016=CARTESIAN_POINT('Ctrl Pts',(-212.38257431687,1.21759174577694,126.039210735021));
#128017=CARTESIAN_POINT('Ctrl Pts',(-212.390064652632,1.08988570174336,
126.006579269289));
#128018=CARTESIAN_POINT('Ctrl Pts',(-212.397554988394,0.961030200037002,
125.979126858922));
#128019=CARTESIAN_POINT('Ctrl Pts',(-212.405045324156,0.831480930678297,
125.95690535481));
#128020=CARTESIAN_POINT('Ctrl Pts',(-212.412819658275,0.697019761395268,
125.933841315615));
#128021=CARTESIAN_POINT('Ctrl Pts',(-212.420593992394,0.561385244984867,
125.916339612538));
#128022=CARTESIAN_POINT('Ctrl Pts',(-212.428368326513,0.425077349810972,
125.904514465984));
#128023=CARTESIAN_POINT('Ctrl Pts',(-212.43613307946,0.288937441936431,
125.892703892865));
#128024=CARTESIAN_POINT('Ctrl Pts',(-212.443897832408,0.152126192273598,
125.886555990081));
#128025=CARTESIAN_POINT('Ctrl Pts',(-212.451662585355,0.0151535969136297,
125.886133962459));
#128026=CARTESIAN_POINT('Ctrl Pts',(-212.45941962624,-0.121682955334768,
125.885712354002));
#128027=CARTESIAN_POINT('Ctrl Pts',(-212.467176667125,-0.258680145940508,
125.891005304476));
#128028=CARTESIAN_POINT('Ctrl Pts',(-212.47493370801,-0.395323376019601,
125.902024185733));
#128029=CARTESIAN_POINT('Ctrl Pts',(-212.48268489925,-0.531863562375405,
125.913034757567));
#128030=CARTESIAN_POINT('Ctrl Pts',(-212.49043609049,-0.668049931377992,
125.929762634228));
#128031=CARTESIAN_POINT('Ctrl Pts',(-212.49818728173,-0.803368763331662,
125.95216712466));
#128032=CARTESIAN_POINT('Ctrl Pts',(-212.505935178507,-0.93863008117182,
125.974562092585));
#128033=CARTESIAN_POINT('Ctrl Pts',(-212.513683075284,-1.07302421042508,
126.00262881185));
#128034=CARTESIAN_POINT('Ctrl Pts',(-212.521430972061,-1.20604364900575,
126.036274861291));
#128035=CARTESIAN_POINT('Ctrl Pts',(-212.529177248145,-1.3390352627878,
126.069913872704));
#128036=CARTESIAN_POINT('Ctrl Pts',(-212.536923524229,-1.47065237907312,
126.109129797104));
#128037=CARTESIAN_POINT('Ctrl Pts',(-212.544669800314,-1.60039916040225,
126.153779407665));
#128038=CARTESIAN_POINT('Ctrl Pts',(-212.552416133579,-1.73014689949246,
126.198429347819));
#128039=CARTESIAN_POINT('Ctrl Pts',(-212.560162466844,-1.85802390638936,
126.248512926951));
#128040=CARTESIAN_POINT('Ctrl Pts',(-212.56790880011,-1.9835513224081,126.303837624194));
#128041=CARTESIAN_POINT('Ctrl Pts',(-212.575656868113,-2.10910684942115,
126.359174711019));
#128042=CARTESIAN_POINT('Ctrl Pts',(-212.583404936116,-2.23231138083907,
126.419755093858));
#128043=CARTESIAN_POINT('Ctrl Pts',(-212.591153004119,-2.35270815506882,
126.4853390386));
#128044=CARTESIAN_POINT('Ctrl Pts',(-212.59890930686,-2.47323288842312,
126.550992686739));
#128045=CARTESIAN_POINT('Ctrl Pts',(-212.606665609602,-2.59094355961426,
126.621660332428));
#128046=CARTESIAN_POINT('Ctrl Pts',(-212.614421912344,-2.70540957191042,
126.697057109093));
#128047=CARTESIAN_POINT('Ctrl Pts',(-212.622182354858,-2.81993667816385,
126.772494127288));
#128048=CARTESIAN_POINT('Ctrl Pts',(-212.629942797372,-2.9312153577612,
126.852665077476));
#128049=CARTESIAN_POINT('Ctrl Pts',(-212.637703239887,-3.03884674388082,
126.937243664369));
#128050=CARTESIAN_POINT('Ctrl Pts',(-212.645476140152,-3.14665090945651,
127.021958024317));
#128051=CARTESIAN_POINT('Ctrl Pts',(-212.653249040417,-3.25079578428155,
127.111093905765));
#128052=CARTESIAN_POINT('Ctrl Pts',(-212.661021940683,-3.3509174723189,
127.204286291082));
#128053=CARTESIAN_POINT('Ctrl Pts',(-212.668512276445,-3.44739948480396,
127.294090898454));
#128054=CARTESIAN_POINT('Ctrl Pts',(-212.676002612207,-3.54014552128071,
127.387661983052));
#128055=CARTESIAN_POINT('Ctrl Pts',(-212.683492947969,-3.62886564654099,
127.484644186626));
#128056=CARTESIAN_POINT('Ctrl Pts',(-212.691183413032,-3.71995622584122,
127.584217593217));
#128057=CARTESIAN_POINT('Ctrl Pts',(-212.698873878095,-3.80710559154992,
127.687718300335));
#128058=CARTESIAN_POINT('Ctrl Pts',(-212.706564343158,-3.88995039074112,
127.794797689154));
#128059=CARTESIAN_POINT('Ctrl Pts',(-212.714245638282,-3.97269640763924,
127.901749398894));
#128060=CARTESIAN_POINT('Ctrl Pts',(-212.721926933406,-4.05114782160935,
128.012270992388));
#128061=CARTESIAN_POINT('Ctrl Pts',(-212.72960822853,-4.12497833315283,
128.125977371367));
#128062=CARTESIAN_POINT('Ctrl Pts',(-212.737280901644,-4.19872597229643,
128.239556118553));
#128063=CARTESIAN_POINT('Ctrl Pts',(-212.744953574759,-4.26786281658607,
128.356312202527));
#128064=CARTESIAN_POINT('Ctrl Pts',(-212.752626247873,-4.33210352833311,
128.475828444221));
#128065=CARTESIAN_POINT('Ctrl Pts',(-212.760293849226,-4.39630177591927,
128.595265683725));
#128066=CARTESIAN_POINT('Ctrl Pts',(-212.767961450578,-4.45561013783136,
128.717459102105));
#128067=CARTESIAN_POINT('Ctrl Pts',(-212.77562905193,-4.50978731104797,
128.841963748528));
#128068=CARTESIAN_POINT('Ctrl Pts',(-212.783293992805,-4.56394568606493,
128.966425194779));
#128069=CARTESIAN_POINT('Ctrl Pts',(-212.790958933681,-4.61297624916482,
129.093195910092));
#128070=CARTESIAN_POINT('Ctrl Pts',(-212.798623874557,-4.65668446113259,
129.221807966958));
#128071=CARTESIAN_POINT('Ctrl Pts',(-212.805703125853,-4.69705286334965,
129.340592584489));
#128072=CARTESIAN_POINT('Ctrl Pts',(-212.812782377149,-4.7328816197208,
129.46094742213));
#128073=CARTESIAN_POINT('Ctrl Pts',(-212.819861628446,-4.76405452823406,
129.582490119308));
#128074=CARTESIAN_POINT('Origin',(213.235140564004,0.,130.804360617566));
#128075=CARTESIAN_POINT('',(-214.915345176019,-4.76405452823394,129.582490119308));
#128076=CARTESIAN_POINT('',(-214.569765644412,-4.76405452823405,129.582490119308));
#128077=CARTESIAN_POINT('',(213.235140564004,-4.76405452823405,129.582490119308));
#128078=CARTESIAN_POINT('',(-213.235140564069,-4.91824975740887,130.80281586917));
#128079=CARTESIAN_POINT('Ctrl Pts',(-213.23514056407,-4.91824975740887,
130.802815869171));
#128080=CARTESIAN_POINT('Ctrl Pts',(-213.242852601799,-4.9182922816069,
130.93820660807));
#128081=CARTESIAN_POINT('Ctrl Pts',(-213.250564639529,-4.91273997424585,
131.073824800331));
#128082=CARTESIAN_POINT('Ctrl Pts',(-213.258276677259,-4.90156264554618,
131.209165131234));
#128083=CARTESIAN_POINT('Ctrl Pts',(-213.265979442628,-4.89039875560677,
131.344342739335));
#128084=CARTESIAN_POINT('Ctrl Pts',(-213.273682207996,-4.87362332935581,
131.479242758052));
#128085=CARTESIAN_POINT('Ctrl Pts',(-213.281384973365,-4.85125815681078,
131.613358366931));
#128086=CARTESIAN_POINT('Ctrl Pts',(-213.289080393618,-4.82891431099335,
131.747346087368));
#128087=CARTESIAN_POINT('Ctrl Pts',(-213.296775813871,-4.80099138833436,
131.88055049623));
#128088=CARTESIAN_POINT('Ctrl Pts',(-213.304471234125,-4.76756306468317,
132.012468843996));
#128089=CARTESIAN_POINT('Ctrl Pts',(-213.312161229336,-4.73415830700125,
132.14429419327));
#128090=CARTESIAN_POINT('Ctrl Pts',(-213.319851224548,-4.69525596895756,
132.274834901479));
#128091=CARTESIAN_POINT('Ctrl Pts',(-213.32754121976,-4.65098090936588,
132.403597824241));
#128092=CARTESIAN_POINT('Ctrl Pts',(-213.335228522826,-4.60672134977473,
132.532315669134));
#128093=CARTESIAN_POINT('Ctrl Pts',(-213.342915825891,-4.55709293612188,
132.659256590072));
#128094=CARTESIAN_POINT('Ctrl Pts',(-213.350603128957,-4.50227046527684,
132.783942320855));
#128095=CARTESIAN_POINT('Ctrl Pts',(-213.358289301112,-4.44745605959028,
132.908609708609));
#128096=CARTESIAN_POINT('Ctrl Pts',(-213.365975473267,-4.38744927623874,
133.031022201947));
#128097=CARTESIAN_POINT('Ctrl Pts',(-213.373661645422,-4.32247296612338,
133.150721740589));
#128098=CARTESIAN_POINT('Ctrl Pts',(-213.38134841673,-4.25749159096851,
133.27043061006));
#128099=CARTESIAN_POINT('Ctrl Pts',(-213.389035188039,-4.18754010838411,
133.387425754647));
#128100=CARTESIAN_POINT('Ctrl Pts',(-213.396721959347,-4.11288697205642,
133.501274375473));
#128101=CARTESIAN_POINT('Ctrl Pts',(-213.404411060001,-4.03821121336109,
133.615157496194));
#128102=CARTESIAN_POINT('Ctrl Pts',(-213.412100160655,-3.95883118507137,
133.725891864193));
#128103=CARTESIAN_POINT('Ctrl Pts',(-213.419789261309,-3.87505794807738,
133.833074694785));
#128104=CARTESIAN_POINT('Ctrl Pts',(-213.427486708261,-3.79119377763857,
133.940373869263));
#128105=CARTESIAN_POINT('Ctrl Pts',(-213.435184155213,-3.70292712355384,
134.044113496638));
#128106=CARTESIAN_POINT('Ctrl Pts',(-213.442881602165,-3.61060874719674,
134.143924591675));
#128107=CARTESIAN_POINT('Ctrl Pts',(-213.450583822761,-3.51823311873419,
134.243797585497));
#128108=CARTESIAN_POINT('Ctrl Pts',(-213.458286043357,-3.42180104588926,
134.339736915968));
#128109=CARTESIAN_POINT('Ctrl Pts',(-213.465988263953,-3.32169834938428,
134.431412194012));
#128110=CARTESIAN_POINT('Ctrl Pts',(-213.473701663331,-3.22145036669574,
134.523220526926));
#128111=CARTESIAN_POINT('Ctrl Pts',(-213.481415062709,-3.1175214283961,
134.610752197681));
#128112=CARTESIAN_POINT('Ctrl Pts',(-213.489128462087,-3.01032876205514,
134.693718380339));
#128113=CARTESIAN_POINT('Ctrl Pts',(-213.492501249141,-2.9634573348724,
134.729996453474));
#128114=CARTESIAN_POINT('Ctrl Pts',(-213.495874036194,-2.91596223817887,
134.76540218225));
#128115=CARTESIAN_POINT('Ctrl Pts',(-213.499246823248,-2.86787988118274,
134.799914152385));
#128116=CARTESIAN_POINT('Ctrl Pts',(-213.507021157367,-2.75704919351243,
134.879464857092));
#128117=CARTESIAN_POINT('Ctrl Pts',(-213.514795491486,-2.64273052294015,
134.95452665304));
#128118=CARTESIAN_POINT('Ctrl Pts',(-213.522569825605,-2.52532352423003,
135.024778151468));
#128119=CARTESIAN_POINT('Ctrl Pts',(-213.530334578552,-2.40806121915254,
135.094943071204));
#128120=CARTESIAN_POINT('Ctrl Pts',(-213.538099331499,-2.28771849119061,
135.160309290077));
#128121=CARTESIAN_POINT('Ctrl Pts',(-213.545864084446,-2.16472632567553,
135.220596910772));
#128122=CARTESIAN_POINT('Ctrl Pts',(-213.553621125331,-2.04185631771346,
135.280824652951));
#128123=CARTESIAN_POINT('Ctrl Pts',(-213.561378166216,-1.91634245770695,
135.335983664043));
#128124=CARTESIAN_POINT('Ctrl Pts',(-213.569135207101,-1.78864254052713,
135.385838645967));
#128125=CARTESIAN_POINT('Ctrl Pts',(-213.576886398341,-1.6610389228477,
135.435656031861));
#128126=CARTESIAN_POINT('Ctrl Pts',(-213.584637589582,-1.53125289200009,
135.480177208357));
#128127=CARTESIAN_POINT('Ctrl Pts',(-213.592388780822,-1.39976422312377,
135.519214081054));
#128128=CARTESIAN_POINT('Ctrl Pts',(-213.600136677599,-1.26833144043982,
135.558234362038));
#128129=CARTESIAN_POINT('Ctrl Pts',(-213.607884574376,-1.13519783305681,
135.591774864318));
#128130=CARTESIAN_POINT('Ctrl Pts',(-213.615632471153,-1.00086021008568,
135.619696732768));
#128131=CARTESIAN_POINT('Ctrl Pts',(-213.623378747237,-0.866550687648937,
135.647612760565));
#128132=CARTESIAN_POINT('Ctrl Pts',(-213.631125023321,-0.731038033117482,
135.669912412751));
#128133=CARTESIAN_POINT('Ctrl Pts',(-213.638871299405,-0.594830786853627,
135.68650762452));
#128134=CARTESIAN_POINT('Ctrl Pts',(-213.64661763267,-0.458622535139378,
135.703102958792));
#128135=CARTESIAN_POINT('Ctrl Pts',(-213.654363965936,-0.321720069556817,
135.713993721337));
#128136=CARTESIAN_POINT('Ctrl Pts',(-213.662110299201,-0.184638221668168,
135.719143602561));
#128137=CARTESIAN_POINT('Ctrl Pts',(-213.669858367204,-0.0475256752495831,
135.724294637066));
#128138=CARTESIAN_POINT('Ctrl Pts',(-213.677606435207,0.0897659427967536,
135.72370221732));
#128139=CARTESIAN_POINT('Ctrl Pts',(-213.68535450321,0.226721022593234,
135.717382156336));
#128140=CARTESIAN_POINT('Ctrl Pts',(-213.693110805952,0.363821659878121,
135.711055378316));
#128141=CARTESIAN_POINT('Ctrl Pts',(-213.700867108694,0.500584653242775,
135.698988816862));
#128142=CARTESIAN_POINT('Ctrl Pts',(-213.708623411436,0.636498182637569,
135.681250315519));
#128143=CARTESIAN_POINT('Ctrl Pts',(-213.71638385395,0.772484253175279,
135.663502346604));
#128144=CARTESIAN_POINT('Ctrl Pts',(-213.724144296464,0.90761957130462,
135.640076472424));
#128145=CARTESIAN_POINT('Ctrl Pts',(-213.731904738978,1.04140273125982,
135.611091670353));
#128146=CARTESIAN_POINT('Ctrl Pts',(-213.739677639243,1.17540065182008,
135.582060339304));
#128147=CARTESIAN_POINT('Ctrl Pts',(-213.747450539509,1.30804169812883,
135.54745234676));
#128148=CARTESIAN_POINT('Ctrl Pts',(-213.755223439774,1.43883897685387,
135.507436787605));
#128149=CARTESIAN_POINT('Ctrl Pts',(-213.762713775536,1.56488144503772,
135.468875894818));
#128150=CARTESIAN_POINT('Ctrl Pts',(-213.770204111298,1.68921157882685,
135.425293868858));
#128151=CARTESIAN_POINT('Ctrl Pts',(-213.77769444706,1.81141322115339,135.376883466577));
#128152=CARTESIAN_POINT('Ctrl Pts',(-213.785468781179,1.93824817589203,
135.32663756918));
#128153=CARTESIAN_POINT('Ctrl Pts',(-213.793243115298,2.06319182451666,
135.271030768151));
#128154=CARTESIAN_POINT('Ctrl Pts',(-213.801017449417,2.18575775039907,
135.210225585886));
#128155=CARTESIAN_POINT('Ctrl Pts',(-213.808782202364,2.30817262473185,
135.149495340574));
#128156=CARTESIAN_POINT('Ctrl Pts',(-213.816546955312,2.42821525993514,
135.083579633217));
#128157=CARTESIAN_POINT('Ctrl Pts',(-213.824311708259,2.5454172123711,135.012689772642));
#128158=CARTESIAN_POINT('Ctrl Pts',(-213.832068749144,2.66250275817564,
134.941870320877));
#128159=CARTESIAN_POINT('Ctrl Pts',(-213.839825790029,2.77675290357153,
134.866086748545));
#128160=CARTESIAN_POINT('Ctrl Pts',(-213.847582830914,2.8877222363102,134.785597027077));
#128161=CARTESIAN_POINT('Ctrl Pts',(-213.855334022154,2.99860788621168,
134.705168003535));
#128162=CARTESIAN_POINT('Ctrl Pts',(-213.863085213394,3.10621733277591,
134.620040123438));
#128163=CARTESIAN_POINT('Ctrl Pts',(-213.870836404634,3.21013299667426,
134.530515365582));
#128164=CARTESIAN_POINT('Ctrl Pts',(-213.878584301411,3.31400449364355,
134.441028658136));
#128165=CARTESIAN_POINT('Ctrl Pts',(-213.886332198188,3.41418503488793,
134.34714904446));
#128166=CARTESIAN_POINT('Ctrl Pts',(-213.894080094965,3.51028926019803,
134.249219449541));
#128167=CARTESIAN_POINT('Ctrl Pts',(-213.901826371049,3.60637338257596,
134.151310339383));
#128168=CARTESIAN_POINT('Ctrl Pts',(-213.909572647133,3.69838261137393,
134.049353211914));
#128169=CARTESIAN_POINT('Ctrl Pts',(-213.917318923217,3.78596797668907,
133.943728315365));
#128170=CARTESIAN_POINT('Ctrl Pts',(-213.925065256483,3.87355398853936,
133.838102639117));
#128171=CARTESIAN_POINT('Ctrl Pts',(-213.932811589748,3.95671582218726,
133.728809440721));
#128172=CARTESIAN_POINT('Ctrl Pts',(-213.940557923013,4.03514465030808,
133.616262236327));
#128173=CARTESIAN_POINT('Ctrl Pts',(-213.948305991016,4.11359104202148,
133.503689827767));
#128174=CARTESIAN_POINT('Ctrl Pts',(-213.956054059019,4.18730209559916,
133.38786228386));
#128175=CARTESIAN_POINT('Ctrl Pts',(-213.963802127022,4.25601241524396,
133.26922194912));
#128176=CARTESIAN_POINT('Ctrl Pts',(-213.971558429764,4.32479576103385,
133.150455522021));
#128177=CARTESIAN_POINT('Ctrl Pts',(-213.979314732506,4.3885675596754,133.028870671166));
#128178=CARTESIAN_POINT('Ctrl Pts',(-213.987071035248,4.4471082386258,132.904934676352));
#128179=CARTESIAN_POINT('Ctrl Pts',(-213.994831477762,4.50568016249934,
132.780932533167));
#128180=CARTESIAN_POINT('Ctrl Pts',(-214.002591920276,4.55901525140929,
132.65457710559));
#128181=CARTESIAN_POINT('Ctrl Pts',(-214.01035236279,4.60694258232605,132.526354550671));
#128182=CARTESIAN_POINT('Ctrl Pts',(-214.018125263056,4.65494685044905,
132.397926161524));
#128183=CARTESIAN_POINT('Ctrl Pts',(-214.025898163321,4.69752589164035,
132.267625027358));
#128184=CARTESIAN_POINT('Ctrl Pts',(-214.033671063587,4.73455879247533,
132.135952185238));
#128185=CARTESIAN_POINT('Ctrl Pts',(-214.041161399349,4.7702454540851,132.009065982591));
#128186=CARTESIAN_POINT('Ctrl Pts',(-214.048651735111,4.80078213558388,
131.880906370238));
#128187=CARTESIAN_POINT('Ctrl Pts',(-214.056142070873,4.82610606571059,
131.751927662693));
#128188=CARTESIAN_POINT('Ctrl Pts',(-214.063916404992,4.85239016034483,
131.618058688252));
#128189=CARTESIAN_POINT('Ctrl Pts',(-214.071690739111,4.87314167777241,
131.482883223848));
#128190=CARTESIAN_POINT('Ctrl Pts',(-214.07946507323,4.88823443261954,131.346898352892));
#128191=CARTESIAN_POINT('Ctrl Pts',(-214.087229826177,4.90330858699525,
131.211081071136));
#128192=CARTESIAN_POINT('Ctrl Pts',(-214.094994579124,4.91273781209716,
131.074456752448));
#128193=CARTESIAN_POINT('Ctrl Pts',(-214.102759332071,4.91644668279933,
130.93753372931));
#128194=CARTESIAN_POINT('Ctrl Pts',(-214.110516372956,4.92015186979883,
130.800746700049));
#128195=CARTESIAN_POINT('Ctrl Pts',(-214.118273413842,4.9181479983951,130.663661945033));
#128196=CARTESIAN_POINT('Ctrl Pts',(-214.126030454727,4.91041135105898,
130.526793642061));
#128197=CARTESIAN_POINT('Ctrl Pts',(-214.133781645967,4.90268053798878,
130.390028552541));
#128198=CARTESIAN_POINT('Ctrl Pts',(-214.141532837207,4.88922557589138,
130.253479978932));
#128199=CARTESIAN_POINT('Ctrl Pts',(-214.149284028447,4.8700748162521,130.117662469464));
#128200=CARTESIAN_POINT('Ctrl Pts',(-214.157031925224,4.85093219619655,
129.981902686061));
#128201=CARTESIAN_POINT('Ctrl Pts',(-214.164779822001,4.82609864799007,
129.846873735122));
#128202=CARTESIAN_POINT('Ctrl Pts',(-214.172527718778,4.7956543875314,129.713085190439));
#128203=CARTESIAN_POINT('Ctrl Pts',(-214.180273994862,4.76521649535572,
129.579324631435));
#128204=CARTESIAN_POINT('Ctrl Pts',(-214.188020270946,4.72917031205577,
129.446804343573));
#128205=CARTESIAN_POINT('Ctrl Pts',(-214.195766547031,4.68764712448072,
129.31602345857));
#128206=CARTESIAN_POINT('Ctrl Pts',(-214.203512880296,4.64612363039088,
129.185241608173));
#128207=CARTESIAN_POINT('Ctrl Pts',(-214.211259213561,4.59912316966279,
129.056199558891));
#128208=CARTESIAN_POINT('Ctrl Pts',(-214.219005546827,4.54682671643361,
128.92938065148));
#128209=CARTESIAN_POINT('Ctrl Pts',(-214.22675361483,4.4945185517764,128.802533343853));
#128210=CARTESIAN_POINT('Ctrl Pts',(-214.234501682833,4.43691218363262,
128.677910530147));
#128211=CARTESIAN_POINT('Ctrl Pts',(-214.242249750835,4.37423631605783,
128.555974593374));
#128212=CARTESIAN_POINT('Ctrl Pts',(-214.250006053577,4.31149383582504,
128.433909061637));
#128213=CARTESIAN_POINT('Ctrl Pts',(-214.257762356319,4.24367127221741,
128.314536459566));
#128214=CARTESIAN_POINT('Ctrl Pts',(-214.265518659061,4.17104307663906,
128.198294095905));
#128215=CARTESIAN_POINT('Ctrl Pts',(-214.273279101575,4.09837611720594,
128.081989690195));
#128216=CARTESIAN_POINT('Ctrl Pts',(-214.281039544089,4.02089863575193,
127.968819174359));
#128217=CARTESIAN_POINT('Ctrl Pts',(-214.288799986604,3.93892726189776,
127.859189130542));
#128218=CARTESIAN_POINT('Ctrl Pts',(-214.296572886869,3.8568243003172,127.749383098847));
#128219=CARTESIAN_POINT('Ctrl Pts',(-214.304345787134,3.7702132776379,127.643129199792));
#128220=CARTESIAN_POINT('Ctrl Pts',(-214.3121186874,3.67945037387307,127.540799984039));
#128221=CARTESIAN_POINT('Ctrl Pts',(-214.319609023162,3.59198693027806,
127.442190693031));
#128222=CARTESIAN_POINT('Ctrl Pts',(-214.327099358924,3.50066844098738,
127.347225917093));
#128223=CARTESIAN_POINT('Ctrl Pts',(-214.334589694686,3.40584320426917,
127.25620403556));
#128224=CARTESIAN_POINT('Ctrl Pts',(-214.342364028805,3.30742263987888,
127.161731031722));
#128225=CARTESIAN_POINT('Ctrl Pts',(-214.350138362924,3.20491239536073,
127.071206552042));
#128226=CARTESIAN_POINT('Ctrl Pts',(-214.357912697043,3.09866247478941,
126.985005445573));
#128227=CARTESIAN_POINT('Ctrl Pts',(-214.365677449991,2.99254349774966,
126.898910574264));
#128228=CARTESIAN_POINT('Ctrl Pts',(-214.373442202938,2.88269431552433,
126.81712871865));
#128229=CARTESIAN_POINT('Ctrl Pts',(-214.381206955885,2.7695018335054,126.739998102151));
#128230=CARTESIAN_POINT('Ctrl Pts',(-214.38896399677,2.65642177585566,126.662944092868));
#128231=CARTESIAN_POINT('Ctrl Pts',(-214.396721037655,2.54000534757768,
126.590532348065));
#128232=CARTESIAN_POINT('Ctrl Pts',(-214.40447807854,2.42067232111235,126.523060747632));
#128233=CARTESIAN_POINT('Ctrl Pts',(-214.41222926978,2.30142928461039,126.455640028057));
#128234=CARTESIAN_POINT('Ctrl Pts',(-214.41998046102,2.17927436670708,126.393152229314));
#128235=CARTESIAN_POINT('Ctrl Pts',(-214.42773165226,2.05465579607173,126.335851624382));
#128236=CARTESIAN_POINT('Ctrl Pts',(-214.435479549037,1.93009019165303,
126.278575373735));
#128237=CARTESIAN_POINT('Ctrl Pts',(-214.443227445814,1.80306337161081,
126.226482094916));
#128238=CARTESIAN_POINT('Ctrl Pts',(-214.450975342591,1.6740474134597,126.179779737098));
#128239=CARTESIAN_POINT('Ctrl Pts',(-214.458721618676,1.54505844266578,
126.133087148407));
#128240=CARTESIAN_POINT('Ctrl Pts',(-214.46646789476,1.41408152876622,126.09178337072));
#128241=CARTESIAN_POINT('Ctrl Pts',(-214.474214170844,1.28160756916159,
126.05602774158));
#128242=CARTESIAN_POINT('Ctrl Pts',(-214.481960504109,1.14913263166411,
126.0202718485));
#128243=CARTESIAN_POINT('Ctrl Pts',(-214.489706837375,1.0151610038684,125.990064287569));
#128244=CARTESIAN_POINT('Ctrl Pts',(-214.49745317064,0.880197154982506,
125.965514057604));
#128245=CARTESIAN_POINT('Ctrl Pts',(-214.505201238643,0.745203081878611,
125.940958329784));
#128246=CARTESIAN_POINT('Ctrl Pts',(-214.512949306646,0.609216730109788,
125.922062523911));
#128247=CARTESIAN_POINT('Ctrl Pts',(-214.520697374649,0.472750735730102,
125.908884154098));
#128248=CARTESIAN_POINT('Ctrl Pts',(-214.528453677391,0.336139703667811,
125.895691778157));
#128249=CARTESIAN_POINT('Ctrl Pts',(-214.536209980133,0.19904840044981,
125.888229014498));
#128250=CARTESIAN_POINT('Ctrl Pts',(-214.543966282875,0.0619930939944813,
125.88650133544));
#128251=CARTESIAN_POINT('Ctrl Pts',(-214.551726725389,-0.0751353630049309,
125.884772734267));
#128252=CARTESIAN_POINT('Ctrl Pts',(-214.559487167903,-0.212227394352379,
125.888785305537));
#128253=CARTESIAN_POINT('Ctrl Pts',(-214.567247610417,-0.348769784930064,
125.898492427366));
#128254=CARTESIAN_POINT('Ctrl Pts',(-214.575020510683,-0.485531365474397,
125.908215131928));
#128255=CARTESIAN_POINT('Ctrl Pts',(-214.582793410948,-0.621741153365783,
125.923650610425));
#128256=CARTESIAN_POINT('Ctrl Pts',(-214.590566311214,-0.756893187184922,
125.944700571257));
#128257=CARTESIAN_POINT('Ctrl Pts',(-214.598056646975,-0.88713210414437,
125.964985312991));
#128258=CARTESIAN_POINT('Ctrl Pts',(-214.605546982737,-1.01638853371941,
125.990483363267));
#128259=CARTESIAN_POINT('Ctrl Pts',(-214.613037318499,-1.14422317720585,
126.021062970205));
#128260=CARTESIAN_POINT('Ctrl Pts',(-214.620811652618,-1.27690471005774,
126.052802012236));
#128261=CARTESIAN_POINT('Ctrl Pts',(-214.628585986737,-1.40847480971311,
126.09011609174));
#128262=CARTESIAN_POINT('Ctrl Pts',(-214.636360320856,-1.5384289192948,
126.132913355445));
#128263=CARTESIAN_POINT('Ctrl Pts',(-214.644125073803,-1.66822287204971,
126.175657875347));
#128264=CARTESIAN_POINT('Ctrl Pts',(-214.651889826751,-1.79640442956711,
126.223872012852));
#128265=CARTESIAN_POINT('Ctrl Pts',(-214.659654579698,-1.92247990309097,
126.277413071513));
#128266=CARTESIAN_POINT('Ctrl Pts',(-214.667411620583,-2.04843015667717,
126.330900952441));
#128267=CARTESIAN_POINT('Ctrl Pts',(-214.675168661468,-2.17227813150008,
126.389705073814));
#128268=CARTESIAN_POINT('Ctrl Pts',(-214.682925702353,-2.29354631551489,
126.453633280547));
#128269=CARTESIAN_POINT('Ctrl Pts',(-214.690676893593,-2.41472305024863,
126.517513278521));
#128270=CARTESIAN_POINT('Ctrl Pts',(-214.698428084833,-2.53332352200339,
126.586509488989));
#128271=CARTESIAN_POINT('Ctrl Pts',(-214.706179276073,-2.64889152517579,
126.660382245234));
#128272=CARTESIAN_POINT('Ctrl Pts',(-214.71392717285,-2.76441040886476,
126.734223603588));
#128273=CARTESIAN_POINT('Ctrl Pts',(-214.721675069627,-2.8768990587289,
126.812937175225));
#128274=CARTESIAN_POINT('Ctrl Pts',(-214.729422966404,-2.98592735181132,
126.89623818957));
#128275=CARTESIAN_POINT('Ctrl Pts',(-214.737169242488,-3.09493283852521,
126.979521779139));
#128276=CARTESIAN_POINT('Ctrl Pts',(-214.744915518572,-3.20047909772844,
127.06739066552));
#128277=CARTESIAN_POINT('Ctrl Pts',(-214.752661794656,-3.3021667321985,
127.159517968663));
#128278=CARTESIAN_POINT('Ctrl Pts',(-214.760408127922,-3.40385511730371,
127.251645951869));
#128279=CARTESIAN_POINT('Ctrl Pts',(-214.768154461187,-3.50168453110043,
127.348032152063));
#128280=CARTESIAN_POINT('Ctrl Pts',(-214.775900794452,-3.59529059186724,
127.448311061536));
#128281=CARTESIAN_POINT('Ctrl Pts',(-214.783648862455,-3.68891761506246,
127.548612427776));
#128282=CARTESIAN_POINT('Ctrl Pts',(-214.791396930458,-3.77831913648335,
127.652807952222));
#128283=CARTESIAN_POINT('Ctrl Pts',(-214.799144998461,-3.86316967556741,
127.760497427428));
#128284=CARTESIAN_POINT('Ctrl Pts',(-214.806901301203,-3.94811039481379,
127.86830135629));
#128285=CARTESIAN_POINT('Ctrl Pts',(-214.814657603945,-4.0284902272672,
127.979606346268));
#128286=CARTESIAN_POINT('Ctrl Pts',(-214.822413906687,-4.10402551349094,
128.093981004465));
#128287=CARTESIAN_POINT('Ctrl Pts',(-214.830174349201,-4.17960111517126,
128.20841670786));
#128288=CARTESIAN_POINT('Ctrl Pts',(-214.837934791715,-4.25032681692145,
128.325925009264));
#128289=CARTESIAN_POINT('Ctrl Pts',(-214.84569523423,-4.31596443774793,
128.446048925996));
#128290=CARTESIAN_POINT('Ctrl Pts',(-214.853468134495,-4.38170742591057,
128.566365676303));
#128291=CARTESIAN_POINT('Ctrl Pts',(-214.86124103476,-4.44234583816004,
128.689306081678));
#128292=CARTESIAN_POINT('Ctrl Pts',(-214.869013935026,-4.49768888549772,
128.814391333439));
#128293=CARTESIAN_POINT('Ctrl Pts',(-214.876504270788,-4.55102007366499,
128.934929421229));
#128294=CARTESIAN_POINT('Ctrl Pts',(-214.88399460655,-4.59943409927662,
129.057458835167));
#128295=CARTESIAN_POINT('Ctrl Pts',(-214.891484942312,-4.64280435724053,
129.181538765702));
#128296=CARTESIAN_POINT('Ctrl Pts',(-214.899438353548,-4.68885589724191,
129.313289697161));
#128297=CARTESIAN_POINT('Ctrl Pts',(-214.907391764783,-4.72932661485808,
129.447086512125));
#128298=CARTESIAN_POINT('Ctrl Pts',(-214.915345176019,-4.76405452823394,
129.582490119308));
#128299=CARTESIAN_POINT('Ctrl Pts',(-213.165046531412,-4.76405452823396,
129.582490119308));
#128300=CARTESIAN_POINT('Ctrl Pts',(-213.17281002151,-4.79810457133673,
129.715250720584));
#128301=CARTESIAN_POINT('Ctrl Pts',(-213.180573511608,-4.82656878613077,
129.849310261608));
#128302=CARTESIAN_POINT('Ctrl Pts',(-213.188337001706,-4.84937648881122,
129.984158976343));
#128303=CARTESIAN_POINT('Ctrl Pts',(-213.196111695209,-4.87221710502965,
130.119202289734));
#128304=CARTESIAN_POINT('Ctrl Pts',(-213.203886388712,-4.88938486259401,
130.255036664043));
#128305=CARTESIAN_POINT('Ctrl Pts',(-213.211661082215,-4.90086100994425,
130.391148294773));
#128306=CARTESIAN_POINT('Ctrl Pts',(-213.214707121288,-4.90535723776683,
130.444475328871));
#128307=CARTESIAN_POINT('Ctrl Pts',(-213.217753160361,-4.90898037685139,
130.497844933484));
#128308=CARTESIAN_POINT('Ctrl Pts',(-213.220799199435,-4.91173147644005,
130.551226333345));
#128309=CARTESIAN_POINT('Ctrl Pts',(-213.225579654294,-4.91604905316183,
130.635003122221));
#128310=CARTESIAN_POINT('Ctrl Pts',(-213.230360109153,-4.91822339794989,
130.718891315629));
#128311=CARTESIAN_POINT('Ctrl Pts',(-213.235140564013,-4.91824975740856,
130.802815868178));
#128312=CARTESIAN_POINT('',(-212.889859436032,-4.91824792006025,130.808883815883));
#128313=CARTESIAN_POINT('Ctrl Pts',(-212.819861628446,-4.76405452823406,
129.582490119308));
#128314=CARTESIAN_POINT('Ctrl Pts',(-212.827525902297,-4.79780353608479,
129.714076988706));
#128315=CARTESIAN_POINT('Ctrl Pts',(-212.835190176148,-4.82609468643265,
129.847055964322));
#128316=CARTESIAN_POINT('Ctrl Pts',(-212.842854449999,-4.84882921225431,
129.980929786901));
#128317=CARTESIAN_POINT('Ctrl Pts',(-212.850688614332,-4.87206768399697,
130.117771129778));
#128318=CARTESIAN_POINT('Ctrl Pts',(-212.858522778665,-4.88950020618528,
130.255547027938));
#128319=CARTESIAN_POINT('Ctrl Pts',(-212.866356942997,-4.90107709067464,
130.393719151364));
#128320=CARTESIAN_POINT('Ctrl Pts',(-212.87419110733,-4.91265397516397,
130.531891274791));
#128321=CARTESIAN_POINT('Ctrl Pts',(-212.882025271663,-4.91837522596484,
130.670459178147));
#128322=CARTESIAN_POINT('Ctrl Pts',(-212.889859435996,-4.91824792006084,
130.808883815247));
#128323=CARTESIAN_POINT('Ctrl Pts',(-212.889859436032,-4.91824792006025,
130.808883815883));
#128324=CARTESIAN_POINT('Ctrl Pts',(-212.899688380504,-4.91808819876975,
130.982554933039));
#128325=CARTESIAN_POINT('Ctrl Pts',(-212.909517324976,-4.90872606161266,
131.155814327766));
#128326=CARTESIAN_POINT('Ctrl Pts',(-212.919346269448,-4.89031323752669,
131.327829338094));
#128327=CARTESIAN_POINT('Ctrl Pts',(-212.929374726559,-4.87152666108868,
131.503335991767));
#128328=CARTESIAN_POINT('Ctrl Pts',(-212.93940318367,-4.84331824636661,
131.677547435274));
#128329=CARTESIAN_POINT('Ctrl Pts',(-212.949431640781,-4.80589734544945,
131.849604018646));
#128330=CARTESIAN_POINT('Ctrl Pts',(-212.953601284448,-4.7903384393498,
131.921141906802));
#128331=CARTESIAN_POINT('Ctrl Pts',(-212.957770928114,-4.77318750011992,
131.992307548351));
#128332=CARTESIAN_POINT('Ctrl Pts',(-212.961940571781,-4.75446197453151,
132.063040241312));
#128333=CARTESIAN_POINT('Ctrl Pts',(-212.9697149059,-4.71954808161507,132.194921915666));
#128334=CARTESIAN_POINT('Ctrl Pts',(-212.977489240019,-4.67908742803143,
132.32555869136));
#128335=CARTESIAN_POINT('Ctrl Pts',(-212.985263574138,-4.63318394857371,
132.454448361045));
#128336=CARTESIAN_POINT('Ctrl Pts',(-212.993028327086,-4.58733704105191,
132.58317918573));
#128337=CARTESIAN_POINT('Ctrl Pts',(-213.000793080033,-4.53606078408245,
132.710166823768));
#128338=CARTESIAN_POINT('Ctrl Pts',(-213.00855783298,-4.4795096801859,132.834921152891));
#128339=CARTESIAN_POINT('Ctrl Pts',(-213.016314873865,-4.42301474364282,
132.959551574257));
#128340=CARTESIAN_POINT('Ctrl Pts',(-213.02407191475,-4.36125554649349,
133.081952747152));
#128341=CARTESIAN_POINT('Ctrl Pts',(-213.031828955635,-4.2944356474614,
133.201651908234));
#128342=CARTESIAN_POINT('Ctrl Pts',(-213.039580146875,-4.22766613783504,
133.321260803248));
#128343=CARTESIAN_POINT('Ctrl Pts',(-213.047331338115,-4.15584371226501,
133.43817140219));
#128344=CARTESIAN_POINT('Ctrl Pts',(-213.055082529355,-4.0792189161274,
133.551933382173));
#128345=CARTESIAN_POINT('Ctrl Pts',(-213.062830426133,-4.00262668757228,
133.665647010279));
#128346=CARTESIAN_POINT('Ctrl Pts',(-213.070578322909,-3.92123636606752,
133.776214357509));
#128347=CARTESIAN_POINT('Ctrl Pts',(-213.078326219686,-3.83534296194653,
133.883212258478));
#128348=CARTESIAN_POINT('Ctrl Pts',(-213.086072495771,-3.74946752487404,
133.990187777793));
#128349=CARTESIAN_POINT('Ctrl Pts',(-213.093818771855,-3.65909112336248,
134.093595031289));
#128350=CARTESIAN_POINT('Ctrl Pts',(-213.101565047939,-3.56455012776312,
134.193042580979));
#128351=CARTESIAN_POINT('Ctrl Pts',(-213.109311381204,-3.47000843428349,
134.29249086477));
#128352=CARTESIAN_POINT('Ctrl Pts',(-213.11705771447,-3.37130235474808,
134.387979103073));
#128353=CARTESIAN_POINT('Ctrl Pts',(-213.124804047735,-3.26880603576509,
134.479151790279));
#128354=CARTESIAN_POINT('Ctrl Pts',(-213.132552115738,-3.16628676344253,
134.570344894975));
#128355=CARTESIAN_POINT('Ctrl Pts',(-213.140300183741,-3.0599758547263,
134.657220265677));
#128356=CARTESIAN_POINT('Ctrl Pts',(-213.148048251744,-2.95028121244969,
134.739462119429));
#128357=CARTESIAN_POINT('Ctrl Pts',(-213.155804554486,-2.84046998540144,
134.821791380802));
#128358=CARTESIAN_POINT('Ctrl Pts',(-213.163560857228,-2.72726815416231,
134.899477052992));
#128359=CARTESIAN_POINT('Ctrl Pts',(-213.171317159969,-2.61111379444569,
134.972245910488));
#128360=CARTESIAN_POINT('Ctrl Pts',(-213.179077602484,-2.49489743964994,
135.045053606914));
#128361=CARTESIAN_POINT('Ctrl Pts',(-213.186838044998,-2.37572575590294,
135.112939066182));
#128362=CARTESIAN_POINT('Ctrl Pts',(-213.194598487512,-2.25406130997421,
135.175675142212));
#128363=CARTESIAN_POINT('Ctrl Pts',(-213.202371387777,-2.132201557476,135.23851192776));
#128364=CARTESIAN_POINT('Ctrl Pts',(-213.210144288043,-2.0078414012049,
135.296182646899));
#128365=CARTESIAN_POINT('Ctrl Pts',(-213.217917188308,-1.88146409036836,
135.348508055662));
#128366=CARTESIAN_POINT('Ctrl Pts',(-213.22540752407,-1.75968091310596,
135.398931304016));
#128367=CARTESIAN_POINT('Ctrl Pts',(-213.232897859832,-1.63602498149208,
135.4443910195));
#128368=CARTESIAN_POINT('Ctrl Pts',(-213.240388195594,-1.51094001630837,
135.484771211693));
#128369=CARTESIAN_POINT('Ctrl Pts',(-213.248162529713,-1.38111241665115,
135.526682431147));
#128370=CARTESIAN_POINT('Ctrl Pts',(-213.255936863832,-1.2493340258649,
135.563254105625));
#128371=CARTESIAN_POINT('Ctrl Pts',(-213.263711197951,-1.11608354451254,
135.594302223073));
#128372=CARTESIAN_POINT('Ctrl Pts',(-213.271475950898,-0.982997282469519,
135.625312076491));
#128373=CARTESIAN_POINT('Ctrl Pts',(-213.279240703846,-0.848442916727878,
135.650811829488));
#128374=CARTESIAN_POINT('Ctrl Pts',(-213.287005456793,-0.712916313416165,
135.670666546355));
#128375=CARTESIAN_POINT('Ctrl Pts',(-213.294762497678,-0.577524317037452,
135.690501543237));
#128376=CARTESIAN_POINT('Ctrl Pts',(-213.302519538563,-0.441162389088791,
135.704702605328));
#128377=CARTESIAN_POINT('Ctrl Pts',(-213.310276579448,-0.30433830722044,
135.713185452214));
#128378=CARTESIAN_POINT('Ctrl Pts',(-213.318027770688,-0.167617405456748,
135.721661902119));
#128379=CARTESIAN_POINT('Ctrl Pts',(-213.325778961928,-0.0304354321061462,
135.724428695799));
#128380=CARTESIAN_POINT('Ctrl Pts',(-213.333530153168,0.106693317536995,
135.721453213653));
#128381=CARTESIAN_POINT('Ctrl Pts',(-213.341278049945,0.243763783803695,
135.718478996166));
#128382=CARTESIAN_POINT('Ctrl Pts',(-213.349025946722,0.38078068130049,
135.709767365526));
#128383=CARTESIAN_POINT('Ctrl Pts',(-213.356773843499,0.517228528714356,
135.695337791054));
#128384=CARTESIAN_POINT('Ctrl Pts',(-213.364520119583,0.653647834180018,
135.680911234939));
#128385=CARTESIAN_POINT('Ctrl Pts',(-213.372266395667,0.789497937775043,
135.660769155131));
#128386=CARTESIAN_POINT('Ctrl Pts',(-213.380012671751,0.924267695244507,
135.634982967743));
#128387=CARTESIAN_POINT('Ctrl Pts',(-213.387759005017,1.05903844755389,
135.609196590006));
#128388=CARTESIAN_POINT('Ctrl Pts',(-213.395505338282,1.19272845382499,
135.577766095025));
#128389=CARTESIAN_POINT('Ctrl Pts',(-213.403251671548,1.32483638173783,
135.540814103469));
#128390=CARTESIAN_POINT('Ctrl Pts',(-213.41099973955,1.45697389430497,135.503853836771));
#128391=CARTESIAN_POINT('Ctrl Pts',(-213.418747807553,1.58752824706523,
135.4613697183));
#128392=CARTESIAN_POINT('Ctrl Pts',(-213.426495875556,1.71601328142853,
135.413534239861));
#128393=CARTESIAN_POINT('Ctrl Pts',(-213.434252178298,1.84463487121552,
135.365647921306));
#128394=CARTESIAN_POINT('Ctrl Pts',(-213.44200848104,1.97118238229435,135.312399018039));
#128395=CARTESIAN_POINT('Ctrl Pts',(-213.449764783782,2.09518915168188,
135.254008410501));
#128396=CARTESIAN_POINT('Ctrl Pts',(-213.457525226296,2.219262107216,135.195586638139));
#128397=CARTESIAN_POINT('Ctrl Pts',(-213.46528566881,2.34079127270939,135.132017874414));
#128398=CARTESIAN_POINT('Ctrl Pts',(-213.473046111324,2.45933551509492,
135.063568511846));
#128399=CARTESIAN_POINT('Ctrl Pts',(-213.48081901159,2.57807005522219,134.995009268284));
#128400=CARTESIAN_POINT('Ctrl Pts',(-213.488591911855,2.69380976668411,
134.921553979131));
#128401=CARTESIAN_POINT('Ctrl Pts',(-213.496364812121,2.80614263845336,
134.843512329888));
#128402=CARTESIAN_POINT('Ctrl Pts',(-213.503855147883,2.91439192738467,
134.76830769117));
#128403=CARTESIAN_POINT('Ctrl Pts',(-213.511345483645,3.01947752500861,
134.688844540419));
#128404=CARTESIAN_POINT('Ctrl Pts',(-213.518835819407,3.12106200337956,
134.605433496841));
#128405=CARTESIAN_POINT('Ctrl Pts',(-213.526610153526,3.22649808812344,
134.518859898194));
#128406=CARTESIAN_POINT('Ctrl Pts',(-213.534384487645,3.32849631271204,
134.427758889236));
#128407=CARTESIAN_POINT('Ctrl Pts',(-213.542158821764,3.42664311324413,
134.332433751297));
#128408=CARTESIAN_POINT('Ctrl Pts',(-213.549923574711,3.5246689566162,134.237226093072));
#128409=CARTESIAN_POINT('Ctrl Pts',(-213.557688327658,3.61885254235966,
134.137804933757));
#128410=CARTESIAN_POINT('Ctrl Pts',(-213.565453080606,3.70881231748571,
134.034514523523));
#128411=CARTESIAN_POINT('Ctrl Pts',(-213.573210121491,3.79868274329489,
133.93132670278));
#128412=CARTESIAN_POINT('Ctrl Pts',(-213.580967162376,3.88433745190876,
133.824277571767));
#128413=CARTESIAN_POINT('Ctrl Pts',(-213.588724203261,3.96543106960454,
133.713748782579));
#128414=CARTESIAN_POINT('Ctrl Pts',(-213.596475394501,4.04646353397251,
133.60330334401));
#128415=CARTESIAN_POINT('Ctrl Pts',(-213.604226585741,4.12294152330685,
133.489383784201));
#128416=CARTESIAN_POINT('Ctrl Pts',(-213.611977776981,4.19455960464572,
133.372405162658));
#128417=CARTESIAN_POINT('Ctrl Pts',(-213.619725673758,4.26614724638944,
133.255476260149));
#128418=CARTESIAN_POINT('Ctrl Pts',(-213.627473570535,4.33287888472626,
133.13549121461));
#128419=CARTESIAN_POINT('Ctrl Pts',(-213.635221467312,4.39449226950757,
133.012894238713));
#128420=CARTESIAN_POINT('Ctrl Pts',(-213.642967743396,4.45609276609701,
132.890322907461));
#128421=CARTESIAN_POINT('Ctrl Pts',(-213.65071401948,4.51257696321814,132.765141081698));
#128422=CARTESIAN_POINT('Ctrl Pts',(-213.658460295564,4.56372865931191,
132.637817403715));
#128423=CARTESIAN_POINT('Ctrl Pts',(-213.66620662883,4.61488073299595,132.510492785857));
#128424=CARTESIAN_POINT('Ctrl Pts',(-213.673952962095,4.66070008135946,
132.381026647013));
#128425=CARTESIAN_POINT('Ctrl Pts',(-213.681699295361,4.70101888628126,
132.249907051731));
#128426=CARTESIAN_POINT('Ctrl Pts',(-213.689447363364,4.74134672031982,
132.118758093124));
#128427=CARTESIAN_POINT('Ctrl Pts',(-213.697195431367,4.77617144487178,
131.98595531489));
#128428=CARTESIAN_POINT('Ctrl Pts',(-213.70494349937,4.80537540158441,131.852000972052));
#128429=CARTESIAN_POINT('Ctrl Pts',(-213.712699802111,4.83461039660973,
131.717904260944));
#128430=CARTESIAN_POINT('Ctrl Pts',(-213.720456104853,4.85821260703629,
131.58265392297));
#128431=CARTESIAN_POINT('Ctrl Pts',(-213.728212407595,4.87611562309497,
131.446761966186));
#128432=CARTESIAN_POINT('Ctrl Pts',(-213.735972850109,4.89402819453241,
131.310797479774));
#128433=CARTESIAN_POINT('Ctrl Pts',(-213.743733292623,4.90623547571352,
131.174191081412));
#128434=CARTESIAN_POINT('Ctrl Pts',(-213.751493735138,4.91272314701169,
131.037457900509));
#128435=CARTESIAN_POINT('Ctrl Pts',(-213.759266635403,4.91922123289577,
130.900505223366));
#128436=CARTESIAN_POINT('Ctrl Pts',(-213.767039535668,4.91998135891421,
130.763425748162));
#128437=CARTESIAN_POINT('Ctrl Pts',(-213.774812435934,4.91504137022605,
130.626733504021));
#128438=CARTESIAN_POINT('Ctrl Pts',(-213.782302771696,4.91028096256978,
130.495010367261));
#128439=CARTESIAN_POINT('Ctrl Pts',(-213.789793107458,4.90022769570384,
130.363647103825));
#128440=CARTESIAN_POINT('Ctrl Pts',(-213.79728344322,4.8849605143164,130.233095498668));
#128441=CARTESIAN_POINT('Ctrl Pts',(-213.805057777339,4.86911447310636,
130.097593989721));
#128442=CARTESIAN_POINT('Ctrl Pts',(-213.812832111458,4.84760114599064,
129.962537674027));
#128443=CARTESIAN_POINT('Ctrl Pts',(-213.820606445577,4.82045215075121,
129.828438425576));
#128444=CARTESIAN_POINT('Ctrl Pts',(-213.828371198524,4.79333661422204,
129.694504442464));
#128445=CARTESIAN_POINT('Ctrl Pts',(-213.836135951471,4.76059930579301,
129.561525559254));
#128446=CARTESIAN_POINT('Ctrl Pts',(-213.843900704418,4.72232361417188,
129.430008862907));
#128447=CARTESIAN_POINT('Ctrl Pts',(-213.851657745303,4.68408593850726,
129.298622790797));
#128448=CARTESIAN_POINT('Ctrl Pts',(-213.859414786189,4.64032093503532,
129.16869638844));
#128449=CARTESIAN_POINT('Ctrl Pts',(-213.867171827074,4.59116301553957,
129.04072652081));
#128450=CARTESIAN_POINT('Ctrl Pts',(-213.874923018314,4.54204216641324,
128.912853156252));
#128451=CARTESIAN_POINT('Ctrl Pts',(-213.882674209554,4.48753663569018,
128.786933753139));
#128452=CARTESIAN_POINT('Ctrl Pts',(-213.890425400794,4.42783053071177,
128.663449630674));
#128453=CARTESIAN_POINT('Ctrl Pts',(-213.898173297571,4.3681498024206,128.540017992254));
#128454=CARTESIAN_POINT('Ctrl Pts',(-213.905921194348,4.30327306598751,
128.419019927071));
#128455=CARTESIAN_POINT('Ctrl Pts',(-213.913669091125,4.23343229750322,
128.300916181403));
#128456=CARTESIAN_POINT('Ctrl Pts',(-213.921415367209,4.1636061382023,128.182837140492));
#128457=CARTESIAN_POINT('Ctrl Pts',(-213.929161643293,4.08881821110166,
128.067651551178));
#128458=CARTESIAN_POINT('Ctrl Pts',(-213.936907919378,4.00934593600885,
127.955794622559));
#128459=CARTESIAN_POINT('Ctrl Pts',(-213.944654252643,3.92987307426966,
127.843936868238));
#128460=CARTESIAN_POINT('Ctrl Pts',(-213.952400585908,3.84571602197914,
127.735408142357));
#128461=CARTESIAN_POINT('Ctrl Pts',(-213.960146919174,3.75719469186991,
127.630613445864));
#128462=CARTESIAN_POINT('Ctrl Pts',(-213.967894987177,3.6686535380227,127.525795281326));
#128463=CARTESIAN_POINT('Ctrl Pts',(-213.97564305518,3.57574641378552,127.424713108749));
#128464=CARTESIAN_POINT('Ctrl Pts',(-213.983391123182,3.47883228332121,
127.327737398547));
#128465=CARTESIAN_POINT('Ctrl Pts',(-213.991147425924,3.38181515136562,
127.230658621406));
#128466=CARTESIAN_POINT('Ctrl Pts',(-213.998903728666,3.28078278279008,
127.137695301976));
#128467=CARTESIAN_POINT('Ctrl Pts',(-214.006660031408,3.17613004837301,
127.049180065539));
#128468=CARTESIAN_POINT('Ctrl Pts',(-214.014420473922,3.07142145764054,
126.960617585855));
#128469=CARTESIAN_POINT('Ctrl Pts',(-214.022180916436,2.96308895946279,
126.876508159358));
#128470=CARTESIAN_POINT('Ctrl Pts',(-214.029941358951,2.85155820669096,
126.797142273583));
#128471=CARTESIAN_POINT('Ctrl Pts',(-214.037714259216,2.73984841485356,
126.717648982642));
#128472=CARTESIAN_POINT('Ctrl Pts',(-214.045487159481,2.62493043675181,
126.642914662395));
#128473=CARTESIAN_POINT('Ctrl Pts',(-214.053260059747,2.50725719587883,
126.573185317934));
#128474=CARTESIAN_POINT('Ctrl Pts',(-214.060750395509,2.39386167371291,
126.505990810783));
#128475=CARTESIAN_POINT('Ctrl Pts',(-214.068240731271,2.27790800347818,
126.443443856307));
#128476=CARTESIAN_POINT('Ctrl Pts',(-214.075731067033,2.15981895618485,
126.38572223691));
#128477=CARTESIAN_POINT('Ctrl Pts',(-214.083505401152,2.03725252677082,
126.325812084769));
#128478=CARTESIAN_POINT('Ctrl Pts',(-214.091279735271,1.91199734458572,
126.270910618594));
#128479=CARTESIAN_POINT('Ctrl Pts',(-214.09905406939,1.7845011538977,126.221267917845));
#128480=CARTESIAN_POINT('Ctrl Pts',(-214.106818822337,1.65716209087004,
126.171686397287));
#128481=CARTESIAN_POINT('Ctrl Pts',(-214.114583575284,1.52758787540842,
126.127350887472));
#128482=CARTESIAN_POINT('Ctrl Pts',(-214.122348328231,1.39625020776847,
126.088465324008));
#128483=CARTESIAN_POINT('Ctrl Pts',(-214.130105369116,1.26504298655157,
126.049618382233));
#128484=CARTESIAN_POINT('Ctrl Pts',(-214.137862410001,1.13207617114529,
126.01621072504));
#128485=CARTESIAN_POINT('Ctrl Pts',(-214.145619450886,0.997840440976765,
125.988397835645));
#128486=CARTESIAN_POINT('Ctrl Pts',(-214.153370642126,0.863705939016377,
125.960605920165));
#128487=CARTESIAN_POINT('Ctrl Pts',(-214.161121833366,0.728304808227223,
125.938400453705));
#128488=CARTESIAN_POINT('Ctrl Pts',(-214.168873024607,0.592141510601337,
125.921886706328));
#128489=CARTESIAN_POINT('Ctrl Pts',(-214.176620921384,0.456036086009031,
125.905379977734));
#128490=CARTESIAN_POINT('Ctrl Pts',(-214.184368818161,0.319169526183115,
125.894560203726));
#128491=CARTESIAN_POINT('Ctrl Pts',(-214.192116714938,0.182054858758954,
125.889481260867));
#128492=CARTESIAN_POINT('Ctrl Pts',(-214.199862991022,0.0449688727677412,
125.884403380414));
#128493=CARTESIAN_POINT('Ctrl Pts',(-214.207609267106,-0.0923647271424954,
125.885063956999));
#128494=CARTESIAN_POINT('Ctrl Pts',(-214.21535554319,-0.229429835048029,
125.89146483063));
#128495=CARTESIAN_POINT('Ctrl Pts',(-214.223101876455,-0.36649595473724,
125.897865751512));
#128496=CARTESIAN_POINT('Ctrl Pts',(-214.230848209721,-0.503293187927333,
125.910007035755));
#128497=CARTESIAN_POINT('Ctrl Pts',(-214.238594542986,-0.639307875204561,
125.927838444623));
#128498=CARTESIAN_POINT('Ctrl Pts',(-214.246342610989,-0.775353022027759,
125.945673846712));
#128499=CARTESIAN_POINT('Ctrl Pts',(-214.254090678992,-0.910614886645424,
125.969201858252));
#128500=CARTESIAN_POINT('Ctrl Pts',(-214.261838746995,-1.04458775290843,
125.998320720835));
#128501=CARTESIAN_POINT('Ctrl Pts',(-214.269595049737,-1.17870300712818,
126.027470531291));
#128502=CARTESIAN_POINT('Ctrl Pts',(-214.277351352479,-1.31152614369052,
126.062222979452));
#128503=CARTESIAN_POINT('Ctrl Pts',(-214.285107655221,-1.44256387822435,
126.102425641437));
#128504=CARTESIAN_POINT('Ctrl Pts',(-214.292868097735,-1.57367155154257,
126.142649760794));
#128505=CARTESIAN_POINT('Ctrl Pts',(-214.300628540249,-1.70299155559054,
126.188329760138));
#128506=CARTESIAN_POINT('Ctrl Pts',(-214.308388982763,-1.83004941921517,
126.239264541279));
#128507=CARTESIAN_POINT('Ctrl Pts',(-214.316161883029,-1.95731124740217,
126.290281087452));
#128508=CARTESIAN_POINT('Ctrl Pts',(-214.323934783294,-2.08230332180388,
126.346569111495));
#128509=CARTESIAN_POINT('Ctrl Pts',(-214.331707683559,-2.20457385515677,
126.407880527806));
#128510=CARTESIAN_POINT('Ctrl Pts',(-214.339198019321,-2.32239954664107,
126.466963119699));
#128511=CARTESIAN_POINT('Ctrl Pts',(-214.346688355083,-2.43769786195061,
126.530710069758));
#128512=CARTESIAN_POINT('Ctrl Pts',(-214.354178690845,-2.55009070965804,
126.598861784489));
#128513=CARTESIAN_POINT('Ctrl Pts',(-214.361954303879,-2.66676415652064,
126.669609128553));
#128514=CARTESIAN_POINT('Ctrl Pts',(-214.369729916912,-2.78067608162571,
126.745327550003));
#128515=CARTESIAN_POINT('Ctrl Pts',(-214.377505529946,-2.89137384784176,
126.825775399864));
#128516=CARTESIAN_POINT('Ctrl Pts',(-214.385516368049,-3.00542040335608,
126.908656929354));
#128517=CARTESIAN_POINT('Ctrl Pts',(-214.393527206152,-3.11605486394476,
126.996558427291));
#128518=CARTESIAN_POINT('Ctrl Pts',(-214.401538044254,-3.22280931507134,
127.089164366869));
#128519=CARTESIAN_POINT('Ctrl Pts',(-214.409294136315,-3.32616895612055,
127.178825421494));
#128520=CARTESIAN_POINT('Ctrl Pts',(-214.417050228375,-3.42589125052493,
127.272896014297));
#128521=CARTESIAN_POINT('Ctrl Pts',(-214.424806320435,-3.52158131705236,
127.371046170871));
#128522=CARTESIAN_POINT('Ctrl Pts',(-214.432557091884,-3.61720574102127,
127.469128997285));
#128523=CARTESIAN_POINT('Ctrl Pts',(-214.440307863332,-3.7088031687662,
127.571285540742));
#128524=CARTESIAN_POINT('Ctrl Pts',(-214.448058634781,-3.79601356772482,
127.677147152491));
#128525=CARTESIAN_POINT('Ctrl Pts',(-214.455805767883,-3.88318302861947,
127.782959070974));
#128526=CARTESIAN_POINT('Ctrl Pts',(-214.463552900986,-3.96596931125054,
127.892472295287));
#128527=CARTESIAN_POINT('Ctrl Pts',(-214.471300034089,-4.04405115289793,
128.005283388327));
#128528=CARTESIAN_POINT('Ctrl Pts',(-214.479045208286,-4.12211325112459,
128.118065956465));
#128529=CARTESIAN_POINT('Ctrl Pts',(-214.486790382484,-4.19547305505162,
128.234144411599));
#128530=CARTESIAN_POINT('Ctrl Pts',(-214.494535556682,-4.26385154744425,
128.353084818343));
#128531=CARTESIAN_POINT('Ctrl Pts',(-214.50228230773,-4.33224396110775,
128.472049440327));
#128532=CARTESIAN_POINT('Ctrl Pts',(-214.510029058778,-4.39565283897423,
128.593876840954));
#128533=CARTESIAN_POINT('Ctrl Pts',(-214.517775809827,-4.45384423488585,
128.718106895251));
#128534=CARTESIAN_POINT('Ctrl Pts',(-214.525523577688,-4.51204326880627,
128.842353255571));
#128535=CARTESIAN_POINT('Ctrl Pts',(-214.533271345549,-4.56502329847948,
128.969002540315));
#128536=CARTESIAN_POINT('Ctrl Pts',(-214.54101911341,-4.6125981490606,129.097573759818));
#128537=CARTESIAN_POINT('Ctrl Pts',(-214.548771782394,-4.66020309478569,
129.226226311565));
#128538=CARTESIAN_POINT('Ctrl Pts',(-214.556524451378,-4.70239590896414,
129.356802855539));
#128539=CARTESIAN_POINT('Ctrl Pts',(-214.564277120362,-4.73903997613716,
129.488806298249));
#128540=CARTESIAN_POINT('Ctrl Pts',(-214.566106628378,-4.74768739998518,
129.519957035778));
#128541=CARTESIAN_POINT('Ctrl Pts',(-214.567936136395,-4.75602604445474,
129.551187182902));
#128542=CARTESIAN_POINT('Ctrl Pts',(-214.569765644412,-4.76405452823405,
129.582490119308));
#128543=CARTESIAN_POINT('Origin',(213.235140564004,0.,130.804360617566));
#128544=CARTESIAN_POINT('',(-216.665311899804,-4.76405452823409,129.582490119308));
#128545=CARTESIAN_POINT('',(-216.320029411505,-4.76405452823406,129.582490119308));
#128546=CARTESIAN_POINT('',(213.235140564004,-4.76405452823405,129.582490119308));
#128547=CARTESIAN_POINT('',(-214.98514056396,-4.91824853507356,130.800564600342));
#128548=CARTESIAN_POINT('Ctrl Pts',(-214.985140564013,-4.91824853507428,
130.800564601278));
#128549=CARTESIAN_POINT('Ctrl Pts',(-214.99288611369,-4.91835442857352,
130.937763840683));
#128550=CARTESIAN_POINT('Ctrl Pts',(-215.000631663367,-4.9127150672855,
131.075028143919));
#128551=CARTESIAN_POINT('Ctrl Pts',(-215.008377213043,-4.90134090327774,
131.211841184411));
#128552=CARTESIAN_POINT('Ctrl Pts',(-215.016121641906,-4.88996838516001,
131.348634427474));
#128553=CARTESIAN_POINT('Ctrl Pts',(-215.023866070769,-4.87286274698048,
131.484976148621));
#128554=CARTESIAN_POINT('Ctrl Pts',(-215.031610499632,-4.85008645906864,
131.620353510954));
#128555=CARTESIAN_POINT('Ctrl Pts',(-215.039355480027,-4.82730854910443,
131.755740514417));
#128556=CARTESIAN_POINT('Ctrl Pts',(-215.047100460423,-4.79885925015112,
131.890162637197));
#128557=CARTESIAN_POINT('Ctrl Pts',(-215.054845440818,-4.76485239545887,
132.023116012217));
#128558=CARTESIAN_POINT('Ctrl Pts',(-215.062592645102,-4.73083577606034,
132.156107563383));
#128559=CARTESIAN_POINT('Ctrl Pts',(-215.070339849386,-4.69125852180174,
132.287629149257));
#128560=CARTESIAN_POINT('Ctrl Pts',(-215.078087053671,-4.64628458195234,
132.417191249099));
#128561=CARTESIAN_POINT('Ctrl Pts',(-215.085843204596,-4.6012587052108,
132.546902970096));
#128562=CARTESIAN_POINT('Ctrl Pts',(-215.093599355522,-4.55082382223927,
132.674650315509));
#128563=CARTESIAN_POINT('Ctrl Pts',(-215.101355506447,-4.49519260513584,
132.799962407812));
#128564=CARTESIAN_POINT('Ctrl Pts',(-215.10911621037,-4.43952873153182,
132.925348060511));
#128565=CARTESIAN_POINT('Ctrl Pts',(-215.116876914292,-4.3786626195065,
133.048295262303));
#128566=CARTESIAN_POINT('Ctrl Pts',(-215.124637618214,-4.31285286816823,
133.168357910296));
#128567=CARTESIAN_POINT('Ctrl Pts',(-215.132411345463,-4.24693268073255,
133.288622036793));
#128568=CARTESIAN_POINT('Ctrl Pts',(-215.140185072711,-4.17605247877902,
133.405991602627));
#128569=CARTESIAN_POINT('Ctrl Pts',(-215.14795879996,-4.10051464529449,
133.520048874017));
#128570=CARTESIAN_POINT('Ctrl Pts',(-215.155283388682,-4.02934112125313,
133.627516318778));
#128571=CARTESIAN_POINT('Ctrl Pts',(-215.162607977403,-3.95403316724271,
133.732043222698));
#128572=CARTESIAN_POINT('Ctrl Pts',(-215.169932566125,-3.87487514656703,
133.833308563804));
#128573=CARTESIAN_POINT('Ctrl Pts',(-215.177706900244,-3.79085665429191,
133.940791813218));
#128574=CARTESIAN_POINT('Ctrl Pts',(-215.185481234363,-3.70222955632382,
134.04494683786));
#128575=CARTESIAN_POINT('Ctrl Pts',(-215.193255568482,-3.60928712226211,
134.145352915009));
#128576=CARTESIAN_POINT('Ctrl Pts',(-215.201020321429,-3.51645923144414,
134.245635250641));
#128577=CARTESIAN_POINT('Ctrl Pts',(-215.208785074376,-3.41932684933196,
134.342177547528));
#128578=CARTESIAN_POINT('Ctrl Pts',(-215.216549827323,-3.3182249707409,
134.434590101504));
#128579=CARTESIAN_POINT('Ctrl Pts',(-215.224306868208,-3.2172235079604,
134.526910870029));
#128580=CARTESIAN_POINT('Ctrl Pts',(-215.232063909093,-3.11226068128255,
134.615109796181));
#128581=CARTESIAN_POINT('Ctrl Pts',(-215.239820949979,-3.00370974487943,
134.698832447098));
#128582=CARTESIAN_POINT('Ctrl Pts',(-215.247572141219,-2.8952406675823,
134.782491962112));
#128583=CARTESIAN_POINT('Ctrl Pts',(-215.255323332459,-2.78318917466306,
134.861681683));
#128584=CARTESIAN_POINT('Ctrl Pts',(-215.263074523699,-2.66796287655237,
134.936086304472));
#128585=CARTESIAN_POINT('Ctrl Pts',(-215.270822420476,-2.55278555269229,
135.010459301995));
#128586=CARTESIAN_POINT('Ctrl Pts',(-215.278570317253,-2.43443643520314,
135.080051033527));
#128587=CARTESIAN_POINT('Ctrl Pts',(-215.28631821403,-2.31335331555439,
135.14458866456));
#128588=CARTESIAN_POINT('Ctrl Pts',(-215.294064490114,-2.19229552388369,
135.209112795712));
#128589=CARTESIAN_POINT('Ctrl Pts',(-215.301810766198,-2.06850521238057,
135.268584745434));
#128590=CARTESIAN_POINT('Ctrl Pts',(-215.309557042282,-1.94244570013637,
135.322777128305));
#128591=CARTESIAN_POINT('Ctrl Pts',(-215.317303375548,-1.81638525734966,
135.376969911212));
#128592=CARTESIAN_POINT('Ctrl Pts',(-215.325049708813,-1.68805593957835,
135.42588289509));
#128593=CARTESIAN_POINT('Ctrl Pts',(-215.332796042078,-1.55794164364699,
135.469336597943));
#128594=CARTESIAN_POINT('Ctrl Pts',(-215.340544110081,-1.42779820952138,
135.51280003195));
#128595=CARTESIAN_POINT('Ctrl Pts',(-215.348292178084,-1.29586937257314,
135.550801628342));
#128596=CARTESIAN_POINT('Ctrl Pts',(-215.356040246087,-1.16265441971338,
135.583211709912));
#128597=CARTESIAN_POINT('Ctrl Pts',(-215.363796548829,-1.02929788441625,
135.615656237303));
#128598=CARTESIAN_POINT('Ctrl Pts',(-215.371552851571,-0.894652883168756,
135.642497286061));
#128599=CARTESIAN_POINT('Ctrl Pts',(-215.379309154313,-0.759229682932765,
135.663656178761));
#128600=CARTESIAN_POINT('Ctrl Pts',(-215.387069596827,-0.623734203257294,
135.6848263646));
#128601=CARTESIAN_POINT('Ctrl Pts',(-215.394830039341,-0.487460085253025,
135.700308307281));
#128602=CARTESIAN_POINT('Ctrl Pts',(-215.402590481855,-0.350921966350669,
135.710075329617));
#128603=CARTESIAN_POINT('Ctrl Pts',(-215.410363382121,-0.214164664338566,
135.719858030844));
#128604=CARTESIAN_POINT('Ctrl Pts',(-215.418136282386,-0.0771429055650763,
135.723907467401));
#128605=CARTESIAN_POINT('Ctrl Pts',(-215.425909182652,0.059628520693869,
135.722249138265));
#128606=CARTESIAN_POINT('Ctrl Pts',(-215.433399518413,0.191427961100384,
135.72065109357));
#128607=CARTESIAN_POINT('Ctrl Pts',(-215.440889854175,0.32299464584498,
135.713753077911));
#128608=CARTESIAN_POINT('Ctrl Pts',(-215.448380189937,0.453875025620668,
135.701623171648));
#128609=CARTESIAN_POINT('Ctrl Pts',(-215.456154524056,0.589717774777498,
135.689033356303));
#128610=CARTESIAN_POINT('Ctrl Pts',(-215.463928858176,0.725251458121523,
135.67076720368));
#128611=CARTESIAN_POINT('Ctrl Pts',(-215.471703192295,0.859963590330364,
135.646844038891));
#128612=CARTESIAN_POINT('Ctrl Pts',(-215.479467945242,0.994509701875095,
135.622950357265));
#128613=CARTESIAN_POINT('Ctrl Pts',(-215.487232698189,1.12823589558778,
135.593413602906));
#128614=CARTESIAN_POINT('Ctrl Pts',(-215.494997451136,1.26063322943629,
135.55830497182));
#128615=CARTESIAN_POINT('Ctrl Pts',(-215.502754492021,1.39289906438635,
135.523231211121));
#128616=CARTESIAN_POINT('Ctrl Pts',(-215.510511532906,1.52383829055938,
135.482596686299));
#128617=CARTESIAN_POINT('Ctrl Pts',(-215.518268573791,1.6529509605536,135.436523847042));
#128618=CARTESIAN_POINT('Ctrl Pts',(-215.526019765031,1.78196626567921,
135.39048575167));
#128619=CARTESIAN_POINT('Ctrl Pts',(-215.533770956271,1.90915738956395,
135.339017635671));
#128620=CARTESIAN_POINT('Ctrl Pts',(-215.541522147511,2.03403873354458,
135.282292003032));
#128621=CARTESIAN_POINT('Ctrl Pts',(-215.549270044288,2.15886699962287,
135.2255904803));
#128622=CARTESIAN_POINT('Ctrl Pts',(-215.557017941065,2.28138708314162,
135.163636046701));
#128623=CARTESIAN_POINT('Ctrl Pts',(-215.564765837842,2.40113280372063,
135.096649554881));
#128624=CARTESIAN_POINT('Ctrl Pts',(-215.572512113927,2.52085347607631,
135.029677075191));
#128625=CARTESIAN_POINT('Ctrl Pts',(-215.580258390011,2.63780059882454,
134.957674821708));
#128626=CARTESIAN_POINT('Ctrl Pts',(-215.588004666095,2.75153243088458,
134.880909690531));
#128627=CARTESIAN_POINT('Ctrl Pts',(-215.59575099936,2.86526510248701,134.804143992691));
#128628=CARTESIAN_POINT('Ctrl Pts',(-215.603497332626,2.9757821119846,134.722615565727));
#128629=CARTESIAN_POINT('Ctrl Pts',(-215.611243665891,3.0826708980365,134.63663451134));
#128630=CARTESIAN_POINT('Ctrl Pts',(-215.618991733894,3.18958362109106,
134.550634202091));
#128631=CARTESIAN_POINT('Ctrl Pts',(-215.626739801897,3.29286619930851,
134.460179526238));
#128632=CARTESIAN_POINT('Ctrl Pts',(-215.6344878699,3.39213965481177,134.365620454303));
#128633=CARTESIAN_POINT('Ctrl Pts',(-215.642244172642,3.49151861932478,
134.27096088386));
#128634=CARTESIAN_POINT('Ctrl Pts',(-215.650000475384,3.58687966588461,
134.17218847345));
#128635=CARTESIAN_POINT('Ctrl Pts',(-215.657756778126,3.67788078918729,
134.069689998046));
#128636=CARTESIAN_POINT('Ctrl Pts',(-215.66551722064,3.76893048252947,133.96713681612));
#128637=CARTESIAN_POINT('Ctrl Pts',(-215.673277663154,3.85561536884039,
133.860853909347));
#128638=CARTESIAN_POINT('Ctrl Pts',(-215.681038105668,3.93763482974399,
133.751259837099));
#128639=CARTESIAN_POINT('Ctrl Pts',(-215.688811005933,4.01978595556757,
133.641489834718));
#128640=CARTESIAN_POINT('Ctrl Pts',(-215.696583906199,4.09725646878812,
133.528398367776));
#128641=CARTESIAN_POINT('Ctrl Pts',(-215.704356806464,4.16978956624069,
133.412432325892));
#128642=CARTESIAN_POINT('Ctrl Pts',(-215.711847142226,4.23968590290239,
133.300681941729));
#128643=CARTESIAN_POINT('Ctrl Pts',(-215.719337477989,4.30499741376793,
133.186262617731));
#128644=CARTESIAN_POINT('Ctrl Pts',(-215.726827813751,4.36553622229401,
133.069592736873));
#128645=CARTESIAN_POINT('Ctrl Pts',(-215.73460214787,4.42837037814476,132.948499282023));
#128646=CARTESIAN_POINT('Ctrl Pts',(-215.742376481989,4.48626181306018,
132.824597654044));
#128647=CARTESIAN_POINT('Ctrl Pts',(-215.750150816108,4.53894977496981,
132.698329467046));
#128648=CARTESIAN_POINT('Ctrl Pts',(-215.757915569055,4.59157280367481,
132.572216894305));
#128649=CARTESIAN_POINT('Ctrl Pts',(-215.765680322002,4.63900496985399,
132.443743923006));
#128650=CARTESIAN_POINT('Ctrl Pts',(-215.773445074949,4.68103107712272,
132.313377223675));
#128651=CARTESIAN_POINT('Ctrl Pts',(-215.781202115834,4.72301544346936,
132.183140006386));
#128652=CARTESIAN_POINT('Ctrl Pts',(-215.788959156719,4.7596043170223,132.051013173795));
#128653=CARTESIAN_POINT('Ctrl Pts',(-215.796716197604,4.79063048438847,
131.917483532858));
#128654=CARTESIAN_POINT('Ctrl Pts',(-215.804467388844,4.82163325468052,
131.784054587661));
#128655=CARTESIAN_POINT('Ctrl Pts',(-215.812218580084,4.84708158031289,
131.649225319021));
#128656=CARTESIAN_POINT('Ctrl Pts',(-215.819969771324,4.86685811583843,
131.513497517464));
#128657=CARTESIAN_POINT('Ctrl Pts',(-215.827717668101,4.88662624580884,
131.377827403844));
#128658=CARTESIAN_POINT('Ctrl Pts',(-215.835465564878,4.90072732404231,
131.241259902949));
#128659=CARTESIAN_POINT('Ctrl Pts',(-215.843213461656,4.90909517824313,
131.104306601787));
#128660=CARTESIAN_POINT('Ctrl Pts',(-215.85095973774,4.91746128206925,130.967381948302));
#128661=CARTESIAN_POINT('Ctrl Pts',(-215.858706013824,4.92009652344186,
130.830072045059));
#128662=CARTESIAN_POINT('Ctrl Pts',(-215.866452289908,4.91698667776376,
130.6928928052));
#128663=CARTESIAN_POINT('Ctrl Pts',(-215.874198623173,4.91387680912948,
130.555712552715));
#128664=CARTESIAN_POINT('Ctrl Pts',(-215.881944956439,4.90502177768142,
130.418663356403));
#128665=CARTESIAN_POINT('Ctrl Pts',(-215.889691289704,4.89045948127991,
130.282259933349));
#128666=CARTESIAN_POINT('Ctrl Pts',(-215.897439357707,4.87589392375314,
130.145825963695));
#128667=CARTESIAN_POINT('Ctrl Pts',(-215.90518742571,4.8556185994924,130.01003844375));
#128668=CARTESIAN_POINT('Ctrl Pts',(-215.912935493713,4.82972310180959,
129.87540538595));
#128669=CARTESIAN_POINT('Ctrl Pts',(-215.920691796455,4.80380008208358,
129.740629238534));
#128670=CARTESIAN_POINT('Ctrl Pts',(-215.928448099196,4.77224503081357,
129.60701038882));
#128671=CARTESIAN_POINT('Ctrl Pts',(-215.936204401938,4.73519849051996,
129.47504563688));
#128672=CARTESIAN_POINT('Ctrl Pts',(-215.943964844452,4.69813217737235,
129.343010451377));
#128673=CARTESIAN_POINT('Ctrl Pts',(-215.951725286967,4.65556865626244,
129.212631494265));
#128674=CARTESIAN_POINT('Ctrl Pts',(-215.959485729481,4.60769758147039,
129.084387925861));
#128675=CARTESIAN_POINT('Ctrl Pts',(-215.967258629746,4.55974965977929,
128.955938489496));
#128676=CARTESIAN_POINT('Ctrl Pts',(-215.975031530012,4.50647731044224,
128.829631652349));
#128677=CARTESIAN_POINT('Ctrl Pts',(-215.982804430277,4.44811770596836,
128.705925024952));
#128678=CARTESIAN_POINT('Ctrl Pts',(-215.990294766039,4.39187962011544,
128.586715445057));
#128679=CARTESIAN_POINT('Ctrl Pts',(-215.997785101801,4.33091786925767,
128.46992058178));
#128680=CARTESIAN_POINT('Ctrl Pts',(-216.005275437563,4.26548289898048,
128.355924647195));
#128681=CARTESIAN_POINT('Ctrl Pts',(-216.013049771683,4.1975669419172,128.237606522104));
#128682=CARTESIAN_POINT('Ctrl Pts',(-216.020824105802,4.12461672787026,
128.12192896195));
#128683=CARTESIAN_POINT('Ctrl Pts',(-216.028598439921,4.04686285643546,
128.009350048051));
#128684=CARTESIAN_POINT('Ctrl Pts',(-216.036363192868,3.96920480969835,
127.896909877601));
#128685=CARTESIAN_POINT('Ctrl Pts',(-216.044127945815,3.88675510481507,
127.787561073731));
#128686=CARTESIAN_POINT('Ctrl Pts',(-216.051892698762,3.79979004601305,
127.681736934072));
#128687=CARTESIAN_POINT('Ctrl Pts',(-216.059649739647,3.71291136213365,
127.57601790044));
#128688=CARTESIAN_POINT('Ctrl Pts',(-216.067406780532,3.6215264957368,127.473816864476));
#128689=CARTESIAN_POINT('Ctrl Pts',(-216.075163821417,3.52595462837755,
127.375537638595));
#128690=CARTESIAN_POINT('Ctrl Pts',(-216.082915012657,3.4304548325068,127.277332525842));
#128691=CARTESIAN_POINT('Ctrl Pts',(-216.090666203897,3.33077459185006,
127.183043615665));
#128692=CARTESIAN_POINT('Ctrl Pts',(-216.098417395138,3.2272726489096,127.093040864149));
#128693=CARTESIAN_POINT('Ctrl Pts',(-216.106165291915,3.12381469705575,
127.003076366204));
#128694=CARTESIAN_POINT('Ctrl Pts',(-216.113913188692,3.01653856798293,
126.917394659643));
#128695=CARTESIAN_POINT('Ctrl Pts',(-216.121661085469,2.90583890658699,
126.836327942365));
#128696=CARTESIAN_POINT('Ctrl Pts',(-216.129407361553,2.79516240117381,
126.755278182496));
#128697=CARTESIAN_POINT('Ctrl Pts',(-216.137153637637,2.68106410308762,
126.678841722612));
#128698=CARTESIAN_POINT('Ctrl Pts',(-216.144899913721,2.56397037592471,
126.607309393923));
#128699=CARTESIAN_POINT('Ctrl Pts',(-216.152646246987,2.44687578440235,
126.535776537199));
#128700=CARTESIAN_POINT('Ctrl Pts',(-216.160392580252,2.32678605331634,
126.469148087725));
#128701=CARTESIAN_POINT('Ctrl Pts',(-216.168138913517,2.20415471344594,
126.407670378114));
#128702=CARTESIAN_POINT('Ctrl Pts',(-216.17588698152,2.08149591113775,126.346178900996));
#128703=CARTESIAN_POINT('Ctrl Pts',(-216.183635049523,1.95629471688963,
126.289840634199));
#128704=CARTESIAN_POINT('Ctrl Pts',(-216.191383117526,1.82902696332566,
126.238854793462));
#128705=CARTESIAN_POINT('Ctrl Pts',(-216.199139420268,1.70162394807853,
126.187814764367));
#128706=CARTESIAN_POINT('Ctrl Pts',(-216.20689572301,1.5721503495455,126.142138670594));
#128707=CARTESIAN_POINT('Ctrl Pts',(-216.214652025752,1.44110010636099,
126.101976802314));
#128708=CARTESIAN_POINT('Ctrl Pts',(-216.222412468266,1.30997991771584,
126.061793498435));
#128709=CARTESIAN_POINT('Ctrl Pts',(-216.23017291078,1.17728178574119,126.027130383204));
#128710=CARTESIAN_POINT('Ctrl Pts',(-216.237933353295,1.04351135435509,
125.998086892961));
#128711=CARTESIAN_POINT('Ctrl Pts',(-216.24570625356,0.909526182796591,
125.968996779528));
#128712=CARTESIAN_POINT('Ctrl Pts',(-216.253479153825,0.774465657443131,
125.945544385083));
#128713=CARTESIAN_POINT('Ctrl Pts',(-216.261252054091,0.638842976528521,
125.927777519346));
#128714=CARTESIAN_POINT('Ctrl Pts',(-216.268742389853,0.508150521681008,
125.910656523932));
#128715=CARTESIAN_POINT('Ctrl Pts',(-216.276232725615,0.376936379995533,
125.898814894981));
#128716=CARTESIAN_POINT('Ctrl Pts',(-216.283723061377,0.245659171928131,
125.892249601542));
#128717=CARTESIAN_POINT('Ctrl Pts',(-216.291497395496,0.109404548613506,
125.885435383006));
#128718=CARTESIAN_POINT('Ctrl Pts',(-216.299271729615,-0.0273496315022193,
125.884283917297));
#128719=CARTESIAN_POINT('Ctrl Pts',(-216.307046063734,-0.164093326920127,
125.888848798583));
#128720=CARTESIAN_POINT('Ctrl Pts',(-216.314810816681,-0.300668497954566,
125.893408054062));
#128721=CARTESIAN_POINT('Ctrl Pts',(-216.322575569628,-0.437232823004622,
125.903669626392));
#128722=CARTESIAN_POINT('Ctrl Pts',(-216.330340322575,-0.57327240731763,
125.919635260956));
#128723=CARTESIAN_POINT('Ctrl Pts',(-216.33809736346,-0.709176875197306,
125.935585038227));
#128724=CARTESIAN_POINT('Ctrl Pts',(-216.345854404345,-0.844557253723871,
125.957227558143));
#128725=CARTESIAN_POINT('Ctrl Pts',(-216.35361144523,-0.978901278650385,
125.984512554695));
#128726=CARTESIAN_POINT('Ctrl Pts',(-216.36136263647,-1.11314399370211,
126.01177697542));
#128727=CARTESIAN_POINT('Ctrl Pts',(-216.36911382771,-1.24635152913388,
126.04467532589));
#128728=CARTESIAN_POINT('Ctrl Pts',(-216.37686501895,-1.37801872132805,
126.083105756179));
#128729=CARTESIAN_POINT('Ctrl Pts',(-216.384612915727,-1.5096299514541,
126.121519852511));
#128730=CARTESIAN_POINT('Ctrl Pts',(-216.392360812504,-1.63970176594521,
126.165461242829));
#128731=CARTESIAN_POINT('Ctrl Pts',(-216.400108709281,-1.76774136209383,
126.214777462285));
#128732=CARTESIAN_POINT('Ctrl Pts',(-216.407854985365,-1.89575417511915,
126.264083365851));
#128733=CARTESIAN_POINT('Ctrl Pts',(-216.41560126145,-2.02173525073432,
126.31876172183));
#128734=CARTESIAN_POINT('Ctrl Pts',(-216.423347537534,-2.14520944446556,
126.378611019828));
#128735=CARTESIAN_POINT('Ctrl Pts',(-216.431093870799,-2.26868454965508,
126.43846075962));
#128736=CARTESIAN_POINT('Ctrl Pts',(-216.438840204064,-2.38965238421982,
126.503481347069));
#128737=CARTESIAN_POINT('Ctrl Pts',(-216.446586537329,-2.50766055709152,
126.57342436268));
#128738=CARTESIAN_POINT('Ctrl Pts',(-216.454334605332,-2.62569515707485,
126.643383041544));
#128739=CARTESIAN_POINT('Ctrl Pts',(-216.462082673335,-2.74076844021403,
126.718266142804));
#128740=CARTESIAN_POINT('Ctrl Pts',(-216.469830741338,-2.85245560150862,
126.79778101597));
#128741=CARTESIAN_POINT('Ctrl Pts',(-216.47758704408,-2.96426146524777,
126.87738039849));
#128742=CARTESIAN_POINT('Ctrl Pts',(-216.485343346822,-3.07267369912862,
126.961621159434));
#128743=CARTESIAN_POINT('Ctrl Pts',(-216.493099649564,-3.17729887387752,
127.050168969747));
#128744=CARTESIAN_POINT('Ctrl Pts',(-216.500860092078,-3.28197989023268,
127.138764040692));
#128745=CARTESIAN_POINT('Ctrl Pts',(-216.508620534592,-3.38286953245154,
127.231670476853));
#128746=CARTESIAN_POINT('Ctrl Pts',(-216.516380977106,-3.47961082903677,
127.32851661345));
#128747=CARTESIAN_POINT('Ctrl Pts',(-216.524153877372,-3.57650742333931,
127.425518216063));
#128748=CARTESIAN_POINT('Ctrl Pts',(-216.531926777637,-3.66924209998222,
127.526471869101));
#128749=CARTESIAN_POINT('Ctrl Pts',(-216.539699677902,-3.75749723911274,
127.630971646677));
#128750=CARTESIAN_POINT('Ctrl Pts',(-216.547190013665,-3.84254408163722,
127.731672594122));
#128751=CARTESIAN_POINT('Ctrl Pts',(-216.554680349427,-3.9234312281144,
127.835666078009));
#128752=CARTESIAN_POINT('Ctrl Pts',(-216.562170685189,-3.99991333301181,
127.942564609655));
#128753=CARTESIAN_POINT('Ctrl Pts',(-216.570019181474,-4.08005253306471,
128.054574638987));
#128754=CARTESIAN_POINT('Ctrl Pts',(-216.577867677758,-4.15560765333159,
128.170127216817));
#128755=CARTESIAN_POINT('Ctrl Pts',(-216.585716174042,-4.22625283006534,
128.28881493544));
#128756=CARTESIAN_POINT('Ctrl Pts',(-216.59355127153,-4.29677740275395,
128.407300032742));
#128757=CARTESIAN_POINT('Ctrl Pts',(-216.601386369017,-4.3624085362298,
128.5289092839));
#128758=CARTESIAN_POINT('Ctrl Pts',(-216.609221466504,-4.42286223498663,
128.65320448357));
#128759=CARTESIAN_POINT('Ctrl Pts',(-216.617048812269,-4.48325612334443,
128.77737671069));
#128760=CARTESIAN_POINT('Ctrl Pts',(-216.624876158033,-4.53848260209349,
128.904229258941));
#128761=CARTESIAN_POINT('Ctrl Pts',(-216.632703503798,-4.58830213122882,
129.03329692163));
#128762=CARTESIAN_POINT('Ctrl Pts',(-216.640523190109,-4.6380729094399,
129.162238285096));
#128763=CARTESIAN_POINT('Ctrl Pts',(-216.648342876421,-4.68244713921057,
129.293390091506));
#128764=CARTESIAN_POINT('Ctrl Pts',(-216.656162562732,-4.72123245764585,
129.426265140695));
#128765=CARTESIAN_POINT('Ctrl Pts',(-216.659212341756,-4.73635923458945,
129.478088132269));
#128766=CARTESIAN_POINT('Ctrl Pts',(-216.66226212078,-4.75063639532078,
129.530173022728));
#128767=CARTESIAN_POINT('Ctrl Pts',(-216.665311899804,-4.76405452823409,
129.582490119308));
#128768=CARTESIAN_POINT('Ctrl Pts',(-214.915345176019,-4.76405452823394,
129.582490119308));
#128769=CARTESIAN_POINT('Ctrl Pts',(-214.924420213177,-4.80367992857624,
129.736988953843));
#128770=CARTESIAN_POINT('Ctrl Pts',(-214.933495250334,-4.83582756235508,
129.893580088636));
#128771=CARTESIAN_POINT('Ctrl Pts',(-214.942570287492,-4.86030047730767,
130.051590843476));
#128772=CARTESIAN_POINT('Ctrl Pts',(-214.951568093968,-4.88456512205087,
130.208256889971));
#128773=CARTESIAN_POINT('Ctrl Pts',(-214.960565900445,-4.90128504720006,
130.366318388601));
#128774=CARTESIAN_POINT('Ctrl Pts',(-214.969563706922,-4.91031530497346,
130.525099685384));
#128775=CARTESIAN_POINT('Ctrl Pts',(-214.974755992601,-4.91552631703969,
130.616726222985));
#128776=CARTESIAN_POINT('Ctrl Pts',(-214.979948278281,-4.91817754857704,
130.708592090226));
#128777=CARTESIAN_POINT('Ctrl Pts',(-214.98514056396,-4.91824853507356,
130.800564600342));
#128778=CARTESIAN_POINT('',(-214.639859436029,-4.91824993606532,130.803567589537));
#128779=CARTESIAN_POINT('Ctrl Pts',(-214.569765644412,-4.76405452823405,
129.582490119308));
#128780=CARTESIAN_POINT('Ctrl Pts',(-214.577527446603,-4.79811587282819,
129.715294784928));
#128781=CARTESIAN_POINT('Ctrl Pts',(-214.585289248795,-4.82659044595685,
129.849410052572));
#128782=CARTESIAN_POINT('Ctrl Pts',(-214.593051050987,-4.84940476436363,
129.984326170809));
#128783=CARTESIAN_POINT('Ctrl Pts',(-214.600824711805,-4.87225393891184,
130.11944841641));
#128784=CARTESIAN_POINT('Ctrl Pts',(-214.608598372623,-4.88942553542031,
130.255373569285));
#128785=CARTESIAN_POINT('Ctrl Pts',(-214.616372033441,-4.9008979999614,
130.391587245757));
#128786=CARTESIAN_POINT('Ctrl Pts',(-214.62179012718,-4.9088940895464,130.486525587547));
#128787=CARTESIAN_POINT('Ctrl Pts',(-214.627208220919,-4.91412273629671,
130.581604036906));
#128788=CARTESIAN_POINT('Ctrl Pts',(-214.632626314659,-4.91659159218293,
130.676649309624));
#128789=CARTESIAN_POINT('Ctrl Pts',(-214.635037355104,-4.91769022791769,
130.718944258313));
#128790=CARTESIAN_POINT('Ctrl Pts',(-214.63744839555,-4.91824311324674,
130.761253444763));
#128791=CARTESIAN_POINT('Ctrl Pts',(-214.639859435996,-4.91824993606523,
130.803567588965));
#128792=CARTESIAN_POINT('Ctrl Pts',(-214.639859436029,-4.91824993606532,
130.803567589537));
#128793=CARTESIAN_POINT('Ctrl Pts',(-214.647599714426,-4.91827183966986,
130.939410709401));
#128794=CARTESIAN_POINT('Ctrl Pts',(-214.655339992823,-4.91266145491847,
131.075477757422));
#128795=CARTESIAN_POINT('Ctrl Pts',(-214.66308027122,-4.90138914671146,
131.211260476253));
#128796=CARTESIAN_POINT('Ctrl Pts',(-214.670811061266,-4.89013065656297,
131.346876747048));
#128797=CARTESIAN_POINT('Ctrl Pts',(-214.678541851312,-4.87322408275251,
131.48220899249));
#128798=CARTESIAN_POINT('Ctrl Pts',(-214.686272641357,-4.85069176530766,
131.616747508448));
#128799=CARTESIAN_POINT('Ctrl Pts',(-214.693995846345,-4.82818155542907,
131.751154022042));
#128800=CARTESIAN_POINT('Ctrl Pts',(-214.701719051331,-4.80005664939924,
131.884767968886));
#128801=CARTESIAN_POINT('Ctrl Pts',(-214.709442256318,-4.76639126647814,
132.017083734086));
#128802=CARTESIAN_POINT('Ctrl Pts',(-214.717159772577,-4.73275068067482,
132.14930203865));
#128803=CARTESIAN_POINT('Ctrl Pts',(-214.724877288835,-4.69357783671161,
132.280223683519));
#128804=CARTESIAN_POINT('Ctrl Pts',(-214.732594805094,-4.64899813726028,
132.409352636939));
#128805=CARTESIAN_POINT('Ctrl Pts',(-214.740309268324,-4.60443607341942,
132.538430507288));
#128806=CARTESIAN_POINT('Ctrl Pts',(-214.748023731553,-4.55447153555235,
132.665716723847));
#128807=CARTESIAN_POINT('Ctrl Pts',(-214.755738194783,-4.49927987544658,
132.790730085943));
#128808=CARTESIAN_POINT('Ctrl Pts',(-214.763451245489,-4.44409832097267,
132.915720558004));
#128809=CARTESIAN_POINT('Ctrl Pts',(-214.771164296195,-4.38369170702797,
133.038438642288));
#128810=CARTESIAN_POINT('Ctrl Pts',(-214.778877346901,-4.31828348084661,
133.15842324238));
#128811=CARTESIAN_POINT('Ctrl Pts',(-214.78659069349,-4.25287274551902,
133.278412445241));
#128812=CARTESIAN_POINT('Ctrl Pts',(-214.794304040078,-4.1824602051556,
133.395667608655));
#128813=CARTESIAN_POINT('Ctrl Pts',(-214.802017386667,-4.10731498489418,
133.509752766103));
#128814=CARTESIAN_POINT('Ctrl Pts',(-214.809732737415,-4.03215023965263,
133.623867566293));
#128815=CARTESIAN_POINT('Ctrl Pts',(-214.817448088162,-3.95225058525506,
133.734810392369));
#128816=CARTESIAN_POINT('Ctrl Pts',(-214.82516343891,-3.86792786982101,
133.842175137309));
#128817=CARTESIAN_POINT('Ctrl Pts',(-214.832887060762,-3.78351475771584,
133.949654980719));
#128818=CARTESIAN_POINT('Ctrl Pts',(-214.840610682614,-3.69466935959324,
134.053548772069));
#128819=CARTESIAN_POINT('Ctrl Pts',(-214.848334304467,-3.60174342374308,
134.15348399123));
#128820=CARTESIAN_POINT('Ctrl Pts',(-214.856062366428,-3.50876406718808,
134.25347666055));
#128821=CARTESIAN_POINT('Ctrl Pts',(-214.86379042839,-3.41169978064607,
134.349505947649));
#128822=CARTESIAN_POINT('Ctrl Pts',(-214.871518490352,-3.31093759543724,
134.441237753464));
#128823=CARTESIAN_POINT('Ctrl Pts',(-214.87925836052,-3.21002144915805,
134.533109722249));
#128824=CARTESIAN_POINT('Ctrl Pts',(-214.886998230688,-3.10539642093301,
134.620670841333));
#128825=CARTESIAN_POINT('Ctrl Pts',(-214.894738100857,-2.99748138846424,
134.7036282909));
#128826=CARTESIAN_POINT('Ctrl Pts',(-214.900183380062,-2.92155925160314,
134.761991863571));
#128827=CARTESIAN_POINT('Ctrl Pts',(-214.905628659266,-2.84400932084468,
134.818077683594));
#128828=CARTESIAN_POINT('Ctrl Pts',(-214.911073938471,-2.7649849903439,
134.871797287715));
#128829=CARTESIAN_POINT('Ctrl Pts',(-214.91884827259,-2.65216037185725,
134.948493841824));
#128830=CARTESIAN_POINT('Ctrl Pts',(-214.92662260671,-2.53596345703543,
135.020613940536));
#128831=CARTESIAN_POINT('Ctrl Pts',(-214.934396940829,-2.41680197188725,
135.087846498386));
#128832=CARTESIAN_POINT('Ctrl Pts',(-214.942161693776,-2.29778734261974,
135.154996198116));
#128833=CARTESIAN_POINT('Ctrl Pts',(-214.949926446723,-2.17581574977439,
135.217270151595));
#128834=CARTESIAN_POINT('Ctrl Pts',(-214.95769119967,-2.05132518092044,
135.274399550799));
#128835=CARTESIAN_POINT('Ctrl Pts',(-214.965448240555,-1.92695825785448,
135.331472208279));
#128836=CARTESIAN_POINT('Ctrl Pts',(-214.97320528144,-1.80007769067526,
135.383410317897));
#128837=CARTESIAN_POINT('Ctrl Pts',(-214.980962322325,-1.67114712965089,
135.429990340486));
#128838=CARTESIAN_POINT('Ctrl Pts',(-214.988713513565,-1.54231379616465,
135.476535236717));
#128839=CARTESIAN_POINT('Ctrl Pts',(-214.996464704805,-1.41143391210209,
135.517729956133));
#128840=CARTESIAN_POINT('Ctrl Pts',(-215.004215896046,-1.27899189626959,
135.553398708777));
#128841=CARTESIAN_POINT('Ctrl Pts',(-215.011963792823,-1.14660617182772,
135.58905230125));
#128842=CARTESIAN_POINT('Ctrl Pts',(-215.0197116896,-1.01266001288096,135.619184496847));
#128843=CARTESIAN_POINT('Ctrl Pts',(-215.027459586377,-0.877653610142368,
135.643669163537));
#128844=CARTESIAN_POINT('Ctrl Pts',(-215.035205862461,-0.742675447832825,
135.668148708562));
#128845=CARTESIAN_POINT('Ctrl Pts',(-215.042952138545,-0.606637867310519,
135.686983004709));
#128846=CARTESIAN_POINT('Ctrl Pts',(-215.050698414629,-0.470051490621363,
135.700096993094));
#128847=CARTESIAN_POINT('Ctrl Pts',(-215.058444747895,-0.333464105682415,
135.713211078282));
#128848=CARTESIAN_POINT('Ctrl Pts',(-215.06619108116,-0.196328305668506,
135.720604734083));
#128849=CARTESIAN_POINT('Ctrl Pts',(-215.073937414425,-0.0591596810558063,
135.72225480051));
#128850=CARTESIAN_POINT('Ctrl Pts',(-215.081685482428,0.0780396615191281,
135.723905236458));
#128851=CARTESIAN_POINT('Ctrl Pts',(-215.089433550431,0.215271452458073,
135.719809518868));
#128852=CARTESIAN_POINT('Ctrl Pts',(-215.097181618434,0.352020653319216,
135.709996613249));
#128853=CARTESIAN_POINT('Ctrl Pts',(-215.104937921176,0.488915192858183,
135.700173278356));
#128854=CARTESIAN_POINT('Ctrl Pts',(-215.112694223918,0.625325727157111,
135.684620645409));
#128855=CARTESIAN_POINT('Ctrl Pts',(-215.12045052666,0.760742334114661,
135.663419596791));
#128856=CARTESIAN_POINT('Ctrl Pts',(-215.128210969174,0.896231216993028,
135.642207232535));
#128857=CARTESIAN_POINT('Ctrl Pts',(-215.135971411688,1.03072473228301,
135.615340522055));
#128858=CARTESIAN_POINT('Ctrl Pts',(-215.143731854202,1.16372467363971,
135.582951199156));
#128859=CARTESIAN_POINT('Ctrl Pts',(-215.151504754468,1.29693811830946,
135.550509882041));
#128860=CARTESIAN_POINT('Ctrl Pts',(-215.159277654733,1.4286528219675,135.512528345024));
#128861=CARTESIAN_POINT('Ctrl Pts',(-215.167050554999,1.55838636490553,
135.469188052764));
#128862=CARTESIAN_POINT('Ctrl Pts',(-215.174540890761,1.68340376677833,
135.427423289295));
#128863=CARTESIAN_POINT('Ctrl Pts',(-215.182031226523,1.80658125956134,
135.380682724186));
#128864=CARTESIAN_POINT('Ctrl Pts',(-215.189521562285,1.92750774059563,
135.329169671266));
#128865=CARTESIAN_POINT('Ctrl Pts',(-215.197295896404,2.05301918591367,
135.275703485287));
#128866=CARTESIAN_POINT('Ctrl Pts',(-215.205070230523,2.17650313823665,
135.216926404965));
#128867=CARTESIAN_POINT('Ctrl Pts',(-215.212844564642,2.29747748668428,
135.153013312445));
#128868=CARTESIAN_POINT('Ctrl Pts',(-215.220609317589,2.41830274505891,
135.0891789871));
#128869=CARTESIAN_POINT('Ctrl Pts',(-215.228374070536,2.53662421106492,
135.020221424605));
#128870=CARTESIAN_POINT('Ctrl Pts',(-215.236138823483,2.65197898592121,
134.946363819005));
#128871=CARTESIAN_POINT('Ctrl Pts',(-215.243895864368,2.76721918878921,
134.87257956982));
#128872=CARTESIAN_POINT('Ctrl Pts',(-215.251652905253,2.87949823716522,
134.793905172115));
#128873=CARTESIAN_POINT('Ctrl Pts',(-215.259409946138,2.98837744692175,
134.710609879611));
#128874=CARTESIAN_POINT('Ctrl Pts',(-215.267161137378,3.0971745500188,134.627377400736));
#128875=CARTESIAN_POINT('Ctrl Pts',(-215.274912328618,3.20257660841183,
134.539531199645));
#128876=CARTESIAN_POINT('Ctrl Pts',(-215.282663519859,3.30417388483606,
134.447383812835));
#128877=CARTESIAN_POINT('Ctrl Pts',(-215.290411416636,3.40572797970774,
134.355275591123));
#128878=CARTESIAN_POINT('Ctrl Pts',(-215.298159313413,3.50348021997888,
134.258870081788));
#128879=CARTESIAN_POINT('Ctrl Pts',(-215.30590721019,3.5970541219015,134.158519932001));
#128880=CARTESIAN_POINT('Ctrl Pts',(-215.313653486274,3.69060845018106,
134.058190773302));
#128881=CARTESIAN_POINT('Ctrl Pts',(-215.321399762358,3.77998591212003,
133.953918901145));
#128882=CARTESIAN_POINT('Ctrl Pts',(-215.329146038442,3.86484735486342,
133.846093345158));
#128883=CARTESIAN_POINT('Ctrl Pts',(-215.336892371707,3.94970942403482,
133.738266993227));
#128884=CARTESIAN_POINT('Ctrl Pts',(-215.344638704973,4.03005516569492,
133.626887212348));
#128885=CARTESIAN_POINT('Ctrl Pts',(-215.352385038238,4.10558640544539,
133.512375264853));
#128886=CARTESIAN_POINT('Ctrl Pts',(-215.360133106241,4.18113455989361,
133.397837673201));
#128887=CARTESIAN_POINT('Ctrl Pts',(-215.367881174244,4.25186585176375,
133.280166845476));
#128888=CARTESIAN_POINT('Ctrl Pts',(-215.375629242247,4.31752625970104,
133.159811754672));
#128889=CARTESIAN_POINT('Ctrl Pts',(-215.383385544989,4.38325645230099,
133.039328749045));
#128890=CARTESIAN_POINT('Ctrl Pts',(-215.391141847731,4.44390480752966,
132.916156125189));
#128891=CARTESIAN_POINT('Ctrl Pts',(-215.398898150473,4.49926374867785,
132.790766613916));
#128892=CARTESIAN_POINT('Ctrl Pts',(-215.406658592987,4.55465223655975,
132.665310178484));
#128893=CARTESIAN_POINT('Ctrl Pts',(-215.414419035501,4.60474554232912,
132.537634861746));
#128894=CARTESIAN_POINT('Ctrl Pts',(-215.422179478015,4.64938520466827,
132.408231024149));
#128895=CARTESIAN_POINT('Ctrl Pts',(-215.42995237828,4.69409652655633,132.278619456023));
#128896=CARTESIAN_POINT('Ctrl Pts',(-215.437725278546,4.73333659840917,
132.147274196973));
#128897=CARTESIAN_POINT('Ctrl Pts',(-215.445498178811,4.76699733194558,
132.014699206443));
#128898=CARTESIAN_POINT('Ctrl Pts',(-215.452988514573,4.7994344130314,131.886943650755));
#128899=CARTESIAN_POINT('Ctrl Pts',(-215.460478850335,4.82669069547001,
131.758046520366));
#128900=CARTESIAN_POINT('Ctrl Pts',(-215.467969186097,4.84871502191527,
131.628463583677));
#128901=CARTESIAN_POINT('Ctrl Pts',(-215.475743520216,4.87157440739208,
131.493967470556));
#128902=CARTESIAN_POINT('Ctrl Pts',(-215.483517854335,4.88886967755753,
131.358306476596));
#128903=CARTESIAN_POINT('Ctrl Pts',(-215.491292188454,4.90048737300637,
131.221980743404));
#128904=CARTESIAN_POINT('Ctrl Pts',(-215.499056941401,4.91209075068382,
131.085823019496));
#128905=CARTESIAN_POINT('Ctrl Pts',(-215.506821694349,4.91803044291591,
130.949002572196));
#128906=CARTESIAN_POINT('Ctrl Pts',(-215.514586447296,4.91824402107567,
130.812029493194));
#128907=CARTESIAN_POINT('Ctrl Pts',(-215.522343488181,4.9184573871066,130.675192457785));
#128908=CARTESIAN_POINT('Ctrl Pts',(-215.530100529066,4.912955956358,130.53820348079));
#128909=CARTESIAN_POINT('Ctrl Pts',(-215.537857569951,4.90172914012527,
130.401577177804));
#128910=CARTESIAN_POINT('Ctrl Pts',(-215.545608761191,4.89051079012195,
130.265053905775));
#128911=CARTESIAN_POINT('Ctrl Pts',(-215.553359952431,4.87357568036007,
130.128893151454));
#128912=CARTESIAN_POINT('Ctrl Pts',(-215.561111143671,4.85096528364601,
129.993608572017));
#128913=CARTESIAN_POINT('Ctrl Pts',(-215.568859040448,4.8283644969538,129.858381492137));
#128914=CARTESIAN_POINT('Ctrl Pts',(-215.576606937225,4.80009328520259,
129.724030231278));
#128915=CARTESIAN_POINT('Ctrl Pts',(-215.584354834002,4.76624484178161,
129.591062150292));
#128916=CARTESIAN_POINT('Ctrl Pts',(-215.592101110086,4.73240347872531,
129.458121883361));
#128917=CARTESIAN_POINT('Ctrl Pts',(-215.599847386171,4.69298730089078,
129.326564599448));
#128918=CARTESIAN_POINT('Ctrl Pts',(-215.607593662255,4.64814028951919,
129.19688591747));
#128919=CARTESIAN_POINT('Ctrl Pts',(-215.61533999552,4.6032929470971,129.067206278234));
#128920=CARTESIAN_POINT('Ctrl Pts',(-215.623086328785,4.55301481892545,
128.939405638098));
#128921=CARTESIAN_POINT('Ctrl Pts',(-215.630832662051,4.49749915438921,
128.813962562209));
#128922=CARTESIAN_POINT('Ctrl Pts',(-215.638580730054,4.44197105750459,
128.688491394213));
#128923=CARTESIAN_POINT('Ctrl Pts',(-215.646328798057,4.38120324849224,
128.565379198493));
#128924=CARTESIAN_POINT('Ctrl Pts',(-215.65407686606,4.31543615629982,128.44508237128));
#128925=CARTESIAN_POINT('Ctrl Pts',(-215.661833168802,4.24959916605946,
128.324657691167));
#128926=CARTESIAN_POINT('Ctrl Pts',(-215.669589471544,4.17875246659923,
128.20705470041));
#128927=CARTESIAN_POINT('Ctrl Pts',(-215.677345774285,4.10318157945714,
128.092703561723));
#128928=CARTESIAN_POINT('Ctrl Pts',(-215.6851062168,4.02757035785719,127.97829139039));
#128929=CARTESIAN_POINT('Ctrl Pts',(-215.692866659314,3.94723015329797,
127.86713484619));
#128930=CARTESIAN_POINT('Ctrl Pts',(-215.700627101828,3.86248786769865,
127.759632298917));
#128931=CARTESIAN_POINT('Ctrl Pts',(-215.708400002093,3.77760954625942,
127.651957179012));
#128932=CARTESIAN_POINT('Ctrl Pts',(-215.716172902359,3.68831527725839,
127.547948074423));
#128933=CARTESIAN_POINT('Ctrl Pts',(-215.723945802624,3.59497063169151,
127.447968325271));
#128934=CARTESIAN_POINT('Ctrl Pts',(-215.731436138386,3.50501929911271,
127.351623091836));
#128935=CARTESIAN_POINT('Ctrl Pts',(-215.738926474148,3.41130717918996,
127.25901956202));
#128936=CARTESIAN_POINT('Ctrl Pts',(-215.74641680991,3.31419007099185,127.1704471299));
#128937=CARTESIAN_POINT('Ctrl Pts',(-215.754191144029,3.21339073811732,
127.078516447095));
#128938=CARTESIAN_POINT('Ctrl Pts',(-215.761965478148,3.10860381776411,
126.990637365538));
#128939=CARTESIAN_POINT('Ctrl Pts',(-215.769739812267,3.00018876565265,
126.907175680595));
#128940=CARTESIAN_POINT('Ctrl Pts',(-215.777504565214,2.89190732540418,
126.823816854721));
#128941=CARTESIAN_POINT('Ctrl Pts',(-215.785269318162,2.78000695687148,
126.744864829635));
#128942=CARTESIAN_POINT('Ctrl Pts',(-215.793034071109,2.66488307044007,
126.670647845326));
#128943=CARTESIAN_POINT('Ctrl Pts',(-215.800791111994,2.54987352667468,
126.596504574371));
#128944=CARTESIAN_POINT('Ctrl Pts',(-215.808548152879,2.43164716289924,
126.527087195661));
#128945=CARTESIAN_POINT('Ctrl Pts',(-215.816305193764,2.31063121633424,
126.46268278007));
#128946=CARTESIAN_POINT('Ctrl Pts',(-215.824056385004,2.18970652883707,
126.398326932351));
#128947=CARTESIAN_POINT('Ctrl Pts',(-215.831807576244,2.06599678946577,
126.3389767062));
#128948=CARTESIAN_POINT('Ctrl Pts',(-215.839558767484,1.93995656961486,
126.28487485362));
#128949=CARTESIAN_POINT('Ctrl Pts',(-215.847306664261,1.81396992021911,
126.230795995771));
#128950=CARTESIAN_POINT('Ctrl Pts',(-215.855054561038,1.68565511891946,
126.181961228694));
#128951=CARTESIAN_POINT('Ctrl Pts',(-215.862802457815,1.55548939607039,
126.138566387083));
#128952=CARTESIAN_POINT('Ctrl Pts',(-215.870548733899,1.4253509010845,126.095180622736));
#128953=CARTESIAN_POINT('Ctrl Pts',(-215.878295009983,1.29336262531912,
126.057232644052));
#128954=CARTESIAN_POINT('Ctrl Pts',(-215.886041286067,1.16001937238477,
126.024869209666));
#128955=CARTESIAN_POINT('Ctrl Pts',(-215.893787619333,1.026675135141,125.99250553638));
#128956=CARTESIAN_POINT('Ctrl Pts',(-215.901533952598,0.89197628070464,
125.965726581864));
#128957=CARTESIAN_POINT('Ctrl Pts',(-215.909280285863,0.756429895499917,
125.944628436088));
#128958=CARTESIAN_POINT('Ctrl Pts',(-215.917028353866,0.620853155622594,
125.923525565529));
#128959=CARTESIAN_POINT('Ctrl Pts',(-215.924776421869,0.484428893539116,
125.908106095316));
#128960=CARTESIAN_POINT('Ctrl Pts',(-215.932524489872,0.347671046042293,
125.898414439076));
#128961=CARTESIAN_POINT('Ctrl Pts',(-215.940280792614,0.210767850677151,
125.888712482428));
#128962=CARTESIAN_POINT('Ctrl Pts',(-215.948037095356,0.0735307522787072,
125.88475052805));
#128963=CARTESIAN_POINT('Ctrl Pts',(-215.955793398098,-0.0635240097127495,
125.886520872039));
#128964=CARTESIAN_POINT('Ctrl Pts',(-215.963553840612,-0.200651921957693,
125.888292160913));
#128965=CARTESIAN_POINT('Ctrl Pts',(-215.971314283126,-0.337596913692748,
125.895801823072));
#128966=CARTESIAN_POINT('Ctrl Pts',(-215.97907472564,-0.473847126655544,
125.908990155276));
#128967=CARTESIAN_POINT('Ctrl Pts',(-215.986847625906,-0.610316060555913,
125.922199658562));
#128968=CARTESIAN_POINT('Ctrl Pts',(-215.994620526171,-0.746087599466408,
125.941105994423));
#128969=CARTESIAN_POINT('Ctrl Pts',(-216.002393426437,-0.880658455000069,
125.965597991839));
#128970=CARTESIAN_POINT('Ctrl Pts',(-216.009883762199,-1.01033732097301,
125.989199643456));
#128971=CARTESIAN_POINT('Ctrl Pts',(-216.017374097961,-1.13890098314221,
126.01798783418));
#128972=CARTESIAN_POINT('Ctrl Pts',(-216.024864433723,-1.26591364798658,
126.051819644745));
#128973=CARTESIAN_POINT('Ctrl Pts',(-216.032638767842,-1.39774203662189,
126.08693419869));
#128974=CARTESIAN_POINT('Ctrl Pts',(-216.040413101961,-1.52831708681475,
126.127593612355));
#128975=CARTESIAN_POINT('Ctrl Pts',(-216.04818743608,-1.65713674996577,
126.173693186794));
#128976=CARTESIAN_POINT('Ctrl Pts',(-216.055952189027,-1.78579765439419,
126.219735947627));
#128977=CARTESIAN_POINT('Ctrl Pts',(-216.063716941974,-1.91270711164699,
126.271205398787));
#128978=CARTESIAN_POINT('Ctrl Pts',(-216.071481694922,-2.03737523515358,
126.32794629205));
#128979=CARTESIAN_POINT('Ctrl Pts',(-216.079238735807,-2.16191953652273,
126.384630829458));
#128980=CARTESIAN_POINT('Ctrl Pts',(-216.086995776692,-2.28422658069359,
126.44657622884));
#128981=CARTESIAN_POINT('Ctrl Pts',(-216.094752817577,-2.40382391465449,
126.513578212242));
#128982=CARTESIAN_POINT('Ctrl Pts',(-216.102504008817,-2.52333105933633,
126.580529668928));
#128983=CARTESIAN_POINT('Ctrl Pts',(-216.110255200057,-2.64013222139294,
126.652529929359));
#128984=CARTESIAN_POINT('Ctrl Pts',(-216.118006391297,-2.75377745974615,
126.729327763135));
#128985=CARTESIAN_POINT('Ctrl Pts',(-216.125754288074,-2.86737439584101,
126.806092955782));
#128986=CARTESIAN_POINT('Ctrl Pts',(-216.133502184851,-2.97781775282151,
126.887651447719));
#128987=CARTESIAN_POINT('Ctrl Pts',(-216.141250081628,-3.08468481474969,
126.973707584968));
#128988=CARTESIAN_POINT('Ctrl Pts',(-216.148996357712,-3.1915295223923,
127.059745721128));
#128989=CARTESIAN_POINT('Ctrl Pts',(-216.156742633797,-3.29479911864613,
127.150279386222));
#128990=CARTESIAN_POINT('Ctrl Pts',(-216.164488909881,-3.39410267787684,
127.244971614587));
#128991=CARTESIAN_POINT('Ctrl Pts',(-216.172235243146,-3.49340697014373,
127.339664541948));
#128992=CARTESIAN_POINT('Ctrl Pts',(-216.179981576411,-3.588744884023,127.438515824027));
#128993=CARTESIAN_POINT('Ctrl Pts',(-216.187727909677,-3.67976148370246,
127.54115077363));
#128994=CARTESIAN_POINT('Ctrl Pts',(-216.19547597768,-3.77079846591823,
127.643808707619));
#128995=CARTESIAN_POINT('Ctrl Pts',(-216.203224045683,-3.85751194891496,
127.750251702754));
#128996=CARTESIAN_POINT('Ctrl Pts',(-216.210972113686,-3.93958677086006,
127.860071376108));
#128997=CARTESIAN_POINT('Ctrl Pts',(-216.218728416428,-4.02174882290297,
127.970007767118));
#128998=CARTESIAN_POINT('Ctrl Pts',(-216.226484719169,-4.09926213121704,
128.08332769164));
#128999=CARTESIAN_POINT('Ctrl Pts',(-216.234241021911,-4.17185413728566,
128.199592658666));
#129000=CARTESIAN_POINT('Ctrl Pts',(-216.242001464426,-4.24448488789342,
128.315919679805));
#129001=CARTESIAN_POINT('Ctrl Pts',(-216.24976190694,-4.31218890953456,
128.435194535666));
#129002=CARTESIAN_POINT('Ctrl Pts',(-216.257522349454,-4.37473976034095,
128.556954314337));
#129003=CARTESIAN_POINT('Ctrl Pts',(-216.265295249719,-4.43739102332606,
128.678909552615));
#129004=CARTESIAN_POINT('Ctrl Pts',(-216.273068149985,-4.49487242069567,
128.803357329896));
#129005=CARTESIAN_POINT('Ctrl Pts',(-216.28084105025,-4.54700544411243,
128.929814124755));
#129006=CARTESIAN_POINT('Ctrl Pts',(-216.288331386012,-4.59724330081212,
129.051673896593));
#129007=CARTESIAN_POINT('Ctrl Pts',(-216.295821721774,-4.64251478037536,
129.175398866962));
#129008=CARTESIAN_POINT('Ctrl Pts',(-216.303312057536,-4.68270456778482,
129.300545139076));
#129009=CARTESIAN_POINT('Ctrl Pts',(-216.308884508859,-4.71260384615303,
129.393647976086));
#129010=CARTESIAN_POINT('Ctrl Pts',(-216.314456960182,-4.73973772792483,
129.487679283962));
#129011=CARTESIAN_POINT('Ctrl Pts',(-216.320029411505,-4.76405452823406,
129.582490119308));
#129012=CARTESIAN_POINT('Origin',(213.235140564004,0.,130.804360617566));
#129013=CARTESIAN_POINT('',(-218.414998772423,-4.76405452823415,129.582490119309));
#129014=CARTESIAN_POINT('',(-218.070061802556,-4.76405452823401,129.582490119308));
#129015=CARTESIAN_POINT('',(213.235140564004,-4.76405452823405,129.582490119308));
#129016=CARTESIAN_POINT('',(-216.735140564067,-4.91824906570699,130.807392147263));
#129017=CARTESIAN_POINT('Ctrl Pts',(-216.735140564067,-4.91824906570699,
130.807392147263));
#129018=CARTESIAN_POINT('Ctrl Pts',(-216.743930376145,-4.91815299469981,
130.963254430834));
#129019=CARTESIAN_POINT('Ctrl Pts',(-216.752720188223,-4.91064364192366,
131.11883983252));
#129020=CARTESIAN_POINT('Ctrl Pts',(-216.761510000301,-4.89582518385855,
131.273486220786));
#129021=CARTESIAN_POINT('Ctrl Pts',(-216.770240213936,-4.88110720086741,
131.427084044672));
#129022=CARTESIAN_POINT('Ctrl Pts',(-216.778970427572,-4.85917909410244,
131.579755377644));
#129023=CARTESIAN_POINT('Ctrl Pts',(-216.787700641208,-4.8301931353919,
131.730868759631));
#129024=CARTESIAN_POINT('Ctrl Pts',(-216.796520252507,-4.80091035954813,
131.883529547426));
#129025=CARTESIAN_POINT('Ctrl Pts',(-216.805339863806,-4.76442450715711,
132.034600100351));
#129026=CARTESIAN_POINT('Ctrl Pts',(-216.814159475105,-4.72094222459015,
132.18345001807));
#129027=CARTESIAN_POINT('Ctrl Pts',(-216.822979086404,-4.67745994202318,
132.332299935789));
#129028=CARTESIAN_POINT('Ctrl Pts',(-216.831798697704,-4.62698137325245,
132.478929048469));
#129029=CARTESIAN_POINT('Ctrl Pts',(-216.840618309003,-4.56976089153752,
132.622730342532));
#129030=CARTESIAN_POINT('Ctrl Pts',(-216.848392643122,-4.51932203111415,
132.749488684696));
#129031=CARTESIAN_POINT('Ctrl Pts',(-216.856166977241,-4.46352515151253,
132.874347564552));
#129032=CARTESIAN_POINT('Ctrl Pts',(-216.86394131136,-4.40253351518442,
132.996820813368));
#129033=CARTESIAN_POINT('Ctrl Pts',(-216.871706064307,-4.3416170455971,
133.119143124851));
#129034=CARTESIAN_POINT('Ctrl Pts',(-216.879470817254,-4.27551873011275,
133.239085308561));
#129035=CARTESIAN_POINT('Ctrl Pts',(-216.887235570201,-4.20445059020745,
133.356179242979));
#129036=CARTESIAN_POINT('Ctrl Pts',(-216.894992611086,-4.13345303618059,
133.47315687805));
#129037=CARTESIAN_POINT('Ctrl Pts',(-216.902749651971,-4.05749568233232,
133.58729156145));
#129038=CARTESIAN_POINT('Ctrl Pts',(-216.910506692856,-3.97683717763647,
133.698138274033));
#129039=CARTESIAN_POINT('Ctrl Pts',(-216.918257884096,-3.89623949814654,
133.808901396248));
#129040=CARTESIAN_POINT('Ctrl Pts',(-216.926009075336,-3.81094795336731,
133.91638116806));
#129041=CARTESIAN_POINT('Ctrl Pts',(-216.933760266576,-3.72126515722831,
134.020160470184));
#129042=CARTESIAN_POINT('Ctrl Pts',(-216.941508163353,-3.63162047866992,
134.123895663336));
#129043=CARTESIAN_POINT('Ctrl Pts',(-216.949256060131,-3.53758851597458,
134.223933219782));
#129044=CARTESIAN_POINT('Ctrl Pts',(-216.957003956908,-3.43951278018621,
134.319888301632));
#129045=CARTESIAN_POINT('Ctrl Pts',(-216.964750232992,-3.3414575597275,
134.415823311748));
#129046=CARTESIAN_POINT('Ctrl Pts',(-216.972496509076,-3.23936052793977,
134.507677272608));
#129047=CARTESIAN_POINT('Ctrl Pts',(-216.98024278516,-3.13360246368624,
134.595101793389));
#129048=CARTESIAN_POINT('Ctrl Pts',(-216.987989118425,-3.02784361875057,
134.682526959518));
#129049=CARTESIAN_POINT('Ctrl Pts',(-216.99573545169,-2.91842398875929,
134.765522371223));
#129050=CARTESIAN_POINT('Ctrl Pts',(-217.003481784956,-2.80575755936771,
134.843779830838));
#129051=CARTESIAN_POINT('Ctrl Pts',(-217.011229852959,-2.69306589911059,
134.922054815669));
#129052=CARTESIAN_POINT('Ctrl Pts',(-217.018977920962,-2.57712631365499,
134.995589514085));
#129053=CARTESIAN_POINT('Ctrl Pts',(-217.026725988965,-2.45838155088886,
135.064119203771));
#129054=CARTESIAN_POINT('Ctrl Pts',(-217.034482291707,-2.33951058477595,
135.132721727627));
#129055=CARTESIAN_POINT('Ctrl Pts',(-217.042238594448,-2.217828824893,135.196308420976));
#129056=CARTESIAN_POINT('Ctrl Pts',(-217.04999489719,-2.09380388464748,
135.25466042265));
#129057=CARTESIAN_POINT('Ctrl Pts',(-217.057755339704,-1.9697127485567,
135.313043568546));
#129058=CARTESIAN_POINT('Ctrl Pts',(-217.065515782218,-1.84327630037177,
135.366186304243));
#129059=CARTESIAN_POINT('Ctrl Pts',(-217.073276224733,-1.71498095669357,
135.413918446759));
#129060=CARTESIAN_POINT('Ctrl Pts',(-217.081049124998,-1.58647966194018,
135.461727213148));
#129061=CARTESIAN_POINT('Ctrl Pts',(-217.088822025264,-1.45611388060796,
135.504107908889));
#129062=CARTESIAN_POINT('Ctrl Pts',(-217.096594925529,-1.32438483319117,
135.540940383189));
#129063=CARTESIAN_POINT('Ctrl Pts',(-217.104085261291,-1.1974444684527,
135.576433904274));
#129064=CARTESIAN_POINT('Ctrl Pts',(-217.111575597053,-1.06923853287591,
135.606775513298));
#129065=CARTESIAN_POINT('Ctrl Pts',(-217.119065932815,-0.940221435976484,
135.631903130463));
#129066=CARTESIAN_POINT('Ctrl Pts',(-217.126840266934,-0.806312616635522,
135.65798346887));
#129067=CARTESIAN_POINT('Ctrl Pts',(-217.134614601053,-0.671105728485961,
135.678529248222));
#129068=CARTESIAN_POINT('Ctrl Pts',(-217.142388935172,-0.535098046395437,
135.693415039767));
#129069=CARTESIAN_POINT('Ctrl Pts',(-217.150153688119,-0.399257981617734,
135.708282485904));
#129070=CARTESIAN_POINT('Ctrl Pts',(-217.157918441066,-0.262619471463193,
135.717503781132));
#129071=CARTESIAN_POINT('Ctrl Pts',(-217.165683194014,-0.125690962610648,
135.721004274007));
#129072=CARTESIAN_POINT('Ctrl Pts',(-217.173440234899,0.0111015469165498,
135.724501290142));
#129073=CARTESIAN_POINT('Ctrl Pts',(-217.181197275784,0.14818309363905,
135.722288801398));
#129074=CARTESIAN_POINT('Ctrl Pts',(-217.188954316669,0.285039464259041,
135.714343872763));
#129075=CARTESIAN_POINT('Ctrl Pts',(-217.196705507909,0.421792630425546,
135.70640493546));
#129076=CARTESIAN_POINT('Ctrl Pts',(-217.204456699149,0.5583205697514,135.692742185259));
#129077=CARTESIAN_POINT('Ctrl Pts',(-217.212207890389,0.694108777748216,
135.673384756667));
#129078=CARTESIAN_POINT('Ctrl Pts',(-217.219955787166,0.829839272134179,
135.654035555499));
#129079=CARTESIAN_POINT('Ctrl Pts',(-217.227703683943,0.964830274277994,
135.628996544972));
#129080=CARTESIAN_POINT('Ctrl Pts',(-217.23545158072,1.09857233305397,135.598348716378));
#129081=CARTESIAN_POINT('Ctrl Pts',(-217.243197856804,1.23228641587475,
135.567707298648));
#129082=CARTESIAN_POINT('Ctrl Pts',(-217.250944132888,1.36475169412645,
135.53145948377));
#129083=CARTESIAN_POINT('Ctrl Pts',(-217.258690408972,1.49546923646382,
135.489737318034));
#129084=CARTESIAN_POINT('Ctrl Pts',(-217.266436742238,1.62618774372821,
135.448014844315));
#129085=CARTESIAN_POINT('Ctrl Pts',(-217.274183075503,1.75515811688103,
135.400818057981));
#129086=CARTESIAN_POINT('Ctrl Pts',(-217.281929408768,1.88189729113848,
135.348328668522));
#129087=CARTESIAN_POINT('Ctrl Pts',(-217.289677476771,2.00866484775509,
135.295827524428));
#129088=CARTESIAN_POINT('Ctrl Pts',(-217.297425544774,2.13319985006438,
135.238031568284));
#129089=CARTESIAN_POINT('Ctrl Pts',(-217.305173612777,2.25504026363577,
135.175170207548));
#129090=CARTESIAN_POINT('Ctrl Pts',(-217.312929915519,2.37701017064879,
135.112242037011));
#129091=CARTESIAN_POINT('Ctrl Pts',(-217.320686218261,2.49627942009138,
135.044237887161));
#129092=CARTESIAN_POINT('Ctrl Pts',(-217.328442521003,2.6124111213954,134.971432874596));
#129093=CARTESIAN_POINT('Ctrl Pts',(-217.336202963517,2.72860480568506,
134.898589003804));
#129094=CARTESIAN_POINT('Ctrl Pts',(-217.343963406031,2.84165728293365,
134.820939385808));
#129095=CARTESIAN_POINT('Ctrl Pts',(-217.351723848545,2.95116245332322,
134.738801268611));
#129096=CARTESIAN_POINT('Ctrl Pts',(-217.359496748811,3.06084341113371,
134.656531296017));
#129097=CARTESIAN_POINT('Ctrl Pts',(-217.367269649076,3.16696537991514,
134.569758673285));
#129098=CARTESIAN_POINT('Ctrl Pts',(-217.375042549341,3.26915635148366,
134.478840146976));
#129099=CARTESIAN_POINT('Ctrl Pts',(-217.382532885104,3.36763242383518,
134.391226738105));
#129100=CARTESIAN_POINT('Ctrl Pts',(-217.390023220866,3.46245811861199,
134.299763834334));
#129101=CARTESIAN_POINT('Ctrl Pts',(-217.397513556628,3.55333558687814,
134.204800187611));
#129102=CARTESIAN_POINT('Ctrl Pts',(-217.405287890747,3.64765870197242,
134.106235965361));
#129103=CARTESIAN_POINT('Ctrl Pts',(-217.413062224866,3.73802707368471,
134.0035880767));
#129104=CARTESIAN_POINT('Ctrl Pts',(-217.420836558985,3.82406638604163,
133.897207095755));
#129105=CARTESIAN_POINT('Ctrl Pts',(-217.428601311932,3.90999966263562,
133.790957219861));
#129106=CARTESIAN_POINT('Ctrl Pts',(-217.436366064879,3.99161425179114,
133.680983706778));
#129107=CARTESIAN_POINT('Ctrl Pts',(-217.444130817827,4.06857251928545,
133.567673976166));
#129108=CARTESIAN_POINT('Ctrl Pts',(-217.451887858712,4.14545435074356,
133.454476786376));
#129109=CARTESIAN_POINT('Ctrl Pts',(-217.459644899597,4.21768884570861,
133.337950294557));
#129110=CARTESIAN_POINT('Ctrl Pts',(-217.467401940482,4.28497876345877,
133.218514725987));
#129111=CARTESIAN_POINT('Ctrl Pts',(-217.475153131722,4.35221793735861,
133.099169224709));
#129112=CARTESIAN_POINT('Ctrl Pts',(-217.482904322962,4.41451976475138,
132.976919352466));
#129113=CARTESIAN_POINT('Ctrl Pts',(-217.490655514202,4.47163065507978,
132.852213724371));
#129114=CARTESIAN_POINT('Ctrl Pts',(-217.498403410979,4.52871727175639,
132.727561099494));
#129115=CARTESIAN_POINT('Ctrl Pts',(-217.506151307756,4.58061717705603,
132.600455149444));
#129116=CARTESIAN_POINT('Ctrl Pts',(-217.513899204533,4.62712314046767,
132.471368267653));
#129117=CARTESIAN_POINT('Ctrl Pts',(-217.521645480617,4.67361937583419,
132.342308388055));
#129118=CARTESIAN_POINT('Ctrl Pts',(-217.529391756702,4.71472378112498,
132.211268768507));
#129119=CARTESIAN_POINT('Ctrl Pts',(-217.537138032786,4.75027776604493,
132.078740548324));
#129120=CARTESIAN_POINT('Ctrl Pts',(-217.544884366051,4.78583201341638,
131.946211349848));
#129121=CARTESIAN_POINT('Ctrl Pts',(-217.552630699316,4.81583565735647,
131.812193906424));
#129122=CARTESIAN_POINT('Ctrl Pts',(-217.560377032582,4.84018046689022,
131.677192852554));
#129123=CARTESIAN_POINT('Ctrl Pts',(-217.568125100585,4.86453072827524,
131.542161566134));
#129124=CARTESIAN_POINT('Ctrl Pts',(-217.575873168588,4.8832195641892,131.406146615636));
#129125=CARTESIAN_POINT('Ctrl Pts',(-217.583621236591,4.89619024072895,
131.269660724046));
#129126=CARTESIAN_POINT('Ctrl Pts',(-217.591377539332,4.9091747026581,131.133029773627));
#129127=CARTESIAN_POINT('Ctrl Pts',(-217.599133842074,4.91642882804909,
130.995927272103));
#129128=CARTESIAN_POINT('Ctrl Pts',(-217.606890144816,4.91794793026193,
130.858869495122));
#129129=CARTESIAN_POINT('Ctrl Pts',(-217.61465058733,4.91946784326536,130.721738566278));
#129130=CARTESIAN_POINT('Ctrl Pts',(-217.622411029845,4.91524664590671,
130.584652800132));
#129131=CARTESIAN_POINT('Ctrl Pts',(-217.630171472359,4.9053317410446,130.448125340256));
#129132=CARTESIAN_POINT('Ctrl Pts',(-217.637944372624,4.895400919897,130.31137871438));
#129133=CARTESIAN_POINT('Ctrl Pts',(-217.64571727289,4.87975817116386,130.175192574388));
#129134=CARTESIAN_POINT('Ctrl Pts',(-217.653490173155,4.85850255631906,
130.04007273153));
#129135=CARTESIAN_POINT('Ctrl Pts',(-217.660980508917,4.83801963661359,
129.909864835307));
#129136=CARTESIAN_POINT('Ctrl Pts',(-217.668470844679,4.81232490958092,
129.780647359098));
#129137=CARTESIAN_POINT('Ctrl Pts',(-217.675961180441,4.7815507954863,129.652859400596));
#129138=CARTESIAN_POINT('Ctrl Pts',(-217.68373551456,4.74960987150215,129.520226322806));
#129139=CARTESIAN_POINT('Ctrl Pts',(-217.691509848679,4.71209560791352,
129.388713161184));
#129140=CARTESIAN_POINT('Ctrl Pts',(-217.699284182798,4.66910062573446,
129.258824332238));
#129141=CARTESIAN_POINT('Ctrl Pts',(-217.707048935745,4.62615863102837,
129.129095579664));
#129142=CARTESIAN_POINT('Ctrl Pts',(-217.714813688693,4.57774947884485,
129.000987544288));
#129143=CARTESIAN_POINT('Ctrl Pts',(-217.72257844164,4.52401661677361,128.874993697134));
#129144=CARTESIAN_POINT('Ctrl Pts',(-217.730335482525,4.47033712293848,
128.749124988845));
#129145=CARTESIAN_POINT('Ctrl Pts',(-217.73809252341,4.41134459412404,128.625366647298));
#129146=CARTESIAN_POINT('Ctrl Pts',(-217.745849564295,4.34723191188681,
128.504195891558));
#129147=CARTESIAN_POINT('Ctrl Pts',(-217.753600755535,4.28316757752189,
128.383116511626));
#129148=CARTESIAN_POINT('Ctrl Pts',(-217.761351946775,4.21399095722072,
128.264621177695));
#129149=CARTESIAN_POINT('Ctrl Pts',(-217.769103138015,4.13994241169063,
128.149165730108));
#129150=CARTESIAN_POINT('Ctrl Pts',(-217.776851034792,4.06592533876761,
128.033759354165));
#129151=CARTESIAN_POINT('Ctrl Pts',(-217.784598931569,3.98704066970332,
127.921390623217));
#129152=CARTESIAN_POINT('Ctrl Pts',(-217.792346828346,3.90357382931725,
127.812489226351));
#129153=CARTESIAN_POINT('Ctrl Pts',(-217.80009310443,3.82012444839508,127.70361060931));
#129154=CARTESIAN_POINT('Ctrl Pts',(-217.807839380515,3.7320950403246,127.598198193815));
#129155=CARTESIAN_POINT('Ctrl Pts',(-217.815585656599,3.63981309259449,
127.49665087917));
#129156=CARTESIAN_POINT('Ctrl Pts',(-217.823331989864,3.54753046365987,
127.395102814926));
#129157=CARTESIAN_POINT('Ctrl Pts',(-217.831078323129,3.45099549536551,
127.297420197803));
#129158=CARTESIAN_POINT('Ctrl Pts',(-217.838824656395,3.35057424952384,
127.203966852861));
#129159=CARTESIAN_POINT('Ctrl Pts',(-217.846572724398,3.25013051504058,
127.11049257969));
#129160=CARTESIAN_POINT('Ctrl Pts',(-217.854320792401,3.14579905735444,
127.021249729646));
#129161=CARTESIAN_POINT('Ctrl Pts',(-217.862068860403,3.03798057877508,
126.936563173867));
#129162=CARTESIAN_POINT('Ctrl Pts',(-217.869825163145,2.93004750943348,
126.851786612209));
#129163=CARTESIAN_POINT('Ctrl Pts',(-217.877581465887,2.81862032392208,
126.771576260081));
#129164=CARTESIAN_POINT('Ctrl Pts',(-217.885337768629,2.70413084632223,
126.696215120086));
#129165=CARTESIAN_POINT('Ctrl Pts',(-217.893098211143,2.58958026224098,
126.620813757581));
#129166=CARTESIAN_POINT('Ctrl Pts',(-217.900858653657,2.47196446443058,
126.550266965361));
#129167=CARTESIAN_POINT('Ctrl Pts',(-217.908619096172,2.35174079751491,
126.484812228694));
#129168=CARTESIAN_POINT('Ctrl Pts',(-217.916391996437,2.23132413689615,
126.419252418274));
#129169=CARTESIAN_POINT('Ctrl Pts',(-217.924164896703,2.10829159254333,
126.358801170611));
#129170=CARTESIAN_POINT('Ctrl Pts',(-217.931937796968,1.98312226293299,
126.30364854582));
#129171=CARTESIAN_POINT('Ctrl Pts',(-217.93942813273,1.86250315373684,126.250500857861));
#129172=CARTESIAN_POINT('Ctrl Pts',(-217.946918468492,1.73990020378354,
126.202273357223));
#129173=CARTESIAN_POINT('Ctrl Pts',(-217.954408804254,1.61575441478483,
126.159091978014));
#129174=CARTESIAN_POINT('Ctrl Pts',(-217.962183138373,1.48690160046274,
126.114273363688));
#129175=CARTESIAN_POINT('Ctrl Pts',(-217.969957472492,1.35597847713742,
126.07474909986));
#129176=CARTESIAN_POINT('Ctrl Pts',(-217.977731806611,1.22345948862323,
126.040713911292));
#129177=CARTESIAN_POINT('Ctrl Pts',(-217.985496559558,1.09110381791882,
126.006720668052));
#129178=CARTESIAN_POINT('Ctrl Pts',(-217.993261312505,0.957156570334292,
125.978203136469));
#129179=CARTESIAN_POINT('Ctrl Pts',(-218.001026065452,0.822110453944658,
125.955307363165));
#129180=CARTESIAN_POINT('Ctrl Pts',(-218.008783106337,0.687198467261639,
125.932434330267));
#129181=CARTESIAN_POINT('Ctrl Pts',(-218.016540147222,0.551190166702867,
125.915172008942));
#129182=CARTESIAN_POINT('Ctrl Pts',(-218.024297188107,0.414591307375536,
125.903616071035));
#129183=CARTESIAN_POINT('Ctrl Pts',(-218.032048379347,0.278095458310422,
125.892068847552));
#129184=CARTESIAN_POINT('Ctrl Pts',(-218.039799570588,0.141010324906225,
125.886219474996));
#129185=CARTESIAN_POINT('Ctrl Pts',(-218.047550761828,0.00384933938717165,
125.886112123937));
#129186=CARTESIAN_POINT('Ctrl Pts',(-218.055298658605,-0.133253349054334,
125.886004818505));
#129187=CARTESIAN_POINT('Ctrl Pts',(-218.063046555382,-0.270431435342874,
125.891634680883));
#129188=CARTESIAN_POINT('Ctrl Pts',(-218.070794452159,-0.407169130793765,
125.902993832533));
#129189=CARTESIAN_POINT('Ctrl Pts',(-218.078540728243,-0.543878223666119,
125.914350608093));
#129190=CARTESIAN_POINT('Ctrl Pts',(-218.086287004327,-0.680146719556824,
125.931434256809));
#129191=CARTESIAN_POINT('Ctrl Pts',(-218.094033280411,-0.815461998196878,
125.954184868998));
#129192=CARTESIAN_POINT('Ctrl Pts',(-218.101779613677,-0.950778275703764,
125.976935649127));
#129193=CARTESIAN_POINT('Ctrl Pts',(-218.109525946942,-1.08514093636551,
126.00535341138));
#129194=CARTESIAN_POINT('Ctrl Pts',(-218.117272280207,-1.21804601850475,
126.039326833918));
#129195=CARTESIAN_POINT('Ctrl Pts',(-218.12502034821,-1.35098086381546,
126.073307864568));
#129196=CARTESIAN_POINT('Ctrl Pts',(-218.132768416213,-1.48245710236326,
126.112846934414));
#129197=CARTESIAN_POINT('Ctrl Pts',(-218.140516484216,-1.61198482147285,
126.157782522038));
#129198=CARTESIAN_POINT('Ctrl Pts',(-218.148272786958,-1.74165020418388,
126.20276586774));
#129199=CARTESIAN_POINT('Ctrl Pts',(-218.1560290897,-1.86936256063338,126.253157060121));
#129200=CARTESIAN_POINT('Ctrl Pts',(-218.163785392442,-1.99465038125361,
126.30874576317));
#129201=CARTESIAN_POINT('Ctrl Pts',(-218.171545834956,-2.12000507175605,
126.364364135584));
#129202=CARTESIAN_POINT('Ctrl Pts',(-218.17930627747,-2.24293229768162,
126.425185372939));
#129203=CARTESIAN_POINT('Ctrl Pts',(-218.187066719984,-2.362985050008,126.490953064837));
#129204=CARTESIAN_POINT('Ctrl Pts',(-218.19483962025,-2.48323052167021,
126.556826332873));
#129205=CARTESIAN_POINT('Ctrl Pts',(-218.202612520515,-2.60059196385641,
126.627661720935));
#129206=CARTESIAN_POINT('Ctrl Pts',(-218.210385420781,-2.71465050918209,
126.703158882038));
#129207=CARTESIAN_POINT('Ctrl Pts',(-218.217875756543,-2.82456273908872,
126.775911531169));
#129208=CARTESIAN_POINT('Ctrl Pts',(-218.225366092304,-2.93140779044264,
126.852992723144));
#129209=CARTESIAN_POINT('Ctrl Pts',(-218.232856428066,-3.03484133911457,
126.934099501194));
#129210=CARTESIAN_POINT('Ctrl Pts',(-218.240535071511,-3.14087521606131,
127.017245310593));
#129211=CARTESIAN_POINT('Ctrl Pts',(-218.248213714956,-3.24367723813166,
127.104899227514));
#129212=CARTESIAN_POINT('Ctrl Pts',(-218.255892358401,-3.34283278498365,
127.196778042747));
#129213=CARTESIAN_POINT('Ctrl Pts',(-218.263562223384,-3.44187497416621,
127.288551819294));
#129214=CARTESIAN_POINT('Ctrl Pts',(-218.271232088368,-3.53727868431221,
127.384540622821));
#129215=CARTESIAN_POINT('Ctrl Pts',(-218.278901953351,-3.62865977266997,
127.484419154723));
#129216=CARTESIAN_POINT('Ctrl Pts',(-218.286564808957,-3.71995734917867,
127.584206409085));
#129217=CARTESIAN_POINT('Ctrl Pts',(-218.294227664562,-3.80723934465359,
127.687876029734));
#129218=CARTESIAN_POINT('Ctrl Pts',(-218.301890520167,-3.89015652682691,
127.795064145085));
#129219=CARTESIAN_POINT('Ctrl Pts',(-218.309548129204,-3.97301693764679,
127.902178871372));
#129220=CARTESIAN_POINT('Ctrl Pts',(-218.317205738241,-4.05151823457572,
128.012806984851));
#129221=CARTESIAN_POINT('Ctrl Pts',(-218.324863347278,-4.12535011066304,
128.126550032974));
#129222=CARTESIAN_POINT('Ctrl Pts',(-218.332518456262,-4.1991578821534,
128.240255946319));
#129223=CARTESIAN_POINT('Ctrl Pts',(-218.340173565246,-4.26829904160328,
128.357074439064));
#129224=CARTESIAN_POINT('Ctrl Pts',(-218.34782867423,-4.33250565152588,
128.476576726824));
#129225=CARTESIAN_POINT('Ctrl Pts',(-218.355482064927,-4.39669784945617,
128.596052190772));
#129226=CARTESIAN_POINT('Ctrl Pts',(-218.363135455624,-4.45595751446596,
128.718209896309));
#129227=CARTESIAN_POINT('Ctrl Pts',(-218.370788846322,-4.51006223187696,
128.842595665515));
#129228=CARTESIAN_POINT('Ctrl Pts',(-218.378445102554,-4.56418720684235,
128.967028006472));
#129229=CARTESIAN_POINT('Ctrl Pts',(-218.386101358787,-4.61315321508459,
129.093689710612));
#129230=CARTESIAN_POINT('Ctrl Pts',(-218.39375761502,-4.65678565856786,
129.222105773157));
#129231=CARTESIAN_POINT('Ctrl Pts',(-218.400838000821,-4.69713625864268,
129.3408629357));
#129232=CARTESIAN_POINT('Ctrl Pts',(-218.407918386622,-4.73292588820427,
129.461120024275));
#129233=CARTESIAN_POINT('Ctrl Pts',(-218.414998772423,-4.76405452823415,
129.582490119309));
#129234=CARTESIAN_POINT('Ctrl Pts',(-216.665311899804,-4.76405452823409,
129.582490119308));
#129235=CARTESIAN_POINT('Ctrl Pts',(-216.673124903711,-4.79842945311828,
129.71651742972));
#129236=CARTESIAN_POINT('Ctrl Pts',(-216.680937907617,-4.82716305674291,
129.852069638674));
#129237=CARTESIAN_POINT('Ctrl Pts',(-216.688750911523,-4.85013176536874,
129.988637060801));
#129238=CARTESIAN_POINT('Ctrl Pts',(-216.696562353585,-4.87309588247662,
130.125177182666));
#129239=CARTESIAN_POINT('Ctrl Pts',(-216.704373795646,-4.8902973289301,
130.262731738906));
#129240=CARTESIAN_POINT('Ctrl Pts',(-216.712185237708,-4.90166363789405,
130.400780831839));
#129241=CARTESIAN_POINT('Ctrl Pts',(-216.719837013143,-4.91279761840987,
130.536008188039));
#129242=CARTESIAN_POINT('Ctrl Pts',(-216.727488788578,-4.91833269816011,
130.67170970144));
#129243=CARTESIAN_POINT('Ctrl Pts',(-216.735140564013,-4.91824906570758,
130.807392146309));
#129244=CARTESIAN_POINT('',(-216.389859435951,-4.91824825810323,130.800221274069));
#129245=CARTESIAN_POINT('Ctrl Pts',(-216.320029411505,-4.76405452823406,
129.582490119308));
#129246=CARTESIAN_POINT('Ctrl Pts',(-216.329357889193,-4.80476169927653,
129.741206761385));
#129247=CARTESIAN_POINT('Ctrl Pts',(-216.338686366881,-4.83757175068434,
129.90210909891));
#129248=CARTESIAN_POINT('Ctrl Pts',(-216.348014844569,-4.86227946236605,
130.064481240672));
#129249=CARTESIAN_POINT('Ctrl Pts',(-216.357241090068,-4.88671639852329,
130.225073921737));
#129250=CARTESIAN_POINT('Ctrl Pts',(-216.366467335568,-4.90322755997727,
130.387104331365));
#129251=CARTESIAN_POINT('Ctrl Pts',(-216.375693581067,-4.91166082555106,
130.549859149501));
#129252=CARTESIAN_POINT('Ctrl Pts',(-216.380415532695,-4.91597693356135,
130.633156345365));
#129253=CARTESIAN_POINT('Ctrl Pts',(-216.385137484323,-4.91817791611439,
130.716642956803));
#129254=CARTESIAN_POINT('Ctrl Pts',(-216.389859435951,-4.91824825810323,
130.800221274069));
#129255=CARTESIAN_POINT('Ctrl Pts',(-216.389859435996,-4.9182482581039,
130.800221274869));
#129256=CARTESIAN_POINT('Ctrl Pts',(-216.397855279552,-4.91836737059673,
130.941747322197));
#129257=CARTESIAN_POINT('Ctrl Pts',(-216.405851123109,-4.91237278108348,
131.083370584201));
#129258=CARTESIAN_POINT('Ctrl Pts',(-216.413846966665,-4.90027025063863,
131.22452074562));
#129259=CARTESIAN_POINT('Ctrl Pts',(-216.421559449529,-4.88859661570527,
131.360668757202));
#129260=CARTESIAN_POINT('Ctrl Pts',(-216.429271932392,-4.87124062050356,
131.496376205221));
#129261=CARTESIAN_POINT('Ctrl Pts',(-216.436984415256,-4.8482604298453,
131.631133782888));
#129262=CARTESIAN_POINT('Ctrl Pts',(-216.444696531458,-4.82528133169602,
131.765884953999));
#129263=CARTESIAN_POINT('Ctrl Pts',(-216.452408647659,-4.79667863591924,
131.899685955664));
#129264=CARTESIAN_POINT('Ctrl Pts',(-216.460120763861,-4.76256195054892,
132.032035953184));
#129265=CARTESIAN_POINT('Ctrl Pts',(-216.467834218713,-4.72843934328693,
132.164408923695));
#129266=CARTESIAN_POINT('Ctrl Pts',(-216.475547673566,-4.68880094066914,
132.295330006971));
#129267=CARTESIAN_POINT('Ctrl Pts',(-216.483261128418,-4.6438065921186,
132.424312282739));
#129268=CARTESIAN_POINT('Ctrl Pts',(-216.490977627811,-4.59879448406275,
132.553345468487));
#129269=CARTESIAN_POINT('Ctrl Pts',(-216.498694127205,-4.54842235383041,
132.68043795203));
#129270=CARTESIAN_POINT('Ctrl Pts',(-216.506410626598,-4.49289850045566,
132.805122004414));
#129271=CARTESIAN_POINT('Ctrl Pts',(-216.51413612443,-4.43730989906964,
132.929951454568));
#129272=CARTESIAN_POINT('Ctrl Pts',(-216.521861622262,-4.37655774306682,
133.052366506946));
#129273=CARTESIAN_POINT('Ctrl Pts',(-216.529587120094,-4.31089685359044,
133.17192294625));
#129274=CARTESIAN_POINT('Ctrl Pts',(-216.537317978554,-4.24519040282833,
133.291562344301));
#129275=CARTESIAN_POINT('Ctrl Pts',(-216.545048837014,-4.17456863917805,
133.408338842937));
#129276=CARTESIAN_POINT('Ctrl Pts',(-216.552779695475,-4.09932953803423,
133.521837462196));
#129277=CARTESIAN_POINT('Ctrl Pts',(-216.560521712347,-4.0239818397777,
133.635499900828));
#129278=CARTESIAN_POINT('Ctrl Pts',(-216.568263729219,-3.94400373330105,
133.745874699803));
#129279=CARTESIAN_POINT('Ctrl Pts',(-216.576005746092,-3.85973344391655,
133.85257990174));
#129280=CARTESIAN_POINT('Ctrl Pts',(-216.577923724511,-3.83885663635282,
133.879014650964));
#129281=CARTESIAN_POINT('Ctrl Pts',(-216.57984170293,-3.8177165790828,133.905224363624));
#129282=CARTESIAN_POINT('Ctrl Pts',(-216.581759681349,-3.79631875262702,
133.931203592669));
#129283=CARTESIAN_POINT('Ctrl Pts',(-216.589534015468,-3.70958479845807,
134.03650780504));
#129284=CARTESIAN_POINT('Ctrl Pts',(-216.597308349587,-3.61832867105896,
134.138367271289));
#129285=CARTESIAN_POINT('Ctrl Pts',(-216.605082683706,-3.52285428078253,
134.236368889536));
#129286=CARTESIAN_POINT('Ctrl Pts',(-216.612847436653,-3.42749755415933,
134.334249729547));
#129287=CARTESIAN_POINT('Ctrl Pts',(-216.6206121896,-3.32793317858773,134.428281904148));
#129288=CARTESIAN_POINT('Ctrl Pts',(-216.628376942547,-3.22450598449832,
134.518084384681));
#129289=CARTESIAN_POINT('Ctrl Pts',(-216.636133983432,-3.12118151575588,
134.607797672124));
#129290=CARTESIAN_POINT('Ctrl Pts',(-216.643891024317,-3.01400215681808,
134.693289370998));
#129291=CARTESIAN_POINT('Ctrl Pts',(-216.651648065202,-2.9033500849385,
134.774214688787));
#129292=CARTESIAN_POINT('Ctrl Pts',(-216.659399256443,-2.79278145664752,
134.855078980164));
#129293=CARTESIAN_POINT('Ctrl Pts',(-216.667150447682,-2.67874564227477,
134.93138351476));
#129294=CARTESIAN_POINT('Ctrl Pts',(-216.674901638923,-2.56165816566304,
135.002823491618));
#129295=CARTESIAN_POINT('Ctrl Pts',(-216.6826495357,-2.44462045435212,135.07423310458));
#129296=CARTESIAN_POINT('Ctrl Pts',(-216.690397432477,-2.32453399356024,
135.140782068828));
#129297=CARTESIAN_POINT('Ctrl Pts',(-216.698145329254,-2.20184339454529,
135.202208810535));
#129298=CARTESIAN_POINT('Ctrl Pts',(-216.705891605338,-2.07917845975876,
135.263622703091));
#129299=CARTESIAN_POINT('Ctrl Pts',(-216.713637881422,-1.95391081962171,
135.319916329375));
#129300=CARTESIAN_POINT('Ctrl Pts',(-216.721384157506,-1.82650944490343,
135.370874201273));
#129301=CARTESIAN_POINT('Ctrl Pts',(-216.729130490772,-1.69910712973698,
135.42183244933));
#129302=CARTESIAN_POINT('Ctrl Pts',(-216.736876824037,-1.56957141156456,
135.467454719211));
#129303=CARTESIAN_POINT('Ctrl Pts',(-216.744623157302,-1.43839060975884,
135.507573935741));
#129304=CARTESIAN_POINT('Ctrl Pts',(-216.752371225305,-1.30718043092263,
135.547702136691));
#129305=CARTESIAN_POINT('Ctrl Pts',(-216.760119293308,-1.17432480916949,
135.582324717695));
#129306=CARTESIAN_POINT('Ctrl Pts',(-216.767867361311,-1.04032617799798,
135.611324784883));
#129307=CARTESIAN_POINT('Ctrl Pts',(-216.775623664053,-0.906185131486111,
135.640355673688));
#129308=CARTESIAN_POINT('Ctrl Pts',(-216.783379966795,-0.770899031582092,
135.663752028793));
#129309=CARTESIAN_POINT('Ctrl Pts',(-216.791136269537,-0.634979986816272,
135.681448219695));
#129310=CARTESIAN_POINT('Ctrl Pts',(-216.798896712051,-0.498988397963817,
135.699153855587));
#129311=CARTESIAN_POINT('Ctrl Pts',(-216.806657154565,-0.362363580386605,
135.711153230949));
#129312=CARTESIAN_POINT('Ctrl Pts',(-216.814417597079,-0.225620684686972,
135.717432810109));
#129313=CARTESIAN_POINT('Ctrl Pts',(-216.822190497345,-0.0886582771516972,
135.723722469808));
#129314=CARTESIAN_POINT('Ctrl Pts',(-216.82996339761,0.0484221960992154,
135.72427398332));
#129315=CARTESIAN_POINT('Ctrl Pts',(-216.837736297876,0.185106764130735,
135.719125978026));
#129316=CARTESIAN_POINT('Ctrl Pts',(-216.845226633638,0.316822503827401,
135.714165115691));
#129317=CARTESIAN_POINT('Ctrl Pts',(-216.8527169694,0.448170315786501,135.703911947942));
#129318=CARTESIAN_POINT('Ctrl Pts',(-216.860207305162,0.578698535716503,
135.688446106914));
#129319=CARTESIAN_POINT('Ctrl Pts',(-216.867981639281,0.714175772777397,
135.672393873823));
#129320=CARTESIAN_POINT('Ctrl Pts',(-216.8757559734,0.849199192456625,135.650675038898));
#129321=CARTESIAN_POINT('Ctrl Pts',(-216.883530307519,0.983256969473938,
135.623321998868));
#129322=CARTESIAN_POINT('Ctrl Pts',(-216.891295060466,1.11714953226253,
135.596002669015));
#129323=CARTESIAN_POINT('Ctrl Pts',(-216.899059813413,1.25007844087534,
135.563063027272));
#129324=CARTESIAN_POINT('Ctrl Pts',(-216.906824566361,1.38153673584142,
135.52458723395));
#129325=CARTESIAN_POINT('Ctrl Pts',(-216.914581607246,1.51286446457534,
135.486149655328));
#129326=CARTESIAN_POINT('Ctrl Pts',(-216.922338648131,1.6427241135948,135.442186976668));
#129327=CARTESIAN_POINT('Ctrl Pts',(-216.930095689016,1.77061902305256,
135.392834365742));
#129328=CARTESIAN_POINT('Ctrl Pts',(-216.937846880256,1.89841748596474,
135.343518972004));
#129329=CARTESIAN_POINT('Ctrl Pts',(-216.945598071496,2.02425379512616,
135.288821876501));
#129330=CARTESIAN_POINT('Ctrl Pts',(-216.953349262736,2.14764691207149,
135.228927918848));
#129331=CARTESIAN_POINT('Ctrl Pts',(-216.961097159513,2.27098758365,135.169059417724));
#129332=CARTESIAN_POINT('Ctrl Pts',(-216.96884505629,2.3918867773697,135.103998617959));
#129333=CARTESIAN_POINT('Ctrl Pts',(-216.976592953067,2.50988410051506,
135.033978196554));
#129334=CARTESIAN_POINT('Ctrl Pts',(-216.984339229152,2.62785674116447,
134.96397242191));
#129335=CARTESIAN_POINT('Ctrl Pts',(-216.992085505236,2.74292838260234,
134.889009288554));
#129336=CARTESIAN_POINT('Ctrl Pts',(-216.99983178132,2.8546642384186,134.809366878284));
#129337=CARTESIAN_POINT('Ctrl Pts',(-217.007578114585,2.9664009190431,134.729723880113));
#129338=CARTESIAN_POINT('Ctrl Pts',(-217.01532444785,3.07480144654163,134.645401763029));
#129339=CARTESIAN_POINT('Ctrl Pts',(-217.023070781116,3.17946130728828,
134.556721055738));
#129340=CARTESIAN_POINT('Ctrl Pts',(-217.030818849119,3.28414460588493,
134.468020489017));
#129341=CARTESIAN_POINT('Ctrl Pts',(-217.038566917121,3.38508527258254,
134.374959642505));
#129342=CARTESIAN_POINT('Ctrl Pts',(-217.046314985124,3.4819133836792,134.277898043743));
#129343=CARTESIAN_POINT('Ctrl Pts',(-217.054071287866,3.57884440484499,
134.180733286759));
#129344=CARTESIAN_POINT('Ctrl Pts',(-217.061827590608,3.67165386255878,
134.07955956083));
#129345=CARTESIAN_POINT('Ctrl Pts',(-217.06958389335,3.76000973284992,133.974772242477));
#129346=CARTESIAN_POINT('Ctrl Pts',(-217.077344335864,3.84841276132963,
133.869928995977));
#129347=CARTESIAN_POINT('Ctrl Pts',(-217.085104778378,3.93235722680857,
133.761468623017));
#129348=CARTESIAN_POINT('Ctrl Pts',(-217.092865220893,4.01155328985978,
133.649817218028));
#129349=CARTESIAN_POINT('Ctrl Pts',(-217.100638121158,4.09087648546188,
133.537986580292));
#129350=CARTESIAN_POINT('Ctrl Pts',(-217.108411021424,4.16543583356797,
133.42295500235));
#129351=CARTESIAN_POINT('Ctrl Pts',(-217.116183921689,4.23498601864203,
133.305175781549));
#129352=CARTESIAN_POINT('Ctrl Pts',(-217.123674257451,4.30200787930193,
133.191678132092));
#129353=CARTESIAN_POINT('Ctrl Pts',(-217.131164593213,4.36437829960137,
133.075629410313));
#129354=CARTESIAN_POINT('Ctrl Pts',(-217.138654928975,4.42192014073003,
132.957452657286));
#129355=CARTESIAN_POINT('Ctrl Pts',(-217.146429263094,4.48164369825481,
132.834795196749));
#129356=CARTESIAN_POINT('Ctrl Pts',(-217.154203597213,4.53635448378965,
132.709456608922));
#129357=CARTESIAN_POINT('Ctrl Pts',(-217.161977931332,4.58580309955537,
132.581885018132));
#129358=CARTESIAN_POINT('Ctrl Pts',(-217.169742684279,4.63519077432152,
132.454470647927));
#129359=CARTESIAN_POINT('Ctrl Pts',(-217.177507437226,4.67932904289815,
132.324829111412));
#129360=CARTESIAN_POINT('Ctrl Pts',(-217.185272190173,4.7180146877614,132.19343241865));
#129361=CARTESIAN_POINT('Ctrl Pts',(-217.193029231058,4.75666190949679,
132.062166230937));
#129362=CARTESIAN_POINT('Ctrl Pts',(-217.200786271943,4.78986717514584,
131.929148728737));
#129363=CARTESIAN_POINT('Ctrl Pts',(-217.208543312828,4.81747574840408,
131.794870827528));
#129364=CARTESIAN_POINT('Ctrl Pts',(-217.216294504068,4.8450635018225,131.660694186329));
#129365=CARTESIAN_POINT('Ctrl Pts',(-217.224045695308,4.86706288509805,
131.525259419392));
#129366=CARTESIAN_POINT('Ctrl Pts',(-217.231796886549,4.88336939599244,
131.389071148328));
#129367=CARTESIAN_POINT('Ctrl Pts',(-217.239544783326,4.89966897618474,
131.252940760913));
#129368=CARTESIAN_POINT('Ctrl Pts',(-217.247292680103,4.91028045005785,
131.116057893722));
#129369=CARTESIAN_POINT('Ctrl Pts',(-217.25504057688,4.91515072185277,130.978935655788));
#129370=CARTESIAN_POINT('Ctrl Pts',(-217.262786852964,4.92001997489181,
130.84184210087));
#129371=CARTESIAN_POINT('Ctrl Pts',(-217.270533129048,4.91915040071098,
130.704509665275));
#129372=CARTESIAN_POINT('Ctrl Pts',(-217.278279405132,4.91254094472982,
130.567454457129));
#129373=CARTESIAN_POINT('Ctrl Pts',(-217.286025738397,4.90593143995914,
130.430398237272));
#129374=CARTESIAN_POINT('Ctrl Pts',(-217.293772071663,4.89358198767317,
130.293619639459));
#129375=CARTESIAN_POINT('Ctrl Pts',(-217.301518404928,4.87554360825335,
130.157632246053));
#129376=CARTESIAN_POINT('Ctrl Pts',(-217.309266472931,4.85750118926352,
130.021614399213));
#129377=CARTESIAN_POINT('Ctrl Pts',(-217.317014540934,4.83376735943609,
129.886388496855));
#129378=CARTESIAN_POINT('Ctrl Pts',(-217.324762608937,4.8044446466761,129.752460099682));
#129379=CARTESIAN_POINT('Ctrl Pts',(-217.332518911679,4.77509076938816,
129.618389361815));
#129380=CARTESIAN_POINT('Ctrl Pts',(-217.340275214421,4.74013622726691,
129.48561926637));
#129381=CARTESIAN_POINT('Ctrl Pts',(-217.348031517162,4.69973419471019,
129.354642865184));
#129382=CARTESIAN_POINT('Ctrl Pts',(-217.355791959677,4.6593105983721,129.223596557949));
#129383=CARTESIAN_POINT('Ctrl Pts',(-217.363552402191,4.61343384889255,
129.094346220834));
#129384=CARTESIAN_POINT('Ctrl Pts',(-217.371312844705,4.56230576629388,
128.967366018406));
#129385=CARTESIAN_POINT('Ctrl Pts',(-217.37908574497,4.51109560835809,128.840181976085));
#129386=CARTESIAN_POINT('Ctrl Pts',(-217.386858645236,4.45461743283658,
128.715275707213));
#129387=CARTESIAN_POINT('Ctrl Pts',(-217.394631545501,4.39312001258564,
128.593098620986));
#129388=CARTESIAN_POINT('Ctrl Pts',(-217.402121881263,4.33385817846364,
128.475362979589));
#129389=CARTESIAN_POINT('Ctrl Pts',(-217.409612217025,4.26993583781402,
128.360161809799));
#129390=CARTESIAN_POINT('Ctrl Pts',(-217.417102552787,4.20161315922065,
128.247872807549));
#129391=CARTESIAN_POINT('Ctrl Pts',(-217.424876886906,4.13070000550227,
128.13132633365));
#129392=CARTESIAN_POINT('Ctrl Pts',(-217.432651221026,4.05482161775692,
128.017548032004));
#129393=CARTESIAN_POINT('Ctrl Pts',(-217.440425555145,3.97422021008183,
127.906989950172));
#129394=CARTESIAN_POINT('Ctrl Pts',(-217.448190308092,3.8937181364377,127.796568121294));
#129395=CARTESIAN_POINT('Ctrl Pts',(-217.455955061039,3.80850485243069,
127.689358928722));
#129396=CARTESIAN_POINT('Ctrl Pts',(-217.463719813986,3.71886762946074,
127.585788478084));
#129397=CARTESIAN_POINT('Ctrl Pts',(-217.471476854871,3.62931943544432,
127.482320895078));
#129398=CARTESIAN_POINT('Ctrl Pts',(-217.479233895756,3.53535630075866,
127.382485155592));
#129399=CARTESIAN_POINT('Ctrl Pts',(-217.486990936641,3.43730760774658,
127.286676795471));
#129400=CARTESIAN_POINT('Ctrl Pts',(-217.494742127881,3.33933285401701,
127.19094068518));
#129401=CARTESIAN_POINT('Ctrl Pts',(-217.502493319121,3.23727895290669,
127.099226181268));
#129402=CARTESIAN_POINT('Ctrl Pts',(-217.510244510361,3.13151397085618,
127.011893964735));
#129403=CARTESIAN_POINT('Ctrl Pts',(-217.517992407138,3.02579394174426,
126.924598866724));
#129404=CARTESIAN_POINT('Ctrl Pts',(-217.525740303916,2.91636626968072,
126.841682599956));
#129405=CARTESIAN_POINT('Ctrl Pts',(-217.533488200693,2.80363394827169,
126.763467183361));
#129406=CARTESIAN_POINT('Ctrl Pts',(-217.541234476777,2.69092520803408,
126.685268127746));
#129407=CARTESIAN_POINT('Ctrl Pts',(-217.548980752861,2.57491351442602,
126.611768189162));
#129408=CARTESIAN_POINT('Ctrl Pts',(-217.556727028945,2.45603251380457,
126.543247223905));
#129409=CARTESIAN_POINT('Ctrl Pts',(-217.56447336221,2.33715063563075,126.474725752843));
#129410=CARTESIAN_POINT('Ctrl Pts',(-217.572219695476,2.21539974690685,
126.411183523685));
#129411=CARTESIAN_POINT('Ctrl Pts',(-217.579966028741,2.09123951678367,
126.352855215352));
#129412=CARTESIAN_POINT('Ctrl Pts',(-217.587714096744,1.96705148183798,
126.294513844799));
#129413=CARTESIAN_POINT('Ctrl Pts',(-217.595462164747,1.8404533856351,126.241388884708));
#129414=CARTESIAN_POINT('Ctrl Pts',(-217.60321023275,1.71192598955102,126.193667343361));
#129415=CARTESIAN_POINT('Ctrl Pts',(-217.610966535492,1.58326199302071,
126.145895082991));
#129416=CARTESIAN_POINT('Ctrl Pts',(-217.618722838234,1.45266496764989,
126.103537849564));
#129417=CARTESIAN_POINT('Ctrl Pts',(-217.626479140976,1.32063252641623,
126.066733279681));
#129418=CARTESIAN_POINT('Ctrl Pts',(-217.63423958349,1.18852961549327,126.029909066092));
#129419=CARTESIAN_POINT('Ctrl Pts',(-217.642000026004,1.05499014262379,
125.9986435104));
#129420=CARTESIAN_POINT('Ctrl Pts',(-217.649760468518,0.920522124538358,
125.973023113237));
#129421=CARTESIAN_POINT('Ctrl Pts',(-217.657533368783,0.785838246452424,
125.947361587938));
#129422=CARTESIAN_POINT('Ctrl Pts',(-217.665306269049,0.650223231495372,
125.927363387218));
#129423=CARTESIAN_POINT('Ctrl Pts',(-217.673079169314,0.514191330814086,
125.913063209126));
#129424=CARTESIAN_POINT('Ctrl Pts',(-217.680569505077,0.383104532364767,
125.899282878527));
#129425=CARTESIAN_POINT('Ctrl Pts',(-217.688059840839,0.251630939041171,
125.890793507873));
#129426=CARTESIAN_POINT('Ctrl Pts',(-217.695550176601,0.120228944602715,
125.887580363845));
#129427=CARTESIAN_POINT('Ctrl Pts',(-217.70332451072,-0.0161551963919251,
125.884245392485));
#129428=CARTESIAN_POINT('Ctrl Pts',(-217.711098844839,-0.15289422594497,
125.886584077853));
#129429=CARTESIAN_POINT('Ctrl Pts',(-217.718873178958,-0.28947690100534,
125.894636981119));
#129430=CARTESIAN_POINT('Ctrl Pts',(-217.726637931905,-0.425891250125812,
125.902679959902));
#129431=CARTESIAN_POINT('Ctrl Pts',(-217.734402684852,-0.562149241614417,
125.916423121787));
#129432=CARTESIAN_POINT('Ctrl Pts',(-217.742167437799,-0.697737103529993,
125.935855097711));
#129433=CARTESIAN_POINT('Ctrl Pts',(-217.749924478684,-0.833190297669292,
125.955267773522));
#129434=CARTESIAN_POINT('Ctrl Pts',(-217.757681519569,-0.967974302267498,
125.980357964092));
#129435=CARTESIAN_POINT('Ctrl Pts',(-217.765438560454,-1.10157830261635,
126.011062347512));
#129436=CARTESIAN_POINT('Ctrl Pts',(-217.773189751695,-1.23508155114943,
126.041743576517));
#129437=CARTESIAN_POINT('Ctrl Pts',(-217.780940942935,-1.3674061871357,
126.078030484222));
#129438=CARTESIAN_POINT('Ctrl Pts',(-217.788692134175,-1.49804981053356,
126.119808362797));
#129439=CARTESIAN_POINT('Ctrl Pts',(-217.796440030952,-1.62863790690626,
126.161568484659));
#129440=CARTESIAN_POINT('Ctrl Pts',(-217.804187927729,-1.75754604011895,
126.208814816788));
#129441=CARTESIAN_POINT('Ctrl Pts',(-217.811935824506,-1.88428545863704,
126.261382368348));
#129442=CARTESIAN_POINT('Ctrl Pts',(-217.81968210059,-2.01099836600097,
126.313938923909));
#129443=CARTESIAN_POINT('Ctrl Pts',(-217.827428376674,-2.13554310009676,
126.371814335222));
#129444=CARTESIAN_POINT('Ctrl Pts',(-217.835174652758,-2.2574498134471,
126.434795032491));
#129445=CARTESIAN_POINT('Ctrl Pts',(-217.842920986024,-2.37935742668561,
126.49777619467));
#129446=CARTESIAN_POINT('Ctrl Pts',(-217.850667319289,-2.49862663297239,
126.565862538553));
#129447=CARTESIAN_POINT('Ctrl Pts',(-217.858413652554,-2.61481152788086,
126.638794181154));
#129448=CARTESIAN_POINT('Ctrl Pts',(-217.866161720557,-2.73102244159018,
126.711742156291));
#129449=CARTESIAN_POINT('Ctrl Pts',(-217.87390978856,-2.84414733841905,
126.789537381492));
#129450=CARTESIAN_POINT('Ctrl Pts',(-217.881657856563,-2.95376901973853,
126.871876461141));
#129451=CARTESIAN_POINT('Ctrl Pts',(-217.889414159305,-3.06350720828588,
126.954303051744));
#129452=CARTESIAN_POINT('Ctrl Pts',(-217.897170462047,-3.16973443061021,
127.041282908588));
#129453=CARTESIAN_POINT('Ctrl Pts',(-217.904926764788,-3.27206591717074,
127.132471771728));
#129454=CARTESIAN_POINT('Ctrl Pts',(-217.912687207303,-3.37445202112679,
127.22370930511));
#129455=CARTESIAN_POINT('Ctrl Pts',(-217.920447649817,-3.47293796558554,
127.319160049115));
#129456=CARTESIAN_POINT('Ctrl Pts',(-217.928208092331,-3.56717637966557,
127.418443350583));
#129457=CARTESIAN_POINT('Ctrl Pts',(-217.935980992596,-3.66156607361398,
127.51788603042));
#129458=CARTESIAN_POINT('Ctrl Pts',(-217.943753892862,-3.75169435442291,
127.621173267348));
#129459=CARTESIAN_POINT('Ctrl Pts',(-217.951526793127,-3.83725406433632,
127.727891162454));
#129460=CARTESIAN_POINT('Ctrl Pts',(-217.959017128889,-3.91970346328225,
127.830729593267));
#129461=CARTESIAN_POINT('Ctrl Pts',(-217.966507464651,-3.99791049985563,
127.936753338652));
#129462=CARTESIAN_POINT('Ctrl Pts',(-217.973997800413,-4.07163979659263,
128.045568775237));
#129463=CARTESIAN_POINT('Ctrl Pts',(-217.982003133925,-4.15043834831716,
128.161865813017));
#129464=CARTESIAN_POINT('Ctrl Pts',(-217.990008467437,-4.2243696337197,
128.281717260381));
#129465=CARTESIAN_POINT('Ctrl Pts',(-217.998013800949,-4.29310342630013,
128.404684382406));
#129466=CARTESIAN_POINT('Ctrl Pts',(-218.005901336472,-4.3608258053641,
128.525842050819));
#129467=CARTESIAN_POINT('Ctrl Pts',(-218.013788871995,-4.42350238015926,
128.650024005891));
#129468=CARTESIAN_POINT('Ctrl Pts',(-218.021676407519,-4.48085866676351,
128.776778641174));
#129469=CARTESIAN_POINT('Ctrl Pts',(-218.029740640025,-4.53949985189756,
128.90637284042));
#129470=CARTESIAN_POINT('Ctrl Pts',(-218.037804872531,-4.59257930400782,
129.038656048285));
#129471=CARTESIAN_POINT('Ctrl Pts',(-218.045869105037,-4.63985180547736,
129.173116219657));
#129472=CARTESIAN_POINT('Ctrl Pts',(-218.053933337543,-4.68712430694703,
129.30757639103));
#129473=CARTESIAN_POINT('Ctrl Pts',(-218.06199757005,-4.72858966366545,
129.44421315061));
#129474=CARTESIAN_POINT('Ctrl Pts',(-218.070061802556,-4.76405452823401,
129.582490119308));
#129475=CARTESIAN_POINT('Origin',(213.235140564004,0.,130.804360617566));
#129476=CARTESIAN_POINT('',(-220.165126569317,-4.76405452823396,129.582490119308));
#129477=CARTESIAN_POINT('',(-219.819723804473,-4.76405452823394,129.582490119308));
#129478=CARTESIAN_POINT('',(213.235140564004,-4.76405452823405,129.582490119308));
#129479=CARTESIAN_POINT('',(-218.485140563976,-4.91824927387013,130.807033177378));
#129480=CARTESIAN_POINT('Ctrl Pts',(-218.485140564013,-4.91824927386977,
130.807033178037));
#129481=CARTESIAN_POINT('Ctrl Pts',(-218.493861726635,-4.91816600161387,
130.960277123876));
#129482=CARTESIAN_POINT('Ctrl Pts',(-218.502582889257,-4.91092116974832,
131.113322683078));
#129483=CARTESIAN_POINT('Ctrl Pts',(-218.511304051879,-4.89656616260664,
131.265687917556));
#129484=CARTESIAN_POINT('Ctrl Pts',(-218.519078385998,-4.88376963230029,
131.401511349852));
#129485=CARTESIAN_POINT('Ctrl Pts',(-218.526852720118,-4.86529724163473,
131.537017078275));
#129486=CARTESIAN_POINT('Ctrl Pts',(-218.534627054237,-4.84116909561546,
131.671692647505));
#129487=CARTESIAN_POINT('Ctrl Pts',(-218.542391807184,-4.81707068537976,
131.806202241132));
#129488=CARTESIAN_POINT('Ctrl Pts',(-218.550156560131,-4.78733045672144,
131.93988333008));
#129489=CARTESIAN_POINT('Ctrl Pts',(-218.557921313078,-4.75202038008617,
132.072227081254));
#129490=CARTESIAN_POINT('Ctrl Pts',(-218.565678353963,-4.71674537391679,
132.20443938675));
#129491=CARTESIAN_POINT('Ctrl Pts',(-218.573435394848,-4.67591162893664,
132.335316622468));
#129492=CARTESIAN_POINT('Ctrl Pts',(-218.581192435733,-4.62964235552562,
132.464359027934));
#129493=CARTESIAN_POINT('Ctrl Pts',(-218.588943626973,-4.58340797413354,
132.593304121518));
#129494=CARTESIAN_POINT('Ctrl Pts',(-218.596694818213,-4.53174635449418,
132.720416772406));
#129495=CARTESIAN_POINT('Ctrl Pts',(-218.604446009453,-4.47483073939558,
132.84521164502));
#129496=CARTESIAN_POINT('Ctrl Pts',(-218.612193906231,-4.41793931495175,
132.969953476484));
#129497=CARTESIAN_POINT('Ctrl Pts',(-218.619941803008,-4.35579849838412,
133.092379134025));
#129498=CARTESIAN_POINT('Ctrl Pts',(-218.627689699785,-4.28862985153125,
133.212022773903));
#129499=CARTESIAN_POINT('Ctrl Pts',(-218.635435975869,-4.22147525491131,
133.33164138691));
#129500=CARTESIAN_POINT('Ctrl Pts',(-218.643182251953,-4.14929511119276,
133.448478799062));
#129501=CARTESIAN_POINT('Ctrl Pts',(-218.650928528037,-4.07235698842037,
133.562093675961));
#129502=CARTESIAN_POINT('Ctrl Pts',(-218.658674861302,-3.99541829770834,
133.675709391538));
#129503=CARTESIAN_POINT('Ctrl Pts',(-218.666421194567,-3.91372177707821,
133.786102200672));
#129504=CARTESIAN_POINT('Ctrl Pts',(-218.674167527833,-3.82757815571865,
133.89286001442));
#129505=CARTESIAN_POINT('Ctrl Pts',(-218.681915595836,-3.74141524309224,
133.99964173584));
#129506=CARTESIAN_POINT('Ctrl Pts',(-218.689663663839,-3.65080349348223,
134.102786537839));
#129507=CARTESIAN_POINT('Ctrl Pts',(-218.697411731842,-3.55609345374474,
134.201915975575));
#129508=CARTESIAN_POINT('Ctrl Pts',(-218.705168034584,-3.46128275505009,
134.301150769256));
#129509=CARTESIAN_POINT('Ctrl Pts',(-218.712924337325,-3.3623653357367,
134.396361390595));
#129510=CARTESIAN_POINT('Ctrl Pts',(-218.720680640067,-3.25972849080631,
134.487206423288));
#129511=CARTESIAN_POINT('Ctrl Pts',(-218.728441082581,-3.15703686550117,
134.578099942711));
#129512=CARTESIAN_POINT('Ctrl Pts',(-218.736201525096,-3.0506221621607,
134.664622984151));
#129513=CARTESIAN_POINT('Ctrl Pts',(-218.74396196761,-2.94090339716407,
134.746475566556));
#129514=CARTESIAN_POINT('Ctrl Pts',(-218.751734867875,-2.83100850186549,
134.828459545992));
#129515=CARTESIAN_POINT('Ctrl Pts',(-218.759507768141,-2.71779926894801,
134.905757863542));
#129516=CARTESIAN_POINT('Ctrl Pts',(-218.767280668406,-2.60172297832326,
134.978114396428));
#129517=CARTESIAN_POINT('Ctrl Pts',(-218.774771004168,-2.4898663532403,
135.047840587089));
#129518=CARTESIAN_POINT('Ctrl Pts',(-218.78226133993,-2.37534776873736,
135.112977895591));
#129519=CARTESIAN_POINT('Ctrl Pts',(-218.789751675692,-2.25858589322123,
135.173339082315));
#129520=CARTESIAN_POINT('Ctrl Pts',(-218.797526009811,-2.13739695570709,
135.23598888178));
#129521=CARTESIAN_POINT('Ctrl Pts',(-218.80530034393,-2.01340737029519,
135.293691692472));
#129522=CARTESIAN_POINT('Ctrl Pts',(-218.813074678049,-1.88705914740581,
135.346187434684));
#129523=CARTESIAN_POINT('Ctrl Pts',(-218.820839430997,-1.76086663740907,
135.398618480585));
#129524=CARTESIAN_POINT('Ctrl Pts',(-218.828604183944,-1.63232163119647,
135.445855077847));
#129525=CARTESIAN_POINT('Ctrl Pts',(-218.836368936891,-1.50189112624523,
135.487682740526));
#129526=CARTESIAN_POINT('Ctrl Pts',(-218.844125977776,-1.37159016671026,
135.529468859381));
#129527=CARTESIAN_POINT('Ctrl Pts',(-218.851883018661,-1.23940780508304,
135.565856616018));
#129528=CARTESIAN_POINT('Ctrl Pts',(-218.859640059546,-1.10583110222529,
135.596679538073));
#129529=CARTESIAN_POINT('Ctrl Pts',(-218.867391250786,-0.972355130598418,
135.627479216324));
#129530=CARTESIAN_POINT('Ctrl Pts',(-218.875142442026,-0.837487290068465,
135.652722325292));
#129531=CARTESIAN_POINT('Ctrl Pts',(-218.882893633266,-0.701729549162282,
135.672292283308));
#129532=CARTESIAN_POINT('Ctrl Pts',(-218.890641530043,-0.566029508917255,
135.691853923569));
#129533=CARTESIAN_POINT('Ctrl Pts',(-218.89838942682,-0.42944070672453,
135.705747152985));
#129534=CARTESIAN_POINT('Ctrl Pts',(-218.906137323597,-0.29247482970181,
135.713906577886));
#129535=CARTESIAN_POINT('Ctrl Pts',(-218.913883599681,-0.155537602987922,
135.72206429601));
#129536=CARTESIAN_POINT('Ctrl Pts',(-218.921629875765,-0.0182238483586181,
135.724490572033));
#129537=CARTESIAN_POINT('Ctrl Pts',(-218.929376151849,0.118950499993249,
135.721171966505));
#129538=CARTESIAN_POINT('Ctrl Pts',(-218.937122485115,0.256125860934807,
135.717853336479));
#129539=CARTESIAN_POINT('Ctrl Pts',(-218.94486881838,0.393161422694661,
135.708789749738));
#129540=CARTESIAN_POINT('Ctrl Pts',(-218.952615151645,0.529542526459238,
135.69401988741));
#129541=CARTESIAN_POINT('Ctrl Pts',(-218.960363219648,0.665954171826218,
135.679246717473));
#129542=CARTESIAN_POINT('Ctrl Pts',(-218.968111287651,0.801710678939786,
135.658764771201));
#129543=CARTESIAN_POINT('Ctrl Pts',(-218.975859355654,0.936304172297377,
135.632664414909));
#129544=CARTESIAN_POINT('Ctrl Pts',(-218.983615658396,1.07104071322157,
135.606536318848));
#129545=CARTESIAN_POINT('Ctrl Pts',(-218.991371961138,1.20461138678995,
135.574777958975));
#129546=CARTESIAN_POINT('Ctrl Pts',(-218.99912826388,1.33651960738935,135.537530633693));
#129547=CARTESIAN_POINT('Ctrl Pts',(-219.006888706394,1.46849823137813,
135.500263428392));
#129548=CARTESIAN_POINT('Ctrl Pts',(-219.014649148908,1.5988122630806,135.457501541991));
#129549=CARTESIAN_POINT('Ctrl Pts',(-219.022409591422,1.72698283135395,
135.409435357753));
#129550=CARTESIAN_POINT('Ctrl Pts',(-219.030182491688,1.8553591504016,135.361292013409));
#129551=CARTESIAN_POINT('Ctrl Pts',(-219.037955391953,1.98158476983939,
135.307827508256));
#129552=CARTESIAN_POINT('Ctrl Pts',(-219.045728292219,2.10520244060309,
135.249279710933));
#129553=CARTESIAN_POINT('Ctrl Pts',(-219.053218627981,2.22432629766242,
135.192860273515));
#129554=CARTESIAN_POINT('Ctrl Pts',(-219.060708963743,2.34102825228591,
135.13172085135));
#129555=CARTESIAN_POINT('Ctrl Pts',(-219.068199299505,2.45492447397956,
135.066112474439));
#129556=CARTESIAN_POINT('Ctrl Pts',(-219.075973633624,2.57313910553523,
134.998016535976));
#129557=CARTESIAN_POINT('Ctrl Pts',(-219.083747967743,2.68870551392837,
134.92489036485));
#129558=CARTESIAN_POINT('Ctrl Pts',(-219.091522301862,2.80116596930678,
134.84696525751));
#129559=CARTESIAN_POINT('Ctrl Pts',(-219.099287054809,2.9134878272245,134.769136185901));
#129560=CARTESIAN_POINT('Ctrl Pts',(-219.107051807757,3.02271103005475,
134.686520166229));
#129561=CARTESIAN_POINT('Ctrl Pts',(-219.114816560704,3.12840270115622,
134.599394161805));
#129562=CARTESIAN_POINT('Ctrl Pts',(-219.122573601589,3.23398939779997,
134.512354692157));
#129563=CARTESIAN_POINT('Ctrl Pts',(-219.130330642474,3.33605124320624,
134.420814399003));
#129564=CARTESIAN_POINT('Ctrl Pts',(-219.138087683359,3.43418491116918,
134.325093078063));
#129565=CARTESIAN_POINT('Ctrl Pts',(-219.145838874599,3.53224457576961,
134.229443941316));
#129566=CARTESIAN_POINT('Ctrl Pts',(-219.153590065839,3.62638168040358,
134.129620324417));
#129567=CARTESIAN_POINT('Ctrl Pts',(-219.161341257079,3.71622681535907,
134.025981532464));
#129568=CARTESIAN_POINT('Ctrl Pts',(-219.169089153856,3.80603376373563,
133.922386789762));
#129569=CARTESIAN_POINT('Ctrl Pts',(-219.176837050633,3.89155211507228,
133.814980391941));
#129570=CARTESIAN_POINT('Ctrl Pts',(-219.18458494741,3.97245027243601,133.70415748899));
#129571=CARTESIAN_POINT('Ctrl Pts',(-219.192331223494,4.05333150764919,
133.593357767802));
#129572=CARTESIAN_POINT('Ctrl Pts',(-219.200077499578,4.12959424083472,
133.47914327856));
#129573=CARTESIAN_POINT('Ctrl Pts',(-219.207823775662,4.20094828997011,
133.361940826963));
#129574=CARTESIAN_POINT('Ctrl Pts',(-219.215570108928,4.27230286582498,
133.244737510203));
#129575=CARTESIAN_POINT('Ctrl Pts',(-219.223316442193,4.33874848201673,
133.124546521022));
#129576=CARTESIAN_POINT('Ctrl Pts',(-219.231062775459,4.40003949641406,
133.001821764548));
#129577=CARTESIAN_POINT('Ctrl Pts',(-219.238810843462,4.46134423650901,
132.879069524716));
#129578=CARTESIAN_POINT('Ctrl Pts',(-219.246558911465,4.51749190316311,
132.753782738198));
#129579=CARTESIAN_POINT('Ctrl Pts',(-219.254306979468,4.56828400500315,
132.626437540238));
#129580=CARTESIAN_POINT('Ctrl Pts',(-219.262063282209,4.61913008929352,
132.498956998285));
#129581=CARTESIAN_POINT('Ctrl Pts',(-219.269819584951,4.66460909339769,
132.369414038441));
#129582=CARTESIAN_POINT('Ctrl Pts',(-219.277575887693,4.70457147901002,
132.238302827484));
#129583=CARTESIAN_POINT('Ctrl Pts',(-219.285336330207,4.7445551937508,132.107121638526));
#129584=CARTESIAN_POINT('Ctrl Pts',(-219.293096772721,4.7790163248749,131.974370908853));
#129585=CARTESIAN_POINT('Ctrl Pts',(-219.300857215236,4.80785620566194,
131.840556433123));
#129586=CARTESIAN_POINT('Ctrl Pts',(-219.308630115501,4.8367423827859,131.706527146517));
#129587=CARTESIAN_POINT('Ctrl Pts',(-219.316403015766,4.85998921094519,
131.57143108701));
#129588=CARTESIAN_POINT('Ctrl Pts',(-219.324175916032,4.87754966147512,
131.435781524999));
#129589=CARTESIAN_POINT('Ctrl Pts',(-219.331666251794,4.89447174539619,
131.305063166248));
#129590=CARTESIAN_POINT('Ctrl Pts',(-219.339156587556,4.90611367504773,
131.173831155561));
#129591=CARTESIAN_POINT('Ctrl Pts',(-219.346646923318,4.91247917932139,
131.042544108249));
#129592=CARTESIAN_POINT('Ctrl Pts',(-219.354421257437,4.91908603362435,
130.906279272634));
#129593=CARTESIAN_POINT('Ctrl Pts',(-219.362195591556,4.92002938141795,
130.769523498542));
#129594=CARTESIAN_POINT('Ctrl Pts',(-219.369969925675,4.91525640479089,
130.632786908443));
#129595=CARTESIAN_POINT('Ctrl Pts',(-219.377734678622,4.91048931043095,
130.496218833971));
#129596=CARTESIAN_POINT('Ctrl Pts',(-219.38549943157,4.9000199223279,130.359670283427));
#129597=CARTESIAN_POINT('Ctrl Pts',(-219.393264184517,4.88384727716248,
130.223655153624));
#129598=CARTESIAN_POINT('Ctrl Pts',(-219.401021225402,4.86769069489623,
130.087775115965));
#129599=CARTESIAN_POINT('Ctrl Pts',(-219.408778266287,4.84584217415149,
129.952427830437));
#129600=CARTESIAN_POINT('Ctrl Pts',(-219.416535307172,4.81835276045784,
129.818125484199));
#129601=CARTESIAN_POINT('Ctrl Pts',(-219.424286498412,4.79088407674486,
129.683924416404));
#129602=CARTESIAN_POINT('Ctrl Pts',(-219.432037689652,4.75778304517731,
129.550767100912));
#129603=CARTESIAN_POINT('Ctrl Pts',(-219.439788880892,4.71915228433671,
129.419158545759));
#129604=CARTESIAN_POINT('Ctrl Pts',(-219.447536777669,4.68053794260003,
129.287605927752));
#129605=CARTESIAN_POINT('Ctrl Pts',(-219.455284674446,4.63639865600589,
129.157601135198));
#129606=CARTESIAN_POINT('Ctrl Pts',(-219.463032571223,4.58688763918803,
129.029636738208));
#129607=CARTESIAN_POINT('Ctrl Pts',(-219.470778847307,4.53738697900755,
128.901699108611));
#129608=CARTESIAN_POINT('Ctrl Pts',(-219.478525123392,4.48251696459341,
128.77580139003));
#129609=CARTESIAN_POINT('Ctrl Pts',(-219.486271399476,4.42247982919597,
128.652418419724));
#129610=CARTESIAN_POINT('Ctrl Pts',(-219.494017732741,4.36244225061795,
128.529034538632));
#129611=CARTESIAN_POINT('Ctrl Pts',(-219.501764066006,4.2972376460098,128.408165794411));
#129612=CARTESIAN_POINT('Ctrl Pts',(-219.509510399272,4.22711512304086,
128.290264199554));
#129613=CARTESIAN_POINT('Ctrl Pts',(-219.517258467275,4.15697689661919,
128.172336201453));
#129614=CARTESIAN_POINT('Ctrl Pts',(-219.525006535278,4.08191876012435,
128.057377010899));
#129615=CARTESIAN_POINT('Ctrl Pts',(-219.53275460328,4.0022340101876,127.945810987037));
#129616=CARTESIAN_POINT('Ctrl Pts',(-219.540510906022,3.92246457035024,
127.834126389477));
#129617=CARTESIAN_POINT('Ctrl Pts',(-219.548267208764,3.838058921991,127.725842481234));
#129618=CARTESIAN_POINT('Ctrl Pts',(-219.556023511506,3.74935199250927,
127.621352182333));
#129619=CARTESIAN_POINT('Ctrl Pts',(-219.56378395402,3.66059771746836,127.516806113813));
#129620=CARTESIAN_POINT('Ctrl Pts',(-219.571544396534,3.56753785203093,
127.416057976203));
#129621=CARTESIAN_POINT('Ctrl Pts',(-219.579304839049,3.47054460379491,
127.319464174977));
#129622=CARTESIAN_POINT('Ctrl Pts',(-219.587077739314,3.37339565338617,
127.222715312806));
#129623=CARTESIAN_POINT('Ctrl Pts',(-219.59485063958,3.27230099085897,127.130134377822));
#129624=CARTESIAN_POINT('Ctrl Pts',(-219.602623539845,3.16766702499355,
127.042038371762));
#129625=CARTESIAN_POINT('Ctrl Pts',(-219.610113875607,3.06683676734468,
126.957144877423));
#129626=CARTESIAN_POINT('Ctrl Pts',(-219.617604211369,2.96272030741638,
126.876416084994));
#129627=CARTESIAN_POINT('Ctrl Pts',(-219.625094547131,2.85570550681664,
126.800096750032));
#129628=CARTESIAN_POINT('Ctrl Pts',(-219.63286888125,2.74463320752525,126.720883744288));
#129629=CARTESIAN_POINT('Ctrl Pts',(-219.640643215369,2.6300866041821,126.64617024273));
#129630=CARTESIAN_POINT('Ctrl Pts',(-219.648417549488,2.51246632789698,
126.576276416219));
#129631=CARTESIAN_POINT('Ctrl Pts',(-219.656182302435,2.39499100809067,
126.506468727602));
#129632=CARTESIAN_POINT('Ctrl Pts',(-219.663947055382,2.27444988526298,
126.441469093369));
#129633=CARTESIAN_POINT('Ctrl Pts',(-219.67171180833,2.15127479466006,126.381556097766));
#129634=CARTESIAN_POINT('Ctrl Pts',(-219.679468849215,2.02822204329359,
126.321702608596));
#129635=CARTESIAN_POINT('Ctrl Pts',(-219.6872258901,1.90254087960268,126.266925874012));
#129636=CARTESIAN_POINT('Ctrl Pts',(-219.694982930985,1.7746898125044,126.217459797634));
#129637=CARTESIAN_POINT('Ctrl Pts',(-219.702734122225,1.64693515889017,
126.168031024009));
#129638=CARTESIAN_POINT('Ctrl Pts',(-219.710485313465,1.51701422205617,
126.123905077765));
#129639=CARTESIAN_POINT('Ctrl Pts',(-219.718236504705,1.38540734741418,
126.085268592162));
#129640=CARTESIAN_POINT('Ctrl Pts',(-219.725984401482,1.25385640920447,
126.046648528096));
#129641=CARTESIAN_POINT('Ctrl Pts',(-219.733732298259,1.1206213327352,126.013513394078));
#129642=CARTESIAN_POINT('Ctrl Pts',(-219.741480195036,0.986199347443375,
125.986000532475));
#129643=CARTESIAN_POINT('Ctrl Pts',(-219.74922647112,0.851805480333436,
125.958493425969));
#129644=CARTESIAN_POINT('Ctrl Pts',(-219.756972747204,0.716225581017021,
125.936606330979));
#129645=CARTESIAN_POINT('Ctrl Pts',(-219.764719023289,0.579968455539898,
125.920425764082));
#129646=CARTESIAN_POINT('Ctrl Pts',(-219.772465356554,0.443710324243442,
125.904245077743));
#129647=CARTESIAN_POINT('Ctrl Pts',(-219.780211689819,0.306775345048278,
125.893771049656));
#129648=CARTESIAN_POINT('Ctrl Pts',(-219.787958023085,0.169678457645862,
125.889038422276));
#129649=CARTESIAN_POINT('Ctrl Pts',(-219.795706091088,0.0325508683458896,
125.884304735057));
#129650=CARTESIAN_POINT('Ctrl Pts',(-219.803454159091,-0.104738310653312,
125.885315020518));
#129651=CARTESIAN_POINT('Ctrl Pts',(-219.811202227094,-0.241673519991771,
125.892051896381));
#129652=CARTESIAN_POINT('Ctrl Pts',(-219.818958529836,-0.378754265700079,
125.898795932275));
#129653=CARTESIAN_POINT('Ctrl Pts',(-219.826714832577,-0.515479899125724,
125.911278697344));
#129654=CARTESIAN_POINT('Ctrl Pts',(-219.834471135319,-0.651338809082206,
125.929430790555));
#129655=CARTESIAN_POINT('Ctrl Pts',(-219.842231577834,-0.787270231029564,
125.947592572084));
#129656=CARTESIAN_POINT('Ctrl Pts',(-219.849992020348,-0.922333622918667,
125.971429643181));
#129657=CARTESIAN_POINT('Ctrl Pts',(-219.857752462862,-1.05602794343241,
126.000821500916));
#129658=CARTESIAN_POINT('Ctrl Pts',(-219.865525363127,-1.18993688193827,
126.03026054107));
#129659=CARTESIAN_POINT('Ctrl Pts',(-219.873298263393,-1.32247197903826,
126.06527208703));
#129660=CARTESIAN_POINT('Ctrl Pts',(-219.881071163658,-1.45314685832208,
126.105685562761));
#129661=CARTESIAN_POINT('Ctrl Pts',(-219.88856149942,-1.57907137659272,
126.144629906853));
#129662=CARTESIAN_POINT('Ctrl Pts',(-219.896051835182,-1.70326828579786,
126.188590149103));
#129663=CARTESIAN_POINT('Ctrl Pts',(-219.903542170944,-1.8253220174828,
126.237372266914));
#129664=CARTESIAN_POINT('Ctrl Pts',(-219.911316827432,-1.95200870645148,
126.288006073033));
#129665=CARTESIAN_POINT('Ctrl Pts',(-219.91909148392,-2.07678762301751,
126.343995445933));
#129666=CARTESIAN_POINT('Ctrl Pts',(-219.926866140409,-2.19917278731122,
126.405176362042));
#129667=CARTESIAN_POINT('Ctrl Pts',(-219.934631141583,-2.32140596197137,
126.466281297822));
#129668=CARTESIAN_POINT('Ctrl Pts',(-219.942396142757,-2.44125095312209,
126.532564774866));
#129669=CARTESIAN_POINT('Ctrl Pts',(-219.950161143931,-2.55823991868953,
126.603814036355));
#129670=CARTESIAN_POINT('Ctrl Pts',(-219.957918359215,-2.67511158058155,
126.674991856916));
#129671=CARTESIAN_POINT('Ctrl Pts',(-219.9656755745,-2.78913258425368,126.751125350685));
#129672=CARTESIAN_POINT('Ctrl Pts',(-219.973432789784,-2.89985827678652,
126.831955170352));
#129673=CARTESIAN_POINT('Ctrl Pts',(-219.981420030598,-3.01386733004928,
126.915181845254));
#129674=CARTESIAN_POINT('Ctrl Pts',(-219.989407271412,-3.1243822208978,
127.003387519341));
#129675=CARTESIAN_POINT('Ctrl Pts',(-219.997394512226,-3.2309475571713,
127.096239672221));
#129676=CARTESIAN_POINT('Ctrl Pts',(-220.005142067531,-3.33431502231414,
127.186305466707));
#129677=CARTESIAN_POINT('Ctrl Pts',(-220.012889622837,-3.43396625633552,
127.280742596255));
#129678=CARTESIAN_POINT('Ctrl Pts',(-220.020637178142,-3.52951803945245,
127.379205807681));
#129679=CARTESIAN_POINT('Ctrl Pts',(-220.028383059044,-3.62504917190008,
127.477647739219));
#129680=CARTESIAN_POINT('Ctrl Pts',(-220.036128939946,-3.71648234431109,
127.580113740925));
#129681=CARTESIAN_POINT('Ctrl Pts',(-220.043874820849,-3.80347097002815,
127.686221486184));
#129682=CARTESIAN_POINT('Ctrl Pts',(-220.05162070513,-3.89045963369587,
127.792329277736));
#129683=CARTESIAN_POINT('Ctrl Pts',(-220.059366589412,-3.97300349954177,
127.902078513306));
#129684=CARTESIAN_POINT('Ctrl Pts',(-220.067112473693,-4.05079633585681,
128.015053874322));
#129685=CARTESIAN_POINT('Ctrl Pts',(-220.074860038761,-4.12860605250429,
128.128053749955));
#129686=CARTESIAN_POINT('Ctrl Pts',(-220.082607603828,-4.20166246736009,
128.244280821682));
#129687=CARTESIAN_POINT('Ctrl Pts',(-220.090355168896,-4.26970295929672,
128.363291240864));
#129688=CARTESIAN_POINT('Ctrl Pts',(-220.098109601356,-4.33780376189924,
128.482407150136));
#129689=CARTESIAN_POINT('Ctrl Pts',(-220.105864033817,-4.40087957149622,
128.604310992629));
#129690=CARTESIAN_POINT('Ctrl Pts',(-220.113618466278,-4.45871384497264,
128.728534538351));
#129691=CARTESIAN_POINT('Ctrl Pts',(-220.121377041106,-4.51657901314775,
128.852824443496));
#129692=CARTESIAN_POINT('Ctrl Pts',(-220.129135615935,-4.56919691659541,
128.979436160509));
#129693=CARTESIAN_POINT('Ctrl Pts',(-220.136894190764,-4.616399729699,129.107882914166));
#129694=CARTESIAN_POINT('Ctrl Pts',(-220.144661999102,-4.66365871904769,
129.236482532786));
#129695=CARTESIAN_POINT('Ctrl Pts',(-220.15242980744,-4.70548963466743,
129.366921176344));
#129696=CARTESIAN_POINT('Ctrl Pts',(-220.160197615777,-4.74177483484259,
129.498698150405));
#129697=CARTESIAN_POINT('Ctrl Pts',(-220.161840600291,-4.74944958933631,
129.526570558962));
#129698=CARTESIAN_POINT('Ctrl Pts',(-220.163483584804,-4.75687642643801,
129.554502809348));
#129699=CARTESIAN_POINT('Ctrl Pts',(-220.165126569317,-4.76405452823397,
129.582490119308));
#129700=CARTESIAN_POINT('Ctrl Pts',(-218.414998772423,-4.76405452823415,
129.582490119309));
#129701=CARTESIAN_POINT('Ctrl Pts',(-218.422662130679,-4.79774618392612,
129.713853373509));
#129702=CARTESIAN_POINT('Ctrl Pts',(-218.430325488935,-4.82597703335009,
129.846520217875));
#129703=CARTESIAN_POINT('Ctrl Pts',(-218.437988847192,-4.84866974835229,
129.979991322945));
#129704=CARTESIAN_POINT('Ctrl Pts',(-218.445847466656,-4.87194067029563,
130.116863251557));
#129705=CARTESIAN_POINT('Ctrl Pts',(-218.45370608612,-4.88938739281945,
130.254580524333));
#129706=CARTESIAN_POINT('Ctrl Pts',(-218.461564705584,-4.90098329172141,
130.392601177155));
#129707=CARTESIAN_POINT('Ctrl Pts',(-218.469423325048,-4.91257919062336,
130.530621829977));
#129708=CARTESIAN_POINT('Ctrl Pts',(-218.477281944512,-4.91832431028879,
130.668945412283));
#129709=CARTESIAN_POINT('Ctrl Pts',(-218.485140563975,-4.91824927387013,
130.807033177379));
#129710=CARTESIAN_POINT('',(-218.139859436045,-4.91824937750444,130.80683512301));
#129711=CARTESIAN_POINT('Ctrl Pts',(-218.070061802556,-4.76405452823401,
129.582490119308));
#129712=CARTESIAN_POINT('Ctrl Pts',(-218.077925797649,-4.79863878913083,
129.717333627655));
#129713=CARTESIAN_POINT('Ctrl Pts',(-218.085789792741,-4.82751692160361,
129.853736466587));
#129714=CARTESIAN_POINT('Ctrl Pts',(-218.093653787834,-4.85055947271794,
129.991184213502));
#129715=CARTESIAN_POINT('Ctrl Pts',(-218.101514136411,-4.87359133905553,
130.12856822622));
#129716=CARTESIAN_POINT('Ctrl Pts',(-218.109374484987,-4.89079294912702,
130.266995813564));
#129717=CARTESIAN_POINT('Ctrl Pts',(-218.117234833564,-4.90208583965905,
130.405941889198));
#129718=CARTESIAN_POINT('Ctrl Pts',(-218.124776367708,-4.91292069242709,
130.539252335087));
#129719=CARTESIAN_POINT('Ctrl Pts',(-218.132317901852,-4.91831669360595,
130.673039704548));
#129720=CARTESIAN_POINT('Ctrl Pts',(-218.139859435996,-4.91824937750488,
130.806835122136));
#129721=CARTESIAN_POINT('Ctrl Pts',(-218.139859436045,-4.91824937750444,
130.806835123011));
#129722=CARTESIAN_POINT('Ctrl Pts',(-218.148385548635,-4.91817327298129,
130.958098085236));
#129723=CARTESIAN_POINT('Ctrl Pts',(-218.156911661225,-4.91111483647233,
131.109122025211));
#129724=CARTESIAN_POINT('Ctrl Pts',(-218.165437773815,-4.89716461096416,
131.259291200864));
#129725=CARTESIAN_POINT('Ctrl Pts',(-218.174008185907,-4.88314190364959,
131.410240617175));
#129726=CARTESIAN_POINT('Ctrl Pts',(-218.182578597998,-4.86215569217589,
131.56032612373));
#129727=CARTESIAN_POINT('Ctrl Pts',(-218.19114901009,-4.83434822261198,
131.708938046551));
#129728=CARTESIAN_POINT('Ctrl Pts',(-218.199742282965,-4.80646657919078,
131.857946377952));
#129729=CARTESIAN_POINT('Ctrl Pts',(-218.208335555839,-4.77172735794309,
132.00547302904));
#129730=CARTESIAN_POINT('Ctrl Pts',(-218.216928828714,-4.73032278608913,
132.150922685169));
#129731=CARTESIAN_POINT('Ctrl Pts',(-218.225552752069,-4.68877053243292,
132.296891131044));
#129732=CARTESIAN_POINT('Ctrl Pts',(-218.234176675425,-4.6405054176299,
132.440767519449));
#129733=CARTESIAN_POINT('Ctrl Pts',(-218.24280059878,-4.58576905108392,
132.581972856672));
#129734=CARTESIAN_POINT('Ctrl Pts',(-218.246015540595,-4.56536369422066,
132.634613276175));
#129735=CARTESIAN_POINT('Ctrl Pts',(-218.24923048241,-4.54405945670397,
132.686882729135));
#129736=CARTESIAN_POINT('Ctrl Pts',(-218.252445424226,-4.52187047538647,
132.738752115254));
#129737=CARTESIAN_POINT('Ctrl Pts',(-218.260219758345,-4.46821334426689,
132.864182048798));
#129738=CARTESIAN_POINT('Ctrl Pts',(-218.267994092464,-4.40924841045326,
132.987576409418));
#129739=CARTESIAN_POINT('Ctrl Pts',(-218.275768426583,-4.34515128957907,
133.108453352933));
#129740=CARTESIAN_POINT('Ctrl Pts',(-218.28353317953,-4.28113316267801,
133.229181326417));
#129741=CARTESIAN_POINT('Ctrl Pts',(-218.291297932477,-4.21199561490571,
133.347397713737));
#129742=CARTESIAN_POINT('Ctrl Pts',(-218.299062685424,-4.13796254450172,
133.462639956311));
#129743=CARTESIAN_POINT('Ctrl Pts',(-218.306819726309,-4.06400300478674,
133.577767738666));
#129744=CARTESIAN_POINT('Ctrl Pts',(-218.314576767194,-3.98515782858715,
133.689926927984));
#129745=CARTESIAN_POINT('Ctrl Pts',(-218.322333808079,-3.90169693691545,
133.798679250405));
#129746=CARTESIAN_POINT('Ctrl Pts',(-218.330084999319,-3.81829898375128,
133.907349561853));
#129747=CARTESIAN_POINT('Ctrl Pts',(-218.33783619056,-3.73029248039418,
134.012617811229));
#129748=CARTESIAN_POINT('Ctrl Pts',(-218.3455873818,-3.63799058652956,134.114074737369));
#129749=CARTESIAN_POINT('Ctrl Pts',(-218.353335278577,-3.54572792343219,
134.215488541609));
#129750=CARTESIAN_POINT('Ctrl Pts',(-218.361083175354,-3.44917376346446,
134.313093955911));
#129751=CARTESIAN_POINT('Ctrl Pts',(-218.368831072131,-3.34868132633162,
134.406515033631));
#129752=CARTESIAN_POINT('Ctrl Pts',(-218.376577348215,-3.24820991005026,
134.499916569676));
#129753=CARTESIAN_POINT('Ctrl Pts',(-218.384323624299,-3.14380214135624,
134.589135244078));
#129754=CARTESIAN_POINT('Ctrl Pts',(-218.392069900383,-3.0358475655595,
134.673832496413));
#129755=CARTESIAN_POINT('Ctrl Pts',(-218.399816233649,-2.92789219286647,
134.758530373963));
#129756=CARTESIAN_POINT('Ctrl Pts',(-218.407562566914,-2.81639026842193,
134.838706521518));
#129757=CARTESIAN_POINT('Ctrl Pts',(-218.415308900179,-2.70176350784062,
134.914063406114));
#129758=CARTESIAN_POINT('Ctrl Pts',(-218.423056968182,-2.5871110773912,
134.989437166362));
#129759=CARTESIAN_POINT('Ctrl Pts',(-218.430805036185,-2.46933274494215,
135.059989301358));
#129760=CARTESIAN_POINT('Ctrl Pts',(-218.438553104188,-2.34887786954401,
135.125466473301));
#129761=CARTESIAN_POINT('Ctrl Pts',(-218.44630940693,-2.2282949732707,135.191013235162));
